ISO-10303-21;
HEADER;
/* Generated by software containing ST-Developer
 * from STEP Tools, Inc. (www.steptools.com) 
 */

FILE_DESCRIPTION(
/* description */ (''),
/* implementation_level */ '2;1');

FILE_NAME(
/* name */ 'Assembly Screw 3.step',
/* time_stamp */ '2026-10-28T16:47:13+01:00',
/* author */ (''),
/* organization */ (''),
/* preprocessor_version */ 'ST-DEVELOPER v20.2',
/* originating_system */ 'Autodesk Translation Framework v15.17.0.0',
/* authorisation */ '');

FILE_SCHEMA (('AUTOMOTIVE_DESIGN { 1 0 10303 214 3 1 1 }'));
ENDSEC;

DATA;
#10=MECHANICAL_DESIGN_GEOMETRIC_PRESENTATION_REPRESENTATION('',(#4608),#459242);
#1080=ELLIPSE('',#103301,0.0947748497909006,0.0898017844795411);
#1081=ELLIPSE('',#103302,0.0972540504460011,0.0908803722731057);
#1082=ELLIPSE('',#103304,0.0972540504441047,0.0908803722721906);
#1083=ELLIPSE('',#103305,0.094774849794112,0.089801784481129);
#1084=ELLIPSE('',#103307,0.0947748497926148,0.0898017844804075);
#1085=ELLIPSE('',#103308,0.0972540504400136,0.0908803722702226);
#1086=ELLIPSE('',#103310,0.094774849789673,0.0898017844789408);
#1087=ELLIPSE('',#103311,0.0972540504453024,0.0908803722727663);
#1088=ELLIPSE('',#103313,0.094774849786822,0.0898017844775384);
#1089=ELLIPSE('',#103314,0.0972540504422525,0.0908803722712843);
#1090=ELLIPSE('',#103316,0.0947748497908327,0.0898017844795387);
#1091=ELLIPSE('',#103317,0.0972540504468864,0.0908803722735133);
#1092=ELLIPSE('',#103319,0.0947748497890312,0.0898017844786284);
#1093=ELLIPSE('',#103320,0.0972540504424856,0.0908803722714283);
#1094=ELLIPSE('',#103322,0.0947748497876344,0.0898017844779163);
#1095=ELLIPSE('',#103323,0.0972540504418127,0.0908803722711085);
#1096=ELLIPSE('',#103325,0.0947748497848643,0.0898017844765636);
#1097=ELLIPSE('',#103326,0.0972540504452924,0.0908803722727769);
#1098=ELLIPSE('',#103328,0.0947748497895253,0.0898017844788167);
#1099=ELLIPSE('',#103329,0.0972540504473756,0.0908803722737362);
#1100=ELLIPSE('',#103331,0.0947748497843389,0.0898017844762829);
#1101=ELLIPSE('',#103332,0.0972540504474796,0.0908803722737873);
#1102=ELLIPSE('',#103334,0.0947748497882029,0.089801784478216);
#1103=ELLIPSE('',#103335,0.0972540504461555,0.0908803722731809);
#1104=ELLIPSE('',#103337,0.0947748497881544,0.0898017844781412);
#1105=ELLIPSE('',#103338,0.097254050445608,0.0908803722729431);
#1106=ELLIPSE('',#103340,0.0947748497883721,0.0898017844782773);
#1107=ELLIPSE('',#103341,0.0972540504426967,0.090880372271529);
#1108=ELLIPSE('',#103343,0.0947748497912198,0.0898017844796705);
#1109=ELLIPSE('',#103344,0.097254050442374,0.0908803722713863);
#1110=ELLIPSE('',#103346,0.0947748497899889,0.0898017844791001);
#1111=ELLIPSE('',#103347,0.09725405044176,0.0908803722710741);
#1112=ELLIPSE('',#103349,0.0947748497919646,0.0898017844800436);
#1113=ELLIPSE('',#103350,0.0972540504477304,0.0908803722739094);
#1114=ELLIPSE('',#103352,0.0947748497877307,0.0898017844779762);
#1115=ELLIPSE('',#103353,0.0972540504444203,0.0908803722723428);
#1116=ELLIPSE('',#103355,0.0947748497875329,0.0898017844778618);
#1117=ELLIPSE('',#103356,0.0972540504420591,0.0908803722711656);
#1118=ELLIPSE('',#103358,0.0947748497891401,0.0898017844787187);
#1119=ELLIPSE('',#103359,0.0972540504458414,0.0908803722730333);
#1120=ELLIPSE('',#103361,0.0947748497842726,0.0898017844762788);
#1121=ELLIPSE('',#103362,0.097254050446,0.0908803722731059);
#1122=ELLIPSE('',#103364,0.0947748497896824,0.0898017844789354);
#1123=ELLIPSE('',#103365,0.0972540504473757,0.0908803722737566);
#1124=ELLIPSE('',#103367,0.0947748497879396,0.0898017844780717);
#1125=ELLIPSE('',#103368,0.0972540504470089,0.0908803722736072);
#1126=ELLIPSE('',#103370,0.0947748497897777,0.0898017844789476);
#1127=ELLIPSE('',#103371,0.0972540504424488,0.0908803722714188);
#1128=ELLIPSE('',#103373,0.0947748497858688,0.089801784477053);
#1129=ELLIPSE('',#103374,0.0972540504452601,0.0908803722727454);
#1130=ELLIPSE('',#103376,0.0947748497860426,0.0898017844771369);
#1131=ELLIPSE('',#103377,0.0972540504427043,0.0908803722715334);
#1132=ELLIPSE('',#103379,0.0947748497911017,0.0898017844796039);
#1133=ELLIPSE('',#103380,0.0972540504471524,0.0908803722736316);
#1134=ELLIPSE('',#103382,0.0947748497922374,0.0898017844801959);
#1135=ELLIPSE('',#103383,0.0972540504445394,0.0908803722723832);
#1136=ELLIPSE('',#103385,0.0947748497900101,0.0898017844790907);
#1137=ELLIPSE('',#103386,0.0972540504431669,0.0908803722717343);
#1138=ELLIPSE('',#103388,0.0947748497928145,0.0898017844805255);
#1139=ELLIPSE('',#103389,0.0972540504431744,0.0908803722717194);
#1140=ELLIPSE('',#103391,0.0947748497892975,0.089801784478741);
#1141=ELLIPSE('',#103392,0.0972540504433099,0.0908803722717966);
#1142=ELLIPSE('',#103394,0.0947748497905813,0.0898017844793987);
#1143=ELLIPSE('',#103395,0.0972540504447271,0.0908803722724841);
#1144=ELLIPSE('',#103397,0.0947748497888503,0.089801784478531);
#1145=ELLIPSE('',#103398,0.0972540504397721,0.0908803722700921);
#1146=ELLIPSE('',#103400,0.0947748497870893,0.0898017844776473);
#1147=ELLIPSE('',#103401,0.097254050445599,0.0908803722729439);
#1148=ELLIPSE('',#103403,0.0947748497869435,0.0898017844776184);
#1149=ELLIPSE('',#103404,0.0972540504398893,0.0908803722701564);
#1150=ELLIPSE('',#103406,0.0947748497885468,0.0898017844783568);
#1151=ELLIPSE('',#103407,0.0972540504452832,0.0908803722727715);
#1152=ELLIPSE('',#103409,0.0947748497938607,0.0898017844810411);
#1153=ELLIPSE('',#103410,0.0972540504442418,0.0908803722722562);
#1154=ELLIPSE('',#103412,0.0947748497932972,0.0898017844807086);
#1155=ELLIPSE('',#103413,0.0972540504442487,0.0908803722722781);
#1156=ELLIPSE('',#103415,0.0947748497875134,0.0898017844778826);
#1157=ELLIPSE('',#103416,0.0972540504437859,0.0908803722720484);
#1158=ELLIPSE('',#103418,0.0947748497930879,0.0898017844806332);
#1159=ELLIPSE('',#103419,0.0972540504418411,0.0908803722711222);
#1160=ELLIPSE('',#103421,0.0947748497905372,0.0898017844793675);
#1161=ELLIPSE('',#103422,0.0972540504448954,0.0908803722725851);
#1162=ELLIPSE('',#103424,0.0947748497895737,0.0898017844788519);
#1163=ELLIPSE('',#103425,0.0972540504458755,0.0908803722730405);
#1164=ELLIPSE('',#103427,0.0947748497952288,0.0898017844816764);
#1165=ELLIPSE('',#103428,0.0972540504431929,0.0908803722717643);
#1166=ELLIPSE('',#103430,0.0947748497907875,0.0898017844794307);
#1167=ELLIPSE('',#103431,0.0972540504433047,0.090880372271786);
#1168=ELLIPSE('',#103433,0.0947748497925041,0.0898017844803797);
#1169=ELLIPSE('',#103434,0.097254050447641,0.0908803722738984);
#1170=ELLIPSE('',#103436,0.0947748497896336,0.0898017844789406);
#1171=ELLIPSE('',#103437,0.0972540504450963,0.0908803722726497);
#1172=ELLIPSE('',#103439,0.0947748497902753,0.0898017844792372);
#1173=ELLIPSE('',#103440,0.0972540504430836,0.0908803722717207);
#1174=ELLIPSE('',#103442,0.0947748497870242,0.0898017844776269);
#1175=ELLIPSE('',#103443,0.0972540504459792,0.090880372273105);
#1176=ELLIPSE('',#103445,0.0947748497890259,0.0898017844786251);
#1177=ELLIPSE('',#103446,0.0972540504488311,0.0908803722744611);
#1178=ELLIPSE('',#103448,0.0947748497922702,0.0898017844801884);
#1179=ELLIPSE('',#103449,0.0972540504411497,0.0908803722707469);
#1180=ELLIPSE('',#103451,0.0947748497905426,0.0898017844793613);
#1181=ELLIPSE('',#103452,0.0972540504401611,0.0908803722702625);
#1182=ELLIPSE('',#103454,0.0947748497905523,0.0898017844793281);
#1183=ELLIPSE('',#103455,0.0972540504497045,0.0908803722748831);
#1184=ELLIPSE('',#103457,0.094774849791047,0.089801784479608);
#1185=ELLIPSE('',#103458,0.0972540504464803,0.0908803722733509);
#1186=ELLIPSE('',#103460,0.0947748497888638,0.08980178447855);
#1187=ELLIPSE('',#103461,0.0972540504428653,0.0908803722716096);
#1188=ELLIPSE('',#103463,0.0947748497937681,0.0898017844809604);
#1189=ELLIPSE('',#103464,0.0972540504468058,0.090880372273465);
#1190=ELLIPSE('',#103466,0.0947748497887476,0.0898017844784555);
#1191=ELLIPSE('',#103467,0.0972540504424136,0.0908803722713366);
#1192=ELLIPSE('',#103469,0.0947748497937203,0.0898017844809448);
#1193=ELLIPSE('',#103470,0.097254050439549,0.0908803722699748);
#1194=ELLIPSE('',#103472,0.0947748497936973,0.089801784480952);
#1195=ELLIPSE('',#103473,0.097254050446727,0.0908803722734838);
#1196=ELLIPSE('',#103475,0.0947748497887032,0.0898017844784639);
#1197=ELLIPSE('',#103476,0.0972540504410564,0.090880372270709);
#1198=ELLIPSE('',#103478,0.0947748497904981,0.0898017844793291);
#1199=ELLIPSE('',#103479,0.0972540504464435,0.0908803722733254);
#1200=ELLIPSE('',#103481,0.0947748497869006,0.0898017844775519);
#1201=ELLIPSE('',#103482,0.0972540504383138,0.0908803722693876);
#1202=ELLIPSE('',#103484,0.0947748497936647,0.0898017844808587);
#1203=ELLIPSE('',#103485,0.0972540504444964,0.090880372272367);
#1204=ELLIPSE('',#103487,0.0947748497914323,0.0898017844798336);
#1205=ELLIPSE('',#103488,0.097254050440378,0.0908803722703976);
#1206=ELLIPSE('',#103490,0.0947748497888831,0.0898017844785387);
#1207=ELLIPSE('',#103491,0.0972540504428949,0.0908803722715775);
#1208=ELLIPSE('',#103493,0.0972540504453366,0.0908803722727811);
#1209=ELLIPSE('',#103494,0.0947748497894938,0.0898017844788294);
#1210=ELLIPSE('',#103496,0.097254050445453,0.0908803722728491);
#1211=ELLIPSE('',#103497,0.0947748497859855,0.0898017844771064);
#1212=ELLIPSE('',#103499,0.097254050440179,0.0908803722702838);
#1213=ELLIPSE('',#103500,0.0947748497888099,0.0898017844785166);
#1214=ELLIPSE('',#103502,0.0972540504444705,0.0908803722723385);
#1215=ELLIPSE('',#103503,0.09477484978895,0.0898017844785994);
#1216=ELLIPSE('',#103505,0.0972540504441078,0.0908803722721443);
#1217=ELLIPSE('',#103506,0.0947748497941903,0.0898017844811543);
#1218=ELLIPSE('',#103508,0.0972540504441623,0.0908803722721518);
#1219=ELLIPSE('',#103509,0.0947748497891558,0.0898017844787237);
#1220=ELLIPSE('',#103511,0.0972540504465191,0.090880372273371);
#1221=ELLIPSE('',#103512,0.0947748497877717,0.0898017844779554);
#1222=ELLIPSE('',#103514,0.0972540504455481,0.0908803722728434);
#1223=ELLIPSE('',#103515,0.0947748497885424,0.089801784478368);
#1224=ELLIPSE('',#103517,0.0972540504450305,0.0908803722726285);
#1225=ELLIPSE('',#103518,0.0947748497924166,0.0898017844803043);
#1226=ELLIPSE('',#103520,0.0972540504423171,0.0908803722713102);
#1227=ELLIPSE('',#103521,0.094774849789829,0.0898017844790031);
#1228=ELLIPSE('',#103523,0.0972540504450714,0.0908803722726709);
#1229=ELLIPSE('',#103524,0.0947748497893594,0.0898017844787876);
#1230=ELLIPSE('',#103526,0.0947748497916052,0.0898017844799109);
#1231=ELLIPSE('',#103527,0.0972540504466488,0.0908803722733968);
#1232=ELLIPSE('',#103529,0.0365824585612681,0.0343843127629441);
#1233=ELLIPSE('',#103530,0.0365824585612681,0.0343843127629441);
#1234=ELLIPSE('',#103532,0.0752932753395665,0.0683396339849831);
#1235=ELLIPSE('',#103534,0.068253186714463,0.0644989639553658);
#1236=ELLIPSE('',#103548,0.0947748497910113,0.0898017844796313);
#1237=ELLIPSE('',#103549,0.0972540504436445,0.0908803722719478);
#1238=ELLIPSE('',#103565,20.5655698940688,0.57588643813926);
#1239=ELLIPSE('',#103579,0.0682531867111947,0.0644989639532992);
#1240=ELLIPSE('',#103581,0.0752932753386038,0.0683396339845777);
#1241=ELLIPSE('',#103583,0.0365824585612599,0.0343843127629419);
#1242=ELLIPSE('',#103584,0.0365824585612599,0.0343843127629419);
#1243=ELLIPSE('',#103587,20.5663229393736,0.575899814551761);
#1244=ELLIPSE('',#103600,0.0682531867094754,0.064498963952367);
#1245=ELLIPSE('',#103602,0.0752932753433806,0.0683396339869066);
#1246=ELLIPSE('',#103604,0.0365824585612664,0.0343843127629435);
#1247=ELLIPSE('',#103605,0.0365824585612664,0.0343843127629435);
#1248=ELLIPSE('',#103608,20.5662371819658,0.575898279112179);
#1249=ELLIPSE('',#103621,0.0682531867098176,0.0644989639525022);
#1250=ELLIPSE('',#103623,0.0752932753414954,0.0683396339859597);
#1251=ELLIPSE('',#103625,0.0365824585612623,0.0343843127629425);
#1252=ELLIPSE('',#103626,0.0365824585612623,0.0343843127629425);
#1253=ELLIPSE('',#103629,20.5664729686215,0.575902484006716);
#1254=ELLIPSE('',#103642,0.0682531867102852,0.0644989639528799);
#1255=ELLIPSE('',#103644,0.0752932753421658,0.0683396339862994);
#1256=ELLIPSE('',#103646,0.0365824585612823,0.0343843127629472);
#1257=ELLIPSE('',#103647,0.0365824585612823,0.0343843127629472);
#1258=ELLIPSE('',#103650,20.5678571921608,0.575927076211219);
#1259=ELLIPSE('',#103663,0.0682531867113445,0.0644989639535526);
#1260=ELLIPSE('',#103665,0.075293275342646,0.0683396339865244);
#1261=ELLIPSE('',#103667,0.0365824585612725,0.0343843127629449);
#1262=ELLIPSE('',#103668,0.0365824585612725,0.0343843127629449);
#1263=ELLIPSE('',#103671,20.5672810058914,0.575916860252127);
#1264=ELLIPSE('',#103684,0.0682531867116232,0.0644989639537626);
#1265=ELLIPSE('',#103686,0.0752932753401903,0.0683396339853526);
#1266=ELLIPSE('',#103688,0.0365824585612739,0.0343843127629457);
#1267=ELLIPSE('',#103689,0.0365824585612739,0.0343843127629457);
#1268=ELLIPSE('',#103692,20.5658263631507,0.575890993606254);
#1269=ELLIPSE('',#103705,0.0682531867065395,0.0644989639503165);
#1270=ELLIPSE('',#103707,0.0752932753395809,0.0683396339850594);
#1271=ELLIPSE('',#103709,0.0365824585612871,0.0343843127629484);
#1272=ELLIPSE('',#103710,0.0365824585612871,0.0343843127629484);
#1273=ELLIPSE('',#103713,20.5645162727811,0.575867690121613);
#1274=ELLIPSE('',#103726,0.0682531867118177,0.0644989639537703);
#1275=ELLIPSE('',#103728,0.075293275340606,0.0683396339855119);
#1276=ELLIPSE('',#103730,0.0365824585612647,0.0343843127629428);
#1277=ELLIPSE('',#103731,0.0365824585612647,0.0343843127629428);
#1278=ELLIPSE('',#103734,20.5647351111823,0.575871593292131);
#1279=ELLIPSE('',#103747,0.0682531867054113,0.0644989639497118);
#1280=ELLIPSE('',#103749,0.0752932753420776,0.0683396339862422);
#1281=ELLIPSE('',#103751,0.0365824585612792,0.0343843127629464);
#1282=ELLIPSE('',#103752,0.0365824585612792,0.0343843127629464);
#1283=ELLIPSE('',#103755,20.5664678496986,0.575902371596359);
#1284=ELLIPSE('',#103768,0.0682531867081726,0.0644989639514463);
#1285=ELLIPSE('',#103770,0.0752932753410852,0.0683396339857466);
#1286=ELLIPSE('',#103772,0.0365824585612641,0.0343843127629426);
#1287=ELLIPSE('',#103773,0.0365824585612641,0.0343843127629426);
#1288=ELLIPSE('',#103776,20.5669390412555,0.575910766874766);
#1289=ELLIPSE('',#103789,0.068253186706991,0.0644989639507338);
#1290=ELLIPSE('',#103791,0.0752932753374719,0.0683396339840305);
#1291=ELLIPSE('',#103793,0.0365824585612722,0.0343843127629447);
#1292=ELLIPSE('',#103794,0.0365824585612722,0.0343843127629447);
#1293=ELLIPSE('',#103797,20.5672143657057,0.575915656399323);
#1294=ELLIPSE('',#103810,0.0682531867126107,0.0644989639543164);
#1295=ELLIPSE('',#103812,0.0752932753438051,0.0683396339870321);
#1296=ELLIPSE('',#103814,0.0365824585612707,0.0343843127629448);
#1297=ELLIPSE('',#103815,0.0365824585612707,0.0343843127629448);
#1298=ELLIPSE('',#103818,20.5666091795923,0.575904895820283);
#1299=ELLIPSE('',#103831,0.0682531867124643,0.0644989639541045);
#1300=ELLIPSE('',#103833,0.0752932753410141,0.0683396339857257);
#1301=ELLIPSE('',#103835,0.0365824585612672,0.0343843127629434);
#1302=ELLIPSE('',#103836,0.0365824585612672,0.0343843127629434);
#1303=ELLIPSE('',#103839,20.5655464083401,0.575886023270062);
#1304=ELLIPSE('',#103852,0.0682531867065658,0.0644989639504541);
#1305=ELLIPSE('',#103854,0.0752932753402659,0.0683396339853328);
#1306=ELLIPSE('',#103856,0.0365824585612715,0.0343843127629447);
#1307=ELLIPSE('',#103857,0.0365824585612715,0.0343843127629447);
#1308=ELLIPSE('',#103860,20.5646822681491,0.575870652388697);
#1309=ELLIPSE('',#103873,0.0682531867120338,0.0644989639538604);
#1310=ELLIPSE('',#103875,0.0752932753391909,0.0683396339848181);
#1311=ELLIPSE('',#103877,0.0365824585612667,0.0343843127629439);
#1312=ELLIPSE('',#103878,0.0365824585612667,0.0343843127629439);
#1313=ELLIPSE('',#103881,20.5655365027352,0.575885832702478);
#1314=ELLIPSE('',#103894,0.0682531867127566,0.0644989639543388);
#1315=ELLIPSE('',#103896,0.0752932753420776,0.0683396339862422);
#1316=ELLIPSE('',#103898,0.0365824585612694,0.0343843127629439);
#1317=ELLIPSE('',#103899,0.0365824585612694,0.0343843127629439);
#1318=ELLIPSE('',#103902,20.5688852559233,0.575945359262387);
#1319=ELLIPSE('',#103915,0.0682531867130963,0.064498963954561);
#1320=ELLIPSE('',#103917,0.0752932753382094,0.0683396339843537);
#1321=ELLIPSE('',#103919,0.0365824585612733,0.034384312762945);
#1322=ELLIPSE('',#103920,0.0365824585612733,0.034384312762945);
#1323=ELLIPSE('',#103923,20.5668625413724,0.575909393256759);
#1324=ELLIPSE('',#103936,0.0682531867084203,0.0644989639516756);
#1325=ELLIPSE('',#103938,0.0752932753436893,0.0683396339869951);
#1326=ELLIPSE('',#103940,0.0365824585612695,0.0343843127629441);
#1327=ELLIPSE('',#103941,0.0365824585612695,0.0343843127629441);
#1328=ELLIPSE('',#103944,20.5665715965953,0.575904239966151);
#1329=ELLIPSE('',#103957,0.068253186708846,0.064498963951929);
#1330=ELLIPSE('',#103959,0.0752932753363512,0.0683396339834891);
#1331=ELLIPSE('',#103961,0.0365824585612623,0.0343843127629426);
#1332=ELLIPSE('',#103962,0.0365824585612623,0.0343843127629426);
#1333=ELLIPSE('',#103965,20.5661257179486,0.575896290425635);
#1334=ELLIPSE('',#103978,0.0682531867104988,0.0644989639528177);
#1335=ELLIPSE('',#103980,0.0752932753396825,0.0683396339850846);
#1336=ELLIPSE('',#103982,0.0365824585612735,0.034384312762945);
#1337=ELLIPSE('',#103983,0.0365824585612735,0.034384312762945);
#1338=ELLIPSE('',#103986,20.5661929652102,0.575897501216388);
#1339=ELLIPSE('',#103999,0.0682531867089655,0.0644989639517745);
#1340=ELLIPSE('',#104001,0.0752932753431176,0.0683396339867453);
#1341=ELLIPSE('',#104003,0.0365824585612691,0.034384312762944);
#1342=ELLIPSE('',#104004,0.0365824585612691,0.034384312762944);
#1343=ELLIPSE('',#104007,20.5650746168456,0.5758776240409);
#1344=ELLIPSE('',#104020,0.0682531867060306,0.0644989639500308);
#1345=ELLIPSE('',#104022,0.0752932753402928,0.0683396339853569);
#1346=ELLIPSE('',#104024,0.036582458561283,0.0343843127629472);
#1347=ELLIPSE('',#104025,0.036582458561283,0.0343843127629472);
#1348=ELLIPSE('',#104028,20.5657406141823,0.575889449951057);
#1349=ELLIPSE('',#104041,0.0682531867074524,0.0644989639509632);
#1350=ELLIPSE('',#104043,0.0752932753386184,0.0683396339845661);
#1351=ELLIPSE('',#104045,0.0365824585612756,0.0343843127629454);
#1352=ELLIPSE('',#104046,0.0365824585612756,0.0343843127629454);
#1353=ELLIPSE('',#104049,20.5643894487282,0.575865453162332);
#1354=ELLIPSE('',#104062,0.0682531867044203,0.0644989639489921);
#1355=ELLIPSE('',#104064,0.0752932753451356,0.0683396339877038);
#1356=ELLIPSE('',#104066,0.0365824585612593,0.0343843127629417);
#1357=ELLIPSE('',#104067,0.0365824585612593,0.0343843127629417);
#1358=ELLIPSE('',#104070,20.5656209986185,0.575887328706856);
#1359=ELLIPSE('',#104083,0.068253186707082,0.0644989639507634);
#1360=ELLIPSE('',#104085,0.0752932753377725,0.0683396339841321);
#1361=ELLIPSE('',#104087,0.0365824585612572,0.0343843127629406);
#1362=ELLIPSE('',#104088,0.0365824585612572,0.0343843127629406);
#1363=ELLIPSE('',#104091,20.5648167949509,0.575873048464462);
#1364=ELLIPSE('',#104104,0.0682531867132729,0.0644989639547264);
#1365=ELLIPSE('',#104106,0.0752932753412577,0.0683396339859388);
#1366=ELLIPSE('',#104108,0.0365824585612782,0.0343843127629461);
#1367=ELLIPSE('',#104109,0.0365824585612782,0.0343843127629461);
#1368=ELLIPSE('',#104112,20.5673748138211,0.575918526296799);
#1369=ELLIPSE('',#104125,0.0682531867117419,0.0644989639536371);
#1370=ELLIPSE('',#104127,0.0752932753379916,0.0683396339842599);
#1371=ELLIPSE('',#104129,0.0365824585612557,0.0343843127629409);
#1372=ELLIPSE('',#104130,0.0365824585612557,0.0343843127629409);
#1373=ELLIPSE('',#104133,20.5657430869869,0.575889508004331);
#1374=ELLIPSE('',#104146,0.068253186712517,0.0644989639542092);
#1375=ELLIPSE('',#104148,0.0752932753416743,0.0683396339860329);
#1376=ELLIPSE('',#104150,0.0365824585612746,0.034384312762945);
#1377=ELLIPSE('',#104151,0.0365824585612746,0.034384312762945);
#1378=ELLIPSE('',#104154,20.5673584002177,0.575918223147289);
#1379=ELLIPSE('',#104167,0.068253186713621,0.0644989639549432);
#1380=ELLIPSE('',#104169,0.0752932753389554,0.0683396339847396);
#1381=ELLIPSE('',#104171,0.0365824585612687,0.0343843127629438);
#1382=ELLIPSE('',#104172,0.0365824585612687,0.0343843127629438);
#1383=ELLIPSE('',#104175,20.5667255038569,0.575906974270808);
#1384=ELLIPSE('',#104188,0.0682531867092921,0.0644989639522078);
#1385=ELLIPSE('',#104190,0.0752932753390765,0.0683396339847818);
#1386=ELLIPSE('',#104192,0.036582458561274,0.0343843127629452);
#1387=ELLIPSE('',#104193,0.036582458561274,0.0343843127629452);
#1388=ELLIPSE('',#104196,20.5667004386175,0.57590654076783);
#1389=ELLIPSE('',#104209,0.0682531867061263,0.0644989639501379);
#1390=ELLIPSE('',#104211,0.0752932753377836,0.0683396339842295);
#1391=ELLIPSE('',#104213,0.0365824585612689,0.034384312762944);
#1392=ELLIPSE('',#104214,0.0365824585612689,0.034384312762944);
#1393=ELLIPSE('',#104217,20.5669358575543,0.575910702097059);
#1394=ELLIPSE('',#104230,0.0682531867090717,0.0644989639519959);
#1395=ELLIPSE('',#104232,0.075293275340053,0.0683396339852434);
#1396=ELLIPSE('',#104234,0.0365824585612704,0.034384312762944);
#1397=ELLIPSE('',#104235,0.0365824585612704,0.034384312762944);
#1398=ELLIPSE('',#104238,20.5662681156164,0.575898853502041);
#1399=ELLIPSE('',#104251,0.0682531867097275,0.0644989639524759);
#1400=ELLIPSE('',#104253,0.0752932753429599,0.0683396339866412);
#1401=ELLIPSE('',#104255,0.0365824585612673,0.0343843127629433);
#1402=ELLIPSE('',#104256,0.0365824585612673,0.0343843127629433);
#1403=ELLIPSE('',#104259,20.5670037655622,0.57591192326816);
#1404=ELLIPSE('',#104272,0.0682531867142658,0.06449896395531);
#1405=ELLIPSE('',#104274,0.0752932753384642,0.0683396339845221);
#1406=ELLIPSE('',#104276,0.03658245856126,0.0343843127629417);
#1407=ELLIPSE('',#104277,0.03658245856126,0.0343843127629417);
#1408=ELLIPSE('',#104280,20.5649490683217,0.575875401255735);
#1409=ELLIPSE('',#104293,0.0682531867126994,0.0644989639543507);
#1410=ELLIPSE('',#104295,0.0752932753421147,0.0683396339862076);
#1411=ELLIPSE('',#104297,0.03658245856127,0.034384312762944);
#1412=ELLIPSE('',#104298,0.03658245856127,0.034384312762944);
#1413=ELLIPSE('',#104301,20.5657460307936,0.575889566336278);
#1414=ELLIPSE('',#104314,0.0682531867125926,0.064498963954206);
#1415=ELLIPSE('',#104316,0.0752932753386351,0.0683396339845576);
#1416=ELLIPSE('',#104318,0.0365824585612653,0.0343843127629431);
#1417=ELLIPSE('',#104319,0.0365824585612653,0.0343843127629431);
#1418=ELLIPSE('',#104322,20.566106933613,0.575895983526128);
#1419=ELLIPSE('',#104335,0.0682531867125118,0.0644989639541397);
#1420=ELLIPSE('',#104337,0.0752932753399427,0.0683396339852131);
#1421=ELLIPSE('',#104339,0.036582458561266,0.0343843127629433);
#1422=ELLIPSE('',#104340,0.036582458561266,0.0343843127629433);
#1423=ELLIPSE('',#104343,20.5662209241031,0.575898008612868);
#1424=ELLIPSE('',#104356,0.0682531867080255,0.0644989639513619);
#1425=ELLIPSE('',#104358,0.0752932753417252,0.0683396339860757);
#1426=ELLIPSE('',#104360,0.0365824585612643,0.0343843127629431);
#1427=ELLIPSE('',#104361,0.0365824585612643,0.0343843127629431);
#1428=ELLIPSE('',#104364,20.5668829564603,0.575909777573919);
#1429=ELLIPSE('',#104377,0.0682531867108673,0.0644989639530764);
#1430=ELLIPSE('',#104379,0.0752932753393979,0.0683396339849238);
#1431=ELLIPSE('',#104381,0.0365824585612754,0.0343843127629457);
#1432=ELLIPSE('',#104382,0.0365824585612754,0.0343843127629457);
#1433=ELLIPSE('',#104385,20.5656204522085,0.575887327180999);
#1434=ELLIPSE('',#104398,0.0682531867121636,0.064498963953902);
#1435=ELLIPSE('',#104400,0.0752932753435212,0.0683396339869279);
#1436=ELLIPSE('',#104402,0.0365824585612717,0.0343843127629449);
#1437=ELLIPSE('',#104403,0.0365824585612717,0.0343843127629449);
#1438=ELLIPSE('',#104406,20.5649985423749,0.575876281188508);
#1439=ELLIPSE('',#104419,0.0682531867100479,0.0644989639525862);
#1440=ELLIPSE('',#104421,0.0752932753365371,0.068339633983568);
#1441=ELLIPSE('',#104423,0.0365824585612617,0.0343843127629418);
#1442=ELLIPSE('',#104424,0.0365824585612617,0.0343843127629418);
#1443=ELLIPSE('',#104427,20.5660877699337,0.575895627154355);
#1444=ELLIPSE('',#104440,0.0682531867089013,0.0644989639519441);
#1445=ELLIPSE('',#104442,0.0752932753417667,0.0683396339860729);
#1446=ELLIPSE('',#104444,0.0365824585612718,0.0343843127629447);
#1447=ELLIPSE('',#104445,0.0365824585612718,0.0343843127629447);
#1448=ELLIPSE('',#104448,20.5667145066123,0.575906772537685);
#1449=ELLIPSE('',#104461,0.0682531867123641,0.0644989639540796);
#1450=ELLIPSE('',#104463,0.0752932753404132,0.0683396339854202);
#1451=ELLIPSE('',#104465,0.0365824585612721,0.0343843127629448);
#1452=ELLIPSE('',#104466,0.0365824585612721,0.0343843127629448);
#1453=ELLIPSE('',#104469,20.5655320840775,0.575885745020712);
#1454=ELLIPSE('',#104482,0.0682531867076054,0.0644989639510852);
#1455=ELLIPSE('',#104484,0.0752932753418868,0.0683396339861622);
#1456=ELLIPSE('',#104486,0.0365824585612703,0.0343843127629439);
#1457=ELLIPSE('',#104487,0.0365824585612703,0.0343843127629439);
#1458=ELLIPSE('',#104490,20.5656645738439,0.575888110796235);
#1459=ELLIPSE('',#104503,0.0682531867104776,0.0644989639529921);
#1460=ELLIPSE('',#104505,0.0752932753402919,0.0683396339853131);
#1461=ELLIPSE('',#104507,0.0365824585612638,0.0343843127629429);
#1462=ELLIPSE('',#104508,0.0365824585612638,0.0343843127629429);
#1463=ELLIPSE('',#104511,20.5649673526229,0.575875718878864);
#1464=ELLIPSE('',#104524,0.0682531867113191,0.064498963953423);
#1465=ELLIPSE('',#104526,0.0752932753419452,0.0683396339861261);
#1466=ELLIPSE('',#104528,0.036582458561263,0.0343843127629426);
#1467=ELLIPSE('',#104529,0.036582458561263,0.0343843127629426);
#1468=ELLIPSE('',#104532,20.5669984446418,0.575911817820984);
#1469=ELLIPSE('',#104545,0.0682531867132061,0.0644989639546646);
#1470=ELLIPSE('',#104547,0.0752932753409153,0.0683396339856607);
#1471=ELLIPSE('',#104549,0.0365824585612572,0.0343843127629414);
#1472=ELLIPSE('',#104550,0.0365824585612572,0.0343843127629414);
#1473=ELLIPSE('',#104553,20.5683868647745,0.575936493679187);
#1474=ELLIPSE('',#104566,0.0682531867051281,0.0644989639495226);
#1475=ELLIPSE('',#104568,0.0752932753371693,0.068339633983922);
#1476=ELLIPSE('',#104570,0.0365824585612551,0.0343843127629402);
#1477=ELLIPSE('',#104571,0.0365824585612551,0.0343843127629402);
#1478=ELLIPSE('',#104574,20.5642184742806,0.575862395393301);
#1479=ELLIPSE('',#104587,0.0682531867130814,0.0644989639545292);
#1480=ELLIPSE('',#104589,0.0752932753382603,0.0683396339843966);
#1481=ELLIPSE('',#104591,0.0365824585612835,0.0343843127629476);
#1482=ELLIPSE('',#104592,0.0365824585612835,0.0343843127629476);
#1483=ELLIPSE('',#104595,20.5674049560068,0.575919072631943);
#1484=ELLIPSE('',#104608,0.0682531867118938,0.0644989639538107);
#1485=ELLIPSE('',#104610,0.0752932753398767,0.0683396339852028);
#1486=ELLIPSE('',#104612,0.0365824585612653,0.0343843127629431);
#1487=ELLIPSE('',#104613,0.0365824585612653,0.0343843127629431);
#1488=ELLIPSE('',#104616,20.5655633575056,0.575886299567876);
#1489=ELLIPSE('',#104629,0.0682531867143369,0.0644989639553002);
#1490=ELLIPSE('',#104631,0.0752932753394289,0.0683396339849304);
#1491=ELLIPSE('',#104633,0.0365824585612765,0.0343843127629459);
#1492=ELLIPSE('',#104634,0.0365824585612765,0.0343843127629459);
#1493=ELLIPSE('',#104637,20.5653921601537,0.575883266585551);
#1494=ELLIPSE('',#104650,0.0682531867093569,0.0644989639522558);
#1495=ELLIPSE('',#104652,0.0752932753403644,0.0683396339854381);
#1496=ELLIPSE('',#104654,0.0365824585612568,0.0343843127629409);
#1497=ELLIPSE('',#104655,0.0365824585612568,0.0343843127629409);
#1498=ELLIPSE('',#104658,20.5661203042729,0.575896214636728);
#1499=ELLIPSE('',#104671,0.0682531867085627,0.0644989639517258);
#1500=ELLIPSE('',#104673,0.0752932753420239,0.0683396339862363);
#1501=ELLIPSE('',#104675,0.0365824585612604,0.0343843127629423);
#1502=ELLIPSE('',#104676,0.0365824585612604,0.0343843127629423);
#1503=ELLIPSE('',#104679,20.565803505481,0.575890582176382);
#1504=ELLIPSE('',#104692,0.0682531867095197,0.0644989639523459);
#1505=ELLIPSE('',#104694,0.0752932753387221,0.0683396339846143);
#1506=ELLIPSE('',#104696,0.0365824585612599,0.0343843127629417);
#1507=ELLIPSE('',#104697,0.0365824585612599,0.0343843127629417);
#1508=ELLIPSE('',#104700,20.5648309710559,0.575873292072556);
#1509=ELLIPSE('',#104713,0.0682531867074291,0.0644989639509719);
#1510=ELLIPSE('',#104715,0.0752932753429965,0.0683396339866554);
#1511=ELLIPSE('',#104717,0.0365824585612629,0.0343843127629425);
#1512=ELLIPSE('',#104718,0.0365824585612629,0.0343843127629425);
#1513=ELLIPSE('',#104721,20.5669825590435,0.57591154955311);
#1514=ELLIPSE('',#104734,0.0682531867130314,0.0644989639545135);
#1515=ELLIPSE('',#104736,0.0752932753441584,0.0683396339872419);
#1516=ELLIPSE('',#104738,0.0365824585612645,0.0343843127629429);
#1517=ELLIPSE('',#104739,0.0365824585612645,0.0343843127629429);
#1518=ELLIPSE('',#104742,20.5662483858826,0.575898493672706);
#1519=ELLIPSE('',#104755,0.0682531867098831,0.0644989639526421);
#1520=ELLIPSE('',#104757,0.0752932753409068,0.0683396339856623);
#1521=ELLIPSE('',#104759,0.0365824585612578,0.034384312762941);
#1522=ELLIPSE('',#104760,0.0365824585612578,0.034384312762941);
#1523=ELLIPSE('',#104763,20.5670224417481,0.575912258561078);
#1524=ELLIPSE('',#104776,0.0682531867061702,0.064498963950201);
#1525=ELLIPSE('',#104778,0.0752932753411104,0.068339633985768);
#1526=ELLIPSE('',#104780,0.0365824585612508,0.0343843127629396);
#1527=ELLIPSE('',#104781,0.0365824585612508,0.0343843127629396);
#1528=ELLIPSE('',#104784,20.5655347324022,0.575885805162513);
#1529=ELLIPSE('',#104797,0.0682531867118699,0.06449896395374);
#1530=ELLIPSE('',#104799,0.0752932753373313,0.068339633983908);
#1531=ELLIPSE('',#104801,0.0365824585612802,0.0343843127629466);
#1532=ELLIPSE('',#104802,0.0365824585612802,0.0343843127629466);
#1533=ELLIPSE('',#104805,20.5668284617458,0.575908795317053);
#1534=ELLIPSE('',#104818,0.0682531867127595,0.0644989639543824);
#1535=ELLIPSE('',#104820,0.0752932753396919,0.0683396339850703);
#1536=ELLIPSE('',#104822,0.0365824585612809,0.0343843127629465);
#1537=ELLIPSE('',#104823,0.0365824585612809,0.0343843127629465);
#1538=ELLIPSE('',#104826,20.5660203821645,0.575894443446422);
#1539=ELLIPSE('',#104839,0.0682531867122131,0.0644989639539199);
#1540=ELLIPSE('',#104841,0.0752932753438411,0.0683396339870888);
#1541=ELLIPSE('',#104843,0.0365824585612538,0.0343843127629404);
#1542=ELLIPSE('',#104844,0.0365824585612538,0.0343843127629404);
#1543=ELLIPSE('',#104847,20.56719128229,0.575915266446949);
#1544=ELLIPSE('',#104860,0.0682531867057307,0.0644989639499098);
#1545=ELLIPSE('',#104862,0.0752932753421604,0.0683396339862518);
#1546=ELLIPSE('',#104864,0.0365824585612703,0.0343843127629442);
#1547=ELLIPSE('',#104865,0.0365824585612703,0.0343843127629442);
#1548=ELLIPSE('',#104868,20.5659951690371,0.575893990843115);
#1549=ELLIPSE('',#104881,0.0682531867104656,0.0644989639528107);
#1550=ELLIPSE('',#104883,0.0752932753453524,0.0683396339878613);
#1551=ELLIPSE('',#104885,0.0365824585612831,0.0343843127629476);
#1552=ELLIPSE('',#104886,0.0365824585612831,0.0343843127629476);
#1553=ELLIPSE('',#104889,20.5657598820384,0.575889811600635);
#1554=ELLIPSE('',#104902,0.0682531867127301,0.0644989639542877);
#1555=ELLIPSE('',#104904,0.0752932753397943,0.0683396339851374);
#1556=ELLIPSE('',#104906,0.0365824585612655,0.0343843127629432);
#1557=ELLIPSE('',#104907,0.0365824585612655,0.0343843127629432);
#1558=ELLIPSE('',#104910,20.5670517301527,0.575912785764959);
#1559=ELLIPSE('',#104923,0.0682531867142145,0.0644989639552584);
#1560=ELLIPSE('',#104925,0.0752932753421681,0.0683396339862674);
#1561=ELLIPSE('',#104927,0.0365824585612741,0.0343843127629453);
#1562=ELLIPSE('',#104928,0.0365824585612741,0.0343843127629453);
#1563=ELLIPSE('',#104931,20.5676060497922,0.575922623380279);
#1564=ELLIPSE('',#104944,0.0682531867068906,0.0644989639506861);
#1565=ELLIPSE('',#104946,0.0752932753417022,0.0683396339860361);
#1566=ELLIPSE('',#104948,0.0365824585612606,0.0343843127629421);
#1567=ELLIPSE('',#104949,0.0365824585612606,0.0343843127629421);
#1568=ELLIPSE('',#104952,20.5663132227207,0.575899648889507);
#1569=ELLIPSE('',#104965,0.0682531867059857,0.064498963949947);
#1570=ELLIPSE('',#104967,0.0752932753409169,0.0683396339856948);
#1571=ELLIPSE('',#104969,0.0365824585612755,0.0343843127629457);
#1572=ELLIPSE('',#104970,0.0365824585612755,0.0343843127629457);
#1573=ELLIPSE('',#104973,20.5655942010141,0.575886853588054);
#1574=ELLIPSE('',#104986,0.0682531867157525,0.0644989639562768);
#1575=ELLIPSE('',#104988,0.0752932753414462,0.0683396339859915);
#1576=ELLIPSE('',#104990,0.0365824585612798,0.0343843127629466);
#1577=ELLIPSE('',#104991,0.0365824585612798,0.0343843127629466);
#1578=ELLIPSE('',#104994,20.5663123862977,0.575899628805844);
#1579=ELLIPSE('',#105007,0.068253186715127,0.064498963955807);
#1580=ELLIPSE('',#105009,0.0752932753417337,0.0683396339861055);
#1581=ELLIPSE('',#105011,0.0365824585612683,0.0343843127629441);
#1582=ELLIPSE('',#105012,0.0365824585612683,0.0343843127629441);
#1583=ELLIPSE('',#105015,20.5655922399963,0.575886817441797);
#1584=ELLIPSE('',#105028,0.0682531867100915,0.0644989639525808);
#1585=ELLIPSE('',#105030,0.0752932753384642,0.0683396339845221);
#1586=ELLIPSE('',#105032,0.0365824585612694,0.0343843127629441);
#1587=ELLIPSE('',#105033,0.0365824585612694,0.0343843127629441);
#1588=ELLIPSE('',#105036,20.5655714685528,0.575886444727038);
#1589=ELLIPSE('',#105049,0.0682531867063946,0.0644989639502737);
#1590=ELLIPSE('',#105051,0.0752932753406007,0.068339633985507);
#1591=ELLIPSE('',#105053,0.0365824585612642,0.034384312762943);
#1592=ELLIPSE('',#105054,0.0365824585612642,0.034384312762943);
#1593=ELLIPSE('',#105057,20.5655513367587,0.575886094758606);
#1594=ELLIPSE('',#105070,0.0682531867133225,0.064498963954612);
#1595=ELLIPSE('',#105072,0.0752932753383297,0.0683396339844693);
#1596=ELLIPSE('',#105074,0.0365824585612559,0.0343843127629409);
#1597=ELLIPSE('',#105075,0.0365824585612559,0.0343843127629409);
#1598=ELLIPSE('',#105078,20.5653884221969,0.575883206356478);
#1599=ELLIPSE('',#105091,0.0682531867116082,0.0644989639535029);
#1600=ELLIPSE('',#105093,0.0752932753428825,0.0683396339866211);
#1601=ELLIPSE('',#105095,0.0365824585612799,0.0343843127629468);
#1602=ELLIPSE('',#105096,0.0365824585612799,0.0343843127629468);
#1603=ELLIPSE('',#105099,20.5654095917158,0.575883579934909);
#1604=ELLIPSE('',#105112,0.0682531867092451,0.0644989639521952);
#1605=ELLIPSE('',#105114,0.0752932753342181,0.068339633982504);
#1606=ELLIPSE('',#105116,0.036582458561269,0.0343843127629441);
#1607=ELLIPSE('',#105117,0.036582458561269,0.0343843127629441);
#1608=ELLIPSE('',#105120,20.5668717945422,0.57590955878625);
#1609=ELLIPSE('',#105133,0.0682531867087737,0.0644989639517802);
#1610=ELLIPSE('',#105135,0.075293275340429,0.068339633985475);
#1611=ELLIPSE('',#105137,0.0365824585612684,0.0343843127629437);
#1612=ELLIPSE('',#105138,0.0365824585612684,0.0343843127629437);
#1613=ELLIPSE('',#105141,20.5665469813456,0.575903803880655);
#1614=ELLIPSE('',#105154,0.0682531867062315,0.0644989639502229);
#1615=ELLIPSE('',#105156,0.0752932753417253,0.0683396339860757);
#1616=ELLIPSE('',#105158,0.0365824585612617,0.0343843127629423);
#1617=ELLIPSE('',#105159,0.0365824585612617,0.0343843127629423);
#1618=ELLIPSE('',#105162,20.5651929436534,0.575879730590434);
#2064=TOROIDAL_SURFACE('',#102728,2.728,0.022);
#2065=TOROIDAL_SURFACE('',#102733,2.728,0.022);
#2066=TOROIDAL_SURFACE('',#102738,2.728,0.022);
#2067=TOROIDAL_SURFACE('',#102743,2.728,0.022);
#2068=TOROIDAL_SURFACE('',#102748,2.728,0.022);
#2069=TOROIDAL_SURFACE('',#102753,2.728,0.022);
#2070=TOROIDAL_SURFACE('',#102758,2.728,0.022);
#2071=TOROIDAL_SURFACE('',#102763,2.728,0.022);
#2072=TOROIDAL_SURFACE('',#102768,2.728,0.022);
#2073=TOROIDAL_SURFACE('',#102773,2.728,0.022);
#2074=TOROIDAL_SURFACE('',#102778,2.728,0.022);
#2075=TOROIDAL_SURFACE('',#102783,2.728,0.022);
#2076=TOROIDAL_SURFACE('',#102788,2.728,0.022);
#2077=TOROIDAL_SURFACE('',#102793,2.728,0.022);
#2078=TOROIDAL_SURFACE('',#102798,2.728,0.022);
#2079=TOROIDAL_SURFACE('',#102803,2.728,0.022);
#2080=TOROIDAL_SURFACE('',#102808,2.728,0.022);
#2081=TOROIDAL_SURFACE('',#102813,2.728,0.022);
#2082=TOROIDAL_SURFACE('',#102818,2.728,0.022);
#2083=TOROIDAL_SURFACE('',#102823,2.728,0.022);
#2084=TOROIDAL_SURFACE('',#102828,2.728,0.022);
#2085=TOROIDAL_SURFACE('',#102833,2.728,0.022);
#2086=TOROIDAL_SURFACE('',#102838,2.728,0.022);
#2087=TOROIDAL_SURFACE('',#102843,2.728,0.022);
#2088=TOROIDAL_SURFACE('',#102848,2.728,0.022);
#2089=TOROIDAL_SURFACE('',#102853,2.728,0.022);
#2090=TOROIDAL_SURFACE('',#102858,2.728,0.022);
#2091=TOROIDAL_SURFACE('',#102863,2.728,0.022);
#2092=TOROIDAL_SURFACE('',#102868,2.728,0.022);
#2093=TOROIDAL_SURFACE('',#102873,2.728,0.022);
#2094=TOROIDAL_SURFACE('',#102878,2.728,0.022);
#2095=TOROIDAL_SURFACE('',#102883,2.728,0.022);
#2096=TOROIDAL_SURFACE('',#102888,2.728,0.022);
#2097=TOROIDAL_SURFACE('',#102893,2.728,0.022);
#2098=TOROIDAL_SURFACE('',#102898,2.728,0.022);
#2099=TOROIDAL_SURFACE('',#102903,2.728,0.022);
#2100=TOROIDAL_SURFACE('',#102908,2.728,0.022);
#2101=TOROIDAL_SURFACE('',#102913,2.728,0.022);
#2102=TOROIDAL_SURFACE('',#102918,2.728,0.022);
#2103=TOROIDAL_SURFACE('',#102923,2.728,0.022);
#2104=TOROIDAL_SURFACE('',#102928,2.728,0.022);
#2105=TOROIDAL_SURFACE('',#102933,2.728,0.022);
#2106=TOROIDAL_SURFACE('',#102938,2.728,0.022);
#2107=TOROIDAL_SURFACE('',#102943,2.728,0.022);
#2108=TOROIDAL_SURFACE('',#102948,2.728,0.022);
#2109=TOROIDAL_SURFACE('',#102953,2.728,0.022);
#2110=TOROIDAL_SURFACE('',#102958,2.728,0.022);
#2111=TOROIDAL_SURFACE('',#102963,2.728,0.022);
#2112=TOROIDAL_SURFACE('',#102968,2.728,0.022);
#2113=TOROIDAL_SURFACE('',#102973,2.728,0.022);
#2114=TOROIDAL_SURFACE('',#102978,2.728,0.022);
#2115=TOROIDAL_SURFACE('',#102983,2.728,0.022);
#2116=TOROIDAL_SURFACE('',#102988,2.728,0.022);
#2117=TOROIDAL_SURFACE('',#102993,2.728,0.022);
#2118=TOROIDAL_SURFACE('',#102998,2.728,0.022);
#2119=TOROIDAL_SURFACE('',#103003,2.728,0.022);
#2120=TOROIDAL_SURFACE('',#103008,2.728,0.022);
#2121=TOROIDAL_SURFACE('',#103013,2.728,0.022);
#2122=TOROIDAL_SURFACE('',#103018,2.728,0.022);
#2123=TOROIDAL_SURFACE('',#103023,2.728,0.022);
#2124=TOROIDAL_SURFACE('',#103028,2.728,0.022);
#2125=TOROIDAL_SURFACE('',#103033,2.728,0.022);
#2126=TOROIDAL_SURFACE('',#103038,2.728,0.022);
#2127=TOROIDAL_SURFACE('',#103043,2.728,0.022);
#2128=TOROIDAL_SURFACE('',#103048,2.728,0.022);
#2129=TOROIDAL_SURFACE('',#103053,2.728,0.022);
#2130=TOROIDAL_SURFACE('',#103058,2.728,0.022);
#2131=TOROIDAL_SURFACE('',#103063,2.728,0.022);
#2132=TOROIDAL_SURFACE('',#103068,2.728,0.022);
#2133=TOROIDAL_SURFACE('',#103073,2.728,0.022);
#2134=TOROIDAL_SURFACE('',#103078,2.728,0.022);
#2135=TOROIDAL_SURFACE('',#103083,2.728,0.022);
#2136=TOROIDAL_SURFACE('',#103088,2.728,0.022);
#2137=TOROIDAL_SURFACE('',#103093,2.728,0.022);
#2138=TOROIDAL_SURFACE('',#103098,2.728,0.022);
#2139=TOROIDAL_SURFACE('',#103103,2.728,0.022);
#2140=TOROIDAL_SURFACE('',#103108,2.728,0.022);
#2141=TOROIDAL_SURFACE('',#103129,2.49354920651122,0.0879999999999989);
#2142=TOROIDAL_SURFACE('',#103135,2.662,0.088000000000018);
#2143=TOROIDAL_SURFACE('',#103219,2.49354920651117,0.0879999999999994);
#2144=TOROIDAL_SURFACE('',#103300,2.662,0.0879999999999984);
#2145=TOROIDAL_SURFACE('',#103303,2.662,0.0879999999999984);
#2146=TOROIDAL_SURFACE('',#103306,2.662,0.0879999999999984);
#2147=TOROIDAL_SURFACE('',#103309,2.662,0.0879999999999984);
#2148=TOROIDAL_SURFACE('',#103312,2.662,0.0879999999999984);
#2149=TOROIDAL_SURFACE('',#103315,2.662,0.0879999999999984);
#2150=TOROIDAL_SURFACE('',#103318,2.662,0.0879999999999984);
#2151=TOROIDAL_SURFACE('',#103321,2.662,0.0879999999999984);
#2152=TOROIDAL_SURFACE('',#103324,2.662,0.0879999999999984);
#2153=TOROIDAL_SURFACE('',#103327,2.662,0.0879999999999984);
#2154=TOROIDAL_SURFACE('',#103330,2.662,0.0879999999999984);
#2155=TOROIDAL_SURFACE('',#103333,2.662,0.0879999999999984);
#2156=TOROIDAL_SURFACE('',#103336,2.662,0.0879999999999984);
#2157=TOROIDAL_SURFACE('',#103339,2.662,0.0879999999999984);
#2158=TOROIDAL_SURFACE('',#103342,2.662,0.0879999999999984);
#2159=TOROIDAL_SURFACE('',#103345,2.662,0.0879999999999984);
#2160=TOROIDAL_SURFACE('',#103348,2.662,0.0879999999999984);
#2161=TOROIDAL_SURFACE('',#103351,2.662,0.0879999999999984);
#2162=TOROIDAL_SURFACE('',#103354,2.662,0.0879999999999984);
#2163=TOROIDAL_SURFACE('',#103357,2.662,0.0879999999999984);
#2164=TOROIDAL_SURFACE('',#103360,2.662,0.0879999999999984);
#2165=TOROIDAL_SURFACE('',#103363,2.662,0.0879999999999984);
#2166=TOROIDAL_SURFACE('',#103366,2.662,0.0879999999999984);
#2167=TOROIDAL_SURFACE('',#103369,2.662,0.0879999999999984);
#2168=TOROIDAL_SURFACE('',#103372,2.662,0.0879999999999984);
#2169=TOROIDAL_SURFACE('',#103375,2.662,0.0879999999999984);
#2170=TOROIDAL_SURFACE('',#103378,2.662,0.0879999999999984);
#2171=TOROIDAL_SURFACE('',#103381,2.662,0.0879999999999984);
#2172=TOROIDAL_SURFACE('',#103384,2.662,0.0879999999999984);
#2173=TOROIDAL_SURFACE('',#103387,2.662,0.0879999999999984);
#2174=TOROIDAL_SURFACE('',#103390,2.662,0.0879999999999984);
#2175=TOROIDAL_SURFACE('',#103393,2.662,0.0879999999999984);
#2176=TOROIDAL_SURFACE('',#103396,2.662,0.0879999999999984);
#2177=TOROIDAL_SURFACE('',#103399,2.662,0.0879999999999984);
#2178=TOROIDAL_SURFACE('',#103402,2.662,0.0879999999999984);
#2179=TOROIDAL_SURFACE('',#103405,2.662,0.0879999999999984);
#2180=TOROIDAL_SURFACE('',#103408,2.662,0.0879999999999984);
#2181=TOROIDAL_SURFACE('',#103411,2.662,0.0879999999999984);
#2182=TOROIDAL_SURFACE('',#103414,2.662,0.0879999999999984);
#2183=TOROIDAL_SURFACE('',#103417,2.662,0.0879999999999984);
#2184=TOROIDAL_SURFACE('',#103420,2.662,0.0879999999999984);
#2185=TOROIDAL_SURFACE('',#103423,2.662,0.0879999999999984);
#2186=TOROIDAL_SURFACE('',#103426,2.662,0.0879999999999984);
#2187=TOROIDAL_SURFACE('',#103429,2.662,0.0879999999999984);
#2188=TOROIDAL_SURFACE('',#103432,2.662,0.0879999999999984);
#2189=TOROIDAL_SURFACE('',#103435,2.662,0.0879999999999984);
#2190=TOROIDAL_SURFACE('',#103438,2.662,0.0879999999999984);
#2191=TOROIDAL_SURFACE('',#103441,2.662,0.0879999999999984);
#2192=TOROIDAL_SURFACE('',#103444,2.662,0.0879999999999984);
#2193=TOROIDAL_SURFACE('',#103447,2.662,0.0879999999999984);
#2194=TOROIDAL_SURFACE('',#103450,2.662,0.0879999999999984);
#2195=TOROIDAL_SURFACE('',#103453,2.662,0.0879999999999984);
#2196=TOROIDAL_SURFACE('',#103456,2.662,0.0879999999999984);
#2197=TOROIDAL_SURFACE('',#103459,2.662,0.0879999999999984);
#2198=TOROIDAL_SURFACE('',#103462,2.662,0.0879999999999984);
#2199=TOROIDAL_SURFACE('',#103465,2.662,0.0879999999999984);
#2200=TOROIDAL_SURFACE('',#103468,2.662,0.0879999999999984);
#2201=TOROIDAL_SURFACE('',#103471,2.662,0.0879999999999984);
#2202=TOROIDAL_SURFACE('',#103474,2.662,0.0879999999999984);
#2203=TOROIDAL_SURFACE('',#103477,2.662,0.0879999999999984);
#2204=TOROIDAL_SURFACE('',#103480,2.662,0.0879999999999984);
#2205=TOROIDAL_SURFACE('',#103483,2.662,0.0879999999999984);
#2206=TOROIDAL_SURFACE('',#103486,2.662,0.0879999999999984);
#2207=TOROIDAL_SURFACE('',#103489,2.662,0.0879999999999984);
#2208=TOROIDAL_SURFACE('',#103492,2.662,0.0879999999999984);
#2209=TOROIDAL_SURFACE('',#103495,2.662,0.0879999999999984);
#2210=TOROIDAL_SURFACE('',#103498,2.662,0.0879999999999984);
#2211=TOROIDAL_SURFACE('',#103501,2.662,0.0879999999999984);
#2212=TOROIDAL_SURFACE('',#103504,2.662,0.0879999999999984);
#2213=TOROIDAL_SURFACE('',#103507,2.662,0.0879999999999984);
#2214=TOROIDAL_SURFACE('',#103510,2.662,0.0879999999999984);
#2215=TOROIDAL_SURFACE('',#103513,2.662,0.0879999999999984);
#2216=TOROIDAL_SURFACE('',#103516,2.662,0.0879999999999984);
#2217=TOROIDAL_SURFACE('',#103519,2.662,0.0879999999999984);
#2218=TOROIDAL_SURFACE('',#103522,2.662,0.0879999999999984);
#2219=TOROIDAL_SURFACE('',#103525,2.662,0.0879999999999984);
#2220=TOROIDAL_SURFACE('',#103547,2.662,0.0879999999999984);
#3301=(
BOUNDED_SURFACE()
B_SPLINE_SURFACE(1,2,((#420151,#420152,#420153,#420154,#420155,#420156,
#420157,#420158,#420159,#420160,#420161,#420162,#420163,#420164,#420165,
#420166,#420167,#420168,#420169,#420170,#420171,#420172,#420173,#420174,
#420175,#420176,#420177,#420178,#420179,#420180,#420181,#420182,#420183,
#420184,#420185,#420186,#420187,#420188,#420189,#420190,#420191,#420192,
#420193,#420194,#420195,#420196,#420197,#420198,#420199,#420200,#420201,
#420202,#420203,#420204,#420205,#420206,#420207,#420208,#420209,#420210,
#420211,#420212,#420213,#420214,#420215,#420216,#420217,#420218,#420219,
#420220,#420221,#420222,#420223,#420224,#420225,#420226,#420227,#420228,
#420229,#420230,#420231,#420232,#420233,#420234,#420235,#420236,#420237,
#420238,#420239,#420240,#420241,#420242,#420243,#420244,#420245,#420246,
#420247,#420248,#420249,#420250,#420251,#420252,#420253,#420254,#420255,
#420256,#420257,#420258,#420259,#420260,#420261,#420262,#420263,#420264,
#420265,#420266,#420267,#420268,#420269,#420270,#420271,#420272,#420273,
#420274,#420275,#420276,#420277,#420278,#420279,#420280,#420281,#420282,
#420283,#420284,#420285,#420286,#420287,#420288,#420289,#420290,#420291,
#420292,#420293,#420294,#420295,#420296,#420297,#420298,#420299,#420300,
#420301,#420302,#420303,#420304,#420305,#420306,#420307,#420308,#420309,
#420310,#420311,#420312,#420313,#420314,#420315,#420316,#420317,#420318,
#420319,#420320,#420321,#420322,#420323,#420324,#420325,#420326,#420327,
#420328,#420329,#420330,#420331,#420332,#420333,#420334,#420335,#420336,
#420337,#420338,#420339,#420340,#420341,#420342,#420343,#420344,#420345,
#420346,#420347,#420348,#420349,#420350,#420351,#420352,#420353,#420354,
#420355,#420356,#420357,#420358,#420359,#420360,#420361,#420362,#420363,
#420364,#420365,#420366,#420367,#420368,#420369,#420370,#420371,#420372,
#420373,#420374,#420375,#420376,#420377,#420378,#420379,#420380,#420381,
#420382,#420383,#420384,#420385,#420386,#420387,#420388,#420389,#420390,
#420391,#420392,#420393,#420394,#420395,#420396,#420397,#420398,#420399,
#420400,#420401,#420402,#420403,#420404,#420405,#420406,#420407,#420408,
#420409,#420410,#420411,#420412,#420413,#420414,#420415,#420416,#420417,
#420418,#420419,#420420,#420421,#420422,#420423,#420424,#420425,#420426,
#420427,#420428,#420429,#420430,#420431,#420432,#420433,#420434,#420435,
#420436,#420437,#420438,#420439,#420440,#420441,#420442,#420443,#420444,
#420445,#420446,#420447,#420448,#420449,#420450,#420451,#420452,#420453,
#420454,#420455,#420456,#420457,#420458,#420459,#420460,#420461,#420462,
#420463,#420464,#420465,#420466,#420467,#420468,#420469,#420470,#420471,
#420472,#420473,#420474,#420475,#420476,#420477,#420478,#420479,#420480,
#420481,#420482,#420483,#420484,#420485,#420486,#420487,#420488,#420489,
#420490,#420491,#420492,#420493,#420494,#420495,#420496,#420497,#420498,
#420499,#420500,#420501,#420502,#420503,#420504,#420505,#420506,#420507,
#420508,#420509,#420510,#420511,#420512,#420513,#420514,#420515,#420516,
#420517,#420518,#420519,#420520,#420521,#420522,#420523,#420524,#420525,
#420526,#420527,#420528,#420529,#420530,#420531,#420532,#420533,#420534,
#420535,#420536,#420537,#420538,#420539,#420540,#420541,#420542,#420543,
#420544,#420545,#420546,#420547,#420548,#420549,#420550,#420551,#420552,
#420553,#420554,#420555,#420556,#420557,#420558,#420559,#420560,#420561,
#420562,#420563,#420564,#420565,#420566,#420567,#420568,#420569,#420570,
#420571,#420572,#420573,#420574,#420575,#420576,#420577,#420578,#420579,
#420580,#420581,#420582,#420583,#420584,#420585,#420586,#420587,#420588,
#420589,#420590,#420591,#420592,#420593,#420594,#420595,#420596,#420597,
#420598,#420599,#420600,#420601,#420602,#420603,#420604,#420605,#420606,
#420607,#420608,#420609,#420610,#420611,#420612,#420613,#420614,#420615,
#420616,#420617,#420618,#420619,#420620,#420621,#420622,#420623,#420624,
#420625,#420626,#420627,#420628,#420629,#420630,#420631,#420632,#420633,
#420634,#420635,#420636,#420637,#420638,#420639,#420640,#420641,#420642,
#420643,#420644,#420645,#420646,#420647,#420648,#420649,#420650,#420651,
#420652,#420653,#420654,#420655,#420656,#420657,#420658,#420659,#420660,
#420661,#420662,#420663,#420664,#420665,#420666,#420667,#420668,#420669,
#420670,#420671,#420672,#420673,#420674,#420675,#420676,#420677,#420678,
#420679,#420680,#420681,#420682,#420683,#420684,#420685,#420686,#420687,
#420688,#420689,#420690,#420691,#420692,#420693,#420694,#420695,#420696,
#420697,#420698,#420699,#420700,#420701,#420702,#420703,#420704,#420705,
#420706,#420707,#420708,#420709,#420710,#420711,#420712,#420713,#420714,
#420715,#420716,#420717,#420718,#420719,#420720,#420721,#420722,#420723,
#420724,#420725,#420726,#420727,#420728,#420729,#420730,#420731,#420732,
#420733,#420734,#420735,#420736,#420737,#420738,#420739,#420740,#420741,
#420742,#420743,#420744,#420745,#420746,#420747,#420748,#420749,#420750,
#420751,#420752,#420753,#420754,#420755,#420756,#420757,#420758,#420759,
#420760,#420761,#420762,#420763),(#420764,#420765,#420766,#420767,#420768,
#420769,#420770,#420771,#420772,#420773,#420774,#420775,#420776,#420777,
#420778,#420779,#420780,#420781,#420782,#420783,#420784,#420785,#420786,
#420787,#420788,#420789,#420790,#420791,#420792,#420793,#420794,#420795,
#420796,#420797,#420798,#420799,#420800,#420801,#420802,#420803,#420804,
#420805,#420806,#420807,#420808,#420809,#420810,#420811,#420812,#420813,
#420814,#420815,#420816,#420817,#420818,#420819,#420820,#420821,#420822,
#420823,#420824,#420825,#420826,#420827,#420828,#420829,#420830,#420831,
#420832,#420833,#420834,#420835,#420836,#420837,#420838,#420839,#420840,
#420841,#420842,#420843,#420844,#420845,#420846,#420847,#420848,#420849,
#420850,#420851,#420852,#420853,#420854,#420855,#420856,#420857,#420858,
#420859,#420860,#420861,#420862,#420863,#420864,#420865,#420866,#420867,
#420868,#420869,#420870,#420871,#420872,#420873,#420874,#420875,#420876,
#420877,#420878,#420879,#420880,#420881,#420882,#420883,#420884,#420885,
#420886,#420887,#420888,#420889,#420890,#420891,#420892,#420893,#420894,
#420895,#420896,#420897,#420898,#420899,#420900,#420901,#420902,#420903,
#420904,#420905,#420906,#420907,#420908,#420909,#420910,#420911,#420912,
#420913,#420914,#420915,#420916,#420917,#420918,#420919,#420920,#420921,
#420922,#420923,#420924,#420925,#420926,#420927,#420928,#420929,#420930,
#420931,#420932,#420933,#420934,#420935,#420936,#420937,#420938,#420939,
#420940,#420941,#420942,#420943,#420944,#420945,#420946,#420947,#420948,
#420949,#420950,#420951,#420952,#420953,#420954,#420955,#420956,#420957,
#420958,#420959,#420960,#420961,#420962,#420963,#420964,#420965,#420966,
#420967,#420968,#420969,#420970,#420971,#420972,#420973,#420974,#420975,
#420976,#420977,#420978,#420979,#420980,#420981,#420982,#420983,#420984,
#420985,#420986,#420987,#420988,#420989,#420990,#420991,#420992,#420993,
#420994,#420995,#420996,#420997,#420998,#420999,#421000,#421001,#421002,
#421003,#421004,#421005,#421006,#421007,#421008,#421009,#421010,#421011,
#421012,#421013,#421014,#421015,#421016,#421017,#421018,#421019,#421020,
#421021,#421022,#421023,#421024,#421025,#421026,#421027,#421028,#421029,
#421030,#421031,#421032,#421033,#421034,#421035,#421036,#421037,#421038,
#421039,#421040,#421041,#421042,#421043,#421044,#421045,#421046,#421047,
#421048,#421049,#421050,#421051,#421052,#421053,#421054,#421055,#421056,
#421057,#421058,#421059,#421060,#421061,#421062,#421063,#421064,#421065,
#421066,#421067,#421068,#421069,#421070,#421071,#421072,#421073,#421074,
#421075,#421076,#421077,#421078,#421079,#421080,#421081,#421082,#421083,
#421084,#421085,#421086,#421087,#421088,#421089,#421090,#421091,#421092,
#421093,#421094,#421095,#421096,#421097,#421098,#421099,#421100,#421101,
#421102,#421103,#421104,#421105,#421106,#421107,#421108,#421109,#421110,
#421111,#421112,#421113,#421114,#421115,#421116,#421117,#421118,#421119,
#421120,#421121,#421122,#421123,#421124,#421125,#421126,#421127,#421128,
#421129,#421130,#421131,#421132,#421133,#421134,#421135,#421136,#421137,
#421138,#421139,#421140,#421141,#421142,#421143,#421144,#421145,#421146,
#421147,#421148,#421149,#421150,#421151,#421152,#421153,#421154,#421155,
#421156,#421157,#421158,#421159,#421160,#421161,#421162,#421163,#421164,
#421165,#421166,#421167,#421168,#421169,#421170,#421171,#421172,#421173,
#421174,#421175,#421176,#421177,#421178,#421179,#421180,#421181,#421182,
#421183,#421184,#421185,#421186,#421187,#421188,#421189,#421190,#421191,
#421192,#421193,#421194,#421195,#421196,#421197,#421198,#421199,#421200,
#421201,#421202,#421203,#421204,#421205,#421206,#421207,#421208,#421209,
#421210,#421211,#421212,#421213,#421214,#421215,#421216,#421217,#421218,
#421219,#421220,#421221,#421222,#421223,#421224,#421225,#421226,#421227,
#421228,#421229,#421230,#421231,#421232,#421233,#421234,#421235,#421236,
#421237,#421238,#421239,#421240,#421241,#421242,#421243,#421244,#421245,
#421246,#421247,#421248,#421249,#421250,#421251,#421252,#421253,#421254,
#421255,#421256,#421257,#421258,#421259,#421260,#421261,#421262,#421263,
#421264,#421265,#421266,#421267,#421268,#421269,#421270,#421271,#421272,
#421273,#421274,#421275,#421276,#421277,#421278,#421279,#421280,#421281,
#421282,#421283,#421284,#421285,#421286,#421287,#421288,#421289,#421290,
#421291,#421292,#421293,#421294,#421295,#421296,#421297,#421298,#421299,
#421300,#421301,#421302,#421303,#421304,#421305,#421306,#421307,#421308,
#421309,#421310,#421311,#421312,#421313,#421314,#421315,#421316,#421317,
#421318,#421319,#421320,#421321,#421322,#421323,#421324,#421325,#421326,
#421327,#421328,#421329,#421330,#421331,#421332,#421333,#421334,#421335,
#421336,#421337,#421338,#421339,#421340,#421341,#421342,#421343,#421344,
#421345,#421346,#421347,#421348,#421349,#421350,#421351,#421352,#421353,
#421354,#421355,#421356,#421357,#421358,#421359,#421360,#421361,#421362,
#421363,#421364,#421365,#421366,#421367,#421368,#421369,#421370,#421371,
#421372,#421373,#421374,#421375,#421376)),.UNSPECIFIED.,.F.,.F.,.F.)
B_SPLINE_SURFACE_WITH_KNOTS((2,2),(3,2,2,2,2,2,2,2,2,2,2,2,2,2,2,2,2,2,
2,2,2,2,2,2,2,2,2,2,2,2,2,2,2,2,2,2,2,2,2,2,2,2,2,2,2,2,2,2,2,2,2,2,2,2,
2,2,2,2,2,2,2,2,2,2,2,2,2,2,2,2,2,2,2,2,2,2,2,2,2,2,2,2,2,2,2,2,2,2,2,2,
2,2,2,2,2,2,2,2,2,2,2,2,2,2,2,2,2,2,2,2,2,2,2,2,2,2,2,2,2,2,2,2,2,2,2,2,
2,2,2,2,2,2,2,2,2,2,2,2,2,2,2,2,2,2,2,2,2,2,2,2,2,2,2,2,2,2,2,2,2,2,2,2,
2,2,2,2,2,2,2,2,2,2,2,2,2,2,2,2,2,2,2,2,2,2,2,2,2,2,2,2,2,2,2,2,2,2,2,2,
2,2,2,2,2,2,2,2,2,2,2,2,2,2,2,2,2,2,2,2,2,2,2,2,2,2,2,2,2,2,2,2,2,2,2,2,
2,2,2,2,2,2,2,2,2,2,2,2,2,2,2,2,2,2,2,2,2,2,2,2,2,2,2,2,2,2,2,2,2,2,2,2,
2,2,2,2,2,2,2,2,2,2,2,2,2,2,2,2,2,2,2,2,2,2,2,2,2,2,2,2,2,2,2,2,2,2,2,2,
3),(0.,1.00001492288347),(0.,0.00326797385620915,0.0065359477124183,0.00980392156862745,
0.0130718954248366,0.0163398692810458,0.0196078431372549,0.0228758169934641,
0.0261437908496732,0.0294117647058824,0.0326797385620915,0.0359477124183007,
0.0392156862745098,0.042483660130719,0.0457516339869281,0.0490196078431373,
0.0522875816993464,0.0555555555555556,0.0588235294117647,0.0620915032679739,
0.065359477124183,0.0686274509803922,0.0718954248366013,0.0751633986928105,
0.0784313725490196,0.0816993464052288,0.0849673202614379,0.0882352941176471,
0.0915032679738562,0.0947712418300654,0.0980392156862745,0.101307189542484,
0.104575163398693,0.107843137254902,0.111111111111111,0.11437908496732,
0.117647058823529,0.120915032679739,0.124183006535948,0.127450980392157,
0.130718954248366,0.133986928104575,0.137254901960784,0.140522875816993,
0.143790849673203,0.147058823529412,0.150326797385621,0.15359477124183,
0.156862745098039,0.160130718954248,0.163398692810458,0.166666666666667,
0.169934640522876,0.173202614379085,0.176470588235294,0.179738562091503,
0.183006535947712,0.186274509803922,0.189542483660131,0.19281045751634,
0.196078431372549,0.199346405228758,0.202614379084967,0.205882352941176,
0.209150326797386,0.212418300653595,0.215686274509804,0.218954248366013,
0.222222222222222,0.225490196078431,0.228758169934641,0.23202614379085,
0.235294117647059,0.238562091503268,0.241830065359477,0.245098039215686,
0.248366013071895,0.251633986928105,0.254901960784314,0.258169934640523,
0.261437908496732,0.264705882352941,0.26797385620915,0.271241830065359,
0.274509803921569,0.277777777777778,0.281045751633987,0.284313725490196,
0.287581699346405,0.290849673202614,0.294117647058824,0.297385620915033,
0.300653594771242,0.303921568627451,0.30718954248366,0.310457516339869,
0.313725490196078,0.316993464052288,0.320261437908497,0.323529411764706,
0.326797385620915,0.330065359477124,0.333333333333333,0.336601307189543,
0.339869281045752,0.343137254901961,0.34640522875817,0.349673202614379,
0.352941176470588,0.356209150326797,0.359477124183007,0.362745098039216,
0.366013071895425,0.369281045751634,0.372549019607843,0.375816993464052,
0.379084967320261,0.382352941176471,0.38562091503268,0.388888888888889,
0.392156862745098,0.395424836601307,0.398692810457516,0.401960784313726,
0.405228758169935,0.408496732026144,0.411764705882353,0.415032679738562,
0.418300653594771,0.42156862745098,0.42483660130719,0.428104575163399,0.431372549019608,
0.434640522875817,0.437908496732026,0.441176470588235,0.444444444444444,
0.447712418300654,0.450980392156863,0.454248366013072,0.457516339869281,
0.46078431372549,0.464052287581699,0.467320261437909,0.470588235294118,
0.473856209150327,0.477124183006536,0.480392156862745,0.483660130718954,
0.486928104575163,0.490196078431373,0.493464052287582,0.496732026143791,
0.5,0.503267973856209,0.506535947712418,0.509803921568627,0.513071895424837,
0.516339869281046,0.519607843137255,0.522875816993464,0.526143790849673,
0.529411764705882,0.532679738562091,0.535947712418301,0.53921568627451,
0.542483660130719,0.545751633986928,0.549019607843137,0.552287581699346,
0.555555555555556,0.558823529411765,0.562091503267974,0.565359477124183,
0.568627450980392,0.571895424836601,0.57516339869281,0.57843137254902,0.581699346405229,
0.584967320261438,0.588235294117647,0.591503267973856,0.594771241830065,
0.598039215686274,0.601307189542484,0.604575163398693,0.607843137254902,
0.611111111111111,0.61437908496732,0.617647058823529,0.620915032679739,
0.624183006535948,0.627450980392157,0.630718954248366,0.633986928104575,
0.637254901960784,0.640522875816993,0.643790849673203,0.647058823529412,
0.650326797385621,0.65359477124183,0.656862745098039,0.660130718954248,
0.663398692810457,0.666666666666667,0.669934640522876,0.673202614379085,
0.676470588235294,0.679738562091503,0.683006535947712,0.686274509803922,
0.689542483660131,0.69281045751634,0.696078431372549,0.699346405228758,
0.702614379084967,0.705882352941177,0.709150326797386,0.712418300653595,
0.715686274509804,0.718954248366013,0.722222222222222,0.725490196078431,
0.72875816993464,0.73202614379085,0.735294117647059,0.738562091503268,0.741830065359477,
0.745098039215686,0.748366013071895,0.751633986928105,0.754901960784314,
0.758169934640523,0.761437908496732,0.764705882352941,0.76797385620915,
0.77124183006536,0.774509803921569,0.777777777777778,0.781045751633987,
0.784313725490196,0.787581699346405,0.790849673202614,0.794117647058823,
0.797385620915033,0.800653594771242,0.803921568627451,0.80718954248366,
0.810457516339869,0.813725490196078,0.816993464052288,0.820261437908497,
0.823529411764706,0.826797385620915,0.830065359477124,0.833333333333333,
0.836601307189543,0.839869281045752,0.843137254901961,0.84640522875817,
0.849673202614379,0.852941176470588,0.856209150326797,0.859477124183007,
0.862745098039216,0.866013071895425,0.869281045751634,0.872549019607843,
0.875816993464052,0.879084967320261,0.882352941176471,0.88562091503268,
0.888888888888889,0.892156862745098,0.895424836601307,0.898692810457516,
0.901960784313726,0.905228758169935,0.908496732026144,0.911764705882353,
0.915032679738562,0.918300653594771,0.92156862745098,0.92483660130719,0.928104575163399,
0.931372549019608,0.934640522875817,0.937908496732026,0.941176470588235,
0.944444444444444,0.947712418300654,0.950980392156863,0.954248366013072,
0.957516339869281,0.96078431372549,0.964052287581699,0.967320261437909,
0.970588235294118,0.973856209150327,0.977124183006536,0.980392156862745,
0.983660130718954,0.986928104575163,0.990196078431373,0.993464052287582,
0.996732026143791,1.),.UNSPECIFIED.)
GEOMETRIC_REPRESENTATION_ITEM()
RATIONAL_B_SPLINE_SURFACE(((1.,0.866025403784439,1.,0.866025403784439,1.,
0.866025403784439,1.,0.866025403784439,1.,0.866025403784439,1.,0.866025403784439,
1.,0.866025403784439,1.,0.866025403784439,1.,0.866025403784439,1.,0.866025403784439,
1.,0.866025403784439,1.,0.866025403784439,1.,0.866025403784439,1.,0.866025403784439,
1.,0.866025403784439,1.,0.866025403784439,1.,0.866025403784439,1.,0.866025403784439,
1.,0.866025403784439,1.,0.866025403784439,1.,0.866025403784439,1.,0.866025403784439,
1.,0.866025403784439,1.,0.866025403784439,1.,0.866025403784439,1.,0.866025403784439,
1.,0.866025403784439,1.,0.866025403784439,1.,0.866025403784439,1.,0.866025403784439,
1.,0.866025403784439,1.,0.866025403784439,1.,0.866025403784439,1.,0.866025403784439,
1.,0.866025403784439,1.,0.866025403784439,1.,0.866025403784439,1.,0.866025403784439,
1.,0.866025403784439,1.,0.866025403784439,1.,0.866025403784439,1.,0.866025403784439,
1.,0.866025403784439,1.,0.866025403784439,1.,0.866025403784439,1.,0.866025403784439,
1.,0.866025403784439,1.,0.866025403784439,1.,0.866025403784439,1.,0.866025403784439,
1.,0.866025403784439,1.,0.866025403784439,1.,0.866025403784439,1.,0.866025403784439,
1.,0.866025403784439,1.,0.866025403784439,1.,0.866025403784439,1.,0.866025403784439,
1.,0.866025403784439,1.,0.866025403784439,1.,0.866025403784439,1.,0.866025403784439,
1.,0.866025403784439,1.,0.866025403784439,1.,0.866025403784439,1.,0.866025403784439,
1.,0.866025403784439,1.,0.866025403784439,1.,0.866025403784439,1.,0.866025403784439,
1.,0.866025403784439,1.,0.866025403784439,1.,0.866025403784439,1.,0.866025403784439,
1.,0.866025403784439,1.,0.866025403784439,1.,0.866025403784439,1.,0.866025403784439,
1.,0.866025403784439,1.,0.866025403784439,1.,0.866025403784439,1.,0.866025403784439,
1.,0.866025403784439,1.,0.866025403784439,1.,0.866025403784439,1.,0.866025403784439,
1.,0.866025403784439,1.,0.866025403784439,1.,0.866025403784439,1.,0.866025403784439,
1.,0.866025403784439,1.,0.866025403784439,1.,0.866025403784439,1.,0.866025403784439,
1.,0.866025403784439,1.,0.866025403784439,1.,0.866025403784439,1.,0.866025403784439,
1.,0.866025403784439,1.,0.866025403784439,1.,0.866025403784439,1.,0.866025403784439,
1.,0.866025403784439,1.,0.866025403784439,1.,0.866025403784439,1.,0.866025403784439,
1.,0.866025403784439,1.,0.866025403784439,1.,0.866025403784439,1.,0.866025403784439,
1.,0.866025403784439,1.,0.866025403784439,1.,0.866025403784439,1.,0.866025403784439,
1.,0.866025403784439,1.,0.866025403784439,1.,0.866025403784439,1.,0.866025403784439,
1.,0.866025403784439,1.,0.866025403784439,1.,0.866025403784439,1.,0.866025403784439,
1.,0.866025403784439,1.,0.866025403784439,1.,0.866025403784439,1.,0.866025403784439,
1.,0.866025403784439,1.,0.866025403784439,1.,0.866025403784439,1.,0.866025403784439,
1.,0.866025403784439,1.,0.866025403784439,1.,0.866025403784439,1.,0.866025403784439,
1.,0.866025403784439,1.,0.866025403784439,1.,0.866025403784439,1.,0.866025403784439,
1.,0.866025403784439,1.,0.866025403784439,1.,0.866025403784439,1.,0.866025403784439,
1.,0.866025403784439,1.,0.866025403784439,1.,0.866025403784439,1.,0.866025403784439,
1.,0.866025403784439,1.,0.866025403784439,1.,0.866025403784439,1.,0.866025403784439,
1.,0.866025403784439,1.,0.866025403784439,1.,0.866025403784439,1.,0.866025403784439,
1.,0.866025403784439,1.,0.866025403784439,1.,0.866025403784439,1.,0.866025403784439,
1.,0.866025403784439,1.,0.866025403784439,1.,0.866025403784439,1.,0.866025403784439,
1.,0.866025403784439,1.,0.866025403784439,1.,0.866025403784439,1.,0.866025403784439,
1.,0.866025403784439,1.,0.866025403784439,1.,0.866025403784439,1.,0.866025403784439,
1.,0.866025403784439,1.,0.866025403784439,1.,0.866025403784439,1.,0.866025403784439,
1.,0.866025403784439,1.,0.866025403784439,1.,0.866025403784439,1.,0.866025403784439,
1.,0.866025403784439,1.,0.866025403784439,1.,0.866025403784439,1.,0.866025403784439,
1.,0.866025403784439,1.,0.866025403784439,1.,0.866025403784439,1.,0.866025403784439,
1.,0.866025403784439,1.,0.866025403784439,1.,0.866025403784439,1.,0.866025403784439,
1.,0.866025403784439,1.,0.866025403784439,1.,0.866025403784439,1.,0.866025403784439,
1.,0.866025403784439,1.,0.866025403784439,1.,0.866025403784439,1.,0.866025403784439,
1.,0.866025403784439,1.,0.866025403784439,1.,0.866025403784439,1.,0.866025403784439,
1.,0.866025403784439,1.,0.866025403784439,1.,0.866025403784439,1.,0.866025403784439,
1.,0.866025403784439,1.,0.866025403784439,1.,0.866025403784439,1.,0.866025403784439,
1.,0.866025403784439,1.,0.866025403784439,1.,0.866025403784439,1.,0.866025403784439,
1.,0.866025403784439,1.,0.866025403784439,1.,0.866025403784439,1.,0.866025403784439,
1.,0.866025403784439,1.,0.866025403784439,1.,0.866025403784439,1.,0.866025403784439,
1.,0.866025403784439,1.,0.866025403784439,1.,0.866025403784439,1.,0.866025403784439,
1.,0.866025403784439,1.,0.866025403784439,1.,0.866025403784439,1.,0.866025403784439,
1.,0.866025403784439,1.,0.866025403784439,1.,0.866025403784439,1.,0.866025403784439,
1.,0.866025403784439,1.,0.866025403784439,1.,0.866025403784439,1.,0.866025403784439,
1.,0.866025403784439,1.,0.866025403784439,1.,0.866025403784439,1.,0.866025403784439,
1.,0.866025403784439,1.,0.866025403784439,1.,0.866025403784439,1.,0.866025403784439,
1.,0.866025403784439,1.,0.866025403784439,1.,0.866025403784439,1.,0.866025403784439,
1.,0.866025403784439,1.,0.866025403784439,1.,0.866025403784439,1.,0.866025403784439,
1.,0.866025403784439,1.,0.866025403784439,1.,0.866025403784439,1.,0.866025403784439,
1.,0.866025403784439,1.,0.866025403784439,1.,0.866025403784439,1.,0.866025403784439,
1.,0.866025403784439,1.,0.866025403784439,1.,0.866025403784439,1.,0.866025403784439,
1.,0.866025403784439,1.,0.866025403784439,1.,0.866025403784439,1.,0.866025403784439,
1.,0.866025403784439,1.,0.866025403784439,1.,0.866025403784439,1.,0.866025403784439,
1.,0.866025403784439,1.,0.866025403784439,1.,0.866025403784439,1.,0.866025403784439,
1.,0.866025403784439,1.,0.866025403784439,1.,0.866025403784439,1.,0.866025403784439,
1.,0.866025403784439,1.,0.866025403784439,1.,0.866025403784439,1.,0.866025403784439,
1.,0.866025403784439,1.,0.866025403784439,1.,0.866025403784439,1.,0.866025403784439,
1.,0.866025403784439,1.,0.866025403784439,1.,0.866025403784439,1.,0.866025403784439,
1.,0.866025403784439,1.,0.866025403784439,1.,0.866025403784439,1.,0.866025403784439,
1.,0.866025403784439,1.,0.866025403784439,1.,0.866025403784439,1.,0.866025403784439,
1.,0.866025403784439,1.,0.866025403784439,1.,0.866025403784439,1.,0.866025403784439,
1.),(1.,0.866025403784439,1.,0.866025403784439,1.,0.866025403784439,1.,
0.866025403784439,1.,0.866025403784439,1.,0.866025403784439,1.,0.866025403784439,
1.,0.866025403784439,1.,0.866025403784439,1.,0.866025403784439,1.,0.866025403784439,
1.,0.866025403784439,1.,0.866025403784439,1.,0.866025403784439,1.,0.866025403784439,
1.,0.866025403784439,1.,0.866025403784439,1.,0.866025403784439,1.,0.866025403784439,
1.,0.866025403784439,1.,0.866025403784439,1.,0.866025403784439,1.,0.866025403784439,
1.,0.866025403784439,1.,0.866025403784439,1.,0.866025403784439,1.,0.866025403784439,
1.,0.866025403784439,1.,0.866025403784439,1.,0.866025403784439,1.,0.866025403784439,
1.,0.866025403784439,1.,0.866025403784439,1.,0.866025403784439,1.,0.866025403784439,
1.,0.866025403784439,1.,0.866025403784439,1.,0.866025403784439,1.,0.866025403784439,
1.,0.866025403784439,1.,0.866025403784439,1.,0.866025403784439,1.,0.866025403784439,
1.,0.866025403784439,1.,0.866025403784439,1.,0.866025403784439,1.,0.866025403784439,
1.,0.866025403784439,1.,0.866025403784439,1.,0.866025403784439,1.,0.866025403784439,
1.,0.866025403784439,1.,0.866025403784439,1.,0.866025403784439,1.,0.866025403784439,
1.,0.866025403784439,1.,0.866025403784439,1.,0.866025403784439,1.,0.866025403784439,
1.,0.866025403784439,1.,0.866025403784439,1.,0.866025403784439,1.,0.866025403784439,
1.,0.866025403784439,1.,0.866025403784439,1.,0.866025403784439,1.,0.866025403784439,
1.,0.866025403784439,1.,0.866025403784439,1.,0.866025403784439,1.,0.866025403784439,
1.,0.866025403784439,1.,0.866025403784439,1.,0.866025403784439,1.,0.866025403784439,
1.,0.866025403784439,1.,0.866025403784439,1.,0.866025403784439,1.,0.866025403784439,
1.,0.866025403784439,1.,0.866025403784439,1.,0.866025403784439,1.,0.866025403784439,
1.,0.866025403784439,1.,0.866025403784439,1.,0.866025403784439,1.,0.866025403784439,
1.,0.866025403784439,1.,0.866025403784439,1.,0.866025403784439,1.,0.866025403784439,
1.,0.866025403784439,1.,0.866025403784439,1.,0.866025403784439,1.,0.866025403784439,
1.,0.866025403784439,1.,0.866025403784439,1.,0.866025403784439,1.,0.866025403784439,
1.,0.866025403784439,1.,0.866025403784439,1.,0.866025403784439,1.,0.866025403784439,
1.,0.866025403784439,1.,0.866025403784439,1.,0.866025403784439,1.,0.866025403784439,
1.,0.866025403784439,1.,0.866025403784439,1.,0.866025403784439,1.,0.866025403784439,
1.,0.866025403784439,1.,0.866025403784439,1.,0.866025403784439,1.,0.866025403784439,
1.,0.866025403784439,1.,0.866025403784439,1.,0.866025403784439,1.,0.866025403784439,
1.,0.866025403784439,1.,0.866025403784439,1.,0.866025403784439,1.,0.866025403784439,
1.,0.866025403784439,1.,0.866025403784439,1.,0.866025403784439,1.,0.866025403784439,
1.,0.866025403784439,1.,0.866025403784439,1.,0.866025403784439,1.,0.866025403784439,
1.,0.866025403784439,1.,0.866025403784439,1.,0.866025403784439,1.,0.866025403784439,
1.,0.866025403784439,1.,0.866025403784439,1.,0.866025403784439,1.,0.866025403784439,
1.,0.866025403784439,1.,0.866025403784439,1.,0.866025403784439,1.,0.866025403784439,
1.,0.866025403784439,1.,0.866025403784439,1.,0.866025403784439,1.,0.866025403784439,
1.,0.866025403784439,1.,0.866025403784439,1.,0.866025403784439,1.,0.866025403784439,
1.,0.866025403784439,1.,0.866025403784439,1.,0.866025403784439,1.,0.866025403784439,
1.,0.866025403784439,1.,0.866025403784439,1.,0.866025403784439,1.,0.866025403784439,
1.,0.866025403784439,1.,0.866025403784439,1.,0.866025403784439,1.,0.866025403784439,
1.,0.866025403784439,1.,0.866025403784439,1.,0.866025403784439,1.,0.866025403784439,
1.,0.866025403784439,1.,0.866025403784439,1.,0.866025403784439,1.,0.866025403784439,
1.,0.866025403784439,1.,0.866025403784439,1.,0.866025403784439,1.,0.866025403784439,
1.,0.866025403784439,1.,0.866025403784439,1.,0.866025403784439,1.,0.866025403784439,
1.,0.866025403784439,1.,0.866025403784439,1.,0.866025403784439,1.,0.866025403784439,
1.,0.866025403784439,1.,0.866025403784439,1.,0.866025403784439,1.,0.866025403784439,
1.,0.866025403784439,1.,0.866025403784439,1.,0.866025403784439,1.,0.866025403784439,
1.,0.866025403784439,1.,0.866025403784439,1.,0.866025403784439,1.,0.866025403784439,
1.,0.866025403784439,1.,0.866025403784439,1.,0.866025403784439,1.,0.866025403784439,
1.,0.866025403784439,1.,0.866025403784439,1.,0.866025403784439,1.,0.866025403784439,
1.,0.866025403784439,1.,0.866025403784439,1.,0.866025403784439,1.,0.866025403784439,
1.,0.866025403784439,1.,0.866025403784439,1.,0.866025403784439,1.,0.866025403784439,
1.,0.866025403784439,1.,0.866025403784439,1.,0.866025403784439,1.,0.866025403784439,
1.,0.866025403784439,1.,0.866025403784439,1.,0.866025403784439,1.,0.866025403784439,
1.,0.866025403784439,1.,0.866025403784439,1.,0.866025403784439,1.,0.866025403784439,
1.,0.866025403784439,1.,0.866025403784439,1.,0.866025403784439,1.,0.866025403784439,
1.,0.866025403784439,1.,0.866025403784439,1.,0.866025403784439,1.,0.866025403784439,
1.,0.866025403784439,1.,0.866025403784439,1.,0.866025403784439,1.,0.866025403784439,
1.,0.866025403784439,1.,0.866025403784439,1.,0.866025403784439,1.,0.866025403784439,
1.,0.866025403784439,1.,0.866025403784439,1.,0.866025403784439,1.,0.866025403784439,
1.,0.866025403784439,1.,0.866025403784439,1.,0.866025403784439,1.,0.866025403784439,
1.,0.866025403784439,1.,0.866025403784439,1.,0.866025403784439,1.,0.866025403784439,
1.,0.866025403784439,1.,0.866025403784439,1.,0.866025403784439,1.,0.866025403784439,
1.,0.866025403784439,1.,0.866025403784439,1.,0.866025403784439,1.,0.866025403784439,
1.,0.866025403784439,1.,0.866025403784439,1.,0.866025403784439,1.,0.866025403784439,
1.,0.866025403784439,1.,0.866025403784439,1.,0.866025403784439,1.,0.866025403784439,
1.,0.866025403784439,1.,0.866025403784439,1.,0.866025403784439,1.,0.866025403784439,
1.,0.866025403784439,1.,0.866025403784439,1.,0.866025403784439,1.,0.866025403784439,
1.,0.866025403784439,1.,0.866025403784439,1.,0.866025403784439,1.,0.866025403784439,
1.,0.866025403784439,1.,0.866025403784439,1.,0.866025403784439,1.,0.866025403784439,
1.,0.866025403784439,1.,0.866025403784439,1.,0.866025403784439,1.,0.866025403784439,
1.,0.866025403784439,1.,0.866025403784439,1.,0.866025403784439,1.,0.866025403784439,
1.,0.866025403784439,1.,0.866025403784439,1.,0.866025403784439,1.,0.866025403784439,
1.,0.866025403784439,1.,0.866025403784439,1.,0.866025403784439,1.,0.866025403784439,
1.,0.866025403784439,1.,0.866025403784439,1.,0.866025403784439,1.,0.866025403784439,
1.,0.866025403784439,1.,0.866025403784439,1.,0.866025403784439,1.)))
REPRESENTATION_ITEM('')
SURFACE()
);
#3302=(
BOUNDED_SURFACE()
B_SPLINE_SURFACE(1,2,((#421390,#421391,#421392,#421393,#421394,#421395,
#421396,#421397,#421398,#421399,#421400,#421401,#421402,#421403,#421404,
#421405,#421406,#421407,#421408,#421409,#421410,#421411,#421412,#421413,
#421414,#421415,#421416,#421417,#421418,#421419,#421420,#421421,#421422,
#421423,#421424,#421425,#421426,#421427,#421428,#421429,#421430,#421431,
#421432,#421433,#421434,#421435,#421436,#421437,#421438,#421439,#421440,
#421441,#421442,#421443,#421444,#421445,#421446,#421447,#421448,#421449,
#421450,#421451,#421452,#421453,#421454,#421455,#421456,#421457,#421458,
#421459,#421460,#421461,#421462,#421463,#421464,#421465,#421466,#421467,
#421468,#421469,#421470,#421471,#421472,#421473,#421474,#421475,#421476,
#421477,#421478,#421479,#421480,#421481,#421482,#421483,#421484,#421485,
#421486,#421487,#421488,#421489,#421490,#421491,#421492,#421493,#421494,
#421495,#421496,#421497,#421498,#421499,#421500,#421501,#421502,#421503,
#421504,#421505,#421506,#421507,#421508,#421509,#421510,#421511,#421512,
#421513,#421514,#421515,#421516,#421517,#421518,#421519,#421520,#421521,
#421522,#421523,#421524,#421525,#421526,#421527,#421528,#421529,#421530,
#421531,#421532,#421533,#421534,#421535,#421536,#421537,#421538,#421539,
#421540,#421541,#421542,#421543,#421544,#421545,#421546,#421547,#421548,
#421549,#421550,#421551,#421552,#421553,#421554,#421555,#421556,#421557,
#421558,#421559,#421560,#421561,#421562,#421563,#421564,#421565,#421566,
#421567,#421568,#421569,#421570,#421571,#421572,#421573,#421574,#421575,
#421576,#421577,#421578,#421579,#421580,#421581,#421582,#421583,#421584,
#421585,#421586,#421587,#421588,#421589,#421590,#421591,#421592,#421593,
#421594,#421595,#421596,#421597,#421598,#421599,#421600,#421601,#421602,
#421603,#421604,#421605,#421606,#421607,#421608,#421609,#421610,#421611,
#421612,#421613,#421614,#421615,#421616,#421617,#421618,#421619,#421620,
#421621,#421622,#421623,#421624,#421625,#421626,#421627,#421628,#421629,
#421630,#421631,#421632,#421633,#421634,#421635,#421636,#421637,#421638,
#421639,#421640,#421641,#421642,#421643,#421644,#421645,#421646,#421647,
#421648,#421649,#421650,#421651,#421652,#421653,#421654,#421655,#421656,
#421657,#421658,#421659,#421660,#421661,#421662,#421663,#421664,#421665,
#421666,#421667,#421668,#421669,#421670,#421671,#421672,#421673,#421674,
#421675,#421676,#421677,#421678,#421679,#421680,#421681,#421682,#421683,
#421684,#421685,#421686,#421687,#421688,#421689,#421690,#421691,#421692,
#421693,#421694,#421695,#421696,#421697,#421698,#421699,#421700,#421701,
#421702,#421703,#421704,#421705,#421706,#421707,#421708,#421709,#421710,
#421711,#421712,#421713,#421714,#421715,#421716,#421717,#421718,#421719,
#421720,#421721,#421722,#421723,#421724,#421725,#421726,#421727,#421728,
#421729,#421730,#421731,#421732,#421733,#421734,#421735,#421736,#421737,
#421738,#421739,#421740,#421741,#421742,#421743,#421744,#421745,#421746,
#421747,#421748,#421749,#421750,#421751,#421752,#421753,#421754,#421755,
#421756,#421757,#421758,#421759,#421760,#421761,#421762,#421763,#421764,
#421765,#421766,#421767,#421768,#421769,#421770,#421771,#421772,#421773,
#421774,#421775,#421776,#421777,#421778,#421779,#421780,#421781,#421782,
#421783,#421784,#421785,#421786,#421787,#421788,#421789,#421790,#421791,
#421792,#421793,#421794,#421795,#421796,#421797,#421798,#421799,#421800,
#421801,#421802,#421803,#421804,#421805,#421806,#421807,#421808,#421809,
#421810,#421811,#421812,#421813,#421814,#421815,#421816,#421817,#421818,
#421819,#421820,#421821,#421822,#421823,#421824,#421825,#421826,#421827,
#421828,#421829,#421830,#421831,#421832,#421833,#421834,#421835,#421836,
#421837,#421838,#421839,#421840,#421841,#421842,#421843,#421844,#421845,
#421846,#421847,#421848,#421849,#421850,#421851,#421852,#421853,#421854,
#421855,#421856,#421857,#421858,#421859,#421860,#421861,#421862,#421863,
#421864,#421865,#421866,#421867,#421868,#421869,#421870,#421871,#421872,
#421873,#421874,#421875,#421876,#421877,#421878,#421879,#421880,#421881,
#421882,#421883,#421884,#421885,#421886,#421887,#421888,#421889,#421890,
#421891,#421892,#421893,#421894,#421895,#421896,#421897,#421898,#421899,
#421900,#421901,#421902,#421903,#421904,#421905,#421906,#421907,#421908,
#421909,#421910,#421911,#421912,#421913,#421914,#421915,#421916,#421917,
#421918,#421919,#421920,#421921,#421922,#421923,#421924,#421925,#421926,
#421927,#421928,#421929,#421930,#421931,#421932,#421933,#421934,#421935,
#421936,#421937,#421938,#421939,#421940,#421941,#421942,#421943,#421944,
#421945,#421946,#421947,#421948,#421949,#421950,#421951,#421952,#421953,
#421954,#421955,#421956,#421957,#421958,#421959,#421960,#421961,#421962,
#421963,#421964,#421965,#421966,#421967,#421968,#421969,#421970,#421971,
#421972,#421973,#421974,#421975,#421976,#421977,#421978,#421979,#421980,
#421981,#421982,#421983,#421984,#421985,#421986,#421987,#421988,#421989,
#421990,#421991,#421992,#421993,#421994,#421995,#421996,#421997,#421998,
#421999,#422000,#422001,#422002),(#422003,#422004,#422005,#422006,#422007,
#422008,#422009,#422010,#422011,#422012,#422013,#422014,#422015,#422016,
#422017,#422018,#422019,#422020,#422021,#422022,#422023,#422024,#422025,
#422026,#422027,#422028,#422029,#422030,#422031,#422032,#422033,#422034,
#422035,#422036,#422037,#422038,#422039,#422040,#422041,#422042,#422043,
#422044,#422045,#422046,#422047,#422048,#422049,#422050,#422051,#422052,
#422053,#422054,#422055,#422056,#422057,#422058,#422059,#422060,#422061,
#422062,#422063,#422064,#422065,#422066,#422067,#422068,#422069,#422070,
#422071,#422072,#422073,#422074,#422075,#422076,#422077,#422078,#422079,
#422080,#422081,#422082,#422083,#422084,#422085,#422086,#422087,#422088,
#422089,#422090,#422091,#422092,#422093,#422094,#422095,#422096,#422097,
#422098,#422099,#422100,#422101,#422102,#422103,#422104,#422105,#422106,
#422107,#422108,#422109,#422110,#422111,#422112,#422113,#422114,#422115,
#422116,#422117,#422118,#422119,#422120,#422121,#422122,#422123,#422124,
#422125,#422126,#422127,#422128,#422129,#422130,#422131,#422132,#422133,
#422134,#422135,#422136,#422137,#422138,#422139,#422140,#422141,#422142,
#422143,#422144,#422145,#422146,#422147,#422148,#422149,#422150,#422151,
#422152,#422153,#422154,#422155,#422156,#422157,#422158,#422159,#422160,
#422161,#422162,#422163,#422164,#422165,#422166,#422167,#422168,#422169,
#422170,#422171,#422172,#422173,#422174,#422175,#422176,#422177,#422178,
#422179,#422180,#422181,#422182,#422183,#422184,#422185,#422186,#422187,
#422188,#422189,#422190,#422191,#422192,#422193,#422194,#422195,#422196,
#422197,#422198,#422199,#422200,#422201,#422202,#422203,#422204,#422205,
#422206,#422207,#422208,#422209,#422210,#422211,#422212,#422213,#422214,
#422215,#422216,#422217,#422218,#422219,#422220,#422221,#422222,#422223,
#422224,#422225,#422226,#422227,#422228,#422229,#422230,#422231,#422232,
#422233,#422234,#422235,#422236,#422237,#422238,#422239,#422240,#422241,
#422242,#422243,#422244,#422245,#422246,#422247,#422248,#422249,#422250,
#422251,#422252,#422253,#422254,#422255,#422256,#422257,#422258,#422259,
#422260,#422261,#422262,#422263,#422264,#422265,#422266,#422267,#422268,
#422269,#422270,#422271,#422272,#422273,#422274,#422275,#422276,#422277,
#422278,#422279,#422280,#422281,#422282,#422283,#422284,#422285,#422286,
#422287,#422288,#422289,#422290,#422291,#422292,#422293,#422294,#422295,
#422296,#422297,#422298,#422299,#422300,#422301,#422302,#422303,#422304,
#422305,#422306,#422307,#422308,#422309,#422310,#422311,#422312,#422313,
#422314,#422315,#422316,#422317,#422318,#422319,#422320,#422321,#422322,
#422323,#422324,#422325,#422326,#422327,#422328,#422329,#422330,#422331,
#422332,#422333,#422334,#422335,#422336,#422337,#422338,#422339,#422340,
#422341,#422342,#422343,#422344,#422345,#422346,#422347,#422348,#422349,
#422350,#422351,#422352,#422353,#422354,#422355,#422356,#422357,#422358,
#422359,#422360,#422361,#422362,#422363,#422364,#422365,#422366,#422367,
#422368,#422369,#422370,#422371,#422372,#422373,#422374,#422375,#422376,
#422377,#422378,#422379,#422380,#422381,#422382,#422383,#422384,#422385,
#422386,#422387,#422388,#422389,#422390,#422391,#422392,#422393,#422394,
#422395,#422396,#422397,#422398,#422399,#422400,#422401,#422402,#422403,
#422404,#422405,#422406,#422407,#422408,#422409,#422410,#422411,#422412,
#422413,#422414,#422415,#422416,#422417,#422418,#422419,#422420,#422421,
#422422,#422423,#422424,#422425,#422426,#422427,#422428,#422429,#422430,
#422431,#422432,#422433,#422434,#422435,#422436,#422437,#422438,#422439,
#422440,#422441,#422442,#422443,#422444,#422445,#422446,#422447,#422448,
#422449,#422450,#422451,#422452,#422453,#422454,#422455,#422456,#422457,
#422458,#422459,#422460,#422461,#422462,#422463,#422464,#422465,#422466,
#422467,#422468,#422469,#422470,#422471,#422472,#422473,#422474,#422475,
#422476,#422477,#422478,#422479,#422480,#422481,#422482,#422483,#422484,
#422485,#422486,#422487,#422488,#422489,#422490,#422491,#422492,#422493,
#422494,#422495,#422496,#422497,#422498,#422499,#422500,#422501,#422502,
#422503,#422504,#422505,#422506,#422507,#422508,#422509,#422510,#422511,
#422512,#422513,#422514,#422515,#422516,#422517,#422518,#422519,#422520,
#422521,#422522,#422523,#422524,#422525,#422526,#422527,#422528,#422529,
#422530,#422531,#422532,#422533,#422534,#422535,#422536,#422537,#422538,
#422539,#422540,#422541,#422542,#422543,#422544,#422545,#422546,#422547,
#422548,#422549,#422550,#422551,#422552,#422553,#422554,#422555,#422556,
#422557,#422558,#422559,#422560,#422561,#422562,#422563,#422564,#422565,
#422566,#422567,#422568,#422569,#422570,#422571,#422572,#422573,#422574,
#422575,#422576,#422577,#422578,#422579,#422580,#422581,#422582,#422583,
#422584,#422585,#422586,#422587,#422588,#422589,#422590,#422591,#422592,
#422593,#422594,#422595,#422596,#422597,#422598,#422599,#422600,#422601,
#422602,#422603,#422604,#422605,#422606,#422607,#422608,#422609,#422610,
#422611,#422612,#422613,#422614,#422615)),.UNSPECIFIED.,.F.,.F.,.F.)
B_SPLINE_SURFACE_WITH_KNOTS((2,2),(3,2,2,2,2,2,2,2,2,2,2,2,2,2,2,2,2,2,
2,2,2,2,2,2,2,2,2,2,2,2,2,2,2,2,2,2,2,2,2,2,2,2,2,2,2,2,2,2,2,2,2,2,2,2,
2,2,2,2,2,2,2,2,2,2,2,2,2,2,2,2,2,2,2,2,2,2,2,2,2,2,2,2,2,2,2,2,2,2,2,2,
2,2,2,2,2,2,2,2,2,2,2,2,2,2,2,2,2,2,2,2,2,2,2,2,2,2,2,2,2,2,2,2,2,2,2,2,
2,2,2,2,2,2,2,2,2,2,2,2,2,2,2,2,2,2,2,2,2,2,2,2,2,2,2,2,2,2,2,2,2,2,2,2,
2,2,2,2,2,2,2,2,2,2,2,2,2,2,2,2,2,2,2,2,2,2,2,2,2,2,2,2,2,2,2,2,2,2,2,2,
2,2,2,2,2,2,2,2,2,2,2,2,2,2,2,2,2,2,2,2,2,2,2,2,2,2,2,2,2,2,2,2,2,2,2,2,
2,2,2,2,2,2,2,2,2,2,2,2,2,2,2,2,2,2,2,2,2,2,2,2,2,2,2,2,2,2,2,2,2,2,2,2,
2,2,2,2,2,2,2,2,2,2,2,2,2,2,2,2,2,2,2,2,2,2,2,2,2,2,2,2,2,2,2,2,2,2,2,2,
3),(0.,1.),(0.,0.00326797385620915,0.0065359477124183,0.00980392156862745,
0.0130718954248366,0.0163398692810458,0.0196078431372549,0.0228758169934641,
0.0261437908496732,0.0294117647058824,0.0326797385620915,0.0359477124183007,
0.0392156862745098,0.042483660130719,0.0457516339869281,0.0490196078431373,
0.0522875816993464,0.0555555555555556,0.0588235294117647,0.0620915032679739,
0.065359477124183,0.0686274509803922,0.0718954248366013,0.0751633986928105,
0.0784313725490196,0.0816993464052288,0.0849673202614379,0.0882352941176471,
0.0915032679738562,0.0947712418300654,0.0980392156862745,0.101307189542484,
0.104575163398693,0.107843137254902,0.111111111111111,0.11437908496732,
0.117647058823529,0.120915032679739,0.124183006535948,0.127450980392157,
0.130718954248366,0.133986928104575,0.137254901960784,0.140522875816993,
0.143790849673203,0.147058823529412,0.150326797385621,0.15359477124183,
0.156862745098039,0.160130718954248,0.163398692810458,0.166666666666667,
0.169934640522876,0.173202614379085,0.176470588235294,0.179738562091503,
0.183006535947712,0.186274509803922,0.189542483660131,0.19281045751634,
0.196078431372549,0.199346405228758,0.202614379084967,0.205882352941176,
0.209150326797386,0.212418300653595,0.215686274509804,0.218954248366013,
0.222222222222222,0.225490196078431,0.228758169934641,0.23202614379085,
0.235294117647059,0.238562091503268,0.241830065359477,0.245098039215686,
0.248366013071895,0.251633986928105,0.254901960784314,0.258169934640523,
0.261437908496732,0.264705882352941,0.26797385620915,0.271241830065359,
0.274509803921569,0.277777777777778,0.281045751633987,0.284313725490196,
0.287581699346405,0.290849673202614,0.294117647058824,0.297385620915033,
0.300653594771242,0.303921568627451,0.30718954248366,0.310457516339869,
0.313725490196078,0.316993464052288,0.320261437908497,0.323529411764706,
0.326797385620915,0.330065359477124,0.333333333333333,0.336601307189543,
0.339869281045752,0.343137254901961,0.34640522875817,0.349673202614379,
0.352941176470588,0.356209150326797,0.359477124183007,0.362745098039216,
0.366013071895425,0.369281045751634,0.372549019607843,0.375816993464052,
0.379084967320261,0.382352941176471,0.38562091503268,0.388888888888889,
0.392156862745098,0.395424836601307,0.398692810457516,0.401960784313726,
0.405228758169935,0.408496732026144,0.411764705882353,0.415032679738562,
0.418300653594771,0.42156862745098,0.42483660130719,0.428104575163399,0.431372549019608,
0.434640522875817,0.437908496732026,0.441176470588235,0.444444444444444,
0.447712418300654,0.450980392156863,0.454248366013072,0.457516339869281,
0.46078431372549,0.464052287581699,0.467320261437909,0.470588235294118,
0.473856209150327,0.477124183006536,0.480392156862745,0.483660130718954,
0.486928104575163,0.490196078431373,0.493464052287582,0.496732026143791,
0.5,0.503267973856209,0.506535947712418,0.509803921568627,0.513071895424837,
0.516339869281046,0.519607843137255,0.522875816993464,0.526143790849673,
0.529411764705882,0.532679738562091,0.535947712418301,0.53921568627451,
0.542483660130719,0.545751633986928,0.549019607843137,0.552287581699346,
0.555555555555556,0.558823529411765,0.562091503267974,0.565359477124183,
0.568627450980392,0.571895424836601,0.57516339869281,0.57843137254902,0.581699346405229,
0.584967320261438,0.588235294117647,0.591503267973856,0.594771241830065,
0.598039215686274,0.601307189542484,0.604575163398693,0.607843137254902,
0.611111111111111,0.61437908496732,0.617647058823529,0.620915032679739,
0.624183006535948,0.627450980392157,0.630718954248366,0.633986928104575,
0.637254901960784,0.640522875816993,0.643790849673203,0.647058823529412,
0.650326797385621,0.65359477124183,0.656862745098039,0.660130718954248,
0.663398692810457,0.666666666666667,0.669934640522876,0.673202614379085,
0.676470588235294,0.679738562091503,0.683006535947712,0.686274509803922,
0.689542483660131,0.69281045751634,0.696078431372549,0.699346405228758,
0.702614379084967,0.705882352941177,0.709150326797386,0.712418300653595,
0.715686274509804,0.718954248366013,0.722222222222222,0.725490196078431,
0.72875816993464,0.73202614379085,0.735294117647059,0.738562091503268,0.741830065359477,
0.745098039215686,0.748366013071895,0.751633986928105,0.754901960784314,
0.758169934640523,0.761437908496732,0.764705882352941,0.76797385620915,
0.77124183006536,0.774509803921569,0.777777777777778,0.781045751633987,
0.784313725490196,0.787581699346405,0.790849673202614,0.794117647058823,
0.797385620915033,0.800653594771242,0.803921568627451,0.80718954248366,
0.810457516339869,0.813725490196078,0.816993464052288,0.820261437908497,
0.823529411764706,0.826797385620915,0.830065359477124,0.833333333333333,
0.836601307189543,0.839869281045752,0.843137254901961,0.84640522875817,
0.849673202614379,0.852941176470588,0.856209150326797,0.859477124183007,
0.862745098039216,0.866013071895425,0.869281045751634,0.872549019607843,
0.875816993464052,0.879084967320261,0.882352941176471,0.88562091503268,
0.888888888888889,0.892156862745098,0.895424836601307,0.898692810457516,
0.901960784313726,0.905228758169935,0.908496732026144,0.911764705882353,
0.915032679738562,0.918300653594771,0.92156862745098,0.92483660130719,0.928104575163399,
0.931372549019608,0.934640522875817,0.937908496732026,0.941176470588235,
0.944444444444444,0.947712418300654,0.950980392156863,0.954248366013072,
0.957516339869281,0.96078431372549,0.964052287581699,0.967320261437909,
0.970588235294118,0.973856209150327,0.977124183006536,0.980392156862745,
0.983660130718954,0.986928104575163,0.990196078431373,0.993464052287582,
0.996732026143791,1.),.UNSPECIFIED.)
GEOMETRIC_REPRESENTATION_ITEM()
RATIONAL_B_SPLINE_SURFACE(((1.,0.866025403784439,1.,0.866025403784439,1.,
0.866025403784439,1.,0.866025403784439,1.,0.866025403784439,1.,0.866025403784439,
1.,0.866025403784439,1.,0.866025403784439,1.,0.866025403784439,1.,0.866025403784439,
1.,0.866025403784439,1.,0.866025403784439,1.,0.866025403784439,1.,0.866025403784439,
1.,0.866025403784439,1.,0.866025403784439,1.,0.866025403784439,1.,0.866025403784439,
1.,0.866025403784439,1.,0.866025403784439,1.,0.866025403784439,1.,0.866025403784439,
1.,0.866025403784439,1.,0.866025403784439,1.,0.866025403784439,1.,0.866025403784439,
1.,0.866025403784439,1.,0.866025403784439,1.,0.866025403784439,1.,0.866025403784439,
1.,0.866025403784439,1.,0.866025403784439,1.,0.866025403784439,1.,0.866025403784439,
1.,0.866025403784439,1.,0.866025403784439,1.,0.866025403784439,1.,0.866025403784439,
1.,0.866025403784439,1.,0.866025403784439,1.,0.866025403784439,1.,0.866025403784439,
1.,0.866025403784439,1.,0.866025403784439,1.,0.866025403784439,1.,0.866025403784439,
1.,0.866025403784439,1.,0.866025403784439,1.,0.866025403784439,1.,0.866025403784439,
1.,0.866025403784439,1.,0.866025403784439,1.,0.866025403784439,1.,0.866025403784439,
1.,0.866025403784439,1.,0.866025403784439,1.,0.866025403784439,1.,0.866025403784439,
1.,0.866025403784439,1.,0.866025403784439,1.,0.866025403784439,1.,0.866025403784439,
1.,0.866025403784439,1.,0.866025403784439,1.,0.866025403784439,1.,0.866025403784439,
1.,0.866025403784439,1.,0.866025403784439,1.,0.866025403784439,1.,0.866025403784439,
1.,0.866025403784439,1.,0.866025403784439,1.,0.866025403784439,1.,0.866025403784439,
1.,0.866025403784439,1.,0.866025403784439,1.,0.866025403784439,1.,0.866025403784439,
1.,0.866025403784439,1.,0.866025403784439,1.,0.866025403784439,1.,0.866025403784439,
1.,0.866025403784439,1.,0.866025403784439,1.,0.866025403784439,1.,0.866025403784439,
1.,0.866025403784439,1.,0.866025403784439,1.,0.866025403784439,1.,0.866025403784439,
1.,0.866025403784439,1.,0.866025403784439,1.,0.866025403784439,1.,0.866025403784439,
1.,0.866025403784439,1.,0.866025403784439,1.,0.866025403784439,1.,0.866025403784439,
1.,0.866025403784439,1.,0.866025403784439,1.,0.866025403784439,1.,0.866025403784439,
1.,0.866025403784439,1.,0.866025403784439,1.,0.866025403784439,1.,0.866025403784439,
1.,0.866025403784439,1.,0.866025403784439,1.,0.866025403784439,1.,0.866025403784439,
1.,0.866025403784439,1.,0.866025403784439,1.,0.866025403784439,1.,0.866025403784439,
1.,0.866025403784439,1.,0.866025403784439,1.,0.866025403784439,1.,0.866025403784439,
1.,0.866025403784439,1.,0.866025403784439,1.,0.866025403784439,1.,0.866025403784439,
1.,0.866025403784439,1.,0.866025403784439,1.,0.866025403784439,1.,0.866025403784439,
1.,0.866025403784439,1.,0.866025403784439,1.,0.866025403784439,1.,0.866025403784439,
1.,0.866025403784439,1.,0.866025403784439,1.,0.866025403784439,1.,0.866025403784439,
1.,0.866025403784439,1.,0.866025403784439,1.,0.866025403784439,1.,0.866025403784439,
1.,0.866025403784439,1.,0.866025403784439,1.,0.866025403784439,1.,0.866025403784439,
1.,0.866025403784439,1.,0.866025403784439,1.,0.866025403784439,1.,0.866025403784439,
1.,0.866025403784439,1.,0.866025403784439,1.,0.866025403784439,1.,0.866025403784439,
1.,0.866025403784439,1.,0.866025403784439,1.,0.866025403784439,1.,0.866025403784439,
1.,0.866025403784439,1.,0.866025403784439,1.,0.866025403784439,1.,0.866025403784439,
1.,0.866025403784439,1.,0.866025403784439,1.,0.866025403784439,1.,0.866025403784439,
1.,0.866025403784439,1.,0.866025403784439,1.,0.866025403784439,1.,0.866025403784439,
1.,0.866025403784439,1.,0.866025403784439,1.,0.866025403784439,1.,0.866025403784439,
1.,0.866025403784439,1.,0.866025403784439,1.,0.866025403784439,1.,0.866025403784439,
1.,0.866025403784439,1.,0.866025403784439,1.,0.866025403784439,1.,0.866025403784439,
1.,0.866025403784439,1.,0.866025403784439,1.,0.866025403784439,1.,0.866025403784439,
1.,0.866025403784439,1.,0.866025403784439,1.,0.866025403784439,1.,0.866025403784439,
1.,0.866025403784439,1.,0.866025403784439,1.,0.866025403784439,1.,0.866025403784439,
1.,0.866025403784439,1.,0.866025403784439,1.,0.866025403784439,1.,0.866025403784439,
1.,0.866025403784439,1.,0.866025403784439,1.,0.866025403784439,1.,0.866025403784439,
1.,0.866025403784439,1.,0.866025403784439,1.,0.866025403784439,1.,0.866025403784439,
1.,0.866025403784439,1.,0.866025403784439,1.,0.866025403784439,1.,0.866025403784439,
1.,0.866025403784439,1.,0.866025403784439,1.,0.866025403784439,1.,0.866025403784439,
1.,0.866025403784439,1.,0.866025403784439,1.,0.866025403784439,1.,0.866025403784439,
1.,0.866025403784439,1.,0.866025403784439,1.,0.866025403784439,1.,0.866025403784439,
1.,0.866025403784439,1.,0.866025403784439,1.,0.866025403784439,1.,0.866025403784439,
1.,0.866025403784439,1.,0.866025403784439,1.,0.866025403784439,1.,0.866025403784439,
1.,0.866025403784439,1.,0.866025403784439,1.,0.866025403784439,1.,0.866025403784439,
1.,0.866025403784439,1.,0.866025403784439,1.,0.866025403784439,1.,0.866025403784439,
1.,0.866025403784439,1.,0.866025403784439,1.,0.866025403784439,1.,0.866025403784439,
1.,0.866025403784439,1.,0.866025403784439,1.,0.866025403784439,1.,0.866025403784439,
1.,0.866025403784439,1.,0.866025403784439,1.,0.866025403784439,1.,0.866025403784439,
1.,0.866025403784439,1.,0.866025403784439,1.,0.866025403784439,1.,0.866025403784439,
1.,0.866025403784439,1.,0.866025403784439,1.,0.866025403784439,1.,0.866025403784439,
1.,0.866025403784439,1.,0.866025403784439,1.,0.866025403784439,1.,0.866025403784439,
1.,0.866025403784439,1.,0.866025403784439,1.,0.866025403784439,1.,0.866025403784439,
1.,0.866025403784439,1.,0.866025403784439,1.,0.866025403784439,1.,0.866025403784439,
1.,0.866025403784439,1.,0.866025403784439,1.,0.866025403784439,1.,0.866025403784439,
1.,0.866025403784439,1.,0.866025403784439,1.,0.866025403784439,1.,0.866025403784439,
1.,0.866025403784439,1.,0.866025403784439,1.,0.866025403784439,1.,0.866025403784439,
1.,0.866025403784439,1.,0.866025403784439,1.,0.866025403784439,1.,0.866025403784439,
1.,0.866025403784439,1.,0.866025403784439,1.,0.866025403784439,1.,0.866025403784439,
1.,0.866025403784439,1.,0.866025403784439,1.,0.866025403784439,1.,0.866025403784439,
1.,0.866025403784439,1.,0.866025403784439,1.,0.866025403784439,1.,0.866025403784439,
1.,0.866025403784439,1.,0.866025403784439,1.,0.866025403784439,1.,0.866025403784439,
1.,0.866025403784439,1.,0.866025403784439,1.,0.866025403784439,1.,0.866025403784439,
1.,0.866025403784439,1.,0.866025403784439,1.,0.866025403784439,1.,0.866025403784439,
1.),(1.,0.866025403784439,1.,0.866025403784439,1.,0.866025403784439,1.,
0.866025403784439,1.,0.866025403784439,1.,0.866025403784439,1.,0.866025403784439,
1.,0.866025403784439,1.,0.866025403784439,1.,0.866025403784439,1.,0.866025403784439,
1.,0.866025403784439,1.,0.866025403784439,1.,0.866025403784439,1.,0.866025403784439,
1.,0.866025403784439,1.,0.866025403784439,1.,0.866025403784439,1.,0.866025403784439,
1.,0.866025403784439,1.,0.866025403784439,1.,0.866025403784439,1.,0.866025403784439,
1.,0.866025403784439,1.,0.866025403784439,1.,0.866025403784439,1.,0.866025403784439,
1.,0.866025403784439,1.,0.866025403784439,1.,0.866025403784439,1.,0.866025403784439,
1.,0.866025403784439,1.,0.866025403784439,1.,0.866025403784439,1.,0.866025403784439,
1.,0.866025403784439,1.,0.866025403784439,1.,0.866025403784439,1.,0.866025403784439,
1.,0.866025403784439,1.,0.866025403784439,1.,0.866025403784439,1.,0.866025403784439,
1.,0.866025403784439,1.,0.866025403784439,1.,0.866025403784439,1.,0.866025403784439,
1.,0.866025403784439,1.,0.866025403784439,1.,0.866025403784439,1.,0.866025403784439,
1.,0.866025403784439,1.,0.866025403784439,1.,0.866025403784439,1.,0.866025403784439,
1.,0.866025403784439,1.,0.866025403784439,1.,0.866025403784439,1.,0.866025403784439,
1.,0.866025403784439,1.,0.866025403784439,1.,0.866025403784439,1.,0.866025403784439,
1.,0.866025403784439,1.,0.866025403784439,1.,0.866025403784439,1.,0.866025403784439,
1.,0.866025403784439,1.,0.866025403784439,1.,0.866025403784439,1.,0.866025403784439,
1.,0.866025403784439,1.,0.866025403784439,1.,0.866025403784439,1.,0.866025403784439,
1.,0.866025403784439,1.,0.866025403784439,1.,0.866025403784439,1.,0.866025403784439,
1.,0.866025403784439,1.,0.866025403784439,1.,0.866025403784439,1.,0.866025403784439,
1.,0.866025403784439,1.,0.866025403784439,1.,0.866025403784439,1.,0.866025403784439,
1.,0.866025403784439,1.,0.866025403784439,1.,0.866025403784439,1.,0.866025403784439,
1.,0.866025403784439,1.,0.866025403784439,1.,0.866025403784439,1.,0.866025403784439,
1.,0.866025403784439,1.,0.866025403784439,1.,0.866025403784439,1.,0.866025403784439,
1.,0.866025403784439,1.,0.866025403784439,1.,0.866025403784439,1.,0.866025403784439,
1.,0.866025403784439,1.,0.866025403784439,1.,0.866025403784439,1.,0.866025403784439,
1.,0.866025403784439,1.,0.866025403784439,1.,0.866025403784439,1.,0.866025403784439,
1.,0.866025403784439,1.,0.866025403784439,1.,0.866025403784439,1.,0.866025403784439,
1.,0.866025403784439,1.,0.866025403784439,1.,0.866025403784439,1.,0.866025403784439,
1.,0.866025403784439,1.,0.866025403784439,1.,0.866025403784439,1.,0.866025403784439,
1.,0.866025403784439,1.,0.866025403784439,1.,0.866025403784439,1.,0.866025403784439,
1.,0.866025403784439,1.,0.866025403784439,1.,0.866025403784439,1.,0.866025403784439,
1.,0.866025403784439,1.,0.866025403784439,1.,0.866025403784439,1.,0.866025403784439,
1.,0.866025403784439,1.,0.866025403784439,1.,0.866025403784439,1.,0.866025403784439,
1.,0.866025403784439,1.,0.866025403784439,1.,0.866025403784439,1.,0.866025403784439,
1.,0.866025403784439,1.,0.866025403784439,1.,0.866025403784439,1.,0.866025403784439,
1.,0.866025403784439,1.,0.866025403784439,1.,0.866025403784439,1.,0.866025403784439,
1.,0.866025403784439,1.,0.866025403784439,1.,0.866025403784439,1.,0.866025403784439,
1.,0.866025403784439,1.,0.866025403784439,1.,0.866025403784439,1.,0.866025403784439,
1.,0.866025403784439,1.,0.866025403784439,1.,0.866025403784439,1.,0.866025403784439,
1.,0.866025403784439,1.,0.866025403784439,1.,0.866025403784439,1.,0.866025403784439,
1.,0.866025403784439,1.,0.866025403784439,1.,0.866025403784439,1.,0.866025403784439,
1.,0.866025403784439,1.,0.866025403784439,1.,0.866025403784439,1.,0.866025403784439,
1.,0.866025403784439,1.,0.866025403784439,1.,0.866025403784439,1.,0.866025403784439,
1.,0.866025403784439,1.,0.866025403784439,1.,0.866025403784439,1.,0.866025403784439,
1.,0.866025403784439,1.,0.866025403784439,1.,0.866025403784439,1.,0.866025403784439,
1.,0.866025403784439,1.,0.866025403784439,1.,0.866025403784439,1.,0.866025403784439,
1.,0.866025403784439,1.,0.866025403784439,1.,0.866025403784439,1.,0.866025403784439,
1.,0.866025403784439,1.,0.866025403784439,1.,0.866025403784439,1.,0.866025403784439,
1.,0.866025403784439,1.,0.866025403784439,1.,0.866025403784439,1.,0.866025403784439,
1.,0.866025403784439,1.,0.866025403784439,1.,0.866025403784439,1.,0.866025403784439,
1.,0.866025403784439,1.,0.866025403784439,1.,0.866025403784439,1.,0.866025403784439,
1.,0.866025403784439,1.,0.866025403784439,1.,0.866025403784439,1.,0.866025403784439,
1.,0.866025403784439,1.,0.866025403784439,1.,0.866025403784439,1.,0.866025403784439,
1.,0.866025403784439,1.,0.866025403784439,1.,0.866025403784439,1.,0.866025403784439,
1.,0.866025403784439,1.,0.866025403784439,1.,0.866025403784439,1.,0.866025403784439,
1.,0.866025403784439,1.,0.866025403784439,1.,0.866025403784439,1.,0.866025403784439,
1.,0.866025403784439,1.,0.866025403784439,1.,0.866025403784439,1.,0.866025403784439,
1.,0.866025403784439,1.,0.866025403784439,1.,0.866025403784439,1.,0.866025403784439,
1.,0.866025403784439,1.,0.866025403784439,1.,0.866025403784439,1.,0.866025403784439,
1.,0.866025403784439,1.,0.866025403784439,1.,0.866025403784439,1.,0.866025403784439,
1.,0.866025403784439,1.,0.866025403784439,1.,0.866025403784439,1.,0.866025403784439,
1.,0.866025403784439,1.,0.866025403784439,1.,0.866025403784439,1.,0.866025403784439,
1.,0.866025403784439,1.,0.866025403784439,1.,0.866025403784439,1.,0.866025403784439,
1.,0.866025403784439,1.,0.866025403784439,1.,0.866025403784439,1.,0.866025403784439,
1.,0.866025403784439,1.,0.866025403784439,1.,0.866025403784439,1.,0.866025403784439,
1.,0.866025403784439,1.,0.866025403784439,1.,0.866025403784439,1.,0.866025403784439,
1.,0.866025403784439,1.,0.866025403784439,1.,0.866025403784439,1.,0.866025403784439,
1.,0.866025403784439,1.,0.866025403784439,1.,0.866025403784439,1.,0.866025403784439,
1.,0.866025403784439,1.,0.866025403784439,1.,0.866025403784439,1.,0.866025403784439,
1.,0.866025403784439,1.,0.866025403784439,1.,0.866025403784439,1.,0.866025403784439,
1.,0.866025403784439,1.,0.866025403784439,1.,0.866025403784439,1.,0.866025403784439,
1.,0.866025403784439,1.,0.866025403784439,1.,0.866025403784439,1.,0.866025403784439,
1.,0.866025403784439,1.,0.866025403784439,1.,0.866025403784439,1.,0.866025403784439,
1.,0.866025403784439,1.,0.866025403784439,1.,0.866025403784439,1.,0.866025403784439,
1.,0.866025403784439,1.,0.866025403784439,1.,0.866025403784439,1.)))
REPRESENTATION_ITEM('')
SURFACE()
);
#3303=(
BOUNDED_SURFACE()
B_SPLINE_SURFACE(3,2,((#422661,#422662,#422663),(#422664,#422665,#422666),
(#422667,#422668,#422669),(#422670,#422671,#422672)),.UNSPECIFIED.,.F.,
 .F.,.F.)
B_SPLINE_SURFACE_WITH_KNOTS((4,4),(3,3),(0.,0.000101260117256738),(0.,1.),
 .UNSPECIFIED.)
GEOMETRIC_REPRESENTATION_ITEM()
RATIONAL_B_SPLINE_SURFACE(((1.,0.79661527883517,1.),(1.,0.795896038055943,
1.),(1.,0.795193354661341,1.),(1.,0.794506193185546,1.)))
REPRESENTATION_ITEM('')
SURFACE()
);
#3304=(
BOUNDED_SURFACE()
B_SPLINE_SURFACE(3,2,((#422705,#422706,#422707),(#422708,#422709,#422710),
(#422711,#422712,#422713),(#422714,#422715,#422716),(#422717,#422718,#422719),
(#422720,#422721,#422722)),.UNSPECIFIED.,.F.,.F.,.F.)
B_SPLINE_SURFACE_WITH_KNOTS((4,2,4),(3,3),(0.,1.66936432462295E-5,3.33872864924589E-5),
(0.,1.),.UNSPECIFIED.)
GEOMETRIC_REPRESENTATION_ITEM()
RATIONAL_B_SPLINE_SURFACE(((1.,0.796615278835174,1.),(1.,0.862310524418132,
1.),(1.,0.923774472010522,1.),(1.,0.923983993203425,1.),(1.,0.862574873720951,
1.),(1.,0.796615278835179,1.)))
REPRESENTATION_ITEM('')
SURFACE()
);
#3305=(
BOUNDED_SURFACE()
B_SPLINE_SURFACE(3,2,((#422724,#422725,#422726),(#422727,#422728,#422729),
(#422730,#422731,#422732),(#422733,#422734,#422735)),.UNSPECIFIED.,.F.,
 .F.,.F.)
B_SPLINE_SURFACE_WITH_KNOTS((4,4),(3,3),(2.85968127239939E-5,9.24681548475817E-5),
(-0.00167900678656536,1.01130827127815),.UNSPECIFIED.)
GEOMETRIC_REPRESENTATION_ITEM()
RATIONAL_B_SPLINE_SURFACE(((1.00059040895218,0.822187541868277,1.00401468696654),
(1.0003652771814,0.889990093671579,1.00248382673389),(1.00016469515013,
0.950399042257932,1.0011199008251),(1.00025604273993,0.922888044286083,
1.0017410499063)))
REPRESENTATION_ITEM('')
SURFACE()
);
#3306=(
BOUNDED_SURFACE()
B_SPLINE_SURFACE(3,2,((#422736,#422737,#422738),(#422739,#422740,#422741),
(#422742,#422743,#422744),(#422745,#422746,#422747)),.UNSPECIFIED.,.F.,
 .F.,.F.)
B_SPLINE_SURFACE_WITH_KNOTS((4,4),(3,3),(-5.22358356749212E-6,5.74594192424277E-5),
(-0.00127120052043463,1.),.UNSPECIFIED.)
GEOMETRIC_REPRESENTATION_ITEM()
RATIONAL_B_SPLINE_SURFACE(((1.0005444931317,0.785835073638803,1.),(1.0004770776747,
0.812351526358854,1.),(1.00044031788582,0.826810216506326,1.),(1.00044777653314,
0.823876514387264,1.)))
REPRESENTATION_ITEM('')
SURFACE()
);
#3307=(
BOUNDED_SURFACE()
B_SPLINE_SURFACE(3,2,((#422749,#422750,#422751),(#422752,#422753,#422754),
(#422755,#422756,#422757),(#422758,#422759,#422760)),.UNSPECIFIED.,.F.,
 .F.,.F.)
B_SPLINE_SURFACE_WITH_KNOTS((4,4),(3,3),(0.,0.000101244905251112),(0.,1.),
 .UNSPECIFIED.)
GEOMETRIC_REPRESENTATION_ITEM()
RATIONAL_B_SPLINE_SURFACE(((1.,0.79661527883517,1.),(1.,0.795896146109807,
1.),(1.,0.795193565796486,1.),(1.,0.794506502889904,1.)))
REPRESENTATION_ITEM('')
SURFACE()
);
#3308=(
BOUNDED_SURFACE()
B_SPLINE_SURFACE(3,2,((#422795,#422796,#422797),(#422798,#422799,#422800),
(#422801,#422802,#422803),(#422804,#422805,#422806)),.UNSPECIFIED.,.F.,
 .F.,.F.)
B_SPLINE_SURFACE_WITH_KNOTS((4,4),(3,3),(-2.71050543121376E-20,4.88747512969881E-5),
(-0.000215805215330801,1.),.UNSPECIFIED.)
GEOMETRIC_REPRESENTATION_ITEM()
RATIONAL_B_SPLINE_SURFACE(((1.00008915600332,0.79343408549978,1.),(1.00008930224985,
0.793095246303315,1.),(1.00008944684607,0.792760230720596,1.),(1.00008958984386,
0.792428918540619,1.)))
REPRESENTATION_ITEM('')
SURFACE()
);
#3309=(
BOUNDED_SURFACE()
B_SPLINE_SURFACE(3,2,((#422808,#422809,#422810),(#422811,#422812,#422813),
(#422814,#422815,#422816),(#422817,#422818,#422819)),.UNSPECIFIED.,.F.,
 .F.,.F.)
B_SPLINE_SURFACE_WITH_KNOTS((4,4),(3,3),(3.22980774337779E-5,9.63764854872251E-5),
(-0.00154325936372869,1.01095292447549),.UNSPECIFIED.)
GEOMETRIC_REPRESENTATION_ITEM()
RATIONAL_B_SPLINE_SURFACE(((1.00023530983299,0.922925743796161,1.00168574728332),
(1.00015136166126,0.950422439594214,1.0010843469906),(1.00033574337398,
0.890029368953955,1.00240524789549),(1.00054260094221,0.822274473168324,
1.0038871646486)))
REPRESENTATION_ITEM('')
SURFACE()
);
#3310=(
BOUNDED_SURFACE()
B_SPLINE_SURFACE(3,2,((#422821,#422822,#422823),(#422824,#422825,#422826),
(#422827,#422828,#422829),(#422830,#422831,#422832),(#422833,#422834,#422835),
(#422836,#422837,#422838)),.UNSPECIFIED.,.F.,.F.,.F.)
B_SPLINE_SURFACE_WITH_KNOTS((4,2,4),(3,3),(3.11708124589583E-19,7.62675010863197E-5,
0.000152535002172639),(0.,1.02152348203076),.UNSPECIFIED.)
GEOMETRIC_REPRESENTATION_ITEM()
RATIONAL_B_SPLINE_SURFACE(((1.,0.789033595401239,1.00908146323695),(1.,
0.857071781054831,1.00615262590431),(1.,0.92208726471071,1.00335390671593),
(1.,0.922394466502383,1.00334068261145),(1.,0.85722438459903,1.00614605678503),
(1.,0.789033595401632,1.00908146323693)))
REPRESENTATION_ITEM('')
SURFACE()
);
#3311=(
BOUNDED_SURFACE()
B_SPLINE_SURFACE(3,2,((#422842,#422843,#422844),(#422845,#422846,#422847),
(#422848,#422849,#422850),(#422851,#422852,#422853)),.UNSPECIFIED.,.F.,
 .F.,.F.)
B_SPLINE_SURFACE_WITH_KNOTS((4,4),(3,3),(3.25260651745651E-19,4.88747512969884E-5),
(-0.000215489857776029,1.),.UNSPECIFIED.)
GEOMETRIC_REPRESENTATION_ITEM()
RATIONAL_B_SPLINE_SURFACE(((1.00008945889744,0.79242898398559,1.),(1.00008931610865,
0.792760296061139,1.),(1.00008917172378,0.793095311538206,1.),(1.000089025691,
0.793434150627846,1.)))
REPRESENTATION_ITEM('')
SURFACE()
);
#3312=(
BOUNDED_SURFACE()
B_SPLINE_SURFACE(3,2,((#422855,#422856,#422857),(#422858,#422859,#422860),
(#422861,#422862,#422863),(#422864,#422865,#422866)),.UNSPECIFIED.,.F.,
 .F.,.F.)
B_SPLINE_SURFACE_WITH_KNOTS((4,4),(3,3),(-5.21974905013087E-6,5.74172395514396E-5),
(-0.00139822857750329,1.00051312364072),.UNSPECIFIED.)
GEOMETRIC_REPRESENTATION_ITEM()
RATIONAL_B_SPLINE_SURFACE(((1.00049256947248,0.823768952244012,1.00018060397851),
(1.00048448215719,0.826662424388296,1.00017763870884),(1.00052427784026,
0.812424361909377,1.00019223006923),(1.00059912365861,0.785646094632743,
1.00021967280233)))
REPRESENTATION_ITEM('')
SURFACE()
);
#3313=(
BOUNDED_SURFACE()
B_SPLINE_SURFACE(3,2,((#422965,#422966,#422967),(#422968,#422969,#422970),
(#422971,#422972,#422973),(#422974,#422975,#422976)),.UNSPECIFIED.,.F.,
 .F.,.F.)
B_SPLINE_SURFACE_WITH_KNOTS((4,4),(3,3),(0.,0.000101260117256738),(0.,1.),
 .UNSPECIFIED.)
GEOMETRIC_REPRESENTATION_ITEM()
RATIONAL_B_SPLINE_SURFACE(((1.,0.796615278835177,1.),(1.,0.795896038055936,
1.),(1.,0.795193354661342,1.),(1.,0.794506193185541,1.)))
REPRESENTATION_ITEM('')
SURFACE()
);
#3314=(
BOUNDED_SURFACE()
B_SPLINE_SURFACE(3,2,((#423014,#423015,#423016),(#423017,#423018,#423019),
(#423020,#423021,#423022),(#423023,#423024,#423025),(#423026,#423027,#423028),
(#423029,#423030,#423031)),.UNSPECIFIED.,.F.,.F.,.F.)
B_SPLINE_SURFACE_WITH_KNOTS((4,2,4),(3,3),(-9.82558218814988E-20,1.66936432462292E-5,
3.33872864924585E-5),(0.,1.),.UNSPECIFIED.)
GEOMETRIC_REPRESENTATION_ITEM()
RATIONAL_B_SPLINE_SURFACE(((1.,0.796615278835176,1.),(1.,0.862310524418132,
1.),(1.,0.923774472010523,1.),(1.,0.923983993203417,1.),(1.,0.86257487372095,
1.),(1.,0.796615278835183,1.)))
REPRESENTATION_ITEM('')
SURFACE()
);
#3315=(
BOUNDED_SURFACE()
B_SPLINE_SURFACE(3,2,((#423068,#423069,#423070),(#423071,#423072,#423073),
(#423074,#423075,#423076),(#423077,#423078,#423079)),.UNSPECIFIED.,.F.,
 .F.,.F.)
B_SPLINE_SURFACE_WITH_KNOTS((4,4),(3,3),(-2.16840434497101E-19,0.000101244905251112),
(0.,1.),.UNSPECIFIED.)
GEOMETRIC_REPRESENTATION_ITEM()
RATIONAL_B_SPLINE_SURFACE(((1.,0.796615278835171,1.),(1.,0.795896146109795,
1.),(1.,0.795193565796499,1.),(1.,0.794506502889901,1.)))
REPRESENTATION_ITEM('')
SURFACE()
);
#3316=(
BOUNDED_SURFACE()
B_SPLINE_SURFACE(3,2,((#423115,#423116,#423117),(#423118,#423119,#423120),
(#423121,#423122,#423123),(#423124,#423125,#423126)),.UNSPECIFIED.,.F.,
 .F.,.F.)
B_SPLINE_SURFACE_WITH_KNOTS((4,4),(3,3),(2.85968127239939E-5,9.24681548475818E-5),
(-0.0016790067865349,1.01130827127819),.UNSPECIFIED.)
GEOMETRIC_REPRESENTATION_ITEM()
RATIONAL_B_SPLINE_SURFACE(((1.00059040895216,0.822187541868271,1.00401468696656),
(1.00036527718139,0.889990093671581,1.0024838267339),(1.00016469515013,
0.950399042257933,1.00111990082511),(1.00025604273992,0.922888044286082,
1.00174104990631)))
REPRESENTATION_ITEM('')
SURFACE()
);
#3317=(
BOUNDED_SURFACE()
B_SPLINE_SURFACE(3,2,((#423130,#423131,#423132),(#423133,#423134,#423135),
(#423136,#423137,#423138),(#423139,#423140,#423141)),.UNSPECIFIED.,.F.,
 .F.,.F.)
B_SPLINE_SURFACE_WITH_KNOTS((4,4),(3,3),(-5.22358356749282E-6,5.74594192424278E-5),
(-0.00127120052060601,1.),.UNSPECIFIED.)
GEOMETRIC_REPRESENTATION_ITEM()
RATIONAL_B_SPLINE_SURFACE(((1.00054449313177,0.785835073638756,1.),(1.00047707767477,
0.81235152635884,1.),(1.00044031788588,0.826810216506276,1.),(1.0004477765332,
0.823876514387247,1.)))
REPRESENTATION_ITEM('')
SURFACE()
);
#3318=(
BOUNDED_SURFACE()
B_SPLINE_SURFACE(3,2,((#423143,#423144,#423145),(#423146,#423147,#423148),
(#423149,#423150,#423151),(#423152,#423153,#423154)),.UNSPECIFIED.,.F.,
 .F.,.F.)
B_SPLINE_SURFACE_WITH_KNOTS((4,4),(3,3),(1.0842021724855E-19,4.88747512969881E-5),
(-0.000215805215834578,1.),.UNSPECIFIED.)
GEOMETRIC_REPRESENTATION_ITEM()
RATIONAL_B_SPLINE_SURFACE(((1.00008915600353,0.793434085499676,1.),(1.00008930225006,
0.793095246303207,1.),(1.00008944684628,0.792760230720503,1.),(1.00008958984407,
0.792428918540515,1.)))
REPRESENTATION_ITEM('')
SURFACE()
);
#3319=(
BOUNDED_SURFACE()
B_SPLINE_SURFACE(3,2,((#423156,#423157,#423158),(#423159,#423160,#423161),
(#423162,#423163,#423164),(#423165,#423166,#423167),(#423168,#423169,#423170),
(#423171,#423172,#423173)),.UNSPECIFIED.,.F.,.F.,.F.)
B_SPLINE_SURFACE_WITH_KNOTS((4,2,4),(3,3),(1.6940658945086E-19,7.62675010863196E-5,
0.000152535002172639),(0.,1.0215234820306),.UNSPECIFIED.)
GEOMETRIC_REPRESENTATION_ITEM()
RATIONAL_B_SPLINE_SURFACE(((1.,0.789033595401268,1.00908146323688),(1.,
0.857071781054856,1.00615262590426),(1.,0.922087264710712,1.00335390671591),
(1.,0.922394466502396,1.00334068261142),(1.,0.857224384599053,1.00614605678498),
(1.,0.789033595401663,1.00908146323686)))
REPRESENTATION_ITEM('')
SURFACE()
);
#3320=(
BOUNDED_SURFACE()
B_SPLINE_SURFACE(3,2,((#423175,#423176,#423177),(#423178,#423179,#423180),
(#423181,#423182,#423183),(#423184,#423185,#423186)),.UNSPECIFIED.,.F.,
 .F.,.F.)
B_SPLINE_SURFACE_WITH_KNOTS((4,4),(3,3),(1.62630325872826E-19,4.88747512969884E-5),
(-0.000215489857172023,1.),.UNSPECIFIED.)
GEOMETRIC_REPRESENTATION_ITEM()
RATIONAL_B_SPLINE_SURFACE(((1.00008945889719,0.792428983985717,1.),(1.0000893161084,
0.792760296061256,1.),(1.00008917172353,0.793095311538344,1.),(1.00008902569076,
0.793434150627968,1.)))
REPRESENTATION_ITEM('')
SURFACE()
);
#3321=(
BOUNDED_SURFACE()
B_SPLINE_SURFACE(3,2,((#423188,#423189,#423190),(#423191,#423192,#423193),
(#423194,#423195,#423196),(#423197,#423198,#423199)),.UNSPECIFIED.,.F.,
 .F.,.F.)
B_SPLINE_SURFACE_WITH_KNOTS((4,4),(3,3),(-5.21974905013089E-6,5.74172395514394E-5),
(-0.00139822857781282,1.00051312364071),.UNSPECIFIED.)
GEOMETRIC_REPRESENTATION_ITEM()
RATIONAL_B_SPLINE_SURFACE(((1.00049256947259,0.823768952243961,1.00018060397851),
(1.0004844821573,0.826662424388242,1.00017763870884),(1.00052427784038,
0.812424361909329,1.00019223006923),(1.00059912365874,0.785646094632678,
1.00021967280233)))
REPRESENTATION_ITEM('')
SURFACE()
);
#3322=(
BOUNDED_SURFACE()
B_SPLINE_SURFACE(3,2,((#423203,#423204,#423205),(#423206,#423207,#423208),
(#423209,#423210,#423211),(#423212,#423213,#423214)),.UNSPECIFIED.,.F.,
 .F.,.F.)
B_SPLINE_SURFACE_WITH_KNOTS((4,4),(3,3),(3.2298077433778E-5,9.63764854872258E-5),
(-0.00154325936401433,1.01095292447554),.UNSPECIFIED.)
GEOMETRIC_REPRESENTATION_ITEM()
RATIONAL_B_SPLINE_SURFACE(((1.00023530983303,0.922925743796134,1.00168574728333),
(1.00015136166128,0.950422439594194,1.00108434699061),(1.00033574337404,
0.890029368953921,1.0024052478955),(1.00054260094231,0.822274473168267,
1.00388716464862)))
REPRESENTATION_ITEM('')
SURFACE()
);
#3323=(
BOUNDED_SURFACE()
B_SPLINE_SURFACE(3,2,((#423314,#423315,#423316),(#423317,#423318,#423319),
(#423320,#423321,#423322),(#423323,#423324,#423325)),.UNSPECIFIED.,.F.,
 .F.,.F.)
B_SPLINE_SURFACE_WITH_KNOTS((4,4),(3,3),(0.,0.000101260117256737),(0.,1.),
 .UNSPECIFIED.)
GEOMETRIC_REPRESENTATION_ITEM()
RATIONAL_B_SPLINE_SURFACE(((1.,0.796615278835173,1.),(1.,0.795896038055955,
1.),(1.,0.795193354661339,1.),(1.,0.794506193185541,1.)))
REPRESENTATION_ITEM('')
SURFACE()
);
#3324=(
BOUNDED_SURFACE()
B_SPLINE_SURFACE(3,2,((#423363,#423364,#423365),(#423366,#423367,#423368),
(#423369,#423370,#423371),(#423372,#423373,#423374),(#423375,#423376,#423377),
(#423378,#423379,#423380)),.UNSPECIFIED.,.F.,.F.,.F.)
B_SPLINE_SURFACE_WITH_KNOTS((4,2,4),(3,3),(1.575481281893E-19,1.66936432462295E-5,
3.33872864924588E-5),(0.,1.),.UNSPECIFIED.)
GEOMETRIC_REPRESENTATION_ITEM()
RATIONAL_B_SPLINE_SURFACE(((1.,0.796615278835179,1.),(1.,0.862310524418127,
1.),(1.,0.923774472010525,1.),(1.,0.923983993203428,1.),(1.,0.86257487372094,
1.),(1.,0.796615278835181,1.)))
REPRESENTATION_ITEM('')
SURFACE()
);
#3325=(
BOUNDED_SURFACE()
B_SPLINE_SURFACE(3,2,((#423417,#423418,#423419),(#423420,#423421,#423422),
(#423423,#423424,#423425),(#423426,#423427,#423428)),.UNSPECIFIED.,.F.,
 .F.,.F.)
B_SPLINE_SURFACE_WITH_KNOTS((4,4),(3,3),(-2.16840434497101E-19,0.000101244905251112),
(0.,1.),.UNSPECIFIED.)
GEOMETRIC_REPRESENTATION_ITEM()
RATIONAL_B_SPLINE_SURFACE(((1.,0.79661527883517,1.),(1.,0.795896146109793,
1.),(1.,0.795193565796494,1.),(1.,0.794506502889899,1.)))
REPRESENTATION_ITEM('')
SURFACE()
);
#3326=(
BOUNDED_SURFACE()
B_SPLINE_SURFACE(3,2,((#423464,#423465,#423466),(#423467,#423468,#423469),
(#423470,#423471,#423472),(#423473,#423474,#423475)),.UNSPECIFIED.,.F.,
 .F.,.F.)
B_SPLINE_SURFACE_WITH_KNOTS((4,4),(3,3),(2.85968127239939E-5,9.24681548475817E-5),
(-0.00167900678765756,1.01130827127822),.UNSPECIFIED.)
GEOMETRIC_REPRESENTATION_ITEM()
RATIONAL_B_SPLINE_SURFACE(((1.00059040895256,0.822187541868073,1.00401468696657),
(1.00036527718164,0.889990093671443,1.00248382673391),(1.00016469515024,
0.95039904225788,1.00111990082511),(1.00025604274009,0.922888044285994,
1.00174104990631)))
REPRESENTATION_ITEM('')
SURFACE()
);
#3327=(
BOUNDED_SURFACE()
B_SPLINE_SURFACE(3,2,((#423479,#423480,#423481),(#423482,#423483,#423484),
(#423485,#423486,#423487),(#423488,#423489,#423490)),.UNSPECIFIED.,.F.,
 .F.,.F.)
B_SPLINE_SURFACE_WITH_KNOTS((4,4),(3,3),(-5.22358356749279E-6,5.74594192424278E-5),
(-0.00127120052058266,1.),.UNSPECIFIED.)
GEOMETRIC_REPRESENTATION_ITEM()
RATIONAL_B_SPLINE_SURFACE(((1.00054449313176,0.785835073638761,1.),(1.00047707767476,
0.812351526358851,1.),(1.00044031788587,0.826810216506278,1.),(1.0004477765332,
0.823876514387255,1.)))
REPRESENTATION_ITEM('')
SURFACE()
);
#3328=(
BOUNDED_SURFACE()
B_SPLINE_SURFACE(3,2,((#423492,#423493,#423494),(#423495,#423496,#423497),
(#423498,#423499,#423500),(#423501,#423502,#423503)),.UNSPECIFIED.,.F.,
 .F.,.F.)
B_SPLINE_SURFACE_WITH_KNOTS((4,4),(3,3),(-5.96311194867027E-19,4.88747512969881E-5),
(-0.000215805215785883,1.),.UNSPECIFIED.)
GEOMETRIC_REPRESENTATION_ITEM()
RATIONAL_B_SPLINE_SURFACE(((1.00008915600351,0.793434085499684,1.),(1.00008930225004,
0.793095246303244,1.),(1.00008944684626,0.79276023072049,1.),(1.00008958984405,
0.792428918540532,1.)))
REPRESENTATION_ITEM('')
SURFACE()
);
#3329=(
BOUNDED_SURFACE()
B_SPLINE_SURFACE(3,2,((#423505,#423506,#423507),(#423508,#423509,#423510),
(#423511,#423512,#423513),(#423514,#423515,#423516),(#423517,#423518,#423519),
(#423520,#423521,#423522)),.UNSPECIFIED.,.F.,.F.,.F.)
B_SPLINE_SURFACE_WITH_KNOTS((4,2,4),(3,3),(1.76182853028894E-19,7.62675010863197E-5,
0.000152535002172639),(0.,1.0215234820307),.UNSPECIFIED.)
GEOMETRIC_REPRESENTATION_ITEM()
RATIONAL_B_SPLINE_SURFACE(((1.,0.789033595401244,1.00908146323693),(1.,
0.857071781054812,1.00615262590429),(1.,0.922087264710758,1.00335390671592),
(1.,0.922394466502343,1.00334068261144),(1.,0.857224384599075,1.00614605678501),
(1.,0.789033595401637,1.00908146323691)))
REPRESENTATION_ITEM('')
SURFACE()
);
#3330=(
BOUNDED_SURFACE()
B_SPLINE_SURFACE(3,2,((#423524,#423525,#423526),(#423527,#423528,#423529),
(#423530,#423531,#423532),(#423533,#423534,#423535)),.UNSPECIFIED.,.F.,
 .F.,.F.)
B_SPLINE_SURFACE_WITH_KNOTS((4,4),(3,3),(5.42101086242752E-20,4.88747512969881E-5),
(-0.00021548985687673,1.),.UNSPECIFIED.)
GEOMETRIC_REPRESENTATION_ITEM()
RATIONAL_B_SPLINE_SURFACE(((1.00008945889707,0.792428983985781,1.),(1.00008931610828,
0.792760296061318,1.),(1.00008917172341,0.793095311538399,1.),(1.00008902569063,
0.793434150628026,1.)))
REPRESENTATION_ITEM('')
SURFACE()
);
#3331=(
BOUNDED_SURFACE()
B_SPLINE_SURFACE(3,2,((#423537,#423538,#423539),(#423540,#423541,#423542),
(#423543,#423544,#423545),(#423546,#423547,#423548)),.UNSPECIFIED.,.F.,
 .F.,.F.)
B_SPLINE_SURFACE_WITH_KNOTS((4,4),(3,3),(-5.2197490501309E-6,5.74172395514395E-5),
(-0.00139822857796642,1.00051312364078),.UNSPECIFIED.)
GEOMETRIC_REPRESENTATION_ITEM()
RATIONAL_B_SPLINE_SURFACE(((1.00049256947265,0.82376895224392,1.00018060397853),
(1.00048448215735,0.826662424388195,1.00017763870886),(1.00052427784044,
0.81242436190929,1.00019223006926),(1.0005991236588,0.785646094632626,1.00021967280236)))
REPRESENTATION_ITEM('')
SURFACE()
);
#3332=(
BOUNDED_SURFACE()
B_SPLINE_SURFACE(3,2,((#423552,#423553,#423554),(#423555,#423556,#423557),
(#423558,#423559,#423560),(#423561,#423562,#423563)),.UNSPECIFIED.,.F.,
 .F.,.F.)
B_SPLINE_SURFACE_WITH_KNOTS((4,4),(3,3),(3.2298077433778E-5,9.6376485487226E-5),
(-0.00154325936299762,1.01095292447557),.UNSPECIFIED.)
GEOMETRIC_REPRESENTATION_ITEM()
RATIONAL_B_SPLINE_SURFACE(((1.00023530983288,0.922925743796211,1.00168574728333),
(1.00015136166118,0.950422439594257,1.00108434699061),(1.00033574337382,
0.89002936895402,1.00240524789551),(1.00054260094195,0.822274473168449,
1.00388716464863)))
REPRESENTATION_ITEM('')
SURFACE()
);
#3333=(
BOUNDED_SURFACE()
B_SPLINE_SURFACE(3,2,((#423663,#423664,#423665),(#423666,#423667,#423668),
(#423669,#423670,#423671),(#423672,#423673,#423674)),.UNSPECIFIED.,.F.,
 .F.,.F.)
B_SPLINE_SURFACE_WITH_KNOTS((4,4),(3,3),(0.,0.000101260117256738),(0.,1.),
 .UNSPECIFIED.)
GEOMETRIC_REPRESENTATION_ITEM()
RATIONAL_B_SPLINE_SURFACE(((1.,0.796615278835171,1.),(1.,0.795896038055935,
1.),(1.,0.795193354661353,1.),(1.,0.794506193185547,1.)))
REPRESENTATION_ITEM('')
SURFACE()
);
#3334=(
BOUNDED_SURFACE()
B_SPLINE_SURFACE(3,2,((#423712,#423713,#423714),(#423715,#423716,#423717),
(#423718,#423719,#423720),(#423721,#423722,#423723),(#423724,#423725,#423726),
(#423727,#423728,#423729)),.UNSPECIFIED.,.F.,.F.,.F.)
B_SPLINE_SURFACE_WITH_KNOTS((4,2,4),(3,3),(2.62580213648833E-19,1.66936432462296E-5,
3.33872864924589E-5),(0.,1.),.UNSPECIFIED.)
GEOMETRIC_REPRESENTATION_ITEM()
RATIONAL_B_SPLINE_SURFACE(((1.,0.796615278835186,1.),(1.,0.86231052441813,
1.),(1.,0.923774472010517,1.),(1.,0.923983993203428,1.),(1.,0.862574873720945,
1.),(1.,0.796615278835189,1.)))
REPRESENTATION_ITEM('')
SURFACE()
);
#3335=(
BOUNDED_SURFACE()
B_SPLINE_SURFACE(3,2,((#423766,#423767,#423768),(#423769,#423770,#423771),
(#423772,#423773,#423774),(#423775,#423776,#423777)),.UNSPECIFIED.,.F.,
 .F.,.F.)
B_SPLINE_SURFACE_WITH_KNOTS((4,4),(3,3),(-2.16840434497101E-19,0.000101244905251112),
(0.,1.),.UNSPECIFIED.)
GEOMETRIC_REPRESENTATION_ITEM()
RATIONAL_B_SPLINE_SURFACE(((1.,0.796615278835176,1.),(1.,0.795896146109783,
1.),(1.,0.795193565796507,1.),(1.,0.794506502889895,1.)))
REPRESENTATION_ITEM('')
SURFACE()
);
#3336=(
BOUNDED_SURFACE()
B_SPLINE_SURFACE(3,2,((#423813,#423814,#423815),(#423816,#423817,#423818),
(#423819,#423820,#423821),(#423822,#423823,#423824)),.UNSPECIFIED.,.F.,
 .F.,.F.)
B_SPLINE_SURFACE_WITH_KNOTS((4,4),(3,3),(2.85968127239939E-5,9.24681548475817E-5),
(-0.00167900678632471,1.0113082712783),.UNSPECIFIED.)
GEOMETRIC_REPRESENTATION_ITEM()
RATIONAL_B_SPLINE_SURFACE(((1.00059040895209,0.822187541868296,1.00401468696659),
(1.00036527718135,0.889990093671586,1.00248382673393),(1.00016469515011,
0.950399042257937,1.00111990082512),(1.00025604273989,0.922888044286091,
1.00174104990632)))
REPRESENTATION_ITEM('')
SURFACE()
);
#3337=(
BOUNDED_SURFACE()
B_SPLINE_SURFACE(3,2,((#423828,#423829,#423830),(#423831,#423832,#423833),
(#423834,#423835,#423836),(#423837,#423838,#423839)),.UNSPECIFIED.,.F.,
 .F.,.F.)
B_SPLINE_SURFACE_WITH_KNOTS((4,4),(3,3),(-5.22358356749309E-6,5.74594192424276E-5),
(-0.00127120052057909,1.),.UNSPECIFIED.)
GEOMETRIC_REPRESENTATION_ITEM()
RATIONAL_B_SPLINE_SURFACE(((1.00054449313176,0.785835073638766,1.),(1.00047707767476,
0.812351526358829,1.),(1.00044031788587,0.826810216506286,1.),(1.00044777653319,
0.823876514387251,1.)))
REPRESENTATION_ITEM('')
SURFACE()
);
#3338=(
BOUNDED_SURFACE()
B_SPLINE_SURFACE(3,2,((#423841,#423842,#423843),(#423844,#423845,#423846),
(#423847,#423848,#423849),(#423850,#423851,#423852)),.UNSPECIFIED.,.F.,
 .F.,.F.)
B_SPLINE_SURFACE_WITH_KNOTS((4,4),(3,3),(1.89735380184963E-19,4.88747512969881E-5),
(-0.000215805215101959,1.),.UNSPECIFIED.)
GEOMETRIC_REPRESENTATION_ITEM()
RATIONAL_B_SPLINE_SURFACE(((1.00008915600322,0.793434085499828,1.),(1.00008930224975,
0.793095246303358,1.),(1.00008944684597,0.792760230720646,1.),(1.00008958984377,
0.792428918540672,1.)))
REPRESENTATION_ITEM('')
SURFACE()
);
#3339=(
BOUNDED_SURFACE()
B_SPLINE_SURFACE(3,2,((#423854,#423855,#423856),(#423857,#423858,#423859),
(#423860,#423861,#423862),(#423863,#423864,#423865),(#423866,#423867,#423868),
(#423869,#423870,#423871)),.UNSPECIFIED.,.F.,.F.,.F.)
B_SPLINE_SURFACE_WITH_KNOTS((4,2,4),(3,3),(3.59141969635823E-19,7.62675010863197E-5,
0.000152535002172639),(0.,1.02152348203076),.UNSPECIFIED.)
GEOMETRIC_REPRESENTATION_ITEM()
RATIONAL_B_SPLINE_SURFACE(((1.,0.789033595401229,1.00908146323695),(1.,
0.857071781054903,1.00615262590431),(1.,0.92208726471063,1.00335390671594),
(1.,0.922394466502466,1.00334068261144),(1.,0.857224384598969,1.00614605678503),
(1.,0.789033595401633,1.00908146323693)))
REPRESENTATION_ITEM('')
SURFACE()
);
#3340=(
BOUNDED_SURFACE()
B_SPLINE_SURFACE(3,2,((#423873,#423874,#423875),(#423876,#423877,#423878),
(#423879,#423880,#423881),(#423882,#423883,#423884)),.UNSPECIFIED.,.F.,
 .F.,.F.)
B_SPLINE_SURFACE_WITH_KNOTS((4,4),(3,3),(2.71050543121376E-19,4.88747512969885E-5),
(-0.000215489856772561,1.),.UNSPECIFIED.)
GEOMETRIC_REPRESENTATION_ITEM()
RATIONAL_B_SPLINE_SURFACE(((1.00008945889702,0.7924289839858,1.),(1.00008931610824,
0.792760296061343,1.),(1.00008917172336,0.793095311538421,1.),(1.00008902569059,
0.793434150628045,1.)))
REPRESENTATION_ITEM('')
SURFACE()
);
#3341=(
BOUNDED_SURFACE()
B_SPLINE_SURFACE(3,2,((#423886,#423887,#423888),(#423889,#423890,#423891),
(#423892,#423893,#423894),(#423895,#423896,#423897)),.UNSPECIFIED.,.F.,
 .F.,.F.)
B_SPLINE_SURFACE_WITH_KNOTS((4,4),(3,3),(-5.21974905013086E-6,5.74172395514396E-5),
(-0.0013982285779389,1.00051312364084),.UNSPECIFIED.)
GEOMETRIC_REPRESENTATION_ITEM()
RATIONAL_B_SPLINE_SURFACE(((1.00049256947264,0.823768952243901,1.00018060397855),
(1.00048448215734,0.826662424388219,1.00017763870888),(1.00052427784043,
0.812424361909253,1.00019223006928),(1.00059912365879,0.785646094632636,
1.00021967280238)))
REPRESENTATION_ITEM('')
SURFACE()
);
#3342=(
BOUNDED_SURFACE()
B_SPLINE_SURFACE(3,2,((#423901,#423902,#423903),(#423904,#423905,#423906),
(#423907,#423908,#423909),(#423910,#423911,#423912)),.UNSPECIFIED.,.F.,
 .F.,.F.)
B_SPLINE_SURFACE_WITH_KNOTS((4,4),(3,3),(3.2298077433778E-5,9.63764854872258E-5),
(-0.00154325936356293,1.01095292447534),.UNSPECIFIED.)
GEOMETRIC_REPRESENTATION_ITEM()
RATIONAL_B_SPLINE_SURFACE(((1.00023530983296,0.922925743796183,1.00168574728329),
(1.00015136166124,0.950422439594232,1.00108434699059),(1.00033574337395,
0.890029368953982,1.00240524789546),(1.00054260094215,0.822274473168385,
1.00388716464855)))
REPRESENTATION_ITEM('')
SURFACE()
);
#3343=(
BOUNDED_SURFACE()
B_SPLINE_SURFACE(3,2,((#424012,#424013,#424014),(#424015,#424016,#424017),
(#424018,#424019,#424020),(#424021,#424022,#424023)),.UNSPECIFIED.,.F.,
 .F.,.F.)
B_SPLINE_SURFACE_WITH_KNOTS((4,4),(3,3),(-2.16840434497101E-19,0.000101260117256738),
(0.,1.),.UNSPECIFIED.)
GEOMETRIC_REPRESENTATION_ITEM()
RATIONAL_B_SPLINE_SURFACE(((1.,0.796615278835176,1.),(1.,0.795896038055943,
1.),(1.,0.795193354661342,1.),(1.,0.794506193185552,1.)))
REPRESENTATION_ITEM('')
SURFACE()
);
#3344=(
BOUNDED_SURFACE()
B_SPLINE_SURFACE(3,2,((#424061,#424062,#424063),(#424064,#424065,#424066),
(#424067,#424068,#424069),(#424070,#424071,#424072),(#424073,#424074,#424075),
(#424076,#424077,#424078)),.UNSPECIFIED.,.F.,.F.,.F.)
B_SPLINE_SURFACE_WITH_KNOTS((4,2,4),(3,3),(-1.66018457661843E-19,1.66936432462294E-5,
3.33872864924589E-5),(0.,1.),.UNSPECIFIED.)
GEOMETRIC_REPRESENTATION_ITEM()
RATIONAL_B_SPLINE_SURFACE(((1.,0.796615278835178,1.),(1.,0.862310524418132,
1.),(1.,0.923774472010519,1.),(1.,0.923983993203425,1.),(1.,0.862574873720943,
1.),(1.,0.79661527883518,1.)))
REPRESENTATION_ITEM('')
SURFACE()
);
#3345=(
BOUNDED_SURFACE()
B_SPLINE_SURFACE(3,2,((#424115,#424116,#424117),(#424118,#424119,#424120),
(#424121,#424122,#424123),(#424124,#424125,#424126)),.UNSPECIFIED.,.F.,
 .F.,.F.)
B_SPLINE_SURFACE_WITH_KNOTS((4,4),(3,3),(0.,0.000101244905251112),(0.,1.),
 .UNSPECIFIED.)
GEOMETRIC_REPRESENTATION_ITEM()
RATIONAL_B_SPLINE_SURFACE(((1.,0.796615278835177,1.),(1.,0.795896146109792,
1.),(1.,0.795193565796491,1.),(1.,0.794506502889901,1.)))
REPRESENTATION_ITEM('')
SURFACE()
);
#3346=(
BOUNDED_SURFACE()
B_SPLINE_SURFACE(3,2,((#424162,#424163,#424164),(#424165,#424166,#424167),
(#424168,#424169,#424170),(#424171,#424172,#424173)),.UNSPECIFIED.,.F.,
 .F.,.F.)
B_SPLINE_SURFACE_WITH_KNOTS((4,4),(3,3),(2.85968127239939E-5,9.24681548475815E-5),
(-0.00167900678742142,1.01130827127822),.UNSPECIFIED.)
GEOMETRIC_REPRESENTATION_ITEM()
RATIONAL_B_SPLINE_SURFACE(((1.00059040895248,0.822187541868115,1.00401468696657),
(1.00036527718159,0.889990093671472,1.00248382673391),(1.00016469515022,
0.950399042257889,1.00111990082511),(1.00025604274006,0.922888044286012,
1.00174104990631)))
REPRESENTATION_ITEM('')
SURFACE()
);
#3347=(
BOUNDED_SURFACE()
B_SPLINE_SURFACE(3,2,((#424177,#424178,#424179),(#424180,#424181,#424182),
(#424183,#424184,#424185),(#424186,#424187,#424188)),.UNSPECIFIED.,.F.,
 .F.,.F.)
B_SPLINE_SURFACE_WITH_KNOTS((4,4),(3,3),(-5.22358356749289E-6,5.74594192424278E-5),
(-0.00127120052080811,1.),.UNSPECIFIED.)
GEOMETRIC_REPRESENTATION_ITEM()
RATIONAL_B_SPLINE_SURFACE(((1.00054449313186,0.785835073638708,1.),(1.00047707767484,
0.812351526358813,1.),(1.00044031788595,0.826810216506238,1.),(1.00044777653328,
0.823876514387215,1.)))
REPRESENTATION_ITEM('')
SURFACE()
);
#3348=(
BOUNDED_SURFACE()
B_SPLINE_SURFACE(3,2,((#424190,#424191,#424192),(#424193,#424194,#424195),
(#424196,#424197,#424198),(#424199,#424200,#424201)),.UNSPECIFIED.,.F.,
 .F.,.F.)
B_SPLINE_SURFACE_WITH_KNOTS((4,4),(3,3),(-1.0842021724855E-19,4.88747512969879E-5),
(-0.000215805215245615,1.),.UNSPECIFIED.)
GEOMETRIC_REPRESENTATION_ITEM()
RATIONAL_B_SPLINE_SURFACE(((1.00008915600328,0.793434085499795,1.),(1.00008930224981,
0.793095246303348,1.),(1.00008944684603,0.792760230720603,1.),(1.00008958984383,
0.792428918540643,1.)))
REPRESENTATION_ITEM('')
SURFACE()
);
#3349=(
BOUNDED_SURFACE()
B_SPLINE_SURFACE(3,2,((#424203,#424204,#424205),(#424206,#424207,#424208),
(#424209,#424210,#424211),(#424212,#424213,#424214),(#424215,#424216,#424217),
(#424218,#424219,#424220)),.UNSPECIFIED.,.F.,.F.,.F.)
B_SPLINE_SURFACE_WITH_KNOTS((4,2,4),(3,3),(2.10064170919066E-19,7.62675010863197E-5,
0.000152535002172639),(0.,1.02152348203067),.UNSPECIFIED.)
GEOMETRIC_REPRESENTATION_ITEM()
RATIONAL_B_SPLINE_SURFACE(((1.,0.789033595401254,1.00908146323691),(1.,
0.857071781054834,1.00615262590428),(1.,0.922087264710736,1.00335390671592),
(1.,0.922394466502371,1.00334068261143),(1.,0.857224384599062,1.006146056785),
(1.,0.789033595401649,1.00908146323689)))
REPRESENTATION_ITEM('')
SURFACE()
);
#3350=(
BOUNDED_SURFACE()
B_SPLINE_SURFACE(3,2,((#424222,#424223,#424224),(#424225,#424226,#424227),
(#424228,#424229,#424230),(#424231,#424232,#424233)),.UNSPECIFIED.,.F.,
 .F.,.F.)
B_SPLINE_SURFACE_WITH_KNOTS((4,4),(3,3),(2.16840434497101E-19,4.88747512969881E-5),
(-0.000215489857883573,1.),.UNSPECIFIED.)
GEOMETRIC_REPRESENTATION_ITEM()
RATIONAL_B_SPLINE_SURFACE(((1.00008945889748,0.792428983985569,1.),(1.0000893161087,
0.792760296061112,1.),(1.00008917172382,0.793095311538197,1.),(1.00008902569105,
0.79343415062782,1.)))
REPRESENTATION_ITEM('')
SURFACE()
);
#3351=(
BOUNDED_SURFACE()
B_SPLINE_SURFACE(3,2,((#424235,#424236,#424237),(#424238,#424239,#424240),
(#424241,#424242,#424243),(#424244,#424245,#424246)),.UNSPECIFIED.,.F.,
 .F.,.F.)
B_SPLINE_SURFACE_WITH_KNOTS((4,4),(3,3),(-5.21974905013082E-6,5.74172395514397E-5),
(-0.00139822857780422,1.00051312364062),.UNSPECIFIED.)
GEOMETRIC_REPRESENTATION_ITEM()
RATIONAL_B_SPLINE_SURFACE(((1.00049256947259,0.823768952243966,1.00018060397847),
(1.00048448215729,0.826662424388277,1.0001776387088),(1.00052427784038,
0.812424361909331,1.00019223006919),(1.00059912365873,0.785646094632703,
1.00021967280229)))
REPRESENTATION_ITEM('')
SURFACE()
);
#3352=(
BOUNDED_SURFACE()
B_SPLINE_SURFACE(3,2,((#424250,#424251,#424252),(#424253,#424254,#424255),
(#424256,#424257,#424258),(#424259,#424260,#424261)),.UNSPECIFIED.,.F.,
 .F.,.F.)
B_SPLINE_SURFACE_WITH_KNOTS((4,4),(3,3),(3.22980774337779E-5,9.63764854872256E-5),
(-0.00154325936392538,1.0109529244754),.UNSPECIFIED.)
GEOMETRIC_REPRESENTATION_ITEM()
RATIONAL_B_SPLINE_SURFACE(((1.00023530983302,0.922925743796147,1.0016857472833),
(1.00015136166127,0.950422439594223,1.00108434699059),(1.00033574337402,
0.890029368953931,1.00240524789547),(1.00054260094228,0.822274473168306,
1.00388716464857)))
REPRESENTATION_ITEM('')
SURFACE()
);
#3353=(
BOUNDED_SURFACE()
B_SPLINE_SURFACE(3,2,((#424361,#424362,#424363),(#424364,#424365,#424366),
(#424367,#424368,#424369),(#424370,#424371,#424372)),.UNSPECIFIED.,.F.,
 .F.,.F.)
B_SPLINE_SURFACE_WITH_KNOTS((4,4),(3,3),(0.,0.000101260117256738),(0.,1.),
 .UNSPECIFIED.)
GEOMETRIC_REPRESENTATION_ITEM()
RATIONAL_B_SPLINE_SURFACE(((1.,0.796615278835174,1.),(1.,0.795896038055941,
1.),(1.,0.795193354661351,1.),(1.,0.794506193185546,1.)))
REPRESENTATION_ITEM('')
SURFACE()
);
#3354=(
BOUNDED_SURFACE()
B_SPLINE_SURFACE(3,2,((#424410,#424411,#424412),(#424413,#424414,#424415),
(#424416,#424417,#424418),(#424419,#424420,#424421),(#424422,#424423,#424424),
(#424425,#424426,#424427)),.UNSPECIFIED.,.F.,.F.,.F.)
B_SPLINE_SURFACE_WITH_KNOTS((4,2,4),(3,3),(-8.470329472543E-20,1.66936432462293E-5,
3.33872864924587E-5),(0.,1.),.UNSPECIFIED.)
GEOMETRIC_REPRESENTATION_ITEM()
RATIONAL_B_SPLINE_SURFACE(((1.,0.796615278835174,1.),(1.,0.862310524418127,
1.),(1.,0.923774472010521,1.),(1.,0.923983993203427,1.),(1.,0.862574873720952,
1.),(1.,0.79661527883518,1.)))
REPRESENTATION_ITEM('')
SURFACE()
);
#3355=(
BOUNDED_SURFACE()
B_SPLINE_SURFACE(3,2,((#424464,#424465,#424466),(#424467,#424468,#424469),
(#424470,#424471,#424472),(#424473,#424474,#424475)),.UNSPECIFIED.,.F.,
 .F.,.F.)
B_SPLINE_SURFACE_WITH_KNOTS((4,4),(3,3),(0.,0.000101244905251112),(0.,1.),
 .UNSPECIFIED.)
GEOMETRIC_REPRESENTATION_ITEM()
RATIONAL_B_SPLINE_SURFACE(((1.,0.796615278835171,1.),(1.,0.79589614610979,
1.),(1.,0.795193565796499,1.),(1.,0.7945065028899,1.)))
REPRESENTATION_ITEM('')
SURFACE()
);
#3356=(
BOUNDED_SURFACE()
B_SPLINE_SURFACE(3,2,((#424511,#424512,#424513),(#424514,#424515,#424516),
(#424517,#424518,#424519),(#424520,#424521,#424522)),.UNSPECIFIED.,.F.,
 .F.,.F.)
B_SPLINE_SURFACE_WITH_KNOTS((4,4),(3,3),(2.85968127239939E-5,9.24681548475818E-5),
(-0.00167900678672291,1.01130827127837),.UNSPECIFIED.)
GEOMETRIC_REPRESENTATION_ITEM()
RATIONAL_B_SPLINE_SURFACE(((1.00059040895223,0.822187541868208,1.00401468696662),
(1.00036527718144,0.889990093671545,1.00248382673394),(1.00016469515015,
0.950399042257912,1.00111990082512),(1.00025604273995,0.922888044286054,
1.00174104990633)))
REPRESENTATION_ITEM('')
SURFACE()
);
#3357=(
BOUNDED_SURFACE()
B_SPLINE_SURFACE(3,2,((#424526,#424527,#424528),(#424529,#424530,#424531),
(#424532,#424533,#424534),(#424535,#424536,#424537)),.UNSPECIFIED.,.F.,
 .F.,.F.)
B_SPLINE_SURFACE_WITH_KNOTS((4,4),(3,3),(-5.22358356749156E-6,5.74594192424276E-5),
(-0.00127120052070892,1.),.UNSPECIFIED.)
GEOMETRIC_REPRESENTATION_ITEM()
RATIONAL_B_SPLINE_SURFACE(((1.00054449313182,0.785835073638731,1.),(1.00047707767481,
0.812351526358835,1.),(1.00044031788592,0.826810216506248,1.),(1.00044777653324,
0.823876514387235,1.)))
REPRESENTATION_ITEM('')
SURFACE()
);
#3358=(
BOUNDED_SURFACE()
B_SPLINE_SURFACE(3,2,((#424539,#424540,#424541),(#424542,#424543,#424544),
(#424545,#424546,#424547),(#424548,#424549,#424550)),.UNSPECIFIED.,.F.,
 .F.,.F.)
B_SPLINE_SURFACE_WITH_KNOTS((4,4),(3,3),(-1.62630325872826E-19,4.8874751296988E-5),
(-0.000215805215067234,1.),.UNSPECIFIED.)
GEOMETRIC_REPRESENTATION_ITEM()
RATIONAL_B_SPLINE_SURFACE(((1.00008915600321,0.793434085499832,1.),(1.00008930224974,
0.793095246303371,1.),(1.00008944684596,0.792760230720652,1.),(1.00008958984375,
0.792428918540681,1.)))
REPRESENTATION_ITEM('')
SURFACE()
);
#3359=(
BOUNDED_SURFACE()
B_SPLINE_SURFACE(3,2,((#424552,#424553,#424554),(#424555,#424556,#424557),
(#424558,#424559,#424560),(#424561,#424562,#424563),(#424564,#424565,#424566),
(#424567,#424568,#424569)),.UNSPECIFIED.,.F.,.F.,.F.)
B_SPLINE_SURFACE_WITH_KNOTS((4,2,4),(3,3),(6.09863722023096E-20,7.62675010863196E-5,
0.000152535002172639),(0.,1.02152348203075),.UNSPECIFIED.)
GEOMETRIC_REPRESENTATION_ITEM()
RATIONAL_B_SPLINE_SURFACE(((1.,0.789033595401234,1.00908146323695),(1.,
0.857071781054814,1.00615262590431),(1.,0.922087264710743,1.00335390671593),
(1.,0.922394466502349,1.00334068261145),(1.,0.857224384599061,1.00614605678502),
(1.,0.789033595401633,1.00908146323693)))
REPRESENTATION_ITEM('')
SURFACE()
);
#3360=(
BOUNDED_SURFACE()
B_SPLINE_SURFACE(3,2,((#424571,#424572,#424573),(#424574,#424575,#424576),
(#424577,#424578,#424579),(#424580,#424581,#424582)),.UNSPECIFIED.,.F.,
 .F.,.F.)
B_SPLINE_SURFACE_WITH_KNOTS((4,4),(3,3),(3.25260651745651E-19,4.88747512969883E-5),
(-0.000215489856881676,1.),.UNSPECIFIED.)
GEOMETRIC_REPRESENTATION_ITEM()
RATIONAL_B_SPLINE_SURFACE(((1.00008945889707,0.792428983985777,1.),(1.00008931610828,
0.792760296061325,1.),(1.00008917172341,0.793095311538386,1.),(1.00008902569064,
0.793434150628026,1.)))
REPRESENTATION_ITEM('')
SURFACE()
);
#3361=(
BOUNDED_SURFACE()
B_SPLINE_SURFACE(3,2,((#424584,#424585,#424586),(#424587,#424588,#424589),
(#424590,#424591,#424592),(#424593,#424594,#424595)),.UNSPECIFIED.,.F.,
 .F.,.F.)
B_SPLINE_SURFACE_WITH_KNOTS((4,4),(3,3),(-5.21974905013085E-6,5.74172395514399E-5),
(-0.00139822857782877,1.00051312364113),.UNSPECIFIED.)
GEOMETRIC_REPRESENTATION_ITEM()
RATIONAL_B_SPLINE_SURFACE(((1.0004925694726,0.823768952243877,1.00018060397866),
(1.0004844821573,0.826662424388176,1.00017763870898),(1.00052427784039,
0.812424361909237,1.00019223006939),(1.00059912365874,0.785646094632581,
1.00021967280251)))
REPRESENTATION_ITEM('')
SURFACE()
);
#3362=(
BOUNDED_SURFACE()
B_SPLINE_SURFACE(3,2,((#424599,#424600,#424601),(#424602,#424603,#424604),
(#424605,#424606,#424607),(#424608,#424609,#424610)),.UNSPECIFIED.,.F.,
 .F.,.F.)
B_SPLINE_SURFACE_WITH_KNOTS((4,4),(3,3),(3.22980774337781E-5,9.63764854872251E-5),
(-0.00154325936250836,1.01095292447547),.UNSPECIFIED.)
GEOMETRIC_REPRESENTATION_ITEM()
RATIONAL_B_SPLINE_SURFACE(((1.0002353098328,0.922925743796259,1.00168574728331),
(1.00015136166114,0.950422439594272,1.0010843469906),(1.00033574337372,
0.890029368954089,1.00240524789548),(1.00054260094178,0.822274473168546,
1.00388716464859)))
REPRESENTATION_ITEM('')
SURFACE()
);
#3363=(
BOUNDED_SURFACE()
B_SPLINE_SURFACE(3,2,((#424710,#424711,#424712),(#424713,#424714,#424715),
(#424716,#424717,#424718),(#424719,#424720,#424721)),.UNSPECIFIED.,.F.,
 .F.,.F.)
B_SPLINE_SURFACE_WITH_KNOTS((4,4),(3,3),(0.,0.000101260117256738),(0.,1.),
 .UNSPECIFIED.)
GEOMETRIC_REPRESENTATION_ITEM()
RATIONAL_B_SPLINE_SURFACE(((1.,0.796615278835171,1.),(1.,0.795896038055945,
1.),(1.,0.795193354661335,1.),(1.,0.794506193185544,1.)))
REPRESENTATION_ITEM('')
SURFACE()
);
#3364=(
BOUNDED_SURFACE()
B_SPLINE_SURFACE(3,2,((#424759,#424760,#424761),(#424762,#424763,#424764),
(#424765,#424766,#424767),(#424768,#424769,#424770),(#424771,#424772,#424773),
(#424774,#424775,#424776)),.UNSPECIFIED.,.F.,.F.,.F.)
B_SPLINE_SURFACE_WITH_KNOTS((4,2,4),(3,3),(-3.11708124589583E-19,1.66936432462293E-5,
3.33872864924589E-5),(0.,1.),.UNSPECIFIED.)
GEOMETRIC_REPRESENTATION_ITEM()
RATIONAL_B_SPLINE_SURFACE(((1.,0.796615278835172,1.),(1.,0.862310524418136,
1.),(1.,0.923774472010518,1.),(1.,0.923983993203427,1.),(1.,0.862574873720949,
1.),(1.,0.796615278835185,1.)))
REPRESENTATION_ITEM('')
SURFACE()
);
#3365=(
BOUNDED_SURFACE()
B_SPLINE_SURFACE(3,2,((#424813,#424814,#424815),(#424816,#424817,#424818),
(#424819,#424820,#424821),(#424822,#424823,#424824)),.UNSPECIFIED.,.F.,
 .F.,.F.)
B_SPLINE_SURFACE_WITH_KNOTS((4,4),(3,3),(0.,0.000101244905251112),(0.,1.),
 .UNSPECIFIED.)
GEOMETRIC_REPRESENTATION_ITEM()
RATIONAL_B_SPLINE_SURFACE(((1.,0.796615278835172,1.),(1.,0.795896146109796,
1.),(1.,0.795193565796497,1.),(1.,0.794506502889904,1.)))
REPRESENTATION_ITEM('')
SURFACE()
);
#3366=(
BOUNDED_SURFACE()
B_SPLINE_SURFACE(3,2,((#424860,#424861,#424862),(#424863,#424864,#424865),
(#424866,#424867,#424868),(#424869,#424870,#424871)),.UNSPECIFIED.,.F.,
 .F.,.F.)
B_SPLINE_SURFACE_WITH_KNOTS((4,4),(3,3),(2.85968127239939E-5,9.24681548475822E-5),
(-0.00167900678647274,1.01130827127832),.UNSPECIFIED.)
GEOMETRIC_REPRESENTATION_ITEM()
RATIONAL_B_SPLINE_SURFACE(((1.00059040895214,0.82218754186827,1.0040146869666),
(1.00036527718138,0.889990093671564,1.00248382673393),(1.00016469515012,
0.950399042257935,1.00111990082512),(1.00025604273991,0.922888044286078,
1.00174104990633)))
REPRESENTATION_ITEM('')
SURFACE()
);
#3367=(
BOUNDED_SURFACE()
B_SPLINE_SURFACE(3,2,((#424875,#424876,#424877),(#424878,#424879,#424880),
(#424881,#424882,#424883),(#424884,#424885,#424886)),.UNSPECIFIED.,.F.,
 .F.,.F.)
B_SPLINE_SURFACE_WITH_KNOTS((4,4),(3,3),(-5.22358356749317E-6,5.74594192424277E-5),
(-0.0012712005206476,1.),.UNSPECIFIED.)
GEOMETRIC_REPRESENTATION_ITEM()
RATIONAL_B_SPLINE_SURFACE(((1.00054449313179,0.785835073638738,1.),(1.00047707767478,
0.812351526358837,1.),(1.0004403178859,0.826810216506266,1.),(1.00044777653322,
0.823876514387239,1.)))
REPRESENTATION_ITEM('')
SURFACE()
);
#3368=(
BOUNDED_SURFACE()
B_SPLINE_SURFACE(3,2,((#424888,#424889,#424890),(#424891,#424892,#424893),
(#424894,#424895,#424896),(#424897,#424898,#424899)),.UNSPECIFIED.,.F.,
 .F.,.F.)
B_SPLINE_SURFACE_WITH_KNOTS((4,4),(3,3),(-2.71050543121376E-19,4.8874751296988E-5),
(-0.000215805215662181,1.),.UNSPECIFIED.)
GEOMETRIC_REPRESENTATION_ITEM()
RATIONAL_B_SPLINE_SURFACE(((1.00008915600345,0.793434085499707,1.),(1.00008930224999,
0.793095246303258,1.),(1.00008944684621,0.792760230720517,1.),(1.000089589844,
0.792428918540555,1.)))
REPRESENTATION_ITEM('')
SURFACE()
);
#3369=(
BOUNDED_SURFACE()
B_SPLINE_SURFACE(3,2,((#424901,#424902,#424903),(#424904,#424905,#424906),
(#424907,#424908,#424909),(#424910,#424911,#424912),(#424913,#424914,#424915),
(#424916,#424917,#424918)),.UNSPECIFIED.,.F.,.F.,.F.)
B_SPLINE_SURFACE_WITH_KNOTS((4,2,4),(3,3),(3.32036915323686E-19,7.62675010863199E-5,
0.000152535002172639),(0.,1.02152348203075),.UNSPECIFIED.)
GEOMETRIC_REPRESENTATION_ITEM()
RATIONAL_B_SPLINE_SURFACE(((1.,0.789033595401233,1.00908146323695),(1.,
0.857071781054844,1.00615262590431),(1.,0.922087264710704,1.00335390671593),
(1.,0.922394466502388,1.00334068261145),(1.,0.857224384599028,1.00614605678503),
(1.,0.789033595401637,1.00908146323693)))
REPRESENTATION_ITEM('')
SURFACE()
);
#3370=(
BOUNDED_SURFACE()
B_SPLINE_SURFACE(3,2,((#424920,#424921,#424922),(#424923,#424924,#424925),
(#424926,#424927,#424928),(#424929,#424930,#424931)),.UNSPECIFIED.,.F.,
 .F.,.F.)
B_SPLINE_SURFACE_WITH_KNOTS((4,4),(3,3),(2.43945488809238E-19,4.88747512969883E-5),
(-0.000215489857039072,1.),.UNSPECIFIED.)
GEOMETRIC_REPRESENTATION_ITEM()
RATIONAL_B_SPLINE_SURFACE(((1.00008945889713,0.792428983985745,1.),(1.00008931610835,
0.792760296061297,1.),(1.00008917172347,0.793095311538356,1.),(1.0000890256907,
0.793434150627995,1.)))
REPRESENTATION_ITEM('')
SURFACE()
);
#3371=(
BOUNDED_SURFACE()
B_SPLINE_SURFACE(3,2,((#424933,#424934,#424935),(#424936,#424937,#424938),
(#424939,#424940,#424941),(#424942,#424943,#424944)),.UNSPECIFIED.,.F.,
 .F.,.F.)
B_SPLINE_SURFACE_WITH_KNOTS((4,4),(3,3),(-5.21974905012875E-6,5.74172395514397E-5),
(-0.00139822857739768,1.00051312364068),.UNSPECIFIED.)
GEOMETRIC_REPRESENTATION_ITEM()
RATIONAL_B_SPLINE_SURFACE(((1.00049256947245,0.82376895224404,1.0001806039785),
(1.00048448215715,0.826662424388324,1.00017763870882),(1.00052427784022,
0.812424361909407,1.00019223006921),(1.00059912365856,0.785646094632773,
1.00021967280231)))
REPRESENTATION_ITEM('')
SURFACE()
);
#3372=(
BOUNDED_SURFACE()
B_SPLINE_SURFACE(3,2,((#424948,#424949,#424950),(#424951,#424952,#424953),
(#424954,#424955,#424956),(#424957,#424958,#424959)),.UNSPECIFIED.,.F.,
 .F.,.F.)
B_SPLINE_SURFACE_WITH_KNOTS((4,4),(3,3),(3.22980774337779E-5,9.63764854872251E-5),
(-0.0015432593636694,1.01095292447539),.UNSPECIFIED.)
GEOMETRIC_REPRESENTATION_ITEM()
RATIONAL_B_SPLINE_SURFACE(((1.00023530983298,0.922925743796173,1.0016857472833),
(1.00015136166125,0.950422439594226,1.00108434699059),(1.00033574337397,
0.890029368953967,1.00240524789547),(1.00054260094219,0.822274473168352,
1.00388716464857)))
REPRESENTATION_ITEM('')
SURFACE()
);
#3373=(
BOUNDED_SURFACE()
B_SPLINE_SURFACE(3,2,((#425059,#425060,#425061),(#425062,#425063,#425064),
(#425065,#425066,#425067),(#425068,#425069,#425070)),.UNSPECIFIED.,.F.,
 .F.,.F.)
B_SPLINE_SURFACE_WITH_KNOTS((4,4),(3,3),(0.,0.000101260117256738),(0.,1.),
 .UNSPECIFIED.)
GEOMETRIC_REPRESENTATION_ITEM()
RATIONAL_B_SPLINE_SURFACE(((1.,0.796615278835169,1.),(1.,0.795896038055937,
1.),(1.,0.795193354661346,1.),(1.,0.794506193185544,1.)))
REPRESENTATION_ITEM('')
SURFACE()
);
#3374=(
BOUNDED_SURFACE()
B_SPLINE_SURFACE(3,2,((#425108,#425109,#425110),(#425111,#425112,#425113),
(#425114,#425115,#425116),(#425117,#425118,#425119),(#425120,#425121,#425122),
(#425123,#425124,#425125)),.UNSPECIFIED.,.F.,.F.,.F.)
B_SPLINE_SURFACE_WITH_KNOTS((4,2,4),(3,3),(7.45388993583784E-20,1.66936432462296E-5,
3.3387286492459E-5),(0.,1.),.UNSPECIFIED.)
GEOMETRIC_REPRESENTATION_ITEM()
RATIONAL_B_SPLINE_SURFACE(((1.,0.796615278835178,1.),(1.,0.862310524418132,
1.),(1.,0.923774472010522,1.),(1.,0.923983993203424,1.),(1.,0.862574873720963,
1.),(1.,0.796615278835185,1.)))
REPRESENTATION_ITEM('')
SURFACE()
);
#3375=(
BOUNDED_SURFACE()
B_SPLINE_SURFACE(3,2,((#425162,#425163,#425164),(#425165,#425166,#425167),
(#425168,#425169,#425170),(#425171,#425172,#425173)),.UNSPECIFIED.,.F.,
 .F.,.F.)
B_SPLINE_SURFACE_WITH_KNOTS((4,4),(3,3),(0.,0.000101244905251112),(0.,1.),
 .UNSPECIFIED.)
GEOMETRIC_REPRESENTATION_ITEM()
RATIONAL_B_SPLINE_SURFACE(((1.,0.796615278835173,1.),(1.,0.79589614610979,
1.),(1.,0.7951935657965,1.),(1.,0.794506502889901,1.)))
REPRESENTATION_ITEM('')
SURFACE()
);
#3376=(
BOUNDED_SURFACE()
B_SPLINE_SURFACE(3,2,((#425209,#425210,#425211),(#425212,#425213,#425214),
(#425215,#425216,#425217),(#425218,#425219,#425220)),.UNSPECIFIED.,.F.,
 .F.,.F.)
B_SPLINE_SURFACE_WITH_KNOTS((4,4),(3,3),(2.85968127239939E-5,9.24681548475816E-5),
(-0.00167900678789399,1.01130827127835),.UNSPECIFIED.)
GEOMETRIC_REPRESENTATION_ITEM()
RATIONAL_B_SPLINE_SURFACE(((1.00059040895264,0.822187541868006,1.00401468696661),
(1.00036527718169,0.889990093671416,1.00248382673394),(1.00016469515026,
0.950399042257849,1.00111990082512),(1.00025604274013,0.922888044285966,
1.00174104990633)))
REPRESENTATION_ITEM('')
SURFACE()
);
#3377=(
BOUNDED_SURFACE()
B_SPLINE_SURFACE(3,2,((#425224,#425225,#425226),(#425227,#425228,#425229),
(#425230,#425231,#425232),(#425233,#425234,#425235)),.UNSPECIFIED.,.F.,
 .F.,.F.)
B_SPLINE_SURFACE_WITH_KNOTS((4,4),(3,3),(-5.22358356749295E-6,5.74594192424276E-5),
(-0.00127120052076198,1.),.UNSPECIFIED.)
GEOMETRIC_REPRESENTATION_ITEM()
RATIONAL_B_SPLINE_SURFACE(((1.00054449313184,0.785835073638721,1.),(1.00047707767483,
0.812351526358804,1.),(1.00044031788594,0.826810216506243,1.),(1.00044777653326,
0.823876514387219,1.)))
REPRESENTATION_ITEM('')
SURFACE()
);
#3378=(
BOUNDED_SURFACE()
B_SPLINE_SURFACE(3,2,((#425237,#425238,#425239),(#425240,#425241,#425242),
(#425243,#425244,#425245),(#425246,#425247,#425248)),.UNSPECIFIED.,.F.,
 .F.,.F.)
B_SPLINE_SURFACE_WITH_KNOTS((4,4),(3,3),(-4.60785923306339E-19,4.88747512969881E-5),
(-0.000215805215153769,1.),.UNSPECIFIED.)
GEOMETRIC_REPRESENTATION_ITEM()
RATIONAL_B_SPLINE_SURFACE(((1.00008915600324,0.793434085499811,1.),(1.00008930224978,
0.793095246303347,1.),(1.000089446846,0.792760230720631,1.),(1.00008958984379,
0.792428918540661,1.)))
REPRESENTATION_ITEM('')
SURFACE()
);
#3379=(
BOUNDED_SURFACE()
B_SPLINE_SURFACE(3,2,((#425250,#425251,#425252),(#425253,#425254,#425255),
(#425256,#425257,#425258),(#425259,#425260,#425261),(#425262,#425263,#425264),
(#425265,#425266,#425267)),.UNSPECIFIED.,.F.,.F.,.F.)
B_SPLINE_SURFACE_WITH_KNOTS((4,2,4),(3,3),(2.84603070277445E-19,7.62675010863198E-5,
0.000152535002172639),(0.,1.02152348203076),.UNSPECIFIED.)
GEOMETRIC_REPRESENTATION_ITEM()
RATIONAL_B_SPLINE_SURFACE(((1.,0.789033595401233,1.00908146323695),(1.,
0.857071781054873,1.00615262590431),(1.,0.922087264710668,1.00335390671593),
(1.,0.92239446650242,1.00334068261145),(1.,0.85722438459901,1.00614605678503),
(1.,0.789033595401633,1.00908146323693)))
REPRESENTATION_ITEM('')
SURFACE()
);
#3380=(
BOUNDED_SURFACE()
B_SPLINE_SURFACE(3,2,((#425269,#425270,#425271),(#425272,#425273,#425274),
(#425275,#425276,#425277),(#425278,#425279,#425280)),.UNSPECIFIED.,.F.,
 .F.,.F.)
B_SPLINE_SURFACE_WITH_KNOTS((4,4),(3,3),(5.42101086242752E-20,4.88747512969882E-5),
(-0.000215489857037421,1.),.UNSPECIFIED.)
GEOMETRIC_REPRESENTATION_ITEM()
RATIONAL_B_SPLINE_SURFACE(((1.00008945889713,0.792428983985742,1.),(1.00008931610835,
0.792760296061293,1.),(1.00008917172347,0.793095311538357,1.),(1.0000890256907,
0.793434150627994,1.)))
REPRESENTATION_ITEM('')
SURFACE()
);
#3381=(
BOUNDED_SURFACE()
B_SPLINE_SURFACE(3,2,((#425282,#425283,#425284),(#425285,#425286,#425287),
(#425288,#425289,#425290),(#425291,#425292,#425293)),.UNSPECIFIED.,.F.,
 .F.,.F.)
B_SPLINE_SURFACE_WITH_KNOTS((4,4),(3,3),(-5.21974905013094E-6,5.74172395514394E-5),
(-0.00139822857773127,1.00051312364078),.UNSPECIFIED.)
GEOMETRIC_REPRESENTATION_ITEM()
RATIONAL_B_SPLINE_SURFACE(((1.00049256947256,0.823768952243962,1.00018060397853),
(1.00048448215727,0.826662424388245,1.00017763870886),(1.00052427784035,
0.812424361909327,1.00019223006925),(1.0005991236587,0.785646094632678,
1.00021967280236)))
REPRESENTATION_ITEM('')
SURFACE()
);
#3382=(
BOUNDED_SURFACE()
B_SPLINE_SURFACE(3,2,((#425297,#425298,#425299),(#425300,#425301,#425302),
(#425303,#425304,#425305),(#425306,#425307,#425308)),.UNSPECIFIED.,.F.,
 .F.,.F.)
B_SPLINE_SURFACE_WITH_KNOTS((4,4),(3,3),(3.22980774337777E-5,9.63764854872245E-5),
(-0.00154325936314989,1.01095292447545),.UNSPECIFIED.)
GEOMETRIC_REPRESENTATION_ITEM()
RATIONAL_B_SPLINE_SURFACE(((1.0002353098329,0.922925743796211,1.00168574728331),
(1.0001513616612,0.950422439594239,1.0010843469906),(1.00033574337386,0.890029368954025,
1.00240524789548),(1.00054260094201,0.822274473168434,1.00388716464859)))
REPRESENTATION_ITEM('')
SURFACE()
);
#3383=(
BOUNDED_SURFACE()
B_SPLINE_SURFACE(3,2,((#425408,#425409,#425410),(#425411,#425412,#425413),
(#425414,#425415,#425416),(#425417,#425418,#425419)),.UNSPECIFIED.,.F.,
 .F.,.F.)
B_SPLINE_SURFACE_WITH_KNOTS((4,4),(3,3),(0.,0.000101260117256736),(0.,1.),
 .UNSPECIFIED.)
GEOMETRIC_REPRESENTATION_ITEM()
RATIONAL_B_SPLINE_SURFACE(((1.,0.796615278835174,1.),(1.,0.795896038055937,
1.),(1.,0.795193354661362,1.),(1.,0.794506193185534,1.)))
REPRESENTATION_ITEM('')
SURFACE()
);
#3384=(
BOUNDED_SURFACE()
B_SPLINE_SURFACE(3,2,((#425457,#425458,#425459),(#425460,#425461,#425462),
(#425463,#425464,#425465),(#425466,#425467,#425468),(#425469,#425470,#425471),
(#425472,#425473,#425474)),.UNSPECIFIED.,.F.,.F.,.F.)
B_SPLINE_SURFACE_WITH_KNOTS((4,2,4),(3,3),(1.01643953670516E-19,1.66936432462293E-5,
3.33872864924585E-5),(0.,1.),.UNSPECIFIED.)
GEOMETRIC_REPRESENTATION_ITEM()
RATIONAL_B_SPLINE_SURFACE(((1.,0.796615278835177,1.),(1.,0.862310524418127,
1.),(1.,0.923774472010516,1.),(1.,0.923983993203427,1.),(1.,0.862574873720946,
1.),(1.,0.79661527883519,1.)))
REPRESENTATION_ITEM('')
SURFACE()
);
#3385=(
BOUNDED_SURFACE()
B_SPLINE_SURFACE(3,2,((#425511,#425512,#425513),(#425514,#425515,#425516),
(#425517,#425518,#425519),(#425520,#425521,#425522)),.UNSPECIFIED.,.F.,
 .F.,.F.)
B_SPLINE_SURFACE_WITH_KNOTS((4,4),(3,3),(-2.16840434497101E-19,0.000101244905251112),
(0.,1.),.UNSPECIFIED.)
GEOMETRIC_REPRESENTATION_ITEM()
RATIONAL_B_SPLINE_SURFACE(((1.,0.79661527883517,1.),(1.,0.795896146109793,
1.),(1.,0.795193565796498,1.),(1.,0.794506502889901,1.)))
REPRESENTATION_ITEM('')
SURFACE()
);
#3386=(
BOUNDED_SURFACE()
B_SPLINE_SURFACE(3,2,((#425558,#425559,#425560),(#425561,#425562,#425563),
(#425564,#425565,#425566),(#425567,#425568,#425569)),.UNSPECIFIED.,.F.,
 .F.,.F.)
B_SPLINE_SURFACE_WITH_KNOTS((4,4),(3,3),(2.85968127239939E-5,9.24681548475815E-5),
(-0.00167900678784821,1.01130827127814),.UNSPECIFIED.)
GEOMETRIC_REPRESENTATION_ITEM()
RATIONAL_B_SPLINE_SURFACE(((1.00059040895263,0.822187541868056,1.00401468696653),
(1.00036527718168,0.889990093671432,1.00248382673389),(1.00016469515026,
0.950399042257876,1.0011199008251),(1.00025604274012,0.922888044285984,
1.0017410499063)))
REPRESENTATION_ITEM('')
SURFACE()
);
#3387=(
BOUNDED_SURFACE()
B_SPLINE_SURFACE(3,2,((#425573,#425574,#425575),(#425576,#425577,#425578),
(#425579,#425580,#425581),(#425582,#425583,#425584)),.UNSPECIFIED.,.F.,
 .F.,.F.)
B_SPLINE_SURFACE_WITH_KNOTS((4,4),(3,3),(-5.22358356749054E-6,5.74594192424279E-5),
(-0.00127120052066195,1.),.UNSPECIFIED.)
GEOMETRIC_REPRESENTATION_ITEM()
RATIONAL_B_SPLINE_SURFACE(((1.0005444931318,0.785835073638738,1.),(1.00047707767479,
0.812351526358848,1.),(1.0004403178859,0.826810216506254,1.),(1.00044777653322,
0.823876514387246,1.)))
REPRESENTATION_ITEM('')
SURFACE()
);
#3388=(
BOUNDED_SURFACE()
B_SPLINE_SURFACE(3,2,((#425586,#425587,#425588),(#425589,#425590,#425591),
(#425592,#425593,#425594),(#425595,#425596,#425597)),.UNSPECIFIED.,.F.,
 .F.,.F.)
B_SPLINE_SURFACE_WITH_KNOTS((4,4),(3,3),(0.,4.88747512969883E-5),(-0.000215805215016013,
1.),.UNSPECIFIED.)
GEOMETRIC_REPRESENTATION_ITEM()
RATIONAL_B_SPLINE_SURFACE(((1.00008915600319,0.793434085499842,1.),(1.00008930224972,
0.793095246303386,1.),(1.00008944684594,0.79276023072066,1.),(1.00008958984373,
0.792428918540691,1.)))
REPRESENTATION_ITEM('')
SURFACE()
);
#3389=(
BOUNDED_SURFACE()
B_SPLINE_SURFACE(3,2,((#425599,#425600,#425601),(#425602,#425603,#425604),
(#425605,#425606,#425607),(#425608,#425609,#425610),(#425611,#425612,#425613),
(#425614,#425615,#425616)),.UNSPECIFIED.,.F.,.F.,.F.)
B_SPLINE_SURFACE_WITH_KNOTS((4,2,4),(3,3),(6.7762635780344E-21,7.62675010863196E-5,
0.000152535002172639),(0.,1.02152348203057),.UNSPECIFIED.)
GEOMETRIC_REPRESENTATION_ITEM()
RATIONAL_B_SPLINE_SURFACE(((1.,0.789033595401272,1.00908146323687),(1.,
0.857071781054866,1.00615262590425),(1.,0.92208726471072,1.0033539067159),
(1.,0.922394466502399,1.00334068261142),(1.,0.857224384599056,1.00614605678497),
(1.,0.789033595401673,1.00908146323685)))
REPRESENTATION_ITEM('')
SURFACE()
);
#3390=(
BOUNDED_SURFACE()
B_SPLINE_SURFACE(3,2,((#425618,#425619,#425620),(#425621,#425622,#425623),
(#425624,#425625,#425626),(#425627,#425628,#425629)),.UNSPECIFIED.,.F.,
 .F.,.F.)
B_SPLINE_SURFACE_WITH_KNOTS((4,4),(3,3),(3.25260651745651E-19,4.88747512969882E-5),
(-0.000215489857000909,1.),.UNSPECIFIED.)
GEOMETRIC_REPRESENTATION_ITEM()
RATIONAL_B_SPLINE_SURFACE(((1.00008945889712,0.792428983985751,1.),(1.00008931610833,
0.792760296061304,1.),(1.00008917172346,0.793095311538362,1.),(1.00008902569068,
0.793434150628,1.)))
REPRESENTATION_ITEM('')
SURFACE()
);
#3391=(
BOUNDED_SURFACE()
B_SPLINE_SURFACE(3,2,((#425631,#425632,#425633),(#425634,#425635,#425636),
(#425637,#425638,#425639),(#425640,#425641,#425642)),.UNSPECIFIED.,.F.,
 .F.,.F.)
B_SPLINE_SURFACE_WITH_KNOTS((4,4),(3,3),(-5.21974905013092E-6,5.74172395514399E-5),
(-0.00139822857802174,1.00051312364098),.UNSPECIFIED.)
GEOMETRIC_REPRESENTATION_ITEM()
RATIONAL_B_SPLINE_SURFACE(((1.00049256947267,0.823768952243878,1.0001806039786),
(1.00048448215737,0.826662424388162,1.00017763870893),(1.00052427784046,
0.812424361909232,1.00019223006933),(1.00059912365883,0.785646094632575,
1.00021967280244)))
REPRESENTATION_ITEM('')
SURFACE()
);
#3392=(
BOUNDED_SURFACE()
B_SPLINE_SURFACE(3,2,((#425646,#425647,#425648),(#425649,#425650,#425651),
(#425652,#425653,#425654),(#425655,#425656,#425657)),.UNSPECIFIED.,.F.,
 .F.,.F.)
B_SPLINE_SURFACE_WITH_KNOTS((4,4),(3,3),(3.22980774337782E-5,9.63764854872257E-5),
(-0.00154325936384171,1.01095292447529),.UNSPECIFIED.)
GEOMETRIC_REPRESENTATION_ITEM()
RATIONAL_B_SPLINE_SURFACE(((1.00023530983301,0.922925743796167,1.00168574728329),
(1.00015136166127,0.950422439594215,1.00108434699058),(1.00033574337401,
0.890029368953956,1.00240524789544),(1.00054260094225,0.822274473168344,
1.00388716464853)))
REPRESENTATION_ITEM('')
SURFACE()
);
#3393=(
BOUNDED_SURFACE()
B_SPLINE_SURFACE(3,2,((#425757,#425758,#425759),(#425760,#425761,#425762),
(#425763,#425764,#425765),(#425766,#425767,#425768)),.UNSPECIFIED.,.F.,
 .F.,.F.)
B_SPLINE_SURFACE_WITH_KNOTS((4,4),(3,3),(-4.33680868994202E-19,0.000101260117256738),
(0.,1.),.UNSPECIFIED.)
GEOMETRIC_REPRESENTATION_ITEM()
RATIONAL_B_SPLINE_SURFACE(((1.,0.796615278835172,1.),(1.,0.795896038055941,
1.),(1.,0.795193354661349,1.),(1.,0.794506193185546,1.)))
REPRESENTATION_ITEM('')
SURFACE()
);
#3394=(
BOUNDED_SURFACE()
B_SPLINE_SURFACE(3,2,((#425806,#425807,#425808),(#425809,#425810,#425811),
(#425812,#425813,#425814),(#425815,#425816,#425817),(#425818,#425819,#425820),
(#425821,#425822,#425823)),.UNSPECIFIED.,.F.,.F.,.F.)
B_SPLINE_SURFACE_WITH_KNOTS((4,2,4),(3,3),(8.97854924089558E-20,1.66936432462293E-5,
3.33872864924585E-5),(0.,1.),.UNSPECIFIED.)
GEOMETRIC_REPRESENTATION_ITEM()
RATIONAL_B_SPLINE_SURFACE(((1.,0.796615278835178,1.),(1.,0.862310524418125,
1.),(1.,0.923774472010522,1.),(1.,0.923983993203424,1.),(1.,0.862574873720937,
1.),(1.,0.796615278835187,1.)))
REPRESENTATION_ITEM('')
SURFACE()
);
#3395=(
BOUNDED_SURFACE()
B_SPLINE_SURFACE(3,2,((#425860,#425861,#425862),(#425863,#425864,#425865),
(#425866,#425867,#425868),(#425869,#425870,#425871)),.UNSPECIFIED.,.F.,
 .F.,.F.)
B_SPLINE_SURFACE_WITH_KNOTS((4,4),(3,3),(-2.16840434497101E-19,0.000101244905251112),
(0.,1.),.UNSPECIFIED.)
GEOMETRIC_REPRESENTATION_ITEM()
RATIONAL_B_SPLINE_SURFACE(((1.,0.796615278835171,1.),(1.,0.795896146109793,
1.),(1.,0.795193565796497,1.),(1.,0.794506502889901,1.)))
REPRESENTATION_ITEM('')
SURFACE()
);
#3396=(
BOUNDED_SURFACE()
B_SPLINE_SURFACE(3,2,((#425907,#425908,#425909),(#425910,#425911,#425912),
(#425913,#425914,#425915),(#425916,#425917,#425918)),.UNSPECIFIED.,.F.,
 .F.,.F.)
B_SPLINE_SURFACE_WITH_KNOTS((4,4),(3,3),(2.85968127239939E-5,9.24681548475819E-5),
(-0.00167900678704925,1.01130827127826),.UNSPECIFIED.)
GEOMETRIC_REPRESENTATION_ITEM()
RATIONAL_B_SPLINE_SURFACE(((1.00059040895235,0.822187541868178,1.00401468696658),
(1.00036527718151,0.889990093671508,1.00248382673392),(1.00016469515018,
0.950399042257906,1.00111990082511),(1.00025604274,0.922888044286039,1.00174104990632)))
REPRESENTATION_ITEM('')
SURFACE()
);
#3397=(
BOUNDED_SURFACE()
B_SPLINE_SURFACE(3,2,((#425922,#425923,#425924),(#425925,#425926,#425927),
(#425928,#425929,#425930),(#425931,#425932,#425933)),.UNSPECIFIED.,.F.,
 .F.,.F.)
B_SPLINE_SURFACE_WITH_KNOTS((4,4),(3,3),(-5.22358356749291E-6,5.74594192424279E-5),
(-0.00127120052059996,1.),.UNSPECIFIED.)
GEOMETRIC_REPRESENTATION_ITEM()
RATIONAL_B_SPLINE_SURFACE(((1.00054449313177,0.785835073638752,1.),(1.00047707767476,
0.812351526358855,1.),(1.00044031788588,0.826810216506264,1.),(1.0004477765332,
0.823876514387255,1.)))
REPRESENTATION_ITEM('')
SURFACE()
);
#3398=(
BOUNDED_SURFACE()
B_SPLINE_SURFACE(3,2,((#425935,#425936,#425937),(#425938,#425939,#425940),
(#425941,#425942,#425943),(#425944,#425945,#425946)),.UNSPECIFIED.,.F.,
 .F.,.F.)
B_SPLINE_SURFACE_WITH_KNOTS((4,4),(3,3),(-2.43945488809238E-19,4.88747512969882E-5),
(-0.000215805215941335,1.),.UNSPECIFIED.)
GEOMETRIC_REPRESENTATION_ITEM()
RATIONAL_B_SPLINE_SURFACE(((1.00008915600357,0.793434085499649,1.),(1.0000893022501,
0.793095246303205,1.),(1.00008944684632,0.792760230720455,1.),(1.00008958984411,
0.792428918540498,1.)))
REPRESENTATION_ITEM('')
SURFACE()
);
#3399=(
BOUNDED_SURFACE()
B_SPLINE_SURFACE(3,2,((#425948,#425949,#425950),(#425951,#425952,#425953),
(#425954,#425955,#425956),(#425957,#425958,#425959),(#425960,#425961,#425962),
(#425963,#425964,#425965)),.UNSPECIFIED.,.F.,.F.,.F.)
B_SPLINE_SURFACE_WITH_KNOTS((4,2,4),(3,3),(1.21972744404619E-19,7.62675010863195E-5,
0.000152535002172639),(0.,1.0215234820305),.UNSPECIFIED.)
GEOMETRIC_REPRESENTATION_ITEM()
RATIONAL_B_SPLINE_SURFACE(((1.,0.789033595401289,1.00908146323684),(1.,
0.85707178105485,1.00615262590423),(1.,0.922087264710762,1.00335390671589),
(1.,0.922394466502367,1.00334068261141),(1.,0.857224384599093,1.00614605678495),
(1.,0.789033595401684,1.00908146323682)))
REPRESENTATION_ITEM('')
SURFACE()
);
#3400=(
BOUNDED_SURFACE()
B_SPLINE_SURFACE(3,2,((#425967,#425968,#425969),(#425970,#425971,#425972),
(#425973,#425974,#425975),(#425976,#425977,#425978)),.UNSPECIFIED.,.F.,
 .F.,.F.)
B_SPLINE_SURFACE_WITH_KNOTS((4,4),(3,3),(3.52365706057789E-19,4.88747512969883E-5),
(-0.000215489857896713,1.),.UNSPECIFIED.)
GEOMETRIC_REPRESENTATION_ITEM()
RATIONAL_B_SPLINE_SURFACE(((1.00008945889749,0.792428983985566,1.),(1.0000893161087,
0.792760296061123,1.),(1.00008917172383,0.793095311538183,1.),(1.00008902569106,
0.793434150627818,1.)))
REPRESENTATION_ITEM('')
SURFACE()
);
#3401=(
BOUNDED_SURFACE()
B_SPLINE_SURFACE(3,2,((#425980,#425981,#425982),(#425983,#425984,#425985),
(#425986,#425987,#425988),(#425989,#425990,#425991)),.UNSPECIFIED.,.F.,
 .F.,.F.)
B_SPLINE_SURFACE_WITH_KNOTS((4,4),(3,3),(-5.21974905012879E-6,5.7417239551441E-5),
(-0.00139822857767231,1.00051312364052),.UNSPECIFIED.)
GEOMETRIC_REPRESENTATION_ITEM()
RATIONAL_B_SPLINE_SURFACE(((1.00049256947254,0.823768952244014,1.00018060397844),
(1.00048448215725,0.826662424388313,1.00017763870877),(1.00052427784033,
0.812424361909371,1.00019223006916),(1.00059912365868,0.785646094632754,
1.00021967280225)))
REPRESENTATION_ITEM('')
SURFACE()
);
#3402=(
BOUNDED_SURFACE()
B_SPLINE_SURFACE(3,2,((#425995,#425996,#425997),(#425998,#425999,#426000),
(#426001,#426002,#426003),(#426004,#426005,#426006)),.UNSPECIFIED.,.F.,
 .F.,.F.)
B_SPLINE_SURFACE_WITH_KNOTS((4,4),(3,3),(3.22980774337777E-5,9.63764854872253E-5),
(-0.00154325936391161,1.01095292447535),.UNSPECIFIED.)
GEOMETRIC_REPRESENTATION_ITEM()
RATIONAL_B_SPLINE_SURFACE(((1.00023530983302,0.922925743796154,1.0016857472833),
(1.00015136166127,0.950422439594211,1.00108434699059),(1.00033574337402,
0.890029368953947,1.00240524789546),(1.00054260094228,0.822274473168314,
1.00388716464855)))
REPRESENTATION_ITEM('')
SURFACE()
);
#3403=(
BOUNDED_SURFACE()
B_SPLINE_SURFACE(3,2,((#426106,#426107,#426108),(#426109,#426110,#426111),
(#426112,#426113,#426114),(#426115,#426116,#426117)),.UNSPECIFIED.,.F.,
 .F.,.F.)
B_SPLINE_SURFACE_WITH_KNOTS((4,4),(3,3),(-6.50521303491303E-19,0.000101260117256738),
(0.,1.),.UNSPECIFIED.)
GEOMETRIC_REPRESENTATION_ITEM()
RATIONAL_B_SPLINE_SURFACE(((1.,0.79661527883517,1.),(1.,0.795896038055941,
1.),(1.,0.795193354661336,1.),(1.,0.794506193185542,1.)))
REPRESENTATION_ITEM('')
SURFACE()
);
#3404=(
BOUNDED_SURFACE()
B_SPLINE_SURFACE(3,2,((#426155,#426156,#426157),(#426158,#426159,#426160),
(#426161,#426162,#426163),(#426164,#426165,#426166),(#426167,#426168,#426169),
(#426170,#426171,#426172)),.UNSPECIFIED.,.F.,.F.,.F.)
B_SPLINE_SURFACE_WITH_KNOTS((4,2,4),(3,3),(3.3881317890172E-20,1.66936432462296E-5,
3.33872864924592E-5),(0.,1.),.UNSPECIFIED.)
GEOMETRIC_REPRESENTATION_ITEM()
RATIONAL_B_SPLINE_SURFACE(((1.,0.796615278835172,1.),(1.,0.862310524418128,
1.),(1.,0.923774472010521,1.),(1.,0.923983993203426,1.),(1.,0.862574873720939,
1.),(1.,0.796615278835185,1.)))
REPRESENTATION_ITEM('')
SURFACE()
);
#3405=(
BOUNDED_SURFACE()
B_SPLINE_SURFACE(3,2,((#426209,#426210,#426211),(#426212,#426213,#426214),
(#426215,#426216,#426217),(#426218,#426219,#426220)),.UNSPECIFIED.,.F.,
 .F.,.F.)
B_SPLINE_SURFACE_WITH_KNOTS((4,4),(3,3),(-2.16840434497101E-19,0.000101244905251112),
(0.,1.),.UNSPECIFIED.)
GEOMETRIC_REPRESENTATION_ITEM()
RATIONAL_B_SPLINE_SURFACE(((1.,0.796615278835169,1.),(1.,0.795896146109794,
1.),(1.,0.795193565796498,1.),(1.,0.7945065028899,1.)))
REPRESENTATION_ITEM('')
SURFACE()
);
#3406=(
BOUNDED_SURFACE()
B_SPLINE_SURFACE(3,2,((#426256,#426257,#426258),(#426259,#426260,#426261),
(#426262,#426263,#426264),(#426265,#426266,#426267)),.UNSPECIFIED.,.F.,
 .F.,.F.)
B_SPLINE_SURFACE_WITH_KNOTS((4,4),(3,3),(2.85968127239939E-5,9.24681548475814E-5),
(-0.00167900678705586,1.01130827127826),.UNSPECIFIED.)
GEOMETRIC_REPRESENTATION_ITEM()
RATIONAL_B_SPLINE_SURFACE(((1.00059040895235,0.82218754186818,1.00401468696658),
(1.00036527718151,0.889990093671503,1.00248382673392),(1.00016469515018,
0.95039904225791,1.00111990082511),(1.00025604274,0.922888044286036,1.00174104990632)))
REPRESENTATION_ITEM('')
SURFACE()
);
#3407=(
BOUNDED_SURFACE()
B_SPLINE_SURFACE(3,2,((#426271,#426272,#426273),(#426274,#426275,#426276),
(#426277,#426278,#426279),(#426280,#426281,#426282)),.UNSPECIFIED.,.F.,
 .F.,.F.)
B_SPLINE_SURFACE_WITH_KNOTS((4,4),(3,3),(-5.22358356749331E-6,5.74594192424277E-5),
(-0.00127120052057017,1.),.UNSPECIFIED.)
GEOMETRIC_REPRESENTATION_ITEM()
RATIONAL_B_SPLINE_SURFACE(((1.00054449313176,0.785835073638767,1.),(1.00047707767475,
0.812351526358833,1.),(1.00044031788587,0.826810216506293,1.),(1.00044777653319,
0.82387651438725,1.)))
REPRESENTATION_ITEM('')
SURFACE()
);
#3408=(
BOUNDED_SURFACE()
B_SPLINE_SURFACE(3,2,((#426284,#426285,#426286),(#426287,#426288,#426289),
(#426290,#426291,#426292),(#426293,#426294,#426295)),.UNSPECIFIED.,.F.,
 .F.,.F.)
B_SPLINE_SURFACE_WITH_KNOTS((4,4),(3,3),(5.42101086242752E-20,4.88747512969877E-5),
(-0.000215805215420418,1.),.UNSPECIFIED.)
GEOMETRIC_REPRESENTATION_ITEM()
RATIONAL_B_SPLINE_SURFACE(((1.00008915600335,0.793434085499756,1.),(1.00008930224989,
0.793095246303299,1.),(1.00008944684611,0.79276023072057,1.),(1.0000895898439,
0.792428918540607,1.)))
REPRESENTATION_ITEM('')
SURFACE()
);
#3409=(
BOUNDED_SURFACE()
B_SPLINE_SURFACE(3,2,((#426297,#426298,#426299),(#426300,#426301,#426302),
(#426303,#426304,#426305),(#426306,#426307,#426308),(#426309,#426310,#426311),
(#426312,#426313,#426314)),.UNSPECIFIED.,.F.,.F.,.F.)
B_SPLINE_SURFACE_WITH_KNOTS((4,2,4),(3,3),(3.52365706057789E-19,7.626750108632E-5,
0.00015253500217264),(0.,1.02152348203043),.UNSPECIFIED.)
GEOMETRIC_REPRESENTATION_ITEM()
RATIONAL_B_SPLINE_SURFACE(((1.,0.7890335954013,1.00908146323681),(1.,0.857071781054874,
1.00615262590421),(1.,0.922087264710739,1.00335390671588),(1.,0.9223944665024,
1.0033406826114),(1.,0.857224384599083,1.00614605678493),(1.,0.789033595401701,
1.00908146323679)))
REPRESENTATION_ITEM('')
SURFACE()
);
#3410=(
BOUNDED_SURFACE()
B_SPLINE_SURFACE(3,2,((#426316,#426317,#426318),(#426319,#426320,#426321),
(#426322,#426323,#426324),(#426325,#426326,#426327)),.UNSPECIFIED.,.F.,
 .F.,.F.)
B_SPLINE_SURFACE_WITH_KNOTS((4,4),(3,3),(2.16840434497101E-19,4.88747512969884E-5),
(-0.000215489857091422,1.),.UNSPECIFIED.)
GEOMETRIC_REPRESENTATION_ITEM()
RATIONAL_B_SPLINE_SURFACE(((1.00008945889715,0.792428983985732,1.),(1.00008931610837,
0.792760296061273,1.),(1.0000891717235,0.793095311538358,1.),(1.00008902569072,
0.793434150627982,1.)))
REPRESENTATION_ITEM('')
SURFACE()
);
#3411=(
BOUNDED_SURFACE()
B_SPLINE_SURFACE(3,2,((#426329,#426330,#426331),(#426332,#426333,#426334),
(#426335,#426336,#426337),(#426338,#426339,#426340)),.UNSPECIFIED.,.F.,
 .F.,.F.)
B_SPLINE_SURFACE_WITH_KNOTS((4,4),(3,3),(-5.21974905013092E-6,5.74172395514398E-5),
(-0.00139822857739479,1.00051312364055),.UNSPECIFIED.)
GEOMETRIC_REPRESENTATION_ITEM()
RATIONAL_B_SPLINE_SURFACE(((1.00049256947244,0.823768952244062,1.00018060397845),
(1.00048448215715,0.826662424388343,1.00017763870878),(1.00052427784022,
0.812424361909432,1.00019223006917),(1.00059912365856,0.785646094632801,
1.00021967280226)))
REPRESENTATION_ITEM('')
SURFACE()
);
#3412=(
BOUNDED_SURFACE()
B_SPLINE_SURFACE(3,2,((#426344,#426345,#426346),(#426347,#426348,#426349),
(#426350,#426351,#426352),(#426353,#426354,#426355)),.UNSPECIFIED.,.F.,
 .F.,.F.)
B_SPLINE_SURFACE_WITH_KNOTS((4,4),(3,3),(3.22980774337781E-5,9.63764854872261E-5),
(-0.00154325936385449,1.01095292447525),.UNSPECIFIED.)
GEOMETRIC_REPRESENTATION_ITEM()
RATIONAL_B_SPLINE_SURFACE(((1.00023530983301,0.922925743796168,1.00168574728328),
(1.00015136166127,0.950422439594217,1.00108434699058),(1.00033574337401,
0.890029368953963,1.00240524789544),(1.00054260094226,0.822274473168349,
1.00388716464852)))
REPRESENTATION_ITEM('')
SURFACE()
);
#3413=(
BOUNDED_SURFACE()
B_SPLINE_SURFACE(3,2,((#426455,#426456,#426457),(#426458,#426459,#426460),
(#426461,#426462,#426463),(#426464,#426465,#426466)),.UNSPECIFIED.,.F.,
 .F.,.F.)
B_SPLINE_SURFACE_WITH_KNOTS((4,4),(3,3),(0.,0.000101260117256737),(0.,1.),
 .UNSPECIFIED.)
GEOMETRIC_REPRESENTATION_ITEM()
RATIONAL_B_SPLINE_SURFACE(((1.,0.79661527883517,1.),(1.,0.795896038055948,
1.),(1.,0.795193354661331,1.),(1.,0.794506193185546,1.)))
REPRESENTATION_ITEM('')
SURFACE()
);
#3414=(
BOUNDED_SURFACE()
B_SPLINE_SURFACE(3,2,((#426504,#426505,#426506),(#426507,#426508,#426509),
(#426510,#426511,#426512),(#426513,#426514,#426515),(#426516,#426517,#426518),
(#426519,#426520,#426521)),.UNSPECIFIED.,.F.,.F.,.F.)
B_SPLINE_SURFACE_WITH_KNOTS((4,2,4),(3,3),(7.45388993583784E-20,1.66936432462299E-5,
3.33872864924597E-5),(0.,1.),.UNSPECIFIED.)
GEOMETRIC_REPRESENTATION_ITEM()
RATIONAL_B_SPLINE_SURFACE(((1.,0.796615278835171,1.),(1.,0.862310524418139,
1.),(1.,0.92377447201052,1.),(1.,0.923983993203424,1.),(1.,0.862574873720947,
1.),(1.,0.79661527883518,1.)))
REPRESENTATION_ITEM('')
SURFACE()
);
#3415=(
BOUNDED_SURFACE()
B_SPLINE_SURFACE(3,2,((#426558,#426559,#426560),(#426561,#426562,#426563),
(#426564,#426565,#426566),(#426567,#426568,#426569)),.UNSPECIFIED.,.F.,
 .F.,.F.)
B_SPLINE_SURFACE_WITH_KNOTS((4,4),(3,3),(0.,0.000101244905251112),(0.,1.),
 .UNSPECIFIED.)
GEOMETRIC_REPRESENTATION_ITEM()
RATIONAL_B_SPLINE_SURFACE(((1.,0.796615278835171,1.),(1.,0.795896146109789,
1.),(1.,0.795193565796504,1.),(1.,0.794506502889899,1.)))
REPRESENTATION_ITEM('')
SURFACE()
);
#3416=(
BOUNDED_SURFACE()
B_SPLINE_SURFACE(3,2,((#426605,#426606,#426607),(#426608,#426609,#426610),
(#426611,#426612,#426613),(#426614,#426615,#426616)),.UNSPECIFIED.,.F.,
 .F.,.F.)
B_SPLINE_SURFACE_WITH_KNOTS((4,4),(3,3),(2.85968127239938E-5,9.24681548475817E-5),
(-0.00167900678654135,1.01130827127837),.UNSPECIFIED.)
GEOMETRIC_REPRESENTATION_ITEM()
RATIONAL_B_SPLINE_SURFACE(((1.00059040895217,0.822187541868246,1.00401468696662),
(1.0003652771814,0.889990093671551,1.00248382673394),(1.00016469515013,
0.950399042257927,1.00111990082512),(1.00025604273992,0.922888044286068,
1.00174104990633)))
REPRESENTATION_ITEM('')
SURFACE()
);
#3417=(
BOUNDED_SURFACE()
B_SPLINE_SURFACE(3,2,((#426620,#426621,#426622),(#426623,#426624,#426625),
(#426626,#426627,#426628),(#426629,#426630,#426631)),.UNSPECIFIED.,.F.,
 .F.,.F.)
B_SPLINE_SURFACE_WITH_KNOTS((4,4),(3,3),(-5.22358356749322E-6,5.74594192424276E-5),
(-0.00127120052062939,1.),.UNSPECIFIED.)
GEOMETRIC_REPRESENTATION_ITEM()
RATIONAL_B_SPLINE_SURFACE(((1.00054449313178,0.785835073638751,1.),(1.00047707767478,
0.812351526358826,1.),(1.00044031788589,0.826810216506275,1.),(1.00044777653321,
0.823876514387242,1.)))
REPRESENTATION_ITEM('')
SURFACE()
);
#3418=(
BOUNDED_SURFACE()
B_SPLINE_SURFACE(3,2,((#426633,#426634,#426635),(#426636,#426637,#426638),
(#426639,#426640,#426641),(#426642,#426643,#426644)),.UNSPECIFIED.,.F.,
 .F.,.F.)
B_SPLINE_SURFACE_WITH_KNOTS((4,4),(3,3),(-8.13151629364128E-20,4.8874751296988E-5),
(-0.000215805215034299,1.),.UNSPECIFIED.)
GEOMETRIC_REPRESENTATION_ITEM()
RATIONAL_B_SPLINE_SURFACE(((1.0000891560032,0.793434085499832,1.),(1.00008930224973,
0.793095246303387,1.),(1.00008944684595,0.79276023072065,1.),(1.00008958984374,
0.792428918540687,1.)))
REPRESENTATION_ITEM('')
SURFACE()
);
#3419=(
BOUNDED_SURFACE()
B_SPLINE_SURFACE(3,2,((#426646,#426647,#426648),(#426649,#426650,#426651),
(#426652,#426653,#426654),(#426655,#426656,#426657),(#426658,#426659,#426660),
(#426661,#426662,#426663)),.UNSPECIFIED.,.F.,.F.,.F.)
B_SPLINE_SURFACE_WITH_KNOTS((4,2,4),(3,3),(-2.03287907341032E-20,7.62675010863199E-5,
0.00015253500217264),(0.,1.02152348203051),.UNSPECIFIED.)
GEOMETRIC_REPRESENTATION_ITEM()
RATIONAL_B_SPLINE_SURFACE(((1.,0.789033595401288,1.00908146323684),(1.,
0.857071781054841,1.00615262590424),(1.,0.922087264710766,1.00335390671589),
(1.,0.922394466502363,1.00334068261141),(1.,0.857224384599088,1.00614605678495),
(1.,0.789033595401688,1.00908146323683)))
REPRESENTATION_ITEM('')
SURFACE()
);
#3420=(
BOUNDED_SURFACE()
B_SPLINE_SURFACE(3,2,((#426665,#426666,#426667),(#426668,#426669,#426670),
(#426671,#426672,#426673),(#426674,#426675,#426676)),.UNSPECIFIED.,.F.,
 .F.,.F.)
B_SPLINE_SURFACE_WITH_KNOTS((4,4),(3,3),(1.0842021724855E-19,4.88747512969883E-5),
(-0.000215489856815771,1.),.UNSPECIFIED.)
GEOMETRIC_REPRESENTATION_ITEM()
RATIONAL_B_SPLINE_SURFACE(((1.00008945889704,0.79242898398579,1.),(1.00008931610826,
0.792760296061347,1.),(1.00008917172338,0.793095311538396,1.),(1.00008902569061,
0.793434150628043,1.)))
REPRESENTATION_ITEM('')
SURFACE()
);
#3421=(
BOUNDED_SURFACE()
B_SPLINE_SURFACE(3,2,((#426678,#426679,#426680),(#426681,#426682,#426683),
(#426684,#426685,#426686),(#426687,#426688,#426689)),.UNSPECIFIED.,.F.,
 .F.,.F.)
B_SPLINE_SURFACE_WITH_KNOTS((4,4),(3,3),(-5.21974905012873E-6,5.74172395514394E-5),
(-0.00139822857773652,1.00051312364074),.UNSPECIFIED.)
GEOMETRIC_REPRESENTATION_ITEM()
RATIONAL_B_SPLINE_SURFACE(((1.00049256947257,0.82376895224397,1.00018060397852),
(1.00048448215727,0.826662424388236,1.00017763870885),(1.00052427784035,
0.812424361909349,1.00019223006924),(1.00059912365871,0.785646094632682,
1.00021967280234)))
REPRESENTATION_ITEM('')
SURFACE()
);
#3422=(
BOUNDED_SURFACE()
B_SPLINE_SURFACE(3,2,((#426693,#426694,#426695),(#426696,#426697,#426698),
(#426699,#426700,#426701),(#426702,#426703,#426704)),.UNSPECIFIED.,.F.,
 .F.,.F.)
B_SPLINE_SURFACE_WITH_KNOTS((4,4),(3,3),(3.22980774337783E-5,9.63764854872258E-5),
(-0.00154325936400768,1.01095292447557),.UNSPECIFIED.)
GEOMETRIC_REPRESENTATION_ITEM()
RATIONAL_B_SPLINE_SURFACE(((1.00023530983303,0.92292574379613,1.00168574728333),
(1.00015136166128,0.950422439594196,1.00108434699061),(1.00033574337404,
0.89002936895391,1.00240524789551),(1.00054260094231,0.82227447316826,1.00388716464863)))
REPRESENTATION_ITEM('')
SURFACE()
);
#3423=(
BOUNDED_SURFACE()
B_SPLINE_SURFACE(3,2,((#426804,#426805,#426806),(#426807,#426808,#426809),
(#426810,#426811,#426812),(#426813,#426814,#426815)),.UNSPECIFIED.,.F.,
 .F.,.F.)
B_SPLINE_SURFACE_WITH_KNOTS((4,4),(3,3),(0.,0.000101260117256738),(0.,1.),
 .UNSPECIFIED.)
GEOMETRIC_REPRESENTATION_ITEM()
RATIONAL_B_SPLINE_SURFACE(((1.,0.796615278835172,1.),(1.,0.795896038055938,
1.),(1.,0.795193354661348,1.),(1.,0.794506193185546,1.)))
REPRESENTATION_ITEM('')
SURFACE()
);
#3424=(
BOUNDED_SURFACE()
B_SPLINE_SURFACE(3,2,((#426853,#426854,#426855),(#426856,#426857,#426858),
(#426859,#426860,#426861),(#426862,#426863,#426864),(#426865,#426866,#426867),
(#426868,#426869,#426870)),.UNSPECIFIED.,.F.,.F.,.F.)
B_SPLINE_SURFACE_WITH_KNOTS((4,2,4),(3,3),(-1.94817577868489E-19,1.66936432462298E-5,
3.33872864924599E-5),(0.,1.),.UNSPECIFIED.)
GEOMETRIC_REPRESENTATION_ITEM()
RATIONAL_B_SPLINE_SURFACE(((1.,0.796615278835165,1.),(1.,0.862310524418136,
1.),(1.,0.923774472010517,1.),(1.,0.923983993203428,1.),(1.,0.862574873720953,
1.),(1.,0.796615278835182,1.)))
REPRESENTATION_ITEM('')
SURFACE()
);
#3425=(
BOUNDED_SURFACE()
B_SPLINE_SURFACE(3,2,((#426907,#426908,#426909),(#426910,#426911,#426912),
(#426913,#426914,#426915),(#426916,#426917,#426918)),.UNSPECIFIED.,.F.,
 .F.,.F.)
B_SPLINE_SURFACE_WITH_KNOTS((4,4),(3,3),(2.16840434497101E-19,0.000101244905251112),
(0.,1.),.UNSPECIFIED.)
GEOMETRIC_REPRESENTATION_ITEM()
RATIONAL_B_SPLINE_SURFACE(((1.,0.796615278835168,1.),(1.,0.795896146109795,
1.),(1.,0.795193565796498,1.),(1.,0.794506502889901,1.)))
REPRESENTATION_ITEM('')
SURFACE()
);
#3426=(
BOUNDED_SURFACE()
B_SPLINE_SURFACE(3,2,((#426954,#426955,#426956),(#426957,#426958,#426959),
(#426960,#426961,#426962),(#426963,#426964,#426965)),.UNSPECIFIED.,.F.,
 .F.,.F.)
B_SPLINE_SURFACE_WITH_KNOTS((4,4),(3,3),(2.85968127239939E-5,9.24681548475819E-5),
(-0.001679006786515,1.01130827127844),.UNSPECIFIED.)
GEOMETRIC_REPRESENTATION_ITEM()
RATIONAL_B_SPLINE_SURFACE(((1.00059040895216,0.822187541868239,1.00401468696665),
(1.00036527718139,0.889990093671552,1.00248382673396),(1.00016469515013,
0.950399042257921,1.00111990082513),(1.00025604273992,0.922888044286066,
1.00174104990634)))
REPRESENTATION_ITEM('')
SURFACE()
);
#3427=(
BOUNDED_SURFACE()
B_SPLINE_SURFACE(3,2,((#426969,#426970,#426971),(#426972,#426973,#426974),
(#426975,#426976,#426977),(#426978,#426979,#426980)),.UNSPECIFIED.,.F.,
 .F.,.F.)
B_SPLINE_SURFACE_WITH_KNOTS((4,4),(3,3),(-5.22358356749305E-6,5.74594192424275E-5),
(-0.0012712005206506,1.),.UNSPECIFIED.)
GEOMETRIC_REPRESENTATION_ITEM()
RATIONAL_B_SPLINE_SURFACE(((1.00054449313179,0.78583507363875,1.),(1.00047707767478,
0.812351526358819,1.),(1.0004403178859,0.826810216506276,1.),(1.00044777653322,
0.823876514387236,1.)))
REPRESENTATION_ITEM('')
SURFACE()
);
#3428=(
BOUNDED_SURFACE()
B_SPLINE_SURFACE(3,2,((#426982,#426983,#426984),(#426985,#426986,#426987),
(#426988,#426989,#426990),(#426991,#426992,#426993)),.UNSPECIFIED.,.F.,
 .F.,.F.)
B_SPLINE_SURFACE_WITH_KNOTS((4,4),(3,3),(2.71050543121376E-20,4.8874751296988E-5),
(-0.000215805214801446,1.),.UNSPECIFIED.)
GEOMETRIC_REPRESENTATION_ITEM()
RATIONAL_B_SPLINE_SURFACE(((1.0000891560031,0.793434085499885,1.),(1.00008930224963,
0.793095246303421,1.),(1.00008944684585,0.792760230720706,1.),(1.00008958984364,
0.792428918540732,1.)))
REPRESENTATION_ITEM('')
SURFACE()
);
#3429=(
BOUNDED_SURFACE()
B_SPLINE_SURFACE(3,2,((#426995,#426996,#426997),(#426998,#426999,#427000),
(#427001,#427002,#427003),(#427004,#427005,#427006),(#427007,#427008,#427009),
(#427010,#427011,#427012)),.UNSPECIFIED.,.F.,.F.,.F.)
B_SPLINE_SURFACE_WITH_KNOTS((4,2,4),(3,3),(1.55854062294791E-19,7.62675010863199E-5,
0.00015253500217264),(0.,1.02152348203048),.UNSPECIFIED.)
GEOMETRIC_REPRESENTATION_ITEM()
RATIONAL_B_SPLINE_SURFACE(((1.,0.789033595401297,1.00908146323683),(1.,
0.857071781054868,1.00615262590423),(1.,0.92208726471074,1.00335390671589),
(1.,0.922394466502395,1.0033406826114),(1.,0.857224384599078,1.00614605678494),
(1.,0.789033595401691,1.00908146323681)))
REPRESENTATION_ITEM('')
SURFACE()
);
#3430=(
BOUNDED_SURFACE()
B_SPLINE_SURFACE(3,2,((#427014,#427015,#427016),(#427017,#427018,#427019),
(#427020,#427021,#427022),(#427023,#427024,#427025)),.UNSPECIFIED.,.F.,
 .F.,.F.)
B_SPLINE_SURFACE_WITH_KNOTS((4,4),(3,3),(2.43945488809238E-19,4.88747512969886E-5),
(-0.000215489856871912,1.),.UNSPECIFIED.)
GEOMETRIC_REPRESENTATION_ITEM()
RATIONAL_B_SPLINE_SURFACE(((1.00008945889706,0.792428983985778,1.),(1.00008931610828,
0.792760296061328,1.),(1.00008917172341,0.793095311538385,1.),(1.00008902569063,
0.793434150628033,1.)))
REPRESENTATION_ITEM('')
SURFACE()
);
#3431=(
BOUNDED_SURFACE()
B_SPLINE_SURFACE(3,2,((#427027,#427028,#427029),(#427030,#427031,#427032),
(#427033,#427034,#427035),(#427036,#427037,#427038)),.UNSPECIFIED.,.F.,
 .F.,.F.)
B_SPLINE_SURFACE_WITH_KNOTS((4,4),(3,3),(-5.21974905013083E-6,5.74172395514396E-5),
(-0.00139822857794668,1.00051312364089),.UNSPECIFIED.)
GEOMETRIC_REPRESENTATION_ITEM()
RATIONAL_B_SPLINE_SURFACE(((1.00049256947264,0.823768952243904,1.00018060397857),
(1.00048448215734,0.826662424388192,1.0001776387089),(1.00052427784043,
0.812424361909265,1.00019223006929),(1.0005991236588,0.785646094632611,
1.0002196728024)))
REPRESENTATION_ITEM('')
SURFACE()
);
#3432=(
BOUNDED_SURFACE()
B_SPLINE_SURFACE(3,2,((#427042,#427043,#427044),(#427045,#427046,#427047),
(#427048,#427049,#427050),(#427051,#427052,#427053)),.UNSPECIFIED.,.F.,
 .F.,.F.)
B_SPLINE_SURFACE_WITH_KNOTS((4,4),(3,3),(3.22980774337778E-5,9.63764854872253E-5),
(-0.00154325936338914,1.01095292447536),.UNSPECIFIED.)
GEOMETRIC_REPRESENTATION_ITEM()
RATIONAL_B_SPLINE_SURFACE(((1.00023530983294,0.922925743796197,1.0016857472833),
(1.00015136166122,0.950422439594232,1.00108434699059),(1.00033574337391,
0.890029368954006,1.00240524789546),(1.00054260094209,0.822274473168407,
1.00388716464856)))
REPRESENTATION_ITEM('')
SURFACE()
);
#3433=(
BOUNDED_SURFACE()
B_SPLINE_SURFACE(3,2,((#427153,#427154,#427155),(#427156,#427157,#427158),
(#427159,#427160,#427161),(#427162,#427163,#427164)),.UNSPECIFIED.,.F.,
 .F.,.F.)
B_SPLINE_SURFACE_WITH_KNOTS((4,4),(3,3),(0.,0.000101260117256736),(0.,1.),
 .UNSPECIFIED.)
GEOMETRIC_REPRESENTATION_ITEM()
RATIONAL_B_SPLINE_SURFACE(((1.,0.796615278835173,1.),(1.,0.79589603805594,
1.),(1.,0.795193354661355,1.),(1.,0.794506193185536,1.)))
REPRESENTATION_ITEM('')
SURFACE()
);
#3434=(
BOUNDED_SURFACE()
B_SPLINE_SURFACE(3,2,((#427202,#427203,#427204),(#427205,#427206,#427207),
(#427208,#427209,#427210),(#427211,#427212,#427213),(#427214,#427215,#427216),
(#427217,#427218,#427219)),.UNSPECIFIED.,.F.,.F.,.F.)
B_SPLINE_SURFACE_WITH_KNOTS((4,2,4),(3,3),(-2.64274279543342E-19,1.66936432462293E-5,
3.33872864924589E-5),(0.,1.),.UNSPECIFIED.)
GEOMETRIC_REPRESENTATION_ITEM()
RATIONAL_B_SPLINE_SURFACE(((1.,0.79661527883517,1.),(1.,0.862310524418132,
1.),(1.,0.923774472010528,1.),(1.,0.923983993203422,1.),(1.,0.86257487372095,
1.),(1.,0.79661527883518,1.)))
REPRESENTATION_ITEM('')
SURFACE()
);
#3435=(
BOUNDED_SURFACE()
B_SPLINE_SURFACE(3,2,((#427256,#427257,#427258),(#427259,#427260,#427261),
(#427262,#427263,#427264),(#427265,#427266,#427267)),.UNSPECIFIED.,.F.,
 .F.,.F.)
B_SPLINE_SURFACE_WITH_KNOTS((4,4),(3,3),(0.,0.000101244905251112),(0.,1.),
 .UNSPECIFIED.)
GEOMETRIC_REPRESENTATION_ITEM()
RATIONAL_B_SPLINE_SURFACE(((1.,0.796615278835166,1.),(1.,0.795896146109796,
1.),(1.,0.795193565796497,1.),(1.,0.794506502889899,1.)))
REPRESENTATION_ITEM('')
SURFACE()
);
#3436=(
BOUNDED_SURFACE()
B_SPLINE_SURFACE(3,2,((#427303,#427304,#427305),(#427306,#427307,#427308),
(#427309,#427310,#427311),(#427312,#427313,#427314)),.UNSPECIFIED.,.F.,
 .F.,.F.)
B_SPLINE_SURFACE_WITH_KNOTS((4,4),(3,3),(2.85968127239939E-5,9.24681548475817E-5),
(-0.00167900678734404,1.01130827127821),.UNSPECIFIED.)
GEOMETRIC_REPRESENTATION_ITEM()
RATIONAL_B_SPLINE_SURFACE(((1.00059040895245,0.822187541868132,1.00401468696656),
(1.00036527718157,0.88999009367148,1.00248382673391),(1.00016469515021,
0.950399042257889,1.00111990082511),(1.00025604274005,0.922888044286016,
1.00174104990631)))
REPRESENTATION_ITEM('')
SURFACE()
);
#3437=(
BOUNDED_SURFACE()
B_SPLINE_SURFACE(3,2,((#427318,#427319,#427320),(#427321,#427322,#427323),
(#427324,#427325,#427326),(#427327,#427328,#427329)),.UNSPECIFIED.,.F.,
 .F.,.F.)
B_SPLINE_SURFACE_WITH_KNOTS((4,4),(3,3),(-5.22358356749204E-6,5.74594192424279E-5),
(-0.00127120052055143,1.),.UNSPECIFIED.)
GEOMETRIC_REPRESENTATION_ITEM()
RATIONAL_B_SPLINE_SURFACE(((1.00054449313175,0.785835073638762,1.),(1.00047707767475,
0.812351526358862,1.),(1.00044031788586,0.826810216506277,1.),(1.00044777653318,
0.823876514387263,1.)))
REPRESENTATION_ITEM('')
SURFACE()
);
#3438=(
BOUNDED_SURFACE()
B_SPLINE_SURFACE(3,2,((#427331,#427332,#427333),(#427334,#427335,#427336),
(#427337,#427338,#427339),(#427340,#427341,#427342)),.UNSPECIFIED.,.F.,
 .F.,.F.)
B_SPLINE_SURFACE_WITH_KNOTS((4,4),(3,3),(0.,4.88747512969878E-5),(-0.000215805215227164,
1.),.UNSPECIFIED.)
GEOMETRIC_REPRESENTATION_ITEM()
RATIONAL_B_SPLINE_SURFACE(((1.00008915600327,0.793434085499794,1.),(1.00008930224981,
0.793095246303354,1.),(1.00008944684603,0.792760230720619,1.),(1.00008958984382,
0.792428918540648,1.)))
REPRESENTATION_ITEM('')
SURFACE()
);
#3439=(
BOUNDED_SURFACE()
B_SPLINE_SURFACE(3,2,((#427344,#427345,#427346),(#427347,#427348,#427349),
(#427350,#427351,#427352),(#427353,#427354,#427355),(#427356,#427357,#427358),
(#427359,#427360,#427361)),.UNSPECIFIED.,.F.,.F.,.F.)
B_SPLINE_SURFACE_WITH_KNOTS((4,2,4),(3,3),(2.98155597433514E-19,7.62675010863198E-5,
0.000152535002172639),(0.,1.02152348203069),.UNSPECIFIED.)
GEOMETRIC_REPRESENTATION_ITEM()
RATIONAL_B_SPLINE_SURFACE(((1.,0.789033595401248,1.00908146323692),(1.,
0.857071781054857,1.00615262590429),(1.,0.922087264710701,1.00335390671592),
(1.,0.9223944665024,1.00334068261144),(1.,0.857224384599027,1.00614605678501),
(1.,0.789033595401649,1.0090814632369)))
REPRESENTATION_ITEM('')
SURFACE()
);
#3440=(
BOUNDED_SURFACE()
B_SPLINE_SURFACE(3,2,((#427363,#427364,#427365),(#427366,#427367,#427368),
(#427369,#427370,#427371),(#427372,#427373,#427374)),.UNSPECIFIED.,.F.,
 .F.,.F.)
B_SPLINE_SURFACE_WITH_KNOTS((4,4),(3,3),(6.50521303491303E-19,4.88747512969885E-5),
(-0.000215489857079631,1.),.UNSPECIFIED.)
GEOMETRIC_REPRESENTATION_ITEM()
RATIONAL_B_SPLINE_SURFACE(((1.00008945889715,0.792428983985734,1.),(1.00008931610837,
0.79276029606128,1.),(1.00008917172349,0.793095311538358,1.),(1.00008902569072,
0.793434150627986,1.)))
REPRESENTATION_ITEM('')
SURFACE()
);
#3441=(
BOUNDED_SURFACE()
B_SPLINE_SURFACE(3,2,((#427376,#427377,#427378),(#427379,#427380,#427381),
(#427382,#427383,#427384),(#427385,#427386,#427387)),.UNSPECIFIED.,.F.,
 .F.,.F.)
B_SPLINE_SURFACE_WITH_KNOTS((4,4),(3,3),(-5.21974905013096E-6,5.74172395514397E-5),
(-0.00139822857719932,1.00051312364059),.UNSPECIFIED.)
GEOMETRIC_REPRESENTATION_ITEM()
RATIONAL_B_SPLINE_SURFACE(((1.00049256947238,0.823768952244082,1.00018060397847),
(1.00048448215708,0.826662424388392,1.00017763870879),(1.00052427784015,
0.812424361909437,1.00019223006918),(1.00059912365847,0.78564609463284,
1.00021967280228)))
REPRESENTATION_ITEM('')
SURFACE()
);
#3442=(
BOUNDED_SURFACE()
B_SPLINE_SURFACE(3,2,((#427391,#427392,#427393),(#427394,#427395,#427396),
(#427397,#427398,#427399),(#427400,#427401,#427402)),.UNSPECIFIED.,.F.,
 .F.,.F.)
B_SPLINE_SURFACE_WITH_KNOTS((4,4),(3,3),(3.22980774337779E-5,9.63764854872255E-5),
(-0.00154325936518139,1.01095292447533),.UNSPECIFIED.)
GEOMETRIC_REPRESENTATION_ITEM()
RATIONAL_B_SPLINE_SURFACE(((1.00023530983321,0.922925743796062,1.00168574728329),
(1.0001513616614,0.95042243959415,1.00108434699059),(1.0003357433743,0.890029368953806,
1.00240524789545),(1.00054260094272,0.82227447316809,1.00388716464854)))
REPRESENTATION_ITEM('')
SURFACE()
);
#3443=(
BOUNDED_SURFACE()
B_SPLINE_SURFACE(3,2,((#427502,#427503,#427504),(#427505,#427506,#427507),
(#427508,#427509,#427510),(#427511,#427512,#427513)),.UNSPECIFIED.,.F.,
 .F.,.F.)
B_SPLINE_SURFACE_WITH_KNOTS((4,4),(3,3),(0.,0.000101260117256737),(0.,1.),
 .UNSPECIFIED.)
GEOMETRIC_REPRESENTATION_ITEM()
RATIONAL_B_SPLINE_SURFACE(((1.,0.79661527883517,1.),(1.,0.795896038055935,
1.),(1.,0.79519335466135,1.),(1.,0.794506193185543,1.)))
REPRESENTATION_ITEM('')
SURFACE()
);
#3444=(
BOUNDED_SURFACE()
B_SPLINE_SURFACE(3,2,((#427551,#427552,#427553),(#427554,#427555,#427556),
(#427557,#427558,#427559),(#427560,#427561,#427562),(#427563,#427564,#427565),
(#427566,#427567,#427568)),.UNSPECIFIED.,.F.,.F.,.F.)
B_SPLINE_SURFACE_WITH_KNOTS((4,2,4),(3,3),(-2.04981973235541E-19,1.66936432462293E-5,
3.33872864924587E-5),(0.,1.),.UNSPECIFIED.)
GEOMETRIC_REPRESENTATION_ITEM()
RATIONAL_B_SPLINE_SURFACE(((1.,0.796615278835175,1.),(1.,0.862310524418114,
1.),(1.,0.923774472010523,1.),(1.,0.923983993203425,1.),(1.,0.862574873720955,
1.),(1.,0.796615278835174,1.)))
REPRESENTATION_ITEM('')
SURFACE()
);
#3445=(
BOUNDED_SURFACE()
B_SPLINE_SURFACE(3,2,((#427605,#427606,#427607),(#427608,#427609,#427610),
(#427611,#427612,#427613),(#427614,#427615,#427616)),.UNSPECIFIED.,.F.,
 .F.,.F.)
B_SPLINE_SURFACE_WITH_KNOTS((4,4),(3,3),(0.,0.000101244905251112),(0.,1.),
 .UNSPECIFIED.)
GEOMETRIC_REPRESENTATION_ITEM()
RATIONAL_B_SPLINE_SURFACE(((1.,0.796615278835171,1.),(1.,0.795896146109795,
1.),(1.,0.795193565796493,1.),(1.,0.794506502889901,1.)))
REPRESENTATION_ITEM('')
SURFACE()
);
#3446=(
BOUNDED_SURFACE()
B_SPLINE_SURFACE(3,2,((#427652,#427653,#427654),(#427655,#427656,#427657),
(#427658,#427659,#427660),(#427661,#427662,#427663)),.UNSPECIFIED.,.F.,
 .F.,.F.)
B_SPLINE_SURFACE_WITH_KNOTS((4,4),(3,3),(2.85968127239939E-5,9.24681548475816E-5),
(-0.00167900678644083,1.01130827127813),.UNSPECIFIED.)
GEOMETRIC_REPRESENTATION_ITEM()
RATIONAL_B_SPLINE_SURFACE(((1.00059040895213,0.822187541868308,1.00401468696653),
(1.00036527718137,0.889990093671593,1.00248382673389),(1.00016469515012,
0.95039904225794,1.0011199008251),(1.00025604273991,0.922888044286096,1.0017410499063)))
REPRESENTATION_ITEM('')
SURFACE()
);
#3447=(
BOUNDED_SURFACE()
B_SPLINE_SURFACE(3,2,((#427667,#427668,#427669),(#427670,#427671,#427672),
(#427673,#427674,#427675),(#427676,#427677,#427678)),.UNSPECIFIED.,.F.,
 .F.,.F.)
B_SPLINE_SURFACE_WITH_KNOTS((4,4),(3,3),(-5.22358356749292E-6,5.74594192424277E-5),
(-0.00127120052058111,1.),.UNSPECIFIED.)
GEOMETRIC_REPRESENTATION_ITEM()
RATIONAL_B_SPLINE_SURFACE(((1.00054449313176,0.785835073638756,1.),(1.00047707767476,
0.812351526358861,1.),(1.00044031788587,0.826810216506268,1.),(1.00044777653319,
0.823876514387252,1.)))
REPRESENTATION_ITEM('')
SURFACE()
);
#3448=(
BOUNDED_SURFACE()
B_SPLINE_SURFACE(3,2,((#427680,#427681,#427682),(#427683,#427684,#427685),
(#427686,#427687,#427688),(#427689,#427690,#427691)),.UNSPECIFIED.,.F.,
 .F.,.F.)
B_SPLINE_SURFACE_WITH_KNOTS((4,4),(3,3),(-2.71050543121376E-20,4.88747512969881E-5),
(-0.0002158052151809,1.),.UNSPECIFIED.)
GEOMETRIC_REPRESENTATION_ITEM()
RATIONAL_B_SPLINE_SURFACE(((1.00008915600326,0.793434085499806,1.),(1.00008930224979,
0.793095246303342,1.),(1.00008944684601,0.792760230720625,1.),(1.0000895898438,
0.792428918540654,1.)))
REPRESENTATION_ITEM('')
SURFACE()
);
#3449=(
BOUNDED_SURFACE()
B_SPLINE_SURFACE(3,2,((#427693,#427694,#427695),(#427696,#427697,#427698),
(#427699,#427700,#427701),(#427702,#427703,#427704),(#427705,#427706,#427707),
(#427708,#427709,#427710)),.UNSPECIFIED.,.F.,.F.,.F.)
B_SPLINE_SURFACE_WITH_KNOTS((4,2,4),(3,3),(-9.48676900924816E-20,7.62675010863194E-5,
0.000152535002172639),(0.,1.02152348203078),.UNSPECIFIED.)
GEOMETRIC_REPRESENTATION_ITEM()
RATIONAL_B_SPLINE_SURFACE(((1.,0.789033595401232,1.00908146323696),(1.,
0.857071781054828,1.00615262590431),(1.,0.922087264710711,1.00335390671594),
(1.,0.922394466502375,1.00334068261145),(1.,0.857224384599031,1.00614605678503),
(1.,0.789033595401628,1.00908146323694)))
REPRESENTATION_ITEM('')
SURFACE()
);
#3450=(
BOUNDED_SURFACE()
B_SPLINE_SURFACE(3,2,((#427712,#427713,#427714),(#427715,#427716,#427717),
(#427718,#427719,#427720),(#427721,#427722,#427723)),.UNSPECIFIED.,.F.,
 .F.,.F.)
B_SPLINE_SURFACE_WITH_KNOTS((4,4),(3,3),(2.71050543121376E-19,4.88747512969886E-5),
(-0.000215489857605897,1.),.UNSPECIFIED.)
GEOMETRIC_REPRESENTATION_ITEM()
RATIONAL_B_SPLINE_SURFACE(((1.00008945889737,0.792428983985626,1.),(1.00008931610858,
0.792760296061186,1.),(1.00008917172371,0.79309531153825,1.),(1.00008902569093,
0.793434150627878,1.)))
REPRESENTATION_ITEM('')
SURFACE()
);
#3451=(
BOUNDED_SURFACE()
B_SPLINE_SURFACE(3,2,((#427725,#427726,#427727),(#427728,#427729,#427730),
(#427731,#427732,#427733),(#427734,#427735,#427736)),.UNSPECIFIED.,.F.,
 .F.,.F.)
B_SPLINE_SURFACE_WITH_KNOTS((4,4),(3,3),(-5.21974905013089E-6,5.74172395514395E-5),
(-0.00139822857804183,1.0005131236408),.UNSPECIFIED.)
GEOMETRIC_REPRESENTATION_ITEM()
RATIONAL_B_SPLINE_SURFACE(((1.00049256947267,0.823768952243908,1.00018060397854),
(1.00048448215738,0.826662424388174,1.00017763870887),(1.00052427784047,
0.812424361909285,1.00019223006926),(1.00059912365884,0.785646094632604,
1.00021967280237)))
REPRESENTATION_ITEM('')
SURFACE()
);
#3452=(
BOUNDED_SURFACE()
B_SPLINE_SURFACE(3,2,((#427740,#427741,#427742),(#427743,#427744,#427745),
(#427746,#427747,#427748),(#427749,#427750,#427751)),.UNSPECIFIED.,.F.,
 .F.,.F.)
B_SPLINE_SURFACE_WITH_KNOTS((4,4),(3,3),(3.22980774337779E-5,9.6376485487225E-5),
(-0.00154325936517141,1.01095292447531),.UNSPECIFIED.)
GEOMETRIC_REPRESENTATION_ITEM()
RATIONAL_B_SPLINE_SURFACE(((1.00023530983321,0.922925743796063,1.00168574728329),
(1.0001513616614,0.950422439594155,1.00108434699058),(1.0003357433743,0.890029368953809,
1.00240524789545),(1.00054260094272,0.822274473168098,1.00388716464854)))
REPRESENTATION_ITEM('')
SURFACE()
);
#3453=(
BOUNDED_SURFACE()
B_SPLINE_SURFACE(3,2,((#427851,#427852,#427853),(#427854,#427855,#427856),
(#427857,#427858,#427859),(#427860,#427861,#427862)),.UNSPECIFIED.,.F.,
 .F.,.F.)
B_SPLINE_SURFACE_WITH_KNOTS((4,4),(3,3),(2.16840434497101E-19,0.000101260117256738),
(0.,1.),.UNSPECIFIED.)
GEOMETRIC_REPRESENTATION_ITEM()
RATIONAL_B_SPLINE_SURFACE(((1.,0.796615278835173,1.),(1.,0.795896038055939,
1.),(1.,0.795193354661347,1.),(1.,0.794506193185548,1.)))
REPRESENTATION_ITEM('')
SURFACE()
);
#3454=(
BOUNDED_SURFACE()
B_SPLINE_SURFACE(3,2,((#427900,#427901,#427902),(#427903,#427904,#427905),
(#427906,#427907,#427908),(#427909,#427910,#427911),(#427912,#427913,#427914),
(#427915,#427916,#427917)),.UNSPECIFIED.,.F.,.F.,.F.)
B_SPLINE_SURFACE_WITH_KNOTS((4,2,4),(3,3),(-1.01643953670516E-19,1.66936432462293E-5,
3.33872864924587E-5),(0.,1.),.UNSPECIFIED.)
GEOMETRIC_REPRESENTATION_ITEM()
RATIONAL_B_SPLINE_SURFACE(((1.,0.796615278835177,1.),(1.,0.86231052441812,
1.),(1.,0.923774472010522,1.),(1.,0.923983993203425,1.),(1.,0.862574873720947,
1.),(1.,0.796615278835186,1.)))
REPRESENTATION_ITEM('')
SURFACE()
);
#3455=(
BOUNDED_SURFACE()
B_SPLINE_SURFACE(3,2,((#427954,#427955,#427956),(#427957,#427958,#427959),
(#427960,#427961,#427962),(#427963,#427964,#427965)),.UNSPECIFIED.,.F.,
 .F.,.F.)
B_SPLINE_SURFACE_WITH_KNOTS((4,4),(3,3),(0.,0.000101244905251112),(0.,1.),
 .UNSPECIFIED.)
GEOMETRIC_REPRESENTATION_ITEM()
RATIONAL_B_SPLINE_SURFACE(((1.,0.796615278835172,1.),(1.,0.795896146109793,
1.),(1.,0.795193565796498,1.),(1.,0.794506502889903,1.)))
REPRESENTATION_ITEM('')
SURFACE()
);
#3456=(
BOUNDED_SURFACE()
B_SPLINE_SURFACE(3,2,((#428001,#428002,#428003),(#428004,#428005,#428006),
(#428007,#428008,#428009),(#428010,#428011,#428012)),.UNSPECIFIED.,.F.,
 .F.,.F.)
B_SPLINE_SURFACE_WITH_KNOTS((4,4),(3,3),(2.85968127239939E-5,9.24681548475816E-5),
(-0.00167900679344736,1.0113082712782),.UNSPECIFIED.)
GEOMETRIC_REPRESENTATION_ITEM()
RATIONAL_B_SPLINE_SURFACE(((1.0005904089546,0.822187541867035,1.00401468696656),
(1.0003652771829,0.88999009367081,1.00248382673391),(1.00016469515081,0.950399042257587,
1.00111990082511),(1.00025604274098,0.922888044285544,1.00174104990631)))
REPRESENTATION_ITEM('')
SURFACE()
);
#3457=(
BOUNDED_SURFACE()
B_SPLINE_SURFACE(3,2,((#428016,#428017,#428018),(#428019,#428020,#428021),
(#428022,#428023,#428024),(#428025,#428026,#428027)),.UNSPECIFIED.,.F.,
 .F.,.F.)
B_SPLINE_SURFACE_WITH_KNOTS((4,4),(3,3),(-5.22358356749297E-6,5.7459419242428E-5),
(-0.00127120052059476,1.),.UNSPECIFIED.)
GEOMETRIC_REPRESENTATION_ITEM()
RATIONAL_B_SPLINE_SURFACE(((1.00054449313177,0.78583507363875,1.),(1.00047707767476,
0.812351526358855,1.),(1.00044031788588,0.826810216506272,1.),(1.0004477765332,
0.823876514387251,1.)))
REPRESENTATION_ITEM('')
SURFACE()
);
#3458=(
BOUNDED_SURFACE()
B_SPLINE_SURFACE(3,2,((#428029,#428030,#428031),(#428032,#428033,#428034),
(#428035,#428036,#428037),(#428038,#428039,#428040)),.UNSPECIFIED.,.F.,
 .F.,.F.)
B_SPLINE_SURFACE_WITH_KNOTS((4,4),(3,3),(-3.25260651745651E-19,4.88747512969879E-5),
(-0.00021580521588161,1.),.UNSPECIFIED.)
GEOMETRIC_REPRESENTATION_ITEM()
RATIONAL_B_SPLINE_SURFACE(((1.00008915600355,0.793434085499665,1.),(1.00008930225008,
0.793095246303214,1.),(1.0000894468463,0.792760230720471,1.),(1.00008958984409,
0.792428918540511,1.)))
REPRESENTATION_ITEM('')
SURFACE()
);
#3459=(
BOUNDED_SURFACE()
B_SPLINE_SURFACE(3,2,((#428042,#428043,#428044),(#428045,#428046,#428047),
(#428048,#428049,#428050),(#428051,#428052,#428053),(#428054,#428055,#428056),
(#428057,#428058,#428059)),.UNSPECIFIED.,.F.,.F.,.F.)
B_SPLINE_SURFACE_WITH_KNOTS((4,2,4),(3,3),(-1.76182853028894E-19,7.62675010863194E-5,
0.000152535002172639),(0.,1.02152348203075),.UNSPECIFIED.)
GEOMETRIC_REPRESENTATION_ITEM()
RATIONAL_B_SPLINE_SURFACE(((1.,0.789033595401239,1.00908146323695),(1.,
0.857071781054839,1.00615262590431),(1.,0.92208726471071,1.00335390671593),
(1.,0.922394466502382,1.00334068261144),(1.,0.857224384599031,1.00614605678502),
(1.,0.789033595401635,1.00908146323693)))
REPRESENTATION_ITEM('')
SURFACE()
);
#3460=(
BOUNDED_SURFACE()
B_SPLINE_SURFACE(3,2,((#428061,#428062,#428063),(#428064,#428065,#428066),
(#428067,#428068,#428069),(#428070,#428071,#428072)),.UNSPECIFIED.,.F.,
 .F.,.F.)
B_SPLINE_SURFACE_WITH_KNOTS((4,4),(3,3),(1.0842021724855E-19,4.88747512969882E-5),
(-0.000215489857601605,1.),.UNSPECIFIED.)
GEOMETRIC_REPRESENTATION_ITEM()
RATIONAL_B_SPLINE_SURFACE(((1.00008945889737,0.792428983985628,1.),(1.00008931610858,
0.792760296061173,1.),(1.00008917172371,0.793095311538253,1.),(1.00008902569093,
0.79343415062788,1.)))
REPRESENTATION_ITEM('')
SURFACE()
);
#3461=(
BOUNDED_SURFACE()
B_SPLINE_SURFACE(3,2,((#428074,#428075,#428076),(#428077,#428078,#428079),
(#428080,#428081,#428082),(#428083,#428084,#428085)),.UNSPECIFIED.,.F.,
 .F.,.F.)
B_SPLINE_SURFACE_WITH_KNOTS((4,4),(3,3),(-5.21974905013089E-6,5.74172395514397E-5),
(-0.00139822857724275,1.00051312364068),.UNSPECIFIED.)
GEOMETRIC_REPRESENTATION_ITEM()
RATIONAL_B_SPLINE_SURFACE(((1.00049256947239,0.823768952244066,1.0001806039785),
(1.0004844821571,0.826662424388356,1.00017763870883),(1.00052427784017,
0.812424361909431,1.00019223006922),(1.00059912365849,0.785646094632812,
1.00021967280231)))
REPRESENTATION_ITEM('')
SURFACE()
);
#3462=(
BOUNDED_SURFACE()
B_SPLINE_SURFACE(3,2,((#428089,#428090,#428091),(#428092,#428093,#428094),
(#428095,#428096,#428097),(#428098,#428099,#428100)),.UNSPECIFIED.,.F.,
 .F.,.F.)
B_SPLINE_SURFACE_WITH_KNOTS((4,4),(3,3),(3.22980774337781E-5,9.63764854872257E-5),
(-0.00154325936397012,1.01095292447533),.UNSPECIFIED.)
GEOMETRIC_REPRESENTATION_ITEM()
RATIONAL_B_SPLINE_SURFACE(((1.00023530983302,0.922925743796151,1.00168574728329),
(1.00015136166128,0.950422439594209,1.00108434699059),(1.00033574337403,
0.890029368953944,1.00240524789545),(1.0005426009423,0.822274473168309,
1.00388716464854)))
REPRESENTATION_ITEM('')
SURFACE()
);
#3463=(
BOUNDED_SURFACE()
B_SPLINE_SURFACE(3,2,((#428200,#428201,#428202),(#428203,#428204,#428205),
(#428206,#428207,#428208),(#428209,#428210,#428211)),.UNSPECIFIED.,.F.,
 .F.,.F.)
B_SPLINE_SURFACE_WITH_KNOTS((4,4),(3,3),(0.,0.000101260117256738),(0.,1.),
 .UNSPECIFIED.)
GEOMETRIC_REPRESENTATION_ITEM()
RATIONAL_B_SPLINE_SURFACE(((1.,0.796615278835171,1.),(1.,0.795896038055936,
1.),(1.,0.795193354661349,1.),(1.,0.794506193185544,1.)))
REPRESENTATION_ITEM('')
SURFACE()
);
#3464=(
BOUNDED_SURFACE()
B_SPLINE_SURFACE(3,2,((#428249,#428250,#428251),(#428252,#428253,#428254),
(#428255,#428256,#428257),(#428258,#428259,#428260),(#428261,#428262,#428263),
(#428264,#428265,#428266)),.UNSPECIFIED.,.F.,.F.,.F.)
B_SPLINE_SURFACE_WITH_KNOTS((4,2,4),(3,3),(1.32137139771671E-19,1.66936432462298E-5,
3.33872864924595E-5),(0.,1.),.UNSPECIFIED.)
GEOMETRIC_REPRESENTATION_ITEM()
RATIONAL_B_SPLINE_SURFACE(((1.,0.796615278835171,1.),(1.,0.862310524418131,
1.),(1.,0.923774472010519,1.),(1.,0.923983993203428,1.),(1.,0.862574873720954,
1.),(1.,0.79661527883518,1.)))
REPRESENTATION_ITEM('')
SURFACE()
);
#3465=(
BOUNDED_SURFACE()
B_SPLINE_SURFACE(3,2,((#428303,#428304,#428305),(#428306,#428307,#428308),
(#428309,#428310,#428311),(#428312,#428313,#428314)),.UNSPECIFIED.,.F.,
 .F.,.F.)
B_SPLINE_SURFACE_WITH_KNOTS((4,4),(3,3),(2.16840434497101E-19,0.000101244905251112),
(0.,1.),.UNSPECIFIED.)
GEOMETRIC_REPRESENTATION_ITEM()
RATIONAL_B_SPLINE_SURFACE(((1.,0.796615278835167,1.),(1.,0.79589614610979,
1.),(1.,0.7951935657965,1.),(1.,0.794506502889897,1.)))
REPRESENTATION_ITEM('')
SURFACE()
);
#3466=(
BOUNDED_SURFACE()
B_SPLINE_SURFACE(3,2,((#428350,#428351,#428352),(#428353,#428354,#428355),
(#428356,#428357,#428358),(#428359,#428360,#428361)),.UNSPECIFIED.,.F.,
 .F.,.F.)
B_SPLINE_SURFACE_WITH_KNOTS((4,4),(3,3),(2.85968127239939E-5,9.24681548475817E-5),
(-0.00167900678656574,1.0113082712785),.UNSPECIFIED.)
GEOMETRIC_REPRESENTATION_ITEM()
RATIONAL_B_SPLINE_SURFACE(((1.00059040895218,0.822187541868215,1.00401468696667),
(1.0003652771814,0.889990093671542,1.00248382673397),(1.00016469515013,
0.95039904225791,1.00111990082514),(1.00025604273993,0.922888044286058,
1.00174104990635)))
REPRESENTATION_ITEM('')
SURFACE()
);
#3467=(
BOUNDED_SURFACE()
B_SPLINE_SURFACE(3,2,((#428365,#428366,#428367),(#428368,#428369,#428370),
(#428371,#428372,#428373),(#428374,#428375,#428376)),.UNSPECIFIED.,.F.,
 .F.,.F.)
B_SPLINE_SURFACE_WITH_KNOTS((4,4),(3,3),(-5.22358356749274E-6,5.74594192424278E-5),
(-0.00127120052085918,1.),.UNSPECIFIED.)
GEOMETRIC_REPRESENTATION_ITEM()
RATIONAL_B_SPLINE_SURFACE(((1.00054449313188,0.785835073638707,1.),(1.00047707767486,
0.812351526358773,1.),(1.00044031788597,0.82681021650624,1.),(1.00044777653329,
0.823876514387199,1.)))
REPRESENTATION_ITEM('')
SURFACE()
);
#3468=(
BOUNDED_SURFACE()
B_SPLINE_SURFACE(3,2,((#428378,#428379,#428380),(#428381,#428382,#428383),
(#428384,#428385,#428386),(#428387,#428388,#428389)),.UNSPECIFIED.,.F.,
 .F.,.F.)
B_SPLINE_SURFACE_WITH_KNOTS((4,4),(3,3),(-1.0842021724855E-19,4.88747512969879E-5),
(-0.000215805215068792,1.),.UNSPECIFIED.)
GEOMETRIC_REPRESENTATION_ITEM()
RATIONAL_B_SPLINE_SURFACE(((1.00008915600321,0.793434085499829,1.),(1.00008930224974,
0.793095246303368,1.),(1.00008944684596,0.792760230720648,1.),(1.00008958984375,
0.792428918540678,1.)))
REPRESENTATION_ITEM('')
SURFACE()
);
#3469=(
BOUNDED_SURFACE()
B_SPLINE_SURFACE(3,2,((#428391,#428392,#428393),(#428394,#428395,#428396),
(#428397,#428398,#428399),(#428400,#428401,#428402),(#428403,#428404,#428405),
(#428406,#428407,#428408)),.UNSPECIFIED.,.F.,.F.,.F.)
B_SPLINE_SURFACE_WITH_KNOTS((4,2,4),(3,3),(-2.03287907341032E-20,7.62675010863198E-5,
0.00015253500217264),(0.,1.02152348203072),.UNSPECIFIED.)
GEOMETRIC_REPRESENTATION_ITEM()
RATIONAL_B_SPLINE_SURFACE(((1.,0.789033595401241,1.00908146323693),(1.,
0.857071781054893,1.0061526259043),(1.,0.922087264710644,1.00335390671593),
(1.,0.922394466502453,1.00334068261144),(1.,0.857224384598993,1.00614605678502),
(1.,0.789033595401637,1.00908146323692)))
REPRESENTATION_ITEM('')
SURFACE()
);
#3470=(
BOUNDED_SURFACE()
B_SPLINE_SURFACE(3,2,((#428410,#428411,#428412),(#428413,#428414,#428415),
(#428416,#428417,#428418),(#428419,#428420,#428421)),.UNSPECIFIED.,.F.,
 .F.,.F.)
B_SPLINE_SURFACE_WITH_KNOTS((4,4),(3,3),(3.25260651745651E-19,4.88747512969886E-5),
(-0.000215489856821933,1.),.UNSPECIFIED.)
GEOMETRIC_REPRESENTATION_ITEM()
RATIONAL_B_SPLINE_SURFACE(((1.00008945889704,0.792428983985787,1.),(1.00008931610826,
0.79276029606134,1.),(1.00008917172338,0.793095311538397,1.),(1.00008902569061,
0.793434150628038,1.)))
REPRESENTATION_ITEM('')
SURFACE()
);
#3471=(
BOUNDED_SURFACE()
B_SPLINE_SURFACE(3,2,((#428423,#428424,#428425),(#428426,#428427,#428428),
(#428429,#428430,#428431),(#428432,#428433,#428434)),.UNSPECIFIED.,.F.,
 .F.,.F.)
B_SPLINE_SURFACE_WITH_KNOTS((4,4),(3,3),(-5.21974905013084E-6,5.74172395514396E-5),
(-0.0013982285780412,1.00051312364079),.UNSPECIFIED.)
GEOMETRIC_REPRESENTATION_ITEM()
RATIONAL_B_SPLINE_SURFACE(((1.00049256947267,0.823768952243902,1.00018060397854),
(1.00048448215738,0.826662424388193,1.00017763870887),(1.00052427784047,
0.812424361909257,1.00019223006926),(1.00059912365884,0.785646094632611,
1.00021967280236)))
REPRESENTATION_ITEM('')
SURFACE()
);
#3472=(
BOUNDED_SURFACE()
B_SPLINE_SURFACE(3,2,((#428438,#428439,#428440),(#428441,#428442,#428443),
(#428444,#428445,#428446),(#428447,#428448,#428449)),.UNSPECIFIED.,.F.,
 .F.,.F.)
B_SPLINE_SURFACE_WITH_KNOTS((4,4),(3,3),(3.22980774337777E-5,9.63764854872247E-5),
(-0.00154325936325689,1.01095292447535),.UNSPECIFIED.)
GEOMETRIC_REPRESENTATION_ITEM()
RATIONAL_B_SPLINE_SURFACE(((1.00023530983292,0.92292574379621,1.0016857472833),
(1.00015136166121,0.950422439594245,1.00108434699059),(1.00033574337388,
0.890029368954018,1.00240524789546),(1.00054260094205,0.822274473168436,
1.00388716464855)))
REPRESENTATION_ITEM('')
SURFACE()
);
#3473=(
BOUNDED_SURFACE()
B_SPLINE_SURFACE(3,2,((#428549,#428550,#428551),(#428552,#428553,#428554),
(#428555,#428556,#428557),(#428558,#428559,#428560)),.UNSPECIFIED.,.F.,
 .F.,.F.)
B_SPLINE_SURFACE_WITH_KNOTS((4,4),(3,3),(0.,0.000101260117256738),(0.,1.),
 .UNSPECIFIED.)
GEOMETRIC_REPRESENTATION_ITEM()
RATIONAL_B_SPLINE_SURFACE(((1.,0.796615278835171,1.),(1.,0.795896038055939,
1.),(1.,0.795193354661346,1.),(1.,0.794506193185548,1.)))
REPRESENTATION_ITEM('')
SURFACE()
);
#3474=(
BOUNDED_SURFACE()
B_SPLINE_SURFACE(3,2,((#428598,#428599,#428600),(#428601,#428602,#428603),
(#428604,#428605,#428606),(#428607,#428608,#428609),(#428610,#428611,#428612),
(#428613,#428614,#428615)),.UNSPECIFIED.,.F.,.F.,.F.)
B_SPLINE_SURFACE_WITH_KNOTS((4,2,4),(3,3),(-1.82959116606929E-19,1.66936432462294E-5,
3.33872864924589E-5),(0.,1.),.UNSPECIFIED.)
GEOMETRIC_REPRESENTATION_ITEM()
RATIONAL_B_SPLINE_SURFACE(((1.,0.796615278835176,1.),(1.,0.862310524418125,
1.),(1.,0.923774472010523,1.),(1.,0.923983993203423,1.),(1.,0.862574873720947,
1.),(1.,0.796615278835187,1.)))
REPRESENTATION_ITEM('')
SURFACE()
);
#3475=(
BOUNDED_SURFACE()
B_SPLINE_SURFACE(3,2,((#428652,#428653,#428654),(#428655,#428656,#428657),
(#428658,#428659,#428660),(#428661,#428662,#428663)),.UNSPECIFIED.,.F.,
 .F.,.F.)
B_SPLINE_SURFACE_WITH_KNOTS((4,4),(3,3),(0.,0.000101244905251112),(0.,1.),
 .UNSPECIFIED.)
GEOMETRIC_REPRESENTATION_ITEM()
RATIONAL_B_SPLINE_SURFACE(((1.,0.796615278835172,1.),(1.,0.795896146109797,
1.),(1.,0.795193565796499,1.),(1.,0.794506502889901,1.)))
REPRESENTATION_ITEM('')
SURFACE()
);
#3476=(
BOUNDED_SURFACE()
B_SPLINE_SURFACE(3,2,((#428699,#428700,#428701),(#428702,#428703,#428704),
(#428705,#428706,#428707),(#428708,#428709,#428710)),.UNSPECIFIED.,.F.,
 .F.,.F.)
B_SPLINE_SURFACE_WITH_KNOTS((4,4),(3,3),(2.85968127239939E-5,9.24681548475817E-5),
(-0.00167900678552175,1.01130827127825),.UNSPECIFIED.)
GEOMETRIC_REPRESENTATION_ITEM()
RATIONAL_B_SPLINE_SURFACE(((1.00059040895181,0.822187541868451,1.00401468696657),
(1.00036527718117,0.889990093671682,1.00248382673392),(1.00016469515003,
0.950399042257977,1.00111990082511),(1.00025604273977,0.92288804428616,
1.00174104990631)))
REPRESENTATION_ITEM('')
SURFACE()
);
#3477=(
BOUNDED_SURFACE()
B_SPLINE_SURFACE(3,2,((#428714,#428715,#428716),(#428717,#428718,#428719),
(#428720,#428721,#428722),(#428723,#428724,#428725)),.UNSPECIFIED.,.F.,
 .F.,.F.)
B_SPLINE_SURFACE_WITH_KNOTS((4,4),(3,3),(-5.22358356749324E-6,5.74594192424276E-5),
(-0.0012712005205181,1.),.UNSPECIFIED.)
GEOMETRIC_REPRESENTATION_ITEM()
RATIONAL_B_SPLINE_SURFACE(((1.00054449313173,0.785835073638774,1.),(1.00047707767473,
0.812351526358856,1.),(1.00044031788585,0.826810216506294,1.),(1.00044777653317,
0.823876514387263,1.)))
REPRESENTATION_ITEM('')
SURFACE()
);
#3478=(
BOUNDED_SURFACE()
B_SPLINE_SURFACE(3,2,((#428727,#428728,#428729),(#428730,#428731,#428732),
(#428733,#428734,#428735),(#428736,#428737,#428738)),.UNSPECIFIED.,.F.,
 .F.,.F.)
B_SPLINE_SURFACE_WITH_KNOTS((4,4),(3,3),(-2.16840434497101E-19,4.88747512969878E-5),
(-0.000215805215532899,1.),.UNSPECIFIED.)
GEOMETRIC_REPRESENTATION_ITEM()
RATIONAL_B_SPLINE_SURFACE(((1.0000891560034,0.793434085499735,1.),(1.00008930224993,
0.793095246303274,1.),(1.00008944684615,0.792760230720554,1.),(1.00008958984395,
0.792428918540581,1.)))
REPRESENTATION_ITEM('')
SURFACE()
);
#3479=(
BOUNDED_SURFACE()
B_SPLINE_SURFACE(3,2,((#428740,#428741,#428742),(#428743,#428744,#428745),
(#428746,#428747,#428748),(#428749,#428750,#428751),(#428752,#428753,#428754),
(#428755,#428756,#428757)),.UNSPECIFIED.,.F.,.F.,.F.)
B_SPLINE_SURFACE_WITH_KNOTS((4,2,4),(3,3),(2.71050543121376E-19,7.62675010863199E-5,
0.00015253500217264),(0.,1.02152348203062),.UNSPECIFIED.)
GEOMETRIC_REPRESENTATION_ITEM()
RATIONAL_B_SPLINE_SURFACE(((1.,0.789033595401262,1.00908146323689),(1.,
0.857071781054858,1.00615262590427),(1.,0.922087264710723,1.00335390671591),
(1.,0.92239446650239,1.00334068261142),(1.,0.857224384599052,1.00614605678498),
(1.,0.78903359540166,1.00908146323687)))
REPRESENTATION_ITEM('')
SURFACE()
);
#3480=(
BOUNDED_SURFACE()
B_SPLINE_SURFACE(3,2,((#428759,#428760,#428761),(#428762,#428763,#428764),
(#428765,#428766,#428767),(#428768,#428769,#428770)),.UNSPECIFIED.,.F.,
 .F.,.F.)
B_SPLINE_SURFACE_WITH_KNOTS((4,4),(3,3),(2.43945488809238E-19,4.88747512969882E-5),
(-0.000215489856995972,1.),.UNSPECIFIED.)
GEOMETRIC_REPRESENTATION_ITEM()
RATIONAL_B_SPLINE_SURFACE(((1.00008945889711,0.792428983985754,1.),(1.00008931610833,
0.792760296061308,1.),(1.00008917172346,0.793095311538361,1.),(1.00008902569068,
0.793434150628005,1.)))
REPRESENTATION_ITEM('')
SURFACE()
);
#3481=(
BOUNDED_SURFACE()
B_SPLINE_SURFACE(3,2,((#428772,#428773,#428774),(#428775,#428776,#428777),
(#428778,#428779,#428780),(#428781,#428782,#428783)),.UNSPECIFIED.,.F.,
 .F.,.F.)
B_SPLINE_SURFACE_WITH_KNOTS((4,4),(3,3),(-5.21974905013083E-6,5.74172395514397E-5),
(-0.00139822857793678,1.00051312364077),.UNSPECIFIED.)
GEOMETRIC_REPRESENTATION_ITEM()
RATIONAL_B_SPLINE_SURFACE(((1.00049256947264,0.823768952243928,1.00018060397853),
(1.00048448215734,0.826662424388221,1.00017763870886),(1.00052427784043,
0.812424361909281,1.00019223006925),(1.00059912365879,0.785646094632644,
1.00021967280236)))
REPRESENTATION_ITEM('')
SURFACE()
);
#3482=(
BOUNDED_SURFACE()
B_SPLINE_SURFACE(3,2,((#428787,#428788,#428789),(#428790,#428791,#428792),
(#428793,#428794,#428795),(#428796,#428797,#428798)),.UNSPECIFIED.,.F.,
 .F.,.F.)
B_SPLINE_SURFACE_WITH_KNOTS((4,4),(3,3),(3.22980774337776E-5,9.63764854872256E-5),
(-0.00154325936406371,1.01095292447559),.UNSPECIFIED.)
GEOMETRIC_REPRESENTATION_ITEM()
RATIONAL_B_SPLINE_SURFACE(((1.00023530983304,0.922925743796126,1.00168574728333),
(1.00015136166129,0.950422439594194,1.00108434699061),(1.00033574337405,
0.890029368953907,1.00240524789551),(1.00054260094233,0.822274473168248,
1.00388716464864)))
REPRESENTATION_ITEM('')
SURFACE()
);
#3483=(
BOUNDED_SURFACE()
B_SPLINE_SURFACE(3,2,((#428898,#428899,#428900),(#428901,#428902,#428903),
(#428904,#428905,#428906),(#428907,#428908,#428909)),.UNSPECIFIED.,.F.,
 .F.,.F.)
B_SPLINE_SURFACE_WITH_KNOTS((4,4),(3,3),(0.,0.000101260117256737),(0.,1.),
 .UNSPECIFIED.)
GEOMETRIC_REPRESENTATION_ITEM()
RATIONAL_B_SPLINE_SURFACE(((1.,0.796615278835169,1.),(1.,0.79589603805594,
1.),(1.,0.795193354661342,1.),(1.,0.794506193185545,1.)))
REPRESENTATION_ITEM('')
SURFACE()
);
#3484=(
BOUNDED_SURFACE()
B_SPLINE_SURFACE(3,2,((#428947,#428948,#428949),(#428950,#428951,#428952),
(#428953,#428954,#428955),(#428956,#428957,#428958),(#428959,#428960,#428961),
(#428962,#428963,#428964)),.UNSPECIFIED.,.F.,.F.,.F.)
B_SPLINE_SURFACE_WITH_KNOTS((4,2,4),(3,3),(-1.99899775552015E-19,1.66936432462289E-5,
3.3387286492458E-5),(0.,1.),.UNSPECIFIED.)
GEOMETRIC_REPRESENTATION_ITEM()
RATIONAL_B_SPLINE_SURFACE(((1.,0.796615278835174,1.),(1.,0.862310524418136,
1.),(1.,0.923774472010518,1.),(1.,0.923983993203428,1.),(1.,0.862574873720939,
1.),(1.,0.796615278835189,1.)))
REPRESENTATION_ITEM('')
SURFACE()
);
#3485=(
BOUNDED_SURFACE()
B_SPLINE_SURFACE(3,2,((#429001,#429002,#429003),(#429004,#429005,#429006),
(#429007,#429008,#429009),(#429010,#429011,#429012)),.UNSPECIFIED.,.F.,
 .F.,.F.)
B_SPLINE_SURFACE_WITH_KNOTS((4,4),(3,3),(0.,0.000101244905251112),(0.,1.),
 .UNSPECIFIED.)
GEOMETRIC_REPRESENTATION_ITEM()
RATIONAL_B_SPLINE_SURFACE(((1.,0.796615278835169,1.),(1.,0.795896146109799,
1.),(1.,0.795193565796492,1.),(1.,0.7945065028899,1.)))
REPRESENTATION_ITEM('')
SURFACE()
);
#3486=(
BOUNDED_SURFACE()
B_SPLINE_SURFACE(3,2,((#429048,#429049,#429050),(#429051,#429052,#429053),
(#429054,#429055,#429056),(#429057,#429058,#429059)),.UNSPECIFIED.,.F.,
 .F.,.F.)
B_SPLINE_SURFACE_WITH_KNOTS((4,4),(3,3),(2.85968127239939E-5,9.24681548475814E-5),
(-0.0016790067864226,1.01130827127812),.UNSPECIFIED.)
GEOMETRIC_REPRESENTATION_ITEM()
RATIONAL_B_SPLINE_SURFACE(((1.00059040895212,0.822187541868312,1.00401468696653),
(1.00036527718137,0.889990093671596,1.00248382673389),(1.00016469515012,
0.950399042257943,1.0011199008251),(1.00025604273991,0.922888044286096,
1.00174104990629)))
REPRESENTATION_ITEM('')
SURFACE()
);
#3487=(
BOUNDED_SURFACE()
B_SPLINE_SURFACE(3,2,((#429063,#429064,#429065),(#429066,#429067,#429068),
(#429069,#429070,#429071),(#429072,#429073,#429074)),.UNSPECIFIED.,.F.,
 .F.,.F.)
B_SPLINE_SURFACE_WITH_KNOTS((4,4),(3,3),(-5.22358356749289E-6,5.74594192424278E-5),
(-0.00127120052075543,1.),.UNSPECIFIED.)
GEOMETRIC_REPRESENTATION_ITEM()
RATIONAL_B_SPLINE_SURFACE(((1.00054449313184,0.785835073638715,1.),(1.00047707767482,
0.81235152635882,1.),(1.00044031788593,0.826810216506243,1.),(1.00044777653326,
0.823876514387217,1.)))
REPRESENTATION_ITEM('')
SURFACE()
);
#3488=(
BOUNDED_SURFACE()
B_SPLINE_SURFACE(3,2,((#429076,#429077,#429078),(#429079,#429080,#429081),
(#429082,#429083,#429084),(#429085,#429086,#429087)),.UNSPECIFIED.,.F.,
 .F.,.F.)
B_SPLINE_SURFACE_WITH_KNOTS((4,4),(3,3),(0.,4.88747512969881E-5),(-0.000215805215095398,
1.),.UNSPECIFIED.)
GEOMETRIC_REPRESENTATION_ITEM()
RATIONAL_B_SPLINE_SURFACE(((1.00008915600322,0.793434085499822,1.),(1.00008930224975,
0.793095246303359,1.),(1.00008944684597,0.792760230720646,1.),(1.00008958984376,
0.79242891854067,1.)))
REPRESENTATION_ITEM('')
SURFACE()
);
#3489=(
BOUNDED_SURFACE()
B_SPLINE_SURFACE(3,2,((#429089,#429090,#429091),(#429092,#429093,#429094),
(#429095,#429096,#429097),(#429098,#429099,#429100),(#429101,#429102,#429103),
(#429104,#429105,#429106)),.UNSPECIFIED.,.F.,.F.,.F.)
B_SPLINE_SURFACE_WITH_KNOTS((4,2,4),(3,3),(-6.7762635780344E-20,7.62675010863195E-5,
0.000152535002172639),(0.,1.02152348203083),.UNSPECIFIED.)
GEOMETRIC_REPRESENTATION_ITEM()
RATIONAL_B_SPLINE_SURFACE(((1.,0.789033595401219,1.00908146323698),(1.,
0.857071781054809,1.00615262590433),(1.,0.922087264710727,1.00335390671594),
(1.,0.922394466502351,1.00334068261146),(1.,0.857224384599042,1.00614605678505),
(1.,0.789033595401617,1.00908146323697)))
REPRESENTATION_ITEM('')
SURFACE()
);
#3490=(
BOUNDED_SURFACE()
B_SPLINE_SURFACE(3,2,((#429108,#429109,#429110),(#429111,#429112,#429113),
(#429114,#429115,#429116),(#429117,#429118,#429119)),.UNSPECIFIED.,.F.,
 .F.,.F.)
B_SPLINE_SURFACE_WITH_KNOTS((4,4),(3,3),(1.89735380184963E-19,4.8874751296988E-5),
(-0.00021548985687891,1.),.UNSPECIFIED.)
GEOMETRIC_REPRESENTATION_ITEM()
RATIONAL_B_SPLINE_SURFACE(((1.00008945889707,0.792428983985783,1.),(1.00008931610828,
0.792760296061324,1.),(1.00008917172341,0.79309531153839,1.),(1.00008902569063,
0.793434150628027,1.)))
REPRESENTATION_ITEM('')
SURFACE()
);
#3491=(
BOUNDED_SURFACE()
B_SPLINE_SURFACE(3,2,((#429121,#429122,#429123),(#429124,#429125,#429126),
(#429127,#429128,#429129),(#429130,#429131,#429132)),.UNSPECIFIED.,.F.,
 .F.,.F.)
B_SPLINE_SURFACE_WITH_KNOTS((4,4),(3,3),(-5.21974905013083E-6,5.74172395514395E-5),
(-0.00139822857813303,1.00051312364079),.UNSPECIFIED.)
GEOMETRIC_REPRESENTATION_ITEM()
RATIONAL_B_SPLINE_SURFACE(((1.00049256947271,0.823768952243883,1.00018060397854),
(1.00048448215741,0.826662424388189,1.00017763870886),(1.0005242778405,
0.812424361909235,1.00019223006926),(1.00059912365888,0.7856460946326,1.00021967280236)))
REPRESENTATION_ITEM('')
SURFACE()
);
#3492=(
BOUNDED_SURFACE()
B_SPLINE_SURFACE(3,2,((#429136,#429137,#429138),(#429139,#429140,#429141),
(#429142,#429143,#429144),(#429145,#429146,#429147)),.UNSPECIFIED.,.F.,
 .F.,.F.)
B_SPLINE_SURFACE_WITH_KNOTS((4,4),(3,3),(3.22980774337778E-5,9.63764854872248E-5),
(-0.00154325936355796,1.01095292447537),.UNSPECIFIED.)
GEOMETRIC_REPRESENTATION_ITEM()
RATIONAL_B_SPLINE_SURFACE(((1.00023530983296,0.922925743796181,1.0016857472833),
(1.00015136166124,0.950422439594237,1.00108434699059),(1.00033574337394,
0.890029368953977,1.00240524789546),(1.00054260094215,0.822274473168379,
1.00388716464856)))
REPRESENTATION_ITEM('')
SURFACE()
);
#3493=(
BOUNDED_SURFACE()
B_SPLINE_SURFACE(3,2,((#429247,#429248,#429249),(#429250,#429251,#429252),
(#429253,#429254,#429255),(#429256,#429257,#429258)),.UNSPECIFIED.,.F.,
 .F.,.F.)
B_SPLINE_SURFACE_WITH_KNOTS((4,4),(3,3),(0.,0.000101260117256737),(0.,1.),
 .UNSPECIFIED.)
GEOMETRIC_REPRESENTATION_ITEM()
RATIONAL_B_SPLINE_SURFACE(((1.,0.796615278835173,1.),(1.,0.795896038055931,
1.),(1.,0.795193354661359,1.),(1.,0.794506193185536,1.)))
REPRESENTATION_ITEM('')
SURFACE()
);
#3494=(
BOUNDED_SURFACE()
B_SPLINE_SURFACE(3,2,((#429296,#429297,#429298),(#429299,#429300,#429301),
(#429302,#429303,#429304),(#429305,#429306,#429307),(#429308,#429309,#429310),
(#429311,#429312,#429313)),.UNSPECIFIED.,.F.,.F.,.F.)
B_SPLINE_SURFACE_WITH_KNOTS((4,2,4),(3,3),(-1.23666810299128E-19,1.66936432462298E-5,
3.33872864924597E-5),(0.,1.),.UNSPECIFIED.)
GEOMETRIC_REPRESENTATION_ITEM()
RATIONAL_B_SPLINE_SURFACE(((1.,0.796615278835171,1.),(1.,0.862310524418122,
1.),(1.,0.92377447201052,1.),(1.,0.92398399320343,1.),(1.,0.862574873720945,
1.),(1.,0.796615278835183,1.)))
REPRESENTATION_ITEM('')
SURFACE()
);
#3495=(
BOUNDED_SURFACE()
B_SPLINE_SURFACE(3,2,((#429350,#429351,#429352),(#429353,#429354,#429355),
(#429356,#429357,#429358),(#429359,#429360,#429361)),.UNSPECIFIED.,.F.,
 .F.,.F.)
B_SPLINE_SURFACE_WITH_KNOTS((4,4),(3,3),(0.,0.000101244905251112),(0.,1.),
 .UNSPECIFIED.)
GEOMETRIC_REPRESENTATION_ITEM()
RATIONAL_B_SPLINE_SURFACE(((1.,0.796615278835171,1.),(1.,0.795896146109787,
1.),(1.,0.795193565796502,1.),(1.,0.794506502889898,1.)))
REPRESENTATION_ITEM('')
SURFACE()
);
#3496=(
BOUNDED_SURFACE()
B_SPLINE_SURFACE(3,2,((#429397,#429398,#429399),(#429400,#429401,#429402),
(#429403,#429404,#429405),(#429406,#429407,#429408)),.UNSPECIFIED.,.F.,
 .F.,.F.)
B_SPLINE_SURFACE_WITH_KNOTS((4,4),(3,3),(2.85968127239939E-5,9.24681548475814E-5),
(-0.00167900678789534,1.01130827127821),.UNSPECIFIED.)
GEOMETRIC_REPRESENTATION_ITEM()
RATIONAL_B_SPLINE_SURFACE(((1.00059040895264,0.822187541868032,1.00401468696656),
(1.00036527718169,0.889990093671424,1.00248382673391),(1.00016469515026,
0.950399042257866,1.00111990082511),(1.00025604274013,0.922888044285976,
1.00174104990631)))
REPRESENTATION_ITEM('')
SURFACE()
);
#3497=(
BOUNDED_SURFACE()
B_SPLINE_SURFACE(3,2,((#429412,#429413,#429414),(#429415,#429416,#429417),
(#429418,#429419,#429420),(#429421,#429422,#429423)),.UNSPECIFIED.,.F.,
 .F.,.F.)
B_SPLINE_SURFACE_WITH_KNOTS((4,4),(3,3),(-5.22358356749297E-6,5.74594192424279E-5),
(-0.00127120052063385,1.),.UNSPECIFIED.)
GEOMETRIC_REPRESENTATION_ITEM()
RATIONAL_B_SPLINE_SURFACE(((1.00054449313178,0.785835073638746,1.),(1.00047707767478,
0.81235152635883,1.),(1.00044031788589,0.826810216506275,1.),(1.00044777653321,
0.823876514387243,1.)))
REPRESENTATION_ITEM('')
SURFACE()
);
#3498=(
BOUNDED_SURFACE()
B_SPLINE_SURFACE(3,2,((#429425,#429426,#429427),(#429428,#429429,#429430),
(#429431,#429432,#429433),(#429434,#429435,#429436)),.UNSPECIFIED.,.F.,
 .F.,.F.)
B_SPLINE_SURFACE_WITH_KNOTS((4,4),(3,3),(-2.71050543121376E-20,4.88747512969882E-5),
(-0.000215805215167394,1.),.UNSPECIFIED.)
GEOMETRIC_REPRESENTATION_ITEM()
RATIONAL_B_SPLINE_SURFACE(((1.00008915600325,0.793434085499807,1.),(1.00008930224978,
0.793095246303351,1.),(1.000089446846,0.792760230720625,1.),(1.00008958984379,
0.792428918540659,1.)))
REPRESENTATION_ITEM('')
SURFACE()
);
#3499=(
BOUNDED_SURFACE()
B_SPLINE_SURFACE(3,2,((#429438,#429439,#429440),(#429441,#429442,#429443),
(#429444,#429445,#429446),(#429447,#429448,#429449),(#429450,#429451,#429452),
(#429453,#429454,#429455)),.UNSPECIFIED.,.F.,.F.,.F.)
B_SPLINE_SURFACE_WITH_KNOTS((4,2,4),(3,3),(5.42101086242752E-20,7.62675010863199E-5,
0.00015253500217264),(0.,1.02152348203028),.UNSPECIFIED.)
GEOMETRIC_REPRESENTATION_ITEM()
RATIONAL_B_SPLINE_SURFACE(((1.,0.789033595401331,1.00908146323675),(1.,
0.857071781054903,1.00615262590417),(1.,0.922087264710748,1.00335390671586),
(1.,0.922394466502417,1.00334068261137),(1.,0.857224384599095,1.00614605678489),
(1.,0.789033595401731,1.00908146323673)))
REPRESENTATION_ITEM('')
SURFACE()
);
#3500=(
BOUNDED_SURFACE()
B_SPLINE_SURFACE(3,2,((#429457,#429458,#429459),(#429460,#429461,#429462),
(#429463,#429464,#429465),(#429466,#429467,#429468)),.UNSPECIFIED.,.F.,
 .F.,.F.)
B_SPLINE_SURFACE_WITH_KNOTS((4,4),(3,3),(5.42101086242752E-19,4.88747512969884E-5),
(-0.000215489857109308,1.),.UNSPECIFIED.)
GEOMETRIC_REPRESENTATION_ITEM()
RATIONAL_B_SPLINE_SURFACE(((1.00008945889716,0.792428983985732,1.),(1.00008931610838,
0.79276029606126,1.),(1.0000891717235,0.793095311538357,1.),(1.00008902569073,
0.793434150627978,1.)))
REPRESENTATION_ITEM('')
SURFACE()
);
#3501=(
BOUNDED_SURFACE()
B_SPLINE_SURFACE(3,2,((#429470,#429471,#429472),(#429473,#429474,#429475),
(#429476,#429477,#429478),(#429479,#429480,#429481)),.UNSPECIFIED.,.F.,
 .F.,.F.)
B_SPLINE_SURFACE_WITH_KNOTS((4,4),(3,3),(-5.21974905012879E-6,5.74172395514404E-5),
(-0.00139822857791635,1.00051312364079),.UNSPECIFIED.)
GEOMETRIC_REPRESENTATION_ITEM()
RATIONAL_B_SPLINE_SURFACE(((1.00049256947263,0.823768952243921,1.00018060397854),
(1.00048448215733,0.826662424388215,1.00017763870886),(1.00052427784042,
0.812424361909278,1.00019223006926),(1.00059912365878,0.785646094632641,
1.00021967280236)))
REPRESENTATION_ITEM('')
SURFACE()
);
#3502=(
BOUNDED_SURFACE()
B_SPLINE_SURFACE(3,2,((#429485,#429486,#429487),(#429488,#429489,#429490),
(#429491,#429492,#429493),(#429494,#429495,#429496)),.UNSPECIFIED.,.F.,
 .F.,.F.)
B_SPLINE_SURFACE_WITH_KNOTS((4,4),(3,3),(3.22980774337777E-5,9.63764854872246E-5),
(-0.00154325936392007,1.01095292447559),.UNSPECIFIED.)
GEOMETRIC_REPRESENTATION_ITEM()
RATIONAL_B_SPLINE_SURFACE(((1.00023530983302,0.922925743796137,1.00168574728333),
(1.00015136166127,0.950422439594199,1.00108434699061),(1.00033574337402,
0.890029368953927,1.00240524789551),(1.00054260094228,0.822274473168269,
1.00388716464864)))
REPRESENTATION_ITEM('')
SURFACE()
);
#3503=(
BOUNDED_SURFACE()
B_SPLINE_SURFACE(3,2,((#429596,#429597,#429598),(#429599,#429600,#429601),
(#429602,#429603,#429604),(#429605,#429606,#429607)),.UNSPECIFIED.,.F.,
 .F.,.F.)
B_SPLINE_SURFACE_WITH_KNOTS((4,4),(3,3),(-2.16840434497101E-19,0.000101260117256737),
(0.,1.),.UNSPECIFIED.)
GEOMETRIC_REPRESENTATION_ITEM()
RATIONAL_B_SPLINE_SURFACE(((1.,0.796615278835171,1.),(1.,0.795896038055954,
1.),(1.,0.795193354661325,1.),(1.,0.794506193185548,1.)))
REPRESENTATION_ITEM('')
SURFACE()
);
#3504=(
BOUNDED_SURFACE()
B_SPLINE_SURFACE(3,2,((#429645,#429646,#429647),(#429648,#429649,#429650),
(#429651,#429652,#429653),(#429654,#429655,#429656),(#429657,#429658,#429659),
(#429660,#429661,#429662)),.UNSPECIFIED.,.F.,.F.,.F.)
B_SPLINE_SURFACE_WITH_KNOTS((4,2,4),(3,3),(1.52465930505774E-20,1.66936432462301E-5,
3.33872864924601E-5),(0.,1.),.UNSPECIFIED.)
GEOMETRIC_REPRESENTATION_ITEM()
RATIONAL_B_SPLINE_SURFACE(((1.,0.796615278835175,1.),(1.,0.862310524418118,
1.),(1.,0.923774472010521,1.),(1.,0.923983993203426,1.),(1.,0.862574873720939,
1.),(1.,0.796615278835187,1.)))
REPRESENTATION_ITEM('')
SURFACE()
);
#3505=(
BOUNDED_SURFACE()
B_SPLINE_SURFACE(3,2,((#429699,#429700,#429701),(#429702,#429703,#429704),
(#429705,#429706,#429707),(#429708,#429709,#429710)),.UNSPECIFIED.,.F.,
 .F.,.F.)
B_SPLINE_SURFACE_WITH_KNOTS((4,4),(3,3),(0.,0.000101244905251112),(0.,1.),
 .UNSPECIFIED.)
GEOMETRIC_REPRESENTATION_ITEM()
RATIONAL_B_SPLINE_SURFACE(((1.,0.796615278835175,1.),(1.,0.795896146109783,
1.),(1.,0.795193565796506,1.),(1.,0.794506502889895,1.)))
REPRESENTATION_ITEM('')
SURFACE()
);
#3506=(
BOUNDED_SURFACE()
B_SPLINE_SURFACE(3,2,((#429746,#429747,#429748),(#429749,#429750,#429751),
(#429752,#429753,#429754),(#429755,#429756,#429757)),.UNSPECIFIED.,.F.,
 .F.,.F.)
B_SPLINE_SURFACE_WITH_KNOTS((4,4),(3,3),(2.85968127239939E-5,9.24681548475819E-5),
(-0.00167900679337037,1.01130827127828),.UNSPECIFIED.)
GEOMETRIC_REPRESENTATION_ITEM()
RATIONAL_B_SPLINE_SURFACE(((1.00059040895457,0.822187541867037,1.00401468696659),
(1.00036527718288,0.889990093670808,1.00248382673392),(1.0001646951508,
0.95039904225759,1.00111990082511),(1.00025604274097,0.922888044285542,
1.00174104990632)))
REPRESENTATION_ITEM('')
SURFACE()
);
#3507=(
BOUNDED_SURFACE()
B_SPLINE_SURFACE(3,2,((#429761,#429762,#429763),(#429764,#429765,#429766),
(#429767,#429768,#429769),(#429770,#429771,#429772)),.UNSPECIFIED.,.F.,
 .F.,.F.)
B_SPLINE_SURFACE_WITH_KNOTS((4,4),(3,3),(-5.22358356749127E-6,5.74594192424277E-5),
(-0.00127120052043637,1.),.UNSPECIFIED.)
GEOMETRIC_REPRESENTATION_ITEM()
RATIONAL_B_SPLINE_SURFACE(((1.0005444931317,0.785835073638799,1.),(1.0004770776747,
0.812351526358858,1.),(1.00044031788582,0.826810216506319,1.),(1.00044777653314,
0.823876514387272,0.999999999999999)))
REPRESENTATION_ITEM('')
SURFACE()
);
#3508=(
BOUNDED_SURFACE()
B_SPLINE_SURFACE(3,2,((#429774,#429775,#429776),(#429777,#429778,#429779),
(#429780,#429781,#429782),(#429783,#429784,#429785)),.UNSPECIFIED.,.F.,
 .F.,.F.)
B_SPLINE_SURFACE_WITH_KNOTS((4,4),(3,3),(-1.62630325872826E-19,4.8874751296988E-5),
(-0.000215805215728941,1.),.UNSPECIFIED.)
GEOMETRIC_REPRESENTATION_ITEM()
RATIONAL_B_SPLINE_SURFACE(((1.00008915600348,0.793434085499697,1.),(1.00008930225001,
0.79309524630324,1.),(1.00008944684623,0.792760230720509,1.),(1.00008958984403,
0.792428918540541,1.)))
REPRESENTATION_ITEM('')
SURFACE()
);
#3509=(
BOUNDED_SURFACE()
B_SPLINE_SURFACE(3,2,((#429787,#429788,#429789),(#429790,#429791,#429792),
(#429793,#429794,#429795),(#429796,#429797,#429798),(#429799,#429800,#429801),
(#429802,#429803,#429804)),.UNSPECIFIED.,.F.,.F.,.F.)
B_SPLINE_SURFACE_WITH_KNOTS((4,2,4),(3,3),(1.21972744404619E-19,7.626750108632E-5,
0.00015253500217264),(0.,1.02152348203059),.UNSPECIFIED.)
GEOMETRIC_REPRESENTATION_ITEM()
RATIONAL_B_SPLINE_SURFACE(((1.,0.789033595401271,1.00908146323688),(1.,
0.857071781054863,1.00615262590426),(1.,0.922087264710716,1.00335390671591),
(1.,0.922394466502397,1.00334068261142),(1.,0.857224384599058,1.00614605678498),
(1.,0.789033595401664,1.00908146323686)))
REPRESENTATION_ITEM('')
SURFACE()
);
#3510=(
BOUNDED_SURFACE()
B_SPLINE_SURFACE(3,2,((#429806,#429807,#429808),(#429809,#429810,#429811),
(#429812,#429813,#429814),(#429815,#429816,#429817)),.UNSPECIFIED.,.F.,
 .F.,.F.)
B_SPLINE_SURFACE_WITH_KNOTS((4,4),(3,3),(3.25260651745651E-19,4.88747512969883E-5),
(-0.000215489857120083,1.),.UNSPECIFIED.)
GEOMETRIC_REPRESENTATION_ITEM()
RATIONAL_B_SPLINE_SURFACE(((1.00008945889717,0.792428983985724,1.),(1.00008931610838,
0.792760296061273,1.),(1.00008917172351,0.793095311538346,1.),(1.00008902569073,
0.793434150627979,1.)))
REPRESENTATION_ITEM('')
SURFACE()
);
#3511=(
BOUNDED_SURFACE()
B_SPLINE_SURFACE(3,2,((#429819,#429820,#429821),(#429822,#429823,#429824),
(#429825,#429826,#429827),(#429828,#429829,#429830)),.UNSPECIFIED.,.F.,
 .F.,.F.)
B_SPLINE_SURFACE_WITH_KNOTS((4,4),(3,3),(-5.219749050131E-6,5.74172395514396E-5),
(-0.00139822857776702,1.00051312364072),.UNSPECIFIED.)
GEOMETRIC_REPRESENTATION_ITEM()
RATIONAL_B_SPLINE_SURFACE(((1.00049256947258,0.823768952243958,1.00018060397851),
(1.00048448215728,0.826662424388262,1.00017763870884),(1.00052427784036,
0.812424361909323,1.00019223006923),(1.00059912365872,0.78564609463269,
1.00021967280233)))
REPRESENTATION_ITEM('')
SURFACE()
);
#3512=(
BOUNDED_SURFACE()
B_SPLINE_SURFACE(3,2,((#429834,#429835,#429836),(#429837,#429838,#429839),
(#429840,#429841,#429842),(#429843,#429844,#429845)),.UNSPECIFIED.,.F.,
 .F.,.F.)
B_SPLINE_SURFACE_WITH_KNOTS((4,4),(3,3),(3.22980774337781E-5,9.63764854872258E-5),
(-0.00154325936368032,1.01095292447566),.UNSPECIFIED.)
GEOMETRIC_REPRESENTATION_ITEM()
RATIONAL_B_SPLINE_SURFACE(((1.00023530983298,0.922925743796149,1.00168574728335),
(1.00015136166125,0.950422439594211,1.00108434699062),(1.00033574337397,
0.890029368953936,1.00240524789553),(1.00054260094219,0.822274473168305,
1.00388716464866)))
REPRESENTATION_ITEM('')
SURFACE()
);
#3513=(
BOUNDED_SURFACE()
B_SPLINE_SURFACE(3,2,((#429945,#429946,#429947),(#429948,#429949,#429950),
(#429951,#429952,#429953),(#429954,#429955,#429956)),.UNSPECIFIED.,.F.,
 .F.,.F.)
B_SPLINE_SURFACE_WITH_KNOTS((4,4),(3,3),(2.16840434497101E-19,0.000101260117256738),
(0.,1.),.UNSPECIFIED.)
GEOMETRIC_REPRESENTATION_ITEM()
RATIONAL_B_SPLINE_SURFACE(((1.,0.796615278835173,1.),(1.,0.795896038055934,
1.),(1.,0.795193354661359,1.),(1.,0.794506193185544,1.)))
REPRESENTATION_ITEM('')
SURFACE()
);
#3514=(
BOUNDED_SURFACE()
B_SPLINE_SURFACE(3,2,((#429994,#429995,#429996),(#429997,#429998,#429999),
(#430000,#430001,#430002),(#430003,#430004,#430005),(#430006,#430007,#430008),
(#430009,#430010,#430011)),.UNSPECIFIED.,.F.,.F.,.F.)
B_SPLINE_SURFACE_WITH_KNOTS((4,2,4),(3,3),(6.09863722023096E-20,1.66936432462294E-5,
3.33872864924587E-5),(0.,1.),.UNSPECIFIED.)
GEOMETRIC_REPRESENTATION_ITEM()
RATIONAL_B_SPLINE_SURFACE(((1.,0.796615278835173,1.),(1.,0.862310524418131,
1.),(1.,0.92377447201052,1.),(1.,0.923983993203426,1.),(1.,0.862574873720942,
1.),(1.,0.796615278835181,1.)))
REPRESENTATION_ITEM('')
SURFACE()
);
#3515=(
BOUNDED_SURFACE()
B_SPLINE_SURFACE(3,2,((#430048,#430049,#430050),(#430051,#430052,#430053),
(#430054,#430055,#430056),(#430057,#430058,#430059)),.UNSPECIFIED.,.F.,
 .F.,.F.)
B_SPLINE_SURFACE_WITH_KNOTS((4,4),(3,3),(0.,0.000101244905251112),(0.,1.),
 .UNSPECIFIED.)
GEOMETRIC_REPRESENTATION_ITEM()
RATIONAL_B_SPLINE_SURFACE(((1.,0.796615278835172,1.),(1.,0.795896146109788,
1.),(1.,0.795193565796502,1.),(1.,0.794506502889901,1.)))
REPRESENTATION_ITEM('')
SURFACE()
);
#3516=(
BOUNDED_SURFACE()
B_SPLINE_SURFACE(3,2,((#430095,#430096,#430097),(#430098,#430099,#430100),
(#430101,#430102,#430103),(#430104,#430105,#430106)),.UNSPECIFIED.,.F.,
 .F.,.F.)
B_SPLINE_SURFACE_WITH_KNOTS((4,4),(3,3),(2.85968127239939E-5,9.24681548475816E-5),
(-0.00167900678720424,1.01130827127828),.UNSPECIFIED.)
GEOMETRIC_REPRESENTATION_ITEM()
RATIONAL_B_SPLINE_SURFACE(((1.0005904089524,0.822187541868145,1.00401468696659),
(1.00036527718154,0.889990093671497,1.00248382673392),(1.0001646951502,
0.950399042257892,1.00111990082511),(1.00025604274003,0.922888044286026,
1.00174104990632)))
REPRESENTATION_ITEM('')
SURFACE()
);
#3517=(
BOUNDED_SURFACE()
B_SPLINE_SURFACE(3,2,((#430110,#430111,#430112),(#430113,#430114,#430115),
(#430116,#430117,#430118),(#430119,#430120,#430121)),.UNSPECIFIED.,.F.,
 .F.,.F.)
B_SPLINE_SURFACE_WITH_KNOTS((4,4),(3,3),(-5.22358356749324E-6,5.74594192424276E-5),
(-0.00127120052082716,1.),.UNSPECIFIED.)
GEOMETRIC_REPRESENTATION_ITEM()
RATIONAL_B_SPLINE_SURFACE(((1.00054449313187,0.785835073638711,1.),(1.00047707767485,
0.812351526358801,1.),(1.00044031788596,0.826810216506234,1.),(1.00044777653328,
0.823876514387217,1.)))
REPRESENTATION_ITEM('')
SURFACE()
);
#3518=(
BOUNDED_SURFACE()
B_SPLINE_SURFACE(3,2,((#430123,#430124,#430125),(#430126,#430127,#430128),
(#430129,#430130,#430131),(#430132,#430133,#430134)),.UNSPECIFIED.,.F.,
 .F.,.F.)
B_SPLINE_SURFACE_WITH_KNOTS((4,4),(3,3),(-5.42101086242752E-20,4.88747512969881E-5),
(-0.000215805215198065,1.),.UNSPECIFIED.)
GEOMETRIC_REPRESENTATION_ITEM()
RATIONAL_B_SPLINE_SURFACE(((1.00008915600326,0.793434085499804,1.),(1.00008930224979,
0.793095246303347,1.),(1.00008944684601,0.792760230720621,1.),(1.00008958984381,
0.792428918540653,1.)))
REPRESENTATION_ITEM('')
SURFACE()
);
#3519=(
BOUNDED_SURFACE()
B_SPLINE_SURFACE(3,2,((#430136,#430137,#430138),(#430139,#430140,#430141),
(#430142,#430143,#430144),(#430145,#430146,#430147),(#430148,#430149,#430150),
(#430151,#430152,#430153)),.UNSPECIFIED.,.F.,.F.,.F.)
B_SPLINE_SURFACE_WITH_KNOTS((4,2,4),(3,3),(1.42301535138722E-19,7.62675010863197E-5,
0.000152535002172639),(0.,1.02152348203077),.UNSPECIFIED.)
GEOMETRIC_REPRESENTATION_ITEM()
RATIONAL_B_SPLINE_SURFACE(((1.,0.78903359540123,1.00908146323696),(1.,0.857071781054831,
1.00615262590431),(1.,0.922087264710718,1.00335390671593),(1.,0.922394466502371,
1.00334068261145),(1.,0.857224384599045,1.00614605678503),(1.,0.789033595401625,
1.00908146323694)))
REPRESENTATION_ITEM('')
SURFACE()
);
#3520=(
BOUNDED_SURFACE()
B_SPLINE_SURFACE(3,2,((#430155,#430156,#430157),(#430158,#430159,#430160),
(#430161,#430162,#430163),(#430164,#430165,#430166)),.UNSPECIFIED.,.F.,
 .F.,.F.)
B_SPLINE_SURFACE_WITH_KNOTS((4,4),(3,3),(3.79470760369927E-19,4.88747512969884E-5),
(-0.000215489856982675,1.),.UNSPECIFIED.)
GEOMETRIC_REPRESENTATION_ITEM()
RATIONAL_B_SPLINE_SURFACE(((1.00008945889711,0.792428983985755,1.),(1.00008931610833,
0.792760296061309,1.),(1.00008917172345,0.793095311538362,1.),(1.00008902569068,
0.793434150628006,1.)))
REPRESENTATION_ITEM('')
SURFACE()
);
#3521=(
BOUNDED_SURFACE()
B_SPLINE_SURFACE(3,2,((#430168,#430169,#430170),(#430171,#430172,#430173),
(#430174,#430175,#430176),(#430177,#430178,#430179)),.UNSPECIFIED.,.F.,
 .F.,.F.)
B_SPLINE_SURFACE_WITH_KNOTS((4,4),(3,3),(-5.21974905013088E-6,5.74172395514398E-5),
(-0.00139822857777732,1.00051312364092),.UNSPECIFIED.)
GEOMETRIC_REPRESENTATION_ITEM()
RATIONAL_B_SPLINE_SURFACE(((1.00049256947258,0.823768952243931,1.00018060397858),
(1.00048448215728,0.826662424388213,1.00017763870891),(1.00052427784037,
0.812424361909292,1.0001922300693),(1.00059912365872,0.785646094632641,
1.00021967280242)))
REPRESENTATION_ITEM('')
SURFACE()
);
#3522=(
BOUNDED_SURFACE()
B_SPLINE_SURFACE(3,2,((#430183,#430184,#430185),(#430186,#430187,#430188),
(#430189,#430190,#430191),(#430192,#430193,#430194)),.UNSPECIFIED.,.F.,
 .F.,.F.)
B_SPLINE_SURFACE_WITH_KNOTS((4,4),(3,3),(3.2298077433778E-5,9.63764854872248E-5),
(-0.00154325936368034,1.01095292447542),.UNSPECIFIED.)
GEOMETRIC_REPRESENTATION_ITEM()
RATIONAL_B_SPLINE_SURFACE(((1.00023530983298,0.922925743796171,1.00168574728331),
(1.00015136166125,0.950422439594218,1.0010843469906),(1.00033574337397,
0.89002936895396,1.00240524789547),(1.00054260094219,0.822274473168348,
1.00388716464858)))
REPRESENTATION_ITEM('')
SURFACE()
);
#3523=(
BOUNDED_SURFACE()
B_SPLINE_SURFACE(3,2,((#430294,#430295,#430296),(#430297,#430298,#430299),
(#430300,#430301,#430302),(#430303,#430304,#430305)),.UNSPECIFIED.,.F.,
 .F.,.F.)
B_SPLINE_SURFACE_WITH_KNOTS((4,4),(3,3),(2.16840434497101E-19,0.000101260117256738),
(0.,1.),.UNSPECIFIED.)
GEOMETRIC_REPRESENTATION_ITEM()
RATIONAL_B_SPLINE_SURFACE(((1.,0.79661527883517,1.),(1.,0.795896038055942,
1.),(1.,0.79519335466135,1.),(1.,0.794506193185549,1.)))
REPRESENTATION_ITEM('')
SURFACE()
);
#3524=(
BOUNDED_SURFACE()
B_SPLINE_SURFACE(3,2,((#430343,#430344,#430345),(#430346,#430347,#430348),
(#430349,#430350,#430351),(#430352,#430353,#430354),(#430355,#430356,#430357),
(#430358,#430359,#430360)),.UNSPECIFIED.,.F.,.F.,.F.)
B_SPLINE_SURFACE_WITH_KNOTS((4,2,4),(3,3),(4.57397791517322E-20,1.66936432462298E-5,
3.33872864924596E-5),(0.,1.),.UNSPECIFIED.)
GEOMETRIC_REPRESENTATION_ITEM()
RATIONAL_B_SPLINE_SURFACE(((1.,0.796615278835178,1.),(1.,0.862310524418128,
1.),(1.,0.923774472010521,1.),(1.,0.923983993203423,1.),(1.,0.862574873720944,
1.),(1.,0.796615278835188,1.)))
REPRESENTATION_ITEM('')
SURFACE()
);
#3525=(
BOUNDED_SURFACE()
B_SPLINE_SURFACE(3,2,((#430397,#430398,#430399),(#430400,#430401,#430402),
(#430403,#430404,#430405),(#430406,#430407,#430408)),.UNSPECIFIED.,.F.,
 .F.,.F.)
B_SPLINE_SURFACE_WITH_KNOTS((4,4),(3,3),(0.,0.000101244905251112),(0.,1.),
 .UNSPECIFIED.)
GEOMETRIC_REPRESENTATION_ITEM()
RATIONAL_B_SPLINE_SURFACE(((1.,0.796615278835173,1.),(1.,0.795896146109794,
1.),(1.,0.795193565796502,1.),(1.,0.794506502889902,1.)))
REPRESENTATION_ITEM('')
SURFACE()
);
#3526=(
BOUNDED_SURFACE()
B_SPLINE_SURFACE(3,2,((#430444,#430445,#430446),(#430447,#430448,#430449),
(#430450,#430451,#430452),(#430453,#430454,#430455)),.UNSPECIFIED.,.F.,
 .F.,.F.)
B_SPLINE_SURFACE_WITH_KNOTS((4,4),(3,3),(2.85968127239939E-5,9.24681548475819E-5),
(-0.00167900678745074,1.01130827127827),.UNSPECIFIED.)
GEOMETRIC_REPRESENTATION_ITEM()
RATIONAL_B_SPLINE_SURFACE(((1.00059040895249,0.822187541868105,1.00401468696658),
(1.00036527718159,0.889990093671465,1.00248382673392),(1.00016469515022,
0.950399042257882,1.00111990082511),(1.00025604274006,0.922888044286007,
1.00174104990632)))
REPRESENTATION_ITEM('')
SURFACE()
);
#3527=(
BOUNDED_SURFACE()
B_SPLINE_SURFACE(3,2,((#430459,#430460,#430461),(#430462,#430463,#430464),
(#430465,#430466,#430467),(#430468,#430469,#430470)),.UNSPECIFIED.,.F.,
 .F.,.F.)
B_SPLINE_SURFACE_WITH_KNOTS((4,4),(3,3),(-5.22358356749293E-6,5.74594192424277E-5),
(-0.00127120052034674,1.),.UNSPECIFIED.)
GEOMETRIC_REPRESENTATION_ITEM()
RATIONAL_B_SPLINE_SURFACE(((1.00054449313166,0.785835073638813,1.),(1.00047707767467,
0.812351526358894,1.),(1.00044031788579,0.826810216506316,1.),(1.00044777653311,
0.823876514387298,1.)))
REPRESENTATION_ITEM('')
SURFACE()
);
#3528=(
BOUNDED_SURFACE()
B_SPLINE_SURFACE(3,2,((#430472,#430473,#430474),(#430475,#430476,#430477),
(#430478,#430479,#430480),(#430481,#430482,#430483)),.UNSPECIFIED.,.F.,
 .F.,.F.)
B_SPLINE_SURFACE_WITH_KNOTS((4,4),(3,3),(1.62630325872826E-19,4.88747512969885E-5),
(-0.000215805215935403,1.),.UNSPECIFIED.)
GEOMETRIC_REPRESENTATION_ITEM()
RATIONAL_B_SPLINE_SURFACE(((1.00008915600357,0.79343408549965,1.),(1.0000893022501,
0.793095246303188,1.),(1.00008944684632,0.792760230720469,1.),(1.00008958984411,
0.792428918540496,1.)))
REPRESENTATION_ITEM('')
SURFACE()
);
#3529=(
BOUNDED_SURFACE()
B_SPLINE_SURFACE(3,2,((#430485,#430486,#430487),(#430488,#430489,#430490),
(#430491,#430492,#430493),(#430494,#430495,#430496),(#430497,#430498,#430499),
(#430500,#430501,#430502)),.UNSPECIFIED.,.F.,.F.,.F.)
B_SPLINE_SURFACE_WITH_KNOTS((4,2,4),(3,3),(1.76182853028894E-19,7.62675010863199E-5,
0.00015253500217264),(0.,1.0215234820306),.UNSPECIFIED.)
GEOMETRIC_REPRESENTATION_ITEM()
RATIONAL_B_SPLINE_SURFACE(((1.,0.789033595401265,1.00908146323688),(1.,
0.857071781054835,1.00615262590426),(1.,0.922087264710755,1.00335390671591),
(1.,0.922394466502361,1.00334068261142),(1.,0.857224384599075,1.00614605678498),
(1.,0.789033595401665,1.00908146323687)))
REPRESENTATION_ITEM('')
SURFACE()
);
#3530=(
BOUNDED_SURFACE()
B_SPLINE_SURFACE(3,2,((#430504,#430505,#430506),(#430507,#430508,#430509),
(#430510,#430511,#430512),(#430513,#430514,#430515)),.UNSPECIFIED.,.F.,
 .F.,.F.)
B_SPLINE_SURFACE_WITH_KNOTS((4,4),(3,3),(5.42101086242752E-20,4.88747512969881E-5),
(-0.000215489856972442,1.),.UNSPECIFIED.)
GEOMETRIC_REPRESENTATION_ITEM()
RATIONAL_B_SPLINE_SURFACE(((1.0000894588971,0.79242898398576,1.),(1.00008931610832,
0.792760296061302,1.),(1.00008917172345,0.793095311538378,1.),(1.00008902569067,
0.793434150628008,1.)))
REPRESENTATION_ITEM('')
SURFACE()
);
#3531=(
BOUNDED_SURFACE()
B_SPLINE_SURFACE(3,2,((#430517,#430518,#430519),(#430520,#430521,#430522),
(#430523,#430524,#430525),(#430526,#430527,#430528)),.UNSPECIFIED.,.F.,
 .F.,.F.)
B_SPLINE_SURFACE_WITH_KNOTS((4,4),(3,3),(-5.21974905013088E-6,5.74172395514395E-5),
(-0.00139822857773102,1.00051312364041),.UNSPECIFIED.)
GEOMETRIC_REPRESENTATION_ITEM()
RATIONAL_B_SPLINE_SURFACE(((1.00049256947256,0.823768952244029,1.0001806039784),
(1.00048448215727,0.826662424388317,1.00017763870873),(1.00052427784035,
0.812424361909394,1.00019223006911),(1.0005991236587,0.785646094632765,
1.0002196728022)))
REPRESENTATION_ITEM('')
SURFACE()
);
#3532=(
BOUNDED_SURFACE()
B_SPLINE_SURFACE(3,2,((#430532,#430533,#430534),(#430535,#430536,#430537),
(#430538,#430539,#430540),(#430541,#430542,#430543)),.UNSPECIFIED.,.F.,
 .F.,.F.)
B_SPLINE_SURFACE_WITH_KNOTS((4,4),(3,3),(3.22980774337783E-5,9.63764854872258E-5),
(-0.0015432593640314,1.01095292447538),.UNSPECIFIED.)
GEOMETRIC_REPRESENTATION_ITEM()
RATIONAL_B_SPLINE_SURFACE(((1.00023530983303,0.922925743796145,1.0016857472833),
(1.00015136166129,0.950422439594196,1.00108434699059),(1.00033574337405,
0.890029368953932,1.00240524789547),(1.00054260094232,0.822274473168291,
1.00388716464856)))
REPRESENTATION_ITEM('')
SURFACE()
);
#3533=(
BOUNDED_SURFACE()
B_SPLINE_SURFACE(3,2,((#430643,#430644,#430645),(#430646,#430647,#430648),
(#430649,#430650,#430651),(#430652,#430653,#430654)),.UNSPECIFIED.,.F.,
 .F.,.F.)
B_SPLINE_SURFACE_WITH_KNOTS((4,4),(3,3),(-2.16840434497101E-19,0.000101260117256738),
(0.,1.),.UNSPECIFIED.)
GEOMETRIC_REPRESENTATION_ITEM()
RATIONAL_B_SPLINE_SURFACE(((1.,0.796615278835167,1.),(1.,0.795896038055943,
1.),(1.,0.795193354661347,1.),(1.,0.794506193185542,1.)))
REPRESENTATION_ITEM('')
SURFACE()
);
#3534=(
BOUNDED_SURFACE()
B_SPLINE_SURFACE(3,2,((#430692,#430693,#430694),(#430695,#430696,#430697),
(#430698,#430699,#430700),(#430701,#430702,#430703),(#430704,#430705,#430706),
(#430707,#430708,#430709)),.UNSPECIFIED.,.F.,.F.,.F.)
B_SPLINE_SURFACE_WITH_KNOTS((4,2,4),(3,3),(5.0821976835258E-20,1.66936432462293E-5,
3.33872864924586E-5),(0.,1.),.UNSPECIFIED.)
GEOMETRIC_REPRESENTATION_ITEM()
RATIONAL_B_SPLINE_SURFACE(((1.,0.796615278835176,1.),(1.,0.86231052441813,
1.),(1.,0.923774472010521,1.),(1.,0.923983993203425,1.),(1.,0.86257487372094,
1.),(1.,0.796615278835182,1.)))
REPRESENTATION_ITEM('')
SURFACE()
);
#3535=(
BOUNDED_SURFACE()
B_SPLINE_SURFACE(3,2,((#430746,#430747,#430748),(#430749,#430750,#430751),
(#430752,#430753,#430754),(#430755,#430756,#430757)),.UNSPECIFIED.,.F.,
 .F.,.F.)
B_SPLINE_SURFACE_WITH_KNOTS((4,4),(3,3),(-2.16840434497101E-19,0.000101244905251112),
(0.,1.),.UNSPECIFIED.)
GEOMETRIC_REPRESENTATION_ITEM()
RATIONAL_B_SPLINE_SURFACE(((1.,0.796615278835169,1.),(1.,0.795896146109793,
1.),(1.,0.7951935657965,1.),(1.,0.794506502889899,1.)))
REPRESENTATION_ITEM('')
SURFACE()
);
#3536=(
BOUNDED_SURFACE()
B_SPLINE_SURFACE(3,2,((#430793,#430794,#430795),(#430796,#430797,#430798),
(#430799,#430800,#430801),(#430802,#430803,#430804)),.UNSPECIFIED.,.F.,
 .F.,.F.)
B_SPLINE_SURFACE_WITH_KNOTS((4,4),(3,3),(2.85968127239939E-5,9.24681548475816E-5),
(-0.00167900678819889,1.01130827127833),.UNSPECIFIED.)
GEOMETRIC_REPRESENTATION_ITEM()
RATIONAL_B_SPLINE_SURFACE(((1.00059040895275,0.822187541867959,1.00401468696661),
(1.00036527718176,0.889990093671379,1.00248382673393),(1.00016469515029,
0.950399042257845,1.00111990082512),(1.00025604274018,0.922888044285941,
1.00174104990633)))
REPRESENTATION_ITEM('')
SURFACE()
);
#3537=(
BOUNDED_SURFACE()
B_SPLINE_SURFACE(3,2,((#430808,#430809,#430810),(#430811,#430812,#430813),
(#430814,#430815,#430816),(#430817,#430818,#430819)),.UNSPECIFIED.,.F.,
 .F.,.F.)
B_SPLINE_SURFACE_WITH_KNOTS((4,4),(3,3),(-5.22358356749291E-6,5.74594192424256E-5),
(-0.00127120052061498,1.),.UNSPECIFIED.)
GEOMETRIC_REPRESENTATION_ITEM()
RATIONAL_B_SPLINE_SURFACE(((1.00054449313178,0.785835073638749,1.),(1.00047707767477,
0.812351526358845,1.),(1.00044031788588,0.826810216506264,1.),(1.00044777653321,
0.823876514387246,1.)))
REPRESENTATION_ITEM('')
SURFACE()
);
#3538=(
BOUNDED_SURFACE()
B_SPLINE_SURFACE(3,2,((#430821,#430822,#430823),(#430824,#430825,#430826),
(#430827,#430828,#430829),(#430830,#430831,#430832)),.UNSPECIFIED.,.F.,
 .F.,.F.)
B_SPLINE_SURFACE_WITH_KNOTS((4,4),(3,3),(-1.0842021724855E-19,4.88747512969882E-5),
(-0.000215805215860785,1.),.UNSPECIFIED.)
GEOMETRIC_REPRESENTATION_ITEM()
RATIONAL_B_SPLINE_SURFACE(((1.00008915600354,0.793434085499667,1.),(1.00008930225007,
0.793095246303216,1.),(1.00008944684629,0.792760230720475,1.),(1.00008958984408,
0.792428918540514,1.)))
REPRESENTATION_ITEM('')
SURFACE()
);
#3539=(
BOUNDED_SURFACE()
B_SPLINE_SURFACE(3,2,((#430834,#430835,#430836),(#430837,#430838,#430839),
(#430840,#430841,#430842),(#430843,#430844,#430845),(#430846,#430847,#430848),
(#430849,#430850,#430851)),.UNSPECIFIED.,.F.,.F.,.F.)
B_SPLINE_SURFACE_WITH_KNOTS((4,2,4),(3,3),(2.98155597433514E-19,7.62675010863196E-5,
0.000152535002172639),(0.,1.02152348203071),.UNSPECIFIED.)
GEOMETRIC_REPRESENTATION_ITEM()
RATIONAL_B_SPLINE_SURFACE(((1.,0.789033595401246,1.00908146323693),(1.,
0.857071781054844,1.00615262590429),(1.,0.922087264710711,1.00335390671592),
(1.,0.922394466502387,1.00334068261144),(1.,0.857224384599034,1.00614605678501),
(1.,0.789033595401642,1.00908146323691)))
REPRESENTATION_ITEM('')
SURFACE()
);
#3540=(
BOUNDED_SURFACE()
B_SPLINE_SURFACE(3,2,((#430853,#430854,#430855),(#430856,#430857,#430858),
(#430859,#430860,#430861),(#430862,#430863,#430864)),.UNSPECIFIED.,.F.,
 .F.,.F.)
B_SPLINE_SURFACE_WITH_KNOTS((4,4),(3,3),(-1.62630325872826E-19,4.88747512969882E-5),
(-0.000215489857814701,1.),.UNSPECIFIED.)
GEOMETRIC_REPRESENTATION_ITEM()
RATIONAL_B_SPLINE_SURFACE(((1.00008945889745,0.792428983985584,1.),(1.00008931610867,
0.79276029606113,1.),(1.0000891717238,0.793095311538205,1.),(1.00008902569102,
0.793434150627835,1.)))
REPRESENTATION_ITEM('')
SURFACE()
);
#3541=(
BOUNDED_SURFACE()
B_SPLINE_SURFACE(3,2,((#430866,#430867,#430868),(#430869,#430870,#430871),
(#430872,#430873,#430874),(#430875,#430876,#430877)),.UNSPECIFIED.,.F.,
 .F.,.F.)
B_SPLINE_SURFACE_WITH_KNOTS((4,4),(3,3),(-5.21974905013086E-6,5.74172395514373E-5),
(-0.00139822857748534,1.00051312364066),.UNSPECIFIED.)
GEOMETRIC_REPRESENTATION_ITEM()
RATIONAL_B_SPLINE_SURFACE(((1.00049256947248,0.823768952244017,1.00018060397849),
(1.00048448215718,0.826662424388332,1.00017763870882),(1.00052427784026,
0.812424361909375,1.00019223006921),(1.0005991236586,0.785646094632768,
1.00021967280231)))
REPRESENTATION_ITEM('')
SURFACE()
);
#3542=(
BOUNDED_SURFACE()
B_SPLINE_SURFACE(3,2,((#430881,#430882,#430883),(#430884,#430885,#430886),
(#430887,#430888,#430889),(#430890,#430891,#430892)),.UNSPECIFIED.,.F.,
 .F.,.F.)
B_SPLINE_SURFACE_WITH_KNOTS((4,4),(3,3),(3.22980774337778E-5,9.63764854872259E-5),
(-0.0015432593635687,1.01095292447554),.UNSPECIFIED.)
GEOMETRIC_REPRESENTATION_ITEM()
RATIONAL_B_SPLINE_SURFACE(((1.00023530983296,0.922925743796169,1.00168574728333),
(1.00015136166124,0.950422439594234,1.00108434699061),(1.00033574337395,
0.890029368953954,1.0024052478955),(1.00054260094215,0.822274473168349,
1.00388716464862)))
REPRESENTATION_ITEM('')
SURFACE()
);
#3543=(
BOUNDED_SURFACE()
B_SPLINE_SURFACE(3,2,((#430992,#430993,#430994),(#430995,#430996,#430997),
(#430998,#430999,#431000),(#431001,#431002,#431003)),.UNSPECIFIED.,.F.,
 .F.,.F.)
B_SPLINE_SURFACE_WITH_KNOTS((4,4),(3,3),(-2.16840434497101E-19,0.000101260117256738),
(0.,1.),.UNSPECIFIED.)
GEOMETRIC_REPRESENTATION_ITEM()
RATIONAL_B_SPLINE_SURFACE(((1.,0.796615278835174,1.),(1.,0.79589603805594,
1.),(1.,0.795193354661341,1.),(1.,0.794506193185547,1.)))
REPRESENTATION_ITEM('')
SURFACE()
);
#3544=(
BOUNDED_SURFACE()
B_SPLINE_SURFACE(3,2,((#431041,#431042,#431043),(#431044,#431045,#431046),
(#431047,#431048,#431049),(#431050,#431051,#431052),(#431053,#431054,#431055),
(#431056,#431057,#431058)),.UNSPECIFIED.,.F.,.F.,.F.)
B_SPLINE_SURFACE_WITH_KNOTS((4,2,4),(3,3),(6.7762635780344E-21,1.66936432462294E-5,
3.33872864924587E-5),(0.,1.),.UNSPECIFIED.)
GEOMETRIC_REPRESENTATION_ITEM()
RATIONAL_B_SPLINE_SURFACE(((1.,0.796615278835177,1.),(1.,0.862310524418125,
1.),(1.,0.923774472010521,1.),(1.,0.923983993203427,1.),(1.,0.86257487372095,
1.),(1.,0.796615278835183,1.)))
REPRESENTATION_ITEM('')
SURFACE()
);
#3545=(
BOUNDED_SURFACE()
B_SPLINE_SURFACE(3,2,((#431095,#431096,#431097),(#431098,#431099,#431100),
(#431101,#431102,#431103),(#431104,#431105,#431106)),.UNSPECIFIED.,.F.,
 .F.,.F.)
B_SPLINE_SURFACE_WITH_KNOTS((4,4),(3,3),(0.,0.000101244905251112),(0.,1.),
 .UNSPECIFIED.)
GEOMETRIC_REPRESENTATION_ITEM()
RATIONAL_B_SPLINE_SURFACE(((1.,0.79661527883517,1.),(1.,0.795896146109795,
1.),(1.,0.795193565796502,1.),(1.,0.794506502889901,1.)))
REPRESENTATION_ITEM('')
SURFACE()
);
#3546=(
BOUNDED_SURFACE()
B_SPLINE_SURFACE(3,2,((#431142,#431143,#431144),(#431145,#431146,#431147),
(#431148,#431149,#431150),(#431151,#431152,#431153)),.UNSPECIFIED.,.F.,
 .F.,.F.)
B_SPLINE_SURFACE_WITH_KNOTS((4,4),(3,3),(2.85968127239939E-5,9.24681548475818E-5),
(-0.00167900678659478,1.01130827127828),.UNSPECIFIED.)
GEOMETRIC_REPRESENTATION_ITEM()
RATIONAL_B_SPLINE_SURFACE(((1.00059040895219,0.822187541868253,1.00401468696659),
(1.00036527718141,0.88999009367156,1.00248382673392),(1.00016469515014,
0.95039904225793,1.00111990082511),(1.00025604273993,0.92288804428607,1.00174104990632)))
REPRESENTATION_ITEM('')
SURFACE()
);
#3547=(
BOUNDED_SURFACE()
B_SPLINE_SURFACE(3,2,((#431157,#431158,#431159),(#431160,#431161,#431162),
(#431163,#431164,#431165),(#431166,#431167,#431168)),.UNSPECIFIED.,.F.,
 .F.,.F.)
B_SPLINE_SURFACE_WITH_KNOTS((4,4),(3,3),(-5.22358356749329E-6,5.74594192424274E-5),
(-0.00127120052065071,1.),.UNSPECIFIED.)
GEOMETRIC_REPRESENTATION_ITEM()
RATIONAL_B_SPLINE_SURFACE(((1.00054449313179,0.785835073638744,1.),(1.00047707767478,
0.812351526358829,1.),(1.0004403178859,0.826810216506268,1.),(1.00044777653322,
0.823876514387243,1.)))
REPRESENTATION_ITEM('')
SURFACE()
);
#3548=(
BOUNDED_SURFACE()
B_SPLINE_SURFACE(3,2,((#431170,#431171,#431172),(#431173,#431174,#431175),
(#431176,#431177,#431178),(#431179,#431180,#431181)),.UNSPECIFIED.,.F.,
 .F.,.F.)
B_SPLINE_SURFACE_WITH_KNOTS((4,4),(3,3),(-4.33680868994202E-19,4.88747512969879E-5),
(-0.000215805215015582,1.),.UNSPECIFIED.)
GEOMETRIC_REPRESENTATION_ITEM()
RATIONAL_B_SPLINE_SURFACE(((1.00008915600319,0.793434085499841,1.),(1.00008930224972,
0.793095246303392,1.),(1.00008944684594,0.792760230720655,1.),(1.00008958984373,
0.79242891854069,1.)))
REPRESENTATION_ITEM('')
SURFACE()
);
#3549=(
BOUNDED_SURFACE()
B_SPLINE_SURFACE(3,2,((#431183,#431184,#431185),(#431186,#431187,#431188),
(#431189,#431190,#431191),(#431192,#431193,#431194),(#431195,#431196,#431197),
(#431198,#431199,#431200)),.UNSPECIFIED.,.F.,.F.,.F.)
B_SPLINE_SURFACE_WITH_KNOTS((4,2,4),(3,3),(2.91379333855479E-19,7.62675010863198E-5,
0.000152535002172639),(0.,1.02152348203076),.UNSPECIFIED.)
GEOMETRIC_REPRESENTATION_ITEM()
RATIONAL_B_SPLINE_SURFACE(((1.,0.789033595401233,1.00908146323695),(1.,
0.857071781054827,1.00615262590431),(1.,0.922087264710726,1.00335390671593),
(1.,0.922394466502363,1.00334068261145),(1.,0.857224384599045,1.00614605678503),
(1.,0.789033595401634,1.00908146323693)))
REPRESENTATION_ITEM('')
SURFACE()
);
#3550=(
BOUNDED_SURFACE()
B_SPLINE_SURFACE(3,2,((#431202,#431203,#431204),(#431205,#431206,#431207),
(#431208,#431209,#431210),(#431211,#431212,#431213)),.UNSPECIFIED.,.F.,
 .F.,.F.)
B_SPLINE_SURFACE_WITH_KNOTS((4,4),(3,3),(3.79470760369927E-19,4.88747512969882E-5),
(-0.000215489857114363,1.),.UNSPECIFIED.)
GEOMETRIC_REPRESENTATION_ITEM()
RATIONAL_B_SPLINE_SURFACE(((1.00008945889716,0.792428983985731,1.),(1.00008931610838,
0.792760296061279,1.),(1.00008917172351,0.793095311538343,1.),(1.00008902569073,
0.793434150627979,1.)))
REPRESENTATION_ITEM('')
SURFACE()
);
#3551=(
BOUNDED_SURFACE()
B_SPLINE_SURFACE(3,2,((#431215,#431216,#431217),(#431218,#431219,#431220),
(#431221,#431222,#431223),(#431224,#431225,#431226)),.UNSPECIFIED.,.F.,
 .F.,.F.)
B_SPLINE_SURFACE_WITH_KNOTS((4,4),(3,3),(-5.21974905013091E-6,5.741723955144E-5),
(-0.0013982285778192,1.0005131236406),.UNSPECIFIED.)
GEOMETRIC_REPRESENTATION_ITEM()
RATIONAL_B_SPLINE_SURFACE(((1.00049256947259,0.823768952243977,1.00018060397847),
(1.0004844821573,0.826662424388274,1.0001776387088),(1.00052427784038,0.812424361909338,
1.00019223006919),(1.00059912365874,0.785646094632704,1.00021967280228)))
REPRESENTATION_ITEM('')
SURFACE()
);
#3552=(
BOUNDED_SURFACE()
B_SPLINE_SURFACE(3,2,((#431230,#431231,#431232),(#431233,#431234,#431235),
(#431236,#431237,#431238),(#431239,#431240,#431241)),.UNSPECIFIED.,.F.,
 .F.,.F.)
B_SPLINE_SURFACE_WITH_KNOTS((4,4),(3,3),(3.22980774337778E-5,9.63764854872254E-5),
(-0.00154325936345388,1.01095292447556),.UNSPECIFIED.)
GEOMETRIC_REPRESENTATION_ITEM()
RATIONAL_B_SPLINE_SURFACE(((1.00023530983295,0.922925743796177,1.00168574728333),
(1.00015136166123,0.95042243959423,1.00108434699061),(1.00033574337392,
0.890029368953974,1.00240524789551),(1.00054260094211,0.82227447316836,
1.00388716464863)))
REPRESENTATION_ITEM('')
SURFACE()
);
#3553=(
BOUNDED_SURFACE()
B_SPLINE_SURFACE(3,2,((#431341,#431342,#431343),(#431344,#431345,#431346),
(#431347,#431348,#431349),(#431350,#431351,#431352)),.UNSPECIFIED.,.F.,
 .F.,.F.)
B_SPLINE_SURFACE_WITH_KNOTS((4,4),(3,3),(2.16840434497101E-19,0.000101260117256738),
(0.,1.),.UNSPECIFIED.)
GEOMETRIC_REPRESENTATION_ITEM()
RATIONAL_B_SPLINE_SURFACE(((1.,0.79661527883517,1.),(1.,0.79589603805594,
1.),(1.,0.795193354661347,1.),(1.,0.794506193185546,1.)))
REPRESENTATION_ITEM('')
SURFACE()
);
#3554=(
BOUNDED_SURFACE()
B_SPLINE_SURFACE(3,2,((#431390,#431391,#431392),(#431393,#431394,#431395),
(#431396,#431397,#431398),(#431399,#431400,#431401),(#431402,#431403,#431404),
(#431405,#431406,#431407)),.UNSPECIFIED.,.F.,.F.,.F.)
B_SPLINE_SURFACE_WITH_KNOTS((4,2,4),(3,3),(8.13151629364128E-20,1.66936432462295E-5,
3.33872864924589E-5),(0.,1.),.UNSPECIFIED.)
GEOMETRIC_REPRESENTATION_ITEM()
RATIONAL_B_SPLINE_SURFACE(((1.,0.796615278835172,1.),(1.,0.862310524418132,
1.),(1.,0.923774472010519,1.),(1.,0.923983993203429,1.),(1.,0.862574873720951,
1.),(1.,0.796615278835181,1.)))
REPRESENTATION_ITEM('')
SURFACE()
);
#3555=(
BOUNDED_SURFACE()
B_SPLINE_SURFACE(3,2,((#431444,#431445,#431446),(#431447,#431448,#431449),
(#431450,#431451,#431452),(#431453,#431454,#431455)),.UNSPECIFIED.,.F.,
 .F.,.F.)
B_SPLINE_SURFACE_WITH_KNOTS((4,4),(3,3),(0.,0.000101244905251112),(0.,1.),
 .UNSPECIFIED.)
GEOMETRIC_REPRESENTATION_ITEM()
RATIONAL_B_SPLINE_SURFACE(((1.,0.796615278835172,1.),(1.,0.795896146109797,
1.),(1.,0.7951935657965,1.),(1.,0.794506502889903,1.)))
REPRESENTATION_ITEM('')
SURFACE()
);
#3556=(
BOUNDED_SURFACE()
B_SPLINE_SURFACE(3,2,((#431491,#431492,#431493),(#431494,#431495,#431496),
(#431497,#431498,#431499),(#431500,#431501,#431502)),.UNSPECIFIED.,.F.,
 .F.,.F.)
B_SPLINE_SURFACE_WITH_KNOTS((4,4),(3,3),(2.85968127239938E-5,9.2468154847582E-5),
(-0.00167900678657004,1.01130827127851),.UNSPECIFIED.)
GEOMETRIC_REPRESENTATION_ITEM()
RATIONAL_B_SPLINE_SURFACE(((1.00059040895218,0.82218754186822,1.00401468696667),
(1.0003652771814,0.889990093671534,1.00248382673397),(1.00016469515013,
0.950399042257918,1.00111990082514),(1.00025604273993,0.922888044286056,
1.00174104990636)))
REPRESENTATION_ITEM('')
SURFACE()
);
#3557=(
BOUNDED_SURFACE()
B_SPLINE_SURFACE(3,2,((#431506,#431507,#431508),(#431509,#431510,#431511),
(#431512,#431513,#431514),(#431515,#431516,#431517)),.UNSPECIFIED.,.F.,
 .F.,.F.)
B_SPLINE_SURFACE_WITH_KNOTS((4,4),(3,3),(-5.22358356749114E-6,5.74594192424275E-5),
(-0.00127120052069131,1.),.UNSPECIFIED.)
GEOMETRIC_REPRESENTATION_ITEM()
RATIONAL_B_SPLINE_SURFACE(((1.00054449313181,0.78583507363874,1.),(1.0004770776748,
0.812351526358814,1.),(1.00044031788591,0.826810216506269,1.),(1.00044777653323,
0.823876514387229,1.)))
REPRESENTATION_ITEM('')
SURFACE()
);
#3558=(
BOUNDED_SURFACE()
B_SPLINE_SURFACE(3,2,((#431519,#431520,#431521),(#431522,#431523,#431524),
(#431525,#431526,#431527),(#431528,#431529,#431530)),.UNSPECIFIED.,.F.,
 .F.,.F.)
B_SPLINE_SURFACE_WITH_KNOTS((4,4),(3,3),(-2.71050543121376E-19,4.8874751296988E-5),
(-0.000215805215089049,1.),.UNSPECIFIED.)
GEOMETRIC_REPRESENTATION_ITEM()
RATIONAL_B_SPLINE_SURFACE(((1.00008915600322,0.793434085499826,1.),(1.00008930224975,
0.793095246303363,1.),(1.00008944684597,0.792760230720644,1.),(1.00008958984376,
0.792428918540672,1.)))
REPRESENTATION_ITEM('')
SURFACE()
);
#3559=(
BOUNDED_SURFACE()
B_SPLINE_SURFACE(3,2,((#431532,#431533,#431534),(#431535,#431536,#431537),
(#431538,#431539,#431540),(#431541,#431542,#431543),(#431544,#431545,#431546),
(#431547,#431548,#431549)),.UNSPECIFIED.,.F.,.F.,.F.)
B_SPLINE_SURFACE_WITH_KNOTS((4,2,4),(3,3),(1.15196480826585E-19,7.62675010863197E-5,
0.000152535002172639),(0.,1.02152348203072),.UNSPECIFIED.)
GEOMETRIC_REPRESENTATION_ITEM()
RATIONAL_B_SPLINE_SURFACE(((1.,0.789033595401238,1.00908146323694),(1.,
0.857071781054832,1.0061526259043),(1.,0.922087264710732,1.00335390671593),
(1.,0.922394466502364,1.00334068261144),(1.,0.857224384599056,1.00614605678502),
(1.,0.78903359540164,1.00908146323692)))
REPRESENTATION_ITEM('')
SURFACE()
);
#3560=(
BOUNDED_SURFACE()
B_SPLINE_SURFACE(3,2,((#431551,#431552,#431553),(#431554,#431555,#431556),
(#431557,#431558,#431559),(#431560,#431561,#431562)),.UNSPECIFIED.,.F.,
 .F.,.F.)
B_SPLINE_SURFACE_WITH_KNOTS((4,4),(3,3),(-8.13151629364128E-20,4.88747512969881E-5),
(-0.000215489856981559,1.),.UNSPECIFIED.)
GEOMETRIC_REPRESENTATION_ITEM()
RATIONAL_B_SPLINE_SURFACE(((1.00008945889711,0.792428983985759,1.),(1.00008931610833,
0.792760296061303,1.),(1.00008917172345,0.793095311538374,1.),(1.00008902569068,
0.793434150628007,1.)))
REPRESENTATION_ITEM('')
SURFACE()
);
#3561=(
BOUNDED_SURFACE()
B_SPLINE_SURFACE(3,2,((#431564,#431565,#431566),(#431567,#431568,#431569),
(#431570,#431571,#431572),(#431573,#431574,#431575)),.UNSPECIFIED.,.F.,
 .F.,.F.)
B_SPLINE_SURFACE_WITH_KNOTS((4,4),(3,3),(-5.2197490501287E-6,5.74172395514394E-5),
(-0.00139822857797119,1.00051312364064),.UNSPECIFIED.)
GEOMETRIC_REPRESENTATION_ITEM()
RATIONAL_B_SPLINE_SURFACE(((1.00049256947265,0.823768952243948,1.00018060397848),
(1.00048448215735,0.826662424388226,1.00017763870881),(1.00052427784044,
0.812424361909317,1.0001922300692),(1.00059912365881,0.785646094632657,
1.0002196728023)))
REPRESENTATION_ITEM('')
SURFACE()
);
#3562=(
BOUNDED_SURFACE()
B_SPLINE_SURFACE(3,2,((#431579,#431580,#431581),(#431582,#431583,#431584),
(#431585,#431586,#431587),(#431588,#431589,#431590)),.UNSPECIFIED.,.F.,
 .F.,.F.)
B_SPLINE_SURFACE_WITH_KNOTS((4,4),(3,3),(3.22980774337777E-5,9.63764854872246E-5),
(-0.00154325936298721,1.01095292447535),.UNSPECIFIED.)
GEOMETRIC_REPRESENTATION_ITEM()
RATIONAL_B_SPLINE_SURFACE(((1.00023530983287,0.922925743796231,1.0016857472833),
(1.00015136166118,0.95042243959425,1.00108434699059),(1.00033574337382,
0.890029368954052,1.00240524789546),(1.00054260094195,0.822274473168482,
1.00388716464855)))
REPRESENTATION_ITEM('')
SURFACE()
);
#3563=(
BOUNDED_SURFACE()
B_SPLINE_SURFACE(3,2,((#431690,#431691,#431692),(#431693,#431694,#431695),
(#431696,#431697,#431698),(#431699,#431700,#431701)),.UNSPECIFIED.,.F.,
 .F.,.F.)
B_SPLINE_SURFACE_WITH_KNOTS((4,4),(3,3),(2.16840434497101E-19,0.000101260117256738),
(0.,1.),.UNSPECIFIED.)
GEOMETRIC_REPRESENTATION_ITEM()
RATIONAL_B_SPLINE_SURFACE(((1.,0.79661527883517,1.),(1.,0.795896038055944,
1.),(1.,0.795193354661343,1.),(1.,0.794506193185549,1.)))
REPRESENTATION_ITEM('')
SURFACE()
);
#3564=(
BOUNDED_SURFACE()
B_SPLINE_SURFACE(3,2,((#431739,#431740,#431741),(#431742,#431743,#431744),
(#431745,#431746,#431747),(#431748,#431749,#431750),(#431751,#431752,#431753),
(#431754,#431755,#431756)),.UNSPECIFIED.,.F.,.F.,.F.)
B_SPLINE_SURFACE_WITH_KNOTS((4,2,4),(3,3),(6.43745039913268E-20,1.66936432462297E-5,
3.33872864924593E-5),(0.,1.),.UNSPECIFIED.)
GEOMETRIC_REPRESENTATION_ITEM()
RATIONAL_B_SPLINE_SURFACE(((1.,0.796615278835177,1.),(1.,0.862310524418133,
1.),(1.,0.92377447201052,1.),(1.,0.923983993203426,1.),(1.,0.862574873720953,
1.),(1.,0.796615278835183,1.)))
REPRESENTATION_ITEM('')
SURFACE()
);
#3565=(
BOUNDED_SURFACE()
B_SPLINE_SURFACE(3,2,((#431793,#431794,#431795),(#431796,#431797,#431798),
(#431799,#431800,#431801),(#431802,#431803,#431804)),.UNSPECIFIED.,.F.,
 .F.,.F.)
B_SPLINE_SURFACE_WITH_KNOTS((4,4),(3,3),(0.,0.000101244905251112),(0.,1.),
 .UNSPECIFIED.)
GEOMETRIC_REPRESENTATION_ITEM()
RATIONAL_B_SPLINE_SURFACE(((1.,0.796615278835172,1.),(1.,0.795896146109793,
1.),(1.,0.795193565796499,1.),(1.,0.7945065028899,1.)))
REPRESENTATION_ITEM('')
SURFACE()
);
#3566=(
BOUNDED_SURFACE()
B_SPLINE_SURFACE(3,2,((#431840,#431841,#431842),(#431843,#431844,#431845),
(#431846,#431847,#431848),(#431849,#431850,#431851)),.UNSPECIFIED.,.F.,
 .F.,.F.)
B_SPLINE_SURFACE_WITH_KNOTS((4,4),(3,3),(2.85968127239939E-5,9.24681548475818E-5),
(-0.0016790067864143,1.01130827127831),.UNSPECIFIED.)
GEOMETRIC_REPRESENTATION_ITEM()
RATIONAL_B_SPLINE_SURFACE(((1.00059040895212,0.822187541868281,1.0040146869666),
(1.00036527718137,0.889990093671572,1.00248382673393),(1.00016469515012,
0.950399042257936,1.00111990082512),(1.0002560427399,0.922888044286082,
1.00174104990632)))
REPRESENTATION_ITEM('')
SURFACE()
);
#3567=(
BOUNDED_SURFACE()
B_SPLINE_SURFACE(3,2,((#431855,#431856,#431857),(#431858,#431859,#431860),
(#431861,#431862,#431863),(#431864,#431865,#431866)),.UNSPECIFIED.,.F.,
 .F.,.F.)
B_SPLINE_SURFACE_WITH_KNOTS((4,4),(3,3),(-5.22358356749296E-6,5.74594192424277E-5),
(-0.00127120052094877,1.),.UNSPECIFIED.)
GEOMETRIC_REPRESENTATION_ITEM()
RATIONAL_B_SPLINE_SURFACE(((1.00054449313192,0.785835073638684,1.),(1.0004770776749,
0.812351526358764,1.),(1.000440317886,0.826810216506224,1.),(1.00044777653332,
0.823876514387182,1.)))
REPRESENTATION_ITEM('')
SURFACE()
);
#3568=(
BOUNDED_SURFACE()
B_SPLINE_SURFACE(3,2,((#431868,#431869,#431870),(#431871,#431872,#431873),
(#431874,#431875,#431876),(#431877,#431878,#431879)),.UNSPECIFIED.,.F.,
 .F.,.F.)
B_SPLINE_SURFACE_WITH_KNOTS((4,4),(3,3),(-2.71050543121376E-20,4.88747512969885E-5),
(-0.000215805215023358,1.),.UNSPECIFIED.)
GEOMETRIC_REPRESENTATION_ITEM()
RATIONAL_B_SPLINE_SURFACE(((1.00008915600319,0.79343408549984,1.),(1.00008930224972,
0.793095246303377,1.),(1.00008944684594,0.792760230720659,1.),(1.00008958984373,
0.792428918540687,1.)))
REPRESENTATION_ITEM('')
SURFACE()
);
#3569=(
BOUNDED_SURFACE()
B_SPLINE_SURFACE(3,2,((#431881,#431882,#431883),(#431884,#431885,#431886),
(#431887,#431888,#431889),(#431890,#431891,#431892),(#431893,#431894,#431895),
(#431896,#431897,#431898)),.UNSPECIFIED.,.F.,.F.,.F.)
B_SPLINE_SURFACE_WITH_KNOTS((4,2,4),(3,3),(8.13151629364128E-20,7.62675010863197E-5,
0.000152535002172639),(0.,1.02152348203076),.UNSPECIFIED.)
GEOMETRIC_REPRESENTATION_ITEM()
RATIONAL_B_SPLINE_SURFACE(((1.,0.789033595401234,1.00908146323695),(1.,
0.857071781054808,1.00615262590431),(1.,0.922087264710746,1.00335390671593),
(1.,0.922394466502346,1.00334068261145),(1.,0.857224384599065,1.00614605678503),
(1.,0.789033595401632,1.00908146323693)))
REPRESENTATION_ITEM('')
SURFACE()
);
#3570=(
BOUNDED_SURFACE()
B_SPLINE_SURFACE(3,2,((#431900,#431901,#431902),(#431903,#431904,#431905),
(#431906,#431907,#431908),(#431909,#431910,#431911)),.UNSPECIFIED.,.F.,
 .F.,.F.)
B_SPLINE_SURFACE_WITH_KNOTS((4,4),(3,3),(3.25260651745651E-19,4.88747512969883E-5),
(-0.000215489856881612,1.),.UNSPECIFIED.)
GEOMETRIC_REPRESENTATION_ITEM()
RATIONAL_B_SPLINE_SURFACE(((1.00008945889707,0.792428983985775,1.),(1.00008931610828,
0.792760296061327,1.),(1.00008917172341,0.793095311538389,1.),(1.00008902569064,
0.793434150628027,1.)))
REPRESENTATION_ITEM('')
SURFACE()
);
#3571=(
BOUNDED_SURFACE()
B_SPLINE_SURFACE(3,2,((#431913,#431914,#431915),(#431916,#431917,#431918),
(#431919,#431920,#431921),(#431922,#431923,#431924)),.UNSPECIFIED.,.F.,
 .F.,.F.)
B_SPLINE_SURFACE_WITH_KNOTS((4,4),(3,3),(-5.21974905013089E-6,5.74172395514398E-5),
(-0.00139822857799824,1.00051312364076),.UNSPECIFIED.)
GEOMETRIC_REPRESENTATION_ITEM()
RATIONAL_B_SPLINE_SURFACE(((1.00049256947266,0.823768952243919,1.00018060397852),
(1.00048448215736,0.826662424388207,1.00017763870885),(1.00052427784045,
0.812424361909281,1.00019223006925),(1.00059912365882,0.785646094632626,
1.00021967280235)))
REPRESENTATION_ITEM('')
SURFACE()
);
#3572=(
BOUNDED_SURFACE()
B_SPLINE_SURFACE(3,2,((#431928,#431929,#431930),(#431931,#431932,#431933),
(#431934,#431935,#431936),(#431937,#431938,#431939)),.UNSPECIFIED.,.F.,
 .F.,.F.)
B_SPLINE_SURFACE_WITH_KNOTS((4,4),(3,3),(3.22980774337781E-5,9.63764854872248E-5),
(-0.00154325936368443,1.01095292447551),.UNSPECIFIED.)
GEOMETRIC_REPRESENTATION_ITEM()
RATIONAL_B_SPLINE_SURFACE(((1.00023530983298,0.922925743796163,1.00168574728332),
(1.00015136166125,0.950422439594214,1.00108434699061),(1.00033574337397,
0.890029368953953,1.00240524789549),(1.0005426009422,0.82227447316833,1.00388716464861)))
REPRESENTATION_ITEM('')
SURFACE()
);
#3573=(
BOUNDED_SURFACE()
B_SPLINE_SURFACE(3,2,((#432039,#432040,#432041),(#432042,#432043,#432044),
(#432045,#432046,#432047),(#432048,#432049,#432050)),.UNSPECIFIED.,.F.,
 .F.,.F.)
B_SPLINE_SURFACE_WITH_KNOTS((4,4),(3,3),(-4.33680868994202E-19,0.000101260117256736),
(0.,1.),.UNSPECIFIED.)
GEOMETRIC_REPRESENTATION_ITEM()
RATIONAL_B_SPLINE_SURFACE(((1.,0.796615278835172,1.),(1.,0.79589603805593,
1.),(1.,0.79519335466136,1.),(1.,0.794506193185535,1.)))
REPRESENTATION_ITEM('')
SURFACE()
);
#3574=(
BOUNDED_SURFACE()
B_SPLINE_SURFACE(3,2,((#432088,#432089,#432090),(#432091,#432092,#432093),
(#432094,#432095,#432096),(#432097,#432098,#432099),(#432100,#432101,#432102),
(#432103,#432104,#432105)),.UNSPECIFIED.,.F.,.F.,.F.)
B_SPLINE_SURFACE_WITH_KNOTS((4,2,4),(3,3),(-1.18584612615602E-20,1.66936432462294E-5,
3.33872864924588E-5),(0.,1.),.UNSPECIFIED.)
GEOMETRIC_REPRESENTATION_ITEM()
RATIONAL_B_SPLINE_SURFACE(((1.,0.796615278835171,1.),(1.,0.862310524418129,
1.),(1.,0.923774472010521,1.),(1.,0.923983993203424,1.),(1.,0.862574873720939,
1.),(1.,0.796615278835184,1.)))
REPRESENTATION_ITEM('')
SURFACE()
);
#3575=(
BOUNDED_SURFACE()
B_SPLINE_SURFACE(3,2,((#432142,#432143,#432144),(#432145,#432146,#432147),
(#432148,#432149,#432150),(#432151,#432152,#432153)),.UNSPECIFIED.,.F.,
 .F.,.F.)
B_SPLINE_SURFACE_WITH_KNOTS((4,4),(3,3),(0.,0.000101244905251112),(0.,1.),
 .UNSPECIFIED.)
GEOMETRIC_REPRESENTATION_ITEM()
RATIONAL_B_SPLINE_SURFACE(((1.,0.796615278835171,1.),(1.,0.795896146109795,
1.),(1.,0.795193565796499,1.),(1.,0.794506502889906,1.)))
REPRESENTATION_ITEM('')
SURFACE()
);
#3576=(
BOUNDED_SURFACE()
B_SPLINE_SURFACE(3,2,((#432189,#432190,#432191),(#432192,#432193,#432194),
(#432195,#432196,#432197),(#432198,#432199,#432200)),.UNSPECIFIED.,.F.,
 .F.,.F.)
B_SPLINE_SURFACE_WITH_KNOTS((4,4),(3,3),(2.85968127239939E-5,9.24681548475815E-5),
(-0.00167900678654101,1.01130827127819),.UNSPECIFIED.)
GEOMETRIC_REPRESENTATION_ITEM()
RATIONAL_B_SPLINE_SURFACE(((1.00059040895217,0.822187541868279,1.00401468696655),
(1.0003652771814,0.889990093671582,1.0024838267339),(1.00016469515013,0.95039904225793,
1.00111990082511),(1.00025604273992,0.922888044286083,1.00174104990631)))
REPRESENTATION_ITEM('')
SURFACE()
);
#3577=(
BOUNDED_SURFACE()
B_SPLINE_SURFACE(3,2,((#432204,#432205,#432206),(#432207,#432208,#432209),
(#432210,#432211,#432212),(#432213,#432214,#432215)),.UNSPECIFIED.,.F.,
 .F.,.F.)
B_SPLINE_SURFACE_WITH_KNOTS((4,4),(3,3),(-5.22358356749296E-6,5.74594192424278E-5),
(-0.0012712005204959,1.),.UNSPECIFIED.)
GEOMETRIC_REPRESENTATION_ITEM()
RATIONAL_B_SPLINE_SURFACE(((1.00054449313172,0.785835073638773,1.),(1.00047707767473,
0.81235152635887,1.),(1.00044031788584,0.8268102165063,1.),(1.00044777653317,
0.823876514387263,1.)))
REPRESENTATION_ITEM('')
SURFACE()
);
#3578=(
BOUNDED_SURFACE()
B_SPLINE_SURFACE(3,2,((#432217,#432218,#432219),(#432220,#432221,#432222),
(#432223,#432224,#432225),(#432226,#432227,#432228)),.UNSPECIFIED.,.F.,
 .F.,.F.)
B_SPLINE_SURFACE_WITH_KNOTS((4,4),(3,3),(-3.52365706057789E-19,4.88747512969879E-5),
(-0.000215805215795982,1.),.UNSPECIFIED.)
GEOMETRIC_REPRESENTATION_ITEM()
RATIONAL_B_SPLINE_SURFACE(((1.00008915600351,0.793434085499681,1.),(1.00008930225004,
0.793095246303237,1.),(1.00008944684626,0.792760230720486,1.),(1.00008958984405,
0.792428918540534,1.)))
REPRESENTATION_ITEM('')
SURFACE()
);
#3579=(
BOUNDED_SURFACE()
B_SPLINE_SURFACE(3,2,((#432230,#432231,#432232),(#432233,#432234,#432235),
(#432236,#432237,#432238),(#432239,#432240,#432241),(#432242,#432243,#432244),
(#432245,#432246,#432247)),.UNSPECIFIED.,.F.,.F.,.F.)
B_SPLINE_SURFACE_WITH_KNOTS((4,2,4),(3,3),(5.48877349820787E-19,7.626750108632E-5,
0.000152535002172639),(0.,1.02152348203067),.UNSPECIFIED.)
GEOMETRIC_REPRESENTATION_ITEM()
RATIONAL_B_SPLINE_SURFACE(((1.,0.789033595401253,1.00908146323691),(1.,
0.857071781054832,1.00615262590428),(1.,0.922087264710739,1.00335390671592),
(1.,0.922394466502362,1.00334068261143),(1.,0.857224384599061,1.006146056785),
(1.,0.78903359540165,1.00908146323689)))
REPRESENTATION_ITEM('')
SURFACE()
);
#3580=(
BOUNDED_SURFACE()
B_SPLINE_SURFACE(3,2,((#432249,#432250,#432251),(#432252,#432253,#432254),
(#432255,#432256,#432257),(#432258,#432259,#432260)),.UNSPECIFIED.,.F.,
 .F.,.F.)
B_SPLINE_SURFACE_WITH_KNOTS((4,4),(3,3),(8.13151629364128E-20,4.88747512969884E-5),
(-0.000215489857882313,1.),.UNSPECIFIED.)
GEOMETRIC_REPRESENTATION_ITEM()
RATIONAL_B_SPLINE_SURFACE(((1.00008945889748,0.79242898398557,1.),(1.0000893161087,
0.79276029606112,1.),(1.00008917172382,0.793095311538191,1.),(1.00008902569105,
0.793434150627821,1.)))
REPRESENTATION_ITEM('')
SURFACE()
);
#3581=(
BOUNDED_SURFACE()
B_SPLINE_SURFACE(3,2,((#432262,#432263,#432264),(#432265,#432266,#432267),
(#432268,#432269,#432270),(#432271,#432272,#432273)),.UNSPECIFIED.,.F.,
 .F.,.F.)
B_SPLINE_SURFACE_WITH_KNOTS((4,4),(3,3),(-5.2197490501287E-6,5.7417239551439E-5),
(-0.00139822857770129,1.00051312364067),.UNSPECIFIED.)
GEOMETRIC_REPRESENTATION_ITEM()
RATIONAL_B_SPLINE_SURFACE(((1.00049256947255,0.823768952243992,1.00018060397849),
(1.00048448215726,0.826662424388284,1.00017763870882),(1.00052427784034,
0.812424361909331,1.00019223006921),(1.00059912365869,0.785646094632718,
1.00021967280231)))
REPRESENTATION_ITEM('')
SURFACE()
);
#3582=(
BOUNDED_SURFACE()
B_SPLINE_SURFACE(3,2,((#432277,#432278,#432279),(#432280,#432281,#432282),
(#432283,#432284,#432285),(#432286,#432287,#432288)),.UNSPECIFIED.,.F.,
 .F.,.F.)
B_SPLINE_SURFACE_WITH_KNOTS((4,4),(3,3),(3.22980774337779E-5,9.63764854872254E-5),
(-0.00154325936357871,1.01095292447542),.UNSPECIFIED.)
GEOMETRIC_REPRESENTATION_ITEM()
RATIONAL_B_SPLINE_SURFACE(((1.00023530983297,0.922925743796177,1.00168574728331),
(1.00015136166124,0.95042243959422,1.0010843469906),(1.00033574337395,0.890029368953977,
1.00240524789547),(1.00054260094216,0.822274473168365,1.00388716464858)))
REPRESENTATION_ITEM('')
SURFACE()
);
#3583=(
BOUNDED_SURFACE()
B_SPLINE_SURFACE(3,2,((#432388,#432389,#432390),(#432391,#432392,#432393),
(#432394,#432395,#432396),(#432397,#432398,#432399)),.UNSPECIFIED.,.F.,
 .F.,.F.)
B_SPLINE_SURFACE_WITH_KNOTS((4,4),(3,3),(0.,0.000101260117256738),(0.,1.),
 .UNSPECIFIED.)
GEOMETRIC_REPRESENTATION_ITEM()
RATIONAL_B_SPLINE_SURFACE(((1.,0.796615278835173,1.),(1.,0.795896038055939,
1.),(1.,0.795193354661356,1.),(1.,0.794506193185549,1.)))
REPRESENTATION_ITEM('')
SURFACE()
);
#3584=(
BOUNDED_SURFACE()
B_SPLINE_SURFACE(3,2,((#432437,#432438,#432439),(#432440,#432441,#432442),
(#432443,#432444,#432445),(#432446,#432447,#432448),(#432449,#432450,#432451),
(#432452,#432453,#432454)),.UNSPECIFIED.,.F.,.F.,.F.)
B_SPLINE_SURFACE_WITH_KNOTS((4,2,4),(3,3),(1.66018457661843E-19,1.66936432462296E-5,
3.3387286492459E-5),(0.,1.),.UNSPECIFIED.)
GEOMETRIC_REPRESENTATION_ITEM()
RATIONAL_B_SPLINE_SURFACE(((1.,0.796615278835173,1.),(1.,0.862310524418134,
1.),(1.,0.923774472010516,1.),(1.,0.923983993203428,1.),(1.,0.862574873720952,
1.),(1.,0.796615278835181,1.)))
REPRESENTATION_ITEM('')
SURFACE()
);
#3585=(
BOUNDED_SURFACE()
B_SPLINE_SURFACE(3,2,((#432491,#432492,#432493),(#432494,#432495,#432496),
(#432497,#432498,#432499),(#432500,#432501,#432502)),.UNSPECIFIED.,.F.,
 .F.,.F.)
B_SPLINE_SURFACE_WITH_KNOTS((4,4),(3,3),(0.,0.000101244905251112),(0.,1.),
 .UNSPECIFIED.)
GEOMETRIC_REPRESENTATION_ITEM()
RATIONAL_B_SPLINE_SURFACE(((1.,0.796615278835171,1.),(1.,0.795896146109787,
1.),(1.,0.795193565796506,1.),(1.,0.7945065028899,1.)))
REPRESENTATION_ITEM('')
SURFACE()
);
#3586=(
BOUNDED_SURFACE()
B_SPLINE_SURFACE(3,2,((#432538,#432539,#432540),(#432541,#432542,#432543),
(#432544,#432545,#432546),(#432547,#432548,#432549)),.UNSPECIFIED.,.F.,
 .F.,.F.)
B_SPLINE_SURFACE_WITH_KNOTS((4,4),(3,3),(2.85968127239939E-5,9.24681548475819E-5),
(-0.0016790067864535,1.01130827127836),.UNSPECIFIED.)
GEOMETRIC_REPRESENTATION_ITEM()
RATIONAL_B_SPLINE_SURFACE(((1.00059040895214,0.822187541868259,1.00401468696661),
(1.00036527718138,0.889990093671583,1.00248382673394),(1.00016469515012,
0.950399042257919,1.00111990082512),(1.00025604273991,0.922888044286074,
1.00174104990633)))
REPRESENTATION_ITEM('')
SURFACE()
);
#3587=(
BOUNDED_SURFACE()
B_SPLINE_SURFACE(3,2,((#432553,#432554,#432555),(#432556,#432557,#432558),
(#432559,#432560,#432561),(#432562,#432563,#432564)),.UNSPECIFIED.,.F.,
 .F.,.F.)
B_SPLINE_SURFACE_WITH_KNOTS((4,4),(3,3),(-5.22358356749225E-6,5.74594192424276E-5),
(-0.0012712005206289,1.),.UNSPECIFIED.)
GEOMETRIC_REPRESENTATION_ITEM()
RATIONAL_B_SPLINE_SURFACE(((1.00054449313178,0.785835073638762,1.),(1.00047707767478,
0.812351526358823,1.),(1.00044031788589,0.82681021650628,1.),(1.00044777653321,
0.82387651438725,1.)))
REPRESENTATION_ITEM('')
SURFACE()
);
#3588=(
BOUNDED_SURFACE()
B_SPLINE_SURFACE(3,2,((#432566,#432567,#432568),(#432569,#432570,#432571),
(#432572,#432573,#432574),(#432575,#432576,#432577)),.UNSPECIFIED.,.F.,
 .F.,.F.)
B_SPLINE_SURFACE_WITH_KNOTS((4,4),(3,3),(-4.87890977618477E-19,4.88747512969881E-5),
(-0.000215805215274508,1.),.UNSPECIFIED.)
GEOMETRIC_REPRESENTATION_ITEM()
RATIONAL_B_SPLINE_SURFACE(((1.00008915600329,0.793434085499789,1.),(1.00008930224983,
0.793095246303343,1.),(1.00008944684605,0.792760230720596,1.),(1.00008958984384,
0.792428918540638,1.)))
REPRESENTATION_ITEM('')
SURFACE()
);
#3589=(
BOUNDED_SURFACE()
B_SPLINE_SURFACE(3,2,((#432579,#432580,#432581),(#432582,#432583,#432584),
(#432585,#432586,#432587),(#432588,#432589,#432590),(#432591,#432592,#432593),
(#432594,#432595,#432596)),.UNSPECIFIED.,.F.,.F.,.F.)
B_SPLINE_SURFACE_WITH_KNOTS((4,2,4),(3,3),(1.01643953670516E-19,7.62675010863196E-5,
0.000152535002172639),(0.,1.02152348203063),.UNSPECIFIED.)
GEOMETRIC_REPRESENTATION_ITEM()
RATIONAL_B_SPLINE_SURFACE(((1.,0.789033595401257,1.0090814632369),(1.,0.857071781054861,
1.00615262590427),(1.,0.922087264710712,1.00335390671591),(1.,0.922394466502399,
1.00334068261143),(1.,0.857224384599035,1.00614605678499),(1.,0.789033595401663,
1.00908146323688)))
REPRESENTATION_ITEM('')
SURFACE()
);
#3590=(
BOUNDED_SURFACE()
B_SPLINE_SURFACE(3,2,((#432598,#432599,#432600),(#432601,#432602,#432603),
(#432604,#432605,#432606),(#432607,#432608,#432609)),.UNSPECIFIED.,.F.,
 .F.,.F.)
B_SPLINE_SURFACE_WITH_KNOTS((4,4),(3,3),(6.50521303491303E-19,4.88747512969886E-5),
(-0.000215489856880668,1.),.UNSPECIFIED.)
GEOMETRIC_REPRESENTATION_ITEM()
RATIONAL_B_SPLINE_SURFACE(((1.00008945889707,0.792428983985776,1.),(1.00008931610828,
0.792760296061328,1.),(1.00008917172341,0.79309531153839,1.),(1.00008902569064,
0.793434150628027,1.)))
REPRESENTATION_ITEM('')
SURFACE()
);
#3591=(
BOUNDED_SURFACE()
B_SPLINE_SURFACE(3,2,((#432611,#432612,#432613),(#432614,#432615,#432616),
(#432617,#432618,#432619),(#432620,#432621,#432622)),.UNSPECIFIED.,.F.,
 .F.,.F.)
B_SPLINE_SURFACE_WITH_KNOTS((4,4),(3,3),(-5.21974905013085E-6,5.74172395514398E-5),
(-0.00139822857786748,1.00051312364076),.UNSPECIFIED.)
GEOMETRIC_REPRESENTATION_ITEM()
RATIONAL_B_SPLINE_SURFACE(((1.00049256947261,0.823768952243938,1.00018060397853),
(1.00048448215732,0.826662424388239,1.00017763870885),(1.0005242778404,
0.812424361909295,1.00019223006925),(1.00059912365876,0.785646094632659,
1.00021967280235)))
REPRESENTATION_ITEM('')
SURFACE()
);
#3592=(
BOUNDED_SURFACE()
B_SPLINE_SURFACE(3,2,((#432626,#432627,#432628),(#432629,#432630,#432631),
(#432632,#432633,#432634),(#432635,#432636,#432637)),.UNSPECIFIED.,.F.,
 .F.,.F.)
B_SPLINE_SURFACE_WITH_KNOTS((4,4),(3,3),(3.22980774337778E-5,9.63764854872252E-5),
(-0.00154325936321,1.01095292447555),.UNSPECIFIED.)
GEOMETRIC_REPRESENTATION_ITEM()
RATIONAL_B_SPLINE_SURFACE(((1.00023530983291,0.922925743796198,1.00168574728333),
(1.0001513616612,0.950422439594237,1.00108434699061),(1.00033574337387,
0.890029368953991,1.0024052478955),(1.00054260094203,0.822274473168418,
1.00388716464862)))
REPRESENTATION_ITEM('')
SURFACE()
);
#3593=(
BOUNDED_SURFACE()
B_SPLINE_SURFACE(3,2,((#432737,#432738,#432739),(#432740,#432741,#432742),
(#432743,#432744,#432745),(#432746,#432747,#432748)),.UNSPECIFIED.,.F.,
 .F.,.F.)
B_SPLINE_SURFACE_WITH_KNOTS((4,4),(3,3),(0.,0.000101260117256737),(0.,1.),
 .UNSPECIFIED.)
GEOMETRIC_REPRESENTATION_ITEM()
RATIONAL_B_SPLINE_SURFACE(((1.,0.796615278835169,1.),(1.,0.795896038055939,
1.),(1.,0.795193354661348,1.),(1.,0.794506193185533,1.)))
REPRESENTATION_ITEM('')
SURFACE()
);
#3594=(
BOUNDED_SURFACE()
B_SPLINE_SURFACE(3,2,((#432786,#432787,#432788),(#432789,#432790,#432791),
(#432792,#432793,#432794),(#432795,#432796,#432797),(#432798,#432799,#432800),
(#432801,#432802,#432803)),.UNSPECIFIED.,.F.,.F.,.F.)
B_SPLINE_SURFACE_WITH_KNOTS((4,2,4),(3,3),(1.16890546721093E-19,1.66936432462296E-5,
3.33872864924591E-5),(0.,1.),.UNSPECIFIED.)
GEOMETRIC_REPRESENTATION_ITEM()
RATIONAL_B_SPLINE_SURFACE(((1.,0.796615278835178,1.),(1.,0.86231052441814,
1.),(1.,0.923774472010522,1.),(1.,0.923983993203428,1.),(1.,0.862574873720943,
1.),(1.,0.796615278835182,1.)))
REPRESENTATION_ITEM('')
SURFACE()
);
#3595=(
BOUNDED_SURFACE()
B_SPLINE_SURFACE(3,2,((#432840,#432841,#432842),(#432843,#432844,#432845),
(#432846,#432847,#432848),(#432849,#432850,#432851)),.UNSPECIFIED.,.F.,
 .F.,.F.)
B_SPLINE_SURFACE_WITH_KNOTS((4,4),(3,3),(0.,0.000101244905251112),(0.,1.),
 .UNSPECIFIED.)
GEOMETRIC_REPRESENTATION_ITEM()
RATIONAL_B_SPLINE_SURFACE(((1.,0.79661527883517,1.),(1.,0.795896146109795,
1.),(1.,0.795193565796498,1.),(1.,0.794506502889894,1.)))
REPRESENTATION_ITEM('')
SURFACE()
);
#3596=(
BOUNDED_SURFACE()
B_SPLINE_SURFACE(3,2,((#432887,#432888,#432889),(#432890,#432891,#432892),
(#432893,#432894,#432895),(#432896,#432897,#432898)),.UNSPECIFIED.,.F.,
 .F.,.F.)
B_SPLINE_SURFACE_WITH_KNOTS((4,4),(3,3),(2.85968127239939E-5,9.24681548475817E-5),
(-0.00167900678641286,1.0113082712782),.UNSPECIFIED.)
GEOMETRIC_REPRESENTATION_ITEM()
RATIONAL_B_SPLINE_SURFACE(((1.00059040895212,0.82218754186829,1.00401468696656),
(1.00036527718137,0.889990093671602,1.00248382673391),(1.00016469515012,
0.95039904225793,1.00111990082511),(1.0002560427399,0.922888044286091,1.00174104990631)))
REPRESENTATION_ITEM('')
SURFACE()
);
#3597=(
BOUNDED_SURFACE()
B_SPLINE_SURFACE(3,2,((#432902,#432903,#432904),(#432905,#432906,#432907),
(#432908,#432909,#432910),(#432911,#432912,#432913)),.UNSPECIFIED.,.F.,
 .F.,.F.)
B_SPLINE_SURFACE_WITH_KNOTS((4,4),(3,3),(-5.22358356749071E-6,5.74594192424274E-5),
(-0.00127120052062342,1.),.UNSPECIFIED.)
GEOMETRIC_REPRESENTATION_ITEM()
RATIONAL_B_SPLINE_SURFACE(((1.00054449313178,0.785835073638754,0.999999999999999),
(1.00047707767477,0.812351526358836,1.),(1.00044031788589,0.826810216506263,
1.),(1.00044777653321,0.823876514387245,1.)))
REPRESENTATION_ITEM('')
SURFACE()
);
#3598=(
BOUNDED_SURFACE()
B_SPLINE_SURFACE(3,2,((#432915,#432916,#432917),(#432918,#432919,#432920),
(#432921,#432922,#432923),(#432924,#432925,#432926)),.UNSPECIFIED.,.F.,
 .F.,.F.)
B_SPLINE_SURFACE_WITH_KNOTS((4,4),(3,3),(5.42101086242752E-20,4.88747512969879E-5),
(-0.000215805215510756,1.),.UNSPECIFIED.)
GEOMETRIC_REPRESENTATION_ITEM()
RATIONAL_B_SPLINE_SURFACE(((1.00008915600339,0.793434085499737,1.),(1.00008930224992,
0.793095246303276,1.),(1.00008944684614,0.792760230720552,1.),(1.00008958984394,
0.792428918540586,1.)))
REPRESENTATION_ITEM('')
SURFACE()
);
#3599=(
BOUNDED_SURFACE()
B_SPLINE_SURFACE(3,2,((#432928,#432929,#432930),(#432931,#432932,#432933),
(#432934,#432935,#432936),(#432937,#432938,#432939),(#432940,#432941,#432942),
(#432943,#432944,#432945)),.UNSPECIFIED.,.F.,.F.,.F.)
B_SPLINE_SURFACE_WITH_KNOTS((4,2,4),(3,3),(2.16840434497101E-19,7.62675010863198E-5,
0.000152535002172639),(0.,1.02152348203062),.UNSPECIFIED.)
GEOMETRIC_REPRESENTATION_ITEM()
RATIONAL_B_SPLINE_SURFACE(((1.,0.789033595401261,1.00908146323689),(1.,
0.857071781054845,1.00615262590427),(1.,0.922087264710742,1.00335390671591),
(1.,0.922394466502365,1.00334068261143),(1.,0.85722438459908,1.00614605678498),
(1.,0.789033595401654,1.00908146323687)))
REPRESENTATION_ITEM('')
SURFACE()
);
#3600=(
BOUNDED_SURFACE()
B_SPLINE_SURFACE(3,2,((#432947,#432948,#432949),(#432950,#432951,#432952),
(#432953,#432954,#432955),(#432956,#432957,#432958)),.UNSPECIFIED.,.F.,
 .F.,.F.)
B_SPLINE_SURFACE_WITH_KNOTS((4,4),(3,3),(5.14996031930615E-19,4.88747512969884E-5),
(-0.00021548985705842,1.),.UNSPECIFIED.)
GEOMETRIC_REPRESENTATION_ITEM()
RATIONAL_B_SPLINE_SURFACE(((1.00008945889714,0.792428983985738,1.),(1.00008931610836,
0.792760296061292,1.),(1.00008917172348,0.79309531153835,1.),(1.00008902569071,
0.793434150627988,1.)))
REPRESENTATION_ITEM('')
SURFACE()
);
#3601=(
BOUNDED_SURFACE()
B_SPLINE_SURFACE(3,2,((#432960,#432961,#432962),(#432963,#432964,#432965),
(#432966,#432967,#432968),(#432969,#432970,#432971)),.UNSPECIFIED.,.F.,
 .F.,.F.)
B_SPLINE_SURFACE_WITH_KNOTS((4,4),(3,3),(-5.21974905013084E-6,5.74172395514398E-5),
(-0.00139822857740927,1.00051312364064),.UNSPECIFIED.)
GEOMETRIC_REPRESENTATION_ITEM()
RATIONAL_B_SPLINE_SURFACE(((1.00049256947245,0.823768952244038,1.00018060397848),
(1.00048448215716,0.826662424388339,1.00017763870881),(1.00052427784023,
0.812424361909396,1.0001922300692),(1.00059912365856,0.78564609463279,1.0002196728023)))
REPRESENTATION_ITEM('')
SURFACE()
);
#3602=(
BOUNDED_SURFACE()
B_SPLINE_SURFACE(3,2,((#432975,#432976,#432977),(#432978,#432979,#432980),
(#432981,#432982,#432983),(#432984,#432985,#432986)),.UNSPECIFIED.,.F.,
 .F.,.F.)
B_SPLINE_SURFACE_WITH_KNOTS((4,4),(3,3),(3.2298077433778E-5,9.63764854872257E-5),
(-0.00154325936370795,1.01095292447541),.UNSPECIFIED.)
GEOMETRIC_REPRESENTATION_ITEM()
RATIONAL_B_SPLINE_SURFACE(((1.00023530983298,0.922925743796168,1.00168574728331),
(1.00015136166125,0.950422439594218,1.0010843469906),(1.00033574337398,
0.890029368953962,1.00240524789547),(1.0005426009422,0.822274473168342,
1.00388716464857)))
REPRESENTATION_ITEM('')
SURFACE()
);
#3603=(
BOUNDED_SURFACE()
B_SPLINE_SURFACE(3,2,((#433086,#433087,#433088),(#433089,#433090,#433091),
(#433092,#433093,#433094),(#433095,#433096,#433097)),.UNSPECIFIED.,.F.,
 .F.,.F.)
B_SPLINE_SURFACE_WITH_KNOTS((4,4),(3,3),(0.,0.000101260117256738),(0.,1.),
 .UNSPECIFIED.)
GEOMETRIC_REPRESENTATION_ITEM()
RATIONAL_B_SPLINE_SURFACE(((1.,0.79661527883517,1.),(1.,0.795896038055932,
1.),(1.,0.795193354661351,1.),(1.,0.794506193185546,1.)))
REPRESENTATION_ITEM('')
SURFACE()
);
#3604=(
BOUNDED_SURFACE()
B_SPLINE_SURFACE(3,2,((#433135,#433136,#433137),(#433138,#433139,#433140),
(#433141,#433142,#433143),(#433144,#433145,#433146),(#433147,#433148,#433149),
(#433150,#433151,#433152)),.UNSPECIFIED.,.F.,.F.,.F.)
B_SPLINE_SURFACE_WITH_KNOTS((4,2,4),(3,3),(-5.0821976835258E-20,1.66936432462296E-5,
3.33872864924593E-5),(0.,1.),.UNSPECIFIED.)
GEOMETRIC_REPRESENTATION_ITEM()
RATIONAL_B_SPLINE_SURFACE(((1.,0.796615278835167,1.),(1.,0.862310524418131,
1.),(1.,0.92377447201052,1.),(1.,0.923983993203425,1.),(1.,0.862574873720948,
1.),(1.,0.796615278835171,1.)))
REPRESENTATION_ITEM('')
SURFACE()
);
#3605=(
BOUNDED_SURFACE()
B_SPLINE_SURFACE(3,2,((#433189,#433190,#433191),(#433192,#433193,#433194),
(#433195,#433196,#433197),(#433198,#433199,#433200)),.UNSPECIFIED.,.F.,
 .F.,.F.)
B_SPLINE_SURFACE_WITH_KNOTS((4,4),(3,3),(0.,0.000101244905251112),(0.,1.),
 .UNSPECIFIED.)
GEOMETRIC_REPRESENTATION_ITEM()
RATIONAL_B_SPLINE_SURFACE(((1.,0.796615278835171,1.),(1.,0.795896146109791,
1.),(1.,0.7951935657965,1.),(1.,0.794506502889901,1.)))
REPRESENTATION_ITEM('')
SURFACE()
);
#3606=(
BOUNDED_SURFACE()
B_SPLINE_SURFACE(3,2,((#433236,#433237,#433238),(#433239,#433240,#433241),
(#433242,#433243,#433244),(#433245,#433246,#433247)),.UNSPECIFIED.,.F.,
 .F.,.F.)
B_SPLINE_SURFACE_WITH_KNOTS((4,4),(3,3),(2.85968127239939E-5,9.24681548475817E-5),
(-0.00167900678782365,1.01130827127822),.UNSPECIFIED.)
GEOMETRIC_REPRESENTATION_ITEM()
RATIONAL_B_SPLINE_SURFACE(((1.00059040895262,0.82218754186804,1.00401468696657),
(1.00036527718167,0.889990093671435,1.00248382673391),(1.00016469515026,
0.950399042257868,1.00111990082511),(1.00025604274012,0.92288804428598,
1.00174104990631)))
REPRESENTATION_ITEM('')
SURFACE()
);
#3607=(
BOUNDED_SURFACE()
B_SPLINE_SURFACE(3,2,((#433251,#433252,#433253),(#433254,#433255,#433256),
(#433257,#433258,#433259),(#433260,#433261,#433262)),.UNSPECIFIED.,.F.,
 .F.,.F.)
B_SPLINE_SURFACE_WITH_KNOTS((4,4),(3,3),(-5.22358356749241E-6,5.74594192424278E-5),
(-0.00127120052040753,1.),.UNSPECIFIED.)
GEOMETRIC_REPRESENTATION_ITEM()
RATIONAL_B_SPLINE_SURFACE(((1.00054449313169,0.785835073638789,1.),(1.00047707767469,
0.812351526358887,1.),(1.00044031788581,0.826810216506305,1.),(1.00044777653313,
0.823876514387289,1.)))
REPRESENTATION_ITEM('')
SURFACE()
);
#3608=(
BOUNDED_SURFACE()
B_SPLINE_SURFACE(3,2,((#433264,#433265,#433266),(#433267,#433268,#433269),
(#433270,#433271,#433272),(#433273,#433274,#433275)),.UNSPECIFIED.,.F.,
 .F.,.F.)
B_SPLINE_SURFACE_WITH_KNOTS((4,4),(3,3),(0.,4.88747512969878E-5),(-0.000215805215457177,
1.),.UNSPECIFIED.)
GEOMETRIC_REPRESENTATION_ITEM()
RATIONAL_B_SPLINE_SURFACE(((1.00008915600337,0.793434085499749,1.),(1.0000893022499,
0.793095246303283,1.),(1.00008944684612,0.792760230720569,1.),(1.00008958984391,
0.792428918540598,1.)))
REPRESENTATION_ITEM('')
SURFACE()
);
#3609=(
BOUNDED_SURFACE()
B_SPLINE_SURFACE(3,2,((#433277,#433278,#433279),(#433280,#433281,#433282),
(#433283,#433284,#433285),(#433286,#433287,#433288),(#433289,#433290,#433291),
(#433292,#433293,#433294)),.UNSPECIFIED.,.F.,.F.,.F.)
B_SPLINE_SURFACE_WITH_KNOTS((4,2,4),(3,3),(2.23616698075135E-19,7.62675010863198E-5,
0.000152535002172639),(0.,1.02152348203061),.UNSPECIFIED.)
GEOMETRIC_REPRESENTATION_ITEM()
RATIONAL_B_SPLINE_SURFACE(((1.,0.789033595401263,1.00908146323688),(1.,
0.857071781054884,1.00615262590426),(1.,0.922087264710692,1.00335390671591),
(1.,0.92239446650242,1.00334068261142),(1.,0.85722438459903,1.00614605678498),
(1.,0.789033595401661,1.00908146323687)))
REPRESENTATION_ITEM('')
SURFACE()
);
#3610=(
BOUNDED_SURFACE()
B_SPLINE_SURFACE(3,2,((#433296,#433297,#433298),(#433299,#433300,#433301),
(#433302,#433303,#433304),(#433305,#433306,#433307)),.UNSPECIFIED.,.F.,
 .F.,.F.)
B_SPLINE_SURFACE_WITH_KNOTS((4,4),(3,3),(3.79470760369927E-19,4.88747512969884E-5),
(-0.000215489857563226,1.),.UNSPECIFIED.)
GEOMETRIC_REPRESENTATION_ITEM()
RATIONAL_B_SPLINE_SURFACE(((1.00008945889735,0.792428983985636,1.),(1.00008931610857,
0.792760296061186,1.),(1.00008917172369,0.793095311538252,1.),(1.00008902569092,
0.793434150627887,1.)))
REPRESENTATION_ITEM('')
SURFACE()
);
#3611=(
BOUNDED_SURFACE()
B_SPLINE_SURFACE(3,2,((#433309,#433310,#433311),(#433312,#433313,#433314),
(#433315,#433316,#433317),(#433318,#433319,#433320)),.UNSPECIFIED.,.F.,
 .F.,.F.)
B_SPLINE_SURFACE_WITH_KNOTS((4,4),(3,3),(-5.2197490501308E-6,5.74172395514396E-5),
(-0.0013982285777185,1.00051312364079),.UNSPECIFIED.)
GEOMETRIC_REPRESENTATION_ITEM()
RATIONAL_B_SPLINE_SURFACE(((1.00049256947256,0.823768952243963,1.00018060397854),
(1.00048448215726,0.826662424388248,1.00017763870886),(1.00052427784034,
0.812424361909325,1.00019223006926),(1.0005991236587,0.785646094632683,
1.00021967280236)))
REPRESENTATION_ITEM('')
SURFACE()
);
#3612=(
BOUNDED_SURFACE()
B_SPLINE_SURFACE(3,2,((#433324,#433325,#433326),(#433327,#433328,#433329),
(#433330,#433331,#433332),(#433333,#433334,#433335)),.UNSPECIFIED.,.F.,
 .F.,.F.)
B_SPLINE_SURFACE_WITH_KNOTS((4,4),(3,3),(3.22980774337779E-5,9.63764854872253E-5),
(-0.00154325936394338,1.01095292447531),.UNSPECIFIED.)
GEOMETRIC_REPRESENTATION_ITEM()
RATIONAL_B_SPLINE_SURFACE(((1.00023530983302,0.922925743796155,1.00168574728329),
(1.00015136166128,0.950422439594212,1.00108434699059),(1.00033574337403,
0.890029368953942,1.00240524789545),(1.00054260094229,0.822274473168318,
1.00388716464854)))
REPRESENTATION_ITEM('')
SURFACE()
);
#3613=(
BOUNDED_SURFACE()
B_SPLINE_SURFACE(3,2,((#433435,#433436,#433437),(#433438,#433439,#433440),
(#433441,#433442,#433443),(#433444,#433445,#433446)),.UNSPECIFIED.,.F.,
 .F.,.F.)
B_SPLINE_SURFACE_WITH_KNOTS((4,4),(3,3),(-2.16840434497101E-19,0.000101260117256738),
(0.,1.),.UNSPECIFIED.)
GEOMETRIC_REPRESENTATION_ITEM()
RATIONAL_B_SPLINE_SURFACE(((1.,0.796615278835171,1.),(1.,0.795896038055945,
1.),(1.,0.795193354661344,1.),(1.,0.794506193185546,1.)))
REPRESENTATION_ITEM('')
SURFACE()
);
#3614=(
BOUNDED_SURFACE()
B_SPLINE_SURFACE(3,2,((#433484,#433485,#433486),(#433487,#433488,#433489),
(#433490,#433491,#433492),(#433493,#433494,#433495),(#433496,#433497,#433498),
(#433499,#433500,#433501)),.UNSPECIFIED.,.F.,.F.,.F.)
B_SPLINE_SURFACE_WITH_KNOTS((4,2,4),(3,3),(1.91429446079472E-19,1.66936432462294E-5,
3.33872864924587E-5),(0.,1.),.UNSPECIFIED.)
GEOMETRIC_REPRESENTATION_ITEM()
RATIONAL_B_SPLINE_SURFACE(((1.,0.79661527883518,1.),(1.,0.862310524418121,
1.),(1.,0.923774472010515,1.),(1.,0.92398399320343,1.),(1.,0.862574873720946,
1.),(1.,0.79661527883519,1.)))
REPRESENTATION_ITEM('')
SURFACE()
);
#3615=(
BOUNDED_SURFACE()
B_SPLINE_SURFACE(3,2,((#433538,#433539,#433540),(#433541,#433542,#433543),
(#433544,#433545,#433546),(#433547,#433548,#433549)),.UNSPECIFIED.,.F.,
 .F.,.F.)
B_SPLINE_SURFACE_WITH_KNOTS((4,4),(3,3),(0.,0.000101244905251112),(0.,1.),
 .UNSPECIFIED.)
GEOMETRIC_REPRESENTATION_ITEM()
RATIONAL_B_SPLINE_SURFACE(((1.,0.796615278835175,1.),(1.,0.795896146109785,
1.),(1.,0.795193565796504,1.),(1.,0.794506502889899,1.)))
REPRESENTATION_ITEM('')
SURFACE()
);
#3616=(
BOUNDED_SURFACE()
B_SPLINE_SURFACE(3,2,((#433585,#433586,#433587),(#433588,#433589,#433590),
(#433591,#433592,#433593),(#433594,#433595,#433596)),.UNSPECIFIED.,.F.,
 .F.,.F.)
B_SPLINE_SURFACE_WITH_KNOTS((4,4),(3,3),(2.85968127239939E-5,9.24681548475817E-5),
(-0.0016790067866049,1.01130827127825),.UNSPECIFIED.)
GEOMETRIC_REPRESENTATION_ITEM()
RATIONAL_B_SPLINE_SURFACE(((1.00059040895219,0.822187541868252,1.00401468696658),
(1.00036527718141,0.889990093671559,1.00248382673392),(1.00016469515014,
0.950399042257932,1.00111990082511),(1.00025604273993,0.922888044286072,
1.00174104990632)))
REPRESENTATION_ITEM('')
SURFACE()
);
#3617=(
BOUNDED_SURFACE()
B_SPLINE_SURFACE(3,2,((#433600,#433601,#433602),(#433603,#433604,#433605),
(#433606,#433607,#433608),(#433609,#433610,#433611)),.UNSPECIFIED.,.F.,
 .F.,.F.)
B_SPLINE_SURFACE_WITH_KNOTS((4,4),(3,3),(-5.22358356749298E-6,5.74594192424276E-5),
(-0.00127120052069362,1.),.UNSPECIFIED.)
GEOMETRIC_REPRESENTATION_ITEM()
RATIONAL_B_SPLINE_SURFACE(((1.00054449313181,0.785835073638747,1.),(1.0004770776748,
0.812351526358807,1.),(1.00044031788591,0.826810216506271,1.),(1.00044777653323,
0.823876514387229,1.)))
REPRESENTATION_ITEM('')
SURFACE()
);
#3618=(
BOUNDED_SURFACE()
B_SPLINE_SURFACE(3,2,((#433613,#433614,#433615),(#433616,#433617,#433618),
(#433619,#433620,#433621),(#433622,#433623,#433624)),.UNSPECIFIED.,.F.,
 .F.,.F.)
B_SPLINE_SURFACE_WITH_KNOTS((4,4),(3,3),(-5.42101086242752E-20,4.88747512969882E-5),
(-0.000215805215169258,1.),.UNSPECIFIED.)
GEOMETRIC_REPRESENTATION_ITEM()
RATIONAL_B_SPLINE_SURFACE(((1.00008915600325,0.793434085499808,1.),(1.00008930224978,
0.793095246303361,1.),(1.000089446846,0.792760230720617,1.),(1.00008958984379,
0.792428918540663,1.)))
REPRESENTATION_ITEM('')
SURFACE()
);
#3619=(
BOUNDED_SURFACE()
B_SPLINE_SURFACE(3,2,((#433626,#433627,#433628),(#433629,#433630,#433631),
(#433632,#433633,#433634),(#433635,#433636,#433637),(#433638,#433639,#433640),
(#433641,#433642,#433643)),.UNSPECIFIED.,.F.,.F.,.F.)
B_SPLINE_SURFACE_WITH_KNOTS((4,2,4),(3,3),(2.84603070277445E-19,7.62675010863197E-5,
0.000152535002172639),(0.,1.02152348203073),.UNSPECIFIED.)
GEOMETRIC_REPRESENTATION_ITEM()
RATIONAL_B_SPLINE_SURFACE(((1.,0.78903359540124,1.00908146323694),(1.,0.857071781054861,
1.0061526259043),(1.,0.922087264710688,1.00335390671593),(1.,0.922394466502408,
1.00334068261144),(1.,0.857224384599018,1.00614605678502),(1.,0.789033595401641,
1.00908146323692)))
REPRESENTATION_ITEM('')
SURFACE()
);
#3620=(
BOUNDED_SURFACE()
B_SPLINE_SURFACE(3,2,((#433645,#433646,#433647),(#433648,#433649,#433650),
(#433651,#433652,#433653),(#433654,#433655,#433656)),.UNSPECIFIED.,.F.,
 .F.,.F.)
B_SPLINE_SURFACE_WITH_KNOTS((4,4),(3,3),(4.87890977618477E-19,4.88747512969886E-5),
(-0.000215489857113495,1.),.UNSPECIFIED.)
GEOMETRIC_REPRESENTATION_ITEM()
RATIONAL_B_SPLINE_SURFACE(((1.00008945889716,0.792428983985728,1.),(1.00008931610838,
0.792760296061271,1.),(1.00008917172351,0.793095311538354,1.),(1.00008902569073,
0.793434150627978,1.)))
REPRESENTATION_ITEM('')
SURFACE()
);
#3621=(
BOUNDED_SURFACE()
B_SPLINE_SURFACE(3,2,((#433658,#433659,#433660),(#433661,#433662,#433663),
(#433664,#433665,#433666),(#433667,#433668,#433669)),.UNSPECIFIED.,.F.,
 .F.,.F.)
B_SPLINE_SURFACE_WITH_KNOTS((4,4),(3,3),(-5.2197490501309E-6,5.74172395514392E-5),
(-0.00139822857766469,1.0005131236408),.UNSPECIFIED.)
GEOMETRIC_REPRESENTATION_ITEM()
RATIONAL_B_SPLINE_SURFACE(((1.00049256947254,0.823768952243971,1.00018060397854),
(1.00048448215724,0.826662424388243,1.00017763870887),(1.00052427784032,
0.812424361909343,1.00019223006926),(1.00059912365867,0.785646094632688,
1.00021967280237)))
REPRESENTATION_ITEM('')
SURFACE()
);
#3622=(
BOUNDED_SURFACE()
B_SPLINE_SURFACE(3,2,((#433673,#433674,#433675),(#433676,#433677,#433678),
(#433679,#433680,#433681),(#433682,#433683,#433684)),.UNSPECIFIED.,.F.,
 .F.,.F.)
B_SPLINE_SURFACE_WITH_KNOTS((4,4),(3,3),(3.2298077433778E-5,9.63764854872256E-5),
(-0.00154325936361246,1.01095292447532),.UNSPECIFIED.)
GEOMETRIC_REPRESENTATION_ITEM()
RATIONAL_B_SPLINE_SURFACE(((1.00023530983297,0.922925743796182,1.00168574728329),
(1.00015136166124,0.95042243959422,1.00108434699059),(1.00033574337396,
0.890029368953983,1.00240524789545),(1.00054260094217,0.822274473168379,
1.00388716464854)))
REPRESENTATION_ITEM('')
SURFACE()
);
#3623=(
BOUNDED_SURFACE()
B_SPLINE_SURFACE(3,2,((#433784,#433785,#433786),(#433787,#433788,#433789),
(#433790,#433791,#433792),(#433793,#433794,#433795)),.UNSPECIFIED.,.F.,
 .F.,.F.)
B_SPLINE_SURFACE_WITH_KNOTS((4,4),(3,3),(-2.16840434497101E-19,0.000101260117256737),
(0.,1.),.UNSPECIFIED.)
GEOMETRIC_REPRESENTATION_ITEM()
RATIONAL_B_SPLINE_SURFACE(((1.,0.796615278835167,1.),(1.,0.795896038055936,
1.),(1.,0.79519335466135,1.),(1.,0.794506193185548,1.)))
REPRESENTATION_ITEM('')
SURFACE()
);
#3624=(
BOUNDED_SURFACE()
B_SPLINE_SURFACE(3,2,((#433833,#433834,#433835),(#433836,#433837,#433838),
(#433839,#433840,#433841),(#433842,#433843,#433844),(#433845,#433846,#433847),
(#433848,#433849,#433850)),.UNSPECIFIED.,.F.,.F.,.F.)
B_SPLINE_SURFACE_WITH_KNOTS((4,2,4),(3,3),(1.71100655345369E-19,1.66936432462295E-5,
3.33872864924587E-5),(0.,1.),.UNSPECIFIED.)
GEOMETRIC_REPRESENTATION_ITEM()
RATIONAL_B_SPLINE_SURFACE(((1.,0.79661527883518,1.),(1.,0.862310524418124,
1.),(1.,0.923774472010515,1.),(1.,0.92398399320343,1.),(1.,0.862574873720945,
1.),(1.,0.796615278835185,1.)))
REPRESENTATION_ITEM('')
SURFACE()
);
#3625=(
BOUNDED_SURFACE()
B_SPLINE_SURFACE(3,2,((#433887,#433888,#433889),(#433890,#433891,#433892),
(#433893,#433894,#433895),(#433896,#433897,#433898)),.UNSPECIFIED.,.F.,
 .F.,.F.)
B_SPLINE_SURFACE_WITH_KNOTS((4,4),(3,3),(-2.16840434497101E-19,0.000101244905251112),
(0.,1.),.UNSPECIFIED.)
GEOMETRIC_REPRESENTATION_ITEM()
RATIONAL_B_SPLINE_SURFACE(((1.,0.796615278835175,1.),(1.,0.795896146109793,
1.),(1.,0.795193565796495,1.),(1.,0.794506502889905,1.)))
REPRESENTATION_ITEM('')
SURFACE()
);
#3626=(
BOUNDED_SURFACE()
B_SPLINE_SURFACE(3,2,((#433934,#433935,#433936),(#433937,#433938,#433939),
(#433940,#433941,#433942),(#433943,#433944,#433945)),.UNSPECIFIED.,.F.,
 .F.,.F.)
B_SPLINE_SURFACE_WITH_KNOTS((4,4),(3,3),(2.85968127239939E-5,9.24681548475817E-5),
(-0.00167900678794363,1.01130827127821),.UNSPECIFIED.)
GEOMETRIC_REPRESENTATION_ITEM()
RATIONAL_B_SPLINE_SURFACE(((1.00059040895266,0.822187541868021,1.00401468696656),
(1.0003652771817,0.889990093671417,1.00248382673391),(1.00016469515027,
0.950399042257861,1.00111990082511),(1.00025604274014,0.922888044285972,
1.00174104990631)))
REPRESENTATION_ITEM('')
SURFACE()
);
#3627=(
BOUNDED_SURFACE()
B_SPLINE_SURFACE(3,2,((#433949,#433950,#433951),(#433952,#433953,#433954),
(#433955,#433956,#433957),(#433958,#433959,#433960)),.UNSPECIFIED.,.F.,
 .F.,.F.)
B_SPLINE_SURFACE_WITH_KNOTS((4,4),(3,3),(-5.22358356749302E-6,5.74594192424276E-5),
(-0.00127120052052642,1.),.UNSPECIFIED.)
GEOMETRIC_REPRESENTATION_ITEM()
RATIONAL_B_SPLINE_SURFACE(((1.00054449313174,0.785835073638765,1.),(1.00047707767474,
0.812351526358866,1.),(1.00044031788585,0.826810216506294,1.),(1.00044777653318,
0.823876514387261,1.)))
REPRESENTATION_ITEM('')
SURFACE()
);
#3628=(
BOUNDED_SURFACE()
B_SPLINE_SURFACE(3,2,((#433962,#433963,#433964),(#433965,#433966,#433967),
(#433968,#433969,#433970),(#433971,#433972,#433973)),.UNSPECIFIED.,.F.,
 .F.,.F.)
B_SPLINE_SURFACE_WITH_KNOTS((4,4),(3,3),(-8.13151629364128E-20,4.88747512969878E-5),
(-0.000215805215605584,1.),.UNSPECIFIED.)
GEOMETRIC_REPRESENTATION_ITEM()
RATIONAL_B_SPLINE_SURFACE(((1.00008915600343,0.793434085499714,1.),(1.00008930224996,
0.793095246303281,1.),(1.00008944684618,0.792760230720533,1.),(1.00008958984398,
0.792428918540569,1.)))
REPRESENTATION_ITEM('')
SURFACE()
);
#3629=(
BOUNDED_SURFACE()
B_SPLINE_SURFACE(3,2,((#433975,#433976,#433977),(#433978,#433979,#433980),
(#433981,#433982,#433983),(#433984,#433985,#433986),(#433987,#433988,#433989),
(#433990,#433991,#433992)),.UNSPECIFIED.,.F.,.F.,.F.)
B_SPLINE_SURFACE_WITH_KNOTS((4,2,4),(3,3),(6.7762635780344E-20,7.62675010863195E-5,
0.000152535002172639),(0.,1.02152348203066),.UNSPECIFIED.)
GEOMETRIC_REPRESENTATION_ITEM()
RATIONAL_B_SPLINE_SURFACE(((1.,0.789033595401255,1.00908146323691),(1.,
0.857071781054837,1.00615262590428),(1.,0.922087264710733,1.00335390671592),
(1.,0.92239446650238,1.00334068261143),(1.,0.857224384599051,1.006146056785),
(1.,0.789033595401652,1.00908146323689)))
REPRESENTATION_ITEM('')
SURFACE()
);
#3630=(
BOUNDED_SURFACE()
B_SPLINE_SURFACE(3,2,((#433994,#433995,#433996),(#433997,#433998,#433999),
(#434000,#434001,#434002),(#434003,#434004,#434005)),.UNSPECIFIED.,.F.,
 .F.,.F.)
B_SPLINE_SURFACE_WITH_KNOTS((4,4),(3,3),(6.50521303491303E-19,4.88747512969884E-5),
(-0.000215489857064291,1.),.UNSPECIFIED.)
GEOMETRIC_REPRESENTATION_ITEM()
RATIONAL_B_SPLINE_SURFACE(((1.00008945889714,0.792428983985734,1.),(1.00008931610836,
0.792760296061303,1.),(1.00008917172349,0.793095311538351,1.),(1.00008902569071,
0.79343415062799,1.)))
REPRESENTATION_ITEM('')
SURFACE()
);
#3631=(
BOUNDED_SURFACE()
B_SPLINE_SURFACE(3,2,((#434007,#434008,#434009),(#434010,#434011,#434012),
(#434013,#434014,#434015),(#434016,#434017,#434018)),.UNSPECIFIED.,.F.,
 .F.,.F.)
B_SPLINE_SURFACE_WITH_KNOTS((4,4),(3,3),(-5.21974905012868E-6,5.74172395514399E-5),
(-0.00139822857733951,1.00051312364071),.UNSPECIFIED.)
GEOMETRIC_REPRESENTATION_ITEM()
RATIONAL_B_SPLINE_SURFACE(((1.00049256947243,0.823768952244043,1.00018060397851),
(1.00048448215713,0.826662424388329,1.00017763870884),(1.0005242778402,
0.812424361909413,1.00019223006923),(1.00059912365854,0.78564609463278,
1.00021967280233)))
REPRESENTATION_ITEM('')
SURFACE()
);
#3632=(
BOUNDED_SURFACE()
B_SPLINE_SURFACE(3,2,((#434022,#434023,#434024),(#434025,#434026,#434027),
(#434028,#434029,#434030),(#434031,#434032,#434033)),.UNSPECIFIED.,.F.,
 .F.,.F.)
B_SPLINE_SURFACE_WITH_KNOTS((4,4),(3,3),(3.22980774337779E-5,9.63764854872252E-5),
(-0.00154325936260306,1.01095292447551),.UNSPECIFIED.)
GEOMETRIC_REPRESENTATION_ITEM()
RATIONAL_B_SPLINE_SURFACE(((1.00023530983282,0.922925743796246,1.00168574728332),
(1.00015136166114,0.950422439594261,1.00108434699061),(1.00033574337374,
0.89002936895408,1.00240524789549),(1.00054260094182,0.822274473168522,
1.00388716464861)))
REPRESENTATION_ITEM('')
SURFACE()
);
#3633=(
BOUNDED_SURFACE()
B_SPLINE_SURFACE(3,2,((#434133,#434134,#434135),(#434136,#434137,#434138),
(#434139,#434140,#434141),(#434142,#434143,#434144)),.UNSPECIFIED.,.F.,
 .F.,.F.)
B_SPLINE_SURFACE_WITH_KNOTS((4,4),(3,3),(0.,0.000101260117256737),(0.,1.),
 .UNSPECIFIED.)
GEOMETRIC_REPRESENTATION_ITEM()
RATIONAL_B_SPLINE_SURFACE(((1.,0.796615278835165,1.),(1.,0.795896038055936,
1.),(1.,0.795193354661363,1.),(1.,0.794506193185527,1.)))
REPRESENTATION_ITEM('')
SURFACE()
);
#3634=(
BOUNDED_SURFACE()
B_SPLINE_SURFACE(3,2,((#434182,#434183,#434184),(#434185,#434186,#434187),
(#434188,#434189,#434190),(#434191,#434192,#434193),(#434194,#434195,#434196),
(#434197,#434198,#434199)),.UNSPECIFIED.,.F.,.F.,.F.)
B_SPLINE_SURFACE_WITH_KNOTS((4,2,4),(3,3),(-1.88041314290455E-19,1.66936432462293E-5,
3.33872864924587E-5),(0.,1.),.UNSPECIFIED.)
GEOMETRIC_REPRESENTATION_ITEM()
RATIONAL_B_SPLINE_SURFACE(((1.,0.796615278835176,1.),(1.,0.862310524418128,
1.),(1.,0.923774472010522,1.),(1.,0.923983993203425,1.),(1.,0.862574873720946,
1.),(1.,0.796615278835188,1.)))
REPRESENTATION_ITEM('')
SURFACE()
);
#3635=(
BOUNDED_SURFACE()
B_SPLINE_SURFACE(3,2,((#434236,#434237,#434238),(#434239,#434240,#434241),
(#434242,#434243,#434244),(#434245,#434246,#434247)),.UNSPECIFIED.,.F.,
 .F.,.F.)
B_SPLINE_SURFACE_WITH_KNOTS((4,4),(3,3),(0.,0.000101244905251112),(0.,1.),
 .UNSPECIFIED.)
GEOMETRIC_REPRESENTATION_ITEM()
RATIONAL_B_SPLINE_SURFACE(((1.,0.796615278835171,1.),(1.,0.795896146109788,
1.),(1.,0.795193565796499,1.),(1.,0.7945065028899,1.)))
REPRESENTATION_ITEM('')
SURFACE()
);
#3636=(
BOUNDED_SURFACE()
B_SPLINE_SURFACE(3,2,((#434283,#434284,#434285),(#434286,#434287,#434288),
(#434289,#434290,#434291),(#434292,#434293,#434294)),.UNSPECIFIED.,.F.,
 .F.,.F.)
B_SPLINE_SURFACE_WITH_KNOTS((4,4),(3,3),(2.85968127239939E-5,9.24681548475816E-5),
(-0.00167900678752855,1.01130827127812),.UNSPECIFIED.)
GEOMETRIC_REPRESENTATION_ITEM()
RATIONAL_B_SPLINE_SURFACE(((1.00059040895251,0.822187541868116,1.00401468696653),
(1.00036527718161,0.889990093671472,1.00248382673389),(1.00016469515023,
0.950399042257892,1.0011199008251),(1.00025604274007,0.92288804428601,1.00174104990629)))
REPRESENTATION_ITEM('')
SURFACE()
);
#3637=(
BOUNDED_SURFACE()
B_SPLINE_SURFACE(3,2,((#434298,#434299,#434300),(#434301,#434302,#434303),
(#434304,#434305,#434306),(#434307,#434308,#434309)),.UNSPECIFIED.,.F.,
 .F.,.F.)
B_SPLINE_SURFACE_WITH_KNOTS((4,4),(3,3),(-5.2235835674927E-6,5.74594192424279E-5),
(-0.00127120052049952,1.),.UNSPECIFIED.)
GEOMETRIC_REPRESENTATION_ITEM()
RATIONAL_B_SPLINE_SURFACE(((1.00054449313173,0.785835073638772,1.),(1.00047707767473,
0.812351526358862,1.),(1.00044031788584,0.826810216506295,1.),(1.00044777653317,
0.823876514387265,1.)))
REPRESENTATION_ITEM('')
SURFACE()
);
#3638=(
BOUNDED_SURFACE()
B_SPLINE_SURFACE(3,2,((#434311,#434312,#434313),(#434314,#434315,#434316),
(#434317,#434318,#434319),(#434320,#434321,#434322)),.UNSPECIFIED.,.F.,
 .F.,.F.)
B_SPLINE_SURFACE_WITH_KNOTS((4,4),(3,3),(-3.52365706057789E-19,4.88747512969882E-5),
(-0.000215805215178045,1.),.UNSPECIFIED.)
GEOMETRIC_REPRESENTATION_ITEM()
RATIONAL_B_SPLINE_SURFACE(((1.00008915600325,0.793434085499806,1.),(1.00008930224979,
0.793095246303358,1.),(1.00008944684601,0.792760230720618,1.),(1.0000895898438,
0.792428918540656,1.)))
REPRESENTATION_ITEM('')
SURFACE()
);
#3639=(
BOUNDED_SURFACE()
B_SPLINE_SURFACE(3,2,((#434324,#434325,#434326),(#434327,#434328,#434329),
(#434330,#434331,#434332),(#434333,#434334,#434335),(#434336,#434337,#434338),
(#434339,#434340,#434341)),.UNSPECIFIED.,.F.,.F.,.F.)
B_SPLINE_SURFACE_WITH_KNOTS((4,2,4),(3,3),(1.35525271560688E-20,7.62675010863196E-5,
0.000152535002172639),(0.,1.02152348203061),.UNSPECIFIED.)
GEOMETRIC_REPRESENTATION_ITEM()
RATIONAL_B_SPLINE_SURFACE(((1.,0.789033595401266,1.00908146323688),(1.,
0.857071781054839,1.00615262590427),(1.,0.92208726471075,1.00335390671591),
(1.,0.922394466502367,1.00334068261142),(1.,0.857224384599071,1.00614605678498),
(1.,0.789033595401665,1.00908146323687)))
REPRESENTATION_ITEM('')
SURFACE()
);
#3640=(
BOUNDED_SURFACE()
B_SPLINE_SURFACE(3,2,((#434343,#434344,#434345),(#434346,#434347,#434348),
(#434349,#434350,#434351),(#434352,#434353,#434354)),.UNSPECIFIED.,.F.,
 .F.,.F.)
B_SPLINE_SURFACE_WITH_KNOTS((4,4),(3,3),(5.42101086242752E-20,4.88747512969884E-5),
(-0.000215489857847948,1.),.UNSPECIFIED.)
GEOMETRIC_REPRESENTATION_ITEM()
RATIONAL_B_SPLINE_SURFACE(((1.00008945889747,0.792428983985572,1.),(1.00008931610868,
0.792760296061129,1.),(1.00008917172381,0.793095311538201,1.),(1.00008902569103,
0.793434150627827,1.)))
REPRESENTATION_ITEM('')
SURFACE()
);
#3641=(
BOUNDED_SURFACE()
B_SPLINE_SURFACE(3,2,((#434356,#434357,#434358),(#434359,#434360,#434361),
(#434362,#434363,#434364),(#434365,#434366,#434367)),.UNSPECIFIED.,.F.,
 .F.,.F.)
B_SPLINE_SURFACE_WITH_KNOTS((4,4),(3,3),(-5.21974905013086E-6,5.74172395514392E-5),
(-0.00139822857736382,1.0005131236406),.UNSPECIFIED.)
GEOMETRIC_REPRESENTATION_ITEM()
RATIONAL_B_SPLINE_SURFACE(((1.00049256947243,0.823768952244056,1.00018060397847),
(1.00048448215714,0.826662424388351,1.0001776387088),(1.00052427784021,
0.812424361909417,1.00019223006919),(1.00059912365855,0.7856460946328,1.00021967280228)))
REPRESENTATION_ITEM('')
SURFACE()
);
#3642=(
BOUNDED_SURFACE()
B_SPLINE_SURFACE(3,2,((#434371,#434372,#434373),(#434374,#434375,#434376),
(#434377,#434378,#434379),(#434380,#434381,#434382)),.UNSPECIFIED.,.F.,
 .F.,.F.)
B_SPLINE_SURFACE_WITH_KNOTS((4,4),(3,3),(3.22980774337782E-5,9.63764854872257E-5),
(-0.0015432593638368,1.01095292447556),.UNSPECIFIED.)
GEOMETRIC_REPRESENTATION_ITEM()
RATIONAL_B_SPLINE_SURFACE(((1.000235309833,0.922925743796148,1.00168574728333),
(1.00015136166127,0.950422439594208,1.00108434699061),(1.000335743374,0.890029368953928,
1.00240524789551),(1.00054260094225,0.822274473168292,1.00388716464863)))
REPRESENTATION_ITEM('')
SURFACE()
);
#3643=(
BOUNDED_SURFACE()
B_SPLINE_SURFACE(3,2,((#434482,#434483,#434484),(#434485,#434486,#434487),
(#434488,#434489,#434490),(#434491,#434492,#434493)),.UNSPECIFIED.,.F.,
 .F.,.F.)
B_SPLINE_SURFACE_WITH_KNOTS((4,4),(3,3),(-2.16840434497101E-19,0.000101260117256738),
(0.,1.),.UNSPECIFIED.)
GEOMETRIC_REPRESENTATION_ITEM()
RATIONAL_B_SPLINE_SURFACE(((1.,0.796615278835173,1.),(1.,0.795896038055939,
1.),(1.,0.79519335466135,1.),(1.,0.794506193185547,1.)))
REPRESENTATION_ITEM('')
SURFACE()
);
#3644=(
BOUNDED_SURFACE()
B_SPLINE_SURFACE(3,2,((#434531,#434532,#434533),(#434534,#434535,#434536),
(#434537,#434538,#434539),(#434540,#434541,#434542),(#434543,#434544,#434545),
(#434546,#434547,#434548)),.UNSPECIFIED.,.F.,.F.,.F.)
B_SPLINE_SURFACE_WITH_KNOTS((4,2,4),(3,3),(-1.575481281893E-19,1.66936432462289E-5,
3.3387286492458E-5),(0.,1.),.UNSPECIFIED.)
GEOMETRIC_REPRESENTATION_ITEM()
RATIONAL_B_SPLINE_SURFACE(((1.,0.796615278835177,1.),(1.,0.862310524418138,
1.),(1.,0.923774472010511,1.),(1.,0.923983993203433,1.),(1.,0.862574873720957,
1.),(1.,0.796615278835182,1.)))
REPRESENTATION_ITEM('')
SURFACE()
);
#3645=(
BOUNDED_SURFACE()
B_SPLINE_SURFACE(3,2,((#434585,#434586,#434587),(#434588,#434589,#434590),
(#434591,#434592,#434593),(#434594,#434595,#434596)),.UNSPECIFIED.,.F.,
 .F.,.F.)
B_SPLINE_SURFACE_WITH_KNOTS((4,4),(3,3),(0.,0.000101244905251112),(0.,1.),
 .UNSPECIFIED.)
GEOMETRIC_REPRESENTATION_ITEM()
RATIONAL_B_SPLINE_SURFACE(((1.,0.796615278835173,1.),(1.,0.795896146109796,
1.),(1.,0.795193565796497,1.),(1.,0.794506502889903,1.)))
REPRESENTATION_ITEM('')
SURFACE()
);
#3646=(
BOUNDED_SURFACE()
B_SPLINE_SURFACE(3,2,((#434632,#434633,#434634),(#434635,#434636,#434637),
(#434638,#434639,#434640),(#434641,#434642,#434643)),.UNSPECIFIED.,.F.,
 .F.,.F.)
B_SPLINE_SURFACE_WITH_KNOTS((4,4),(3,3),(2.85968127239938E-5,9.24681548475818E-5),
(-0.00167900679475807,1.01130827127815),.UNSPECIFIED.)
GEOMETRIC_REPRESENTATION_ITEM()
RATIONAL_B_SPLINE_SURFACE(((1.00059040895506,0.82218754186681,1.00401468696654),
(1.00036527718319,0.88999009367067,1.00248382673389),(1.00016469515094,
0.950399042257525,1.0011199008251),(1.00025604274118,0.922888044285446,
1.0017410499063)))
REPRESENTATION_ITEM('')
SURFACE()
);
#3647=(
BOUNDED_SURFACE()
B_SPLINE_SURFACE(3,2,((#434647,#434648,#434649),(#434650,#434651,#434652),
(#434653,#434654,#434655),(#434656,#434657,#434658)),.UNSPECIFIED.,.F.,
 .F.,.F.)
B_SPLINE_SURFACE_WITH_KNOTS((4,4),(3,3),(-5.22358356749288E-6,5.74594192424277E-5),
(-0.00127120052068723,1.),.UNSPECIFIED.)
GEOMETRIC_REPRESENTATION_ITEM()
RATIONAL_B_SPLINE_SURFACE(((1.00054449313181,0.785835073638737,1.),(1.0004770776748,
0.81235152635883,1.),(1.00044031788591,0.82681021650626,1.),(1.00044777653323,
0.823876514387234,1.)))
REPRESENTATION_ITEM('')
SURFACE()
);
#3648=(
BOUNDED_SURFACE()
B_SPLINE_SURFACE(3,2,((#434660,#434661,#434662),(#434663,#434664,#434665),
(#434666,#434667,#434668),(#434669,#434670,#434671)),.UNSPECIFIED.,.F.,
 .F.,.F.)
B_SPLINE_SURFACE_WITH_KNOTS((4,4),(3,3),(-5.42101086242752E-19,4.8874751296988E-5),
(-0.000215805215632062,1.),.UNSPECIFIED.)
GEOMETRIC_REPRESENTATION_ITEM()
RATIONAL_B_SPLINE_SURFACE(((1.00008915600344,0.793434085499716,1.),(1.00008930224997,
0.793095246303267,1.),(1.00008944684619,0.792760230720526,1.),(1.00008958984399,
0.792428918540563,1.)))
REPRESENTATION_ITEM('')
SURFACE()
);
#3649=(
BOUNDED_SURFACE()
B_SPLINE_SURFACE(3,2,((#434673,#434674,#434675),(#434676,#434677,#434678),
(#434679,#434680,#434681),(#434682,#434683,#434684),(#434685,#434686,#434687),
(#434688,#434689,#434690)),.UNSPECIFIED.,.F.,.F.,.F.)
B_SPLINE_SURFACE_WITH_KNOTS((4,2,4),(3,3),(4.60785923306339E-19,7.62675010863196E-5,
0.000152535002172639),(0.,1.02152348203067),.UNSPECIFIED.)
GEOMETRIC_REPRESENTATION_ITEM()
RATIONAL_B_SPLINE_SURFACE(((1.,0.789033595401251,1.00908146323691),(1.,
0.85707178105489,1.00615262590428),(1.,0.922087264710668,1.00335390671592),
(1.,0.922394466502437,1.00334068261143),(1.,0.857224384599004,1.006146056785),
(1.,0.789033595401654,1.0090814632369)))
REPRESENTATION_ITEM('')
SURFACE()
);
#3650=(
BOUNDED_SURFACE()
B_SPLINE_SURFACE(3,2,((#434692,#434693,#434694),(#434695,#434696,#434697),
(#434698,#434699,#434700),(#434701,#434702,#434703)),.UNSPECIFIED.,.F.,
 .F.,.F.)
B_SPLINE_SURFACE_WITH_KNOTS((4,4),(3,3),(1.0842021724855E-19,4.88747512969884E-5),
(-0.000215489857023976,1.),.UNSPECIFIED.)
GEOMETRIC_REPRESENTATION_ITEM()
RATIONAL_B_SPLINE_SURFACE(((1.00008945889713,0.792428983985749,1.),(1.00008931610834,
0.792760296061302,1.),(1.00008917172347,0.793095311538355,1.),(1.00008902569069,
0.793434150627999,1.)))
REPRESENTATION_ITEM('')
SURFACE()
);
#3651=(
BOUNDED_SURFACE()
B_SPLINE_SURFACE(3,2,((#434705,#434706,#434707),(#434708,#434709,#434710),
(#434711,#434712,#434713),(#434714,#434715,#434716)),.UNSPECIFIED.,.F.,
 .F.,.F.)
B_SPLINE_SURFACE_WITH_KNOTS((4,4),(3,3),(-5.21974905013105E-6,5.74172395514412E-5),
(-0.001398228577509,1.00051312364061),.UNSPECIFIED.)
GEOMETRIC_REPRESENTATION_ITEM()
RATIONAL_B_SPLINE_SURFACE(((1.00049256947249,0.823768952244033,1.00018060397847),
(1.00048448215719,0.82666242438832,1.0001776387088),(1.00052427784027,0.812424361909404,
1.00019223006919),(1.00059912365861,0.785646094632767,1.00021967280229)))
REPRESENTATION_ITEM('')
SURFACE()
);
#3652=(
BOUNDED_SURFACE()
B_SPLINE_SURFACE(3,2,((#434720,#434721,#434722),(#434723,#434724,#434725),
(#434726,#434727,#434728),(#434729,#434730,#434731)),.UNSPECIFIED.,.F.,
 .F.,.F.)
B_SPLINE_SURFACE_WITH_KNOTS((4,4),(3,3),(3.22980774337781E-5,9.63764854872249E-5),
(-0.00154325936313331,1.01095292447533),.UNSPECIFIED.)
GEOMETRIC_REPRESENTATION_ITEM()
RATIONAL_B_SPLINE_SURFACE(((1.0002353098329,0.922925743796218,1.00168574728329),
(1.0001513616612,0.950422439594243,1.00108434699059),(1.00033574337385,
0.890029368954043,1.00240524789545),(1.000542600942,0.822274473168454,1.00388716464855)))
REPRESENTATION_ITEM('')
SURFACE()
);
#3653=(
BOUNDED_SURFACE()
B_SPLINE_SURFACE(3,2,((#434831,#434832,#434833),(#434834,#434835,#434836),
(#434837,#434838,#434839),(#434840,#434841,#434842)),.UNSPECIFIED.,.F.,
 .F.,.F.)
B_SPLINE_SURFACE_WITH_KNOTS((4,4),(3,3),(0.,0.000101260117256738),(0.,1.),
 .UNSPECIFIED.)
GEOMETRIC_REPRESENTATION_ITEM()
RATIONAL_B_SPLINE_SURFACE(((1.,0.796615278835171,1.),(1.,0.795896038055938,
1.),(1.,0.795193354661344,1.),(1.,0.794506193185546,1.)))
REPRESENTATION_ITEM('')
SURFACE()
);
#3654=(
BOUNDED_SURFACE()
B_SPLINE_SURFACE(3,2,((#434880,#434881,#434882),(#434883,#434884,#434885),
(#434886,#434887,#434888),(#434889,#434890,#434891),(#434892,#434893,#434894),
(#434895,#434896,#434897)),.UNSPECIFIED.,.F.,.F.,.F.)
B_SPLINE_SURFACE_WITH_KNOTS((4,2,4),(3,3),(-3.89635155736978E-20,1.66936432462297E-5,
3.33872864924594E-5),(0.,1.),.UNSPECIFIED.)
GEOMETRIC_REPRESENTATION_ITEM()
RATIONAL_B_SPLINE_SURFACE(((1.,0.796615278835171,1.),(1.,0.862310524418127,
1.),(1.,0.923774472010524,1.),(1.,0.923983993203424,1.),(1.,0.862574873720943,
1.),(1.,0.796615278835183,1.)))
REPRESENTATION_ITEM('')
SURFACE()
);
#3655=(
BOUNDED_SURFACE()
B_SPLINE_SURFACE(3,2,((#434934,#434935,#434936),(#434937,#434938,#434939),
(#434940,#434941,#434942),(#434943,#434944,#434945)),.UNSPECIFIED.,.F.,
 .F.,.F.)
B_SPLINE_SURFACE_WITH_KNOTS((4,4),(3,3),(0.,0.000101244905251112),(0.,1.),
 .UNSPECIFIED.)
GEOMETRIC_REPRESENTATION_ITEM()
RATIONAL_B_SPLINE_SURFACE(((1.,0.796615278835171,1.),(1.,0.795896146109796,
1.),(1.,0.795193565796499,1.),(1.,0.794506502889901,1.)))
REPRESENTATION_ITEM('')
SURFACE()
);
#3656=(
BOUNDED_SURFACE()
B_SPLINE_SURFACE(3,2,((#434981,#434982,#434983),(#434984,#434985,#434986),
(#434987,#434988,#434989),(#434990,#434991,#434992)),.UNSPECIFIED.,.F.,
 .F.,.F.)
B_SPLINE_SURFACE_WITH_KNOTS((4,4),(3,3),(2.85968127239939E-5,9.24681548475815E-5),
(-0.00167900678695995,1.01130827127814),.UNSPECIFIED.)
GEOMETRIC_REPRESENTATION_ITEM()
RATIONAL_B_SPLINE_SURFACE(((1.00059040895231,0.822187541868214,1.00401468696654),
(1.00036527718149,0.88999009367153,1.00248382673389),(1.00016469515017,
0.950399042257915,1.0011199008251),(1.00025604273999,0.922888044286055,
1.0017410499063)))
REPRESENTATION_ITEM('')
SURFACE()
);
#3657=(
BOUNDED_SURFACE()
B_SPLINE_SURFACE(3,2,((#434996,#434997,#434998),(#434999,#435000,#435001),
(#435002,#435003,#435004),(#435005,#435006,#435007)),.UNSPECIFIED.,.F.,
 .F.,.F.)
B_SPLINE_SURFACE_WITH_KNOTS((4,4),(3,3),(-5.2235835674929E-6,5.74594192424278E-5),
(-0.00127120052009694,1.),.UNSPECIFIED.)
GEOMETRIC_REPRESENTATION_ITEM()
RATIONAL_B_SPLINE_SURFACE(((1.00054449313155,0.785835073638853,1.),(1.00047707767458,
0.812351526358946,1.),(1.00044031788571,0.826810216506354,1.),(1.00044777653302,
0.823876514387337,1.)))
REPRESENTATION_ITEM('')
SURFACE()
);
#3658=(
BOUNDED_SURFACE()
B_SPLINE_SURFACE(3,2,((#435009,#435010,#435011),(#435012,#435013,#435014),
(#435015,#435016,#435017),(#435018,#435019,#435020)),.UNSPECIFIED.,.F.,
 .F.,.F.)
B_SPLINE_SURFACE_WITH_KNOTS((4,4),(3,3),(-3.79470760369927E-19,4.8874751296988E-5),
(-0.000215805215000492,1.),.UNSPECIFIED.)
GEOMETRIC_REPRESENTATION_ITEM()
RATIONAL_B_SPLINE_SURFACE(((1.00008915600318,0.793434085499843,1.),(1.00008930224971,
0.793095246303396,1.),(1.00008944684593,0.792760230720653,1.),(1.00008958984372,
0.792428918540692,1.)))
REPRESENTATION_ITEM('')
SURFACE()
);
#3659=(
BOUNDED_SURFACE()
B_SPLINE_SURFACE(3,2,((#435022,#435023,#435024),(#435025,#435026,#435027),
(#435028,#435029,#435030),(#435031,#435032,#435033),(#435034,#435035,#435036),
(#435037,#435038,#435039)),.UNSPECIFIED.,.F.,.F.,.F.)
B_SPLINE_SURFACE_WITH_KNOTS((4,2,4),(3,3),(4.26904605416167E-19,7.62675010863201E-5,
0.00015253500217264),(0.,1.0215234820307),.UNSPECIFIED.)
GEOMETRIC_REPRESENTATION_ITEM()
RATIONAL_B_SPLINE_SURFACE(((1.,0.789033595401245,1.00908146323693),(1.,
0.857071781054831,1.00615262590429),(1.,0.922087264710729,1.00335390671592),
(1.,0.92239446650237,1.00334068261144),(1.,0.857224384599049,1.00614605678501),
(1.,0.789033595401646,1.00908146323691)))
REPRESENTATION_ITEM('')
SURFACE()
);
#3660=(
BOUNDED_SURFACE()
B_SPLINE_SURFACE(3,2,((#435041,#435042,#435043),(#435044,#435045,#435046),
(#435047,#435048,#435049),(#435050,#435051,#435052)),.UNSPECIFIED.,.F.,
 .F.,.F.)
B_SPLINE_SURFACE_WITH_KNOTS((4,4),(3,3),(1.0842021724855E-19,4.88747512969882E-5),
(-0.000215489857076501,1.),.UNSPECIFIED.)
GEOMETRIC_REPRESENTATION_ITEM()
RATIONAL_B_SPLINE_SURFACE(((1.00008945889715,0.792428983985737,1.),(1.00008931610836,
0.792760296061283,1.),(1.00008917172349,0.793095311538362,1.),(1.00008902569072,
0.793434150627989,1.)))
REPRESENTATION_ITEM('')
SURFACE()
);
#3661=(
BOUNDED_SURFACE()
B_SPLINE_SURFACE(3,2,((#435054,#435055,#435056),(#435057,#435058,#435059),
(#435060,#435061,#435062),(#435063,#435064,#435065)),.UNSPECIFIED.,.F.,
 .F.,.F.)
B_SPLINE_SURFACE_WITH_KNOTS((4,4),(3,3),(-5.21974905013086E-6,5.74172395514395E-5),
(-0.00139822857795002,1.00051312364059),.UNSPECIFIED.)
GEOMETRIC_REPRESENTATION_ITEM()
RATIONAL_B_SPLINE_SURFACE(((1.00049256947264,0.823768952243958,1.00018060397847),
(1.00048448215734,0.826662424388247,1.0001776387088),(1.00052427784043,
0.812424361909319,1.00019223006918),(1.0005991236588,0.785646094632676,
1.00021967280228)))
REPRESENTATION_ITEM('')
SURFACE()
);
#3662=(
BOUNDED_SURFACE()
B_SPLINE_SURFACE(3,2,((#435069,#435070,#435071),(#435072,#435073,#435074),
(#435075,#435076,#435077),(#435078,#435079,#435080)),.UNSPECIFIED.,.F.,
 .F.,.F.)
B_SPLINE_SURFACE_WITH_KNOTS((4,4),(3,3),(3.22980774337779E-5,9.63764854872253E-5),
(-0.00154325936359312,1.01095292447535),.UNSPECIFIED.)
GEOMETRIC_REPRESENTATION_ITEM()
RATIONAL_B_SPLINE_SURFACE(((1.00023530983297,0.922925743796184,1.0016857472833),
(1.00015136166124,0.950422439594233,1.00108434699059),(1.00033574337395,
0.890029368953977,1.00240524789546),(1.00054260094216,0.82227447316838,
1.00388716464855)))
REPRESENTATION_ITEM('')
SURFACE()
);
#3663=(
BOUNDED_SURFACE()
B_SPLINE_SURFACE(3,2,((#435180,#435181,#435182),(#435183,#435184,#435185),
(#435186,#435187,#435188),(#435189,#435190,#435191)),.UNSPECIFIED.,.F.,
 .F.,.F.)
B_SPLINE_SURFACE_WITH_KNOTS((4,4),(3,3),(0.,0.000101260117256738),(0.,1.),
 .UNSPECIFIED.)
GEOMETRIC_REPRESENTATION_ITEM()
RATIONAL_B_SPLINE_SURFACE(((1.,0.796615278835172,1.),(1.,0.795896038055935,
1.),(1.,0.79519335466135,1.),(1.,0.794506193185544,1.)))
REPRESENTATION_ITEM('')
SURFACE()
);
#3664=(
BOUNDED_SURFACE()
B_SPLINE_SURFACE(3,2,((#435229,#435230,#435231),(#435232,#435233,#435234),
(#435235,#435236,#435237),(#435238,#435239,#435240),(#435241,#435242,#435243),
(#435244,#435245,#435246)),.UNSPECIFIED.,.F.,.F.,.F.)
B_SPLINE_SURFACE_WITH_KNOTS((4,2,4),(3,3),(1.06726151354042E-19,1.66936432462295E-5,
3.3387286492459E-5),(0.,1.),.UNSPECIFIED.)
GEOMETRIC_REPRESENTATION_ITEM()
RATIONAL_B_SPLINE_SURFACE(((1.,0.796615278835174,1.),(1.,0.86231052441814,
1.),(1.,0.92377447201052,1.),(1.,0.923983993203425,1.),(1.,0.862574873720945,
1.),(1.,0.79661527883518,1.)))
REPRESENTATION_ITEM('')
SURFACE()
);
#3665=(
BOUNDED_SURFACE()
B_SPLINE_SURFACE(3,2,((#435283,#435284,#435285),(#435286,#435287,#435288),
(#435289,#435290,#435291),(#435292,#435293,#435294)),.UNSPECIFIED.,.F.,
 .F.,.F.)
B_SPLINE_SURFACE_WITH_KNOTS((4,4),(3,3),(-2.16840434497101E-19,0.000101244905251112),
(0.,1.),.UNSPECIFIED.)
GEOMETRIC_REPRESENTATION_ITEM()
RATIONAL_B_SPLINE_SURFACE(((1.,0.79661527883517,1.),(1.,0.795896146109793,
1.),(1.,0.795193565796497,1.),(1.,0.794506502889899,1.)))
REPRESENTATION_ITEM('')
SURFACE()
);
#3666=(
BOUNDED_SURFACE()
B_SPLINE_SURFACE(3,2,((#435330,#435331,#435332),(#435333,#435334,#435335),
(#435336,#435337,#435338),(#435339,#435340,#435341)),.UNSPECIFIED.,.F.,
 .F.,.F.)
B_SPLINE_SURFACE_WITH_KNOTS((4,4),(3,3),(2.85968127239939E-5,9.24681548475817E-5),
(-0.00167900678672043,1.01130827127829),.UNSPECIFIED.)
GEOMETRIC_REPRESENTATION_ITEM()
RATIONAL_B_SPLINE_SURFACE(((1.00059040895223,0.82218754186823,1.00401468696659),
(1.00036527718143,0.889990093671546,1.00248382673392),(1.00016469515015,
0.950399042257917,1.00111990082511),(1.00025604273995,0.922888044286061,
1.00174104990632)))
REPRESENTATION_ITEM('')
SURFACE()
);
#3667=(
BOUNDED_SURFACE()
B_SPLINE_SURFACE(3,2,((#435345,#435346,#435347),(#435348,#435349,#435350),
(#435351,#435352,#435353),(#435354,#435355,#435356)),.UNSPECIFIED.,.F.,
 .F.,.F.)
B_SPLINE_SURFACE_WITH_KNOTS((4,4),(3,3),(-5.22358356749122E-6,5.74594192424277E-5),
(-0.00127120052070634,1.),.UNSPECIFIED.)
GEOMETRIC_REPRESENTATION_ITEM()
RATIONAL_B_SPLINE_SURFACE(((1.00054449313181,0.785835073638735,0.999999999999999),
(1.0004770776748,0.812351526358825,1.),(1.00044031788592,0.826810216506249,
1.),(1.00044777653324,0.82387651438723,1.)))
REPRESENTATION_ITEM('')
SURFACE()
);
#3668=(
BOUNDED_SURFACE()
B_SPLINE_SURFACE(3,2,((#435358,#435359,#435360),(#435361,#435362,#435363),
(#435364,#435365,#435366),(#435367,#435368,#435369)),.UNSPECIFIED.,.F.,
 .F.,.F.)
B_SPLINE_SURFACE_WITH_KNOTS((4,4),(3,3),(-2.16840434497101E-19,4.88747512969878E-5),
(-0.00021580521512041,1.),.UNSPECIFIED.)
GEOMETRIC_REPRESENTATION_ITEM()
RATIONAL_B_SPLINE_SURFACE(((1.00008915600323,0.793434085499819,1.),(1.00008930224976,
0.79309524630335,1.),(1.00008944684598,0.792760230720642,1.),(1.00008958984377,
0.792428918540667,1.)))
REPRESENTATION_ITEM('')
SURFACE()
);
#3669=(
BOUNDED_SURFACE()
B_SPLINE_SURFACE(3,2,((#435371,#435372,#435373),(#435374,#435375,#435376),
(#435377,#435378,#435379),(#435380,#435381,#435382),(#435383,#435384,#435385),
(#435386,#435387,#435388)),.UNSPECIFIED.,.F.,.F.,.F.)
B_SPLINE_SURFACE_WITH_KNOTS((4,2,4),(3,3),(-1.15196480826585E-19,7.62675010863196E-5,
0.000152535002172639),(0.,1.02152348203041),.UNSPECIFIED.)
GEOMETRIC_REPRESENTATION_ITEM()
RATIONAL_B_SPLINE_SURFACE(((1.,0.789033595401306,1.0090814632368),(1.,0.85707178105488,
1.00615262590421),(1.,0.922087264710749,1.00335390671588),(1.,0.922394466502395,
1.00334068261139),(1.,0.857224384599093,1.00614605678492),(1.,0.789033595401704,
1.00908146323678)))
REPRESENTATION_ITEM('')
SURFACE()
);
#3670=(
BOUNDED_SURFACE()
B_SPLINE_SURFACE(3,2,((#435390,#435391,#435392),(#435393,#435394,#435395),
(#435396,#435397,#435398),(#435399,#435400,#435401)),.UNSPECIFIED.,.F.,
 .F.,.F.)
B_SPLINE_SURFACE_WITH_KNOTS((4,4),(3,3),(2.98155597433514E-19,4.88747512969883E-5),
(-0.000215489856871959,1.),.UNSPECIFIED.)
GEOMETRIC_REPRESENTATION_ITEM()
RATIONAL_B_SPLINE_SURFACE(((1.00008945889706,0.792428983985777,1.),(1.00008931610828,
0.79276029606132,1.),(1.00008917172341,0.793095311538403,1.),(1.00008902569063,
0.793434150628028,1.)))
REPRESENTATION_ITEM('')
SURFACE()
);
#3671=(
BOUNDED_SURFACE()
B_SPLINE_SURFACE(3,2,((#435403,#435404,#435405),(#435406,#435407,#435408),
(#435409,#435410,#435411),(#435412,#435413,#435414)),.UNSPECIFIED.,.F.,
 .F.,.F.)
B_SPLINE_SURFACE_WITH_KNOTS((4,4),(3,3),(-5.21974905013095E-6,5.74172395514395E-5),
(-0.00139822857774113,1.00051312364093),.UNSPECIFIED.)
GEOMETRIC_REPRESENTATION_ITEM()
RATIONAL_B_SPLINE_SURFACE(((1.00049256947257,0.823768952243928,1.00018060397858),
(1.00048448215727,0.826662424388224,1.00017763870891),(1.00052427784035,
0.812424361909291,1.00019223006931),(1.00059912365871,0.785646094632647,
1.00021967280242)))
REPRESENTATION_ITEM('')
SURFACE()
);
#3672=(
BOUNDED_SURFACE()
B_SPLINE_SURFACE(3,2,((#435418,#435419,#435420),(#435421,#435422,#435423),
(#435424,#435425,#435426),(#435427,#435428,#435429)),.UNSPECIFIED.,.F.,
 .F.,.F.)
B_SPLINE_SURFACE_WITH_KNOTS((4,4),(3,3),(3.22980774337778E-5,9.63764854872251E-5),
(-0.00154325936392601,1.0109529244756),.UNSPECIFIED.)
GEOMETRIC_REPRESENTATION_ITEM()
RATIONAL_B_SPLINE_SURFACE(((1.00023530983302,0.922925743796135,1.00168574728334),
(1.00015136166127,0.950422439594195,1.00108434699061),(1.00033574337402,
0.890029368953922,1.00240524789552),(1.00054260094228,0.822274473168269,
1.00388716464864)))
REPRESENTATION_ITEM('')
SURFACE()
);
#3673=(
BOUNDED_SURFACE()
B_SPLINE_SURFACE(3,2,((#435529,#435530,#435531),(#435532,#435533,#435534),
(#435535,#435536,#435537),(#435538,#435539,#435540)),.UNSPECIFIED.,.F.,
 .F.,.F.)
B_SPLINE_SURFACE_WITH_KNOTS((4,4),(3,3),(-2.16840434497101E-19,0.000101260117256738),
(0.,1.),.UNSPECIFIED.)
GEOMETRIC_REPRESENTATION_ITEM()
RATIONAL_B_SPLINE_SURFACE(((1.,0.796615278835172,1.),(1.,0.795896038055936,
1.),(1.,0.795193354661352,1.),(1.,0.794506193185545,1.)))
REPRESENTATION_ITEM('')
SURFACE()
);
#3674=(
BOUNDED_SURFACE()
B_SPLINE_SURFACE(3,2,((#435578,#435579,#435580),(#435581,#435582,#435583),
(#435584,#435585,#435586),(#435587,#435588,#435589),(#435590,#435591,#435592),
(#435593,#435594,#435595)),.UNSPECIFIED.,.F.,.F.,.F.)
B_SPLINE_SURFACE_WITH_KNOTS((4,2,4),(3,3),(1.77876918923403E-19,1.66936432462295E-5,
3.33872864924589E-5),(0.,1.),.UNSPECIFIED.)
GEOMETRIC_REPRESENTATION_ITEM()
RATIONAL_B_SPLINE_SURFACE(((1.,0.796615278835179,1.),(1.,0.862310524418131,
1.),(1.,0.923774472010521,1.),(1.,0.923983993203423,1.),(1.,0.862574873720948,
1.),(1.,0.796615278835186,1.)))
REPRESENTATION_ITEM('')
SURFACE()
);
#3675=(
BOUNDED_SURFACE()
B_SPLINE_SURFACE(3,2,((#435632,#435633,#435634),(#435635,#435636,#435637),
(#435638,#435639,#435640),(#435641,#435642,#435643)),.UNSPECIFIED.,.F.,
 .F.,.F.)
B_SPLINE_SURFACE_WITH_KNOTS((4,4),(3,3),(-2.16840434497101E-19,0.000101244905251112),
(0.,1.),.UNSPECIFIED.)
GEOMETRIC_REPRESENTATION_ITEM()
RATIONAL_B_SPLINE_SURFACE(((1.,0.79661527883517,1.),(1.,0.795896146109795,
1.),(1.,0.795193565796499,1.),(1.,0.7945065028899,1.)))
REPRESENTATION_ITEM('')
SURFACE()
);
#3676=(
BOUNDED_SURFACE()
B_SPLINE_SURFACE(3,2,((#435679,#435680,#435681),(#435682,#435683,#435684),
(#435685,#435686,#435687),(#435688,#435689,#435690)),.UNSPECIFIED.,.F.,
 .F.,.F.)
B_SPLINE_SURFACE_WITH_KNOTS((4,4),(3,3),(2.85968127239938E-5,9.2468154847582E-5),
(-0.00167900678625328,1.01130827127842),.UNSPECIFIED.)
GEOMETRIC_REPRESENTATION_ITEM()
RATIONAL_B_SPLINE_SURFACE(((1.00059040895207,0.822187541868287,1.00401468696664),
(1.00036527718133,0.889990093671587,1.00248382673395),(1.0001646951501,
0.950399042257936,1.00111990082513),(1.00025604273988,0.922888044286088,
1.00174104990634)))
REPRESENTATION_ITEM('')
SURFACE()
);
#3677=(
BOUNDED_SURFACE()
B_SPLINE_SURFACE(3,2,((#435694,#435695,#435696),(#435697,#435698,#435699),
(#435700,#435701,#435702),(#435703,#435704,#435705)),.UNSPECIFIED.,.F.,
 .F.,.F.)
B_SPLINE_SURFACE_WITH_KNOTS((4,4),(3,3),(-5.22358356749338E-6,5.74594192424277E-5),
(-0.00127120052079804,1.),.UNSPECIFIED.)
GEOMETRIC_REPRESENTATION_ITEM()
RATIONAL_B_SPLINE_SURFACE(((1.00054449313185,0.785835073638721,1.),(1.00047707767484,
0.812351526358789,1.),(1.00044031788595,0.826810216506256,1.),(1.00044777653327,
0.823876514387212,1.)))
REPRESENTATION_ITEM('')
SURFACE()
);
#3678=(
BOUNDED_SURFACE()
B_SPLINE_SURFACE(3,2,((#435707,#435708,#435709),(#435710,#435711,#435712),
(#435713,#435714,#435715),(#435716,#435717,#435718)),.UNSPECIFIED.,.F.,
 .F.,.F.)
B_SPLINE_SURFACE_WITH_KNOTS((4,4),(3,3),(-5.42101086242752E-20,4.8874751296988E-5),
(-0.000215805214956234,1.),.UNSPECIFIED.)
GEOMETRIC_REPRESENTATION_ITEM()
RATIONAL_B_SPLINE_SURFACE(((1.00008915600316,0.793434085499853,1.),(1.00008930224969,
0.793095246303394,1.),(1.00008944684591,0.792760230720669,1.),(1.00008958984371,
0.792428918540704,1.)))
REPRESENTATION_ITEM('')
SURFACE()
);
#3679=(
BOUNDED_SURFACE()
B_SPLINE_SURFACE(3,2,((#435720,#435721,#435722),(#435723,#435724,#435725),
(#435726,#435727,#435728),(#435729,#435730,#435731),(#435732,#435733,#435734),
(#435735,#435736,#435737)),.UNSPECIFIED.,.F.,.F.,.F.)
B_SPLINE_SURFACE_WITH_KNOTS((4,2,4),(3,3),(1.28749007982654E-19,7.62675010863196E-5,
0.000152535002172639),(0.,1.02152348203102),.UNSPECIFIED.)
GEOMETRIC_REPRESENTATION_ITEM()
RATIONAL_B_SPLINE_SURFACE(((1.,0.789033595401182,1.00908146323706),(1.,
0.857071781054781,1.00615262590438),(1.,0.922087264710715,1.00335390671597),
(1.,0.922394466502335,1.00334068261149),(1.,0.857224384599015,1.0061460567851),
(1.,0.789033595401579,1.00908146323704)))
REPRESENTATION_ITEM('')
SURFACE()
);
#3680=(
BOUNDED_SURFACE()
B_SPLINE_SURFACE(3,2,((#435739,#435740,#435741),(#435742,#435743,#435744),
(#435745,#435746,#435747),(#435748,#435749,#435750)),.UNSPECIFIED.,.F.,
 .F.,.F.)
B_SPLINE_SURFACE_WITH_KNOTS((4,4),(3,3),(5.14996031930615E-19,4.88747512969886E-5),
(-0.000215489857762071,1.),.UNSPECIFIED.)
GEOMETRIC_REPRESENTATION_ITEM()
RATIONAL_B_SPLINE_SURFACE(((1.00008945889743,0.792428983985592,1.),(1.00008931610865,
0.792760296061145,1.),(1.00008917172377,0.793095311538216,1.),(1.000089025691,
0.793434150627846,1.)))
REPRESENTATION_ITEM('')
SURFACE()
);
#3681=(
BOUNDED_SURFACE()
B_SPLINE_SURFACE(3,2,((#435752,#435753,#435754),(#435755,#435756,#435757),
(#435758,#435759,#435760),(#435761,#435762,#435763)),.UNSPECIFIED.,.F.,
 .F.,.F.)
B_SPLINE_SURFACE_WITH_KNOTS((4,4),(3,3),(-5.21974905012869E-6,5.74172395514394E-5),
(-0.00139822857793504,1.00051312364104),.UNSPECIFIED.)
GEOMETRIC_REPRESENTATION_ITEM()
RATIONAL_B_SPLINE_SURFACE(((1.00049256947264,0.823768952243878,1.00018060397862),
(1.00048448215734,0.826662424388174,1.00017763870895),(1.00052427784043,
0.812424361909233,1.00019223006935),(1.00059912365879,0.785646094632582,
1.00021967280247)))
REPRESENTATION_ITEM('')
SURFACE()
);
#3682=(
BOUNDED_SURFACE()
B_SPLINE_SURFACE(3,2,((#435767,#435768,#435769),(#435770,#435771,#435772),
(#435773,#435774,#435775),(#435776,#435777,#435778)),.UNSPECIFIED.,.F.,
 .F.,.F.)
B_SPLINE_SURFACE_WITH_KNOTS((4,4),(3,3),(3.22980774337778E-5,9.63764854872257E-5),
(-0.00154325936384009,1.01095292447553),.UNSPECIFIED.)
GEOMETRIC_REPRESENTATION_ITEM()
RATIONAL_B_SPLINE_SURFACE(((1.000235309833,0.922925743796147,1.00168574728333),
(1.00015136166127,0.950422439594206,1.00108434699061),(1.00033574337401,
0.890029368953931,1.0024052478955),(1.00054260094225,0.822274473168301,
1.00388716464862)))
REPRESENTATION_ITEM('')
SURFACE()
);
#3683=(
BOUNDED_SURFACE()
B_SPLINE_SURFACE(3,2,((#435878,#435879,#435880),(#435881,#435882,#435883),
(#435884,#435885,#435886),(#435887,#435888,#435889)),.UNSPECIFIED.,.F.,
 .F.,.F.)
B_SPLINE_SURFACE_WITH_KNOTS((4,4),(3,3),(0.,0.000101260117256737),(0.,1.),
 .UNSPECIFIED.)
GEOMETRIC_REPRESENTATION_ITEM()
RATIONAL_B_SPLINE_SURFACE(((1.,0.796615278835173,1.),(1.,0.795896038055925,
1.),(1.,0.795193354661367,1.),(1.,0.794506193185532,1.)))
REPRESENTATION_ITEM('')
SURFACE()
);
#3684=(
BOUNDED_SURFACE()
B_SPLINE_SURFACE(3,2,((#435927,#435928,#435929),(#435930,#435931,#435932),
(#435933,#435934,#435935),(#435936,#435937,#435938),(#435939,#435940,#435941),
(#435942,#435943,#435944)),.UNSPECIFIED.,.F.,.F.,.F.)
B_SPLINE_SURFACE_WITH_KNOTS((4,2,4),(3,3),(-8.13151629364128E-20,1.66936432462297E-5,
3.33872864924594E-5),(0.,1.),.UNSPECIFIED.)
GEOMETRIC_REPRESENTATION_ITEM()
RATIONAL_B_SPLINE_SURFACE(((1.,0.79661527883517,1.),(1.,0.862310524418116,
1.),(1.,0.923774472010523,1.),(1.,0.923983993203425,1.),(1.,0.86257487372094,
1.),(1.,0.796615278835185,1.)))
REPRESENTATION_ITEM('')
SURFACE()
);
#3685=(
BOUNDED_SURFACE()
B_SPLINE_SURFACE(3,2,((#435981,#435982,#435983),(#435984,#435985,#435986),
(#435987,#435988,#435989),(#435990,#435991,#435992)),.UNSPECIFIED.,.F.,
 .F.,.F.)
B_SPLINE_SURFACE_WITH_KNOTS((4,4),(3,3),(0.,0.000101244905251112),(0.,1.),
 .UNSPECIFIED.)
GEOMETRIC_REPRESENTATION_ITEM()
RATIONAL_B_SPLINE_SURFACE(((1.,0.79661527883517,1.),(1.,0.79589614610979,
1.),(1.,0.795193565796501,1.),(1.,0.7945065028899,1.)))
REPRESENTATION_ITEM('')
SURFACE()
);
#3686=(
BOUNDED_SURFACE()
B_SPLINE_SURFACE(3,2,((#436028,#436029,#436030),(#436031,#436032,#436033),
(#436034,#436035,#436036),(#436037,#436038,#436039)),.UNSPECIFIED.,.F.,
 .F.,.F.)
B_SPLINE_SURFACE_WITH_KNOTS((4,4),(3,3),(2.85968127239939E-5,9.24681548475817E-5),
(-0.00167900678781028,1.01130827127812),.UNSPECIFIED.)
GEOMETRIC_REPRESENTATION_ITEM()
RATIONAL_B_SPLINE_SURFACE(((1.00059040895261,0.822187541868062,1.00401468696653),
(1.00036527718167,0.889990093671442,1.00248382673389),(1.00016469515025,
0.950399042257876,1.0011199008251),(1.00025604274012,0.92288804428599,1.00174104990629)))
REPRESENTATION_ITEM('')
SURFACE()
);
#3687=(
BOUNDED_SURFACE()
B_SPLINE_SURFACE(3,2,((#436043,#436044,#436045),(#436046,#436047,#436048),
(#436049,#436050,#436051),(#436052,#436053,#436054)),.UNSPECIFIED.,.F.,
 .F.,.F.)
B_SPLINE_SURFACE_WITH_KNOTS((4,4),(3,3),(-5.22358356749345E-6,5.74594192424276E-5),
(-0.00127120052056582,1.),.UNSPECIFIED.)
GEOMETRIC_REPRESENTATION_ITEM()
RATIONAL_B_SPLINE_SURFACE(((1.00054449313175,0.785835073638759,1.),(1.00047707767475,
0.812351526358855,1.),(1.00044031788587,0.826810216506281,1.),(1.00044777653319,
0.823876514387254,1.)))
REPRESENTATION_ITEM('')
SURFACE()
);
#3688=(
BOUNDED_SURFACE()
B_SPLINE_SURFACE(3,2,((#436056,#436057,#436058),(#436059,#436060,#436061),
(#436062,#436063,#436064),(#436065,#436066,#436067)),.UNSPECIFIED.,.F.,
 .F.,.F.)
B_SPLINE_SURFACE_WITH_KNOTS((4,4),(3,3),(-2.71050543121376E-19,4.88747512969877E-5),
(-0.000215805215438253,1.),.UNSPECIFIED.)
GEOMETRIC_REPRESENTATION_ITEM()
RATIONAL_B_SPLINE_SURFACE(((1.00008915600336,0.793434085499752,1.),(1.00008930224989,
0.793095246303316,1.),(1.00008944684611,0.792760230720558,1.),(1.00008958984391,
0.792428918540604,1.)))
REPRESENTATION_ITEM('')
SURFACE()
);
#3689=(
BOUNDED_SURFACE()
B_SPLINE_SURFACE(3,2,((#436069,#436070,#436071),(#436072,#436073,#436074),
(#436075,#436076,#436077),(#436078,#436079,#436080),(#436081,#436082,#436083),
(#436084,#436085,#436086)),.UNSPECIFIED.,.F.,.F.,.F.)
B_SPLINE_SURFACE_WITH_KNOTS((4,2,4),(3,3),(2.91379333855479E-19,7.62675010863199E-5,
0.000152535002172639),(0.,1.02152348203046),.UNSPECIFIED.)
GEOMETRIC_REPRESENTATION_ITEM()
RATIONAL_B_SPLINE_SURFACE(((1.,0.789033595401292,1.00908146323682),(1.,
0.857071781054872,1.00615262590422),(1.,0.922087264710747,1.00335390671588),
(1.,0.92239446650239,1.0033406826114),(1.,0.857224384599083,1.00614605678494),
(1.,0.789033595401694,1.0090814632368)))
REPRESENTATION_ITEM('')
SURFACE()
);
#3690=(
BOUNDED_SURFACE()
B_SPLINE_SURFACE(3,2,((#436088,#436089,#436090),(#436091,#436092,#436093),
(#436094,#436095,#436096),(#436097,#436098,#436099)),.UNSPECIFIED.,.F.,
 .F.,.F.)
B_SPLINE_SURFACE_WITH_KNOTS((4,4),(3,3),(3.25260651745651E-19,4.88747512969886E-5),
(-0.000215489857342165,1.),.UNSPECIFIED.)
GEOMETRIC_REPRESENTATION_ITEM()
RATIONAL_B_SPLINE_SURFACE(((1.00008945889726,0.792428983985683,1.),(1.00008931610847,
0.792760296061223,1.),(1.0000891717236,0.793095311538305,1.),(1.00008902569083,
0.793434150627931,1.)))
REPRESENTATION_ITEM('')
SURFACE()
);
#3691=(
BOUNDED_SURFACE()
B_SPLINE_SURFACE(3,2,((#436101,#436102,#436103),(#436104,#436105,#436106),
(#436107,#436108,#436109),(#436110,#436111,#436112)),.UNSPECIFIED.,.F.,
 .F.,.F.)
B_SPLINE_SURFACE_WITH_KNOTS((4,4),(3,3),(-5.21974905012869E-6,5.74172395514397E-5),
(-0.00139822857729007,1.00051312364051),.UNSPECIFIED.)
GEOMETRIC_REPRESENTATION_ITEM()
RATIONAL_B_SPLINE_SURFACE(((1.00049256947241,0.823768952244086,1.00018060397844),
(1.00048448215711,0.826662424388373,1.00017763870877),(1.00052427784018,
0.812424361909455,1.00019223006915),(1.00059912365851,0.785646094632833,
1.00021967280224)))
REPRESENTATION_ITEM('')
SURFACE()
);
#3692=(
BOUNDED_SURFACE()
B_SPLINE_SURFACE(3,2,((#436116,#436117,#436118),(#436119,#436120,#436121),
(#436122,#436123,#436124),(#436125,#436126,#436127)),.UNSPECIFIED.,.F.,
 .F.,.F.)
B_SPLINE_SURFACE_WITH_KNOTS((4,4),(3,3),(3.2298077433778E-5,9.63764854872252E-5),
(-0.00154325936375228,1.01095292447535),.UNSPECIFIED.)
GEOMETRIC_REPRESENTATION_ITEM()
RATIONAL_B_SPLINE_SURFACE(((1.00023530983299,0.922925743796169,1.0016857472833),
(1.00015136166126,0.95042243959422,1.00108434699059),(1.00033574337399,
0.890029368953975,1.00240524789546),(1.00054260094222,0.822274473168344,
1.00388716464855)))
REPRESENTATION_ITEM('')
SURFACE()
);
#3693=(
BOUNDED_SURFACE()
B_SPLINE_SURFACE(3,2,((#436227,#436228,#436229),(#436230,#436231,#436232),
(#436233,#436234,#436235),(#436236,#436237,#436238)),.UNSPECIFIED.,.F.,
 .F.,.F.)
B_SPLINE_SURFACE_WITH_KNOTS((4,4),(3,3),(0.,0.000101260117256738),(0.,1.),
 .UNSPECIFIED.)
GEOMETRIC_REPRESENTATION_ITEM()
RATIONAL_B_SPLINE_SURFACE(((1.,0.79661527883517,1.),(1.,0.795896038055943,
1.),(1.,0.795193354661343,1.),(1.,0.794506193185546,1.)))
REPRESENTATION_ITEM('')
SURFACE()
);
#3694=(
BOUNDED_SURFACE()
B_SPLINE_SURFACE(3,2,((#436276,#436277,#436278),(#436279,#436280,#436281),
(#436282,#436283,#436284),(#436285,#436286,#436287),(#436288,#436289,#436290),
(#436291,#436292,#436293)),.UNSPECIFIED.,.F.,.F.,.F.)
B_SPLINE_SURFACE_WITH_KNOTS((4,2,4),(3,3),(-1.10114283143059E-19,1.66936432462291E-5,
3.33872864924584E-5),(0.,1.),.UNSPECIFIED.)
GEOMETRIC_REPRESENTATION_ITEM()
RATIONAL_B_SPLINE_SURFACE(((1.,0.796615278835174,1.),(1.,0.86231052441814,
1.),(1.,0.92377447201052,1.),(1.,0.923983993203428,1.),(1.,0.862574873720945,
1.),(1.,0.796615278835184,1.)))
REPRESENTATION_ITEM('')
SURFACE()
);
#3695=(
BOUNDED_SURFACE()
B_SPLINE_SURFACE(3,2,((#436330,#436331,#436332),(#436333,#436334,#436335),
(#436336,#436337,#436338),(#436339,#436340,#436341)),.UNSPECIFIED.,.F.,
 .F.,.F.)
B_SPLINE_SURFACE_WITH_KNOTS((4,4),(3,3),(-2.16840434497101E-19,0.000101244905251112),
(0.,1.),.UNSPECIFIED.)
GEOMETRIC_REPRESENTATION_ITEM()
RATIONAL_B_SPLINE_SURFACE(((1.,0.796615278835169,1.),(1.,0.795896146109785,
1.),(1.,0.795193565796503,1.),(1.,0.794506502889899,1.)))
REPRESENTATION_ITEM('')
SURFACE()
);
#3696=(
BOUNDED_SURFACE()
B_SPLINE_SURFACE(3,2,((#436377,#436378,#436379),(#436380,#436381,#436382),
(#436383,#436384,#436385),(#436386,#436387,#436388)),.UNSPECIFIED.,.F.,
 .F.,.F.)
B_SPLINE_SURFACE_WITH_KNOTS((4,4),(3,3),(2.85968127239939E-5,9.24681548475814E-5),
(-0.00167900678689317,1.01130827127832),.UNSPECIFIED.)
GEOMETRIC_REPRESENTATION_ITEM()
RATIONAL_B_SPLINE_SURFACE(((1.00059040895229,0.822187541868193,1.0040146869666),
(1.00036527718147,0.889990093671525,1.00248382673393),(1.00016469515016,
0.950399042257908,1.00111990082512),(1.00025604273998,0.922888044286044,
1.00174104990633)))
REPRESENTATION_ITEM('')
SURFACE()
);
#3697=(
BOUNDED_SURFACE()
B_SPLINE_SURFACE(3,2,((#436392,#436393,#436394),(#436395,#436396,#436397),
(#436398,#436399,#436400),(#436401,#436402,#436403)),.UNSPECIFIED.,.F.,
 .F.,.F.)
B_SPLINE_SURFACE_WITH_KNOTS((4,4),(3,3),(-5.22358356749165E-6,5.74594192424277E-5),
(-0.00127120052054818,1.),.UNSPECIFIED.)
GEOMETRIC_REPRESENTATION_ITEM()
RATIONAL_B_SPLINE_SURFACE(((1.00054449313175,0.785835073638764,1.),(1.00047707767475,
0.812351526358859,1.),(1.00044031788586,0.826810216506276,1.),(1.00044777653318,
0.823876514387259,1.)))
REPRESENTATION_ITEM('')
SURFACE()
);
#3698=(
BOUNDED_SURFACE()
B_SPLINE_SURFACE(3,2,((#436405,#436406,#436407),(#436408,#436409,#436410),
(#436411,#436412,#436413),(#436414,#436415,#436416)),.UNSPECIFIED.,.F.,
 .F.,.F.)
B_SPLINE_SURFACE_WITH_KNOTS((4,4),(3,3),(-2.98155597433514E-19,4.88747512969879E-5),
(-0.00021580521504422,1.),.UNSPECIFIED.)
GEOMETRIC_REPRESENTATION_ITEM()
RATIONAL_B_SPLINE_SURFACE(((1.0000891560032,0.793434085499835,1.),(1.00008930224973,
0.793095246303373,1.),(1.00008944684595,0.792760230720652,1.),(1.00008958984374,
0.792428918540684,1.)))
REPRESENTATION_ITEM('')
SURFACE()
);
#3699=(
BOUNDED_SURFACE()
B_SPLINE_SURFACE(3,2,((#436418,#436419,#436420),(#436421,#436422,#436423),
(#436424,#436425,#436426),(#436427,#436428,#436429),(#436430,#436431,#436432),
(#436433,#436434,#436435)),.UNSPECIFIED.,.F.,.F.,.F.)
B_SPLINE_SURFACE_WITH_KNOTS((4,2,4),(3,3),(0.,7.62675010863195E-5,0.000152535002172639),
(0.,1.02152348203079),.UNSPECIFIED.)
GEOMETRIC_REPRESENTATION_ITEM()
RATIONAL_B_SPLINE_SURFACE(((1.,0.789033595401228,1.00908146323696),(1.,
0.857071781054826,1.00615262590432),(1.,0.922087264710717,1.00335390671594),
(1.,0.922394466502367,1.00334068261145),(1.,0.857224384599037,1.00614605678503),
(1.,0.789033595401621,1.00908146323695)))
REPRESENTATION_ITEM('')
SURFACE()
);
#3700=(
BOUNDED_SURFACE()
B_SPLINE_SURFACE(3,2,((#436437,#436438,#436439),(#436440,#436441,#436442),
(#436443,#436444,#436445),(#436446,#436447,#436448)),.UNSPECIFIED.,.F.,
 .F.,.F.)
B_SPLINE_SURFACE_WITH_KNOTS((4,4),(3,3),(1.0842021724855E-19,4.88747512969883E-5),
(-0.000215489857070327,1.),.UNSPECIFIED.)
GEOMETRIC_REPRESENTATION_ITEM()
RATIONAL_B_SPLINE_SURFACE(((1.00008945889715,0.792428983985738,1.),(1.00008931610836,
0.792760296061282,1.),(1.00008917172349,0.793095311538351,1.),(1.00008902569071,
0.793434150627988,1.)))
REPRESENTATION_ITEM('')
SURFACE()
);
#3701=(
BOUNDED_SURFACE()
B_SPLINE_SURFACE(3,2,((#436450,#436451,#436452),(#436453,#436454,#436455),
(#436456,#436457,#436458),(#436459,#436460,#436461)),.UNSPECIFIED.,.F.,
 .F.,.F.)
B_SPLINE_SURFACE_WITH_KNOTS((4,4),(3,3),(-5.21974905013086E-6,5.74172395514391E-5),
(-0.00139822857771562,1.00051312364077),.UNSPECIFIED.)
GEOMETRIC_REPRESENTATION_ITEM()
RATIONAL_B_SPLINE_SURFACE(((1.00049256947256,0.823768952243966,1.00018060397853),
(1.00048448215726,0.826662424388255,1.00017763870886),(1.00052427784034,
0.812424361909324,1.00019223006925),(1.0005991236587,0.78564609463269,1.00021967280235)))
REPRESENTATION_ITEM('')
SURFACE()
);
#3702=(
BOUNDED_SURFACE()
B_SPLINE_SURFACE(3,2,((#436465,#436466,#436467),(#436468,#436469,#436470),
(#436471,#436472,#436473),(#436474,#436475,#436476)),.UNSPECIFIED.,.F.,
 .F.,.F.)
B_SPLINE_SURFACE_WITH_KNOTS((4,4),(3,3),(3.22980774337782E-5,9.63764854872247E-5),
(-0.00154325936386019,1.0109529244756),.UNSPECIFIED.)
GEOMETRIC_REPRESENTATION_ITEM()
RATIONAL_B_SPLINE_SURFACE(((1.00023530983301,0.922925743796141,1.00168574728334),
(1.00015136166127,0.950422439594195,1.00108434699061),(1.00033574337401,
0.890029368953938,1.00240524789551),(1.00054260094226,0.822274473168278,
1.00388716464864)))
REPRESENTATION_ITEM('')
SURFACE()
);
#3703=(
BOUNDED_SURFACE()
B_SPLINE_SURFACE(3,2,((#436576,#436577,#436578),(#436579,#436580,#436581),
(#436582,#436583,#436584),(#436585,#436586,#436587)),.UNSPECIFIED.,.F.,
 .F.,.F.)
B_SPLINE_SURFACE_WITH_KNOTS((4,4),(3,3),(-2.16840434497101E-19,0.000101260117256737),
(0.,1.),.UNSPECIFIED.)
GEOMETRIC_REPRESENTATION_ITEM()
RATIONAL_B_SPLINE_SURFACE(((1.,0.796615278835171,1.),(1.,0.79589603805593,
1.),(1.,0.795193354661352,1.),(1.,0.794506193185539,1.)))
REPRESENTATION_ITEM('')
SURFACE()
);
#3704=(
BOUNDED_SURFACE()
B_SPLINE_SURFACE(3,2,((#436625,#436626,#436627),(#436628,#436629,#436630),
(#436631,#436632,#436633),(#436634,#436635,#436636),(#436637,#436638,#436639),
(#436640,#436641,#436642)),.UNSPECIFIED.,.F.,.F.,.F.)
B_SPLINE_SURFACE_WITH_KNOTS((4,2,4),(3,3),(7.28448334638698E-20,1.66936432462294E-5,
3.33872864924587E-5),(0.,1.),.UNSPECIFIED.)
GEOMETRIC_REPRESENTATION_ITEM()
RATIONAL_B_SPLINE_SURFACE(((1.,0.796615278835177,1.),(1.,0.862310524418129,
1.),(1.,0.923774472010524,1.),(1.,0.923983993203422,1.),(1.,0.862574873720948,
1.),(1.,0.796615278835187,1.)))
REPRESENTATION_ITEM('')
SURFACE()
);
#3705=(
BOUNDED_SURFACE()
B_SPLINE_SURFACE(3,2,((#436679,#436680,#436681),(#436682,#436683,#436684),
(#436685,#436686,#436687),(#436688,#436689,#436690)),.UNSPECIFIED.,.F.,
 .F.,.F.)
B_SPLINE_SURFACE_WITH_KNOTS((4,4),(3,3),(2.16840434497101E-19,0.000101244905251112),
(0.,1.),.UNSPECIFIED.)
GEOMETRIC_REPRESENTATION_ITEM()
RATIONAL_B_SPLINE_SURFACE(((1.,0.796615278835172,1.),(1.,0.79589614610979,
1.),(1.,0.795193565796502,1.),(1.,0.794506502889901,1.)))
REPRESENTATION_ITEM('')
SURFACE()
);
#3706=(
BOUNDED_SURFACE()
B_SPLINE_SURFACE(3,2,((#436726,#436727,#436728),(#436729,#436730,#436731),
(#436732,#436733,#436734),(#436735,#436736,#436737)),.UNSPECIFIED.,.F.,
 .F.,.F.)
B_SPLINE_SURFACE_WITH_KNOTS((4,4),(3,3),(2.85968127239939E-5,9.24681548475817E-5),
(-0.00167900678662011,1.01130827127831),.UNSPECIFIED.)
GEOMETRIC_REPRESENTATION_ITEM()
RATIONAL_B_SPLINE_SURFACE(((1.00059040895219,0.822187541868238,1.0040146869666),
(1.00036527718141,0.889990093671566,1.00248382673393),(1.00016469515014,
0.950399042257916,1.00111990082512),(1.00025604273994,0.922888044286067,
1.00174104990632)))
REPRESENTATION_ITEM('')
SURFACE()
);
#3707=(
BOUNDED_SURFACE()
B_SPLINE_SURFACE(3,2,((#436741,#436742,#436743),(#436744,#436745,#436746),
(#436747,#436748,#436749),(#436750,#436751,#436752)),.UNSPECIFIED.,.F.,
 .F.,.F.)
B_SPLINE_SURFACE_WITH_KNOTS((4,4),(3,3),(-5.22358356749333E-6,5.74594192424276E-5),
(-0.00127120052061989,1.),.UNSPECIFIED.)
GEOMETRIC_REPRESENTATION_ITEM()
RATIONAL_B_SPLINE_SURFACE(((1.00054449313178,0.785835073638753,1.),(1.00047707767477,
0.812351526358838,1.),(1.00044031788589,0.826810216506273,1.),(1.00044777653321,
0.823876514387244,1.)))
REPRESENTATION_ITEM('')
SURFACE()
);
#3708=(
BOUNDED_SURFACE()
B_SPLINE_SURFACE(3,2,((#436754,#436755,#436756),(#436757,#436758,#436759),
(#436760,#436761,#436762),(#436763,#436764,#436765)),.UNSPECIFIED.,.F.,
 .F.,.F.)
B_SPLINE_SURFACE_WITH_KNOTS((4,4),(3,3),(5.42101086242752E-20,4.88747512969881E-5),
(-0.000215805215480362,1.),.UNSPECIFIED.)
GEOMETRIC_REPRESENTATION_ITEM()
RATIONAL_B_SPLINE_SURFACE(((1.00008915600338,0.793434085499743,1.),(1.00008930224991,
0.793095246303286,1.),(1.00008944684613,0.792760230720563,1.),(1.00008958984392,
0.792428918540595,1.)))
REPRESENTATION_ITEM('')
SURFACE()
);
#3709=(
BOUNDED_SURFACE()
B_SPLINE_SURFACE(3,2,((#436767,#436768,#436769),(#436770,#436771,#436772),
(#436773,#436774,#436775),(#436776,#436777,#436778),(#436779,#436780,#436781),
(#436782,#436783,#436784)),.UNSPECIFIED.,.F.,.F.,.F.)
B_SPLINE_SURFACE_WITH_KNOTS((4,2,4),(3,3),(3.04931861011548E-19,7.62675010863197E-5,
0.000152535002172639),(0.,1.02152348203062),.UNSPECIFIED.)
GEOMETRIC_REPRESENTATION_ITEM()
RATIONAL_B_SPLINE_SURFACE(((1.,0.789033595401263,1.00908146323689),(1.,
0.857071781054836,1.00615262590427),(1.,0.922087264710742,1.00335390671591),
(1.,0.922394466502368,1.00334068261143),(1.,0.857224384599067,1.00614605678499),
(1.,0.789033595401662,1.00908146323687)))
REPRESENTATION_ITEM('')
SURFACE()
);
#3710=(
BOUNDED_SURFACE()
B_SPLINE_SURFACE(3,2,((#436786,#436787,#436788),(#436789,#436790,#436791),
(#436792,#436793,#436794),(#436795,#436796,#436797)),.UNSPECIFIED.,.F.,
 .F.,.F.)
B_SPLINE_SURFACE_WITH_KNOTS((4,4),(3,3),(-1.0842021724855E-19,4.8874751296988E-5),
(-0.000215489856966908,1.),.UNSPECIFIED.)
GEOMETRIC_REPRESENTATION_ITEM()
RATIONAL_B_SPLINE_SURFACE(((1.0000894588971,0.792428983985754,1.),(1.00008931610832,
0.792760296061314,1.),(1.00008917172344,0.793095311538369,1.),(1.00008902569067,
0.79343415062801,1.)))
REPRESENTATION_ITEM('')
SURFACE()
);
#3711=(
BOUNDED_SURFACE()
B_SPLINE_SURFACE(3,2,((#436799,#436800,#436801),(#436802,#436803,#436804),
(#436805,#436806,#436807),(#436808,#436809,#436810)),.UNSPECIFIED.,.F.,
 .F.,.F.)
B_SPLINE_SURFACE_WITH_KNOTS((4,4),(3,3),(-5.21974905013083E-6,5.74172395514388E-5),
(-0.00139822857789422,1.00051312364094),.UNSPECIFIED.)
GEOMETRIC_REPRESENTATION_ITEM()
RATIONAL_B_SPLINE_SURFACE(((1.00049256947262,0.823768952243901,1.00018060397859),
(1.00048448215732,0.826662424388206,1.00017763870891),(1.00052427784041,
0.812424361909259,1.00019223006931),(1.00059912365877,0.785646094632617,
1.00021967280243)))
REPRESENTATION_ITEM('')
SURFACE()
);
#3712=(
BOUNDED_SURFACE()
B_SPLINE_SURFACE(3,2,((#436814,#436815,#436816),(#436817,#436818,#436819),
(#436820,#436821,#436822),(#436823,#436824,#436825)),.UNSPECIFIED.,.F.,
 .F.,.F.)
B_SPLINE_SURFACE_WITH_KNOTS((4,4),(3,3),(3.22980774337778E-5,9.63764854872253E-5),
(-0.00154325936380046,1.01095292447544),.UNSPECIFIED.)
GEOMETRIC_REPRESENTATION_ITEM()
RATIONAL_B_SPLINE_SURFACE(((1.000235309833,0.922925743796158,1.00168574728331),
(1.00015136166126,0.950422439594206,1.0010843469906),(1.000335743374,0.890029368953957,
1.00240524789548),(1.00054260094224,0.822274473168322,1.00388716464858)))
REPRESENTATION_ITEM('')
SURFACE()
);
#3713=(
BOUNDED_SURFACE()
B_SPLINE_SURFACE(3,2,((#436925,#436926,#436927),(#436928,#436929,#436930),
(#436931,#436932,#436933),(#436934,#436935,#436936)),.UNSPECIFIED.,.F.,
 .F.,.F.)
B_SPLINE_SURFACE_WITH_KNOTS((4,4),(3,3),(-2.16840434497101E-19,0.000101260117256738),
(0.,1.),.UNSPECIFIED.)
GEOMETRIC_REPRESENTATION_ITEM()
RATIONAL_B_SPLINE_SURFACE(((1.,0.796615278835174,1.),(1.,0.79589603805594,
1.),(1.,0.795193354661349,1.),(1.,0.794506193185548,1.)))
REPRESENTATION_ITEM('')
SURFACE()
);
#3714=(
BOUNDED_SURFACE()
B_SPLINE_SURFACE(3,2,((#436974,#436975,#436976),(#436977,#436978,#436979),
(#436980,#436981,#436982),(#436983,#436984,#436985),(#436986,#436987,#436988),
(#436989,#436990,#436991)),.UNSPECIFIED.,.F.,.F.,.F.)
B_SPLINE_SURFACE_WITH_KNOTS((4,2,4),(3,3),(5.0821976835258E-21,1.66936432462294E-5,
3.33872864924587E-5),(0.,1.),.UNSPECIFIED.)
GEOMETRIC_REPRESENTATION_ITEM()
RATIONAL_B_SPLINE_SURFACE(((1.,0.79661527883518,1.),(1.,0.862310524418134,
1.),(1.,0.923774472010521,1.),(1.,0.923983993203426,1.),(1.,0.862574873720943,
1.),(1.,0.796615278835189,1.)))
REPRESENTATION_ITEM('')
SURFACE()
);
#3715=(
BOUNDED_SURFACE()
B_SPLINE_SURFACE(3,2,((#437028,#437029,#437030),(#437031,#437032,#437033),
(#437034,#437035,#437036),(#437037,#437038,#437039)),.UNSPECIFIED.,.F.,
 .F.,.F.)
B_SPLINE_SURFACE_WITH_KNOTS((4,4),(3,3),(0.,0.000101244905251112),(0.,1.),
 .UNSPECIFIED.)
GEOMETRIC_REPRESENTATION_ITEM()
RATIONAL_B_SPLINE_SURFACE(((1.,0.796615278835174,1.),(1.,0.795896146109795,
1.),(1.,0.795193565796497,1.),(1.,0.794506502889902,1.)))
REPRESENTATION_ITEM('')
SURFACE()
);
#3716=(
BOUNDED_SURFACE()
B_SPLINE_SURFACE(3,2,((#437075,#437076,#437077),(#437078,#437079,#437080),
(#437081,#437082,#437083),(#437084,#437085,#437086)),.UNSPECIFIED.,.F.,
 .F.,.F.)
B_SPLINE_SURFACE_WITH_KNOTS((4,4),(3,3),(2.85968127239939E-5,9.24681548475814E-5),
(-0.00167900678654074,1.0113082712781),.UNSPECIFIED.)
GEOMETRIC_REPRESENTATION_ITEM()
RATIONAL_B_SPLINE_SURFACE(((1.00059040895217,0.822187541868294,1.00401468696652),
(1.0003652771814,0.889990093671587,1.00248382673388),(1.00016469515013,
0.950399042257939,1.0011199008251),(1.00025604273992,0.922888044286088,
1.00174104990629)))
REPRESENTATION_ITEM('')
SURFACE()
);
#3717=(
BOUNDED_SURFACE()
B_SPLINE_SURFACE(3,2,((#437090,#437091,#437092),(#437093,#437094,#437095),
(#437096,#437097,#437098),(#437099,#437100,#437101)),.UNSPECIFIED.,.F.,
 .F.,.F.)
B_SPLINE_SURFACE_WITH_KNOTS((4,4),(3,3),(-5.22358356749296E-6,5.74594192424277E-5),
(-0.00127120052090352,1.),.UNSPECIFIED.)
GEOMETRIC_REPRESENTATION_ITEM()
RATIONAL_B_SPLINE_SURFACE(((1.0005444931319,0.785835073638689,1.),(1.00047707767488,
0.812351526358792,1.),(1.00044031788598,0.826810216506226,1.),(1.00044777653331,
0.823876514387197,1.)))
REPRESENTATION_ITEM('')
SURFACE()
);
#3718=(
BOUNDED_SURFACE()
B_SPLINE_SURFACE(3,2,((#437103,#437104,#437105),(#437106,#437107,#437108),
(#437109,#437110,#437111),(#437112,#437113,#437114)),.UNSPECIFIED.,.F.,
 .F.,.F.)
B_SPLINE_SURFACE_WITH_KNOTS((4,4),(3,3),(-2.71050543121376E-19,4.88747512969881E-5),
(-0.000215805215783492,1.),.UNSPECIFIED.)
GEOMETRIC_REPRESENTATION_ITEM()
RATIONAL_B_SPLINE_SURFACE(((1.0000891560035,0.793434085499686,1.),(1.00008930225004,
0.793095246303234,1.),(1.00008944684626,0.792760230720494,1.),(1.00008958984405,
0.792428918540536,1.)))
REPRESENTATION_ITEM('')
SURFACE()
);
#3719=(
BOUNDED_SURFACE()
B_SPLINE_SURFACE(3,2,((#437116,#437117,#437118),(#437119,#437120,#437121),
(#437122,#437123,#437124),(#437125,#437126,#437127),(#437128,#437129,#437130),
(#437131,#437132,#437133)),.UNSPECIFIED.,.F.,.F.,.F.)
B_SPLINE_SURFACE_WITH_KNOTS((4,2,4),(3,3),(2.91379333855479E-19,7.62675010863198E-5,
0.000152535002172639),(0.,1.02152348203046),.UNSPECIFIED.)
GEOMETRIC_REPRESENTATION_ITEM()
RATIONAL_B_SPLINE_SURFACE(((1.,0.789033595401294,1.00908146323682),(1.,
0.857071781054879,1.00615262590422),(1.,0.922087264710734,1.00335390671588),
(1.,0.9223944665024,1.0033406826114),(1.,0.857224384599077,1.00614605678494),
(1.,0.789033595401694,1.0090814632368)))
REPRESENTATION_ITEM('')
SURFACE()
);
#3720=(
BOUNDED_SURFACE()
B_SPLINE_SURFACE(3,2,((#437135,#437136,#437137),(#437138,#437139,#437140),
(#437141,#437142,#437143),(#437144,#437145,#437146)),.UNSPECIFIED.,.F.,
 .F.,.F.)
B_SPLINE_SURFACE_WITH_KNOTS((4,4),(3,3),(3.25260651745651E-19,4.88747512969884E-5),
(-0.000215489857083527,1.),.UNSPECIFIED.)
GEOMETRIC_REPRESENTATION_ITEM()
RATIONAL_B_SPLINE_SURFACE(((1.00008945889715,0.792428983985737,1.),(1.00008931610837,
0.792760296061273,1.),(1.00008917172349,0.793095311538366,1.),(1.00008902569072,
0.793434150627984,1.)))
REPRESENTATION_ITEM('')
SURFACE()
);
#3721=(
BOUNDED_SURFACE()
B_SPLINE_SURFACE(3,2,((#437148,#437149,#437150),(#437151,#437152,#437153),
(#437154,#437155,#437156),(#437157,#437158,#437159)),.UNSPECIFIED.,.F.,
 .F.,.F.)
B_SPLINE_SURFACE_WITH_KNOTS((4,4),(3,3),(-5.21974905013089E-6,5.74172395514386E-5),
(-0.00139822857702801,1.00051312364039),.UNSPECIFIED.)
GEOMETRIC_REPRESENTATION_ITEM()
RATIONAL_B_SPLINE_SURFACE(((1.00049256947232,0.823768952244153,1.0001806039784),
(1.00048448215702,0.826662424388442,1.00017763870873),(1.00052427784009,
0.81242436190953,1.00019223006911),(1.0005991236584,0.785646094632913,1.00021967280219)))
REPRESENTATION_ITEM('')
SURFACE()
);
#3722=(
BOUNDED_SURFACE()
B_SPLINE_SURFACE(3,2,((#437163,#437164,#437165),(#437166,#437167,#437168),
(#437169,#437170,#437171),(#437172,#437173,#437174)),.UNSPECIFIED.,.F.,
 .F.,.F.)
B_SPLINE_SURFACE_WITH_KNOTS((4,4),(3,3),(3.22980774337781E-5,9.63764854872258E-5),
(-0.00154325936375446,1.01095292447528),.UNSPECIFIED.)
GEOMETRIC_REPRESENTATION_ITEM()
RATIONAL_B_SPLINE_SURFACE(((1.00023530983299,0.922925743796172,1.00168574728329),
(1.00015136166126,0.950422439594222,1.00108434699058),(1.00033574337399,
0.89002936895397,1.00240524789544),(1.00054260094222,0.822274473168358,
1.00388716464853)))
REPRESENTATION_ITEM('')
SURFACE()
);
#3723=(
BOUNDED_SURFACE()
B_SPLINE_SURFACE(3,2,((#437274,#437275,#437276),(#437277,#437278,#437279),
(#437280,#437281,#437282),(#437283,#437284,#437285)),.UNSPECIFIED.,.F.,
 .F.,.F.)
B_SPLINE_SURFACE_WITH_KNOTS((4,4),(3,3),(0.,0.000101260117256736),(0.,1.),
 .UNSPECIFIED.)
GEOMETRIC_REPRESENTATION_ITEM()
RATIONAL_B_SPLINE_SURFACE(((1.,0.79661527883517,1.),(1.,0.795896038055932,
1.),(1.,0.795193354661359,1.),(1.,0.794506193185534,1.)))
REPRESENTATION_ITEM('')
SURFACE()
);
#3724=(
BOUNDED_SURFACE()
B_SPLINE_SURFACE(3,2,((#437323,#437324,#437325),(#437326,#437327,#437328),
(#437329,#437330,#437331),(#437332,#437333,#437334),(#437335,#437336,#437337),
(#437338,#437339,#437340)),.UNSPECIFIED.,.F.,.F.,.F.)
B_SPLINE_SURFACE_WITH_KNOTS((4,2,4),(3,3),(1.21972744404619E-19,1.66936432462291E-5,
3.33872864924582E-5),(0.,1.),.UNSPECIFIED.)
GEOMETRIC_REPRESENTATION_ITEM()
RATIONAL_B_SPLINE_SURFACE(((1.,0.796615278835175,1.),(1.,0.862310524418131,
1.),(1.,0.923774472010521,1.),(1.,0.923983993203428,1.),(1.,0.862574873720943,
1.),(1.,0.796615278835187,1.)))
REPRESENTATION_ITEM('')
SURFACE()
);
#3725=(
BOUNDED_SURFACE()
B_SPLINE_SURFACE(3,2,((#437377,#437378,#437379),(#437380,#437381,#437382),
(#437383,#437384,#437385),(#437386,#437387,#437388)),.UNSPECIFIED.,.F.,
 .F.,.F.)
B_SPLINE_SURFACE_WITH_KNOTS((4,4),(3,3),(0.,0.000101244905251112),(0.,1.),
 .UNSPECIFIED.)
GEOMETRIC_REPRESENTATION_ITEM()
RATIONAL_B_SPLINE_SURFACE(((1.,0.796615278835171,1.),(1.,0.795896146109793,
1.),(1.,0.7951935657965,1.),(1.,0.794506502889898,1.)))
REPRESENTATION_ITEM('')
SURFACE()
);
#3726=(
BOUNDED_SURFACE()
B_SPLINE_SURFACE(3,2,((#437424,#437425,#437426),(#437427,#437428,#437429),
(#437430,#437431,#437432),(#437433,#437434,#437435)),.UNSPECIFIED.,.F.,
 .F.,.F.)
B_SPLINE_SURFACE_WITH_KNOTS((4,4),(3,3),(2.85968127239939E-5,9.24681548475816E-5),
(-0.00167900678767833,1.01130827127821),.UNSPECIFIED.)
GEOMETRIC_REPRESENTATION_ITEM()
RATIONAL_B_SPLINE_SURFACE(((1.00059040895257,0.822187541868073,1.00401468696656),
(1.00036527718164,0.889990093671444,1.00248382673391),(1.00016469515024,
0.950399042257875,1.00111990082511),(1.0002560427401,0.922888044285992,
1.00174104990631)))
REPRESENTATION_ITEM('')
SURFACE()
);
#3727=(
BOUNDED_SURFACE()
B_SPLINE_SURFACE(3,2,((#437439,#437440,#437441),(#437442,#437443,#437444),
(#437445,#437446,#437447),(#437448,#437449,#437450)),.UNSPECIFIED.,.F.,
 .F.,.F.)
B_SPLINE_SURFACE_WITH_KNOTS((4,4),(3,3),(-5.22358356749301E-6,5.7459419242428E-5),
(-0.00127120052059091,1.),.UNSPECIFIED.)
GEOMETRIC_REPRESENTATION_ITEM()
RATIONAL_B_SPLINE_SURFACE(((1.00054449313177,0.785835073638755,1.),(1.00047707767476,
0.812351526358847,1.),(1.00044031788588,0.82681021650628,1.),(1.0004477765332,
0.823876514387243,1.)))
REPRESENTATION_ITEM('')
SURFACE()
);
#3728=(
BOUNDED_SURFACE()
B_SPLINE_SURFACE(3,2,((#437452,#437453,#437454),(#437455,#437456,#437457),
(#437458,#437459,#437460),(#437461,#437462,#437463)),.UNSPECIFIED.,.F.,
 .F.,.F.)
B_SPLINE_SURFACE_WITH_KNOTS((4,4),(3,3),(-1.35525271560688E-19,4.88747512969881E-5),
(-0.000215805216124583,1.),.UNSPECIFIED.)
GEOMETRIC_REPRESENTATION_ITEM()
RATIONAL_B_SPLINE_SURFACE(((1.00008915600365,0.793434085499612,1.),(1.00008930225018,
0.793095246303167,1.),(1.0000894468464,0.792760230720414,1.),(1.00008958984419,
0.792428918540462,1.)))
REPRESENTATION_ITEM('')
SURFACE()
);
#3729=(
BOUNDED_SURFACE()
B_SPLINE_SURFACE(3,2,((#437465,#437466,#437467),(#437468,#437469,#437470),
(#437471,#437472,#437473),(#437474,#437475,#437476),(#437477,#437478,#437479),
(#437480,#437481,#437482)),.UNSPECIFIED.,.F.,.F.,.F.)
B_SPLINE_SURFACE_WITH_KNOTS((4,2,4),(3,3),(-2.71050543121376E-20,7.62675010863192E-5,
0.000152535002172638),(0.,1.02152348203063),.UNSPECIFIED.)
GEOMETRIC_REPRESENTATION_ITEM()
RATIONAL_B_SPLINE_SURFACE(((1.,0.789033595401261,1.0090814632369),(1.,0.857071781054855,
1.00615262590427),(1.,0.922087264710718,1.00335390671591),(1.,0.922394466502388,
1.00334068261143),(1.,0.857224384599047,1.00614605678499),(1.,0.789033595401658,
1.00908146323688)))
REPRESENTATION_ITEM('')
SURFACE()
);
#3730=(
BOUNDED_SURFACE()
B_SPLINE_SURFACE(3,2,((#437484,#437485,#437486),(#437487,#437488,#437489),
(#437490,#437491,#437492),(#437493,#437494,#437495)),.UNSPECIFIED.,.F.,
 .F.,.F.)
B_SPLINE_SURFACE_WITH_KNOTS((4,4),(3,3),(3.79470760369927E-19,4.88747512969882E-5),
(-0.000215489857057505,1.),.UNSPECIFIED.)
GEOMETRIC_REPRESENTATION_ITEM()
RATIONAL_B_SPLINE_SURFACE(((1.00008945889714,0.792428983985739,1.),(1.00008931610836,
0.792760296061291,1.),(1.00008917172348,0.793095311538347,1.),(1.00008902569071,
0.793434150627992,1.)))
REPRESENTATION_ITEM('')
SURFACE()
);
#3731=(
BOUNDED_SURFACE()
B_SPLINE_SURFACE(3,2,((#437497,#437498,#437499),(#437500,#437501,#437502),
(#437503,#437504,#437505),(#437506,#437507,#437508)),.UNSPECIFIED.,.F.,
 .F.,.F.)
B_SPLINE_SURFACE_WITH_KNOTS((4,4),(3,3),(-5.21974905012869E-6,5.74172395514399E-5),
(-0.00139822857743797,1.00051312364057),.UNSPECIFIED.)
GEOMETRIC_REPRESENTATION_ITEM()
RATIONAL_B_SPLINE_SURFACE(((1.00049256947246,0.823768952244043,1.00018060397846),
(1.00048448215717,0.826662424388345,1.00017763870879),(1.00052427784024,
0.812424361909404,1.00019223006918),(1.00059912365858,0.785646094632793,
1.00021967280227)))
REPRESENTATION_ITEM('')
SURFACE()
);
#3732=(
BOUNDED_SURFACE()
B_SPLINE_SURFACE(3,2,((#437512,#437513,#437514),(#437515,#437516,#437517),
(#437518,#437519,#437520),(#437521,#437522,#437523)),.UNSPECIFIED.,.F.,
 .F.,.F.)
B_SPLINE_SURFACE_WITH_KNOTS((4,4),(3,3),(3.22980774337777E-5,9.6376485487225E-5),
(-0.00154325936378919,1.01095292447567),.UNSPECIFIED.)
GEOMETRIC_REPRESENTATION_ITEM()
RATIONAL_B_SPLINE_SURFACE(((1.000235309833,0.922925743796142,1.00168574728335),
(1.00015136166126,0.9504224395942,1.00108434699062),(1.000335743374,0.890029368953935,
1.00240524789553),(1.00054260094223,0.822274473168277,1.00388716464867)))
REPRESENTATION_ITEM('')
SURFACE()
);
#3733=(
BOUNDED_SURFACE()
B_SPLINE_SURFACE(3,2,((#437623,#437624,#437625),(#437626,#437627,#437628),
(#437629,#437630,#437631),(#437632,#437633,#437634)),.UNSPECIFIED.,.F.,
 .F.,.F.)
B_SPLINE_SURFACE_WITH_KNOTS((4,4),(3,3),(0.,0.000101260117256738),(0.,1.),
 .UNSPECIFIED.)
GEOMETRIC_REPRESENTATION_ITEM()
RATIONAL_B_SPLINE_SURFACE(((1.,0.796615278835171,1.),(1.,0.795896038055941,
1.),(1.,0.795193354661341,1.),(1.,0.794506193185546,1.)))
REPRESENTATION_ITEM('')
SURFACE()
);
#3734=(
BOUNDED_SURFACE()
B_SPLINE_SURFACE(3,2,((#437672,#437673,#437674),(#437675,#437676,#437677),
(#437678,#437679,#437680),(#437681,#437682,#437683),(#437684,#437685,#437686),
(#437687,#437688,#437689)),.UNSPECIFIED.,.F.,.F.,.F.)
B_SPLINE_SURFACE_WITH_KNOTS((4,2,4),(3,3),(4.45539330255762E-19,1.66936432462296E-5,
3.33872864924588E-5),(0.,1.),.UNSPECIFIED.)
GEOMETRIC_REPRESENTATION_ITEM()
RATIONAL_B_SPLINE_SURFACE(((1.,0.79661527883518,1.),(1.,0.862310524418132,
1.),(1.,0.923774472010522,1.),(1.,0.923983993203426,1.),(1.,0.862574873720932,
1.),(1.,0.796615278835189,1.)))
REPRESENTATION_ITEM('')
SURFACE()
);
#3735=(
BOUNDED_SURFACE()
B_SPLINE_SURFACE(3,2,((#437726,#437727,#437728),(#437729,#437730,#437731),
(#437732,#437733,#437734),(#437735,#437736,#437737)),.UNSPECIFIED.,.F.,
 .F.,.F.)
B_SPLINE_SURFACE_WITH_KNOTS((4,4),(3,3),(-2.16840434497101E-19,0.000101244905251112),
(0.,1.),.UNSPECIFIED.)
GEOMETRIC_REPRESENTATION_ITEM()
RATIONAL_B_SPLINE_SURFACE(((1.,0.796615278835168,1.),(1.,0.795896146109797,
1.),(1.,0.795193565796497,1.),(1.,0.794506502889899,1.)))
REPRESENTATION_ITEM('')
SURFACE()
);
#3736=(
BOUNDED_SURFACE()
B_SPLINE_SURFACE(3,2,((#437773,#437774,#437775),(#437776,#437777,#437778),
(#437779,#437780,#437781),(#437782,#437783,#437784)),.UNSPECIFIED.,.F.,
 .F.,.F.)
B_SPLINE_SURFACE_WITH_KNOTS((4,4),(3,3),(2.85968127239939E-5,9.24681548475815E-5),
(-0.00167900678606714,1.01130827127823),.UNSPECIFIED.)
GEOMETRIC_REPRESENTATION_ITEM()
RATIONAL_B_SPLINE_SURFACE(((1.000590408952,0.822187541868358,1.00401468696657),
(1.00036527718129,0.889990093671623,1.00248382673391),(1.00016469515008,
0.950399042257955,1.00111990082511),(1.00025604273985,0.922888044286117,
1.00174104990631)))
REPRESENTATION_ITEM('')
SURFACE()
);
#3737=(
BOUNDED_SURFACE()
B_SPLINE_SURFACE(3,2,((#437788,#437789,#437790),(#437791,#437792,#437793),
(#437794,#437795,#437796),(#437797,#437798,#437799)),.UNSPECIFIED.,.F.,
 .F.,.F.)
B_SPLINE_SURFACE_WITH_KNOTS((4,4),(3,3),(-5.22358356749019E-6,5.74594192424278E-5),
(-0.00127120052048488,1.),.UNSPECIFIED.)
GEOMETRIC_REPRESENTATION_ITEM()
RATIONAL_B_SPLINE_SURFACE(((1.00054449313172,0.785835073638779,0.999999999999999),
(1.00047707767472,0.812351526358877,1.),(1.00044031788584,0.826810216506281,
1.),(1.00044777653316,0.823876514387274,1.)))
REPRESENTATION_ITEM('')
SURFACE()
);
#3738=(
BOUNDED_SURFACE()
B_SPLINE_SURFACE(3,2,((#437801,#437802,#437803),(#437804,#437805,#437806),
(#437807,#437808,#437809),(#437810,#437811,#437812)),.UNSPECIFIED.,.F.,
 .F.,.F.)
B_SPLINE_SURFACE_WITH_KNOTS((4,4),(3,3),(-2.43945488809238E-19,4.88747512969881E-5),
(-0.000215805215277963,1.),.UNSPECIFIED.)
GEOMETRIC_REPRESENTATION_ITEM()
RATIONAL_B_SPLINE_SURFACE(((1.0000891560033,0.793434085499786,1.),(1.00008930224983,
0.793095246303339,1.),(1.00008944684605,0.792760230720593,1.),(1.00008958984384,
0.792428918540633,1.)))
REPRESENTATION_ITEM('')
SURFACE()
);
#3739=(
BOUNDED_SURFACE()
B_SPLINE_SURFACE(3,2,((#437814,#437815,#437816),(#437817,#437818,#437819),
(#437820,#437821,#437822),(#437823,#437824,#437825),(#437826,#437827,#437828),
(#437829,#437830,#437831)),.UNSPECIFIED.,.F.,.F.,.F.)
B_SPLINE_SURFACE_WITH_KNOTS((4,2,4),(3,3),(1.89735380184963E-19,7.62675010863193E-5,
0.000152535002172638),(0.,1.02152348203076),.UNSPECIFIED.)
GEOMETRIC_REPRESENTATION_ITEM()
RATIONAL_B_SPLINE_SURFACE(((1.,0.789033595401233,1.00908146323695),(1.,
0.85707178105484,1.00615262590431),(1.,0.922087264710706,1.00335390671593),
(1.,0.922394466502385,1.00334068261145),(1.,0.857224384599031,1.00614605678503),
(1.,0.789033595401629,1.00908146323694)))
REPRESENTATION_ITEM('')
SURFACE()
);
#3740=(
BOUNDED_SURFACE()
B_SPLINE_SURFACE(3,2,((#437833,#437834,#437835),(#437836,#437837,#437838),
(#437839,#437840,#437841),(#437842,#437843,#437844)),.UNSPECIFIED.,.F.,
 .F.,.F.)
B_SPLINE_SURFACE_WITH_KNOTS((4,4),(3,3),(1.0842021724855E-19,4.88747512969883E-5),
(-0.000215489856960214,1.),.UNSPECIFIED.)
GEOMETRIC_REPRESENTATION_ITEM()
RATIONAL_B_SPLINE_SURFACE(((1.0000894588971,0.79242898398576,1.),(1.00008931610832,
0.792760296061308,1.),(1.00008917172344,0.793095311538373,1.),(1.00008902569067,
0.79343415062801,1.)))
REPRESENTATION_ITEM('')
SURFACE()
);
#3741=(
BOUNDED_SURFACE()
B_SPLINE_SURFACE(3,2,((#437846,#437847,#437848),(#437849,#437850,#437851),
(#437852,#437853,#437854),(#437855,#437856,#437857)),.UNSPECIFIED.,.F.,
 .F.,.F.)
B_SPLINE_SURFACE_WITH_KNOTS((4,4),(3,3),(-5.21974905012869E-6,5.74172395514386E-5),
(-0.00139822857769568,1.00051312364042),.UNSPECIFIED.)
GEOMETRIC_REPRESENTATION_ITEM()
RATIONAL_B_SPLINE_SURFACE(((1.00049256947255,0.823768952244027,1.0001806039784),
(1.00048448215726,0.826662424388324,1.00017763870874),(1.00052427784034,
0.812424361909387,1.00019223006912),(1.00059912365869,0.785646094632771,
1.0002196728022)))
REPRESENTATION_ITEM('')
SURFACE()
);
#3742=(
BOUNDED_SURFACE()
B_SPLINE_SURFACE(3,2,((#437861,#437862,#437863),(#437864,#437865,#437866),
(#437867,#437868,#437869),(#437870,#437871,#437872)),.UNSPECIFIED.,.F.,
 .F.,.F.)
B_SPLINE_SURFACE_WITH_KNOTS((4,4),(3,3),(3.22980774337778E-5,9.63764854872255E-5),
(-0.00154325936389316,1.01095292447562),.UNSPECIFIED.)
GEOMETRIC_REPRESENTATION_ITEM()
RATIONAL_B_SPLINE_SURFACE(((1.00023530983301,0.922925743796137,1.00168574728334),
(1.00015136166127,0.950422439594205,1.00108434699062),(1.00033574337402,
0.890029368953915,1.00240524789552),(1.00054260094227,0.822274473168278,
1.00388716464865)))
REPRESENTATION_ITEM('')
SURFACE()
);
#3743=(
BOUNDED_SURFACE()
B_SPLINE_SURFACE(3,2,((#437972,#437973,#437974),(#437975,#437976,#437977),
(#437978,#437979,#437980),(#437981,#437982,#437983)),.UNSPECIFIED.,.F.,
 .F.,.F.)
B_SPLINE_SURFACE_WITH_KNOTS((4,4),(3,3),(2.16840434497101E-19,0.000101260117256738),
(0.,1.),.UNSPECIFIED.)
GEOMETRIC_REPRESENTATION_ITEM()
RATIONAL_B_SPLINE_SURFACE(((1.,0.796615278835169,1.),(1.,0.795896038055941,
1.),(1.,0.795193354661347,1.),(1.,0.794506193185546,1.)))
REPRESENTATION_ITEM('')
SURFACE()
);
#3744=(
BOUNDED_SURFACE()
B_SPLINE_SURFACE(3,2,((#438021,#438022,#438023),(#438024,#438025,#438026),
(#438027,#438028,#438029),(#438030,#438031,#438032),(#438033,#438034,#438035),
(#438036,#438037,#438038)),.UNSPECIFIED.,.F.,.F.,.F.)
B_SPLINE_SURFACE_WITH_KNOTS((4,2,4),(3,3),(1.77876918923403E-19,1.66936432462298E-5,
3.33872864924594E-5),(0.,1.),.UNSPECIFIED.)
GEOMETRIC_REPRESENTATION_ITEM()
RATIONAL_B_SPLINE_SURFACE(((1.,0.796615278835173,1.),(1.,0.862310524418123,
1.),(1.,0.923774472010521,1.),(1.,0.923983993203424,1.),(1.,0.862574873720951,
1.),(1.,0.796615278835182,1.)))
REPRESENTATION_ITEM('')
SURFACE()
);
#3745=(
BOUNDED_SURFACE()
B_SPLINE_SURFACE(3,2,((#438075,#438076,#438077),(#438078,#438079,#438080),
(#438081,#438082,#438083),(#438084,#438085,#438086)),.UNSPECIFIED.,.F.,
 .F.,.F.)
B_SPLINE_SURFACE_WITH_KNOTS((4,4),(3,3),(0.,0.000101244905251112),(0.,1.),
 .UNSPECIFIED.)
GEOMETRIC_REPRESENTATION_ITEM()
RATIONAL_B_SPLINE_SURFACE(((1.,0.796615278835169,1.),(1.,0.795896146109798,
1.),(1.,0.795193565796496,1.),(1.,0.794506502889901,1.)))
REPRESENTATION_ITEM('')
SURFACE()
);
#3746=(
BOUNDED_SURFACE()
B_SPLINE_SURFACE(3,2,((#438122,#438123,#438124),(#438125,#438126,#438127),
(#438128,#438129,#438130),(#438131,#438132,#438133)),.UNSPECIFIED.,.F.,
 .F.,.F.)
B_SPLINE_SURFACE_WITH_KNOTS((4,4),(3,3),(2.85968127239939E-5,9.24681548475816E-5),
(-0.00167900679302498,1.01130827127816),.UNSPECIFIED.)
GEOMETRIC_REPRESENTATION_ITEM()
RATIONAL_B_SPLINE_SURFACE(((1.00059040895445,0.822187541867124,1.00401468696654),
(1.00036527718281,0.889990093670864,1.0024838267339),(1.00016469515077,
0.950399042257607,1.0011199008251),(1.00025604274091,0.922888044285581,
1.0017410499063)))
REPRESENTATION_ITEM('')
SURFACE()
);
#3747=(
BOUNDED_SURFACE()
B_SPLINE_SURFACE(3,2,((#438137,#438138,#438139),(#438140,#438141,#438142),
(#438143,#438144,#438145),(#438146,#438147,#438148)),.UNSPECIFIED.,.F.,
 .F.,.F.)
B_SPLINE_SURFACE_WITH_KNOTS((4,4),(3,3),(-5.22358356749285E-6,5.74594192424277E-5),
(-0.00127120052057846,1.),.UNSPECIFIED.)
GEOMETRIC_REPRESENTATION_ITEM()
RATIONAL_B_SPLINE_SURFACE(((1.00054449313176,0.785835073638763,1.),(1.00047707767476,
0.812351526358834,1.),(1.00044031788587,0.826810216506288,1.),(1.00044777653319,
0.82387651438725,1.)))
REPRESENTATION_ITEM('')
SURFACE()
);
#3748=(
BOUNDED_SURFACE()
B_SPLINE_SURFACE(3,2,((#438150,#438151,#438152),(#438153,#438154,#438155),
(#438156,#438157,#438158),(#438159,#438160,#438161)),.UNSPECIFIED.,.F.,
 .F.,.F.)
B_SPLINE_SURFACE_WITH_KNOTS((4,4),(3,3),(-8.13151629364128E-20,4.8874751296988E-5),
(-0.000215805215388037,1.),.UNSPECIFIED.)
GEOMETRIC_REPRESENTATION_ITEM()
RATIONAL_B_SPLINE_SURFACE(((1.00008915600334,0.793434085499765,1.),(1.00008930224987,
0.793095246303302,1.),(1.00008944684609,0.792760230720584,1.),(1.00008958984389,
0.792428918540612,1.)))
REPRESENTATION_ITEM('')
SURFACE()
);
#3749=(
BOUNDED_SURFACE()
B_SPLINE_SURFACE(3,2,((#438163,#438164,#438165),(#438166,#438167,#438168),
(#438169,#438170,#438171),(#438172,#438173,#438174),(#438175,#438176,#438177),
(#438178,#438179,#438180)),.UNSPECIFIED.,.F.,.F.,.F.)
B_SPLINE_SURFACE_WITH_KNOTS((4,2,4),(3,3),(8.13151629364128E-20,7.62675010863197E-5,
0.000152535002172639),(0.,1.02152348203066),.UNSPECIFIED.)
GEOMETRIC_REPRESENTATION_ITEM()
RATIONAL_B_SPLINE_SURFACE(((1.,0.789033595401252,1.00908146323691),(1.,
0.857071781054831,1.00615262590428),(1.,0.922087264710747,1.00335390671592),
(1.,0.922394466502359,1.00334068261143),(1.,0.857224384599067,1.006146056785),
(1.,0.789033595401652,1.00908146323689)))
REPRESENTATION_ITEM('')
SURFACE()
);
#3750=(
BOUNDED_SURFACE()
B_SPLINE_SURFACE(3,2,((#438182,#438183,#438184),(#438185,#438186,#438187),
(#438188,#438189,#438190),(#438191,#438192,#438193)),.UNSPECIFIED.,.F.,
 .F.,.F.)
B_SPLINE_SURFACE_WITH_KNOTS((4,4),(3,3),(2.71050543121376E-19,4.88747512969882E-5),
(-0.00021548985699875,1.),.UNSPECIFIED.)
GEOMETRIC_REPRESENTATION_ITEM()
RATIONAL_B_SPLINE_SURFACE(((1.00008945889712,0.792428983985752,1.),(1.00008931610833,
0.792760296061301,1.),(1.00008917172346,0.793095311538365,1.),(1.00008902569068,
0.793434150628002,1.)))
REPRESENTATION_ITEM('')
SURFACE()
);
#3751=(
BOUNDED_SURFACE()
B_SPLINE_SURFACE(3,2,((#438195,#438196,#438197),(#438198,#438199,#438200),
(#438201,#438202,#438203),(#438204,#438205,#438206)),.UNSPECIFIED.,.F.,
 .F.,.F.)
B_SPLINE_SURFACE_WITH_KNOTS((4,4),(3,3),(-5.21974905013094E-6,5.74172395514392E-5),
(-0.00139822857772714,1.00051312364077),.UNSPECIFIED.)
GEOMETRIC_REPRESENTATION_ITEM()
RATIONAL_B_SPLINE_SURFACE(((1.00049256947256,0.823768952243963,1.00018060397853),
(1.00048448215727,0.826662424388249,1.00017763870886),(1.00052427784035,
0.812424361909331,1.00019223006925),(1.0005991236587,0.785646094632682,
1.00021967280235)))
REPRESENTATION_ITEM('')
SURFACE()
);
#3752=(
BOUNDED_SURFACE()
B_SPLINE_SURFACE(3,2,((#438210,#438211,#438212),(#438213,#438214,#438215),
(#438216,#438217,#438218),(#438219,#438220,#438221)),.UNSPECIFIED.,.F.,
 .F.,.F.)
B_SPLINE_SURFACE_WITH_KNOTS((4,4),(3,3),(3.22980774337784E-5,9.63764854872253E-5),
(-0.0015432593633078,1.01095292447534),.UNSPECIFIED.)
GEOMETRIC_REPRESENTATION_ITEM()
RATIONAL_B_SPLINE_SURFACE(((1.00023530983292,0.922925743796203,1.0016857472833),
(1.00015136166121,0.950422439594246,1.00108434699059),(1.00033574337389,
0.890029368954014,1.00240524789546),(1.00054260094206,0.822274473168425,
1.00388716464855)))
REPRESENTATION_ITEM('')
SURFACE()
);
#3753=(
BOUNDED_SURFACE()
B_SPLINE_SURFACE(3,2,((#438321,#438322,#438323),(#438324,#438325,#438326),
(#438327,#438328,#438329),(#438330,#438331,#438332)),.UNSPECIFIED.,.F.,
 .F.,.F.)
B_SPLINE_SURFACE_WITH_KNOTS((4,4),(3,3),(-2.16840434497101E-19,0.000101260117256738),
(0.,1.),.UNSPECIFIED.)
GEOMETRIC_REPRESENTATION_ITEM()
RATIONAL_B_SPLINE_SURFACE(((1.,0.796615278835171,1.),(1.,0.795896038055941,
1.),(1.,0.795193354661347,1.),(1.,0.794506193185546,1.)))
REPRESENTATION_ITEM('')
SURFACE()
);
#3754=(
BOUNDED_SURFACE()
B_SPLINE_SURFACE(3,2,((#438370,#438371,#438372),(#438373,#438374,#438375),
(#438376,#438377,#438378),(#438379,#438380,#438381),(#438382,#438383,#438384),
(#438385,#438386,#438387)),.UNSPECIFIED.,.F.,.F.,.F.)
B_SPLINE_SURFACE_WITH_KNOTS((4,2,4),(3,3),(8.30092288309214E-20,1.66936432462294E-5,
3.33872864924587E-5),(0.,1.),.UNSPECIFIED.)
GEOMETRIC_REPRESENTATION_ITEM()
RATIONAL_B_SPLINE_SURFACE(((1.,0.796615278835175,1.),(1.,0.862310524418132,
1.),(1.,0.92377447201052,1.),(1.,0.923983993203425,1.),(1.,0.862574873720945,
1.),(1.,0.796615278835182,1.)))
REPRESENTATION_ITEM('')
SURFACE()
);
#3755=(
BOUNDED_SURFACE()
B_SPLINE_SURFACE(3,2,((#438424,#438425,#438426),(#438427,#438428,#438429),
(#438430,#438431,#438432),(#438433,#438434,#438435)),.UNSPECIFIED.,.F.,
 .F.,.F.)
B_SPLINE_SURFACE_WITH_KNOTS((4,4),(3,3),(-2.16840434497101E-19,0.000101244905251112),
(0.,1.),.UNSPECIFIED.)
GEOMETRIC_REPRESENTATION_ITEM()
RATIONAL_B_SPLINE_SURFACE(((1.,0.796615278835169,1.),(1.,0.795896146109793,
1.),(1.,0.795193565796498,1.),(1.,0.794506502889898,1.)))
REPRESENTATION_ITEM('')
SURFACE()
);
#3756=(
BOUNDED_SURFACE()
B_SPLINE_SURFACE(3,2,((#438471,#438472,#438473),(#438474,#438475,#438476),
(#438477,#438478,#438479),(#438480,#438481,#438482)),.UNSPECIFIED.,.F.,
 .F.,.F.)
B_SPLINE_SURFACE_WITH_KNOTS((4,4),(3,3),(2.85968127239939E-5,9.24681548475819E-5),
(-0.0016790067865302,1.01130827127821),.UNSPECIFIED.)
GEOMETRIC_REPRESENTATION_ITEM()
RATIONAL_B_SPLINE_SURFACE(((1.00059040895216,0.822187541868273,1.00401468696656),
(1.00036527718139,0.889990093671574,1.00248382673391),(1.00016469515013,
0.950399042257933,1.00111990082511),(1.00025604273992,0.922888044286081,
1.00174104990631)))
REPRESENTATION_ITEM('')
SURFACE()
);
#3757=(
BOUNDED_SURFACE()
B_SPLINE_SURFACE(3,2,((#438486,#438487,#438488),(#438489,#438490,#438491),
(#438492,#438493,#438494),(#438495,#438496,#438497)),.UNSPECIFIED.,.F.,
 .F.,.F.)
B_SPLINE_SURFACE_WITH_KNOTS((4,4),(3,3),(-5.22358356749259E-6,5.7459419242428E-5),
(-0.00127120052070354,1.),.UNSPECIFIED.)
GEOMETRIC_REPRESENTATION_ITEM()
RATIONAL_B_SPLINE_SURFACE(((1.00054449313181,0.785835073638736,1.),(1.0004770776748,
0.812351526358819,1.),(1.00044031788592,0.826810216506259,1.),(1.00044777653324,
0.82387651438723,1.)))
REPRESENTATION_ITEM('')
SURFACE()
);
#3758=(
BOUNDED_SURFACE()
B_SPLINE_SURFACE(3,2,((#438499,#438500,#438501),(#438502,#438503,#438504),
(#438505,#438506,#438507),(#438508,#438509,#438510)),.UNSPECIFIED.,.F.,
 .F.,.F.)
B_SPLINE_SURFACE_WITH_KNOTS((4,4),(3,3),(-4.60785923306339E-19,4.88747512969879E-5),
(-0.000215805215175112,1.),.UNSPECIFIED.)
GEOMETRIC_REPRESENTATION_ITEM()
RATIONAL_B_SPLINE_SURFACE(((1.00008915600325,0.793434085499807,1.),(1.00008930224978,
0.793095246303347,1.),(1.000089446846,0.792760230720625,1.),(1.0000895898438,
0.792428918540656,1.)))
REPRESENTATION_ITEM('')
SURFACE()
);
#3759=(
BOUNDED_SURFACE()
B_SPLINE_SURFACE(3,2,((#438512,#438513,#438514),(#438515,#438516,#438517),
(#438518,#438519,#438520),(#438521,#438522,#438523),(#438524,#438525,#438526),
(#438527,#438528,#438529)),.UNSPECIFIED.,.F.,.F.,.F.)
B_SPLINE_SURFACE_WITH_KNOTS((4,2,4),(3,3),(4.26904605416167E-19,7.62675010863197E-5,
0.000152535002172639),(0.,1.02152348203057),.UNSPECIFIED.)
GEOMETRIC_REPRESENTATION_ITEM()
RATIONAL_B_SPLINE_SURFACE(((1.,0.789033595401272,1.00908146323687),(1.,
0.85707178105485,1.00615262590425),(1.,0.922087264710744,1.0033539067159),
(1.,0.922394466502376,1.00334068261142),(1.,0.857224384599074,1.00614605678497),
(1.,0.789033595401675,1.00908146323685)))
REPRESENTATION_ITEM('')
SURFACE()
);
#3760=(
BOUNDED_SURFACE()
B_SPLINE_SURFACE(3,2,((#438531,#438532,#438533),(#438534,#438535,#438536),
(#438537,#438538,#438539),(#438540,#438541,#438542)),.UNSPECIFIED.,.F.,
 .F.,.F.)
B_SPLINE_SURFACE_WITH_KNOTS((4,4),(3,3),(1.0842021724855E-19,4.88747512969884E-5),
(-0.00021548985702727,1.),.UNSPECIFIED.)
GEOMETRIC_REPRESENTATION_ITEM()
RATIONAL_B_SPLINE_SURFACE(((1.00008945889713,0.792428983985747,1.),(1.00008931610834,
0.792760296061294,1.),(1.00008917172347,0.793095311538357,1.),(1.0000890256907,
0.793434150627996,1.)))
REPRESENTATION_ITEM('')
SURFACE()
);
#3761=(
BOUNDED_SURFACE()
B_SPLINE_SURFACE(3,2,((#438544,#438545,#438546),(#438547,#438548,#438549),
(#438550,#438551,#438552),(#438553,#438554,#438555)),.UNSPECIFIED.,.F.,
 .F.,.F.)
B_SPLINE_SURFACE_WITH_KNOTS((4,4),(3,3),(-5.21974905013087E-6,5.74172395514396E-5),
(-0.00139822857741233,1.00051312364074),.UNSPECIFIED.)
GEOMETRIC_REPRESENTATION_ITEM()
RATIONAL_B_SPLINE_SURFACE(((1.00049256947245,0.823768952244018,1.00018060397852),
(1.00048448215716,0.826662424388315,1.00017763870885),(1.00052427784023,
0.812424361909384,1.00019223006924),(1.00059912365857,0.785646094632756,
1.00021967280234)))
REPRESENTATION_ITEM('')
SURFACE()
);
#3762=(
BOUNDED_SURFACE()
B_SPLINE_SURFACE(3,2,((#438559,#438560,#438561),(#438562,#438563,#438564),
(#438565,#438566,#438567),(#438568,#438569,#438570)),.UNSPECIFIED.,.F.,
 .F.,.F.)
B_SPLINE_SURFACE_WITH_KNOTS((4,4),(3,3),(3.22980774337782E-5,9.63764854872258E-5),
(-0.00154325936371964,1.01095292447535),.UNSPECIFIED.)
GEOMETRIC_REPRESENTATION_ITEM()
RATIONAL_B_SPLINE_SURFACE(((1.00023530983299,0.922925743796172,1.0016857472833),
(1.00015136166125,0.95042243959421,1.00108434699059),(1.00033574337398,
0.890029368953975,1.00240524789546),(1.00054260094221,0.82227447316835,
1.00388716464855)))
REPRESENTATION_ITEM('')
SURFACE()
);
#3763=(
BOUNDED_SURFACE()
B_SPLINE_SURFACE(3,2,((#438670,#438671,#438672),(#438673,#438674,#438675),
(#438676,#438677,#438678),(#438679,#438680,#438681)),.UNSPECIFIED.,.F.,
 .F.,.F.)
B_SPLINE_SURFACE_WITH_KNOTS((4,4),(3,3),(0.,0.000101260117256738),(0.,1.),
 .UNSPECIFIED.)
GEOMETRIC_REPRESENTATION_ITEM()
RATIONAL_B_SPLINE_SURFACE(((1.,0.796615278835171,1.),(1.,0.795896038055943,
1.),(1.,0.795193354661344,1.),(1.,0.794506193185545,1.)))
REPRESENTATION_ITEM('')
SURFACE()
);
#3764=(
BOUNDED_SURFACE()
B_SPLINE_SURFACE(3,2,((#438719,#438720,#438721),(#438722,#438723,#438724),
(#438725,#438726,#438727),(#438728,#438729,#438730),(#438731,#438732,#438733),
(#438734,#438735,#438736)),.UNSPECIFIED.,.F.,.F.,.F.)
B_SPLINE_SURFACE_WITH_KNOTS((4,2,4),(3,3),(6.60685698858354E-20,1.66936432462295E-5,
3.3387286492459E-5),(0.,1.),.UNSPECIFIED.)
GEOMETRIC_REPRESENTATION_ITEM()
RATIONAL_B_SPLINE_SURFACE(((1.,0.796615278835176,1.),(1.,0.862310524418131,
1.),(1.,0.923774472010521,1.),(1.,0.923983993203423,1.),(1.,0.862574873720945,
1.),(1.,0.796615278835188,1.)))
REPRESENTATION_ITEM('')
SURFACE()
);
#3765=(
BOUNDED_SURFACE()
B_SPLINE_SURFACE(3,2,((#438773,#438774,#438775),(#438776,#438777,#438778),
(#438779,#438780,#438781),(#438782,#438783,#438784)),.UNSPECIFIED.,.F.,
 .F.,.F.)
B_SPLINE_SURFACE_WITH_KNOTS((4,4),(3,3),(0.,0.000101244905251112),(0.,1.),
 .UNSPECIFIED.)
GEOMETRIC_REPRESENTATION_ITEM()
RATIONAL_B_SPLINE_SURFACE(((1.,0.796615278835171,1.),(1.,0.795896146109794,
1.),(1.,0.795193565796499,1.),(1.,0.794506502889906,1.)))
REPRESENTATION_ITEM('')
SURFACE()
);
#3766=(
BOUNDED_SURFACE()
B_SPLINE_SURFACE(3,2,((#438820,#438821,#438822),(#438823,#438824,#438825),
(#438826,#438827,#438828),(#438829,#438830,#438831)),.UNSPECIFIED.,.F.,
 .F.,.F.)
B_SPLINE_SURFACE_WITH_KNOTS((4,4),(3,3),(2.85968127239939E-5,9.24681548475817E-5),
(-0.00167900678770357,1.01130827127811),.UNSPECIFIED.)
GEOMETRIC_REPRESENTATION_ITEM()
RATIONAL_B_SPLINE_SURFACE(((1.00059040895258,0.822187541868087,1.00401468696653),
(1.00036527718165,0.889990093671452,1.00248382673389),(1.00016469515024,
0.950399042257882,1.0011199008251),(1.0002560427401,0.922888044285998,1.00174104990629)))
REPRESENTATION_ITEM('')
SURFACE()
);
#3767=(
BOUNDED_SURFACE()
B_SPLINE_SURFACE(3,2,((#438835,#438836,#438837),(#438838,#438839,#438840),
(#438841,#438842,#438843),(#438844,#438845,#438846)),.UNSPECIFIED.,.F.,
 .F.,.F.)
B_SPLINE_SURFACE_WITH_KNOTS((4,4),(3,3),(-5.22358356749358E-6,5.74594192424274E-5),
(-0.00127120052056364,1.),.UNSPECIFIED.)
GEOMETRIC_REPRESENTATION_ITEM()
RATIONAL_B_SPLINE_SURFACE(((1.00054449313175,0.785835073638748,1.),(1.00047707767475,
0.812351526358867,1.),(1.00044031788587,0.826810216506277,1.),(1.00044777653319,
0.823876514387257,1.)))
REPRESENTATION_ITEM('')
SURFACE()
);
#3768=(
BOUNDED_SURFACE()
B_SPLINE_SURFACE(3,2,((#438848,#438849,#438850),(#438851,#438852,#438853),
(#438854,#438855,#438856),(#438857,#438858,#438859)),.UNSPECIFIED.,.F.,
 .F.,.F.)
B_SPLINE_SURFACE_WITH_KNOTS((4,4),(3,3),(-4.60785923306339E-19,4.8874751296988E-5),
(-0.00021580521618408,1.),.UNSPECIFIED.)
GEOMETRIC_REPRESENTATION_ITEM()
RATIONAL_B_SPLINE_SURFACE(((1.00008915600367,0.793434085499599,1.),(1.0000893022502,
0.793095246303154,1.),(1.00008944684642,0.792760230720409,1.),(1.00008958984422,
0.792428918540447,1.)))
REPRESENTATION_ITEM('')
SURFACE()
);
#3769=(
BOUNDED_SURFACE()
B_SPLINE_SURFACE(3,2,((#438861,#438862,#438863),(#438864,#438865,#438866),
(#438867,#438868,#438869),(#438870,#438871,#438872),(#438873,#438874,#438875),
(#438876,#438877,#438878)),.UNSPECIFIED.,.F.,.F.,.F.)
B_SPLINE_SURFACE_WITH_KNOTS((4,2,4),(3,3),(4.26904605416167E-19,7.62675010863198E-5,
0.000152535002172639),(0.,1.02152348203057),.UNSPECIFIED.)
GEOMETRIC_REPRESENTATION_ITEM()
RATIONAL_B_SPLINE_SURFACE(((1.,0.789033595401273,1.00908146323687),(1.,
0.857071781054841,1.00615262590426),(1.,0.922087264710753,1.0033539067159),
(1.,0.922394466502368,1.00334068261142),(1.,0.857224384599077,1.00614605678497),
(1.,0.789033595401671,1.00908146323685)))
REPRESENTATION_ITEM('')
SURFACE()
);
#3770=(
BOUNDED_SURFACE()
B_SPLINE_SURFACE(3,2,((#438880,#438881,#438882),(#438883,#438884,#438885),
(#438886,#438887,#438888),(#438889,#438890,#438891)),.UNSPECIFIED.,.F.,
 .F.,.F.)
B_SPLINE_SURFACE_WITH_KNOTS((4,4),(3,3),(3.79470760369927E-19,4.88747512969885E-5),
(-0.000215489857867463,1.),.UNSPECIFIED.)
GEOMETRIC_REPRESENTATION_ITEM()
RATIONAL_B_SPLINE_SURFACE(((1.00008945889748,0.792428983985573,1.),(1.00008931610869,
0.792760296061128,1.),(1.00008917172382,0.793095311538193,1.),(1.00008902569104,
0.793434150627825,1.)))
REPRESENTATION_ITEM('')
SURFACE()
);
#3771=(
BOUNDED_SURFACE()
B_SPLINE_SURFACE(3,2,((#438893,#438894,#438895),(#438896,#438897,#438898),
(#438899,#438900,#438901),(#438902,#438903,#438904)),.UNSPECIFIED.,.F.,
 .F.,.F.)
B_SPLINE_SURFACE_WITH_KNOTS((4,4),(3,3),(-5.21974905012871E-6,5.74172395514387E-5),
(-0.00139822857711726,1.00051312364057),.UNSPECIFIED.)
GEOMETRIC_REPRESENTATION_ITEM()
RATIONAL_B_SPLINE_SURFACE(((1.00049256947235,0.823768952244105,1.00018060397846),
(1.00048448215706,0.826662424388402,1.00017763870879),(1.00052427784012,
0.812424361909468,1.00019223006917),(1.00059912365844,0.785646094632864,
1.00021967280227)))
REPRESENTATION_ITEM('')
SURFACE()
);
#3772=(
BOUNDED_SURFACE()
B_SPLINE_SURFACE(3,2,((#438908,#438909,#438910),(#438911,#438912,#438913),
(#438914,#438915,#438916),(#438917,#438918,#438919)),.UNSPECIFIED.,.F.,
 .F.,.F.)
B_SPLINE_SURFACE_WITH_KNOTS((4,4),(3,3),(3.2298077433778E-5,9.63764854872255E-5),
(-0.00154325936389459,1.01095292447531),.UNSPECIFIED.)
GEOMETRIC_REPRESENTATION_ITEM()
RATIONAL_B_SPLINE_SURFACE(((1.00023530983301,0.922925743796162,1.00168574728329),
(1.00015136166127,0.950422439594216,1.00108434699058),(1.00033574337402,
0.890029368953956,1.00240524789545),(1.00054260094227,0.822274473168327,
1.00388716464854)))
REPRESENTATION_ITEM('')
SURFACE()
);
#3773=(
BOUNDED_SURFACE()
B_SPLINE_SURFACE(3,2,((#439019,#439020,#439021),(#439022,#439023,#439024),
(#439025,#439026,#439027),(#439028,#439029,#439030)),.UNSPECIFIED.,.F.,
 .F.,.F.)
B_SPLINE_SURFACE_WITH_KNOTS((4,4),(3,3),(2.16840434497101E-19,0.000101260117256737),
(0.,1.),.UNSPECIFIED.)
GEOMETRIC_REPRESENTATION_ITEM()
RATIONAL_B_SPLINE_SURFACE(((1.,0.79661527883517,1.),(1.,0.795896038055935,
1.),(1.,0.795193354661354,1.),(1.,0.794506193185532,1.)))
REPRESENTATION_ITEM('')
SURFACE()
);
#3774=(
BOUNDED_SURFACE()
B_SPLINE_SURFACE(3,2,((#439068,#439069,#439070),(#439071,#439072,#439073),
(#439074,#439075,#439076),(#439077,#439078,#439079),(#439080,#439081,#439082),
(#439083,#439084,#439085)),.UNSPECIFIED.,.F.,.F.,.F.)
B_SPLINE_SURFACE_WITH_KNOTS((4,2,4),(3,3),(-6.09863722023096E-20,1.66936432462294E-5,
3.33872864924589E-5),(0.,1.),.UNSPECIFIED.)
GEOMETRIC_REPRESENTATION_ITEM()
RATIONAL_B_SPLINE_SURFACE(((1.,0.796615278835177,1.),(1.,0.862310524418133,
1.),(1.,0.923774472010523,1.),(1.,0.923983993203423,1.),(1.,0.862574873720948,
1.),(1.,0.79661527883519,1.)))
REPRESENTATION_ITEM('')
SURFACE()
);
#3775=(
BOUNDED_SURFACE()
B_SPLINE_SURFACE(3,2,((#439122,#439123,#439124),(#439125,#439126,#439127),
(#439128,#439129,#439130),(#439131,#439132,#439133)),.UNSPECIFIED.,.F.,
 .F.,.F.)
B_SPLINE_SURFACE_WITH_KNOTS((4,4),(3,3),(0.,0.000101244905251112),(0.,1.),
 .UNSPECIFIED.)
GEOMETRIC_REPRESENTATION_ITEM()
RATIONAL_B_SPLINE_SURFACE(((1.,0.796615278835172,1.),(1.,0.795896146109789,
1.),(1.,0.795193565796498,1.),(1.,0.794506502889901,1.)))
REPRESENTATION_ITEM('')
SURFACE()
);
#3776=(
BOUNDED_SURFACE()
B_SPLINE_SURFACE(3,2,((#439169,#439170,#439171),(#439172,#439173,#439174),
(#439175,#439176,#439177),(#439178,#439179,#439180)),.UNSPECIFIED.,.F.,
 .F.,.F.)
B_SPLINE_SURFACE_WITH_KNOTS((4,4),(3,3),(2.85968127239939E-5,9.24681548475817E-5),
(-0.00167900678778285,1.01130827127811),.UNSPECIFIED.)
GEOMETRIC_REPRESENTATION_ITEM()
RATIONAL_B_SPLINE_SURFACE(((1.0005904089526,0.822187541868067,1.00401468696652),
(1.00036527718167,0.889990093671455,1.00248382673388),(1.00016469515025,
0.950399042257867,1.0011199008251),(1.00025604274011,0.922888044285994,
1.00174104990629)))
REPRESENTATION_ITEM('')
SURFACE()
);
#3777=(
BOUNDED_SURFACE()
B_SPLINE_SURFACE(3,2,((#439184,#439185,#439186),(#439187,#439188,#439189),
(#439190,#439191,#439192),(#439193,#439194,#439195)),.UNSPECIFIED.,.F.,
 .F.,.F.)
B_SPLINE_SURFACE_WITH_KNOTS((4,4),(3,3),(-5.2235835674933E-6,5.74594192424276E-5),
(-0.00127120052052763,1.),.UNSPECIFIED.)
GEOMETRIC_REPRESENTATION_ITEM()
RATIONAL_B_SPLINE_SURFACE(((1.00054449313174,0.785835073638757,1.),(1.00047707767474,
0.812351526358864,1.),(1.00044031788585,0.826810216506289,1.),(1.00044777653318,
0.823876514387253,1.)))
REPRESENTATION_ITEM('')
SURFACE()
);
#3778=(
BOUNDED_SURFACE()
B_SPLINE_SURFACE(3,2,((#439197,#439198,#439199),(#439200,#439201,#439202),
(#439203,#439204,#439205),(#439206,#439207,#439208)),.UNSPECIFIED.,.F.,
 .F.,.F.)
B_SPLINE_SURFACE_WITH_KNOTS((4,4),(3,3),(-8.13151629364128E-20,4.88747512969877E-5),
(-0.00021580521555644,1.),.UNSPECIFIED.)
GEOMETRIC_REPRESENTATION_ITEM()
RATIONAL_B_SPLINE_SURFACE(((1.00008915600341,0.793434085499729,1.),(1.00008930224994,
0.793095246303277,1.),(1.00008944684616,0.792760230720541,1.),(1.00008958984396,
0.792428918540576,1.)))
REPRESENTATION_ITEM('')
SURFACE()
);
#3779=(
BOUNDED_SURFACE()
B_SPLINE_SURFACE(3,2,((#439210,#439211,#439212),(#439213,#439214,#439215),
(#439216,#439217,#439218),(#439219,#439220,#439221),(#439222,#439223,#439224),
(#439225,#439226,#439227)),.UNSPECIFIED.,.F.,.F.,.F.)
B_SPLINE_SURFACE_WITH_KNOTS((4,2,4),(3,3),(-1.28749007982654E-19,7.62675010863193E-5,
0.000152535002172639),(0.,1.02152348203056),.UNSPECIFIED.)
GEOMETRIC_REPRESENTATION_ITEM()
RATIONAL_B_SPLINE_SURFACE(((1.,0.789033595401272,1.00908146323686),(1.,
0.857071781054882,1.00615262590425),(1.,0.922087264710708,1.0033539067159),
(1.,0.92239446650241,1.00334068261141),(1.,0.857224384599053,1.00614605678497),
(1.,0.789033595401675,1.00908146323685)))
REPRESENTATION_ITEM('')
SURFACE()
);
#3780=(
BOUNDED_SURFACE()
B_SPLINE_SURFACE(3,2,((#439229,#439230,#439231),(#439232,#439233,#439234),
(#439235,#439236,#439237),(#439238,#439239,#439240)),.UNSPECIFIED.,.F.,
 .F.,.F.)
B_SPLINE_SURFACE_WITH_KNOTS((4,4),(3,3),(4.33680868994202E-19,4.88747512969882E-5),
(-0.00021548985691637,1.),.UNSPECIFIED.)
GEOMETRIC_REPRESENTATION_ITEM()
RATIONAL_B_SPLINE_SURFACE(((1.00008945889708,0.792428983985768,1.),(1.0000893161083,
0.792760296061316,1.),(1.00008917172342,0.793095311538391,1.),(1.00008902569065,
0.793434150628016,1.)))
REPRESENTATION_ITEM('')
SURFACE()
);
#3781=(
BOUNDED_SURFACE()
B_SPLINE_SURFACE(3,2,((#439242,#439243,#439244),(#439245,#439246,#439247),
(#439248,#439249,#439250),(#439251,#439252,#439253)),.UNSPECIFIED.,.F.,
 .F.,.F.)
B_SPLINE_SURFACE_WITH_KNOTS((4,4),(3,3),(-5.21974905012869E-6,5.74172395514398E-5),
(-0.00139822857789765,1.0005131236408),.UNSPECIFIED.)
GEOMETRIC_REPRESENTATION_ITEM()
RATIONAL_B_SPLINE_SURFACE(((1.00049256947262,0.82376895224393,1.00018060397854),
(1.00048448215733,0.826662424388206,1.00017763870887),(1.00052427784041,
0.812424361909297,1.00019223006926),(1.00059912365877,0.78564609463264,
1.00021967280237)))
REPRESENTATION_ITEM('')
SURFACE()
);
#3782=(
BOUNDED_SURFACE()
B_SPLINE_SURFACE(3,2,((#439257,#439258,#439259),(#439260,#439261,#439262),
(#439263,#439264,#439265),(#439266,#439267,#439268)),.UNSPECIFIED.,.F.,
 .F.,.F.)
B_SPLINE_SURFACE_WITH_KNOTS((4,4),(3,3),(3.22980774337777E-5,9.63764854872253E-5),
(-0.00154325936345656,1.01095292447531),.UNSPECIFIED.)
GEOMETRIC_REPRESENTATION_ITEM()
RATIONAL_B_SPLINE_SURFACE(((1.00023530983295,0.922925743796197,1.00168574728329),
(1.00015136166123,0.95042243959425,1.00108434699059),(1.00033574337392,
0.890029368953986,1.00240524789545),(1.00054260094212,0.82227447316841,
1.00388716464854)))
REPRESENTATION_ITEM('')
SURFACE()
);
#3783=(
BOUNDED_SURFACE()
B_SPLINE_SURFACE(3,2,((#439368,#439369,#439370),(#439371,#439372,#439373),
(#439374,#439375,#439376),(#439377,#439378,#439379)),.UNSPECIFIED.,.F.,
 .F.,.F.)
B_SPLINE_SURFACE_WITH_KNOTS((4,4),(3,3),(0.,0.000101260117256738),(0.,1.),
 .UNSPECIFIED.)
GEOMETRIC_REPRESENTATION_ITEM()
RATIONAL_B_SPLINE_SURFACE(((1.,0.796615278835172,1.),(1.,0.795896038055944,
1.),(1.,0.795193354661338,1.),(1.,0.794506193185553,1.)))
REPRESENTATION_ITEM('')
SURFACE()
);
#3784=(
BOUNDED_SURFACE()
B_SPLINE_SURFACE(3,2,((#439417,#439418,#439419),(#439420,#439421,#439422),
(#439423,#439424,#439425),(#439426,#439427,#439428),(#439429,#439430,#439431),
(#439432,#439433,#439434)),.UNSPECIFIED.,.F.,.F.,.F.)
B_SPLINE_SURFACE_WITH_KNOTS((4,2,4),(3,3),(-5.42101086242752E-20,1.66936432462296E-5,
3.33872864924593E-5),(0.,1.),.UNSPECIFIED.)
GEOMETRIC_REPRESENTATION_ITEM()
RATIONAL_B_SPLINE_SURFACE(((1.,0.796615278835171,1.),(1.,0.86231052441812,
1.),(1.,0.923774472010524,1.),(1.,0.923983993203427,1.),(1.,0.86257487372094,
1.),(1.,0.79661527883518,1.)))
REPRESENTATION_ITEM('')
SURFACE()
);
#3785=(
BOUNDED_SURFACE()
B_SPLINE_SURFACE(3,2,((#439471,#439472,#439473),(#439474,#439475,#439476),
(#439477,#439478,#439479),(#439480,#439481,#439482)),.UNSPECIFIED.,.F.,
 .F.,.F.)
B_SPLINE_SURFACE_WITH_KNOTS((4,4),(3,3),(0.,0.000101244905251112),(0.,1.),
 .UNSPECIFIED.)
GEOMETRIC_REPRESENTATION_ITEM()
RATIONAL_B_SPLINE_SURFACE(((1.,0.796615278835172,1.),(1.,0.795896146109793,
1.),(1.,0.795193565796501,1.),(1.,0.7945065028899,1.)))
REPRESENTATION_ITEM('')
SURFACE()
);
#3786=(
BOUNDED_SURFACE()
B_SPLINE_SURFACE(3,2,((#439518,#439519,#439520),(#439521,#439522,#439523),
(#439524,#439525,#439526),(#439527,#439528,#439529)),.UNSPECIFIED.,.F.,
 .F.,.F.)
B_SPLINE_SURFACE_WITH_KNOTS((4,4),(3,3),(2.85968127239939E-5,9.24681548475817E-5),
(-0.00167900678776883,1.01130827127819),.UNSPECIFIED.)
GEOMETRIC_REPRESENTATION_ITEM()
RATIONAL_B_SPLINE_SURFACE(((1.0005904089526,0.822187541868058,1.00401468696655),
(1.00036527718166,0.889990093671439,1.0024838267339),(1.00016469515025,
0.950399042257874,1.00111990082511),(1.00025604274011,0.922888044285987,
1.00174104990631)))
REPRESENTATION_ITEM('')
SURFACE()
);
#3787=(
BOUNDED_SURFACE()
B_SPLINE_SURFACE(3,2,((#439533,#439534,#439535),(#439536,#439537,#439538),
(#439539,#439540,#439541),(#439542,#439543,#439544)),.UNSPECIFIED.,.F.,
 .F.,.F.)
B_SPLINE_SURFACE_WITH_KNOTS((4,4),(3,3),(-5.22358356749338E-6,5.74594192424275E-5),
(-0.00127120052062783,1.),.UNSPECIFIED.)
GEOMETRIC_REPRESENTATION_ITEM()
RATIONAL_B_SPLINE_SURFACE(((1.00054449313178,0.785835073638751,1.),(1.00047707767478,
0.812351526358847,1.),(1.00044031788589,0.826810216506263,1.),(1.00044777653321,
0.823876514387255,1.)))
REPRESENTATION_ITEM('')
SURFACE()
);
#3788=(
BOUNDED_SURFACE()
B_SPLINE_SURFACE(3,2,((#439546,#439547,#439548),(#439549,#439550,#439551),
(#439552,#439553,#439554),(#439555,#439556,#439557)),.UNSPECIFIED.,.F.,
 .F.,.F.)
B_SPLINE_SURFACE_WITH_KNOTS((4,4),(3,3),(1.35525271560688E-19,4.88747512969878E-5),
(-0.000215805215419202,1.),.UNSPECIFIED.)
GEOMETRIC_REPRESENTATION_ITEM()
RATIONAL_B_SPLINE_SURFACE(((1.00008915600335,0.793434085499754,1.),(1.00008930224989,
0.793095246303315,1.),(1.00008944684611,0.792760230720557,1.),(1.0000895898439,
0.792428918540612,1.)))
REPRESENTATION_ITEM('')
SURFACE()
);
#3789=(
BOUNDED_SURFACE()
B_SPLINE_SURFACE(3,2,((#439559,#439560,#439561),(#439562,#439563,#439564),
(#439565,#439566,#439567),(#439568,#439569,#439570),(#439571,#439572,#439573),
(#439574,#439575,#439576)),.UNSPECIFIED.,.F.,.F.,.F.)
B_SPLINE_SURFACE_WITH_KNOTS((4,2,4),(3,3),(5.48877349820787E-19,7.62675010863201E-5,
0.00015253500217264),(0.,1.02152348203065),.UNSPECIFIED.)
GEOMETRIC_REPRESENTATION_ITEM()
RATIONAL_B_SPLINE_SURFACE(((1.,0.789033595401257,1.0090814632369),(1.,0.857071781054821,
1.00615262590428),(1.,0.922087264710762,1.00335390671591),(1.,0.922394466502347,
1.00334068261143),(1.,0.857224384599071,1.00614605678499),(1.,0.789033595401659,
1.00908146323689)))
REPRESENTATION_ITEM('')
SURFACE()
);
#3790=(
BOUNDED_SURFACE()
B_SPLINE_SURFACE(3,2,((#439578,#439579,#439580),(#439581,#439582,#439583),
(#439584,#439585,#439586),(#439587,#439588,#439589)),.UNSPECIFIED.,.F.,
 .F.,.F.)
B_SPLINE_SURFACE_WITH_KNOTS((4,4),(3,3),(2.98155597433514E-19,4.88747512969884E-5),
(-0.00021548985766335,1.),.UNSPECIFIED.)
GEOMETRIC_REPRESENTATION_ITEM()
RATIONAL_B_SPLINE_SURFACE(((1.00008945889739,0.792428983985614,1.),(1.00008931610861,
0.792760296061149,1.),(1.00008917172373,0.793095311538248,1.),(1.00008902569096,
0.793434150627866,1.)))
REPRESENTATION_ITEM('')
SURFACE()
);
#3791=(
BOUNDED_SURFACE()
B_SPLINE_SURFACE(3,2,((#439591,#439592,#439593),(#439594,#439595,#439596),
(#439597,#439598,#439599),(#439600,#439601,#439602)),.UNSPECIFIED.,.F.,
 .F.,.F.)
B_SPLINE_SURFACE_WITH_KNOTS((4,4),(3,3),(-5.21974905012878E-6,5.74172395514398E-5),
(-0.00139822857730411,1.00051312364056),.UNSPECIFIED.)
GEOMETRIC_REPRESENTATION_ITEM()
RATIONAL_B_SPLINE_SURFACE(((1.00049256947241,0.823768952244084,1.00018060397846),
(1.00048448215712,0.826662424388355,1.00017763870879),(1.00052427784019,
0.812424361909443,1.00019223006917),(1.00059912365852,0.78564609463282,
1.00021967280226)))
REPRESENTATION_ITEM('')
SURFACE()
);
#3792=(
BOUNDED_SURFACE()
B_SPLINE_SURFACE(3,2,((#439606,#439607,#439608),(#439609,#439610,#439611),
(#439612,#439613,#439614),(#439615,#439616,#439617)),.UNSPECIFIED.,.F.,
 .F.,.F.)
B_SPLINE_SURFACE_WITH_KNOTS((4,4),(3,3),(3.22980774337779E-5,9.63764854872255E-5),
(-0.00154325936375083,1.01095292447563),.UNSPECIFIED.)
GEOMETRIC_REPRESENTATION_ITEM()
RATIONAL_B_SPLINE_SURFACE(((1.00023530983299,0.92292574379615,1.00168574728334),
(1.00015136166126,0.950422439594203,1.00108434699062),(1.00033574337399,
0.890029368953946,1.00240524789552),(1.00054260094222,0.822274473168293,
1.00388716464865)))
REPRESENTATION_ITEM('')
SURFACE()
);
#3793=(
BOUNDED_SURFACE()
B_SPLINE_SURFACE(3,2,((#439717,#439718,#439719),(#439720,#439721,#439722),
(#439723,#439724,#439725),(#439726,#439727,#439728)),.UNSPECIFIED.,.F.,
 .F.,.F.)
B_SPLINE_SURFACE_WITH_KNOTS((4,4),(3,3),(0.,0.000101260117256737),(0.,1.),
 .UNSPECIFIED.)
GEOMETRIC_REPRESENTATION_ITEM()
RATIONAL_B_SPLINE_SURFACE(((1.,0.796615278835171,1.),(1.,0.795896038055945,
1.),(1.,0.795193354661351,1.),(1.,0.794506193185534,1.)))
REPRESENTATION_ITEM('')
SURFACE()
);
#3794=(
BOUNDED_SURFACE()
B_SPLINE_SURFACE(3,2,((#439766,#439767,#439768),(#439769,#439770,#439771),
(#439772,#439773,#439774),(#439775,#439776,#439777),(#439778,#439779,#439780),
(#439781,#439782,#439783)),.UNSPECIFIED.,.F.,.F.,.F.)
B_SPLINE_SURFACE_WITH_KNOTS((4,2,4),(3,3),(2.04981973235541E-19,1.66936432462297E-5,
3.33872864924591E-5),(0.,1.),.UNSPECIFIED.)
GEOMETRIC_REPRESENTATION_ITEM()
RATIONAL_B_SPLINE_SURFACE(((1.,0.796615278835174,1.),(1.,0.862310524418132,
1.),(1.,0.923774472010519,1.),(1.,0.923983993203426,1.),(1.,0.862574873720943,
1.),(1.,0.79661527883518,1.)))
REPRESENTATION_ITEM('')
SURFACE()
);
#3795=(
BOUNDED_SURFACE()
B_SPLINE_SURFACE(3,2,((#439820,#439821,#439822),(#439823,#439824,#439825),
(#439826,#439827,#439828),(#439829,#439830,#439831)),.UNSPECIFIED.,.F.,
 .F.,.F.)
B_SPLINE_SURFACE_WITH_KNOTS((4,4),(3,3),(-2.16840434497101E-19,0.000101244905251112),
(0.,1.),.UNSPECIFIED.)
GEOMETRIC_REPRESENTATION_ITEM()
RATIONAL_B_SPLINE_SURFACE(((1.,0.79661527883517,1.),(1.,0.795896146109799,
1.),(1.,0.795193565796492,1.),(1.,0.794506502889898,1.)))
REPRESENTATION_ITEM('')
SURFACE()
);
#3796=(
BOUNDED_SURFACE()
B_SPLINE_SURFACE(3,2,((#439867,#439868,#439869),(#439870,#439871,#439872),
(#439873,#439874,#439875),(#439876,#439877,#439878)),.UNSPECIFIED.,.F.,
 .F.,.F.)
B_SPLINE_SURFACE_WITH_KNOTS((4,4),(3,3),(2.85968127239939E-5,9.24681548475816E-5),
(-0.00167900678652977,1.01130827127818),.UNSPECIFIED.)
GEOMETRIC_REPRESENTATION_ITEM()
RATIONAL_B_SPLINE_SURFACE(((1.00059040895216,0.822187541868281,1.00401468696655),
(1.00036527718139,0.889990093671574,1.0024838267339),(1.00016469515013,
0.950399042257945,1.0011199008251),(1.00025604273992,0.922888044286082,
1.0017410499063)))
REPRESENTATION_ITEM('')
SURFACE()
);
#3797=(
BOUNDED_SURFACE()
B_SPLINE_SURFACE(3,2,((#439882,#439883,#439884),(#439885,#439886,#439887),
(#439888,#439889,#439890),(#439891,#439892,#439893)),.UNSPECIFIED.,.F.,
 .F.,.F.)
B_SPLINE_SURFACE_WITH_KNOTS((4,4),(3,3),(-5.22358356749313E-6,5.74594192424277E-5),
(-0.00127120052051313,1.),.UNSPECIFIED.)
GEOMETRIC_REPRESENTATION_ITEM()
RATIONAL_B_SPLINE_SURFACE(((1.00054449313173,0.785835073638764,1.),(1.00047707767473,
0.812351526358878,1.),(1.00044031788585,0.82681021650628,1.),(1.00044777653317,
0.823876514387266,1.)))
REPRESENTATION_ITEM('')
SURFACE()
);
#3798=(
BOUNDED_SURFACE()
B_SPLINE_SURFACE(3,2,((#439895,#439896,#439897),(#439898,#439899,#439900),
(#439901,#439902,#439903),(#439904,#439905,#439906)),.UNSPECIFIED.,.F.,
 .F.,.F.)
B_SPLINE_SURFACE_WITH_KNOTS((4,4),(3,3),(8.13151629364128E-20,4.88747512969883E-5),
(-0.000215805215948565,1.),.UNSPECIFIED.)
GEOMETRIC_REPRESENTATION_ITEM()
RATIONAL_B_SPLINE_SURFACE(((1.00008915600357,0.793434085499649,1.),(1.0000893022501,
0.793095246303197,1.),(1.00008944684633,0.792760230720471,1.),(1.00008958984412,
0.792428918540492,1.)))
REPRESENTATION_ITEM('')
SURFACE()
);
#3799=(
BOUNDED_SURFACE()
B_SPLINE_SURFACE(3,2,((#439908,#439909,#439910),(#439911,#439912,#439913),
(#439914,#439915,#439916),(#439917,#439918,#439919),(#439920,#439921,#439922),
(#439923,#439924,#439925)),.UNSPECIFIED.,.F.,.F.,.F.)
B_SPLINE_SURFACE_WITH_KNOTS((4,2,4),(3,3),(8.13151629364128E-20,7.62675010863196E-5,
0.000152535002172639),(0.,1.02152348203066),.UNSPECIFIED.)
GEOMETRIC_REPRESENTATION_ITEM()
RATIONAL_B_SPLINE_SURFACE(((1.,0.789033595401254,1.00908146323691),(1.,
0.857071781054843,1.00615262590428),(1.,0.922087264710728,1.00335390671592),
(1.,0.922394466502372,1.00334068261143),(1.,0.857224384599056,1.006146056785),
(1.,0.789033595401653,1.00908146323689)))
REPRESENTATION_ITEM('')
SURFACE()
);
#3800=(
BOUNDED_SURFACE()
B_SPLINE_SURFACE(3,2,((#439927,#439928,#439929),(#439930,#439931,#439932),
(#439933,#439934,#439935),(#439936,#439937,#439938)),.UNSPECIFIED.,.F.,
 .F.,.F.)
B_SPLINE_SURFACE_WITH_KNOTS((4,4),(3,3),(2.16840434497101E-19,4.88747512969884E-5),
(-0.000215489857764122,1.),.UNSPECIFIED.)
GEOMETRIC_REPRESENTATION_ITEM()
RATIONAL_B_SPLINE_SURFACE(((1.00008945889743,0.792428983985588,1.),(1.00008931610865,
0.792760296061136,1.),(1.00008917172377,0.793095311538216,1.),(1.000089025691,
0.793434150627844,1.)))
REPRESENTATION_ITEM('')
SURFACE()
);
#3801=(
BOUNDED_SURFACE()
B_SPLINE_SURFACE(3,2,((#439940,#439941,#439942),(#439943,#439944,#439945),
(#439946,#439947,#439948),(#439949,#439950,#439951)),.UNSPECIFIED.,.F.,
 .F.,.F.)
B_SPLINE_SURFACE_WITH_KNOTS((4,4),(3,3),(-5.21974905013083E-6,5.74172395514394E-5),
(-0.00139822857767231,1.00051312364078),.UNSPECIFIED.)
GEOMETRIC_REPRESENTATION_ITEM()
RATIONAL_B_SPLINE_SURFACE(((1.00049256947254,0.823768952243962,1.00018060397853),
(1.00048448215725,0.826662424388261,1.00017763870886),(1.00052427784033,
0.812424361909332,1.00019223006925),(1.00059912365868,0.785646094632691,
1.00021967280236)))
REPRESENTATION_ITEM('')
SURFACE()
);
#3802=(
BOUNDED_SURFACE()
B_SPLINE_SURFACE(3,2,((#439955,#439956,#439957),(#439958,#439959,#439960),
(#439961,#439962,#439963),(#439964,#439965,#439966)),.UNSPECIFIED.,.F.,
 .F.,.F.)
B_SPLINE_SURFACE_WITH_KNOTS((4,4),(3,3),(3.22980774337779E-5,9.63764854872257E-5),
(-0.00154325936399881,1.01095292447533),.UNSPECIFIED.)
GEOMETRIC_REPRESENTATION_ITEM()
RATIONAL_B_SPLINE_SURFACE(((1.00023530983303,0.922925743796152,1.00168574728329),
(1.00015136166128,0.950422439594205,1.00108434699059),(1.00033574337404,
0.890029368953934,1.00240524789545),(1.00054260094231,0.822274473168315,
1.00388716464855)))
REPRESENTATION_ITEM('')
SURFACE()
);
#3803=(
BOUNDED_SURFACE()
B_SPLINE_SURFACE(3,2,((#440066,#440067,#440068),(#440069,#440070,#440071),
(#440072,#440073,#440074),(#440075,#440076,#440077)),.UNSPECIFIED.,.F.,
 .F.,.F.)
B_SPLINE_SURFACE_WITH_KNOTS((4,4),(3,3),(0.,0.000101260117256738),(0.,1.),
 .UNSPECIFIED.)
GEOMETRIC_REPRESENTATION_ITEM()
RATIONAL_B_SPLINE_SURFACE(((1.,0.796615278835166,1.),(1.,0.795896038055944,
1.),(1.,0.795193354661345,1.),(1.,0.794506193185547,1.)))
REPRESENTATION_ITEM('')
SURFACE()
);
#3804=(
BOUNDED_SURFACE()
B_SPLINE_SURFACE(3,2,((#440115,#440116,#440117),(#440118,#440119,#440120),
(#440121,#440122,#440123),(#440124,#440125,#440126),(#440127,#440128,#440129),
(#440130,#440131,#440132)),.UNSPECIFIED.,.F.,.F.,.F.)
B_SPLINE_SURFACE_WITH_KNOTS((4,2,4),(3,3),(2.40557357020221E-19,1.66936432462298E-5,
3.33872864924593E-5),(0.,1.),.UNSPECIFIED.)
GEOMETRIC_REPRESENTATION_ITEM()
RATIONAL_B_SPLINE_SURFACE(((1.,0.796615278835179,1.),(1.,0.862310524418132,
1.),(1.,0.923774472010519,1.),(1.,0.923983993203427,1.),(1.,0.862574873720955,
1.),(1.,0.796615278835182,1.)))
REPRESENTATION_ITEM('')
SURFACE()
);
#3805=(
BOUNDED_SURFACE()
B_SPLINE_SURFACE(3,2,((#440169,#440170,#440171),(#440172,#440173,#440174),
(#440175,#440176,#440177),(#440178,#440179,#440180)),.UNSPECIFIED.,.F.,
 .F.,.F.)
B_SPLINE_SURFACE_WITH_KNOTS((4,4),(3,3),(0.,0.000101244905251112),(0.,1.),
 .UNSPECIFIED.)
GEOMETRIC_REPRESENTATION_ITEM()
RATIONAL_B_SPLINE_SURFACE(((1.,0.796615278835175,1.),(1.,0.795896146109791,
1.),(1.,0.795193565796496,1.),(1.,0.7945065028899,1.)))
REPRESENTATION_ITEM('')
SURFACE()
);
#3806=(
BOUNDED_SURFACE()
B_SPLINE_SURFACE(3,2,((#440216,#440217,#440218),(#440219,#440220,#440221),
(#440222,#440223,#440224),(#440225,#440226,#440227)),.UNSPECIFIED.,.F.,
 .F.,.F.)
B_SPLINE_SURFACE_WITH_KNOTS((4,4),(3,3),(2.85968127239939E-5,9.24681548475817E-5),
(-0.00167900678654135,1.01130827127829),.UNSPECIFIED.)
GEOMETRIC_REPRESENTATION_ITEM()
RATIONAL_B_SPLINE_SURFACE(((1.00059040895217,0.822187541868258,1.00401468696659),
(1.0003652771814,0.889990093671561,1.00248382673393),(1.00016469515013,
0.950399042257935,1.00111990082511),(1.00025604273992,0.922888044286072,
1.00174104990632)))
REPRESENTATION_ITEM('')
SURFACE()
);
#3807=(
BOUNDED_SURFACE()
B_SPLINE_SURFACE(3,2,((#440231,#440232,#440233),(#440234,#440235,#440236),
(#440237,#440238,#440239),(#440240,#440241,#440242)),.UNSPECIFIED.,.F.,
 .F.,.F.)
B_SPLINE_SURFACE_WITH_KNOTS((4,4),(3,3),(-5.22358356749291E-6,5.74594192424275E-5),
(-0.00127120052073408,1.),.UNSPECIFIED.)
GEOMETRIC_REPRESENTATION_ITEM()
RATIONAL_B_SPLINE_SURFACE(((1.00054449313183,0.785835073638734,1.),(1.00047707767482,
0.812351526358796,1.),(1.00044031788593,0.82681021650626,1.),(1.00044777653325,
0.823876514387224,1.)))
REPRESENTATION_ITEM('')
SURFACE()
);
#3808=(
BOUNDED_SURFACE()
B_SPLINE_SURFACE(3,2,((#440244,#440245,#440246),(#440247,#440248,#440249),
(#440250,#440251,#440252),(#440253,#440254,#440255)),.UNSPECIFIED.,.F.,
 .F.,.F.)
B_SPLINE_SURFACE_WITH_KNOTS((4,4),(3,3),(5.42101086242752E-20,4.88747512969882E-5),
(-0.000215805215285131,1.),.UNSPECIFIED.)
GEOMETRIC_REPRESENTATION_ITEM()
RATIONAL_B_SPLINE_SURFACE(((1.0000891560033,0.793434085499786,1.),(1.00008930224983,
0.793095246303321,1.),(1.00008944684605,0.79276023072061,1.),(1.00008958984384,
0.79242891854063,1.)))
REPRESENTATION_ITEM('')
SURFACE()
);
#3809=(
BOUNDED_SURFACE()
B_SPLINE_SURFACE(3,2,((#440257,#440258,#440259),(#440260,#440261,#440262),
(#440263,#440264,#440265),(#440266,#440267,#440268),(#440269,#440270,#440271),
(#440272,#440273,#440274)),.UNSPECIFIED.,.F.,.F.,.F.)
B_SPLINE_SURFACE_WITH_KNOTS((4,2,4),(3,3),(1.35525271560688E-19,7.62675010863197E-5,
0.000152535002172639),(0.,1.02152348203077),.UNSPECIFIED.)
GEOMETRIC_REPRESENTATION_ITEM()
RATIONAL_B_SPLINE_SURFACE(((1.,0.789033595401232,1.00908146323695),(1.,
0.857071781054877,1.00615262590431),(1.,0.922087264710654,1.00335390671594),
(1.,0.922394466502435,1.00334068261145),(1.,0.857224384598992,1.00614605678503),
(1.,0.78903359540163,1.00908146323694)))
REPRESENTATION_ITEM('')
SURFACE()
);
#3810=(
BOUNDED_SURFACE()
B_SPLINE_SURFACE(3,2,((#440276,#440277,#440278),(#440279,#440280,#440281),
(#440282,#440283,#440284),(#440285,#440286,#440287)),.UNSPECIFIED.,.F.,
 .F.,.F.)
B_SPLINE_SURFACE_WITH_KNOTS((4,4),(3,3),(3.79470760369927E-19,4.88747512969884E-5),
(-0.000215489856846097,1.),.UNSPECIFIED.)
GEOMETRIC_REPRESENTATION_ITEM()
RATIONAL_B_SPLINE_SURFACE(((1.00008945889705,0.792428983985783,1.),(1.00008931610827,
0.792760296061333,1.),(1.00008917172339,0.793095311538396,1.),(1.00008902569062,
0.793434150628034,1.)))
REPRESENTATION_ITEM('')
SURFACE()
);
#3811=(
BOUNDED_SURFACE()
B_SPLINE_SURFACE(3,2,((#440289,#440290,#440291),(#440292,#440293,#440294),
(#440295,#440296,#440297),(#440298,#440299,#440300)),.UNSPECIFIED.,.F.,
 .F.,.F.)
B_SPLINE_SURFACE_WITH_KNOTS((4,4),(3,3),(-5.21974905012864E-6,5.74172395514396E-5),
(-0.0013982285777479,1.00051312364095),.UNSPECIFIED.)
GEOMETRIC_REPRESENTATION_ITEM()
RATIONAL_B_SPLINE_SURFACE(((1.00049256947257,0.823768952243935,1.00018060397859),
(1.00048448215727,0.826662424388207,1.00017763870892),(1.00052427784036,
0.812424361909287,1.00019223006932),(1.00059912365871,0.785646094632647,
1.00021967280243)))
REPRESENTATION_ITEM('')
SURFACE()
);
#3812=(
BOUNDED_SURFACE()
B_SPLINE_SURFACE(3,2,((#440304,#440305,#440306),(#440307,#440308,#440309),
(#440310,#440311,#440312),(#440313,#440314,#440315)),.UNSPECIFIED.,.F.,
 .F.,.F.)
B_SPLINE_SURFACE_WITH_KNOTS((4,4),(3,3),(3.22980774337779E-5,9.6376485487225E-5),
(-0.00154325936373299,1.01095292447548),.UNSPECIFIED.)
GEOMETRIC_REPRESENTATION_ITEM()
RATIONAL_B_SPLINE_SURFACE(((1.00023530983299,0.922925743796163,1.00168574728332),
(1.00015136166126,0.950422439594215,1.0010843469906),(1.00033574337398,
0.89002936895396,1.00240524789549),(1.00054260094221,0.822274473168319,
1.0038871646486)))
REPRESENTATION_ITEM('')
SURFACE()
);
#3813=(
BOUNDED_SURFACE()
B_SPLINE_SURFACE(3,2,((#440415,#440416,#440417),(#440418,#440419,#440420),
(#440421,#440422,#440423),(#440424,#440425,#440426)),.UNSPECIFIED.,.F.,
 .F.,.F.)
B_SPLINE_SURFACE_WITH_KNOTS((4,4),(3,3),(-4.33680868994202E-19,0.000101260117256738),
(0.,1.),.UNSPECIFIED.)
GEOMETRIC_REPRESENTATION_ITEM()
RATIONAL_B_SPLINE_SURFACE(((1.,0.796615278835173,1.),(1.,0.795896038055942,
1.),(1.,0.795193354661347,1.),(1.,0.794506193185554,1.)))
REPRESENTATION_ITEM('')
SURFACE()
);
#3814=(
BOUNDED_SURFACE()
B_SPLINE_SURFACE(3,2,((#440464,#440465,#440466),(#440467,#440468,#440469),
(#440470,#440471,#440472),(#440473,#440474,#440475),(#440476,#440477,#440478),
(#440479,#440480,#440481)),.UNSPECIFIED.,.F.,.F.,.F.)
B_SPLINE_SURFACE_WITH_KNOTS((4,2,4),(3,3),(1.76182853028894E-19,1.66936432462295E-5,
3.33872864924588E-5),(0.,1.),.UNSPECIFIED.)
GEOMETRIC_REPRESENTATION_ITEM()
RATIONAL_B_SPLINE_SURFACE(((1.,0.796615278835175,1.),(1.,0.862310524418126,
1.),(1.,0.92377447201052,1.),(1.,0.923983993203426,1.),(1.,0.862574873720947,
1.),(1.,0.796615278835184,1.)))
REPRESENTATION_ITEM('')
SURFACE()
);
#3815=(
BOUNDED_SURFACE()
B_SPLINE_SURFACE(3,2,((#440518,#440519,#440520),(#440521,#440522,#440523),
(#440524,#440525,#440526),(#440527,#440528,#440529)),.UNSPECIFIED.,.F.,
 .F.,.F.)
B_SPLINE_SURFACE_WITH_KNOTS((4,4),(3,3),(0.,0.000101244905251112),(0.,1.),
 .UNSPECIFIED.)
GEOMETRIC_REPRESENTATION_ITEM()
RATIONAL_B_SPLINE_SURFACE(((1.,0.796615278835171,1.),(1.,0.795896146109794,
1.),(1.,0.795193565796501,1.),(1.,0.7945065028899,1.)))
REPRESENTATION_ITEM('')
SURFACE()
);
#3816=(
BOUNDED_SURFACE()
B_SPLINE_SURFACE(3,2,((#440565,#440566,#440567),(#440568,#440569,#440570),
(#440571,#440572,#440573),(#440574,#440575,#440576)),.UNSPECIFIED.,.F.,
 .F.,.F.)
B_SPLINE_SURFACE_WITH_KNOTS((4,4),(3,3),(2.85968127239939E-5,9.24681548475816E-5),
(-0.0016790067933083,1.01130827127841),.UNSPECIFIED.)
GEOMETRIC_REPRESENTATION_ITEM()
RATIONAL_B_SPLINE_SURFACE(((1.00059040895455,0.822187541867025,1.00401468696663),
(1.00036527718287,0.889990093670798,1.00248382673395),(1.00016469515079,
0.950399042257587,1.00111990082513),(1.00025604274096,0.922888044285538,
1.00174104990634)))
REPRESENTATION_ITEM('')
SURFACE()
);
#3817=(
BOUNDED_SURFACE()
B_SPLINE_SURFACE(3,2,((#440580,#440581,#440582),(#440583,#440584,#440585),
(#440586,#440587,#440588),(#440589,#440590,#440591)),.UNSPECIFIED.,.F.,
 .F.,.F.)
B_SPLINE_SURFACE_WITH_KNOTS((4,4),(3,3),(-5.22358356749145E-6,5.74594192424276E-5),
(-0.00127120052070219,1.),.UNSPECIFIED.)
GEOMETRIC_REPRESENTATION_ITEM()
RATIONAL_B_SPLINE_SURFACE(((1.00054449313181,0.785835073638729,1.),(1.0004770776748,
0.812351526358837,1.),(1.00044031788592,0.826810216506255,1.),(1.00044777653324,
0.823876514387233,1.)))
REPRESENTATION_ITEM('')
SURFACE()
);
#3818=(
BOUNDED_SURFACE()
B_SPLINE_SURFACE(3,2,((#440593,#440594,#440595),(#440596,#440597,#440598),
(#440599,#440600,#440601),(#440602,#440603,#440604)),.UNSPECIFIED.,.F.,
 .F.,.F.)
B_SPLINE_SURFACE_WITH_KNOTS((4,4),(3,3),(-1.35525271560688E-19,4.88747512969876E-5),
(-0.000215805215528143,1.),.UNSPECIFIED.)
GEOMETRIC_REPRESENTATION_ITEM()
RATIONAL_B_SPLINE_SURFACE(((1.0000891560034,0.793434085499736,1.),(1.00008930224993,
0.793095246303264,1.),(1.00008944684615,0.79276023072058,1.),(1.00008958984394,
0.79242891854058,1.)))
REPRESENTATION_ITEM('')
SURFACE()
);
#3819=(
BOUNDED_SURFACE()
B_SPLINE_SURFACE(3,2,((#440606,#440607,#440608),(#440609,#440610,#440611),
(#440612,#440613,#440614),(#440615,#440616,#440617),(#440618,#440619,#440620),
(#440621,#440622,#440623)),.UNSPECIFIED.,.F.,.F.,.F.)
B_SPLINE_SURFACE_WITH_KNOTS((4,2,4),(3,3),(3.72694496791892E-19,7.62675010863197E-5,
0.000152535002172639),(0.,1.02152348203055),.UNSPECIFIED.)
GEOMETRIC_REPRESENTATION_ITEM()
RATIONAL_B_SPLINE_SURFACE(((1.,0.789033595401277,1.00908146323686),(1.,
0.857071781054852,1.00615262590425),(1.,0.922087264710738,1.0033539067159),
(1.,0.922394466502381,1.00334068261141),(1.,0.857224384599074,1.00614605678497),
(1.,0.78903359540167,1.00908146323685)))
REPRESENTATION_ITEM('')
SURFACE()
);
#3820=(
BOUNDED_SURFACE()
B_SPLINE_SURFACE(3,2,((#440625,#440626,#440627),(#440628,#440629,#440630),
(#440631,#440632,#440633),(#440634,#440635,#440636)),.UNSPECIFIED.,.F.,
 .F.,.F.)
B_SPLINE_SURFACE_WITH_KNOTS((4,4),(3,3),(5.42101086242752E-19,4.88747512969886E-5),
(-0.000215489857798702,1.),.UNSPECIFIED.)
GEOMETRIC_REPRESENTATION_ITEM()
RATIONAL_B_SPLINE_SURFACE(((1.00008945889745,0.792428983985586,1.),(1.00008931610866,
0.792760296061132,1.),(1.00008917172379,0.79309531153821,1.),(1.00008902569101,
0.793434150627838,1.)))
REPRESENTATION_ITEM('')
SURFACE()
);
#3821=(
BOUNDED_SURFACE()
B_SPLINE_SURFACE(3,2,((#440638,#440639,#440640),(#440641,#440642,#440643),
(#440644,#440645,#440646),(#440647,#440648,#440649)),.UNSPECIFIED.,.F.,
 .F.,.F.)
B_SPLINE_SURFACE_WITH_KNOTS((4,4),(3,3),(-5.21974905013097E-6,5.74172395514412E-5),
(-0.00139822857775902,1.00051312364059),.UNSPECIFIED.)
GEOMETRIC_REPRESENTATION_ITEM()
RATIONAL_B_SPLINE_SURFACE(((1.00049256947257,0.823768952243987,1.00018060397847),
(1.00048448215728,0.826662424388286,1.0001776387088),(1.00052427784036,
0.812424361909344,1.00019223006918),(1.00059912365871,0.785646094632718,
1.00021967280228)))
REPRESENTATION_ITEM('')
SURFACE()
);
#3822=(
BOUNDED_SURFACE()
B_SPLINE_SURFACE(3,2,((#440653,#440654,#440655),(#440656,#440657,#440658),
(#440659,#440660,#440661),(#440662,#440663,#440664)),.UNSPECIFIED.,.F.,
 .F.,.F.)
B_SPLINE_SURFACE_WITH_KNOTS((4,4),(3,3),(3.22980774337779E-5,9.63764854872251E-5),
(-0.00154325936285191,1.01095292447548),.UNSPECIFIED.)
GEOMETRIC_REPRESENTATION_ITEM()
RATIONAL_B_SPLINE_SURFACE(((1.00023530983285,0.922925743796228,1.00168574728332),
(1.00015136166117,0.950422439594265,1.0010843469906),(1.00033574337379,
0.890029368954041,1.00240524789549),(1.0005426009419,0.822274473168488,
1.0038871646486)))
REPRESENTATION_ITEM('')
SURFACE()
);
#3823=(
BOUNDED_SURFACE()
B_SPLINE_SURFACE(3,2,((#440764,#440765,#440766),(#440767,#440768,#440769),
(#440770,#440771,#440772),(#440773,#440774,#440775)),.UNSPECIFIED.,.F.,
 .F.,.F.)
B_SPLINE_SURFACE_WITH_KNOTS((4,4),(3,3),(0.,0.000101260117256737),(0.,1.),
 .UNSPECIFIED.)
GEOMETRIC_REPRESENTATION_ITEM()
RATIONAL_B_SPLINE_SURFACE(((1.,0.796615278835173,1.),(1.,0.795896038055929,
1.),(1.,0.795193354661366,1.),(1.,0.794506193185535,1.)))
REPRESENTATION_ITEM('')
SURFACE()
);
#3824=(
BOUNDED_SURFACE()
B_SPLINE_SURFACE(3,2,((#440813,#440814,#440815),(#440816,#440817,#440818),
(#440819,#440820,#440821),(#440822,#440823,#440824),(#440825,#440826,#440827),
(#440828,#440829,#440830)),.UNSPECIFIED.,.F.,.F.,.F.)
B_SPLINE_SURFACE_WITH_KNOTS((4,2,4),(3,3),(-1.575481281893E-19,1.66936432462296E-5,
3.33872864924593E-5),(0.,1.),.UNSPECIFIED.)
GEOMETRIC_REPRESENTATION_ITEM()
RATIONAL_B_SPLINE_SURFACE(((1.,0.796615278835169,1.),(1.,0.862310524418131,
1.),(1.,0.923774472010519,1.),(1.,0.923983993203425,1.),(1.,0.862574873720939,
1.),(1.,0.796615278835181,1.)))
REPRESENTATION_ITEM('')
SURFACE()
);
#3825=(
BOUNDED_SURFACE()
B_SPLINE_SURFACE(3,2,((#440867,#440868,#440869),(#440870,#440871,#440872),
(#440873,#440874,#440875),(#440876,#440877,#440878)),.UNSPECIFIED.,.F.,
 .F.,.F.)
B_SPLINE_SURFACE_WITH_KNOTS((4,4),(3,3),(2.16840434497101E-19,0.000101244905251112),
(0.,1.),.UNSPECIFIED.)
GEOMETRIC_REPRESENTATION_ITEM()
RATIONAL_B_SPLINE_SURFACE(((1.,0.796615278835173,1.),(1.,0.795896146109799,
1.),(1.,0.795193565796499,1.),(1.,0.794506502889902,1.)))
REPRESENTATION_ITEM('')
SURFACE()
);
#3826=(
BOUNDED_SURFACE()
B_SPLINE_SURFACE(3,2,((#440914,#440915,#440916),(#440917,#440918,#440919),
(#440920,#440921,#440922),(#440923,#440924,#440925)),.UNSPECIFIED.,.F.,
 .F.,.F.)
B_SPLINE_SURFACE_WITH_KNOTS((4,4),(3,3),(2.85968127239939E-5,9.24681548475817E-5),
(-0.00167900678819985,1.01130827127813),.UNSPECIFIED.)
GEOMETRIC_REPRESENTATION_ITEM()
RATIONAL_B_SPLINE_SURFACE(((1.00059040895275,0.82218754186799,1.00401468696653),
(1.00036527718176,0.889990093671399,1.00248382673389),(1.00016469515029,
0.950399042257849,1.0011199008251),(1.00025604274018,0.922888044285957,
1.0017410499063)))
REPRESENTATION_ITEM('')
SURFACE()
);
#3827=(
BOUNDED_SURFACE()
B_SPLINE_SURFACE(3,2,((#440929,#440930,#440931),(#440932,#440933,#440934),
(#440935,#440936,#440937),(#440938,#440939,#440940)),.UNSPECIFIED.,.F.,
 .F.,.F.)
B_SPLINE_SURFACE_WITH_KNOTS((4,4),(3,3),(-5.22358356749294E-6,5.74594192424276E-5),
(-0.00127120052064046,1.),.UNSPECIFIED.)
GEOMETRIC_REPRESENTATION_ITEM()
RATIONAL_B_SPLINE_SURFACE(((1.00054449313179,0.785835073638756,1.),(1.00047707767478,
0.812351526358813,1.),(1.00044031788589,0.826810216506291,1.),(1.00044777653322,
0.823876514387238,1.)))
REPRESENTATION_ITEM('')
SURFACE()
);
#3828=(
BOUNDED_SURFACE()
B_SPLINE_SURFACE(3,2,((#440942,#440943,#440944),(#440945,#440946,#440947),
(#440948,#440949,#440950),(#440951,#440952,#440953)),.UNSPECIFIED.,.F.,
 .F.,.F.)
B_SPLINE_SURFACE_WITH_KNOTS((4,4),(3,3),(-8.13151629364128E-20,4.88747512969884E-5),
(-0.000215805215829361,1.),.UNSPECIFIED.)
GEOMETRIC_REPRESENTATION_ITEM()
RATIONAL_B_SPLINE_SURFACE(((1.00008915600352,0.793434085499674,1.),(1.00008930225006,
0.793095246303229,1.),(1.00008944684628,0.792760230720482,1.),(1.00008958984407,
0.792428918540523,1.)))
REPRESENTATION_ITEM('')
SURFACE()
);
#3829=(
BOUNDED_SURFACE()
B_SPLINE_SURFACE(3,2,((#440955,#440956,#440957),(#440958,#440959,#440960),
(#440961,#440962,#440963),(#440964,#440965,#440966),(#440967,#440968,#440969),
(#440970,#440971,#440972)),.UNSPECIFIED.,.F.,.F.,.F.)
B_SPLINE_SURFACE_WITH_KNOTS((4,2,4),(3,3),(2.10064170919066E-19,7.62675010863199E-5,
0.00015253500217264),(0.,1.02152348203051),.UNSPECIFIED.)
GEOMETRIC_REPRESENTATION_ITEM()
RATIONAL_B_SPLINE_SURFACE(((1.,0.789033595401284,1.00908146323684),(1.,
0.857071781054853,1.00615262590424),(1.,0.922087264710752,1.00335390671589),
(1.,0.922394466502378,1.00334068261141),(1.,0.857224384599074,1.00614605678495),
(1.,0.78903359540169,1.00908146323683)))
REPRESENTATION_ITEM('')
SURFACE()
);
#3830=(
BOUNDED_SURFACE()
B_SPLINE_SURFACE(3,2,((#440974,#440975,#440976),(#440977,#440978,#440979),
(#440980,#440981,#440982),(#440983,#440984,#440985)),.UNSPECIFIED.,.F.,
 .F.,.F.)
B_SPLINE_SURFACE_WITH_KNOTS((4,4),(3,3),(2.98155597433514E-19,4.88747512969883E-5),
(-0.000215489857094047,1.),.UNSPECIFIED.)
GEOMETRIC_REPRESENTATION_ITEM()
RATIONAL_B_SPLINE_SURFACE(((1.00008945889716,0.792428983985731,1.),(1.00008931610837,
0.792760296061287,1.),(1.0000891717235,0.793095311538365,1.),(1.00008902569072,
0.793434150627986,1.)))
REPRESENTATION_ITEM('')
SURFACE()
);
#3831=(
BOUNDED_SURFACE()
B_SPLINE_SURFACE(3,2,((#440987,#440988,#440989),(#440990,#440991,#440992),
(#440993,#440994,#440995),(#440996,#440997,#440998)),.UNSPECIFIED.,.F.,
 .F.,.F.)
B_SPLINE_SURFACE_WITH_KNOTS((4,4),(3,3),(-5.2197490501308E-6,5.74172395514384E-5),
(-0.00139822857742788,1.00051312364056),.UNSPECIFIED.)
GEOMETRIC_REPRESENTATION_ITEM()
RATIONAL_B_SPLINE_SURFACE(((1.00049256947246,0.823768952244055,1.00018060397845),
(1.00048448215716,0.826662424388338,1.00017763870878),(1.00052427784024,
0.81242436190943,1.00019223006917),(1.00059912365857,0.785646094632794,
1.00021967280226)))
REPRESENTATION_ITEM('')
SURFACE()
);
#3832=(
BOUNDED_SURFACE()
B_SPLINE_SURFACE(3,2,((#441002,#441003,#441004),(#441005,#441006,#441007),
(#441008,#441009,#441010),(#441011,#441012,#441013)),.UNSPECIFIED.,.F.,
 .F.,.F.)
B_SPLINE_SURFACE_WITH_KNOTS((4,4),(3,3),(3.2298077433778E-5,9.6376485487225E-5),
(-0.00154325936375615,1.01095292447547),.UNSPECIFIED.)
GEOMETRIC_REPRESENTATION_ITEM()
RATIONAL_B_SPLINE_SURFACE(((1.00023530983299,0.922925743796159,1.00168574728332),
(1.00015136166126,0.950422439594215,1.0010843469906),(1.00033574337399,
0.890029368953947,1.00240524789549),(1.00054260094222,0.822274473168324,
1.00388716464859)))
REPRESENTATION_ITEM('')
SURFACE()
);
#3833=(
BOUNDED_SURFACE()
B_SPLINE_SURFACE(3,2,((#441113,#441114,#441115),(#441116,#441117,#441118),
(#441119,#441120,#441121),(#441122,#441123,#441124)),.UNSPECIFIED.,.F.,
 .F.,.F.)
B_SPLINE_SURFACE_WITH_KNOTS((4,4),(3,3),(0.,0.000101260117256738),(0.,1.),
 .UNSPECIFIED.)
GEOMETRIC_REPRESENTATION_ITEM()
RATIONAL_B_SPLINE_SURFACE(((1.,0.796615278835173,1.),(1.,0.795896038055945,
1.),(1.,0.795193354661346,1.),(1.,0.794506193185549,1.)))
REPRESENTATION_ITEM('')
SURFACE()
);
#3834=(
BOUNDED_SURFACE()
B_SPLINE_SURFACE(3,2,((#441162,#441163,#441164),(#441165,#441166,#441167),
(#441168,#441169,#441170),(#441171,#441172,#441173),(#441174,#441175,#441176),
(#441177,#441178,#441179)),.UNSPECIFIED.,.F.,.F.,.F.)
B_SPLINE_SURFACE_WITH_KNOTS((4,2,4),(3,3),(-1.9312351197398E-19,1.66936432462293E-5,
3.33872864924588E-5),(0.,1.),.UNSPECIFIED.)
GEOMETRIC_REPRESENTATION_ITEM()
RATIONAL_B_SPLINE_SURFACE(((1.,0.796615278835169,1.),(1.,0.862310524418132,
1.),(1.,0.92377447201052,1.),(1.,0.923983993203426,1.),(1.,0.86257487372095,
1.),(1.,0.796615278835187,1.)))
REPRESENTATION_ITEM('')
SURFACE()
);
#3835=(
BOUNDED_SURFACE()
B_SPLINE_SURFACE(3,2,((#441216,#441217,#441218),(#441219,#441220,#441221),
(#441222,#441223,#441224),(#441225,#441226,#441227)),.UNSPECIFIED.,.F.,
 .F.,.F.)
B_SPLINE_SURFACE_WITH_KNOTS((4,4),(3,3),(2.16840434497101E-19,0.000101244905251112),
(0.,1.),.UNSPECIFIED.)
GEOMETRIC_REPRESENTATION_ITEM()
RATIONAL_B_SPLINE_SURFACE(((1.,0.796615278835169,1.),(1.,0.795896146109799,
1.),(1.,0.795193565796484,1.),(1.,0.794506502889905,1.)))
REPRESENTATION_ITEM('')
SURFACE()
);
#3836=(
BOUNDED_SURFACE()
B_SPLINE_SURFACE(3,2,((#441263,#441264,#441265),(#441266,#441267,#441268),
(#441269,#441270,#441271),(#441272,#441273,#441274)),.UNSPECIFIED.,.F.,
 .F.,.F.)
B_SPLINE_SURFACE_WITH_KNOTS((4,4),(3,3),(2.85968127239939E-5,9.24681548475816E-5),
(-0.00167900678719404,1.01130827127821),.UNSPECIFIED.)
GEOMETRIC_REPRESENTATION_ITEM()
RATIONAL_B_SPLINE_SURFACE(((1.0005904089524,0.822187541868157,1.00401468696656),
(1.00036527718154,0.889990093671496,1.00248382673391),(1.00016469515019,
0.950399042257903,1.00111990082511),(1.00025604274002,0.922888044286031,
1.00174104990631)))
REPRESENTATION_ITEM('')
SURFACE()
);
#3837=(
BOUNDED_SURFACE()
B_SPLINE_SURFACE(3,2,((#441278,#441279,#441280),(#441281,#441282,#441283),
(#441284,#441285,#441286),(#441287,#441288,#441289)),.UNSPECIFIED.,.F.,
 .F.,.F.)
B_SPLINE_SURFACE_WITH_KNOTS((4,4),(3,3),(-5.22358356749284E-6,5.74594192424277E-5),
(-0.00127120052058705,1.),.UNSPECIFIED.)
GEOMETRIC_REPRESENTATION_ITEM()
RATIONAL_B_SPLINE_SURFACE(((1.00054449313176,0.785835073638765,1.),(1.00047707767476,
0.812351526358836,1.),(1.00044031788588,0.826810216506289,1.),(1.0004477765332,
0.82387651438725,1.)))
REPRESENTATION_ITEM('')
SURFACE()
);
#3838=(
BOUNDED_SURFACE()
B_SPLINE_SURFACE(3,2,((#441291,#441292,#441293),(#441294,#441295,#441296),
(#441297,#441298,#441299),(#441300,#441301,#441302)),.UNSPECIFIED.,.F.,
 .F.,.F.)
B_SPLINE_SURFACE_WITH_KNOTS((4,4),(3,3),(-4.60785923306339E-19,4.88747512969882E-5),
(-0.00021580521588719,1.),.UNSPECIFIED.)
GEOMETRIC_REPRESENTATION_ITEM()
RATIONAL_B_SPLINE_SURFACE(((1.00008915600355,0.793434085499662,1.),(1.00008930225008,
0.793095246303215,1.),(1.0000894468463,0.792760230720473,1.),(1.00008958984409,
0.792428918540512,1.)))
REPRESENTATION_ITEM('')
SURFACE()
);
#3839=(
BOUNDED_SURFACE()
B_SPLINE_SURFACE(3,2,((#441304,#441305,#441306),(#441307,#441308,#441309),
(#441310,#441311,#441312),(#441313,#441314,#441315),(#441316,#441317,#441318),
(#441319,#441320,#441321)),.UNSPECIFIED.,.F.,.F.,.F.)
B_SPLINE_SURFACE_WITH_KNOTS((4,2,4),(3,3),(2.71050543121376E-19,7.62675010863194E-5,
0.000152535002172639),(0.,1.02152348203075),.UNSPECIFIED.)
GEOMETRIC_REPRESENTATION_ITEM()
RATIONAL_B_SPLINE_SURFACE(((1.,0.789033595401236,1.00908146323695),(1.,
0.857071781054828,1.00615262590431),(1.,0.922087264710721,1.00335390671593),
(1.,0.922394466502373,1.00334068261145),(1.,0.857224384599039,1.00614605678502),
(1.,0.789033595401634,1.00908146323693)))
REPRESENTATION_ITEM('')
SURFACE()
);
#3840=(
BOUNDED_SURFACE()
B_SPLINE_SURFACE(3,2,((#441323,#441324,#441325),(#441326,#441327,#441328),
(#441329,#441330,#441331),(#441332,#441333,#441334)),.UNSPECIFIED.,.F.,
 .F.,.F.)
B_SPLINE_SURFACE_WITH_KNOTS((4,4),(3,3),(3.52365706057789E-19,4.88747512969884E-5),
(-0.000215489857661774,1.),.UNSPECIFIED.)
GEOMETRIC_REPRESENTATION_ITEM()
RATIONAL_B_SPLINE_SURFACE(((1.00008945889739,0.792428983985612,1.),(1.00008931610861,
0.792760296061157,1.),(1.00008917172373,0.79309531153824,1.),(1.00008902569096,
0.793434150627865,1.)))
REPRESENTATION_ITEM('')
SURFACE()
);
#3841=(
BOUNDED_SURFACE()
B_SPLINE_SURFACE(3,2,((#441336,#441337,#441338),(#441339,#441340,#441341),
(#441342,#441343,#441344),(#441345,#441346,#441347)),.UNSPECIFIED.,.F.,
 .F.,.F.)
B_SPLINE_SURFACE_WITH_KNOTS((4,4),(3,3),(-5.21974905013096E-6,5.74172395514412E-5),
(-0.00139822857786666,1.00051312364074),.UNSPECIFIED.)
GEOMETRIC_REPRESENTATION_ITEM()
RATIONAL_B_SPLINE_SURFACE(((1.00049256947261,0.823768952243954,1.00018060397852),
(1.00048448215732,0.826662424388216,1.00017763870884),(1.0005242778404,
0.812424361909314,1.00019223006924),(1.00059912365876,0.785646094632656,
1.00021967280234)))
REPRESENTATION_ITEM('')
SURFACE()
);
#3842=(
BOUNDED_SURFACE()
B_SPLINE_SURFACE(3,2,((#441351,#441352,#441353),(#441354,#441355,#441356),
(#441357,#441358,#441359),(#441360,#441361,#441362)),.UNSPECIFIED.,.F.,
 .F.,.F.)
B_SPLINE_SURFACE_WITH_KNOTS((4,4),(3,3),(3.22980774337779E-5,9.63764854872255E-5),
(-0.00154325936374115,1.01095292447532),.UNSPECIFIED.)
GEOMETRIC_REPRESENTATION_ITEM()
RATIONAL_B_SPLINE_SURFACE(((1.00023530983299,0.92292574379617,1.00168574728329),
(1.00015136166126,0.950422439594228,1.00108434699059),(1.00033574337398,
0.890029368953965,1.00240524789545),(1.00054260094222,0.822274473168348,
1.00388716464854)))
REPRESENTATION_ITEM('')
SURFACE()
);
#3843=(
BOUNDED_SURFACE()
B_SPLINE_SURFACE(3,2,((#441462,#441463,#441464),(#441465,#441466,#441467),
(#441468,#441469,#441470),(#441471,#441472,#441473)),.UNSPECIFIED.,.F.,
 .F.,.F.)
B_SPLINE_SURFACE_WITH_KNOTS((4,4),(3,3),(0.,0.000101260117256738),(0.,1.),
 .UNSPECIFIED.)
GEOMETRIC_REPRESENTATION_ITEM()
RATIONAL_B_SPLINE_SURFACE(((1.,0.796615278835171,1.),(1.,0.795896038055941,
1.),(1.,0.795193354661349,1.),(1.,0.794506193185546,1.)))
REPRESENTATION_ITEM('')
SURFACE()
);
#3844=(
BOUNDED_SURFACE()
B_SPLINE_SURFACE(3,2,((#441511,#441512,#441513),(#441514,#441515,#441516),
(#441517,#441518,#441519),(#441520,#441521,#441522),(#441523,#441524,#441525),
(#441526,#441527,#441528)),.UNSPECIFIED.,.F.,.F.,.F.)
B_SPLINE_SURFACE_WITH_KNOTS((4,2,4),(3,3),(-5.0821976835258E-20,1.66936432462292E-5,
3.33872864924585E-5),(0.,1.),.UNSPECIFIED.)
GEOMETRIC_REPRESENTATION_ITEM()
RATIONAL_B_SPLINE_SURFACE(((1.,0.796615278835176,1.),(1.,0.86231052441814,
1.),(1.,0.923774472010514,1.),(1.,0.923983993203431,1.),(1.,0.862574873720946,
1.),(1.,0.79661527883519,1.)))
REPRESENTATION_ITEM('')
SURFACE()
);
#3845=(
BOUNDED_SURFACE()
B_SPLINE_SURFACE(3,2,((#441565,#441566,#441567),(#441568,#441569,#441570),
(#441571,#441572,#441573),(#441574,#441575,#441576)),.UNSPECIFIED.,.F.,
 .F.,.F.)
B_SPLINE_SURFACE_WITH_KNOTS((4,4),(3,3),(0.,0.000101244905251112),(0.,1.),
 .UNSPECIFIED.)
GEOMETRIC_REPRESENTATION_ITEM()
RATIONAL_B_SPLINE_SURFACE(((1.,0.796615278835168,1.),(1.,0.795896146109792,
1.),(1.,0.795193565796498,1.),(1.,0.794506502889897,1.)))
REPRESENTATION_ITEM('')
SURFACE()
);
#3846=(
BOUNDED_SURFACE()
B_SPLINE_SURFACE(3,2,((#441612,#441613,#441614),(#441615,#441616,#441617),
(#441618,#441619,#441620),(#441621,#441622,#441623)),.UNSPECIFIED.,.F.,
 .F.,.F.)
B_SPLINE_SURFACE_WITH_KNOTS((4,4),(3,3),(2.85968127239939E-5,9.24681548475815E-5),
(-0.00167900678670198,1.01130827127827),.UNSPECIFIED.)
GEOMETRIC_REPRESENTATION_ITEM()
RATIONAL_B_SPLINE_SURFACE(((1.00059040895222,0.822187541868232,1.00401468696659),
(1.00036527718143,0.889990093671556,1.00248382673392),(1.00016469515015,
0.950399042257909,1.00111990082511),(1.00025604273995,0.922888044286064,
1.00174104990632)))
REPRESENTATION_ITEM('')
SURFACE()
);
#3847=(
BOUNDED_SURFACE()
B_SPLINE_SURFACE(3,2,((#441627,#441628,#441629),(#441630,#441631,#441632),
(#441633,#441634,#441635),(#441636,#441637,#441638)),.UNSPECIFIED.,.F.,
 .F.,.F.)
B_SPLINE_SURFACE_WITH_KNOTS((4,4),(3,3),(-5.22358356749263E-6,5.74594192424276E-5),
(-0.00127120052053174,1.),.UNSPECIFIED.)
GEOMETRIC_REPRESENTATION_ITEM()
RATIONAL_B_SPLINE_SURFACE(((1.00054449313174,0.785835073638776,1.),(1.00047707767474,
0.812351526358855,1.),(1.00044031788586,0.826810216506291,1.),(1.00044777653318,
0.823876514387259,1.)))
REPRESENTATION_ITEM('')
SURFACE()
);
#3848=(
BOUNDED_SURFACE()
B_SPLINE_SURFACE(3,2,((#441640,#441641,#441642),(#441643,#441644,#441645),
(#441646,#441647,#441648),(#441649,#441650,#441651)),.UNSPECIFIED.,.F.,
 .F.,.F.)
B_SPLINE_SURFACE_WITH_KNOTS((4,4),(3,3),(-3.25260651745651E-19,4.88747512969878E-5),
(-0.000215805214925867,1.),.UNSPECIFIED.)
GEOMETRIC_REPRESENTATION_ITEM()
RATIONAL_B_SPLINE_SURFACE(((1.00008915600315,0.793434085499861,1.),(1.00008930224968,
0.793095246303394,1.),(1.0000894468459,0.79276023072068,1.),(1.00008958984369,
0.79242891854071,1.)))
REPRESENTATION_ITEM('')
SURFACE()
);
#3849=(
BOUNDED_SURFACE()
B_SPLINE_SURFACE(3,2,((#441653,#441654,#441655),(#441656,#441657,#441658),
(#441659,#441660,#441661),(#441662,#441663,#441664),(#441665,#441666,#441667),
(#441668,#441669,#441670)),.UNSPECIFIED.,.F.,.F.,.F.)
B_SPLINE_SURFACE_WITH_KNOTS((4,2,4),(3,3),(1.0842021724855E-19,7.62675010863196E-5,
0.000152535002172639),(0.,1.02152348203107),.UNSPECIFIED.)
GEOMETRIC_REPRESENTATION_ITEM()
RATIONAL_B_SPLINE_SURFACE(((1.,0.789033595401171,1.00908146323708),(1.,
0.857071781054833,1.0061526259044),(1.,0.922087264710633,1.00335390671598),
(1.,0.922394466502411,1.00334068261149),(1.,0.857224384598956,1.00614605678512),
(1.,0.789033595401567,1.00908146323707)))
REPRESENTATION_ITEM('')
SURFACE()
);
#3850=(
BOUNDED_SURFACE()
B_SPLINE_SURFACE(3,2,((#441672,#441673,#441674),(#441675,#441676,#441677),
(#441678,#441679,#441680),(#441681,#441682,#441683)),.UNSPECIFIED.,.F.,
 .F.,.F.)
B_SPLINE_SURFACE_WITH_KNOTS((4,4),(3,3),(4.87890977618477E-19,4.88747512969882E-5),
(-0.000215489856788559,1.),.UNSPECIFIED.)
GEOMETRIC_REPRESENTATION_ITEM()
RATIONAL_B_SPLINE_SURFACE(((1.00008945889703,0.792428983985793,1.),(1.00008931610825,
0.792760296061348,1.),(1.00008917172337,0.793095311538401,1.),(1.0000890256906,
0.793434150628046,1.)))
REPRESENTATION_ITEM('')
SURFACE()
);
#3851=(
BOUNDED_SURFACE()
B_SPLINE_SURFACE(3,2,((#441685,#441686,#441687),(#441688,#441689,#441690),
(#441691,#441692,#441693),(#441694,#441695,#441696)),.UNSPECIFIED.,.F.,
 .F.,.F.)
B_SPLINE_SURFACE_WITH_KNOTS((4,4),(3,3),(-5.21974905012872E-6,5.74172395514387E-5),
(-0.00139822857731876,1.00051312364056),.UNSPECIFIED.)
GEOMETRIC_REPRESENTATION_ITEM()
RATIONAL_B_SPLINE_SURFACE(((1.00049256947242,0.82376895224407,1.00018060397845),
(1.00048448215713,0.826662424388353,1.00017763870878),(1.00052427784019,
0.812424361909445,1.00019223006917),(1.00059912365853,0.785646094632814,
1.00021967280226)))
REPRESENTATION_ITEM('')
SURFACE()
);
#3852=(
BOUNDED_SURFACE()
B_SPLINE_SURFACE(3,2,((#441700,#441701,#441702),(#441703,#441704,#441705),
(#441706,#441707,#441708),(#441709,#441710,#441711)),.UNSPECIFIED.,.F.,
 .F.,.F.)
B_SPLINE_SURFACE_WITH_KNOTS((4,4),(3,3),(3.22980774337779E-5,9.63764854872246E-5),
(-0.00154325936327203,1.01095292447554),.UNSPECIFIED.)
GEOMETRIC_REPRESENTATION_ITEM()
RATIONAL_B_SPLINE_SURFACE(((1.00023530983292,0.922925743796195,1.00168574728333),
(1.00015136166121,0.950422439594221,1.00108434699061),(1.00033574337388,
0.890029368954008,1.0024052478955),(1.00054260094205,0.822274473168397,
1.00388716464862)))
REPRESENTATION_ITEM('')
SURFACE()
);
#3853=(
BOUNDED_SURFACE()
B_SPLINE_SURFACE(3,2,((#441811,#441812,#441813),(#441814,#441815,#441816),
(#441817,#441818,#441819),(#441820,#441821,#441822)),.UNSPECIFIED.,.F.,
 .F.,.F.)
B_SPLINE_SURFACE_WITH_KNOTS((4,4),(3,3),(0.,0.000101260117256738),(0.,1.),
 .UNSPECIFIED.)
GEOMETRIC_REPRESENTATION_ITEM()
RATIONAL_B_SPLINE_SURFACE(((1.,0.796615278835171,1.),(1.,0.795896038055938,
1.),(1.,0.795193354661346,1.),(1.,0.79450619318555,1.)))
REPRESENTATION_ITEM('')
SURFACE()
);
#3854=(
BOUNDED_SURFACE()
B_SPLINE_SURFACE(3,2,((#441860,#441861,#441862),(#441863,#441864,#441865),
(#441866,#441867,#441868),(#441869,#441870,#441871),(#441872,#441873,#441874),
(#441875,#441876,#441877)),.UNSPECIFIED.,.F.,.F.,.F.)
B_SPLINE_SURFACE_WITH_KNOTS((4,2,4),(3,3),(1.55854062294791E-19,1.66936432462295E-5,
3.33872864924588E-5),(0.,1.),.UNSPECIFIED.)
GEOMETRIC_REPRESENTATION_ITEM()
RATIONAL_B_SPLINE_SURFACE(((1.,0.796615278835172,1.),(1.,0.862310524418129,
1.),(1.,0.92377447201052,1.),(1.,0.923983993203427,1.),(1.,0.862574873720937,
1.),(1.,0.796615278835187,1.)))
REPRESENTATION_ITEM('')
SURFACE()
);
#3855=(
BOUNDED_SURFACE()
B_SPLINE_SURFACE(3,2,((#441914,#441915,#441916),(#441917,#441918,#441919),
(#441920,#441921,#441922),(#441923,#441924,#441925)),.UNSPECIFIED.,.F.,
 .F.,.F.)
B_SPLINE_SURFACE_WITH_KNOTS((4,4),(3,3),(0.,0.000101244905251113),(0.,1.),
 .UNSPECIFIED.)
GEOMETRIC_REPRESENTATION_ITEM()
RATIONAL_B_SPLINE_SURFACE(((1.,0.796615278835168,1.),(1.,0.795896146109794,
1.),(1.,0.795193565796498,1.),(1.,0.794506502889898,1.)))
REPRESENTATION_ITEM('')
SURFACE()
);
#3856=(
BOUNDED_SURFACE()
B_SPLINE_SURFACE(3,2,((#441961,#441962,#441963),(#441964,#441965,#441966),
(#441967,#441968,#441969),(#441970,#441971,#441972)),.UNSPECIFIED.,.F.,
 .F.,.F.)
B_SPLINE_SURFACE_WITH_KNOTS((4,4),(3,3),(2.85968127239939E-5,9.24681548475813E-5),
(-0.00167900678669566,1.01130827127813),.UNSPECIFIED.)
GEOMETRIC_REPRESENTATION_ITEM()
RATIONAL_B_SPLINE_SURFACE(((1.00059040895222,0.822187541868261,1.00401468696653),
(1.00036527718143,0.88999009367157,1.00248382673389),(1.00016469515015,
0.950399042257926,1.0011199008251),(1.00025604273995,0.922888044286076,
1.0017410499063)))
REPRESENTATION_ITEM('')
SURFACE()
);
#3857=(
BOUNDED_SURFACE()
B_SPLINE_SURFACE(3,2,((#441976,#441977,#441978),(#441979,#441980,#441981),
(#441982,#441983,#441984),(#441985,#441986,#441987)),.UNSPECIFIED.,.F.,
 .F.,.F.)
B_SPLINE_SURFACE_WITH_KNOTS((4,4),(3,3),(-5.22358356749252E-6,5.74594192424278E-5),
(-0.00127120052064908,1.),.UNSPECIFIED.)
GEOMETRIC_REPRESENTATION_ITEM()
RATIONAL_B_SPLINE_SURFACE(((1.00054449313179,0.785835073638743,1.),(1.00047707767478,
0.812351526358841,1.),(1.0004403178859,0.82681021650626,1.),(1.00044777653322,
0.823876514387243,1.)))
REPRESENTATION_ITEM('')
SURFACE()
);
#3858=(
BOUNDED_SURFACE()
B_SPLINE_SURFACE(3,2,((#441989,#441990,#441991),(#441992,#441993,#441994),
(#441995,#441996,#441997),(#441998,#441999,#442000)),.UNSPECIFIED.,.F.,
 .F.,.F.)
B_SPLINE_SURFACE_WITH_KNOTS((4,4),(3,3),(5.42101086242752E-20,4.88747512969879E-5),
(-0.000215805215441692,1.),.UNSPECIFIED.)
GEOMETRIC_REPRESENTATION_ITEM()
RATIONAL_B_SPLINE_SURFACE(((1.00008915600336,0.793434085499753,1.),(1.00008930224989,
0.793095246303307,1.),(1.00008944684611,0.792760230720563,1.),(1.00008958984391,
0.792428918540602,1.)))
REPRESENTATION_ITEM('')
SURFACE()
);
#3859=(
BOUNDED_SURFACE()
B_SPLINE_SURFACE(3,2,((#442002,#442003,#442004),(#442005,#442006,#442007),
(#442008,#442009,#442010),(#442011,#442012,#442013),(#442014,#442015,#442016),
(#442017,#442018,#442019)),.UNSPECIFIED.,.F.,.F.,.F.)
B_SPLINE_SURFACE_WITH_KNOTS((4,2,4),(3,3),(3.25260651745651E-19,7.62675010863198E-5,
0.000152535002172639),(0.,1.02152348203058),.UNSPECIFIED.)
GEOMETRIC_REPRESENTATION_ITEM()
RATIONAL_B_SPLINE_SURFACE(((1.,0.789033595401269,1.00908146323687),(1.,
0.857071781054852,1.00615262590426),(1.,0.922087264710738,1.0033539067159),
(1.,0.922394466502381,1.00334068261142),(1.,0.85722438459907,1.00614605678497),
(1.,0.789033595401667,1.00908146323686)))
REPRESENTATION_ITEM('')
SURFACE()
);
#3860=(
BOUNDED_SURFACE()
B_SPLINE_SURFACE(3,2,((#442021,#442022,#442023),(#442024,#442025,#442026),
(#442027,#442028,#442029),(#442030,#442031,#442032)),.UNSPECIFIED.,.F.,
 .F.,.F.)
B_SPLINE_SURFACE_WITH_KNOTS((4,4),(3,3),(3.79470760369927E-19,4.88747512969882E-5),
(-0.000215489857128971,1.),.UNSPECIFIED.)
GEOMETRIC_REPRESENTATION_ITEM()
RATIONAL_B_SPLINE_SURFACE(((1.00008945889717,0.792428983985724,1.),(1.00008931610839,
0.792760296061274,1.),(1.00008917172351,0.793095311538338,1.),(1.00008902569074,
0.793434150627974,1.)))
REPRESENTATION_ITEM('')
SURFACE()
);
#3861=(
BOUNDED_SURFACE()
B_SPLINE_SURFACE(3,2,((#442034,#442035,#442036),(#442037,#442038,#442039),
(#442040,#442041,#442042),(#442043,#442044,#442045)),.UNSPECIFIED.,.F.,
 .F.,.F.)
B_SPLINE_SURFACE_WITH_KNOTS((4,4),(3,3),(-5.21974905013103E-6,5.74172395514409E-5),
(-0.00139822857735267,1.00051312364046),.UNSPECIFIED.)
GEOMETRIC_REPRESENTATION_ITEM()
RATIONAL_B_SPLINE_SURFACE(((1.00049256947243,0.82376895224408,1.00018060397842),
(1.00048448215714,0.826662424388374,1.00017763870875),(1.00052427784021,
0.812424361909455,1.00019223006913),(1.00059912365854,0.78564609463283,
1.00021967280222)))
REPRESENTATION_ITEM('')
SURFACE()
);
#3862=(
BOUNDED_SURFACE()
B_SPLINE_SURFACE(3,2,((#442049,#442050,#442051),(#442052,#442053,#442054),
(#442055,#442056,#442057),(#442058,#442059,#442060)),.UNSPECIFIED.,.F.,
 .F.,.F.)
B_SPLINE_SURFACE_WITH_KNOTS((4,4),(3,3),(3.22980774337778E-5,9.63764854872252E-5),
(-0.00154325936387336,1.01095292447545),.UNSPECIFIED.)
GEOMETRIC_REPRESENTATION_ITEM()
RATIONAL_B_SPLINE_SURFACE(((1.00023530983301,0.922925743796151,1.00168574728331),
(1.00015136166127,0.95042243959421,1.0010843469906),(1.00033574337401,0.890029368953935,
1.00240524789548),(1.00054260094226,0.822274473168311,1.00388716464859)))
REPRESENTATION_ITEM('')
SURFACE()
);
#3863=(
BOUNDED_SURFACE()
B_SPLINE_SURFACE(3,2,((#442160,#442161,#442162),(#442163,#442164,#442165),
(#442166,#442167,#442168),(#442169,#442170,#442171)),.UNSPECIFIED.,.F.,
 .F.,.F.)
B_SPLINE_SURFACE_WITH_KNOTS((4,4),(3,3),(0.,0.000101260117256738),(0.,1.),
 .UNSPECIFIED.)
GEOMETRIC_REPRESENTATION_ITEM()
RATIONAL_B_SPLINE_SURFACE(((1.,0.79661527883517,1.),(1.,0.795896038055938,
1.),(1.,0.795193354661352,1.),(1.,0.794506193185546,1.)))
REPRESENTATION_ITEM('')
SURFACE()
);
#3864=(
BOUNDED_SURFACE()
B_SPLINE_SURFACE(3,2,((#442209,#442210,#442211),(#442212,#442213,#442214),
(#442215,#442216,#442217),(#442218,#442219,#442220),(#442221,#442222,#442223),
(#442224,#442225,#442226)),.UNSPECIFIED.,.F.,.F.,.F.)
B_SPLINE_SURFACE_WITH_KNOTS((4,2,4),(3,3),(1.18584612615602E-19,1.66936432462296E-5,
3.33872864924591E-5),(0.,1.),.UNSPECIFIED.)
GEOMETRIC_REPRESENTATION_ITEM()
RATIONAL_B_SPLINE_SURFACE(((1.,0.796615278835173,1.),(1.,0.862310524418132,
1.),(1.,0.923774472010519,1.),(1.,0.923983993203429,1.),(1.,0.862574873720937,
1.),(1.,0.796615278835185,1.)))
REPRESENTATION_ITEM('')
SURFACE()
);
#3865=(
BOUNDED_SURFACE()
B_SPLINE_SURFACE(3,2,((#442263,#442264,#442265),(#442266,#442267,#442268),
(#442269,#442270,#442271),(#442272,#442273,#442274)),.UNSPECIFIED.,.F.,
 .F.,.F.)
B_SPLINE_SURFACE_WITH_KNOTS((4,4),(3,3),(0.,0.000101244905251112),(0.,1.),
 .UNSPECIFIED.)
GEOMETRIC_REPRESENTATION_ITEM()
RATIONAL_B_SPLINE_SURFACE(((1.,0.796615278835173,1.),(1.,0.795896146109791,
1.),(1.,0.795193565796504,1.),(1.,0.794506502889902,1.)))
REPRESENTATION_ITEM('')
SURFACE()
);
#3866=(
BOUNDED_SURFACE()
B_SPLINE_SURFACE(3,2,((#442310,#442311,#442312),(#442313,#442314,#442315),
(#442316,#442317,#442318),(#442319,#442320,#442321)),.UNSPECIFIED.,.F.,
 .F.,.F.)
B_SPLINE_SURFACE_WITH_KNOTS((4,4),(3,3),(2.85968127239939E-5,9.24681548475818E-5),
(-0.00167900678658251,1.01130827127826),.UNSPECIFIED.)
GEOMETRIC_REPRESENTATION_ITEM()
RATIONAL_B_SPLINE_SURFACE(((1.00059040895218,0.822187541868258,1.00401468696658),
(1.0003652771814,0.889990093671564,1.00248382673392),(1.00016469515013,
0.950399042257928,1.00111990082511),(1.00025604273993,0.922888044286075,
1.00174104990632)))
REPRESENTATION_ITEM('')
SURFACE()
);
#3867=(
BOUNDED_SURFACE()
B_SPLINE_SURFACE(3,2,((#442325,#442326,#442327),(#442328,#442329,#442330),
(#442331,#442332,#442333),(#442334,#442335,#442336)),.UNSPECIFIED.,.F.,
 .F.,.F.)
B_SPLINE_SURFACE_WITH_KNOTS((4,4),(3,3),(-5.22358356749274E-6,5.74594192424278E-5),
(-0.0012712005206484,1.),.UNSPECIFIED.)
GEOMETRIC_REPRESENTATION_ITEM()
RATIONAL_B_SPLINE_SURFACE(((1.00054449313179,0.78583507363874,1.),(1.00047707767478,
0.812351526358843,1.),(1.0004403178859,0.826810216506262,1.),(1.00044777653322,
0.823876514387242,0.999999999999999)))
REPRESENTATION_ITEM('')
SURFACE()
);
#3868=(
BOUNDED_SURFACE()
B_SPLINE_SURFACE(3,2,((#442338,#442339,#442340),(#442341,#442342,#442343),
(#442344,#442345,#442346),(#442347,#442348,#442349)),.UNSPECIFIED.,.F.,
 .F.,.F.)
B_SPLINE_SURFACE_WITH_KNOTS((4,4),(3,3),(-5.42101086242752E-20,4.88747512969881E-5),
(-0.000215805215096801,1.),.UNSPECIFIED.)
GEOMETRIC_REPRESENTATION_ITEM()
RATIONAL_B_SPLINE_SURFACE(((1.00008915600322,0.793434085499825,1.),(1.00008930224975,
0.793095246303367,1.),(1.00008944684597,0.792760230720641,1.),(1.00008958984376,
0.792428918540674,1.)))
REPRESENTATION_ITEM('')
SURFACE()
);
#3869=(
BOUNDED_SURFACE()
B_SPLINE_SURFACE(3,2,((#442351,#442352,#442353),(#442354,#442355,#442356),
(#442357,#442358,#442359),(#442360,#442361,#442362),(#442363,#442364,#442365),
(#442366,#442367,#442368)),.UNSPECIFIED.,.F.,.F.,.F.)
B_SPLINE_SURFACE_WITH_KNOTS((4,2,4),(3,3),(6.09863722023096E-20,7.62675010863195E-5,
0.000152535002172639),(0.,1.02152348203069),.UNSPECIFIED.)
GEOMETRIC_REPRESENTATION_ITEM()
RATIONAL_B_SPLINE_SURFACE(((1.,0.789033595401248,1.00908146323692),(1.,
0.857071781054843,1.00615262590429),(1.,0.92208726471072,1.00335390671592),
(1.,0.922394466502381,1.00334068261144),(1.,0.857224384599051,1.00614605678501),
(1.,0.789033595401646,1.0090814632369)))
REPRESENTATION_ITEM('')
SURFACE()
);
#3870=(
BOUNDED_SURFACE()
B_SPLINE_SURFACE(3,2,((#442370,#442371,#442372),(#442373,#442374,#442375),
(#442376,#442377,#442378),(#442379,#442380,#442381)),.UNSPECIFIED.,.F.,
 .F.,.F.)
B_SPLINE_SURFACE_WITH_KNOTS((4,4),(3,3),(8.13151629364128E-20,4.88747512969882E-5),
(-0.000215489857699746,1.),.UNSPECIFIED.)
GEOMETRIC_REPRESENTATION_ITEM()
RATIONAL_B_SPLINE_SURFACE(((1.00008945889741,0.792428983985608,1.),(1.00008931610862,
0.792760296061175,1.),(1.00008917172375,0.793095311538219,1.),(1.00008902569097,
0.793434150627864,1.)))
REPRESENTATION_ITEM('')
SURFACE()
);
#3871=(
BOUNDED_SURFACE()
B_SPLINE_SURFACE(3,2,((#442383,#442384,#442385),(#442386,#442387,#442388),
(#442389,#442390,#442391),(#442392,#442393,#442394)),.UNSPECIFIED.,.F.,
 .F.,.F.)
B_SPLINE_SURFACE_WITH_KNOTS((4,4),(3,3),(-5.21974905013091E-6,5.74172395514411E-5),
(-0.00139822857775922,1.00051312364068),.UNSPECIFIED.)
GEOMETRIC_REPRESENTATION_ITEM()
RATIONAL_B_SPLINE_SURFACE(((1.00049256947257,0.823768952243979,1.00018060397849),
(1.00048448215728,0.826662424388264,1.00017763870882),(1.00052427784036,
0.812424361909345,1.00019223006921),(1.00059912365872,0.785646094632693,
1.00021967280231)))
REPRESENTATION_ITEM('')
SURFACE()
);
#3872=(
BOUNDED_SURFACE()
B_SPLINE_SURFACE(3,2,((#442398,#442399,#442400),(#442401,#442402,#442403),
(#442404,#442405,#442406),(#442407,#442408,#442409)),.UNSPECIFIED.,.F.,
 .F.,.F.)
B_SPLINE_SURFACE_WITH_KNOTS((4,4),(3,3),(3.2298077433778E-5,9.63764854872256E-5),
(-0.00154325936351672,1.01095292447559),.UNSPECIFIED.)
GEOMETRIC_REPRESENTATION_ITEM()
RATIONAL_B_SPLINE_SURFACE(((1.00023530983296,0.922925743796168,1.00168574728333),
(1.00015136166123,0.950422439594232,1.00108434699061),(1.00033574337394,
0.890029368953954,1.00240524789551),(1.00054260094214,0.822274473168349,
1.00388716464864)))
REPRESENTATION_ITEM('')
SURFACE()
);
#3873=(
BOUNDED_SURFACE()
B_SPLINE_SURFACE(3,2,((#442509,#442510,#442511),(#442512,#442513,#442514),
(#442515,#442516,#442517),(#442518,#442519,#442520)),.UNSPECIFIED.,.F.,
 .F.,.F.)
B_SPLINE_SURFACE_WITH_KNOTS((4,4),(3,3),(0.,0.000101260117256738),(0.,1.),
 .UNSPECIFIED.)
GEOMETRIC_REPRESENTATION_ITEM()
RATIONAL_B_SPLINE_SURFACE(((1.,0.796615278835173,1.),(1.,0.79589603805594,
1.),(1.,0.795193354661347,1.),(1.,0.794506193185548,1.)))
REPRESENTATION_ITEM('')
SURFACE()
);
#3874=(
BOUNDED_SURFACE()
B_SPLINE_SURFACE(3,2,((#442558,#442559,#442560),(#442561,#442562,#442563),
(#442564,#442565,#442566),(#442567,#442568,#442569),(#442570,#442571,#442572),
(#442573,#442574,#442575)),.UNSPECIFIED.,.F.,.F.,.F.)
B_SPLINE_SURFACE_WITH_KNOTS((4,2,4),(3,3),(2.28698895758661E-19,1.66936432462294E-5,
3.33872864924585E-5),(0.,1.),.UNSPECIFIED.)
GEOMETRIC_REPRESENTATION_ITEM()
RATIONAL_B_SPLINE_SURFACE(((1.,0.796615278835184,1.),(1.,0.862310524418132,
1.),(1.,0.923774472010521,1.),(1.,0.923983993203422,1.),(1.,0.862574873720953,
1.),(1.,0.796615278835186,1.)))
REPRESENTATION_ITEM('')
SURFACE()
);
#3875=(
BOUNDED_SURFACE()
B_SPLINE_SURFACE(3,2,((#442612,#442613,#442614),(#442615,#442616,#442617),
(#442618,#442619,#442620),(#442621,#442622,#442623)),.UNSPECIFIED.,.F.,
 .F.,.F.)
B_SPLINE_SURFACE_WITH_KNOTS((4,4),(3,3),(-2.16840434497101E-19,0.000101244905251112),
(0.,1.),.UNSPECIFIED.)
GEOMETRIC_REPRESENTATION_ITEM()
RATIONAL_B_SPLINE_SURFACE(((1.,0.796615278835171,1.),(1.,0.795896146109791,
1.),(1.,0.795193565796496,1.),(1.,0.794506502889899,1.)))
REPRESENTATION_ITEM('')
SURFACE()
);
#3876=(
BOUNDED_SURFACE()
B_SPLINE_SURFACE(3,2,((#442659,#442660,#442661),(#442662,#442663,#442664),
(#442665,#442666,#442667),(#442668,#442669,#442670)),.UNSPECIFIED.,.F.,
 .F.,.F.)
B_SPLINE_SURFACE_WITH_KNOTS((4,4),(3,3),(2.85968127239939E-5,9.24681548475819E-5),
(-0.0016790067946991,1.01130827127835),.UNSPECIFIED.)
GEOMETRIC_REPRESENTATION_ITEM()
RATIONAL_B_SPLINE_SURFACE(((1.00059040895504,0.822187541866784,1.00401468696661),
(1.00036527718317,0.889990093670652,1.00248382673394),(1.00016469515093,
0.950399042257517,1.00111990082512),(1.00025604274117,0.922888044285435,
1.00174104990633)))
REPRESENTATION_ITEM('')
SURFACE()
);
#3877=(
BOUNDED_SURFACE()
B_SPLINE_SURFACE(3,2,((#442674,#442675,#442676),(#442677,#442678,#442679),
(#442680,#442681,#442682),(#442683,#442684,#442685)),.UNSPECIFIED.,.F.,
 .F.,.F.)
B_SPLINE_SURFACE_WITH_KNOTS((4,4),(3,3),(-5.22358356749143E-6,5.74594192424279E-5),
(-0.00127120052051176,1.),.UNSPECIFIED.)
GEOMETRIC_REPRESENTATION_ITEM()
RATIONAL_B_SPLINE_SURFACE(((1.00054449313173,0.78583507363877,1.),(1.00047707767473,
0.812351526358871,1.),(1.00044031788585,0.826810216506278,1.),(1.00044777653317,
0.823876514387267,0.999999999999999)))
REPRESENTATION_ITEM('')
SURFACE()
);
#3878=(
BOUNDED_SURFACE()
B_SPLINE_SURFACE(3,2,((#442687,#442688,#442689),(#442690,#442691,#442692),
(#442693,#442694,#442695),(#442696,#442697,#442698)),.UNSPECIFIED.,.F.,
 .F.,.F.)
B_SPLINE_SURFACE_WITH_KNOTS((4,4),(3,3),(2.71050543121376E-20,4.8874751296988E-5),
(-0.000215805215085956,1.),.UNSPECIFIED.)
GEOMETRIC_REPRESENTATION_ITEM()
RATIONAL_B_SPLINE_SURFACE(((1.00008915600322,0.793434085499825,1.),(1.00008930224975,
0.793095246303369,1.),(1.00008944684597,0.792760230720644,1.),(1.00008958984376,
0.792428918540674,1.)))
REPRESENTATION_ITEM('')
SURFACE()
);
#3879=(
BOUNDED_SURFACE()
B_SPLINE_SURFACE(3,2,((#442700,#442701,#442702),(#442703,#442704,#442705),
(#442706,#442707,#442708),(#442709,#442710,#442711),(#442712,#442713,#442714),
(#442715,#442716,#442717)),.UNSPECIFIED.,.F.,.F.,.F.)
B_SPLINE_SURFACE_WITH_KNOTS((4,2,4),(3,3),(2.03287907341032E-20,7.62675010863199E-5,
0.00015253500217264),(0.,1.02152348203066),.UNSPECIFIED.)
GEOMETRIC_REPRESENTATION_ITEM()
RATIONAL_B_SPLINE_SURFACE(((1.,0.789033595401254,1.00908146323691),(1.,
0.857071781054841,1.00615262590428),(1.,0.922087264710727,1.00335390671592),
(1.,0.922394466502377,1.00334068261143),(1.,0.857224384599056,1.006146056785),
(1.,0.789033595401652,1.00908146323689)))
REPRESENTATION_ITEM('')
SURFACE()
);
#3880=(
BOUNDED_SURFACE()
B_SPLINE_SURFACE(3,2,((#442719,#442720,#442721),(#442722,#442723,#442724),
(#442725,#442726,#442727),(#442728,#442729,#442730)),.UNSPECIFIED.,.F.,
 .F.,.F.)
B_SPLINE_SURFACE_WITH_KNOTS((4,4),(3,3),(4.33680868994202E-19,4.88747512969881E-5),
(-0.000215489856948962,1.),.UNSPECIFIED.)
GEOMETRIC_REPRESENTATION_ITEM()
RATIONAL_B_SPLINE_SURFACE(((1.00008945889709,0.792428983985764,1.),(1.00008931610831,
0.792760296061302,1.),(1.00008917172344,0.793095311538389,1.),(1.00008902569066,
0.793434150628012,1.)))
REPRESENTATION_ITEM('')
SURFACE()
);
#3881=(
BOUNDED_SURFACE()
B_SPLINE_SURFACE(3,2,((#442732,#442733,#442734),(#442735,#442736,#442737),
(#442738,#442739,#442740),(#442741,#442742,#442743)),.UNSPECIFIED.,.F.,
 .F.,.F.)
B_SPLINE_SURFACE_WITH_KNOTS((4,4),(3,3),(-5.21974905012881E-6,5.74172395514414E-5),
(-0.00139822857773428,1.0005131236407),.UNSPECIFIED.)
GEOMETRIC_REPRESENTATION_ITEM()
RATIONAL_B_SPLINE_SURFACE(((1.00049256947256,0.823768952243969,1.0001806039785),
(1.00048448215727,0.826662424388272,1.00017763870883),(1.00052427784035,
0.812424361909323,1.00019223006923),(1.0005991236587,0.785646094632698,
1.00021967280233)))
REPRESENTATION_ITEM('')
SURFACE()
);
#3882=(
BOUNDED_SURFACE()
B_SPLINE_SURFACE(3,2,((#442747,#442748,#442749),(#442750,#442751,#442752),
(#442753,#442754,#442755),(#442756,#442757,#442758)),.UNSPECIFIED.,.F.,
 .F.,.F.)
B_SPLINE_SURFACE_WITH_KNOTS((4,4),(3,3),(3.22980774337778E-5,9.63764854872253E-5),
(-0.00154325936372609,1.01095292447536),.UNSPECIFIED.)
GEOMETRIC_REPRESENTATION_ITEM()
RATIONAL_B_SPLINE_SURFACE(((1.00023530983299,0.922925743796169,1.0016857472833),
(1.00015136166125,0.950422439594221,1.00108434699059),(1.00033574337398,
0.890029368953967,1.00240524789546),(1.00054260094221,0.822274473168345,
1.00388716464856)))
REPRESENTATION_ITEM('')
SURFACE()
);
#3883=(
BOUNDED_SURFACE()
B_SPLINE_SURFACE(3,2,((#442858,#442859,#442860),(#442861,#442862,#442863),
(#442864,#442865,#442866),(#442867,#442868,#442869)),.UNSPECIFIED.,.F.,
 .F.,.F.)
B_SPLINE_SURFACE_WITH_KNOTS((4,4),(3,3),(0.,0.000101260117256738),(0.,1.),
 .UNSPECIFIED.)
GEOMETRIC_REPRESENTATION_ITEM()
RATIONAL_B_SPLINE_SURFACE(((1.,0.79661527883517,1.),(1.,0.795896038055939,
1.),(1.,0.79519335466135,1.),(1.,0.794506193185545,1.)))
REPRESENTATION_ITEM('')
SURFACE()
);
#3884=(
BOUNDED_SURFACE()
B_SPLINE_SURFACE(3,2,((#442907,#442908,#442909),(#442910,#442911,#442912),
(#442913,#442914,#442915),(#442916,#442917,#442918),(#442919,#442920,#442921),
(#442922,#442923,#442924)),.UNSPECIFIED.,.F.,.F.,.F.)
B_SPLINE_SURFACE_WITH_KNOTS((4,2,4),(3,3),(-1.06726151354042E-19,1.66936432462298E-5,
3.33872864924597E-5),(0.,1.),.UNSPECIFIED.)
GEOMETRIC_REPRESENTATION_ITEM()
RATIONAL_B_SPLINE_SURFACE(((1.,0.796615278835171,1.),(1.,0.862310524418125,
1.),(1.,0.923774472010519,1.),(1.,0.923983993203426,1.),(1.,0.862574873720946,
1.),(1.,0.796615278835184,1.)))
REPRESENTATION_ITEM('')
SURFACE()
);
#3885=(
BOUNDED_SURFACE()
B_SPLINE_SURFACE(3,2,((#442961,#442962,#442963),(#442964,#442965,#442966),
(#442967,#442968,#442969),(#442970,#442971,#442972)),.UNSPECIFIED.,.F.,
 .F.,.F.)
B_SPLINE_SURFACE_WITH_KNOTS((4,4),(3,3),(0.,0.000101244905251112),(0.,1.),
 .UNSPECIFIED.)
GEOMETRIC_REPRESENTATION_ITEM()
RATIONAL_B_SPLINE_SURFACE(((1.,0.79661527883517,1.),(1.,0.795896146109796,
1.),(1.,0.7951935657965,1.),(1.,0.794506502889897,1.)))
REPRESENTATION_ITEM('')
SURFACE()
);
#3886=(
BOUNDED_SURFACE()
B_SPLINE_SURFACE(3,2,((#443008,#443009,#443010),(#443011,#443012,#443013),
(#443014,#443015,#443016),(#443017,#443018,#443019)),.UNSPECIFIED.,.F.,
 .F.,.F.)
B_SPLINE_SURFACE_WITH_KNOTS((4,4),(3,3),(2.85968127239938E-5,9.24681548475817E-5),
(-0.00167900678627269,1.01130827127815),.UNSPECIFIED.)
GEOMETRIC_REPRESENTATION_ITEM()
RATIONAL_B_SPLINE_SURFACE(((1.00059040895207,0.822187541868334,1.00401468696654),
(1.00036527718134,0.889990093671605,1.00248382673389),(1.0001646951501,
0.950399042257946,1.0011199008251),(1.00025604273988,0.922888044286107,
1.0017410499063)))
REPRESENTATION_ITEM('')
SURFACE()
);
#3887=(
BOUNDED_SURFACE()
B_SPLINE_SURFACE(3,2,((#443023,#443024,#443025),(#443026,#443027,#443028),
(#443029,#443030,#443031),(#443032,#443033,#443034)),.UNSPECIFIED.,.F.,
 .F.,.F.)
B_SPLINE_SURFACE_WITH_KNOTS((4,4),(3,3),(-5.22358356749279E-6,5.74594192424277E-5),
(-0.00127120052061258,1.),.UNSPECIFIED.)
GEOMETRIC_REPRESENTATION_ITEM()
RATIONAL_B_SPLINE_SURFACE(((1.00054449313177,0.785835073638748,1.),(1.00047707767477,
0.812351526358847,1.),(1.00044031788588,0.826810216506265,1.),(1.00044777653321,
0.82387651438725,1.)))
REPRESENTATION_ITEM('')
SURFACE()
);
#3888=(
BOUNDED_SURFACE()
B_SPLINE_SURFACE(3,2,((#443036,#443037,#443038),(#443039,#443040,#443041),
(#443042,#443043,#443044),(#443045,#443046,#443047)),.UNSPECIFIED.,.F.,
 .F.,.F.)
B_SPLINE_SURFACE_WITH_KNOTS((4,4),(3,3),(-1.62630325872826E-19,4.88747512969879E-5),
(-0.000215805215084324,1.),.UNSPECIFIED.)
GEOMETRIC_REPRESENTATION_ITEM()
RATIONAL_B_SPLINE_SURFACE(((1.00008915600322,0.793434085499825,1.),(1.00008930224975,
0.793095246303363,1.),(1.00008944684597,0.792760230720643,1.),(1.00008958984376,
0.792428918540676,1.)))
REPRESENTATION_ITEM('')
SURFACE()
);
#3889=(
BOUNDED_SURFACE()
B_SPLINE_SURFACE(3,2,((#443049,#443050,#443051),(#443052,#443053,#443054),
(#443055,#443056,#443057),(#443058,#443059,#443060),(#443061,#443062,#443063),
(#443064,#443065,#443066)),.UNSPECIFIED.,.F.,.F.,.F.)
B_SPLINE_SURFACE_WITH_KNOTS((4,2,4),(3,3),(1.89735380184963E-19,7.62675010863201E-5,
0.00015253500217264),(0.,1.02152348203042),.UNSPECIFIED.)
GEOMETRIC_REPRESENTATION_ITEM()
RATIONAL_B_SPLINE_SURFACE(((1.,0.789033595401301,1.0090814632368),(1.,0.857071781054865,
1.00615262590421),(1.,0.922087264710765,1.00335390671588),(1.,0.922394466502376,
1.00334068261139),(1.,0.857224384599105,1.00614605678493),(1.,0.7890335954017,
1.00908146323679)))
REPRESENTATION_ITEM('')
SURFACE()
);
#3890=(
BOUNDED_SURFACE()
B_SPLINE_SURFACE(3,2,((#443068,#443069,#443070),(#443071,#443072,#443073),
(#443074,#443075,#443076),(#443077,#443078,#443079)),.UNSPECIFIED.,.F.,
 .F.,.F.)
B_SPLINE_SURFACE_WITH_KNOTS((4,4),(3,3),(1.62630325872826E-19,4.88747512969885E-5),
(-0.000215489856958563,1.),.UNSPECIFIED.)
GEOMETRIC_REPRESENTATION_ITEM()
RATIONAL_B_SPLINE_SURFACE(((1.0000894588971,0.792428983985762,1.),(1.00008931610832,
0.792760296061314,1.),(1.00008917172344,0.793095311538372,1.),(1.00008902569067,
0.793434150628011,1.)))
REPRESENTATION_ITEM('')
SURFACE()
);
#3891=(
BOUNDED_SURFACE()
B_SPLINE_SURFACE(3,2,((#443081,#443082,#443083),(#443084,#443085,#443086),
(#443087,#443088,#443089),(#443090,#443091,#443092)),.UNSPECIFIED.,.F.,
 .F.,.F.)
B_SPLINE_SURFACE_WITH_KNOTS((4,4),(3,3),(-5.21974905013081E-6,5.74172395514397E-5),
(-0.00139822857806521,1.00051312364087),.UNSPECIFIED.)
GEOMETRIC_REPRESENTATION_ITEM()
RATIONAL_B_SPLINE_SURFACE(((1.00049256947268,0.823768952243879,1.00018060397856),
(1.00048448215738,0.826662424388185,1.00017763870889),(1.00052427784047,
0.81242436190924,1.00019223006929),(1.00059912365885,0.785646094632593,
1.0002196728024)))
REPRESENTATION_ITEM('')
SURFACE()
);
#3892=(
BOUNDED_SURFACE()
B_SPLINE_SURFACE(3,2,((#443096,#443097,#443098),(#443099,#443100,#443101),
(#443102,#443103,#443104),(#443105,#443106,#443107)),.UNSPECIFIED.,.F.,
 .F.,.F.)
B_SPLINE_SURFACE_WITH_KNOTS((4,4),(3,3),(3.22980774337778E-5,9.63764854872243E-5),
(-0.0015432593634407,1.0109529244754),.UNSPECIFIED.)
GEOMETRIC_REPRESENTATION_ITEM()
RATIONAL_B_SPLINE_SURFACE(((1.00023530983294,0.922925743796191,1.0016857472833),
(1.00015136166123,0.950422439594233,1.00108434699059),(1.00033574337392,
0.89002936895399,1.00240524789547),(1.00054260094211,0.822274473168393,
1.00388716464857)))
REPRESENTATION_ITEM('')
SURFACE()
);
#3893=(
BOUNDED_SURFACE()
B_SPLINE_SURFACE(3,2,((#443207,#443208,#443209),(#443210,#443211,#443212),
(#443213,#443214,#443215),(#443216,#443217,#443218)),.UNSPECIFIED.,.F.,
 .F.,.F.)
B_SPLINE_SURFACE_WITH_KNOTS((4,4),(3,3),(-2.16840434497101E-19,0.000101260117256737),
(0.,1.),.UNSPECIFIED.)
GEOMETRIC_REPRESENTATION_ITEM()
RATIONAL_B_SPLINE_SURFACE(((1.,0.796615278835171,1.),(1.,0.795896038055952,
1.),(1.,0.795193354661332,1.),(1.,0.794506193185545,1.)))
REPRESENTATION_ITEM('')
SURFACE()
);
#3894=(
BOUNDED_SURFACE()
B_SPLINE_SURFACE(3,2,((#443256,#443257,#443258),(#443259,#443260,#443261),
(#443262,#443263,#443264),(#443265,#443266,#443267),(#443268,#443269,#443270),
(#443271,#443272,#443273)),.UNSPECIFIED.,.F.,.F.,.F.)
B_SPLINE_SURFACE_WITH_KNOTS((4,2,4),(3,3),(-2.03287907341032E-20,1.66936432462293E-5,
3.33872864924587E-5),(0.,1.),.UNSPECIFIED.)
GEOMETRIC_REPRESENTATION_ITEM()
RATIONAL_B_SPLINE_SURFACE(((1.,0.796615278835177,1.),(1.,0.862310524418135,
1.),(1.,0.92377447201052,1.),(1.,0.923983993203427,1.),(1.,0.862574873720944,
1.),(1.,0.796615278835187,1.)))
REPRESENTATION_ITEM('')
SURFACE()
);
#3895=(
BOUNDED_SURFACE()
B_SPLINE_SURFACE(3,2,((#443310,#443311,#443312),(#443313,#443314,#443315),
(#443316,#443317,#443318),(#443319,#443320,#443321)),.UNSPECIFIED.,.F.,
 .F.,.F.)
B_SPLINE_SURFACE_WITH_KNOTS((4,4),(3,3),(0.,0.000101244905251112),(0.,1.),
 .UNSPECIFIED.)
GEOMETRIC_REPRESENTATION_ITEM()
RATIONAL_B_SPLINE_SURFACE(((1.,0.79661527883517,1.),(1.,0.795896146109793,
1.),(1.,0.795193565796498,1.),(1.,0.794506502889899,1.)))
REPRESENTATION_ITEM('')
SURFACE()
);
#3896=(
BOUNDED_SURFACE()
B_SPLINE_SURFACE(3,2,((#443357,#443358,#443359),(#443360,#443361,#443362),
(#443363,#443364,#443365),(#443366,#443367,#443368)),.UNSPECIFIED.,.F.,
 .F.,.F.)
B_SPLINE_SURFACE_WITH_KNOTS((4,4),(3,3),(2.85968127239939E-5,9.24681548475817E-5),
(-0.00167900678708718,1.01130827127833),.UNSPECIFIED.)
GEOMETRIC_REPRESENTATION_ITEM()
RATIONAL_B_SPLINE_SURFACE(((1.00059040895236,0.82218754186816,1.00401468696661),
(1.00036527718151,0.889990093671499,1.00248382673393),(1.00016469515018,
0.950399042257896,1.00111990082512),(1.00025604274001,0.922888044286031,
1.00174104990633)))
REPRESENTATION_ITEM('')
SURFACE()
);
#3897=(
BOUNDED_SURFACE()
B_SPLINE_SURFACE(3,2,((#443372,#443373,#443374),(#443375,#443376,#443377),
(#443378,#443379,#443380),(#443381,#443382,#443383)),.UNSPECIFIED.,.F.,
 .F.,.F.)
B_SPLINE_SURFACE_WITH_KNOTS((4,4),(3,3),(-5.22358356749297E-6,5.74594192424277E-5),
(-0.00127120052032446,1.),.UNSPECIFIED.)
GEOMETRIC_REPRESENTATION_ITEM()
RATIONAL_B_SPLINE_SURFACE(((1.00054449313165,0.785835073638822,1.),(1.00047707767466,
0.812351526358885,1.),(1.00044031788578,0.826810216506333,1.),(1.0004477765331,
0.823876514387295,1.)))
REPRESENTATION_ITEM('')
SURFACE()
);
#3898=(
BOUNDED_SURFACE()
B_SPLINE_SURFACE(3,2,((#443385,#443386,#443387),(#443388,#443389,#443390),
(#443391,#443392,#443393),(#443394,#443395,#443396)),.UNSPECIFIED.,.F.,
 .F.,.F.)
B_SPLINE_SURFACE_WITH_KNOTS((4,4),(3,3),(-1.35525271560688E-19,4.8874751296988E-5),
(-0.000215805215246867,1.),.UNSPECIFIED.)
GEOMETRIC_REPRESENTATION_ITEM()
RATIONAL_B_SPLINE_SURFACE(((1.00008915600328,0.793434085499793,1.),(1.00008930224981,
0.79309524630333,1.),(1.00008944684603,0.792760230720615,1.),(1.00008958984383,
0.792428918540643,1.)))
REPRESENTATION_ITEM('')
SURFACE()
);
#3899=(
BOUNDED_SURFACE()
B_SPLINE_SURFACE(3,2,((#443398,#443399,#443400),(#443401,#443402,#443403),
(#443404,#443405,#443406),(#443407,#443408,#443409),(#443410,#443411,#443412),
(#443413,#443414,#443415)),.UNSPECIFIED.,.F.,.F.,.F.)
B_SPLINE_SURFACE_WITH_KNOTS((4,2,4),(3,3),(2.57498015965307E-19,7.62675010863198E-5,
0.000152535002172639),(0.,1.02152348203072),.UNSPECIFIED.)
GEOMETRIC_REPRESENTATION_ITEM()
RATIONAL_B_SPLINE_SURFACE(((1.,0.78903359540124,1.00908146323694),(1.,0.857071781054825,
1.0061526259043),(1.,0.922087264710737,1.00335390671593),(1.,0.922394466502358,
1.00334068261144),(1.,0.857224384599055,1.00614605678502),(1.,0.789033595401639,
1.00908146323692)))
REPRESENTATION_ITEM('')
SURFACE()
);
#3900=(
BOUNDED_SURFACE()
B_SPLINE_SURFACE(3,2,((#443417,#443418,#443419),(#443420,#443421,#443422),
(#443423,#443424,#443425),(#443426,#443427,#443428)),.UNSPECIFIED.,.F.,
 .F.,.F.)
B_SPLINE_SURFACE_WITH_KNOTS((4,4),(3,3),(2.43945488809238E-19,4.88747512969884E-5),
(-0.000215489857031757,1.),.UNSPECIFIED.)
GEOMETRIC_REPRESENTATION_ITEM()
RATIONAL_B_SPLINE_SURFACE(((1.00008945889713,0.792428983985742,1.),(1.00008931610835,
0.792760296061288,1.),(1.00008917172347,0.793095311538377,1.),(1.0000890256907,
0.793434150627996,1.)))
REPRESENTATION_ITEM('')
SURFACE()
);
#3901=(
BOUNDED_SURFACE()
B_SPLINE_SURFACE(3,2,((#443430,#443431,#443432),(#443433,#443434,#443435),
(#443436,#443437,#443438),(#443439,#443440,#443441)),.UNSPECIFIED.,.F.,
 .F.,.F.)
B_SPLINE_SURFACE_WITH_KNOTS((4,4),(3,3),(-5.21974905013094E-6,5.74172395514396E-5),
(-0.00139822857774065,1.00051312364089),.UNSPECIFIED.)
GEOMETRIC_REPRESENTATION_ITEM()
RATIONAL_B_SPLINE_SURFACE(((1.00049256947257,0.823768952243939,1.00018060397857),
(1.00048448215727,0.826662424388233,1.0001776387089),(1.00052427784035,
0.812424361909294,1.00019223006929),(1.00059912365871,0.785646094632658,
1.0002196728024)))
REPRESENTATION_ITEM('')
SURFACE()
);
#3902=(
BOUNDED_SURFACE()
B_SPLINE_SURFACE(3,2,((#443445,#443446,#443447),(#443448,#443449,#443450),
(#443451,#443452,#443453),(#443454,#443455,#443456)),.UNSPECIFIED.,.F.,
 .F.,.F.)
B_SPLINE_SURFACE_WITH_KNOTS((4,4),(3,3),(3.22980774337778E-5,9.63764854872255E-5),
(-0.0015432593638328,1.01095292447545),.UNSPECIFIED.)
GEOMETRIC_REPRESENTATION_ITEM()
RATIONAL_B_SPLINE_SURFACE(((1.000235309833,0.922925743796155,1.00168574728331),
(1.00015136166127,0.950422439594211,1.0010843469906),(1.000335743374,0.890029368953947,
1.00240524789548),(1.00054260094225,0.822274473168314,1.00388716464859)))
REPRESENTATION_ITEM('')
SURFACE()
);
#3903=(
BOUNDED_SURFACE()
B_SPLINE_SURFACE(3,2,((#443556,#443557,#443558),(#443559,#443560,#443561),
(#443562,#443563,#443564),(#443565,#443566,#443567)),.UNSPECIFIED.,.F.,
 .F.,.F.)
B_SPLINE_SURFACE_WITH_KNOTS((4,4),(3,3),(-2.16840434497101E-19,0.000101260117256738),
(0.,1.),.UNSPECIFIED.)
GEOMETRIC_REPRESENTATION_ITEM()
RATIONAL_B_SPLINE_SURFACE(((1.,0.796615278835171,1.),(1.,0.795896038055942,
1.),(1.,0.795193354661349,1.),(1.,0.794506193185546,1.)))
REPRESENTATION_ITEM('')
SURFACE()
);
#3904=(
BOUNDED_SURFACE()
B_SPLINE_SURFACE(3,2,((#443605,#443606,#443607),(#443608,#443609,#443610),
(#443611,#443612,#443613),(#443614,#443615,#443616),(#443617,#443618,#443619),
(#443620,#443621,#443622)),.UNSPECIFIED.,.F.,.F.,.F.)
B_SPLINE_SURFACE_WITH_KNOTS((4,2,4),(3,3),(1.25360876193636E-19,1.66936432462297E-5,
3.33872864924592E-5),(0.,1.),.UNSPECIFIED.)
GEOMETRIC_REPRESENTATION_ITEM()
RATIONAL_B_SPLINE_SURFACE(((1.,0.796615278835178,1.),(1.,0.862310524418135,
1.),(1.,0.923774472010519,1.),(1.,0.923983993203426,1.),(1.,0.862574873720954,
1.),(1.,0.796615278835182,1.)))
REPRESENTATION_ITEM('')
SURFACE()
);
#3905=(
BOUNDED_SURFACE()
B_SPLINE_SURFACE(3,2,((#443659,#443660,#443661),(#443662,#443663,#443664),
(#443665,#443666,#443667),(#443668,#443669,#443670)),.UNSPECIFIED.,.F.,
 .F.,.F.)
B_SPLINE_SURFACE_WITH_KNOTS((4,4),(3,3),(-2.16840434497101E-19,0.000101244905251112),
(0.,1.),.UNSPECIFIED.)
GEOMETRIC_REPRESENTATION_ITEM()
RATIONAL_B_SPLINE_SURFACE(((1.,0.79661527883517,1.),(1.,0.795896146109798,
1.),(1.,0.795193565796495,1.),(1.,0.794506502889903,1.)))
REPRESENTATION_ITEM('')
SURFACE()
);
#3906=(
BOUNDED_SURFACE()
B_SPLINE_SURFACE(3,2,((#443706,#443707,#443708),(#443709,#443710,#443711),
(#443712,#443713,#443714),(#443715,#443716,#443717)),.UNSPECIFIED.,.F.,
 .F.,.F.)
B_SPLINE_SURFACE_WITH_KNOTS((4,4),(3,3),(2.85968127239938E-5,9.24681548475816E-5),
(-0.0016790067878167,1.01130827127815),.UNSPECIFIED.)
GEOMETRIC_REPRESENTATION_ITEM()
RATIONAL_B_SPLINE_SURFACE(((1.00059040895262,0.82218754186806,1.00401468696654),
(1.00036527718167,0.889990093671433,1.00248382673389),(1.00016469515026,
0.950399042257871,1.0011199008251),(1.00025604274012,0.922888044285985,
1.0017410499063)))
REPRESENTATION_ITEM('')
SURFACE()
);
#3907=(
BOUNDED_SURFACE()
B_SPLINE_SURFACE(3,2,((#443721,#443722,#443723),(#443724,#443725,#443726),
(#443727,#443728,#443729),(#443730,#443731,#443732)),.UNSPECIFIED.,.F.,
 .F.,.F.)
B_SPLINE_SURFACE_WITH_KNOTS((4,4),(3,3),(-5.22358356749278E-6,5.74594192424278E-5),
(-0.0012712005204861,1.),.UNSPECIFIED.)
GEOMETRIC_REPRESENTATION_ITEM()
RATIONAL_B_SPLINE_SURFACE(((1.00054449313172,0.785835073638772,1.),(1.00047707767472,
0.812351526358881,1.),(1.00044031788584,0.826810216506285,1.),(1.00044777653316,
0.823876514387271,1.)))
REPRESENTATION_ITEM('')
SURFACE()
);
#3908=(
BOUNDED_SURFACE()
B_SPLINE_SURFACE(3,2,((#443734,#443735,#443736),(#443737,#443738,#443739),
(#443740,#443741,#443742),(#443743,#443744,#443745)),.UNSPECIFIED.,.F.,
 .F.,.F.)
B_SPLINE_SURFACE_WITH_KNOTS((4,4),(3,3),(-3.25260651745651E-19,4.8874751296988E-5),
(-0.000215805215234466,1.),.UNSPECIFIED.)
GEOMETRIC_REPRESENTATION_ITEM()
RATIONAL_B_SPLINE_SURFACE(((1.00008915600328,0.793434085499797,1.),(1.00008930224981,
0.793095246303335,1.),(1.00008944684603,0.792760230720615,1.),(1.00008958984382,
0.792428918540643,1.)))
REPRESENTATION_ITEM('')
SURFACE()
);
#3909=(
BOUNDED_SURFACE()
B_SPLINE_SURFACE(3,2,((#443747,#443748,#443749),(#443750,#443751,#443752),
(#443753,#443754,#443755),(#443756,#443757,#443758),(#443759,#443760,#443761),
(#443762,#443763,#443764)),.UNSPECIFIED.,.F.,.F.,.F.)
B_SPLINE_SURFACE_WITH_KNOTS((4,2,4),(3,3),(1.62630325872826E-19,7.626750108632E-5,
0.00015253500217264),(0.,1.02152348203049),.UNSPECIFIED.)
GEOMETRIC_REPRESENTATION_ITEM()
RATIONAL_B_SPLINE_SURFACE(((1.,0.789033595401288,1.00908146323684),(1.,
0.857071781054874,1.00615262590423),(1.,0.922087264710735,1.00335390671589),
(1.,0.922394466502399,1.0033406826114),(1.,0.857224384599066,1.00614605678495),
(1.,0.78903359540169,1.00908146323682)))
REPRESENTATION_ITEM('')
SURFACE()
);
#3910=(
BOUNDED_SURFACE()
B_SPLINE_SURFACE(3,2,((#443766,#443767,#443768),(#443769,#443770,#443771),
(#443772,#443773,#443774),(#443775,#443776,#443777)),.UNSPECIFIED.,.F.,
 .F.,.F.)
B_SPLINE_SURFACE_WITH_KNOTS((4,4),(3,3),(1.89735380184963E-19,4.88747512969881E-5),
(-0.000215489857082434,1.),.UNSPECIFIED.)
GEOMETRIC_REPRESENTATION_ITEM()
RATIONAL_B_SPLINE_SURFACE(((1.00008945889715,0.792428983985737,1.),(1.00008931610837,
0.792760296061274,1.),(1.00008917172349,0.793095311538363,1.),(1.00008902569072,
0.793434150627986,1.)))
REPRESENTATION_ITEM('')
SURFACE()
);
#3911=(
BOUNDED_SURFACE()
B_SPLINE_SURFACE(3,2,((#443779,#443780,#443781),(#443782,#443783,#443784),
(#443785,#443786,#443787),(#443788,#443789,#443790)),.UNSPECIFIED.,.F.,
 .F.,.F.)
B_SPLINE_SURFACE_WITH_KNOTS((4,4),(3,3),(-5.219749050131E-6,5.74172395514409E-5),
(-0.00139822857753858,1.00051312364028),.UNSPECIFIED.)
GEOMETRIC_REPRESENTATION_ITEM()
RATIONAL_B_SPLINE_SURFACE(((1.0004925694725,0.823768952244087,1.00018060397836),
(1.0004844821572,0.826662424388369,1.00017763870869),(1.00052427784028,
0.81242436190945,1.00019223006907),(1.00059912365862,0.785646094632834,
1.00021967280214)))
REPRESENTATION_ITEM('')
SURFACE()
);
#3912=(
BOUNDED_SURFACE()
B_SPLINE_SURFACE(3,2,((#443794,#443795,#443796),(#443797,#443798,#443799),
(#443800,#443801,#443802),(#443803,#443804,#443805)),.UNSPECIFIED.,.F.,
 .F.,.F.)
B_SPLINE_SURFACE_WITH_KNOTS((4,4),(3,3),(3.22980774337778E-5,9.63764854872256E-5),
(-0.00154325936393493,1.01095292447551),.UNSPECIFIED.)
GEOMETRIC_REPRESENTATION_ITEM()
RATIONAL_B_SPLINE_SURFACE(((1.00023530983302,0.92292574379614,1.00168574728332),
(1.00015136166128,0.950422439594204,1.00108434699061),(1.00033574337403,
0.890029368953927,1.00240524789549),(1.00054260094228,0.822274473168288,
1.00388716464861)))
REPRESENTATION_ITEM('')
SURFACE()
);
#3913=(
BOUNDED_SURFACE()
B_SPLINE_SURFACE(3,2,((#443905,#443906,#443907),(#443908,#443909,#443910),
(#443911,#443912,#443913),(#443914,#443915,#443916)),.UNSPECIFIED.,.F.,
 .F.,.F.)
B_SPLINE_SURFACE_WITH_KNOTS((4,4),(3,3),(-2.16840434497101E-19,0.000101260117256738),
(0.,1.),.UNSPECIFIED.)
GEOMETRIC_REPRESENTATION_ITEM()
RATIONAL_B_SPLINE_SURFACE(((1.,0.796615278835172,1.),(1.,0.795896038055946,
1.),(1.,0.795193354661346,1.),(1.,0.794506193185549,1.)))
REPRESENTATION_ITEM('')
SURFACE()
);
#3914=(
BOUNDED_SURFACE()
B_SPLINE_SURFACE(3,2,((#443954,#443955,#443956),(#443957,#443958,#443959),
(#443960,#443961,#443962),(#443963,#443964,#443965),(#443966,#443967,#443968),
(#443969,#443970,#443971)),.UNSPECIFIED.,.F.,.F.,.F.)
B_SPLINE_SURFACE_WITH_KNOTS((4,2,4),(3,3),(-1.67712523556351E-19,1.66936432462289E-5,
3.3387286492458E-5),(0.,1.),.UNSPECIFIED.)
GEOMETRIC_REPRESENTATION_ITEM()
RATIONAL_B_SPLINE_SURFACE(((1.,0.796615278835171,1.),(1.,0.862310524418131,
1.),(1.,0.923774472010519,1.),(1.,0.923983993203428,1.),(1.,0.862574873720941,
1.),(1.,0.796615278835185,1.)))
REPRESENTATION_ITEM('')
SURFACE()
);
#3915=(
BOUNDED_SURFACE()
B_SPLINE_SURFACE(3,2,((#444008,#444009,#444010),(#444011,#444012,#444013),
(#444014,#444015,#444016),(#444017,#444018,#444019)),.UNSPECIFIED.,.F.,
 .F.,.F.)
B_SPLINE_SURFACE_WITH_KNOTS((4,4),(3,3),(0.,0.000101244905251112),(0.,1.),
 .UNSPECIFIED.)
GEOMETRIC_REPRESENTATION_ITEM()
RATIONAL_B_SPLINE_SURFACE(((1.,0.796615278835171,1.),(1.,0.7958961461098,
1.),(1.,0.795193565796498,1.),(1.,0.794506502889905,1.)))
REPRESENTATION_ITEM('')
SURFACE()
);
#3916=(
BOUNDED_SURFACE()
B_SPLINE_SURFACE(3,2,((#444055,#444056,#444057),(#444058,#444059,#444060),
(#444061,#444062,#444063),(#444064,#444065,#444066)),.UNSPECIFIED.,.F.,
 .F.,.F.)
B_SPLINE_SURFACE_WITH_KNOTS((4,4),(3,3),(2.85968127239939E-5,9.24681548475817E-5),
(-0.00167900678787809,1.01130827127808),.UNSPECIFIED.)
GEOMETRIC_REPRESENTATION_ITEM()
RATIONAL_B_SPLINE_SURFACE(((1.00059040895264,0.822187541868059,1.00401468696652),
(1.00036527718169,0.88999009367143,1.00248382673388),(1.00016469515026,
0.950399042257877,1.00111990082509),(1.00025604274013,0.922888044285986,
1.00174104990629)))
REPRESENTATION_ITEM('')
SURFACE()
);
#3917=(
BOUNDED_SURFACE()
B_SPLINE_SURFACE(3,2,((#444070,#444071,#444072),(#444073,#444074,#444075),
(#444076,#444077,#444078),(#444079,#444080,#444081)),.UNSPECIFIED.,.F.,
 .F.,.F.)
B_SPLINE_SURFACE_WITH_KNOTS((4,4),(3,3),(-5.22358356749313E-6,5.74594192424276E-5),
(-0.00127120052068568,1.),.UNSPECIFIED.)
GEOMETRIC_REPRESENTATION_ITEM()
RATIONAL_B_SPLINE_SURFACE(((1.00054449313181,0.785835073638733,1.),(1.0004770776748,
0.812351526358834,1.),(1.00044031788591,0.826810216506262,1.),(1.00044777653323,
0.823876514387234,1.)))
REPRESENTATION_ITEM('')
SURFACE()
);
#3918=(
BOUNDED_SURFACE()
B_SPLINE_SURFACE(3,2,((#444083,#444084,#444085),(#444086,#444087,#444088),
(#444089,#444090,#444091),(#444092,#444093,#444094)),.UNSPECIFIED.,.F.,
 .F.,.F.)
B_SPLINE_SURFACE_WITH_KNOTS((4,4),(3,3),(-4.60785923306339E-19,4.8874751296988E-5),
(-0.000215805216141731,1.),.UNSPECIFIED.)
GEOMETRIC_REPRESENTATION_ITEM()
RATIONAL_B_SPLINE_SURFACE(((1.00008915600365,0.793434085499609,1.),(1.00008930225018,
0.793095246303164,1.),(1.00008944684641,0.792760230720417,1.),(1.0000895898442,
0.792428918540459,1.)))
REPRESENTATION_ITEM('')
SURFACE()
);
#3919=(
BOUNDED_SURFACE()
B_SPLINE_SURFACE(3,2,((#444096,#444097,#444098),(#444099,#444100,#444101),
(#444102,#444103,#444104),(#444105,#444106,#444107),(#444108,#444109,#444110),
(#444111,#444112,#444113)),.UNSPECIFIED.,.F.,.F.,.F.)
B_SPLINE_SURFACE_WITH_KNOTS((4,2,4),(3,3),(1.35525271560688E-19,7.62675010863194E-5,
0.000152535002172639),(0.,1.02152348203065),.UNSPECIFIED.)
GEOMETRIC_REPRESENTATION_ITEM()
RATIONAL_B_SPLINE_SURFACE(((1.,0.789033595401256,1.00908146323691),(1.,
0.857071781054846,1.00615262590428),(1.,0.922087264710725,1.00335390671592),
(1.,0.922394466502383,1.00334068261143),(1.,0.857224384599043,1.006146056785),
(1.,0.789033595401655,1.00908146323689)))
REPRESENTATION_ITEM('')
SURFACE()
);
#3920=(
BOUNDED_SURFACE()
B_SPLINE_SURFACE(3,2,((#444115,#444116,#444117),(#444118,#444119,#444120),
(#444121,#444122,#444123),(#444124,#444125,#444126)),.UNSPECIFIED.,.F.,
 .F.,.F.)
B_SPLINE_SURFACE_WITH_KNOTS((4,4),(3,3),(3.52365706057789E-19,4.88747512969884E-5),
(-0.000215489857101505,1.),.UNSPECIFIED.)
GEOMETRIC_REPRESENTATION_ITEM()
RATIONAL_B_SPLINE_SURFACE(((1.00008945889716,0.792428983985735,1.),(1.00008931610838,
0.792760296061276,1.),(1.0000891717235,0.793095311538357,1.),(1.00008902569073,
0.793434150627985,1.)))
REPRESENTATION_ITEM('')
SURFACE()
);
#3921=(
BOUNDED_SURFACE()
B_SPLINE_SURFACE(3,2,((#444128,#444129,#444130),(#444131,#444132,#444133),
(#444134,#444135,#444136),(#444137,#444138,#444139)),.UNSPECIFIED.,.F.,
 .F.,.F.)
B_SPLINE_SURFACE_WITH_KNOTS((4,4),(3,3),(-5.21974905013088E-6,5.74172395514369E-5),
(-0.00139822857783258,1.0005131236407),.UNSPECIFIED.)
GEOMETRIC_REPRESENTATION_ITEM()
RATIONAL_B_SPLINE_SURFACE(((1.0004925694726,0.823768952243959,1.00018060397851),
(1.0004844821573,0.826662424388252,1.00017763870883),(1.00052427784039,
0.812424361909319,1.00019223006923),(1.00059912365875,0.785646094632685,
1.00021967280233)))
REPRESENTATION_ITEM('')
SURFACE()
);
#3922=(
BOUNDED_SURFACE()
B_SPLINE_SURFACE(3,2,((#444143,#444144,#444145),(#444146,#444147,#444148),
(#444149,#444150,#444151),(#444152,#444153,#444154)),.UNSPECIFIED.,.F.,
 .F.,.F.)
B_SPLINE_SURFACE_WITH_KNOTS((4,4),(3,3),(3.22980774337779E-5,9.63764854872245E-5),
(-0.00154325936379329,1.01095292447549),.UNSPECIFIED.)
GEOMETRIC_REPRESENTATION_ITEM()
RATIONAL_B_SPLINE_SURFACE(((1.000235309833,0.922925743796154,1.00168574728332),
(1.00015136166126,0.950422439594211,1.0010843469906),(1.000335743374,0.890029368953942,
1.00240524789549),(1.00054260094223,0.822274473168313,1.0038871646486)))
REPRESENTATION_ITEM('')
SURFACE()
);
#3923=(
BOUNDED_SURFACE()
B_SPLINE_SURFACE(3,2,((#444254,#444255,#444256),(#444257,#444258,#444259),
(#444260,#444261,#444262),(#444263,#444264,#444265)),.UNSPECIFIED.,.F.,
 .F.,.F.)
B_SPLINE_SURFACE_WITH_KNOTS((4,4),(3,3),(0.,0.000101260117256738),(0.,1.),
 .UNSPECIFIED.)
GEOMETRIC_REPRESENTATION_ITEM()
RATIONAL_B_SPLINE_SURFACE(((1.,0.796615278835172,1.),(1.,0.795896038055945,
1.),(1.,0.795193354661348,1.),(1.,0.794506193185548,1.)))
REPRESENTATION_ITEM('')
SURFACE()
);
#3924=(
BOUNDED_SURFACE()
B_SPLINE_SURFACE(3,2,((#444303,#444304,#444305),(#444306,#444307,#444308),
(#444309,#444310,#444311),(#444312,#444313,#444314),(#444315,#444316,#444317),
(#444318,#444319,#444320)),.UNSPECIFIED.,.F.,.F.,.F.)
B_SPLINE_SURFACE_WITH_KNOTS((4,2,4),(3,3),(-2.37169225231204E-20,1.66936432462295E-5,
3.33872864924591E-5),(0.,1.),.UNSPECIFIED.)
GEOMETRIC_REPRESENTATION_ITEM()
RATIONAL_B_SPLINE_SURFACE(((1.,0.796615278835175,1.),(1.,0.862310524418127,
1.),(1.,0.92377447201052,1.),(1.,0.923983993203425,1.),(1.,0.86257487372095,
1.),(1.,0.796615278835181,1.)))
REPRESENTATION_ITEM('')
SURFACE()
);
#3925=(
BOUNDED_SURFACE()
B_SPLINE_SURFACE(3,2,((#444357,#444358,#444359),(#444360,#444361,#444362),
(#444363,#444364,#444365),(#444366,#444367,#444368)),.UNSPECIFIED.,.F.,
 .F.,.F.)
B_SPLINE_SURFACE_WITH_KNOTS((4,4),(3,3),(0.,0.000101244905251112),(0.,1.),
 .UNSPECIFIED.)
GEOMETRIC_REPRESENTATION_ITEM()
RATIONAL_B_SPLINE_SURFACE(((1.,0.79661527883517,1.),(1.,0.795896146109792,
1.),(1.,0.7951935657965,1.),(1.,0.794506502889901,1.)))
REPRESENTATION_ITEM('')
SURFACE()
);
#3926=(
BOUNDED_SURFACE()
B_SPLINE_SURFACE(3,2,((#444404,#444405,#444406),(#444407,#444408,#444409),
(#444410,#444411,#444412),(#444413,#444414,#444415)),.UNSPECIFIED.,.F.,
 .F.,.F.)
B_SPLINE_SURFACE_WITH_KNOTS((4,4),(3,3),(2.85968127239938E-5,9.24681548475814E-5),
(-0.00167900678701706,1.0113082712782),.UNSPECIFIED.)
GEOMETRIC_REPRESENTATION_ITEM()
RATIONAL_B_SPLINE_SURFACE(((1.00059040895233,0.82218754186819,1.00401468696656),
(1.0003652771815,0.889990093671522,1.00248382673391),(1.00016469515018,
0.950399042257911,1.00111990082511),(1.00025604274,0.922888044286047,1.00174104990631)))
REPRESENTATION_ITEM('')
SURFACE()
);
#3927=(
BOUNDED_SURFACE()
B_SPLINE_SURFACE(3,2,((#444419,#444420,#444421),(#444422,#444423,#444424),
(#444425,#444426,#444427),(#444428,#444429,#444430)),.UNSPECIFIED.,.F.,
 .F.,.F.)
B_SPLINE_SURFACE_WITH_KNOTS((4,4),(3,3),(-5.2235835674934E-6,5.74594192424275E-5),
(-0.00127120052040424,1.),.UNSPECIFIED.)
GEOMETRIC_REPRESENTATION_ITEM()
RATIONAL_B_SPLINE_SURFACE(((1.00054449313169,0.785835073638797,1.),(1.00047707767469,
0.812351526358888,1.),(1.00044031788581,0.826810216506311,1.),(1.00044777653313,
0.823876514387279,1.)))
REPRESENTATION_ITEM('')
SURFACE()
);
#3928=(
BOUNDED_SURFACE()
B_SPLINE_SURFACE(3,2,((#444432,#444433,#444434),(#444435,#444436,#444437),
(#444438,#444439,#444440),(#444441,#444442,#444443)),.UNSPECIFIED.,.F.,
 .F.,.F.)
B_SPLINE_SURFACE_WITH_KNOTS((4,4),(3,3),(-2.71050543121376E-19,4.88747512969877E-5),
(-0.000215805216116114,1.),.UNSPECIFIED.)
GEOMETRIC_REPRESENTATION_ITEM()
RATIONAL_B_SPLINE_SURFACE(((1.00008915600364,0.793434085499616,1.),(1.00008930225017,
0.793095246303171,1.),(1.00008944684639,0.792760230720422,1.),(1.00008958984419,
0.792428918540464,1.)))
REPRESENTATION_ITEM('')
SURFACE()
);
#3929=(
BOUNDED_SURFACE()
B_SPLINE_SURFACE(3,2,((#444445,#444446,#444447),(#444448,#444449,#444450),
(#444451,#444452,#444453),(#444454,#444455,#444456),(#444457,#444458,#444459),
(#444460,#444461,#444462)),.UNSPECIFIED.,.F.,.F.,.F.)
B_SPLINE_SURFACE_WITH_KNOTS((4,2,4),(3,3),(3.93023287525995E-19,7.626750108632E-5,
0.00015253500217264),(0.,1.02152348203056),.UNSPECIFIED.)
GEOMETRIC_REPRESENTATION_ITEM()
RATIONAL_B_SPLINE_SURFACE(((1.,0.789033595401277,1.00908146323686),(1.,
0.857071781054839,1.00615262590425),(1.,0.922087264710758,1.0033539067159),
(1.,0.92239446650236,1.00334068261142),(1.,0.857224384599083,1.00614605678497),
(1.,0.789033595401673,1.00908146323685)))
REPRESENTATION_ITEM('')
SURFACE()
);
#3930=(
BOUNDED_SURFACE()
B_SPLINE_SURFACE(3,2,((#444464,#444465,#444466),(#444467,#444468,#444469),
(#444470,#444471,#444472),(#444473,#444474,#444475)),.UNSPECIFIED.,.F.,
 .F.,.F.)
B_SPLINE_SURFACE_WITH_KNOTS((4,4),(3,3),(2.16840434497101E-19,4.88747512969882E-5),
(-0.000215489857183668,1.),.UNSPECIFIED.)
GEOMETRIC_REPRESENTATION_ITEM()
RATIONAL_B_SPLINE_SURFACE(((1.00008945889719,0.792428983985715,1.),(1.00008931610841,
0.792760296061256,1.),(1.00008917172353,0.793095311538336,1.),(1.00008902569076,
0.793434150627967,1.)))
REPRESENTATION_ITEM('')
SURFACE()
);
#3931=(
BOUNDED_SURFACE()
B_SPLINE_SURFACE(3,2,((#444477,#444478,#444479),(#444480,#444481,#444482),
(#444483,#444484,#444485),(#444486,#444487,#444488)),.UNSPECIFIED.,.F.,
 .F.,.F.)
B_SPLINE_SURFACE_WITH_KNOTS((4,4),(3,3),(-5.2197490501309E-6,5.74172395514396E-5),
(-0.00139822857793751,1.0005131236405),.UNSPECIFIED.)
GEOMETRIC_REPRESENTATION_ITEM()
RATIONAL_B_SPLINE_SURFACE(((1.00049256947264,0.823768952243972,1.00018060397843),
(1.00048448215734,0.826662424388268,1.00017763870876),(1.00052427784043,
0.812424361909329,1.00019223006915),(1.00059912365879,0.785646094632703,
1.00021967280224)))
REPRESENTATION_ITEM('')
SURFACE()
);
#3932=(
BOUNDED_SURFACE()
B_SPLINE_SURFACE(3,2,((#444492,#444493,#444494),(#444495,#444496,#444497),
(#444498,#444499,#444500),(#444501,#444502,#444503)),.UNSPECIFIED.,.F.,
 .F.,.F.)
B_SPLINE_SURFACE_WITH_KNOTS((4,4),(3,3),(3.2298077433778E-5,9.63764854872254E-5),
(-0.00154325936349561,1.01095292447536),.UNSPECIFIED.)
GEOMETRIC_REPRESENTATION_ITEM()
RATIONAL_B_SPLINE_SURFACE(((1.00023530983295,0.922925743796188,1.0016857472833),
(1.00015136166123,0.950422439594238,1.00108434699059),(1.00033574337393,
0.890029368953987,1.00240524789546),(1.00054260094213,0.822274473168394,
1.00388716464855)))
REPRESENTATION_ITEM('')
SURFACE()
);
#3933=(
BOUNDED_SURFACE()
B_SPLINE_SURFACE(3,2,((#444603,#444604,#444605),(#444606,#444607,#444608),
(#444609,#444610,#444611),(#444612,#444613,#444614)),.UNSPECIFIED.,.F.,
 .F.,.F.)
B_SPLINE_SURFACE_WITH_KNOTS((4,4),(3,3),(0.,0.000101260117256737),(0.,1.),
 .UNSPECIFIED.)
GEOMETRIC_REPRESENTATION_ITEM()
RATIONAL_B_SPLINE_SURFACE(((1.,0.796615278835171,1.),(1.,0.795896038055939,
1.),(1.,0.795193354661347,1.),(1.,0.794506193185534,1.)))
REPRESENTATION_ITEM('')
SURFACE()
);
#3934=(
BOUNDED_SURFACE()
B_SPLINE_SURFACE(3,2,((#444652,#444653,#444654),(#444655,#444656,#444657),
(#444658,#444659,#444660),(#444661,#444662,#444663),(#444664,#444665,#444666),
(#444667,#444668,#444669)),.UNSPECIFIED.,.F.,.F.,.F.)
B_SPLINE_SURFACE_WITH_KNOTS((4,2,4),(3,3),(2.3039296165317E-19,1.66936432462298E-5,
3.33872864924594E-5),(0.,1.),.UNSPECIFIED.)
GEOMETRIC_REPRESENTATION_ITEM()
RATIONAL_B_SPLINE_SURFACE(((1.,0.796615278835177,1.),(1.,0.862310524418133,
1.),(1.,0.923774472010522,1.),(1.,0.923983993203425,1.),(1.,0.862574873720947,
1.),(1.,0.796615278835184,1.)))
REPRESENTATION_ITEM('')
SURFACE()
);
#3935=(
BOUNDED_SURFACE()
B_SPLINE_SURFACE(3,2,((#444706,#444707,#444708),(#444709,#444710,#444711),
(#444712,#444713,#444714),(#444715,#444716,#444717)),.UNSPECIFIED.,.F.,
 .F.,.F.)
B_SPLINE_SURFACE_WITH_KNOTS((4,4),(3,3),(-2.16840434497101E-19,0.000101244905251112),
(0.,1.),.UNSPECIFIED.)
GEOMETRIC_REPRESENTATION_ITEM()
RATIONAL_B_SPLINE_SURFACE(((1.,0.796615278835171,1.),(1.,0.795896146109795,
1.),(1.,0.795193565796498,1.),(1.,0.794506502889903,1.)))
REPRESENTATION_ITEM('')
SURFACE()
);
#3936=(
BOUNDED_SURFACE()
B_SPLINE_SURFACE(3,2,((#444753,#444754,#444755),(#444756,#444757,#444758),
(#444759,#444760,#444761),(#444762,#444763,#444764)),.UNSPECIFIED.,.F.,
 .F.,.F.)
B_SPLINE_SURFACE_WITH_KNOTS((4,4),(3,3),(2.85968127239939E-5,9.24681548475817E-5),
(-0.00167900678690871,1.01130827127831),.UNSPECIFIED.)
GEOMETRIC_REPRESENTATION_ITEM()
RATIONAL_B_SPLINE_SURFACE(((1.0005904089523,0.822187541868189,1.0040146869666),
(1.00036527718148,0.889990093671519,1.00248382673393),(1.00016469515017,
0.950399042257909,1.00111990082512),(1.00025604273998,0.922888044286045,
1.00174104990632)))
REPRESENTATION_ITEM('')
SURFACE()
);
#3937=(
BOUNDED_SURFACE()
B_SPLINE_SURFACE(3,2,((#444768,#444769,#444770),(#444771,#444772,#444773),
(#444774,#444775,#444776),(#444777,#444778,#444779)),.UNSPECIFIED.,.F.,
 .F.,.F.)
B_SPLINE_SURFACE_WITH_KNOTS((4,4),(3,3),(-5.22358356749282E-6,5.74594192424277E-5),
(-0.00127120052078626,1.),.UNSPECIFIED.)
GEOMETRIC_REPRESENTATION_ITEM()
RATIONAL_B_SPLINE_SURFACE(((1.00054449313185,0.785835073638714,1.),(1.00047707767483,
0.812351526358813,1.),(1.00044031788594,0.826810216506242,1.),(1.00044777653327,
0.823876514387215,1.)))
REPRESENTATION_ITEM('')
SURFACE()
);
#3938=(
BOUNDED_SURFACE()
B_SPLINE_SURFACE(3,2,((#444781,#444782,#444783),(#444784,#444785,#444786),
(#444787,#444788,#444789),(#444790,#444791,#444792)),.UNSPECIFIED.,.F.,
 .F.,.F.)
B_SPLINE_SURFACE_WITH_KNOTS((4,4),(3,3),(-2.71050543121376E-19,4.88747512969883E-5),
(-0.000215805215133611,1.),.UNSPECIFIED.)
GEOMETRIC_REPRESENTATION_ITEM()
RATIONAL_B_SPLINE_SURFACE(((1.00008915600324,0.793434085499815,1.),(1.00008930224977,
0.793095246303358,1.),(1.00008944684599,0.792760230720632,1.),(1.00008958984378,
0.792428918540665,1.)))
REPRESENTATION_ITEM('')
SURFACE()
);
#3939=(
BOUNDED_SURFACE()
B_SPLINE_SURFACE(3,2,((#444794,#444795,#444796),(#444797,#444798,#444799),
(#444800,#444801,#444802),(#444803,#444804,#444805),(#444806,#444807,#444808),
(#444809,#444810,#444811)),.UNSPECIFIED.,.F.,.F.,.F.)
B_SPLINE_SURFACE_WITH_KNOTS((4,2,4),(3,3),(2.03287907341032E-19,7.62675010863199E-5,
0.00015253500217264),(0.,1.02152348203091),.UNSPECIFIED.)
GEOMETRIC_REPRESENTATION_ITEM()
RATIONAL_B_SPLINE_SURFACE(((1.,0.789033595401203,1.00908146323702),(1.,
0.857071781054809,1.00615262590435),(1.,0.922087264710707,1.00335390671596),
(1.,0.922394466502357,1.00334068261147),(1.,0.857224384599022,1.00614605678507),
(1.,0.789033595401601,1.009081463237)))
REPRESENTATION_ITEM('')
SURFACE()
);
#3940=(
BOUNDED_SURFACE()
B_SPLINE_SURFACE(3,2,((#444813,#444814,#444815),(#444816,#444817,#444818),
(#444819,#444820,#444821),(#444822,#444823,#444824)),.UNSPECIFIED.,.F.,
 .F.,.F.)
B_SPLINE_SURFACE_WITH_KNOTS((4,4),(3,3),(1.35525271560688E-19,4.88747512969882E-5),
(-0.000215489856921436,1.),.UNSPECIFIED.)
GEOMETRIC_REPRESENTATION_ITEM()
RATIONAL_B_SPLINE_SURFACE(((1.00008945889708,0.792428983985769,1.),(1.0000893161083,
0.792760296061308,1.),(1.00008917172343,0.793095311538394,1.),(1.00008902569065,
0.79343415062802,1.)))
REPRESENTATION_ITEM('')
SURFACE()
);
#3941=(
BOUNDED_SURFACE()
B_SPLINE_SURFACE(3,2,((#444826,#444827,#444828),(#444829,#444830,#444831),
(#444832,#444833,#444834),(#444835,#444836,#444837)),.UNSPECIFIED.,.F.,
 .F.,.F.)
B_SPLINE_SURFACE_WITH_KNOTS((4,4),(3,3),(-5.21974905012869E-6,5.74172395514383E-5),
(-0.0013982285776812,1.00051312364052),.UNSPECIFIED.)
GEOMETRIC_REPRESENTATION_ITEM()
RATIONAL_B_SPLINE_SURFACE(((1.00049256947255,0.823768952244018,1.00018060397844),
(1.00048448215725,0.826662424388302,1.00017763870877),(1.00052427784033,
0.812424361909381,1.00019223006916),(1.00059912365868,0.78564609463275,
1.00021967280225)))
REPRESENTATION_ITEM('')
SURFACE()
);
#3942=(
BOUNDED_SURFACE()
B_SPLINE_SURFACE(3,2,((#444841,#444842,#444843),(#444844,#444845,#444846),
(#444847,#444848,#444849),(#444850,#444851,#444852)),.UNSPECIFIED.,.F.,
 .F.,.F.)
B_SPLINE_SURFACE_WITH_KNOTS((4,4),(3,3),(3.22980774337779E-5,9.63764854872253E-5),
(-0.00154325936290737,1.01095292447553),.UNSPECIFIED.)
GEOMETRIC_REPRESENTATION_ITEM()
RATIONAL_B_SPLINE_SURFACE(((1.00023530983286,0.92292574379622,1.00168574728332),
(1.00015136166117,0.950422439594252,1.00108434699061),(1.0003357433738,
0.890029368954036,1.0024052478955),(1.00054260094192,0.822274473168471,
1.00388716464861)))
REPRESENTATION_ITEM('')
SURFACE()
);
#3943=(
BOUNDED_SURFACE()
B_SPLINE_SURFACE(3,2,((#444952,#444953,#444954),(#444955,#444956,#444957),
(#444958,#444959,#444960),(#444961,#444962,#444963)),.UNSPECIFIED.,.F.,
 .F.,.F.)
B_SPLINE_SURFACE_WITH_KNOTS((4,4),(3,3),(0.,0.000101260117256737),(0.,1.),
 .UNSPECIFIED.)
GEOMETRIC_REPRESENTATION_ITEM()
RATIONAL_B_SPLINE_SURFACE(((1.,0.796615278835171,1.),(1.,0.79589603805594,
1.),(1.,0.795193354661346,1.),(1.,0.794506193185533,1.)))
REPRESENTATION_ITEM('')
SURFACE()
);
#3944=(
BOUNDED_SURFACE()
B_SPLINE_SURFACE(3,2,((#445001,#445002,#445003),(#445004,#445005,#445006),
(#445007,#445008,#445009),(#445010,#445011,#445012),(#445013,#445014,#445015),
(#445016,#445017,#445018)),.UNSPECIFIED.,.F.,.F.,.F.)
B_SPLINE_SURFACE_WITH_KNOTS((4,2,4),(3,3),(-2.11758236813575E-19,1.66936432462294E-5,
3.3387286492459E-5),(0.,1.),.UNSPECIFIED.)
GEOMETRIC_REPRESENTATION_ITEM()
RATIONAL_B_SPLINE_SURFACE(((1.,0.796615278835173,1.),(1.,0.862310524418121,
1.),(1.,0.923774472010524,1.),(1.,0.923983993203421,1.),(1.,0.862574873720939,
1.),(1.,0.796615278835189,1.)))
REPRESENTATION_ITEM('')
SURFACE()
);
#3945=(
BOUNDED_SURFACE()
B_SPLINE_SURFACE(3,2,((#445055,#445056,#445057),(#445058,#445059,#445060),
(#445061,#445062,#445063),(#445064,#445065,#445066)),.UNSPECIFIED.,.F.,
 .F.,.F.)
B_SPLINE_SURFACE_WITH_KNOTS((4,4),(3,3),(0.,0.000101244905251112),(0.,1.),
 .UNSPECIFIED.)
GEOMETRIC_REPRESENTATION_ITEM()
RATIONAL_B_SPLINE_SURFACE(((1.,0.796615278835172,1.),(1.,0.795896146109794,
1.),(1.,0.795193565796497,1.),(1.,0.7945065028899,1.)))
REPRESENTATION_ITEM('')
SURFACE()
);
#3946=(
BOUNDED_SURFACE()
B_SPLINE_SURFACE(3,2,((#445102,#445103,#445104),(#445105,#445106,#445107),
(#445108,#445109,#445110),(#445111,#445112,#445113)),.UNSPECIFIED.,.F.,
 .F.,.F.)
B_SPLINE_SURFACE_WITH_KNOTS((4,4),(3,3),(2.85968127239939E-5,9.24681548475818E-5),
(-0.00167900678679091,1.01130827127834),.UNSPECIFIED.)
GEOMETRIC_REPRESENTATION_ITEM()
RATIONAL_B_SPLINE_SURFACE(((1.00059040895225,0.822187541868203,1.00401468696661),
(1.00036527718145,0.889990093671535,1.00248382673394),(1.00016469515015,
0.950399042257911,1.00111990082512),(1.00025604273996,0.922888044286052,
1.00174104990633)))
REPRESENTATION_ITEM('')
SURFACE()
);
#3947=(
BOUNDED_SURFACE()
B_SPLINE_SURFACE(3,2,((#445117,#445118,#445119),(#445120,#445121,#445122),
(#445123,#445124,#445125),(#445126,#445127,#445128)),.UNSPECIFIED.,.F.,
 .F.,.F.)
B_SPLINE_SURFACE_WITH_KNOTS((4,4),(3,3),(-5.22358356749289E-6,5.74594192424278E-5),
(-0.00127120052035666,1.),.UNSPECIFIED.)
GEOMETRIC_REPRESENTATION_ITEM()
RATIONAL_B_SPLINE_SURFACE(((1.00054449313166,0.785835073638806,1.),(1.00047707767467,
0.812351526358888,1.),(1.0004403178858,0.826810216506318,1.),(1.00044777653312,
0.823876514387286,1.)))
REPRESENTATION_ITEM('')
SURFACE()
);
#3948=(
BOUNDED_SURFACE()
B_SPLINE_SURFACE(3,2,((#445130,#445131,#445132),(#445133,#445134,#445135),
(#445136,#445137,#445138),(#445139,#445140,#445141)),.UNSPECIFIED.,.F.,
 .F.,.F.)
B_SPLINE_SURFACE_WITH_KNOTS((4,4),(3,3),(-1.0842021724855E-19,4.8874751296988E-5),
(-0.000215805215040772,1.),.UNSPECIFIED.)
GEOMETRIC_REPRESENTATION_ITEM()
RATIONAL_B_SPLINE_SURFACE(((1.0000891560032,0.793434085499837,1.),(1.00008930224973,
0.793095246303369,1.),(1.00008944684595,0.792760230720652,1.),(1.00008958984374,
0.792428918540683,1.)))
REPRESENTATION_ITEM('')
SURFACE()
);
#3949=(
BOUNDED_SURFACE()
B_SPLINE_SURFACE(3,2,((#445143,#445144,#445145),(#445146,#445147,#445148),
(#445149,#445150,#445151),(#445152,#445153,#445154),(#445155,#445156,#445157),
(#445158,#445159,#445160)),.UNSPECIFIED.,.F.,.F.,.F.)
B_SPLINE_SURFACE_WITH_KNOTS((4,2,4),(3,3),(6.7762635780344E-20,7.62675010863195E-5,
0.000152535002172639),(0.,1.0215234820307),.UNSPECIFIED.)
GEOMETRIC_REPRESENTATION_ITEM()
RATIONAL_B_SPLINE_SURFACE(((1.,0.789033595401244,1.00908146323692),(1.,
0.85707178105484,1.00615262590429),(1.,0.922087264710726,1.00335390671592),
(1.,0.922394466502372,1.00334068261144),(1.,0.857224384599049,1.00614605678501),
(1.,0.789033595401646,1.00908146323691)))
REPRESENTATION_ITEM('')
SURFACE()
);
#3950=(
BOUNDED_SURFACE()
B_SPLINE_SURFACE(3,2,((#445162,#445163,#445164),(#445165,#445166,#445167),
(#445168,#445169,#445170),(#445171,#445172,#445173)),.UNSPECIFIED.,.F.,
 .F.,.F.)
B_SPLINE_SURFACE_WITH_KNOTS((4,4),(3,3),(2.16840434497101E-19,4.8874751296988E-5),
(-0.000215489856918745,1.),.UNSPECIFIED.)
GEOMETRIC_REPRESENTATION_ITEM()
RATIONAL_B_SPLINE_SURFACE(((1.00008945889708,0.79242898398577,1.),(1.0000893161083,
0.792760296061318,1.),(1.00008917172342,0.793095311538385,1.),(1.00008902569065,
0.793434150628019,1.)))
REPRESENTATION_ITEM('')
SURFACE()
);
#3951=(
BOUNDED_SURFACE()
B_SPLINE_SURFACE(3,2,((#445175,#445176,#445177),(#445178,#445179,#445180),
(#445181,#445182,#445183),(#445184,#445185,#445186)),.UNSPECIFIED.,.F.,
 .F.,.F.)
B_SPLINE_SURFACE_WITH_KNOTS((4,4),(3,3),(-5.21974905013088E-6,5.7417239551438E-5),
(-0.00139822857722359,1.00051312364048),.UNSPECIFIED.)
GEOMETRIC_REPRESENTATION_ITEM()
RATIONAL_B_SPLINE_SURFACE(((1.00049256947238,0.823768952244102,1.00018060397842),
(1.00048448215709,0.826662424388395,1.00017763870876),(1.00052427784016,
0.812424361909474,1.00019223006914),(1.00059912365849,0.78564609463286,
1.00021967280223)))
REPRESENTATION_ITEM('')
SURFACE()
);
#3952=(
BOUNDED_SURFACE()
B_SPLINE_SURFACE(3,2,((#445190,#445191,#445192),(#445193,#445194,#445195),
(#445196,#445197,#445198),(#445199,#445200,#445201)),.UNSPECIFIED.,.F.,
 .F.,.F.)
B_SPLINE_SURFACE_WITH_KNOTS((4,4),(3,3),(3.2298077433778E-5,9.63764854872249E-5),
(-0.00154325936386665,1.01095292447556),.UNSPECIFIED.)
GEOMETRIC_REPRESENTATION_ITEM()
RATIONAL_B_SPLINE_SURFACE(((1.00023530983301,0.922925743796142,1.00168574728333),
(1.00015136166127,0.95042243959421,1.00108434699061),(1.00033574337401,
0.890029368953932,1.0024052478955),(1.00054260094226,0.822274473168286,
1.00388716464863)))
REPRESENTATION_ITEM('')
SURFACE()
);
#3953=(
BOUNDED_SURFACE()
B_SPLINE_SURFACE(3,2,((#445301,#445302,#445303),(#445304,#445305,#445306),
(#445307,#445308,#445309),(#445310,#445311,#445312)),.UNSPECIFIED.,.F.,
 .F.,.F.)
B_SPLINE_SURFACE_WITH_KNOTS((4,4),(3,3),(-4.33680868994202E-19,0.000101260117256737),
(0.,1.),.UNSPECIFIED.)
GEOMETRIC_REPRESENTATION_ITEM()
RATIONAL_B_SPLINE_SURFACE(((1.,0.796615278835171,1.),(1.,0.795896038055937,
1.),(1.,0.795193354661347,1.),(1.,0.794506193185543,1.)))
REPRESENTATION_ITEM('')
SURFACE()
);
#3954=(
BOUNDED_SURFACE()
B_SPLINE_SURFACE(3,2,((#445350,#445351,#445352),(#445353,#445354,#445355),
(#445356,#445357,#445358),(#445359,#445360,#445361),(#445362,#445363,#445364),
(#445365,#445366,#445367)),.UNSPECIFIED.,.F.,.F.,.F.)
B_SPLINE_SURFACE_WITH_KNOTS((4,2,4),(3,3),(1.35525271560688E-20,1.66936432462295E-5,
3.33872864924589E-5),(0.,1.),.UNSPECIFIED.)
GEOMETRIC_REPRESENTATION_ITEM()
RATIONAL_B_SPLINE_SURFACE(((1.,0.796615278835177,1.),(1.,0.862310524418129,
1.),(1.,0.92377447201052,1.),(1.,0.923983993203425,1.),(1.,0.862574873720951,
1.),(1.,0.796615278835181,1.)))
REPRESENTATION_ITEM('')
SURFACE()
);
#3955=(
BOUNDED_SURFACE()
B_SPLINE_SURFACE(3,2,((#445404,#445405,#445406),(#445407,#445408,#445409),
(#445410,#445411,#445412),(#445413,#445414,#445415)),.UNSPECIFIED.,.F.,
 .F.,.F.)
B_SPLINE_SURFACE_WITH_KNOTS((4,4),(3,3),(-2.16840434497101E-19,0.000101244905251112),
(0.,1.),.UNSPECIFIED.)
GEOMETRIC_REPRESENTATION_ITEM()
RATIONAL_B_SPLINE_SURFACE(((1.,0.796615278835172,1.),(1.,0.795896146109783,
1.),(1.,0.795193565796517,1.),(1.,0.794506502889896,1.)))
REPRESENTATION_ITEM('')
SURFACE()
);
#3956=(
BOUNDED_SURFACE()
B_SPLINE_SURFACE(3,2,((#445451,#445452,#445453),(#445454,#445455,#445456),
(#445457,#445458,#445459),(#445460,#445461,#445462)),.UNSPECIFIED.,.F.,
 .F.,.F.)
B_SPLINE_SURFACE_WITH_KNOTS((4,4),(3,3),(2.85968127239939E-5,9.24681548475817E-5),
(-0.00167900678782723,1.01130827127812),.UNSPECIFIED.)
GEOMETRIC_REPRESENTATION_ITEM()
RATIONAL_B_SPLINE_SURFACE(((1.00059040895262,0.822187541868066,1.00401468696653),
(1.00036527718168,0.88999009367143,1.00248382673389),(1.00016469515026,
0.950399042257876,1.0011199008251),(1.00025604274012,0.922888044285988,
1.0017410499063)))
REPRESENTATION_ITEM('')
SURFACE()
);
#3957=(
BOUNDED_SURFACE()
B_SPLINE_SURFACE(3,2,((#445466,#445467,#445468),(#445469,#445470,#445471),
(#445472,#445473,#445474),(#445475,#445476,#445477)),.UNSPECIFIED.,.F.,
 .F.,.F.)
B_SPLINE_SURFACE_WITH_KNOTS((4,4),(3,3),(-5.22358356749287E-6,5.74594192424278E-5),
(-0.00127120052040456,1.),.UNSPECIFIED.)
GEOMETRIC_REPRESENTATION_ITEM()
RATIONAL_B_SPLINE_SURFACE(((1.00054449313169,0.785835073638795,1.),(1.00047707767469,
0.812351526358882,1.),(1.00044031788581,0.826810216506303,1.),(1.00044777653313,
0.823876514387282,1.)))
REPRESENTATION_ITEM('')
SURFACE()
);
#3958=(
BOUNDED_SURFACE()
B_SPLINE_SURFACE(3,2,((#445479,#445480,#445481),(#445482,#445483,#445484),
(#445485,#445486,#445487),(#445488,#445489,#445490)),.UNSPECIFIED.,.F.,
 .F.,.F.)
B_SPLINE_SURFACE_WITH_KNOTS((4,4),(3,3),(-4.06575814682064E-19,4.88747512969879E-5),
(-0.000215805216148118,1.),.UNSPECIFIED.)
GEOMETRIC_REPRESENTATION_ITEM()
RATIONAL_B_SPLINE_SURFACE(((1.00008915600365,0.793434085499607,1.),(1.00008930225019,
0.793095246303155,1.),(1.00008944684641,0.792760230720426,1.),(1.0000895898442,
0.792428918540454,1.)))
REPRESENTATION_ITEM('')
SURFACE()
);
#3959=(
BOUNDED_SURFACE()
B_SPLINE_SURFACE(3,2,((#445492,#445493,#445494),(#445495,#445496,#445497),
(#445498,#445499,#445500),(#445501,#445502,#445503),(#445504,#445505,#445506),
(#445507,#445508,#445509)),.UNSPECIFIED.,.F.,.F.,.F.)
B_SPLINE_SURFACE_WITH_KNOTS((4,2,4),(3,3),(4.94667241196511E-19,7.626750108632E-5,
0.000152535002172639),(0.,1.0215234820307),.UNSPECIFIED.)
GEOMETRIC_REPRESENTATION_ITEM()
RATIONAL_B_SPLINE_SURFACE(((1.,0.789033595401248,1.00908146323693),(1.,
0.857071781054843,1.00615262590429),(1.,0.922087264710718,1.00335390671592),
(1.,0.922394466502379,1.00334068261144),(1.,0.857224384599044,1.00614605678501),
(1.,0.789033595401645,1.00908146323691)))
REPRESENTATION_ITEM('')
SURFACE()
);
#3960=(
BOUNDED_SURFACE()
B_SPLINE_SURFACE(3,2,((#445511,#445512,#445513),(#445514,#445515,#445516),
(#445517,#445518,#445519),(#445520,#445521,#445522)),.UNSPECIFIED.,.F.,
 .F.,.F.)
B_SPLINE_SURFACE_WITH_KNOTS((4,4),(3,3),(3.52365706057789E-19,4.88747512969884E-5),
(-0.000215489857968907,1.),.UNSPECIFIED.)
GEOMETRIC_REPRESENTATION_ITEM()
RATIONAL_B_SPLINE_SURFACE(((1.00008945889752,0.792428983985552,1.),(1.00008931610873,
0.792760296061093,1.),(1.00008917172386,0.793095311538178,1.),(1.00008902569108,
0.793434150627804,1.)))
REPRESENTATION_ITEM('')
SURFACE()
);
#3961=(
BOUNDED_SURFACE()
B_SPLINE_SURFACE(3,2,((#445524,#445525,#445526),(#445527,#445528,#445529),
(#445530,#445531,#445532),(#445533,#445534,#445535)),.UNSPECIFIED.,.F.,
 .F.,.F.)
B_SPLINE_SURFACE_WITH_KNOTS((4,4),(3,3),(-5.21974905012869E-6,5.74172395514398E-5),
(-0.00139822857721556,1.00051312364053),.UNSPECIFIED.)
GEOMETRIC_REPRESENTATION_ITEM()
RATIONAL_B_SPLINE_SURFACE(((1.00049256947238,0.823768952244095,1.00018060397845),
(1.00048448215709,0.826662424388383,1.00017763870878),(1.00052427784016,
0.812424361909465,1.00019223006916),(1.00059912365848,0.785646094632845,
1.00021967280225)))
REPRESENTATION_ITEM('')
SURFACE()
);
#3962=(
BOUNDED_SURFACE()
B_SPLINE_SURFACE(3,2,((#445539,#445540,#445541),(#445542,#445543,#445544),
(#445545,#445546,#445547),(#445548,#445549,#445550)),.UNSPECIFIED.,.F.,
 .F.,.F.)
B_SPLINE_SURFACE_WITH_KNOTS((4,4),(3,3),(3.22980774337778E-5,9.63764854872256E-5),
(-0.0015432593639103,1.01095292447531),.UNSPECIFIED.)
GEOMETRIC_REPRESENTATION_ITEM()
RATIONAL_B_SPLINE_SURFACE(((1.00023530983302,0.922925743796159,1.00168574728329),
(1.00015136166127,0.950422439594222,1.00108434699058),(1.00033574337402,
0.890029368953943,1.00240524789545),(1.00054260094228,0.822274473168331,
1.00388716464854)))
REPRESENTATION_ITEM('')
SURFACE()
);
#3963=(
BOUNDED_SURFACE()
B_SPLINE_SURFACE(3,2,((#445650,#445651,#445652),(#445653,#445654,#445655),
(#445656,#445657,#445658),(#445659,#445660,#445661)),.UNSPECIFIED.,.F.,
 .F.,.F.)
B_SPLINE_SURFACE_WITH_KNOTS((4,4),(3,3),(-4.33680868994202E-19,0.000101260117256737),
(0.,1.),.UNSPECIFIED.)
GEOMETRIC_REPRESENTATION_ITEM()
RATIONAL_B_SPLINE_SURFACE(((1.,0.796615278835173,1.),(1.,0.795896038055939,
1.),(1.,0.79519335466135,1.),(1.,0.794506193185544,1.)))
REPRESENTATION_ITEM('')
SURFACE()
);
#3964=(
BOUNDED_SURFACE()
B_SPLINE_SURFACE(3,2,((#445699,#445700,#445701),(#445702,#445703,#445704),
(#445705,#445706,#445707),(#445708,#445709,#445710),(#445711,#445712,#445713),
(#445714,#445715,#445716)),.UNSPECIFIED.,.F.,.F.,.F.)
B_SPLINE_SURFACE_WITH_KNOTS((4,2,4),(3,3),(5.75982404132924E-20,1.66936432462296E-5,
3.33872864924592E-5),(0.,1.),.UNSPECIFIED.)
GEOMETRIC_REPRESENTATION_ITEM()
RATIONAL_B_SPLINE_SURFACE(((1.,0.796615278835172,1.),(1.,0.862310524418126,
1.),(1.,0.923774472010521,1.),(1.,0.923983993203426,1.),(1.,0.862574873720941,
1.),(1.,0.796615278835176,1.)))
REPRESENTATION_ITEM('')
SURFACE()
);
#3965=(
BOUNDED_SURFACE()
B_SPLINE_SURFACE(3,2,((#445753,#445754,#445755),(#445756,#445757,#445758),
(#445759,#445760,#445761),(#445762,#445763,#445764)),.UNSPECIFIED.,.F.,
 .F.,.F.)
B_SPLINE_SURFACE_WITH_KNOTS((4,4),(3,3),(0.,0.000101244905251112),(0.,1.),
 .UNSPECIFIED.)
GEOMETRIC_REPRESENTATION_ITEM()
RATIONAL_B_SPLINE_SURFACE(((1.,0.796615278835172,1.),(1.,0.795896146109795,
1.),(1.,0.79519356579651,1.),(1.,0.794506502889903,1.)))
REPRESENTATION_ITEM('')
SURFACE()
);
#3966=(
BOUNDED_SURFACE()
B_SPLINE_SURFACE(3,2,((#445800,#445801,#445802),(#445803,#445804,#445805),
(#445806,#445807,#445808),(#445809,#445810,#445811)),.UNSPECIFIED.,.F.,
 .F.,.F.)
B_SPLINE_SURFACE_WITH_KNOTS((4,4),(3,3),(2.85968127239939E-5,9.24681548475815E-5),
(-0.00167900678670585,1.01130827127827),.UNSPECIFIED.)
GEOMETRIC_REPRESENTATION_ITEM()
RATIONAL_B_SPLINE_SURFACE(((1.00059040895222,0.822187541868234,1.00401468696658),
(1.00036527718143,0.889990093671548,1.00248382673392),(1.00016469515015,
0.950399042257928,1.00111990082511),(1.00025604273995,0.922888044286062,
1.00174104990632)))
REPRESENTATION_ITEM('')
SURFACE()
);
#3967=(
BOUNDED_SURFACE()
B_SPLINE_SURFACE(3,2,((#445815,#445816,#445817),(#445818,#445819,#445820),
(#445821,#445822,#445823),(#445824,#445825,#445826)),.UNSPECIFIED.,.F.,
 .F.,.F.)
B_SPLINE_SURFACE_WITH_KNOTS((4,4),(3,3),(-5.22358356749319E-6,5.74594192424276E-5),
(-0.00127120052051403,1.),.UNSPECIFIED.)
GEOMETRIC_REPRESENTATION_ITEM()
RATIONAL_B_SPLINE_SURFACE(((1.00054449313173,0.78583507363877,1.),(1.00047707767473,
0.812351526358864,1.),(1.00044031788585,0.82681021650629,1.),(1.00044777653317,
0.823876514387265,1.)))
REPRESENTATION_ITEM('')
SURFACE()
);
#3968=(
BOUNDED_SURFACE()
B_SPLINE_SURFACE(3,2,((#445828,#445829,#445830),(#445831,#445832,#445833),
(#445834,#445835,#445836),(#445837,#445838,#445839)),.UNSPECIFIED.,.F.,
 .F.,.F.)
B_SPLINE_SURFACE_WITH_KNOTS((4,4),(3,3),(2.71050543121376E-20,4.88747512969881E-5),
(-0.00021580521507922,1.),.UNSPECIFIED.)
GEOMETRIC_REPRESENTATION_ITEM()
RATIONAL_B_SPLINE_SURFACE(((1.00008915600321,0.793434085499829,1.),(1.00008930224974,
0.79309524630337,1.),(1.00008944684596,0.792760230720645,1.),(1.00008958984376,
0.792428918540678,1.)))
REPRESENTATION_ITEM('')
SURFACE()
);
#3969=(
BOUNDED_SURFACE()
B_SPLINE_SURFACE(3,2,((#445841,#445842,#445843),(#445844,#445845,#445846),
(#445847,#445848,#445849),(#445850,#445851,#445852),(#445853,#445854,#445855),
(#445856,#445857,#445858)),.UNSPECIFIED.,.F.,.F.,.F.)
B_SPLINE_SURFACE_WITH_KNOTS((4,2,4),(3,3),(-1.76182853028894E-19,7.62675010863195E-5,
0.000152535002172639),(0.,1.02152348203063),.UNSPECIFIED.)
GEOMETRIC_REPRESENTATION_ITEM()
RATIONAL_B_SPLINE_SURFACE(((1.,0.78903359540126,1.00908146323689),(1.,0.857071781054843,
1.00615262590427),(1.,0.922087264710726,1.00335390671591),(1.,0.922394466502384,
1.00334068261143),(1.,0.857224384599053,1.00614605678499),(1.,0.78903359540166,
1.00908146323688)))
REPRESENTATION_ITEM('')
SURFACE()
);
#3970=(
BOUNDED_SURFACE()
B_SPLINE_SURFACE(3,2,((#445860,#445861,#445862),(#445863,#445864,#445865),
(#445866,#445867,#445868),(#445869,#445870,#445871)),.UNSPECIFIED.,.F.,
 .F.,.F.)
B_SPLINE_SURFACE_WITH_KNOTS((4,4),(3,3),(6.23416249179165E-19,4.88747512969881E-5),
(-0.000215489857056772,1.),.UNSPECIFIED.)
GEOMETRIC_REPRESENTATION_ITEM()
RATIONAL_B_SPLINE_SURFACE(((1.00008945889714,0.792428983985737,1.),(1.00008931610836,
0.792760296061305,1.),(1.00008917172348,0.793095311538342,1.),(1.00008902569071,
0.793434150627993,1.)))
REPRESENTATION_ITEM('')
SURFACE()
);
#3971=(
BOUNDED_SURFACE()
B_SPLINE_SURFACE(3,2,((#445873,#445874,#445875),(#445876,#445877,#445878),
(#445879,#445880,#445881),(#445882,#445883,#445884)),.UNSPECIFIED.,.F.,
 .F.,.F.)
B_SPLINE_SURFACE_WITH_KNOTS((4,4),(3,3),(-5.21974905012868E-6,5.74172395514396E-5),
(-0.00139822857796667,1.00051312364096),.UNSPECIFIED.)
GEOMETRIC_REPRESENTATION_ITEM()
RATIONAL_B_SPLINE_SURFACE(((1.00049256947265,0.823768952243889,1.00018060397859),
(1.00048448215735,0.82666242438818,1.00017763870892),(1.00052427784044,
0.812424361909243,1.00019223006932),(1.0005991236588,0.785646094632596,
1.00021967280243)))
REPRESENTATION_ITEM('')
SURFACE()
);
#3972=(
BOUNDED_SURFACE()
B_SPLINE_SURFACE(3,2,((#445888,#445889,#445890),(#445891,#445892,#445893),
(#445894,#445895,#445896),(#445897,#445898,#445899)),.UNSPECIFIED.,.F.,
 .F.,.F.)
B_SPLINE_SURFACE_WITH_KNOTS((4,4),(3,3),(3.22980774337781E-5,9.63764854872251E-5),
(-0.00154325936385716,1.01095292447533),.UNSPECIFIED.)
GEOMETRIC_REPRESENTATION_ITEM()
RATIONAL_B_SPLINE_SURFACE(((1.00023530983301,0.922925743796162,1.00168574728329),
(1.00015136166127,0.950422439594222,1.00108434699059),(1.00033574337401,
0.890029368953952,1.00240524789545),(1.00054260094226,0.822274473168332,
1.00388716464854)))
REPRESENTATION_ITEM('')
SURFACE()
);
#3973=(
BOUNDED_SURFACE()
B_SPLINE_SURFACE(3,2,((#445999,#446000,#446001),(#446002,#446003,#446004),
(#446005,#446006,#446007),(#446008,#446009,#446010)),.UNSPECIFIED.,.F.,
 .F.,.F.)
B_SPLINE_SURFACE_WITH_KNOTS((4,4),(3,3),(0.,0.000101260117256738),(0.,1.),
 .UNSPECIFIED.)
GEOMETRIC_REPRESENTATION_ITEM()
RATIONAL_B_SPLINE_SURFACE(((1.,0.796615278835168,1.),(1.,0.795896038055949,
1.),(1.,0.795193354661346,1.),(1.,0.794506193185548,1.)))
REPRESENTATION_ITEM('')
SURFACE()
);
#3974=(
BOUNDED_SURFACE()
B_SPLINE_SURFACE(3,2,((#446048,#446049,#446050),(#446051,#446052,#446053),
(#446054,#446055,#446056),(#446057,#446058,#446059),(#446060,#446061,#446062),
(#446063,#446064,#446065)),.UNSPECIFIED.,.F.,.F.,.F.)
B_SPLINE_SURFACE_WITH_KNOTS((4,2,4),(3,3),(-2.4225142291473E-19,1.6693643246229E-5,
3.33872864924583E-5),(0.,1.),.UNSPECIFIED.)
GEOMETRIC_REPRESENTATION_ITEM()
RATIONAL_B_SPLINE_SURFACE(((1.,0.796615278835185,1.),(1.,0.862310524418132,
1.),(1.,0.92377447201052,1.),(1.,0.923983993203428,1.),(1.,0.862574873720944,
1.),(1.,0.796615278835193,1.)))
REPRESENTATION_ITEM('')
SURFACE()
);
#3975=(
BOUNDED_SURFACE()
B_SPLINE_SURFACE(3,2,((#446102,#446103,#446104),(#446105,#446106,#446107),
(#446108,#446109,#446110),(#446111,#446112,#446113)),.UNSPECIFIED.,.F.,
 .F.,.F.)
B_SPLINE_SURFACE_WITH_KNOTS((4,4),(3,3),(0.,0.000101244905251112),(0.,1.),
 .UNSPECIFIED.)
GEOMETRIC_REPRESENTATION_ITEM()
RATIONAL_B_SPLINE_SURFACE(((1.,0.796615278835176,1.),(1.,0.795896146109792,
1.),(1.,0.795193565796492,1.),(1.,0.794506502889906,1.)))
REPRESENTATION_ITEM('')
SURFACE()
);
#3976=(
BOUNDED_SURFACE()
B_SPLINE_SURFACE(3,2,((#446149,#446150,#446151),(#446152,#446153,#446154),
(#446155,#446156,#446157),(#446158,#446159,#446160)),.UNSPECIFIED.,.F.,
 .F.,.F.)
B_SPLINE_SURFACE_WITH_KNOTS((4,4),(3,3),(2.85968127239939E-5,9.24681548475817E-5),
(-0.00167900678634675,1.01130827127812),.UNSPECIFIED.)
GEOMETRIC_REPRESENTATION_ITEM()
RATIONAL_B_SPLINE_SURFACE(((1.0005904089521,0.822187541868325,1.00401468696653),
(1.00036527718135,0.889990093671606,1.00248382673389),(1.00016469515011,
0.950399042257947,1.0011199008251),(1.00025604273989,0.922888044286103,
1.0017410499063)))
REPRESENTATION_ITEM('')
SURFACE()
);
#3977=(
BOUNDED_SURFACE()
B_SPLINE_SURFACE(3,2,((#446164,#446165,#446166),(#446167,#446168,#446169),
(#446170,#446171,#446172),(#446173,#446174,#446175)),.UNSPECIFIED.,.F.,
 .F.,.F.)
B_SPLINE_SURFACE_WITH_KNOTS((4,4),(3,3),(-5.22358356749342E-6,5.74594192424275E-5),
(-0.00127120052036188,1.),.UNSPECIFIED.)
GEOMETRIC_REPRESENTATION_ITEM()
RATIONAL_B_SPLINE_SURFACE(((1.00054449313167,0.785835073638801,1.),(1.00047707767468,
0.812351526358897,1.),(1.0004403178858,0.826810216506308,1.),(1.00044777653312,
0.823876514387295,1.)))
REPRESENTATION_ITEM('')
SURFACE()
);
#3978=(
BOUNDED_SURFACE()
B_SPLINE_SURFACE(3,2,((#446177,#446178,#446179),(#446180,#446181,#446182),
(#446183,#446184,#446185),(#446186,#446187,#446188)),.UNSPECIFIED.,.F.,
 .F.,.F.)
B_SPLINE_SURFACE_WITH_KNOTS((4,4),(3,3),(-4.06575814682064E-19,4.88747512969881E-5),
(-0.000215805216127666,1.),.UNSPECIFIED.)
GEOMETRIC_REPRESENTATION_ITEM()
RATIONAL_B_SPLINE_SURFACE(((1.00008915600365,0.793434085499612,1.),(1.00008930225018,
0.793095246303167,1.),(1.0000894468464,0.792760230720418,1.),(1.00008958984419,
0.792428918540461,1.)))
REPRESENTATION_ITEM('')
SURFACE()
);
#3979=(
BOUNDED_SURFACE()
B_SPLINE_SURFACE(3,2,((#446190,#446191,#446192),(#446193,#446194,#446195),
(#446196,#446197,#446198),(#446199,#446200,#446201),(#446202,#446203,#446204),
(#446205,#446206,#446207)),.UNSPECIFIED.,.F.,.F.,.F.)
B_SPLINE_SURFACE_WITH_KNOTS((4,2,4),(3,3),(2.57498015965307E-19,7.62675010863196E-5,
0.000152535002172639),(0.,1.02152348203073),.UNSPECIFIED.)
GEOMETRIC_REPRESENTATION_ITEM()
RATIONAL_B_SPLINE_SURFACE(((1.,0.78903359540124,1.00908146323694),(1.,0.857071781054815,
1.0061526259043),(1.,0.922087264710745,1.00335390671593),(1.,0.922394466502351,
1.00334068261144),(1.,0.857224384599061,1.00614605678502),(1.,0.789033595401638,
1.00908146323692)))
REPRESENTATION_ITEM('')
SURFACE()
);
#3980=(
BOUNDED_SURFACE()
B_SPLINE_SURFACE(3,2,((#446209,#446210,#446211),(#446212,#446213,#446214),
(#446215,#446216,#446217),(#446218,#446219,#446220)),.UNSPECIFIED.,.F.,
 .F.,.F.)
B_SPLINE_SURFACE_WITH_KNOTS((4,4),(3,3),(2.71050543121376E-19,4.88747512969884E-5),
(-0.000215489857776657,1.),.UNSPECIFIED.)
GEOMETRIC_REPRESENTATION_ITEM()
RATIONAL_B_SPLINE_SURFACE(((1.00008945889744,0.792428983985584,1.),(1.00008931610865,
0.792760296061136,1.),(1.00008917172378,0.793095311538218,1.),(1.00008902569101,
0.793434150627841,1.)))
REPRESENTATION_ITEM('')
SURFACE()
);
#3981=(
BOUNDED_SURFACE()
B_SPLINE_SURFACE(3,2,((#446222,#446223,#446224),(#446225,#446226,#446227),
(#446228,#446229,#446230),(#446231,#446232,#446233)),.UNSPECIFIED.,.F.,
 .F.,.F.)
B_SPLINE_SURFACE_WITH_KNOTS((4,4),(3,3),(-5.21974905013089E-6,5.74172395514396E-5),
(-0.00139822857761498,1.00051312364071),.UNSPECIFIED.)
GEOMETRIC_REPRESENTATION_ITEM()
RATIONAL_B_SPLINE_SURFACE(((1.00049256947252,0.823768952243994,1.00018060397851),
(1.00048448215723,0.826662424388281,1.00017763870884),(1.00052427784031,
0.812424361909353,1.00019223006923),(1.00059912365865,0.785646094632723,
1.00021967280233)))
REPRESENTATION_ITEM('')
SURFACE()
);
#3982=(
BOUNDED_SURFACE()
B_SPLINE_SURFACE(3,2,((#446237,#446238,#446239),(#446240,#446241,#446242),
(#446243,#446244,#446245),(#446246,#446247,#446248)),.UNSPECIFIED.,.F.,
 .F.,.F.)
B_SPLINE_SURFACE_WITH_KNOTS((4,4),(3,3),(3.22980774337779E-5,9.6376485487225E-5),
(-0.00154325936391278,1.01095292447534),.UNSPECIFIED.)
GEOMETRIC_REPRESENTATION_ITEM()
RATIONAL_B_SPLINE_SURFACE(((1.00023530983302,0.922925743796155,1.0016857472833),
(1.00015136166127,0.95042243959421,1.00108434699059),(1.00033574337402,
0.890029368953955,1.00240524789546),(1.00054260094228,0.822274473168319,
1.00388716464855)))
REPRESENTATION_ITEM('')
SURFACE()
);
#3983=(
BOUNDED_SURFACE()
B_SPLINE_SURFACE(3,2,((#446348,#446349,#446350),(#446351,#446352,#446353),
(#446354,#446355,#446356),(#446357,#446358,#446359)),.UNSPECIFIED.,.F.,
 .F.,.F.)
B_SPLINE_SURFACE_WITH_KNOTS((4,4),(3,3),(-2.16840434497101E-19,0.000101260117256737),
(0.,1.),.UNSPECIFIED.)
GEOMETRIC_REPRESENTATION_ITEM()
RATIONAL_B_SPLINE_SURFACE(((1.,0.796615278835167,1.),(1.,0.795896038055957,
1.),(1.,0.795193354661325,1.),(1.,0.794506193185552,1.)))
REPRESENTATION_ITEM('')
SURFACE()
);
#3984=(
BOUNDED_SURFACE()
B_SPLINE_SURFACE(3,2,((#446397,#446398,#446399),(#446400,#446401,#446402),
(#446403,#446404,#446405),(#446406,#446407,#446408),(#446409,#446410,#446411),
(#446412,#446413,#446414)),.UNSPECIFIED.,.F.,.F.,.F.)
B_SPLINE_SURFACE_WITH_KNOTS((4,2,4),(3,3),(-9.65617559869902E-20,1.66936432462292E-5,
3.33872864924584E-5),(0.,1.),.UNSPECIFIED.)
GEOMETRIC_REPRESENTATION_ITEM()
RATIONAL_B_SPLINE_SURFACE(((1.,0.796615278835172,1.),(1.,0.862310524418138,
1.),(1.,0.923774472010516,1.),(1.,0.923983993203424,1.),(1.,0.862574873720945,
1.),(1.,0.796615278835193,1.)))
REPRESENTATION_ITEM('')
SURFACE()
);
#3985=(
BOUNDED_SURFACE()
B_SPLINE_SURFACE(3,2,((#446451,#446452,#446453),(#446454,#446455,#446456),
(#446457,#446458,#446459),(#446460,#446461,#446462)),.UNSPECIFIED.,.F.,
 .F.,.F.)
B_SPLINE_SURFACE_WITH_KNOTS((4,4),(3,3),(0.,0.000101244905251112),(0.,1.),
 .UNSPECIFIED.)
GEOMETRIC_REPRESENTATION_ITEM()
RATIONAL_B_SPLINE_SURFACE(((1.,0.796615278835168,1.),(1.,0.795896146109815,
1.),(1.,0.795193565796487,1.),(1.,0.794506502889903,1.)))
REPRESENTATION_ITEM('')
SURFACE()
);
#3986=(
BOUNDED_SURFACE()
B_SPLINE_SURFACE(3,2,((#446498,#446499,#446500),(#446501,#446502,#446503),
(#446504,#446505,#446506),(#446507,#446508,#446509)),.UNSPECIFIED.,.F.,
 .F.,.F.)
B_SPLINE_SURFACE_WITH_KNOTS((4,4),(3,3),(2.85968127239939E-5,9.24681548475817E-5),
(-0.00167900678566562,1.0113082712783),.UNSPECIFIED.)
GEOMETRIC_REPRESENTATION_ITEM()
RATIONAL_B_SPLINE_SURFACE(((1.00059040895186,0.822187541868416,1.00401468696659),
(1.0003652771812,0.889990093671664,1.00248382673393),(1.00016469515004,
0.950399042257967,1.00111990082512),(1.00025604273979,0.922888044286144,
1.00174104990632)))
REPRESENTATION_ITEM('')
SURFACE()
);
#3987=(
BOUNDED_SURFACE()
B_SPLINE_SURFACE(3,2,((#446513,#446514,#446515),(#446516,#446517,#446518),
(#446519,#446520,#446521),(#446522,#446523,#446524)),.UNSPECIFIED.,.F.,
 .F.,.F.)
B_SPLINE_SURFACE_WITH_KNOTS((4,4),(3,3),(-5.2235835674927E-6,5.74594192424276E-5),
(-0.00127120052072291,1.),.UNSPECIFIED.)
GEOMETRIC_REPRESENTATION_ITEM()
RATIONAL_B_SPLINE_SURFACE(((1.00054449313182,0.785835073638727,1.),(1.00047707767481,
0.812351526358816,1.),(1.00044031788592,0.826810216506266,1.),(1.00044777653324,
0.823876514387224,0.999999999999999)))
REPRESENTATION_ITEM('')
SURFACE()
);
#3988=(
BOUNDED_SURFACE()
B_SPLINE_SURFACE(3,2,((#446526,#446527,#446528),(#446529,#446530,#446531),
(#446532,#446533,#446534),(#446535,#446536,#446537)),.UNSPECIFIED.,.F.,
 .F.,.F.)
B_SPLINE_SURFACE_WITH_KNOTS((4,4),(3,3),(8.13151629364128E-20,4.88747512969881E-5),
(-0.000215805215461378,1.),.UNSPECIFIED.)
GEOMETRIC_REPRESENTATION_ITEM()
RATIONAL_B_SPLINE_SURFACE(((1.00008915600337,0.793434085499749,1.),(1.0000893022499,
0.793095246303298,1.),(1.00008944684612,0.792760230720561,1.),(1.00008958984392,
0.792428918540598,1.)))
REPRESENTATION_ITEM('')
SURFACE()
);
#3989=(
BOUNDED_SURFACE()
B_SPLINE_SURFACE(3,2,((#446539,#446540,#446541),(#446542,#446543,#446544),
(#446545,#446546,#446547),(#446548,#446549,#446550),(#446551,#446552,#446553),
(#446554,#446555,#446556)),.UNSPECIFIED.,.F.,.F.,.F.)
B_SPLINE_SURFACE_WITH_KNOTS((4,2,4),(3,3),(3.3881317890172E-19,7.62675010863196E-5,
0.000152535002172639),(0.,1.02152348203084),.UNSPECIFIED.)
GEOMETRIC_REPRESENTATION_ITEM()
RATIONAL_B_SPLINE_SURFACE(((1.,0.789033595401216,1.00908146323698),(1.,
0.857071781054838,1.00615262590433),(1.,0.922087264710683,1.00335390671595),
(1.,0.922394466502394,1.00334068261146),(1.,0.857224384599003,1.00614605678505),
(1.,0.789033595401619,1.00908146323697)))
REPRESENTATION_ITEM('')
SURFACE()
);
#3990=(
BOUNDED_SURFACE()
B_SPLINE_SURFACE(3,2,((#446558,#446559,#446560),(#446561,#446562,#446563),
(#446564,#446565,#446566),(#446567,#446568,#446569)),.UNSPECIFIED.,.F.,
 .F.,.F.)
B_SPLINE_SURFACE_WITH_KNOTS((4,4),(3,3),(3.79470760369927E-19,4.88747512969887E-5),
(-0.000215489857685973,1.),.UNSPECIFIED.)
GEOMETRIC_REPRESENTATION_ITEM()
RATIONAL_B_SPLINE_SURFACE(((1.0000894588974,0.792428983985612,1.),(1.00008931610862,
0.792760296061168,1.),(1.00008917172374,0.793095311538222,1.),(1.00008902569097,
0.793434150627863,1.)))
REPRESENTATION_ITEM('')
SURFACE()
);
#3991=(
BOUNDED_SURFACE()
B_SPLINE_SURFACE(3,2,((#446571,#446572,#446573),(#446574,#446575,#446576),
(#446577,#446578,#446579),(#446580,#446581,#446582)),.UNSPECIFIED.,.F.,
 .F.,.F.)
B_SPLINE_SURFACE_WITH_KNOTS((4,4),(3,3),(-5.21974905012865E-6,5.74172395514394E-5),
(-0.00139822857779505,1.00051312364059),.UNSPECIFIED.)
GEOMETRIC_REPRESENTATION_ITEM()
RATIONAL_B_SPLINE_SURFACE(((1.00049256947259,0.823768952243974,1.00018060397847),
(1.00048448215729,0.82666242438829,1.00017763870879),(1.00052427784037,
0.812424361909337,1.00019223006918),(1.00059912365873,0.785646094632719,
1.00021967280228)))
REPRESENTATION_ITEM('')
SURFACE()
);
#3992=(
BOUNDED_SURFACE()
B_SPLINE_SURFACE(3,2,((#446586,#446587,#446588),(#446589,#446590,#446591),
(#446592,#446593,#446594),(#446595,#446596,#446597)),.UNSPECIFIED.,.F.,
 .F.,.F.)
B_SPLINE_SURFACE_WITH_KNOTS((4,4),(3,3),(3.22980774337779E-5,9.63764854872255E-5),
(-0.00154325936373564,1.01095292447558),.UNSPECIFIED.)
GEOMETRIC_REPRESENTATION_ITEM()
RATIONAL_B_SPLINE_SURFACE(((1.00023530983299,0.922925743796153,1.00168574728333),
(1.00015136166126,0.950422439594224,1.00108434699061),(1.00033574337398,
0.890029368953923,1.00240524789551),(1.00054260094221,0.822274473168319,
1.00388716464863)))
REPRESENTATION_ITEM('')
SURFACE()
);
#3993=(
BOUNDED_SURFACE()
B_SPLINE_SURFACE(3,2,((#446697,#446698,#446699),(#446700,#446701,#446702),
(#446703,#446704,#446705),(#446706,#446707,#446708)),.UNSPECIFIED.,.F.,
 .F.,.F.)
B_SPLINE_SURFACE_WITH_KNOTS((4,4),(3,3),(0.,0.000101260117256737),(0.,1.),
 .UNSPECIFIED.)
GEOMETRIC_REPRESENTATION_ITEM()
RATIONAL_B_SPLINE_SURFACE(((1.,0.796615278835172,1.),(1.,0.795896038055943,
1.),(1.,0.795193354661353,1.),(1.,0.794506193185535,1.)))
REPRESENTATION_ITEM('')
SURFACE()
);
#3994=(
BOUNDED_SURFACE()
B_SPLINE_SURFACE(3,2,((#446746,#446747,#446748),(#446749,#446750,#446751),
(#446752,#446753,#446754),(#446755,#446756,#446757),(#446758,#446759,#446760),
(#446761,#446762,#446763)),.UNSPECIFIED.,.F.,.F.,.F.)
B_SPLINE_SURFACE_WITH_KNOTS((4,2,4),(3,3),(6.7762635780344E-21,1.66936432462296E-5,
3.33872864924592E-5),(0.,1.),.UNSPECIFIED.)
GEOMETRIC_REPRESENTATION_ITEM()
RATIONAL_B_SPLINE_SURFACE(((1.,0.796615278835168,1.),(1.,0.862310524418132,
1.),(1.,0.923774472010516,1.),(1.,0.92398399320343,1.),(1.,0.862574873720948,
1.),(1.,0.796615278835173,1.)))
REPRESENTATION_ITEM('')
SURFACE()
);
#3995=(
BOUNDED_SURFACE()
B_SPLINE_SURFACE(3,2,((#446800,#446801,#446802),(#446803,#446804,#446805),
(#446806,#446807,#446808),(#446809,#446810,#446811)),.UNSPECIFIED.,.F.,
 .F.,.F.)
B_SPLINE_SURFACE_WITH_KNOTS((4,4),(3,3),(0.,0.000101244905251112),(0.,1.),
 .UNSPECIFIED.)
GEOMETRIC_REPRESENTATION_ITEM()
RATIONAL_B_SPLINE_SURFACE(((1.,0.796615278835173,1.),(1.,0.795896146109806,
1.),(1.,0.795193565796486,1.),(1.,0.794506502889902,1.)))
REPRESENTATION_ITEM('')
SURFACE()
);
#3996=(
BOUNDED_SURFACE()
B_SPLINE_SURFACE(3,2,((#446847,#446848,#446849),(#446850,#446851,#446852),
(#446853,#446854,#446855),(#446856,#446857,#446858)),.UNSPECIFIED.,.F.,
 .F.,.F.)
B_SPLINE_SURFACE_WITH_KNOTS((4,4),(3,3),(2.85968127239939E-5,9.24681548475817E-5),
(-0.00167900678653656,1.01130827127818),.UNSPECIFIED.)
GEOMETRIC_REPRESENTATION_ITEM()
RATIONAL_B_SPLINE_SURFACE(((1.00059040895217,0.822187541868281,1.00401468696655),
(1.00036527718139,0.889990093671577,1.0024838267339),(1.00016469515013,
0.950399042257933,1.0011199008251),(1.00025604273992,0.922888044286085,
1.0017410499063)))
REPRESENTATION_ITEM('')
SURFACE()
);
#3997=(
BOUNDED_SURFACE()
B_SPLINE_SURFACE(3,2,((#446862,#446863,#446864),(#446865,#446866,#446867),
(#446868,#446869,#446870),(#446871,#446872,#446873)),.UNSPECIFIED.,.F.,
 .F.,.F.)
B_SPLINE_SURFACE_WITH_KNOTS((4,4),(3,3),(-5.22358356749152E-6,5.74594192424278E-5),
(-0.00127120052060224,1.),.UNSPECIFIED.)
GEOMETRIC_REPRESENTATION_ITEM()
RATIONAL_B_SPLINE_SURFACE(((1.00054449313177,0.785835073638743,1.),(1.00047707767477,
0.812351526358862,1.),(1.00044031788588,0.826810216506264,1.),(1.0004477765332,
0.82387651438726,1.)))
REPRESENTATION_ITEM('')
SURFACE()
);
#3998=(
BOUNDED_SURFACE()
B_SPLINE_SURFACE(3,2,((#446875,#446876,#446877),(#446878,#446879,#446880),
(#446881,#446882,#446883),(#446884,#446885,#446886)),.UNSPECIFIED.,.F.,
 .F.,.F.)
B_SPLINE_SURFACE_WITH_KNOTS((4,4),(3,3),(5.42101086242752E-20,4.88747512969882E-5),
(-0.000215805215310359,1.),.UNSPECIFIED.)
GEOMETRIC_REPRESENTATION_ITEM()
RATIONAL_B_SPLINE_SURFACE(((1.00008915600331,0.793434085499782,1.),(1.00008930224984,
0.793095246303326,1.),(1.00008944684606,0.792760230720599,1.),(1.00008958984385,
0.792428918540626,1.)))
REPRESENTATION_ITEM('')
SURFACE()
);
#3999=(
BOUNDED_SURFACE()
B_SPLINE_SURFACE(3,2,((#446888,#446889,#446890),(#446891,#446892,#446893),
(#446894,#446895,#446896),(#446897,#446898,#446899),(#446900,#446901,#446902),
(#446903,#446904,#446905)),.UNSPECIFIED.,.F.,.F.,.F.)
B_SPLINE_SURFACE_WITH_KNOTS((4,2,4),(3,3),(5.42101086242752E-20,7.62675010863198E-5,
0.00015253500217264),(0.,1.02152348203056),.UNSPECIFIED.)
GEOMETRIC_REPRESENTATION_ITEM()
RATIONAL_B_SPLINE_SURFACE(((1.,0.789033595401273,1.00908146323687),(1.,
0.857071781054834,1.00615262590425),(1.,0.922087264710764,1.0033539067159),
(1.,0.922394466502349,1.00334068261142),(1.,0.857224384599092,1.00614605678497),
(1.,0.789033595401673,1.00908146323685)))
REPRESENTATION_ITEM('')
SURFACE()
);
#4000=(
BOUNDED_SURFACE()
B_SPLINE_SURFACE(3,2,((#446907,#446908,#446909),(#446910,#446911,#446912),
(#446913,#446914,#446915),(#446916,#446917,#446918)),.UNSPECIFIED.,.F.,
 .F.,.F.)
B_SPLINE_SURFACE_WITH_KNOTS((4,4),(3,3),(2.16840434497101E-19,4.88747512969882E-5),
(-0.00021548985710036,1.),.UNSPECIFIED.)
GEOMETRIC_REPRESENTATION_ITEM()
RATIONAL_B_SPLINE_SURFACE(((1.00008945889716,0.792428983985733,1.),(1.00008931610837,
0.792760296061284,1.),(1.0000891717235,0.79309531153835,1.),(1.00008902569073,
0.793434150627984,1.)))
REPRESENTATION_ITEM('')
SURFACE()
);
#4001=(
BOUNDED_SURFACE()
B_SPLINE_SURFACE(3,2,((#446920,#446921,#446922),(#446923,#446924,#446925),
(#446926,#446927,#446928),(#446929,#446930,#446931)),.UNSPECIFIED.,.F.,
 .F.,.F.)
B_SPLINE_SURFACE_WITH_KNOTS((4,4),(3,3),(-5.21974905013085E-6,5.74172395514395E-5),
(-0.00139822857727288,1.00051312364058),.UNSPECIFIED.)
GEOMETRIC_REPRESENTATION_ITEM()
RATIONAL_B_SPLINE_SURFACE(((1.0004925694724,0.823768952244077,1.00018060397846),
(1.00048448215711,0.826662424388372,1.00017763870879),(1.00052427784018,
0.812424361909439,1.00019223006918),(1.00059912365851,0.785646094632826,
1.00021967280227)))
REPRESENTATION_ITEM('')
SURFACE()
);
#4002=(
BOUNDED_SURFACE()
B_SPLINE_SURFACE(3,2,((#446935,#446936,#446937),(#446938,#446939,#446940),
(#446941,#446942,#446943),(#446944,#446945,#446946)),.UNSPECIFIED.,.F.,
 .F.,.F.)
B_SPLINE_SURFACE_WITH_KNOTS((4,4),(3,3),(3.22980774337779E-5,9.63764854872249E-5),
(-0.00154325936381161,1.01095292447546),.UNSPECIFIED.)
GEOMETRIC_REPRESENTATION_ITEM()
RATIONAL_B_SPLINE_SURFACE(((1.000235309833,0.922925743796154,1.00168574728331),
(1.00015136166126,0.950422439594223,1.0010843469906),(1.000335743374,0.890029368953939,
1.00240524789548),(1.00054260094224,0.822274473168318,1.00388716464859)))
REPRESENTATION_ITEM('')
SURFACE()
);
#4003=(
BOUNDED_SURFACE()
B_SPLINE_SURFACE(3,2,((#447046,#447047,#447048),(#447049,#447050,#447051),
(#447052,#447053,#447054),(#447055,#447056,#447057)),.UNSPECIFIED.,.F.,
 .F.,.F.)
B_SPLINE_SURFACE_WITH_KNOTS((4,4),(3,3),(0.,0.000101260117256738),(0.,1.),
 .UNSPECIFIED.)
GEOMETRIC_REPRESENTATION_ITEM()
RATIONAL_B_SPLINE_SURFACE(((1.,0.796615278835172,1.),(1.,0.795896038055937,
1.),(1.,0.795193354661345,1.),(1.,0.794506193185552,1.)))
REPRESENTATION_ITEM('')
SURFACE()
);
#4004=(
BOUNDED_SURFACE()
B_SPLINE_SURFACE(3,2,((#447095,#447096,#447097),(#447098,#447099,#447100),
(#447101,#447102,#447103),(#447104,#447105,#447106),(#447107,#447108,#447109),
(#447110,#447111,#447112)),.UNSPECIFIED.,.F.,.F.,.F.)
B_SPLINE_SURFACE_WITH_KNOTS((4,2,4),(3,3),(-2.3039296165317E-19,1.66936432462291E-5,
3.33872864924584E-5),(0.,1.),.UNSPECIFIED.)
GEOMETRIC_REPRESENTATION_ITEM()
RATIONAL_B_SPLINE_SURFACE(((1.,0.796615278835176,1.),(1.,0.862310524418132,
1.),(1.,0.923774472010524,1.),(1.,0.923983993203423,1.),(1.,0.862574873720957,
1.),(1.,0.796615278835182,1.)))
REPRESENTATION_ITEM('')
SURFACE()
);
#4005=(
BOUNDED_SURFACE()
B_SPLINE_SURFACE(3,2,((#447149,#447150,#447151),(#447152,#447153,#447154),
(#447155,#447156,#447157),(#447158,#447159,#447160)),.UNSPECIFIED.,.F.,
 .F.,.F.)
B_SPLINE_SURFACE_WITH_KNOTS((4,4),(3,3),(0.,0.000101244905251112),(0.,1.),
 .UNSPECIFIED.)
GEOMETRIC_REPRESENTATION_ITEM()
RATIONAL_B_SPLINE_SURFACE(((1.,0.796615278835172,1.),(1.,0.795896146109801,
1.),(1.,0.795193565796489,1.),(1.,0.794506502889901,1.)))
REPRESENTATION_ITEM('')
SURFACE()
);
#4006=(
BOUNDED_SURFACE()
B_SPLINE_SURFACE(3,2,((#447196,#447197,#447198),(#447199,#447200,#447201),
(#447202,#447203,#447204),(#447205,#447206,#447207)),.UNSPECIFIED.,.F.,
 .F.,.F.)
B_SPLINE_SURFACE_WITH_KNOTS((4,4),(3,3),(2.85968127239939E-5,9.24681548475818E-5),
(-0.00167900678649614,1.01130827127826),.UNSPECIFIED.)
GEOMETRIC_REPRESENTATION_ITEM()
RATIONAL_B_SPLINE_SURFACE(((1.00059040895215,0.822187541868272,1.00401468696658),
(1.00036527718139,0.889990093671571,1.00248382673392),(1.00016469515013,
0.950399042257931,1.00111990082511),(1.00025604273992,0.92288804428608,
1.00174104990632)))
REPRESENTATION_ITEM('')
SURFACE()
);
#4007=(
BOUNDED_SURFACE()
B_SPLINE_SURFACE(3,2,((#447211,#447212,#447213),(#447214,#447215,#447216),
(#447217,#447218,#447219),(#447220,#447221,#447222)),.UNSPECIFIED.,.F.,
 .F.,.F.)
B_SPLINE_SURFACE_WITH_KNOTS((4,4),(3,3),(-5.22358356749255E-6,5.74594192424278E-5),
(-0.00127120052063573,1.),.UNSPECIFIED.)
GEOMETRIC_REPRESENTATION_ITEM()
RATIONAL_B_SPLINE_SURFACE(((1.00054449313178,0.785835073638738,1.),(1.00047707767478,
0.812351526358855,1.),(1.00044031788589,0.826810216506258,1.),(1.00044777653321,
0.823876514387244,1.)))
REPRESENTATION_ITEM('')
SURFACE()
);
#4008=(
BOUNDED_SURFACE()
B_SPLINE_SURFACE(3,2,((#447224,#447225,#447226),(#447227,#447228,#447229),
(#447230,#447231,#447232),(#447233,#447234,#447235)),.UNSPECIFIED.,.F.,
 .F.,.F.)
B_SPLINE_SURFACE_WITH_KNOTS((4,4),(3,3),(2.71050543121376E-20,4.88747512969881E-5),
(-0.000215805215194671,1.),.UNSPECIFIED.)
GEOMETRIC_REPRESENTATION_ITEM()
RATIONAL_B_SPLINE_SURFACE(((1.00008915600326,0.793434085499798,1.),(1.00008930224979,
0.793095246303346,1.),(1.00008944684601,0.792760230720619,1.),(1.0000895898438,
0.792428918540652,1.)))
REPRESENTATION_ITEM('')
SURFACE()
);
#4009=(
BOUNDED_SURFACE()
B_SPLINE_SURFACE(3,2,((#447237,#447238,#447239),(#447240,#447241,#447242),
(#447243,#447244,#447245),(#447246,#447247,#447248),(#447249,#447250,#447251),
(#447252,#447253,#447254)),.UNSPECIFIED.,.F.,.F.,.F.)
B_SPLINE_SURFACE_WITH_KNOTS((4,2,4),(3,3),(5.21772295508649E-19,7.62675010863198E-5,
0.000152535002172639),(0.,1.02152348203077),.UNSPECIFIED.)
GEOMETRIC_REPRESENTATION_ITEM()
RATIONAL_B_SPLINE_SURFACE(((1.,0.789033595401235,1.00908146323695),(1.,
0.857071781054861,1.00615262590431),(1.,0.92208726471068,1.00335390671594),
(1.,0.922394466502408,1.00334068261145),(1.,0.85722438459901,1.00614605678503),
(1.,0.789033595401628,1.00908146323694)))
REPRESENTATION_ITEM('')
SURFACE()
);
#4010=(
BOUNDED_SURFACE()
B_SPLINE_SURFACE(3,2,((#447256,#447257,#447258),(#447259,#447260,#447261),
(#447262,#447263,#447264),(#447265,#447266,#447267)),.UNSPECIFIED.,.F.,
 .F.,.F.)
B_SPLINE_SURFACE_WITH_KNOTS((4,4),(3,3),(2.16840434497101E-19,4.88747512969882E-5),
(-0.000215489857075741,1.),.UNSPECIFIED.)
GEOMETRIC_REPRESENTATION_ITEM()
RATIONAL_B_SPLINE_SURFACE(((1.00008945889715,0.792428983985742,1.),(1.00008931610836,
0.792760296061281,1.),(1.00008917172349,0.793095311538358,1.),(1.00008902569072,
0.793434150627989,1.)))
REPRESENTATION_ITEM('')
SURFACE()
);
#4011=(
BOUNDED_SURFACE()
B_SPLINE_SURFACE(3,2,((#447269,#447270,#447271),(#447272,#447273,#447274),
(#447275,#447276,#447277),(#447278,#447279,#447280)),.UNSPECIFIED.,.F.,
 .F.,.F.)
B_SPLINE_SURFACE_WITH_KNOTS((4,4),(3,3),(-5.2197490501309E-6,5.74172395514397E-5),
(-0.00139822857767823,1.00051312364072),.UNSPECIFIED.)
GEOMETRIC_REPRESENTATION_ITEM()
RATIONAL_B_SPLINE_SURFACE(((1.00049256947254,0.823768952243982,1.00018060397851),
(1.00048448215725,0.826662424388278,1.00017763870884),(1.00052427784033,
0.812424361909341,1.00019223006923),(1.00059912365868,0.785646094632709,
1.00021967280233)))
REPRESENTATION_ITEM('')
SURFACE()
);
#4012=(
BOUNDED_SURFACE()
B_SPLINE_SURFACE(3,2,((#447284,#447285,#447286),(#447287,#447288,#447289),
(#447290,#447291,#447292),(#447293,#447294,#447295)),.UNSPECIFIED.,.F.,
 .F.,.F.)
B_SPLINE_SURFACE_WITH_KNOTS((4,4),(3,3),(3.22980774337779E-5,9.63764854872255E-5),
(-0.00154325936377236,1.01095292447541),.UNSPECIFIED.)
GEOMETRIC_REPRESENTATION_ITEM()
RATIONAL_B_SPLINE_SURFACE(((1.00023530983299,0.922925743796161,1.00168574728331),
(1.00015136166126,0.950422439594217,1.0010843469906),(1.00033574337399,
0.890029368953947,1.00240524789547),(1.00054260094223,0.822274473168337,
1.00388716464857)))
REPRESENTATION_ITEM('')
SURFACE()
);
#4013=(
BOUNDED_SURFACE()
B_SPLINE_SURFACE(3,2,((#447395,#447396,#447397),(#447398,#447399,#447400),
(#447401,#447402,#447403),(#447404,#447405,#447406)),.UNSPECIFIED.,.F.,
 .F.,.F.)
B_SPLINE_SURFACE_WITH_KNOTS((4,4),(3,3),(0.,0.000101260117256738),(0.,1.),
 .UNSPECIFIED.)
GEOMETRIC_REPRESENTATION_ITEM()
RATIONAL_B_SPLINE_SURFACE(((1.,0.796615278835173,1.),(1.,0.795896038055938,
1.),(1.,0.795193354661348,1.),(1.,0.794506193185554,1.)))
REPRESENTATION_ITEM('')
SURFACE()
);
#4014=(
BOUNDED_SURFACE()
B_SPLINE_SURFACE(3,2,((#447444,#447445,#447446),(#447447,#447448,#447449),
(#447450,#447451,#447452),(#447453,#447454,#447455),(#447456,#447457,#447458),
(#447459,#447460,#447461)),.UNSPECIFIED.,.F.,.F.,.F.)
B_SPLINE_SURFACE_WITH_KNOTS((4,2,4),(3,3),(1.18584612615602E-20,1.66936432462294E-5,
3.33872864924588E-5),(0.,1.),.UNSPECIFIED.)
GEOMETRIC_REPRESENTATION_ITEM()
RATIONAL_B_SPLINE_SURFACE(((1.,0.796615278835176,1.),(1.,0.862310524418132,
1.),(1.,0.923774472010525,1.),(1.,0.923983993203423,1.),(1.,0.862574873720945,
1.),(1.,0.796615278835186,1.)))
REPRESENTATION_ITEM('')
SURFACE()
);
#4015=(
BOUNDED_SURFACE()
B_SPLINE_SURFACE(3,2,((#447498,#447499,#447500),(#447501,#447502,#447503),
(#447504,#447505,#447506),(#447507,#447508,#447509)),.UNSPECIFIED.,.F.,
 .F.,.F.)
B_SPLINE_SURFACE_WITH_KNOTS((4,4),(3,3),(-2.16840434497101E-19,0.000101244905251112),
(0.,1.),.UNSPECIFIED.)
GEOMETRIC_REPRESENTATION_ITEM()
RATIONAL_B_SPLINE_SURFACE(((1.,0.796615278835172,1.),(1.,0.795896146109798,
1.),(1.,0.795193565796494,1.),(1.,0.794506502889905,1.)))
REPRESENTATION_ITEM('')
SURFACE()
);
#4016=(
BOUNDED_SURFACE()
B_SPLINE_SURFACE(3,2,((#447545,#447546,#447547),(#447548,#447549,#447550),
(#447551,#447552,#447553),(#447554,#447555,#447556)),.UNSPECIFIED.,.F.,
 .F.,.F.)
B_SPLINE_SURFACE_WITH_KNOTS((4,4),(3,3),(2.85968127239939E-5,9.24681548475818E-5),
(-0.00167900678790481,1.01130827127829),.UNSPECIFIED.)
GEOMETRIC_REPRESENTATION_ITEM()
RATIONAL_B_SPLINE_SURFACE(((1.00059040895265,0.822187541868015,1.00401468696659),
(1.00036527718169,0.889990093671412,1.00248382673393),(1.00016469515026,
0.950399042257863,1.00111990082512),(1.00025604274013,0.922888044285965,
1.00174104990632)))
REPRESENTATION_ITEM('')
SURFACE()
);
#4017=(
BOUNDED_SURFACE()
B_SPLINE_SURFACE(3,2,((#447560,#447561,#447562),(#447563,#447564,#447565),
(#447566,#447567,#447568),(#447569,#447570,#447571)),.UNSPECIFIED.,.F.,
 .F.,.F.)
B_SPLINE_SURFACE_WITH_KNOTS((4,4),(3,3),(-5.22358356749333E-6,5.74594192424277E-5),
(-0.00127120052062949,1.),.UNSPECIFIED.)
GEOMETRIC_REPRESENTATION_ITEM()
RATIONAL_B_SPLINE_SURFACE(((1.00054449313178,0.785835073638757,1.),(1.00047707767478,
0.812351526358823,1.),(1.00044031788589,0.826810216506297,1.),(1.00044777653321,
0.823876514387231,1.)))
REPRESENTATION_ITEM('')
SURFACE()
);
#4018=(
BOUNDED_SURFACE()
B_SPLINE_SURFACE(3,2,((#447573,#447574,#447575),(#447576,#447577,#447578),
(#447579,#447580,#447581),(#447582,#447583,#447584)),.UNSPECIFIED.,.F.,
 .F.,.F.)
B_SPLINE_SURFACE_WITH_KNOTS((4,4),(3,3),(-2.98155597433514E-19,4.88747512969879E-5),
(-0.000215805215320105,1.),.UNSPECIFIED.)
GEOMETRIC_REPRESENTATION_ITEM()
RATIONAL_B_SPLINE_SURFACE(((1.00008915600331,0.793434085499779,1.),(1.00008930224984,
0.79309524630333,1.),(1.00008944684606,0.792760230720593,1.),(1.00008958984386,
0.792428918540629,1.)))
REPRESENTATION_ITEM('')
SURFACE()
);
#4019=(
BOUNDED_SURFACE()
B_SPLINE_SURFACE(3,2,((#447586,#447587,#447588),(#447589,#447590,#447591),
(#447592,#447593,#447594),(#447595,#447596,#447597),(#447598,#447599,#447600),
(#447601,#447602,#447603)),.UNSPECIFIED.,.F.,.F.,.F.)
B_SPLINE_SURFACE_WITH_KNOTS((4,2,4),(3,3),(2.91379333855479E-19,7.62675010863198E-5,
0.000152535002172639),(0.,1.02152348203072),.UNSPECIFIED.)
GEOMETRIC_REPRESENTATION_ITEM()
RATIONAL_B_SPLINE_SURFACE(((1.,0.789033595401243,1.00908146323693),(1.,
0.857071781054836,1.0061526259043),(1.,0.922087264710717,1.00335390671593),
(1.,0.922394466502379,1.00334068261144),(1.,0.857224384599041,1.00614605678501),
(1.,0.78903359540164,1.00908146323692)))
REPRESENTATION_ITEM('')
SURFACE()
);
#4020=(
BOUNDED_SURFACE()
B_SPLINE_SURFACE(3,2,((#447605,#447606,#447607),(#447608,#447609,#447610),
(#447611,#447612,#447613),(#447614,#447615,#447616)),.UNSPECIFIED.,.F.,
 .F.,.F.)
B_SPLINE_SURFACE_WITH_KNOTS((4,4),(3,3),(3.79470760369927E-19,4.88747512969886E-5),
(-0.000215489857667756,1.),.UNSPECIFIED.)
GEOMETRIC_REPRESENTATION_ITEM()
RATIONAL_B_SPLINE_SURFACE(((1.00008945889739,0.792428983985614,1.),(1.00008931610861,
0.79276029606116,1.),(1.00008917172374,0.793095311538243,1.),(1.00008902569096,
0.793434150627865,1.)))
REPRESENTATION_ITEM('')
SURFACE()
);
#4021=(
BOUNDED_SURFACE()
B_SPLINE_SURFACE(3,2,((#447618,#447619,#447620),(#447621,#447622,#447623),
(#447624,#447625,#447626),(#447627,#447628,#447629)),.UNSPECIFIED.,.F.,
 .F.,.F.)
B_SPLINE_SURFACE_WITH_KNOTS((4,4),(3,3),(-5.21974905013081E-6,5.74172395514399E-5),
(-0.00139822857725879,1.00051312364054),.UNSPECIFIED.)
GEOMETRIC_REPRESENTATION_ITEM()
RATIONAL_B_SPLINE_SURFACE(((1.0004925694724,0.823768952244095,1.00018060397845),
(1.0004844821571,0.826662424388373,1.00017763870878),(1.00052427784017,
0.812424361909455,1.00019223006916),(1.0005991236585,0.785646094632837,
1.00021967280225)))
REPRESENTATION_ITEM('')
SURFACE()
);
#4022=(
BOUNDED_SURFACE()
B_SPLINE_SURFACE(3,2,((#447633,#447634,#447635),(#447636,#447637,#447638),
(#447639,#447640,#447641),(#447642,#447643,#447644)),.UNSPECIFIED.,.F.,
 .F.,.F.)
B_SPLINE_SURFACE_WITH_KNOTS((4,4),(3,3),(3.22980774337778E-5,9.63764854872249E-5),
(-0.0015432593637765,1.01095292447533),.UNSPECIFIED.)
GEOMETRIC_REPRESENTATION_ITEM()
RATIONAL_B_SPLINE_SURFACE(((1.000235309833,0.922925743796168,1.00168574728329),
(1.00015136166126,0.950422439594216,1.00108434699059),(1.00033574337399,
0.890029368953968,1.00240524789545),(1.00054260094223,0.822274473168339,
1.00388716464855)))
REPRESENTATION_ITEM('')
SURFACE()
);
#4023=(
BOUNDED_SURFACE()
B_SPLINE_SURFACE(3,2,((#447744,#447745,#447746),(#447747,#447748,#447749),
(#447750,#447751,#447752),(#447753,#447754,#447755)),.UNSPECIFIED.,.F.,
 .F.,.F.)
B_SPLINE_SURFACE_WITH_KNOTS((4,4),(3,3),(-2.16840434497101E-19,0.000101260117256738),
(0.,1.),.UNSPECIFIED.)
GEOMETRIC_REPRESENTATION_ITEM()
RATIONAL_B_SPLINE_SURFACE(((1.,0.79661527883517,1.),(1.,0.795896038055935,
1.),(1.,0.795193354661348,1.),(1.,0.794506193185538,1.)))
REPRESENTATION_ITEM('')
SURFACE()
);
#4024=(
BOUNDED_SURFACE()
B_SPLINE_SURFACE(3,2,((#447793,#447794,#447795),(#447796,#447797,#447798),
(#447799,#447800,#447801),(#447802,#447803,#447804),(#447805,#447806,#447807),
(#447808,#447809,#447810)),.UNSPECIFIED.,.F.,.F.,.F.)
B_SPLINE_SURFACE_WITH_KNOTS((4,2,4),(3,3),(-2.3039296165317E-19,1.66936432462292E-5,
3.33872864924587E-5),(0.,1.),.UNSPECIFIED.)
GEOMETRIC_REPRESENTATION_ITEM()
RATIONAL_B_SPLINE_SURFACE(((1.,0.79661527883517,1.),(1.,0.862310524418134,
1.),(1.,0.923774472010517,1.),(1.,0.923983993203428,1.),(1.,0.862574873720944,
1.),(1.,0.796615278835184,1.)))
REPRESENTATION_ITEM('')
SURFACE()
);
#4025=(
BOUNDED_SURFACE()
B_SPLINE_SURFACE(3,2,((#447847,#447848,#447849),(#447850,#447851,#447852),
(#447853,#447854,#447855),(#447856,#447857,#447858)),.UNSPECIFIED.,.F.,
 .F.,.F.)
B_SPLINE_SURFACE_WITH_KNOTS((4,4),(3,3),(0.,0.000101244905251112),(0.,1.),
 .UNSPECIFIED.)
GEOMETRIC_REPRESENTATION_ITEM()
RATIONAL_B_SPLINE_SURFACE(((1.,0.79661527883517,1.),(1.,0.795896146109801,
1.),(1.,0.795193565796499,1.),(1.,0.794506502889901,1.)))
REPRESENTATION_ITEM('')
SURFACE()
);
#4026=(
BOUNDED_SURFACE()
B_SPLINE_SURFACE(3,2,((#447894,#447895,#447896),(#447897,#447898,#447899),
(#447900,#447901,#447902),(#447903,#447904,#447905)),.UNSPECIFIED.,.F.,
 .F.,.F.)
B_SPLINE_SURFACE_WITH_KNOTS((4,4),(3,3),(2.85968127239939E-5,9.24681548475816E-5),
(-0.0016790067878601,1.01130827127821),.UNSPECIFIED.)
GEOMETRIC_REPRESENTATION_ITEM()
RATIONAL_B_SPLINE_SURFACE(((1.00059040895263,0.822187541868038,1.00401468696656),
(1.00036527718168,0.889990093671423,1.00248382673391),(1.00016469515026,
0.950399042257866,1.00111990082511),(1.00025604274013,0.922888044285977,
1.00174104990631)))
REPRESENTATION_ITEM('')
SURFACE()
);
#4027=(
BOUNDED_SURFACE()
B_SPLINE_SURFACE(3,2,((#447909,#447910,#447911),(#447912,#447913,#447914),
(#447915,#447916,#447917),(#447918,#447919,#447920)),.UNSPECIFIED.,.F.,
 .F.,.F.)
B_SPLINE_SURFACE_WITH_KNOTS((4,4),(3,3),(-5.22358356749301E-6,5.74594192424277E-5),
(-0.00127120052063902,1.),.UNSPECIFIED.)
GEOMETRIC_REPRESENTATION_ITEM()
RATIONAL_B_SPLINE_SURFACE(((1.00054449313179,0.785835073638746,1.),(1.00047707767478,
0.812351526358838,1.),(1.00044031788589,0.826810216506265,1.),(1.00044777653322,
0.823876514387241,1.)))
REPRESENTATION_ITEM('')
SURFACE()
);
#4028=(
BOUNDED_SURFACE()
B_SPLINE_SURFACE(3,2,((#447922,#447923,#447924),(#447925,#447926,#447927),
(#447928,#447929,#447930),(#447931,#447932,#447933)),.UNSPECIFIED.,.F.,
 .F.,.F.)
B_SPLINE_SURFACE_WITH_KNOTS((4,4),(3,3),(-2.71050543121376E-20,4.88747512969879E-5),
(-0.000215805215354959,1.),.UNSPECIFIED.)
GEOMETRIC_REPRESENTATION_ITEM()
RATIONAL_B_SPLINE_SURFACE(((1.00008915600333,0.793434085499769,1.),(1.00008930224986,
0.793095246303308,1.),(1.00008944684608,0.792760230720586,1.),(1.00008958984387,
0.792428918540619,1.)))
REPRESENTATION_ITEM('')
SURFACE()
);
#4029=(
BOUNDED_SURFACE()
B_SPLINE_SURFACE(3,2,((#447935,#447936,#447937),(#447938,#447939,#447940),
(#447941,#447942,#447943),(#447944,#447945,#447946),(#447947,#447948,#447949),
(#447950,#447951,#447952)),.UNSPECIFIED.,.F.,.F.,.F.)
B_SPLINE_SURFACE_WITH_KNOTS((4,2,4),(3,3),(4.74338450462408E-20,7.62675010863196E-5,
0.000152535002172639),(0.,1.02152348203074),.UNSPECIFIED.)
GEOMETRIC_REPRESENTATION_ITEM()
RATIONAL_B_SPLINE_SURFACE(((1.,0.78903359540124,1.00908146323694),(1.,0.857071781054833,
1.0061526259043),(1.,0.922087264710719,1.00335390671593),(1.,0.922394466502377,
1.00334068261144),(1.,0.857224384599036,1.00614605678502),(1.,0.789033595401636,
1.00908146323692)))
REPRESENTATION_ITEM('')
SURFACE()
);
#4030=(
BOUNDED_SURFACE()
B_SPLINE_SURFACE(3,2,((#447954,#447955,#447956),(#447957,#447958,#447959),
(#447960,#447961,#447962),(#447963,#447964,#447965)),.UNSPECIFIED.,.F.,
 .F.,.F.)
B_SPLINE_SURFACE_WITH_KNOTS((4,4),(3,3),(-1.0842021724855E-19,4.88747512969881E-5),
(-0.000215489857626116,1.),.UNSPECIFIED.)
GEOMETRIC_REPRESENTATION_ITEM()
RATIONAL_B_SPLINE_SURFACE(((1.00008945889738,0.792428983985623,1.),(1.00008931610859,
0.792760296061174,1.),(1.00008917172372,0.793095311538236,1.),(1.00008902569094,
0.793434150627873,1.)))
REPRESENTATION_ITEM('')
SURFACE()
);
#4031=(
BOUNDED_SURFACE()
B_SPLINE_SURFACE(3,2,((#447967,#447968,#447969),(#447970,#447971,#447972),
(#447973,#447974,#447975),(#447976,#447977,#447978)),.UNSPECIFIED.,.F.,
 .F.,.F.)
B_SPLINE_SURFACE_WITH_KNOTS((4,4),(3,3),(-5.21974905012888E-6,5.7417239551441E-5),
(-0.00139822857724751,1.00051312364062),.UNSPECIFIED.)
GEOMETRIC_REPRESENTATION_ITEM()
RATIONAL_B_SPLINE_SURFACE(((1.00049256947239,0.823768952244076,1.00018060397848),
(1.0004844821571,0.82666242438836,1.0001776387088),(1.00052427784017,0.812424361909453,
1.00019223006919),(1.0005991236585,0.785646094632817,1.00021967280229)))
REPRESENTATION_ITEM('')
SURFACE()
);
#4032=(
BOUNDED_SURFACE()
B_SPLINE_SURFACE(3,2,((#447982,#447983,#447984),(#447985,#447986,#447987),
(#447988,#447989,#447990),(#447991,#447992,#447993)),.UNSPECIFIED.,.F.,
 .F.,.F.)
B_SPLINE_SURFACE_WITH_KNOTS((4,4),(3,3),(3.22980774337779E-5,9.63764854872253E-5),
(-0.00154325936389752,1.01095292447534),.UNSPECIFIED.)
GEOMETRIC_REPRESENTATION_ITEM()
RATIONAL_B_SPLINE_SURFACE(((1.00023530983301,0.922925743796159,1.0016857472833),
(1.00015136166127,0.950422439594206,1.00108434699059),(1.00033574337402,
0.890029368953955,1.00240524789546),(1.00054260094227,0.822274473168315,
1.00388716464855)))
REPRESENTATION_ITEM('')
SURFACE()
);
#4033=(
BOUNDED_SURFACE()
B_SPLINE_SURFACE(3,2,((#448093,#448094,#448095),(#448096,#448097,#448098),
(#448099,#448100,#448101),(#448102,#448103,#448104)),.UNSPECIFIED.,.F.,
 .F.,.F.)
B_SPLINE_SURFACE_WITH_KNOTS((4,4),(3,3),(-2.16840434497101E-19,0.000101260117256738),
(0.,1.),.UNSPECIFIED.)
GEOMETRIC_REPRESENTATION_ITEM()
RATIONAL_B_SPLINE_SURFACE(((1.,0.796615278835172,1.),(1.,0.79589603805594,
1.),(1.,0.79519335466135,1.),(1.,0.794506193185548,1.)))
REPRESENTATION_ITEM('')
SURFACE()
);
#4034=(
BOUNDED_SURFACE()
B_SPLINE_SURFACE(3,2,((#448142,#448143,#448144),(#448145,#448146,#448147),
(#448148,#448149,#448150),(#448151,#448152,#448153),(#448154,#448155,#448156),
(#448157,#448158,#448159)),.UNSPECIFIED.,.F.,.F.,.F.)
B_SPLINE_SURFACE_WITH_KNOTS((4,2,4),(3,3),(-8.63973606199386E-20,1.66936432462294E-5,
3.33872864924588E-5),(0.,1.),.UNSPECIFIED.)
GEOMETRIC_REPRESENTATION_ITEM()
RATIONAL_B_SPLINE_SURFACE(((1.,0.796615278835177,1.),(1.,0.862310524418125,
1.),(1.,0.923774472010521,1.),(1.,0.923983993203424,1.),(1.,0.86257487372095,
1.),(1.,0.796615278835179,1.)))
REPRESENTATION_ITEM('')
SURFACE()
);
#4035=(
BOUNDED_SURFACE()
B_SPLINE_SURFACE(3,2,((#448196,#448197,#448198),(#448199,#448200,#448201),
(#448202,#448203,#448204),(#448205,#448206,#448207)),.UNSPECIFIED.,.F.,
 .F.,.F.)
B_SPLINE_SURFACE_WITH_KNOTS((4,4),(3,3),(-2.16840434497101E-19,0.000101244905251112),
(0.,1.),.UNSPECIFIED.)
GEOMETRIC_REPRESENTATION_ITEM()
RATIONAL_B_SPLINE_SURFACE(((1.,0.796615278835169,1.),(1.,0.795896146109794,
1.),(1.,0.795193565796499,1.),(1.,0.794506502889899,1.)))
REPRESENTATION_ITEM('')
SURFACE()
);
#4036=(
BOUNDED_SURFACE()
B_SPLINE_SURFACE(3,2,((#448243,#448244,#448245),(#448246,#448247,#448248),
(#448249,#448250,#448251),(#448252,#448253,#448254)),.UNSPECIFIED.,.F.,
 .F.,.F.)
B_SPLINE_SURFACE_WITH_KNOTS((4,4),(3,3),(2.85968127239939E-5,9.24681548475818E-5),
(-0.00167900678733353,1.01130827127828),.UNSPECIFIED.)
GEOMETRIC_REPRESENTATION_ITEM()
RATIONAL_B_SPLINE_SURFACE(((1.00059040895245,0.82218754186812,1.00401468696659),
(1.00036527718157,0.889990093671481,1.00248382673392),(1.00016469515021,
0.950399042257883,1.00111990082511),(1.00025604274004,0.922888044286016,
1.00174104990632)))
REPRESENTATION_ITEM('')
SURFACE()
);
#4037=(
BOUNDED_SURFACE()
B_SPLINE_SURFACE(3,2,((#448258,#448259,#448260),(#448261,#448262,#448263),
(#448264,#448265,#448266),(#448267,#448268,#448269)),.UNSPECIFIED.,.F.,
 .F.,.F.)
B_SPLINE_SURFACE_WITH_KNOTS((4,4),(3,3),(-5.22358356749328E-6,5.74594192424278E-5),
(-0.00127120052054192,1.),.UNSPECIFIED.)
GEOMETRIC_REPRESENTATION_ITEM()
RATIONAL_B_SPLINE_SURFACE(((1.00054449313174,0.785835073638759,1.),(1.00047707767474,
0.812351526358873,1.),(1.00044031788586,0.826810216506272,1.),(1.00044777653318,
0.823876514387262,1.)))
REPRESENTATION_ITEM('')
SURFACE()
);
#4038=(
BOUNDED_SURFACE()
B_SPLINE_SURFACE(3,2,((#448271,#448272,#448273),(#448274,#448275,#448276),
(#448277,#448278,#448279),(#448280,#448281,#448282)),.UNSPECIFIED.,.F.,
 .F.,.F.)
B_SPLINE_SURFACE_WITH_KNOTS((4,4),(3,3),(1.89735380184963E-19,4.88747512969881E-5),
(-0.000215805215098437,1.),.UNSPECIFIED.)
GEOMETRIC_REPRESENTATION_ITEM()
RATIONAL_B_SPLINE_SURFACE(((1.00008915600322,0.793434085499826,1.),(1.00008930224975,
0.793095246303361,1.),(1.00008944684597,0.792760230720644,1.),(1.00008958984376,
0.792428918540672,1.)))
REPRESENTATION_ITEM('')
SURFACE()
);
#4039=(
BOUNDED_SURFACE()
B_SPLINE_SURFACE(3,2,((#448284,#448285,#448286),(#448287,#448288,#448289),
(#448290,#448291,#448292),(#448293,#448294,#448295),(#448296,#448297,#448298),
(#448299,#448300,#448301)),.UNSPECIFIED.,.F.,.F.,.F.)
B_SPLINE_SURFACE_WITH_KNOTS((4,2,4),(3,3),(3.65918233213858E-19,7.626750108632E-5,
0.00015253500217264),(0.,1.0215234820306),.UNSPECIFIED.)
GEOMETRIC_REPRESENTATION_ITEM()
RATIONAL_B_SPLINE_SURFACE(((1.,0.789033595401266,1.00908146323688),(1.,
0.857071781054849,1.00615262590426),(1.,0.922087264710724,1.00335390671591),
(1.,0.922394466502391,1.00334068261142),(1.,0.857224384599052,1.00614605678498),
(1.,0.789033595401665,1.00908146323687)))
REPRESENTATION_ITEM('')
SURFACE()
);
#4040=(
BOUNDED_SURFACE()
B_SPLINE_SURFACE(3,2,((#448303,#448304,#448305),(#448306,#448307,#448308),
(#448309,#448310,#448311),(#448312,#448313,#448314)),.UNSPECIFIED.,.F.,
 .F.,.F.)
B_SPLINE_SURFACE_WITH_KNOTS((4,4),(3,3),(3.52365706057789E-19,4.88747512969885E-5),
(-0.000215489857907747,1.),.UNSPECIFIED.)
GEOMETRIC_REPRESENTATION_ITEM()
RATIONAL_B_SPLINE_SURFACE(((1.00008945889749,0.792428983985561,1.),(1.00008931610871,
0.792760296061118,1.),(1.00008917172383,0.793095311538185,1.),(1.00008902569106,
0.793434150627815,1.)))
REPRESENTATION_ITEM('')
SURFACE()
);
#4041=(
BOUNDED_SURFACE()
B_SPLINE_SURFACE(3,2,((#448316,#448317,#448318),(#448319,#448320,#448321),
(#448322,#448323,#448324),(#448325,#448326,#448327)),.UNSPECIFIED.,.F.,
 .F.,.F.)
B_SPLINE_SURFACE_WITH_KNOTS((4,4),(3,3),(-5.219749050131E-6,5.74172395514409E-5),
(-0.00139822857747908,1.00051312364054),.UNSPECIFIED.)
GEOMETRIC_REPRESENTATION_ITEM()
RATIONAL_B_SPLINE_SURFACE(((1.00049256947247,0.823768952244047,1.00018060397845),
(1.00048448215718,0.826662424388334,1.00017763870878),(1.00052427784026,
0.812424361909417,1.00019223006916),(1.0005991236586,0.785646094632787,
1.00021967280225)))
REPRESENTATION_ITEM('')
SURFACE()
);
#4042=(
BOUNDED_SURFACE()
B_SPLINE_SURFACE(3,2,((#448331,#448332,#448333),(#448334,#448335,#448336),
(#448337,#448338,#448339),(#448340,#448341,#448342)),.UNSPECIFIED.,.F.,
 .F.,.F.)
B_SPLINE_SURFACE_WITH_KNOTS((4,4),(3,3),(3.22980774337781E-5,9.63764854872256E-5),
(-0.00154325936487747,1.01095292447528),.UNSPECIFIED.)
GEOMETRIC_REPRESENTATION_ITEM()
RATIONAL_B_SPLINE_SURFACE(((1.00023530983316,0.92292574379609,1.00168574728329),
(1.00015136166137,0.950422439594164,1.00108434699058),(1.00033574337423,
0.890029368953841,1.00240524789544),(1.00054260094262,0.822274473168158,
1.00388716464853)))
REPRESENTATION_ITEM('')
SURFACE()
);
#4043=(
BOUNDED_SURFACE()
B_SPLINE_SURFACE(3,2,((#448442,#448443,#448444),(#448445,#448446,#448447),
(#448448,#448449,#448450),(#448451,#448452,#448453)),.UNSPECIFIED.,.F.,
 .F.,.F.)
B_SPLINE_SURFACE_WITH_KNOTS((4,4),(3,3),(0.,0.000101260117256738),(0.,1.),
 .UNSPECIFIED.)
GEOMETRIC_REPRESENTATION_ITEM()
RATIONAL_B_SPLINE_SURFACE(((1.,0.796615278835173,1.),(1.,0.795896038055939,
1.),(1.,0.795193354661348,1.),(1.,0.794506193185548,1.)))
REPRESENTATION_ITEM('')
SURFACE()
);
#4044=(
BOUNDED_SURFACE()
B_SPLINE_SURFACE(3,2,((#448491,#448492,#448493),(#448494,#448495,#448496),
(#448497,#448498,#448499),(#448500,#448501,#448502),(#448503,#448504,#448505),
(#448506,#448507,#448508)),.UNSPECIFIED.,.F.,.F.,.F.)
B_SPLINE_SURFACE_WITH_KNOTS((4,2,4),(3,3),(-1.10114283143059E-19,1.66936432462296E-5,
3.33872864924593E-5),(0.,1.),.UNSPECIFIED.)
GEOMETRIC_REPRESENTATION_ITEM()
RATIONAL_B_SPLINE_SURFACE(((1.,0.796615278835173,1.),(1.,0.862310524418128,
1.),(1.,0.923774472010522,1.),(1.,0.923983993203426,1.),(1.,0.862574873720947,
1.),(1.,0.796615278835177,1.)))
REPRESENTATION_ITEM('')
SURFACE()
);
#4045=(
BOUNDED_SURFACE()
B_SPLINE_SURFACE(3,2,((#448545,#448546,#448547),(#448548,#448549,#448550),
(#448551,#448552,#448553),(#448554,#448555,#448556)),.UNSPECIFIED.,.F.,
 .F.,.F.)
B_SPLINE_SURFACE_WITH_KNOTS((4,4),(3,3),(0.,0.000101244905251112),(0.,1.),
 .UNSPECIFIED.)
GEOMETRIC_REPRESENTATION_ITEM()
RATIONAL_B_SPLINE_SURFACE(((1.,0.796615278835173,1.),(1.,0.795896146109793,
1.),(1.,0.795193565796502,1.),(1.,0.794506502889902,1.)))
REPRESENTATION_ITEM('')
SURFACE()
);
#4046=(
BOUNDED_SURFACE()
B_SPLINE_SURFACE(3,2,((#448592,#448593,#448594),(#448595,#448596,#448597),
(#448598,#448599,#448600),(#448601,#448602,#448603)),.UNSPECIFIED.,.F.,
 .F.,.F.)
B_SPLINE_SURFACE_WITH_KNOTS((4,4),(3,3),(2.85968127239938E-5,9.24681548475818E-5),
(-0.00167900678711253,1.01130827127809),.UNSPECIFIED.)
GEOMETRIC_REPRESENTATION_ITEM()
RATIONAL_B_SPLINE_SURFACE(((1.00059040895237,0.822187541868192,1.00401468696652),
(1.00036527718152,0.889990093671527,1.00248382673388),(1.00016469515019,
0.950399042257907,1.00111990082509),(1.00025604274001,0.922888044286047,
1.00174104990629)))
REPRESENTATION_ITEM('')
SURFACE()
);
#4047=(
BOUNDED_SURFACE()
B_SPLINE_SURFACE(3,2,((#448607,#448608,#448609),(#448610,#448611,#448612),
(#448613,#448614,#448615),(#448616,#448617,#448618)),.UNSPECIFIED.,.F.,
 .F.,.F.)
B_SPLINE_SURFACE_WITH_KNOTS((4,4),(3,3),(-5.22358356749311E-6,5.74594192424278E-5),
(-0.00127120052062198,1.),.UNSPECIFIED.)
GEOMETRIC_REPRESENTATION_ITEM()
RATIONAL_B_SPLINE_SURFACE(((1.00054449313178,0.785835073638755,1.),(1.00047707767477,
0.812351526358825,1.),(1.00044031788589,0.826810216506286,1.),(1.00044777653321,
0.82387651438724,1.)))
REPRESENTATION_ITEM('')
SURFACE()
);
#4048=(
BOUNDED_SURFACE()
B_SPLINE_SURFACE(3,2,((#448620,#448621,#448622),(#448623,#448624,#448625),
(#448626,#448627,#448628),(#448629,#448630,#448631)),.UNSPECIFIED.,.F.,
 .F.,.F.)
B_SPLINE_SURFACE_WITH_KNOTS((4,4),(3,3),(-1.89735380184963E-19,4.88747512969879E-5),
(-0.000215805215091942,1.),.UNSPECIFIED.)
GEOMETRIC_REPRESENTATION_ITEM()
RATIONAL_B_SPLINE_SURFACE(((1.00008915600322,0.793434085499825,1.),(1.00008930224975,
0.793095246303367,1.),(1.00008944684597,0.79276023072064,1.),(1.00008958984376,
0.792428918540676,1.)))
REPRESENTATION_ITEM('')
SURFACE()
);
#4049=(
BOUNDED_SURFACE()
B_SPLINE_SURFACE(3,2,((#448633,#448634,#448635),(#448636,#448637,#448638),
(#448639,#448640,#448641),(#448642,#448643,#448644),(#448645,#448646,#448647),
(#448648,#448649,#448650)),.UNSPECIFIED.,.F.,.F.,.F.)
B_SPLINE_SURFACE_WITH_KNOTS((4,2,4),(3,3),(3.3881317890172E-20,7.62675010863199E-5,
0.00015253500217264),(0.,1.02152348203045),.UNSPECIFIED.)
GEOMETRIC_REPRESENTATION_ITEM()
RATIONAL_B_SPLINE_SURFACE(((1.,0.789033595401298,1.00908146323682),(1.,
0.857071781054873,1.00615262590422),(1.,0.922087264710742,1.00335390671588),
(1.,0.922394466502397,1.0033406826114),(1.,0.857224384599075,1.00614605678494),
(1.,0.789033595401696,1.0090814632368)))
REPRESENTATION_ITEM('')
SURFACE()
);
#4050=(
BOUNDED_SURFACE()
B_SPLINE_SURFACE(3,2,((#448652,#448653,#448654),(#448655,#448656,#448657),
(#448658,#448659,#448660),(#448661,#448662,#448663)),.UNSPECIFIED.,.F.,
 .F.,.F.)
B_SPLINE_SURFACE_WITH_KNOTS((4,4),(3,3),(3.79470760369927E-19,4.88747512969883E-5),
(-0.000215489857081522,1.),.UNSPECIFIED.)
GEOMETRIC_REPRESENTATION_ITEM()
RATIONAL_B_SPLINE_SURFACE(((1.00008945889715,0.792428983985735,1.),(1.00008931610837,
0.792760296061283,1.),(1.00008917172349,0.793095311538361,1.),(1.00008902569072,
0.793434150627989,1.)))
REPRESENTATION_ITEM('')
SURFACE()
);
#4051=(
BOUNDED_SURFACE()
B_SPLINE_SURFACE(3,2,((#448665,#448666,#448667),(#448668,#448669,#448670),
(#448671,#448672,#448673),(#448674,#448675,#448676)),.UNSPECIFIED.,.F.,
 .F.,.F.)
B_SPLINE_SURFACE_WITH_KNOTS((4,4),(3,3),(-5.21974905013089E-6,5.74172395514398E-5),
(-0.00139822857803481,1.00051312364081),.UNSPECIFIED.)
GEOMETRIC_REPRESENTATION_ITEM()
RATIONAL_B_SPLINE_SURFACE(((1.00049256947267,0.823768952243903,1.00018060397854),
(1.00048448215737,0.826662424388194,1.00017763870887),(1.00052427784046,
0.812424361909265,1.00019223006927),(1.00059912365883,0.785646094632609,
1.00021967280237)))
REPRESENTATION_ITEM('')
SURFACE()
);
#4052=(
BOUNDED_SURFACE()
B_SPLINE_SURFACE(3,2,((#448680,#448681,#448682),(#448683,#448684,#448685),
(#448686,#448687,#448688),(#448689,#448690,#448691)),.UNSPECIFIED.,.F.,
 .F.,.F.)
B_SPLINE_SURFACE_WITH_KNOTS((4,4),(3,3),(3.22980774337777E-5,9.6376485487225E-5),
(-0.00154325936392724,1.01095292447545),.UNSPECIFIED.)
GEOMETRIC_REPRESENTATION_ITEM()
RATIONAL_B_SPLINE_SURFACE(((1.00023530983302,0.922925743796147,1.00168574728331),
(1.00015136166127,0.950422439594206,1.0010843469906),(1.00033574337403,
0.890029368953936,1.00240524789548),(1.00054260094228,0.822274473168295,
1.00388716464859)))
REPRESENTATION_ITEM('')
SURFACE()
);
#4053=(
BOUNDED_SURFACE()
B_SPLINE_SURFACE(3,2,((#448791,#448792,#448793),(#448794,#448795,#448796),
(#448797,#448798,#448799),(#448800,#448801,#448802)),.UNSPECIFIED.,.F.,
 .F.,.F.)
B_SPLINE_SURFACE_WITH_KNOTS((4,4),(3,3),(0.,0.000101260117256738),(0.,1.),
 .UNSPECIFIED.)
GEOMETRIC_REPRESENTATION_ITEM()
RATIONAL_B_SPLINE_SURFACE(((1.,0.79661527883517,1.),(1.,0.795896038055943,
1.),(1.,0.795193354661348,1.),(1.,0.794506193185545,1.)))
REPRESENTATION_ITEM('')
SURFACE()
);
#4054=(
BOUNDED_SURFACE()
B_SPLINE_SURFACE(3,2,((#448840,#448841,#448842),(#448843,#448844,#448845),
(#448846,#448847,#448848),(#448849,#448850,#448851),(#448852,#448853,#448854),
(#448855,#448856,#448857)),.UNSPECIFIED.,.F.,.F.,.F.)
B_SPLINE_SURFACE_WITH_KNOTS((4,2,4),(3,3),(1.42301535138722E-19,1.66936432462299E-5,
3.33872864924596E-5),(0.,1.),.UNSPECIFIED.)
GEOMETRIC_REPRESENTATION_ITEM()
RATIONAL_B_SPLINE_SURFACE(((1.,0.796615278835174,1.),(1.,0.862310524418123,
1.),(1.,0.923774472010524,1.),(1.,0.923983993203422,1.),(1.,0.86257487372094,
1.),(1.,0.796615278835185,1.)))
REPRESENTATION_ITEM('')
SURFACE()
);
#4055=(
BOUNDED_SURFACE()
B_SPLINE_SURFACE(3,2,((#448894,#448895,#448896),(#448897,#448898,#448899),
(#448900,#448901,#448902),(#448903,#448904,#448905)),.UNSPECIFIED.,.F.,
 .F.,.F.)
B_SPLINE_SURFACE_WITH_KNOTS((4,4),(3,3),(-2.16840434497101E-19,0.000101244905251112),
(0.,1.),.UNSPECIFIED.)
GEOMETRIC_REPRESENTATION_ITEM()
RATIONAL_B_SPLINE_SURFACE(((1.,0.79661527883517,1.),(1.,0.795896146109792,
1.),(1.,0.795193565796506,1.),(1.,0.794506502889899,1.)))
REPRESENTATION_ITEM('')
SURFACE()
);
#4056=(
BOUNDED_SURFACE()
B_SPLINE_SURFACE(3,2,((#448941,#448942,#448943),(#448944,#448945,#448946),
(#448947,#448948,#448949),(#448950,#448951,#448952)),.UNSPECIFIED.,.F.,
 .F.,.F.)
B_SPLINE_SURFACE_WITH_KNOTS((4,4),(3,3),(2.85968127239939E-5,9.24681548475821E-5),
(-0.00167900678649206,1.01130827127841),.UNSPECIFIED.)
GEOMETRIC_REPRESENTATION_ITEM()
RATIONAL_B_SPLINE_SURFACE(((1.00059040895215,0.822187541868248,1.00401468696663),
(1.00036527718138,0.889990093671552,1.00248382673395),(1.00016469515012,
0.950399042257925,1.00111990082513),(1.00025604273992,0.922888044286069,
1.00174104990634)))
REPRESENTATION_ITEM('')
SURFACE()
);
#4057=(
BOUNDED_SURFACE()
B_SPLINE_SURFACE(3,2,((#448956,#448957,#448958),(#448959,#448960,#448961),
(#448962,#448963,#448964),(#448965,#448966,#448967)),.UNSPECIFIED.,.F.,
 .F.,.F.)
B_SPLINE_SURFACE_WITH_KNOTS((4,4),(3,3),(-5.22358356749231E-6,5.74594192424277E-5),
(-0.00127120052066043,1.),.UNSPECIFIED.)
GEOMETRIC_REPRESENTATION_ITEM()
RATIONAL_B_SPLINE_SURFACE(((1.0005444931318,0.785835073638737,1.),(1.00047707767479,
0.812351526358842,1.),(1.0004403178859,0.82681021650626,1.),(1.00044777653322,
0.82387651438724,1.)))
REPRESENTATION_ITEM('')
SURFACE()
);
#4058=(
BOUNDED_SURFACE()
B_SPLINE_SURFACE(3,2,((#448969,#448970,#448971),(#448972,#448973,#448974),
(#448975,#448976,#448977),(#448978,#448979,#448980)),.UNSPECIFIED.,.F.,
 .F.,.F.)
B_SPLINE_SURFACE_WITH_KNOTS((4,4),(3,3),(-1.0842021724855E-19,4.88747512969881E-5),
(-0.000215805215184123,1.),.UNSPECIFIED.)
GEOMETRIC_REPRESENTATION_ITEM()
RATIONAL_B_SPLINE_SURFACE(((1.00008915600326,0.793434085499805,1.),(1.00008930224979,
0.79309524630336,1.),(1.00008944684601,0.792760230720614,1.),(1.0000895898438,
0.792428918540653,1.)))
REPRESENTATION_ITEM('')
SURFACE()
);
#4059=(
BOUNDED_SURFACE()
B_SPLINE_SURFACE(3,2,((#448982,#448983,#448984),(#448985,#448986,#448987),
(#448988,#448989,#448990),(#448991,#448992,#448993),(#448994,#448995,#448996),
(#448997,#448998,#448999)),.UNSPECIFIED.,.F.,.F.,.F.)
B_SPLINE_SURFACE_WITH_KNOTS((4,2,4),(3,3),(6.09863722023096E-20,7.62675010863199E-5,
0.00015253500217264),(0.,1.02152348203022),.UNSPECIFIED.)
GEOMETRIC_REPRESENTATION_ITEM()
RATIONAL_B_SPLINE_SURFACE(((1.,0.789033595401343,1.00908146323672),(1.,
0.857071781054904,1.00615262590415),(1.,0.922087264710765,1.00335390671585),
(1.,0.922394466502406,1.00334068261136),(1.,0.857224384599113,1.00614605678487),
(1.,0.789033595401744,1.0090814632367)))
REPRESENTATION_ITEM('')
SURFACE()
);
#4060=(
BOUNDED_SURFACE()
B_SPLINE_SURFACE(3,2,((#449001,#449002,#449003),(#449004,#449005,#449006),
(#449007,#449008,#449009),(#449010,#449011,#449012)),.UNSPECIFIED.,.F.,
 .F.,.F.)
B_SPLINE_SURFACE_WITH_KNOTS((4,4),(3,3),(1.0842021724855E-19,4.88747512969882E-5),
(-0.0002154898570242,1.),.UNSPECIFIED.)
GEOMETRIC_REPRESENTATION_ITEM()
RATIONAL_B_SPLINE_SURFACE(((1.00008945889713,0.792428983985745,1.),(1.00008931610834,
0.792760296061291,1.),(1.00008917172347,0.793095311538371,1.),(1.00008902569069,
0.793434150627998,1.)))
REPRESENTATION_ITEM('')
SURFACE()
);
#4061=(
BOUNDED_SURFACE()
B_SPLINE_SURFACE(3,2,((#449014,#449015,#449016),(#449017,#449018,#449019),
(#449020,#449021,#449022),(#449023,#449024,#449025)),.UNSPECIFIED.,.F.,
 .F.,.F.)
B_SPLINE_SURFACE_WITH_KNOTS((4,4),(3,3),(-5.21974905013085E-6,5.74172395514398E-5),
(-0.00139822857777821,1.00051312364075),.UNSPECIFIED.)
GEOMETRIC_REPRESENTATION_ITEM()
RATIONAL_B_SPLINE_SURFACE(((1.00049256947258,0.823768952243957,1.00018060397852),
(1.00048448215728,0.826662424388249,1.00017763870885),(1.00052427784037,
0.812424361909315,1.00019223006924),(1.00059912365872,0.785646094632677,
1.00021967280235)))
REPRESENTATION_ITEM('')
SURFACE()
);
#4062=(
BOUNDED_SURFACE()
B_SPLINE_SURFACE(3,2,((#449029,#449030,#449031),(#449032,#449033,#449034),
(#449035,#449036,#449037),(#449038,#449039,#449040)),.UNSPECIFIED.,.F.,
 .F.,.F.)
B_SPLINE_SURFACE_WITH_KNOTS((4,4),(3,3),(3.22980774337779E-5,9.63764854872257E-5),
(-0.00154325936360782,1.01095292447527),.UNSPECIFIED.)
GEOMETRIC_REPRESENTATION_ITEM()
RATIONAL_B_SPLINE_SURFACE(((1.00023530983297,0.922925743796185,1.00168574728329),
(1.00015136166124,0.950422439594226,1.00108434699058),(1.00033574337396,
0.890029368953995,1.00240524789544),(1.00054260094217,0.822274473168382,
1.00388716464852)))
REPRESENTATION_ITEM('')
SURFACE()
);
#4063=(
BOUNDED_SURFACE()
B_SPLINE_SURFACE(3,2,((#449140,#449141,#449142),(#449143,#449144,#449145),
(#449146,#449147,#449148),(#449149,#449150,#449151)),.UNSPECIFIED.,.F.,
 .F.,.F.)
B_SPLINE_SURFACE_WITH_KNOTS((4,4),(3,3),(0.,0.000101260117256737),(0.,1.),
 .UNSPECIFIED.)
GEOMETRIC_REPRESENTATION_ITEM()
RATIONAL_B_SPLINE_SURFACE(((1.,0.79661527883517,1.),(1.,0.795896038055935,
1.),(1.,0.79519335466136,1.),(1.,0.794506193185533,1.)))
REPRESENTATION_ITEM('')
SURFACE()
);
#4064=(
BOUNDED_SURFACE()
B_SPLINE_SURFACE(3,2,((#449189,#449190,#449191),(#449192,#449193,#449194),
(#449195,#449196,#449197),(#449198,#449199,#449200),(#449201,#449202,#449203),
(#449204,#449205,#449206)),.UNSPECIFIED.,.F.,.F.,.F.)
B_SPLINE_SURFACE_WITH_KNOTS((4,2,4),(3,3),(1.55854062294791E-19,1.66936432462294E-5,
3.33872864924587E-5),(0.,1.),.UNSPECIFIED.)
GEOMETRIC_REPRESENTATION_ITEM()
RATIONAL_B_SPLINE_SURFACE(((1.,0.796615278835177,1.),(1.,0.862310524418132,
1.),(1.,0.923774472010521,1.),(1.,0.923983993203426,1.),(1.,0.862574873720942,
1.),(1.,0.796615278835183,1.)))
REPRESENTATION_ITEM('')
SURFACE()
);
#4065=(
BOUNDED_SURFACE()
B_SPLINE_SURFACE(3,2,((#449243,#449244,#449245),(#449246,#449247,#449248),
(#449249,#449250,#449251),(#449252,#449253,#449254)),.UNSPECIFIED.,.F.,
 .F.,.F.)
B_SPLINE_SURFACE_WITH_KNOTS((4,4),(3,3),(0.,0.000101244905251112),(0.,1.),
 .UNSPECIFIED.)
GEOMETRIC_REPRESENTATION_ITEM()
RATIONAL_B_SPLINE_SURFACE(((1.,0.796615278835169,1.),(1.,0.795896146109794,
1.),(1.,0.795193565796497,1.),(1.,0.794506502889899,1.)))
REPRESENTATION_ITEM('')
SURFACE()
);
#4066=(
BOUNDED_SURFACE()
B_SPLINE_SURFACE(3,2,((#449290,#449291,#449292),(#449293,#449294,#449295),
(#449296,#449297,#449298),(#449299,#449300,#449301)),.UNSPECIFIED.,.F.,
 .F.,.F.)
B_SPLINE_SURFACE_WITH_KNOTS((4,4),(3,3),(2.85968127239938E-5,9.24681548475816E-5),
(-0.00167900678746727,1.01130827127807),.UNSPECIFIED.)
GEOMETRIC_REPRESENTATION_ITEM()
RATIONAL_B_SPLINE_SURFACE(((1.00059040895249,0.822187541868134,1.00401468696651),
(1.0003652771816,0.889990093671489,1.00248382673388),(1.00016469515022,
0.950399042257892,1.00111990082509),(1.00025604274006,0.92288804428602,
1.00174104990629)))
REPRESENTATION_ITEM('')
SURFACE()
);
#4067=(
BOUNDED_SURFACE()
B_SPLINE_SURFACE(3,2,((#449305,#449306,#449307),(#449308,#449309,#449310),
(#449311,#449312,#449313),(#449314,#449315,#449316)),.UNSPECIFIED.,.F.,
 .F.,.F.)
B_SPLINE_SURFACE_WITH_KNOTS((4,4),(3,3),(-5.22358356749317E-6,5.74594192424277E-5),
(-0.00127120052063584,1.),.UNSPECIFIED.)
GEOMETRIC_REPRESENTATION_ITEM()
RATIONAL_B_SPLINE_SURFACE(((1.00054449313178,0.785835073638741,1.),(1.00047707767478,
0.812351526358851,1.),(1.00044031788589,0.826810216506262,1.),(1.00044777653321,
0.823876514387244,1.)))
REPRESENTATION_ITEM('')
SURFACE()
);
#4068=(
BOUNDED_SURFACE()
B_SPLINE_SURFACE(3,2,((#449318,#449319,#449320),(#449321,#449322,#449323),
(#449324,#449325,#449326),(#449327,#449328,#449329)),.UNSPECIFIED.,.F.,
 .F.,.F.)
B_SPLINE_SURFACE_WITH_KNOTS((4,4),(3,3),(-8.13151629364128E-20,4.8874751296988E-5),
(-0.00021580521548104,1.),.UNSPECIFIED.)
GEOMETRIC_REPRESENTATION_ITEM()
RATIONAL_B_SPLINE_SURFACE(((1.00008915600338,0.793434085499746,1.),(1.00008930224991,
0.793095246303297,1.),(1.00008944684613,0.792760230720554,1.),(1.00008958984392,
0.792428918540594,1.)))
REPRESENTATION_ITEM('')
SURFACE()
);
#4069=(
BOUNDED_SURFACE()
B_SPLINE_SURFACE(3,2,((#449331,#449332,#449333),(#449334,#449335,#449336),
(#449337,#449338,#449339),(#449340,#449341,#449342),(#449343,#449344,#449345),
(#449346,#449347,#449348)),.UNSPECIFIED.,.F.,.F.,.F.)
B_SPLINE_SURFACE_WITH_KNOTS((4,2,4),(3,3),(-1.0842021724855E-19,7.62675010863192E-5,
0.000152535002172638),(0.,1.02152348203042),.UNSPECIFIED.)
GEOMETRIC_REPRESENTATION_ITEM()
RATIONAL_B_SPLINE_SURFACE(((1.,0.789033595401302,1.0090814632368),(1.,0.857071781054877,
1.00615262590421),(1.,0.922087264710747,1.00335390671588),(1.,0.922394466502397,
1.00334068261139),(1.,0.857224384599085,1.00614605678493),(1.,0.789033595401703,
1.00908146323679)))
REPRESENTATION_ITEM('')
SURFACE()
);
#4070=(
BOUNDED_SURFACE()
B_SPLINE_SURFACE(3,2,((#449350,#449351,#449352),(#449353,#449354,#449355),
(#449356,#449357,#449358),(#449359,#449360,#449361)),.UNSPECIFIED.,.F.,
 .F.,.F.)
B_SPLINE_SURFACE_WITH_KNOTS((4,4),(3,3),(1.62630325872826E-19,4.88747512969882E-5),
(-0.000215489857674331,1.),.UNSPECIFIED.)
GEOMETRIC_REPRESENTATION_ITEM()
RATIONAL_B_SPLINE_SURFACE(((1.0000894588974,0.792428983985611,1.),(1.00008931610861,
0.792760296061153,1.),(1.00008917172374,0.793095311538236,1.),(1.00008902569096,
0.793434150627863,1.)))
REPRESENTATION_ITEM('')
SURFACE()
);
#4071=(
BOUNDED_SURFACE()
B_SPLINE_SURFACE(3,2,((#449363,#449364,#449365),(#449366,#449367,#449368),
(#449369,#449370,#449371),(#449372,#449373,#449374)),.UNSPECIFIED.,.F.,
 .F.,.F.)
B_SPLINE_SURFACE_WITH_KNOTS((4,4),(3,3),(-5.21974905013085E-6,5.74172395514395E-5),
(-0.00139822857732513,1.00051312364061),.UNSPECIFIED.)
GEOMETRIC_REPRESENTATION_ITEM()
RATIONAL_B_SPLINE_SURFACE(((1.00049256947242,0.82376895224406,1.00018060397847),
(1.00048448215713,0.82666242438835,1.0001776387088),(1.0005242778402,0.812424361909424,
1.00019223006919),(1.00059912365853,0.785646094632805,1.00021967280229)))
REPRESENTATION_ITEM('')
SURFACE()
);
#4072=(
BOUNDED_SURFACE()
B_SPLINE_SURFACE(3,2,((#449378,#449379,#449380),(#449381,#449382,#449383),
(#449384,#449385,#449386),(#449387,#449388,#449389)),.UNSPECIFIED.,.F.,
 .F.,.F.)
B_SPLINE_SURFACE_WITH_KNOTS((4,4),(3,3),(3.22980774337778E-5,9.6376485487225E-5),
(-0.00154325936394921,1.01095292447551),.UNSPECIFIED.)
GEOMETRIC_REPRESENTATION_ITEM()
RATIONAL_B_SPLINE_SURFACE(((1.00023530983302,0.92292574379614,1.00168574728332),
(1.00015136166128,0.950422439594194,1.00108434699061),(1.00033574337403,
0.890029368953931,1.00240524789549),(1.00054260094229,0.822274473168285,
1.00388716464861)))
REPRESENTATION_ITEM('')
SURFACE()
);
#4326=(
BOUNDED_CURVE()
B_SPLINE_CURVE(2,(#409628,#409629,#409630),.UNSPECIFIED.,.F.,.F.)
B_SPLINE_CURVE_WITH_KNOTS((3,3),(0.00739537155986661,0.00980392156862745),
 .UNSPECIFIED.)
CURVE()
GEOMETRIC_REPRESENTATION_ITEM()
RATIONAL_B_SPLINE_CURVE((0.948065210722634,0.901258538444052,1.))
REPRESENTATION_ITEM('')
);
#4327=(
BOUNDED_CURVE()
B_SPLINE_CURVE(2,(#409636,#409637,#409638,#409639,#409640,#409641,#409642,
#409643,#409644,#409645,#409646,#409647,#409648),.UNSPECIFIED.,.F.,.F.)
B_SPLINE_CURVE_WITH_KNOTS((3,2,2,2,2,2,3),(0.00980392156862745,0.0130718954248366,
0.0163398692810458,0.0196078431372549,0.0228758169934641,0.0261437908496732,
0.0294117647058824),.UNSPECIFIED.)
CURVE()
GEOMETRIC_REPRESENTATION_ITEM()
RATIONAL_B_SPLINE_CURVE((1.,0.866025403784439,1.,0.866025403784439,1.,0.866025403784439,
1.,0.866025403784439,1.,0.866025403784439,1.,0.866025403784439,1.))
REPRESENTATION_ITEM('')
);
#4328=(
BOUNDED_CURVE()
B_SPLINE_CURVE(2,(#409649,#409650,#409651,#409652,#409653,#409654,#409655,
#409656,#409657,#409658,#409659,#409660,#409661),.UNSPECIFIED.,.F.,.F.)
B_SPLINE_CURVE_WITH_KNOTS((3,2,2,2,2,2,3),(0.00980392156862746,0.0130718954248366,
0.0163398692810458,0.0196078431372549,0.0228758169934641,0.0261437908496732,
0.0294117647058824),.UNSPECIFIED.)
CURVE()
GEOMETRIC_REPRESENTATION_ITEM()
RATIONAL_B_SPLINE_CURVE((1.,0.866025403784439,1.,0.866025403784439,1.,0.866025403784439,
1.,0.866025403784439,1.,0.866025403784439,1.,0.866025403784439,1.))
REPRESENTATION_ITEM('')
);
#4329=(
BOUNDED_CURVE()
B_SPLINE_CURVE(2,(#409666,#409667,#409668,#409669,#409670,#409671,#409672,
#409673,#409674,#409675,#409676,#409677,#409678),.UNSPECIFIED.,.F.,.F.)
B_SPLINE_CURVE_WITH_KNOTS((3,2,2,2,2,2,3),(0.0294117647058824,0.0326797385620915,
0.0359477124183007,0.0392156862745098,0.042483660130719,0.0457516339869281,
0.0490196078431373),.UNSPECIFIED.)
CURVE()
GEOMETRIC_REPRESENTATION_ITEM()
RATIONAL_B_SPLINE_CURVE((1.,0.866025403784439,1.,0.866025403784439,1.,0.866025403784439,
1.,0.866025403784439,1.,0.866025403784439,1.,0.866025403784439,1.))
REPRESENTATION_ITEM('')
);
#4330=(
BOUNDED_CURVE()
B_SPLINE_CURVE(2,(#409679,#409680,#409681,#409682,#409683,#409684,#409685,
#409686,#409687,#409688,#409689,#409690,#409691),.UNSPECIFIED.,.F.,.F.)
B_SPLINE_CURVE_WITH_KNOTS((3,2,2,2,2,2,3),(0.0294117647058824,0.0326797385620915,
0.0359477124183007,0.0392156862745098,0.042483660130719,0.0457516339869281,
0.0490196078431373),.UNSPECIFIED.)
CURVE()
GEOMETRIC_REPRESENTATION_ITEM()
RATIONAL_B_SPLINE_CURVE((1.,0.866025403784439,1.,0.866025403784439,1.,0.866025403784439,
1.,0.866025403784439,1.,0.866025403784439,1.,0.866025403784439,1.))
REPRESENTATION_ITEM('')
);
#4331=(
BOUNDED_CURVE()
B_SPLINE_CURVE(2,(#409696,#409697,#409698,#409699,#409700,#409701,#409702,
#409703,#409704,#409705,#409706,#409707,#409708),.UNSPECIFIED.,.F.,.F.)
B_SPLINE_CURVE_WITH_KNOTS((3,2,2,2,2,2,3),(0.0490196078431373,0.0522875816993464,
0.0555555555555556,0.0588235294117647,0.0620915032679739,0.065359477124183,
0.0686274509803922),.UNSPECIFIED.)
CURVE()
GEOMETRIC_REPRESENTATION_ITEM()
RATIONAL_B_SPLINE_CURVE((1.,0.866025403784439,1.,0.866025403784439,1.,0.866025403784439,
1.,0.866025403784439,1.,0.866025403784439,1.,0.866025403784439,1.))
REPRESENTATION_ITEM('')
);
#4332=(
BOUNDED_CURVE()
B_SPLINE_CURVE(2,(#409709,#409710,#409711,#409712,#409713,#409714,#409715,
#409716,#409717,#409718,#409719,#409720,#409721),.UNSPECIFIED.,.F.,.F.)
B_SPLINE_CURVE_WITH_KNOTS((3,2,2,2,2,2,3),(0.0490196078431373,0.0522875816993464,
0.0555555555555556,0.0588235294117647,0.0620915032679739,0.065359477124183,
0.0686274509803922),.UNSPECIFIED.)
CURVE()
GEOMETRIC_REPRESENTATION_ITEM()
RATIONAL_B_SPLINE_CURVE((1.,0.866025403784439,1.,0.866025403784439,1.,0.866025403784439,
1.,0.866025403784439,1.,0.866025403784439,1.,0.866025403784439,1.))
REPRESENTATION_ITEM('')
);
#4333=(
BOUNDED_CURVE()
B_SPLINE_CURVE(2,(#409726,#409727,#409728,#409729,#409730,#409731,#409732,
#409733,#409734,#409735,#409736,#409737,#409738),.UNSPECIFIED.,.F.,.F.)
B_SPLINE_CURVE_WITH_KNOTS((3,2,2,2,2,2,3),(0.0686274509803922,0.0718954248366013,
0.0751633986928105,0.0784313725490196,0.0816993464052288,0.0849673202614379,
0.0882352941176471),.UNSPECIFIED.)
CURVE()
GEOMETRIC_REPRESENTATION_ITEM()
RATIONAL_B_SPLINE_CURVE((1.,0.866025403784439,1.,0.866025403784439,1.,0.866025403784439,
1.,0.866025403784439,1.,0.866025403784439,1.,0.866025403784439,1.))
REPRESENTATION_ITEM('')
);
#4334=(
BOUNDED_CURVE()
B_SPLINE_CURVE(2,(#409739,#409740,#409741,#409742,#409743,#409744,#409745,
#409746,#409747,#409748,#409749,#409750,#409751),.UNSPECIFIED.,.F.,.F.)
B_SPLINE_CURVE_WITH_KNOTS((3,2,2,2,2,2,3),(0.0686274509803922,0.0718954248366013,
0.0751633986928105,0.0784313725490196,0.0816993464052288,0.0849673202614379,
0.0882352941176471),.UNSPECIFIED.)
CURVE()
GEOMETRIC_REPRESENTATION_ITEM()
RATIONAL_B_SPLINE_CURVE((1.,0.866025403784439,1.,0.866025403784439,1.,0.866025403784439,
1.,0.866025403784439,1.,0.866025403784439,1.,0.866025403784439,1.))
REPRESENTATION_ITEM('')
);
#4335=(
BOUNDED_CURVE()
B_SPLINE_CURVE(2,(#409756,#409757,#409758,#409759,#409760,#409761,#409762,
#409763,#409764,#409765,#409766,#409767,#409768),.UNSPECIFIED.,.F.,.F.)
B_SPLINE_CURVE_WITH_KNOTS((3,2,2,2,2,2,3),(0.0882352941176471,0.0915032679738562,
0.0947712418300654,0.0980392156862745,0.101307189542484,0.104575163398693,
0.107843137254902),.UNSPECIFIED.)
CURVE()
GEOMETRIC_REPRESENTATION_ITEM()
RATIONAL_B_SPLINE_CURVE((1.,0.866025403784439,1.,0.866025403784439,1.,0.866025403784439,
1.,0.866025403784439,1.,0.866025403784439,1.,0.866025403784439,1.))
REPRESENTATION_ITEM('')
);
#4336=(
BOUNDED_CURVE()
B_SPLINE_CURVE(2,(#409769,#409770,#409771,#409772,#409773,#409774,#409775,
#409776,#409777,#409778,#409779,#409780,#409781),.UNSPECIFIED.,.F.,.F.)
B_SPLINE_CURVE_WITH_KNOTS((3,2,2,2,2,2,3),(0.0882352941176471,0.0915032679738562,
0.0947712418300654,0.0980392156862745,0.101307189542484,0.104575163398693,
0.107843137254902),.UNSPECIFIED.)
CURVE()
GEOMETRIC_REPRESENTATION_ITEM()
RATIONAL_B_SPLINE_CURVE((1.,0.866025403784439,1.,0.866025403784439,1.,0.866025403784439,
1.,0.866025403784439,1.,0.866025403784439,1.,0.866025403784439,1.))
REPRESENTATION_ITEM('')
);
#4337=(
BOUNDED_CURVE()
B_SPLINE_CURVE(2,(#409786,#409787,#409788,#409789,#409790,#409791,#409792,
#409793,#409794,#409795,#409796,#409797,#409798),.UNSPECIFIED.,.F.,.F.)
B_SPLINE_CURVE_WITH_KNOTS((3,2,2,2,2,2,3),(0.107843137254902,0.111111111111111,
0.11437908496732,0.117647058823529,0.120915032679739,0.124183006535948,
0.127450980392157),.UNSPECIFIED.)
CURVE()
GEOMETRIC_REPRESENTATION_ITEM()
RATIONAL_B_SPLINE_CURVE((1.,0.866025403784439,1.,0.866025403784439,1.,0.866025403784439,
1.,0.866025403784439,1.,0.866025403784439,1.,0.866025403784439,1.))
REPRESENTATION_ITEM('')
);
#4338=(
BOUNDED_CURVE()
B_SPLINE_CURVE(2,(#409799,#409800,#409801,#409802,#409803,#409804,#409805,
#409806,#409807,#409808,#409809,#409810,#409811),.UNSPECIFIED.,.F.,.F.)
B_SPLINE_CURVE_WITH_KNOTS((3,2,2,2,2,2,3),(0.107843137254902,0.111111111111111,
0.11437908496732,0.117647058823529,0.120915032679739,0.124183006535948,
0.127450980392157),.UNSPECIFIED.)
CURVE()
GEOMETRIC_REPRESENTATION_ITEM()
RATIONAL_B_SPLINE_CURVE((1.,0.866025403784439,1.,0.866025403784439,1.,0.866025403784439,
1.,0.866025403784439,1.,0.866025403784439,1.,0.866025403784439,1.))
REPRESENTATION_ITEM('')
);
#4339=(
BOUNDED_CURVE()
B_SPLINE_CURVE(2,(#409816,#409817,#409818,#409819,#409820,#409821,#409822,
#409823,#409824,#409825,#409826,#409827,#409828),.UNSPECIFIED.,.F.,.F.)
B_SPLINE_CURVE_WITH_KNOTS((3,2,2,2,2,2,3),(0.127450980392157,0.130718954248366,
0.133986928104575,0.137254901960784,0.140522875816993,0.143790849673203,
0.147058823529412),.UNSPECIFIED.)
CURVE()
GEOMETRIC_REPRESENTATION_ITEM()
RATIONAL_B_SPLINE_CURVE((1.,0.866025403784439,1.,0.866025403784439,1.,0.866025403784439,
1.,0.866025403784439,1.,0.866025403784439,1.,0.866025403784439,1.))
REPRESENTATION_ITEM('')
);
#4340=(
BOUNDED_CURVE()
B_SPLINE_CURVE(2,(#409829,#409830,#409831,#409832,#409833,#409834,#409835,
#409836,#409837,#409838,#409839,#409840,#409841),.UNSPECIFIED.,.F.,.F.)
B_SPLINE_CURVE_WITH_KNOTS((3,2,2,2,2,2,3),(0.127450980392157,0.130718954248366,
0.133986928104575,0.137254901960784,0.140522875816993,0.143790849673203,
0.147058823529412),.UNSPECIFIED.)
CURVE()
GEOMETRIC_REPRESENTATION_ITEM()
RATIONAL_B_SPLINE_CURVE((1.,0.866025403784439,1.,0.866025403784439,1.,0.866025403784439,
1.,0.866025403784439,1.,0.866025403784439,1.,0.866025403784439,1.))
REPRESENTATION_ITEM('')
);
#4341=(
BOUNDED_CURVE()
B_SPLINE_CURVE(2,(#409846,#409847,#409848,#409849,#409850,#409851,#409852,
#409853,#409854,#409855,#409856,#409857,#409858),.UNSPECIFIED.,.F.,.F.)
B_SPLINE_CURVE_WITH_KNOTS((3,2,2,2,2,2,3),(0.147058823529412,0.150326797385621,
0.15359477124183,0.156862745098039,0.160130718954248,0.163398692810458,
0.166666666666667),.UNSPECIFIED.)
CURVE()
GEOMETRIC_REPRESENTATION_ITEM()
RATIONAL_B_SPLINE_CURVE((1.,0.866025403784439,1.,0.866025403784439,1.,0.866025403784439,
1.,0.866025403784439,1.,0.866025403784439,1.,0.866025403784439,1.))
REPRESENTATION_ITEM('')
);
#4342=(
BOUNDED_CURVE()
B_SPLINE_CURVE(2,(#409859,#409860,#409861,#409862,#409863,#409864,#409865,
#409866,#409867,#409868,#409869,#409870,#409871),.UNSPECIFIED.,.F.,.F.)
B_SPLINE_CURVE_WITH_KNOTS((3,2,2,2,2,2,3),(0.147058823529412,0.150326797385621,
0.15359477124183,0.156862745098039,0.160130718954248,0.163398692810458,
0.166666666666667),.UNSPECIFIED.)
CURVE()
GEOMETRIC_REPRESENTATION_ITEM()
RATIONAL_B_SPLINE_CURVE((1.,0.866025403784439,1.,0.866025403784439,1.,0.866025403784439,
1.,0.866025403784439,1.,0.866025403784439,1.,0.866025403784439,1.))
REPRESENTATION_ITEM('')
);
#4343=(
BOUNDED_CURVE()
B_SPLINE_CURVE(2,(#409876,#409877,#409878,#409879,#409880,#409881,#409882,
#409883,#409884,#409885,#409886,#409887,#409888),.UNSPECIFIED.,.F.,.F.)
B_SPLINE_CURVE_WITH_KNOTS((3,2,2,2,2,2,3),(0.166666666666667,0.169934640522876,
0.173202614379085,0.176470588235294,0.179738562091503,0.183006535947712,
0.186274509803922),.UNSPECIFIED.)
CURVE()
GEOMETRIC_REPRESENTATION_ITEM()
RATIONAL_B_SPLINE_CURVE((1.,0.866025403784439,1.,0.866025403784439,1.,0.866025403784439,
1.,0.866025403784439,1.,0.866025403784439,1.,0.866025403784439,1.))
REPRESENTATION_ITEM('')
);
#4344=(
BOUNDED_CURVE()
B_SPLINE_CURVE(2,(#409889,#409890,#409891,#409892,#409893,#409894,#409895,
#409896,#409897,#409898,#409899,#409900,#409901),.UNSPECIFIED.,.F.,.F.)
B_SPLINE_CURVE_WITH_KNOTS((3,2,2,2,2,2,3),(0.166666666666667,0.169934640522876,
0.173202614379085,0.176470588235294,0.179738562091503,0.183006535947712,
0.186274509803922),.UNSPECIFIED.)
CURVE()
GEOMETRIC_REPRESENTATION_ITEM()
RATIONAL_B_SPLINE_CURVE((1.,0.866025403784439,1.,0.866025403784439,1.,0.866025403784439,
1.,0.866025403784439,1.,0.866025403784439,1.,0.866025403784439,1.))
REPRESENTATION_ITEM('')
);
#4345=(
BOUNDED_CURVE()
B_SPLINE_CURVE(2,(#409906,#409907,#409908,#409909,#409910,#409911,#409912,
#409913,#409914,#409915,#409916,#409917,#409918),.UNSPECIFIED.,.F.,.F.)
B_SPLINE_CURVE_WITH_KNOTS((3,2,2,2,2,2,3),(0.186274509803922,0.189542483660131,
0.19281045751634,0.196078431372549,0.199346405228758,0.202614379084967,
0.205882352941176),.UNSPECIFIED.)
CURVE()
GEOMETRIC_REPRESENTATION_ITEM()
RATIONAL_B_SPLINE_CURVE((1.,0.866025403784439,1.,0.866025403784439,1.,0.866025403784439,
1.,0.866025403784439,1.,0.866025403784439,1.,0.866025403784439,1.))
REPRESENTATION_ITEM('')
);
#4346=(
BOUNDED_CURVE()
B_SPLINE_CURVE(2,(#409919,#409920,#409921,#409922,#409923,#409924,#409925,
#409926,#409927,#409928,#409929,#409930,#409931),.UNSPECIFIED.,.F.,.F.)
B_SPLINE_CURVE_WITH_KNOTS((3,2,2,2,2,2,3),(0.186274509803922,0.189542483660131,
0.19281045751634,0.196078431372549,0.199346405228758,0.202614379084967,
0.205882352941177),.UNSPECIFIED.)
CURVE()
GEOMETRIC_REPRESENTATION_ITEM()
RATIONAL_B_SPLINE_CURVE((1.,0.866025403784439,1.,0.866025403784439,1.,0.866025403784439,
1.,0.866025403784439,1.,0.866025403784439,1.,0.866025403784439,1.))
REPRESENTATION_ITEM('')
);
#4347=(
BOUNDED_CURVE()
B_SPLINE_CURVE(2,(#409936,#409937,#409938,#409939,#409940,#409941,#409942,
#409943,#409944,#409945,#409946,#409947,#409948),.UNSPECIFIED.,.F.,.F.)
B_SPLINE_CURVE_WITH_KNOTS((3,2,2,2,2,2,3),(0.205882352941176,0.209150326797386,
0.212418300653595,0.215686274509804,0.218954248366013,0.222222222222222,
0.225490196078431),.UNSPECIFIED.)
CURVE()
GEOMETRIC_REPRESENTATION_ITEM()
RATIONAL_B_SPLINE_CURVE((1.,0.866025403784439,1.,0.866025403784439,1.,0.866025403784439,
1.,0.866025403784439,1.,0.866025403784439,1.,0.866025403784439,1.))
REPRESENTATION_ITEM('')
);
#4348=(
BOUNDED_CURVE()
B_SPLINE_CURVE(2,(#409949,#409950,#409951,#409952,#409953,#409954,#409955,
#409956,#409957,#409958,#409959,#409960,#409961),.UNSPECIFIED.,.F.,.F.)
B_SPLINE_CURVE_WITH_KNOTS((3,2,2,2,2,2,3),(0.205882352941177,0.209150326797386,
0.212418300653595,0.215686274509804,0.218954248366013,0.222222222222222,
0.225490196078431),.UNSPECIFIED.)
CURVE()
GEOMETRIC_REPRESENTATION_ITEM()
RATIONAL_B_SPLINE_CURVE((1.,0.866025403784439,1.,0.866025403784439,1.,0.866025403784439,
1.,0.866025403784439,1.,0.866025403784439,1.,0.866025403784439,1.))
REPRESENTATION_ITEM('')
);
#4349=(
BOUNDED_CURVE()
B_SPLINE_CURVE(2,(#409966,#409967,#409968,#409969,#409970,#409971,#409972,
#409973,#409974,#409975,#409976,#409977,#409978),.UNSPECIFIED.,.F.,.F.)
B_SPLINE_CURVE_WITH_KNOTS((3,2,2,2,2,2,3),(0.225490196078431,0.22875816993464,
0.23202614379085,0.235294117647059,0.238562091503268,0.241830065359477,
0.245098039215686),.UNSPECIFIED.)
CURVE()
GEOMETRIC_REPRESENTATION_ITEM()
RATIONAL_B_SPLINE_CURVE((1.,0.866025403784439,1.,0.866025403784439,1.,0.866025403784439,
1.,0.866025403784439,1.,0.866025403784439,1.,0.866025403784439,1.))
REPRESENTATION_ITEM('')
);
#4350=(
BOUNDED_CURVE()
B_SPLINE_CURVE(2,(#409979,#409980,#409981,#409982,#409983,#409984,#409985,
#409986,#409987,#409988,#409989,#409990,#409991),.UNSPECIFIED.,.F.,.F.)
B_SPLINE_CURVE_WITH_KNOTS((3,2,2,2,2,2,3),(0.225490196078431,0.228758169934641,
0.23202614379085,0.235294117647059,0.238562091503268,0.241830065359477,
0.245098039215686),.UNSPECIFIED.)
CURVE()
GEOMETRIC_REPRESENTATION_ITEM()
RATIONAL_B_SPLINE_CURVE((1.,0.866025403784439,1.,0.866025403784439,1.,0.866025403784439,
1.,0.866025403784439,1.,0.866025403784439,1.,0.866025403784439,1.))
REPRESENTATION_ITEM('')
);
#4351=(
BOUNDED_CURVE()
B_SPLINE_CURVE(2,(#409996,#409997,#409998,#409999,#410000,#410001,#410002,
#410003,#410004,#410005,#410006,#410007,#410008),.UNSPECIFIED.,.F.,.F.)
B_SPLINE_CURVE_WITH_KNOTS((3,2,2,2,2,2,3),(0.245098039215686,0.248366013071895,
0.251633986928105,0.254901960784314,0.258169934640523,0.261437908496732,
0.264705882352941),.UNSPECIFIED.)
CURVE()
GEOMETRIC_REPRESENTATION_ITEM()
RATIONAL_B_SPLINE_CURVE((1.,0.866025403784439,1.,0.866025403784439,1.,0.866025403784439,
1.,0.866025403784439,1.,0.866025403784439,1.,0.866025403784439,1.))
REPRESENTATION_ITEM('')
);
#4352=(
BOUNDED_CURVE()
B_SPLINE_CURVE(2,(#410009,#410010,#410011,#410012,#410013,#410014,#410015,
#410016,#410017,#410018,#410019,#410020,#410021),.UNSPECIFIED.,.F.,.F.)
B_SPLINE_CURVE_WITH_KNOTS((3,2,2,2,2,2,3),(0.245098039215686,0.248366013071895,
0.251633986928105,0.254901960784314,0.258169934640523,0.261437908496732,
0.264705882352941),.UNSPECIFIED.)
CURVE()
GEOMETRIC_REPRESENTATION_ITEM()
RATIONAL_B_SPLINE_CURVE((1.,0.866025403784439,1.,0.866025403784439,1.,0.866025403784439,
1.,0.866025403784439,1.,0.866025403784439,1.,0.866025403784439,1.))
REPRESENTATION_ITEM('')
);
#4353=(
BOUNDED_CURVE()
B_SPLINE_CURVE(2,(#410026,#410027,#410028,#410029,#410030,#410031,#410032,
#410033,#410034,#410035,#410036,#410037,#410038),.UNSPECIFIED.,.F.,.F.)
B_SPLINE_CURVE_WITH_KNOTS((3,2,2,2,2,2,3),(0.264705882352941,0.26797385620915,
0.271241830065359,0.274509803921569,0.277777777777778,0.281045751633987,
0.284313725490196),.UNSPECIFIED.)
CURVE()
GEOMETRIC_REPRESENTATION_ITEM()
RATIONAL_B_SPLINE_CURVE((1.,0.866025403784439,1.,0.866025403784439,1.,0.866025403784439,
1.,0.866025403784439,1.,0.866025403784439,1.,0.866025403784439,1.))
REPRESENTATION_ITEM('')
);
#4354=(
BOUNDED_CURVE()
B_SPLINE_CURVE(2,(#410039,#410040,#410041,#410042,#410043,#410044,#410045,
#410046,#410047,#410048,#410049,#410050,#410051),.UNSPECIFIED.,.F.,.F.)
B_SPLINE_CURVE_WITH_KNOTS((3,2,2,2,2,2,3),(0.264705882352941,0.26797385620915,
0.271241830065359,0.274509803921569,0.277777777777778,0.281045751633987,
0.284313725490196),.UNSPECIFIED.)
CURVE()
GEOMETRIC_REPRESENTATION_ITEM()
RATIONAL_B_SPLINE_CURVE((1.,0.866025403784439,1.,0.866025403784439,1.,0.866025403784439,
1.,0.866025403784439,1.,0.866025403784439,1.,0.866025403784439,1.))
REPRESENTATION_ITEM('')
);
#4355=(
BOUNDED_CURVE()
B_SPLINE_CURVE(2,(#410056,#410057,#410058,#410059,#410060,#410061,#410062,
#410063,#410064,#410065,#410066,#410067,#410068),.UNSPECIFIED.,.F.,.F.)
B_SPLINE_CURVE_WITH_KNOTS((3,2,2,2,2,2,3),(0.284313725490196,0.287581699346405,
0.290849673202614,0.294117647058823,0.297385620915033,0.300653594771242,
0.303921568627451),.UNSPECIFIED.)
CURVE()
GEOMETRIC_REPRESENTATION_ITEM()
RATIONAL_B_SPLINE_CURVE((1.,0.866025403784439,1.,0.866025403784439,1.,0.866025403784439,
1.,0.866025403784439,1.,0.866025403784439,1.,0.866025403784439,1.))
REPRESENTATION_ITEM('')
);
#4356=(
BOUNDED_CURVE()
B_SPLINE_CURVE(2,(#410069,#410070,#410071,#410072,#410073,#410074,#410075,
#410076,#410077,#410078,#410079,#410080,#410081),.UNSPECIFIED.,.F.,.F.)
B_SPLINE_CURVE_WITH_KNOTS((3,2,2,2,2,2,3),(0.284313725490196,0.287581699346405,
0.290849673202614,0.294117647058824,0.297385620915033,0.300653594771242,
0.303921568627451),.UNSPECIFIED.)
CURVE()
GEOMETRIC_REPRESENTATION_ITEM()
RATIONAL_B_SPLINE_CURVE((1.,0.866025403784439,1.,0.866025403784439,1.,0.866025403784439,
1.,0.866025403784439,1.,0.866025403784439,1.,0.866025403784439,1.))
REPRESENTATION_ITEM('')
);
#4357=(
BOUNDED_CURVE()
B_SPLINE_CURVE(2,(#410086,#410087,#410088,#410089,#410090,#410091,#410092,
#410093,#410094,#410095,#410096,#410097,#410098),.UNSPECIFIED.,.F.,.F.)
B_SPLINE_CURVE_WITH_KNOTS((3,2,2,2,2,2,3),(0.303921568627451,0.30718954248366,
0.310457516339869,0.313725490196078,0.316993464052288,0.320261437908497,
0.323529411764706),.UNSPECIFIED.)
CURVE()
GEOMETRIC_REPRESENTATION_ITEM()
RATIONAL_B_SPLINE_CURVE((1.,0.866025403784439,1.,0.866025403784439,1.,0.866025403784439,
1.,0.866025403784439,1.,0.866025403784439,1.,0.866025403784439,1.))
REPRESENTATION_ITEM('')
);
#4358=(
BOUNDED_CURVE()
B_SPLINE_CURVE(2,(#410099,#410100,#410101,#410102,#410103,#410104,#410105,
#410106,#410107,#410108,#410109,#410110,#410111),.UNSPECIFIED.,.F.,.F.)
B_SPLINE_CURVE_WITH_KNOTS((3,2,2,2,2,2,3),(0.303921568627451,0.30718954248366,
0.310457516339869,0.313725490196078,0.316993464052288,0.320261437908497,
0.323529411764706),.UNSPECIFIED.)
CURVE()
GEOMETRIC_REPRESENTATION_ITEM()
RATIONAL_B_SPLINE_CURVE((1.,0.866025403784439,1.,0.866025403784439,1.,0.866025403784439,
1.,0.866025403784439,1.,0.866025403784439,1.,0.866025403784439,1.))
REPRESENTATION_ITEM('')
);
#4359=(
BOUNDED_CURVE()
B_SPLINE_CURVE(2,(#410116,#410117,#410118,#410119,#410120,#410121,#410122,
#410123,#410124,#410125,#410126,#410127,#410128),.UNSPECIFIED.,.F.,.F.)
B_SPLINE_CURVE_WITH_KNOTS((3,2,2,2,2,2,3),(0.323529411764706,0.326797385620915,
0.330065359477124,0.333333333333333,0.336601307189543,0.339869281045752,
0.343137254901961),.UNSPECIFIED.)
CURVE()
GEOMETRIC_REPRESENTATION_ITEM()
RATIONAL_B_SPLINE_CURVE((1.,0.866025403784439,1.,0.866025403784439,1.,0.866025403784439,
1.,0.866025403784439,1.,0.866025403784439,1.,0.866025403784439,1.))
REPRESENTATION_ITEM('')
);
#4360=(
BOUNDED_CURVE()
B_SPLINE_CURVE(2,(#410129,#410130,#410131,#410132,#410133,#410134,#410135,
#410136,#410137,#410138,#410139,#410140,#410141),.UNSPECIFIED.,.F.,.F.)
B_SPLINE_CURVE_WITH_KNOTS((3,2,2,2,2,2,3),(0.323529411764706,0.326797385620915,
0.330065359477124,0.333333333333333,0.336601307189543,0.339869281045752,
0.343137254901961),.UNSPECIFIED.)
CURVE()
GEOMETRIC_REPRESENTATION_ITEM()
RATIONAL_B_SPLINE_CURVE((1.,0.866025403784439,1.,0.866025403784439,1.,0.866025403784439,
1.,0.866025403784439,1.,0.866025403784439,1.,0.866025403784439,1.))
REPRESENTATION_ITEM('')
);
#4361=(
BOUNDED_CURVE()
B_SPLINE_CURVE(2,(#410146,#410147,#410148,#410149,#410150,#410151,#410152,
#410153,#410154,#410155,#410156,#410157,#410158),.UNSPECIFIED.,.F.,.F.)
B_SPLINE_CURVE_WITH_KNOTS((3,2,2,2,2,2,3),(0.343137254901961,0.34640522875817,
0.349673202614379,0.352941176470588,0.356209150326797,0.359477124183006,
0.362745098039216),.UNSPECIFIED.)
CURVE()
GEOMETRIC_REPRESENTATION_ITEM()
RATIONAL_B_SPLINE_CURVE((1.,0.866025403784439,1.,0.866025403784439,1.,0.866025403784439,
1.,0.866025403784439,1.,0.866025403784439,1.,0.866025403784439,1.))
REPRESENTATION_ITEM('')
);
#4362=(
BOUNDED_CURVE()
B_SPLINE_CURVE(2,(#410159,#410160,#410161,#410162,#410163,#410164,#410165,
#410166,#410167,#410168,#410169,#410170,#410171),.UNSPECIFIED.,.F.,.F.)
B_SPLINE_CURVE_WITH_KNOTS((3,2,2,2,2,2,3),(0.343137254901961,0.34640522875817,
0.349673202614379,0.352941176470588,0.356209150326797,0.359477124183007,
0.362745098039216),.UNSPECIFIED.)
CURVE()
GEOMETRIC_REPRESENTATION_ITEM()
RATIONAL_B_SPLINE_CURVE((1.,0.866025403784439,1.,0.866025403784439,1.,0.866025403784439,
1.,0.866025403784439,1.,0.866025403784439,1.,0.866025403784439,1.))
REPRESENTATION_ITEM('')
);
#4363=(
BOUNDED_CURVE()
B_SPLINE_CURVE(2,(#410176,#410177,#410178,#410179,#410180,#410181,#410182,
#410183,#410184,#410185,#410186,#410187,#410188),.UNSPECIFIED.,.F.,.F.)
B_SPLINE_CURVE_WITH_KNOTS((3,2,2,2,2,2,3),(0.362745098039216,0.366013071895425,
0.369281045751634,0.372549019607843,0.375816993464052,0.379084967320261,
0.382352941176471),.UNSPECIFIED.)
CURVE()
GEOMETRIC_REPRESENTATION_ITEM()
RATIONAL_B_SPLINE_CURVE((1.,0.866025403784439,1.,0.866025403784439,1.,0.866025403784439,
1.,0.866025403784439,1.,0.866025403784439,1.,0.866025403784439,1.))
REPRESENTATION_ITEM('')
);
#4364=(
BOUNDED_CURVE()
B_SPLINE_CURVE(2,(#410189,#410190,#410191,#410192,#410193,#410194,#410195,
#410196,#410197,#410198,#410199,#410200,#410201),.UNSPECIFIED.,.F.,.F.)
B_SPLINE_CURVE_WITH_KNOTS((3,2,2,2,2,2,3),(0.362745098039216,0.366013071895425,
0.369281045751634,0.372549019607843,0.375816993464052,0.379084967320261,
0.382352941176471),.UNSPECIFIED.)
CURVE()
GEOMETRIC_REPRESENTATION_ITEM()
RATIONAL_B_SPLINE_CURVE((1.,0.866025403784439,1.,0.866025403784439,1.,0.866025403784439,
1.,0.866025403784439,1.,0.866025403784439,1.,0.866025403784439,1.))
REPRESENTATION_ITEM('')
);
#4365=(
BOUNDED_CURVE()
B_SPLINE_CURVE(2,(#410206,#410207,#410208,#410209,#410210,#410211,#410212,
#410213,#410214,#410215,#410216,#410217,#410218),.UNSPECIFIED.,.F.,.F.)
B_SPLINE_CURVE_WITH_KNOTS((3,2,2,2,2,2,3),(0.382352941176471,0.38562091503268,
0.388888888888889,0.392156862745098,0.395424836601307,0.398692810457516,
0.401960784313726),.UNSPECIFIED.)
CURVE()
GEOMETRIC_REPRESENTATION_ITEM()
RATIONAL_B_SPLINE_CURVE((1.,0.866025403784439,1.,0.866025403784439,1.,0.866025403784439,
1.,0.866025403784439,1.,0.866025403784439,1.,0.866025403784439,1.))
REPRESENTATION_ITEM('')
);
#4366=(
BOUNDED_CURVE()
B_SPLINE_CURVE(2,(#410219,#410220,#410221,#410222,#410223,#410224,#410225,
#410226,#410227,#410228,#410229,#410230,#410231),.UNSPECIFIED.,.F.,.F.)
B_SPLINE_CURVE_WITH_KNOTS((3,2,2,2,2,2,3),(0.382352941176471,0.38562091503268,
0.388888888888889,0.392156862745098,0.395424836601307,0.398692810457516,
0.401960784313726),.UNSPECIFIED.)
CURVE()
GEOMETRIC_REPRESENTATION_ITEM()
RATIONAL_B_SPLINE_CURVE((1.,0.866025403784439,1.,0.866025403784439,1.,0.866025403784439,
1.,0.866025403784439,1.,0.866025403784439,1.,0.866025403784439,1.))
REPRESENTATION_ITEM('')
);
#4367=(
BOUNDED_CURVE()
B_SPLINE_CURVE(2,(#410236,#410237,#410238,#410239,#410240,#410241,#410242,
#410243,#410244,#410245,#410246,#410247,#410248),.UNSPECIFIED.,.F.,.F.)
B_SPLINE_CURVE_WITH_KNOTS((3,2,2,2,2,2,3),(0.401960784313726,0.405228758169935,
0.408496732026144,0.411764705882353,0.415032679738562,0.418300653594771,
0.42156862745098),.UNSPECIFIED.)
CURVE()
GEOMETRIC_REPRESENTATION_ITEM()
RATIONAL_B_SPLINE_CURVE((1.,0.866025403784439,1.,0.866025403784439,1.,0.866025403784439,
1.,0.866025403784439,1.,0.866025403784439,1.,0.866025403784439,1.))
REPRESENTATION_ITEM('')
);
#4368=(
BOUNDED_CURVE()
B_SPLINE_CURVE(2,(#410249,#410250,#410251,#410252,#410253,#410254,#410255,
#410256,#410257,#410258,#410259,#410260,#410261),.UNSPECIFIED.,.F.,.F.)
B_SPLINE_CURVE_WITH_KNOTS((3,2,2,2,2,2,3),(0.401960784313726,0.405228758169935,
0.408496732026144,0.411764705882353,0.415032679738562,0.418300653594771,
0.42156862745098),.UNSPECIFIED.)
CURVE()
GEOMETRIC_REPRESENTATION_ITEM()
RATIONAL_B_SPLINE_CURVE((1.,0.866025403784439,1.,0.866025403784439,1.,0.866025403784439,
1.,0.866025403784439,1.,0.866025403784439,1.,0.866025403784439,1.))
REPRESENTATION_ITEM('')
);
#4369=(
BOUNDED_CURVE()
B_SPLINE_CURVE(2,(#410266,#410267,#410268,#410269,#410270,#410271,#410272,
#410273,#410274,#410275,#410276,#410277,#410278),.UNSPECIFIED.,.F.,.F.)
B_SPLINE_CURVE_WITH_KNOTS((3,2,2,2,2,2,3),(0.42156862745098,0.424836601307189,
0.428104575163399,0.431372549019608,0.434640522875817,0.437908496732026,
0.441176470588235),.UNSPECIFIED.)
CURVE()
GEOMETRIC_REPRESENTATION_ITEM()
RATIONAL_B_SPLINE_CURVE((1.,0.866025403784439,1.,0.866025403784439,1.,0.866025403784439,
1.,0.866025403784439,1.,0.866025403784439,1.,0.866025403784439,1.))
REPRESENTATION_ITEM('')
);
#4370=(
BOUNDED_CURVE()
B_SPLINE_CURVE(2,(#410279,#410280,#410281,#410282,#410283,#410284,#410285,
#410286,#410287,#410288,#410289,#410290,#410291),.UNSPECIFIED.,.F.,.F.)
B_SPLINE_CURVE_WITH_KNOTS((3,2,2,2,2,2,3),(0.42156862745098,0.42483660130719,
0.428104575163399,0.431372549019608,0.434640522875817,0.437908496732026,
0.441176470588235),.UNSPECIFIED.)
CURVE()
GEOMETRIC_REPRESENTATION_ITEM()
RATIONAL_B_SPLINE_CURVE((1.,0.866025403784439,1.,0.866025403784439,1.,0.866025403784439,
1.,0.866025403784439,1.,0.866025403784439,1.,0.866025403784439,1.))
REPRESENTATION_ITEM('')
);
#4371=(
BOUNDED_CURVE()
B_SPLINE_CURVE(2,(#410296,#410297,#410298,#410299,#410300,#410301,#410302,
#410303,#410304,#410305,#410306,#410307,#410308),.UNSPECIFIED.,.F.,.F.)
B_SPLINE_CURVE_WITH_KNOTS((3,2,2,2,2,2,3),(0.441176470588235,0.444444444444444,
0.447712418300654,0.450980392156863,0.454248366013072,0.457516339869281,
0.46078431372549),.UNSPECIFIED.)
CURVE()
GEOMETRIC_REPRESENTATION_ITEM()
RATIONAL_B_SPLINE_CURVE((1.,0.866025403784439,1.,0.866025403784439,1.,0.866025403784439,
1.,0.866025403784439,1.,0.866025403784439,1.,0.866025403784439,1.))
REPRESENTATION_ITEM('')
);
#4372=(
BOUNDED_CURVE()
B_SPLINE_CURVE(2,(#410309,#410310,#410311,#410312,#410313,#410314,#410315,
#410316,#410317,#410318,#410319,#410320,#410321),.UNSPECIFIED.,.F.,.F.)
B_SPLINE_CURVE_WITH_KNOTS((3,2,2,2,2,2,3),(0.441176470588235,0.444444444444444,
0.447712418300654,0.450980392156863,0.454248366013072,0.457516339869281,
0.46078431372549),.UNSPECIFIED.)
CURVE()
GEOMETRIC_REPRESENTATION_ITEM()
RATIONAL_B_SPLINE_CURVE((1.,0.866025403784439,1.,0.866025403784439,1.,0.866025403784439,
1.,0.866025403784439,1.,0.866025403784439,1.,0.866025403784439,1.))
REPRESENTATION_ITEM('')
);
#4373=(
BOUNDED_CURVE()
B_SPLINE_CURVE(2,(#410326,#410327,#410328,#410329,#410330,#410331,#410332,
#410333,#410334,#410335,#410336,#410337,#410338),.UNSPECIFIED.,.F.,.F.)
B_SPLINE_CURVE_WITH_KNOTS((3,2,2,2,2,2,3),(0.46078431372549,0.464052287581699,
0.467320261437909,0.470588235294118,0.473856209150327,0.477124183006536,
0.480392156862745),.UNSPECIFIED.)
CURVE()
GEOMETRIC_REPRESENTATION_ITEM()
RATIONAL_B_SPLINE_CURVE((1.,0.866025403784439,1.,0.866025403784439,1.,0.866025403784439,
1.,0.866025403784439,1.,0.866025403784439,1.,0.866025403784439,1.))
REPRESENTATION_ITEM('')
);
#4374=(
BOUNDED_CURVE()
B_SPLINE_CURVE(2,(#410339,#410340,#410341,#410342,#410343,#410344,#410345,
#410346,#410347,#410348,#410349,#410350,#410351),.UNSPECIFIED.,.F.,.F.)
B_SPLINE_CURVE_WITH_KNOTS((3,2,2,2,2,2,3),(0.46078431372549,0.464052287581699,
0.467320261437908,0.470588235294118,0.473856209150327,0.477124183006536,
0.480392156862745),.UNSPECIFIED.)
CURVE()
GEOMETRIC_REPRESENTATION_ITEM()
RATIONAL_B_SPLINE_CURVE((1.,0.866025403784439,1.,0.866025403784439,1.,0.866025403784439,
1.,0.866025403784439,1.,0.866025403784439,1.,0.866025403784439,1.))
REPRESENTATION_ITEM('')
);
#4375=(
BOUNDED_CURVE()
B_SPLINE_CURVE(2,(#410356,#410357,#410358,#410359,#410360,#410361,#410362,
#410363,#410364,#410365,#410366,#410367,#410368),.UNSPECIFIED.,.F.,.F.)
B_SPLINE_CURVE_WITH_KNOTS((3,2,2,2,2,2,3),(0.480392156862745,0.483660130718954,
0.486928104575163,0.490196078431372,0.493464052287582,0.496732026143791,
0.5),.UNSPECIFIED.)
CURVE()
GEOMETRIC_REPRESENTATION_ITEM()
RATIONAL_B_SPLINE_CURVE((1.,0.866025403784439,1.,0.866025403784439,1.,0.866025403784439,
1.,0.866025403784439,1.,0.866025403784439,1.,0.866025403784439,1.))
REPRESENTATION_ITEM('')
);
#4376=(
BOUNDED_CURVE()
B_SPLINE_CURVE(2,(#410369,#410370,#410371,#410372,#410373,#410374,#410375,
#410376,#410377,#410378,#410379,#410380,#410381),.UNSPECIFIED.,.F.,.F.)
B_SPLINE_CURVE_WITH_KNOTS((3,2,2,2,2,2,3),(0.480392156862745,0.483660130718954,
0.486928104575163,0.490196078431373,0.493464052287582,0.496732026143791,
0.5),.UNSPECIFIED.)
CURVE()
GEOMETRIC_REPRESENTATION_ITEM()
RATIONAL_B_SPLINE_CURVE((1.,0.866025403784439,1.,0.866025403784439,1.,0.866025403784439,
1.,0.866025403784439,1.,0.866025403784439,1.,0.866025403784439,1.))
REPRESENTATION_ITEM('')
);
#4377=(
BOUNDED_CURVE()
B_SPLINE_CURVE(2,(#410386,#410387,#410388,#410389,#410390,#410391,#410392,
#410393,#410394,#410395,#410396,#410397,#410398),.UNSPECIFIED.,.F.,.F.)
B_SPLINE_CURVE_WITH_KNOTS((3,2,2,2,2,2,3),(0.5,0.503267973856209,0.506535947712418,
0.509803921568627,0.513071895424837,0.516339869281046,0.519607843137255),
 .UNSPECIFIED.)
CURVE()
GEOMETRIC_REPRESENTATION_ITEM()
RATIONAL_B_SPLINE_CURVE((1.,0.866025403784439,1.,0.866025403784439,1.,0.866025403784439,
1.,0.866025403784439,1.,0.866025403784439,1.,0.866025403784439,1.))
REPRESENTATION_ITEM('')
);
#4378=(
BOUNDED_CURVE()
B_SPLINE_CURVE(2,(#410399,#410400,#410401,#410402,#410403,#410404,#410405,
#410406,#410407,#410408,#410409,#410410,#410411),.UNSPECIFIED.,.F.,.F.)
B_SPLINE_CURVE_WITH_KNOTS((3,2,2,2,2,2,3),(0.5,0.503267973856209,0.506535947712418,
0.509803921568627,0.513071895424837,0.516339869281046,0.519607843137255),
 .UNSPECIFIED.)
CURVE()
GEOMETRIC_REPRESENTATION_ITEM()
RATIONAL_B_SPLINE_CURVE((1.,0.866025403784439,1.,0.866025403784439,1.,0.866025403784439,
1.,0.866025403784439,1.,0.866025403784439,1.,0.866025403784439,1.))
REPRESENTATION_ITEM('')
);
#4379=(
BOUNDED_CURVE()
B_SPLINE_CURVE(2,(#410416,#410417,#410418,#410419,#410420,#410421,#410422,
#410423,#410424,#410425,#410426,#410427,#410428),.UNSPECIFIED.,.F.,.F.)
B_SPLINE_CURVE_WITH_KNOTS((3,2,2,2,2,2,3),(0.519607843137255,0.522875816993464,
0.526143790849673,0.529411764705882,0.532679738562091,0.535947712418301,
0.53921568627451),.UNSPECIFIED.)
CURVE()
GEOMETRIC_REPRESENTATION_ITEM()
RATIONAL_B_SPLINE_CURVE((1.,0.866025403784439,1.,0.866025403784439,1.,0.866025403784439,
1.,0.866025403784439,1.,0.866025403784439,1.,0.866025403784439,1.))
REPRESENTATION_ITEM('')
);
#4380=(
BOUNDED_CURVE()
B_SPLINE_CURVE(2,(#410429,#410430,#410431,#410432,#410433,#410434,#410435,
#410436,#410437,#410438,#410439,#410440,#410441),.UNSPECIFIED.,.F.,.F.)
B_SPLINE_CURVE_WITH_KNOTS((3,2,2,2,2,2,3),(0.519607843137255,0.522875816993464,
0.526143790849673,0.529411764705882,0.532679738562091,0.535947712418301,
0.53921568627451),.UNSPECIFIED.)
CURVE()
GEOMETRIC_REPRESENTATION_ITEM()
RATIONAL_B_SPLINE_CURVE((1.,0.866025403784439,1.,0.866025403784439,1.,0.866025403784439,
1.,0.866025403784439,1.,0.866025403784439,1.,0.866025403784439,1.))
REPRESENTATION_ITEM('')
);
#4381=(
BOUNDED_CURVE()
B_SPLINE_CURVE(2,(#410446,#410447,#410448,#410449,#410450,#410451,#410452,
#410453,#410454,#410455,#410456,#410457,#410458),.UNSPECIFIED.,.F.,.F.)
B_SPLINE_CURVE_WITH_KNOTS((3,2,2,2,2,2,3),(0.53921568627451,0.542483660130719,
0.545751633986928,0.549019607843137,0.552287581699346,0.555555555555556,
0.558823529411765),.UNSPECIFIED.)
CURVE()
GEOMETRIC_REPRESENTATION_ITEM()
RATIONAL_B_SPLINE_CURVE((1.,0.866025403784439,1.,0.866025403784439,1.,0.866025403784439,
1.,0.866025403784439,1.,0.866025403784439,1.,0.866025403784439,1.))
REPRESENTATION_ITEM('')
);
#4382=(
BOUNDED_CURVE()
B_SPLINE_CURVE(2,(#410459,#410460,#410461,#410462,#410463,#410464,#410465,
#410466,#410467,#410468,#410469,#410470,#410471),.UNSPECIFIED.,.F.,.F.)
B_SPLINE_CURVE_WITH_KNOTS((3,2,2,2,2,2,3),(0.53921568627451,0.542483660130719,
0.545751633986928,0.549019607843137,0.552287581699346,0.555555555555556,
0.558823529411765),.UNSPECIFIED.)
CURVE()
GEOMETRIC_REPRESENTATION_ITEM()
RATIONAL_B_SPLINE_CURVE((1.,0.866025403784439,1.,0.866025403784439,1.,0.866025403784439,
1.,0.866025403784439,1.,0.866025403784439,1.,0.866025403784439,1.))
REPRESENTATION_ITEM('')
);
#4383=(
BOUNDED_CURVE()
B_SPLINE_CURVE(2,(#410476,#410477,#410478,#410479,#410480,#410481,#410482,
#410483,#410484,#410485,#410486,#410487,#410488),.UNSPECIFIED.,.F.,.F.)
B_SPLINE_CURVE_WITH_KNOTS((3,2,2,2,2,2,3),(0.558823529411765,0.562091503267974,
0.565359477124183,0.568627450980392,0.571895424836601,0.57516339869281,
0.57843137254902),.UNSPECIFIED.)
CURVE()
GEOMETRIC_REPRESENTATION_ITEM()
RATIONAL_B_SPLINE_CURVE((1.,0.866025403784439,1.,0.866025403784439,1.,0.866025403784439,
1.,0.866025403784439,1.,0.866025403784439,1.,0.866025403784439,1.))
REPRESENTATION_ITEM('')
);
#4384=(
BOUNDED_CURVE()
B_SPLINE_CURVE(2,(#410489,#410490,#410491,#410492,#410493,#410494,#410495,
#410496,#410497,#410498,#410499,#410500,#410501),.UNSPECIFIED.,.F.,.F.)
B_SPLINE_CURVE_WITH_KNOTS((3,2,2,2,2,2,3),(0.558823529411765,0.562091503267974,
0.565359477124183,0.568627450980392,0.571895424836601,0.57516339869281,
0.57843137254902),.UNSPECIFIED.)
CURVE()
GEOMETRIC_REPRESENTATION_ITEM()
RATIONAL_B_SPLINE_CURVE((1.,0.866025403784439,1.,0.866025403784439,1.,0.866025403784439,
1.,0.866025403784439,1.,0.866025403784439,1.,0.866025403784439,1.))
REPRESENTATION_ITEM('')
);
#4385=(
BOUNDED_CURVE()
B_SPLINE_CURVE(2,(#410506,#410507,#410508,#410509,#410510,#410511,#410512,
#410513,#410514,#410515,#410516,#410517,#410518),.UNSPECIFIED.,.F.,.F.)
B_SPLINE_CURVE_WITH_KNOTS((3,2,2,2,2,2,3),(0.57843137254902,0.581699346405229,
0.584967320261438,0.588235294117647,0.591503267973856,0.594771241830065,
0.598039215686274),.UNSPECIFIED.)
CURVE()
GEOMETRIC_REPRESENTATION_ITEM()
RATIONAL_B_SPLINE_CURVE((1.,0.866025403784439,1.,0.866025403784439,1.,0.866025403784439,
1.,0.866025403784439,1.,0.866025403784439,1.,0.866025403784439,1.))
REPRESENTATION_ITEM('')
);
#4386=(
BOUNDED_CURVE()
B_SPLINE_CURVE(2,(#410519,#410520,#410521,#410522,#410523,#410524,#410525,
#410526,#410527,#410528,#410529,#410530,#410531),.UNSPECIFIED.,.F.,.F.)
B_SPLINE_CURVE_WITH_KNOTS((3,2,2,2,2,2,3),(0.57843137254902,0.581699346405229,
0.584967320261438,0.588235294117647,0.591503267973856,0.594771241830065,
0.598039215686274),.UNSPECIFIED.)
CURVE()
GEOMETRIC_REPRESENTATION_ITEM()
RATIONAL_B_SPLINE_CURVE((1.,0.866025403784439,1.,0.866025403784439,1.,0.866025403784439,
1.,0.866025403784439,1.,0.866025403784439,1.,0.866025403784439,1.))
REPRESENTATION_ITEM('')
);
#4387=(
BOUNDED_CURVE()
B_SPLINE_CURVE(2,(#410536,#410537,#410538,#410539,#410540,#410541,#410542,
#410543,#410544,#410545,#410546,#410547,#410548),.UNSPECIFIED.,.F.,.F.)
B_SPLINE_CURVE_WITH_KNOTS((3,2,2,2,2,2,3),(0.598039215686274,0.601307189542484,
0.604575163398693,0.607843137254902,0.611111111111111,0.61437908496732,
0.617647058823529),.UNSPECIFIED.)
CURVE()
GEOMETRIC_REPRESENTATION_ITEM()
RATIONAL_B_SPLINE_CURVE((1.,0.866025403784439,1.,0.866025403784439,1.,0.866025403784439,
1.,0.866025403784439,1.,0.866025403784439,1.,0.866025403784439,1.))
REPRESENTATION_ITEM('')
);
#4388=(
BOUNDED_CURVE()
B_SPLINE_CURVE(2,(#410549,#410550,#410551,#410552,#410553,#410554,#410555,
#410556,#410557,#410558,#410559,#410560,#410561),.UNSPECIFIED.,.F.,.F.)
B_SPLINE_CURVE_WITH_KNOTS((3,2,2,2,2,2,3),(0.598039215686274,0.601307189542484,
0.604575163398693,0.607843137254902,0.611111111111111,0.61437908496732,
0.617647058823529),.UNSPECIFIED.)
CURVE()
GEOMETRIC_REPRESENTATION_ITEM()
RATIONAL_B_SPLINE_CURVE((1.,0.866025403784439,1.,0.866025403784439,1.,0.866025403784439,
1.,0.866025403784439,1.,0.866025403784439,1.,0.866025403784439,1.))
REPRESENTATION_ITEM('')
);
#4389=(
BOUNDED_CURVE()
B_SPLINE_CURVE(2,(#410566,#410567,#410568,#410569,#410570,#410571,#410572,
#410573,#410574,#410575,#410576,#410577,#410578),.UNSPECIFIED.,.F.,.F.)
B_SPLINE_CURVE_WITH_KNOTS((3,2,2,2,2,2,3),(0.617647058823529,0.620915032679739,
0.624183006535948,0.627450980392157,0.630718954248366,0.633986928104575,
0.637254901960784),.UNSPECIFIED.)
CURVE()
GEOMETRIC_REPRESENTATION_ITEM()
RATIONAL_B_SPLINE_CURVE((1.,0.866025403784439,1.,0.866025403784439,1.,0.866025403784439,
1.,0.866025403784439,1.,0.866025403784439,1.,0.866025403784439,1.))
REPRESENTATION_ITEM('')
);
#4390=(
BOUNDED_CURVE()
B_SPLINE_CURVE(2,(#410579,#410580,#410581,#410582,#410583,#410584,#410585,
#410586,#410587,#410588,#410589,#410590,#410591),.UNSPECIFIED.,.F.,.F.)
B_SPLINE_CURVE_WITH_KNOTS((3,2,2,2,2,2,3),(0.617647058823529,0.620915032679739,
0.624183006535948,0.627450980392157,0.630718954248366,0.633986928104575,
0.637254901960784),.UNSPECIFIED.)
CURVE()
GEOMETRIC_REPRESENTATION_ITEM()
RATIONAL_B_SPLINE_CURVE((1.,0.866025403784439,1.,0.866025403784439,1.,0.866025403784439,
1.,0.866025403784439,1.,0.866025403784439,1.,0.866025403784439,1.))
REPRESENTATION_ITEM('')
);
#4391=(
BOUNDED_CURVE()
B_SPLINE_CURVE(2,(#410596,#410597,#410598,#410599,#410600,#410601,#410602,
#410603,#410604,#410605,#410606,#410607,#410608),.UNSPECIFIED.,.F.,.F.)
B_SPLINE_CURVE_WITH_KNOTS((3,2,2,2,2,2,3),(0.637254901960784,0.640522875816993,
0.643790849673203,0.647058823529412,0.650326797385621,0.65359477124183,
0.656862745098039),.UNSPECIFIED.)
CURVE()
GEOMETRIC_REPRESENTATION_ITEM()
RATIONAL_B_SPLINE_CURVE((1.,0.866025403784439,1.,0.866025403784439,1.,0.866025403784439,
1.,0.866025403784439,1.,0.866025403784439,1.,0.866025403784439,1.))
REPRESENTATION_ITEM('')
);
#4392=(
BOUNDED_CURVE()
B_SPLINE_CURVE(2,(#410609,#410610,#410611,#410612,#410613,#410614,#410615,
#410616,#410617,#410618,#410619,#410620,#410621),.UNSPECIFIED.,.F.,.F.)
B_SPLINE_CURVE_WITH_KNOTS((3,2,2,2,2,2,3),(0.637254901960784,0.640522875816993,
0.643790849673203,0.647058823529412,0.650326797385621,0.65359477124183,
0.656862745098039),.UNSPECIFIED.)
CURVE()
GEOMETRIC_REPRESENTATION_ITEM()
RATIONAL_B_SPLINE_CURVE((1.,0.866025403784439,1.,0.866025403784439,1.,0.866025403784439,
1.,0.866025403784439,1.,0.866025403784439,1.,0.866025403784439,1.))
REPRESENTATION_ITEM('')
);
#4393=(
BOUNDED_CURVE()
B_SPLINE_CURVE(2,(#410626,#410627,#410628,#410629,#410630,#410631,#410632,
#410633,#410634,#410635,#410636,#410637,#410638),.UNSPECIFIED.,.F.,.F.)
B_SPLINE_CURVE_WITH_KNOTS((3,2,2,2,2,2,3),(0.656862745098039,0.660130718954248,
0.663398692810457,0.666666666666667,0.669934640522876,0.673202614379085,
0.676470588235294),.UNSPECIFIED.)
CURVE()
GEOMETRIC_REPRESENTATION_ITEM()
RATIONAL_B_SPLINE_CURVE((1.,0.866025403784439,1.,0.866025403784439,1.,0.866025403784439,
1.,0.866025403784439,1.,0.866025403784439,1.,0.866025403784439,1.))
REPRESENTATION_ITEM('')
);
#4394=(
BOUNDED_CURVE()
B_SPLINE_CURVE(2,(#410639,#410640,#410641,#410642,#410643,#410644,#410645,
#410646,#410647,#410648,#410649,#410650,#410651),.UNSPECIFIED.,.F.,.F.)
B_SPLINE_CURVE_WITH_KNOTS((3,2,2,2,2,2,3),(0.656862745098039,0.660130718954248,
0.663398692810457,0.666666666666667,0.669934640522876,0.673202614379085,
0.676470588235294),.UNSPECIFIED.)
CURVE()
GEOMETRIC_REPRESENTATION_ITEM()
RATIONAL_B_SPLINE_CURVE((1.,0.866025403784439,1.,0.866025403784439,1.,0.866025403784439,
1.,0.866025403784439,1.,0.866025403784439,1.,0.866025403784439,1.))
REPRESENTATION_ITEM('')
);
#4395=(
BOUNDED_CURVE()
B_SPLINE_CURVE(2,(#410656,#410657,#410658,#410659,#410660,#410661,#410662,
#410663,#410664,#410665,#410666,#410667,#410668),.UNSPECIFIED.,.F.,.F.)
B_SPLINE_CURVE_WITH_KNOTS((3,2,2,2,2,2,3),(0.676470588235294,0.679738562091503,
0.683006535947712,0.686274509803922,0.689542483660131,0.69281045751634,
0.696078431372549),.UNSPECIFIED.)
CURVE()
GEOMETRIC_REPRESENTATION_ITEM()
RATIONAL_B_SPLINE_CURVE((1.,0.866025403784439,1.,0.866025403784439,1.,0.866025403784439,
1.,0.866025403784439,1.,0.866025403784439,1.,0.866025403784439,1.))
REPRESENTATION_ITEM('')
);
#4396=(
BOUNDED_CURVE()
B_SPLINE_CURVE(2,(#410669,#410670,#410671,#410672,#410673,#410674,#410675,
#410676,#410677,#410678,#410679,#410680,#410681),.UNSPECIFIED.,.F.,.F.)
B_SPLINE_CURVE_WITH_KNOTS((3,2,2,2,2,2,3),(0.676470588235294,0.679738562091503,
0.683006535947712,0.686274509803922,0.689542483660131,0.69281045751634,
0.696078431372549),.UNSPECIFIED.)
CURVE()
GEOMETRIC_REPRESENTATION_ITEM()
RATIONAL_B_SPLINE_CURVE((1.,0.866025403784439,1.,0.866025403784439,1.,0.866025403784439,
1.,0.866025403784439,1.,0.866025403784439,1.,0.866025403784439,1.))
REPRESENTATION_ITEM('')
);
#4397=(
BOUNDED_CURVE()
B_SPLINE_CURVE(2,(#414250,#414251,#414252),.UNSPECIFIED.,.F.,.F.)
B_SPLINE_CURVE_WITH_KNOTS((3,3),(0.127655147271297,0.355324362692749),
 .UNSPECIFIED.)
CURVE()
GEOMETRIC_REPRESENTATION_ITEM()
RATIONAL_B_SPLINE_CURVE((1.37128129211021,1.58341924626905,1.37128129211021))
REPRESENTATION_ITEM('')
);
#4398=(
BOUNDED_CURVE()
B_SPLINE_CURVE(2,(#420116,#420117,#420118),.UNSPECIFIED.,.F.,.F.)
B_SPLINE_CURVE_WITH_KNOTS((3,3),(-0.35532436269275,-0.127655147271297),
 .UNSPECIFIED.)
CURVE()
GEOMETRIC_REPRESENTATION_ITEM()
RATIONAL_B_SPLINE_CURVE((1.37128129211021,1.58341924626905,1.37128129211021))
REPRESENTATION_ITEM('')
);
#4399=(
BOUNDED_CURVE()
B_SPLINE_CURVE(2,(#420126,#420127,#420128),.UNSPECIFIED.,.F.,.F.)
B_SPLINE_CURVE_WITH_KNOTS((3,3),(-0.355324362692752,-0.127655147271298),
 .UNSPECIFIED.)
CURVE()
GEOMETRIC_REPRESENTATION_ITEM()
RATIONAL_B_SPLINE_CURVE((1.37128129211021,1.58341924626906,1.37128129211021))
REPRESENTATION_ITEM('')
);
#4400=(
BOUNDED_CURVE()
B_SPLINE_CURVE(2,(#420131,#420132,#420133),.UNSPECIFIED.,.F.,.F.)
B_SPLINE_CURVE_WITH_KNOTS((3,3),(-0.355324362692752,-0.127655147271297),
 .UNSPECIFIED.)
CURVE()
GEOMETRIC_REPRESENTATION_ITEM()
RATIONAL_B_SPLINE_CURVE((1.37128129211021,1.58341924626906,1.37128129211021))
REPRESENTATION_ITEM('')
);
#4401=(
BOUNDED_CURVE()
B_SPLINE_CURVE(2,(#420136,#420137,#420138),.UNSPECIFIED.,.F.,.F.)
B_SPLINE_CURVE_WITH_KNOTS((3,3),(-0.35532436269275,-0.127655147271297),
 .UNSPECIFIED.)
CURVE()
GEOMETRIC_REPRESENTATION_ITEM()
RATIONAL_B_SPLINE_CURVE((1.37128129211021,1.58341924626905,1.37128129211021))
REPRESENTATION_ITEM('')
);
#4402=(
BOUNDED_CURVE()
B_SPLINE_CURVE(2,(#420140,#420141,#420142),.UNSPECIFIED.,.F.,.F.)
B_SPLINE_CURVE_WITH_KNOTS((3,3),(-0.35532436269275,-0.127655147271297),
 .UNSPECIFIED.)
CURVE()
GEOMETRIC_REPRESENTATION_ITEM()
RATIONAL_B_SPLINE_CURVE((1.37128129211021,1.58341924626905,1.37128129211021))
REPRESENTATION_ITEM('')
);
#4403=(
BOUNDED_CURVE()
B_SPLINE_CURVE(2,(#421377,#421378,#421379,#421380,#421381),
 .UNSPECIFIED.,.F.,.F.)
B_SPLINE_CURVE_WITH_KNOTS((3,2,3),(0.696078431372549,0.699346405228758,
0.700529377982283),.UNSPECIFIED.)
CURVE()
GEOMETRIC_REPRESENTATION_ITEM()
RATIONAL_B_SPLINE_CURVE((1.,0.866025403784439,1.,0.951502581121805,0.938116290834926))
REPRESENTATION_ITEM('')
);
#4404=(
BOUNDED_CURVE()
B_SPLINE_CURVE(2,(#421383,#421384,#421385,#421386,#421387,#421388,#421389),
 .UNSPECIFIED.,.F.,.F.)
B_SPLINE_CURVE_WITH_KNOTS((3,2,2,3),(0.696078431372549,0.699346405228758,
0.702614379084967,0.7029856219326),.UNSPECIFIED.)
CURVE()
GEOMETRIC_REPRESENTATION_ITEM()
RATIONAL_B_SPLINE_CURVE((1.,0.866025403784439,1.,0.866025403784439,1.,0.984780444153479,
0.973018780873287))
REPRESENTATION_ITEM('')
);
#4420=SHAPE_REPRESENTATION_RELATIONSHIP('SRR','None',#459346,#4441);
#4441=ADVANCED_BREP_SHAPE_REPRESENTATION('',(#4488),#459235);
#4488=MANIFOLD_SOLID_BREP('Body',#94666);
#4608=STYLED_ITEM('',(#459533),#4488);
#5014=CONICAL_SURFACE('',#102686,999.999999999989,0.785398163397443);
#5015=CONICAL_SURFACE('',#102688,1.17524047358087,0.785398163397454);
#5016=CONICAL_SURFACE('',#103115,1.17524047358087,0.785398163397454);
#5017=CONICAL_SURFACE('',#103117,1.50000000000006,0.785398163397447);
#5018=CONICAL_SURFACE('',#103119,999.999999999989,0.785398163397443);
#5019=CONICAL_SURFACE('',#103120,1.25,1.0471975511966);
#5020=CONICAL_SURFACE('',#103127,1.44337567297406,0.78539816339745);
#5021=CONICAL_SURFACE('',#103133,2.55577460325564,0.785398163397375);
#5022=CONICAL_SURFACE('',#103138,2.72422539674441,0.785398163397447);
#5023=CONICAL_SURFACE('',#103557,1.44337567297406,0.78539816339745);
#5024=CONICAL_SURFACE('',#103558,1.44337567297406,0.78539816339745);
#5025=CONICAL_SURFACE('',#103559,1.44337567297406,0.78539816339745);
#5026=CONICAL_SURFACE('',#103560,1.44337567297406,0.78539816339745);
#5027=CONICAL_SURFACE('',#103561,1.44337567297406,0.78539816339745);
#5028=CONICAL_SURFACE('',#103564,2.75,0.78539816339745);
#5029=CONICAL_SURFACE('',#103598,2.75,0.78539816339745);
#5030=CONICAL_SURFACE('',#103619,2.75,0.78539816339745);
#5031=CONICAL_SURFACE('',#103640,2.75,0.78539816339745);
#5032=CONICAL_SURFACE('',#103661,2.75,0.78539816339745);
#5033=CONICAL_SURFACE('',#103682,2.75,0.78539816339745);
#5034=CONICAL_SURFACE('',#103703,2.75,0.78539816339745);
#5035=CONICAL_SURFACE('',#103724,2.75,0.78539816339745);
#5036=CONICAL_SURFACE('',#103745,2.75,0.78539816339745);
#5037=CONICAL_SURFACE('',#103766,2.75,0.78539816339745);
#5038=CONICAL_SURFACE('',#103787,2.75,0.78539816339745);
#5039=CONICAL_SURFACE('',#103808,2.75,0.78539816339745);
#5040=CONICAL_SURFACE('',#103829,2.75,0.78539816339745);
#5041=CONICAL_SURFACE('',#103850,2.75,0.78539816339745);
#5042=CONICAL_SURFACE('',#103871,2.75,0.78539816339745);
#5043=CONICAL_SURFACE('',#103892,2.75,0.78539816339745);
#5044=CONICAL_SURFACE('',#103913,2.75,0.78539816339745);
#5045=CONICAL_SURFACE('',#103934,2.75,0.78539816339745);
#5046=CONICAL_SURFACE('',#103955,2.75,0.78539816339745);
#5047=CONICAL_SURFACE('',#103976,2.75,0.78539816339745);
#5048=CONICAL_SURFACE('',#103997,2.75,0.78539816339745);
#5049=CONICAL_SURFACE('',#104018,2.75,0.78539816339745);
#5050=CONICAL_SURFACE('',#104039,2.75,0.78539816339745);
#5051=CONICAL_SURFACE('',#104060,2.75,0.78539816339745);
#5052=CONICAL_SURFACE('',#104081,2.75,0.78539816339745);
#5053=CONICAL_SURFACE('',#104102,2.75,0.78539816339745);
#5054=CONICAL_SURFACE('',#104123,2.75,0.78539816339745);
#5055=CONICAL_SURFACE('',#104144,2.75,0.78539816339745);
#5056=CONICAL_SURFACE('',#104165,2.75,0.78539816339745);
#5057=CONICAL_SURFACE('',#104186,2.75,0.78539816339745);
#5058=CONICAL_SURFACE('',#104207,2.75,0.78539816339745);
#5059=CONICAL_SURFACE('',#104228,2.75,0.78539816339745);
#5060=CONICAL_SURFACE('',#104249,2.75,0.78539816339745);
#5061=CONICAL_SURFACE('',#104270,2.75,0.78539816339745);
#5062=CONICAL_SURFACE('',#104291,2.75,0.78539816339745);
#5063=CONICAL_SURFACE('',#104312,2.75,0.78539816339745);
#5064=CONICAL_SURFACE('',#104333,2.75,0.78539816339745);
#5065=CONICAL_SURFACE('',#104354,2.75,0.78539816339745);
#5066=CONICAL_SURFACE('',#104375,2.75,0.78539816339745);
#5067=CONICAL_SURFACE('',#104396,2.75,0.78539816339745);
#5068=CONICAL_SURFACE('',#104417,2.75,0.78539816339745);
#5069=CONICAL_SURFACE('',#104438,2.75,0.78539816339745);
#5070=CONICAL_SURFACE('',#104459,2.75,0.78539816339745);
#5071=CONICAL_SURFACE('',#104480,2.75,0.78539816339745);
#5072=CONICAL_SURFACE('',#104501,2.75,0.78539816339745);
#5073=CONICAL_SURFACE('',#104522,2.75,0.78539816339745);
#5074=CONICAL_SURFACE('',#104543,2.75,0.78539816339745);
#5075=CONICAL_SURFACE('',#104564,2.75,0.78539816339745);
#5076=CONICAL_SURFACE('',#104585,2.75,0.78539816339745);
#5077=CONICAL_SURFACE('',#104606,2.75,0.78539816339745);
#5078=CONICAL_SURFACE('',#104627,2.75,0.78539816339745);
#5079=CONICAL_SURFACE('',#104648,2.75,0.78539816339745);
#5080=CONICAL_SURFACE('',#104669,2.75,0.78539816339745);
#5081=CONICAL_SURFACE('',#104690,2.75,0.78539816339745);
#5082=CONICAL_SURFACE('',#104711,2.75,0.78539816339745);
#5083=CONICAL_SURFACE('',#104732,2.75,0.78539816339745);
#5084=CONICAL_SURFACE('',#104753,2.75,0.78539816339745);
#5085=CONICAL_SURFACE('',#104774,2.75,0.78539816339745);
#5086=CONICAL_SURFACE('',#104795,2.75,0.78539816339745);
#5087=CONICAL_SURFACE('',#104816,2.75,0.78539816339745);
#5088=CONICAL_SURFACE('',#104837,2.75,0.78539816339745);
#5089=CONICAL_SURFACE('',#104858,2.75,0.78539816339745);
#5090=CONICAL_SURFACE('',#104879,2.75,0.78539816339745);
#5091=CONICAL_SURFACE('',#104900,2.75,0.78539816339745);
#5092=CONICAL_SURFACE('',#104921,2.75,0.78539816339745);
#5093=CONICAL_SURFACE('',#104942,2.75,0.78539816339745);
#5094=CONICAL_SURFACE('',#104963,2.75,0.78539816339745);
#5095=CONICAL_SURFACE('',#104984,2.75,0.78539816339745);
#5096=CONICAL_SURFACE('',#105005,2.75,0.78539816339745);
#5097=CONICAL_SURFACE('',#105026,2.75,0.78539816339745);
#5098=CONICAL_SURFACE('',#105047,2.75,0.78539816339745);
#5099=CONICAL_SURFACE('',#105068,2.75,0.78539816339745);
#5100=CONICAL_SURFACE('',#105089,2.75,0.78539816339745);
#5101=CONICAL_SURFACE('',#105110,2.75,0.78539816339745);
#5102=CONICAL_SURFACE('',#105131,2.75,0.78539816339745);
#5103=CONICAL_SURFACE('',#105152,2.75,0.78539816339745);
#5104=CONICAL_SURFACE('',#105173,2.75,0.78539816339745);
#5228=FACE_BOUND('',#16574,.T.);
#5229=FACE_BOUND('',#16581,.T.);
#5937=PLANE('',#103531);
#5938=PLANE('',#103533);
#5939=PLANE('',#103535);
#5940=PLANE('',#103536);
#5941=PLANE('',#103537);
#5942=PLANE('',#103538);
#5943=PLANE('',#103539);
#5944=PLANE('',#103540);
#5945=PLANE('',#103541);
#5946=PLANE('',#103550);
#5947=PLANE('',#103551);
#5948=PLANE('',#103552);
#5949=PLANE('',#103553);
#5950=PLANE('',#103554);
#5951=PLANE('',#103555);
#5952=PLANE('',#103556);
#5953=PLANE('',#103562);
#5954=PLANE('',#103578);
#5955=PLANE('',#103580);
#5956=PLANE('',#103599);
#5957=PLANE('',#103601);
#5958=PLANE('',#103620);
#5959=PLANE('',#103622);
#5960=PLANE('',#103641);
#5961=PLANE('',#103643);
#5962=PLANE('',#103662);
#5963=PLANE('',#103664);
#5964=PLANE('',#103683);
#5965=PLANE('',#103685);
#5966=PLANE('',#103704);
#5967=PLANE('',#103706);
#5968=PLANE('',#103725);
#5969=PLANE('',#103727);
#5970=PLANE('',#103746);
#5971=PLANE('',#103748);
#5972=PLANE('',#103767);
#5973=PLANE('',#103769);
#5974=PLANE('',#103788);
#5975=PLANE('',#103790);
#5976=PLANE('',#103809);
#5977=PLANE('',#103811);
#5978=PLANE('',#103830);
#5979=PLANE('',#103832);
#5980=PLANE('',#103851);
#5981=PLANE('',#103853);
#5982=PLANE('',#103872);
#5983=PLANE('',#103874);
#5984=PLANE('',#103893);
#5985=PLANE('',#103895);
#5986=PLANE('',#103914);
#5987=PLANE('',#103916);
#5988=PLANE('',#103935);
#5989=PLANE('',#103937);
#5990=PLANE('',#103956);
#5991=PLANE('',#103958);
#5992=PLANE('',#103977);
#5993=PLANE('',#103979);
#5994=PLANE('',#103998);
#5995=PLANE('',#104000);
#5996=PLANE('',#104019);
#5997=PLANE('',#104021);
#5998=PLANE('',#104040);
#5999=PLANE('',#104042);
#6000=PLANE('',#104061);
#6001=PLANE('',#104063);
#6002=PLANE('',#104082);
#6003=PLANE('',#104084);
#6004=PLANE('',#104103);
#6005=PLANE('',#104105);
#6006=PLANE('',#104124);
#6007=PLANE('',#104126);
#6008=PLANE('',#104145);
#6009=PLANE('',#104147);
#6010=PLANE('',#104166);
#6011=PLANE('',#104168);
#6012=PLANE('',#104187);
#6013=PLANE('',#104189);
#6014=PLANE('',#104208);
#6015=PLANE('',#104210);
#6016=PLANE('',#104229);
#6017=PLANE('',#104231);
#6018=PLANE('',#104250);
#6019=PLANE('',#104252);
#6020=PLANE('',#104271);
#6021=PLANE('',#104273);
#6022=PLANE('',#104292);
#6023=PLANE('',#104294);
#6024=PLANE('',#104313);
#6025=PLANE('',#104315);
#6026=PLANE('',#104334);
#6027=PLANE('',#104336);
#6028=PLANE('',#104355);
#6029=PLANE('',#104357);
#6030=PLANE('',#104376);
#6031=PLANE('',#104378);
#6032=PLANE('',#104397);
#6033=PLANE('',#104399);
#6034=PLANE('',#104418);
#6035=PLANE('',#104420);
#6036=PLANE('',#104439);
#6037=PLANE('',#104441);
#6038=PLANE('',#104460);
#6039=PLANE('',#104462);
#6040=PLANE('',#104481);
#6041=PLANE('',#104483);
#6042=PLANE('',#104502);
#6043=PLANE('',#104504);
#6044=PLANE('',#104523);
#6045=PLANE('',#104525);
#6046=PLANE('',#104544);
#6047=PLANE('',#104546);
#6048=PLANE('',#104565);
#6049=PLANE('',#104567);
#6050=PLANE('',#104586);
#6051=PLANE('',#104588);
#6052=PLANE('',#104607);
#6053=PLANE('',#104609);
#6054=PLANE('',#104628);
#6055=PLANE('',#104630);
#6056=PLANE('',#104649);
#6057=PLANE('',#104651);
#6058=PLANE('',#104670);
#6059=PLANE('',#104672);
#6060=PLANE('',#104691);
#6061=PLANE('',#104693);
#6062=PLANE('',#104712);
#6063=PLANE('',#104714);
#6064=PLANE('',#104733);
#6065=PLANE('',#104735);
#6066=PLANE('',#104754);
#6067=PLANE('',#104756);
#6068=PLANE('',#104775);
#6069=PLANE('',#104777);
#6070=PLANE('',#104796);
#6071=PLANE('',#104798);
#6072=PLANE('',#104817);
#6073=PLANE('',#104819);
#6074=PLANE('',#104838);
#6075=PLANE('',#104840);
#6076=PLANE('',#104859);
#6077=PLANE('',#104861);
#6078=PLANE('',#104880);
#6079=PLANE('',#104882);
#6080=PLANE('',#104901);
#6081=PLANE('',#104903);
#6082=PLANE('',#104922);
#6083=PLANE('',#104924);
#6084=PLANE('',#104943);
#6085=PLANE('',#104945);
#6086=PLANE('',#104964);
#6087=PLANE('',#104966);
#6088=PLANE('',#104985);
#6089=PLANE('',#104987);
#6090=PLANE('',#105006);
#6091=PLANE('',#105008);
#6092=PLANE('',#105027);
#6093=PLANE('',#105029);
#6094=PLANE('',#105048);
#6095=PLANE('',#105050);
#6096=PLANE('',#105069);
#6097=PLANE('',#105071);
#6098=PLANE('',#105090);
#6099=PLANE('',#105092);
#6100=PLANE('',#105111);
#6101=PLANE('',#105113);
#6102=PLANE('',#105132);
#6103=PLANE('',#105134);
#6104=PLANE('',#105153);
#6105=PLANE('',#105155);
#10409=FACE_OUTER_BOUND('',#16332,.T.);
#10410=FACE_OUTER_BOUND('',#16333,.T.);
#10411=FACE_OUTER_BOUND('',#16334,.T.);
#10412=FACE_OUTER_BOUND('',#16335,.T.);
#10413=FACE_OUTER_BOUND('',#16336,.T.);
#10414=FACE_OUTER_BOUND('',#16337,.T.);
#10415=FACE_OUTER_BOUND('',#16338,.T.);
#10416=FACE_OUTER_BOUND('',#16339,.T.);
#10417=FACE_OUTER_BOUND('',#16340,.T.);
#10418=FACE_OUTER_BOUND('',#16341,.T.);
#10419=FACE_OUTER_BOUND('',#16342,.T.);
#10420=FACE_OUTER_BOUND('',#16343,.T.);
#10421=FACE_OUTER_BOUND('',#16344,.T.);
#10422=FACE_OUTER_BOUND('',#16345,.T.);
#10423=FACE_OUTER_BOUND('',#16346,.T.);
#10424=FACE_OUTER_BOUND('',#16347,.T.);
#10425=FACE_OUTER_BOUND('',#16348,.T.);
#10426=FACE_OUTER_BOUND('',#16349,.T.);
#10427=FACE_OUTER_BOUND('',#16350,.T.);
#10428=FACE_OUTER_BOUND('',#16351,.T.);
#10429=FACE_OUTER_BOUND('',#16352,.T.);
#10430=FACE_OUTER_BOUND('',#16353,.T.);
#10431=FACE_OUTER_BOUND('',#16354,.T.);
#10432=FACE_OUTER_BOUND('',#16355,.T.);
#10433=FACE_OUTER_BOUND('',#16356,.T.);
#10434=FACE_OUTER_BOUND('',#16357,.T.);
#10435=FACE_OUTER_BOUND('',#16358,.T.);
#10436=FACE_OUTER_BOUND('',#16359,.T.);
#10437=FACE_OUTER_BOUND('',#16360,.T.);
#10438=FACE_OUTER_BOUND('',#16361,.T.);
#10439=FACE_OUTER_BOUND('',#16362,.T.);
#10440=FACE_OUTER_BOUND('',#16363,.T.);
#10441=FACE_OUTER_BOUND('',#16364,.T.);
#10442=FACE_OUTER_BOUND('',#16365,.T.);
#10443=FACE_OUTER_BOUND('',#16366,.T.);
#10444=FACE_OUTER_BOUND('',#16367,.T.);
#10445=FACE_OUTER_BOUND('',#16368,.T.);
#10446=FACE_OUTER_BOUND('',#16369,.T.);
#10447=FACE_OUTER_BOUND('',#16370,.T.);
#10448=FACE_OUTER_BOUND('',#16371,.T.);
#10449=FACE_OUTER_BOUND('',#16372,.T.);
#10450=FACE_OUTER_BOUND('',#16373,.T.);
#10451=FACE_OUTER_BOUND('',#16374,.T.);
#10452=FACE_OUTER_BOUND('',#16375,.T.);
#10453=FACE_OUTER_BOUND('',#16376,.T.);
#10454=FACE_OUTER_BOUND('',#16377,.T.);
#10455=FACE_OUTER_BOUND('',#16378,.T.);
#10456=FACE_OUTER_BOUND('',#16379,.T.);
#10457=FACE_OUTER_BOUND('',#16380,.T.);
#10458=FACE_OUTER_BOUND('',#16381,.T.);
#10459=FACE_OUTER_BOUND('',#16382,.T.);
#10460=FACE_OUTER_BOUND('',#16383,.T.);
#10461=FACE_OUTER_BOUND('',#16384,.T.);
#10462=FACE_OUTER_BOUND('',#16385,.T.);
#10463=FACE_OUTER_BOUND('',#16386,.T.);
#10464=FACE_OUTER_BOUND('',#16387,.T.);
#10465=FACE_OUTER_BOUND('',#16388,.T.);
#10466=FACE_OUTER_BOUND('',#16389,.T.);
#10467=FACE_OUTER_BOUND('',#16390,.T.);
#10468=FACE_OUTER_BOUND('',#16391,.T.);
#10469=FACE_OUTER_BOUND('',#16392,.T.);
#10470=FACE_OUTER_BOUND('',#16393,.T.);
#10471=FACE_OUTER_BOUND('',#16394,.T.);
#10472=FACE_OUTER_BOUND('',#16395,.T.);
#10473=FACE_OUTER_BOUND('',#16396,.T.);
#10474=FACE_OUTER_BOUND('',#16397,.T.);
#10475=FACE_OUTER_BOUND('',#16398,.T.);
#10476=FACE_OUTER_BOUND('',#16399,.T.);
#10477=FACE_OUTER_BOUND('',#16400,.T.);
#10478=FACE_OUTER_BOUND('',#16401,.T.);
#10479=FACE_OUTER_BOUND('',#16402,.T.);
#10480=FACE_OUTER_BOUND('',#16403,.T.);
#10481=FACE_OUTER_BOUND('',#16404,.T.);
#10482=FACE_OUTER_BOUND('',#16405,.T.);
#10483=FACE_OUTER_BOUND('',#16406,.T.);
#10484=FACE_OUTER_BOUND('',#16407,.T.);
#10485=FACE_OUTER_BOUND('',#16408,.T.);
#10486=FACE_OUTER_BOUND('',#16409,.T.);
#10487=FACE_OUTER_BOUND('',#16410,.T.);
#10488=FACE_OUTER_BOUND('',#16411,.T.);
#10489=FACE_OUTER_BOUND('',#16412,.T.);
#10490=FACE_OUTER_BOUND('',#16413,.T.);
#10491=FACE_OUTER_BOUND('',#16414,.T.);
#10492=FACE_OUTER_BOUND('',#16415,.T.);
#10493=FACE_OUTER_BOUND('',#16416,.T.);
#10494=FACE_OUTER_BOUND('',#16417,.T.);
#10495=FACE_OUTER_BOUND('',#16418,.T.);
#10496=FACE_OUTER_BOUND('',#16419,.T.);
#10497=FACE_OUTER_BOUND('',#16420,.T.);
#10498=FACE_OUTER_BOUND('',#16421,.T.);
#10499=FACE_OUTER_BOUND('',#16422,.T.);
#10500=FACE_OUTER_BOUND('',#16423,.T.);
#10501=FACE_OUTER_BOUND('',#16424,.T.);
#10502=FACE_OUTER_BOUND('',#16425,.T.);
#10503=FACE_OUTER_BOUND('',#16426,.T.);
#10504=FACE_OUTER_BOUND('',#16427,.T.);
#10505=FACE_OUTER_BOUND('',#16428,.T.);
#10506=FACE_OUTER_BOUND('',#16429,.T.);
#10507=FACE_OUTER_BOUND('',#16430,.T.);
#10508=FACE_OUTER_BOUND('',#16431,.T.);
#10509=FACE_OUTER_BOUND('',#16432,.T.);
#10510=FACE_OUTER_BOUND('',#16433,.T.);
#10511=FACE_OUTER_BOUND('',#16434,.T.);
#10512=FACE_OUTER_BOUND('',#16435,.T.);
#10513=FACE_OUTER_BOUND('',#16436,.T.);
#10514=FACE_OUTER_BOUND('',#16437,.T.);
#10515=FACE_OUTER_BOUND('',#16438,.T.);
#10516=FACE_OUTER_BOUND('',#16439,.T.);
#10517=FACE_OUTER_BOUND('',#16440,.T.);
#10518=FACE_OUTER_BOUND('',#16441,.T.);
#10519=FACE_OUTER_BOUND('',#16442,.T.);
#10520=FACE_OUTER_BOUND('',#16443,.T.);
#10521=FACE_OUTER_BOUND('',#16444,.T.);
#10522=FACE_OUTER_BOUND('',#16445,.T.);
#10523=FACE_OUTER_BOUND('',#16446,.T.);
#10524=FACE_OUTER_BOUND('',#16447,.T.);
#10525=FACE_OUTER_BOUND('',#16448,.T.);
#10526=FACE_OUTER_BOUND('',#16449,.T.);
#10527=FACE_OUTER_BOUND('',#16450,.T.);
#10528=FACE_OUTER_BOUND('',#16451,.T.);
#10529=FACE_OUTER_BOUND('',#16452,.T.);
#10530=FACE_OUTER_BOUND('',#16453,.T.);
#10531=FACE_OUTER_BOUND('',#16454,.T.);
#10532=FACE_OUTER_BOUND('',#16455,.T.);
#10533=FACE_OUTER_BOUND('',#16456,.T.);
#10534=FACE_OUTER_BOUND('',#16457,.T.);
#10535=FACE_OUTER_BOUND('',#16458,.T.);
#10536=FACE_OUTER_BOUND('',#16459,.T.);
#10537=FACE_OUTER_BOUND('',#16460,.T.);
#10538=FACE_OUTER_BOUND('',#16461,.T.);
#10539=FACE_OUTER_BOUND('',#16462,.T.);
#10540=FACE_OUTER_BOUND('',#16463,.T.);
#10541=FACE_OUTER_BOUND('',#16464,.T.);
#10542=FACE_OUTER_BOUND('',#16465,.T.);
#10543=FACE_OUTER_BOUND('',#16466,.T.);
#10544=FACE_OUTER_BOUND('',#16467,.T.);
#10545=FACE_OUTER_BOUND('',#16468,.T.);
#10546=FACE_OUTER_BOUND('',#16469,.T.);
#10547=FACE_OUTER_BOUND('',#16470,.T.);
#10548=FACE_OUTER_BOUND('',#16471,.T.);
#10549=FACE_OUTER_BOUND('',#16472,.T.);
#10550=FACE_OUTER_BOUND('',#16473,.T.);
#10551=FACE_OUTER_BOUND('',#16474,.T.);
#10552=FACE_OUTER_BOUND('',#16475,.T.);
#10553=FACE_OUTER_BOUND('',#16476,.T.);
#10554=FACE_OUTER_BOUND('',#16477,.T.);
#10555=FACE_OUTER_BOUND('',#16478,.T.);
#10556=FACE_OUTER_BOUND('',#16479,.T.);
#10557=FACE_OUTER_BOUND('',#16480,.T.);
#10558=FACE_OUTER_BOUND('',#16481,.T.);
#10559=FACE_OUTER_BOUND('',#16482,.T.);
#10560=FACE_OUTER_BOUND('',#16483,.T.);
#10561=FACE_OUTER_BOUND('',#16484,.T.);
#10562=FACE_OUTER_BOUND('',#16485,.T.);
#10563=FACE_OUTER_BOUND('',#16486,.T.);
#10564=FACE_OUTER_BOUND('',#16487,.T.);
#10565=FACE_OUTER_BOUND('',#16488,.T.);
#10566=FACE_OUTER_BOUND('',#16489,.T.);
#10567=FACE_OUTER_BOUND('',#16490,.T.);
#10568=FACE_OUTER_BOUND('',#16491,.T.);
#10569=FACE_OUTER_BOUND('',#16492,.T.);
#10570=FACE_OUTER_BOUND('',#16493,.T.);
#10571=FACE_OUTER_BOUND('',#16494,.T.);
#10572=FACE_OUTER_BOUND('',#16495,.T.);
#10573=FACE_OUTER_BOUND('',#16496,.T.);
#10574=FACE_OUTER_BOUND('',#16497,.T.);
#10575=FACE_OUTER_BOUND('',#16498,.T.);
#10576=FACE_OUTER_BOUND('',#16499,.T.);
#10577=FACE_OUTER_BOUND('',#16500,.T.);
#10578=FACE_OUTER_BOUND('',#16501,.T.);
#10579=FACE_OUTER_BOUND('',#16502,.T.);
#10580=FACE_OUTER_BOUND('',#16503,.T.);
#10581=FACE_OUTER_BOUND('',#16504,.T.);
#10582=FACE_OUTER_BOUND('',#16505,.T.);
#10583=FACE_OUTER_BOUND('',#16506,.T.);
#10584=FACE_OUTER_BOUND('',#16507,.T.);
#10585=FACE_OUTER_BOUND('',#16508,.T.);
#10586=FACE_OUTER_BOUND('',#16509,.T.);
#10587=FACE_OUTER_BOUND('',#16510,.T.);
#10588=FACE_OUTER_BOUND('',#16511,.T.);
#10589=FACE_OUTER_BOUND('',#16512,.T.);
#10590=FACE_OUTER_BOUND('',#16513,.T.);
#10591=FACE_OUTER_BOUND('',#16514,.T.);
#10592=FACE_OUTER_BOUND('',#16515,.T.);
#10593=FACE_OUTER_BOUND('',#16516,.T.);
#10594=FACE_OUTER_BOUND('',#16517,.T.);
#10595=FACE_OUTER_BOUND('',#16518,.T.);
#10596=FACE_OUTER_BOUND('',#16519,.T.);
#10597=FACE_OUTER_BOUND('',#16520,.T.);
#10598=FACE_OUTER_BOUND('',#16521,.T.);
#10599=FACE_OUTER_BOUND('',#16522,.T.);
#10600=FACE_OUTER_BOUND('',#16523,.T.);
#10601=FACE_OUTER_BOUND('',#16524,.T.);
#10602=FACE_OUTER_BOUND('',#16525,.T.);
#10603=FACE_OUTER_BOUND('',#16526,.T.);
#10604=FACE_OUTER_BOUND('',#16527,.T.);
#10605=FACE_OUTER_BOUND('',#16528,.T.);
#10606=FACE_OUTER_BOUND('',#16529,.T.);
#10607=FACE_OUTER_BOUND('',#16530,.T.);
#10608=FACE_OUTER_BOUND('',#16531,.T.);
#10609=FACE_OUTER_BOUND('',#16532,.T.);
#10610=FACE_OUTER_BOUND('',#16533,.T.);
#10611=FACE_OUTER_BOUND('',#16534,.T.);
#10612=FACE_OUTER_BOUND('',#16535,.T.);
#10613=FACE_OUTER_BOUND('',#16536,.T.);
#10614=FACE_OUTER_BOUND('',#16537,.T.);
#10615=FACE_OUTER_BOUND('',#16538,.T.);
#10616=FACE_OUTER_BOUND('',#16539,.T.);
#10617=FACE_OUTER_BOUND('',#16540,.T.);
#10618=FACE_OUTER_BOUND('',#16541,.T.);
#10619=FACE_OUTER_BOUND('',#16542,.T.);
#10620=FACE_OUTER_BOUND('',#16543,.T.);
#10621=FACE_OUTER_BOUND('',#16544,.T.);
#10622=FACE_OUTER_BOUND('',#16545,.T.);
#10623=FACE_OUTER_BOUND('',#16546,.T.);
#10624=FACE_OUTER_BOUND('',#16547,.T.);
#10625=FACE_OUTER_BOUND('',#16548,.T.);
#10626=FACE_OUTER_BOUND('',#16549,.T.);
#10627=FACE_OUTER_BOUND('',#16550,.T.);
#10628=FACE_OUTER_BOUND('',#16551,.T.);
#10629=FACE_OUTER_BOUND('',#16552,.T.);
#10630=FACE_OUTER_BOUND('',#16553,.T.);
#10631=FACE_OUTER_BOUND('',#16554,.T.);
#10632=FACE_OUTER_BOUND('',#16555,.T.);
#10633=FACE_OUTER_BOUND('',#16556,.T.);
#10634=FACE_OUTER_BOUND('',#16557,.T.);
#10635=FACE_OUTER_BOUND('',#16558,.T.);
#10636=FACE_OUTER_BOUND('',#16559,.T.);
#10637=FACE_OUTER_BOUND('',#16560,.T.);
#10638=FACE_OUTER_BOUND('',#16561,.T.);
#10639=FACE_OUTER_BOUND('',#16562,.T.);
#10640=FACE_OUTER_BOUND('',#16563,.T.);
#10641=FACE_OUTER_BOUND('',#16564,.T.);
#10642=FACE_OUTER_BOUND('',#16565,.T.);
#10643=FACE_OUTER_BOUND('',#16566,.T.);
#10644=FACE_OUTER_BOUND('',#16567,.T.);
#10645=FACE_OUTER_BOUND('',#16568,.T.);
#10646=FACE_OUTER_BOUND('',#16569,.T.);
#10647=FACE_OUTER_BOUND('',#16570,.T.);
#10648=FACE_OUTER_BOUND('',#16571,.T.);
#10649=FACE_OUTER_BOUND('',#16572,.T.);
#10650=FACE_OUTER_BOUND('',#16573,.T.);
#10651=FACE_OUTER_BOUND('',#16575,.T.);
#10652=FACE_OUTER_BOUND('',#16576,.T.);
#10653=FACE_OUTER_BOUND('',#16577,.T.);
#10654=FACE_OUTER_BOUND('',#16578,.T.);
#10655=FACE_OUTER_BOUND('',#16579,.T.);
#10656=FACE_OUTER_BOUND('',#16580,.T.);
#10657=FACE_OUTER_BOUND('',#16582,.T.);
#10658=FACE_OUTER_BOUND('',#16583,.T.);
#10659=FACE_OUTER_BOUND('',#16584,.T.);
#10660=FACE_OUTER_BOUND('',#16585,.T.);
#10661=FACE_OUTER_BOUND('',#16586,.T.);
#10662=FACE_OUTER_BOUND('',#16587,.T.);
#10663=FACE_OUTER_BOUND('',#16588,.T.);
#10664=FACE_OUTER_BOUND('',#16589,.T.);
#10665=FACE_OUTER_BOUND('',#16590,.T.);
#10666=FACE_OUTER_BOUND('',#16591,.T.);
#10667=FACE_OUTER_BOUND('',#16592,.T.);
#10668=FACE_OUTER_BOUND('',#16593,.T.);
#10669=FACE_OUTER_BOUND('',#16594,.T.);
#10670=FACE_OUTER_BOUND('',#16595,.T.);
#10671=FACE_OUTER_BOUND('',#16596,.T.);
#10672=FACE_OUTER_BOUND('',#16597,.T.);
#10673=FACE_OUTER_BOUND('',#16598,.T.);
#10674=FACE_OUTER_BOUND('',#16599,.T.);
#10675=FACE_OUTER_BOUND('',#16600,.T.);
#10676=FACE_OUTER_BOUND('',#16601,.T.);
#10677=FACE_OUTER_BOUND('',#16602,.T.);
#10678=FACE_OUTER_BOUND('',#16603,.T.);
#10679=FACE_OUTER_BOUND('',#16604,.T.);
#10680=FACE_OUTER_BOUND('',#16605,.T.);
#10681=FACE_OUTER_BOUND('',#16606,.T.);
#10682=FACE_OUTER_BOUND('',#16607,.T.);
#10683=FACE_OUTER_BOUND('',#16608,.T.);
#10684=FACE_OUTER_BOUND('',#16609,.T.);
#10685=FACE_OUTER_BOUND('',#16610,.T.);
#10686=FACE_OUTER_BOUND('',#16611,.T.);
#10687=FACE_OUTER_BOUND('',#16612,.T.);
#10688=FACE_OUTER_BOUND('',#16613,.T.);
#10689=FACE_OUTER_BOUND('',#16614,.T.);
#10690=FACE_OUTER_BOUND('',#16615,.T.);
#10691=FACE_OUTER_BOUND('',#16616,.T.);
#10692=FACE_OUTER_BOUND('',#16617,.T.);
#10693=FACE_OUTER_BOUND('',#16618,.T.);
#10694=FACE_OUTER_BOUND('',#16619,.T.);
#10695=FACE_OUTER_BOUND('',#16620,.T.);
#10696=FACE_OUTER_BOUND('',#16621,.T.);
#10697=FACE_OUTER_BOUND('',#16622,.T.);
#10698=FACE_OUTER_BOUND('',#16623,.T.);
#10699=FACE_OUTER_BOUND('',#16624,.T.);
#10700=FACE_OUTER_BOUND('',#16625,.T.);
#10701=FACE_OUTER_BOUND('',#16626,.T.);
#10702=FACE_OUTER_BOUND('',#16627,.T.);
#10703=FACE_OUTER_BOUND('',#16628,.T.);
#10704=FACE_OUTER_BOUND('',#16629,.T.);
#10705=FACE_OUTER_BOUND('',#16630,.T.);
#10706=FACE_OUTER_BOUND('',#16631,.T.);
#10707=FACE_OUTER_BOUND('',#16632,.T.);
#10708=FACE_OUTER_BOUND('',#16633,.T.);
#10709=FACE_OUTER_BOUND('',#16634,.T.);
#10710=FACE_OUTER_BOUND('',#16635,.T.);
#10711=FACE_OUTER_BOUND('',#16636,.T.);
#10712=FACE_OUTER_BOUND('',#16637,.T.);
#10713=FACE_OUTER_BOUND('',#16638,.T.);
#10714=FACE_OUTER_BOUND('',#16639,.T.);
#10715=FACE_OUTER_BOUND('',#16640,.T.);
#10716=FACE_OUTER_BOUND('',#16641,.T.);
#10717=FACE_OUTER_BOUND('',#16642,.T.);
#10718=FACE_OUTER_BOUND('',#16643,.T.);
#10719=FACE_OUTER_BOUND('',#16644,.T.);
#10720=FACE_OUTER_BOUND('',#16645,.T.);
#10721=FACE_OUTER_BOUND('',#16646,.T.);
#10722=FACE_OUTER_BOUND('',#16647,.T.);
#10723=FACE_OUTER_BOUND('',#16648,.T.);
#10724=FACE_OUTER_BOUND('',#16649,.T.);
#10725=FACE_OUTER_BOUND('',#16650,.T.);
#10726=FACE_OUTER_BOUND('',#16651,.T.);
#10727=FACE_OUTER_BOUND('',#16652,.T.);
#10728=FACE_OUTER_BOUND('',#16653,.T.);
#10729=FACE_OUTER_BOUND('',#16654,.T.);
#10730=FACE_OUTER_BOUND('',#16655,.T.);
#10731=FACE_OUTER_BOUND('',#16656,.T.);
#10732=FACE_OUTER_BOUND('',#16657,.T.);
#10733=FACE_OUTER_BOUND('',#16658,.T.);
#10734=FACE_OUTER_BOUND('',#16659,.T.);
#10735=FACE_OUTER_BOUND('',#16660,.T.);
#10736=FACE_OUTER_BOUND('',#16661,.T.);
#10737=FACE_OUTER_BOUND('',#16662,.T.);
#10738=FACE_OUTER_BOUND('',#16663,.T.);
#10739=FACE_OUTER_BOUND('',#16664,.T.);
#10740=FACE_OUTER_BOUND('',#16665,.T.);
#10741=FACE_OUTER_BOUND('',#16666,.T.);
#10742=FACE_OUTER_BOUND('',#16667,.T.);
#10743=FACE_OUTER_BOUND('',#16668,.T.);
#10744=FACE_OUTER_BOUND('',#16669,.T.);
#10745=FACE_OUTER_BOUND('',#16670,.T.);
#10746=FACE_OUTER_BOUND('',#16671,.T.);
#10747=FACE_OUTER_BOUND('',#16672,.T.);
#10748=FACE_OUTER_BOUND('',#16673,.T.);
#10749=FACE_OUTER_BOUND('',#16674,.T.);
#10750=FACE_OUTER_BOUND('',#16675,.T.);
#10751=FACE_OUTER_BOUND('',#16676,.T.);
#10752=FACE_OUTER_BOUND('',#16677,.T.);
#10753=FACE_OUTER_BOUND('',#16678,.T.);
#10754=FACE_OUTER_BOUND('',#16679,.T.);
#10755=FACE_OUTER_BOUND('',#16680,.T.);
#10756=FACE_OUTER_BOUND('',#16681,.T.);
#10757=FACE_OUTER_BOUND('',#16682,.T.);
#10758=FACE_OUTER_BOUND('',#16683,.T.);
#10759=FACE_OUTER_BOUND('',#16684,.T.);
#10760=FACE_OUTER_BOUND('',#16685,.T.);
#10761=FACE_OUTER_BOUND('',#16686,.T.);
#10762=FACE_OUTER_BOUND('',#16687,.T.);
#10763=FACE_OUTER_BOUND('',#16688,.T.);
#10764=FACE_OUTER_BOUND('',#16689,.T.);
#10765=FACE_OUTER_BOUND('',#16690,.T.);
#10766=FACE_OUTER_BOUND('',#16691,.T.);
#10767=FACE_OUTER_BOUND('',#16692,.T.);
#10768=FACE_OUTER_BOUND('',#16693,.T.);
#10769=FACE_OUTER_BOUND('',#16694,.T.);
#10770=FACE_OUTER_BOUND('',#16695,.T.);
#10771=FACE_OUTER_BOUND('',#16696,.T.);
#10772=FACE_OUTER_BOUND('',#16697,.T.);
#10773=FACE_OUTER_BOUND('',#16698,.T.);
#10774=FACE_OUTER_BOUND('',#16699,.T.);
#10775=FACE_OUTER_BOUND('',#16700,.T.);
#10776=FACE_OUTER_BOUND('',#16701,.T.);
#10777=FACE_OUTER_BOUND('',#16702,.T.);
#10778=FACE_OUTER_BOUND('',#16703,.T.);
#10779=FACE_OUTER_BOUND('',#16704,.T.);
#10780=FACE_OUTER_BOUND('',#16705,.T.);
#10781=FACE_OUTER_BOUND('',#16706,.T.);
#10782=FACE_OUTER_BOUND('',#16707,.T.);
#10783=FACE_OUTER_BOUND('',#16708,.T.);
#10784=FACE_OUTER_BOUND('',#16709,.T.);
#10785=FACE_OUTER_BOUND('',#16710,.T.);
#10786=FACE_OUTER_BOUND('',#16711,.T.);
#10787=FACE_OUTER_BOUND('',#16712,.T.);
#10788=FACE_OUTER_BOUND('',#16713,.T.);
#10789=FACE_OUTER_BOUND('',#16714,.T.);
#10790=FACE_OUTER_BOUND('',#16715,.T.);
#10791=FACE_OUTER_BOUND('',#16716,.T.);
#10792=FACE_OUTER_BOUND('',#16717,.T.);
#10793=FACE_OUTER_BOUND('',#16718,.T.);
#10794=FACE_OUTER_BOUND('',#16719,.T.);
#10795=FACE_OUTER_BOUND('',#16720,.T.);
#10796=FACE_OUTER_BOUND('',#16721,.T.);
#10797=FACE_OUTER_BOUND('',#16722,.T.);
#10798=FACE_OUTER_BOUND('',#16723,.T.);
#10799=FACE_OUTER_BOUND('',#16724,.T.);
#10800=FACE_OUTER_BOUND('',#16725,.T.);
#10801=FACE_OUTER_BOUND('',#16726,.T.);
#10802=FACE_OUTER_BOUND('',#16727,.T.);
#10803=FACE_OUTER_BOUND('',#16728,.T.);
#10804=FACE_OUTER_BOUND('',#16729,.T.);
#10805=FACE_OUTER_BOUND('',#16730,.T.);
#10806=FACE_OUTER_BOUND('',#16731,.T.);
#10807=FACE_OUTER_BOUND('',#16732,.T.);
#10808=FACE_OUTER_BOUND('',#16733,.T.);
#10809=FACE_OUTER_BOUND('',#16734,.T.);
#10810=FACE_OUTER_BOUND('',#16735,.T.);
#10811=FACE_OUTER_BOUND('',#16736,.T.);
#10812=FACE_OUTER_BOUND('',#16737,.T.);
#10813=FACE_OUTER_BOUND('',#16738,.T.);
#10814=FACE_OUTER_BOUND('',#16739,.T.);
#10815=FACE_OUTER_BOUND('',#16740,.T.);
#10816=FACE_OUTER_BOUND('',#16741,.T.);
#10817=FACE_OUTER_BOUND('',#16742,.T.);
#10818=FACE_OUTER_BOUND('',#16743,.T.);
#10819=FACE_OUTER_BOUND('',#16744,.T.);
#10820=FACE_OUTER_BOUND('',#16745,.T.);
#10821=FACE_OUTER_BOUND('',#16746,.T.);
#10822=FACE_OUTER_BOUND('',#16747,.T.);
#10823=FACE_OUTER_BOUND('',#16748,.T.);
#10824=FACE_OUTER_BOUND('',#16749,.T.);
#10825=FACE_OUTER_BOUND('',#16750,.T.);
#10826=FACE_OUTER_BOUND('',#16751,.T.);
#10827=FACE_OUTER_BOUND('',#16752,.T.);
#10828=FACE_OUTER_BOUND('',#16753,.T.);
#10829=FACE_OUTER_BOUND('',#16754,.T.);
#10830=FACE_OUTER_BOUND('',#16755,.T.);
#10831=FACE_OUTER_BOUND('',#16756,.T.);
#10832=FACE_OUTER_BOUND('',#16757,.T.);
#10833=FACE_OUTER_BOUND('',#16758,.T.);
#10834=FACE_OUTER_BOUND('',#16759,.T.);
#10835=FACE_OUTER_BOUND('',#16760,.T.);
#10836=FACE_OUTER_BOUND('',#16761,.T.);
#10837=FACE_OUTER_BOUND('',#16762,.T.);
#10838=FACE_OUTER_BOUND('',#16763,.T.);
#10839=FACE_OUTER_BOUND('',#16764,.T.);
#10840=FACE_OUTER_BOUND('',#16765,.T.);
#10841=FACE_OUTER_BOUND('',#16766,.T.);
#10842=FACE_OUTER_BOUND('',#16767,.T.);
#10843=FACE_OUTER_BOUND('',#16768,.T.);
#10844=FACE_OUTER_BOUND('',#16769,.T.);
#10845=FACE_OUTER_BOUND('',#16770,.T.);
#10846=FACE_OUTER_BOUND('',#16771,.T.);
#10847=FACE_OUTER_BOUND('',#16772,.T.);
#10848=FACE_OUTER_BOUND('',#16773,.T.);
#10849=FACE_OUTER_BOUND('',#16774,.T.);
#10850=FACE_OUTER_BOUND('',#16775,.T.);
#10851=FACE_OUTER_BOUND('',#16776,.T.);
#10852=FACE_OUTER_BOUND('',#16777,.T.);
#10853=FACE_OUTER_BOUND('',#16778,.T.);
#10854=FACE_OUTER_BOUND('',#16779,.T.);
#10855=FACE_OUTER_BOUND('',#16780,.T.);
#10856=FACE_OUTER_BOUND('',#16781,.T.);
#10857=FACE_OUTER_BOUND('',#16782,.T.);
#10858=FACE_OUTER_BOUND('',#16783,.T.);
#10859=FACE_OUTER_BOUND('',#16784,.T.);
#10860=FACE_OUTER_BOUND('',#16785,.T.);
#10861=FACE_OUTER_BOUND('',#16786,.T.);
#10862=FACE_OUTER_BOUND('',#16787,.T.);
#10863=FACE_OUTER_BOUND('',#16788,.T.);
#10864=FACE_OUTER_BOUND('',#16789,.T.);
#10865=FACE_OUTER_BOUND('',#16790,.T.);
#10866=FACE_OUTER_BOUND('',#16791,.T.);
#10867=FACE_OUTER_BOUND('',#16792,.T.);
#10868=FACE_OUTER_BOUND('',#16793,.T.);
#10869=FACE_OUTER_BOUND('',#16794,.T.);
#10870=FACE_OUTER_BOUND('',#16795,.T.);
#10871=FACE_OUTER_BOUND('',#16796,.T.);
#10872=FACE_OUTER_BOUND('',#16797,.T.);
#10873=FACE_OUTER_BOUND('',#16798,.T.);
#10874=FACE_OUTER_BOUND('',#16799,.T.);
#10875=FACE_OUTER_BOUND('',#16800,.T.);
#10876=FACE_OUTER_BOUND('',#16801,.T.);
#10877=FACE_OUTER_BOUND('',#16802,.T.);
#10878=FACE_OUTER_BOUND('',#16803,.T.);
#10879=FACE_OUTER_BOUND('',#16804,.T.);
#10880=FACE_OUTER_BOUND('',#16805,.T.);
#10881=FACE_OUTER_BOUND('',#16806,.T.);
#10882=FACE_OUTER_BOUND('',#16807,.T.);
#10883=FACE_OUTER_BOUND('',#16808,.T.);
#10884=FACE_OUTER_BOUND('',#16809,.T.);
#10885=FACE_OUTER_BOUND('',#16810,.T.);
#10886=FACE_OUTER_BOUND('',#16811,.T.);
#10887=FACE_OUTER_BOUND('',#16812,.T.);
#10888=FACE_OUTER_BOUND('',#16813,.T.);
#10889=FACE_OUTER_BOUND('',#16814,.T.);
#10890=FACE_OUTER_BOUND('',#16815,.T.);
#10891=FACE_OUTER_BOUND('',#16816,.T.);
#10892=FACE_OUTER_BOUND('',#16817,.T.);
#10893=FACE_OUTER_BOUND('',#16818,.T.);
#10894=FACE_OUTER_BOUND('',#16819,.T.);
#10895=FACE_OUTER_BOUND('',#16820,.T.);
#10896=FACE_OUTER_BOUND('',#16821,.T.);
#10897=FACE_OUTER_BOUND('',#16822,.T.);
#10898=FACE_OUTER_BOUND('',#16823,.T.);
#10899=FACE_OUTER_BOUND('',#16824,.T.);
#10900=FACE_OUTER_BOUND('',#16825,.T.);
#10901=FACE_OUTER_BOUND('',#16826,.T.);
#10902=FACE_OUTER_BOUND('',#16827,.T.);
#10903=FACE_OUTER_BOUND('',#16828,.T.);
#10904=FACE_OUTER_BOUND('',#16829,.T.);
#10905=FACE_OUTER_BOUND('',#16830,.T.);
#10906=FACE_OUTER_BOUND('',#16831,.T.);
#10907=FACE_OUTER_BOUND('',#16832,.T.);
#10908=FACE_OUTER_BOUND('',#16833,.T.);
#10909=FACE_OUTER_BOUND('',#16834,.T.);
#10910=FACE_OUTER_BOUND('',#16835,.T.);
#10911=FACE_OUTER_BOUND('',#16836,.T.);
#10912=FACE_OUTER_BOUND('',#16837,.T.);
#10913=FACE_OUTER_BOUND('',#16838,.T.);
#10914=FACE_OUTER_BOUND('',#16839,.T.);
#10915=FACE_OUTER_BOUND('',#16840,.T.);
#10916=FACE_OUTER_BOUND('',#16841,.T.);
#10917=FACE_OUTER_BOUND('',#16842,.T.);
#10918=FACE_OUTER_BOUND('',#16843,.T.);
#10919=FACE_OUTER_BOUND('',#16844,.T.);
#10920=FACE_OUTER_BOUND('',#16845,.T.);
#10921=FACE_OUTER_BOUND('',#16846,.T.);
#10922=FACE_OUTER_BOUND('',#16847,.T.);
#10923=FACE_OUTER_BOUND('',#16848,.T.);
#10924=FACE_OUTER_BOUND('',#16849,.T.);
#10925=FACE_OUTER_BOUND('',#16850,.T.);
#10926=FACE_OUTER_BOUND('',#16851,.T.);
#10927=FACE_OUTER_BOUND('',#16852,.T.);
#10928=FACE_OUTER_BOUND('',#16853,.T.);
#10929=FACE_OUTER_BOUND('',#16854,.T.);
#10930=FACE_OUTER_BOUND('',#16855,.T.);
#10931=FACE_OUTER_BOUND('',#16856,.T.);
#10932=FACE_OUTER_BOUND('',#16857,.T.);
#10933=FACE_OUTER_BOUND('',#16858,.T.);
#10934=FACE_OUTER_BOUND('',#16859,.T.);
#10935=FACE_OUTER_BOUND('',#16860,.T.);
#10936=FACE_OUTER_BOUND('',#16861,.T.);
#10937=FACE_OUTER_BOUND('',#16862,.T.);
#10938=FACE_OUTER_BOUND('',#16863,.T.);
#10939=FACE_OUTER_BOUND('',#16864,.T.);
#10940=FACE_OUTER_BOUND('',#16865,.T.);
#10941=FACE_OUTER_BOUND('',#16866,.T.);
#10942=FACE_OUTER_BOUND('',#16867,.T.);
#10943=FACE_OUTER_BOUND('',#16868,.T.);
#10944=FACE_OUTER_BOUND('',#16869,.T.);
#10945=FACE_OUTER_BOUND('',#16870,.T.);
#10946=FACE_OUTER_BOUND('',#16871,.T.);
#10947=FACE_OUTER_BOUND('',#16872,.T.);
#10948=FACE_OUTER_BOUND('',#16873,.T.);
#10949=FACE_OUTER_BOUND('',#16874,.T.);
#10950=FACE_OUTER_BOUND('',#16875,.T.);
#10951=FACE_OUTER_BOUND('',#16876,.T.);
#10952=FACE_OUTER_BOUND('',#16877,.T.);
#10953=FACE_OUTER_BOUND('',#16878,.T.);
#10954=FACE_OUTER_BOUND('',#16879,.T.);
#10955=FACE_OUTER_BOUND('',#16880,.T.);
#10956=FACE_OUTER_BOUND('',#16881,.T.);
#10957=FACE_OUTER_BOUND('',#16882,.T.);
#10958=FACE_OUTER_BOUND('',#16883,.T.);
#10959=FACE_OUTER_BOUND('',#16884,.T.);
#10960=FACE_OUTER_BOUND('',#16885,.T.);
#10961=FACE_OUTER_BOUND('',#16886,.T.);
#10962=FACE_OUTER_BOUND('',#16887,.T.);
#10963=FACE_OUTER_BOUND('',#16888,.T.);
#10964=FACE_OUTER_BOUND('',#16889,.T.);
#10965=FACE_OUTER_BOUND('',#16890,.T.);
#10966=FACE_OUTER_BOUND('',#16891,.T.);
#10967=FACE_OUTER_BOUND('',#16892,.T.);
#10968=FACE_OUTER_BOUND('',#16893,.T.);
#10969=FACE_OUTER_BOUND('',#16894,.T.);
#10970=FACE_OUTER_BOUND('',#16895,.T.);
#10971=FACE_OUTER_BOUND('',#16896,.T.);
#10972=FACE_OUTER_BOUND('',#16897,.T.);
#10973=FACE_OUTER_BOUND('',#16898,.T.);
#10974=FACE_OUTER_BOUND('',#16899,.T.);
#10975=FACE_OUTER_BOUND('',#16900,.T.);
#10976=FACE_OUTER_BOUND('',#16901,.T.);
#10977=FACE_OUTER_BOUND('',#16902,.T.);
#10978=FACE_OUTER_BOUND('',#16903,.T.);
#10979=FACE_OUTER_BOUND('',#16904,.T.);
#10980=FACE_OUTER_BOUND('',#16905,.T.);
#10981=FACE_OUTER_BOUND('',#16906,.T.);
#10982=FACE_OUTER_BOUND('',#16907,.T.);
#10983=FACE_OUTER_BOUND('',#16908,.T.);
#10984=FACE_OUTER_BOUND('',#16909,.T.);
#10985=FACE_OUTER_BOUND('',#16910,.T.);
#10986=FACE_OUTER_BOUND('',#16911,.T.);
#10987=FACE_OUTER_BOUND('',#16912,.T.);
#10988=FACE_OUTER_BOUND('',#16913,.T.);
#10989=FACE_OUTER_BOUND('',#16914,.T.);
#10990=FACE_OUTER_BOUND('',#16915,.T.);
#10991=FACE_OUTER_BOUND('',#16916,.T.);
#10992=FACE_OUTER_BOUND('',#16917,.T.);
#10993=FACE_OUTER_BOUND('',#16918,.T.);
#10994=FACE_OUTER_BOUND('',#16919,.T.);
#10995=FACE_OUTER_BOUND('',#16920,.T.);
#10996=FACE_OUTER_BOUND('',#16921,.T.);
#10997=FACE_OUTER_BOUND('',#16922,.T.);
#10998=FACE_OUTER_BOUND('',#16923,.T.);
#10999=FACE_OUTER_BOUND('',#16924,.T.);
#11000=FACE_OUTER_BOUND('',#16925,.T.);
#11001=FACE_OUTER_BOUND('',#16926,.T.);
#11002=FACE_OUTER_BOUND('',#16927,.T.);
#11003=FACE_OUTER_BOUND('',#16928,.T.);
#11004=FACE_OUTER_BOUND('',#16929,.T.);
#11005=FACE_OUTER_BOUND('',#16930,.T.);
#11006=FACE_OUTER_BOUND('',#16931,.T.);
#11007=FACE_OUTER_BOUND('',#16932,.T.);
#11008=FACE_OUTER_BOUND('',#16933,.T.);
#11009=FACE_OUTER_BOUND('',#16934,.T.);
#11010=FACE_OUTER_BOUND('',#16935,.T.);
#11011=FACE_OUTER_BOUND('',#16936,.T.);
#11012=FACE_OUTER_BOUND('',#16937,.T.);
#11013=FACE_OUTER_BOUND('',#16938,.T.);
#11014=FACE_OUTER_BOUND('',#16939,.T.);
#11015=FACE_OUTER_BOUND('',#16940,.T.);
#11016=FACE_OUTER_BOUND('',#16941,.T.);
#11017=FACE_OUTER_BOUND('',#16942,.T.);
#11018=FACE_OUTER_BOUND('',#16943,.T.);
#11019=FACE_OUTER_BOUND('',#16944,.T.);
#11020=FACE_OUTER_BOUND('',#16945,.T.);
#11021=FACE_OUTER_BOUND('',#16946,.T.);
#11022=FACE_OUTER_BOUND('',#16947,.T.);
#11023=FACE_OUTER_BOUND('',#16948,.T.);
#11024=FACE_OUTER_BOUND('',#16949,.T.);
#11025=FACE_OUTER_BOUND('',#16950,.T.);
#11026=FACE_OUTER_BOUND('',#16951,.T.);
#11027=FACE_OUTER_BOUND('',#16952,.T.);
#11028=FACE_OUTER_BOUND('',#16953,.T.);
#11029=FACE_OUTER_BOUND('',#16954,.T.);
#11030=FACE_OUTER_BOUND('',#16955,.T.);
#11031=FACE_OUTER_BOUND('',#16956,.T.);
#11032=FACE_OUTER_BOUND('',#16957,.T.);
#11033=FACE_OUTER_BOUND('',#16958,.T.);
#11034=FACE_OUTER_BOUND('',#16959,.T.);
#11035=FACE_OUTER_BOUND('',#16960,.T.);
#11036=FACE_OUTER_BOUND('',#16961,.T.);
#11037=FACE_OUTER_BOUND('',#16962,.T.);
#11038=FACE_OUTER_BOUND('',#16963,.T.);
#11039=FACE_OUTER_BOUND('',#16964,.T.);
#11040=FACE_OUTER_BOUND('',#16965,.T.);
#11041=FACE_OUTER_BOUND('',#16966,.T.);
#11042=FACE_OUTER_BOUND('',#16967,.T.);
#11043=FACE_OUTER_BOUND('',#16968,.T.);
#11044=FACE_OUTER_BOUND('',#16969,.T.);
#11045=FACE_OUTER_BOUND('',#16970,.T.);
#11046=FACE_OUTER_BOUND('',#16971,.T.);
#11047=FACE_OUTER_BOUND('',#16972,.T.);
#11048=FACE_OUTER_BOUND('',#16973,.T.);
#11049=FACE_OUTER_BOUND('',#16974,.T.);
#11050=FACE_OUTER_BOUND('',#16975,.T.);
#11051=FACE_OUTER_BOUND('',#16976,.T.);
#11052=FACE_OUTER_BOUND('',#16977,.T.);
#11053=FACE_OUTER_BOUND('',#16978,.T.);
#11054=FACE_OUTER_BOUND('',#16979,.T.);
#11055=FACE_OUTER_BOUND('',#16980,.T.);
#11056=FACE_OUTER_BOUND('',#16981,.T.);
#11057=FACE_OUTER_BOUND('',#16982,.T.);
#11058=FACE_OUTER_BOUND('',#16983,.T.);
#11059=FACE_OUTER_BOUND('',#16984,.T.);
#11060=FACE_OUTER_BOUND('',#16985,.T.);
#11061=FACE_OUTER_BOUND('',#16986,.T.);
#11062=FACE_OUTER_BOUND('',#16987,.T.);
#11063=FACE_OUTER_BOUND('',#16988,.T.);
#11064=FACE_OUTER_BOUND('',#16989,.T.);
#11065=FACE_OUTER_BOUND('',#16990,.T.);
#11066=FACE_OUTER_BOUND('',#16991,.T.);
#11067=FACE_OUTER_BOUND('',#16992,.T.);
#11068=FACE_OUTER_BOUND('',#16993,.T.);
#11069=FACE_OUTER_BOUND('',#16994,.T.);
#11070=FACE_OUTER_BOUND('',#16995,.T.);
#11071=FACE_OUTER_BOUND('',#16996,.T.);
#11072=FACE_OUTER_BOUND('',#16997,.T.);
#11073=FACE_OUTER_BOUND('',#16998,.T.);
#11074=FACE_OUTER_BOUND('',#16999,.T.);
#11075=FACE_OUTER_BOUND('',#17000,.T.);
#11076=FACE_OUTER_BOUND('',#17001,.T.);
#11077=FACE_OUTER_BOUND('',#17002,.T.);
#11078=FACE_OUTER_BOUND('',#17003,.T.);
#11079=FACE_OUTER_BOUND('',#17004,.T.);
#11080=FACE_OUTER_BOUND('',#17005,.T.);
#11081=FACE_OUTER_BOUND('',#17006,.T.);
#11082=FACE_OUTER_BOUND('',#17007,.T.);
#11083=FACE_OUTER_BOUND('',#17008,.T.);
#11084=FACE_OUTER_BOUND('',#17009,.T.);
#11085=FACE_OUTER_BOUND('',#17010,.T.);
#11086=FACE_OUTER_BOUND('',#17011,.T.);
#11087=FACE_OUTER_BOUND('',#17012,.T.);
#11088=FACE_OUTER_BOUND('',#17013,.T.);
#11089=FACE_OUTER_BOUND('',#17014,.T.);
#11090=FACE_OUTER_BOUND('',#17015,.T.);
#11091=FACE_OUTER_BOUND('',#17016,.T.);
#11092=FACE_OUTER_BOUND('',#17017,.T.);
#11093=FACE_OUTER_BOUND('',#17018,.T.);
#11094=FACE_OUTER_BOUND('',#17019,.T.);
#11095=FACE_OUTER_BOUND('',#17020,.T.);
#11096=FACE_OUTER_BOUND('',#17021,.T.);
#11097=FACE_OUTER_BOUND('',#17022,.T.);
#11098=FACE_OUTER_BOUND('',#17023,.T.);
#11099=FACE_OUTER_BOUND('',#17024,.T.);
#11100=FACE_OUTER_BOUND('',#17025,.T.);
#11101=FACE_OUTER_BOUND('',#17026,.T.);
#11102=FACE_OUTER_BOUND('',#17027,.T.);
#11103=FACE_OUTER_BOUND('',#17028,.T.);
#11104=FACE_OUTER_BOUND('',#17029,.T.);
#11105=FACE_OUTER_BOUND('',#17030,.T.);
#11106=FACE_OUTER_BOUND('',#17031,.T.);
#11107=FACE_OUTER_BOUND('',#17032,.T.);
#11108=FACE_OUTER_BOUND('',#17033,.T.);
#11109=FACE_OUTER_BOUND('',#17034,.T.);
#11110=FACE_OUTER_BOUND('',#17035,.T.);
#11111=FACE_OUTER_BOUND('',#17036,.T.);
#11112=FACE_OUTER_BOUND('',#17037,.T.);
#11113=FACE_OUTER_BOUND('',#17038,.T.);
#11114=FACE_OUTER_BOUND('',#17039,.T.);
#11115=FACE_OUTER_BOUND('',#17040,.T.);
#11116=FACE_OUTER_BOUND('',#17041,.T.);
#11117=FACE_OUTER_BOUND('',#17042,.T.);
#11118=FACE_OUTER_BOUND('',#17043,.T.);
#11119=FACE_OUTER_BOUND('',#17044,.T.);
#11120=FACE_OUTER_BOUND('',#17045,.T.);
#11121=FACE_OUTER_BOUND('',#17046,.T.);
#11122=FACE_OUTER_BOUND('',#17047,.T.);
#11123=FACE_OUTER_BOUND('',#17048,.T.);
#11124=FACE_OUTER_BOUND('',#17049,.T.);
#11125=FACE_OUTER_BOUND('',#17050,.T.);
#11126=FACE_OUTER_BOUND('',#17051,.T.);
#11127=FACE_OUTER_BOUND('',#17052,.T.);
#11128=FACE_OUTER_BOUND('',#17053,.T.);
#11129=FACE_OUTER_BOUND('',#17054,.T.);
#11130=FACE_OUTER_BOUND('',#17055,.T.);
#11131=FACE_OUTER_BOUND('',#17056,.T.);
#11132=FACE_OUTER_BOUND('',#17057,.T.);
#11133=FACE_OUTER_BOUND('',#17058,.T.);
#11134=FACE_OUTER_BOUND('',#17059,.T.);
#11135=FACE_OUTER_BOUND('',#17060,.T.);
#11136=FACE_OUTER_BOUND('',#17061,.T.);
#11137=FACE_OUTER_BOUND('',#17062,.T.);
#11138=FACE_OUTER_BOUND('',#17063,.T.);
#11139=FACE_OUTER_BOUND('',#17064,.T.);
#11140=FACE_OUTER_BOUND('',#17065,.T.);
#11141=FACE_OUTER_BOUND('',#17066,.T.);
#11142=FACE_OUTER_BOUND('',#17067,.T.);
#11143=FACE_OUTER_BOUND('',#17068,.T.);
#11144=FACE_OUTER_BOUND('',#17069,.T.);
#11145=FACE_OUTER_BOUND('',#17070,.T.);
#11146=FACE_OUTER_BOUND('',#17071,.T.);
#11147=FACE_OUTER_BOUND('',#17072,.T.);
#11148=FACE_OUTER_BOUND('',#17073,.T.);
#11149=FACE_OUTER_BOUND('',#17074,.T.);
#11150=FACE_OUTER_BOUND('',#17075,.T.);
#11151=FACE_OUTER_BOUND('',#17076,.T.);
#11152=FACE_OUTER_BOUND('',#17077,.T.);
#11153=FACE_OUTER_BOUND('',#17078,.T.);
#11154=FACE_OUTER_BOUND('',#17079,.T.);
#11155=FACE_OUTER_BOUND('',#17080,.T.);
#11156=FACE_OUTER_BOUND('',#17081,.T.);
#11157=FACE_OUTER_BOUND('',#17082,.T.);
#11158=FACE_OUTER_BOUND('',#17083,.T.);
#11159=FACE_OUTER_BOUND('',#17084,.T.);
#11160=FACE_OUTER_BOUND('',#17085,.T.);
#11161=FACE_OUTER_BOUND('',#17086,.T.);
#11162=FACE_OUTER_BOUND('',#17087,.T.);
#11163=FACE_OUTER_BOUND('',#17088,.T.);
#11164=FACE_OUTER_BOUND('',#17089,.T.);
#11165=FACE_OUTER_BOUND('',#17090,.T.);
#11166=FACE_OUTER_BOUND('',#17091,.T.);
#11167=FACE_OUTER_BOUND('',#17092,.T.);
#11168=FACE_OUTER_BOUND('',#17093,.T.);
#11169=FACE_OUTER_BOUND('',#17094,.T.);
#11170=FACE_OUTER_BOUND('',#17095,.T.);
#11171=FACE_OUTER_BOUND('',#17096,.T.);
#11172=FACE_OUTER_BOUND('',#17097,.T.);
#11173=FACE_OUTER_BOUND('',#17098,.T.);
#11174=FACE_OUTER_BOUND('',#17099,.T.);
#11175=FACE_OUTER_BOUND('',#17100,.T.);
#11176=FACE_OUTER_BOUND('',#17101,.T.);
#11177=FACE_OUTER_BOUND('',#17102,.T.);
#11178=FACE_OUTER_BOUND('',#17103,.T.);
#11179=FACE_OUTER_BOUND('',#17104,.T.);
#11180=FACE_OUTER_BOUND('',#17105,.T.);
#11181=FACE_OUTER_BOUND('',#17106,.T.);
#11182=FACE_OUTER_BOUND('',#17107,.T.);
#11183=FACE_OUTER_BOUND('',#17108,.T.);
#11184=FACE_OUTER_BOUND('',#17109,.T.);
#11185=FACE_OUTER_BOUND('',#17110,.T.);
#11186=FACE_OUTER_BOUND('',#17111,.T.);
#11187=FACE_OUTER_BOUND('',#17112,.T.);
#11188=FACE_OUTER_BOUND('',#17113,.T.);
#11189=FACE_OUTER_BOUND('',#17114,.T.);
#11190=FACE_OUTER_BOUND('',#17115,.T.);
#11191=FACE_OUTER_BOUND('',#17116,.T.);
#11192=FACE_OUTER_BOUND('',#17117,.T.);
#11193=FACE_OUTER_BOUND('',#17118,.T.);
#11194=FACE_OUTER_BOUND('',#17119,.T.);
#11195=FACE_OUTER_BOUND('',#17120,.T.);
#11196=FACE_OUTER_BOUND('',#17121,.T.);
#11197=FACE_OUTER_BOUND('',#17122,.T.);
#11198=FACE_OUTER_BOUND('',#17123,.T.);
#11199=FACE_OUTER_BOUND('',#17124,.T.);
#11200=FACE_OUTER_BOUND('',#17125,.T.);
#11201=FACE_OUTER_BOUND('',#17126,.T.);
#11202=FACE_OUTER_BOUND('',#17127,.T.);
#11203=FACE_OUTER_BOUND('',#17128,.T.);
#11204=FACE_OUTER_BOUND('',#17129,.T.);
#11205=FACE_OUTER_BOUND('',#17130,.T.);
#11206=FACE_OUTER_BOUND('',#17131,.T.);
#11207=FACE_OUTER_BOUND('',#17132,.T.);
#11208=FACE_OUTER_BOUND('',#17133,.T.);
#11209=FACE_OUTER_BOUND('',#17134,.T.);
#11210=FACE_OUTER_BOUND('',#17135,.T.);
#11211=FACE_OUTER_BOUND('',#17136,.T.);
#11212=FACE_OUTER_BOUND('',#17137,.T.);
#11213=FACE_OUTER_BOUND('',#17138,.T.);
#11214=FACE_OUTER_BOUND('',#17139,.T.);
#11215=FACE_OUTER_BOUND('',#17140,.T.);
#11216=FACE_OUTER_BOUND('',#17141,.T.);
#11217=FACE_OUTER_BOUND('',#17142,.T.);
#11218=FACE_OUTER_BOUND('',#17143,.T.);
#11219=FACE_OUTER_BOUND('',#17144,.T.);
#11220=FACE_OUTER_BOUND('',#17145,.T.);
#11221=FACE_OUTER_BOUND('',#17146,.T.);
#11222=FACE_OUTER_BOUND('',#17147,.T.);
#11223=FACE_OUTER_BOUND('',#17148,.T.);
#11224=FACE_OUTER_BOUND('',#17149,.T.);
#11225=FACE_OUTER_BOUND('',#17150,.T.);
#11226=FACE_OUTER_BOUND('',#17151,.T.);
#11227=FACE_OUTER_BOUND('',#17152,.T.);
#11228=FACE_OUTER_BOUND('',#17153,.T.);
#11229=FACE_OUTER_BOUND('',#17154,.T.);
#11230=FACE_OUTER_BOUND('',#17155,.T.);
#11231=FACE_OUTER_BOUND('',#17156,.T.);
#11232=FACE_OUTER_BOUND('',#17157,.T.);
#11233=FACE_OUTER_BOUND('',#17158,.T.);
#11234=FACE_OUTER_BOUND('',#17159,.T.);
#11235=FACE_OUTER_BOUND('',#17160,.T.);
#11236=FACE_OUTER_BOUND('',#17161,.T.);
#11237=FACE_OUTER_BOUND('',#17162,.T.);
#11238=FACE_OUTER_BOUND('',#17163,.T.);
#11239=FACE_OUTER_BOUND('',#17164,.T.);
#11240=FACE_OUTER_BOUND('',#17165,.T.);
#11241=FACE_OUTER_BOUND('',#17166,.T.);
#11242=FACE_OUTER_BOUND('',#17167,.T.);
#11243=FACE_OUTER_BOUND('',#17168,.T.);
#11244=FACE_OUTER_BOUND('',#17169,.T.);
#11245=FACE_OUTER_BOUND('',#17170,.T.);
#11246=FACE_OUTER_BOUND('',#17171,.T.);
#11247=FACE_OUTER_BOUND('',#17172,.T.);
#11248=FACE_OUTER_BOUND('',#17173,.T.);
#11249=FACE_OUTER_BOUND('',#17174,.T.);
#11250=FACE_OUTER_BOUND('',#17175,.T.);
#11251=FACE_OUTER_BOUND('',#17176,.T.);
#11252=FACE_OUTER_BOUND('',#17177,.T.);
#11253=FACE_OUTER_BOUND('',#17178,.T.);
#11254=FACE_OUTER_BOUND('',#17179,.T.);
#11255=FACE_OUTER_BOUND('',#17180,.T.);
#11256=FACE_OUTER_BOUND('',#17181,.T.);
#11257=FACE_OUTER_BOUND('',#17182,.T.);
#11258=FACE_OUTER_BOUND('',#17183,.T.);
#11259=FACE_OUTER_BOUND('',#17184,.T.);
#11260=FACE_OUTER_BOUND('',#17185,.T.);
#11261=FACE_OUTER_BOUND('',#17186,.T.);
#11262=FACE_OUTER_BOUND('',#17187,.T.);
#11263=FACE_OUTER_BOUND('',#17188,.T.);
#11264=FACE_OUTER_BOUND('',#17189,.T.);
#11265=FACE_OUTER_BOUND('',#17190,.T.);
#11266=FACE_OUTER_BOUND('',#17191,.T.);
#11267=FACE_OUTER_BOUND('',#17192,.T.);
#11268=FACE_OUTER_BOUND('',#17193,.T.);
#11269=FACE_OUTER_BOUND('',#17194,.T.);
#11270=FACE_OUTER_BOUND('',#17195,.T.);
#11271=FACE_OUTER_BOUND('',#17196,.T.);
#11272=FACE_OUTER_BOUND('',#17197,.T.);
#11273=FACE_OUTER_BOUND('',#17198,.T.);
#11274=FACE_OUTER_BOUND('',#17199,.T.);
#11275=FACE_OUTER_BOUND('',#17200,.T.);
#11276=FACE_OUTER_BOUND('',#17201,.T.);
#11277=FACE_OUTER_BOUND('',#17202,.T.);
#11278=FACE_OUTER_BOUND('',#17203,.T.);
#11279=FACE_OUTER_BOUND('',#17204,.T.);
#11280=FACE_OUTER_BOUND('',#17205,.T.);
#11281=FACE_OUTER_BOUND('',#17206,.T.);
#11282=FACE_OUTER_BOUND('',#17207,.T.);
#11283=FACE_OUTER_BOUND('',#17208,.T.);
#11284=FACE_OUTER_BOUND('',#17209,.T.);
#11285=FACE_OUTER_BOUND('',#17210,.T.);
#11286=FACE_OUTER_BOUND('',#17211,.T.);
#11287=FACE_OUTER_BOUND('',#17212,.T.);
#11288=FACE_OUTER_BOUND('',#17213,.T.);
#11289=FACE_OUTER_BOUND('',#17214,.T.);
#11290=FACE_OUTER_BOUND('',#17215,.T.);
#11291=FACE_OUTER_BOUND('',#17216,.T.);
#11292=FACE_OUTER_BOUND('',#17217,.T.);
#11293=FACE_OUTER_BOUND('',#17218,.T.);
#11294=FACE_OUTER_BOUND('',#17219,.T.);
#11295=FACE_OUTER_BOUND('',#17220,.T.);
#11296=FACE_OUTER_BOUND('',#17221,.T.);
#11297=FACE_OUTER_BOUND('',#17222,.T.);
#11298=FACE_OUTER_BOUND('',#17223,.T.);
#11299=FACE_OUTER_BOUND('',#17224,.T.);
#11300=FACE_OUTER_BOUND('',#17225,.T.);
#11301=FACE_OUTER_BOUND('',#17226,.T.);
#11302=FACE_OUTER_BOUND('',#17227,.T.);
#11303=FACE_OUTER_BOUND('',#17228,.T.);
#11304=FACE_OUTER_BOUND('',#17229,.T.);
#11305=FACE_OUTER_BOUND('',#17230,.T.);
#11306=FACE_OUTER_BOUND('',#17231,.T.);
#11307=FACE_OUTER_BOUND('',#17232,.T.);
#11308=FACE_OUTER_BOUND('',#17233,.T.);
#11309=FACE_OUTER_BOUND('',#17234,.T.);
#11310=FACE_OUTER_BOUND('',#17235,.T.);
#11311=FACE_OUTER_BOUND('',#17236,.T.);
#11312=FACE_OUTER_BOUND('',#17237,.T.);
#11313=FACE_OUTER_BOUND('',#17238,.T.);
#11314=FACE_OUTER_BOUND('',#17239,.T.);
#11315=FACE_OUTER_BOUND('',#17240,.T.);
#11316=FACE_OUTER_BOUND('',#17241,.T.);
#11317=FACE_OUTER_BOUND('',#17242,.T.);
#11318=FACE_OUTER_BOUND('',#17243,.T.);
#11319=FACE_OUTER_BOUND('',#17244,.T.);
#11320=FACE_OUTER_BOUND('',#17245,.T.);
#11321=FACE_OUTER_BOUND('',#17246,.T.);
#11322=FACE_OUTER_BOUND('',#17247,.T.);
#11323=FACE_OUTER_BOUND('',#17248,.T.);
#11324=FACE_OUTER_BOUND('',#17249,.T.);
#11325=FACE_OUTER_BOUND('',#17250,.T.);
#11326=FACE_OUTER_BOUND('',#17251,.T.);
#11327=FACE_OUTER_BOUND('',#17252,.T.);
#11328=FACE_OUTER_BOUND('',#17253,.T.);
#11329=FACE_OUTER_BOUND('',#17254,.T.);
#11330=FACE_OUTER_BOUND('',#17255,.T.);
#11331=FACE_OUTER_BOUND('',#17256,.T.);
#11332=FACE_OUTER_BOUND('',#17257,.T.);
#11333=FACE_OUTER_BOUND('',#17258,.T.);
#11334=FACE_OUTER_BOUND('',#17259,.T.);
#11335=FACE_OUTER_BOUND('',#17260,.T.);
#11336=FACE_OUTER_BOUND('',#17261,.T.);
#11337=FACE_OUTER_BOUND('',#17262,.T.);
#11338=FACE_OUTER_BOUND('',#17263,.T.);
#11339=FACE_OUTER_BOUND('',#17264,.T.);
#11340=FACE_OUTER_BOUND('',#17265,.T.);
#11341=FACE_OUTER_BOUND('',#17266,.T.);
#11342=FACE_OUTER_BOUND('',#17267,.T.);
#11343=FACE_OUTER_BOUND('',#17268,.T.);
#11344=FACE_OUTER_BOUND('',#17269,.T.);
#11345=FACE_OUTER_BOUND('',#17270,.T.);
#11346=FACE_OUTER_BOUND('',#17271,.T.);
#11347=FACE_OUTER_BOUND('',#17272,.T.);
#11348=FACE_OUTER_BOUND('',#17273,.T.);
#11349=FACE_OUTER_BOUND('',#17274,.T.);
#11350=FACE_OUTER_BOUND('',#17275,.T.);
#11351=FACE_OUTER_BOUND('',#17276,.T.);
#11352=FACE_OUTER_BOUND('',#17277,.T.);
#11353=FACE_OUTER_BOUND('',#17278,.T.);
#11354=FACE_OUTER_BOUND('',#17279,.T.);
#11355=FACE_OUTER_BOUND('',#17280,.T.);
#11356=FACE_OUTER_BOUND('',#17281,.T.);
#11357=FACE_OUTER_BOUND('',#17282,.T.);
#11358=FACE_OUTER_BOUND('',#17283,.T.);
#11359=FACE_OUTER_BOUND('',#17284,.T.);
#11360=FACE_OUTER_BOUND('',#17285,.T.);
#11361=FACE_OUTER_BOUND('',#17286,.T.);
#11362=FACE_OUTER_BOUND('',#17287,.T.);
#11363=FACE_OUTER_BOUND('',#17288,.T.);
#11364=FACE_OUTER_BOUND('',#17289,.T.);
#11365=FACE_OUTER_BOUND('',#17290,.T.);
#11366=FACE_OUTER_BOUND('',#17291,.T.);
#11367=FACE_OUTER_BOUND('',#17292,.T.);
#11368=FACE_OUTER_BOUND('',#17293,.T.);
#11369=FACE_OUTER_BOUND('',#17294,.T.);
#11370=FACE_OUTER_BOUND('',#17295,.T.);
#11371=FACE_OUTER_BOUND('',#17296,.T.);
#11372=FACE_OUTER_BOUND('',#17297,.T.);
#11373=FACE_OUTER_BOUND('',#17298,.T.);
#11374=FACE_OUTER_BOUND('',#17299,.T.);
#11375=FACE_OUTER_BOUND('',#17300,.T.);
#11376=FACE_OUTER_BOUND('',#17301,.T.);
#11377=FACE_OUTER_BOUND('',#17302,.T.);
#11378=FACE_OUTER_BOUND('',#17303,.T.);
#11379=FACE_OUTER_BOUND('',#17304,.T.);
#11380=FACE_OUTER_BOUND('',#17305,.T.);
#11381=FACE_OUTER_BOUND('',#17306,.T.);
#11382=FACE_OUTER_BOUND('',#17307,.T.);
#11383=FACE_OUTER_BOUND('',#17308,.T.);
#11384=FACE_OUTER_BOUND('',#17309,.T.);
#11385=FACE_OUTER_BOUND('',#17310,.T.);
#11386=FACE_OUTER_BOUND('',#17311,.T.);
#11387=FACE_OUTER_BOUND('',#17312,.T.);
#11388=FACE_OUTER_BOUND('',#17313,.T.);
#11389=FACE_OUTER_BOUND('',#17314,.T.);
#11390=FACE_OUTER_BOUND('',#17315,.T.);
#11391=FACE_OUTER_BOUND('',#17316,.T.);
#11392=FACE_OUTER_BOUND('',#17317,.T.);
#11393=FACE_OUTER_BOUND('',#17318,.T.);
#11394=FACE_OUTER_BOUND('',#17319,.T.);
#11395=FACE_OUTER_BOUND('',#17320,.T.);
#11396=FACE_OUTER_BOUND('',#17321,.T.);
#11397=FACE_OUTER_BOUND('',#17322,.T.);
#11398=FACE_OUTER_BOUND('',#17323,.T.);
#11399=FACE_OUTER_BOUND('',#17324,.T.);
#11400=FACE_OUTER_BOUND('',#17325,.T.);
#11401=FACE_OUTER_BOUND('',#17326,.T.);
#11402=FACE_OUTER_BOUND('',#17327,.T.);
#11403=FACE_OUTER_BOUND('',#17328,.T.);
#11404=FACE_OUTER_BOUND('',#17329,.T.);
#11405=FACE_OUTER_BOUND('',#17330,.T.);
#11406=FACE_OUTER_BOUND('',#17331,.T.);
#11407=FACE_OUTER_BOUND('',#17332,.T.);
#11408=FACE_OUTER_BOUND('',#17333,.T.);
#11409=FACE_OUTER_BOUND('',#17334,.T.);
#11410=FACE_OUTER_BOUND('',#17335,.T.);
#11411=FACE_OUTER_BOUND('',#17336,.T.);
#11412=FACE_OUTER_BOUND('',#17337,.T.);
#11413=FACE_OUTER_BOUND('',#17338,.T.);
#11414=FACE_OUTER_BOUND('',#17339,.T.);
#11415=FACE_OUTER_BOUND('',#17340,.T.);
#11416=FACE_OUTER_BOUND('',#17341,.T.);
#11417=FACE_OUTER_BOUND('',#17342,.T.);
#11418=FACE_OUTER_BOUND('',#17343,.T.);
#11419=FACE_OUTER_BOUND('',#17344,.T.);
#11420=FACE_OUTER_BOUND('',#17345,.T.);
#11421=FACE_OUTER_BOUND('',#17346,.T.);
#11422=FACE_OUTER_BOUND('',#17347,.T.);
#11423=FACE_OUTER_BOUND('',#17348,.T.);
#11424=FACE_OUTER_BOUND('',#17349,.T.);
#11425=FACE_OUTER_BOUND('',#17350,.T.);
#11426=FACE_OUTER_BOUND('',#17351,.T.);
#11427=FACE_OUTER_BOUND('',#17352,.T.);
#11428=FACE_OUTER_BOUND('',#17353,.T.);
#11429=FACE_OUTER_BOUND('',#17354,.T.);
#11430=FACE_OUTER_BOUND('',#17355,.T.);
#11431=FACE_OUTER_BOUND('',#17356,.T.);
#11432=FACE_OUTER_BOUND('',#17357,.T.);
#11433=FACE_OUTER_BOUND('',#17358,.T.);
#11434=FACE_OUTER_BOUND('',#17359,.T.);
#11435=FACE_OUTER_BOUND('',#17360,.T.);
#11436=FACE_OUTER_BOUND('',#17361,.T.);
#11437=FACE_OUTER_BOUND('',#17362,.T.);
#11438=FACE_OUTER_BOUND('',#17363,.T.);
#11439=FACE_OUTER_BOUND('',#17364,.T.);
#11440=FACE_OUTER_BOUND('',#17365,.T.);
#11441=FACE_OUTER_BOUND('',#17366,.T.);
#11442=FACE_OUTER_BOUND('',#17367,.T.);
#11443=FACE_OUTER_BOUND('',#17368,.T.);
#11444=FACE_OUTER_BOUND('',#17369,.T.);
#11445=FACE_OUTER_BOUND('',#17370,.T.);
#11446=FACE_OUTER_BOUND('',#17371,.T.);
#11447=FACE_OUTER_BOUND('',#17372,.T.);
#11448=FACE_OUTER_BOUND('',#17373,.T.);
#11449=FACE_OUTER_BOUND('',#17374,.T.);
#11450=FACE_OUTER_BOUND('',#17375,.T.);
#11451=FACE_OUTER_BOUND('',#17376,.T.);
#11452=FACE_OUTER_BOUND('',#17377,.T.);
#11453=FACE_OUTER_BOUND('',#17378,.T.);
#11454=FACE_OUTER_BOUND('',#17379,.T.);
#11455=FACE_OUTER_BOUND('',#17380,.T.);
#11456=FACE_OUTER_BOUND('',#17381,.T.);
#11457=FACE_OUTER_BOUND('',#17382,.T.);
#11458=FACE_OUTER_BOUND('',#17383,.T.);
#11459=FACE_OUTER_BOUND('',#17384,.T.);
#11460=FACE_OUTER_BOUND('',#17385,.T.);
#11461=FACE_OUTER_BOUND('',#17386,.T.);
#11462=FACE_OUTER_BOUND('',#17387,.T.);
#11463=FACE_OUTER_BOUND('',#17388,.T.);
#11464=FACE_OUTER_BOUND('',#17389,.T.);
#11465=FACE_OUTER_BOUND('',#17390,.T.);
#11466=FACE_OUTER_BOUND('',#17391,.T.);
#11467=FACE_OUTER_BOUND('',#17392,.T.);
#11468=FACE_OUTER_BOUND('',#17393,.T.);
#11469=FACE_OUTER_BOUND('',#17394,.T.);
#11470=FACE_OUTER_BOUND('',#17395,.T.);
#11471=FACE_OUTER_BOUND('',#17396,.T.);
#11472=FACE_OUTER_BOUND('',#17397,.T.);
#11473=FACE_OUTER_BOUND('',#17398,.T.);
#11474=FACE_OUTER_BOUND('',#17399,.T.);
#11475=FACE_OUTER_BOUND('',#17400,.T.);
#11476=FACE_OUTER_BOUND('',#17401,.T.);
#11477=FACE_OUTER_BOUND('',#17402,.T.);
#11478=FACE_OUTER_BOUND('',#17403,.T.);
#11479=FACE_OUTER_BOUND('',#17404,.T.);
#11480=FACE_OUTER_BOUND('',#17405,.T.);
#11481=FACE_OUTER_BOUND('',#17406,.T.);
#11482=FACE_OUTER_BOUND('',#17407,.T.);
#11483=FACE_OUTER_BOUND('',#17408,.T.);
#11484=FACE_OUTER_BOUND('',#17409,.T.);
#11485=FACE_OUTER_BOUND('',#17410,.T.);
#11486=FACE_OUTER_BOUND('',#17411,.T.);
#11487=FACE_OUTER_BOUND('',#17412,.T.);
#11488=FACE_OUTER_BOUND('',#17413,.T.);
#11489=FACE_OUTER_BOUND('',#17414,.T.);
#11490=FACE_OUTER_BOUND('',#17415,.T.);
#11491=FACE_OUTER_BOUND('',#17416,.T.);
#11492=FACE_OUTER_BOUND('',#17417,.T.);
#11493=FACE_OUTER_BOUND('',#17418,.T.);
#11494=FACE_OUTER_BOUND('',#17419,.T.);
#11495=FACE_OUTER_BOUND('',#17420,.T.);
#11496=FACE_OUTER_BOUND('',#17421,.T.);
#11497=FACE_OUTER_BOUND('',#17422,.T.);
#11498=FACE_OUTER_BOUND('',#17423,.T.);
#11499=FACE_OUTER_BOUND('',#17424,.T.);
#11500=FACE_OUTER_BOUND('',#17425,.T.);
#11501=FACE_OUTER_BOUND('',#17426,.T.);
#11502=FACE_OUTER_BOUND('',#17427,.T.);
#11503=FACE_OUTER_BOUND('',#17428,.T.);
#11504=FACE_OUTER_BOUND('',#17429,.T.);
#11505=FACE_OUTER_BOUND('',#17430,.T.);
#11506=FACE_OUTER_BOUND('',#17431,.T.);
#11507=FACE_OUTER_BOUND('',#17432,.T.);
#11508=FACE_OUTER_BOUND('',#17433,.T.);
#11509=FACE_OUTER_BOUND('',#17434,.T.);
#11510=FACE_OUTER_BOUND('',#17435,.T.);
#11511=FACE_OUTER_BOUND('',#17436,.T.);
#11512=FACE_OUTER_BOUND('',#17437,.T.);
#11513=FACE_OUTER_BOUND('',#17438,.T.);
#11514=FACE_OUTER_BOUND('',#17439,.T.);
#11515=FACE_OUTER_BOUND('',#17440,.T.);
#11516=FACE_OUTER_BOUND('',#17441,.T.);
#11517=FACE_OUTER_BOUND('',#17442,.T.);
#11518=FACE_OUTER_BOUND('',#17443,.T.);
#11519=FACE_OUTER_BOUND('',#17444,.T.);
#11520=FACE_OUTER_BOUND('',#17445,.T.);
#11521=FACE_OUTER_BOUND('',#17446,.T.);
#11522=FACE_OUTER_BOUND('',#17447,.T.);
#11523=FACE_OUTER_BOUND('',#17448,.T.);
#11524=FACE_OUTER_BOUND('',#17449,.T.);
#11525=FACE_OUTER_BOUND('',#17450,.T.);
#11526=FACE_OUTER_BOUND('',#17451,.T.);
#11527=FACE_OUTER_BOUND('',#17452,.T.);
#11528=FACE_OUTER_BOUND('',#17453,.T.);
#11529=FACE_OUTER_BOUND('',#17454,.T.);
#11530=FACE_OUTER_BOUND('',#17455,.T.);
#11531=FACE_OUTER_BOUND('',#17456,.T.);
#11532=FACE_OUTER_BOUND('',#17457,.T.);
#11533=FACE_OUTER_BOUND('',#17458,.T.);
#11534=FACE_OUTER_BOUND('',#17459,.T.);
#11535=FACE_OUTER_BOUND('',#17460,.T.);
#11536=FACE_OUTER_BOUND('',#17461,.T.);
#11537=FACE_OUTER_BOUND('',#17462,.T.);
#11538=FACE_OUTER_BOUND('',#17463,.T.);
#11539=FACE_OUTER_BOUND('',#17464,.T.);
#11540=FACE_OUTER_BOUND('',#17465,.T.);
#11541=FACE_OUTER_BOUND('',#17466,.T.);
#11542=FACE_OUTER_BOUND('',#17467,.T.);
#11543=FACE_OUTER_BOUND('',#17468,.T.);
#11544=FACE_OUTER_BOUND('',#17469,.T.);
#11545=FACE_OUTER_BOUND('',#17470,.T.);
#11546=FACE_OUTER_BOUND('',#17471,.T.);
#11547=FACE_OUTER_BOUND('',#17472,.T.);
#11548=FACE_OUTER_BOUND('',#17473,.T.);
#11549=FACE_OUTER_BOUND('',#17474,.T.);
#11550=FACE_OUTER_BOUND('',#17475,.T.);
#11551=FACE_OUTER_BOUND('',#17476,.T.);
#11552=FACE_OUTER_BOUND('',#17477,.T.);
#11553=FACE_OUTER_BOUND('',#17478,.T.);
#11554=FACE_OUTER_BOUND('',#17479,.T.);
#11555=FACE_OUTER_BOUND('',#17480,.T.);
#11556=FACE_OUTER_BOUND('',#17481,.T.);
#11557=FACE_OUTER_BOUND('',#17482,.T.);
#11558=FACE_OUTER_BOUND('',#17483,.T.);
#11559=FACE_OUTER_BOUND('',#17484,.T.);
#11560=FACE_OUTER_BOUND('',#17485,.T.);
#11561=FACE_OUTER_BOUND('',#17486,.T.);
#11562=FACE_OUTER_BOUND('',#17487,.T.);
#11563=FACE_OUTER_BOUND('',#17488,.T.);
#11564=FACE_OUTER_BOUND('',#17489,.T.);
#11565=FACE_OUTER_BOUND('',#17490,.T.);
#11566=FACE_OUTER_BOUND('',#17491,.T.);
#11567=FACE_OUTER_BOUND('',#17492,.T.);
#11568=FACE_OUTER_BOUND('',#17493,.T.);
#11569=FACE_OUTER_BOUND('',#17494,.T.);
#11570=FACE_OUTER_BOUND('',#17495,.T.);
#11571=FACE_OUTER_BOUND('',#17496,.T.);
#11572=FACE_OUTER_BOUND('',#17497,.T.);
#11573=FACE_OUTER_BOUND('',#17498,.T.);
#11574=FACE_OUTER_BOUND('',#17499,.T.);
#11575=FACE_OUTER_BOUND('',#17500,.T.);
#11576=FACE_OUTER_BOUND('',#17501,.T.);
#11577=FACE_OUTER_BOUND('',#17502,.T.);
#11578=FACE_OUTER_BOUND('',#17503,.T.);
#11579=FACE_OUTER_BOUND('',#17504,.T.);
#11580=FACE_OUTER_BOUND('',#17505,.T.);
#11581=FACE_OUTER_BOUND('',#17506,.T.);
#11582=FACE_OUTER_BOUND('',#17507,.T.);
#11583=FACE_OUTER_BOUND('',#17508,.T.);
#11584=FACE_OUTER_BOUND('',#17509,.T.);
#11585=FACE_OUTER_BOUND('',#17510,.T.);
#11586=FACE_OUTER_BOUND('',#17511,.T.);
#11587=FACE_OUTER_BOUND('',#17512,.T.);
#11588=FACE_OUTER_BOUND('',#17513,.T.);
#11589=FACE_OUTER_BOUND('',#17514,.T.);
#11590=FACE_OUTER_BOUND('',#17515,.T.);
#11591=FACE_OUTER_BOUND('',#17516,.T.);
#11592=FACE_OUTER_BOUND('',#17517,.T.);
#11593=FACE_OUTER_BOUND('',#17518,.T.);
#11594=FACE_OUTER_BOUND('',#17519,.T.);
#11595=FACE_OUTER_BOUND('',#17520,.T.);
#11596=FACE_OUTER_BOUND('',#17521,.T.);
#11597=FACE_OUTER_BOUND('',#17522,.T.);
#11598=FACE_OUTER_BOUND('',#17523,.T.);
#11599=FACE_OUTER_BOUND('',#17524,.T.);
#11600=FACE_OUTER_BOUND('',#17525,.T.);
#11601=FACE_OUTER_BOUND('',#17526,.T.);
#11602=FACE_OUTER_BOUND('',#17527,.T.);
#11603=FACE_OUTER_BOUND('',#17528,.T.);
#11604=FACE_OUTER_BOUND('',#17529,.T.);
#11605=FACE_OUTER_BOUND('',#17530,.T.);
#11606=FACE_OUTER_BOUND('',#17531,.T.);
#11607=FACE_OUTER_BOUND('',#17532,.T.);
#11608=FACE_OUTER_BOUND('',#17533,.T.);
#11609=FACE_OUTER_BOUND('',#17534,.T.);
#11610=FACE_OUTER_BOUND('',#17535,.T.);
#11611=FACE_OUTER_BOUND('',#17536,.T.);
#11612=FACE_OUTER_BOUND('',#17537,.T.);
#11613=FACE_OUTER_BOUND('',#17538,.T.);
#11614=FACE_OUTER_BOUND('',#17539,.T.);
#11615=FACE_OUTER_BOUND('',#17540,.T.);
#11616=FACE_OUTER_BOUND('',#17541,.T.);
#11617=FACE_OUTER_BOUND('',#17542,.T.);
#11618=FACE_OUTER_BOUND('',#17543,.T.);
#11619=FACE_OUTER_BOUND('',#17544,.T.);
#11620=FACE_OUTER_BOUND('',#17545,.T.);
#11621=FACE_OUTER_BOUND('',#17546,.T.);
#11622=FACE_OUTER_BOUND('',#17547,.T.);
#11623=FACE_OUTER_BOUND('',#17548,.T.);
#11624=FACE_OUTER_BOUND('',#17549,.T.);
#11625=FACE_OUTER_BOUND('',#17550,.T.);
#11626=FACE_OUTER_BOUND('',#17551,.T.);
#11627=FACE_OUTER_BOUND('',#17552,.T.);
#11628=FACE_OUTER_BOUND('',#17553,.T.);
#11629=FACE_OUTER_BOUND('',#17554,.T.);
#11630=FACE_OUTER_BOUND('',#17555,.T.);
#11631=FACE_OUTER_BOUND('',#17556,.T.);
#11632=FACE_OUTER_BOUND('',#17557,.T.);
#11633=FACE_OUTER_BOUND('',#17558,.T.);
#11634=FACE_OUTER_BOUND('',#17559,.T.);
#11635=FACE_OUTER_BOUND('',#17560,.T.);
#11636=FACE_OUTER_BOUND('',#17561,.T.);
#11637=FACE_OUTER_BOUND('',#17562,.T.);
#11638=FACE_OUTER_BOUND('',#17563,.T.);
#11639=FACE_OUTER_BOUND('',#17564,.T.);
#11640=FACE_OUTER_BOUND('',#17565,.T.);
#11641=FACE_OUTER_BOUND('',#17566,.T.);
#11642=FACE_OUTER_BOUND('',#17567,.T.);
#11643=FACE_OUTER_BOUND('',#17568,.T.);
#11644=FACE_OUTER_BOUND('',#17569,.T.);
#11645=FACE_OUTER_BOUND('',#17570,.T.);
#11646=FACE_OUTER_BOUND('',#17571,.T.);
#11647=FACE_OUTER_BOUND('',#17572,.T.);
#11648=FACE_OUTER_BOUND('',#17573,.T.);
#11649=FACE_OUTER_BOUND('',#17574,.T.);
#11650=FACE_OUTER_BOUND('',#17575,.T.);
#11651=FACE_OUTER_BOUND('',#17576,.T.);
#11652=FACE_OUTER_BOUND('',#17577,.T.);
#11653=FACE_OUTER_BOUND('',#17578,.T.);
#11654=FACE_OUTER_BOUND('',#17579,.T.);
#11655=FACE_OUTER_BOUND('',#17580,.T.);
#11656=FACE_OUTER_BOUND('',#17581,.T.);
#11657=FACE_OUTER_BOUND('',#17582,.T.);
#11658=FACE_OUTER_BOUND('',#17583,.T.);
#11659=FACE_OUTER_BOUND('',#17584,.T.);
#11660=FACE_OUTER_BOUND('',#17585,.T.);
#11661=FACE_OUTER_BOUND('',#17586,.T.);
#11662=FACE_OUTER_BOUND('',#17587,.T.);
#11663=FACE_OUTER_BOUND('',#17588,.T.);
#11664=FACE_OUTER_BOUND('',#17589,.T.);
#11665=FACE_OUTER_BOUND('',#17590,.T.);
#11666=FACE_OUTER_BOUND('',#17591,.T.);
#11667=FACE_OUTER_BOUND('',#17592,.T.);
#11668=FACE_OUTER_BOUND('',#17593,.T.);
#11669=FACE_OUTER_BOUND('',#17594,.T.);
#11670=FACE_OUTER_BOUND('',#17595,.T.);
#11671=FACE_OUTER_BOUND('',#17596,.T.);
#11672=FACE_OUTER_BOUND('',#17597,.T.);
#11673=FACE_OUTER_BOUND('',#17598,.T.);
#11674=FACE_OUTER_BOUND('',#17599,.T.);
#11675=FACE_OUTER_BOUND('',#17600,.T.);
#11676=FACE_OUTER_BOUND('',#17601,.T.);
#11677=FACE_OUTER_BOUND('',#17602,.T.);
#11678=FACE_OUTER_BOUND('',#17603,.T.);
#11679=FACE_OUTER_BOUND('',#17604,.T.);
#11680=FACE_OUTER_BOUND('',#17605,.T.);
#11681=FACE_OUTER_BOUND('',#17606,.T.);
#11682=FACE_OUTER_BOUND('',#17607,.T.);
#11683=FACE_OUTER_BOUND('',#17608,.T.);
#11684=FACE_OUTER_BOUND('',#17609,.T.);
#11685=FACE_OUTER_BOUND('',#17610,.T.);
#11686=FACE_OUTER_BOUND('',#17611,.T.);
#11687=FACE_OUTER_BOUND('',#17612,.T.);
#11688=FACE_OUTER_BOUND('',#17613,.T.);
#11689=FACE_OUTER_BOUND('',#17614,.T.);
#11690=FACE_OUTER_BOUND('',#17615,.T.);
#11691=FACE_OUTER_BOUND('',#17616,.T.);
#11692=FACE_OUTER_BOUND('',#17617,.T.);
#11693=FACE_OUTER_BOUND('',#17618,.T.);
#11694=FACE_OUTER_BOUND('',#17619,.T.);
#11695=FACE_OUTER_BOUND('',#17620,.T.);
#11696=FACE_OUTER_BOUND('',#17621,.T.);
#11697=FACE_OUTER_BOUND('',#17622,.T.);
#11698=FACE_OUTER_BOUND('',#17623,.T.);
#11699=FACE_OUTER_BOUND('',#17624,.T.);
#11700=FACE_OUTER_BOUND('',#17625,.T.);
#11701=FACE_OUTER_BOUND('',#17626,.T.);
#11702=FACE_OUTER_BOUND('',#17627,.T.);
#11703=FACE_OUTER_BOUND('',#17628,.T.);
#11704=FACE_OUTER_BOUND('',#17629,.T.);
#11705=FACE_OUTER_BOUND('',#17630,.T.);
#11706=FACE_OUTER_BOUND('',#17631,.T.);
#11707=FACE_OUTER_BOUND('',#17632,.T.);
#11708=FACE_OUTER_BOUND('',#17633,.T.);
#11709=FACE_OUTER_BOUND('',#17634,.T.);
#11710=FACE_OUTER_BOUND('',#17635,.T.);
#11711=FACE_OUTER_BOUND('',#17636,.T.);
#11712=FACE_OUTER_BOUND('',#17637,.T.);
#11713=FACE_OUTER_BOUND('',#17638,.T.);
#11714=FACE_OUTER_BOUND('',#17639,.T.);
#11715=FACE_OUTER_BOUND('',#17640,.T.);
#11716=FACE_OUTER_BOUND('',#17641,.T.);
#11717=FACE_OUTER_BOUND('',#17642,.T.);
#11718=FACE_OUTER_BOUND('',#17643,.T.);
#11719=FACE_OUTER_BOUND('',#17644,.T.);
#11720=FACE_OUTER_BOUND('',#17645,.T.);
#11721=FACE_OUTER_BOUND('',#17646,.T.);
#11722=FACE_OUTER_BOUND('',#17647,.T.);
#11723=FACE_OUTER_BOUND('',#17648,.T.);
#11724=FACE_OUTER_BOUND('',#17649,.T.);
#11725=FACE_OUTER_BOUND('',#17650,.T.);
#11726=FACE_OUTER_BOUND('',#17651,.T.);
#11727=FACE_OUTER_BOUND('',#17652,.T.);
#11728=FACE_OUTER_BOUND('',#17653,.T.);
#11729=FACE_OUTER_BOUND('',#17654,.T.);
#11730=FACE_OUTER_BOUND('',#17655,.T.);
#11731=FACE_OUTER_BOUND('',#17656,.T.);
#11732=FACE_OUTER_BOUND('',#17657,.T.);
#11733=FACE_OUTER_BOUND('',#17658,.T.);
#11734=FACE_OUTER_BOUND('',#17659,.T.);
#11735=FACE_OUTER_BOUND('',#17660,.T.);
#11736=FACE_OUTER_BOUND('',#17661,.T.);
#11737=FACE_OUTER_BOUND('',#17662,.T.);
#11738=FACE_OUTER_BOUND('',#17663,.T.);
#11739=FACE_OUTER_BOUND('',#17664,.T.);
#11740=FACE_OUTER_BOUND('',#17665,.T.);
#11741=FACE_OUTER_BOUND('',#17666,.T.);
#11742=FACE_OUTER_BOUND('',#17667,.T.);
#11743=FACE_OUTER_BOUND('',#17668,.T.);
#11744=FACE_OUTER_BOUND('',#17669,.T.);
#11745=FACE_OUTER_BOUND('',#17670,.T.);
#11746=FACE_OUTER_BOUND('',#17671,.T.);
#11747=FACE_OUTER_BOUND('',#17672,.T.);
#11748=FACE_OUTER_BOUND('',#17673,.T.);
#11749=FACE_OUTER_BOUND('',#17674,.T.);
#11750=FACE_OUTER_BOUND('',#17675,.T.);
#11751=FACE_OUTER_BOUND('',#17676,.T.);
#11752=FACE_OUTER_BOUND('',#17677,.T.);
#11753=FACE_OUTER_BOUND('',#17678,.T.);
#11754=FACE_OUTER_BOUND('',#17679,.T.);
#11755=FACE_OUTER_BOUND('',#17680,.T.);
#11756=FACE_OUTER_BOUND('',#17681,.T.);
#11757=FACE_OUTER_BOUND('',#17682,.T.);
#11758=FACE_OUTER_BOUND('',#17683,.T.);
#11759=FACE_OUTER_BOUND('',#17684,.T.);
#11760=FACE_OUTER_BOUND('',#17685,.T.);
#11761=FACE_OUTER_BOUND('',#17686,.T.);
#11762=FACE_OUTER_BOUND('',#17687,.T.);
#11763=FACE_OUTER_BOUND('',#17688,.T.);
#11764=FACE_OUTER_BOUND('',#17689,.T.);
#11765=FACE_OUTER_BOUND('',#17690,.T.);
#11766=FACE_OUTER_BOUND('',#17691,.T.);
#11767=FACE_OUTER_BOUND('',#17692,.T.);
#11768=FACE_OUTER_BOUND('',#17693,.T.);
#11769=FACE_OUTER_BOUND('',#17694,.T.);
#11770=FACE_OUTER_BOUND('',#17695,.T.);
#11771=FACE_OUTER_BOUND('',#17696,.T.);
#11772=FACE_OUTER_BOUND('',#17697,.T.);
#11773=FACE_OUTER_BOUND('',#17698,.T.);
#11774=FACE_OUTER_BOUND('',#17699,.T.);
#11775=FACE_OUTER_BOUND('',#17700,.T.);
#11776=FACE_OUTER_BOUND('',#17701,.T.);
#11777=FACE_OUTER_BOUND('',#17702,.T.);
#11778=FACE_OUTER_BOUND('',#17703,.T.);
#11779=FACE_OUTER_BOUND('',#17704,.T.);
#11780=FACE_OUTER_BOUND('',#17705,.T.);
#11781=FACE_OUTER_BOUND('',#17706,.T.);
#11782=FACE_OUTER_BOUND('',#17707,.T.);
#11783=FACE_OUTER_BOUND('',#17708,.T.);
#11784=FACE_OUTER_BOUND('',#17709,.T.);
#11785=FACE_OUTER_BOUND('',#17710,.T.);
#11786=FACE_OUTER_BOUND('',#17711,.T.);
#11787=FACE_OUTER_BOUND('',#17712,.T.);
#11788=FACE_OUTER_BOUND('',#17713,.T.);
#11789=FACE_OUTER_BOUND('',#17714,.T.);
#11790=FACE_OUTER_BOUND('',#17715,.T.);
#11791=FACE_OUTER_BOUND('',#17716,.T.);
#11792=FACE_OUTER_BOUND('',#17717,.T.);
#11793=FACE_OUTER_BOUND('',#17718,.T.);
#11794=FACE_OUTER_BOUND('',#17719,.T.);
#11795=FACE_OUTER_BOUND('',#17720,.T.);
#11796=FACE_OUTER_BOUND('',#17721,.T.);
#11797=FACE_OUTER_BOUND('',#17722,.T.);
#11798=FACE_OUTER_BOUND('',#17723,.T.);
#11799=FACE_OUTER_BOUND('',#17724,.T.);
#11800=FACE_OUTER_BOUND('',#17725,.T.);
#11801=FACE_OUTER_BOUND('',#17726,.T.);
#11802=FACE_OUTER_BOUND('',#17727,.T.);
#11803=FACE_OUTER_BOUND('',#17728,.T.);
#11804=FACE_OUTER_BOUND('',#17729,.T.);
#11805=FACE_OUTER_BOUND('',#17730,.T.);
#11806=FACE_OUTER_BOUND('',#17731,.T.);
#11807=FACE_OUTER_BOUND('',#17732,.T.);
#11808=FACE_OUTER_BOUND('',#17733,.T.);
#11809=FACE_OUTER_BOUND('',#17734,.T.);
#11810=FACE_OUTER_BOUND('',#17735,.T.);
#11811=FACE_OUTER_BOUND('',#17736,.T.);
#11812=FACE_OUTER_BOUND('',#17737,.T.);
#11813=FACE_OUTER_BOUND('',#17738,.T.);
#11814=FACE_OUTER_BOUND('',#17739,.T.);
#11815=FACE_OUTER_BOUND('',#17740,.T.);
#11816=FACE_OUTER_BOUND('',#17741,.T.);
#11817=FACE_OUTER_BOUND('',#17742,.T.);
#11818=FACE_OUTER_BOUND('',#17743,.T.);
#11819=FACE_OUTER_BOUND('',#17744,.T.);
#11820=FACE_OUTER_BOUND('',#17745,.T.);
#11821=FACE_OUTER_BOUND('',#17746,.T.);
#11822=FACE_OUTER_BOUND('',#17747,.T.);
#11823=FACE_OUTER_BOUND('',#17748,.T.);
#11824=FACE_OUTER_BOUND('',#17749,.T.);
#11825=FACE_OUTER_BOUND('',#17750,.T.);
#11826=FACE_OUTER_BOUND('',#17751,.T.);
#11827=FACE_OUTER_BOUND('',#17752,.T.);
#11828=FACE_OUTER_BOUND('',#17753,.T.);
#11829=FACE_OUTER_BOUND('',#17754,.T.);
#11830=FACE_OUTER_BOUND('',#17755,.T.);
#11831=FACE_OUTER_BOUND('',#17756,.T.);
#11832=FACE_OUTER_BOUND('',#17757,.T.);
#11833=FACE_OUTER_BOUND('',#17758,.T.);
#11834=FACE_OUTER_BOUND('',#17759,.T.);
#11835=FACE_OUTER_BOUND('',#17760,.T.);
#11836=FACE_OUTER_BOUND('',#17761,.T.);
#11837=FACE_OUTER_BOUND('',#17762,.T.);
#11838=FACE_OUTER_BOUND('',#17763,.T.);
#11839=FACE_OUTER_BOUND('',#17764,.T.);
#11840=FACE_OUTER_BOUND('',#17765,.T.);
#11841=FACE_OUTER_BOUND('',#17766,.T.);
#11842=FACE_OUTER_BOUND('',#17767,.T.);
#11843=FACE_OUTER_BOUND('',#17768,.T.);
#11844=FACE_OUTER_BOUND('',#17769,.T.);
#11845=FACE_OUTER_BOUND('',#17770,.T.);
#11846=FACE_OUTER_BOUND('',#17771,.T.);
#11847=FACE_OUTER_BOUND('',#17772,.T.);
#11848=FACE_OUTER_BOUND('',#17773,.T.);
#11849=FACE_OUTER_BOUND('',#17774,.T.);
#11850=FACE_OUTER_BOUND('',#17775,.T.);
#11851=FACE_OUTER_BOUND('',#17776,.T.);
#11852=FACE_OUTER_BOUND('',#17777,.T.);
#11853=FACE_OUTER_BOUND('',#17778,.T.);
#11854=FACE_OUTER_BOUND('',#17779,.T.);
#11855=FACE_OUTER_BOUND('',#17780,.T.);
#11856=FACE_OUTER_BOUND('',#17781,.T.);
#11857=FACE_OUTER_BOUND('',#17782,.T.);
#11858=FACE_OUTER_BOUND('',#17783,.T.);
#11859=FACE_OUTER_BOUND('',#17784,.T.);
#11860=FACE_OUTER_BOUND('',#17785,.T.);
#11861=FACE_OUTER_BOUND('',#17786,.T.);
#11862=FACE_OUTER_BOUND('',#17787,.T.);
#11863=FACE_OUTER_BOUND('',#17788,.T.);
#11864=FACE_OUTER_BOUND('',#17789,.T.);
#11865=FACE_OUTER_BOUND('',#17790,.T.);
#11866=FACE_OUTER_BOUND('',#17791,.T.);
#11867=FACE_OUTER_BOUND('',#17792,.T.);
#11868=FACE_OUTER_BOUND('',#17793,.T.);
#11869=FACE_OUTER_BOUND('',#17794,.T.);
#11870=FACE_OUTER_BOUND('',#17795,.T.);
#11871=FACE_OUTER_BOUND('',#17796,.T.);
#11872=FACE_OUTER_BOUND('',#17797,.T.);
#11873=FACE_OUTER_BOUND('',#17798,.T.);
#11874=FACE_OUTER_BOUND('',#17799,.T.);
#11875=FACE_OUTER_BOUND('',#17800,.T.);
#11876=FACE_OUTER_BOUND('',#17801,.T.);
#11877=FACE_OUTER_BOUND('',#17802,.T.);
#11878=FACE_OUTER_BOUND('',#17803,.T.);
#11879=FACE_OUTER_BOUND('',#17804,.T.);
#11880=FACE_OUTER_BOUND('',#17805,.T.);
#11881=FACE_OUTER_BOUND('',#17806,.T.);
#11882=FACE_OUTER_BOUND('',#17807,.T.);
#11883=FACE_OUTER_BOUND('',#17808,.T.);
#11884=FACE_OUTER_BOUND('',#17809,.T.);
#11885=FACE_OUTER_BOUND('',#17810,.T.);
#11886=FACE_OUTER_BOUND('',#17811,.T.);
#11887=FACE_OUTER_BOUND('',#17812,.T.);
#11888=FACE_OUTER_BOUND('',#17813,.T.);
#11889=FACE_OUTER_BOUND('',#17814,.T.);
#11890=FACE_OUTER_BOUND('',#17815,.T.);
#11891=FACE_OUTER_BOUND('',#17816,.T.);
#11892=FACE_OUTER_BOUND('',#17817,.T.);
#11893=FACE_OUTER_BOUND('',#17818,.T.);
#11894=FACE_OUTER_BOUND('',#17819,.T.);
#11895=FACE_OUTER_BOUND('',#17820,.T.);
#11896=FACE_OUTER_BOUND('',#17821,.T.);
#11897=FACE_OUTER_BOUND('',#17822,.T.);
#11898=FACE_OUTER_BOUND('',#17823,.T.);
#11899=FACE_OUTER_BOUND('',#17824,.T.);
#11900=FACE_OUTER_BOUND('',#17825,.T.);
#11901=FACE_OUTER_BOUND('',#17826,.T.);
#11902=FACE_OUTER_BOUND('',#17827,.T.);
#16332=EDGE_LOOP('',(#78450,#78451,#78452));
#16333=EDGE_LOOP('',(#78453,#78454,#78455,#78456));
#16334=EDGE_LOOP('',(#78457,#78458,#78459,#78460));
#16335=EDGE_LOOP('',(#78461,#78462,#78463,#78464));
#16336=EDGE_LOOP('',(#78465,#78466,#78467,#78468));
#16337=EDGE_LOOP('',(#78469,#78470,#78471,#78472));
#16338=EDGE_LOOP('',(#78473,#78474,#78475,#78476));
#16339=EDGE_LOOP('',(#78477,#78478,#78479,#78480));
#16340=EDGE_LOOP('',(#78481,#78482,#78483,#78484));
#16341=EDGE_LOOP('',(#78485,#78486,#78487,#78488));
#16342=EDGE_LOOP('',(#78489,#78490,#78491,#78492));
#16343=EDGE_LOOP('',(#78493,#78494,#78495,#78496));
#16344=EDGE_LOOP('',(#78497,#78498,#78499,#78500));
#16345=EDGE_LOOP('',(#78501,#78502,#78503,#78504));
#16346=EDGE_LOOP('',(#78505,#78506,#78507,#78508));
#16347=EDGE_LOOP('',(#78509,#78510,#78511,#78512));
#16348=EDGE_LOOP('',(#78513,#78514,#78515,#78516));
#16349=EDGE_LOOP('',(#78517,#78518,#78519,#78520));
#16350=EDGE_LOOP('',(#78521,#78522,#78523,#78524));
#16351=EDGE_LOOP('',(#78525,#78526,#78527,#78528));
#16352=EDGE_LOOP('',(#78529,#78530,#78531,#78532));
#16353=EDGE_LOOP('',(#78533,#78534,#78535,#78536));
#16354=EDGE_LOOP('',(#78537,#78538,#78539,#78540));
#16355=EDGE_LOOP('',(#78541,#78542,#78543,#78544));
#16356=EDGE_LOOP('',(#78545,#78546,#78547,#78548));
#16357=EDGE_LOOP('',(#78549,#78550,#78551,#78552));
#16358=EDGE_LOOP('',(#78553,#78554,#78555,#78556));
#16359=EDGE_LOOP('',(#78557,#78558,#78559,#78560));
#16360=EDGE_LOOP('',(#78561,#78562,#78563,#78564));
#16361=EDGE_LOOP('',(#78565,#78566,#78567,#78568));
#16362=EDGE_LOOP('',(#78569,#78570,#78571,#78572));
#16363=EDGE_LOOP('',(#78573,#78574,#78575,#78576));
#16364=EDGE_LOOP('',(#78577,#78578,#78579,#78580));
#16365=EDGE_LOOP('',(#78581,#78582,#78583,#78584));
#16366=EDGE_LOOP('',(#78585,#78586,#78587,#78588));
#16367=EDGE_LOOP('',(#78589,#78590,#78591,#78592));
#16368=EDGE_LOOP('',(#78593,#78594,#78595,#78596));
#16369=EDGE_LOOP('',(#78597,#78598,#78599));
#16370=EDGE_LOOP('',(#78600,#78601,#78602,#78603));
#16371=EDGE_LOOP('',(#78604,#78605,#78606,#78607));
#16372=EDGE_LOOP('',(#78608,#78609,#78610,#78611));
#16373=EDGE_LOOP('',(#78612,#78613,#78614,#78615));
#16374=EDGE_LOOP('',(#78616,#78617,#78618,#78619));
#16375=EDGE_LOOP('',(#78620,#78621,#78622,#78623));
#16376=EDGE_LOOP('',(#78624,#78625,#78626,#78627));
#16377=EDGE_LOOP('',(#78628,#78629,#78630,#78631));
#16378=EDGE_LOOP('',(#78632,#78633,#78634,#78635));
#16379=EDGE_LOOP('',(#78636,#78637,#78638,#78639));
#16380=EDGE_LOOP('',(#78640,#78641,#78642,#78643));
#16381=EDGE_LOOP('',(#78644,#78645,#78646,#78647));
#16382=EDGE_LOOP('',(#78648,#78649,#78650,#78651));
#16383=EDGE_LOOP('',(#78652,#78653,#78654,#78655));
#16384=EDGE_LOOP('',(#78656,#78657,#78658,#78659));
#16385=EDGE_LOOP('',(#78660,#78661,#78662,#78663));
#16386=EDGE_LOOP('',(#78664,#78665,#78666,#78667));
#16387=EDGE_LOOP('',(#78668,#78669,#78670,#78671));
#16388=EDGE_LOOP('',(#78672,#78673,#78674,#78675));
#16389=EDGE_LOOP('',(#78676,#78677,#78678,#78679));
#16390=EDGE_LOOP('',(#78680,#78681,#78682,#78683));
#16391=EDGE_LOOP('',(#78684,#78685,#78686,#78687));
#16392=EDGE_LOOP('',(#78688,#78689,#78690,#78691));
#16393=EDGE_LOOP('',(#78692,#78693,#78694,#78695));
#16394=EDGE_LOOP('',(#78696,#78697,#78698,#78699));
#16395=EDGE_LOOP('',(#78700,#78701,#78702,#78703));
#16396=EDGE_LOOP('',(#78704,#78705,#78706,#78707));
#16397=EDGE_LOOP('',(#78708,#78709,#78710,#78711));
#16398=EDGE_LOOP('',(#78712,#78713,#78714,#78715));
#16399=EDGE_LOOP('',(#78716,#78717,#78718,#78719));
#16400=EDGE_LOOP('',(#78720,#78721,#78722,#78723));
#16401=EDGE_LOOP('',(#78724,#78725,#78726,#78727,#78728));
#16402=EDGE_LOOP('',(#78729,#78730,#78731,#78732));
#16403=EDGE_LOOP('',(#78733,#78734,#78735,#78736));
#16404=EDGE_LOOP('',(#78737,#78738,#78739,#78740,#78741,#78742,#78743));
#16405=EDGE_LOOP('',(#78744,#78745,#78746,#78747));
#16406=EDGE_LOOP('',(#78748,#78749,#78750,#78751));
#16407=EDGE_LOOP('',(#78752,#78753,#78754,#78755));
#16408=EDGE_LOOP('',(#78756,#78757,#78758,#78759));
#16409=EDGE_LOOP('',(#78760,#78761,#78762,#78763));
#16410=EDGE_LOOP('',(#78764,#78765,#78766,#78767));
#16411=EDGE_LOOP('',(#78768,#78769,#78770,#78771));
#16412=EDGE_LOOP('',(#78772,#78773,#78774,#78775));
#16413=EDGE_LOOP('',(#78776,#78777,#78778,#78779));
#16414=EDGE_LOOP('',(#78780,#78781,#78782,#78783));
#16415=EDGE_LOOP('',(#78784,#78785,#78786,#78787));
#16416=EDGE_LOOP('',(#78788,#78789,#78790,#78791));
#16417=EDGE_LOOP('',(#78792,#78793,#78794,#78795));
#16418=EDGE_LOOP('',(#78796,#78797,#78798,#78799));
#16419=EDGE_LOOP('',(#78800,#78801,#78802,#78803));
#16420=EDGE_LOOP('',(#78804,#78805,#78806,#78807));
#16421=EDGE_LOOP('',(#78808,#78809,#78810,#78811));
#16422=EDGE_LOOP('',(#78812,#78813,#78814,#78815));
#16423=EDGE_LOOP('',(#78816,#78817,#78818,#78819));
#16424=EDGE_LOOP('',(#78820,#78821,#78822,#78823));
#16425=EDGE_LOOP('',(#78824,#78825,#78826,#78827));
#16426=EDGE_LOOP('',(#78828,#78829,#78830,#78831));
#16427=EDGE_LOOP('',(#78832,#78833,#78834,#78835));
#16428=EDGE_LOOP('',(#78836,#78837,#78838,#78839));
#16429=EDGE_LOOP('',(#78840,#78841,#78842,#78843));
#16430=EDGE_LOOP('',(#78844,#78845,#78846,#78847));
#16431=EDGE_LOOP('',(#78848,#78849,#78850,#78851));
#16432=EDGE_LOOP('',(#78852,#78853,#78854,#78855));
#16433=EDGE_LOOP('',(#78856,#78857,#78858,#78859));
#16434=EDGE_LOOP('',(#78860,#78861,#78862,#78863));
#16435=EDGE_LOOP('',(#78864,#78865,#78866,#78867));
#16436=EDGE_LOOP('',(#78868,#78869,#78870,#78871));
#16437=EDGE_LOOP('',(#78872,#78873,#78874,#78875));
#16438=EDGE_LOOP('',(#78876,#78877,#78878,#78879));
#16439=EDGE_LOOP('',(#78880,#78881,#78882,#78883));
#16440=EDGE_LOOP('',(#78884,#78885,#78886,#78887));
#16441=EDGE_LOOP('',(#78888,#78889,#78890,#78891));
#16442=EDGE_LOOP('',(#78892,#78893,#78894,#78895));
#16443=EDGE_LOOP('',(#78896,#78897,#78898,#78899));
#16444=EDGE_LOOP('',(#78900,#78901,#78902,#78903));
#16445=EDGE_LOOP('',(#78904,#78905,#78906,#78907));
#16446=EDGE_LOOP('',(#78908,#78909,#78910,#78911));
#16447=EDGE_LOOP('',(#78912,#78913,#78914,#78915));
#16448=EDGE_LOOP('',(#78916,#78917,#78918,#78919));
#16449=EDGE_LOOP('',(#78920,#78921,#78922,#78923));
#16450=EDGE_LOOP('',(#78924,#78925,#78926,#78927));
#16451=EDGE_LOOP('',(#78928,#78929,#78930,#78931));
#16452=EDGE_LOOP('',(#78932,#78933,#78934,#78935));
#16453=EDGE_LOOP('',(#78936,#78937,#78938,#78939));
#16454=EDGE_LOOP('',(#78940,#78941,#78942,#78943));
#16455=EDGE_LOOP('',(#78944,#78945,#78946,#78947));
#16456=EDGE_LOOP('',(#78948,#78949,#78950,#78951));
#16457=EDGE_LOOP('',(#78952,#78953,#78954,#78955));
#16458=EDGE_LOOP('',(#78956,#78957,#78958,#78959));
#16459=EDGE_LOOP('',(#78960,#78961,#78962,#78963));
#16460=EDGE_LOOP('',(#78964,#78965,#78966,#78967));
#16461=EDGE_LOOP('',(#78968,#78969,#78970,#78971));
#16462=EDGE_LOOP('',(#78972,#78973,#78974,#78975));
#16463=EDGE_LOOP('',(#78976,#78977,#78978,#78979));
#16464=EDGE_LOOP('',(#78980,#78981,#78982,#78983));
#16465=EDGE_LOOP('',(#78984,#78985,#78986,#78987));
#16466=EDGE_LOOP('',(#78988,#78989,#78990,#78991));
#16467=EDGE_LOOP('',(#78992,#78993,#78994,#78995));
#16468=EDGE_LOOP('',(#78996,#78997,#78998,#78999));
#16469=EDGE_LOOP('',(#79000,#79001,#79002,#79003));
#16470=EDGE_LOOP('',(#79004,#79005,#79006,#79007));
#16471=EDGE_LOOP('',(#79008,#79009,#79010,#79011));
#16472=EDGE_LOOP('',(#79012,#79013,#79014,#79015));
#16473=EDGE_LOOP('',(#79016,#79017,#79018,#79019));
#16474=EDGE_LOOP('',(#79020,#79021,#79022,#79023));
#16475=EDGE_LOOP('',(#79024,#79025,#79026,#79027));
#16476=EDGE_LOOP('',(#79028,#79029,#79030,#79031));
#16477=EDGE_LOOP('',(#79032,#79033,#79034,#79035));
#16478=EDGE_LOOP('',(#79036,#79037,#79038,#79039));
#16479=EDGE_LOOP('',(#79040,#79041,#79042,#79043));
#16480=EDGE_LOOP('',(#79044,#79045,#79046,#79047));
#16481=EDGE_LOOP('',(#79048,#79049,#79050,#79051,#79052));
#16482=EDGE_LOOP('',(#79053,#79054,#79055,#79056));
#16483=EDGE_LOOP('',(#79057,#79058,#79059,#79060,#79061));
#16484=EDGE_LOOP('',(#79062,#79063,#79064,#79065));
#16485=EDGE_LOOP('',(#79066,#79067,#79068));
#16486=EDGE_LOOP('',(#79069,#79070,#79071,#79072,#79073,#79074,#79075,#79076));
#16487=EDGE_LOOP('',(#79077,#79078));
#16488=EDGE_LOOP('',(#79079,#79080,#79081,#79082));
#16489=EDGE_LOOP('',(#79083,#79084,#79085,#79086));
#16490=EDGE_LOOP('',(#79087,#79088,#79089,#79090));
#16491=EDGE_LOOP('',(#79091,#79092,#79093,#79094,#79095,#79096,#79097,#79098,
#79099,#79100,#79101,#79102,#79103,#79104,#79105,#79106,#79107,#79108,#79109,
#79110,#79111,#79112,#79113,#79114,#79115,#79116,#79117,#79118,#79119,#79120,
#79121,#79122,#79123,#79124,#79125,#79126,#79127,#79128,#79129,#79130,#79131,
#79132,#79133,#79134,#79135,#79136,#79137,#79138,#79139,#79140,#79141,#79142,
#79143,#79144,#79145,#79146,#79147,#79148,#79149,#79150,#79151,#79152,#79153,
#79154,#79155,#79156,#79157,#79158,#79159,#79160,#79161,#79162,#79163,#79164,
#79165,#79166,#79167,#79168,#79169,#79170,#79171,#79172,#79173,#79174,#79175,
#79176,#79177,#79178,#79179,#79180,#79181,#79182,#79183,#79184,#79185,#79186,
#79187,#79188,#79189,#79190,#79191,#79192,#79193,#79194,#79195,#79196,#79197,
#79198,#79199,#79200,#79201,#79202,#79203,#79204,#79205,#79206,#79207,#79208,
#79209,#79210,#79211,#79212,#79213,#79214,#79215,#79216,#79217,#79218,#79219,
#79220,#79221,#79222,#79223,#79224,#79225,#79226,#79227,#79228,#79229,#79230,
#79231,#79232,#79233,#79234,#79235,#79236,#79237,#79238,#79239,#79240,#79241,
#79242,#79243,#79244,#79245,#79246,#79247,#79248,#79249,#79250,#79251,#79252,
#79253,#79254,#79255,#79256,#79257,#79258,#79259,#79260,#79261,#79262,#79263,
#79264,#79265,#79266,#79267,#79268,#79269,#79270,#79271,#79272,#79273,#79274,
#79275,#79276,#79277,#79278,#79279,#79280,#79281,#79282,#79283,#79284,#79285,
#79286,#79287,#79288,#79289,#79290,#79291,#79292,#79293,#79294,#79295,#79296,
#79297,#79298,#79299,#79300,#79301,#79302,#79303,#79304,#79305,#79306,#79307,
#79308,#79309,#79310,#79311,#79312,#79313,#79314,#79315,#79316,#79317,#79318,
#79319,#79320,#79321,#79322,#79323,#79324,#79325,#79326,#79327,#79328,#79329,
#79330,#79331,#79332,#79333,#79334,#79335,#79336,#79337,#79338,#79339,#79340,
#79341,#79342,#79343,#79344,#79345,#79346,#79347,#79348,#79349,#79350,#79351,
#79352,#79353,#79354,#79355,#79356,#79357,#79358,#79359,#79360,#79361,#79362,
#79363,#79364,#79365,#79366,#79367,#79368,#79369,#79370,#79371,#79372,#79373,
#79374,#79375,#79376,#79377,#79378,#79379,#79380,#79381,#79382,#79383,#79384,
#79385,#79386,#79387,#79388,#79389,#79390,#79391,#79392,#79393,#79394,#79395,
#79396,#79397,#79398,#79399,#79400,#79401,#79402,#79403,#79404));
#16492=EDGE_LOOP('',(#79405,#79406,#79407,#79408,#79409));
#16493=EDGE_LOOP('',(#79410,#79411,#79412,#79413,#79414,#79415,#79416,#79417,
#79418,#79419,#79420,#79421,#79422,#79423,#79424,#79425,#79426,#79427,#79428,
#79429,#79430,#79431,#79432,#79433,#79434,#79435,#79436,#79437,#79438,#79439,
#79440,#79441,#79442,#79443,#79444,#79445,#79446,#79447,#79448,#79449,#79450,
#79451,#79452,#79453,#79454,#79455,#79456,#79457,#79458,#79459,#79460,#79461,
#79462,#79463,#79464,#79465,#79466,#79467,#79468,#79469,#79470,#79471,#79472,
#79473,#79474,#79475,#79476,#79477,#79478,#79479,#79480,#79481,#79482,#79483,
#79484,#79485,#79486,#79487,#79488,#79489,#79490,#79491,#79492,#79493,#79494,
#79495,#79496,#79497,#79498,#79499,#79500,#79501,#79502,#79503,#79504,#79505,
#79506,#79507,#79508,#79509,#79510,#79511,#79512,#79513,#79514,#79515,#79516,
#79517,#79518,#79519,#79520,#79521,#79522,#79523,#79524,#79525,#79526,#79527,
#79528,#79529,#79530,#79531,#79532,#79533,#79534,#79535,#79536,#79537,#79538,
#79539,#79540,#79541,#79542,#79543,#79544,#79545,#79546,#79547,#79548,#79549,
#79550,#79551,#79552,#79553,#79554,#79555,#79556,#79557,#79558,#79559,#79560,
#79561,#79562,#79563,#79564,#79565,#79566,#79567,#79568,#79569,#79570,#79571,
#79572,#79573,#79574,#79575,#79576,#79577,#79578,#79579,#79580,#79581,#79582,
#79583,#79584,#79585,#79586,#79587,#79588,#79589,#79590,#79591,#79592,#79593,
#79594,#79595,#79596,#79597,#79598,#79599,#79600,#79601,#79602,#79603,#79604,
#79605,#79606,#79607,#79608,#79609,#79610,#79611,#79612,#79613,#79614,#79615,
#79616,#79617,#79618,#79619,#79620,#79621,#79622,#79623,#79624,#79625,#79626,
#79627,#79628,#79629,#79630,#79631,#79632,#79633,#79634,#79635,#79636,#79637,
#79638,#79639,#79640,#79641,#79642,#79643,#79644,#79645,#79646,#79647,#79648,
#79649,#79650,#79651,#79652,#79653,#79654,#79655,#79656,#79657,#79658,#79659,
#79660,#79661,#79662,#79663,#79664,#79665,#79666,#79667,#79668,#79669,#79670,
#79671,#79672,#79673,#79674,#79675,#79676,#79677,#79678,#79679,#79680,#79681,
#79682,#79683,#79684,#79685,#79686,#79687,#79688,#79689,#79690,#79691,#79692,
#79693,#79694,#79695,#79696,#79697,#79698,#79699,#79700,#79701,#79702,#79703,
#79704,#79705,#79706,#79707,#79708,#79709,#79710,#79711,#79712,#79713,#79714,
#79715,#79716,#79717,#79718,#79719,#79720,#79721,#79722,#79723,#79724,#79725,
#79726,#79727,#79728,#79729,#79730,#79731,#79732,#79733,#79734,#79735,#79736,
#79737,#79738,#79739,#79740,#79741,#79742,#79743,#79744,#79745,#79746,#79747,
#79748,#79749,#79750,#79751,#79752,#79753,#79754,#79755,#79756,#79757,#79758,
#79759,#79760,#79761,#79762,#79763,#79764,#79765,#79766,#79767,#79768,#79769,
#79770,#79771,#79772,#79773,#79774,#79775,#79776,#79777,#79778,#79779,#79780,
#79781,#79782,#79783,#79784,#79785,#79786,#79787,#79788,#79789,#79790,#79791,
#79792,#79793,#79794,#79795,#79796,#79797,#79798,#79799,#79800,#79801,#79802,
#79803,#79804,#79805,#79806,#79807,#79808,#79809,#79810,#79811,#79812,#79813,
#79814,#79815,#79816,#79817,#79818,#79819,#79820,#79821,#79822,#79823,#79824,
#79825,#79826,#79827,#79828,#79829,#79830,#79831,#79832,#79833,#79834,#79835,
#79836,#79837,#79838,#79839,#79840,#79841,#79842,#79843,#79844,#79845,#79846,
#79847,#79848,#79849,#79850,#79851,#79852,#79853,#79854,#79855,#79856,#79857,
#79858,#79859,#79860,#79861,#79862,#79863,#79864,#79865,#79866,#79867,#79868,
#79869,#79870,#79871,#79872,#79873,#79874,#79875));
#16494=EDGE_LOOP('',(#79876,#79877,#79878,#79879,#79880));
#16495=EDGE_LOOP('',(#79881,#79882,#79883,#79884));
#16496=EDGE_LOOP('',(#79885,#79886,#79887,#79888));
#16497=EDGE_LOOP('',(#79889,#79890,#79891,#79892));
#16498=EDGE_LOOP('',(#79893,#79894,#79895,#79896));
#16499=EDGE_LOOP('',(#79897,#79898,#79899,#79900));
#16500=EDGE_LOOP('',(#79901,#79902,#79903,#79904));
#16501=EDGE_LOOP('',(#79905,#79906,#79907,#79908));
#16502=EDGE_LOOP('',(#79909,#79910,#79911,#79912));
#16503=EDGE_LOOP('',(#79913,#79914,#79915,#79916));
#16504=EDGE_LOOP('',(#79917,#79918,#79919,#79920));
#16505=EDGE_LOOP('',(#79921,#79922,#79923,#79924));
#16506=EDGE_LOOP('',(#79925,#79926,#79927,#79928));
#16507=EDGE_LOOP('',(#79929,#79930,#79931,#79932));
#16508=EDGE_LOOP('',(#79933,#79934,#79935,#79936));
#16509=EDGE_LOOP('',(#79937,#79938,#79939,#79940));
#16510=EDGE_LOOP('',(#79941,#79942,#79943,#79944));
#16511=EDGE_LOOP('',(#79945,#79946,#79947,#79948));
#16512=EDGE_LOOP('',(#79949,#79950,#79951,#79952));
#16513=EDGE_LOOP('',(#79953,#79954,#79955,#79956));
#16514=EDGE_LOOP('',(#79957,#79958,#79959,#79960));
#16515=EDGE_LOOP('',(#79961,#79962,#79963,#79964));
#16516=EDGE_LOOP('',(#79965,#79966,#79967,#79968));
#16517=EDGE_LOOP('',(#79969,#79970,#79971,#79972));
#16518=EDGE_LOOP('',(#79973,#79974,#79975,#79976));
#16519=EDGE_LOOP('',(#79977,#79978,#79979,#79980));
#16520=EDGE_LOOP('',(#79981,#79982,#79983,#79984));
#16521=EDGE_LOOP('',(#79985,#79986,#79987,#79988));
#16522=EDGE_LOOP('',(#79989,#79990,#79991,#79992));
#16523=EDGE_LOOP('',(#79993,#79994,#79995,#79996));
#16524=EDGE_LOOP('',(#79997,#79998,#79999,#80000));
#16525=EDGE_LOOP('',(#80001,#80002,#80003,#80004));
#16526=EDGE_LOOP('',(#80005,#80006,#80007,#80008));
#16527=EDGE_LOOP('',(#80009,#80010,#80011,#80012));
#16528=EDGE_LOOP('',(#80013,#80014,#80015,#80016));
#16529=EDGE_LOOP('',(#80017,#80018,#80019,#80020));
#16530=EDGE_LOOP('',(#80021,#80022,#80023,#80024));
#16531=EDGE_LOOP('',(#80025,#80026,#80027,#80028));
#16532=EDGE_LOOP('',(#80029,#80030,#80031,#80032));
#16533=EDGE_LOOP('',(#80033,#80034,#80035,#80036));
#16534=EDGE_LOOP('',(#80037,#80038,#80039,#80040));
#16535=EDGE_LOOP('',(#80041,#80042,#80043,#80044));
#16536=EDGE_LOOP('',(#80045,#80046,#80047,#80048));
#16537=EDGE_LOOP('',(#80049,#80050,#80051,#80052));
#16538=EDGE_LOOP('',(#80053,#80054,#80055,#80056));
#16539=EDGE_LOOP('',(#80057,#80058,#80059,#80060));
#16540=EDGE_LOOP('',(#80061,#80062,#80063,#80064));
#16541=EDGE_LOOP('',(#80065,#80066,#80067,#80068));
#16542=EDGE_LOOP('',(#80069,#80070,#80071,#80072));
#16543=EDGE_LOOP('',(#80073,#80074,#80075,#80076));
#16544=EDGE_LOOP('',(#80077,#80078,#80079,#80080));
#16545=EDGE_LOOP('',(#80081,#80082,#80083,#80084));
#16546=EDGE_LOOP('',(#80085,#80086,#80087,#80088));
#16547=EDGE_LOOP('',(#80089,#80090,#80091,#80092));
#16548=EDGE_LOOP('',(#80093,#80094,#80095,#80096));
#16549=EDGE_LOOP('',(#80097,#80098,#80099,#80100));
#16550=EDGE_LOOP('',(#80101,#80102,#80103,#80104));
#16551=EDGE_LOOP('',(#80105,#80106,#80107,#80108));
#16552=EDGE_LOOP('',(#80109,#80110,#80111,#80112));
#16553=EDGE_LOOP('',(#80113,#80114,#80115,#80116));
#16554=EDGE_LOOP('',(#80117,#80118,#80119,#80120));
#16555=EDGE_LOOP('',(#80121,#80122,#80123,#80124));
#16556=EDGE_LOOP('',(#80125,#80126,#80127,#80128));
#16557=EDGE_LOOP('',(#80129,#80130,#80131,#80132));
#16558=EDGE_LOOP('',(#80133,#80134,#80135,#80136));
#16559=EDGE_LOOP('',(#80137,#80138,#80139,#80140));
#16560=EDGE_LOOP('',(#80141,#80142,#80143,#80144));
#16561=EDGE_LOOP('',(#80145,#80146,#80147,#80148));
#16562=EDGE_LOOP('',(#80149,#80150,#80151,#80152));
#16563=EDGE_LOOP('',(#80153,#80154,#80155,#80156));
#16564=EDGE_LOOP('',(#80157,#80158,#80159,#80160));
#16565=EDGE_LOOP('',(#80161,#80162,#80163,#80164));
#16566=EDGE_LOOP('',(#80165,#80166,#80167,#80168));
#16567=EDGE_LOOP('',(#80169,#80170,#80171,#80172));
#16568=EDGE_LOOP('',(#80173,#80174,#80175,#80176));
#16569=EDGE_LOOP('',(#80177,#80178,#80179,#80180));
#16570=EDGE_LOOP('',(#80181,#80182,#80183,#80184,#80185,#80186));
#16571=EDGE_LOOP('',(#80187,#80188,#80189,#80190,#80191));
#16572=EDGE_LOOP('',(#80192,#80193,#80194,#80195,#80196));
#16573=EDGE_LOOP('',(#80197));
#16574=EDGE_LOOP('',(#80198));
#16575=EDGE_LOOP('',(#80199,#80200,#80201));
#16576=EDGE_LOOP('',(#80202,#80203,#80204));
#16577=EDGE_LOOP('',(#80205,#80206,#80207));
#16578=EDGE_LOOP('',(#80208,#80209,#80210));
#16579=EDGE_LOOP('',(#80211,#80212,#80213));
#16580=EDGE_LOOP('',(#80214));
#16581=EDGE_LOOP('',(#80215,#80216,#80217,#80218,#80219,#80220));
#16582=EDGE_LOOP('',(#80221,#80222,#80223,#80224));
#16583=EDGE_LOOP('',(#80225,#80226,#80227,#80228,#80229));
#16584=EDGE_LOOP('',(#80230,#80231,#80232,#80233,#80234));
#16585=EDGE_LOOP('',(#80235,#80236,#80237,#80238,#80239));
#16586=EDGE_LOOP('',(#80240,#80241,#80242,#80243,#80244));
#16587=EDGE_LOOP('',(#80245,#80246,#80247,#80248,#80249));
#16588=EDGE_LOOP('',(#80250,#80251,#80252,#80253,#80254));
#16589=EDGE_LOOP('',(#80255,#80256,#80257));
#16590=EDGE_LOOP('',(#80258,#80259));
#16591=EDGE_LOOP('',(#80260,#80261));
#16592=EDGE_LOOP('',(#80262,#80263));
#16593=EDGE_LOOP('',(#80264,#80265));
#16594=EDGE_LOOP('',(#80266,#80267));
#16595=EDGE_LOOP('',(#80268,#80269,#80270));
#16596=EDGE_LOOP('',(#80271,#80272,#80273,#80274,#80275,#80276,#80277,#80278,
#80279,#80280,#80281,#80282,#80283,#80284,#80285,#80286,#80287,#80288,#80289,
#80290,#80291,#80292,#80293,#80294,#80295,#80296,#80297,#80298,#80299,#80300,
#80301,#80302,#80303,#80304,#80305,#80306,#80307,#80308,#80309,#80310,#80311,
#80312,#80313,#80314,#80315,#80316,#80317,#80318,#80319,#80320,#80321,#80322,
#80323,#80324,#80325,#80326,#80327,#80328,#80329,#80330,#80331,#80332,#80333,
#80334,#80335,#80336,#80337,#80338,#80339,#80340,#80341,#80342,#80343,#80344,
#80345,#80346));
#16597=EDGE_LOOP('',(#80347,#80348,#80349,#80350));
#16598=EDGE_LOOP('',(#80351,#80352,#80353,#80354,#80355,#80356,#80357,#80358,
#80359,#80360,#80361,#80362,#80363,#80364,#80365,#80366,#80367,#80368,#80369,
#80370,#80371,#80372,#80373,#80374,#80375,#80376,#80377,#80378,#80379,#80380,
#80381,#80382,#80383,#80384,#80385,#80386,#80387,#80388,#80389,#80390,#80391,
#80392,#80393,#80394,#80395,#80396,#80397,#80398,#80399,#80400,#80401,#80402,
#80403,#80404,#80405,#80406,#80407,#80408,#80409,#80410,#80411,#80412,#80413,
#80414,#80415,#80416,#80417,#80418,#80419,#80420,#80421,#80422,#80423,#80424,
#80425,#80426));
#16599=EDGE_LOOP('',(#80427,#80428,#80429,#80430));
#16600=EDGE_LOOP('',(#80431,#80432,#80433,#80434));
#16601=EDGE_LOOP('',(#80435,#80436,#80437,#80438));
#16602=EDGE_LOOP('',(#80439,#80440,#80441,#80442,#80443));
#16603=EDGE_LOOP('',(#80444,#80445,#80446,#80447));
#16604=EDGE_LOOP('',(#80448,#80449,#80450,#80451));
#16605=EDGE_LOOP('',(#80452,#80453,#80454,#80455));
#16606=EDGE_LOOP('',(#80456,#80457,#80458,#80459));
#16607=EDGE_LOOP('',(#80460,#80461,#80462,#80463));
#16608=EDGE_LOOP('',(#80464,#80465,#80466,#80467,#80468,#80469));
#16609=EDGE_LOOP('',(#80470,#80471,#80472,#80473));
#16610=EDGE_LOOP('',(#80474,#80475,#80476,#80477));
#16611=EDGE_LOOP('',(#80478,#80479,#80480,#80481));
#16612=EDGE_LOOP('',(#80482,#80483,#80484,#80485,#80486));
#16613=EDGE_LOOP('',(#80487,#80488,#80489,#80490,#80491));
#16614=EDGE_LOOP('',(#80492,#80493,#80494,#80495,#80496,#80497));
#16615=EDGE_LOOP('',(#80498,#80499,#80500,#80501));
#16616=EDGE_LOOP('',(#80502,#80503,#80504,#80505,#80506));
#16617=EDGE_LOOP('',(#80507,#80508,#80509,#80510));
#16618=EDGE_LOOP('',(#80511,#80512,#80513,#80514));
#16619=EDGE_LOOP('',(#80515,#80516,#80517,#80518));
#16620=EDGE_LOOP('',(#80519,#80520,#80521,#80522));
#16621=EDGE_LOOP('',(#80523,#80524,#80525,#80526));
#16622=EDGE_LOOP('',(#80527,#80528,#80529,#80530,#80531));
#16623=EDGE_LOOP('',(#80532,#80533,#80534,#80535));
#16624=EDGE_LOOP('',(#80536,#80537,#80538,#80539));
#16625=EDGE_LOOP('',(#80540,#80541,#80542,#80543));
#16626=EDGE_LOOP('',(#80544,#80545,#80546,#80547));
#16627=EDGE_LOOP('',(#80548,#80549,#80550,#80551));
#16628=EDGE_LOOP('',(#80552,#80553,#80554,#80555,#80556));
#16629=EDGE_LOOP('',(#80557,#80558,#80559,#80560,#80561));
#16630=EDGE_LOOP('',(#80562,#80563,#80564,#80565,#80566,#80567));
#16631=EDGE_LOOP('',(#80568,#80569,#80570,#80571));
#16632=EDGE_LOOP('',(#80572,#80573,#80574,#80575,#80576));
#16633=EDGE_LOOP('',(#80577,#80578,#80579,#80580));
#16634=EDGE_LOOP('',(#80581,#80582,#80583,#80584));
#16635=EDGE_LOOP('',(#80585,#80586,#80587,#80588));
#16636=EDGE_LOOP('',(#80589,#80590,#80591,#80592));
#16637=EDGE_LOOP('',(#80593,#80594,#80595,#80596));
#16638=EDGE_LOOP('',(#80597,#80598,#80599,#80600,#80601));
#16639=EDGE_LOOP('',(#80602,#80603,#80604,#80605));
#16640=EDGE_LOOP('',(#80606,#80607,#80608,#80609));
#16641=EDGE_LOOP('',(#80610,#80611,#80612,#80613));
#16642=EDGE_LOOP('',(#80614,#80615,#80616,#80617));
#16643=EDGE_LOOP('',(#80618,#80619,#80620,#80621));
#16644=EDGE_LOOP('',(#80622,#80623,#80624,#80625,#80626));
#16645=EDGE_LOOP('',(#80627,#80628,#80629,#80630,#80631));
#16646=EDGE_LOOP('',(#80632,#80633,#80634,#80635,#80636,#80637));
#16647=EDGE_LOOP('',(#80638,#80639,#80640,#80641));
#16648=EDGE_LOOP('',(#80642,#80643,#80644,#80645,#80646));
#16649=EDGE_LOOP('',(#80647,#80648,#80649,#80650));
#16650=EDGE_LOOP('',(#80651,#80652,#80653,#80654));
#16651=EDGE_LOOP('',(#80655,#80656,#80657,#80658));
#16652=EDGE_LOOP('',(#80659,#80660,#80661,#80662));
#16653=EDGE_LOOP('',(#80663,#80664,#80665,#80666));
#16654=EDGE_LOOP('',(#80667,#80668,#80669,#80670,#80671));
#16655=EDGE_LOOP('',(#80672,#80673,#80674,#80675));
#16656=EDGE_LOOP('',(#80676,#80677,#80678,#80679));
#16657=EDGE_LOOP('',(#80680,#80681,#80682,#80683));
#16658=EDGE_LOOP('',(#80684,#80685,#80686,#80687));
#16659=EDGE_LOOP('',(#80688,#80689,#80690,#80691));
#16660=EDGE_LOOP('',(#80692,#80693,#80694,#80695,#80696));
#16661=EDGE_LOOP('',(#80697,#80698,#80699,#80700,#80701));
#16662=EDGE_LOOP('',(#80702,#80703,#80704,#80705,#80706,#80707));
#16663=EDGE_LOOP('',(#80708,#80709,#80710,#80711));
#16664=EDGE_LOOP('',(#80712,#80713,#80714,#80715,#80716));
#16665=EDGE_LOOP('',(#80717,#80718,#80719,#80720));
#16666=EDGE_LOOP('',(#80721,#80722,#80723,#80724));
#16667=EDGE_LOOP('',(#80725,#80726,#80727,#80728));
#16668=EDGE_LOOP('',(#80729,#80730,#80731,#80732));
#16669=EDGE_LOOP('',(#80733,#80734,#80735,#80736));
#16670=EDGE_LOOP('',(#80737,#80738,#80739,#80740,#80741));
#16671=EDGE_LOOP('',(#80742,#80743,#80744,#80745));
#16672=EDGE_LOOP('',(#80746,#80747,#80748,#80749));
#16673=EDGE_LOOP('',(#80750,#80751,#80752,#80753));
#16674=EDGE_LOOP('',(#80754,#80755,#80756,#80757));
#16675=EDGE_LOOP('',(#80758,#80759,#80760,#80761));
#16676=EDGE_LOOP('',(#80762,#80763,#80764,#80765,#80766));
#16677=EDGE_LOOP('',(#80767,#80768,#80769,#80770,#80771));
#16678=EDGE_LOOP('',(#80772,#80773,#80774,#80775,#80776,#80777));
#16679=EDGE_LOOP('',(#80778,#80779,#80780,#80781));
#16680=EDGE_LOOP('',(#80782,#80783,#80784,#80785,#80786));
#16681=EDGE_LOOP('',(#80787,#80788,#80789,#80790));
#16682=EDGE_LOOP('',(#80791,#80792,#80793,#80794));
#16683=EDGE_LOOP('',(#80795,#80796,#80797,#80798));
#16684=EDGE_LOOP('',(#80799,#80800,#80801,#80802));
#16685=EDGE_LOOP('',(#80803,#80804,#80805,#80806));
#16686=EDGE_LOOP('',(#80807,#80808,#80809,#80810,#80811));
#16687=EDGE_LOOP('',(#80812,#80813,#80814,#80815));
#16688=EDGE_LOOP('',(#80816,#80817,#80818,#80819));
#16689=EDGE_LOOP('',(#80820,#80821,#80822,#80823));
#16690=EDGE_LOOP('',(#80824,#80825,#80826,#80827));
#16691=EDGE_LOOP('',(#80828,#80829,#80830,#80831));
#16692=EDGE_LOOP('',(#80832,#80833,#80834,#80835,#80836));
#16693=EDGE_LOOP('',(#80837,#80838,#80839,#80840,#80841));
#16694=EDGE_LOOP('',(#80842,#80843,#80844,#80845,#80846,#80847));
#16695=EDGE_LOOP('',(#80848,#80849,#80850,#80851));
#16696=EDGE_LOOP('',(#80852,#80853,#80854,#80855,#80856));
#16697=EDGE_LOOP('',(#80857,#80858,#80859,#80860));
#16698=EDGE_LOOP('',(#80861,#80862,#80863,#80864));
#16699=EDGE_LOOP('',(#80865,#80866,#80867,#80868));
#16700=EDGE_LOOP('',(#80869,#80870,#80871,#80872));
#16701=EDGE_LOOP('',(#80873,#80874,#80875,#80876));
#16702=EDGE_LOOP('',(#80877,#80878,#80879,#80880,#80881));
#16703=EDGE_LOOP('',(#80882,#80883,#80884,#80885));
#16704=EDGE_LOOP('',(#80886,#80887,#80888,#80889));
#16705=EDGE_LOOP('',(#80890,#80891,#80892,#80893));
#16706=EDGE_LOOP('',(#80894,#80895,#80896,#80897));
#16707=EDGE_LOOP('',(#80898,#80899,#80900,#80901));
#16708=EDGE_LOOP('',(#80902,#80903,#80904,#80905,#80906));
#16709=EDGE_LOOP('',(#80907,#80908,#80909,#80910,#80911));
#16710=EDGE_LOOP('',(#80912,#80913,#80914,#80915,#80916,#80917));
#16711=EDGE_LOOP('',(#80918,#80919,#80920,#80921));
#16712=EDGE_LOOP('',(#80922,#80923,#80924,#80925,#80926));
#16713=EDGE_LOOP('',(#80927,#80928,#80929,#80930));
#16714=EDGE_LOOP('',(#80931,#80932,#80933,#80934));
#16715=EDGE_LOOP('',(#80935,#80936,#80937,#80938));
#16716=EDGE_LOOP('',(#80939,#80940,#80941,#80942));
#16717=EDGE_LOOP('',(#80943,#80944,#80945,#80946));
#16718=EDGE_LOOP('',(#80947,#80948,#80949,#80950,#80951));
#16719=EDGE_LOOP('',(#80952,#80953,#80954,#80955));
#16720=EDGE_LOOP('',(#80956,#80957,#80958,#80959));
#16721=EDGE_LOOP('',(#80960,#80961,#80962,#80963));
#16722=EDGE_LOOP('',(#80964,#80965,#80966,#80967));
#16723=EDGE_LOOP('',(#80968,#80969,#80970,#80971));
#16724=EDGE_LOOP('',(#80972,#80973,#80974,#80975,#80976));
#16725=EDGE_LOOP('',(#80977,#80978,#80979,#80980,#80981));
#16726=EDGE_LOOP('',(#80982,#80983,#80984,#80985,#80986,#80987));
#16727=EDGE_LOOP('',(#80988,#80989,#80990,#80991));
#16728=EDGE_LOOP('',(#80992,#80993,#80994,#80995,#80996));
#16729=EDGE_LOOP('',(#80997,#80998,#80999,#81000));
#16730=EDGE_LOOP('',(#81001,#81002,#81003,#81004));
#16731=EDGE_LOOP('',(#81005,#81006,#81007,#81008));
#16732=EDGE_LOOP('',(#81009,#81010,#81011,#81012));
#16733=EDGE_LOOP('',(#81013,#81014,#81015,#81016));
#16734=EDGE_LOOP('',(#81017,#81018,#81019,#81020,#81021));
#16735=EDGE_LOOP('',(#81022,#81023,#81024,#81025));
#16736=EDGE_LOOP('',(#81026,#81027,#81028,#81029));
#16737=EDGE_LOOP('',(#81030,#81031,#81032,#81033));
#16738=EDGE_LOOP('',(#81034,#81035,#81036,#81037));
#16739=EDGE_LOOP('',(#81038,#81039,#81040,#81041));
#16740=EDGE_LOOP('',(#81042,#81043,#81044,#81045,#81046));
#16741=EDGE_LOOP('',(#81047,#81048,#81049,#81050,#81051));
#16742=EDGE_LOOP('',(#81052,#81053,#81054,#81055,#81056,#81057));
#16743=EDGE_LOOP('',(#81058,#81059,#81060,#81061));
#16744=EDGE_LOOP('',(#81062,#81063,#81064,#81065,#81066));
#16745=EDGE_LOOP('',(#81067,#81068,#81069,#81070));
#16746=EDGE_LOOP('',(#81071,#81072,#81073,#81074));
#16747=EDGE_LOOP('',(#81075,#81076,#81077,#81078));
#16748=EDGE_LOOP('',(#81079,#81080,#81081,#81082));
#16749=EDGE_LOOP('',(#81083,#81084,#81085,#81086));
#16750=EDGE_LOOP('',(#81087,#81088,#81089,#81090,#81091));
#16751=EDGE_LOOP('',(#81092,#81093,#81094,#81095));
#16752=EDGE_LOOP('',(#81096,#81097,#81098,#81099));
#16753=EDGE_LOOP('',(#81100,#81101,#81102,#81103));
#16754=EDGE_LOOP('',(#81104,#81105,#81106,#81107));
#16755=EDGE_LOOP('',(#81108,#81109,#81110,#81111));
#16756=EDGE_LOOP('',(#81112,#81113,#81114,#81115,#81116));
#16757=EDGE_LOOP('',(#81117,#81118,#81119,#81120,#81121));
#16758=EDGE_LOOP('',(#81122,#81123,#81124,#81125,#81126,#81127));
#16759=EDGE_LOOP('',(#81128,#81129,#81130,#81131));
#16760=EDGE_LOOP('',(#81132,#81133,#81134,#81135,#81136));
#16761=EDGE_LOOP('',(#81137,#81138,#81139,#81140));
#16762=EDGE_LOOP('',(#81141,#81142,#81143,#81144));
#16763=EDGE_LOOP('',(#81145,#81146,#81147,#81148));
#16764=EDGE_LOOP('',(#81149,#81150,#81151,#81152));
#16765=EDGE_LOOP('',(#81153,#81154,#81155,#81156));
#16766=EDGE_LOOP('',(#81157,#81158,#81159,#81160,#81161));
#16767=EDGE_LOOP('',(#81162,#81163,#81164,#81165));
#16768=EDGE_LOOP('',(#81166,#81167,#81168,#81169));
#16769=EDGE_LOOP('',(#81170,#81171,#81172,#81173));
#16770=EDGE_LOOP('',(#81174,#81175,#81176,#81177));
#16771=EDGE_LOOP('',(#81178,#81179,#81180,#81181));
#16772=EDGE_LOOP('',(#81182,#81183,#81184,#81185,#81186));
#16773=EDGE_LOOP('',(#81187,#81188,#81189,#81190,#81191));
#16774=EDGE_LOOP('',(#81192,#81193,#81194,#81195,#81196,#81197));
#16775=EDGE_LOOP('',(#81198,#81199,#81200,#81201));
#16776=EDGE_LOOP('',(#81202,#81203,#81204,#81205,#81206));
#16777=EDGE_LOOP('',(#81207,#81208,#81209,#81210));
#16778=EDGE_LOOP('',(#81211,#81212,#81213,#81214));
#16779=EDGE_LOOP('',(#81215,#81216,#81217,#81218));
#16780=EDGE_LOOP('',(#81219,#81220,#81221,#81222));
#16781=EDGE_LOOP('',(#81223,#81224,#81225,#81226));
#16782=EDGE_LOOP('',(#81227,#81228,#81229,#81230,#81231));
#16783=EDGE_LOOP('',(#81232,#81233,#81234,#81235));
#16784=EDGE_LOOP('',(#81236,#81237,#81238,#81239));
#16785=EDGE_LOOP('',(#81240,#81241,#81242,#81243));
#16786=EDGE_LOOP('',(#81244,#81245,#81246,#81247));
#16787=EDGE_LOOP('',(#81248,#81249,#81250,#81251));
#16788=EDGE_LOOP('',(#81252,#81253,#81254,#81255,#81256));
#16789=EDGE_LOOP('',(#81257,#81258,#81259,#81260,#81261));
#16790=EDGE_LOOP('',(#81262,#81263,#81264,#81265,#81266,#81267));
#16791=EDGE_LOOP('',(#81268,#81269,#81270,#81271));
#16792=EDGE_LOOP('',(#81272,#81273,#81274,#81275,#81276));
#16793=EDGE_LOOP('',(#81277,#81278,#81279,#81280));
#16794=EDGE_LOOP('',(#81281,#81282,#81283,#81284));
#16795=EDGE_LOOP('',(#81285,#81286,#81287,#81288));
#16796=EDGE_LOOP('',(#81289,#81290,#81291,#81292));
#16797=EDGE_LOOP('',(#81293,#81294,#81295,#81296));
#16798=EDGE_LOOP('',(#81297,#81298,#81299,#81300,#81301));
#16799=EDGE_LOOP('',(#81302,#81303,#81304,#81305));
#16800=EDGE_LOOP('',(#81306,#81307,#81308,#81309));
#16801=EDGE_LOOP('',(#81310,#81311,#81312,#81313));
#16802=EDGE_LOOP('',(#81314,#81315,#81316,#81317));
#16803=EDGE_LOOP('',(#81318,#81319,#81320,#81321));
#16804=EDGE_LOOP('',(#81322,#81323,#81324,#81325,#81326));
#16805=EDGE_LOOP('',(#81327,#81328,#81329,#81330,#81331));
#16806=EDGE_LOOP('',(#81332,#81333,#81334,#81335,#81336,#81337));
#16807=EDGE_LOOP('',(#81338,#81339,#81340,#81341));
#16808=EDGE_LOOP('',(#81342,#81343,#81344,#81345,#81346));
#16809=EDGE_LOOP('',(#81347,#81348,#81349,#81350));
#16810=EDGE_LOOP('',(#81351,#81352,#81353,#81354));
#16811=EDGE_LOOP('',(#81355,#81356,#81357,#81358));
#16812=EDGE_LOOP('',(#81359,#81360,#81361,#81362));
#16813=EDGE_LOOP('',(#81363,#81364,#81365,#81366));
#16814=EDGE_LOOP('',(#81367,#81368,#81369,#81370,#81371));
#16815=EDGE_LOOP('',(#81372,#81373,#81374,#81375));
#16816=EDGE_LOOP('',(#81376,#81377,#81378,#81379));
#16817=EDGE_LOOP('',(#81380,#81381,#81382,#81383));
#16818=EDGE_LOOP('',(#81384,#81385,#81386,#81387));
#16819=EDGE_LOOP('',(#81388,#81389,#81390,#81391));
#16820=EDGE_LOOP('',(#81392,#81393,#81394,#81395,#81396));
#16821=EDGE_LOOP('',(#81397,#81398,#81399,#81400,#81401));
#16822=EDGE_LOOP('',(#81402,#81403,#81404,#81405,#81406,#81407));
#16823=EDGE_LOOP('',(#81408,#81409,#81410,#81411));
#16824=EDGE_LOOP('',(#81412,#81413,#81414,#81415,#81416));
#16825=EDGE_LOOP('',(#81417,#81418,#81419,#81420));
#16826=EDGE_LOOP('',(#81421,#81422,#81423,#81424));
#16827=EDGE_LOOP('',(#81425,#81426,#81427,#81428));
#16828=EDGE_LOOP('',(#81429,#81430,#81431,#81432));
#16829=EDGE_LOOP('',(#81433,#81434,#81435,#81436));
#16830=EDGE_LOOP('',(#81437,#81438,#81439,#81440,#81441));
#16831=EDGE_LOOP('',(#81442,#81443,#81444,#81445));
#16832=EDGE_LOOP('',(#81446,#81447,#81448,#81449));
#16833=EDGE_LOOP('',(#81450,#81451,#81452,#81453));
#16834=EDGE_LOOP('',(#81454,#81455,#81456,#81457));
#16835=EDGE_LOOP('',(#81458,#81459,#81460,#81461));
#16836=EDGE_LOOP('',(#81462,#81463,#81464,#81465,#81466));
#16837=EDGE_LOOP('',(#81467,#81468,#81469,#81470,#81471));
#16838=EDGE_LOOP('',(#81472,#81473,#81474,#81475,#81476,#81477));
#16839=EDGE_LOOP('',(#81478,#81479,#81480,#81481));
#16840=EDGE_LOOP('',(#81482,#81483,#81484,#81485,#81486));
#16841=EDGE_LOOP('',(#81487,#81488,#81489,#81490));
#16842=EDGE_LOOP('',(#81491,#81492,#81493,#81494));
#16843=EDGE_LOOP('',(#81495,#81496,#81497,#81498));
#16844=EDGE_LOOP('',(#81499,#81500,#81501,#81502));
#16845=EDGE_LOOP('',(#81503,#81504,#81505,#81506));
#16846=EDGE_LOOP('',(#81507,#81508,#81509,#81510,#81511));
#16847=EDGE_LOOP('',(#81512,#81513,#81514,#81515));
#16848=EDGE_LOOP('',(#81516,#81517,#81518,#81519));
#16849=EDGE_LOOP('',(#81520,#81521,#81522,#81523));
#16850=EDGE_LOOP('',(#81524,#81525,#81526,#81527));
#16851=EDGE_LOOP('',(#81528,#81529,#81530,#81531));
#16852=EDGE_LOOP('',(#81532,#81533,#81534,#81535,#81536));
#16853=EDGE_LOOP('',(#81537,#81538,#81539,#81540,#81541));
#16854=EDGE_LOOP('',(#81542,#81543,#81544,#81545,#81546,#81547));
#16855=EDGE_LOOP('',(#81548,#81549,#81550,#81551));
#16856=EDGE_LOOP('',(#81552,#81553,#81554,#81555,#81556));
#16857=EDGE_LOOP('',(#81557,#81558,#81559,#81560));
#16858=EDGE_LOOP('',(#81561,#81562,#81563,#81564));
#16859=EDGE_LOOP('',(#81565,#81566,#81567,#81568));
#16860=EDGE_LOOP('',(#81569,#81570,#81571,#81572));
#16861=EDGE_LOOP('',(#81573,#81574,#81575,#81576));
#16862=EDGE_LOOP('',(#81577,#81578,#81579,#81580,#81581));
#16863=EDGE_LOOP('',(#81582,#81583,#81584,#81585));
#16864=EDGE_LOOP('',(#81586,#81587,#81588,#81589));
#16865=EDGE_LOOP('',(#81590,#81591,#81592,#81593));
#16866=EDGE_LOOP('',(#81594,#81595,#81596,#81597));
#16867=EDGE_LOOP('',(#81598,#81599,#81600,#81601));
#16868=EDGE_LOOP('',(#81602,#81603,#81604,#81605,#81606));
#16869=EDGE_LOOP('',(#81607,#81608,#81609,#81610,#81611));
#16870=EDGE_LOOP('',(#81612,#81613,#81614,#81615,#81616,#81617));
#16871=EDGE_LOOP('',(#81618,#81619,#81620,#81621));
#16872=EDGE_LOOP('',(#81622,#81623,#81624,#81625,#81626));
#16873=EDGE_LOOP('',(#81627,#81628,#81629,#81630));
#16874=EDGE_LOOP('',(#81631,#81632,#81633,#81634));
#16875=EDGE_LOOP('',(#81635,#81636,#81637,#81638));
#16876=EDGE_LOOP('',(#81639,#81640,#81641,#81642));
#16877=EDGE_LOOP('',(#81643,#81644,#81645,#81646));
#16878=EDGE_LOOP('',(#81647,#81648,#81649,#81650,#81651));
#16879=EDGE_LOOP('',(#81652,#81653,#81654,#81655));
#16880=EDGE_LOOP('',(#81656,#81657,#81658,#81659));
#16881=EDGE_LOOP('',(#81660,#81661,#81662,#81663));
#16882=EDGE_LOOP('',(#81664,#81665,#81666,#81667));
#16883=EDGE_LOOP('',(#81668,#81669,#81670,#81671));
#16884=EDGE_LOOP('',(#81672,#81673,#81674,#81675,#81676));
#16885=EDGE_LOOP('',(#81677,#81678,#81679,#81680,#81681));
#16886=EDGE_LOOP('',(#81682,#81683,#81684,#81685,#81686,#81687));
#16887=EDGE_LOOP('',(#81688,#81689,#81690,#81691));
#16888=EDGE_LOOP('',(#81692,#81693,#81694,#81695,#81696));
#16889=EDGE_LOOP('',(#81697,#81698,#81699,#81700));
#16890=EDGE_LOOP('',(#81701,#81702,#81703,#81704));
#16891=EDGE_LOOP('',(#81705,#81706,#81707,#81708));
#16892=EDGE_LOOP('',(#81709,#81710,#81711,#81712));
#16893=EDGE_LOOP('',(#81713,#81714,#81715,#81716));
#16894=EDGE_LOOP('',(#81717,#81718,#81719,#81720,#81721));
#16895=EDGE_LOOP('',(#81722,#81723,#81724,#81725));
#16896=EDGE_LOOP('',(#81726,#81727,#81728,#81729));
#16897=EDGE_LOOP('',(#81730,#81731,#81732,#81733));
#16898=EDGE_LOOP('',(#81734,#81735,#81736,#81737));
#16899=EDGE_LOOP('',(#81738,#81739,#81740,#81741));
#16900=EDGE_LOOP('',(#81742,#81743,#81744,#81745,#81746));
#16901=EDGE_LOOP('',(#81747,#81748,#81749,#81750,#81751));
#16902=EDGE_LOOP('',(#81752,#81753,#81754,#81755,#81756,#81757));
#16903=EDGE_LOOP('',(#81758,#81759,#81760,#81761));
#16904=EDGE_LOOP('',(#81762,#81763,#81764,#81765,#81766));
#16905=EDGE_LOOP('',(#81767,#81768,#81769,#81770));
#16906=EDGE_LOOP('',(#81771,#81772,#81773,#81774));
#16907=EDGE_LOOP('',(#81775,#81776,#81777,#81778));
#16908=EDGE_LOOP('',(#81779,#81780,#81781,#81782));
#16909=EDGE_LOOP('',(#81783,#81784,#81785,#81786));
#16910=EDGE_LOOP('',(#81787,#81788,#81789,#81790,#81791));
#16911=EDGE_LOOP('',(#81792,#81793,#81794,#81795));
#16912=EDGE_LOOP('',(#81796,#81797,#81798,#81799));
#16913=EDGE_LOOP('',(#81800,#81801,#81802,#81803));
#16914=EDGE_LOOP('',(#81804,#81805,#81806,#81807));
#16915=EDGE_LOOP('',(#81808,#81809,#81810,#81811));
#16916=EDGE_LOOP('',(#81812,#81813,#81814,#81815,#81816));
#16917=EDGE_LOOP('',(#81817,#81818,#81819,#81820,#81821));
#16918=EDGE_LOOP('',(#81822,#81823,#81824,#81825,#81826,#81827));
#16919=EDGE_LOOP('',(#81828,#81829,#81830,#81831));
#16920=EDGE_LOOP('',(#81832,#81833,#81834,#81835,#81836));
#16921=EDGE_LOOP('',(#81837,#81838,#81839,#81840));
#16922=EDGE_LOOP('',(#81841,#81842,#81843,#81844));
#16923=EDGE_LOOP('',(#81845,#81846,#81847,#81848));
#16924=EDGE_LOOP('',(#81849,#81850,#81851,#81852));
#16925=EDGE_LOOP('',(#81853,#81854,#81855,#81856));
#16926=EDGE_LOOP('',(#81857,#81858,#81859,#81860,#81861));
#16927=EDGE_LOOP('',(#81862,#81863,#81864,#81865));
#16928=EDGE_LOOP('',(#81866,#81867,#81868,#81869));
#16929=EDGE_LOOP('',(#81870,#81871,#81872,#81873));
#16930=EDGE_LOOP('',(#81874,#81875,#81876,#81877));
#16931=EDGE_LOOP('',(#81878,#81879,#81880,#81881));
#16932=EDGE_LOOP('',(#81882,#81883,#81884,#81885,#81886));
#16933=EDGE_LOOP('',(#81887,#81888,#81889,#81890,#81891));
#16934=EDGE_LOOP('',(#81892,#81893,#81894,#81895,#81896,#81897));
#16935=EDGE_LOOP('',(#81898,#81899,#81900,#81901));
#16936=EDGE_LOOP('',(#81902,#81903,#81904,#81905,#81906));
#16937=EDGE_LOOP('',(#81907,#81908,#81909,#81910));
#16938=EDGE_LOOP('',(#81911,#81912,#81913,#81914));
#16939=EDGE_LOOP('',(#81915,#81916,#81917,#81918));
#16940=EDGE_LOOP('',(#81919,#81920,#81921,#81922));
#16941=EDGE_LOOP('',(#81923,#81924,#81925,#81926));
#16942=EDGE_LOOP('',(#81927,#81928,#81929,#81930,#81931));
#16943=EDGE_LOOP('',(#81932,#81933,#81934,#81935));
#16944=EDGE_LOOP('',(#81936,#81937,#81938,#81939));
#16945=EDGE_LOOP('',(#81940,#81941,#81942,#81943));
#16946=EDGE_LOOP('',(#81944,#81945,#81946,#81947));
#16947=EDGE_LOOP('',(#81948,#81949,#81950,#81951));
#16948=EDGE_LOOP('',(#81952,#81953,#81954,#81955,#81956));
#16949=EDGE_LOOP('',(#81957,#81958,#81959,#81960,#81961));
#16950=EDGE_LOOP('',(#81962,#81963,#81964,#81965,#81966,#81967));
#16951=EDGE_LOOP('',(#81968,#81969,#81970,#81971));
#16952=EDGE_LOOP('',(#81972,#81973,#81974,#81975,#81976));
#16953=EDGE_LOOP('',(#81977,#81978,#81979,#81980));
#16954=EDGE_LOOP('',(#81981,#81982,#81983,#81984));
#16955=EDGE_LOOP('',(#81985,#81986,#81987,#81988));
#16956=EDGE_LOOP('',(#81989,#81990,#81991,#81992));
#16957=EDGE_LOOP('',(#81993,#81994,#81995,#81996));
#16958=EDGE_LOOP('',(#81997,#81998,#81999,#82000,#82001));
#16959=EDGE_LOOP('',(#82002,#82003,#82004,#82005));
#16960=EDGE_LOOP('',(#82006,#82007,#82008,#82009));
#16961=EDGE_LOOP('',(#82010,#82011,#82012,#82013));
#16962=EDGE_LOOP('',(#82014,#82015,#82016,#82017));
#16963=EDGE_LOOP('',(#82018,#82019,#82020,#82021));
#16964=EDGE_LOOP('',(#82022,#82023,#82024,#82025,#82026));
#16965=EDGE_LOOP('',(#82027,#82028,#82029,#82030,#82031));
#16966=EDGE_LOOP('',(#82032,#82033,#82034,#82035,#82036,#82037));
#16967=EDGE_LOOP('',(#82038,#82039,#82040,#82041));
#16968=EDGE_LOOP('',(#82042,#82043,#82044,#82045,#82046));
#16969=EDGE_LOOP('',(#82047,#82048,#82049,#82050));
#16970=EDGE_LOOP('',(#82051,#82052,#82053,#82054));
#16971=EDGE_LOOP('',(#82055,#82056,#82057,#82058));
#16972=EDGE_LOOP('',(#82059,#82060,#82061,#82062));
#16973=EDGE_LOOP('',(#82063,#82064,#82065,#82066));
#16974=EDGE_LOOP('',(#82067,#82068,#82069,#82070,#82071));
#16975=EDGE_LOOP('',(#82072,#82073,#82074,#82075));
#16976=EDGE_LOOP('',(#82076,#82077,#82078,#82079));
#16977=EDGE_LOOP('',(#82080,#82081,#82082,#82083));
#16978=EDGE_LOOP('',(#82084,#82085,#82086,#82087));
#16979=EDGE_LOOP('',(#82088,#82089,#82090,#82091));
#16980=EDGE_LOOP('',(#82092,#82093,#82094,#82095,#82096));
#16981=EDGE_LOOP('',(#82097,#82098,#82099,#82100,#82101));
#16982=EDGE_LOOP('',(#82102,#82103,#82104,#82105,#82106,#82107));
#16983=EDGE_LOOP('',(#82108,#82109,#82110,#82111));
#16984=EDGE_LOOP('',(#82112,#82113,#82114,#82115,#82116));
#16985=EDGE_LOOP('',(#82117,#82118,#82119,#82120));
#16986=EDGE_LOOP('',(#82121,#82122,#82123,#82124));
#16987=EDGE_LOOP('',(#82125,#82126,#82127,#82128));
#16988=EDGE_LOOP('',(#82129,#82130,#82131,#82132));
#16989=EDGE_LOOP('',(#82133,#82134,#82135,#82136));
#16990=EDGE_LOOP('',(#82137,#82138,#82139,#82140,#82141));
#16991=EDGE_LOOP('',(#82142,#82143,#82144,#82145));
#16992=EDGE_LOOP('',(#82146,#82147,#82148,#82149));
#16993=EDGE_LOOP('',(#82150,#82151,#82152,#82153));
#16994=EDGE_LOOP('',(#82154,#82155,#82156,#82157));
#16995=EDGE_LOOP('',(#82158,#82159,#82160,#82161));
#16996=EDGE_LOOP('',(#82162,#82163,#82164,#82165,#82166));
#16997=EDGE_LOOP('',(#82167,#82168,#82169,#82170,#82171));
#16998=EDGE_LOOP('',(#82172,#82173,#82174,#82175,#82176,#82177));
#16999=EDGE_LOOP('',(#82178,#82179,#82180,#82181));
#17000=EDGE_LOOP('',(#82182,#82183,#82184,#82185,#82186));
#17001=EDGE_LOOP('',(#82187,#82188,#82189,#82190));
#17002=EDGE_LOOP('',(#82191,#82192,#82193,#82194));
#17003=EDGE_LOOP('',(#82195,#82196,#82197,#82198));
#17004=EDGE_LOOP('',(#82199,#82200,#82201,#82202));
#17005=EDGE_LOOP('',(#82203,#82204,#82205,#82206));
#17006=EDGE_LOOP('',(#82207,#82208,#82209,#82210,#82211));
#17007=EDGE_LOOP('',(#82212,#82213,#82214,#82215));
#17008=EDGE_LOOP('',(#82216,#82217,#82218,#82219));
#17009=EDGE_LOOP('',(#82220,#82221,#82222,#82223));
#17010=EDGE_LOOP('',(#82224,#82225,#82226,#82227));
#17011=EDGE_LOOP('',(#82228,#82229,#82230,#82231));
#17012=EDGE_LOOP('',(#82232,#82233,#82234,#82235,#82236));
#17013=EDGE_LOOP('',(#82237,#82238,#82239,#82240,#82241));
#17014=EDGE_LOOP('',(#82242,#82243,#82244,#82245,#82246,#82247));
#17015=EDGE_LOOP('',(#82248,#82249,#82250,#82251));
#17016=EDGE_LOOP('',(#82252,#82253,#82254,#82255,#82256));
#17017=EDGE_LOOP('',(#82257,#82258,#82259,#82260));
#17018=EDGE_LOOP('',(#82261,#82262,#82263,#82264));
#17019=EDGE_LOOP('',(#82265,#82266,#82267,#82268));
#17020=EDGE_LOOP('',(#82269,#82270,#82271,#82272));
#17021=EDGE_LOOP('',(#82273,#82274,#82275,#82276));
#17022=EDGE_LOOP('',(#82277,#82278,#82279,#82280,#82281));
#17023=EDGE_LOOP('',(#82282,#82283,#82284,#82285));
#17024=EDGE_LOOP('',(#82286,#82287,#82288,#82289));
#17025=EDGE_LOOP('',(#82290,#82291,#82292,#82293));
#17026=EDGE_LOOP('',(#82294,#82295,#82296,#82297));
#17027=EDGE_LOOP('',(#82298,#82299,#82300,#82301));
#17028=EDGE_LOOP('',(#82302,#82303,#82304,#82305,#82306));
#17029=EDGE_LOOP('',(#82307,#82308,#82309,#82310,#82311));
#17030=EDGE_LOOP('',(#82312,#82313,#82314,#82315,#82316,#82317));
#17031=EDGE_LOOP('',(#82318,#82319,#82320,#82321));
#17032=EDGE_LOOP('',(#82322,#82323,#82324,#82325,#82326));
#17033=EDGE_LOOP('',(#82327,#82328,#82329,#82330));
#17034=EDGE_LOOP('',(#82331,#82332,#82333,#82334));
#17035=EDGE_LOOP('',(#82335,#82336,#82337,#82338));
#17036=EDGE_LOOP('',(#82339,#82340,#82341,#82342));
#17037=EDGE_LOOP('',(#82343,#82344,#82345,#82346));
#17038=EDGE_LOOP('',(#82347,#82348,#82349,#82350,#82351));
#17039=EDGE_LOOP('',(#82352,#82353,#82354,#82355));
#17040=EDGE_LOOP('',(#82356,#82357,#82358,#82359));
#17041=EDGE_LOOP('',(#82360,#82361,#82362,#82363));
#17042=EDGE_LOOP('',(#82364,#82365,#82366,#82367));
#17043=EDGE_LOOP('',(#82368,#82369,#82370,#82371));
#17044=EDGE_LOOP('',(#82372,#82373,#82374,#82375,#82376));
#17045=EDGE_LOOP('',(#82377,#82378,#82379,#82380,#82381));
#17046=EDGE_LOOP('',(#82382,#82383,#82384,#82385,#82386,#82387));
#17047=EDGE_LOOP('',(#82388,#82389,#82390,#82391));
#17048=EDGE_LOOP('',(#82392,#82393,#82394,#82395,#82396));
#17049=EDGE_LOOP('',(#82397,#82398,#82399,#82400));
#17050=EDGE_LOOP('',(#82401,#82402,#82403,#82404));
#17051=EDGE_LOOP('',(#82405,#82406,#82407,#82408));
#17052=EDGE_LOOP('',(#82409,#82410,#82411,#82412));
#17053=EDGE_LOOP('',(#82413,#82414,#82415,#82416));
#17054=EDGE_LOOP('',(#82417,#82418,#82419,#82420,#82421));
#17055=EDGE_LOOP('',(#82422,#82423,#82424,#82425));
#17056=EDGE_LOOP('',(#82426,#82427,#82428,#82429));
#17057=EDGE_LOOP('',(#82430,#82431,#82432,#82433));
#17058=EDGE_LOOP('',(#82434,#82435,#82436,#82437));
#17059=EDGE_LOOP('',(#82438,#82439,#82440,#82441));
#17060=EDGE_LOOP('',(#82442,#82443,#82444,#82445,#82446));
#17061=EDGE_LOOP('',(#82447,#82448,#82449,#82450,#82451));
#17062=EDGE_LOOP('',(#82452,#82453,#82454,#82455,#82456,#82457));
#17063=EDGE_LOOP('',(#82458,#82459,#82460,#82461));
#17064=EDGE_LOOP('',(#82462,#82463,#82464,#82465,#82466));
#17065=EDGE_LOOP('',(#82467,#82468,#82469,#82470));
#17066=EDGE_LOOP('',(#82471,#82472,#82473,#82474));
#17067=EDGE_LOOP('',(#82475,#82476,#82477,#82478));
#17068=EDGE_LOOP('',(#82479,#82480,#82481,#82482));
#17069=EDGE_LOOP('',(#82483,#82484,#82485,#82486));
#17070=EDGE_LOOP('',(#82487,#82488,#82489,#82490,#82491));
#17071=EDGE_LOOP('',(#82492,#82493,#82494,#82495));
#17072=EDGE_LOOP('',(#82496,#82497,#82498,#82499));
#17073=EDGE_LOOP('',(#82500,#82501,#82502,#82503));
#17074=EDGE_LOOP('',(#82504,#82505,#82506,#82507));
#17075=EDGE_LOOP('',(#82508,#82509,#82510,#82511));
#17076=EDGE_LOOP('',(#82512,#82513,#82514,#82515,#82516));
#17077=EDGE_LOOP('',(#82517,#82518,#82519,#82520,#82521));
#17078=EDGE_LOOP('',(#82522,#82523,#82524,#82525,#82526,#82527));
#17079=EDGE_LOOP('',(#82528,#82529,#82530,#82531));
#17080=EDGE_LOOP('',(#82532,#82533,#82534,#82535,#82536));
#17081=EDGE_LOOP('',(#82537,#82538,#82539,#82540));
#17082=EDGE_LOOP('',(#82541,#82542,#82543,#82544));
#17083=EDGE_LOOP('',(#82545,#82546,#82547,#82548));
#17084=EDGE_LOOP('',(#82549,#82550,#82551,#82552));
#17085=EDGE_LOOP('',(#82553,#82554,#82555,#82556));
#17086=EDGE_LOOP('',(#82557,#82558,#82559,#82560,#82561));
#17087=EDGE_LOOP('',(#82562,#82563,#82564,#82565));
#17088=EDGE_LOOP('',(#82566,#82567,#82568,#82569));
#17089=EDGE_LOOP('',(#82570,#82571,#82572,#82573));
#17090=EDGE_LOOP('',(#82574,#82575,#82576,#82577));
#17091=EDGE_LOOP('',(#82578,#82579,#82580,#82581));
#17092=EDGE_LOOP('',(#82582,#82583,#82584,#82585,#82586));
#17093=EDGE_LOOP('',(#82587,#82588,#82589,#82590,#82591));
#17094=EDGE_LOOP('',(#82592,#82593,#82594,#82595,#82596,#82597));
#17095=EDGE_LOOP('',(#82598,#82599,#82600,#82601));
#17096=EDGE_LOOP('',(#82602,#82603,#82604,#82605,#82606));
#17097=EDGE_LOOP('',(#82607,#82608,#82609,#82610));
#17098=EDGE_LOOP('',(#82611,#82612,#82613,#82614));
#17099=EDGE_LOOP('',(#82615,#82616,#82617,#82618));
#17100=EDGE_LOOP('',(#82619,#82620,#82621,#82622));
#17101=EDGE_LOOP('',(#82623,#82624,#82625,#82626));
#17102=EDGE_LOOP('',(#82627,#82628,#82629,#82630,#82631));
#17103=EDGE_LOOP('',(#82632,#82633,#82634,#82635));
#17104=EDGE_LOOP('',(#82636,#82637,#82638,#82639));
#17105=EDGE_LOOP('',(#82640,#82641,#82642,#82643));
#17106=EDGE_LOOP('',(#82644,#82645,#82646,#82647));
#17107=EDGE_LOOP('',(#82648,#82649,#82650,#82651));
#17108=EDGE_LOOP('',(#82652,#82653,#82654,#82655,#82656));
#17109=EDGE_LOOP('',(#82657,#82658,#82659,#82660,#82661));
#17110=EDGE_LOOP('',(#82662,#82663,#82664,#82665,#82666,#82667));
#17111=EDGE_LOOP('',(#82668,#82669,#82670,#82671));
#17112=EDGE_LOOP('',(#82672,#82673,#82674,#82675,#82676));
#17113=EDGE_LOOP('',(#82677,#82678,#82679,#82680));
#17114=EDGE_LOOP('',(#82681,#82682,#82683,#82684));
#17115=EDGE_LOOP('',(#82685,#82686,#82687,#82688));
#17116=EDGE_LOOP('',(#82689,#82690,#82691,#82692));
#17117=EDGE_LOOP('',(#82693,#82694,#82695,#82696));
#17118=EDGE_LOOP('',(#82697,#82698,#82699,#82700,#82701));
#17119=EDGE_LOOP('',(#82702,#82703,#82704,#82705));
#17120=EDGE_LOOP('',(#82706,#82707,#82708,#82709));
#17121=EDGE_LOOP('',(#82710,#82711,#82712,#82713));
#17122=EDGE_LOOP('',(#82714,#82715,#82716,#82717));
#17123=EDGE_LOOP('',(#82718,#82719,#82720,#82721));
#17124=EDGE_LOOP('',(#82722,#82723,#82724,#82725,#82726));
#17125=EDGE_LOOP('',(#82727,#82728,#82729,#82730,#82731));
#17126=EDGE_LOOP('',(#82732,#82733,#82734,#82735,#82736,#82737));
#17127=EDGE_LOOP('',(#82738,#82739,#82740,#82741));
#17128=EDGE_LOOP('',(#82742,#82743,#82744,#82745,#82746));
#17129=EDGE_LOOP('',(#82747,#82748,#82749,#82750));
#17130=EDGE_LOOP('',(#82751,#82752,#82753,#82754));
#17131=EDGE_LOOP('',(#82755,#82756,#82757,#82758));
#17132=EDGE_LOOP('',(#82759,#82760,#82761,#82762));
#17133=EDGE_LOOP('',(#82763,#82764,#82765,#82766));
#17134=EDGE_LOOP('',(#82767,#82768,#82769,#82770,#82771));
#17135=EDGE_LOOP('',(#82772,#82773,#82774,#82775));
#17136=EDGE_LOOP('',(#82776,#82777,#82778,#82779));
#17137=EDGE_LOOP('',(#82780,#82781,#82782,#82783));
#17138=EDGE_LOOP('',(#82784,#82785,#82786,#82787));
#17139=EDGE_LOOP('',(#82788,#82789,#82790,#82791));
#17140=EDGE_LOOP('',(#82792,#82793,#82794,#82795,#82796));
#17141=EDGE_LOOP('',(#82797,#82798,#82799,#82800,#82801));
#17142=EDGE_LOOP('',(#82802,#82803,#82804,#82805,#82806,#82807));
#17143=EDGE_LOOP('',(#82808,#82809,#82810,#82811));
#17144=EDGE_LOOP('',(#82812,#82813,#82814,#82815,#82816));
#17145=EDGE_LOOP('',(#82817,#82818,#82819,#82820));
#17146=EDGE_LOOP('',(#82821,#82822,#82823,#82824));
#17147=EDGE_LOOP('',(#82825,#82826,#82827,#82828));
#17148=EDGE_LOOP('',(#82829,#82830,#82831,#82832));
#17149=EDGE_LOOP('',(#82833,#82834,#82835,#82836));
#17150=EDGE_LOOP('',(#82837,#82838,#82839,#82840,#82841));
#17151=EDGE_LOOP('',(#82842,#82843,#82844,#82845));
#17152=EDGE_LOOP('',(#82846,#82847,#82848,#82849));
#17153=EDGE_LOOP('',(#82850,#82851,#82852,#82853));
#17154=EDGE_LOOP('',(#82854,#82855,#82856,#82857));
#17155=EDGE_LOOP('',(#82858,#82859,#82860,#82861));
#17156=EDGE_LOOP('',(#82862,#82863,#82864,#82865,#82866));
#17157=EDGE_LOOP('',(#82867,#82868,#82869,#82870,#82871));
#17158=EDGE_LOOP('',(#82872,#82873,#82874,#82875,#82876,#82877));
#17159=EDGE_LOOP('',(#82878,#82879,#82880,#82881));
#17160=EDGE_LOOP('',(#82882,#82883,#82884,#82885,#82886));
#17161=EDGE_LOOP('',(#82887,#82888,#82889,#82890));
#17162=EDGE_LOOP('',(#82891,#82892,#82893,#82894));
#17163=EDGE_LOOP('',(#82895,#82896,#82897,#82898));
#17164=EDGE_LOOP('',(#82899,#82900,#82901,#82902));
#17165=EDGE_LOOP('',(#82903,#82904,#82905,#82906));
#17166=EDGE_LOOP('',(#82907,#82908,#82909,#82910,#82911));
#17167=EDGE_LOOP('',(#82912,#82913,#82914,#82915));
#17168=EDGE_LOOP('',(#82916,#82917,#82918,#82919));
#17169=EDGE_LOOP('',(#82920,#82921,#82922,#82923));
#17170=EDGE_LOOP('',(#82924,#82925,#82926,#82927));
#17171=EDGE_LOOP('',(#82928,#82929,#82930,#82931));
#17172=EDGE_LOOP('',(#82932,#82933,#82934,#82935,#82936));
#17173=EDGE_LOOP('',(#82937,#82938,#82939,#82940,#82941));
#17174=EDGE_LOOP('',(#82942,#82943,#82944,#82945,#82946,#82947));
#17175=EDGE_LOOP('',(#82948,#82949,#82950,#82951));
#17176=EDGE_LOOP('',(#82952,#82953,#82954,#82955,#82956));
#17177=EDGE_LOOP('',(#82957,#82958,#82959,#82960));
#17178=EDGE_LOOP('',(#82961,#82962,#82963,#82964));
#17179=EDGE_LOOP('',(#82965,#82966,#82967,#82968));
#17180=EDGE_LOOP('',(#82969,#82970,#82971,#82972));
#17181=EDGE_LOOP('',(#82973,#82974,#82975,#82976));
#17182=EDGE_LOOP('',(#82977,#82978,#82979,#82980,#82981));
#17183=EDGE_LOOP('',(#82982,#82983,#82984,#82985));
#17184=EDGE_LOOP('',(#82986,#82987,#82988,#82989));
#17185=EDGE_LOOP('',(#82990,#82991,#82992,#82993));
#17186=EDGE_LOOP('',(#82994,#82995,#82996,#82997));
#17187=EDGE_LOOP('',(#82998,#82999,#83000,#83001));
#17188=EDGE_LOOP('',(#83002,#83003,#83004,#83005,#83006));
#17189=EDGE_LOOP('',(#83007,#83008,#83009,#83010,#83011));
#17190=EDGE_LOOP('',(#83012,#83013,#83014,#83015,#83016,#83017));
#17191=EDGE_LOOP('',(#83018,#83019,#83020,#83021));
#17192=EDGE_LOOP('',(#83022,#83023,#83024,#83025,#83026));
#17193=EDGE_LOOP('',(#83027,#83028,#83029,#83030));
#17194=EDGE_LOOP('',(#83031,#83032,#83033,#83034));
#17195=EDGE_LOOP('',(#83035,#83036,#83037,#83038));
#17196=EDGE_LOOP('',(#83039,#83040,#83041,#83042));
#17197=EDGE_LOOP('',(#83043,#83044,#83045,#83046));
#17198=EDGE_LOOP('',(#83047,#83048,#83049,#83050,#83051));
#17199=EDGE_LOOP('',(#83052,#83053,#83054,#83055));
#17200=EDGE_LOOP('',(#83056,#83057,#83058,#83059));
#17201=EDGE_LOOP('',(#83060,#83061,#83062,#83063));
#17202=EDGE_LOOP('',(#83064,#83065,#83066,#83067));
#17203=EDGE_LOOP('',(#83068,#83069,#83070,#83071));
#17204=EDGE_LOOP('',(#83072,#83073,#83074,#83075,#83076));
#17205=EDGE_LOOP('',(#83077,#83078,#83079,#83080,#83081));
#17206=EDGE_LOOP('',(#83082,#83083,#83084,#83085,#83086,#83087));
#17207=EDGE_LOOP('',(#83088,#83089,#83090,#83091));
#17208=EDGE_LOOP('',(#83092,#83093,#83094,#83095,#83096));
#17209=EDGE_LOOP('',(#83097,#83098,#83099,#83100));
#17210=EDGE_LOOP('',(#83101,#83102,#83103,#83104));
#17211=EDGE_LOOP('',(#83105,#83106,#83107,#83108));
#17212=EDGE_LOOP('',(#83109,#83110,#83111,#83112));
#17213=EDGE_LOOP('',(#83113,#83114,#83115,#83116));
#17214=EDGE_LOOP('',(#83117,#83118,#83119,#83120,#83121));
#17215=EDGE_LOOP('',(#83122,#83123,#83124,#83125));
#17216=EDGE_LOOP('',(#83126,#83127,#83128,#83129));
#17217=EDGE_LOOP('',(#83130,#83131,#83132,#83133));
#17218=EDGE_LOOP('',(#83134,#83135,#83136,#83137));
#17219=EDGE_LOOP('',(#83138,#83139,#83140,#83141));
#17220=EDGE_LOOP('',(#83142,#83143,#83144,#83145,#83146));
#17221=EDGE_LOOP('',(#83147,#83148,#83149,#83150,#83151));
#17222=EDGE_LOOP('',(#83152,#83153,#83154,#83155,#83156,#83157));
#17223=EDGE_LOOP('',(#83158,#83159,#83160,#83161));
#17224=EDGE_LOOP('',(#83162,#83163,#83164,#83165,#83166));
#17225=EDGE_LOOP('',(#83167,#83168,#83169,#83170));
#17226=EDGE_LOOP('',(#83171,#83172,#83173,#83174));
#17227=EDGE_LOOP('',(#83175,#83176,#83177,#83178));
#17228=EDGE_LOOP('',(#83179,#83180,#83181,#83182));
#17229=EDGE_LOOP('',(#83183,#83184,#83185,#83186));
#17230=EDGE_LOOP('',(#83187,#83188,#83189,#83190,#83191));
#17231=EDGE_LOOP('',(#83192,#83193,#83194,#83195));
#17232=EDGE_LOOP('',(#83196,#83197,#83198,#83199));
#17233=EDGE_LOOP('',(#83200,#83201,#83202,#83203));
#17234=EDGE_LOOP('',(#83204,#83205,#83206,#83207));
#17235=EDGE_LOOP('',(#83208,#83209,#83210,#83211));
#17236=EDGE_LOOP('',(#83212,#83213,#83214,#83215,#83216));
#17237=EDGE_LOOP('',(#83217,#83218,#83219,#83220,#83221));
#17238=EDGE_LOOP('',(#83222,#83223,#83224,#83225,#83226,#83227));
#17239=EDGE_LOOP('',(#83228,#83229,#83230,#83231));
#17240=EDGE_LOOP('',(#83232,#83233,#83234,#83235,#83236));
#17241=EDGE_LOOP('',(#83237,#83238,#83239,#83240));
#17242=EDGE_LOOP('',(#83241,#83242,#83243,#83244));
#17243=EDGE_LOOP('',(#83245,#83246,#83247,#83248));
#17244=EDGE_LOOP('',(#83249,#83250,#83251,#83252));
#17245=EDGE_LOOP('',(#83253,#83254,#83255,#83256));
#17246=EDGE_LOOP('',(#83257,#83258,#83259,#83260,#83261));
#17247=EDGE_LOOP('',(#83262,#83263,#83264,#83265));
#17248=EDGE_LOOP('',(#83266,#83267,#83268,#83269));
#17249=EDGE_LOOP('',(#83270,#83271,#83272,#83273));
#17250=EDGE_LOOP('',(#83274,#83275,#83276,#83277));
#17251=EDGE_LOOP('',(#83278,#83279,#83280,#83281));
#17252=EDGE_LOOP('',(#83282,#83283,#83284,#83285,#83286));
#17253=EDGE_LOOP('',(#83287,#83288,#83289,#83290,#83291));
#17254=EDGE_LOOP('',(#83292,#83293,#83294,#83295,#83296,#83297));
#17255=EDGE_LOOP('',(#83298,#83299,#83300,#83301));
#17256=EDGE_LOOP('',(#83302,#83303,#83304,#83305,#83306));
#17257=EDGE_LOOP('',(#83307,#83308,#83309,#83310));
#17258=EDGE_LOOP('',(#83311,#83312,#83313,#83314));
#17259=EDGE_LOOP('',(#83315,#83316,#83317,#83318));
#17260=EDGE_LOOP('',(#83319,#83320,#83321,#83322));
#17261=EDGE_LOOP('',(#83323,#83324,#83325,#83326));
#17262=EDGE_LOOP('',(#83327,#83328,#83329,#83330,#83331));
#17263=EDGE_LOOP('',(#83332,#83333,#83334,#83335));
#17264=EDGE_LOOP('',(#83336,#83337,#83338,#83339));
#17265=EDGE_LOOP('',(#83340,#83341,#83342,#83343));
#17266=EDGE_LOOP('',(#83344,#83345,#83346,#83347));
#17267=EDGE_LOOP('',(#83348,#83349,#83350,#83351));
#17268=EDGE_LOOP('',(#83352,#83353,#83354,#83355,#83356));
#17269=EDGE_LOOP('',(#83357,#83358,#83359,#83360,#83361));
#17270=EDGE_LOOP('',(#83362,#83363,#83364,#83365,#83366,#83367));
#17271=EDGE_LOOP('',(#83368,#83369,#83370,#83371));
#17272=EDGE_LOOP('',(#83372,#83373,#83374,#83375,#83376));
#17273=EDGE_LOOP('',(#83377,#83378,#83379,#83380));
#17274=EDGE_LOOP('',(#83381,#83382,#83383,#83384));
#17275=EDGE_LOOP('',(#83385,#83386,#83387,#83388));
#17276=EDGE_LOOP('',(#83389,#83390,#83391,#83392));
#17277=EDGE_LOOP('',(#83393,#83394,#83395,#83396));
#17278=EDGE_LOOP('',(#83397,#83398,#83399,#83400,#83401));
#17279=EDGE_LOOP('',(#83402,#83403,#83404,#83405));
#17280=EDGE_LOOP('',(#83406,#83407,#83408,#83409));
#17281=EDGE_LOOP('',(#83410,#83411,#83412,#83413));
#17282=EDGE_LOOP('',(#83414,#83415,#83416,#83417));
#17283=EDGE_LOOP('',(#83418,#83419,#83420,#83421));
#17284=EDGE_LOOP('',(#83422,#83423,#83424,#83425,#83426));
#17285=EDGE_LOOP('',(#83427,#83428,#83429,#83430,#83431));
#17286=EDGE_LOOP('',(#83432,#83433,#83434,#83435,#83436,#83437));
#17287=EDGE_LOOP('',(#83438,#83439,#83440,#83441));
#17288=EDGE_LOOP('',(#83442,#83443,#83444,#83445,#83446));
#17289=EDGE_LOOP('',(#83447,#83448,#83449,#83450));
#17290=EDGE_LOOP('',(#83451,#83452,#83453,#83454));
#17291=EDGE_LOOP('',(#83455,#83456,#83457,#83458));
#17292=EDGE_LOOP('',(#83459,#83460,#83461,#83462));
#17293=EDGE_LOOP('',(#83463,#83464,#83465,#83466));
#17294=EDGE_LOOP('',(#83467,#83468,#83469,#83470,#83471));
#17295=EDGE_LOOP('',(#83472,#83473,#83474,#83475));
#17296=EDGE_LOOP('',(#83476,#83477,#83478,#83479));
#17297=EDGE_LOOP('',(#83480,#83481,#83482,#83483));
#17298=EDGE_LOOP('',(#83484,#83485,#83486,#83487));
#17299=EDGE_LOOP('',(#83488,#83489,#83490,#83491));
#17300=EDGE_LOOP('',(#83492,#83493,#83494,#83495,#83496));
#17301=EDGE_LOOP('',(#83497,#83498,#83499,#83500,#83501));
#17302=EDGE_LOOP('',(#83502,#83503,#83504,#83505,#83506,#83507));
#17303=EDGE_LOOP('',(#83508,#83509,#83510,#83511));
#17304=EDGE_LOOP('',(#83512,#83513,#83514,#83515,#83516));
#17305=EDGE_LOOP('',(#83517,#83518,#83519,#83520));
#17306=EDGE_LOOP('',(#83521,#83522,#83523,#83524));
#17307=EDGE_LOOP('',(#83525,#83526,#83527,#83528));
#17308=EDGE_LOOP('',(#83529,#83530,#83531,#83532));
#17309=EDGE_LOOP('',(#83533,#83534,#83535,#83536));
#17310=EDGE_LOOP('',(#83537,#83538,#83539,#83540,#83541));
#17311=EDGE_LOOP('',(#83542,#83543,#83544,#83545));
#17312=EDGE_LOOP('',(#83546,#83547,#83548,#83549));
#17313=EDGE_LOOP('',(#83550,#83551,#83552,#83553));
#17314=EDGE_LOOP('',(#83554,#83555,#83556,#83557));
#17315=EDGE_LOOP('',(#83558,#83559,#83560,#83561));
#17316=EDGE_LOOP('',(#83562,#83563,#83564,#83565,#83566));
#17317=EDGE_LOOP('',(#83567,#83568,#83569,#83570,#83571));
#17318=EDGE_LOOP('',(#83572,#83573,#83574,#83575,#83576,#83577));
#17319=EDGE_LOOP('',(#83578,#83579,#83580,#83581));
#17320=EDGE_LOOP('',(#83582,#83583,#83584,#83585,#83586));
#17321=EDGE_LOOP('',(#83587,#83588,#83589,#83590));
#17322=EDGE_LOOP('',(#83591,#83592,#83593,#83594));
#17323=EDGE_LOOP('',(#83595,#83596,#83597,#83598));
#17324=EDGE_LOOP('',(#83599,#83600,#83601,#83602));
#17325=EDGE_LOOP('',(#83603,#83604,#83605,#83606));
#17326=EDGE_LOOP('',(#83607,#83608,#83609,#83610,#83611));
#17327=EDGE_LOOP('',(#83612,#83613,#83614,#83615));
#17328=EDGE_LOOP('',(#83616,#83617,#83618,#83619));
#17329=EDGE_LOOP('',(#83620,#83621,#83622,#83623));
#17330=EDGE_LOOP('',(#83624,#83625,#83626,#83627));
#17331=EDGE_LOOP('',(#83628,#83629,#83630,#83631));
#17332=EDGE_LOOP('',(#83632,#83633,#83634,#83635,#83636));
#17333=EDGE_LOOP('',(#83637,#83638,#83639,#83640,#83641));
#17334=EDGE_LOOP('',(#83642,#83643,#83644,#83645,#83646,#83647));
#17335=EDGE_LOOP('',(#83648,#83649,#83650,#83651));
#17336=EDGE_LOOP('',(#83652,#83653,#83654,#83655,#83656));
#17337=EDGE_LOOP('',(#83657,#83658,#83659,#83660));
#17338=EDGE_LOOP('',(#83661,#83662,#83663,#83664));
#17339=EDGE_LOOP('',(#83665,#83666,#83667,#83668));
#17340=EDGE_LOOP('',(#83669,#83670,#83671,#83672));
#17341=EDGE_LOOP('',(#83673,#83674,#83675,#83676));
#17342=EDGE_LOOP('',(#83677,#83678,#83679,#83680,#83681));
#17343=EDGE_LOOP('',(#83682,#83683,#83684,#83685));
#17344=EDGE_LOOP('',(#83686,#83687,#83688,#83689));
#17345=EDGE_LOOP('',(#83690,#83691,#83692,#83693));
#17346=EDGE_LOOP('',(#83694,#83695,#83696,#83697));
#17347=EDGE_LOOP('',(#83698,#83699,#83700,#83701));
#17348=EDGE_LOOP('',(#83702,#83703,#83704,#83705,#83706));
#17349=EDGE_LOOP('',(#83707,#83708,#83709,#83710,#83711));
#17350=EDGE_LOOP('',(#83712,#83713,#83714,#83715,#83716,#83717));
#17351=EDGE_LOOP('',(#83718,#83719,#83720,#83721));
#17352=EDGE_LOOP('',(#83722,#83723,#83724,#83725,#83726));
#17353=EDGE_LOOP('',(#83727,#83728,#83729,#83730));
#17354=EDGE_LOOP('',(#83731,#83732,#83733,#83734));
#17355=EDGE_LOOP('',(#83735,#83736,#83737,#83738));
#17356=EDGE_LOOP('',(#83739,#83740,#83741,#83742));
#17357=EDGE_LOOP('',(#83743,#83744,#83745,#83746));
#17358=EDGE_LOOP('',(#83747,#83748,#83749,#83750,#83751));
#17359=EDGE_LOOP('',(#83752,#83753,#83754,#83755));
#17360=EDGE_LOOP('',(#83756,#83757,#83758,#83759));
#17361=EDGE_LOOP('',(#83760,#83761,#83762,#83763));
#17362=EDGE_LOOP('',(#83764,#83765,#83766,#83767));
#17363=EDGE_LOOP('',(#83768,#83769,#83770,#83771));
#17364=EDGE_LOOP('',(#83772,#83773,#83774,#83775,#83776));
#17365=EDGE_LOOP('',(#83777,#83778,#83779,#83780,#83781));
#17366=EDGE_LOOP('',(#83782,#83783,#83784,#83785,#83786,#83787));
#17367=EDGE_LOOP('',(#83788,#83789,#83790,#83791));
#17368=EDGE_LOOP('',(#83792,#83793,#83794,#83795,#83796));
#17369=EDGE_LOOP('',(#83797,#83798,#83799,#83800));
#17370=EDGE_LOOP('',(#83801,#83802,#83803,#83804));
#17371=EDGE_LOOP('',(#83805,#83806,#83807,#83808));
#17372=EDGE_LOOP('',(#83809,#83810,#83811,#83812));
#17373=EDGE_LOOP('',(#83813,#83814,#83815,#83816));
#17374=EDGE_LOOP('',(#83817,#83818,#83819,#83820,#83821));
#17375=EDGE_LOOP('',(#83822,#83823,#83824,#83825));
#17376=EDGE_LOOP('',(#83826,#83827,#83828,#83829));
#17377=EDGE_LOOP('',(#83830,#83831,#83832,#83833));
#17378=EDGE_LOOP('',(#83834,#83835,#83836,#83837));
#17379=EDGE_LOOP('',(#83838,#83839,#83840,#83841));
#17380=EDGE_LOOP('',(#83842,#83843,#83844,#83845,#83846));
#17381=EDGE_LOOP('',(#83847,#83848,#83849,#83850,#83851));
#17382=EDGE_LOOP('',(#83852,#83853,#83854,#83855,#83856,#83857));
#17383=EDGE_LOOP('',(#83858,#83859,#83860,#83861));
#17384=EDGE_LOOP('',(#83862,#83863,#83864,#83865,#83866));
#17385=EDGE_LOOP('',(#83867,#83868,#83869,#83870));
#17386=EDGE_LOOP('',(#83871,#83872,#83873,#83874));
#17387=EDGE_LOOP('',(#83875,#83876,#83877,#83878));
#17388=EDGE_LOOP('',(#83879,#83880,#83881,#83882));
#17389=EDGE_LOOP('',(#83883,#83884,#83885,#83886));
#17390=EDGE_LOOP('',(#83887,#83888,#83889,#83890,#83891));
#17391=EDGE_LOOP('',(#83892,#83893,#83894,#83895));
#17392=EDGE_LOOP('',(#83896,#83897,#83898,#83899));
#17393=EDGE_LOOP('',(#83900,#83901,#83902,#83903));
#17394=EDGE_LOOP('',(#83904,#83905,#83906,#83907));
#17395=EDGE_LOOP('',(#83908,#83909,#83910,#83911));
#17396=EDGE_LOOP('',(#83912,#83913,#83914,#83915,#83916));
#17397=EDGE_LOOP('',(#83917,#83918,#83919,#83920,#83921));
#17398=EDGE_LOOP('',(#83922,#83923,#83924,#83925,#83926,#83927));
#17399=EDGE_LOOP('',(#83928,#83929,#83930,#83931));
#17400=EDGE_LOOP('',(#83932,#83933,#83934,#83935,#83936));
#17401=EDGE_LOOP('',(#83937,#83938,#83939,#83940));
#17402=EDGE_LOOP('',(#83941,#83942,#83943,#83944));
#17403=EDGE_LOOP('',(#83945,#83946,#83947,#83948));
#17404=EDGE_LOOP('',(#83949,#83950,#83951,#83952));
#17405=EDGE_LOOP('',(#83953,#83954,#83955,#83956));
#17406=EDGE_LOOP('',(#83957,#83958,#83959,#83960,#83961));
#17407=EDGE_LOOP('',(#83962,#83963,#83964,#83965));
#17408=EDGE_LOOP('',(#83966,#83967,#83968,#83969));
#17409=EDGE_LOOP('',(#83970,#83971,#83972,#83973));
#17410=EDGE_LOOP('',(#83974,#83975,#83976,#83977));
#17411=EDGE_LOOP('',(#83978,#83979,#83980,#83981));
#17412=EDGE_LOOP('',(#83982,#83983,#83984,#83985,#83986));
#17413=EDGE_LOOP('',(#83987,#83988,#83989,#83990,#83991));
#17414=EDGE_LOOP('',(#83992,#83993,#83994,#83995,#83996,#83997));
#17415=EDGE_LOOP('',(#83998,#83999,#84000,#84001));
#17416=EDGE_LOOP('',(#84002,#84003,#84004,#84005,#84006));
#17417=EDGE_LOOP('',(#84007,#84008,#84009,#84010));
#17418=EDGE_LOOP('',(#84011,#84012,#84013,#84014));
#17419=EDGE_LOOP('',(#84015,#84016,#84017,#84018));
#17420=EDGE_LOOP('',(#84019,#84020,#84021,#84022));
#17421=EDGE_LOOP('',(#84023,#84024,#84025,#84026));
#17422=EDGE_LOOP('',(#84027,#84028,#84029,#84030,#84031));
#17423=EDGE_LOOP('',(#84032,#84033,#84034,#84035));
#17424=EDGE_LOOP('',(#84036,#84037,#84038,#84039));
#17425=EDGE_LOOP('',(#84040,#84041,#84042,#84043));
#17426=EDGE_LOOP('',(#84044,#84045,#84046,#84047));
#17427=EDGE_LOOP('',(#84048,#84049,#84050,#84051));
#17428=EDGE_LOOP('',(#84052,#84053,#84054,#84055,#84056));
#17429=EDGE_LOOP('',(#84057,#84058,#84059,#84060,#84061));
#17430=EDGE_LOOP('',(#84062,#84063,#84064,#84065,#84066,#84067));
#17431=EDGE_LOOP('',(#84068,#84069,#84070,#84071));
#17432=EDGE_LOOP('',(#84072,#84073,#84074,#84075,#84076));
#17433=EDGE_LOOP('',(#84077,#84078,#84079,#84080));
#17434=EDGE_LOOP('',(#84081,#84082,#84083,#84084));
#17435=EDGE_LOOP('',(#84085,#84086,#84087,#84088));
#17436=EDGE_LOOP('',(#84089,#84090,#84091,#84092));
#17437=EDGE_LOOP('',(#84093,#84094,#84095,#84096));
#17438=EDGE_LOOP('',(#84097,#84098,#84099,#84100,#84101));
#17439=EDGE_LOOP('',(#84102,#84103,#84104,#84105));
#17440=EDGE_LOOP('',(#84106,#84107,#84108,#84109));
#17441=EDGE_LOOP('',(#84110,#84111,#84112,#84113));
#17442=EDGE_LOOP('',(#84114,#84115,#84116,#84117));
#17443=EDGE_LOOP('',(#84118,#84119,#84120,#84121));
#17444=EDGE_LOOP('',(#84122,#84123,#84124,#84125,#84126));
#17445=EDGE_LOOP('',(#84127,#84128,#84129,#84130,#84131));
#17446=EDGE_LOOP('',(#84132,#84133,#84134,#84135,#84136,#84137));
#17447=EDGE_LOOP('',(#84138,#84139,#84140,#84141));
#17448=EDGE_LOOP('',(#84142,#84143,#84144,#84145,#84146));
#17449=EDGE_LOOP('',(#84147,#84148,#84149,#84150));
#17450=EDGE_LOOP('',(#84151,#84152,#84153,#84154));
#17451=EDGE_LOOP('',(#84155,#84156,#84157,#84158));
#17452=EDGE_LOOP('',(#84159,#84160,#84161,#84162));
#17453=EDGE_LOOP('',(#84163,#84164,#84165,#84166));
#17454=EDGE_LOOP('',(#84167,#84168,#84169,#84170,#84171));
#17455=EDGE_LOOP('',(#84172,#84173,#84174,#84175));
#17456=EDGE_LOOP('',(#84176,#84177,#84178,#84179));
#17457=EDGE_LOOP('',(#84180,#84181,#84182,#84183));
#17458=EDGE_LOOP('',(#84184,#84185,#84186,#84187));
#17459=EDGE_LOOP('',(#84188,#84189,#84190,#84191));
#17460=EDGE_LOOP('',(#84192,#84193,#84194,#84195,#84196));
#17461=EDGE_LOOP('',(#84197,#84198,#84199,#84200,#84201));
#17462=EDGE_LOOP('',(#84202,#84203,#84204,#84205,#84206,#84207));
#17463=EDGE_LOOP('',(#84208,#84209,#84210,#84211));
#17464=EDGE_LOOP('',(#84212,#84213,#84214,#84215,#84216));
#17465=EDGE_LOOP('',(#84217,#84218,#84219,#84220));
#17466=EDGE_LOOP('',(#84221,#84222,#84223,#84224));
#17467=EDGE_LOOP('',(#84225,#84226,#84227,#84228));
#17468=EDGE_LOOP('',(#84229,#84230,#84231,#84232));
#17469=EDGE_LOOP('',(#84233,#84234,#84235,#84236));
#17470=EDGE_LOOP('',(#84237,#84238,#84239,#84240,#84241));
#17471=EDGE_LOOP('',(#84242,#84243,#84244,#84245));
#17472=EDGE_LOOP('',(#84246,#84247,#84248,#84249));
#17473=EDGE_LOOP('',(#84250,#84251,#84252,#84253));
#17474=EDGE_LOOP('',(#84254,#84255,#84256,#84257));
#17475=EDGE_LOOP('',(#84258,#84259,#84260,#84261));
#17476=EDGE_LOOP('',(#84262,#84263,#84264,#84265,#84266));
#17477=EDGE_LOOP('',(#84267,#84268,#84269,#84270,#84271));
#17478=EDGE_LOOP('',(#84272,#84273,#84274,#84275,#84276,#84277));
#17479=EDGE_LOOP('',(#84278,#84279,#84280,#84281));
#17480=EDGE_LOOP('',(#84282,#84283,#84284,#84285,#84286));
#17481=EDGE_LOOP('',(#84287,#84288,#84289,#84290));
#17482=EDGE_LOOP('',(#84291,#84292,#84293,#84294));
#17483=EDGE_LOOP('',(#84295,#84296,#84297,#84298));
#17484=EDGE_LOOP('',(#84299,#84300,#84301,#84302));
#17485=EDGE_LOOP('',(#84303,#84304,#84305,#84306));
#17486=EDGE_LOOP('',(#84307,#84308,#84309,#84310,#84311));
#17487=EDGE_LOOP('',(#84312,#84313,#84314,#84315));
#17488=EDGE_LOOP('',(#84316,#84317,#84318,#84319));
#17489=EDGE_LOOP('',(#84320,#84321,#84322,#84323));
#17490=EDGE_LOOP('',(#84324,#84325,#84326,#84327));
#17491=EDGE_LOOP('',(#84328,#84329,#84330,#84331));
#17492=EDGE_LOOP('',(#84332,#84333,#84334,#84335,#84336));
#17493=EDGE_LOOP('',(#84337,#84338,#84339,#84340,#84341));
#17494=EDGE_LOOP('',(#84342,#84343,#84344,#84345,#84346,#84347));
#17495=EDGE_LOOP('',(#84348,#84349,#84350,#84351));
#17496=EDGE_LOOP('',(#84352,#84353,#84354,#84355,#84356));
#17497=EDGE_LOOP('',(#84357,#84358,#84359,#84360));
#17498=EDGE_LOOP('',(#84361,#84362,#84363,#84364));
#17499=EDGE_LOOP('',(#84365,#84366,#84367,#84368));
#17500=EDGE_LOOP('',(#84369,#84370,#84371,#84372));
#17501=EDGE_LOOP('',(#84373,#84374,#84375,#84376));
#17502=EDGE_LOOP('',(#84377,#84378,#84379,#84380,#84381));
#17503=EDGE_LOOP('',(#84382,#84383,#84384,#84385));
#17504=EDGE_LOOP('',(#84386,#84387,#84388,#84389));
#17505=EDGE_LOOP('',(#84390,#84391,#84392,#84393));
#17506=EDGE_LOOP('',(#84394,#84395,#84396,#84397));
#17507=EDGE_LOOP('',(#84398,#84399,#84400,#84401));
#17508=EDGE_LOOP('',(#84402,#84403,#84404,#84405,#84406));
#17509=EDGE_LOOP('',(#84407,#84408,#84409,#84410,#84411));
#17510=EDGE_LOOP('',(#84412,#84413,#84414,#84415,#84416,#84417));
#17511=EDGE_LOOP('',(#84418,#84419,#84420,#84421));
#17512=EDGE_LOOP('',(#84422,#84423,#84424,#84425,#84426));
#17513=EDGE_LOOP('',(#84427,#84428,#84429,#84430));
#17514=EDGE_LOOP('',(#84431,#84432,#84433,#84434));
#17515=EDGE_LOOP('',(#84435,#84436,#84437,#84438));
#17516=EDGE_LOOP('',(#84439,#84440,#84441,#84442));
#17517=EDGE_LOOP('',(#84443,#84444,#84445,#84446));
#17518=EDGE_LOOP('',(#84447,#84448,#84449,#84450,#84451));
#17519=EDGE_LOOP('',(#84452,#84453,#84454,#84455));
#17520=EDGE_LOOP('',(#84456,#84457,#84458,#84459));
#17521=EDGE_LOOP('',(#84460,#84461,#84462,#84463));
#17522=EDGE_LOOP('',(#84464,#84465,#84466,#84467));
#17523=EDGE_LOOP('',(#84468,#84469,#84470,#84471));
#17524=EDGE_LOOP('',(#84472,#84473,#84474,#84475,#84476));
#17525=EDGE_LOOP('',(#84477,#84478,#84479,#84480,#84481));
#17526=EDGE_LOOP('',(#84482,#84483,#84484,#84485,#84486,#84487));
#17527=EDGE_LOOP('',(#84488,#84489,#84490,#84491));
#17528=EDGE_LOOP('',(#84492,#84493,#84494,#84495,#84496));
#17529=EDGE_LOOP('',(#84497,#84498,#84499,#84500));
#17530=EDGE_LOOP('',(#84501,#84502,#84503,#84504));
#17531=EDGE_LOOP('',(#84505,#84506,#84507,#84508));
#17532=EDGE_LOOP('',(#84509,#84510,#84511,#84512));
#17533=EDGE_LOOP('',(#84513,#84514,#84515,#84516));
#17534=EDGE_LOOP('',(#84517,#84518,#84519,#84520,#84521));
#17535=EDGE_LOOP('',(#84522,#84523,#84524,#84525));
#17536=EDGE_LOOP('',(#84526,#84527,#84528,#84529));
#17537=EDGE_LOOP('',(#84530,#84531,#84532,#84533));
#17538=EDGE_LOOP('',(#84534,#84535,#84536,#84537));
#17539=EDGE_LOOP('',(#84538,#84539,#84540,#84541));
#17540=EDGE_LOOP('',(#84542,#84543,#84544,#84545,#84546));
#17541=EDGE_LOOP('',(#84547,#84548,#84549,#84550,#84551));
#17542=EDGE_LOOP('',(#84552,#84553,#84554,#84555,#84556,#84557));
#17543=EDGE_LOOP('',(#84558,#84559,#84560,#84561));
#17544=EDGE_LOOP('',(#84562,#84563,#84564,#84565,#84566));
#17545=EDGE_LOOP('',(#84567,#84568,#84569,#84570));
#17546=EDGE_LOOP('',(#84571,#84572,#84573,#84574));
#17547=EDGE_LOOP('',(#84575,#84576,#84577,#84578));
#17548=EDGE_LOOP('',(#84579,#84580,#84581,#84582));
#17549=EDGE_LOOP('',(#84583,#84584,#84585,#84586));
#17550=EDGE_LOOP('',(#84587,#84588,#84589,#84590,#84591));
#17551=EDGE_LOOP('',(#84592,#84593,#84594,#84595));
#17552=EDGE_LOOP('',(#84596,#84597,#84598,#84599));
#17553=EDGE_LOOP('',(#84600,#84601,#84602,#84603));
#17554=EDGE_LOOP('',(#84604,#84605,#84606,#84607));
#17555=EDGE_LOOP('',(#84608,#84609,#84610,#84611));
#17556=EDGE_LOOP('',(#84612,#84613,#84614,#84615,#84616));
#17557=EDGE_LOOP('',(#84617,#84618,#84619,#84620,#84621));
#17558=EDGE_LOOP('',(#84622,#84623,#84624,#84625,#84626,#84627));
#17559=EDGE_LOOP('',(#84628,#84629,#84630,#84631));
#17560=EDGE_LOOP('',(#84632,#84633,#84634,#84635,#84636));
#17561=EDGE_LOOP('',(#84637,#84638,#84639,#84640));
#17562=EDGE_LOOP('',(#84641,#84642,#84643,#84644));
#17563=EDGE_LOOP('',(#84645,#84646,#84647,#84648));
#17564=EDGE_LOOP('',(#84649,#84650,#84651,#84652));
#17565=EDGE_LOOP('',(#84653,#84654,#84655,#84656));
#17566=EDGE_LOOP('',(#84657,#84658,#84659,#84660,#84661));
#17567=EDGE_LOOP('',(#84662,#84663,#84664,#84665));
#17568=EDGE_LOOP('',(#84666,#84667,#84668,#84669));
#17569=EDGE_LOOP('',(#84670,#84671,#84672,#84673));
#17570=EDGE_LOOP('',(#84674,#84675,#84676,#84677));
#17571=EDGE_LOOP('',(#84678,#84679,#84680,#84681));
#17572=EDGE_LOOP('',(#84682,#84683,#84684,#84685,#84686));
#17573=EDGE_LOOP('',(#84687,#84688,#84689,#84690,#84691));
#17574=EDGE_LOOP('',(#84692,#84693,#84694,#84695,#84696,#84697));
#17575=EDGE_LOOP('',(#84698,#84699,#84700,#84701));
#17576=EDGE_LOOP('',(#84702,#84703,#84704,#84705,#84706));
#17577=EDGE_LOOP('',(#84707,#84708,#84709,#84710));
#17578=EDGE_LOOP('',(#84711,#84712,#84713,#84714));
#17579=EDGE_LOOP('',(#84715,#84716,#84717,#84718));
#17580=EDGE_LOOP('',(#84719,#84720,#84721,#84722));
#17581=EDGE_LOOP('',(#84723,#84724,#84725,#84726));
#17582=EDGE_LOOP('',(#84727,#84728,#84729,#84730,#84731));
#17583=EDGE_LOOP('',(#84732,#84733,#84734,#84735));
#17584=EDGE_LOOP('',(#84736,#84737,#84738,#84739));
#17585=EDGE_LOOP('',(#84740,#84741,#84742,#84743));
#17586=EDGE_LOOP('',(#84744,#84745,#84746,#84747));
#17587=EDGE_LOOP('',(#84748,#84749,#84750,#84751));
#17588=EDGE_LOOP('',(#84752,#84753,#84754,#84755,#84756));
#17589=EDGE_LOOP('',(#84757,#84758,#84759,#84760,#84761));
#17590=EDGE_LOOP('',(#84762,#84763,#84764,#84765,#84766,#84767));
#17591=EDGE_LOOP('',(#84768,#84769,#84770,#84771));
#17592=EDGE_LOOP('',(#84772,#84773,#84774,#84775,#84776));
#17593=EDGE_LOOP('',(#84777,#84778,#84779,#84780));
#17594=EDGE_LOOP('',(#84781,#84782,#84783,#84784));
#17595=EDGE_LOOP('',(#84785,#84786,#84787,#84788));
#17596=EDGE_LOOP('',(#84789,#84790,#84791,#84792));
#17597=EDGE_LOOP('',(#84793,#84794,#84795,#84796));
#17598=EDGE_LOOP('',(#84797,#84798,#84799,#84800,#84801));
#17599=EDGE_LOOP('',(#84802,#84803,#84804,#84805));
#17600=EDGE_LOOP('',(#84806,#84807,#84808,#84809));
#17601=EDGE_LOOP('',(#84810,#84811,#84812,#84813));
#17602=EDGE_LOOP('',(#84814,#84815,#84816,#84817));
#17603=EDGE_LOOP('',(#84818,#84819,#84820,#84821));
#17604=EDGE_LOOP('',(#84822,#84823,#84824,#84825,#84826));
#17605=EDGE_LOOP('',(#84827,#84828,#84829,#84830,#84831));
#17606=EDGE_LOOP('',(#84832,#84833,#84834,#84835,#84836,#84837));
#17607=EDGE_LOOP('',(#84838,#84839,#84840,#84841));
#17608=EDGE_LOOP('',(#84842,#84843,#84844,#84845,#84846));
#17609=EDGE_LOOP('',(#84847,#84848,#84849,#84850));
#17610=EDGE_LOOP('',(#84851,#84852,#84853,#84854));
#17611=EDGE_LOOP('',(#84855,#84856,#84857,#84858));
#17612=EDGE_LOOP('',(#84859,#84860,#84861,#84862));
#17613=EDGE_LOOP('',(#84863,#84864,#84865,#84866));
#17614=EDGE_LOOP('',(#84867,#84868,#84869,#84870,#84871));
#17615=EDGE_LOOP('',(#84872,#84873,#84874,#84875));
#17616=EDGE_LOOP('',(#84876,#84877,#84878,#84879));
#17617=EDGE_LOOP('',(#84880,#84881,#84882,#84883));
#17618=EDGE_LOOP('',(#84884,#84885,#84886,#84887));
#17619=EDGE_LOOP('',(#84888,#84889,#84890,#84891));
#17620=EDGE_LOOP('',(#84892,#84893,#84894,#84895,#84896));
#17621=EDGE_LOOP('',(#84897,#84898,#84899,#84900,#84901));
#17622=EDGE_LOOP('',(#84902,#84903,#84904,#84905,#84906,#84907));
#17623=EDGE_LOOP('',(#84908,#84909,#84910,#84911));
#17624=EDGE_LOOP('',(#84912,#84913,#84914,#84915,#84916));
#17625=EDGE_LOOP('',(#84917,#84918,#84919,#84920));
#17626=EDGE_LOOP('',(#84921,#84922,#84923,#84924));
#17627=EDGE_LOOP('',(#84925,#84926,#84927,#84928));
#17628=EDGE_LOOP('',(#84929,#84930,#84931,#84932));
#17629=EDGE_LOOP('',(#84933,#84934,#84935,#84936));
#17630=EDGE_LOOP('',(#84937,#84938,#84939,#84940,#84941));
#17631=EDGE_LOOP('',(#84942,#84943,#84944,#84945));
#17632=EDGE_LOOP('',(#84946,#84947,#84948,#84949));
#17633=EDGE_LOOP('',(#84950,#84951,#84952,#84953));
#17634=EDGE_LOOP('',(#84954,#84955,#84956,#84957));
#17635=EDGE_LOOP('',(#84958,#84959,#84960,#84961));
#17636=EDGE_LOOP('',(#84962,#84963,#84964,#84965,#84966));
#17637=EDGE_LOOP('',(#84967,#84968,#84969,#84970,#84971));
#17638=EDGE_LOOP('',(#84972,#84973,#84974,#84975,#84976,#84977));
#17639=EDGE_LOOP('',(#84978,#84979,#84980,#84981));
#17640=EDGE_LOOP('',(#84982,#84983,#84984,#84985,#84986));
#17641=EDGE_LOOP('',(#84987,#84988,#84989,#84990));
#17642=EDGE_LOOP('',(#84991,#84992,#84993,#84994));
#17643=EDGE_LOOP('',(#84995,#84996,#84997,#84998));
#17644=EDGE_LOOP('',(#84999,#85000,#85001,#85002));
#17645=EDGE_LOOP('',(#85003,#85004,#85005,#85006));
#17646=EDGE_LOOP('',(#85007,#85008,#85009,#85010,#85011));
#17647=EDGE_LOOP('',(#85012,#85013,#85014,#85015));
#17648=EDGE_LOOP('',(#85016,#85017,#85018,#85019));
#17649=EDGE_LOOP('',(#85020,#85021,#85022,#85023));
#17650=EDGE_LOOP('',(#85024,#85025,#85026,#85027));
#17651=EDGE_LOOP('',(#85028,#85029,#85030,#85031));
#17652=EDGE_LOOP('',(#85032,#85033,#85034,#85035,#85036));
#17653=EDGE_LOOP('',(#85037,#85038,#85039,#85040,#85041));
#17654=EDGE_LOOP('',(#85042,#85043,#85044,#85045,#85046,#85047));
#17655=EDGE_LOOP('',(#85048,#85049,#85050,#85051));
#17656=EDGE_LOOP('',(#85052,#85053,#85054,#85055,#85056));
#17657=EDGE_LOOP('',(#85057,#85058,#85059,#85060));
#17658=EDGE_LOOP('',(#85061,#85062,#85063,#85064));
#17659=EDGE_LOOP('',(#85065,#85066,#85067,#85068));
#17660=EDGE_LOOP('',(#85069,#85070,#85071,#85072));
#17661=EDGE_LOOP('',(#85073,#85074,#85075,#85076));
#17662=EDGE_LOOP('',(#85077,#85078,#85079,#85080,#85081));
#17663=EDGE_LOOP('',(#85082,#85083,#85084,#85085));
#17664=EDGE_LOOP('',(#85086,#85087,#85088,#85089));
#17665=EDGE_LOOP('',(#85090,#85091,#85092,#85093));
#17666=EDGE_LOOP('',(#85094,#85095,#85096,#85097));
#17667=EDGE_LOOP('',(#85098,#85099,#85100,#85101));
#17668=EDGE_LOOP('',(#85102,#85103,#85104,#85105,#85106));
#17669=EDGE_LOOP('',(#85107,#85108,#85109,#85110,#85111));
#17670=EDGE_LOOP('',(#85112,#85113,#85114,#85115,#85116,#85117));
#17671=EDGE_LOOP('',(#85118,#85119,#85120,#85121));
#17672=EDGE_LOOP('',(#85122,#85123,#85124,#85125,#85126));
#17673=EDGE_LOOP('',(#85127,#85128,#85129,#85130));
#17674=EDGE_LOOP('',(#85131,#85132,#85133,#85134));
#17675=EDGE_LOOP('',(#85135,#85136,#85137,#85138));
#17676=EDGE_LOOP('',(#85139,#85140,#85141,#85142));
#17677=EDGE_LOOP('',(#85143,#85144,#85145,#85146));
#17678=EDGE_LOOP('',(#85147,#85148,#85149,#85150,#85151));
#17679=EDGE_LOOP('',(#85152,#85153,#85154,#85155));
#17680=EDGE_LOOP('',(#85156,#85157,#85158,#85159));
#17681=EDGE_LOOP('',(#85160,#85161,#85162,#85163));
#17682=EDGE_LOOP('',(#85164,#85165,#85166,#85167));
#17683=EDGE_LOOP('',(#85168,#85169,#85170,#85171));
#17684=EDGE_LOOP('',(#85172,#85173,#85174,#85175,#85176));
#17685=EDGE_LOOP('',(#85177,#85178,#85179,#85180,#85181));
#17686=EDGE_LOOP('',(#85182,#85183,#85184,#85185,#85186,#85187));
#17687=EDGE_LOOP('',(#85188,#85189,#85190,#85191));
#17688=EDGE_LOOP('',(#85192,#85193,#85194,#85195,#85196));
#17689=EDGE_LOOP('',(#85197,#85198,#85199,#85200));
#17690=EDGE_LOOP('',(#85201,#85202,#85203,#85204));
#17691=EDGE_LOOP('',(#85205,#85206,#85207,#85208));
#17692=EDGE_LOOP('',(#85209,#85210,#85211,#85212));
#17693=EDGE_LOOP('',(#85213,#85214,#85215,#85216));
#17694=EDGE_LOOP('',(#85217,#85218,#85219,#85220,#85221));
#17695=EDGE_LOOP('',(#85222,#85223,#85224,#85225));
#17696=EDGE_LOOP('',(#85226,#85227,#85228,#85229));
#17697=EDGE_LOOP('',(#85230,#85231,#85232,#85233));
#17698=EDGE_LOOP('',(#85234,#85235,#85236,#85237));
#17699=EDGE_LOOP('',(#85238,#85239,#85240,#85241));
#17700=EDGE_LOOP('',(#85242,#85243,#85244,#85245,#85246));
#17701=EDGE_LOOP('',(#85247,#85248,#85249,#85250,#85251));
#17702=EDGE_LOOP('',(#85252,#85253,#85254,#85255,#85256,#85257));
#17703=EDGE_LOOP('',(#85258,#85259,#85260,#85261));
#17704=EDGE_LOOP('',(#85262,#85263,#85264,#85265,#85266));
#17705=EDGE_LOOP('',(#85267,#85268,#85269,#85270));
#17706=EDGE_LOOP('',(#85271,#85272,#85273,#85274));
#17707=EDGE_LOOP('',(#85275,#85276,#85277,#85278));
#17708=EDGE_LOOP('',(#85279,#85280,#85281,#85282));
#17709=EDGE_LOOP('',(#85283,#85284,#85285,#85286));
#17710=EDGE_LOOP('',(#85287,#85288,#85289,#85290,#85291));
#17711=EDGE_LOOP('',(#85292,#85293,#85294,#85295));
#17712=EDGE_LOOP('',(#85296,#85297,#85298,#85299));
#17713=EDGE_LOOP('',(#85300,#85301,#85302,#85303));
#17714=EDGE_LOOP('',(#85304,#85305,#85306,#85307));
#17715=EDGE_LOOP('',(#85308,#85309,#85310,#85311));
#17716=EDGE_LOOP('',(#85312,#85313,#85314,#85315,#85316));
#17717=EDGE_LOOP('',(#85317,#85318,#85319,#85320,#85321));
#17718=EDGE_LOOP('',(#85322,#85323,#85324,#85325,#85326,#85327));
#17719=EDGE_LOOP('',(#85328,#85329,#85330,#85331));
#17720=EDGE_LOOP('',(#85332,#85333,#85334,#85335,#85336));
#17721=EDGE_LOOP('',(#85337,#85338,#85339,#85340));
#17722=EDGE_LOOP('',(#85341,#85342,#85343,#85344));
#17723=EDGE_LOOP('',(#85345,#85346,#85347,#85348));
#17724=EDGE_LOOP('',(#85349,#85350,#85351,#85352));
#17725=EDGE_LOOP('',(#85353,#85354,#85355,#85356));
#17726=EDGE_LOOP('',(#85357,#85358,#85359,#85360,#85361));
#17727=EDGE_LOOP('',(#85362,#85363,#85364,#85365));
#17728=EDGE_LOOP('',(#85366,#85367,#85368,#85369));
#17729=EDGE_LOOP('',(#85370,#85371,#85372,#85373));
#17730=EDGE_LOOP('',(#85374,#85375,#85376,#85377));
#17731=EDGE_LOOP('',(#85378,#85379,#85380,#85381));
#17732=EDGE_LOOP('',(#85382,#85383,#85384,#85385,#85386));
#17733=EDGE_LOOP('',(#85387,#85388,#85389,#85390,#85391));
#17734=EDGE_LOOP('',(#85392,#85393,#85394,#85395,#85396,#85397));
#17735=EDGE_LOOP('',(#85398,#85399,#85400,#85401));
#17736=EDGE_LOOP('',(#85402,#85403,#85404,#85405,#85406));
#17737=EDGE_LOOP('',(#85407,#85408,#85409,#85410));
#17738=EDGE_LOOP('',(#85411,#85412,#85413,#85414));
#17739=EDGE_LOOP('',(#85415,#85416,#85417,#85418));
#17740=EDGE_LOOP('',(#85419,#85420,#85421,#85422));
#17741=EDGE_LOOP('',(#85423,#85424,#85425,#85426));
#17742=EDGE_LOOP('',(#85427,#85428,#85429,#85430,#85431));
#17743=EDGE_LOOP('',(#85432,#85433,#85434,#85435));
#17744=EDGE_LOOP('',(#85436,#85437,#85438,#85439));
#17745=EDGE_LOOP('',(#85440,#85441,#85442,#85443));
#17746=EDGE_LOOP('',(#85444,#85445,#85446,#85447));
#17747=EDGE_LOOP('',(#85448,#85449,#85450,#85451));
#17748=EDGE_LOOP('',(#85452,#85453,#85454,#85455,#85456));
#17749=EDGE_LOOP('',(#85457,#85458,#85459,#85460,#85461));
#17750=EDGE_LOOP('',(#85462,#85463,#85464,#85465,#85466,#85467));
#17751=EDGE_LOOP('',(#85468,#85469,#85470,#85471));
#17752=EDGE_LOOP('',(#85472,#85473,#85474,#85475,#85476));
#17753=EDGE_LOOP('',(#85477,#85478,#85479,#85480));
#17754=EDGE_LOOP('',(#85481,#85482,#85483,#85484));
#17755=EDGE_LOOP('',(#85485,#85486,#85487,#85488));
#17756=EDGE_LOOP('',(#85489,#85490,#85491,#85492));
#17757=EDGE_LOOP('',(#85493,#85494,#85495,#85496));
#17758=EDGE_LOOP('',(#85497,#85498,#85499,#85500,#85501));
#17759=EDGE_LOOP('',(#85502,#85503,#85504,#85505));
#17760=EDGE_LOOP('',(#85506,#85507,#85508,#85509));
#17761=EDGE_LOOP('',(#85510,#85511,#85512,#85513));
#17762=EDGE_LOOP('',(#85514,#85515,#85516,#85517));
#17763=EDGE_LOOP('',(#85518,#85519,#85520,#85521));
#17764=EDGE_LOOP('',(#85522,#85523,#85524,#85525,#85526));
#17765=EDGE_LOOP('',(#85527,#85528,#85529,#85530,#85531));
#17766=EDGE_LOOP('',(#85532,#85533,#85534,#85535,#85536,#85537));
#17767=EDGE_LOOP('',(#85538,#85539,#85540,#85541));
#17768=EDGE_LOOP('',(#85542,#85543,#85544,#85545,#85546));
#17769=EDGE_LOOP('',(#85547,#85548,#85549,#85550));
#17770=EDGE_LOOP('',(#85551,#85552,#85553,#85554));
#17771=EDGE_LOOP('',(#85555,#85556,#85557,#85558));
#17772=EDGE_LOOP('',(#85559,#85560,#85561,#85562));
#17773=EDGE_LOOP('',(#85563,#85564,#85565,#85566));
#17774=EDGE_LOOP('',(#85567,#85568,#85569,#85570,#85571));
#17775=EDGE_LOOP('',(#85572,#85573,#85574,#85575));
#17776=EDGE_LOOP('',(#85576,#85577,#85578,#85579));
#17777=EDGE_LOOP('',(#85580,#85581,#85582,#85583));
#17778=EDGE_LOOP('',(#85584,#85585,#85586,#85587));
#17779=EDGE_LOOP('',(#85588,#85589,#85590,#85591));
#17780=EDGE_LOOP('',(#85592,#85593,#85594,#85595,#85596));
#17781=EDGE_LOOP('',(#85597,#85598,#85599,#85600,#85601));
#17782=EDGE_LOOP('',(#85602,#85603,#85604,#85605,#85606,#85607));
#17783=EDGE_LOOP('',(#85608,#85609,#85610,#85611));
#17784=EDGE_LOOP('',(#85612,#85613,#85614,#85615,#85616));
#17785=EDGE_LOOP('',(#85617,#85618,#85619,#85620));
#17786=EDGE_LOOP('',(#85621,#85622,#85623,#85624));
#17787=EDGE_LOOP('',(#85625,#85626,#85627,#85628));
#17788=EDGE_LOOP('',(#85629,#85630,#85631,#85632));
#17789=EDGE_LOOP('',(#85633,#85634,#85635,#85636));
#17790=EDGE_LOOP('',(#85637,#85638,#85639,#85640,#85641));
#17791=EDGE_LOOP('',(#85642,#85643,#85644,#85645));
#17792=EDGE_LOOP('',(#85646,#85647,#85648,#85649));
#17793=EDGE_LOOP('',(#85650,#85651,#85652,#85653));
#17794=EDGE_LOOP('',(#85654,#85655,#85656,#85657));
#17795=EDGE_LOOP('',(#85658,#85659,#85660,#85661));
#17796=EDGE_LOOP('',(#85662,#85663,#85664,#85665,#85666));
#17797=EDGE_LOOP('',(#85667,#85668,#85669,#85670,#85671));
#17798=EDGE_LOOP('',(#85672,#85673,#85674,#85675,#85676,#85677));
#17799=EDGE_LOOP('',(#85678,#85679,#85680,#85681));
#17800=EDGE_LOOP('',(#85682,#85683,#85684,#85685,#85686));
#17801=EDGE_LOOP('',(#85687,#85688,#85689,#85690));
#17802=EDGE_LOOP('',(#85691,#85692,#85693,#85694));
#17803=EDGE_LOOP('',(#85695,#85696,#85697,#85698));
#17804=EDGE_LOOP('',(#85699,#85700,#85701,#85702));
#17805=EDGE_LOOP('',(#85703,#85704,#85705,#85706));
#17806=EDGE_LOOP('',(#85707,#85708,#85709,#85710,#85711));
#17807=EDGE_LOOP('',(#85712,#85713,#85714,#85715));
#17808=EDGE_LOOP('',(#85716,#85717,#85718,#85719));
#17809=EDGE_LOOP('',(#85720,#85721,#85722,#85723));
#17810=EDGE_LOOP('',(#85724,#85725,#85726,#85727));
#17811=EDGE_LOOP('',(#85728,#85729,#85730,#85731));
#17812=EDGE_LOOP('',(#85732,#85733,#85734,#85735,#85736));
#17813=EDGE_LOOP('',(#85737,#85738,#85739,#85740,#85741));
#17814=EDGE_LOOP('',(#85742,#85743,#85744,#85745,#85746,#85747));
#17815=EDGE_LOOP('',(#85748,#85749,#85750,#85751));
#17816=EDGE_LOOP('',(#85752,#85753,#85754,#85755,#85756));
#17817=EDGE_LOOP('',(#85757,#85758,#85759,#85760));
#17818=EDGE_LOOP('',(#85761,#85762,#85763,#85764));
#17819=EDGE_LOOP('',(#85765,#85766,#85767,#85768));
#17820=EDGE_LOOP('',(#85769,#85770,#85771,#85772));
#17821=EDGE_LOOP('',(#85773,#85774,#85775,#85776));
#17822=EDGE_LOOP('',(#85777,#85778,#85779,#85780,#85781));
#17823=EDGE_LOOP('',(#85782,#85783,#85784,#85785));
#17824=EDGE_LOOP('',(#85786,#85787,#85788,#85789));
#17825=EDGE_LOOP('',(#85790,#85791,#85792,#85793));
#17826=EDGE_LOOP('',(#85794,#85795,#85796,#85797));
#17827=EDGE_LOOP('',(#85798,#85799,#85800,#85801));
#22110=CIRCLE('',#102650,1.17524047358087);
#22111=CIRCLE('',#102687,1.17524047358085);
#22112=CIRCLE('',#102689,1.17524047358087);
#22113=CIRCLE('',#102691,1.50000000000006);
#22114=CIRCLE('',#102726,1.50000000000006);
#22115=CIRCLE('',#102727,1.50000000000005);
#22116=CIRCLE('',#102729,2.7435563491861);
#22117=CIRCLE('',#102730,0.0220000000000001);
#22118=CIRCLE('',#102731,2.75);
#22119=CIRCLE('',#102732,0.0219999999999999);
#22120=CIRCLE('',#102734,2.7435563491861);
#22121=CIRCLE('',#102735,0.0219999999999998);
#22122=CIRCLE('',#102736,2.75);
#22123=CIRCLE('',#102737,0.0219999999999999);
#22124=CIRCLE('',#102739,2.7435563491861);
#22125=CIRCLE('',#102740,0.022);
#22126=CIRCLE('',#102741,2.75);
#22127=CIRCLE('',#102742,0.0220000000000001);
#22128=CIRCLE('',#102744,2.7435563491861);
#22129=CIRCLE('',#102745,0.0219999999999999);
#22130=CIRCLE('',#102746,2.75);
#22131=CIRCLE('',#102747,0.0220000000000001);
#22132=CIRCLE('',#102749,2.7435563491861);
#22133=CIRCLE('',#102750,0.0219999999999999);
#22134=CIRCLE('',#102751,2.75);
#22135=CIRCLE('',#102752,0.0219999999999998);
#22136=CIRCLE('',#102754,2.7435563491861);
#22137=CIRCLE('',#102755,0.0220000000000001);
#22138=CIRCLE('',#102756,2.75);
#22139=CIRCLE('',#102757,0.0220000000000001);
#22140=CIRCLE('',#102759,2.7435563491861);
#22141=CIRCLE('',#102760,0.0220000000000001);
#22142=CIRCLE('',#102761,2.75);
#22143=CIRCLE('',#102762,0.022);
#22144=CIRCLE('',#102764,2.7435563491861);
#22145=CIRCLE('',#102765,0.022);
#22146=CIRCLE('',#102766,2.75);
#22147=CIRCLE('',#102767,0.0219999999999998);
#22148=CIRCLE('',#102769,2.74355634918611);
#22149=CIRCLE('',#102770,0.0220000000000002);
#22150=CIRCLE('',#102771,2.75);
#22151=CIRCLE('',#102772,0.022);
#22152=CIRCLE('',#102774,2.7435563491861);
#22153=CIRCLE('',#102775,0.0220000000000002);
#22154=CIRCLE('',#102776,2.75);
#22155=CIRCLE('',#102777,0.0220000000000002);
#22156=CIRCLE('',#102779,2.74355634918611);
#22157=CIRCLE('',#102780,0.0219999999999998);
#22158=CIRCLE('',#102781,2.75);
#22159=CIRCLE('',#102782,0.0219999999999998);
#22160=CIRCLE('',#102784,2.7435563491861);
#22161=CIRCLE('',#102785,0.022);
#22162=CIRCLE('',#102786,2.75);
#22163=CIRCLE('',#102787,0.0219999999999998);
#22164=CIRCLE('',#102789,2.7435563491861);
#22165=CIRCLE('',#102790,0.0220000000000001);
#22166=CIRCLE('',#102791,2.75);
#22167=CIRCLE('',#102792,0.0219999999999998);
#22168=CIRCLE('',#102794,2.7435563491861);
#22169=CIRCLE('',#102795,0.022);
#22170=CIRCLE('',#102796,2.75);
#22171=CIRCLE('',#102797,0.0220000000000002);
#22172=CIRCLE('',#102799,2.7435563491861);
#22173=CIRCLE('',#102800,0.0219999999999998);
#22174=CIRCLE('',#102801,2.75);
#22175=CIRCLE('',#102802,0.022);
#22176=CIRCLE('',#102804,2.7435563491861);
#22177=CIRCLE('',#102805,0.0219999999999998);
#22178=CIRCLE('',#102806,2.75);
#22179=CIRCLE('',#102807,0.0220000000000002);
#22180=CIRCLE('',#102809,2.7435563491861);
#22181=CIRCLE('',#102810,0.022);
#22182=CIRCLE('',#102811,2.75);
#22183=CIRCLE('',#102812,0.022);
#22184=CIRCLE('',#102814,2.7435563491861);
#22185=CIRCLE('',#102815,0.0219999999999999);
#22186=CIRCLE('',#102816,2.75);
#22187=CIRCLE('',#102817,0.0220000000000001);
#22188=CIRCLE('',#102819,2.7435563491861);
#22189=CIRCLE('',#102820,0.022);
#22190=CIRCLE('',#102821,2.75);
#22191=CIRCLE('',#102822,0.0220000000000001);
#22192=CIRCLE('',#102824,2.7435563491861);
#22193=CIRCLE('',#102825,0.0220000000000001);
#22194=CIRCLE('',#102826,2.75);
#22195=CIRCLE('',#102827,0.022);
#22196=CIRCLE('',#102829,2.7435563491861);
#22197=CIRCLE('',#102830,0.022);
#22198=CIRCLE('',#102831,2.75);
#22199=CIRCLE('',#102832,0.0219999999999999);
#22200=CIRCLE('',#102834,2.7435563491861);
#22201=CIRCLE('',#102835,0.022);
#22202=CIRCLE('',#102836,2.75);
#22203=CIRCLE('',#102837,0.0219999999999998);
#22204=CIRCLE('',#102839,2.74355634918611);
#22205=CIRCLE('',#102840,0.0220000000000002);
#22206=CIRCLE('',#102841,2.75);
#22207=CIRCLE('',#102842,0.022);
#22208=CIRCLE('',#102844,2.7435563491861);
#22209=CIRCLE('',#102845,0.0220000000000001);
#22210=CIRCLE('',#102846,2.75);
#22211=CIRCLE('',#102847,0.0219999999999998);
#22212=CIRCLE('',#102849,2.7435563491861);
#22213=CIRCLE('',#102850,0.0220000000000001);
#22214=CIRCLE('',#102851,2.75);
#22215=CIRCLE('',#102852,0.0219999999999998);
#22216=CIRCLE('',#102854,2.7435563491861);
#22217=CIRCLE('',#102855,0.0219999999999999);
#22218=CIRCLE('',#102856,2.75);
#22219=CIRCLE('',#102857,0.0219999999999999);
#22220=CIRCLE('',#102859,2.74355634918611);
#22221=CIRCLE('',#102860,0.0219999999999999);
#22222=CIRCLE('',#102861,2.75);
#22223=CIRCLE('',#102862,0.0220000000000002);
#22224=CIRCLE('',#102864,2.7435563491861);
#22225=CIRCLE('',#102865,0.0220000000000002);
#22226=CIRCLE('',#102866,2.75);
#22227=CIRCLE('',#102867,0.0219999999999999);
#22228=CIRCLE('',#102869,2.74355634918611);
#22229=CIRCLE('',#102870,0.0219999999999999);
#22230=CIRCLE('',#102871,2.75);
#22231=CIRCLE('',#102872,0.0219999999999999);
#22232=CIRCLE('',#102874,2.7435563491861);
#22233=CIRCLE('',#102875,0.0219999999999998);
#22234=CIRCLE('',#102876,2.75);
#22235=CIRCLE('',#102877,0.022);
#22236=CIRCLE('',#102879,2.7435563491861);
#22237=CIRCLE('',#102880,0.0220000000000001);
#22238=CIRCLE('',#102881,2.75);
#22239=CIRCLE('',#102882,0.022);
#22240=CIRCLE('',#102884,2.7435563491861);
#22241=CIRCLE('',#102885,0.022);
#22242=CIRCLE('',#102886,2.75);
#22243=CIRCLE('',#102887,0.022);
#22244=CIRCLE('',#102889,2.7435563491861);
#22245=CIRCLE('',#102890,0.0220000000000001);
#22246=CIRCLE('',#102891,2.75);
#22247=CIRCLE('',#102892,0.0219999999999998);
#22248=CIRCLE('',#102894,2.7435563491861);
#22249=CIRCLE('',#102895,0.0220000000000002);
#22250=CIRCLE('',#102896,2.75);
#22251=CIRCLE('',#102897,0.0220000000000001);
#22252=CIRCLE('',#102899,2.7435563491861);
#22253=CIRCLE('',#102900,0.0220000000000002);
#22254=CIRCLE('',#102901,2.75);
#22255=CIRCLE('',#102902,0.022);
#22256=CIRCLE('',#102904,2.7435563491861);
#22257=CIRCLE('',#102905,0.022);
#22258=CIRCLE('',#102906,2.75);
#22259=CIRCLE('',#102907,0.0219999999999998);
#22260=CIRCLE('',#102909,2.7435563491861);
#22261=CIRCLE('',#102910,0.0220000000000001);
#22262=CIRCLE('',#102911,2.75);
#22263=CIRCLE('',#102912,0.0220000000000001);
#22264=CIRCLE('',#102914,2.7435563491861);
#22265=CIRCLE('',#102915,0.0220000000000001);
#22266=CIRCLE('',#102916,2.75);
#22267=CIRCLE('',#102917,0.0219999999999999);
#22268=CIRCLE('',#102919,2.7435563491861);
#22269=CIRCLE('',#102920,0.022);
#22270=CIRCLE('',#102921,2.75);
#22271=CIRCLE('',#102922,0.0219999999999999);
#22272=CIRCLE('',#102924,2.7435563491861);
#22273=CIRCLE('',#102925,0.0219999999999998);
#22274=CIRCLE('',#102926,2.75);
#22275=CIRCLE('',#102927,0.022);
#22276=CIRCLE('',#102929,2.7435563491861);
#22277=CIRCLE('',#102930,0.0219999999999999);
#22278=CIRCLE('',#102931,2.75);
#22279=CIRCLE('',#102932,0.0220000000000001);
#22280=CIRCLE('',#102934,2.7435563491861);
#22281=CIRCLE('',#102935,0.0219999999999999);
#22282=CIRCLE('',#102936,2.75);
#22283=CIRCLE('',#102937,0.0220000000000002);
#22284=CIRCLE('',#102939,2.74355634918611);
#22285=CIRCLE('',#102940,0.0219999999999999);
#22286=CIRCLE('',#102941,2.75);
#22287=CIRCLE('',#102942,0.022);
#22288=CIRCLE('',#102944,2.7435563491861);
#22289=CIRCLE('',#102945,0.0219999999999999);
#22290=CIRCLE('',#102946,2.75);
#22291=CIRCLE('',#102947,0.0219999999999999);
#22292=CIRCLE('',#102949,2.7435563491861);
#22293=CIRCLE('',#102950,0.0219999999999998);
#22294=CIRCLE('',#102951,2.75);
#22295=CIRCLE('',#102952,0.0219999999999998);
#22296=CIRCLE('',#102954,2.74355634918611);
#22297=CIRCLE('',#102955,0.022);
#22298=CIRCLE('',#102956,2.75);
#22299=CIRCLE('',#102957,0.0220000000000002);
#22300=CIRCLE('',#102959,2.7435563491861);
#22301=CIRCLE('',#102960,0.0219999999999998);
#22302=CIRCLE('',#102961,2.75);
#22303=CIRCLE('',#102962,0.022);
#22304=CIRCLE('',#102964,2.7435563491861);
#22305=CIRCLE('',#102965,0.022);
#22306=CIRCLE('',#102966,2.75);
#22307=CIRCLE('',#102967,0.0220000000000001);
#22308=CIRCLE('',#102969,2.7435563491861);
#22309=CIRCLE('',#102970,0.0220000000000001);
#22310=CIRCLE('',#102971,2.75);
#22311=CIRCLE('',#102972,0.022);
#22312=CIRCLE('',#102974,2.7435563491861);
#22313=CIRCLE('',#102975,0.0220000000000002);
#22314=CIRCLE('',#102976,2.75);
#22315=CIRCLE('',#102977,0.0219999999999999);
#22316=CIRCLE('',#102979,2.74355634918611);
#22317=CIRCLE('',#102980,0.022);
#22318=CIRCLE('',#102981,2.75);
#22319=CIRCLE('',#102982,0.0220000000000002);
#22320=CIRCLE('',#102984,2.7435563491861);
#22321=CIRCLE('',#102985,0.022);
#22322=CIRCLE('',#102986,2.75);
#22323=CIRCLE('',#102987,0.0219999999999999);
#22324=CIRCLE('',#102989,2.7435563491861);
#22325=CIRCLE('',#102990,0.0220000000000002);
#22326=CIRCLE('',#102991,2.75);
#22327=CIRCLE('',#102992,0.0220000000000001);
#22328=CIRCLE('',#102994,2.7435563491861);
#22329=CIRCLE('',#102995,0.0220000000000001);
#22330=CIRCLE('',#102996,2.75);
#22331=CIRCLE('',#102997,0.022);
#22332=CIRCLE('',#102999,2.7435563491861);
#22333=CIRCLE('',#103000,0.0220000000000001);
#22334=CIRCLE('',#103001,2.75);
#22335=CIRCLE('',#103002,0.022);
#22336=CIRCLE('',#103004,2.7435563491861);
#22337=CIRCLE('',#103005,0.0220000000000001);
#22338=CIRCLE('',#103006,2.75);
#22339=CIRCLE('',#103007,0.0220000000000001);
#22340=CIRCLE('',#103009,2.7435563491861);
#22341=CIRCLE('',#103010,0.0220000000000001);
#22342=CIRCLE('',#103011,2.75);
#22343=CIRCLE('',#103012,0.0219999999999999);
#22344=CIRCLE('',#103014,2.7435563491861);
#22345=CIRCLE('',#103015,0.0219999999999999);
#22346=CIRCLE('',#103016,2.75);
#22347=CIRCLE('',#103017,0.0220000000000001);
#22348=CIRCLE('',#103019,2.7435563491861);
#22349=CIRCLE('',#103020,0.0220000000000001);
#22350=CIRCLE('',#103021,2.75);
#22351=CIRCLE('',#103022,0.0220000000000001);
#22352=CIRCLE('',#103024,2.7435563491861);
#22353=CIRCLE('',#103025,0.0219999999999998);
#22354=CIRCLE('',#103026,2.75);
#22355=CIRCLE('',#103027,0.022);
#22356=CIRCLE('',#103029,2.7435563491861);
#22357=CIRCLE('',#103030,0.0219999999999999);
#22358=CIRCLE('',#103031,2.75);
#22359=CIRCLE('',#103032,0.022);
#22360=CIRCLE('',#103034,2.74355634918611);
#22361=CIRCLE('',#103035,0.0219999999999999);
#22362=CIRCLE('',#103036,2.75);
#22363=CIRCLE('',#103037,0.0220000000000001);
#22364=CIRCLE('',#103039,2.7435563491861);
#22365=CIRCLE('',#103040,0.0219999999999998);
#22366=CIRCLE('',#103041,2.75);
#22367=CIRCLE('',#103042,0.022);
#22368=CIRCLE('',#103044,2.7435563491861);
#22369=CIRCLE('',#103045,0.022);
#22370=CIRCLE('',#103046,2.75);
#22371=CIRCLE('',#103047,0.0219999999999999);
#22372=CIRCLE('',#103049,2.74355634918611);
#22373=CIRCLE('',#103050,0.0220000000000001);
#22374=CIRCLE('',#103051,2.75);
#22375=CIRCLE('',#103052,0.0219999999999999);
#22376=CIRCLE('',#103054,2.74355634918611);
#22377=CIRCLE('',#103055,0.0219999999999999);
#22378=CIRCLE('',#103056,2.75);
#22379=CIRCLE('',#103057,0.022);
#22380=CIRCLE('',#103059,2.7435563491861);
#22381=CIRCLE('',#103060,0.0220000000000001);
#22382=CIRCLE('',#103061,2.75);
#22383=CIRCLE('',#103062,0.0219999999999999);
#22384=CIRCLE('',#103064,2.7435563491861);
#22385=CIRCLE('',#103065,0.022);
#22386=CIRCLE('',#103066,2.75);
#22387=CIRCLE('',#103067,0.0220000000000001);
#22388=CIRCLE('',#103069,2.7435563491861);
#22389=CIRCLE('',#103070,0.022);
#22390=CIRCLE('',#103071,2.75);
#22391=CIRCLE('',#103072,0.022);
#22392=CIRCLE('',#103074,2.74355634918611);
#22393=CIRCLE('',#103075,0.0219999999999999);
#22394=CIRCLE('',#103076,2.75);
#22395=CIRCLE('',#103077,0.0220000000000001);
#22396=CIRCLE('',#103079,2.7435563491861);
#22397=CIRCLE('',#103080,0.0219999999999999);
#22398=CIRCLE('',#103081,2.75);
#22399=CIRCLE('',#103082,0.0220000000000002);
#22400=CIRCLE('',#103084,2.7435563491861);
#22401=CIRCLE('',#103085,0.022);
#22402=CIRCLE('',#103086,2.75);
#22403=CIRCLE('',#103087,0.0219999999999998);
#22404=CIRCLE('',#103089,2.7435563491861);
#22405=CIRCLE('',#103090,0.0219999999999999);
#22406=CIRCLE('',#103091,2.75);
#22407=CIRCLE('',#103092,0.0220000000000002);
#22408=CIRCLE('',#103094,2.74355634918611);
#22409=CIRCLE('',#103095,0.0219999999999999);
#22410=CIRCLE('',#103096,2.75);
#22411=CIRCLE('',#103097,0.0219999999999999);
#22412=CIRCLE('',#103099,2.7435563491861);
#22413=CIRCLE('',#103100,0.0220000000000001);
#22414=CIRCLE('',#103101,2.75);
#22415=CIRCLE('',#103102,0.0219999999999999);
#22416=CIRCLE('',#103104,2.7435563491861);
#22417=CIRCLE('',#103105,0.0219999999999999);
#22418=CIRCLE('',#103106,2.75);
#22419=CIRCLE('',#103107,0.0220000000000001);
#22420=CIRCLE('',#103109,2.7435563491861);
#22421=CIRCLE('',#103110,0.0220000000000001);
#22422=CIRCLE('',#103111,2.75);
#22423=CIRCLE('',#103112,2.75);
#22424=CIRCLE('',#103113,0.0220000000000001);
#22425=CIRCLE('',#103116,1.17524047358087);
#22426=CIRCLE('',#103118,1.62500000000006);
#22427=CIRCLE('',#103121,1.25);
#22428=CIRCLE('',#103122,1.25);
#22429=CIRCLE('',#103123,1.25);
#22430=CIRCLE('',#103124,1.25);
#22431=CIRCLE('',#103125,1.25);
#22432=CIRCLE('',#103126,1.25);
#22433=CIRCLE('',#103128,1.44337567297406);
#22434=CIRCLE('',#103130,2.55577460325564);
#22435=CIRCLE('',#103131,0.0879999999999989);
#22436=CIRCLE('',#103132,2.49354920651122);
#22437=CIRCLE('',#103134,2.72422539674443);
#22438=CIRCLE('',#103136,2.75);
#22439=CIRCLE('',#103137,0.088000000000018);
#22440=CIRCLE('',#103139,2.72422539674441);
#22441=CIRCLE('',#103140,2.72422539674441);
#22442=CIRCLE('',#103141,2.72422539674441);
#22443=CIRCLE('',#103142,2.72422539674441);
#22444=CIRCLE('',#103143,2.72422539674441);
#22445=CIRCLE('',#103144,2.72422539674441);
#22446=CIRCLE('',#103145,2.72422539674441);
#22447=CIRCLE('',#103146,2.72422539674441);
#22448=CIRCLE('',#103147,2.72422539674441);
#22449=CIRCLE('',#103148,2.72422539674441);
#22450=CIRCLE('',#103149,2.72422539674441);
#22451=CIRCLE('',#103150,2.72422539674441);
#22452=CIRCLE('',#103151,2.72422539674441);
#22453=CIRCLE('',#103152,2.72422539674441);
#22454=CIRCLE('',#103153,2.72422539674441);
#22455=CIRCLE('',#103154,2.72422539674441);
#22456=CIRCLE('',#103155,2.72422539674441);
#22457=CIRCLE('',#103156,2.72422539674441);
#22458=CIRCLE('',#103157,2.72422539674441);
#22459=CIRCLE('',#103158,2.72422539674441);
#22460=CIRCLE('',#103159,2.72422539674441);
#22461=CIRCLE('',#103160,2.72422539674441);
#22462=CIRCLE('',#103161,2.72422539674441);
#22463=CIRCLE('',#103162,2.72422539674441);
#22464=CIRCLE('',#103163,2.72422539674441);
#22465=CIRCLE('',#103164,2.72422539674441);
#22466=CIRCLE('',#103165,2.72422539674441);
#22467=CIRCLE('',#103166,2.72422539674441);
#22468=CIRCLE('',#103167,2.72422539674441);
#22469=CIRCLE('',#103168,2.72422539674441);
#22470=CIRCLE('',#103169,2.72422539674441);
#22471=CIRCLE('',#103170,2.72422539674441);
#22472=CIRCLE('',#103171,2.72422539674441);
#22473=CIRCLE('',#103172,2.72422539674441);
#22474=CIRCLE('',#103173,2.72422539674441);
#22475=CIRCLE('',#103174,2.72422539674441);
#22476=CIRCLE('',#103175,2.72422539674441);
#22477=CIRCLE('',#103176,2.72422539674441);
#22478=CIRCLE('',#103177,2.72422539674441);
#22479=CIRCLE('',#103178,2.55577460325558);
#22480=CIRCLE('',#103179,2.55577460325558);
#22481=CIRCLE('',#103180,2.72422539674441);
#22482=CIRCLE('',#103181,2.72422539674441);
#22483=CIRCLE('',#103182,2.72422539674441);
#22484=CIRCLE('',#103183,2.72422539674441);
#22485=CIRCLE('',#103184,2.72422539674441);
#22486=CIRCLE('',#103185,2.72422539674441);
#22487=CIRCLE('',#103186,2.72422539674441);
#22488=CIRCLE('',#103187,2.72422539674441);
#22489=CIRCLE('',#103188,2.72422539674441);
#22490=CIRCLE('',#103189,2.72422539674441);
#22491=CIRCLE('',#103190,2.72422539674441);
#22492=CIRCLE('',#103191,2.72422539674441);
#22493=CIRCLE('',#103192,2.72422539674441);
#22494=CIRCLE('',#103193,2.72422539674441);
#22495=CIRCLE('',#103194,2.72422539674441);
#22496=CIRCLE('',#103195,2.72422539674441);
#22497=CIRCLE('',#103196,2.72422539674441);
#22498=CIRCLE('',#103197,2.72422539674441);
#22499=CIRCLE('',#103198,2.72422539674441);
#22500=CIRCLE('',#103199,2.72422539674441);
#22501=CIRCLE('',#103200,2.72422539674441);
#22502=CIRCLE('',#103201,2.72422539674441);
#22503=CIRCLE('',#103202,2.72422539674441);
#22504=CIRCLE('',#103203,2.72422539674441);
#22505=CIRCLE('',#103204,2.72422539674441);
#22506=CIRCLE('',#103205,2.72422539674441);
#22507=CIRCLE('',#103206,2.72422539674441);
#22508=CIRCLE('',#103207,2.72422539674441);
#22509=CIRCLE('',#103208,2.72422539674441);
#22510=CIRCLE('',#103209,2.72422539674441);
#22511=CIRCLE('',#103210,2.72422539674441);
#22512=CIRCLE('',#103211,2.72422539674441);
#22513=CIRCLE('',#103212,2.72422539674441);
#22514=CIRCLE('',#103213,2.72422539674441);
#22515=CIRCLE('',#103214,2.72422539674441);
#22516=CIRCLE('',#103215,2.72422539674441);
#22517=CIRCLE('',#103216,2.72422539674441);
#22518=CIRCLE('',#103217,2.72422539674441);
#22519=CIRCLE('',#103218,2.72422539674441);
#22520=CIRCLE('',#103220,2.49354920651117);
#22521=CIRCLE('',#103221,0.0879999999999994);
#22522=CIRCLE('',#103223,2.75);
#22523=CIRCLE('',#103224,2.75);
#22524=CIRCLE('',#103225,2.75);
#22525=CIRCLE('',#103226,2.75);
#22526=CIRCLE('',#103227,2.75);
#22527=CIRCLE('',#103228,2.75);
#22528=CIRCLE('',#103229,2.75);
#22529=CIRCLE('',#103230,2.75);
#22530=CIRCLE('',#103231,2.75);
#22531=CIRCLE('',#103232,2.75);
#22532=CIRCLE('',#103233,2.75);
#22533=CIRCLE('',#103234,2.75);
#22534=CIRCLE('',#103235,2.75);
#22535=CIRCLE('',#103236,2.75);
#22536=CIRCLE('',#103237,2.75);
#22537=CIRCLE('',#103238,2.75);
#22538=CIRCLE('',#103239,2.75);
#22539=CIRCLE('',#103240,2.75);
#22540=CIRCLE('',#103241,2.75);
#22541=CIRCLE('',#103242,2.75);
#22542=CIRCLE('',#103243,2.75);
#22543=CIRCLE('',#103244,2.75);
#22544=CIRCLE('',#103245,2.75);
#22545=CIRCLE('',#103246,2.75);
#22546=CIRCLE('',#103247,2.75);
#22547=CIRCLE('',#103248,2.75);
#22548=CIRCLE('',#103249,2.75);
#22549=CIRCLE('',#103250,2.75);
#22550=CIRCLE('',#103251,2.75);
#22551=CIRCLE('',#103252,2.75);
#22552=CIRCLE('',#103253,2.75);
#22553=CIRCLE('',#103254,2.75);
#22554=CIRCLE('',#103255,2.75);
#22555=CIRCLE('',#103256,2.75);
#22556=CIRCLE('',#103257,2.75);
#22557=CIRCLE('',#103258,2.75);
#22558=CIRCLE('',#103259,2.75);
#22559=CIRCLE('',#103260,2.75);
#22560=CIRCLE('',#103261,2.75);
#22561=CIRCLE('',#103262,2.75);
#22562=CIRCLE('',#103263,2.75);
#22563=CIRCLE('',#103264,2.75);
#22564=CIRCLE('',#103265,2.75);
#22565=CIRCLE('',#103266,2.75);
#22566=CIRCLE('',#103267,2.75);
#22567=CIRCLE('',#103268,2.75);
#22568=CIRCLE('',#103269,2.75);
#22569=CIRCLE('',#103270,2.75);
#22570=CIRCLE('',#103271,2.75);
#22571=CIRCLE('',#103272,2.75);
#22572=CIRCLE('',#103273,2.75);
#22573=CIRCLE('',#103274,2.75);
#22574=CIRCLE('',#103275,2.75);
#22575=CIRCLE('',#103276,2.75);
#22576=CIRCLE('',#103277,2.75);
#22577=CIRCLE('',#103278,2.75);
#22578=CIRCLE('',#103279,2.75);
#22579=CIRCLE('',#103280,2.75);
#22580=CIRCLE('',#103281,2.75);
#22581=CIRCLE('',#103282,2.75);
#22582=CIRCLE('',#103283,2.75);
#22583=CIRCLE('',#103284,2.75);
#22584=CIRCLE('',#103285,2.75);
#22585=CIRCLE('',#103286,2.75);
#22586=CIRCLE('',#103287,2.75);
#22587=CIRCLE('',#103288,2.75);
#22588=CIRCLE('',#103289,2.75);
#22589=CIRCLE('',#103290,2.75);
#22590=CIRCLE('',#103291,2.75);
#22591=CIRCLE('',#103292,2.75);
#22592=CIRCLE('',#103293,2.75);
#22593=CIRCLE('',#103294,2.75);
#22594=CIRCLE('',#103295,2.75);
#22595=CIRCLE('',#103296,2.75);
#22596=CIRCLE('',#103297,2.75);
#22597=CIRCLE('',#103298,2.75);
#22598=CIRCLE('',#103299,2.75);
#22599=CIRCLE('',#103542,1.44337567297406);
#22600=CIRCLE('',#103543,1.44337567297406);
#22601=CIRCLE('',#103544,1.44337567297406);
#22602=CIRCLE('',#103545,1.44337567297406);
#22603=CIRCLE('',#103546,1.44337567297406);
#22604=CIRCLE('',#103566,0.0220000000000002);
#22605=CIRCLE('',#103568,0.022);
#22606=CIRCLE('',#103569,0.022);
#22607=CIRCLE('',#103570,0.0220000000000002);
#22608=CIRCLE('',#103571,0.0219999999999993);
#22609=CIRCLE('',#103572,0.0220000000000001);
#22610=CIRCLE('',#103573,0.022);
#22611=CIRCLE('',#103574,0.0220000000000001);
#22612=CIRCLE('',#103576,0.022);
#22613=CIRCLE('',#103577,0.0219999999999993);
#22614=CIRCLE('',#103585,0.0220000000000002);
#22615=CIRCLE('',#103586,0.0220000000000002);
#22616=CIRCLE('',#103588,0.022);
#22617=CIRCLE('',#103590,0.022);
#22618=CIRCLE('',#103591,0.0219999999999995);
#22619=CIRCLE('',#103592,0.022);
#22620=CIRCLE('',#103593,0.0220000000000001);
#22621=CIRCLE('',#103594,0.0219999999999995);
#22622=CIRCLE('',#103595,0.022);
#22623=CIRCLE('',#103597,0.022);
#22624=CIRCLE('',#103606,0.0220000000000002);
#22625=CIRCLE('',#103607,0.0220000000000002);
#22626=CIRCLE('',#103609,0.022);
#22627=CIRCLE('',#103611,0.022);
#22628=CIRCLE('',#103612,0.0219999999999995);
#22629=CIRCLE('',#103613,0.022);
#22630=CIRCLE('',#103614,0.022);
#22631=CIRCLE('',#103615,0.0219999999999995);
#22632=CIRCLE('',#103616,0.022);
#22633=CIRCLE('',#103618,0.022);
#22634=CIRCLE('',#103627,0.0220000000000004);
#22635=CIRCLE('',#103628,0.0220000000000004);
#22636=CIRCLE('',#103630,0.022);
#22637=CIRCLE('',#103632,0.022);
#22638=CIRCLE('',#103633,0.0219999999999993);
#22639=CIRCLE('',#103634,0.0220000000000002);
#22640=CIRCLE('',#103635,0.0220000000000002);
#22641=CIRCLE('',#103636,0.0219999999999993);
#22642=CIRCLE('',#103637,0.022);
#22643=CIRCLE('',#103639,0.022);
#22644=CIRCLE('',#103648,0.0220000000000002);
#22645=CIRCLE('',#103649,0.0220000000000002);
#22646=CIRCLE('',#103651,0.022);
#22647=CIRCLE('',#103653,0.022);
#22648=CIRCLE('',#103654,0.0219999999999996);
#22649=CIRCLE('',#103655,0.0220000000000001);
#22650=CIRCLE('',#103656,0.0220000000000001);
#22651=CIRCLE('',#103657,0.0219999999999993);
#22652=CIRCLE('',#103658,0.022);
#22653=CIRCLE('',#103660,0.022);
#22654=CIRCLE('',#103669,0.0220000000000002);
#22655=CIRCLE('',#103670,0.0220000000000002);
#22656=CIRCLE('',#103672,0.022);
#22657=CIRCLE('',#103674,0.022);
#22658=CIRCLE('',#103675,0.0219999999999993);
#22659=CIRCLE('',#103676,0.0220000000000002);
#22660=CIRCLE('',#103677,0.0220000000000002);
#22661=CIRCLE('',#103678,0.0219999999999993);
#22662=CIRCLE('',#103679,0.022);
#22663=CIRCLE('',#103681,0.0220000000000001);
#22664=CIRCLE('',#103690,0.0220000000000004);
#22665=CIRCLE('',#103691,0.0220000000000004);
#22666=CIRCLE('',#103693,0.022);
#22667=CIRCLE('',#103695,0.022);
#22668=CIRCLE('',#103696,0.0219999999999993);
#22669=CIRCLE('',#103697,0.0220000000000002);
#22670=CIRCLE('',#103698,0.0220000000000002);
#22671=CIRCLE('',#103699,0.0219999999999993);
#22672=CIRCLE('',#103700,0.022);
#22673=CIRCLE('',#103702,0.022);
#22674=CIRCLE('',#103711,0.0220000000000004);
#22675=CIRCLE('',#103712,0.0220000000000004);
#22676=CIRCLE('',#103714,0.022);
#22677=CIRCLE('',#103716,0.022);
#22678=CIRCLE('',#103717,0.0219999999999995);
#22679=CIRCLE('',#103718,0.0220000000000001);
#22680=CIRCLE('',#103719,0.0220000000000001);
#22681=CIRCLE('',#103720,0.0219999999999995);
#22682=CIRCLE('',#103721,0.022);
#22683=CIRCLE('',#103723,0.022);
#22684=CIRCLE('',#103732,0.0220000000000003);
#22685=CIRCLE('',#103733,0.0220000000000003);
#22686=CIRCLE('',#103735,0.022);
#22687=CIRCLE('',#103737,0.022);
#22688=CIRCLE('',#103738,0.0219999999999994);
#22689=CIRCLE('',#103739,0.0220000000000003);
#22690=CIRCLE('',#103740,0.0220000000000003);
#22691=CIRCLE('',#103741,0.0219999999999994);
#22692=CIRCLE('',#103742,0.022);
#22693=CIRCLE('',#103744,0.0219999999999999);
#22694=CIRCLE('',#103753,0.0220000000000003);
#22695=CIRCLE('',#103754,0.0220000000000003);
#22696=CIRCLE('',#103756,0.0219999999999999);
#22697=CIRCLE('',#103758,0.0219999999999999);
#22698=CIRCLE('',#103759,0.0219999999999994);
#22699=CIRCLE('',#103760,0.0220000000000002);
#22700=CIRCLE('',#103761,0.0220000000000002);
#22701=CIRCLE('',#103762,0.0219999999999994);
#22702=CIRCLE('',#103763,0.0219999999999999);
#22703=CIRCLE('',#103765,0.022);
#22704=CIRCLE('',#103774,0.0220000000000003);
#22705=CIRCLE('',#103775,0.0220000000000003);
#22706=CIRCLE('',#103777,0.022);
#22707=CIRCLE('',#103779,0.022);
#22708=CIRCLE('',#103780,0.0219999999999994);
#22709=CIRCLE('',#103781,0.0220000000000002);
#22710=CIRCLE('',#103782,0.0220000000000001);
#22711=CIRCLE('',#103783,0.0219999999999994);
#22712=CIRCLE('',#103784,0.022);
#22713=CIRCLE('',#103786,0.0219999999999999);
#22714=CIRCLE('',#103795,0.0220000000000003);
#22715=CIRCLE('',#103796,0.0220000000000003);
#22716=CIRCLE('',#103798,0.022);
#22717=CIRCLE('',#103800,0.022);
#22718=CIRCLE('',#103801,0.0219999999999995);
#22719=CIRCLE('',#103802,0.0220000000000001);
#22720=CIRCLE('',#103803,0.0220000000000001);
#22721=CIRCLE('',#103804,0.0219999999999995);
#22722=CIRCLE('',#103805,0.0220000000000002);
#22723=CIRCLE('',#103807,0.0219999999999999);
#22724=CIRCLE('',#103816,0.0220000000000002);
#22725=CIRCLE('',#103817,0.0220000000000002);
#22726=CIRCLE('',#103819,0.0219999999999999);
#22727=CIRCLE('',#103821,0.0219999999999999);
#22728=CIRCLE('',#103822,0.0219999999999996);
#22729=CIRCLE('',#103823,0.0220000000000001);
#22730=CIRCLE('',#103824,0.0220000000000001);
#22731=CIRCLE('',#103825,0.0219999999999996);
#22732=CIRCLE('',#103826,0.0219999999999999);
#22733=CIRCLE('',#103828,0.0220000000000001);
#22734=CIRCLE('',#103837,0.0220000000000004);
#22735=CIRCLE('',#103838,0.0220000000000004);
#22736=CIRCLE('',#103840,0.022);
#22737=CIRCLE('',#103842,0.022);
#22738=CIRCLE('',#103843,0.0219999999999994);
#22739=CIRCLE('',#103844,0.0220000000000002);
#22740=CIRCLE('',#103845,0.0220000000000002);
#22741=CIRCLE('',#103846,0.0219999999999994);
#22742=CIRCLE('',#103847,0.022);
#22743=CIRCLE('',#103849,0.022);
#22744=CIRCLE('',#103858,0.0220000000000002);
#22745=CIRCLE('',#103859,0.0220000000000002);
#22746=CIRCLE('',#103861,0.022);
#22747=CIRCLE('',#103863,0.022);
#22748=CIRCLE('',#103864,0.0219999999999994);
#22749=CIRCLE('',#103865,0.0220000000000002);
#22750=CIRCLE('',#103866,0.0220000000000002);
#22751=CIRCLE('',#103867,0.0219999999999994);
#22752=CIRCLE('',#103868,0.022);
#22753=CIRCLE('',#103870,0.022);
#22754=CIRCLE('',#103879,0.0220000000000003);
#22755=CIRCLE('',#103880,0.0220000000000003);
#22756=CIRCLE('',#103882,0.022);
#22757=CIRCLE('',#103884,0.0220000000000001);
#22758=CIRCLE('',#103885,0.0219999999999994);
#22759=CIRCLE('',#103886,0.0220000000000002);
#22760=CIRCLE('',#103887,0.0220000000000002);
#22761=CIRCLE('',#103888,0.0219999999999994);
#22762=CIRCLE('',#103889,0.0220000000000001);
#22763=CIRCLE('',#103891,0.0220000000000001);
#22764=CIRCLE('',#103900,0.0220000000000004);
#22765=CIRCLE('',#103901,0.0220000000000004);
#22766=CIRCLE('',#103903,0.022);
#22767=CIRCLE('',#103905,0.022);
#22768=CIRCLE('',#103906,0.0219999999999994);
#22769=CIRCLE('',#103907,0.0220000000000003);
#22770=CIRCLE('',#103908,0.0220000000000003);
#22771=CIRCLE('',#103909,0.0219999999999994);
#22772=CIRCLE('',#103910,0.022);
#22773=CIRCLE('',#103912,0.022);
#22774=CIRCLE('',#103921,0.0220000000000004);
#22775=CIRCLE('',#103922,0.0220000000000004);
#22776=CIRCLE('',#103924,0.022);
#22777=CIRCLE('',#103926,0.022);
#22778=CIRCLE('',#103927,0.0219999999999996);
#22779=CIRCLE('',#103928,0.0220000000000002);
#22780=CIRCLE('',#103929,0.0220000000000002);
#22781=CIRCLE('',#103930,0.0219999999999996);
#22782=CIRCLE('',#103931,0.022);
#22783=CIRCLE('',#103933,0.022);
#22784=CIRCLE('',#103942,0.0220000000000004);
#22785=CIRCLE('',#103943,0.0220000000000004);
#22786=CIRCLE('',#103945,0.022);
#22787=CIRCLE('',#103947,0.022);
#22788=CIRCLE('',#103948,0.0219999999999994);
#22789=CIRCLE('',#103949,0.0220000000000001);
#22790=CIRCLE('',#103950,0.0220000000000001);
#22791=CIRCLE('',#103951,0.0219999999999994);
#22792=CIRCLE('',#103952,0.022);
#22793=CIRCLE('',#103954,0.022);
#22794=CIRCLE('',#103963,0.0220000000000004);
#22795=CIRCLE('',#103964,0.0220000000000004);
#22796=CIRCLE('',#103966,0.022);
#22797=CIRCLE('',#103968,0.022);
#22798=CIRCLE('',#103969,0.0219999999999995);
#22799=CIRCLE('',#103970,0.0220000000000001);
#22800=CIRCLE('',#103971,0.0220000000000001);
#22801=CIRCLE('',#103972,0.0219999999999995);
#22802=CIRCLE('',#103973,0.022);
#22803=CIRCLE('',#103975,0.022);
#22804=CIRCLE('',#103984,0.0220000000000004);
#22805=CIRCLE('',#103985,0.0220000000000004);
#22806=CIRCLE('',#103987,0.0220000000000001);
#22807=CIRCLE('',#103989,0.0220000000000001);
#22808=CIRCLE('',#103990,0.0219999999999995);
#22809=CIRCLE('',#103991,0.0220000000000001);
#22810=CIRCLE('',#103992,0.0220000000000002);
#22811=CIRCLE('',#103993,0.0219999999999995);
#22812=CIRCLE('',#103994,0.0220000000000001);
#22813=CIRCLE('',#103996,0.022);
#22814=CIRCLE('',#104005,0.0220000000000002);
#22815=CIRCLE('',#104006,0.0220000000000003);
#22816=CIRCLE('',#104008,0.022);
#22817=CIRCLE('',#104010,0.022);
#22818=CIRCLE('',#104011,0.0219999999999994);
#22819=CIRCLE('',#104012,0.022);
#22820=CIRCLE('',#104013,0.0220000000000002);
#22821=CIRCLE('',#104014,0.0219999999999995);
#22822=CIRCLE('',#104015,0.022);
#22823=CIRCLE('',#104017,0.022);
#22824=CIRCLE('',#104026,0.0220000000000004);
#22825=CIRCLE('',#104027,0.0220000000000004);
#22826=CIRCLE('',#104029,0.0220000000000001);
#22827=CIRCLE('',#104031,0.0220000000000001);
#22828=CIRCLE('',#104032,0.0219999999999995);
#22829=CIRCLE('',#104033,0.0220000000000001);
#22830=CIRCLE('',#104034,0.0220000000000001);
#22831=CIRCLE('',#104035,0.0219999999999995);
#22832=CIRCLE('',#104036,0.0220000000000001);
#22833=CIRCLE('',#104038,0.022);
#22834=CIRCLE('',#104047,0.0220000000000004);
#22835=CIRCLE('',#104048,0.0220000000000004);
#22836=CIRCLE('',#104050,0.0219999999999999);
#22837=CIRCLE('',#104052,0.0219999999999999);
#22838=CIRCLE('',#104053,0.0219999999999995);
#22839=CIRCLE('',#104054,0.0220000000000001);
#22840=CIRCLE('',#104055,0.0220000000000001);
#22841=CIRCLE('',#104056,0.0219999999999995);
#22842=CIRCLE('',#104057,0.0219999999999999);
#22843=CIRCLE('',#104059,0.022);
#22844=CIRCLE('',#104068,0.0220000000000003);
#22845=CIRCLE('',#104069,0.0220000000000003);
#22846=CIRCLE('',#104071,0.0220000000000001);
#22847=CIRCLE('',#104073,0.0220000000000001);
#22848=CIRCLE('',#104074,0.0219999999999996);
#22849=CIRCLE('',#104075,0.0220000000000003);
#22850=CIRCLE('',#104076,0.0220000000000003);
#22851=CIRCLE('',#104077,0.0219999999999996);
#22852=CIRCLE('',#104078,0.0220000000000001);
#22853=CIRCLE('',#104080,0.0220000000000001);
#22854=CIRCLE('',#104089,0.0220000000000002);
#22855=CIRCLE('',#104090,0.0220000000000002);
#22856=CIRCLE('',#104092,0.022);
#22857=CIRCLE('',#104094,0.022);
#22858=CIRCLE('',#104095,0.0219999999999996);
#22859=CIRCLE('',#104096,0.0220000000000002);
#22860=CIRCLE('',#104097,0.0220000000000002);
#22861=CIRCLE('',#104098,0.0219999999999993);
#22862=CIRCLE('',#104099,0.022);
#22863=CIRCLE('',#104101,0.022);
#22864=CIRCLE('',#104110,0.0220000000000003);
#22865=CIRCLE('',#104111,0.0220000000000003);
#22866=CIRCLE('',#104113,0.0220000000000001);
#22867=CIRCLE('',#104115,0.0220000000000001);
#22868=CIRCLE('',#104116,0.0219999999999994);
#22869=CIRCLE('',#104117,0.0220000000000002);
#22870=CIRCLE('',#104118,0.0220000000000002);
#22871=CIRCLE('',#104119,0.0219999999999994);
#22872=CIRCLE('',#104120,0.0220000000000001);
#22873=CIRCLE('',#104122,0.0219999999999999);
#22874=CIRCLE('',#104131,0.0220000000000003);
#22875=CIRCLE('',#104132,0.0220000000000003);
#22876=CIRCLE('',#104134,0.022);
#22877=CIRCLE('',#104136,0.022);
#22878=CIRCLE('',#104137,0.0219999999999994);
#22879=CIRCLE('',#104138,0.0220000000000002);
#22880=CIRCLE('',#104139,0.0220000000000002);
#22881=CIRCLE('',#104140,0.0219999999999994);
#22882=CIRCLE('',#104141,0.022);
#22883=CIRCLE('',#104143,0.022);
#22884=CIRCLE('',#104152,0.0220000000000002);
#22885=CIRCLE('',#104153,0.0220000000000002);
#22886=CIRCLE('',#104155,0.022);
#22887=CIRCLE('',#104157,0.022);
#22888=CIRCLE('',#104158,0.0219999999999993);
#22889=CIRCLE('',#104159,0.0220000000000001);
#22890=CIRCLE('',#104160,0.0220000000000001);
#22891=CIRCLE('',#104161,0.0219999999999993);
#22892=CIRCLE('',#104162,0.022);
#22893=CIRCLE('',#104164,0.022);
#22894=CIRCLE('',#104173,0.0220000000000002);
#22895=CIRCLE('',#104174,0.0220000000000002);
#22896=CIRCLE('',#104176,0.022);
#22897=CIRCLE('',#104178,0.022);
#22898=CIRCLE('',#104179,0.0219999999999995);
#22899=CIRCLE('',#104180,0.0220000000000003);
#22900=CIRCLE('',#104181,0.0220000000000003);
#22901=CIRCLE('',#104182,0.0219999999999995);
#22902=CIRCLE('',#104183,0.022);
#22903=CIRCLE('',#104185,0.022);
#22904=CIRCLE('',#104194,0.0220000000000003);
#22905=CIRCLE('',#104195,0.0220000000000003);
#22906=CIRCLE('',#104197,0.022);
#22907=CIRCLE('',#104199,0.022);
#22908=CIRCLE('',#104200,0.0219999999999994);
#22909=CIRCLE('',#104201,0.0220000000000002);
#22910=CIRCLE('',#104202,0.0220000000000002);
#22911=CIRCLE('',#104203,0.0219999999999994);
#22912=CIRCLE('',#104204,0.022);
#22913=CIRCLE('',#104206,0.022);
#22914=CIRCLE('',#104215,0.0220000000000004);
#22915=CIRCLE('',#104216,0.0220000000000004);
#22916=CIRCLE('',#104218,0.022);
#22917=CIRCLE('',#104220,0.022);
#22918=CIRCLE('',#104221,0.0219999999999996);
#22919=CIRCLE('',#104222,0.0220000000000002);
#22920=CIRCLE('',#104223,0.0220000000000002);
#22921=CIRCLE('',#104224,0.0219999999999996);
#22922=CIRCLE('',#104225,0.022);
#22923=CIRCLE('',#104227,0.022);
#22924=CIRCLE('',#104236,0.0220000000000004);
#22925=CIRCLE('',#104237,0.0220000000000004);
#22926=CIRCLE('',#104239,0.022);
#22927=CIRCLE('',#104241,0.022);
#22928=CIRCLE('',#104242,0.0219999999999996);
#22929=CIRCLE('',#104243,0.0220000000000002);
#22930=CIRCLE('',#104244,0.0220000000000002);
#22931=CIRCLE('',#104245,0.0219999999999993);
#22932=CIRCLE('',#104246,0.022);
#22933=CIRCLE('',#104248,0.022);
#22934=CIRCLE('',#104257,0.0220000000000002);
#22935=CIRCLE('',#104258,0.0220000000000002);
#22936=CIRCLE('',#104260,0.022);
#22937=CIRCLE('',#104262,0.022);
#22938=CIRCLE('',#104263,0.0219999999999995);
#22939=CIRCLE('',#104264,0.0220000000000003);
#22940=CIRCLE('',#104265,0.0220000000000003);
#22941=CIRCLE('',#104266,0.0219999999999995);
#22942=CIRCLE('',#104267,0.022);
#22943=CIRCLE('',#104269,0.022);
#22944=CIRCLE('',#104278,0.0220000000000004);
#22945=CIRCLE('',#104279,0.0220000000000004);
#22946=CIRCLE('',#104281,0.022);
#22947=CIRCLE('',#104283,0.022);
#22948=CIRCLE('',#104284,0.0219999999999996);
#22949=CIRCLE('',#104285,0.0220000000000001);
#22950=CIRCLE('',#104286,0.0220000000000001);
#22951=CIRCLE('',#104287,0.0219999999999996);
#22952=CIRCLE('',#104288,0.022);
#22953=CIRCLE('',#104290,0.0220000000000001);
#22954=CIRCLE('',#104299,0.0220000000000003);
#22955=CIRCLE('',#104300,0.0220000000000003);
#22956=CIRCLE('',#104302,0.022);
#22957=CIRCLE('',#104304,0.022);
#22958=CIRCLE('',#104305,0.0219999999999996);
#22959=CIRCLE('',#104306,0.0220000000000002);
#22960=CIRCLE('',#104307,0.0220000000000002);
#22961=CIRCLE('',#104308,0.0219999999999996);
#22962=CIRCLE('',#104309,0.022);
#22963=CIRCLE('',#104311,0.022);
#22964=CIRCLE('',#104320,0.0220000000000004);
#22965=CIRCLE('',#104321,0.0220000000000004);
#22966=CIRCLE('',#104323,0.0219999999999998);
#22967=CIRCLE('',#104325,0.0219999999999998);
#22968=CIRCLE('',#104326,0.0219999999999995);
#22969=CIRCLE('',#104327,0.0220000000000002);
#22970=CIRCLE('',#104328,0.0220000000000002);
#22971=CIRCLE('',#104329,0.0219999999999995);
#22972=CIRCLE('',#104330,0.0219999999999998);
#22973=CIRCLE('',#104332,0.022);
#22974=CIRCLE('',#104341,0.0220000000000003);
#22975=CIRCLE('',#104342,0.0220000000000003);
#22976=CIRCLE('',#104344,0.022);
#22977=CIRCLE('',#104346,0.022);
#22978=CIRCLE('',#104347,0.0219999999999996);
#22979=CIRCLE('',#104348,0.0220000000000002);
#22980=CIRCLE('',#104349,0.0220000000000002);
#22981=CIRCLE('',#104350,0.0219999999999996);
#22982=CIRCLE('',#104351,0.022);
#22983=CIRCLE('',#104353,0.0219999999999999);
#22984=CIRCLE('',#104362,0.0220000000000002);
#22985=CIRCLE('',#104363,0.0220000000000002);
#22986=CIRCLE('',#104365,0.0219999999999999);
#22987=CIRCLE('',#104367,0.0219999999999999);
#22988=CIRCLE('',#104368,0.0219999999999994);
#22989=CIRCLE('',#104369,0.0220000000000001);
#22990=CIRCLE('',#104370,0.0220000000000001);
#22991=CIRCLE('',#104371,0.0219999999999994);
#22992=CIRCLE('',#104372,0.0219999999999999);
#22993=CIRCLE('',#104374,0.0219999999999998);
#22994=CIRCLE('',#104383,0.0220000000000004);
#22995=CIRCLE('',#104384,0.0220000000000004);
#22996=CIRCLE('',#104386,0.0219999999999998);
#22997=CIRCLE('',#104388,0.0219999999999998);
#22998=CIRCLE('',#104389,0.0219999999999995);
#22999=CIRCLE('',#104390,0.0220000000000003);
#23000=CIRCLE('',#104391,0.0220000000000003);
#23001=CIRCLE('',#104392,0.0219999999999995);
#23002=CIRCLE('',#104393,0.0219999999999998);
#23003=CIRCLE('',#104395,0.0219999999999999);
#23004=CIRCLE('',#104404,0.0220000000000003);
#23005=CIRCLE('',#104405,0.0220000000000003);
#23006=CIRCLE('',#104407,0.0220000000000002);
#23007=CIRCLE('',#104409,0.0220000000000002);
#23008=CIRCLE('',#104410,0.0219999999999995);
#23009=CIRCLE('',#104411,0.0220000000000001);
#23010=CIRCLE('',#104412,0.0220000000000001);
#23011=CIRCLE('',#104413,0.0219999999999995);
#23012=CIRCLE('',#104414,0.0219999999999999);
#23013=CIRCLE('',#104416,0.022);
#23014=CIRCLE('',#104425,0.0220000000000003);
#23015=CIRCLE('',#104426,0.0220000000000003);
#23016=CIRCLE('',#104428,0.0219999999999999);
#23017=CIRCLE('',#104430,0.0219999999999999);
#23018=CIRCLE('',#104431,0.0219999999999996);
#23019=CIRCLE('',#104432,0.0220000000000002);
#23020=CIRCLE('',#104433,0.0220000000000002);
#23021=CIRCLE('',#104434,0.0219999999999996);
#23022=CIRCLE('',#104435,0.0219999999999999);
#23023=CIRCLE('',#104437,0.022);
#23024=CIRCLE('',#104446,0.0220000000000003);
#23025=CIRCLE('',#104447,0.0220000000000003);
#23026=CIRCLE('',#104449,0.0220000000000001);
#23027=CIRCLE('',#104451,0.0220000000000001);
#23028=CIRCLE('',#104452,0.0219999999999995);
#23029=CIRCLE('',#104453,0.0220000000000003);
#23030=CIRCLE('',#104454,0.0220000000000003);
#23031=CIRCLE('',#104455,0.0219999999999995);
#23032=CIRCLE('',#104456,0.0220000000000001);
#23033=CIRCLE('',#104458,0.0219999999999999);
#23034=CIRCLE('',#104467,0.0220000000000004);
#23035=CIRCLE('',#104468,0.0220000000000004);
#23036=CIRCLE('',#104470,0.022);
#23037=CIRCLE('',#104472,0.022);
#23038=CIRCLE('',#104473,0.0219999999999994);
#23039=CIRCLE('',#104474,0.0220000000000001);
#23040=CIRCLE('',#104475,0.0220000000000001);
#23041=CIRCLE('',#104476,0.0219999999999994);
#23042=CIRCLE('',#104477,0.022);
#23043=CIRCLE('',#104479,0.0220000000000001);
#23044=CIRCLE('',#104488,0.0220000000000003);
#23045=CIRCLE('',#104489,0.0220000000000003);
#23046=CIRCLE('',#104491,0.0220000000000001);
#23047=CIRCLE('',#104493,0.0220000000000001);
#23048=CIRCLE('',#104494,0.0219999999999994);
#23049=CIRCLE('',#104495,0.0220000000000001);
#23050=CIRCLE('',#104496,0.0220000000000001);
#23051=CIRCLE('',#104497,0.0219999999999994);
#23052=CIRCLE('',#104498,0.0220000000000001);
#23053=CIRCLE('',#104500,0.0220000000000001);
#23054=CIRCLE('',#104509,0.0220000000000003);
#23055=CIRCLE('',#104510,0.0220000000000003);
#23056=CIRCLE('',#104512,0.022);
#23057=CIRCLE('',#104514,0.0219999999999999);
#23058=CIRCLE('',#104515,0.0219999999999994);
#23059=CIRCLE('',#104516,0.0220000000000003);
#23060=CIRCLE('',#104517,0.0220000000000003);
#23061=CIRCLE('',#104518,0.0219999999999994);
#23062=CIRCLE('',#104519,0.0219999999999999);
#23063=CIRCLE('',#104521,0.0220000000000001);
#23064=CIRCLE('',#104530,0.0220000000000002);
#23065=CIRCLE('',#104531,0.0220000000000002);
#23066=CIRCLE('',#104533,0.0219999999999999);
#23067=CIRCLE('',#104535,0.0219999999999999);
#23068=CIRCLE('',#104536,0.0219999999999994);
#23069=CIRCLE('',#104537,0.0220000000000001);
#23070=CIRCLE('',#104538,0.0220000000000001);
#23071=CIRCLE('',#104539,0.0219999999999994);
#23072=CIRCLE('',#104540,0.0219999999999999);
#23073=CIRCLE('',#104542,0.022);
#23074=CIRCLE('',#104551,0.0220000000000003);
#23075=CIRCLE('',#104552,0.0220000000000003);
#23076=CIRCLE('',#104554,0.022);
#23077=CIRCLE('',#104556,0.0220000000000001);
#23078=CIRCLE('',#104557,0.0219999999999994);
#23079=CIRCLE('',#104558,0.0220000000000001);
#23080=CIRCLE('',#104559,0.022);
#23081=CIRCLE('',#104560,0.0219999999999994);
#23082=CIRCLE('',#104561,0.022);
#23083=CIRCLE('',#104563,0.022);
#23084=CIRCLE('',#104572,0.0220000000000003);
#23085=CIRCLE('',#104573,0.0220000000000003);
#23086=CIRCLE('',#104575,0.022);
#23087=CIRCLE('',#104577,0.022);
#23088=CIRCLE('',#104578,0.0219999999999994);
#23089=CIRCLE('',#104579,0.0220000000000002);
#23090=CIRCLE('',#104580,0.0220000000000002);
#23091=CIRCLE('',#104581,0.0219999999999994);
#23092=CIRCLE('',#104582,0.022);
#23093=CIRCLE('',#104584,0.022);
#23094=CIRCLE('',#104593,0.0220000000000004);
#23095=CIRCLE('',#104594,0.0220000000000004);
#23096=CIRCLE('',#104596,0.022);
#23097=CIRCLE('',#104598,0.022);
#23098=CIRCLE('',#104599,0.0219999999999994);
#23099=CIRCLE('',#104600,0.022);
#23100=CIRCLE('',#104601,0.022);
#23101=CIRCLE('',#104602,0.0219999999999994);
#23102=CIRCLE('',#104603,0.022);
#23103=CIRCLE('',#104605,0.022);
#23104=CIRCLE('',#104614,0.0220000000000004);
#23105=CIRCLE('',#104615,0.0220000000000004);
#23106=CIRCLE('',#104617,0.022);
#23107=CIRCLE('',#104619,0.022);
#23108=CIRCLE('',#104620,0.0219999999999994);
#23109=CIRCLE('',#104621,0.022);
#23110=CIRCLE('',#104622,0.022);
#23111=CIRCLE('',#104623,0.0219999999999994);
#23112=CIRCLE('',#104624,0.022);
#23113=CIRCLE('',#104626,0.022);
#23114=CIRCLE('',#104635,0.0220000000000003);
#23115=CIRCLE('',#104636,0.0220000000000003);
#23116=CIRCLE('',#104638,0.022);
#23117=CIRCLE('',#104640,0.022);
#23118=CIRCLE('',#104641,0.0219999999999994);
#23119=CIRCLE('',#104642,0.0220000000000002);
#23120=CIRCLE('',#104643,0.0220000000000002);
#23121=CIRCLE('',#104644,0.0219999999999994);
#23122=CIRCLE('',#104645,0.022);
#23123=CIRCLE('',#104647,0.022);
#23124=CIRCLE('',#104656,0.0220000000000003);
#23125=CIRCLE('',#104657,0.0220000000000003);
#23126=CIRCLE('',#104659,0.022);
#23127=CIRCLE('',#104661,0.022);
#23128=CIRCLE('',#104662,0.0219999999999994);
#23129=CIRCLE('',#104663,0.0220000000000001);
#23130=CIRCLE('',#104664,0.0220000000000001);
#23131=CIRCLE('',#104665,0.0219999999999994);
#23132=CIRCLE('',#104666,0.022);
#23133=CIRCLE('',#104668,0.022);
#23134=CIRCLE('',#104677,0.0220000000000002);
#23135=CIRCLE('',#104678,0.0220000000000002);
#23136=CIRCLE('',#104680,0.022);
#23137=CIRCLE('',#104682,0.022);
#23138=CIRCLE('',#104683,0.0219999999999995);
#23139=CIRCLE('',#104684,0.0220000000000001);
#23140=CIRCLE('',#104685,0.0220000000000001);
#23141=CIRCLE('',#104686,0.0219999999999995);
#23142=CIRCLE('',#104687,0.022);
#23143=CIRCLE('',#104689,0.022);
#23144=CIRCLE('',#104698,0.0220000000000004);
#23145=CIRCLE('',#104699,0.0220000000000004);
#23146=CIRCLE('',#104701,0.0220000000000001);
#23147=CIRCLE('',#104703,0.0220000000000001);
#23148=CIRCLE('',#104704,0.0219999999999995);
#23149=CIRCLE('',#104705,0.022);
#23150=CIRCLE('',#104706,0.0220000000000001);
#23151=CIRCLE('',#104707,0.0219999999999995);
#23152=CIRCLE('',#104708,0.0220000000000001);
#23153=CIRCLE('',#104710,0.022);
#23154=CIRCLE('',#104719,0.0220000000000003);
#23155=CIRCLE('',#104720,0.0220000000000003);
#23156=CIRCLE('',#104722,0.0219999999999999);
#23157=CIRCLE('',#104724,0.0219999999999999);
#23158=CIRCLE('',#104725,0.0219999999999995);
#23159=CIRCLE('',#104726,0.0220000000000002);
#23160=CIRCLE('',#104727,0.0220000000000002);
#23161=CIRCLE('',#104728,0.0219999999999995);
#23162=CIRCLE('',#104729,0.0219999999999999);
#23163=CIRCLE('',#104731,0.0220000000000001);
#23164=CIRCLE('',#104740,0.0220000000000002);
#23165=CIRCLE('',#104741,0.0220000000000002);
#23166=CIRCLE('',#104743,0.0220000000000001);
#23167=CIRCLE('',#104745,0.0220000000000001);
#23168=CIRCLE('',#104746,0.0219999999999995);
#23169=CIRCLE('',#104747,0.0220000000000002);
#23170=CIRCLE('',#104748,0.0220000000000002);
#23171=CIRCLE('',#104749,0.0219999999999995);
#23172=CIRCLE('',#104750,0.0220000000000001);
#23173=CIRCLE('',#104752,0.0219999999999998);
#23174=CIRCLE('',#104761,0.0220000000000003);
#23175=CIRCLE('',#104762,0.0220000000000003);
#23176=CIRCLE('',#104764,0.0219999999999999);
#23177=CIRCLE('',#104766,0.0219999999999999);
#23178=CIRCLE('',#104767,0.0219999999999996);
#23179=CIRCLE('',#104768,0.0220000000000001);
#23180=CIRCLE('',#104769,0.0220000000000001);
#23181=CIRCLE('',#104770,0.0219999999999995);
#23182=CIRCLE('',#104771,0.0219999999999999);
#23183=CIRCLE('',#104773,0.0219999999999999);
#23184=CIRCLE('',#104782,0.0220000000000003);
#23185=CIRCLE('',#104783,0.0220000000000003);
#23186=CIRCLE('',#104785,0.022);
#23187=CIRCLE('',#104787,0.022);
#23188=CIRCLE('',#104788,0.0219999999999994);
#23189=CIRCLE('',#104789,0.0220000000000002);
#23190=CIRCLE('',#104790,0.0220000000000002);
#23191=CIRCLE('',#104791,0.0219999999999994);
#23192=CIRCLE('',#104792,0.022);
#23193=CIRCLE('',#104794,0.022);
#23194=CIRCLE('',#104803,0.0220000000000003);
#23195=CIRCLE('',#104804,0.0220000000000003);
#23196=CIRCLE('',#104806,0.022);
#23197=CIRCLE('',#104808,0.022);
#23198=CIRCLE('',#104809,0.0219999999999995);
#23199=CIRCLE('',#104810,0.0220000000000001);
#23200=CIRCLE('',#104811,0.0220000000000003);
#23201=CIRCLE('',#104812,0.0219999999999995);
#23202=CIRCLE('',#104813,0.022);
#23203=CIRCLE('',#104815,0.0219999999999999);
#23204=CIRCLE('',#104824,0.0220000000000003);
#23205=CIRCLE('',#104825,0.0220000000000003);
#23206=CIRCLE('',#104827,0.022);
#23207=CIRCLE('',#104829,0.022);
#23208=CIRCLE('',#104830,0.0219999999999994);
#23209=CIRCLE('',#104831,0.0220000000000002);
#23210=CIRCLE('',#104832,0.0220000000000002);
#23211=CIRCLE('',#104833,0.0219999999999994);
#23212=CIRCLE('',#104834,0.022);
#23213=CIRCLE('',#104836,0.022);
#23214=CIRCLE('',#104845,0.0220000000000004);
#23215=CIRCLE('',#104846,0.0220000000000004);
#23216=CIRCLE('',#104848,0.0220000000000001);
#23217=CIRCLE('',#104850,0.0220000000000001);
#23218=CIRCLE('',#104851,0.0219999999999993);
#23219=CIRCLE('',#104852,0.0220000000000003);
#23220=CIRCLE('',#104853,0.0220000000000003);
#23221=CIRCLE('',#104854,0.0219999999999993);
#23222=CIRCLE('',#104855,0.0220000000000001);
#23223=CIRCLE('',#104857,0.0219999999999999);
#23224=CIRCLE('',#104866,0.0220000000000002);
#23225=CIRCLE('',#104867,0.0220000000000002);
#23226=CIRCLE('',#104869,0.022);
#23227=CIRCLE('',#104871,0.022);
#23228=CIRCLE('',#104872,0.0219999999999995);
#23229=CIRCLE('',#104873,0.0220000000000002);
#23230=CIRCLE('',#104874,0.0220000000000002);
#23231=CIRCLE('',#104875,0.0219999999999995);
#23232=CIRCLE('',#104876,0.022);
#23233=CIRCLE('',#104878,0.022);
#23234=CIRCLE('',#104887,0.0220000000000003);
#23235=CIRCLE('',#104888,0.0220000000000003);
#23236=CIRCLE('',#104890,0.022);
#23237=CIRCLE('',#104892,0.022);
#23238=CIRCLE('',#104893,0.0219999999999995);
#23239=CIRCLE('',#104894,0.0220000000000002);
#23240=CIRCLE('',#104895,0.0220000000000002);
#23241=CIRCLE('',#104896,0.0219999999999994);
#23242=CIRCLE('',#104897,0.022);
#23243=CIRCLE('',#104899,0.022);
#23244=CIRCLE('',#104908,0.0220000000000002);
#23245=CIRCLE('',#104909,0.0220000000000002);
#23246=CIRCLE('',#104911,0.0219999999999999);
#23247=CIRCLE('',#104913,0.022);
#23248=CIRCLE('',#104914,0.0219999999999995);
#23249=CIRCLE('',#104915,0.0220000000000002);
#23250=CIRCLE('',#104916,0.0220000000000002);
#23251=CIRCLE('',#104917,0.0219999999999995);
#23252=CIRCLE('',#104918,0.022);
#23253=CIRCLE('',#104920,0.022);
#23254=CIRCLE('',#104929,0.0220000000000004);
#23255=CIRCLE('',#104930,0.0220000000000004);
#23256=CIRCLE('',#104932,0.0220000000000001);
#23257=CIRCLE('',#104934,0.0220000000000001);
#23258=CIRCLE('',#104935,0.0219999999999995);
#23259=CIRCLE('',#104936,0.0220000000000001);
#23260=CIRCLE('',#104937,0.022);
#23261=CIRCLE('',#104938,0.0219999999999995);
#23262=CIRCLE('',#104939,0.0220000000000001);
#23263=CIRCLE('',#104941,0.022);
#23264=CIRCLE('',#104950,0.0220000000000004);
#23265=CIRCLE('',#104951,0.0220000000000004);
#23266=CIRCLE('',#104953,0.022);
#23267=CIRCLE('',#104955,0.022);
#23268=CIRCLE('',#104956,0.0219999999999995);
#23269=CIRCLE('',#104957,0.0220000000000002);
#23270=CIRCLE('',#104958,0.0220000000000002);
#23271=CIRCLE('',#104959,0.0219999999999995);
#23272=CIRCLE('',#104960,0.022);
#23273=CIRCLE('',#104962,0.022);
#23274=CIRCLE('',#104971,0.0220000000000004);
#23275=CIRCLE('',#104972,0.0220000000000004);
#23276=CIRCLE('',#104974,0.022);
#23277=CIRCLE('',#104976,0.022);
#23278=CIRCLE('',#104977,0.0219999999999996);
#23279=CIRCLE('',#104978,0.0220000000000002);
#23280=CIRCLE('',#104979,0.0220000000000002);
#23281=CIRCLE('',#104980,0.0219999999999996);
#23282=CIRCLE('',#104981,0.022);
#23283=CIRCLE('',#104983,0.022);
#23284=CIRCLE('',#104992,0.0220000000000004);
#23285=CIRCLE('',#104993,0.0220000000000004);
#23286=CIRCLE('',#104995,0.022);
#23287=CIRCLE('',#104997,0.022);
#23288=CIRCLE('',#104998,0.0219999999999996);
#23289=CIRCLE('',#104999,0.0220000000000002);
#23290=CIRCLE('',#105000,0.0220000000000002);
#23291=CIRCLE('',#105001,0.0219999999999996);
#23292=CIRCLE('',#105002,0.022);
#23293=CIRCLE('',#105004,0.022);
#23294=CIRCLE('',#105013,0.0220000000000003);
#23295=CIRCLE('',#105014,0.0220000000000003);
#23296=CIRCLE('',#105016,0.022);
#23297=CIRCLE('',#105018,0.022);
#23298=CIRCLE('',#105019,0.0219999999999994);
#23299=CIRCLE('',#105020,0.0220000000000002);
#23300=CIRCLE('',#105021,0.0220000000000002);
#23301=CIRCLE('',#105022,0.0219999999999994);
#23302=CIRCLE('',#105023,0.022);
#23303=CIRCLE('',#105025,0.022);
#23304=CIRCLE('',#105034,0.0220000000000003);
#23305=CIRCLE('',#105035,0.0220000000000003);
#23306=CIRCLE('',#105037,0.022);
#23307=CIRCLE('',#105039,0.022);
#23308=CIRCLE('',#105040,0.0219999999999995);
#23309=CIRCLE('',#105041,0.0220000000000003);
#23310=CIRCLE('',#105042,0.0220000000000003);
#23311=CIRCLE('',#105043,0.0219999999999995);
#23312=CIRCLE('',#105044,0.022);
#23313=CIRCLE('',#105046,0.022);
#23314=CIRCLE('',#105055,0.0220000000000002);
#23315=CIRCLE('',#105056,0.0220000000000002);
#23316=CIRCLE('',#105058,0.022);
#23317=CIRCLE('',#105060,0.022);
#23318=CIRCLE('',#105061,0.0219999999999994);
#23319=CIRCLE('',#105062,0.0220000000000001);
#23320=CIRCLE('',#105063,0.0220000000000001);
#23321=CIRCLE('',#105064,0.0219999999999994);
#23322=CIRCLE('',#105065,0.022);
#23323=CIRCLE('',#105067,0.022);
#23324=CIRCLE('',#105076,0.0220000000000004);
#23325=CIRCLE('',#105077,0.0220000000000004);
#23326=CIRCLE('',#105079,0.022);
#23327=CIRCLE('',#105081,0.022);
#23328=CIRCLE('',#105082,0.0219999999999994);
#23329=CIRCLE('',#105083,0.0220000000000003);
#23330=CIRCLE('',#105084,0.0220000000000003);
#23331=CIRCLE('',#105085,0.0219999999999994);
#23332=CIRCLE('',#105086,0.022);
#23333=CIRCLE('',#105088,0.022);
#23334=CIRCLE('',#105097,0.0220000000000003);
#23335=CIRCLE('',#105098,0.0220000000000003);
#23336=CIRCLE('',#105100,0.0219999999999999);
#23337=CIRCLE('',#105102,0.022);
#23338=CIRCLE('',#105103,0.0219999999999995);
#23339=CIRCLE('',#105104,0.0220000000000002);
#23340=CIRCLE('',#105105,0.0220000000000002);
#23341=CIRCLE('',#105106,0.0219999999999995);
#23342=CIRCLE('',#105107,0.022);
#23343=CIRCLE('',#105109,0.0219999999999999);
#23344=CIRCLE('',#105118,0.0220000000000002);
#23345=CIRCLE('',#105119,0.0220000000000002);
#23346=CIRCLE('',#105121,0.022);
#23347=CIRCLE('',#105123,0.022);
#23348=CIRCLE('',#105124,0.0219999999999994);
#23349=CIRCLE('',#105125,0.0220000000000003);
#23350=CIRCLE('',#105126,0.0220000000000003);
#23351=CIRCLE('',#105127,0.0219999999999994);
#23352=CIRCLE('',#105128,0.022);
#23353=CIRCLE('',#105130,0.022);
#23354=CIRCLE('',#105139,0.0220000000000004);
#23355=CIRCLE('',#105140,0.0220000000000004);
#23356=CIRCLE('',#105142,0.0219999999999999);
#23357=CIRCLE('',#105144,0.0219999999999999);
#23358=CIRCLE('',#105145,0.0219999999999994);
#23359=CIRCLE('',#105146,0.0220000000000003);
#23360=CIRCLE('',#105147,0.0220000000000003);
#23361=CIRCLE('',#105148,0.0219999999999994);
#23362=CIRCLE('',#105149,0.0219999999999999);
#23363=CIRCLE('',#105151,0.0220000000000001);
#23364=CIRCLE('',#105160,0.0220000000000002);
#23365=CIRCLE('',#105161,0.0220000000000002);
#23366=CIRCLE('',#105163,0.022);
#23367=CIRCLE('',#105165,0.022);
#23368=CIRCLE('',#105166,0.0219999999999996);
#23369=CIRCLE('',#105167,0.0220000000000002);
#23370=CIRCLE('',#105168,0.0220000000000002);
#23371=CIRCLE('',#105169,0.0219999999999995);
#23372=CIRCLE('',#105170,0.022);
#23373=CIRCLE('',#105172,0.0220000000000001);
#25853=B_SPLINE_CURVE_WITH_KNOTS('',3,(#410687,#410688,#410689,#410690,
#410691,#410692,#410693,#410694,#410695,#410696,#410697,#410698,#410699,
#410700),.UNSPECIFIED.,.F.,.F.,(4,2,2,2,2,2,4),(9.99952789110385E-7,0.0186719180275584,
0.0311918990740491,0.0543270273300624,0.071245591780139,0.0801745768203788,
0.0885356940042009),.UNSPECIFIED.);
#25854=B_SPLINE_CURVE_WITH_KNOTS('',3,(#410703,#410704,#410705,#410706,
#410707,#410708,#410709,#410710,#410711,#410712),.UNSPECIFIED.,.F.,.F.,
(4,2,2,2,4),(0.,0.0261563177202213,0.0514794122059591,0.0956126325182896,
0.112636617654083),.UNSPECIFIED.);
#25855=B_SPLINE_CURVE_WITH_KNOTS('',3,(#410717,#410718,#410719,#410720,
#410721,#410722,#410723,#410724,#410725,#410726,#410727,#410728,#410729,
#410730,#410731,#410732,#410733,#410734,#410735,#410736),.UNSPECIFIED.,
 .F.,.F.,(4,2,2,2,2,2,2,2,2,4),(-0.318111909131838,-0.302523038044006,-0.254842438467261,
-0.203675597428167,-0.169345881177067,-0.144533555287107,-0.118262221883461,
-0.0861048668116298,-0.0439870055810665,0.),.UNSPECIFIED.);
#25856=B_SPLINE_CURVE_WITH_KNOTS('',3,(#410743,#410744,#410745,#410746,
#410747,#410748,#410749,#410750,#410751,#410752,#410753,#410754,#410755,
#410756,#410757,#410758,#410759,#410760),.UNSPECIFIED.,.F.,.F.,(4,2,2,2,
2,2,2,2,4),(-0.448684784030478,-0.402273095639563,-0.343067075576419,-0.285995793781911,
-0.226278926910573,-0.167718843647999,-0.110407379121187,-0.0552345699471347,
-1.00000016339807E-6),.UNSPECIFIED.);
#25857=B_SPLINE_CURVE_WITH_KNOTS('',3,(#410763,#410764,#410765,#410766,
#410767,#410768,#410769,#410770,#410771,#410772,#410773,#410774,#410775,
#410776,#410777,#410778),.UNSPECIFIED.,.F.,.F.,(4,2,2,2,2,2,2,4),(-29.252097766018,
-29.2214975192493,-29.1900261579108,-29.1309979348172,-29.0708070130408,
-29.0132351605879,-28.9534122905398,-28.9187969711258),.UNSPECIFIED.);
#25858=B_SPLINE_CURVE_WITH_KNOTS('',3,(#410783,#410784,#410785,#410786,
#410787,#410788,#410789,#410790,#410791,#410792,#410793,#410794,#410795,
#410796,#410797,#410798,#410799,#410800,#410801,#410802,#410803,#410804,
#410805,#410806,#410807,#410808,#410809,#410810,#410811,#410812,#410813,
#410814,#410815,#410816,#410817,#410818),.UNSPECIFIED.,.F.,.F.,(4,2,2,2,
2,2,2,2,2,2,2,2,2,2,2,2,2,4),(-1.39493487964975,-1.33933536140023,-1.28047085435749,
-1.22343374849274,-1.16371361805528,-1.10549950745885,-1.04770400873729,
-0.987904720665793,-0.930362048538481,-0.870679137285274,-0.811661333086154,
-0.75465483523098,-0.694950459322707,-0.636580836693497,-0.579072284415414,
-0.51909849981813,-0.461399377221561,-0.448684784030478),.UNSPECIFIED.);
#25859=B_SPLINE_CURVE_WITH_KNOTS('',3,(#410819,#410820,#410821,#410822,
#410823,#410824,#410825,#410826,#410827,#410828,#410829,#410830,#410831,
#410832,#410833,#410834,#410835,#410836,#410837,#410838,#410839,#410840,
#410841,#410842,#410843,#410844,#410845,#410846,#410847,#410848,#410849,
#410850,#410851,#410852,#410853,#410854),.UNSPECIFIED.,.F.,.F.,(4,2,2,2,
2,2,2,2,2,2,2,2,2,2,2,2,2,4),(-28.9187969711258,-28.8952823866813,-28.8370354169342,
-28.7771755690868,-28.7199637678638,-28.6610635136513,-28.6012229559858,
-28.5437786457582,-28.484099470417,-28.4254825927288,-28.3673557383989,
-28.3069171786156,-28.2495271665763,-28.1907246371527,-28.1308478746926,
-28.0735736519825,-28.014124865578,-27.9698505015162),.UNSPECIFIED.);
#25860=B_SPLINE_CURVE_WITH_KNOTS('',3,(#410859,#410860,#410861,#410862,
#410863,#410864,#410865,#410866,#410867,#410868,#410869,#410870,#410871,
#410872,#410873,#410874,#410875,#410876,#410877,#410878,#410879,#410880,
#410881,#410882,#410883,#410884,#410885,#410886,#410887,#410888,#410889,
#410890,#410891,#410892,#410893,#410894,#410895,#410896),.UNSPECIFIED.,
 .F.,.F.,(4,2,2,2,2,2,2,2,2,2,2,2,2,2,2,2,2,2,4),(-2.34124852806073,-2.33690126303019,
-2.27724350495715,-2.21871612127065,-2.16148516986521,-2.10133374186191,
-2.04347846587669,-1.98493722241918,-1.92554377967373,-1.86833924331538,
-1.80863346889893,-1.74988209422244,-1.69273225729192,-1.6329697831651,
-1.57487144052691,-1.51672143261483,-1.45705664513422,-1.39963367235311,
-1.39493487964975),.UNSPECIFIED.);
#25861=B_SPLINE_CURVE_WITH_KNOTS('',3,(#410897,#410898,#410899,#410900,
#410901,#410902,#410903,#410904,#410905,#410906,#410907,#410908,#410909,
#410910,#410911,#410912,#410913,#410914,#410915,#410916,#410917,#410918,
#410919,#410920,#410921,#410922,#410923,#410924,#410925,#410926,#410927,
#410928,#410929,#410930,#410931,#410932),.UNSPECIFIED.,.F.,.F.,(4,2,2,2,
2,2,2,2,2,2,2,2,2,2,2,2,2,4),(-27.9698505015162,-27.955092905267,-27.8971690368431,
-27.8369554028138,-27.7794155920712,-27.720819041241,-27.6609693585283,
-27.603807699935,-27.5445624577898,-27.4850125493338,-27.4272615418296,
-27.367240259664,-27.3094538969521,-27.2510306695638,-27.1911785131228,
-27.1340307959517,-27.0749567020895,-27.0213445386482),.UNSPECIFIED.);
#25862=B_SPLINE_CURVE_WITH_KNOTS('',3,(#410937,#410938,#410939,#410940,
#410941,#410942,#410943,#410944,#410945,#410946,#410947,#410948,#410949,
#410950,#410951,#410952,#410953,#410954,#410955,#410956,#410957,#410958,
#410959,#410960,#410961,#410962,#410963,#410964,#410965,#410966,#410967,
#410968,#410969,#410970,#410971,#410972),.UNSPECIFIED.,.F.,.F.,(4,2,2,2,
2,2,2,2,2,2,2,2,2,2,2,2,2,4),(-3.28643685670557,-3.27350661120751,-3.21586205750387,
-3.15594429548082,-3.098512889948,-3.0401985470805,-2.98056057243175,-2.92361641153634,
-2.86465472519906,-2.8050704439123,-2.74758405487526,-2.68784265002696,
-2.63012907375782,-2.57197212213701,-2.5123199119751,-2.455350141073,-2.39654364425808,
-2.34124852806073),.UNSPECIFIED.);
#25863=B_SPLINE_CURVE_WITH_KNOTS('',3,(#410973,#410974,#410975,#410976,
#410977,#410978,#410979,#410980,#410981,#410982,#410983,#410984,#410985,
#410986,#410987,#410988,#410989,#410990,#410991,#410992,#410993,#410994,
#410995,#410996,#410997,#410998,#410999,#411000,#411001,#411002,#411003,
#411004,#411005,#411006,#411007,#411008,#411009,#411010),.UNSPECIFIED.,
 .F.,.F.,(4,2,2,2,2,2,2,2,2,2,2,2,2,2,2,2,2,2,4),(-27.0213445386482,-27.0148137389868,
-26.9572008257476,-26.8973340689325,-26.8392212916929,-26.7809336352533,
-26.7210515782496,-26.6638279821658,-26.6048870671248,-26.5450228255409,
-26.4875402157774,-26.4278201148169,-26.3692342439642,-26.3110698385162,
-26.2505905031186,-26.1932005595953,-26.1343598543634,-26.0744661565355,
-26.0721220179853),.UNSPECIFIED.);
#25864=B_SPLINE_CURVE_WITH_KNOTS('',3,(#411015,#411016,#411017,#411018,
#411019,#411020,#411021,#411022,#411023,#411024,#411025,#411026,#411027,
#411028,#411029,#411030,#411031,#411032,#411033,#411034,#411035,#411036,
#411037,#411038,#411039,#411040,#411041,#411042,#411043,#411044,#411045,
#411046,#411047,#411048,#411049,#411050),.UNSPECIFIED.,.F.,.F.,(4,2,2,2,
2,2,2,2,2,2,2,2,2,2,2,2,2,4),(-4.23227875089979,-4.19308958251698,-4.15252126808739,
-4.09276835801667,-4.03561843556799,-3.97689033723292,-3.91719298824817,
-3.86001020997198,-3.80063980222867,-3.74206692752785,-3.68423228988271,
-3.62410352474105,-3.56686359207517,-3.50835716243747,-3.44870502120367,
-3.39169065880464,-3.33253914286054,-3.28643685670557),.UNSPECIFIED.);
#25865=B_SPLINE_CURVE_WITH_KNOTS('',3,(#411051,#411052,#411053,#411054,
#411055,#411056,#411057,#411058,#411059,#411060,#411061,#411062,#411063,
#411064,#411065,#411066,#411067,#411068,#411069,#411070,#411071,#411072,
#411073,#411074,#411075,#411076,#411077,#411078,#411079,#411080,#411081,
#411082,#411083,#411084,#411085,#411086),.UNSPECIFIED.,.F.,.F.,(4,2,2,2,
2,2,2,2,2,2,2,2,2,2,2,2,2,4),(-26.0721220179853,-26.017160626507,-25.9576738740858,
-25.8986866001961,-25.8407285543548,-25.7804777660194,-25.7229503409938,
-25.6643192415877,-25.6044563774412,-25.5472754027841,-25.487995756455,
-25.4285015946258,-25.3707203304554,-25.3106661519921,-25.2529032223508,
-25.1944497076039,-25.1345878127328,-25.1233625871879),.UNSPECIFIED.);
#25866=B_SPLINE_CURVE_WITH_KNOTS('',3,(#411091,#411092,#411093,#411094,
#411095,#411096,#411097,#411098,#411099,#411100,#411101,#411102,#411103,
#411104,#411105,#411106,#411107,#411108,#411109,#411110,#411111,#411112,
#411113,#411114,#411115,#411116,#411117,#411118,#411119,#411120,#411121,
#411122,#411123,#411124,#411125,#411126),.UNSPECIFIED.,.F.,.F.,(4,2,2,2,
2,2,2,2,2,2,2,2,2,2,2,2,2,4),(-0.944730488315757,-0.89891383387179,-0.839824556627243,
-0.78287389958975,-0.723293190895891,-0.664848091483223,-0.60768489144294,
-0.547618518959442,-0.489844548217535,-0.431362885084828,-0.372053706579833,
-0.31493020374114,-0.255302759125205,-0.196634951286046,-0.13955662032141,
-0.079873041517757,-0.0392464748727053,-9.99999999806711E-7),
 .UNSPECIFIED.);
#25867=B_SPLINE_CURVE_WITH_KNOTS('',3,(#411127,#411128,#411129,#411130,
#411131,#411132,#411133,#411134,#411135,#411136,#411137,#411138,#411139,
#411140,#411141,#411142,#411143,#411144,#411145,#411146,#411147,#411148,
#411149,#411150,#411151,#411152,#411153,#411154,#411155,#411156,#411157,
#411158,#411159,#411160,#411161,#411162),.UNSPECIFIED.,.F.,.F.,(4,2,2,2,
2,2,2,2,2,2,2,2,2,2,2,2,2,4),(-25.1233625871879,-25.0774324454709,-25.0183282037482,
-24.9582481821066,-24.9006094766757,-24.840714684202,-24.7826335346738,
-24.7243204209327,-24.6644318447055,-24.6072106427378,-24.5482444597356,
-24.4883721594139,-24.4308662178888,-24.3711207220799,-24.3125804351149,
-24.2543935715963,-24.1938891267832,-24.1742281370664),.UNSPECIFIED.);
#25868=B_SPLINE_CURVE_WITH_KNOTS('',3,(#411167,#411168,#411169,#411170,
#411171,#411172,#411173,#411174,#411175,#411176,#411177,#411178,#411179,
#411180,#411181,#411182,#411183,#411184,#411185,#411186,#411187,#411188,
#411189,#411190,#411191,#411192,#411193,#411194,#411195,#411196,#411197,
#411198,#411199,#411200,#411201,#411202),.UNSPECIFIED.,.F.,.F.,(4,2,2,2,
2,2,2,2,2,2,2,2,2,2,2,2,2,4),(-1.88876307323747,-1.83374485867437,-1.77500354530042,
-1.71810670339158,-1.65852871296345,-1.60043603772057,-1.54280856206037,
-1.48313244688252,-1.42570940700207,-1.3662265269564,-1.30732839246978,
-1.25045268050273,-1.19088756813138,-1.13263588100429,-1.07528621171883,
-1.01543214034352,-0.957849461381783,-0.944730488315757),.UNSPECIFIED.);
#25869=B_SPLINE_CURVE_WITH_KNOTS('',3,(#411203,#411204,#411205,#411206,
#411207,#411208,#411209,#411210,#411211,#411212,#411213,#411214,#411215,
#411216,#411217,#411218,#411219,#411220,#411221,#411222,#411223,#411224,
#411225,#411226,#411227,#411228,#411229,#411230,#411231,#411232,#411233,
#411234,#411235,#411236,#411237,#411238),.UNSPECIFIED.,.F.,.F.,(4,2,2,2,
2,2,2,2,2,2,2,2,2,2,2,2,2,4),(-24.1742281370664,-24.1365133939231,-24.0776497602422,
-24.0177548187665,-23.9604318660005,-23.900922584465,-23.8419950479497,
-23.784017836623,-23.7237454632829,-23.6662448206979,-23.6075943276575,
-23.5477340504698,-23.490547683915,-23.431248972548,-23.3718262730906,-23.3140296905872,
-23.2539581003242,-23.2253117019651),.UNSPECIFIED.);
#25870=B_SPLINE_CURVE_WITH_KNOTS('',3,(#411243,#411244,#411245,#411246,
#411247,#411248,#411249,#411250,#411251,#411252,#411253,#411254,#411255,
#411256,#411257,#411258,#411259,#411260,#411261,#411262,#411263,#411264,
#411265,#411266,#411267,#411268,#411269,#411270,#411271,#411272,#411273,
#411274,#411275,#411276,#411277,#411278,#411279,#411280),.UNSPECIFIED.,
 .F.,.F.,(4,2,2,2,2,2,2,2,2,2,2,2,2,2,2,2,2,2,4),(-2.83384756662789,-2.82992577270359,
-2.77028071294861,-2.71174863608066,-2.65454520039306,-2.59438770365034,
-2.53652788636405,-2.47803964435339,-2.41863952240411,-2.3614616687963,
-2.30186610646549,-2.24324200557333,-2.18624034144377,-2.12662278956109,
-2.0686498962575,-2.01067448075632,-1.95113688511984,-1.89383724909564,
-1.88876307323747),.UNSPECIFIED.);
#25871=B_SPLINE_CURVE_WITH_KNOTS('',3,(#411281,#411282,#411283,#411284,
#411285,#411286,#411287,#411288,#411289,#411290,#411291,#411292,#411293,
#411294,#411295,#411296,#411297,#411298,#411299,#411300,#411301,#411302,
#411303,#411304,#411305,#411306,#411307,#411308,#411309,#411310,#411311,
#411312,#411313,#411314,#411315,#411316),.UNSPECIFIED.,.F.,.F.,(4,2,2,2,
2,2,2,2,2,2,2,2,2,2,2,2,2,4),(-23.2253117019651,-23.1962333650746,-23.1377646400003,
-23.07790884712,-23.0207599950722,-22.9616408595193,-22.901640253111,-22.8439906425578,
-22.7840832422152,-22.7260491100111,-22.6677255703613,-22.607846381989,
-22.5506421242094,-22.4916658766836,-22.4318013315578,-22.3742868685931,
-22.3145313196031,-22.2764817495763),.UNSPECIFIED.);
#25872=B_SPLINE_CURVE_WITH_KNOTS('',3,(#411321,#411322,#411323,#411324,
#411325,#411326,#411327,#411328,#411329,#411330,#411331,#411332,#411333,
#411334,#411335,#411336,#411337,#411338,#411339,#411340,#411341,#411342,
#411343,#411344,#411345,#411346,#411347,#411348,#411349,#411350,#411351,
#411352,#411353,#411354,#411355,#411356),.UNSPECIFIED.,.F.,.F.,(4,2,2,2,
2,2,2,2,2,2,2,2,2,2,2,2,2,4),(-3.77882842551939,-3.76608750396215,-3.70645290327603,
-3.64828276634858,-3.59063907211679,-3.53088137745131,-3.47338129154192,
-3.41391599771162,-3.35493498255763,-3.29799778855135,-3.23837239214353,
-3.18003818569917,-3.12266132771161,-3.06272059889875,-3.00505620957078,
-2.94612783742944,-2.88695126997501,-2.83384756662789),.UNSPECIFIED.);
#25873=B_SPLINE_CURVE_WITH_KNOTS('',3,(#411357,#411358,#411359,#411360,
#411361,#411362,#411363,#411364,#411365,#411366,#411367,#411368,#411369,
#411370,#411371,#411372,#411373,#411374,#411375,#411376,#411377,#411378,
#411379,#411380,#411381,#411382,#411383,#411384,#411385,#411386,#411387,
#411388,#411389,#411390,#411391,#411392),.UNSPECIFIED.,.F.,.F.,(4,2,2,2,
2,2,2,2,2,2,2,2,2,2,2,2,2,4),(-22.2764817495763,-22.2560524818532,-22.1978581171903,
-22.1373440487818,-22.0799972717364,-22.0211258149661,-21.9612456561173,
-21.9039190783511,-21.8444025770243,-21.7855514269224,-21.7275699960986,
-21.6672915008503,-21.6098329067871,-21.5511781074627,-21.4913366101491,
-21.4341589326486,-21.3748564408681,-21.3276223997873),.UNSPECIFIED.);
#25874=B_SPLINE_CURVE_WITH_KNOTS('',3,(#411397,#411398,#411399,#411400,
#411401,#411402,#411403,#411404,#411405,#411406,#411407,#411408,#411409,
#411410,#411411,#411412,#411413,#411414,#411415,#411416,#411417,#411418,
#411419,#411420,#411421,#411422,#411423,#411424,#411425,#411426,#411427,
#411428,#411429,#411430,#411431,#411432),.UNSPECIFIED.,.F.,.F.,(4,2,2,2,
2,2,2,2,2,2,2,2,2,2,2,2,2,4),(-4.72451512913708,-4.70335422218615,-4.64312396621101,
-4.58519588309839,-4.52671311480439,-4.46724031581326,-4.40999362694196,
-4.35034348430204,-4.29164723103953,-4.23460643249447,-4.1749357076431,
-4.11689093893578,-4.05890677016987,-3.99929325395434,-3.94192176952015,
-3.88185265443699,-3.82303353231637,-3.77882842551939),.UNSPECIFIED.);
#25875=B_SPLINE_CURVE_WITH_KNOTS('',3,(#411433,#411434,#411435,#411436,
#411437,#411438,#411439,#411440,#411441,#411442,#411443,#411444,#411445,
#411446,#411447,#411448,#411449,#411450,#411451,#411452,#411453,#411454,
#411455,#411456,#411457,#411458,#411459,#411460,#411461,#411462,#411463,
#411464,#411465,#411466,#411467,#411468),.UNSPECIFIED.,.F.,.F.,(4,2,2,2,
2,2,2,2,2,2,2,2,2,2,2,2,2,4),(-21.3276223997873,-21.315522792052,-21.2577258448043,
-21.1976523083246,-21.1399816112249,-21.0815127725348,-21.0216794298315,
-20.9645516701281,-20.905432926813,-20.8455302924166,-20.7878847716901,
-20.7279802727358,-20.6700098901345,-20.6116910755317,-20.5518377670118,
-20.494665655196,-20.4356946787015,-20.3793176857869),.UNSPECIFIED.);
#25876=B_SPLINE_CURVE_WITH_KNOTS('',3,(#411473,#411474,#411475,#411476,
#411477,#411478,#411479,#411480,#411481,#411482,#411483,#411484,#411485,
#411486,#411487,#411488,#411489,#411490,#411491,#411492,#411493,#411494,
#411495,#411496,#411497,#411498,#411499,#411500,#411501,#411502,#411503,
#411504,#411505,#411506,#411507,#411508),.UNSPECIFIED.,.F.,.F.,(4,2,2,2,
2,2,2,2,2,2,2,2,2,2,2,2,2,4),(-5.6703237369621,-5.6401640324469,-5.58034229299679,
-5.52278198432739,-5.46334602502765,-5.40429963955564,-5.34731581221613,
-5.28764667344074,-5.22924728617809,-5.17185644587178,-5.1118469911605,
-5.05411807632568,-4.99520867883528,-4.93596276363503,-4.87887805740263,
-4.81918542463239,-4.76058413611294,-4.72451512913708),.UNSPECIFIED.);
#25877=B_SPLINE_CURVE_WITH_KNOTS('',3,(#411509,#411510,#411511,#411512,
#411513,#411514,#411515,#411516,#411517,#411518,#411519,#411520,#411521,
#411522,#411523,#411524,#411525,#411526,#411527,#411528,#411529,#411530,
#411531,#411532,#411533,#411534,#411535,#411536,#411537,#411538,#411539,
#411540,#411541,#411542,#411543,#411544,#411545,#411546),.UNSPECIFIED.,
 .F.,.F.,(4,2,2,2,2,2,2,2,2,2,2,2,2,2,2,2,2,2,4),(-20.3793176857869,-20.3758542519859,
-20.3183462325325,-20.258596103042,-20.2001962515831,-20.1420095197077,
-20.0815014526744,-20.0241992831074,-19.965335281199,-19.9054866447767,
-19.8481703716897,-19.7886621540349,-19.7299060833526,-19.6719356291545,
-19.6116666905878,-19.5542666265083,-19.4956228575489,-19.4358171532103,
-19.430746292065),.UNSPECIFIED.);
#25878=B_SPLINE_CURVE_WITH_KNOTS('',3,(#411551,#411552,#411553,#411554,
#411555,#411556,#411557,#411558,#411559,#411560,#411561,#411562,#411563,
#411564,#411565,#411566,#411567,#411568,#411569,#411570,#411571,#411572,
#411573,#411574,#411575,#411576,#411577,#411578,#411579,#411580,#411581,
#411582,#411583,#411584,#411585,#411586),.UNSPECIFIED.,.F.,.F.,(4,2,2,2,
2,2,2,2,2,2,2,2,2,2,2,2,2,4),(-6.61638032040915,-6.57683132059212,-6.51730270007273,
-6.46000337416112,-6.40031485620181,-6.3415631731461,-6.28449742901715,
-6.22478976022181,-6.16668968388983,-6.10870989485898,-6.04903759303528,
-5.99161071586561,-5.93157704581943,-5.87269722883836,-5.81571640218553,
-5.75604157196716,-5.69781092401279,-5.6703237369621),.UNSPECIFIED.);
#25879=B_SPLINE_CURVE_WITH_KNOTS('',3,(#411587,#411588,#411589,#411590,
#411591,#411592,#411593,#411594,#411595,#411596,#411597,#411598,#411599,
#411600,#411601,#411602,#411603,#411604,#411605,#411606,#411607,#411608,
#411609,#411610,#411611,#411612,#411613,#411614,#411615,#411616,#411617,
#411618,#411619,#411620,#411621,#411622),.UNSPECIFIED.,.F.,.F.,(4,2,2,2,
2,2,2,2,2,2,2,2,2,2,2,2,2,4),(-19.430746292065,-19.3786626458029,-19.3193719271923,
-19.2601473120078,-19.202365288945,-19.1423055783792,-19.0847064067758,
-19.0262528917624,-18.9664592661961,-18.9093678742006,-18.8502651679771,
-18.7904817479002,-18.7328557461471,-18.6729700713912,-18.6150819830984,
-18.5567834921217,-18.4969735651087,-18.4831085248443),.UNSPECIFIED.);
#25880=B_SPLINE_CURVE_WITH_KNOTS('',3,(#411627,#411628,#411629,#411630,
#411631,#411632,#411633,#411634,#411635,#411636,#411637,#411638,#411639,
#411640,#411641,#411642,#411643,#411644,#411645,#411646,#411647,#411648,
#411649,#411650,#411651,#411652,#411653,#411654,#411655,#411656,#411657,
#411658,#411659,#411660,#411661,#411662),.UNSPECIFIED.,.F.,.F.,(4,2,2,2,
2,2,2,2,2,2,2,2,2,2,2,2,2,4),(-7.56280299453309,-7.51397579813351,-7.45488040556703,
-7.39786421449172,-7.33816724403201,-7.27971887007593,-7.2223274578691,
-7.16226598726619,-7.10448859217055,-7.04561085958982,-6.98631222207624,
-6.92918301214771,-6.86945880028599,-6.81080474940593,-6.75356199202847,
-6.69327594632736,-6.63529587538185,-6.61638032040915),.UNSPECIFIED.);
#25881=B_SPLINE_CURVE_WITH_KNOTS('',3,(#411663,#411664,#411665,#411666,
#411667,#411668,#411669,#411670,#411671,#411672,#411673,#411674,#411675,
#411676,#411677,#411678,#411679,#411680,#411681,#411682,#411683,#411684,
#411685,#411686,#411687,#411688,#411689,#411690,#411691,#411692,#411693,
#411694,#411695,#411696,#411697,#411698),.UNSPECIFIED.,.F.,.F.,(4,2,2,2,
2,2,2,2,2,2,2,2,2,2,2,2,2,4),(-18.4831085248443,-18.4398497946047,-18.380899890151,
-18.3204993686696,-18.2629925038568,-18.2032407246096,-18.1449965661139,
-18.0868132197128,-18.0269603906926,-17.9697223292667,-17.9108849184451,
-17.8510886466108,-17.7938001957988,-17.7343196761421,-17.67568170974,-17.6177412516345,
-17.5575015042724,-17.5352552553618),.UNSPECIFIED.);
#25882=B_SPLINE_CURVE_WITH_KNOTS('',3,(#411703,#411704,#411705,#411706,
#411707,#411708,#411709,#411710,#411711,#411712,#411713,#411714,#411715,
#411716,#411717,#411718,#411719,#411720,#411721,#411722,#411723,#411724,
#411725,#411726,#411727,#411728,#411729,#411730,#411731,#411732,#411733,
#411734,#411735,#411736,#411737,#411738),.UNSPECIFIED.,.F.,.F.,(4,2,2,2,
2,2,2,2,2,2,2,2,2,2,2,2,2,4),(-8.50901833843302,-8.45124527059382,-8.39245399423659,
-8.33537735697918,-8.27564850600765,-8.21750880066048,-8.15954706413863,
-8.09983214948009,-8.04236543464371,-7.98238065207383,-7.92345623462138,
-7.86645466749089,-7.80675544179799,-7.74848021261672,-7.69084355693561,
-7.63097421057873,-7.57336947764254,-7.56280299453309),.UNSPECIFIED.);
#25883=B_SPLINE_CURVE_WITH_KNOTS('',3,(#411739,#411740,#411741,#411742,
#411743,#411744,#411745,#411746,#411747,#411748,#411749,#411750,#411751,
#411752,#411753,#411754,#411755,#411756,#411757,#411758,#411759,#411760,
#411761,#411762,#411763,#411764,#411765,#411766,#411767,#411768,#411769,
#411770,#411771,#411772,#411773,#411774),.UNSPECIFIED.,.F.,.F.,(4,2,2,2,
2,2,2,2,2,2,2,2,2,2,2,2,2,4),(-17.5352552553618,-17.500180410977,-17.4415668719403,
-17.3818181228442,-17.3247049097442,-17.2654454327972,-17.206354372399,
-17.1486063958803,-17.0885802481066,-17.0310741987563,-16.9726553175311,
-16.9129228707841,-16.8558868680907,-16.7968197671686,-16.7371815652351,
-16.6795943612501,-16.6197474148233,-16.5884934184433),.UNSPECIFIED.);
#25884=B_SPLINE_CURVE_WITH_KNOTS('',3,(#411779,#411780,#411781,#411782,
#411783,#411784,#411785,#411786,#411787,#411788,#411789,#411790,#411791,
#411792,#411793,#411794,#411795,#411796,#411797,#411798,#411799,#411800,
#411801,#411802,#411803,#411804,#411805,#411806,#411807,#411808,#411809,
#411810,#411811,#411812,#411813,#411814,#411815,#411816),.UNSPECIFIED.,
 .F.,.F.,(4,2,2,2,2,2,2,2,2,2,2,2,2,2,2,2,2,2,4),(-9.45584958042892,-9.44911444362682,
-9.38940529455709,-9.33092340536227,-9.27354521692587,-9.21344765892337,
-9.155637109888,-9.09680483889744,-9.03746929681846,-8.98030972495833,-8.92056958790122,
-8.86187841179889,-8.8046365842075,-8.74431084730452,-8.68629426447876,
-8.62786150582668,-8.56829303638661,-8.51095644498227,-8.50901833843302),
 .UNSPECIFIED.);
#25885=B_SPLINE_CURVE_WITH_KNOTS('',3,(#411817,#411818,#411819,#411820,
#411821,#411822,#411823,#411824,#411825,#411826,#411827,#411828,#411829,
#411830,#411831,#411832,#411833,#411834,#411835,#411836,#411837,#411838,
#411839,#411840,#411841,#411842,#411843,#411844,#411845,#411846,#411847,
#411848,#411849,#411850,#411851,#411852),.UNSPECIFIED.,.F.,.F.,(4,2,2,2,
2,2,2,2,2,2,2,2,2,2,2,2,2,4),(-16.5884934184433,-16.5619644526248,-16.503705774757,
-16.4439609680891,-16.3869056210481,-16.3279965296225,-16.2677480157603,
-16.2102853322193,-16.1505781319643,-16.0924474020868,-16.0343096714123,
-15.9745257154597,-15.9173667627273,-15.858576053134,-15.7988139394776,
-15.7414738213889,-15.6819049547259,-15.6412631971223),.UNSPECIFIED.);
#25886=B_SPLINE_CURVE_WITH_KNOTS('',3,(#411857,#411858,#411859,#411860,
#411861,#411862,#411863,#411864,#411865,#411866,#411867,#411868,#411869,
#411870,#411871,#411872,#411873,#411874,#411875,#411876,#411877,#411878,
#411879,#411880,#411881,#411882,#411883,#411884,#411885,#411886,#411887,
#411888,#411889,#411890,#411891,#411892),.UNSPECIFIED.,.F.,.F.,(4,2,2,2,
2,2,2,2,2,2,2,2,2,2,2,2,2,4),(-10.4021183806393,-10.386719146917,-10.3269847666313,
-10.2688206008513,-10.2108913298445,-10.151149408754,-10.0936578908522,
-10.0337368539799,-9.97478331397539,-9.91777498482906,-9.85806701687237,
-9.799762515331,-9.7421501230139,-9.68224892850401,-9.62461494536425,-9.56527779334546,
-9.50614904066621,-9.45584958042892),.UNSPECIFIED.);
#25887=B_SPLINE_CURVE_WITH_KNOTS('',3,(#411893,#411894,#411895,#411896,
#411897,#411898,#411899,#411900,#411901,#411902,#411903,#411904,#411905,
#411906,#411907,#411908,#411909,#411910,#411911,#411912,#411913,#411914,
#411915,#411916,#411917,#411918,#411919,#411920,#411921,#411922,#411923,
#411924,#411925,#411926,#411927,#411928),.UNSPECIFIED.,.F.,.F.,(4,2,2,2,
2,2,2,2,2,2,2,2,2,2,2,2,2,4),(-15.6412631971223,-15.6232621654782,-15.5652383608721,
-15.5049100990898,-15.4475507430787,-15.3888527523259,-15.3290420567482,
-15.2718562157653,-15.2125120001521,-15.1534299096715,-15.0956026159645,
-15.0354923063713,-14.9779609251807,-14.9194619385247,-14.859671528249,
-14.7998614516463,-14.7407724105526,-14.6934485066097),.UNSPECIFIED.);
#25888=B_SPLINE_CURVE_WITH_KNOTS('',3,(#411933,#411934,#411935,#411936,
#411937,#411938,#411939,#411940,#411941,#411942,#411943,#411944,#411945,
#411946,#411947,#411948,#411949,#411950,#411951,#411952,#411953,#411954,
#411955,#411956,#411957,#411958,#411959,#411960,#411961,#411962,#411963,
#411964,#411965,#411966,#411967,#411968),.UNSPECIFIED.,.F.,.F.,(4,2,2,2,
2,2,2,2,2,2,2,2,2,2,2,2,2,4),(-11.3489937993946,-11.3249843416779,-11.2648662095898,
-11.2070374667164,-11.1482657581736,-11.0889086914385,-11.0317325945659,
-10.9719921941038,-10.9132790829149,-10.8560523203481,-10.7957024975594,
-10.7376644394895,-10.6792780872413,-10.6196852385539,-10.5623262920233,
-10.5026080478968,-10.4437925103076,-10.4021183806393),.UNSPECIFIED.);
#25889=B_SPLINE_CURVE_WITH_KNOTS('',3,(#411969,#411970,#411971,#411972,
#411973,#411974,#411975,#411976,#411977,#411978,#411979,#411980,#411981,
#411982,#411983,#411984,#411985,#411986,#411987,#411988,#411989,#411990,
#411991,#411992,#411993,#411994,#411995,#411996,#411997,#411998,#411999,
#412000,#412001,#412002,#412003,#412004),.UNSPECIFIED.,.F.,.F.,(4,2,2,2,
2,2,2,2,2,2,2,2,2,2,2,2,2,4),(-14.6934485066097,-14.6836861362662,-14.6238970756216,
-14.5654572878687,-14.5078495561536,-14.4478047028095,-14.3900363319137,
-14.3307889482682,-14.2715136232438,-14.214369456016,-14.1545698698913,
-14.0959415700337,-14.0385380206706,-13.9782856780034,-13.920330482637,
-13.861557025611,-13.8020656366167,-13.7456759924953),.UNSPECIFIED.);
#25890=B_SPLINE_CURVE_WITH_KNOTS('',3,(#412009,#412010,#412011,#412012,
#412013,#412014,#412015,#412016,#412017,#412018,#412019,#412020,#412021,
#412022,#412023,#412024,#412025,#412026,#412027,#412028,#412029,#412030,
#412031,#412032,#412033,#412034,#412035,#412036,#412037,#412038,#412039,
#412040,#412041,#412042,#412043,#412044),.UNSPECIFIED.,.F.,.F.,(4,2,2,2,
2,2,2,2,2,2,2,2,2,2,2,2,2,4),(-12.2951758260951,-12.2622146747337,-12.2024611309874,
-12.1449596563198,-12.0851189116652,-12.0261514566002,-11.9691505120521,
-11.9094496220735,-11.8511308784967,-11.7935575205291,-11.7336399120256,
-11.6759915704143,-11.6167267251397,-11.5575798993392,-11.5005407874677,
-11.4408352033144,-11.3823349014934,-11.3489937993946),.UNSPECIFIED.);
#25891=B_SPLINE_CURVE_WITH_KNOTS('',3,(#412045,#412046,#412047,#412048,
#412049,#412050,#412051,#412052,#412053,#412054,#412055,#412056,#412057,
#412058,#412059,#412060,#412061,#412062,#412063,#412064,#412065,#412066,
#412067,#412068,#412069,#412070,#412071,#412072,#412073,#412074,#412075,
#412076,#412077,#412078,#412079,#412080,#412081,#412082),.UNSPECIFIED.,
 .F.,.F.,(4,2,2,2,2,2,2,2,2,2,2,2,2,2,2,2,2,2,4),(-13.7456759924953,-13.7447648028767,
-13.6849239856238,-13.6260769231875,-13.5687767156984,-13.5082867134724,
-13.4501166203179,-13.3917056147048,-13.33197351399,-13.274482363316,-13.2146526609845,
-13.1556995000451,-13.0985341732067,-13.0386908974151,-12.9803898917325,
-12.9224141846065,-12.8625287398785,-12.8049010444645,-12.7971116521498),
 .UNSPECIFIED.);
#25892=B_SPLINE_CURVE_WITH_KNOTS('',3,(#412087,#412088,#412089,#412090,
#412091,#412092,#412093,#412094,#412095,#412096,#412097,#412098,#412099,
#412100,#412101,#412102,#412103,#412104,#412105,#412106,#412107,#412108,
#412109,#412110,#412111,#412112,#412113,#412114,#412115,#412116,#412117,
#412118,#412119,#412120,#412121,#412122),.UNSPECIFIED.,.F.,.F.,(4,2,2,2,
2,2,2,2,2,2,2,2,2,2,2,2,2,4),(-13.2418576554979,-13.1994627179258,-13.1400993991086,
-13.0829205413793,-13.0231958951588,-12.9644759169146,-12.9072789732011,
-12.8469205098662,-12.7888758968419,-12.7305518663979,-12.6709499395033,
-12.6135834105728,-12.5538738930924,-12.4950492574587,-12.4379937120229,
-12.3782696936795,-12.320096058402,-12.2951758260951),.UNSPECIFIED.);
#25893=B_SPLINE_CURVE_WITH_KNOTS('',3,(#412123,#412124,#412125,#412126,
#412127,#412128,#412129,#412130,#412131,#412132,#412133,#412134,#412135,
#412136,#412137,#412138,#412139,#412140,#412141,#412142,#412143,#412144,
#412145,#412146,#412147,#412148,#412149,#412150,#412151,#412152,#412153,
#412154,#412155,#412156,#412157,#412158),.UNSPECIFIED.,.F.,.F.,(4,2,2,2,
2,2,2,2,2,2,2,2,2,2,2,2,2,4),(-12.7971116521498,-12.7449803461602,-12.6858813644011,
-12.6287647223206,-12.5689427484863,-12.5104936506619,-12.4528213673699,
-12.3927688262555,-12.3349914868138,-12.2756431323407,-12.2163620826767,
-12.1592003952585,-12.0993717077836,-12.0407383394206,-11.9832827998924,
-11.9230269897282,-11.8650667255099,-11.8489689543484),.UNSPECIFIED.);
#25894=B_SPLINE_CURVE_WITH_KNOTS('',3,(#412163,#412164,#412165,#412166,
#412167,#412168,#412169,#412170,#412171,#412172,#412173,#412174,#412175,
#412176,#412177,#412178,#412179,#412180,#412181,#412182,#412183,#412184,
#412185,#412186,#412187,#412188,#412189,#412190,#412191,#412192,#412193,
#412194,#412195,#412196,#412197,#412198),.UNSPECIFIED.,.F.,.F.,(4,2,2,2,
2,2,2,2,2,2,2,2,2,2,2,2,2,4),(-14.1877310170691,-14.135988915634,-14.0770228047692,
-14.0200438189143,-13.960366357188,-13.9020484410295,-13.8445300138478,
-13.7846114265274,-13.7269636528436,-13.6677887881959,-13.6086391417175,
-13.5516095772968,-13.491923747917,-13.4334200881425,-13.376112447951,-13.3159891690372,
-13.2581571460718,-13.2418576554979),.UNSPECIFIED.);
#25895=B_SPLINE_CURVE_WITH_KNOTS('',3,(#412199,#412200,#412201,#412202,
#412203,#412204,#412205,#412206,#412207,#412208,#412209,#412210,#412211,
#412212,#412213,#412214,#412215,#412216,#412217,#412218,#412219,#412220,
#412221,#412222,#412223,#412224,#412225,#412226,#412227,#412228,#412229,
#412230,#412231,#412232,#412233,#412234),.UNSPECIFIED.,.F.,.F.,(4,2,2,2,
2,2,2,2,2,2,2,2,2,2,2,2,2,4),(-11.8489689543484,-11.8062057019271,-11.7467120479489,
-11.6894063080904,-11.6295405390255,-11.5706919501455,-11.5133533098025,
-11.4528633639609,-11.3946915114793,-11.3362085317373,-11.2764770094769,
-11.218985220445,-11.1591378012859,-11.1001853146456,-11.0429938067333,
-10.9831311077197,-10.9248312492268,-10.9000724301687),.UNSPECIFIED.);
#25896=B_SPLINE_CURVE_WITH_KNOTS('',3,(#412239,#412240,#412241,#412242,
#412243,#412244,#412245,#412246,#412247,#412248,#412249,#412250,#412251,
#412252,#412253,#412254,#412255,#412256,#412257,#412258,#412259,#412260,
#412261,#412262,#412263,#412264,#412265,#412266,#412267,#412268,#412269,
#412270,#412271,#412272,#412273,#412274,#412275,#412276),.UNSPECIFIED.,
 .F.,.F.,(4,2,2,2,2,2,2,2,2,2,2,2,2,2,2,2,2,2,4),(-15.1339667326515,-15.1328138533434,
-15.0755472853668,-15.0160533390152,-14.9575818405722,-14.8996342065864,
-14.8393828666999,-14.7811387689155,-14.7215432153836,-14.6641840504559,
-14.6044996275074,-14.5456812087575,-14.4886586947663,-14.4289615372059,
-14.3707935623025,-14.3129768521214,-14.2532271707844,-14.1957307128446,
-14.1877310170691),.UNSPECIFIED.);
#25897=B_SPLINE_CURVE_WITH_KNOTS('',3,(#412277,#412278,#412279,#412280,
#412281,#412282,#412283,#412284,#412285,#412286,#412287,#412288,#412289,
#412290,#412291,#412292,#412293,#412294,#412295,#412296,#412297,#412298,
#412299,#412300,#412301,#412302,#412303,#412304,#412305,#412306,#412307,
#412308,#412309,#412310,#412311,#412312),.UNSPECIFIED.,.F.,.F.,(4,2,2,2,
2,2,2,2,2,2,2,2,2,2,2,2,2,4),(-10.9000724301687,-10.8667984467609,-10.8069161060488,
-10.7492901312385,-10.6892789248494,-10.6301854632589,-10.5730534177407,
-10.5132153838967,-10.4547722371732,-10.3970522395411,-10.3370076193401,
-10.2792364263307,-10.2198060794502,-10.1605347102306,-10.1033697946133,
-10.0435286456608,-9.98490540550661,-9.95172763366354),.UNSPECIFIED.);
#25898=B_SPLINE_CURVE_WITH_KNOTS('',3,(#412317,#412318,#412319,#412320,
#412321,#412322,#412323,#412324,#412325,#412326,#412327,#412328,#412329,
#412330,#412331,#412332,#412333,#412334,#412335,#412336,#412337,#412338,
#412339,#412340,#412341,#412342,#412343,#412344,#412345,#412346,#412347,
#412348,#412349,#412350,#412351,#412352),.UNSPECIFIED.,.F.,.F.,(4,2,2,2,
2,2,2,2,2,2,2,2,2,2,2,2,2,4),(-16.0794051131266,-16.0696407503467,-16.0121174534365,
-15.9523350001075,-15.8946932109278,-15.8364997791912,-15.7768508439869,
-15.7198928362282,-15.6610503748176,-15.6010001801705,-15.5436076054625,
-15.4839716393591,-15.4259926693996,-15.3679268902092,-15.3082432723521,
-15.2511947878248,-15.1924775074701,-15.1339667326515),.UNSPECIFIED.);
#25899=B_SPLINE_CURVE_WITH_KNOTS('',3,(#412353,#412354,#412355,#412356,
#412357,#412358,#412359,#412360,#412361,#412362,#412363,#412364,#412365,
#412366,#412367,#412368,#412369,#412370,#412371,#412372,#412373,#412374,
#412375,#412376,#412377,#412378,#412379,#412380,#412381,#412382,#412383,
#412384,#412385,#412386,#412387,#412388),.UNSPECIFIED.,.F.,.F.,(4,2,2,2,
2,2,2,2,2,2,2,2,2,2,2,2,2,4),(-9.95172763366354,-9.92741383632888,-9.86717010987739,
-9.80921983279747,-9.75028907798721,-9.69080854346615,-9.63351174591108,
-9.57363743547837,-9.51480248845095,-9.4574406720365,-9.39696631029004,
-9.33880772125035,-9.28026960018865,-9.22055403493478,-9.16307647023736,
-9.10322743464804,-9.04429086314863,-9.00274133888152),.UNSPECIFIED.);
#25900=B_SPLINE_CURVE_WITH_KNOTS('',3,(#412393,#412394,#412395,#412396,
#412397,#412398,#412399,#412400,#412401,#412402,#412403,#412404,#412405,
#412406,#412407,#412408,#412409,#412410,#412411,#412412,#412413,#412414,
#412415,#412416,#412417,#412418,#412419,#412420,#412421,#412422,#412423,
#412424,#412425,#412426,#412427,#412428),.UNSPECIFIED.,.F.,.F.,(4,2,2,2,
2,2,2,2,2,2,2,2,2,2,2,2,2,4),(-17.0248696573777,-17.0067626855016,-16.9488761285404,
-16.8886900492831,-16.831478331547,-16.7729191403435,-16.7132565323447,
-16.6562083651293,-16.5970046577124,-16.5380880417454,-16.4803985525618,
-16.4204310100632,-16.3630513473235,-16.3046917953613,-16.2450505258361,
-16.1880961783059,-16.1290897695364,-16.0794051131266),.UNSPECIFIED.);
#25901=B_SPLINE_CURVE_WITH_KNOTS('',3,(#412429,#412430,#412431,#412432,
#412433,#412434,#412435,#412436,#412437,#412438,#412439,#412440,#412441,
#412442,#412443,#412444,#412445,#412446,#412447,#412448,#412449,#412450,
#412451,#412452,#412453,#412454,#412455,#412456,#412457,#412458,#412459,
#412460,#412461,#412462,#412463,#412464),.UNSPECIFIED.,.F.,.F.,(4,2,2,2,
2,2,2,2,2,2,2,2,2,2,2,2,2,4),(-9.00274133888152,-8.98708808222356,-8.92722217436779,
-8.86893852475257,-8.81086478778761,-8.75100098495595,-8.69339164115971,
-8.6333076147785,-8.57423490357275,-8.51710183575562,-8.45726384338693,
-8.39884169405584,-8.34108927130448,-8.28106800117714,-8.22331785961894,
-8.16382232926111,-8.1045759025698,-8.05441325037715),.UNSPECIFIED.);
#25902=B_SPLINE_CURVE_WITH_KNOTS('',3,(#412469,#412470,#412471,#412472,
#412473,#412474,#412475,#412476,#412477,#412478,#412479,#412480,#412481,
#412482,#412483,#412484,#412485,#412486,#412487,#412488,#412489,#412490,
#412491,#412492,#412493,#412494,#412495,#412496,#412497,#412498,#412499,
#412500,#412501,#412502,#412503,#412504),.UNSPECIFIED.,.F.,.F.,(4,2,2,2,
2,2,2,2,2,2,2,2,2,2,2,2,2,4),(-17.9697860632053,-17.9431621937315,-17.8850387122403,
-17.8254391869702,-17.7685240651178,-17.7097518301889,-17.6496732375117,
-17.5923452314049,-17.5327776023798,-17.4748017460718,-17.4168005153958,
-17.3571629468064,-17.3001474078506,-17.2414948860682,-17.1818786968149,
-17.1246738065254,-17.0652450862675,-17.0248696573777),.UNSPECIFIED.);
#25903=B_SPLINE_CURVE_WITH_KNOTS('',3,(#412505,#412506,#412507,#412508,
#412509,#412510,#412511,#412512,#412513,#412514,#412515,#412516,#412517,
#412518,#412519,#412520,#412521,#412522,#412523,#412524,#412525,#412526,
#412527,#412528,#412529,#412530,#412531,#412532,#412533,#412534,#412535,
#412536,#412537,#412538,#412539,#412540,#412541,#412542),.UNSPECIFIED.,
 .F.,.F.,(4,2,2,2,2,2,2,2,2,2,2,2,2,2,2,2,2,2,4),(-8.05441325037715,-8.04742174586969,
-7.98758411506632,-7.92898607371866,-7.87147336403557,-7.81125718161243,
-7.75333182043714,-7.69434731743895,-7.63489521713669,-7.5776211614932,
-7.51775415880984,-7.45894797080115,-7.40157745295303,-7.34113418679424,
-7.28300382792094,-7.22442589013463,-7.1647416525545,-7.1072931406182,-7.10557406287411),
 .UNSPECIFIED.);
#25904=B_SPLINE_CURVE_WITH_KNOTS('',3,(#412547,#412548,#412549,#412550,
#412551,#412552,#412553,#412554,#412555,#412556,#412557,#412558,#412559,
#412560,#412561,#412562,#412563,#412564,#412565,#412566,#412567,#412568,
#412569,#412570,#412571,#412572,#412573,#412574,#412575,#412576,#412577,
#412578,#412579,#412580,#412581,#412582),.UNSPECIFIED.,.F.,.F.,(4,2,2,2,
2,2,2,2,2,2,2,2,2,2,2,2,2,4),(-18.9142706847603,-18.879112817184,-18.8206326702126,
-18.7610269812058,-18.7040467074318,-18.644922279731,-18.5859934242845,
-18.5283780156482,-18.4684891649703,-18.4111309770561,-18.3528462472636,
-18.2932579801719,-18.2363585809717,-18.1774272809653,-18.1179557281923,
-18.0605020205951,-18.0007933709383,-17.9697860632053),.UNSPECIFIED.);
#25905=B_SPLINE_CURVE_WITH_KNOTS('',3,(#412583,#412584,#412585,#412586,
#412587,#412588,#412589,#412590,#412591,#412592,#412593,#412594,#412595,
#412596,#412597,#412598,#412599,#412600,#412601,#412602,#412603,#412604,
#412605,#412606,#412607,#412608,#412609,#412610,#412611,#412612,#412613,
#412614,#412615,#412616,#412617,#412618),.UNSPECIFIED.,.F.,.F.,(4,2,2,2,
2,2,2,2,2,2,2,2,2,2,2,2,2,4),(-7.10557406287411,-7.04745818303111,-6.98855275914176,
-6.93135307843427,-6.87149973761286,-6.81324736108095,-6.75514765506272,
-6.6953178670604,-6.63774007839259,-6.57759901578035,-6.51856237664589,
-6.46144235798614,-6.40162014413745,-6.34323414046294,-6.28546377651572,
-6.22548142888577,-6.16776734990896,-6.15740376012386),.UNSPECIFIED.);
#25906=B_SPLINE_CURVE_WITH_KNOTS('',3,(#412623,#412624,#412625,#412626,
#412627,#412628,#412629,#412630,#412631,#412632,#412633,#412634,#412635,
#412636,#412637,#412638,#412639,#412640,#412641,#412642,#412643,#412644,
#412645,#412646,#412647,#412648,#412649,#412650,#412651,#412652,#412653,
#412654,#412655,#412656,#412657,#412658),.UNSPECIFIED.,.F.,.F.,(4,2,2,2,
2,2,2,2,2,2,2,2,2,2,2,2,2,4),(-19.8584422835686,-19.8152073934546,-19.7565232896875,
-19.6964277594369,-19.6391814863779,-19.5797000820731,-19.5217402307493,
-19.4638208175453,-19.404245965306,-19.3472777488811,-19.2887074085738,
-19.2291553359313,-19.1720289787636,-19.1126830374294,-19.0542020436924,
-18.9963934826294,-18.9362903222569,-18.9142706847603),.UNSPECIFIED.);
#25907=B_SPLINE_CURVE_WITH_KNOTS('',3,(#412659,#412660,#412661,#412662,
#412663,#412664,#412665,#412666,#412667,#412668,#412669,#412670,#412671,
#412672,#412673,#412674,#412675,#412676,#412677,#412678,#412679,#412680,
#412681,#412682,#412683,#412684,#412685,#412686,#412687,#412688,#412689,
#412690,#412691,#412692,#412693,#412694),.UNSPECIFIED.,.F.,.F.,(4,2,2,2,
2,2,2,2,2,2,2,2,2,2,2,2,2,4),(-6.15740376012386,-6.10822172720228,-6.0490156838889,
-5.99188620823853,-5.93206779050262,-5.87351020829041,-5.81599049092837,
-5.75581754399223,-5.69793221518616,-5.63890848208477,-5.57950038364006,
-5.5222630440661,-5.46241899964079,-5.40365695283083,-5.34629170825762,
-5.28589535541311,-5.22780845186964,-5.20907703509223),.UNSPECIFIED.);
#25908=B_SPLINE_CURVE_WITH_KNOTS('',3,(#412699,#412700,#412701,#412702,
#412703,#412704,#412705,#412706,#412707,#412708,#412709,#412710,#412711,
#412712,#412713,#412714,#412715,#412716,#412717,#412718,#412719,#412720,
#412721,#412722,#412723,#412724,#412725,#412726,#412727,#412728,#412729,
#412730,#412731,#412732,#412733,#412734),.UNSPECIFIED.,.F.,.F.,(4,2,2,2,
2,2,2,2,2,2,2,2,2,2,2,2,2,4),(-20.8017161031817,-20.7496789559818,-20.6906526416135,
-20.6317226295974,-20.5741993586506,-20.5144080614634,-20.4570845025018,
-20.3988928086463,-20.3393746294764,-20.282545486662,-20.2237076825146,
-20.1642246610779,-20.1068581592809,-20.0472416921874,-19.9896339732113,
-19.9315981829693,-19.8720649377923,-19.8584422835686),.UNSPECIFIED.);
#25909=B_SPLINE_CURVE_WITH_KNOTS('',3,(#412735,#412736,#412737,#412738,
#412739,#412740,#412741,#412742,#412743,#412744,#412745,#412746,#412747,
#412748,#412749,#412750,#412751,#412752,#412753,#412754,#412755,#412756,
#412757,#412758,#412759,#412760,#412761,#412762,#412763,#412764,#412765,
#412766,#412767,#412768,#412769,#412770),.UNSPECIFIED.,.F.,.F.,(4,2,2,2,
2,2,2,2,2,2,2,2,2,2,2,2,2,4),(-5.20907703509223,-5.16920485068219,-5.10956762673631,
-5.0521632757907,-4.99235803428031,-4.93349930655624,-4.87631684158672,
-4.81649176115974,-4.75828604527994,-4.70017445432352,-4.6403945310797,
-4.58286355547662,-4.52267968715453,-4.46369486316409,-4.40660190807755,
-4.34681119824301,-4.28847691628623,-4.26116841327561),.UNSPECIFIED.);
#25910=B_SPLINE_CURVE_WITH_KNOTS('',3,(#412775,#412776,#412777,#412778,
#412779,#412780,#412781,#412782,#412783,#412784,#412785,#412786,#412787,
#412788,#412789,#412790,#412791,#412792,#412793,#412794,#412795,#412796,
#412797,#412798,#412799,#412800,#412801,#412802,#412803,#412804,#412805,
#412806,#412807,#412808,#412809,#412810,#412811,#412812),.UNSPECIFIED.,
 .F.,.F.,(4,2,2,2,2,2,2,2,2,2,2,2,2,2,2,2,2,2,4),(-21.7459617623565,-21.7423453853052,
-21.6850922827677,-21.6256066051595,-21.5674881210864,-21.5095596509136,
-21.4493195364772,-21.392283120407,-21.3336802984165,-21.2741047422002,
-21.2170434942016,-21.1577995546806,-21.0993315343373,-21.0416194317091,
-20.9816184985961,-20.924489018422,-20.8661065715194,-20.8065751181493,
-20.8017161031817),.UNSPECIFIED.);
#25911=B_SPLINE_CURVE_WITH_KNOTS('',3,(#412813,#412814,#412815,#412816,
#412817,#412818,#412819,#412820,#412821,#412822,#412823,#412824,#412825,
#412826,#412827,#412828,#412829,#412830,#412831,#412832,#412833,#412834,
#412835,#412836,#412837,#412838,#412839,#412840,#412841,#412842,#412843,
#412844,#412845,#412846,#412847,#412848),.UNSPECIFIED.,.F.,.F.,(4,2,2,2,
2,2,2,2,2,2,2,2,2,2,2,2,2,4),(-4.26116841327561,-4.23070237710342,-4.17077500320315,
-4.11311242933797,-4.05353038859324,-3.99438068331312,-3.9372899857969,
-3.87750654045149,-3.81900520002606,-3.7614921033953,-3.70137865717443,
-3.64354899639362,-3.58449934635719,-3.52515141514432,-3.46796518308394,
-3.40815989357924,-3.34945797488407,-3.31355979035892),.UNSPECIFIED.);
#25912=B_SPLINE_CURVE_WITH_KNOTS('',3,(#412853,#412854,#412855,#412856,
#412857,#412858,#412859,#412860,#412861,#412862,#412863,#412864,#412865,
#412866,#412867,#412868,#412869,#412870,#412871,#412872,#412873,#412874,
#412875,#412876,#412877,#412878,#412879,#412880,#412881,#412882,#412883,
#412884,#412885,#412886,#412887,#412888),.UNSPECIFIED.,.F.,.F.,(4,2,2,2,
2,2,2,2,2,2,2,2,2,2,2,2,2,4),(-22.68998065011,-22.6777707860463,-22.6202279402948,
-22.5604180217573,-22.5030176125001,-22.4448059003209,-22.3852427307347,
-22.328372598661,-22.2695139987459,-22.2099052437004,-22.152514528674,-22.0928743951815,
-22.0351787158555,-21.9771178573061,-21.917535881535,-21.8606250794884,
-21.801915096849,-21.7459617623565),.UNSPECIFIED.);
#25913=B_SPLINE_CURVE_WITH_KNOTS('',3,(#412889,#412890,#412891,#412892,
#412893,#412894,#412895,#412896,#412897,#412898,#412899,#412900,#412901,
#412902,#412903,#412904,#412905,#412906,#412907,#412908,#412909,#412910,
#412911,#412912,#412913,#412914,#412915,#412916,#412917,#412918,#412919,
#412920,#412921,#412922,#412923,#412924),.UNSPECIFIED.,.F.,.F.,(4,2,2,2,
2,2,2,2,2,2,2,2,2,2,2,2,2,4),(-3.31355979035892,-3.29211171904543,-3.23177875334416,
-3.17375112630324,-3.11513507891545,-3.05556122121513,-2.99821675833727,
-2.93845715871131,-2.87966134450814,-2.8225102089605,-2.76272934872894,
-2.70458635428677,-2.64647631832303,-2.58676284615983,-2.52929462550545,
-2.46908084307281,-2.4101643664363,-2.36612653176872),.UNSPECIFIED.);
#25914=B_SPLINE_CURVE_WITH_KNOTS('',3,(#412929,#412930,#412931,#412932,
#412933,#412934,#412935,#412936,#412937,#412938,#412939,#412940,#412941,
#412942,#412943,#412944,#412945,#412946,#412947,#412948,#412949,#412950,
#412951,#412952,#412953,#412954,#412955,#412956,#412957,#412958,#412959,
#412960,#412961,#412962,#412963,#412964),.UNSPECIFIED.,.F.,.F.,(4,2,2,2,
2,2,2,2,2,2,2,2,2,2,2,2,2,4),(-23.6345898267855,-23.6140949491887,-23.5561542444433,
-23.4959033790334,-23.4388176101368,-23.3802026881221,-23.320590507054,
-23.2635147517929,-23.2042578136158,-23.1456890151044,-23.0879613142637,
-23.0279460580427,-22.970753042941,-22.912354902148,-22.8527824648407,-22.7958587610358,
-22.736815942826,-22.68998065011),.UNSPECIFIED.);
#25915=B_SPLINE_CURVE_WITH_KNOTS('',3,(#412965,#412966,#412967,#412968,
#412969,#412970,#412971,#412972,#412973,#412974,#412975,#412976,#412977,
#412978,#412979,#412980,#412981,#412982,#412983,#412984,#412985,#412986,
#412987,#412988,#412989,#412990,#412991,#412992,#412993,#412994,#412995,
#412996,#412997,#412998,#412999,#413000),.UNSPECIFIED.,.F.,.F.,(4,2,2,2,
2,2,2,2,2,2,2,2,2,2,2,2,2,4),(-2.36612653176872,-2.35311268006124,-2.29336954071319,
-2.2351033487007,-2.17733789322699,-2.11748240192008,-2.05988757144052,
-2.00028154453617,-1.94120503286711,-1.88416763920247,-1.82443534589591,
-1.76600693231654,-1.70851378499439,-1.64847707345954,-1.59071961453085,
-1.53165630513777,-1.47238570404183,-1.41945372484329),.UNSPECIFIED.);
#25916=B_SPLINE_CURVE_WITH_KNOTS('',3,(#413005,#413006,#413007,#413008,
#413009,#413010,#413011,#413012,#413013,#413014,#413015,#413016,#413017,
#413018,#413019,#413020,#413021,#413022,#413023,#413024,#413025,#413026,
#413027,#413028,#413029,#413030,#413031,#413032,#413033,#413034,#413035,
#413036,#413037,#413038,#413039,#413040),.UNSPECIFIED.,.F.,.F.,(4,2,2,2,
2,2,2,2,2,2,2,2,2,2,2,2,2,4),(-24.5792059929108,-24.5500970949004,-24.4918809036154,
-24.4322903051749,-24.3753946654069,-24.3165310225285,-24.2568186477746,
-24.1994192812253,-24.1397715290208,-24.0820070150704,-24.0239368230827,
-23.964323943516,-23.907376385801,-23.8486564673835,-23.7890576529927,-23.7317935555424,
-23.672297753621,-23.6345898267855),.UNSPECIFIED.);
#25917=B_SPLINE_CURVE_WITH_KNOTS('',3,(#413041,#413042,#413043,#413044,
#413045,#413046,#413047,#413048,#413049,#413050,#413051,#413052,#413053,
#413054,#413055,#413056,#413057,#413058,#413059,#413060,#413061,#413062,
#413063,#413064,#413065,#413066,#413067,#413068,#413069,#413070,#413071,
#413072,#413073,#413074,#413075,#413076,#413077,#413078),.UNSPECIFIED.,
 .F.,.F.,(4,2,2,2,2,2,2,2,2,2,2,2,2,2,2,2,2,2,4),(-1.41945372484329,-1.41526566454244,
-1.35551543195448,-1.29689062832757,-1.23957703033406,-1.17932499202215,
-1.12137345130017,-1.0627573841339,-1.00326432523307,-0.945996493022722,
-0.886299119599774,-0.827583520519354,-0.770478077590893,-0.710758038954895,
-0.652694913124193,-0.594599400688255,-0.53497013529226,-0.477581710315112,
-0.472734891726342),.UNSPECIFIED.);
#25918=B_SPLINE_CURVE_WITH_KNOTS('',3,(#413083,#413084,#413085,#413086,
#413087,#413088,#413089,#413090,#413091,#413092,#413093,#413094,#413095,
#413096,#413097,#413098,#413099,#413100,#413101,#413102,#413103,#413104,
#413105,#413106,#413107,#413108,#413109,#413110,#413111,#413112,#413113,
#413114,#413115,#413116,#413117,#413118),.UNSPECIFIED.,.F.,.F.,(4,2,2,2,
2,2,2,2,2,2,2,2,2,2,2,2,2,4),(-25.5239437797376,-25.4862365841868,-25.4276248886421,
-25.3679930479258,-25.3109167358137,-25.2516623582473,-25.1930121222715,
-25.1352840929817,-25.0752702538568,-25.018030561544,-24.9596321363847,
-24.9000359896044,-24.8430993324249,-24.7840556434341,-24.7249160932499,
-24.667369062466,-24.6075563852897,-24.5792059929108),.UNSPECIFIED.);
#25919=B_SPLINE_CURVE_WITH_KNOTS('',3,(#413120,#413121,#413122,#413123,
#413124,#413125,#413126,#413127,#413128,#413129,#413130,#413131,#413132,
#413133,#413134,#413135,#413136,#413137,#413138,#413139),.UNSPECIFIED.,
 .F.,.F.,(4,2,2,2,2,2,2,2,2,4),(-0.472734891726342,-0.41734976808456,-0.358519527533459,
-0.301523884178399,-0.241845235162269,-0.183664856566032,-0.125921516552503,
-0.0661562618768071,-0.0325226499984521,-1.00000007524637E-6),
 .UNSPECIFIED.);
#25920=B_SPLINE_CURVE_WITH_KNOTS('',3,(#413140,#413141,#413142,#413143,
#413144,#413145,#413146,#413147,#413148,#413149,#413150,#413151,#413152,
#413153,#413154,#413155,#413156,#413157,#413158,#413159),.UNSPECIFIED.,
 .F.,.F.,(4,2,2,2,2,2,2,2,2,4),(-4.25182450433022,-4.21324482415993,-4.17330760656305,
-4.11300975566751,-4.05588823658734,-3.99722796799383,-3.93757504645253,
-3.88045584389487,-3.82115322980259,-3.77909511501224),.UNSPECIFIED.);
#25921=B_SPLINE_CURVE_WITH_KNOTS('',3,(#413164,#413165,#413166,#413167,
#413168,#413169,#413170,#413171,#413172,#413173,#413174,#413175,#413176,
#413177,#413178,#413179,#413180,#413181,#413182,#413183,#413184,#413185,
#413186,#413187,#413188,#413189,#413190,#413191,#413192,#413193,#413194,
#413195,#413196,#413197,#413198,#413199),.UNSPECIFIED.,.F.,.F.,(4,2,2,2,
2,2,2,2,2,2,2,2,2,2,2,2,2,4),(-26.4689340794109,-26.4230444975284,-26.3641911040406,
-26.3043943197107,-26.2470013265531,-26.187361485941,-26.1295452860473,
-26.0714809446919,-26.0118538369996,-25.9548849192215,-25.8961704376275,
-25.8365590552678,-25.7792989717176,-25.719808553885,-25.6615394891026,
-25.6036017340092,-25.5433557799967,-25.5239437797376),.UNSPECIFIED.);
#25922=B_SPLINE_CURVE_WITH_KNOTS('',3,(#413200,#413201,#413202,#413203,
#413204,#413205,#413206,#413207,#413208,#413209,#413210,#413211,#413212,
#413213,#413214,#413215,#413216,#413217,#413218,#413219,#413220,#413221,
#413222,#413223,#413224,#413225,#413226,#413227,#413228,#413229,#413230,
#413231,#413232,#413233,#413234,#413235),.UNSPECIFIED.,.F.,.F.,(4,2,2,2,
2,2,2,2,2,2,2,2,2,2,2,2,2,4),(-3.77909511501224,-3.76255879084929,-3.70478712467392,
-3.64472574486189,-3.58749989775137,-3.52905726514817,-3.46944495073968,
-3.41248069251164,-3.35339303043433,-3.29432488526653,-3.23673911082507,
-3.17688419430657,-3.11945369884331,-3.06119861064818,-3.00159645144949,
-2.94468876957472,-2.88578643339366,-2.83439253495563),.UNSPECIFIED.);
#25923=B_SPLINE_CURVE_WITH_KNOTS('',3,(#413240,#413241,#413242,#413243,
#413244,#413245,#413246,#413247,#413248,#413249,#413250,#413251,#413252,
#413253,#413254,#413255,#413256,#413257,#413258,#413259,#413260,#413261,
#413262,#413263,#413264,#413265,#413266,#413267,#413268,#413269,#413270,
#413271,#413272,#413273,#413274,#413275),.UNSPECIFIED.,.F.,.F.,(4,2,2,2,
2,2,2,2,2,2,2,2,2,2,2,2,2,4),(-27.413585014475,-27.3586963183019,-27.2994597685197,
-27.2407452322649,-27.1830317971469,-27.1230348017685,-27.0657639571981,
-27.0073803107202,-26.9477767793054,-26.8908412827537,-26.8318119875776,
-26.7725962122378,-26.7150599514713,-26.6552599714108,-26.5977580446488,
-26.5395524732983,-26.4799509530169,-26.4689340794109),.UNSPECIFIED.);
#25924=B_SPLINE_CURVE_WITH_KNOTS('',3,(#413276,#413277,#413278,#413279,
#413280,#413281,#413282,#413283,#413284,#413285,#413286,#413287,#413288,
#413289,#413290,#413291,#413292,#413293,#413294,#413295,#413296,#413297,
#413298,#413299,#413300,#413301,#413302,#413303,#413304,#413305,#413306,
#413307,#413308,#413309,#413310,#413311,#413312,#413313),.UNSPECIFIED.,
 .F.,.F.,(4,2,2,2,2,2,2,2,2,2,2,2,2,2,2,2,2,2,4),(-2.83439253495563,-2.8261565099365,
-2.76872402181225,-2.70904015089222,-2.6513165569579,-2.59321356797793,
-2.5335934094535,-2.4766477076658,-2.41789524058402,-2.35828692277368,-2.30099269164597,
-2.24146397083721,-2.18332091803267,-2.12535108784111,-2.06740821026071,
-2.00919870111594,-1.94970082154406,-1.8924346470782,-1.88939598835329),
 .UNSPECIFIED.);
#25925=B_SPLINE_CURVE_WITH_KNOTS('',3,(#413321,#413322,#413323,#413324,
#413325,#413326,#413327,#413328,#413329,#413330,#413331,#413332,#413333,
#413334,#413335,#413336,#413337,#413338,#413339,#413340,#413341,#413342,
#413343,#413344,#413345,#413346,#413347,#413348,#413349,#413350,#413351,
#413352),.UNSPECIFIED.,.F.,.F.,(4,2,2,2,2,2,2,2,2,2,2,2,2,2,2,4),(-29.1863963535123,
-29.1497109670899,-29.1134166088123,-29.055062847062,-28.9954677920218,
-28.9385474105555,-28.8795478027661,-28.8202720404545,-28.7627614641067,
-28.7029896310345,-28.6454600774267,-28.5872801805647,-28.527683695153,
-28.4707806921121,-28.4119527827778,-28.3587334199921),.UNSPECIFIED.);
#25926=B_SPLINE_CURVE_WITH_KNOTS('',3,(#413355,#413356,#413357,#413358,
#413359,#413360,#413361,#413362,#413363,#413364,#413365,#413366,#413367,
#413368,#413369,#413370,#413371,#413372,#413373,#413374,#413375,#413376,
#413377,#413378,#413379,#413380,#413381,#413382,#413383,#413384,#413385,
#413386,#413387,#413388,#413389,#413390),.UNSPECIFIED.,.F.,.F.,(4,2,2,2,
2,2,2,2,2,2,2,2,2,2,2,2,2,4),(-0.944879082372548,-0.897379451402566,-0.838334347307847,
-0.781395526853323,-0.721796519477892,-0.663396730448959,-0.606152751521145,
-0.546137618568464,-0.488408239163712,-0.42975149823817,-0.370495918980581,
-0.313418221859422,-0.253783772254139,-0.195170931018825,-0.138048281270193,
-0.0778012501110445,-0.038228735137851,-1.0000000948418E-6),
 .UNSPECIFIED.);
#25927=B_SPLINE_CURVE_WITH_KNOTS('',3,(#414087,#414088,#414089,#414090,
#414091,#414092,#414093,#414094,#414095,#414096,#414097,#414098,#414099,
#414100,#414101,#414102,#414103,#414104,#414105,#414106,#414107,#414108,
#414109,#414110,#414111,#414112,#414113,#414114,#414115,#414116,#414117,
#414118,#414119,#414120,#414121,#414122,#414123,#414124),.UNSPECIFIED.,
 .F.,.F.,(4,2,2,2,2,2,2,2,2,2,2,2,2,2,2,2,2,2,4),(-28.3587334199921,-28.3520886310235,
-28.2947168329376,-28.2351002552499,-28.1772480545876,-28.1192045326099,
-28.0595791702464,-28.0026035429005,-27.943909641482,-27.8843015620247,
-27.8270602519875,-27.767590499069,-27.7092714269571,-27.6513515336446,
-27.5911259178804,-27.5339882142317,-27.4753948036166,-27.4157594323402,
-27.413585014475),.UNSPECIFIED.);
#25928=B_SPLINE_CURVE_WITH_KNOTS('',3,(#414125,#414126,#414127,#414128,
#414129,#414130,#414131,#414132,#414133,#414134,#414135,#414136,#414137,
#414138,#414139,#414140,#414141,#414142,#414143,#414144,#414145,#414146,
#414147,#414148,#414149,#414150,#414151,#414152,#414153,#414154,#414155,
#414156,#414157,#414158,#414159,#414160),.UNSPECIFIED.,.F.,.F.,(4,2,2,2,
2,2,2,2,2,2,2,2,2,2,2,2,2,4),(-1.88939598835329,-1.83283257048709,-1.77411060750807,
-1.71715934398323,-1.65754309113281,-1.5994709081347,-1.54170066531609,
-1.48205099193883,-1.42464969478967,-1.36492936779628,-1.30606398664382,
-1.24916533957941,-1.18957158552469,-1.13135370679887,-1.07388930634909,
-1.01407501167343,-0.956526329448152,-0.944879082372548),.UNSPECIFIED.);
#25929=B_SPLINE_CURVE_WITH_KNOTS('',3,(#414163,#414164,#414165,#414166,
#414167,#414168,#414169,#414170,#414171,#414172,#414173,#414174),
 .UNSPECIFIED.,.F.,.F.,(4,2,2,2,2,4),(-0.202065267427624,-0.17829348393292,
-0.153313184261408,-0.110608381314549,-0.0554673983154286,-1.00000018307678E-6),
 .UNSPECIFIED.);
#25930=B_SPLINE_CURVE_WITH_KNOTS('',3,(#414175,#414176,#414177,#414178,
#414179,#414180,#414181,#414182,#414183,#414184,#414185,#414186,#414187,
#414188,#414189,#414190,#414191,#414192,#414193,#414194),.UNSPECIFIED.,
 .F.,.F.,(4,2,2,2,2,2,2,2,2,4),(-0.723442842076705,-0.67470994600901,-0.637171178726302,
-0.599047155987729,-0.559110341325991,-0.520318538599342,-0.477726281559118,
-0.416471543823766,-0.3571169726445,-0.318111909131838),.UNSPECIFIED.);
#25931=B_SPLINE_CURVE_WITH_KNOTS('',3,(#414200,#414201,#414202,#414203,
#414204,#414205,#414206,#414207,#414208,#414209,#414210,#414211,#414212,
#414213,#414214,#414215,#414216,#414217,#414218,#414219,#414220,#414221,
#414222,#414223,#414224,#414225,#414226,#414227,#414228,#414229,#414230,
#414231),.UNSPECIFIED.,.F.,.F.,(4,2,2,2,2,2,2,2,2,2,2,2,2,2,2,4),(0.112636617654083,
0.149377717472863,0.209192138323285,0.265054851856284,0.319884610918571,
0.367155139827267,0.416337427526782,0.463897142310362,0.515169975267158,
0.580416230184428,0.669070279346709,0.762049043445549,0.852742975916796,
0.94658012568358,1.02412072733907,1.1048615181955),.UNSPECIFIED.);
#25932=B_SPLINE_CURVE_WITH_KNOTS('',3,(#414271,#414272,#414273,#414274,
#414275,#414276,#414277,#414278,#414279,#414280,#414281,#414282,#414283,
#414284,#414285,#414286),.UNSPECIFIED.,.F.,.F.,(4,3,3,3,3,4),(7.65824322177166E-5,
7.91451746290967E-5,9.26886647076421E-5,0.000106465540579908,0.000127678760140906,
0.000152977955413166),.UNSPECIFIED.);
#25933=B_SPLINE_CURVE_WITH_KNOTS('',3,(#414294,#414295,#414296,#414297,
#414298,#414299,#414300,#414301,#414302,#414303,#414304,#414305,#414306,
#414307,#414308,#414309,#414310,#414311,#414312,#414313,#414314,#414315,
#414316,#414317,#414318),.UNSPECIFIED.,.F.,.F.,(4,3,3,3,3,3,3,3,4),(0.,
2.85550478878829E-5,4.78559032675579E-5,6.34108981925975E-5,7.91451746296059E-5,
9.26886647080578E-5,0.000106465540580229,0.00012767876014108,0.000152977955413166),
 .UNSPECIFIED.);
#25934=B_SPLINE_CURVE_WITH_KNOTS('',3,(#414326,#414327,#414328,#414329,
#414330,#414331,#414332,#414333,#414334,#414335,#414336,#414337,#414338,
#414339,#414340,#414341,#414342,#414343,#414344,#414345,#414346,#414347,
#414348,#414349,#414350),.UNSPECIFIED.,.F.,.F.,(4,3,3,3,3,3,3,3,4),(0.,
2.85550478878828E-5,4.78559032675579E-5,6.34108981925975E-5,7.91451746296059E-5,
9.2688664708058E-5,0.000106465540580229,0.000127678760141081,0.000152977955413166),
 .UNSPECIFIED.);
#25935=B_SPLINE_CURVE_WITH_KNOTS('',3,(#414358,#414359,#414360,#414361,
#414362,#414363,#414364,#414365,#414366,#414367,#414368,#414369,#414370,
#414371,#414372,#414373,#414374,#414375,#414376,#414377,#414378,#414379,
#414380,#414381,#414382),.UNSPECIFIED.,.F.,.F.,(4,3,3,3,3,3,3,3,4),(0.,
2.85550478878827E-5,4.78559032675579E-5,6.34108981925976E-5,7.91451746296058E-5,
9.26886647080579E-5,0.000106465540580229,0.000127678760141081,0.000152977955413166),
 .UNSPECIFIED.);
#25936=B_SPLINE_CURVE_WITH_KNOTS('',3,(#414390,#414391,#414392,#414393,
#414394,#414395,#414396,#414397,#414398,#414399,#414400,#414401,#414402,
#414403,#414404,#414405,#414406,#414407,#414408,#414409,#414410,#414411,
#414412,#414413,#414414),.UNSPECIFIED.,.F.,.F.,(4,3,3,3,3,3,3,3,4),(0.,
2.85550478878826E-5,4.78559032675577E-5,6.34108981925974E-5,7.91451746296057E-5,
9.26886647080577E-5,0.000106465540580228,0.00012767876014108,0.000152977955413165),
 .UNSPECIFIED.);
#25937=B_SPLINE_CURVE_WITH_KNOTS('',3,(#414422,#414423,#414424,#414425,
#414426,#414427,#414428,#414429,#414430,#414431,#414432,#414433,#414434,
#414435,#414436,#414437,#414438,#414439,#414440,#414441,#414442,#414443,
#414444,#414445,#414446),.UNSPECIFIED.,.F.,.F.,(4,3,3,3,3,3,3,3,4),(0.,
2.85550478878828E-5,4.78559032675581E-5,6.34108981925978E-5,7.91451746296063E-5,
9.26886647080584E-5,0.000106465540580229,0.000127678760141081,0.000152977955413167),
 .UNSPECIFIED.);
#25938=B_SPLINE_CURVE_WITH_KNOTS('',3,(#414454,#414455,#414456,#414457,
#414458,#414459,#414460,#414461,#414462,#414463,#414464,#414465,#414466,
#414467,#414468,#414469,#414470,#414471,#414472,#414473,#414474,#414475,
#414476,#414477,#414478),.UNSPECIFIED.,.F.,.F.,(4,3,3,3,3,3,3,3,4),(0.,
2.85550478878825E-5,4.78559032675575E-5,6.34108981925973E-5,7.91451746296055E-5,
9.26886647080577E-5,0.000106465540580229,0.000127678760141081,0.000152977955413166),
 .UNSPECIFIED.);
#25939=B_SPLINE_CURVE_WITH_KNOTS('',3,(#414486,#414487,#414488,#414489,
#414490,#414491,#414492,#414493,#414494,#414495,#414496,#414497,#414498,
#414499,#414500,#414501,#414502,#414503,#414504,#414505,#414506,#414507,
#414508,#414509,#414510),.UNSPECIFIED.,.F.,.F.,(4,3,3,3,3,3,3,3,4),(0.,
2.85550478878825E-5,4.78559032675577E-5,6.34108981925977E-5,7.91451746296061E-5,
9.2688664708058E-5,0.000106465540580229,0.000127678760141081,0.000152977955413166),
 .UNSPECIFIED.);
#25940=B_SPLINE_CURVE_WITH_KNOTS('',3,(#414518,#414519,#414520,#414521,
#414522,#414523,#414524,#414525,#414526,#414527,#414528,#414529,#414530,
#414531,#414532,#414533,#414534,#414535,#414536,#414537,#414538,#414539,
#414540,#414541,#414542),.UNSPECIFIED.,.F.,.F.,(4,3,3,3,3,3,3,3,4),(0.,
2.85550478878828E-5,4.78559032675575E-5,6.34108981925974E-5,7.91451746296058E-5,
9.26886647080578E-5,0.000106465540580229,0.000127678760141081,0.000152977955413166),
 .UNSPECIFIED.);
#25941=B_SPLINE_CURVE_WITH_KNOTS('',3,(#414550,#414551,#414552,#414553,
#414554,#414555,#414556,#414557,#414558,#414559,#414560,#414561,#414562,
#414563,#414564,#414565,#414566,#414567,#414568,#414569,#414570,#414571,
#414572,#414573,#414574),.UNSPECIFIED.,.F.,.F.,(4,3,3,3,3,3,3,3,4),(0.,
2.85550478878827E-5,4.78559032675581E-5,6.34108981925978E-5,7.9145174629606E-5,
9.26886647080583E-5,0.000106465540580229,0.000127678760141081,0.000152977955413166),
 .UNSPECIFIED.);
#25942=B_SPLINE_CURVE_WITH_KNOTS('',3,(#414582,#414583,#414584,#414585,
#414586,#414587,#414588,#414589,#414590,#414591,#414592,#414593,#414594,
#414595,#414596,#414597,#414598,#414599,#414600,#414601,#414602,#414603,
#414604,#414605,#414606),.UNSPECIFIED.,.F.,.F.,(4,3,3,3,3,3,3,3,4),(0.,
2.85550478878827E-5,4.78559032675578E-5,6.34108981925974E-5,7.91451746296058E-5,
9.26886647080578E-5,0.000106465540580229,0.00012767876014108,0.000152977955413166),
 .UNSPECIFIED.);
#25943=B_SPLINE_CURVE_WITH_KNOTS('',3,(#414614,#414615,#414616,#414617,
#414618,#414619,#414620,#414621,#414622,#414623,#414624,#414625,#414626,
#414627,#414628,#414629,#414630,#414631,#414632,#414633,#414634,#414635,
#414636,#414637,#414638),.UNSPECIFIED.,.F.,.F.,(4,3,3,3,3,3,3,3,4),(0.,
2.85550478878825E-5,4.78559032675576E-5,6.34108981925974E-5,7.91451746296056E-5,
9.26886647080575E-5,0.000106465540580228,0.00012767876014108,0.000152977955413165),
 .UNSPECIFIED.);
#25944=B_SPLINE_CURVE_WITH_KNOTS('',3,(#414646,#414647,#414648,#414649,
#414650,#414651,#414652,#414653,#414654,#414655,#414656,#414657,#414658,
#414659,#414660,#414661,#414662,#414663,#414664,#414665,#414666,#414667,
#414668,#414669,#414670),.UNSPECIFIED.,.F.,.F.,(4,3,3,3,3,3,3,3,4),(0.,
2.85550478878826E-5,4.78559032675575E-5,6.34108981925975E-5,7.91451746296052E-5,
9.26886647080576E-5,0.000106465540580228,0.00012767876014108,0.000152977955413165),
 .UNSPECIFIED.);
#25945=B_SPLINE_CURVE_WITH_KNOTS('',3,(#414678,#414679,#414680,#414681,
#414682,#414683,#414684,#414685,#414686,#414687,#414688,#414689,#414690,
#414691,#414692,#414693,#414694,#414695,#414696,#414697,#414698,#414699,
#414700,#414701,#414702),.UNSPECIFIED.,.F.,.F.,(4,3,3,3,3,3,3,3,4),(0.,
2.85550478878826E-5,4.78559032675576E-5,6.34108981925974E-5,7.91451746296057E-5,
9.26886647080577E-5,0.000106465540580229,0.00012767876014108,0.000152977955413165),
 .UNSPECIFIED.);
#25946=B_SPLINE_CURVE_WITH_KNOTS('',3,(#414710,#414711,#414712,#414713,
#414714,#414715,#414716,#414717,#414718,#414719,#414720,#414721,#414722,
#414723,#414724,#414725,#414726,#414727,#414728,#414729,#414730,#414731,
#414732,#414733,#414734),.UNSPECIFIED.,.F.,.F.,(4,3,3,3,3,3,3,3,4),(0.,
2.85550478878829E-5,4.78559032675581E-5,6.34108981925978E-5,7.91451746296064E-5,
9.26886647080586E-5,0.000106465540580229,0.000127678760141081,0.000152977955413166),
 .UNSPECIFIED.);
#25947=B_SPLINE_CURVE_WITH_KNOTS('',3,(#414742,#414743,#414744,#414745,
#414746,#414747,#414748,#414749,#414750,#414751,#414752,#414753,#414754,
#414755,#414756,#414757,#414758,#414759,#414760,#414761,#414762,#414763,
#414764,#414765,#414766),.UNSPECIFIED.,.F.,.F.,(4,3,3,3,3,3,3,3,4),(0.,
2.85550478878828E-5,4.78559032675579E-5,6.34108981925976E-5,7.9145174629606E-5,
9.26886647080582E-5,0.000106465540580229,0.000127678760141081,0.000152977955413167),
 .UNSPECIFIED.);
#25948=B_SPLINE_CURVE_WITH_KNOTS('',3,(#414774,#414775,#414776,#414777,
#414778,#414779,#414780,#414781,#414782,#414783,#414784,#414785,#414786,
#414787,#414788,#414789,#414790,#414791,#414792,#414793,#414794,#414795,
#414796,#414797,#414798),.UNSPECIFIED.,.F.,.F.,(4,3,3,3,3,3,3,3,4),(0.,
2.85550478878827E-5,4.78559032675579E-5,6.34108981925975E-5,7.9145174629606E-5,
9.26886647080579E-5,0.000106465540580229,0.000127678760141081,0.000152977955413166),
 .UNSPECIFIED.);
#25949=B_SPLINE_CURVE_WITH_KNOTS('',3,(#414806,#414807,#414808,#414809,
#414810,#414811,#414812,#414813,#414814,#414815,#414816,#414817,#414818,
#414819,#414820,#414821,#414822,#414823,#414824,#414825,#414826,#414827,
#414828,#414829,#414830),.UNSPECIFIED.,.F.,.F.,(4,3,3,3,3,3,3,3,4),(0.,
2.85550478878826E-5,4.78559032675578E-5,6.34108981925975E-5,7.91451746296059E-5,
9.26886647080579E-5,0.000106465540580229,0.00012767876014108,0.000152977955413166),
 .UNSPECIFIED.);
#25950=B_SPLINE_CURVE_WITH_KNOTS('',3,(#414838,#414839,#414840,#414841,
#414842,#414843,#414844,#414845,#414846,#414847,#414848,#414849,#414850,
#414851,#414852,#414853,#414854,#414855,#414856,#414857,#414858,#414859,
#414860,#414861,#414862),.UNSPECIFIED.,.F.,.F.,(4,3,3,3,3,3,3,3,4),(0.,
2.85550478878826E-5,4.78559032675579E-5,6.34108981925975E-5,7.91451746296058E-5,
9.26886647080578E-5,0.000106465540580229,0.000127678760141081,0.000152977955413166),
 .UNSPECIFIED.);
#25951=B_SPLINE_CURVE_WITH_KNOTS('',3,(#414870,#414871,#414872,#414873,
#414874,#414875,#414876,#414877,#414878,#414879,#414880,#414881,#414882,
#414883,#414884,#414885,#414886,#414887,#414888,#414889,#414890,#414891,
#414892,#414893,#414894),.UNSPECIFIED.,.F.,.F.,(4,3,3,3,3,3,3,3,4),(0.,
2.85550478878828E-5,4.78559032675579E-5,6.34108981925976E-5,7.91451746296061E-5,
9.26886647080581E-5,0.000106465540580229,0.000127678760141081,0.000152977955413166),
 .UNSPECIFIED.);
#25952=B_SPLINE_CURVE_WITH_KNOTS('',3,(#414902,#414903,#414904,#414905,
#414906,#414907,#414908,#414909,#414910,#414911,#414912,#414913,#414914,
#414915,#414916,#414917,#414918,#414919,#414920,#414921,#414922,#414923,
#414924,#414925,#414926),.UNSPECIFIED.,.F.,.F.,(4,3,3,3,3,3,3,3,4),(0.,
2.85550478878828E-5,4.78559032675579E-5,6.34108981925974E-5,7.91451746296058E-5,
9.26886647080578E-5,0.000106465540580229,0.000127678760141081,0.000152977955413166),
 .UNSPECIFIED.);
#25953=B_SPLINE_CURVE_WITH_KNOTS('',3,(#414934,#414935,#414936,#414937,
#414938,#414939,#414940,#414941,#414942,#414943,#414944,#414945,#414946,
#414947,#414948,#414949,#414950,#414951,#414952,#414953,#414954,#414955,
#414956,#414957,#414958),.UNSPECIFIED.,.F.,.F.,(4,3,3,3,3,3,3,3,4),(0.,
2.85550478878826E-5,4.78559032675577E-5,6.34108981925974E-5,7.91451746296057E-5,
9.26886647080578E-5,0.000106465540580229,0.00012767876014108,0.000152977955413166),
 .UNSPECIFIED.);
#25954=B_SPLINE_CURVE_WITH_KNOTS('',3,(#414966,#414967,#414968,#414969,
#414970,#414971,#414972,#414973,#414974,#414975,#414976,#414977,#414978,
#414979,#414980,#414981,#414982,#414983,#414984,#414985,#414986,#414987,
#414988,#414989,#414990),.UNSPECIFIED.,.F.,.F.,(4,3,3,3,3,3,3,3,4),(0.,
2.85550478878827E-5,4.78559032675582E-5,6.34108981925978E-5,7.91451746296061E-5,
9.26886647080581E-5,0.000106465540580229,0.000127678760141081,0.000152977955413166),
 .UNSPECIFIED.);
#25955=B_SPLINE_CURVE_WITH_KNOTS('',3,(#414998,#414999,#415000,#415001,
#415002,#415003,#415004,#415005,#415006,#415007,#415008,#415009,#415010,
#415011,#415012,#415013,#415014,#415015,#415016,#415017,#415018,#415019,
#415020,#415021,#415022),.UNSPECIFIED.,.F.,.F.,(4,3,3,3,3,3,3,3,4),(0.,
2.8555047887883E-5,4.7855903267558E-5,6.34108981925975E-5,7.9145174629606E-5,
9.2688664708058E-5,0.000106465540580229,0.000127678760141081,0.000152977955413166),
 .UNSPECIFIED.);
#25956=B_SPLINE_CURVE_WITH_KNOTS('',3,(#415030,#415031,#415032,#415033,
#415034,#415035,#415036,#415037,#415038,#415039,#415040,#415041,#415042,
#415043,#415044,#415045,#415046,#415047,#415048,#415049,#415050,#415051,
#415052,#415053,#415054),.UNSPECIFIED.,.F.,.F.,(4,3,3,3,3,3,3,3,4),(0.,
2.85550478878827E-5,4.78559032675577E-5,6.34108981925973E-5,7.91451746296059E-5,
9.2688664708058E-5,0.000106465540580229,0.000127678760141081,0.000152977955413166),
 .UNSPECIFIED.);
#25957=B_SPLINE_CURVE_WITH_KNOTS('',3,(#415062,#415063,#415064,#415065,
#415066,#415067,#415068,#415069,#415070,#415071,#415072,#415073,#415074,
#415075,#415076,#415077,#415078,#415079,#415080,#415081,#415082,#415083,
#415084,#415085,#415086),.UNSPECIFIED.,.F.,.F.,(4,3,3,3,3,3,3,3,4),(0.,
2.85550478878828E-5,4.78559032675577E-5,6.34108981925974E-5,7.91451746296058E-5,
9.26886647080579E-5,0.000106465540580229,0.000127678760141081,0.000152977955413166),
 .UNSPECIFIED.);
#25958=B_SPLINE_CURVE_WITH_KNOTS('',3,(#415094,#415095,#415096,#415097,
#415098,#415099,#415100,#415101,#415102,#415103,#415104,#415105,#415106,
#415107,#415108,#415109,#415110,#415111,#415112,#415113,#415114,#415115,
#415116,#415117,#415118),.UNSPECIFIED.,.F.,.F.,(4,3,3,3,3,3,3,3,4),(0.,
2.85550478878826E-5,4.78559032675579E-5,6.34108981925973E-5,7.9145174629606E-5,
9.26886647080578E-5,0.000106465540580229,0.000127678760141081,0.000152977955413166),
 .UNSPECIFIED.);
#25959=B_SPLINE_CURVE_WITH_KNOTS('',3,(#415126,#415127,#415128,#415129,
#415130,#415131,#415132,#415133,#415134,#415135,#415136,#415137,#415138,
#415139,#415140,#415141,#415142,#415143,#415144,#415145,#415146,#415147,
#415148,#415149,#415150),.UNSPECIFIED.,.F.,.F.,(4,3,3,3,3,3,3,3,4),(0.,
2.85550478878826E-5,4.78559032675574E-5,6.3410898192597E-5,7.91451746296055E-5,
9.26886647080575E-5,0.000106465540580229,0.00012767876014108,0.000152977955413165),
 .UNSPECIFIED.);
#25960=B_SPLINE_CURVE_WITH_KNOTS('',3,(#415158,#415159,#415160,#415161,
#415162,#415163,#415164,#415165,#415166,#415167,#415168,#415169,#415170,
#415171,#415172,#415173,#415174,#415175,#415176,#415177,#415178,#415179,
#415180,#415181,#415182),.UNSPECIFIED.,.F.,.F.,(4,3,3,3,3,3,3,3,4),(0.,
2.85550478878822E-5,4.78559032675576E-5,6.34108981925971E-5,7.91451746296059E-5,
9.26886647080578E-5,0.000106465540580228,0.00012767876014108,0.000152977955413165),
 .UNSPECIFIED.);
#25961=B_SPLINE_CURVE_WITH_KNOTS('',3,(#415190,#415191,#415192,#415193,
#415194,#415195,#415196,#415197,#415198,#415199,#415200,#415201,#415202,
#415203,#415204,#415205,#415206,#415207,#415208,#415209,#415210,#415211,
#415212,#415213,#415214),.UNSPECIFIED.,.F.,.F.,(4,3,3,3,3,3,3,3,4),(0.,
2.85550478878825E-5,4.78559032675578E-5,6.34108981925973E-5,7.91451746296057E-5,
9.26886647080579E-5,0.000106465540580229,0.00012767876014108,0.000152977955413165),
 .UNSPECIFIED.);
#25962=B_SPLINE_CURVE_WITH_KNOTS('',3,(#415222,#415223,#415224,#415225,
#415226,#415227,#415228,#415229,#415230,#415231,#415232,#415233,#415234,
#415235,#415236,#415237,#415238,#415239,#415240,#415241,#415242,#415243,
#415244,#415245,#415246),.UNSPECIFIED.,.F.,.F.,(4,3,3,3,3,3,3,3,4),(0.,
2.85550478878828E-5,4.7855903267558E-5,6.34108981925976E-5,7.91451746296062E-5,
9.2688664708058E-5,0.000106465540580229,0.000127678760141081,0.000152977955413166),
 .UNSPECIFIED.);
#25963=B_SPLINE_CURVE_WITH_KNOTS('',3,(#415254,#415255,#415256,#415257,
#415258,#415259,#415260,#415261,#415262,#415263,#415264,#415265,#415266,
#415267,#415268,#415269,#415270,#415271,#415272,#415273,#415274,#415275,
#415276,#415277,#415278),.UNSPECIFIED.,.F.,.F.,(4,3,3,3,3,3,3,3,4),(0.,
2.85550478878827E-5,4.78559032675579E-5,6.34108981925976E-5,7.91451746296059E-5,
9.2688664708058E-5,0.000106465540580229,0.00012767876014108,0.000152977955413165),
 .UNSPECIFIED.);
#25964=B_SPLINE_CURVE_WITH_KNOTS('',3,(#415286,#415287,#415288,#415289,
#415290,#415291,#415292,#415293,#415294,#415295,#415296,#415297,#415298,
#415299,#415300,#415301,#415302,#415303,#415304,#415305,#415306,#415307,
#415308,#415309,#415310),.UNSPECIFIED.,.F.,.F.,(4,3,3,3,3,3,3,3,4),(0.,
2.85550478878827E-5,4.78559032675579E-5,6.34108981925976E-5,7.91451746296062E-5,
9.2688664708058E-5,0.000106465540580229,0.000127678760141081,0.000152977955413166),
 .UNSPECIFIED.);
#25965=B_SPLINE_CURVE_WITH_KNOTS('',3,(#415318,#415319,#415320,#415321,
#415322,#415323,#415324,#415325,#415326,#415327,#415328,#415329,#415330,
#415331,#415332,#415333,#415334,#415335,#415336,#415337,#415338,#415339,
#415340,#415341,#415342),.UNSPECIFIED.,.F.,.F.,(4,3,3,3,3,3,3,3,4),(0.,
2.85550478878825E-5,4.78559032675579E-5,6.34108981925974E-5,7.91451746296058E-5,
9.26886647080579E-5,0.000106465540580229,0.000127678760141081,0.000152977955413166),
 .UNSPECIFIED.);
#25966=B_SPLINE_CURVE_WITH_KNOTS('',3,(#415350,#415351,#415352,#415353,
#415354,#415355,#415356,#415357,#415358,#415359,#415360,#415361,#415362,
#415363,#415364,#415365,#415366,#415367,#415368,#415369,#415370,#415371,
#415372,#415373,#415374),.UNSPECIFIED.,.F.,.F.,(4,3,3,3,3,3,3,3,4),(0.,
2.85550478878828E-5,4.78559032675578E-5,6.34108981925973E-5,7.91451746296057E-5,
9.26886647080578E-5,0.000106465540580228,0.00012767876014108,0.000152977955413166),
 .UNSPECIFIED.);
#25967=B_SPLINE_CURVE_WITH_KNOTS('',3,(#415382,#415383,#415384,#415385,
#415386,#415387,#415388,#415389,#415390,#415391,#415392,#415393,#415394,
#415395,#415396,#415397,#415398,#415399,#415400,#415401,#415402,#415403,
#415404,#415405,#415406),.UNSPECIFIED.,.F.,.F.,(4,3,3,3,3,3,3,3,4),(0.,
2.85550478878823E-5,4.78559032675575E-5,6.34108981925972E-5,7.91451746296055E-5,
9.26886647080575E-5,0.000106465540580228,0.00012767876014108,0.000152977955413165),
 .UNSPECIFIED.);
#25968=B_SPLINE_CURVE_WITH_KNOTS('',3,(#415414,#415415,#415416,#415417,
#415418,#415419,#415420,#415421,#415422,#415423,#415424,#415425,#415426,
#415427,#415428,#415429,#415430,#415431,#415432,#415433,#415434,#415435,
#415436,#415437,#415438),.UNSPECIFIED.,.F.,.F.,(4,3,3,3,3,3,3,3,4),(0.,
2.85550478878827E-5,4.78559032675578E-5,6.34108981925974E-5,7.91451746296058E-5,
9.26886647080577E-5,0.000106465540580229,0.00012767876014108,0.000152977955413165),
 .UNSPECIFIED.);
#25969=B_SPLINE_CURVE_WITH_KNOTS('',3,(#415446,#415447,#415448,#415449,
#415450,#415451,#415452,#415453,#415454,#415455,#415456,#415457,#415458,
#415459,#415460,#415461,#415462,#415463,#415464,#415465,#415466,#415467,
#415468,#415469,#415470),.UNSPECIFIED.,.F.,.F.,(4,3,3,3,3,3,3,3,4),(0.,
2.85550478878824E-5,4.78559032675577E-5,6.34108981925974E-5,7.91451746296058E-5,
9.26886647080578E-5,0.000106465540580229,0.000127678760141081,0.000152977955413166),
 .UNSPECIFIED.);
#25970=B_SPLINE_CURVE_WITH_KNOTS('',3,(#415478,#415479,#415480,#415481,
#415482,#415483,#415484,#415485,#415486,#415487,#415488,#415489,#415490,
#415491,#415492,#415493,#415494,#415495,#415496,#415497,#415498,#415499,
#415500,#415501,#415502),.UNSPECIFIED.,.F.,.F.,(4,3,3,3,3,3,3,3,4),(0.,
2.85550478878823E-5,4.78559032675579E-5,6.34108981925974E-5,7.91451746296058E-5,
9.26886647080579E-5,0.000106465540580229,0.000127678760141081,0.000152977955413166),
 .UNSPECIFIED.);
#25971=B_SPLINE_CURVE_WITH_KNOTS('',3,(#415517,#415518,#415519,#415520,
#415521,#415522,#415523,#415524,#415525,#415526,#415527,#415528,#415529,
#415530,#415531,#415532,#415533,#415534,#415535,#415536,#415537,#415538,
#415539,#415540,#415541),.UNSPECIFIED.,.F.,.F.,(4,3,3,3,3,3,3,3,4),(0.,
2.85550478878826E-5,4.78559032675578E-5,6.34108981925975E-5,7.91451746296059E-5,
9.26886647080581E-5,0.000106465540580229,0.000127678760141081,0.000152977955413166),
 .UNSPECIFIED.);
#25972=B_SPLINE_CURVE_WITH_KNOTS('',3,(#415549,#415550,#415551,#415552,
#415553,#415554,#415555,#415556,#415557,#415558,#415559,#415560,#415561,
#415562,#415563,#415564,#415565,#415566,#415567,#415568,#415569,#415570,
#415571,#415572,#415573),.UNSPECIFIED.,.F.,.F.,(4,3,3,3,3,3,3,3,4),(0.,
2.85550478878824E-5,4.78559032675578E-5,6.34108981925974E-5,7.91451746296058E-5,
9.26886647080579E-5,0.000106465540580229,0.000127678760141081,0.000152977955413166),
 .UNSPECIFIED.);
#25973=B_SPLINE_CURVE_WITH_KNOTS('',3,(#415581,#415582,#415583,#415584,
#415585,#415586,#415587,#415588,#415589,#415590,#415591,#415592,#415593,
#415594,#415595,#415596,#415597,#415598,#415599,#415600,#415601,#415602,
#415603,#415604,#415605),.UNSPECIFIED.,.F.,.F.,(4,3,3,3,3,3,3,3,4),(0.,
2.85550478878827E-5,4.78559032675578E-5,6.34108981925973E-5,7.91451746296058E-5,
9.26886647080578E-5,0.000106465540580229,0.000127678760141081,0.000152977955413166),
 .UNSPECIFIED.);
#25974=B_SPLINE_CURVE_WITH_KNOTS('',3,(#415613,#415614,#415615,#415616,
#415617,#415618,#415619,#415620,#415621,#415622,#415623,#415624,#415625,
#415626,#415627,#415628,#415629,#415630,#415631,#415632,#415633,#415634,
#415635,#415636,#415637),.UNSPECIFIED.,.F.,.F.,(4,3,3,3,3,3,3,3,4),(0.,
2.85550478878828E-5,4.78559032675581E-5,6.34108981925975E-5,7.91451746296059E-5,
9.26886647080578E-5,0.000106465540580229,0.00012767876014108,0.000152977955413165),
 .UNSPECIFIED.);
#25975=B_SPLINE_CURVE_WITH_KNOTS('',3,(#415645,#415646,#415647,#415648,
#415649,#415650,#415651,#415652,#415653,#415654,#415655,#415656,#415657,
#415658,#415659,#415660,#415661,#415662,#415663,#415664,#415665,#415666,
#415667,#415668,#415669),.UNSPECIFIED.,.F.,.F.,(4,3,3,3,3,3,3,3,4),(0.,
2.85550478878827E-5,4.78559032675577E-5,6.34108981925976E-5,7.91451746296059E-5,
9.26886647080578E-5,0.000106465540580229,0.00012767876014108,0.000152977955413166),
 .UNSPECIFIED.);
#25976=B_SPLINE_CURVE_WITH_KNOTS('',3,(#415677,#415678,#415679,#415680,
#415681,#415682,#415683,#415684,#415685,#415686,#415687,#415688,#415689,
#415690,#415691,#415692,#415693,#415694,#415695,#415696,#415697,#415698,
#415699,#415700,#415701),.UNSPECIFIED.,.F.,.F.,(4,3,3,3,3,3,3,3,4),(0.,
2.85550478878825E-5,4.78559032675577E-5,6.34108981925973E-5,7.91451746296055E-5,
9.26886647080577E-5,0.000106465540580229,0.00012767876014108,0.000152977955413165),
 .UNSPECIFIED.);
#25977=B_SPLINE_CURVE_WITH_KNOTS('',3,(#415709,#415710,#415711,#415712,
#415713,#415714,#415715,#415716,#415717,#415718,#415719,#415720,#415721,
#415722,#415723,#415724,#415725,#415726,#415727,#415728,#415729,#415730,
#415731,#415732,#415733),.UNSPECIFIED.,.F.,.F.,(4,3,3,3,3,3,3,3,4),(0.,
2.85550478878829E-5,4.78559032675578E-5,6.34108981925974E-5,7.91451746296059E-5,
9.26886647080576E-5,0.000106465540580228,0.00012767876014108,0.000152977955413165),
 .UNSPECIFIED.);
#25978=B_SPLINE_CURVE_WITH_KNOTS('',3,(#415741,#415742,#415743,#415744,
#415745,#415746,#415747,#415748,#415749,#415750,#415751,#415752,#415753,
#415754,#415755,#415756,#415757,#415758,#415759,#415760,#415761,#415762,
#415763,#415764,#415765),.UNSPECIFIED.,.F.,.F.,(4,3,3,3,3,3,3,3,4),(0.,
2.85550478878826E-5,4.78559032675578E-5,6.34108981925975E-5,7.91451746296058E-5,
9.26886647080576E-5,0.000106465540580229,0.000127678760141081,0.000152977955413166),
 .UNSPECIFIED.);
#25979=B_SPLINE_CURVE_WITH_KNOTS('',3,(#415773,#415774,#415775,#415776,
#415777,#415778,#415779,#415780,#415781,#415782,#415783,#415784,#415785,
#415786,#415787,#415788,#415789,#415790,#415791,#415792,#415793,#415794,
#415795,#415796,#415797),.UNSPECIFIED.,.F.,.F.,(4,3,3,3,3,3,3,3,4),(0.,
2.85550478878825E-5,4.78559032675576E-5,6.34108981925972E-5,7.91451746296057E-5,
9.26886647080577E-5,0.000106465540580229,0.000127678760141081,0.000152977955413166),
 .UNSPECIFIED.);
#25980=B_SPLINE_CURVE_WITH_KNOTS('',3,(#415805,#415806,#415807,#415808,
#415809,#415810,#415811,#415812,#415813,#415814,#415815,#415816,#415817,
#415818,#415819,#415820,#415821,#415822,#415823,#415824,#415825,#415826,
#415827,#415828,#415829),.UNSPECIFIED.,.F.,.F.,(4,3,3,3,3,3,3,3,4),(0.,
2.85550478878827E-5,4.7855903267558E-5,6.34108981925976E-5,7.9145174629606E-5,
9.26886647080582E-5,0.000106465540580229,0.000127678760141081,0.000152977955413166),
 .UNSPECIFIED.);
#25981=B_SPLINE_CURVE_WITH_KNOTS('',3,(#415837,#415838,#415839,#415840,
#415841,#415842,#415843,#415844,#415845,#415846,#415847,#415848,#415849,
#415850,#415851,#415852,#415853,#415854,#415855,#415856,#415857,#415858,
#415859,#415860,#415861),.UNSPECIFIED.,.F.,.F.,(4,3,3,3,3,3,3,3,4),(0.,
2.85550478878827E-5,4.78559032675578E-5,6.34108981925974E-5,7.9145174629606E-5,
9.26886647080581E-5,0.000106465540580229,0.000127678760141081,0.000152977955413166),
 .UNSPECIFIED.);
#25982=B_SPLINE_CURVE_WITH_KNOTS('',3,(#415869,#415870,#415871,#415872,
#415873,#415874,#415875,#415876,#415877,#415878,#415879,#415880,#415881,
#415882,#415883,#415884,#415885,#415886,#415887,#415888,#415889,#415890,
#415891,#415892,#415893),.UNSPECIFIED.,.F.,.F.,(4,3,3,3,3,3,3,3,4),(0.,
2.85550478878826E-5,4.78559032675578E-5,6.34108981925974E-5,7.91451746296056E-5,
9.26886647080576E-5,0.000106465540580228,0.000127678760141081,0.000152977955413165),
 .UNSPECIFIED.);
#25983=B_SPLINE_CURVE_WITH_KNOTS('',3,(#415901,#415902,#415903,#415904,
#415905,#415906,#415907,#415908,#415909,#415910,#415911,#415912,#415913,
#415914,#415915,#415916,#415917,#415918,#415919,#415920,#415921,#415922,
#415923,#415924,#415925),.UNSPECIFIED.,.F.,.F.,(4,3,3,3,3,3,3,3,4),(0.,
2.85550478878827E-5,4.7855903267558E-5,6.34108981925976E-5,7.91451746296059E-5,
9.26886647080581E-5,0.000106465540580229,0.000127678760141081,0.000152977955413166),
 .UNSPECIFIED.);
#25984=B_SPLINE_CURVE_WITH_KNOTS('',3,(#415933,#415934,#415935,#415936,
#415937,#415938,#415939,#415940,#415941,#415942,#415943,#415944,#415945,
#415946,#415947,#415948,#415949,#415950,#415951,#415952,#415953,#415954,
#415955,#415956,#415957),.UNSPECIFIED.,.F.,.F.,(4,3,3,3,3,3,3,3,4),(0.,
2.85550478878827E-5,4.78559032675581E-5,6.34108981925976E-5,7.91451746296061E-5,
9.2688664708058E-5,0.000106465540580229,0.000127678760141081,0.000152977955413166),
 .UNSPECIFIED.);
#25985=B_SPLINE_CURVE_WITH_KNOTS('',3,(#415965,#415966,#415967,#415968,
#415969,#415970,#415971,#415972,#415973,#415974,#415975,#415976,#415977,
#415978,#415979,#415980,#415981,#415982,#415983,#415984,#415985,#415986,
#415987,#415988,#415989),.UNSPECIFIED.,.F.,.F.,(4,3,3,3,3,3,3,3,4),(0.,
2.85550478878826E-5,4.7855903267558E-5,6.34108981925975E-5,7.91451746296057E-5,
9.26886647080582E-5,0.000106465540580229,0.000127678760141081,0.000152977955413166),
 .UNSPECIFIED.);
#25986=B_SPLINE_CURVE_WITH_KNOTS('',3,(#415997,#415998,#415999,#416000,
#416001,#416002,#416003,#416004,#416005,#416006,#416007,#416008,#416009,
#416010,#416011,#416012,#416013,#416014,#416015,#416016,#416017,#416018,
#416019,#416020,#416021),.UNSPECIFIED.,.F.,.F.,(4,3,3,3,3,3,3,3,4),(0.,
2.85550478878828E-5,4.78559032675581E-5,6.34108981925976E-5,7.91451746296059E-5,
9.26886647080581E-5,0.000106465540580229,0.000127678760141081,0.000152977955413166),
 .UNSPECIFIED.);
#25987=B_SPLINE_CURVE_WITH_KNOTS('',3,(#416029,#416030,#416031,#416032,
#416033,#416034,#416035,#416036,#416037,#416038,#416039,#416040,#416041,
#416042,#416043,#416044,#416045,#416046,#416047,#416048,#416049,#416050,
#416051,#416052,#416053),.UNSPECIFIED.,.F.,.F.,(4,3,3,3,3,3,3,3,4),(0.,
2.85550478878829E-5,4.7855903267558E-5,6.34108981925976E-5,7.91451746296061E-5,
9.26886647080581E-5,0.000106465540580229,0.000127678760141081,0.000152977955413166),
 .UNSPECIFIED.);
#25988=B_SPLINE_CURVE_WITH_KNOTS('',3,(#416061,#416062,#416063,#416064,
#416065,#416066,#416067,#416068,#416069,#416070,#416071,#416072,#416073,
#416074,#416075,#416076,#416077,#416078,#416079,#416080,#416081,#416082,
#416083,#416084,#416085),.UNSPECIFIED.,.F.,.F.,(4,3,3,3,3,3,3,3,4),(0.,
2.85550478878825E-5,4.78559032675577E-5,6.34108981925974E-5,7.91451746296058E-5,
9.26886647080578E-5,0.000106465540580228,0.000127678760141081,0.000152977955413166),
 .UNSPECIFIED.);
#25989=B_SPLINE_CURVE_WITH_KNOTS('',3,(#416093,#416094,#416095,#416096,
#416097,#416098,#416099,#416100,#416101,#416102,#416103,#416104,#416105,
#416106,#416107,#416108,#416109,#416110,#416111,#416112,#416113,#416114,
#416115,#416116,#416117),.UNSPECIFIED.,.F.,.F.,(4,3,3,3,3,3,3,3,4),(0.,
2.85550478878829E-5,4.7855903267558E-5,6.34108981925975E-5,7.91451746296059E-5,
9.26886647080578E-5,0.000106465540580229,0.000127678760141081,0.000152977955413166),
 .UNSPECIFIED.);
#25990=B_SPLINE_CURVE_WITH_KNOTS('',3,(#416125,#416126,#416127,#416128,
#416129,#416130,#416131,#416132,#416133,#416134,#416135,#416136,#416137,
#416138,#416139,#416140,#416141,#416142,#416143,#416144,#416145,#416146,
#416147,#416148,#416149),.UNSPECIFIED.,.F.,.F.,(4,3,3,3,3,3,3,3,4),(0.,
2.85550478878826E-5,4.78559032675579E-5,6.34108981925974E-5,7.91451746296059E-5,
9.2688664708058E-5,0.000106465540580229,0.000127678760141081,0.000152977955413166),
 .UNSPECIFIED.);
#25991=B_SPLINE_CURVE_WITH_KNOTS('',3,(#416157,#416158,#416159,#416160,
#416161,#416162,#416163,#416164,#416165,#416166,#416167,#416168,#416169,
#416170,#416171,#416172,#416173,#416174,#416175,#416176,#416177,#416178,
#416179,#416180,#416181),.UNSPECIFIED.,.F.,.F.,(4,3,3,3,3,3,3,3,4),(0.,
2.85550478878828E-5,4.78559032675581E-5,6.34108981925976E-5,7.91451746296059E-5,
9.2688664708058E-5,0.000106465540580229,0.000127678760141081,0.000152977955413166),
 .UNSPECIFIED.);
#25992=B_SPLINE_CURVE_WITH_KNOTS('',3,(#416189,#416190,#416191,#416192,
#416193,#416194,#416195,#416196,#416197,#416198,#416199,#416200,#416201,
#416202,#416203,#416204,#416205,#416206,#416207,#416208,#416209,#416210,
#416211,#416212,#416213),.UNSPECIFIED.,.F.,.F.,(4,3,3,3,3,3,3,3,4),(0.,
2.85550478878829E-5,4.7855903267558E-5,6.34108981925977E-5,7.9145174629606E-5,
9.26886647080579E-5,0.000106465540580229,0.000127678760141081,0.000152977955413166),
 .UNSPECIFIED.);
#25993=B_SPLINE_CURVE_WITH_KNOTS('',3,(#416221,#416222,#416223,#416224,
#416225,#416226,#416227,#416228,#416229,#416230,#416231,#416232,#416233,
#416234,#416235,#416236,#416237,#416238,#416239,#416240,#416241,#416242,
#416243,#416244,#416245),.UNSPECIFIED.,.F.,.F.,(4,3,3,3,3,3,3,3,4),(0.,
2.85550478878826E-5,4.78559032675575E-5,6.34108981925974E-5,7.9145174629606E-5,
9.26886647080579E-5,0.000106465540580229,0.000127678760141081,0.000152977955413166),
 .UNSPECIFIED.);
#25994=B_SPLINE_CURVE_WITH_KNOTS('',3,(#416253,#416254,#416255,#416256,
#416257,#416258,#416259,#416260,#416261,#416262,#416263,#416264,#416265,
#416266,#416267,#416268,#416269,#416270,#416271,#416272,#416273,#416274,
#416275,#416276,#416277),.UNSPECIFIED.,.F.,.F.,(4,3,3,3,3,3,3,3,4),(0.,
2.85550478878826E-5,4.78559032675579E-5,6.34108981925973E-5,7.91451746296058E-5,
9.26886647080579E-5,0.000106465540580229,0.000127678760141081,0.000152977955413166),
 .UNSPECIFIED.);
#25995=B_SPLINE_CURVE_WITH_KNOTS('',3,(#416285,#416286,#416287,#416288,
#416289,#416290,#416291,#416292,#416293,#416294,#416295,#416296,#416297,
#416298,#416299,#416300,#416301,#416302,#416303,#416304,#416305,#416306,
#416307,#416308,#416309),.UNSPECIFIED.,.F.,.F.,(4,3,3,3,3,3,3,3,4),(0.,
2.85550478878825E-5,4.78559032675578E-5,6.34108981925975E-5,7.9145174629606E-5,
9.2688664708058E-5,0.000106465540580229,0.000127678760141081,0.000152977955413166),
 .UNSPECIFIED.);
#25996=B_SPLINE_CURVE_WITH_KNOTS('',3,(#416317,#416318,#416319,#416320,
#416321,#416322,#416323,#416324,#416325,#416326,#416327,#416328,#416329,
#416330,#416331,#416332,#416333,#416334,#416335,#416336,#416337,#416338,
#416339,#416340,#416341),.UNSPECIFIED.,.F.,.F.,(4,3,3,3,3,3,3,3,4),(0.,
2.85550478878826E-5,4.7855903267558E-5,6.34108981925976E-5,7.91451746296062E-5,
9.26886647080583E-5,0.000106465540580229,0.000127678760141081,0.000152977955413167),
 .UNSPECIFIED.);
#25997=B_SPLINE_CURVE_WITH_KNOTS('',3,(#416349,#416350,#416351,#416352,
#416353,#416354,#416355,#416356,#416357,#416358,#416359,#416360,#416361,
#416362,#416363,#416364,#416365,#416366,#416367,#416368,#416369,#416370,
#416371,#416372,#416373),.UNSPECIFIED.,.F.,.F.,(4,3,3,3,3,3,3,3,4),(0.,
2.85550478878827E-5,4.78559032675575E-5,6.34108981925974E-5,7.91451746296055E-5,
9.26886647080577E-5,0.000106465540580228,0.00012767876014108,0.000152977955413165),
 .UNSPECIFIED.);
#25998=B_SPLINE_CURVE_WITH_KNOTS('',3,(#416381,#416382,#416383,#416384,
#416385,#416386,#416387,#416388,#416389,#416390,#416391,#416392,#416393,
#416394,#416395,#416396,#416397,#416398,#416399,#416400,#416401,#416402,
#416403,#416404,#416405),.UNSPECIFIED.,.F.,.F.,(4,3,3,3,3,3,3,3,4),(0.,
2.85550478878827E-5,4.78559032675578E-5,6.34108981925978E-5,7.91451746296065E-5,
9.26886647080582E-5,0.000106465540580229,0.000127678760141082,0.000152977955413167),
 .UNSPECIFIED.);
#25999=B_SPLINE_CURVE_WITH_KNOTS('',3,(#416413,#416414,#416415,#416416,
#416417,#416418,#416419,#416420,#416421,#416422,#416423,#416424,#416425,
#416426,#416427,#416428,#416429,#416430,#416431,#416432,#416433,#416434,
#416435,#416436,#416437),.UNSPECIFIED.,.F.,.F.,(4,3,3,3,3,3,3,3,4),(0.,
2.85550478878827E-5,4.78559032675576E-5,6.34108981925972E-5,7.91451746296057E-5,
9.26886647080576E-5,0.000106465540580229,0.00012767876014108,0.000152977955413166),
 .UNSPECIFIED.);
#26000=B_SPLINE_CURVE_WITH_KNOTS('',3,(#416445,#416446,#416447,#416448,
#416449,#416450,#416451,#416452,#416453,#416454,#416455,#416456,#416457,
#416458,#416459,#416460,#416461,#416462,#416463,#416464,#416465,#416466,
#416467,#416468,#416469),.UNSPECIFIED.,.F.,.F.,(4,3,3,3,3,3,3,3,4),(0.,
2.85550478878827E-5,4.78559032675579E-5,6.34108981925976E-5,7.9145174629606E-5,
9.26886647080581E-5,0.000106465540580229,0.000127678760141081,0.000152977955413166),
 .UNSPECIFIED.);
#26001=B_SPLINE_CURVE_WITH_KNOTS('',3,(#416477,#416478,#416479,#416480,
#416481,#416482,#416483,#416484,#416485,#416486,#416487,#416488,#416489,
#416490,#416491,#416492,#416493,#416494,#416495,#416496,#416497,#416498,
#416499,#416500,#416501),.UNSPECIFIED.,.F.,.F.,(4,3,3,3,3,3,3,3,4),(0.,
2.85550478878828E-5,4.78559032675579E-5,6.34108981925975E-5,7.91451746296059E-5,
9.2688664708058E-5,0.000106465540580229,0.00012767876014108,0.000152977955413165),
 .UNSPECIFIED.);
#26002=B_SPLINE_CURVE_WITH_KNOTS('',3,(#416509,#416510,#416511,#416512,
#416513,#416514,#416515,#416516,#416517,#416518,#416519,#416520,#416521,
#416522,#416523,#416524,#416525,#416526,#416527,#416528,#416529,#416530,
#416531,#416532,#416533),.UNSPECIFIED.,.F.,.F.,(4,3,3,3,3,3,3,3,4),(0.,
2.85550478878826E-5,4.78559032675578E-5,6.34108981925975E-5,7.91451746296059E-5,
9.2688664708058E-5,0.000106465540580229,0.000127678760141081,0.000152977955413166),
 .UNSPECIFIED.);
#26003=B_SPLINE_CURVE_WITH_KNOTS('',3,(#416541,#416542,#416543,#416544,
#416545,#416546,#416547,#416548,#416549,#416550,#416551,#416552,#416553,
#416554,#416555,#416556,#416557,#416558,#416559,#416560,#416561,#416562,
#416563,#416564,#416565),.UNSPECIFIED.,.F.,.F.,(4,3,3,3,3,3,3,3,4),(0.,
2.85550478878828E-5,4.78559032675578E-5,6.34108981925975E-5,7.9145174629606E-5,
9.26886647080578E-5,0.000106465540580229,0.000127678760141081,0.000152977955413166),
 .UNSPECIFIED.);
#26004=B_SPLINE_CURVE_WITH_KNOTS('',3,(#416573,#416574,#416575,#416576,
#416577,#416578,#416579,#416580,#416581,#416582,#416583,#416584,#416585,
#416586,#416587,#416588,#416589,#416590,#416591,#416592,#416593,#416594,
#416595,#416596,#416597),.UNSPECIFIED.,.F.,.F.,(4,3,3,3,3,3,3,3,4),(0.,
2.85550478878824E-5,4.78559032675577E-5,6.34108981925973E-5,7.91451746296057E-5,
9.26886647080576E-5,0.000106465540580228,0.00012767876014108,0.000152977955413165),
 .UNSPECIFIED.);
#26005=B_SPLINE_CURVE_WITH_KNOTS('',3,(#416605,#416606,#416607,#416608,
#416609,#416610,#416611,#416612,#416613,#416614,#416615,#416616,#416617,
#416618,#416619,#416620,#416621,#416622,#416623,#416624,#416625,#416626,
#416627,#416628,#416629),.UNSPECIFIED.,.F.,.F.,(4,3,3,3,3,3,3,3,4),(0.,
2.85550478878829E-5,4.7855903267558E-5,6.34108981925977E-5,7.91451746296061E-5,
9.26886647080582E-5,0.000106465540580229,0.000127678760141081,0.000152977955413166),
 .UNSPECIFIED.);
#26006=B_SPLINE_CURVE_WITH_KNOTS('',3,(#416637,#416638,#416639,#416640,
#416641,#416642,#416643,#416644,#416645,#416646,#416647,#416648,#416649,
#416650,#416651,#416652,#416653,#416654,#416655,#416656,#416657,#416658,
#416659,#416660,#416661),.UNSPECIFIED.,.F.,.F.,(4,3,3,3,3,3,3,3,4),(0.,
2.85550478878826E-5,4.78559032675577E-5,6.34108981925972E-5,7.91451746296056E-5,
9.26886647080577E-5,0.000106465540580228,0.000127678760141081,0.000152977955413165),
 .UNSPECIFIED.);
#26007=B_SPLINE_CURVE_WITH_KNOTS('',3,(#416669,#416670,#416671,#416672,
#416673,#416674,#416675,#416676,#416677,#416678,#416679,#416680,#416681,
#416682,#416683,#416684,#416685,#416686,#416687,#416688,#416689,#416690,
#416691,#416692,#416693),.UNSPECIFIED.,.F.,.F.,(4,3,3,3,3,3,3,3,4),(0.,
2.85550478878825E-5,4.78559032675577E-5,6.34108981925973E-5,7.91451746296057E-5,
9.26886647080579E-5,0.000106465540580228,0.000127678760141081,0.000152977955413166),
 .UNSPECIFIED.);
#26008=B_SPLINE_CURVE_WITH_KNOTS('',3,(#416701,#416702,#416703,#416704,
#416705,#416706,#416707,#416708,#416709,#416710,#416711,#416712,#416713,
#416714,#416715,#416716,#416717,#416718,#416719,#416720,#416721,#416722,
#416723,#416724,#416725),.UNSPECIFIED.,.F.,.F.,(4,3,3,3,3,3,3,3,4),(0.,
2.85550478878828E-5,4.78559032675579E-5,6.34108981925977E-5,7.9145174629606E-5,
9.26886647080581E-5,0.000106465540580229,0.000127678760141081,0.000152977955413166),
 .UNSPECIFIED.);
#26009=B_SPLINE_CURVE_WITH_KNOTS('',3,(#416732,#416733,#416734,#416735,
#416736,#416737,#416738,#416739,#416740,#416741,#416742,#416743,#416744),
 .UNSPECIFIED.,.F.,.F.,(4,3,3,3,4),(0.,2.85550478876862E-5,4.78559032672286E-5,
6.34108981921613E-5,7.65824322177166E-5),.UNSPECIFIED.);
#26010=B_SPLINE_CURVE_WITH_KNOTS('',3,(#416755,#416756,#416757,#416758,
#416759,#416760,#416761,#416762,#416763,#416764,#416765,#416766,#416767,
#416768,#416769,#416770),.UNSPECIFIED.,.F.,.F.,(4,3,3,3,3,4),(0.,6.54397980774373E-6,
1.78746088883289E-5,2.90961555784964E-5,4.25056718483935E-5,6.52023395140211E-5),
 .UNSPECIFIED.);
#26011=B_SPLINE_CURVE_WITH_KNOTS('',3,(#416772,#416773,#416774,#416775,
#416776,#416777,#416778,#416779,#416780,#416781,#416782,#416783,#416784,
#416785,#416786,#416787),.UNSPECIFIED.,.F.,.F.,(4,3,3,3,3,4),(2.71050543121376E-20,
1.81271519801731E-5,3.33528222530966E-5,4.35246196643646E-5,5.39830173117273E-5,
6.44389677343626E-5),.UNSPECIFIED.);
#26012=B_SPLINE_CURVE_WITH_KNOTS('',3,(#416794,#416795,#416796,#416797,
#416798,#416799,#416800,#416801,#416802,#416803,#416804,#416805,#416806,
#416807,#416808,#416809),.UNSPECIFIED.,.F.,.F.,(4,3,3,3,3,4),(0.,6.54397980774379E-6,
1.78746088883289E-5,2.90961555784964E-5,4.25056718483935E-5,6.52023395140209E-5),
 .UNSPECIFIED.);
#26013=B_SPLINE_CURVE_WITH_KNOTS('',3,(#416811,#416812,#416813,#416814,
#416815,#416816,#416817,#416818,#416819,#416820,#416821,#416822,#416823,
#416824,#416825,#416826),.UNSPECIFIED.,.F.,.F.,(4,3,3,3,3,4),(5.42101086242752E-20,
1.81271519801731E-5,3.33528222530966E-5,4.35246196643646E-5,5.39830173117273E-5,
6.44389677343626E-5),.UNSPECIFIED.);
#26014=B_SPLINE_CURVE_WITH_KNOTS('',3,(#416833,#416834,#416835,#416836,
#416837,#416838,#416839,#416840,#416841,#416842,#416843,#416844,#416845,
#416846,#416847,#416848),.UNSPECIFIED.,.F.,.F.,(4,3,3,3,3,4),(0.,6.5439798077437E-6,
1.78746088883288E-5,2.90961555784963E-5,4.25056718483934E-5,6.52023395140209E-5),
 .UNSPECIFIED.);
#26015=B_SPLINE_CURVE_WITH_KNOTS('',3,(#416850,#416851,#416852,#416853,
#416854,#416855,#416856,#416857,#416858,#416859,#416860,#416861,#416862,
#416863,#416864,#416865),.UNSPECIFIED.,.F.,.F.,(4,3,3,3,3,4),(0.,1.81271519801731E-5,
3.33528222530966E-5,4.35246196643646E-5,5.39830173117273E-5,6.44389677343627E-5),
 .UNSPECIFIED.);
#26016=B_SPLINE_CURVE_WITH_KNOTS('',3,(#416872,#416873,#416874,#416875,
#416876,#416877,#416878,#416879,#416880,#416881,#416882,#416883,#416884,
#416885,#416886,#416887),.UNSPECIFIED.,.F.,.F.,(4,3,3,3,3,4),(0.,6.54397980774353E-6,
1.78746088883287E-5,2.90961555784963E-5,4.25056718483933E-5,6.52023395140208E-5),
 .UNSPECIFIED.);
#26017=B_SPLINE_CURVE_WITH_KNOTS('',3,(#416889,#416890,#416891,#416892,
#416893,#416894,#416895,#416896,#416897,#416898,#416899,#416900,#416901,
#416902,#416903,#416904),.UNSPECIFIED.,.F.,.F.,(4,3,3,3,3,4),(0.,1.81271519801731E-5,
3.33528222530967E-5,4.35246196643647E-5,5.39830173117274E-5,6.44389677343627E-5),
 .UNSPECIFIED.);
#26018=B_SPLINE_CURVE_WITH_KNOTS('',3,(#416911,#416912,#416913,#416914,
#416915,#416916,#416917,#416918,#416919,#416920,#416921,#416922,#416923,
#416924,#416925,#416926),.UNSPECIFIED.,.F.,.F.,(4,3,3,3,3,4),(0.,6.54397980774348E-6,
1.78746088883288E-5,2.90961555784961E-5,4.25056718483932E-5,6.52023395140207E-5),
 .UNSPECIFIED.);
#26019=B_SPLINE_CURVE_WITH_KNOTS('',3,(#416928,#416929,#416930,#416931,
#416932,#416933,#416934,#416935,#416936,#416937,#416938,#416939,#416940,
#416941,#416942,#416943),.UNSPECIFIED.,.F.,.F.,(4,3,3,3,3,4),(0.,1.81271519801731E-5,
3.33528222530967E-5,4.35246196643646E-5,5.39830173117275E-5,6.44389677343628E-5),
 .UNSPECIFIED.);
#26020=B_SPLINE_CURVE_WITH_KNOTS('',3,(#416950,#416951,#416952,#416953,
#416954,#416955,#416956,#416957,#416958,#416959,#416960,#416961,#416962,
#416963,#416964,#416965),.UNSPECIFIED.,.F.,.F.,(4,3,3,3,3,4),(0.,6.54397980774384E-6,
1.78746088883289E-5,2.90961555784964E-5,4.25056718483935E-5,6.5202339514021E-5),
 .UNSPECIFIED.);
#26021=B_SPLINE_CURVE_WITH_KNOTS('',3,(#416967,#416968,#416969,#416970,
#416971,#416972,#416973,#416974,#416975,#416976,#416977,#416978,#416979,
#416980,#416981,#416982),.UNSPECIFIED.,.F.,.F.,(4,3,3,3,3,4),(0.,1.81271519801731E-5,
3.33528222530965E-5,4.35246196643645E-5,5.39830173117272E-5,6.44389677343626E-5),
 .UNSPECIFIED.);
#26022=B_SPLINE_CURVE_WITH_KNOTS('',3,(#416989,#416990,#416991,#416992,
#416993,#416994,#416995,#416996,#416997,#416998,#416999,#417000,#417001,
#417002,#417003,#417004),.UNSPECIFIED.,.F.,.F.,(4,3,3,3,3,4),(0.,6.54397980774374E-6,
1.78746088883286E-5,2.90961555784963E-5,4.25056718483934E-5,6.5202339514021E-5),
 .UNSPECIFIED.);
#26023=B_SPLINE_CURVE_WITH_KNOTS('',3,(#417006,#417007,#417008,#417009,
#417010,#417011,#417012,#417013,#417014,#417015,#417016,#417017,#417018,
#417019,#417020,#417021),.UNSPECIFIED.,.F.,.F.,(4,3,3,3,3,4),(0.,1.81271519801732E-5,
3.33528222530967E-5,4.35246196643648E-5,5.39830173117271E-5,6.44389677343624E-5),
 .UNSPECIFIED.);
#26024=B_SPLINE_CURVE_WITH_KNOTS('',3,(#417028,#417029,#417030,#417031,
#417032,#417033,#417034,#417035,#417036,#417037,#417038,#417039,#417040,
#417041,#417042,#417043),.UNSPECIFIED.,.F.,.F.,(4,3,3,3,3,4),(0.,6.54397980774362E-6,
1.78746088883288E-5,2.90961555784963E-5,4.25056718483934E-5,6.52023395140209E-5),
 .UNSPECIFIED.);
#26025=B_SPLINE_CURVE_WITH_KNOTS('',3,(#417045,#417046,#417047,#417048,
#417049,#417050,#417051,#417052,#417053,#417054,#417055,#417056,#417057,
#417058,#417059,#417060),.UNSPECIFIED.,.F.,.F.,(4,3,3,3,3,4),(0.,1.81271519801732E-5,
3.33528222530965E-5,4.35246196643646E-5,5.39830173117272E-5,6.44389677343625E-5),
 .UNSPECIFIED.);
#26026=B_SPLINE_CURVE_WITH_KNOTS('',3,(#417067,#417068,#417069,#417070,
#417071,#417072,#417073,#417074,#417075,#417076,#417077,#417078,#417079,
#417080,#417081,#417082),.UNSPECIFIED.,.F.,.F.,(4,3,3,3,3,4),(0.,6.54397980774392E-6,
1.78746088883292E-5,2.90961555784966E-5,4.25056718483937E-5,6.52023395140214E-5),
 .UNSPECIFIED.);
#26027=B_SPLINE_CURVE_WITH_KNOTS('',3,(#417084,#417085,#417086,#417087,
#417088,#417089,#417090,#417091,#417092,#417093,#417094,#417095,#417096,
#417097,#417098,#417099),.UNSPECIFIED.,.F.,.F.,(4,3,3,3,3,4),(0.,1.81271519801731E-5,
3.33528222530967E-5,4.35246196643647E-5,5.39830173117272E-5,6.44389677343625E-5),
 .UNSPECIFIED.);
#26028=B_SPLINE_CURVE_WITH_KNOTS('',3,(#417106,#417107,#417108,#417109,
#417110,#417111,#417112,#417113,#417114,#417115,#417116,#417117,#417118,
#417119,#417120,#417121),.UNSPECIFIED.,.F.,.F.,(4,3,3,3,3,4),(0.,6.54397980774367E-6,
1.78746088883289E-5,2.90961555784963E-5,4.25056718483934E-5,6.52023395140208E-5),
 .UNSPECIFIED.);
#26029=B_SPLINE_CURVE_WITH_KNOTS('',3,(#417123,#417124,#417125,#417126,
#417127,#417128,#417129,#417130,#417131,#417132,#417133,#417134,#417135,
#417136,#417137,#417138),.UNSPECIFIED.,.F.,.F.,(4,3,3,3,3,4),(0.,1.81271519801731E-5,
3.33528222530965E-5,4.35246196643647E-5,5.39830173117273E-5,6.44389677343627E-5),
 .UNSPECIFIED.);
#26030=B_SPLINE_CURVE_WITH_KNOTS('',3,(#417145,#417146,#417147,#417148,
#417149,#417150,#417151,#417152,#417153,#417154,#417155,#417156,#417157,
#417158,#417159,#417160),.UNSPECIFIED.,.F.,.F.,(4,3,3,3,3,4),(0.,6.54397980774391E-6,
1.7874608888329E-5,2.90961555784965E-5,4.25056718483936E-5,6.52023395140211E-5),
 .UNSPECIFIED.);
#26031=B_SPLINE_CURVE_WITH_KNOTS('',3,(#417162,#417163,#417164,#417165,
#417166,#417167,#417168,#417169,#417170,#417171,#417172,#417173,#417174,
#417175,#417176,#417177),.UNSPECIFIED.,.F.,.F.,(4,3,3,3,3,4),(0.,1.8127151980173E-5,
3.33528222530963E-5,4.35246196643646E-5,5.39830173117274E-5,6.44389677343629E-5),
 .UNSPECIFIED.);
#26032=B_SPLINE_CURVE_WITH_KNOTS('',3,(#417184,#417185,#417186,#417187,
#417188,#417189,#417190,#417191,#417192,#417193,#417194,#417195,#417196,
#417197,#417198,#417199),.UNSPECIFIED.,.F.,.F.,(4,3,3,3,3,4),(0.,6.54397980774351E-6,
1.78746088883289E-5,2.90961555784962E-5,4.25056718483934E-5,6.52023395140209E-5),
 .UNSPECIFIED.);
#26033=B_SPLINE_CURVE_WITH_KNOTS('',3,(#417201,#417202,#417203,#417204,
#417205,#417206,#417207,#417208,#417209,#417210,#417211,#417212,#417213,
#417214,#417215,#417216),.UNSPECIFIED.,.F.,.F.,(4,3,3,3,3,4),(0.,1.81271519801732E-5,
3.33528222530968E-5,4.35246196643648E-5,5.39830173117279E-5,6.44389677343633E-5),
 .UNSPECIFIED.);
#26034=B_SPLINE_CURVE_WITH_KNOTS('',3,(#417223,#417224,#417225,#417226,
#417227,#417228,#417229,#417230,#417231,#417232,#417233,#417234,#417235,
#417236,#417237,#417238),.UNSPECIFIED.,.F.,.F.,(4,3,3,3,3,4),(0.,6.5439798077437E-6,
1.78746088883288E-5,2.90961555784963E-5,4.25056718483932E-5,6.52023395140205E-5),
 .UNSPECIFIED.);
#26035=B_SPLINE_CURVE_WITH_KNOTS('',3,(#417240,#417241,#417242,#417243,
#417244,#417245,#417246,#417247,#417248,#417249,#417250,#417251,#417252,
#417253,#417254,#417255),.UNSPECIFIED.,.F.,.F.,(4,3,3,3,3,4),(0.,1.81271519801731E-5,
3.33528222530966E-5,4.35246196643646E-5,5.39830173117274E-5,6.44389677343625E-5),
 .UNSPECIFIED.);
#26036=B_SPLINE_CURVE_WITH_KNOTS('',3,(#417262,#417263,#417264,#417265,
#417266,#417267,#417268,#417269,#417270,#417271,#417272,#417273,#417274,
#417275,#417276,#417277),.UNSPECIFIED.,.F.,.F.,(4,3,3,3,3,4),(0.,6.54397980774372E-6,
1.78746088883288E-5,2.90961555784962E-5,4.25056718483931E-5,6.52023395140206E-5),
 .UNSPECIFIED.);
#26037=B_SPLINE_CURVE_WITH_KNOTS('',3,(#417279,#417280,#417281,#417282,
#417283,#417284,#417285,#417286,#417287,#417288,#417289,#417290,#417291,
#417292,#417293,#417294),.UNSPECIFIED.,.F.,.F.,(4,3,3,3,3,4),(0.,1.81271519801731E-5,
3.33528222530966E-5,4.35246196643646E-5,5.39830173117274E-5,6.4438967734363E-5),
 .UNSPECIFIED.);
#26038=B_SPLINE_CURVE_WITH_KNOTS('',3,(#417301,#417302,#417303,#417304,
#417305,#417306,#417307,#417308,#417309,#417310,#417311,#417312,#417313,
#417314,#417315,#417316),.UNSPECIFIED.,.F.,.F.,(4,3,3,3,3,4),(0.,6.54397980774378E-6,
1.78746088883289E-5,2.90961555784965E-5,4.25056718483935E-5,6.52023395140212E-5),
 .UNSPECIFIED.);
#26039=B_SPLINE_CURVE_WITH_KNOTS('',3,(#417318,#417319,#417320,#417321,
#417322,#417323,#417324,#417325,#417326,#417327,#417328,#417329,#417330,
#417331,#417332,#417333),.UNSPECIFIED.,.F.,.F.,(4,3,3,3,3,4),(0.,1.81271519801731E-5,
3.33528222530964E-5,4.35246196643642E-5,5.39830173117271E-5,6.44389677343626E-5),
 .UNSPECIFIED.);
#26040=B_SPLINE_CURVE_WITH_KNOTS('',3,(#417340,#417341,#417342,#417343,
#417344,#417345,#417346,#417347,#417348,#417349,#417350,#417351,#417352,
#417353,#417354,#417355),.UNSPECIFIED.,.F.,.F.,(4,3,3,3,3,4),(0.,6.54397980774373E-6,
1.78746088883289E-5,2.90961555784964E-5,4.25056718483935E-5,6.52023395140208E-5),
 .UNSPECIFIED.);
#26041=B_SPLINE_CURVE_WITH_KNOTS('',3,(#417357,#417358,#417359,#417360,
#417361,#417362,#417363,#417364,#417365,#417366,#417367,#417368,#417369,
#417370,#417371,#417372),.UNSPECIFIED.,.F.,.F.,(4,3,3,3,3,4),(0.,1.81271519801731E-5,
3.33528222530966E-5,4.35246196643646E-5,5.39830173117274E-5,6.44389677343629E-5),
 .UNSPECIFIED.);
#26042=B_SPLINE_CURVE_WITH_KNOTS('',3,(#417379,#417380,#417381,#417382,
#417383,#417384,#417385,#417386,#417387,#417388,#417389,#417390,#417391,
#417392,#417393,#417394),.UNSPECIFIED.,.F.,.F.,(4,3,3,3,3,4),(0.,6.54397980774365E-6,
1.78746088883288E-5,2.90961555784964E-5,4.25056718483935E-5,6.52023395140211E-5),
 .UNSPECIFIED.);
#26043=B_SPLINE_CURVE_WITH_KNOTS('',3,(#417396,#417397,#417398,#417399,
#417400,#417401,#417402,#417403,#417404,#417405,#417406,#417407,#417408,
#417409,#417410,#417411),.UNSPECIFIED.,.F.,.F.,(4,3,3,3,3,4),(0.,1.81271519801731E-5,
3.33528222530965E-5,4.35246196643645E-5,5.39830173117272E-5,6.44389677343626E-5),
 .UNSPECIFIED.);
#26044=B_SPLINE_CURVE_WITH_KNOTS('',3,(#417418,#417419,#417420,#417421,
#417422,#417423,#417424,#417425,#417426,#417427,#417428,#417429,#417430,
#417431,#417432,#417433),.UNSPECIFIED.,.F.,.F.,(4,3,3,3,3,4),(0.,6.54397980774371E-6,
1.78746088883289E-5,2.90961555784963E-5,4.25056718483935E-5,6.52023395140209E-5),
 .UNSPECIFIED.);
#26045=B_SPLINE_CURVE_WITH_KNOTS('',3,(#417435,#417436,#417437,#417438,
#417439,#417440,#417441,#417442,#417443,#417444,#417445,#417446,#417447,
#417448,#417449,#417450),.UNSPECIFIED.,.F.,.F.,(4,3,3,3,3,4),(5.42101086242752E-20,
1.81271519801731E-5,3.33528222530966E-5,4.35246196643646E-5,5.39830173117274E-5,
6.44389677343628E-5),.UNSPECIFIED.);
#26046=B_SPLINE_CURVE_WITH_KNOTS('',3,(#417457,#417458,#417459,#417460,
#417461,#417462,#417463,#417464,#417465,#417466,#417467,#417468,#417469,
#417470,#417471,#417472),.UNSPECIFIED.,.F.,.F.,(4,3,3,3,3,4),(0.,6.54397980774374E-6,
1.78746088883289E-5,2.90961555784964E-5,4.25056718483934E-5,6.52023395140209E-5),
 .UNSPECIFIED.);
#26047=B_SPLINE_CURVE_WITH_KNOTS('',3,(#417474,#417475,#417476,#417477,
#417478,#417479,#417480,#417481,#417482,#417483,#417484,#417485,#417486,
#417487,#417488,#417489),.UNSPECIFIED.,.F.,.F.,(4,3,3,3,3,4),(2.71050543121376E-20,
1.81271519801731E-5,3.33528222530966E-5,4.35246196643646E-5,5.39830173117273E-5,
6.44389677343626E-5),.UNSPECIFIED.);
#26048=B_SPLINE_CURVE_WITH_KNOTS('',3,(#417496,#417497,#417498,#417499,
#417500,#417501,#417502,#417503,#417504,#417505,#417506,#417507,#417508,
#417509,#417510,#417511),.UNSPECIFIED.,.F.,.F.,(4,3,3,3,3,4),(0.,6.54397980774373E-6,
1.78746088883289E-5,2.90961555784963E-5,4.25056718483934E-5,6.52023395140208E-5),
 .UNSPECIFIED.);
#26049=B_SPLINE_CURVE_WITH_KNOTS('',3,(#417513,#417514,#417515,#417516,
#417517,#417518,#417519,#417520,#417521,#417522,#417523,#417524,#417525,
#417526,#417527,#417528),.UNSPECIFIED.,.F.,.F.,(4,3,3,3,3,4),(2.71050543121376E-20,
1.81271519801731E-5,3.33528222530966E-5,4.35246196643646E-5,5.39830173117273E-5,
6.44389677343626E-5),.UNSPECIFIED.);
#26050=B_SPLINE_CURVE_WITH_KNOTS('',3,(#417535,#417536,#417537,#417538,
#417539,#417540,#417541,#417542,#417543,#417544,#417545,#417546,#417547,
#417548,#417549,#417550),.UNSPECIFIED.,.F.,.F.,(4,3,3,3,3,4),(0.,6.54397980774376E-6,
1.78746088883289E-5,2.90961555784964E-5,4.25056718483935E-5,6.5202339514021E-5),
 .UNSPECIFIED.);
#26051=B_SPLINE_CURVE_WITH_KNOTS('',3,(#417552,#417553,#417554,#417555,
#417556,#417557,#417558,#417559,#417560,#417561,#417562,#417563,#417564,
#417565,#417566,#417567),.UNSPECIFIED.,.F.,.F.,(4,3,3,3,3,4),(5.42101086242752E-20,
1.81271519801731E-5,3.33528222530966E-5,4.35246196643646E-5,5.39830173117273E-5,
6.44389677343626E-5),.UNSPECIFIED.);
#26052=B_SPLINE_CURVE_WITH_KNOTS('',3,(#417574,#417575,#417576,#417577,
#417578,#417579,#417580,#417581,#417582,#417583,#417584,#417585,#417586,
#417587,#417588,#417589),.UNSPECIFIED.,.F.,.F.,(4,3,3,3,3,4),(0.,6.54397980774373E-6,
1.78746088883289E-5,2.90961555784964E-5,4.25056718483934E-5,6.52023395140209E-5),
 .UNSPECIFIED.);
#26053=B_SPLINE_CURVE_WITH_KNOTS('',3,(#417591,#417592,#417593,#417594,
#417595,#417596,#417597,#417598,#417599,#417600,#417601,#417602,#417603,
#417604,#417605,#417606),.UNSPECIFIED.,.F.,.F.,(4,3,3,3,3,4),(0.,1.81271519801731E-5,
3.33528222530965E-5,4.35246196643645E-5,5.39830173117274E-5,6.44389677343627E-5),
 .UNSPECIFIED.);
#26054=B_SPLINE_CURVE_WITH_KNOTS('',3,(#417613,#417614,#417615,#417616,
#417617,#417618,#417619,#417620,#417621,#417622,#417623,#417624,#417625,
#417626,#417627,#417628),.UNSPECIFIED.,.F.,.F.,(4,3,3,3,3,4),(0.,6.54397980774377E-6,
1.78746088883288E-5,2.90961555784963E-5,4.25056718483935E-5,6.52023395140211E-5),
 .UNSPECIFIED.);
#26055=B_SPLINE_CURVE_WITH_KNOTS('',3,(#417630,#417631,#417632,#417633,
#417634,#417635,#417636,#417637,#417638,#417639,#417640,#417641,#417642,
#417643,#417644,#417645),.UNSPECIFIED.,.F.,.F.,(4,3,3,3,3,4),(0.,1.81271519801731E-5,
3.33528222530966E-5,4.35246196643646E-5,5.39830173117272E-5,6.44389677343625E-5),
 .UNSPECIFIED.);
#26056=B_SPLINE_CURVE_WITH_KNOTS('',3,(#417652,#417653,#417654,#417655,
#417656,#417657,#417658,#417659,#417660,#417661,#417662,#417663,#417664,
#417665,#417666,#417667),.UNSPECIFIED.,.F.,.F.,(4,3,3,3,3,4),(0.,6.54397980774367E-6,
1.78746088883288E-5,2.90961555784963E-5,4.25056718483934E-5,6.52023395140209E-5),
 .UNSPECIFIED.);
#26057=B_SPLINE_CURVE_WITH_KNOTS('',3,(#417669,#417670,#417671,#417672,
#417673,#417674,#417675,#417676,#417677,#417678,#417679,#417680,#417681,
#417682,#417683,#417684),.UNSPECIFIED.,.F.,.F.,(4,3,3,3,3,4),(0.,1.81271519801731E-5,
3.33528222530967E-5,4.35246196643647E-5,5.39830173117276E-5,6.4438967734363E-5),
 .UNSPECIFIED.);
#26058=B_SPLINE_CURVE_WITH_KNOTS('',3,(#417691,#417692,#417693,#417694,
#417695,#417696,#417697,#417698,#417699,#417700,#417701,#417702,#417703,
#417704,#417705,#417706),.UNSPECIFIED.,.F.,.F.,(4,3,3,3,3,4),(0.,6.54397980774349E-6,
1.78746088883288E-5,2.90961555784963E-5,4.25056718483933E-5,6.52023395140206E-5),
 .UNSPECIFIED.);
#26059=B_SPLINE_CURVE_WITH_KNOTS('',3,(#417708,#417709,#417710,#417711,
#417712,#417713,#417714,#417715,#417716,#417717,#417718,#417719,#417720,
#417721,#417722,#417723),.UNSPECIFIED.,.F.,.F.,(4,3,3,3,3,4),(0.,1.81271519801732E-5,
3.33528222530966E-5,4.35246196643646E-5,5.39830173117274E-5,6.4438967734363E-5),
 .UNSPECIFIED.);
#26060=B_SPLINE_CURVE_WITH_KNOTS('',3,(#417730,#417731,#417732,#417733,
#417734,#417735,#417736,#417737,#417738,#417739,#417740,#417741,#417742,
#417743,#417744,#417745),.UNSPECIFIED.,.F.,.F.,(4,3,3,3,3,4),(0.,6.5439798077438E-6,
1.78746088883289E-5,2.90961555784962E-5,4.25056718483932E-5,6.52023395140206E-5),
 .UNSPECIFIED.);
#26061=B_SPLINE_CURVE_WITH_KNOTS('',3,(#417747,#417748,#417749,#417750,
#417751,#417752,#417753,#417754,#417755,#417756,#417757,#417758,#417759,
#417760,#417761,#417762),.UNSPECIFIED.,.F.,.F.,(4,3,3,3,3,4),(0.,1.81271519801732E-5,
3.33528222530965E-5,4.35246196643647E-5,5.39830173117274E-5,6.44389677343628E-5),
 .UNSPECIFIED.);
#26062=B_SPLINE_CURVE_WITH_KNOTS('',3,(#417769,#417770,#417771,#417772,
#417773,#417774,#417775,#417776,#417777,#417778,#417779,#417780,#417781,
#417782,#417783,#417784),.UNSPECIFIED.,.F.,.F.,(4,3,3,3,3,4),(0.,6.54397980774388E-6,
1.78746088883289E-5,2.90961555784964E-5,4.25056718483935E-5,6.52023395140211E-5),
 .UNSPECIFIED.);
#26063=B_SPLINE_CURVE_WITH_KNOTS('',3,(#417786,#417787,#417788,#417789,
#417790,#417791,#417792,#417793,#417794,#417795,#417796,#417797,#417798,
#417799,#417800,#417801),.UNSPECIFIED.,.F.,.F.,(4,3,3,3,3,4),(0.,1.8127151980173E-5,
3.33528222530964E-5,4.35246196643643E-5,5.39830173117268E-5,6.44389677343624E-5),
 .UNSPECIFIED.);
#26064=B_SPLINE_CURVE_WITH_KNOTS('',3,(#417808,#417809,#417810,#417811,
#417812,#417813,#417814,#417815,#417816,#417817,#417818,#417819,#417820,
#417821,#417822,#417823),.UNSPECIFIED.,.F.,.F.,(4,3,3,3,3,4),(0.,6.54397980774362E-6,
1.78746088883289E-5,2.90961555784964E-5,4.25056718483934E-5,6.52023395140208E-5),
 .UNSPECIFIED.);
#26065=B_SPLINE_CURVE_WITH_KNOTS('',3,(#417825,#417826,#417827,#417828,
#417829,#417830,#417831,#417832,#417833,#417834,#417835,#417836,#417837,
#417838,#417839,#417840),.UNSPECIFIED.,.F.,.F.,(4,3,3,3,3,4),(0.,1.81271519801731E-5,
3.33528222530967E-5,4.35246196643645E-5,5.39830173117272E-5,6.44389677343627E-5),
 .UNSPECIFIED.);
#26066=B_SPLINE_CURVE_WITH_KNOTS('',3,(#417847,#417848,#417849,#417850,
#417851,#417852,#417853,#417854,#417855,#417856,#417857,#417858,#417859,
#417860,#417861,#417862),.UNSPECIFIED.,.F.,.F.,(4,3,3,3,3,4),(0.,6.54397980774398E-6,
1.7874608888329E-5,2.90961555784965E-5,4.25056718483937E-5,6.52023395140213E-5),
 .UNSPECIFIED.);
#26067=B_SPLINE_CURVE_WITH_KNOTS('',3,(#417864,#417865,#417866,#417867,
#417868,#417869,#417870,#417871,#417872,#417873,#417874,#417875,#417876,
#417877,#417878,#417879),.UNSPECIFIED.,.F.,.F.,(4,3,3,3,3,4),(0.,1.81271519801732E-5,
3.33528222530968E-5,4.35246196643646E-5,5.39830173117275E-5,6.44389677343627E-5),
 .UNSPECIFIED.);
#26068=B_SPLINE_CURVE_WITH_KNOTS('',3,(#417886,#417887,#417888,#417889,
#417890,#417891,#417892,#417893,#417894,#417895,#417896,#417897,#417898,
#417899,#417900,#417901),.UNSPECIFIED.,.F.,.F.,(4,3,3,3,3,4),(0.,6.54397980774373E-6,
1.78746088883286E-5,2.90961555784964E-5,4.25056718483933E-5,6.52023395140207E-5),
 .UNSPECIFIED.);
#26069=B_SPLINE_CURVE_WITH_KNOTS('',3,(#417903,#417904,#417905,#417906,
#417907,#417908,#417909,#417910,#417911,#417912,#417913,#417914,#417915,
#417916,#417917,#417918),.UNSPECIFIED.,.F.,.F.,(4,3,3,3,3,4),(0.,1.81271519801732E-5,
3.33528222530965E-5,4.35246196643643E-5,5.39830173117273E-5,6.44389677343627E-5),
 .UNSPECIFIED.);
#26070=B_SPLINE_CURVE_WITH_KNOTS('',3,(#417925,#417926,#417927,#417928,
#417929,#417930,#417931,#417932,#417933,#417934,#417935,#417936,#417937,
#417938,#417939,#417940),.UNSPECIFIED.,.F.,.F.,(4,3,3,3,3,4),(0.,6.54397980774373E-6,
1.78746088883289E-5,2.90961555784966E-5,4.25056718483937E-5,6.52023395140213E-5),
 .UNSPECIFIED.);
#26071=B_SPLINE_CURVE_WITH_KNOTS('',3,(#417942,#417943,#417944,#417945,
#417946,#417947,#417948,#417949,#417950,#417951,#417952,#417953,#417954,
#417955,#417956,#417957),.UNSPECIFIED.,.F.,.F.,(4,3,3,3,3,4),(0.,1.81271519801731E-5,
3.33528222530965E-5,4.35246196643644E-5,5.39830173117273E-5,6.44389677343629E-5),
 .UNSPECIFIED.);
#26072=B_SPLINE_CURVE_WITH_KNOTS('',3,(#417964,#417965,#417966,#417967,
#417968,#417969,#417970,#417971,#417972,#417973,#417974,#417975,#417976,
#417977,#417978,#417979),.UNSPECIFIED.,.F.,.F.,(4,3,3,3,3,4),(0.,6.54397980774386E-6,
1.78746088883289E-5,2.90961555784964E-5,4.25056718483936E-5,6.52023395140211E-5),
 .UNSPECIFIED.);
#26073=B_SPLINE_CURVE_WITH_KNOTS('',3,(#417981,#417982,#417983,#417984,
#417985,#417986,#417987,#417988,#417989,#417990,#417991,#417992,#417993,
#417994,#417995,#417996),.UNSPECIFIED.,.F.,.F.,(4,3,3,3,3,4),(0.,1.81271519801731E-5,
3.33528222530964E-5,4.35246196643646E-5,5.39830173117272E-5,6.44389677343629E-5),
 .UNSPECIFIED.);
#26074=B_SPLINE_CURVE_WITH_KNOTS('',3,(#418003,#418004,#418005,#418006,
#418007,#418008,#418009,#418010,#418011,#418012,#418013,#418014,#418015,
#418016,#418017,#418018),.UNSPECIFIED.,.F.,.F.,(4,3,3,3,3,4),(0.,6.5439798077436E-6,
1.78746088883289E-5,2.90961555784965E-5,4.25056718483935E-5,6.52023395140211E-5),
 .UNSPECIFIED.);
#26075=B_SPLINE_CURVE_WITH_KNOTS('',3,(#418020,#418021,#418022,#418023,
#418024,#418025,#418026,#418027,#418028,#418029,#418030,#418031,#418032,
#418033,#418034,#418035),.UNSPECIFIED.,.F.,.F.,(4,3,3,3,3,4),(0.,1.81271519801731E-5,
3.33528222530965E-5,4.35246196643644E-5,5.39830173117273E-5,6.44389677343625E-5),
 .UNSPECIFIED.);
#26076=B_SPLINE_CURVE_WITH_KNOTS('',3,(#418042,#418043,#418044,#418045,
#418046,#418047,#418048,#418049,#418050,#418051,#418052,#418053,#418054,
#418055,#418056,#418057),.UNSPECIFIED.,.F.,.F.,(4,3,3,3,3,4),(0.,6.54397980774372E-6,
1.78746088883287E-5,2.90961555784964E-5,4.25056718483934E-5,6.52023395140209E-5),
 .UNSPECIFIED.);
#26077=B_SPLINE_CURVE_WITH_KNOTS('',3,(#418059,#418060,#418061,#418062,
#418063,#418064,#418065,#418066,#418067,#418068,#418069,#418070,#418071,
#418072,#418073,#418074),.UNSPECIFIED.,.F.,.F.,(4,3,3,3,3,4),(0.,1.8127151980173E-5,
3.33528222530966E-5,4.35246196643645E-5,5.39830173117273E-5,6.44389677343627E-5),
 .UNSPECIFIED.);
#26078=B_SPLINE_CURVE_WITH_KNOTS('',3,(#418081,#418082,#418083,#418084,
#418085,#418086,#418087,#418088,#418089,#418090,#418091,#418092,#418093,
#418094,#418095,#418096),.UNSPECIFIED.,.F.,.F.,(4,3,3,3,3,4),(0.,6.54397980774384E-6,
1.7874608888329E-5,2.90961555784964E-5,4.25056718483935E-5,6.52023395140211E-5),
 .UNSPECIFIED.);
#26079=B_SPLINE_CURVE_WITH_KNOTS('',3,(#418098,#418099,#418100,#418101,
#418102,#418103,#418104,#418105,#418106,#418107,#418108,#418109,#418110,
#418111,#418112,#418113),.UNSPECIFIED.,.F.,.F.,(4,3,3,3,3,4),(0.,1.81271519801731E-5,
3.33528222530964E-5,4.35246196643645E-5,5.39830173117271E-5,6.44389677343624E-5),
 .UNSPECIFIED.);
#26080=B_SPLINE_CURVE_WITH_KNOTS('',3,(#418120,#418121,#418122,#418123,
#418124,#418125,#418126,#418127,#418128,#418129,#418130,#418131,#418132,
#418133,#418134,#418135),.UNSPECIFIED.,.F.,.F.,(4,3,3,3,3,4),(0.,6.54397980774382E-6,
1.78746088883289E-5,2.90961555784965E-5,4.25056718483936E-5,6.52023395140212E-5),
 .UNSPECIFIED.);
#26081=B_SPLINE_CURVE_WITH_KNOTS('',3,(#418137,#418138,#418139,#418140,
#418141,#418142,#418143,#418144,#418145,#418146,#418147,#418148,#418149,
#418150,#418151,#418152),.UNSPECIFIED.,.F.,.F.,(4,3,3,3,3,4),(0.,1.81271519801731E-5,
3.33528222530966E-5,4.35246196643645E-5,5.39830173117275E-5,6.44389677343628E-5),
 .UNSPECIFIED.);
#26082=B_SPLINE_CURVE_WITH_KNOTS('',3,(#418159,#418160,#418161,#418162,
#418163,#418164,#418165,#418166,#418167,#418168,#418169,#418170,#418171,
#418172,#418173,#418174),.UNSPECIFIED.,.F.,.F.,(4,3,3,3,3,4),(0.,6.54397980774367E-6,
1.78746088883288E-5,2.90961555784963E-5,4.25056718483933E-5,6.52023395140207E-5),
 .UNSPECIFIED.);
#26083=B_SPLINE_CURVE_WITH_KNOTS('',3,(#418176,#418177,#418178,#418179,
#418180,#418181,#418182,#418183,#418184,#418185,#418186,#418187,#418188,
#418189,#418190,#418191),.UNSPECIFIED.,.F.,.F.,(4,3,3,3,3,4),(5.42101086242752E-20,
1.81271519801731E-5,3.33528222530966E-5,4.35246196643646E-5,5.39830173117274E-5,
6.44389677343627E-5),.UNSPECIFIED.);
#26084=B_SPLINE_CURVE_WITH_KNOTS('',3,(#418198,#418199,#418200,#418201,
#418202,#418203,#418204,#418205,#418206,#418207,#418208,#418209,#418210,
#418211,#418212,#418213),.UNSPECIFIED.,.F.,.F.,(4,3,3,3,3,4),(0.,6.54397980774372E-6,
1.78746088883289E-5,2.90961555784964E-5,4.25056718483934E-5,6.5202339514021E-5),
 .UNSPECIFIED.);
#26085=B_SPLINE_CURVE_WITH_KNOTS('',3,(#418215,#418216,#418217,#418218,
#418219,#418220,#418221,#418222,#418223,#418224,#418225,#418226,#418227,
#418228,#418229,#418230),.UNSPECIFIED.,.F.,.F.,(4,3,3,3,3,4),(2.71050543121376E-20,
1.81271519801731E-5,3.33528222530966E-5,4.35246196643646E-5,5.39830173117273E-5,
6.44389677343625E-5),.UNSPECIFIED.);
#26086=B_SPLINE_CURVE_WITH_KNOTS('',3,(#418237,#418238,#418239,#418240,
#418241,#418242,#418243,#418244,#418245,#418246,#418247,#418248,#418249,
#418250,#418251,#418252),.UNSPECIFIED.,.F.,.F.,(4,3,3,3,3,4),(0.,6.54397980774373E-6,
1.78746088883289E-5,2.90961555784964E-5,4.25056718483934E-5,6.52023395140209E-5),
 .UNSPECIFIED.);
#26087=B_SPLINE_CURVE_WITH_KNOTS('',3,(#418255,#418256,#418257,#418258,
#418259,#418260,#418261,#418262,#418263,#418264,#418265,#418266,#418267,
#418268,#418269,#418270),.UNSPECIFIED.,.F.,.F.,(4,3,3,3,3,4),(0.,1.81271519801731E-5,
3.33528222530966E-5,4.35246196643646E-5,5.39830173117274E-5,6.44389677343629E-5),
 .UNSPECIFIED.);
#26088=B_SPLINE_CURVE_WITH_KNOTS('',3,(#418277,#418278,#418279,#418280,
#418281,#418282,#418283,#418284,#418285,#418286,#418287,#418288,#418289,
#418290,#418291,#418292),.UNSPECIFIED.,.F.,.F.,(4,3,3,3,3,4),(0.,6.54397980774374E-6,
1.78746088883289E-5,2.90961555784964E-5,4.25056718483934E-5,6.52023395140209E-5),
 .UNSPECIFIED.);
#26089=B_SPLINE_CURVE_WITH_KNOTS('',3,(#418294,#418295,#418296,#418297,
#418298,#418299,#418300,#418301,#418302,#418303,#418304,#418305,#418306,
#418307,#418308,#418309),.UNSPECIFIED.,.F.,.F.,(4,3,3,3,3,4),(5.42101086242752E-20,
1.81271519801731E-5,3.33528222530966E-5,4.35246196643646E-5,5.39830173117273E-5,
6.44389677343625E-5),.UNSPECIFIED.);
#26090=B_SPLINE_CURVE_WITH_KNOTS('',3,(#418316,#418317,#418318,#418319,
#418320,#418321,#418322,#418323,#418324,#418325,#418326,#418327,#418328,
#418329,#418330,#418331),.UNSPECIFIED.,.F.,.F.,(4,3,3,3,3,4),(0.,6.54397980774378E-6,
1.78746088883288E-5,2.90961555784963E-5,4.25056718483934E-5,6.52023395140208E-5),
 .UNSPECIFIED.);
#26091=B_SPLINE_CURVE_WITH_KNOTS('',3,(#418333,#418334,#418335,#418336,
#418337,#418338,#418339,#418340,#418341,#418342,#418343,#418344,#418345,
#418346,#418347,#418348),.UNSPECIFIED.,.F.,.F.,(4,3,3,3,3,4),(0.,1.81271519801731E-5,
3.33528222530966E-5,4.35246196643645E-5,5.39830173117272E-5,6.44389677343625E-5),
 .UNSPECIFIED.);
#26092=B_SPLINE_CURVE_WITH_KNOTS('',3,(#418355,#418356,#418357,#418358,
#418359,#418360,#418361,#418362,#418363,#418364,#418365,#418366,#418367,
#418368,#418369,#418370),.UNSPECIFIED.,.F.,.F.,(4,3,3,3,3,4),(0.,6.54397980774369E-6,
1.78746088883288E-5,2.90961555784963E-5,4.25056718483934E-5,6.52023395140209E-5),
 .UNSPECIFIED.);
#26093=B_SPLINE_CURVE_WITH_KNOTS('',3,(#418372,#418373,#418374,#418375,
#418376,#418377,#418378,#418379,#418380,#418381,#418382,#418383,#418384,
#418385,#418386,#418387),.UNSPECIFIED.,.F.,.F.,(4,3,3,3,3,4),(0.,1.81271519801732E-5,
3.33528222530966E-5,4.35246196643647E-5,5.39830173117272E-5,6.44389677343626E-5),
 .UNSPECIFIED.);
#26094=B_SPLINE_CURVE_WITH_KNOTS('',3,(#418394,#418395,#418396,#418397,
#418398,#418399,#418400,#418401,#418402,#418403,#418404,#418405,#418406,
#418407,#418408,#418409),.UNSPECIFIED.,.F.,.F.,(4,3,3,3,3,4),(0.,6.5439798077436E-6,
1.78746088883288E-5,2.90961555784963E-5,4.25056718483933E-5,6.52023395140209E-5),
 .UNSPECIFIED.);
#26095=B_SPLINE_CURVE_WITH_KNOTS('',3,(#418411,#418412,#418413,#418414,
#418415,#418416,#418417,#418418,#418419,#418420,#418421,#418422,#418423,
#418424,#418425,#418426),.UNSPECIFIED.,.F.,.F.,(4,3,3,3,3,4),(0.,1.81271519801731E-5,
3.33528222530967E-5,4.35246196643647E-5,5.39830173117274E-5,6.4438967734363E-5),
 .UNSPECIFIED.);
#26096=B_SPLINE_CURVE_WITH_KNOTS('',3,(#418433,#418434,#418435,#418436,
#418437,#418438,#418439,#418440,#418441,#418442,#418443,#418444,#418445,
#418446,#418447,#418448),.UNSPECIFIED.,.F.,.F.,(4,3,3,3,3,4),(0.,6.54397980774359E-6,
1.78746088883289E-5,2.90961555784964E-5,4.25056718483934E-5,6.52023395140208E-5),
 .UNSPECIFIED.);
#26097=B_SPLINE_CURVE_WITH_KNOTS('',3,(#418450,#418451,#418452,#418453,
#418454,#418455,#418456,#418457,#418458,#418459,#418460,#418461,#418462,
#418463,#418464,#418465),.UNSPECIFIED.,.F.,.F.,(4,3,3,3,3,4),(0.,1.81271519801731E-5,
3.33528222530964E-5,4.35246196643645E-5,5.39830173117274E-5,6.44389677343629E-5),
 .UNSPECIFIED.);
#26098=B_SPLINE_CURVE_WITH_KNOTS('',3,(#418472,#418473,#418474,#418475,
#418476,#418477,#418478,#418479,#418480,#418481,#418482,#418483,#418484,
#418485,#418486,#418487),.UNSPECIFIED.,.F.,.F.,(4,3,3,3,3,4),(0.,6.54397980774364E-6,
1.7874608888329E-5,2.90961555784965E-5,4.25056718483936E-5,6.52023395140211E-5),
 .UNSPECIFIED.);
#26099=B_SPLINE_CURVE_WITH_KNOTS('',3,(#418489,#418490,#418491,#418492,
#418493,#418494,#418495,#418496,#418497,#418498,#418499,#418500,#418501,
#418502,#418503,#418504),.UNSPECIFIED.,.F.,.F.,(4,3,3,3,3,4),(0.,1.81271519801731E-5,
3.33528222530965E-5,4.35246196643648E-5,5.39830173117276E-5,6.44389677343631E-5),
 .UNSPECIFIED.);
#26100=B_SPLINE_CURVE_WITH_KNOTS('',3,(#418511,#418512,#418513,#418514,
#418515,#418516,#418517,#418518,#418519,#418520,#418521,#418522,#418523,
#418524,#418525,#418526),.UNSPECIFIED.,.F.,.F.,(4,3,3,3,3,4),(0.,6.5439798077437E-6,
1.78746088883287E-5,2.90961555784963E-5,4.25056718483934E-5,6.52023395140209E-5),
 .UNSPECIFIED.);
#26101=B_SPLINE_CURVE_WITH_KNOTS('',3,(#418528,#418529,#418530,#418531,
#418532,#418533,#418534,#418535,#418536,#418537,#418538,#418539,#418540,
#418541,#418542,#418543),.UNSPECIFIED.,.F.,.F.,(4,3,3,3,3,4),(0.,1.81271519801732E-5,
3.33528222530966E-5,4.35246196643647E-5,5.39830173117273E-5,6.44389677343626E-5),
 .UNSPECIFIED.);
#26102=B_SPLINE_CURVE_WITH_KNOTS('',3,(#418550,#418551,#418552,#418553,
#418554,#418555,#418556,#418557,#418558,#418559,#418560,#418561,#418562,
#418563,#418564,#418565),.UNSPECIFIED.,.F.,.F.,(4,3,3,3,3,4),(0.,6.54397980774401E-6,
1.78746088883291E-5,2.90961555784967E-5,4.25056718483938E-5,6.52023395140214E-5),
 .UNSPECIFIED.);
#26103=B_SPLINE_CURVE_WITH_KNOTS('',3,(#418567,#418568,#418569,#418570,
#418571,#418572,#418573,#418574,#418575,#418576,#418577,#418578,#418579,
#418580,#418581,#418582),.UNSPECIFIED.,.F.,.F.,(4,3,3,3,3,4),(0.,1.81271519801731E-5,
3.33528222530967E-5,4.35246196643648E-5,5.39830173117277E-5,6.44389677343627E-5),
 .UNSPECIFIED.);
#26104=B_SPLINE_CURVE_WITH_KNOTS('',3,(#418589,#418590,#418591,#418592,
#418593,#418594,#418595,#418596,#418597,#418598,#418599,#418600,#418601,
#418602,#418603,#418604),.UNSPECIFIED.,.F.,.F.,(4,3,3,3,3,4),(0.,6.54397980774356E-6,
1.7874608888329E-5,2.90961555784964E-5,4.25056718483936E-5,6.52023395140211E-5),
 .UNSPECIFIED.);
#26105=B_SPLINE_CURVE_WITH_KNOTS('',3,(#418606,#418607,#418608,#418609,
#418610,#418611,#418612,#418613,#418614,#418615,#418616,#418617,#418618,
#418619,#418620,#418621),.UNSPECIFIED.,.F.,.F.,(4,3,3,3,3,4),(0.,1.8127151980173E-5,
3.33528222530964E-5,4.35246196643645E-5,5.3983017311727E-5,6.44389677343624E-5),
 .UNSPECIFIED.);
#26106=B_SPLINE_CURVE_WITH_KNOTS('',3,(#418628,#418629,#418630,#418631,
#418632,#418633,#418634,#418635,#418636,#418637,#418638,#418639,#418640,
#418641,#418642,#418643),.UNSPECIFIED.,.F.,.F.,(4,3,3,3,3,4),(0.,6.54397980774394E-6,
1.78746088883292E-5,2.90961555784967E-5,4.25056718483935E-5,6.52023395140211E-5),
 .UNSPECIFIED.);
#26107=B_SPLINE_CURVE_WITH_KNOTS('',3,(#418645,#418646,#418647,#418648,
#418649,#418650,#418651,#418652,#418653,#418654,#418655,#418656,#418657,
#418658,#418659,#418660),.UNSPECIFIED.,.F.,.F.,(4,3,3,3,3,4),(0.,1.81271519801731E-5,
3.33528222530967E-5,4.35246196643646E-5,5.39830173117274E-5,6.44389677343627E-5),
 .UNSPECIFIED.);
#26108=B_SPLINE_CURVE_WITH_KNOTS('',3,(#418667,#418668,#418669,#418670,
#418671,#418672,#418673,#418674,#418675,#418676,#418677,#418678,#418679,
#418680,#418681,#418682),.UNSPECIFIED.,.F.,.F.,(4,3,3,3,3,4),(0.,6.54397980774397E-6,
1.78746088883291E-5,2.90961555784962E-5,4.25056718483934E-5,6.52023395140212E-5),
 .UNSPECIFIED.);
#26109=B_SPLINE_CURVE_WITH_KNOTS('',3,(#418684,#418685,#418686,#418687,
#418688,#418689,#418690,#418691,#418692,#418693,#418694,#418695,#418696,
#418697,#418698,#418699),.UNSPECIFIED.,.F.,.F.,(4,3,3,3,3,4),(0.,1.81271519801731E-5,
3.33528222530966E-5,4.35246196643644E-5,5.39830173117273E-5,6.44389677343626E-5),
 .UNSPECIFIED.);
#26110=B_SPLINE_CURVE_WITH_KNOTS('',3,(#418706,#418707,#418708,#418709,
#418710,#418711,#418712,#418713,#418714,#418715,#418716,#418717,#418718,
#418719,#418720,#418721),.UNSPECIFIED.,.F.,.F.,(4,3,3,3,3,4),(0.,6.54397980774329E-6,
1.78746088883288E-5,2.90961555784961E-5,4.25056718483933E-5,6.52023395140208E-5),
 .UNSPECIFIED.);
#26111=B_SPLINE_CURVE_WITH_KNOTS('',3,(#418723,#418724,#418725,#418726,
#418727,#418728,#418729,#418730,#418731,#418732,#418733,#418734,#418735,
#418736,#418737,#418738),.UNSPECIFIED.,.F.,.F.,(4,3,3,3,3,4),(0.,1.81271519801731E-5,
3.33528222530966E-5,4.35246196643647E-5,5.39830173117277E-5,6.44389677343631E-5),
 .UNSPECIFIED.);
#26112=B_SPLINE_CURVE_WITH_KNOTS('',3,(#418745,#418746,#418747,#418748,
#418749,#418750,#418751,#418752,#418753,#418754,#418755,#418756,#418757,
#418758,#418759,#418760),.UNSPECIFIED.,.F.,.F.,(4,3,3,3,3,4),(0.,6.54397980774385E-6,
1.78746088883287E-5,2.90961555784962E-5,4.25056718483931E-5,6.52023395140203E-5),
 .UNSPECIFIED.);
#26113=B_SPLINE_CURVE_WITH_KNOTS('',3,(#418762,#418763,#418764,#418765,
#418766,#418767,#418768,#418769,#418770,#418771,#418772,#418773,#418774,
#418775,#418776,#418777),.UNSPECIFIED.,.F.,.F.,(4,3,3,3,3,4),(0.,1.81271519801732E-5,
3.33528222530966E-5,4.35246196643644E-5,5.39830173117271E-5,6.44389677343623E-5),
 .UNSPECIFIED.);
#26114=B_SPLINE_CURVE_WITH_KNOTS('',3,(#418784,#418785,#418786,#418787,
#418788,#418789,#418790,#418791,#418792,#418793,#418794,#418795,#418796,
#418797,#418798,#418799),.UNSPECIFIED.,.F.,.F.,(4,3,3,3,3,4),(0.,6.54397980774368E-6,
1.78746088883288E-5,2.90961555784964E-5,4.25056718483934E-5,6.5202339514021E-5),
 .UNSPECIFIED.);
#26115=B_SPLINE_CURVE_WITH_KNOTS('',3,(#418801,#418802,#418803,#418804,
#418805,#418806,#418807,#418808,#418809,#418810,#418811,#418812,#418813,
#418814,#418815,#418816),.UNSPECIFIED.,.F.,.F.,(4,3,3,3,3,4),(0.,1.81271519801731E-5,
3.33528222530967E-5,4.35246196643647E-5,5.39830173117274E-5,6.44389677343628E-5),
 .UNSPECIFIED.);
#26116=B_SPLINE_CURVE_WITH_KNOTS('',3,(#418823,#418824,#418825,#418826,
#418827,#418828,#418829,#418830,#418831,#418832,#418833,#418834,#418835,
#418836,#418837,#418838),.UNSPECIFIED.,.F.,.F.,(4,3,3,3,3,4),(0.,6.54397980774364E-6,
1.78746088883288E-5,2.90961555784963E-5,4.25056718483933E-5,6.52023395140208E-5),
 .UNSPECIFIED.);
#26117=B_SPLINE_CURVE_WITH_KNOTS('',3,(#418840,#418841,#418842,#418843,
#418844,#418845,#418846,#418847,#418848,#418849,#418850,#418851,#418852,
#418853,#418854,#418855),.UNSPECIFIED.,.F.,.F.,(4,3,3,3,3,4),(0.,1.8127151980173E-5,
3.33528222530965E-5,4.35246196643644E-5,5.39830173117271E-5,6.44389677343624E-5),
 .UNSPECIFIED.);
#26118=B_SPLINE_CURVE_WITH_KNOTS('',3,(#418862,#418863,#418864,#418865,
#418866,#418867,#418868,#418869,#418870,#418871,#418872,#418873,#418874,
#418875,#418876,#418877),.UNSPECIFIED.,.F.,.F.,(4,3,3,3,3,4),(0.,6.54397980774372E-6,
1.78746088883289E-5,2.90961555784963E-5,4.25056718483934E-5,6.52023395140209E-5),
 .UNSPECIFIED.);
#26119=B_SPLINE_CURVE_WITH_KNOTS('',3,(#418879,#418880,#418881,#418882,
#418883,#418884,#418885,#418886,#418887,#418888,#418889,#418890,#418891,
#418892,#418893,#418894),.UNSPECIFIED.,.F.,.F.,(4,3,3,3,3,4),(0.,1.81271519801731E-5,
3.33528222530967E-5,4.35246196643646E-5,5.39830173117274E-5,6.44389677343626E-5),
 .UNSPECIFIED.);
#26120=B_SPLINE_CURVE_WITH_KNOTS('',3,(#418901,#418902,#418903,#418904,
#418905,#418906,#418907,#418908,#418909,#418910,#418911,#418912,#418913,
#418914,#418915,#418916),.UNSPECIFIED.,.F.,.F.,(4,3,3,3,3,4),(0.,6.54397980774376E-6,
1.78746088883289E-5,2.90961555784963E-5,4.25056718483934E-5,6.52023395140209E-5),
 .UNSPECIFIED.);
#26121=B_SPLINE_CURVE_WITH_KNOTS('',3,(#418918,#418919,#418920,#418921,
#418922,#418923,#418924,#418925,#418926,#418927,#418928,#418929,#418930,
#418931,#418932,#418933),.UNSPECIFIED.,.F.,.F.,(4,3,3,3,3,4),(5.42101086242752E-20,
1.81271519801732E-5,3.33528222530966E-5,4.35246196643646E-5,5.39830173117274E-5,
6.44389677343629E-5),.UNSPECIFIED.);
#26122=B_SPLINE_CURVE_WITH_KNOTS('',3,(#418940,#418941,#418942,#418943,
#418944,#418945,#418946,#418947,#418948,#418949,#418950,#418951,#418952,
#418953,#418954,#418955),.UNSPECIFIED.,.F.,.F.,(4,3,3,3,3,4),(0.,6.54397980774381E-6,
1.78746088883288E-5,2.90961555784963E-5,4.25056718483934E-5,6.52023395140208E-5),
 .UNSPECIFIED.);
#26123=B_SPLINE_CURVE_WITH_KNOTS('',3,(#418957,#418958,#418959,#418960,
#418961,#418962,#418963,#418964,#418965,#418966,#418967,#418968,#418969,
#418970,#418971,#418972),.UNSPECIFIED.,.F.,.F.,(4,3,3,3,3,4),(2.71050543121376E-20,
1.81271519801731E-5,3.33528222530966E-5,4.35246196643646E-5,5.39830173117273E-5,
6.44389677343626E-5),.UNSPECIFIED.);
#26124=B_SPLINE_CURVE_WITH_KNOTS('',3,(#418979,#418980,#418981,#418982,
#418983,#418984,#418985,#418986,#418987,#418988,#418989,#418990,#418991,
#418992,#418993,#418994),.UNSPECIFIED.,.F.,.F.,(4,3,3,3,3,4),(0.,6.54397980774374E-6,
1.78746088883289E-5,2.90961555784963E-5,4.25056718483934E-5,6.52023395140209E-5),
 .UNSPECIFIED.);
#26125=B_SPLINE_CURVE_WITH_KNOTS('',3,(#418996,#418997,#418998,#418999,
#419000,#419001,#419002,#419003,#419004,#419005,#419006,#419007,#419008,
#419009,#419010,#419011),.UNSPECIFIED.,.F.,.F.,(4,3,3,3,3,4),(3.04931861011548E-20,
1.81271519801731E-5,3.33528222530966E-5,4.35246196643646E-5,5.39830173117273E-5,
6.44389677343626E-5),.UNSPECIFIED.);
#26126=B_SPLINE_CURVE_WITH_KNOTS('',3,(#419018,#419019,#419020,#419021,
#419022,#419023,#419024,#419025,#419026,#419027,#419028,#419029,#419030,
#419031,#419032,#419033),.UNSPECIFIED.,.F.,.F.,(4,3,3,3,3,4),(0.,6.54397980774372E-6,
1.78746088883289E-5,2.90961555784964E-5,4.25056718483934E-5,6.52023395140209E-5),
 .UNSPECIFIED.);
#26127=B_SPLINE_CURVE_WITH_KNOTS('',3,(#419035,#419036,#419037,#419038,
#419039,#419040,#419041,#419042,#419043,#419044,#419045,#419046,#419047,
#419048,#419049,#419050),.UNSPECIFIED.,.F.,.F.,(4,3,3,3,3,4),(2.71050543121376E-20,
1.81271519801731E-5,3.33528222530966E-5,4.35246196643646E-5,5.39830173117274E-5,
6.44389677343626E-5),.UNSPECIFIED.);
#26128=B_SPLINE_CURVE_WITH_KNOTS('',3,(#419057,#419058,#419059,#419060,
#419061,#419062,#419063,#419064,#419065,#419066,#419067,#419068,#419069,
#419070,#419071,#419072),.UNSPECIFIED.,.F.,.F.,(4,3,3,3,3,4),(0.,6.5439798077437E-6,
1.78746088883288E-5,2.90961555784964E-5,4.25056718483934E-5,6.52023395140209E-5),
 .UNSPECIFIED.);
#26129=B_SPLINE_CURVE_WITH_KNOTS('',3,(#419074,#419075,#419076,#419077,
#419078,#419079,#419080,#419081,#419082,#419083,#419084,#419085,#419086,
#419087,#419088,#419089),.UNSPECIFIED.,.F.,.F.,(4,3,3,3,3,4),(5.42101086242752E-20,
1.81271519801731E-5,3.33528222530966E-5,4.35246196643646E-5,5.39830173117275E-5,
6.44389677343629E-5),.UNSPECIFIED.);
#26130=B_SPLINE_CURVE_WITH_KNOTS('',3,(#419096,#419097,#419098,#419099,
#419100,#419101,#419102,#419103,#419104,#419105,#419106,#419107,#419108,
#419109,#419110,#419111),.UNSPECIFIED.,.F.,.F.,(4,3,3,3,3,4),(0.,6.54397980774373E-6,
1.78746088883289E-5,2.90961555784964E-5,4.25056718483935E-5,6.52023395140211E-5),
 .UNSPECIFIED.);
#26131=B_SPLINE_CURVE_WITH_KNOTS('',3,(#419113,#419114,#419115,#419116,
#419117,#419118,#419119,#419120,#419121,#419122,#419123,#419124,#419125,
#419126,#419127,#419128),.UNSPECIFIED.,.F.,.F.,(4,3,3,3,3,4),(0.,1.81271519801731E-5,
3.33528222530966E-5,4.35246196643647E-5,5.39830173117275E-5,6.44389677343629E-5),
 .UNSPECIFIED.);
#26132=B_SPLINE_CURVE_WITH_KNOTS('',3,(#419135,#419136,#419137,#419138,
#419139,#419140,#419141,#419142,#419143,#419144,#419145,#419146,#419147,
#419148,#419149,#419150),.UNSPECIFIED.,.F.,.F.,(4,3,3,3,3,4),(0.,6.54397980774369E-6,
1.78746088883289E-5,2.90961555784963E-5,4.25056718483934E-5,6.52023395140208E-5),
 .UNSPECIFIED.);
#26133=B_SPLINE_CURVE_WITH_KNOTS('',3,(#419152,#419153,#419154,#419155,
#419156,#419157,#419158,#419159,#419160,#419161,#419162,#419163,#419164,
#419165,#419166,#419167),.UNSPECIFIED.,.F.,.F.,(4,3,3,3,3,4),(0.,1.81271519801732E-5,
3.33528222530967E-5,4.35246196643647E-5,5.39830173117272E-5,6.44389677343624E-5),
 .UNSPECIFIED.);
#26134=B_SPLINE_CURVE_WITH_KNOTS('',3,(#419174,#419175,#419176,#419177,
#419178,#419179,#419180,#419181,#419182,#419183,#419184,#419185,#419186,
#419187,#419188,#419189),.UNSPECIFIED.,.F.,.F.,(4,3,3,3,3,4),(0.,6.54397980774364E-6,
1.78746088883289E-5,2.90961555784963E-5,4.25056718483934E-5,6.52023395140209E-5),
 .UNSPECIFIED.);
#26135=B_SPLINE_CURVE_WITH_KNOTS('',3,(#419191,#419192,#419193,#419194,
#419195,#419196,#419197,#419198,#419199,#419200,#419201,#419202,#419203,
#419204,#419205,#419206),.UNSPECIFIED.,.F.,.F.,(4,3,3,3,3,4),(0.,1.81271519801732E-5,
3.33528222530968E-5,4.35246196643649E-5,5.39830173117278E-5,6.4438967734363E-5),
 .UNSPECIFIED.);
#26136=B_SPLINE_CURVE_WITH_KNOTS('',3,(#419213,#419214,#419215,#419216,
#419217,#419218,#419219,#419220,#419221,#419222,#419223,#419224,#419225,
#419226,#419227,#419228),.UNSPECIFIED.,.F.,.F.,(4,3,3,3,3,4),(0.,6.54397980774374E-6,
1.78746088883289E-5,2.90961555784962E-5,4.25056718483933E-5,6.52023395140208E-5),
 .UNSPECIFIED.);
#26137=B_SPLINE_CURVE_WITH_KNOTS('',3,(#419230,#419231,#419232,#419233,
#419234,#419235,#419236,#419237,#419238,#419239,#419240,#419241,#419242,
#419243,#419244,#419245),.UNSPECIFIED.,.F.,.F.,(4,3,3,3,3,4),(0.,1.81271519801732E-5,
3.33528222530967E-5,4.35246196643645E-5,5.39830173117275E-5,6.4438967734363E-5),
 .UNSPECIFIED.);
#26138=B_SPLINE_CURVE_WITH_KNOTS('',3,(#419252,#419253,#419254,#419255,
#419256,#419257,#419258,#419259,#419260,#419261,#419262,#419263,#419264,
#419265,#419266,#419267),.UNSPECIFIED.,.F.,.F.,(4,3,3,3,3,4),(0.,6.54397980774345E-6,
1.78746088883287E-5,2.90961555784962E-5,4.25056718483933E-5,6.52023395140207E-5),
 .UNSPECIFIED.);
#26139=B_SPLINE_CURVE_WITH_KNOTS('',3,(#419269,#419270,#419271,#419272,
#419273,#419274,#419275,#419276,#419277,#419278,#419279,#419280,#419281,
#419282,#419283,#419284),.UNSPECIFIED.,.F.,.F.,(4,3,3,3,3,4),(0.,1.81271519801731E-5,
3.33528222530967E-5,4.35246196643646E-5,5.39830173117276E-5,6.44389677343627E-5),
 .UNSPECIFIED.);
#26140=B_SPLINE_CURVE_WITH_KNOTS('',3,(#419291,#419292,#419293,#419294,
#419295,#419296,#419297,#419298,#419299,#419300,#419301,#419302,#419303,
#419304,#419305,#419306),.UNSPECIFIED.,.F.,.F.,(4,3,3,3,3,4),(0.,6.5439798077436E-6,
1.78746088883289E-5,2.90961555784961E-5,4.25056718483932E-5,6.52023395140208E-5),
 .UNSPECIFIED.);
#26141=B_SPLINE_CURVE_WITH_KNOTS('',3,(#419308,#419309,#419310,#419311,
#419312,#419313,#419314,#419315,#419316,#419317,#419318,#419319,#419320,
#419321,#419322,#419323),.UNSPECIFIED.,.F.,.F.,(4,3,3,3,3,4),(0.,1.81271519801732E-5,
3.33528222530966E-5,4.35246196643646E-5,5.39830173117277E-5,6.44389677343631E-5),
 .UNSPECIFIED.);
#26142=B_SPLINE_CURVE_WITH_KNOTS('',3,(#419330,#419331,#419332,#419333,
#419334,#419335,#419336,#419337,#419338,#419339,#419340,#419341,#419342,
#419343,#419344,#419345),.UNSPECIFIED.,.F.,.F.,(4,3,3,3,3,4),(0.,6.54397980774355E-6,
1.78746088883288E-5,2.90961555784961E-5,4.25056718483933E-5,6.52023395140206E-5),
 .UNSPECIFIED.);
#26143=B_SPLINE_CURVE_WITH_KNOTS('',3,(#419347,#419348,#419349,#419350,
#419351,#419352,#419353,#419354,#419355,#419356,#419357,#419358,#419359,
#419360,#419361,#419362),.UNSPECIFIED.,.F.,.F.,(4,3,3,3,3,4),(0.,1.81271519801731E-5,
3.33528222530965E-5,4.35246196643647E-5,5.39830173117274E-5,6.44389677343627E-5),
 .UNSPECIFIED.);
#26144=B_SPLINE_CURVE_WITH_KNOTS('',3,(#419369,#419370,#419371,#419372,
#419373,#419374,#419375,#419376,#419377,#419378,#419379,#419380,#419381,
#419382,#419383,#419384),.UNSPECIFIED.,.F.,.F.,(4,3,3,3,3,4),(0.,6.54397980774366E-6,
1.78746088883287E-5,2.90961555784963E-5,4.25056718483933E-5,6.52023395140209E-5),
 .UNSPECIFIED.);
#26145=B_SPLINE_CURVE_WITH_KNOTS('',3,(#419386,#419387,#419388,#419389,
#419390,#419391,#419392,#419393,#419394,#419395,#419396,#419397,#419398,
#419399,#419400,#419401),.UNSPECIFIED.,.F.,.F.,(4,3,3,3,3,4),(0.,1.81271519801732E-5,
3.33528222530969E-5,4.3524619664365E-5,5.39830173117279E-5,6.44389677343629E-5),
 .UNSPECIFIED.);
#26146=B_SPLINE_CURVE_WITH_KNOTS('',3,(#419408,#419409,#419410,#419411,
#419412,#419413,#419414,#419415,#419416,#419417,#419418,#419419,#419420,
#419421,#419422,#419423),.UNSPECIFIED.,.F.,.F.,(4,3,3,3,3,4),(0.,6.54397980774377E-6,
1.78746088883288E-5,2.90961555784961E-5,4.25056718483931E-5,6.52023395140207E-5),
 .UNSPECIFIED.);
#26147=B_SPLINE_CURVE_WITH_KNOTS('',3,(#419425,#419426,#419427,#419428,
#419429,#419430,#419431,#419432,#419433,#419434,#419435,#419436,#419437,
#419438,#419439,#419440),.UNSPECIFIED.,.F.,.F.,(4,3,3,3,3,4),(0.,1.81271519801731E-5,
3.33528222530965E-5,4.35246196643647E-5,5.39830173117273E-5,6.44389677343631E-5),
 .UNSPECIFIED.);
#26148=B_SPLINE_CURVE_WITH_KNOTS('',3,(#419447,#419448,#419449,#419450,
#419451,#419452,#419453,#419454,#419455,#419456,#419457,#419458,#419459,
#419460,#419461,#419462),.UNSPECIFIED.,.F.,.F.,(4,3,3,3,3,4),(0.,6.54397980774363E-6,
1.78746088883288E-5,2.90961555784963E-5,4.25056718483932E-5,6.52023395140206E-5),
 .UNSPECIFIED.);
#26149=B_SPLINE_CURVE_WITH_KNOTS('',3,(#419464,#419465,#419466,#419467,
#419468,#419469,#419470,#419471,#419472,#419473,#419474,#419475,#419476,
#419477,#419478,#419479),.UNSPECIFIED.,.F.,.F.,(4,3,3,3,3,4),(0.,1.81271519801732E-5,
3.33528222530967E-5,4.35246196643648E-5,5.39830173117274E-5,6.44389677343624E-5),
 .UNSPECIFIED.);
#26150=B_SPLINE_CURVE_WITH_KNOTS('',3,(#419486,#419487,#419488,#419489,
#419490,#419491,#419492,#419493,#419494,#419495,#419496,#419497,#419498,
#419499,#419500,#419501),.UNSPECIFIED.,.F.,.F.,(4,3,3,3,3,4),(0.,6.5439798077438E-6,
1.78746088883289E-5,2.90961555784965E-5,4.25056718483936E-5,6.52023395140211E-5),
 .UNSPECIFIED.);
#26151=B_SPLINE_CURVE_WITH_KNOTS('',3,(#419503,#419504,#419505,#419506,
#419507,#419508,#419509,#419510,#419511,#419512,#419513,#419514,#419515,
#419516,#419517,#419518),.UNSPECIFIED.,.F.,.F.,(4,3,3,3,3,4),(0.,1.81271519801732E-5,
3.33528222530968E-5,4.35246196643648E-5,5.39830173117278E-5,6.44389677343629E-5),
 .UNSPECIFIED.);
#26152=B_SPLINE_CURVE_WITH_KNOTS('',3,(#419525,#419526,#419527,#419528,
#419529,#419530,#419531,#419532,#419533,#419534,#419535,#419536,#419537,
#419538,#419539,#419540),.UNSPECIFIED.,.F.,.F.,(4,3,3,3,3,4),(0.,6.54397980774342E-6,
1.78746088883288E-5,2.90961555784962E-5,4.25056718483932E-5,6.52023395140207E-5),
 .UNSPECIFIED.);
#26153=B_SPLINE_CURVE_WITH_KNOTS('',3,(#419542,#419543,#419544,#419545,
#419546,#419547,#419548,#419549,#419550,#419551,#419552,#419553,#419554,
#419555,#419556,#419557),.UNSPECIFIED.,.F.,.F.,(4,3,3,3,3,4),(0.,1.81271519801731E-5,
3.33528222530964E-5,4.35246196643644E-5,5.39830173117272E-5,6.44389677343626E-5),
 .UNSPECIFIED.);
#26154=B_SPLINE_CURVE_WITH_KNOTS('',3,(#419564,#419565,#419566,#419567,
#419568,#419569,#419570,#419571,#419572,#419573,#419574,#419575,#419576,
#419577,#419578,#419579),.UNSPECIFIED.,.F.,.F.,(4,3,3,3,3,4),(0.,6.54397980774389E-6,
1.7874608888329E-5,2.90961555784964E-5,4.25056718483935E-5,6.5202339514021E-5),
 .UNSPECIFIED.);
#26155=B_SPLINE_CURVE_WITH_KNOTS('',3,(#419581,#419582,#419583,#419584,
#419585,#419586,#419587,#419588,#419589,#419590,#419591,#419592,#419593,
#419594,#419595,#419596),.UNSPECIFIED.,.F.,.F.,(4,3,3,3,3,4),(0.,1.81271519801731E-5,
3.33528222530965E-5,4.35246196643644E-5,5.39830173117275E-5,6.44389677343631E-5),
 .UNSPECIFIED.);
#26156=B_SPLINE_CURVE_WITH_KNOTS('',3,(#419603,#419604,#419605,#419606,
#419607,#419608,#419609,#419610,#419611,#419612,#419613,#419614,#419615,
#419616,#419617,#419618),.UNSPECIFIED.,.F.,.F.,(4,3,3,3,3,4),(0.,6.54397980774396E-6,
1.7874608888329E-5,2.90961555784966E-5,4.25056718483937E-5,6.52023395140212E-5),
 .UNSPECIFIED.);
#26157=B_SPLINE_CURVE_WITH_KNOTS('',3,(#419620,#419621,#419622,#419623,
#419624,#419625,#419626,#419627,#419628,#419629,#419630,#419631,#419632,
#419633,#419634,#419635),.UNSPECIFIED.,.F.,.F.,(4,3,3,3,3,4),(0.,1.81271519801731E-5,
3.33528222530966E-5,4.35246196643646E-5,5.39830173117271E-5,6.44389677343625E-5),
 .UNSPECIFIED.);
#26158=B_SPLINE_CURVE_WITH_KNOTS('',3,(#419642,#419643,#419644,#419645,
#419646,#419647,#419648,#419649,#419650,#419651,#419652,#419653,#419654,
#419655,#419656,#419657),.UNSPECIFIED.,.F.,.F.,(4,3,3,3,3,4),(0.,6.54397980774352E-6,
1.78746088883288E-5,2.90961555784962E-5,4.25056718483933E-5,6.52023395140208E-5),
 .UNSPECIFIED.);
#26159=B_SPLINE_CURVE_WITH_KNOTS('',3,(#419659,#419660,#419661,#419662,
#419663,#419664,#419665,#419666,#419667,#419668,#419669,#419670,#419671,
#419672,#419673,#419674),.UNSPECIFIED.,.F.,.F.,(4,3,3,3,3,4),(5.42101086242752E-20,
1.81271519801732E-5,3.33528222530967E-5,4.35246196643647E-5,5.39830173117276E-5,
6.4438967734363E-5),.UNSPECIFIED.);
#26160=B_SPLINE_CURVE_WITH_KNOTS('',3,(#419681,#419682,#419683,#419684,
#419685,#419686,#419687,#419688,#419689,#419690,#419691,#419692,#419693,
#419694,#419695,#419696),.UNSPECIFIED.,.F.,.F.,(4,3,3,3,3,4),(0.,6.54397980774381E-6,
1.7874608888329E-5,2.90961555784965E-5,4.25056718483935E-5,6.52023395140209E-5),
 .UNSPECIFIED.);
#26161=B_SPLINE_CURVE_WITH_KNOTS('',3,(#419698,#419699,#419700,#419701,
#419702,#419703,#419704,#419705,#419706,#419707,#419708,#419709,#419710,
#419711,#419712,#419713),.UNSPECIFIED.,.F.,.F.,(4,3,3,3,3,4),(5.42101086242752E-20,
1.81271519801731E-5,3.33528222530966E-5,4.35246196643646E-5,5.39830173117274E-5,
6.44389677343628E-5),.UNSPECIFIED.);
#26162=B_SPLINE_CURVE_WITH_KNOTS('',3,(#419720,#419721,#419722,#419723,
#419724,#419725,#419726,#419727,#419728,#419729,#419730,#419731,#419732,
#419733,#419734,#419735),.UNSPECIFIED.,.F.,.F.,(4,3,3,3,3,4),(0.,6.54397980774374E-6,
1.78746088883289E-5,2.90961555784964E-5,4.25056718483934E-5,6.52023395140209E-5),
 .UNSPECIFIED.);
#26163=B_SPLINE_CURVE_WITH_KNOTS('',3,(#419737,#419738,#419739,#419740,
#419741,#419742,#419743,#419744,#419745,#419746,#419747,#419748,#419749,
#419750,#419751,#419752),.UNSPECIFIED.,.F.,.F.,(4,3,3,3,3,4),(2.71050543121376E-20,
1.81271519801731E-5,3.33528222530966E-5,4.35246196643646E-5,5.39830173117275E-5,
6.44389677343629E-5),.UNSPECIFIED.);
#26164=B_SPLINE_CURVE_WITH_KNOTS('',3,(#419987,#419988,#419989,#419990,
#419991,#419992,#419993,#419994,#419995,#419996,#419997,#419998,#419999,
#420000,#420001,#420002,#420003,#420004,#420005,#420006,#420007,#420008,
#420009,#420010,#420011,#420012,#420013,#420014,#420015,#420016,#420017,
#420018,#420019,#420020,#420021,#420022,#420023),.UNSPECIFIED.,.F.,.F.,
(4,3,3,3,3,3,3,3,3,3,3,3,4),(0.,9.59031527198933E-6,1.94769411222704E-5,
2.02405092183152E-5,3.21374138577714E-5,3.60302195070439E-5,4.42640648818668E-5,
4.53660204229443E-5,5.03633762302166E-5,5.17708036292896E-5,5.37928993851989E-5,
5.541037554602E-5,5.64557889510063E-5),.UNSPECIFIED.);
#26165=B_SPLINE_CURVE_WITH_KNOTS('',3,(#420025,#420026,#420027,#420028,
#420029,#420030,#420031,#420032,#420033,#420034,#420035,#420036,#420037,
#420038,#420039,#420040,#420041,#420042,#420043,#420044,#420045,#420046,
#420047,#420048,#420049,#420050,#420051,#420052),.UNSPECIFIED.,.F.,.F.,
(4,3,3,3,3,3,3,3,3,4),(5.64557889510063E-5,5.98940966493751E-5,6.3421400387338E-5,
7.22241476085188E-5,7.38322796533364E-5,8.36529189331468E-5,8.80714278222499E-5,
9.84837568501108E-5,0.000108624704079211,0.000110823272382853),
 .UNSPECIFIED.);
#26166=B_SPLINE_CURVE_WITH_KNOTS('',3,(#420064,#420065,#420066,#420067),
 .UNSPECIFIED.,.F.,.F.,(4,4),(4.43935777737106E-19,7.70025630629237E-5),
 .UNSPECIFIED.);
#26167=B_SPLINE_CURVE_WITH_KNOTS('',3,(#420076,#420077,#420078,#420079),
 .UNSPECIFIED.,.F.,.F.,(4,4),(0.,7.7002563062924E-5),.UNSPECIFIED.);
#26168=B_SPLINE_CURVE_WITH_KNOTS('',3,(#422619,#422620,#422621,#422622,
#422623,#422624,#422625,#422626,#422627,#422628,#422629,#422630,#422631,
#422632,#422633,#422634,#422635,#422636,#422637,#422638,#422639,#422640,
#422641,#422642,#422643,#422644,#422645,#422646,#422647,#422648,#422649,
#422650,#422651,#422652),.UNSPECIFIED.,.F.,.F.,(4,3,3,3,3,3,3,3,3,3,3,4),
(0.,4.2915783730415E-6,5.42772623795336E-6,1.00901698482348E-5,1.31279195068639E-5,
1.57383542265889E-5,1.61011507492104E-5,1.67166789291755E-5,1.95343262811359E-5,
2.29377234674649E-5,2.71556047620058E-5,3.34407099942658E-5),
 .UNSPECIFIED.);
#26169=B_SPLINE_CURVE_WITH_KNOTS('',3,(#422654,#422655,#422656,#422657,
#422658,#422659,#422660),.UNSPECIFIED.,.F.,.F.,(4,3,4),(0.,4.40000041065376E-5,
9.89910850773113E-5),.UNSPECIFIED.);
#26170=B_SPLINE_CURVE_WITH_KNOTS('',3,(#422673,#422674,#422675,#422676,
#422677,#422678,#422679,#422680,#422681,#422682,#422683,#422684,#422685,
#422686,#422687,#422688,#422689,#422690,#422691,#422692,#422693,#422694,
#422695,#422696,#422697,#422698,#422699,#422700),.UNSPECIFIED.,.F.,.F.,
(4,3,3,3,3,3,3,3,3,4),(0.,8.6603962858312E-6,1.64707715200666E-5,2.24502894132279E-5,
2.49975961757824E-5,2.88526003690281E-5,3.10661348995016E-5,3.4305354351696E-5,
3.66410545653559E-5,4.00504537627887E-5),.UNSPECIFIED.);
#26171=B_SPLINE_CURVE_WITH_KNOTS('',3,(#422761,#422762,#422763,#422764,
#422765,#422766,#422767,#422768,#422769,#422770,#422771,#422772,#422773,
#422774,#422775,#422776,#422777,#422778,#422779,#422780,#422781,#422782,
#422783,#422784,#422785,#422786,#422787,#422788,#422789,#422790,#422791,
#422792,#422793,#422794),.UNSPECIFIED.,.F.,.F.,(4,3,3,3,3,3,3,3,3,3,3,4),
(8.80914265144472E-20,3.71309426656646E-6,5.39981071559417E-6,8.78933289332424E-6,
9.0027235706752E-6,1.07143984504149E-5,1.60780299679549E-5,1.65806081157686E-5,
2.30369726850657E-5,2.67819200416086E-5,3.59736924187689E-5,4.03862783807E-5),
 .UNSPECIFIED.);
#26172=B_SPLINE_CURVE_WITH_KNOTS('',3,(#422877,#422878,#422879,#422880),
 .UNSPECIFIED.,.F.,.F.,(4,4),(0.,7.7002563062924E-5),.UNSPECIFIED.);
#26173=B_SPLINE_CURVE_WITH_KNOTS('',3,(#422890,#422891,#422892,#422893),
 .UNSPECIFIED.,.F.,.F.,(4,4),(4.47028007668187E-19,7.70025630629238E-5),
 .UNSPECIFIED.);
#26174=B_SPLINE_CURVE_WITH_KNOTS('',3,(#422897,#422898,#422899,#422900,
#422901,#422902,#422903,#422904,#422905,#422906,#422907,#422908,#422909,
#422910,#422911,#422912,#422913,#422914,#422915,#422916,#422917,#422918,
#422919,#422920,#422921,#422922,#422923,#422924,#422925,#422926,#422927,
#422928,#422929,#422930,#422931,#422932,#422933),.UNSPECIFIED.,.F.,.F.,
(4,3,3,3,3,3,3,3,3,3,3,3,4),(0.,9.59031527200574E-6,1.94769411222917E-5,
2.02405092183154E-5,3.21374138577699E-5,3.6030219507044E-5,4.42640648818861E-5,
4.53660204229444E-5,5.03633762302092E-5,5.17708036292896E-5,5.37928993851989E-5,
5.541037554602E-5,5.64557889507966E-5),.UNSPECIFIED.);
#26175=B_SPLINE_CURVE_WITH_KNOTS('',3,(#422934,#422935,#422936,#422937,
#422938,#422939,#422940,#422941,#422942,#422943,#422944,#422945,#422946,
#422947,#422948,#422949,#422950,#422951,#422952,#422953,#422954,#422955,
#422956,#422957,#422958,#422959,#422960,#422961),.UNSPECIFIED.,.F.,.F.,
(4,3,3,3,3,3,3,3,3,4),(5.64557889507966E-5,5.98940966493751E-5,6.34214003873381E-5,
7.22241476085334E-5,7.38322796533363E-5,8.3652918933141E-5,8.80714278222501E-5,
9.8483756850102E-5,0.000108624704079186,0.000110823272382853),
 .UNSPECIFIED.);
#26176=B_SPLINE_CURVE_WITH_KNOTS('',3,(#422977,#422978,#422979,#422980,
#422981,#422982,#422983,#422984,#422985,#422986,#422987,#422988,#422989,
#422990,#422991,#422992,#422993,#422994,#422995,#422996,#422997,#422998,
#422999,#423000,#423001,#423002,#423003,#423004),.UNSPECIFIED.,.F.,.F.,
(4,3,3,3,3,3,3,3,3,4),(0.,8.6603962857854E-6,1.64707715200666E-5,2.24502894132548E-5,
2.49975961757822E-5,2.8852600369028E-5,3.10661348995016E-5,3.43053543516959E-5,
3.66410545653558E-5,4.00504537627886E-5),.UNSPECIFIED.);
#26177=B_SPLINE_CURVE_WITH_KNOTS('',3,(#423007,#423008,#423009,#423010,
#423011,#423012,#423013),.UNSPECIFIED.,.F.,.F.,(4,3,4),(0.,4.40000041065377E-5,
9.89910850773114E-5),.UNSPECIFIED.);
#26178=B_SPLINE_CURVE_WITH_KNOTS('',3,(#423034,#423035,#423036,#423037,
#423038,#423039,#423040,#423041,#423042,#423043,#423044,#423045,#423046,
#423047,#423048,#423049,#423050,#423051,#423052,#423053,#423054,#423055,
#423056,#423057,#423058,#423059,#423060,#423061,#423062,#423063,#423064,
#423065,#423066,#423067),.UNSPECIFIED.,.F.,.F.,(4,3,3,3,3,3,3,3,3,3,3,4),
(0.,4.29157837303072E-6,5.42772623795326E-6,1.00901698482348E-5,1.31279195068639E-5,
1.57383542265865E-5,1.61011507492105E-5,1.67166789291757E-5,1.9534326281136E-5,
2.29377234674651E-5,2.7155604762006E-5,3.34407099942659E-5),
 .UNSPECIFIED.);
#26179=B_SPLINE_CURVE_WITH_KNOTS('',3,(#423080,#423081,#423082,#423083,
#423084,#423085,#423086,#423087,#423088,#423089,#423090,#423091,#423092,
#423093,#423094,#423095,#423096,#423097,#423098,#423099,#423100,#423101,
#423102,#423103,#423104,#423105,#423106,#423107,#423108,#423109,#423110,
#423111,#423112,#423113),.UNSPECIFIED.,.F.,.F.,(4,3,3,3,3,3,3,3,3,3,3,4),
(5.42101086242752E-20,3.71309426656642E-6,5.39981071559419E-6,8.78933289366534E-6,
9.00272357067523E-6,1.0714398450415E-5,1.60780299679576E-5,1.65806081157688E-5,
2.30369726850415E-5,2.67819200416087E-5,3.59736924187938E-5,4.03862783807003E-5),
 .UNSPECIFIED.);
#26180=B_SPLINE_CURVE_WITH_KNOTS('',3,(#423226,#423227,#423228,#423229),
 .UNSPECIFIED.,.F.,.F.,(4,4),(0.,7.70025630629239E-5),.UNSPECIFIED.);
#26181=B_SPLINE_CURVE_WITH_KNOTS('',3,(#423239,#423240,#423241,#423242),
 .UNSPECIFIED.,.F.,.F.,(4,4),(4.41238316394827E-19,7.70025630629238E-5),
 .UNSPECIFIED.);
#26182=B_SPLINE_CURVE_WITH_KNOTS('',3,(#423246,#423247,#423248,#423249,
#423250,#423251,#423252,#423253,#423254,#423255,#423256,#423257,#423258,
#423259,#423260,#423261,#423262,#423263,#423264,#423265,#423266,#423267,
#423268,#423269,#423270,#423271,#423272,#423273,#423274,#423275,#423276,
#423277,#423278,#423279,#423280,#423281,#423282),.UNSPECIFIED.,.F.,.F.,
(4,3,3,3,3,3,3,3,3,3,3,3,4),(0.,9.59031527201346E-6,1.94769411223158E-5,
2.02405092183153E-5,3.21374138577746E-5,3.6030219507044E-5,4.42640648818315E-5,
4.53660204229444E-5,5.03633762302215E-5,5.17708036292896E-5,5.37928993851989E-5,
5.54103755460195E-5,5.64557889513096E-5),.UNSPECIFIED.);
#26183=B_SPLINE_CURVE_WITH_KNOTS('',3,(#423283,#423284,#423285,#423286,
#423287,#423288,#423289,#423290,#423291,#423292,#423293,#423294,#423295,
#423296,#423297,#423298,#423299,#423300,#423301,#423302,#423303,#423304,
#423305,#423306,#423307,#423308,#423309,#423310),.UNSPECIFIED.,.F.,.F.,
(4,3,3,3,3,3,3,3,3,4),(5.64557889513096E-5,5.98940966493751E-5,6.3421400387338E-5,
7.22241476084388E-5,7.38322796533364E-5,8.36529189331415E-5,8.807142782225E-5,
9.84837568500727E-5,0.000108624704079135,0.000110823272382853),
 .UNSPECIFIED.);
#26184=B_SPLINE_CURVE_WITH_KNOTS('',3,(#423326,#423327,#423328,#423329,
#423330,#423331,#423332,#423333,#423334,#423335,#423336,#423337,#423338,
#423339,#423340,#423341,#423342,#423343,#423344,#423345,#423346,#423347,
#423348,#423349,#423350,#423351,#423352,#423353),.UNSPECIFIED.,.F.,.F.,
(4,3,3,3,3,3,3,3,3,4),(0.,8.66039628581207E-6,1.64707715200665E-5,2.24502894132646E-5,
2.49975961757823E-5,2.8852600369028E-5,3.10661348995016E-5,3.43053543516961E-5,
3.66410545653561E-5,4.00504537627889E-5),.UNSPECIFIED.);
#26185=B_SPLINE_CURVE_WITH_KNOTS('',3,(#423356,#423357,#423358,#423359,
#423360,#423361,#423362),.UNSPECIFIED.,.F.,.F.,(4,3,4),(0.,4.40000041065374E-5,
9.89910850773114E-5),.UNSPECIFIED.);
#26186=B_SPLINE_CURVE_WITH_KNOTS('',3,(#423383,#423384,#423385,#423386,
#423387,#423388,#423389,#423390,#423391,#423392,#423393,#423394,#423395,
#423396,#423397,#423398,#423399,#423400,#423401,#423402,#423403,#423404,
#423405,#423406,#423407,#423408,#423409,#423410,#423411,#423412,#423413,
#423414,#423415,#423416),.UNSPECIFIED.,.F.,.F.,(4,3,3,3,3,3,3,3,3,3,3,4),
(0.,4.29157837302144E-6,5.4277262379533E-6,1.00901698482348E-5,1.3127919506864E-5,
1.57383542265789E-5,1.61011507492104E-5,1.67166789291755E-5,1.95343262811359E-5,
2.29377234674649E-5,2.71556047620059E-5,3.34407099942658E-5),
 .UNSPECIFIED.);
#26187=B_SPLINE_CURVE_WITH_KNOTS('',3,(#423429,#423430,#423431,#423432,
#423433,#423434,#423435,#423436,#423437,#423438,#423439,#423440,#423441,
#423442,#423443,#423444,#423445,#423446,#423447,#423448,#423449,#423450,
#423451,#423452,#423453,#423454,#423455,#423456,#423457,#423458,#423459,
#423460,#423461,#423462),.UNSPECIFIED.,.F.,.F.,(4,3,3,3,3,3,3,3,3,3,3,4),
(5.42101086242752E-20,3.71309426656648E-6,5.39981071559418E-6,8.78933289330926E-6,
9.0027235706753E-6,1.0714398450415E-5,1.60780299679585E-5,1.65806081157688E-5,
2.3036972685038E-5,2.67819200416088E-5,3.59736924188206E-5,4.03862783807005E-5),
 .UNSPECIFIED.);
#26188=B_SPLINE_CURVE_WITH_KNOTS('',3,(#423575,#423576,#423577,#423578),
 .UNSPECIFIED.,.F.,.F.,(4,4),(0.,7.70025630629239E-5),.UNSPECIFIED.);
#26189=B_SPLINE_CURVE_WITH_KNOTS('',3,(#423588,#423589,#423590,#423591),
 .UNSPECIFIED.,.F.,.F.,(4,4),(4.37055868292169E-19,7.70025630629239E-5),
 .UNSPECIFIED.);
#26190=B_SPLINE_CURVE_WITH_KNOTS('',3,(#423595,#423596,#423597,#423598,
#423599,#423600,#423601,#423602,#423603,#423604,#423605,#423606,#423607,
#423608,#423609,#423610,#423611,#423612,#423613,#423614,#423615,#423616,
#423617,#423618,#423619,#423620,#423621,#423622,#423623,#423624,#423625,
#423626,#423627,#423628,#423629,#423630,#423631),.UNSPECIFIED.,.F.,.F.,
(4,3,3,3,3,3,3,3,3,3,3,3,4),(0.,9.59031527200032E-6,1.94769411222912E-5,
2.02405092183152E-5,3.21374138577754E-5,3.60302195070438E-5,4.42640648818326E-5,
4.53660204229441E-5,5.03633762302261E-5,5.17708036292895E-5,5.37928993851988E-5,
5.54103755460196E-5,5.64557889505696E-5),.UNSPECIFIED.);
#26191=B_SPLINE_CURVE_WITH_KNOTS('',3,(#423632,#423633,#423634,#423635,
#423636,#423637,#423638,#423639,#423640,#423641,#423642,#423643,#423644,
#423645,#423646,#423647,#423648,#423649,#423650,#423651,#423652,#423653,
#423654,#423655,#423656,#423657,#423658,#423659),.UNSPECIFIED.,.F.,.F.,
(4,3,3,3,3,3,3,3,3,4),(5.64557889505696E-5,5.98940966493749E-5,6.34214003873378E-5,
7.22241476084911E-5,7.38322796533361E-5,8.3652918933132E-5,8.80714278222497E-5,
9.84837568500572E-5,0.000108624704079099,0.000110823272382853),
 .UNSPECIFIED.);
#26192=B_SPLINE_CURVE_WITH_KNOTS('',3,(#423675,#423676,#423677,#423678,
#423679,#423680,#423681,#423682,#423683,#423684,#423685,#423686,#423687,
#423688,#423689,#423690,#423691,#423692,#423693,#423694,#423695,#423696,
#423697,#423698,#423699,#423700,#423701,#423702),.UNSPECIFIED.,.F.,.F.,
(4,3,3,3,3,3,3,3,3,4),(0.,8.6603962858033E-6,1.64707715200666E-5,2.24502894132316E-5,
2.49975961757823E-5,2.8852600369028E-5,3.10661348995016E-5,3.43053543516961E-5,
3.6641054565356E-5,4.00504537627889E-5),.UNSPECIFIED.);
#26193=B_SPLINE_CURVE_WITH_KNOTS('',3,(#423705,#423706,#423707,#423708,
#423709,#423710,#423711),.UNSPECIFIED.,.F.,.F.,(4,3,4),(0.,4.40000041065376E-5,
9.89910850773116E-5),.UNSPECIFIED.);
#26194=B_SPLINE_CURVE_WITH_KNOTS('',3,(#423732,#423733,#423734,#423735,
#423736,#423737,#423738,#423739,#423740,#423741,#423742,#423743,#423744,
#423745,#423746,#423747,#423748,#423749,#423750,#423751,#423752,#423753,
#423754,#423755,#423756,#423757,#423758,#423759,#423760,#423761,#423762,
#423763,#423764,#423765),.UNSPECIFIED.,.F.,.F.,(4,3,3,3,3,3,3,3,3,3,3,4),
(0.,4.29157837303003E-6,5.42772623795338E-6,1.00901698482344E-5,1.31279195068639E-5,
1.57383542265823E-5,1.61011507492103E-5,1.67166789291752E-5,1.95343262811357E-5,
2.29377234674648E-5,2.71556047620056E-5,3.34407099942655E-5),
 .UNSPECIFIED.);
#26195=B_SPLINE_CURVE_WITH_KNOTS('',3,(#423778,#423779,#423780,#423781,
#423782,#423783,#423784,#423785,#423786,#423787,#423788,#423789,#423790,
#423791,#423792,#423793,#423794,#423795,#423796,#423797,#423798,#423799,
#423800,#423801,#423802,#423803,#423804,#423805,#423806,#423807,#423808,
#423809,#423810,#423811),.UNSPECIFIED.,.F.,.F.,(4,3,3,3,3,3,3,3,3,3,3,4),
(5.42101086242752E-20,3.71309426656649E-6,5.39981071559419E-6,8.78933289329362E-6,
9.00272357067532E-6,1.0714398450415E-5,1.60780299679622E-5,1.65806081157688E-5,
2.30369726850379E-5,2.67819200416089E-5,3.59736924187726E-5,4.03862783807006E-5),
 .UNSPECIFIED.);
#26196=B_SPLINE_CURVE_WITH_KNOTS('',3,(#423924,#423925,#423926,#423927),
 .UNSPECIFIED.,.F.,.F.,(4,4),(0.,7.70025630629241E-5),.UNSPECIFIED.);
#26197=B_SPLINE_CURVE_WITH_KNOTS('',3,(#423937,#423938,#423939,#423940),
 .UNSPECIFIED.,.F.,.F.,(4,4),(4.33680868994202E-19,7.70025630629239E-5),
 .UNSPECIFIED.);
#26198=B_SPLINE_CURVE_WITH_KNOTS('',3,(#423944,#423945,#423946,#423947,
#423948,#423949,#423950,#423951,#423952,#423953,#423954,#423955,#423956,
#423957,#423958,#423959,#423960,#423961,#423962,#423963,#423964,#423965,
#423966,#423967,#423968,#423969,#423970,#423971,#423972,#423973,#423974,
#423975,#423976,#423977,#423978,#423979,#423980),.UNSPECIFIED.,.F.,.F.,
(4,3,3,3,3,3,3,3,3,3,3,3,4),(0.,9.5903152720106E-6,1.94769411223126E-5,
2.02405092183153E-5,3.21374138577666E-5,3.60302195070438E-5,4.42640648818143E-5,
4.53660204229444E-5,5.0363376230216E-5,5.17708036292896E-5,5.37928993851988E-5,
5.54103755460201E-5,5.64557889507744E-5),.UNSPECIFIED.);
#26199=B_SPLINE_CURVE_WITH_KNOTS('',3,(#423981,#423982,#423983,#423984,
#423985,#423986,#423987,#423988,#423989,#423990,#423991,#423992,#423993,
#423994,#423995,#423996,#423997,#423998,#423999,#424000,#424001,#424002,
#424003,#424004,#424005,#424006,#424007,#424008),.UNSPECIFIED.,.F.,.F.,
(4,3,3,3,3,3,3,3,3,4),(5.64557889507744E-5,5.98940966493751E-5,6.34214003873379E-5,
7.22241476084577E-5,7.38322796533363E-5,8.36529189331507E-5,8.80714278222499E-5,
9.84837568500952E-5,0.000108624704079183,0.000110823272382853),
 .UNSPECIFIED.);
#26200=B_SPLINE_CURVE_WITH_KNOTS('',3,(#424024,#424025,#424026,#424027,
#424028,#424029,#424030,#424031,#424032,#424033,#424034,#424035,#424036,
#424037,#424038,#424039,#424040,#424041,#424042,#424043,#424044,#424045,
#424046,#424047,#424048,#424049,#424050,#424051),.UNSPECIFIED.,.F.,.F.,
(4,3,3,3,3,3,3,3,3,4),(0.,8.66039628581227E-6,1.64707715200666E-5,2.24502894132344E-5,
2.49975961757823E-5,2.8852600369028E-5,3.10661348995015E-5,3.4305354351696E-5,
3.66410545653559E-5,4.00504537627887E-5),.UNSPECIFIED.);
#26201=B_SPLINE_CURVE_WITH_KNOTS('',3,(#424054,#424055,#424056,#424057,
#424058,#424059,#424060),.UNSPECIFIED.,.F.,.F.,(4,3,4),(0.,4.40000041065374E-5,
9.8991085077311E-5),.UNSPECIFIED.);
#26202=B_SPLINE_CURVE_WITH_KNOTS('',3,(#424081,#424082,#424083,#424084,
#424085,#424086,#424087,#424088,#424089,#424090,#424091,#424092,#424093,
#424094,#424095,#424096,#424097,#424098,#424099,#424100,#424101,#424102,
#424103,#424104,#424105,#424106,#424107,#424108,#424109,#424110,#424111,
#424112,#424113,#424114),.UNSPECIFIED.,.F.,.F.,(4,3,3,3,3,3,3,3,3,3,3,4),
(0.,4.29157837303544E-6,5.42772623795348E-6,1.0090169848235E-5,1.31279195068642E-5,
1.5738354226584E-5,1.61011507492107E-5,1.67166789291759E-5,1.95343262811362E-5,
2.29377234674651E-5,2.71556047620061E-5,3.34407099942662E-5),
 .UNSPECIFIED.);
#26203=B_SPLINE_CURVE_WITH_KNOTS('',3,(#424127,#424128,#424129,#424130,
#424131,#424132,#424133,#424134,#424135,#424136,#424137,#424138,#424139,
#424140,#424141,#424142,#424143,#424144,#424145,#424146,#424147,#424148,
#424149,#424150,#424151,#424152,#424153,#424154,#424155,#424156,#424157,
#424158,#424159,#424160),.UNSPECIFIED.,.F.,.F.,(4,3,3,3,3,3,3,3,3,3,3,4),
(1.0842021724855E-19,3.71309426656642E-6,5.39981071559425E-6,8.78933289331666E-6,
9.00272357067523E-6,1.07143984504148E-5,1.60780299679651E-5,1.65806081157685E-5,
2.30369726850497E-5,2.67819200416083E-5,3.59736924187557E-5,4.03862783806994E-5),
 .UNSPECIFIED.);
#26204=B_SPLINE_CURVE_WITH_KNOTS('',3,(#424273,#424274,#424275,#424276),
 .UNSPECIFIED.,.F.,.F.,(4,4),(0.,7.70025630629238E-5),.UNSPECIFIED.);
#26205=B_SPLINE_CURVE_WITH_KNOTS('',3,(#424286,#424287,#424288,#424289),
 .UNSPECIFIED.,.F.,.F.,(4,4),(4.33680868994202E-19,7.70025630629238E-5),
 .UNSPECIFIED.);
#26206=B_SPLINE_CURVE_WITH_KNOTS('',3,(#424293,#424294,#424295,#424296,
#424297,#424298,#424299,#424300,#424301,#424302,#424303,#424304,#424305,
#424306,#424307,#424308,#424309,#424310,#424311,#424312,#424313,#424314,
#424315,#424316,#424317,#424318,#424319,#424320,#424321,#424322,#424323,
#424324,#424325,#424326,#424327,#424328,#424329),.UNSPECIFIED.,.F.,.F.,
(4,3,3,3,3,3,3,3,3,3,3,3,4),(0.,9.5903152719965E-6,1.94769411222866E-5,
2.02405092183151E-5,3.21374138577523E-5,3.60302195070439E-5,4.42640648818848E-5,
4.53660204229442E-5,5.03633762302146E-5,5.17708036292897E-5,5.3792899385199E-5,
5.54103755460205E-5,5.64557889509545E-5),.UNSPECIFIED.);
#26207=B_SPLINE_CURVE_WITH_KNOTS('',3,(#424330,#424331,#424332,#424333,
#424334,#424335,#424336,#424337,#424338,#424339,#424340,#424341,#424342,
#424343,#424344,#424345,#424346,#424347,#424348,#424349,#424350,#424351,
#424352,#424353,#424354,#424355,#424356,#424357),.UNSPECIFIED.,.F.,.F.,
(4,3,3,3,3,3,3,3,3,4),(5.64557889509545E-5,5.98940966493752E-5,6.34214003873382E-5,
7.22241476085202E-5,7.38322796533367E-5,8.36529189331274E-5,8.80714278222504E-5,
9.84837568500655E-5,0.000108624704079124,0.000110823272382854),
 .UNSPECIFIED.);
#26208=B_SPLINE_CURVE_WITH_KNOTS('',3,(#424373,#424374,#424375,#424376,
#424377,#424378,#424379,#424380,#424381,#424382,#424383,#424384,#424385,
#424386,#424387,#424388,#424389,#424390,#424391,#424392,#424393,#424394,
#424395,#424396,#424397,#424398,#424399,#424400),.UNSPECIFIED.,.F.,.F.,
(4,3,3,3,3,3,3,3,3,4),(0.,8.66039628584811E-6,1.64707715200668E-5,2.24502894132374E-5,
2.49975961757828E-5,2.88526003690285E-5,3.10661348995021E-5,3.43053543516967E-5,
3.66410545653568E-5,4.00504537627891E-5),.UNSPECIFIED.);
#26209=B_SPLINE_CURVE_WITH_KNOTS('',3,(#424403,#424404,#424405,#424406,
#424407,#424408,#424409),.UNSPECIFIED.,.F.,.F.,(4,3,4),(0.,4.40000041065375E-5,
9.89910850773109E-5),.UNSPECIFIED.);
#26210=B_SPLINE_CURVE_WITH_KNOTS('',3,(#424430,#424431,#424432,#424433,
#424434,#424435,#424436,#424437,#424438,#424439,#424440,#424441,#424442,
#424443,#424444,#424445,#424446,#424447,#424448,#424449,#424450,#424451,
#424452,#424453,#424454,#424455,#424456,#424457,#424458,#424459,#424460,
#424461,#424462,#424463),.UNSPECIFIED.,.F.,.F.,(4,3,3,3,3,3,3,3,3,3,3,4),
(0.,4.29157837303359E-6,5.42772623795353E-6,1.00901698482349E-5,1.31279195068641E-5,
1.57383542265853E-5,1.61011507492106E-5,1.67166789291759E-5,1.95343262811364E-5,
2.29377234674653E-5,2.71556047620062E-5,3.34407099942664E-5),
 .UNSPECIFIED.);
#26211=B_SPLINE_CURVE_WITH_KNOTS('',3,(#424476,#424477,#424478,#424479,
#424480,#424481,#424482,#424483,#424484,#424485,#424486,#424487,#424488,
#424489,#424490,#424491,#424492,#424493,#424494,#424495,#424496,#424497,
#424498,#424499,#424500,#424501,#424502,#424503,#424504,#424505,#424506,
#424507,#424508,#424509),.UNSPECIFIED.,.F.,.F.,(4,3,3,3,3,3,3,3,3,3,3,4),
(0.,3.71309426656636E-6,5.39981071559408E-6,8.78933289330066E-6,9.00272357067524E-6,
1.07143984504147E-5,1.60780299679589E-5,1.65806081157685E-5,2.30369726850456E-5,
2.67819200416083E-5,3.59736924187622E-5,4.03862783806998E-5),
 .UNSPECIFIED.);
#26212=B_SPLINE_CURVE_WITH_KNOTS('',3,(#424622,#424623,#424624,#424625),
 .UNSPECIFIED.,.F.,.F.,(4,4),(0.,7.70025630629239E-5),.UNSPECIFIED.);
#26213=B_SPLINE_CURVE_WITH_KNOTS('',3,(#424635,#424636,#424637,#424638),
 .UNSPECIFIED.,.F.,.F.,(4,4),(4.33680868994202E-19,7.70025630629237E-5),
 .UNSPECIFIED.);
#26214=B_SPLINE_CURVE_WITH_KNOTS('',3,(#424642,#424643,#424644,#424645,
#424646,#424647,#424648,#424649,#424650,#424651,#424652,#424653,#424654,
#424655,#424656,#424657,#424658,#424659,#424660,#424661,#424662,#424663,
#424664,#424665,#424666,#424667,#424668,#424669,#424670,#424671,#424672,
#424673,#424674,#424675,#424676,#424677,#424678),.UNSPECIFIED.,.F.,.F.,
(4,3,3,3,3,3,3,3,3,3,3,3,4),(0.,9.59031527199588E-6,1.94769411222848E-5,
2.02405092183153E-5,3.21374138577599E-5,3.60302195070438E-5,4.42640648819043E-5,
4.53660204229442E-5,5.03633762301906E-5,5.17708036292898E-5,5.37928993851988E-5,
5.54103755460198E-5,5.64557889507646E-5),.UNSPECIFIED.);
#26215=B_SPLINE_CURVE_WITH_KNOTS('',3,(#424679,#424680,#424681,#424682,
#424683,#424684,#424685,#424686,#424687,#424688,#424689,#424690,#424691,
#424692,#424693,#424694,#424695,#424696,#424697,#424698,#424699,#424700,
#424701,#424702,#424703,#424704,#424705,#424706),.UNSPECIFIED.,.F.,.F.,
(4,3,3,3,3,3,3,3,3,4),(5.64557889507646E-5,5.98940966493748E-5,6.3421400387338E-5,
7.22241476084039E-5,7.38322796533363E-5,8.36529189331441E-5,8.80714278222497E-5,
9.84837568500709E-5,0.000108624704079132,0.000110823272382853),
 .UNSPECIFIED.);
#26216=B_SPLINE_CURVE_WITH_KNOTS('',3,(#424722,#424723,#424724,#424725,
#424726,#424727,#424728,#424729,#424730,#424731,#424732,#424733,#424734,
#424735,#424736,#424737,#424738,#424739,#424740,#424741,#424742,#424743,
#424744,#424745,#424746,#424747,#424748,#424749),.UNSPECIFIED.,.F.,.F.,
(4,3,3,3,3,3,3,3,3,4),(0.,8.66039628583738E-6,1.6470771520067E-5,2.2450289413233E-5,
2.49975961757828E-5,2.88526003690285E-5,3.10661348995021E-5,3.43053543516966E-5,
3.66410545653567E-5,4.00504537627891E-5),.UNSPECIFIED.);
#26217=B_SPLINE_CURVE_WITH_KNOTS('',3,(#424752,#424753,#424754,#424755,
#424756,#424757,#424758),.UNSPECIFIED.,.F.,.F.,(4,3,4),(0.,4.40000041065374E-5,
9.89910850773109E-5),.UNSPECIFIED.);
#26218=B_SPLINE_CURVE_WITH_KNOTS('',3,(#424779,#424780,#424781,#424782,
#424783,#424784,#424785,#424786,#424787,#424788,#424789,#424790,#424791,
#424792,#424793,#424794,#424795,#424796,#424797,#424798,#424799,#424800,
#424801,#424802,#424803,#424804,#424805,#424806,#424807,#424808,#424809,
#424810,#424811,#424812),.UNSPECIFIED.,.F.,.F.,(4,3,3,3,3,3,3,3,3,3,3,4),
(0.,4.29157837302829E-6,5.42772623795352E-6,1.0090169848235E-5,1.31279195068643E-5,
1.57383542265904E-5,1.61011507492108E-5,1.67166789291759E-5,1.9534326281136E-5,
2.29377234674649E-5,2.71556047620058E-5,3.34407099942657E-5),
 .UNSPECIFIED.);
#26219=B_SPLINE_CURVE_WITH_KNOTS('',3,(#424825,#424826,#424827,#424828,
#424829,#424830,#424831,#424832,#424833,#424834,#424835,#424836,#424837,
#424838,#424839,#424840,#424841,#424842,#424843,#424844,#424845,#424846,
#424847,#424848,#424849,#424850,#424851,#424852,#424853,#424854,#424855,
#424856,#424857,#424858),.UNSPECIFIED.,.F.,.F.,(4,3,3,3,3,3,3,3,3,3,3,4),
(2.16840434497101E-19,3.71309426656633E-6,5.39981071559424E-6,8.78933289369172E-6,
9.00272357067502E-6,1.07143984504147E-5,1.6078029967956E-5,1.65806081157685E-5,
2.30369726850514E-5,2.67819200416083E-5,3.59736924187967E-5,4.03862783806995E-5),
 .UNSPECIFIED.);
#26220=B_SPLINE_CURVE_WITH_KNOTS('',3,(#424971,#424972,#424973,#424974),
 .UNSPECIFIED.,.F.,.F.,(4,4),(0.,7.70025630629238E-5),.UNSPECIFIED.);
#26221=B_SPLINE_CURVE_WITH_KNOTS('',3,(#424984,#424985,#424986,#424987),
 .UNSPECIFIED.,.F.,.F.,(4,4),(4.33680868994202E-19,7.70025630629236E-5),
 .UNSPECIFIED.);
#26222=B_SPLINE_CURVE_WITH_KNOTS('',3,(#424991,#424992,#424993,#424994,
#424995,#424996,#424997,#424998,#424999,#425000,#425001,#425002,#425003,
#425004,#425005,#425006,#425007,#425008,#425009,#425010,#425011,#425012,
#425013,#425014,#425015,#425016,#425017,#425018,#425019,#425020,#425021,
#425022,#425023,#425024,#425025,#425026,#425027),.UNSPECIFIED.,.F.,.F.,
(4,3,3,3,3,3,3,3,3,3,3,3,4),(0.,9.59031527196868E-6,1.94769411222495E-5,
2.02405092183152E-5,3.21374138577699E-5,3.60302195070441E-5,4.42640648818247E-5,
4.53660204229442E-5,5.03633762302055E-5,5.17708036292895E-5,5.37928993851988E-5,
5.54103755460197E-5,5.64557889510261E-5),.UNSPECIFIED.);
#26223=B_SPLINE_CURVE_WITH_KNOTS('',3,(#425028,#425029,#425030,#425031,
#425032,#425033,#425034,#425035,#425036,#425037,#425038,#425039,#425040,
#425041,#425042,#425043,#425044,#425045,#425046,#425047,#425048,#425049,
#425050,#425051,#425052,#425053,#425054,#425055),.UNSPECIFIED.,.F.,.F.,
(4,3,3,3,3,3,3,3,3,4),(5.64557889510261E-5,5.98940966493748E-5,6.34214003873378E-5,
7.22241476084834E-5,7.38322796533361E-5,8.36529189331444E-5,8.80714278222496E-5,
9.84837568500701E-5,0.000108624704079139,0.000110823272382853),
 .UNSPECIFIED.);
#26224=B_SPLINE_CURVE_WITH_KNOTS('',3,(#425071,#425072,#425073,#425074,
#425075,#425076,#425077,#425078,#425079,#425080,#425081,#425082,#425083,
#425084,#425085,#425086,#425087,#425088,#425089,#425090,#425091,#425092,
#425093,#425094,#425095,#425096,#425097,#425098),.UNSPECIFIED.,.F.,.F.,
(4,3,3,3,3,3,3,3,3,4),(0.,8.66039628582221E-6,1.64707715200666E-5,2.24502894132205E-5,
2.49975961757824E-5,2.88526003690279E-5,3.10661348995017E-5,3.43053543516962E-5,
3.66410545653564E-5,4.00504537627889E-5),.UNSPECIFIED.);
#26225=B_SPLINE_CURVE_WITH_KNOTS('',3,(#425101,#425102,#425103,#425104,
#425105,#425106,#425107),.UNSPECIFIED.,.F.,.F.,(4,3,4),(0.,4.40000041065378E-5,
9.89910850773116E-5),.UNSPECIFIED.);
#26226=B_SPLINE_CURVE_WITH_KNOTS('',3,(#425128,#425129,#425130,#425131,
#425132,#425133,#425134,#425135,#425136,#425137,#425138,#425139,#425140,
#425141,#425142,#425143,#425144,#425145,#425146,#425147,#425148,#425149,
#425150,#425151,#425152,#425153,#425154,#425155,#425156,#425157,#425158,
#425159,#425160,#425161),.UNSPECIFIED.,.F.,.F.,(4,3,3,3,3,3,3,3,3,3,3,4),
(0.,4.29157837302005E-6,5.42772623795335E-6,1.00901698482347E-5,1.31279195068638E-5,
1.57383542265804E-5,1.61011507492102E-5,1.67166789291744E-5,1.95343262811357E-5,
2.29377234674647E-5,2.71556047620055E-5,3.34407099942655E-5),
 .UNSPECIFIED.);
#26227=B_SPLINE_CURVE_WITH_KNOTS('',3,(#425174,#425175,#425176,#425177,
#425178,#425179,#425180,#425181,#425182,#425183,#425184,#425185,#425186,
#425187,#425188,#425189,#425190,#425191,#425192,#425193,#425194,#425195,
#425196,#425197,#425198,#425199,#425200,#425201,#425202,#425203,#425204,
#425205,#425206,#425207),.UNSPECIFIED.,.F.,.F.,(4,3,3,3,3,3,3,3,3,3,3,4),
(0.,3.7130942665666E-6,5.39981071559435E-6,8.78933289368458E-6,9.0027235706753E-6,
1.0714398450415E-5,1.60780299679457E-5,1.65806081157687E-5,2.30369726850392E-5,
2.67819200416082E-5,3.59736924188217E-5,4.03862783806992E-5),
 .UNSPECIFIED.);
#26228=B_SPLINE_CURVE_WITH_KNOTS('',3,(#425320,#425321,#425322,#425323),
 .UNSPECIFIED.,.F.,.F.,(4,4),(0.,7.70025630629239E-5),.UNSPECIFIED.);
#26229=B_SPLINE_CURVE_WITH_KNOTS('',3,(#425333,#425334,#425335,#425336),
 .UNSPECIFIED.,.F.,.F.,(4,4),(4.33680868994202E-19,7.70025630629233E-5),
 .UNSPECIFIED.);
#26230=B_SPLINE_CURVE_WITH_KNOTS('',3,(#425340,#425341,#425342,#425343,
#425344,#425345,#425346,#425347,#425348,#425349,#425350,#425351,#425352,
#425353,#425354,#425355,#425356,#425357,#425358,#425359,#425360,#425361,
#425362,#425363,#425364,#425365,#425366,#425367,#425368,#425369,#425370,
#425371,#425372,#425373,#425374,#425375,#425376),.UNSPECIFIED.,.F.,.F.,
(4,3,3,3,3,3,3,3,3,3,3,3,4),(0.,9.59031527199996E-6,1.94769411222853E-5,
2.02405092183151E-5,3.2137413857757E-5,3.60302195070436E-5,4.42640648819028E-5,
4.53660204229443E-5,5.03633762301884E-5,5.17708036292894E-5,5.37928993851986E-5,
5.54103755460202E-5,5.64557889513433E-5),.UNSPECIFIED.);
#26231=B_SPLINE_CURVE_WITH_KNOTS('',3,(#425377,#425378,#425379,#425380,
#425381,#425382,#425383,#425384,#425385,#425386,#425387,#425388,#425389,
#425390,#425391,#425392,#425393,#425394,#425395,#425396,#425397,#425398,
#425399,#425400,#425401,#425402,#425403,#425404),.UNSPECIFIED.,.F.,.F.,
(4,3,3,3,3,3,3,3,3,4),(5.64557889513433E-5,5.9894096649375E-5,6.3421400387338E-5,
7.22241476084518E-5,7.38322796533362E-5,8.3652918933141E-5,8.80714278222498E-5,
9.84837568500725E-5,0.000108624704079137,0.000110823272382853),
 .UNSPECIFIED.);
#26232=B_SPLINE_CURVE_WITH_KNOTS('',3,(#425420,#425421,#425422,#425423,
#425424,#425425,#425426,#425427,#425428,#425429,#425430,#425431,#425432,
#425433,#425434,#425435,#425436,#425437,#425438,#425439,#425440,#425441,
#425442,#425443,#425444,#425445,#425446,#425447),.UNSPECIFIED.,.F.,.F.,
(4,3,3,3,3,3,3,3,3,4),(0.,8.66039628581385E-6,1.64707715200667E-5,2.2450289413247E-5,
2.49975961757824E-5,2.88526003690282E-5,3.10661348995018E-5,3.43053543516961E-5,
3.66410545653561E-5,4.00504537627887E-5),.UNSPECIFIED.);
#26233=B_SPLINE_CURVE_WITH_KNOTS('',3,(#425450,#425451,#425452,#425453,
#425454,#425455,#425456),.UNSPECIFIED.,.F.,.F.,(4,3,4),(0.,4.40000041065375E-5,
9.89910850773115E-5),.UNSPECIFIED.);
#26234=B_SPLINE_CURVE_WITH_KNOTS('',3,(#425477,#425478,#425479,#425480,
#425481,#425482,#425483,#425484,#425485,#425486,#425487,#425488,#425489,
#425490,#425491,#425492,#425493,#425494,#425495,#425496,#425497,#425498,
#425499,#425500,#425501,#425502,#425503,#425504,#425505,#425506,#425507,
#425508,#425509,#425510),.UNSPECIFIED.,.F.,.F.,(4,3,3,3,3,3,3,3,3,3,3,4),
(0.,4.29157837304995E-6,5.42772623795321E-6,1.00901698482345E-5,1.31279195068636E-5,
1.57383542265953E-5,1.61011507492102E-5,1.67166789291755E-5,1.95343262811355E-5,
2.29377234674644E-5,2.71556047620056E-5,3.34407099942655E-5),
 .UNSPECIFIED.);
#26235=B_SPLINE_CURVE_WITH_KNOTS('',3,(#425523,#425524,#425525,#425526,
#425527,#425528,#425529,#425530,#425531,#425532,#425533,#425534,#425535,
#425536,#425537,#425538,#425539,#425540,#425541,#425542,#425543,#425544,
#425545,#425546,#425547,#425548,#425549,#425550,#425551,#425552,#425553,
#425554,#425555,#425556),.UNSPECIFIED.,.F.,.F.,(4,3,3,3,3,3,3,3,3,3,3,4),
(0.,3.71309426656671E-6,5.39981071559432E-6,8.78933289371078E-6,9.00272357067543E-6,
1.07143984504152E-5,1.60780299679494E-5,1.65806081157689E-5,2.30369726850434E-5,
2.67819200416089E-5,3.59736924188055E-5,4.03862783807004E-5),
 .UNSPECIFIED.);
#26236=B_SPLINE_CURVE_WITH_KNOTS('',3,(#425669,#425670,#425671,#425672),
 .UNSPECIFIED.,.F.,.F.,(4,4),(0.,7.7002563062924E-5),.UNSPECIFIED.);
#26237=B_SPLINE_CURVE_WITH_KNOTS('',3,(#425682,#425683,#425684,#425685),
 .UNSPECIFIED.,.F.,.F.,(4,4),(4.84869951806108E-19,7.70025630629238E-5),
 .UNSPECIFIED.);
#26238=B_SPLINE_CURVE_WITH_KNOTS('',3,(#425689,#425690,#425691,#425692,
#425693,#425694,#425695,#425696,#425697,#425698,#425699,#425700,#425701,
#425702,#425703,#425704,#425705,#425706,#425707,#425708,#425709,#425710,
#425711,#425712,#425713,#425714,#425715,#425716,#425717,#425718,#425719,
#425720,#425721,#425722,#425723,#425724,#425725),.UNSPECIFIED.,.F.,.F.,
(4,3,3,3,3,3,3,3,3,3,3,3,4),(0.,9.59031527201029E-6,1.94769411223069E-5,
2.0240509218315E-5,3.21374138577701E-5,3.60302195070435E-5,4.42640648818496E-5,
4.53660204229439E-5,5.03633762302282E-5,5.17708036292892E-5,5.37928993851987E-5,
5.54103755460199E-5,5.64557889512175E-5),.UNSPECIFIED.);
#26239=B_SPLINE_CURVE_WITH_KNOTS('',3,(#425726,#425727,#425728,#425729,
#425730,#425731,#425732,#425733,#425734,#425735,#425736,#425737,#425738,
#425739,#425740,#425741,#425742,#425743,#425744,#425745,#425746,#425747,
#425748,#425749,#425750,#425751,#425752,#425753),.UNSPECIFIED.,.F.,.F.,
(4,3,3,3,3,3,3,3,3,4),(5.64557889512175E-5,5.98940966493747E-5,6.34214003873375E-5,
7.22241476083973E-5,7.38322796533362E-5,8.36529189331593E-5,8.80714278222496E-5,
9.84837568501165E-5,0.000108624704079233,0.000110823272382853),
 .UNSPECIFIED.);
#26240=B_SPLINE_CURVE_WITH_KNOTS('',3,(#425769,#425770,#425771,#425772,
#425773,#425774,#425775,#425776,#425777,#425778,#425779,#425780,#425781,
#425782,#425783,#425784,#425785,#425786,#425787,#425788,#425789,#425790,
#425791,#425792,#425793,#425794,#425795,#425796),.UNSPECIFIED.,.F.,.F.,
(4,3,3,3,3,3,3,3,3,4),(0.,8.66039628584176E-6,1.64707715200667E-5,2.24502894132358E-5,
2.49975961757823E-5,2.88526003690282E-5,3.10661348995017E-5,3.4305354351696E-5,
3.6641054565356E-5,4.00504537627888E-5),.UNSPECIFIED.);
#26241=B_SPLINE_CURVE_WITH_KNOTS('',3,(#425799,#425800,#425801,#425802,
#425803,#425804,#425805),.UNSPECIFIED.,.F.,.F.,(4,3,4),(0.,4.40000041065377E-5,
9.89910850773114E-5),.UNSPECIFIED.);
#26242=B_SPLINE_CURVE_WITH_KNOTS('',3,(#425826,#425827,#425828,#425829,
#425830,#425831,#425832,#425833,#425834,#425835,#425836,#425837,#425838,
#425839,#425840,#425841,#425842,#425843,#425844,#425845,#425846,#425847,
#425848,#425849,#425850,#425851,#425852,#425853,#425854,#425855,#425856,
#425857,#425858,#425859),.UNSPECIFIED.,.F.,.F.,(4,3,3,3,3,3,3,3,3,3,3,4),
(0.,4.29157837302334E-6,5.42772623795342E-6,1.00901698482347E-5,1.3127919506864E-5,
1.57383542265795E-5,1.61011507492107E-5,1.67166789291751E-5,1.95343262811362E-5,
2.29377234674651E-5,2.71556047620059E-5,3.34407099942661E-5),
 .UNSPECIFIED.);
#26243=B_SPLINE_CURVE_WITH_KNOTS('',3,(#425872,#425873,#425874,#425875,
#425876,#425877,#425878,#425879,#425880,#425881,#425882,#425883,#425884,
#425885,#425886,#425887,#425888,#425889,#425890,#425891,#425892,#425893,
#425894,#425895,#425896,#425897,#425898,#425899,#425900,#425901,#425902,
#425903,#425904,#425905),.UNSPECIFIED.,.F.,.F.,(4,3,3,3,3,3,3,3,3,3,3,4),
(0.,3.7130942665666E-6,5.39981071559416E-6,8.78933289328906E-6,9.0027235706754E-6,
1.07143984504151E-5,1.60780299679608E-5,1.65806081157689E-5,2.30369726850439E-5,
2.67819200416086E-5,3.59736924187639E-5,4.03862783807002E-5),
 .UNSPECIFIED.);
#26244=B_SPLINE_CURVE_WITH_KNOTS('',3,(#426018,#426019,#426020,#426021),
 .UNSPECIFIED.,.F.,.F.,(4,4),(0.,7.70025630629238E-5),.UNSPECIFIED.);
#26245=B_SPLINE_CURVE_WITH_KNOTS('',3,(#426031,#426032,#426033,#426034),
 .UNSPECIFIED.,.F.,.F.,(4,4),(0.,7.70025630629238E-5),.UNSPECIFIED.);
#26246=B_SPLINE_CURVE_WITH_KNOTS('',3,(#426038,#426039,#426040,#426041,
#426042,#426043,#426044,#426045,#426046,#426047,#426048,#426049,#426050,
#426051,#426052,#426053,#426054,#426055,#426056,#426057,#426058,#426059,
#426060,#426061,#426062,#426063,#426064,#426065,#426066,#426067,#426068,
#426069,#426070,#426071,#426072,#426073,#426074),.UNSPECIFIED.,.F.,.F.,
(4,3,3,3,3,3,3,3,3,3,3,3,4),(0.,9.5903152720036E-6,1.94769411222964E-5,
2.02405092183154E-5,3.21374138577761E-5,3.60302195070438E-5,4.4264064881776E-5,
4.53660204229443E-5,5.03633762302123E-5,5.17708036292897E-5,5.37928993851989E-5,
5.54103755460199E-5,5.64557889509958E-5),.UNSPECIFIED.);
#26247=B_SPLINE_CURVE_WITH_KNOTS('',3,(#426075,#426076,#426077,#426078,
#426079,#426080,#426081,#426082,#426083,#426084,#426085,#426086,#426087,
#426088,#426089,#426090,#426091,#426092,#426093,#426094,#426095,#426096,
#426097,#426098,#426099,#426100,#426101,#426102),.UNSPECIFIED.,.F.,.F.,
(4,3,3,3,3,3,3,3,3,4),(5.64557889509958E-5,5.98940966493749E-5,6.3421400387338E-5,
7.22241476085281E-5,7.38322796533361E-5,8.3652918933147E-5,8.80714278222493E-5,
9.84837568501112E-5,0.000108624704079221,0.000110823272382852),
 .UNSPECIFIED.);
#26248=B_SPLINE_CURVE_WITH_KNOTS('',3,(#426118,#426119,#426120,#426121,
#426122,#426123,#426124,#426125,#426126,#426127,#426128,#426129,#426130,
#426131,#426132,#426133,#426134,#426135,#426136,#426137,#426138,#426139,
#426140,#426141,#426142,#426143,#426144,#426145),.UNSPECIFIED.,.F.,.F.,
(4,3,3,3,3,3,3,3,3,4),(0.,8.66039628579918E-6,1.64707715200669E-5,2.2450289413237E-5,
2.49975961757828E-5,2.88526003690285E-5,3.10661348995021E-5,3.43053543516965E-5,
3.66410545653566E-5,4.00504537627887E-5),.UNSPECIFIED.);
#26249=B_SPLINE_CURVE_WITH_KNOTS('',3,(#426148,#426149,#426150,#426151,
#426152,#426153,#426154),.UNSPECIFIED.,.F.,.F.,(4,3,4),(0.,4.40000041065375E-5,
9.8991085077311E-5),.UNSPECIFIED.);
#26250=B_SPLINE_CURVE_WITH_KNOTS('',3,(#426175,#426176,#426177,#426178,
#426179,#426180,#426181,#426182,#426183,#426184,#426185,#426186,#426187,
#426188,#426189,#426190,#426191,#426192,#426193,#426194,#426195,#426196,
#426197,#426198,#426199,#426200,#426201,#426202,#426203,#426204,#426205,
#426206,#426207,#426208),.UNSPECIFIED.,.F.,.F.,(4,3,3,3,3,3,3,3,3,3,3,4),
(0.,4.29157837302442E-6,5.42772623795322E-6,1.00901698482346E-5,1.31279195068638E-5,
1.57383542265859E-5,1.61011507492107E-5,1.67166789291753E-5,1.9534326281136E-5,
2.29377234674649E-5,2.71556047620057E-5,3.34407099942659E-5),
 .UNSPECIFIED.);
#26251=B_SPLINE_CURVE_WITH_KNOTS('',3,(#426221,#426222,#426223,#426224,
#426225,#426226,#426227,#426228,#426229,#426230,#426231,#426232,#426233,
#426234,#426235,#426236,#426237,#426238,#426239,#426240,#426241,#426242,
#426243,#426244,#426245,#426246,#426247,#426248,#426249,#426250,#426251,
#426252,#426253,#426254),.UNSPECIFIED.,.F.,.F.,(4,3,3,3,3,3,3,3,3,3,3,4),
(0.,3.71309426656662E-6,5.39981071559435E-6,8.78933289332053E-6,9.00272357067553E-6,
1.07143984504153E-5,1.60780299679585E-5,1.6580608115769E-5,2.30369726850372E-5,
2.67819200416089E-5,3.59736924188161E-5,4.03862783807003E-5),
 .UNSPECIFIED.);
#26252=B_SPLINE_CURVE_WITH_KNOTS('',3,(#426367,#426368,#426369,#426370),
 .UNSPECIFIED.,.F.,.F.,(4,4),(0.,7.70025630629237E-5),.UNSPECIFIED.);
#26253=B_SPLINE_CURVE_WITH_KNOTS('',3,(#426380,#426381,#426382,#426383),
 .UNSPECIFIED.,.F.,.F.,(4,4),(0.,7.70025630629238E-5),.UNSPECIFIED.);
#26254=B_SPLINE_CURVE_WITH_KNOTS('',3,(#426387,#426388,#426389,#426390,
#426391,#426392,#426393,#426394,#426395,#426396,#426397,#426398,#426399,
#426400,#426401,#426402,#426403,#426404,#426405,#426406,#426407,#426408,
#426409,#426410,#426411,#426412,#426413,#426414,#426415,#426416,#426417,
#426418,#426419,#426420,#426421,#426422,#426423),.UNSPECIFIED.,.F.,.F.,
(4,3,3,3,3,3,3,3,3,3,3,3,4),(0.,9.59031527200642E-6,1.94769411222944E-5,
2.02405092183152E-5,3.21374138577678E-5,3.6030219507044E-5,4.42640648819271E-5,
4.53660204229444E-5,5.03633762302186E-5,5.17708036292897E-5,5.37928993851991E-5,
5.54103755460196E-5,5.64557889512567E-5),.UNSPECIFIED.);
#26255=B_SPLINE_CURVE_WITH_KNOTS('',3,(#426424,#426425,#426426,#426427,
#426428,#426429,#426430,#426431,#426432,#426433,#426434,#426435,#426436,
#426437,#426438,#426439,#426440,#426441,#426442,#426443,#426444,#426445,
#426446,#426447,#426448,#426449,#426450,#426451),.UNSPECIFIED.,.F.,.F.,
(4,3,3,3,3,3,3,3,3,4),(5.64557889512567E-5,5.9894096649375E-5,6.34214003873379E-5,
7.22241476083888E-5,7.38322796533364E-5,8.36529189331357E-5,8.807142782225E-5,
9.84837568500544E-5,0.000108624704079104,0.000110823272382853),
 .UNSPECIFIED.);
#26256=B_SPLINE_CURVE_WITH_KNOTS('',3,(#426467,#426468,#426469,#426470,
#426471,#426472,#426473,#426474,#426475,#426476,#426477,#426478,#426479,
#426480,#426481,#426482,#426483,#426484,#426485,#426486,#426487,#426488,
#426489,#426490,#426491,#426492,#426493,#426494),.UNSPECIFIED.,.F.,.F.,
(4,3,3,3,3,3,3,3,3,4),(0.,8.66039628580946E-6,1.64707715200666E-5,2.24502894132521E-5,
2.49975961757823E-5,2.88526003690281E-5,3.10661348995017E-5,3.43053543516962E-5,
3.66410545653556E-5,4.00504537627888E-5),.UNSPECIFIED.);
#26257=B_SPLINE_CURVE_WITH_KNOTS('',3,(#426497,#426498,#426499,#426500,
#426501,#426502,#426503),.UNSPECIFIED.,.F.,.F.,(4,3,4),(0.,4.40000041065375E-5,
9.89910850773113E-5),.UNSPECIFIED.);
#26258=B_SPLINE_CURVE_WITH_KNOTS('',3,(#426524,#426525,#426526,#426527,
#426528,#426529,#426530,#426531,#426532,#426533,#426534,#426535,#426536,
#426537,#426538,#426539,#426540,#426541,#426542,#426543,#426544,#426545,
#426546,#426547,#426548,#426549,#426550,#426551,#426552,#426553,#426554,
#426555,#426556,#426557),.UNSPECIFIED.,.F.,.F.,(4,3,3,3,3,3,3,3,3,3,3,4),
(0.,4.29157837303971E-6,5.4277262379535E-6,1.00901698482348E-5,1.3127919506864E-5,
1.57383542265878E-5,1.61011507492106E-5,1.67166789291757E-5,1.9534326281136E-5,
2.29377234674647E-5,2.71556047620058E-5,3.34407099942659E-5),
 .UNSPECIFIED.);
#26259=B_SPLINE_CURVE_WITH_KNOTS('',3,(#426570,#426571,#426572,#426573,
#426574,#426575,#426576,#426577,#426578,#426579,#426580,#426581,#426582,
#426583,#426584,#426585,#426586,#426587,#426588,#426589,#426590,#426591,
#426592,#426593,#426594,#426595,#426596,#426597,#426598,#426599,#426600,
#426601,#426602,#426603),.UNSPECIFIED.,.F.,.F.,(4,3,3,3,3,3,3,3,3,3,3,4),
(6.1331736667335E-19,3.71309426656605E-6,5.399810715594E-6,8.78933289331522E-6,
9.00272357067485E-6,1.07143984504146E-5,1.60780299679516E-5,1.65806081157683E-5,
2.3036972685016E-5,2.6781920041608E-5,3.59736924187877E-5,4.03862783806992E-5),
 .UNSPECIFIED.);
#26260=B_SPLINE_CURVE_WITH_KNOTS('',3,(#426716,#426717,#426718,#426719),
 .UNSPECIFIED.,.F.,.F.,(4,4),(0.,7.70025630629241E-5),.UNSPECIFIED.);
#26261=B_SPLINE_CURVE_WITH_KNOTS('',3,(#426729,#426730,#426731,#426732),
 .UNSPECIFIED.,.F.,.F.,(4,4),(2.16840434497101E-19,7.70025630629238E-5),
 .UNSPECIFIED.);
#26262=B_SPLINE_CURVE_WITH_KNOTS('',3,(#426736,#426737,#426738,#426739,
#426740,#426741,#426742,#426743,#426744,#426745,#426746,#426747,#426748,
#426749,#426750,#426751,#426752,#426753,#426754,#426755,#426756,#426757,
#426758,#426759,#426760,#426761,#426762,#426763,#426764,#426765,#426766,
#426767,#426768,#426769,#426770,#426771,#426772),.UNSPECIFIED.,.F.,.F.,
(4,3,3,3,3,3,3,3,3,3,3,3,4),(0.,9.590315272008E-6,1.94769411222952E-5,2.02405092183151E-5,
3.21374138577707E-5,3.60302195070438E-5,4.42640648818693E-5,4.53660204229443E-5,
5.03633762301991E-5,5.17708036292894E-5,5.37928993851986E-5,5.54103755460196E-5,
5.64557889511543E-5),.UNSPECIFIED.);
#26263=B_SPLINE_CURVE_WITH_KNOTS('',3,(#426773,#426774,#426775,#426776,
#426777,#426778,#426779,#426780,#426781,#426782,#426783,#426784,#426785,
#426786,#426787,#426788,#426789,#426790,#426791,#426792,#426793,#426794,
#426795,#426796,#426797,#426798,#426799,#426800),.UNSPECIFIED.,.F.,.F.,
(4,3,3,3,3,3,3,3,3,4),(5.64557889511543E-5,5.98940966493751E-5,6.34214003873378E-5,
7.22241476084624E-5,7.3832279653336E-5,8.36529189331399E-5,8.80714278222494E-5,
9.8483756850071E-5,0.000108624704079142,0.000110823272382852),
 .UNSPECIFIED.);
#26264=B_SPLINE_CURVE_WITH_KNOTS('',3,(#426816,#426817,#426818,#426819,
#426820,#426821,#426822,#426823,#426824,#426825,#426826,#426827,#426828,
#426829,#426830,#426831,#426832,#426833,#426834,#426835,#426836,#426837,
#426838,#426839,#426840,#426841,#426842,#426843),.UNSPECIFIED.,.F.,.F.,
(4,3,3,3,3,3,3,3,3,4),(0.,8.66039628583704E-6,1.64707715200666E-5,2.24502894132115E-5,
2.49975961757823E-5,2.8852600369028E-5,3.10661348995016E-5,3.4305354351696E-5,
3.66410545653559E-5,4.00504537627888E-5),.UNSPECIFIED.);
#26265=B_SPLINE_CURVE_WITH_KNOTS('',3,(#426846,#426847,#426848,#426849,
#426850,#426851,#426852),.UNSPECIFIED.,.F.,.F.,(4,3,4),(0.,4.40000041065373E-5,
9.89910850773113E-5),.UNSPECIFIED.);
#26266=B_SPLINE_CURVE_WITH_KNOTS('',3,(#426873,#426874,#426875,#426876,
#426877,#426878,#426879,#426880,#426881,#426882,#426883,#426884,#426885,
#426886,#426887,#426888,#426889,#426890,#426891,#426892,#426893,#426894,
#426895,#426896,#426897,#426898,#426899,#426900,#426901,#426902,#426903,
#426904,#426905,#426906),.UNSPECIFIED.,.F.,.F.,(4,3,3,3,3,3,3,3,3,3,3,4),
(0.,4.29157837303212E-6,5.4277262379533E-6,1.00901698482348E-5,1.31279195068639E-5,
1.57383542265859E-5,1.61011507492106E-5,1.67166789291755E-5,1.95343262811357E-5,
2.2937723467465E-5,2.71556047620056E-5,3.34407099942654E-5),
 .UNSPECIFIED.);
#26267=B_SPLINE_CURVE_WITH_KNOTS('',3,(#426919,#426920,#426921,#426922,
#426923,#426924,#426925,#426926,#426927,#426928,#426929,#426930,#426931,
#426932,#426933,#426934,#426935,#426936,#426937,#426938,#426939,#426940,
#426941,#426942,#426943,#426944,#426945,#426946,#426947,#426948,#426949,
#426950,#426951,#426952),.UNSPECIFIED.,.F.,.F.,(4,3,3,3,3,3,3,3,3,3,3,4),
(0.,3.71309426656661E-6,5.39981071559432E-6,8.78933289364816E-6,9.00272357067536E-6,
1.07143984504151E-5,1.60780299679642E-5,1.65806081157689E-5,2.30369726850498E-5,
2.6781920041609E-5,3.59736924187643E-5,4.03862783807005E-5),
 .UNSPECIFIED.);
#26268=B_SPLINE_CURVE_WITH_KNOTS('',3,(#427065,#427066,#427067,#427068),
 .UNSPECIFIED.,.F.,.F.,(4,4),(0.,7.70025630629238E-5),.UNSPECIFIED.);
#26269=B_SPLINE_CURVE_WITH_KNOTS('',3,(#427078,#427079,#427080,#427081),
 .UNSPECIFIED.,.F.,.F.,(4,4),(4.63171371119878E-19,7.70025630629236E-5),
 .UNSPECIFIED.);
#26270=B_SPLINE_CURVE_WITH_KNOTS('',3,(#427085,#427086,#427087,#427088,
#427089,#427090,#427091,#427092,#427093,#427094,#427095,#427096,#427097,
#427098,#427099,#427100,#427101,#427102,#427103,#427104,#427105,#427106,
#427107,#427108,#427109,#427110,#427111,#427112,#427113,#427114,#427115,
#427116,#427117,#427118,#427119,#427120,#427121),.UNSPECIFIED.,.F.,.F.,
(4,3,3,3,3,3,3,3,3,3,3,3,4),(0.,9.59031527200658E-6,1.94769411222967E-5,
2.02405092183153E-5,3.21374138577672E-5,3.60302195070438E-5,4.42640648818944E-5,
4.53660204229444E-5,5.03633762302181E-5,5.17708036292896E-5,5.37928993851989E-5,
5.54103755460198E-5,5.64557889511992E-5),.UNSPECIFIED.);
#26271=B_SPLINE_CURVE_WITH_KNOTS('',3,(#427122,#427123,#427124,#427125,
#427126,#427127,#427128,#427129,#427130,#427131,#427132,#427133,#427134,
#427135,#427136,#427137,#427138,#427139,#427140,#427141,#427142,#427143,
#427144,#427145,#427146,#427147,#427148,#427149),.UNSPECIFIED.,.F.,.F.,
(4,3,3,3,3,3,3,3,3,4),(5.64557889511992E-5,5.98940966493751E-5,6.34214003873379E-5,
7.22241476084401E-5,7.38322796533362E-5,8.36529189331593E-5,8.80714278222498E-5,
9.8483756850112E-5,0.000108624704079221,0.000110823272382853),
 .UNSPECIFIED.);
#26272=B_SPLINE_CURVE_WITH_KNOTS('',3,(#427165,#427166,#427167,#427168,
#427169,#427170,#427171,#427172,#427173,#427174,#427175,#427176,#427177,
#427178,#427179,#427180,#427181,#427182,#427183,#427184,#427185,#427186,
#427187,#427188,#427189,#427190,#427191,#427192),.UNSPECIFIED.,.F.,.F.,
(4,3,3,3,3,3,3,3,3,4),(0.,8.66039628577747E-6,1.64707715200665E-5,2.24502894132765E-5,
2.49975961757823E-5,2.88526003690281E-5,3.10661348995017E-5,3.43053543516961E-5,
3.66410545653561E-5,4.00504537627891E-5),.UNSPECIFIED.);
#26273=B_SPLINE_CURVE_WITH_KNOTS('',3,(#427195,#427196,#427197,#427198,
#427199,#427200,#427201),.UNSPECIFIED.,.F.,.F.,(4,3,4),(0.,4.40000041065372E-5,
9.89910850773113E-5),.UNSPECIFIED.);
#26274=B_SPLINE_CURVE_WITH_KNOTS('',3,(#427222,#427223,#427224,#427225,
#427226,#427227,#427228,#427229,#427230,#427231,#427232,#427233,#427234,
#427235,#427236,#427237,#427238,#427239,#427240,#427241,#427242,#427243,
#427244,#427245,#427246,#427247,#427248,#427249,#427250,#427251,#427252,
#427253,#427254,#427255),.UNSPECIFIED.,.F.,.F.,(4,3,3,3,3,3,3,3,3,3,3,4),
(0.,4.29157837302174E-6,5.42772623795324E-6,1.00901698482348E-5,1.31279195068638E-5,
1.57383542265879E-5,1.61011507492104E-5,1.67166789291754E-5,1.95343262811358E-5,
2.2937723467465E-5,2.71556047620057E-5,3.34407099942658E-5),
 .UNSPECIFIED.);
#26275=B_SPLINE_CURVE_WITH_KNOTS('',3,(#427268,#427269,#427270,#427271,
#427272,#427273,#427274,#427275,#427276,#427277,#427278,#427279,#427280,
#427281,#427282,#427283,#427284,#427285,#427286,#427287,#427288,#427289,
#427290,#427291,#427292,#427293,#427294,#427295,#427296,#427297,#427298,
#427299,#427300,#427301),.UNSPECIFIED.,.F.,.F.,(4,3,3,3,3,3,3,3,3,3,3,4),
(5.42101086242752E-20,3.71309426656656E-6,5.39981071559424E-6,8.78933289329387E-6,
9.00272357067524E-6,1.0714398450415E-5,1.60780299679569E-5,1.65806081157688E-5,
2.30369726850531E-5,2.67819200416085E-5,3.59736924187559E-5,4.03862783807002E-5),
 .UNSPECIFIED.);
#26276=B_SPLINE_CURVE_WITH_KNOTS('',3,(#427414,#427415,#427416,#427417),
 .UNSPECIFIED.,.F.,.F.,(4,4),(0.,7.70025630629241E-5),.UNSPECIFIED.);
#26277=B_SPLINE_CURVE_WITH_KNOTS('',3,(#427427,#427428,#427429,#427430),
 .UNSPECIFIED.,.F.,.F.,(4,4),(1.0842021724855E-19,7.70025630629236E-5),
 .UNSPECIFIED.);
#26278=B_SPLINE_CURVE_WITH_KNOTS('',3,(#427434,#427435,#427436,#427437,
#427438,#427439,#427440,#427441,#427442,#427443,#427444,#427445,#427446,
#427447,#427448,#427449,#427450,#427451,#427452,#427453,#427454,#427455,
#427456,#427457,#427458,#427459,#427460,#427461,#427462,#427463,#427464,
#427465,#427466,#427467,#427468,#427469,#427470),.UNSPECIFIED.,.F.,.F.,
(4,3,3,3,3,3,3,3,3,3,3,3,4),(0.,9.59031527199611E-6,1.9476941122284E-5,
2.02405092183151E-5,3.21374138577688E-5,3.60302195070439E-5,4.42640648818978E-5,
4.53660204229444E-5,5.03633762302136E-5,5.17708036292894E-5,5.37928993851988E-5,
5.54103755460199E-5,5.64557889511083E-5),.UNSPECIFIED.);
#26279=B_SPLINE_CURVE_WITH_KNOTS('',3,(#427471,#427472,#427473,#427474,
#427475,#427476,#427477,#427478,#427479,#427480,#427481,#427482,#427483,
#427484,#427485,#427486,#427487,#427488,#427489,#427490,#427491,#427492,
#427493,#427494,#427495,#427496,#427497,#427498),.UNSPECIFIED.,.F.,.F.,
(4,3,3,3,3,3,3,3,3,4),(5.64557889511083E-5,5.98940966493748E-5,6.34214003873378E-5,
7.22241476084839E-5,7.38322796533364E-5,8.36529189331476E-5,8.80714278222498E-5,
9.84837568500776E-5,0.000108624704079139,0.000110823272382853),
 .UNSPECIFIED.);
#26280=B_SPLINE_CURVE_WITH_KNOTS('',3,(#427514,#427515,#427516,#427517,
#427518,#427519,#427520,#427521,#427522,#427523,#427524,#427525,#427526,
#427527,#427528,#427529,#427530,#427531,#427532,#427533,#427534,#427535,
#427536,#427537,#427538,#427539,#427540,#427541),.UNSPECIFIED.,.F.,.F.,
(4,3,3,3,3,3,3,3,3,4),(0.,8.66039628580465E-6,1.64707715200667E-5,2.24502894132612E-5,
2.49975961757825E-5,2.88526003690282E-5,3.10661348995018E-5,3.43053543516961E-5,
3.66410545653559E-5,4.00504537627886E-5),.UNSPECIFIED.);
#26281=B_SPLINE_CURVE_WITH_KNOTS('',3,(#427544,#427545,#427546,#427547,
#427548,#427549,#427550),.UNSPECIFIED.,.F.,.F.,(4,3,4),(0.,4.40000041065375E-5,
9.89910850773114E-5),.UNSPECIFIED.);
#26282=B_SPLINE_CURVE_WITH_KNOTS('',3,(#427571,#427572,#427573,#427574,
#427575,#427576,#427577,#427578,#427579,#427580,#427581,#427582,#427583,
#427584,#427585,#427586,#427587,#427588,#427589,#427590,#427591,#427592,
#427593,#427594,#427595,#427596,#427597,#427598,#427599,#427600,#427601,
#427602,#427603,#427604),.UNSPECIFIED.,.F.,.F.,(4,3,3,3,3,3,3,3,3,3,3,4),
(0.,4.29157837304268E-6,5.42772623795342E-6,1.00901698482348E-5,1.31279195068639E-5,
1.57383542265942E-5,1.61011507492105E-5,1.67166789291756E-5,1.95343262811359E-5,
2.29377234674649E-5,2.71556047620056E-5,3.3440709994266E-5),
 .UNSPECIFIED.);
#26283=B_SPLINE_CURVE_WITH_KNOTS('',3,(#427617,#427618,#427619,#427620,
#427621,#427622,#427623,#427624,#427625,#427626,#427627,#427628,#427629,
#427630,#427631,#427632,#427633,#427634,#427635,#427636,#427637,#427638,
#427639,#427640,#427641,#427642,#427643,#427644,#427645,#427646,#427647,
#427648,#427649,#427650),.UNSPECIFIED.,.F.,.F.,(4,3,3,3,3,3,3,3,3,3,3,4),
(1.0842021724855E-19,3.71309426656654E-6,5.39981071559418E-6,8.7893328933137E-6,
9.00272357067519E-6,1.0714398450415E-5,1.6078029967963E-5,1.65806081157686E-5,
2.30369726850455E-5,2.67819200416086E-5,3.59736924187525E-5,4.03862783806999E-5),
 .UNSPECIFIED.);
#26284=B_SPLINE_CURVE_WITH_KNOTS('',3,(#427763,#427764,#427765,#427766),
 .UNSPECIFIED.,.F.,.F.,(4,4),(0.,7.70025630629241E-5),.UNSPECIFIED.);
#26285=B_SPLINE_CURVE_WITH_KNOTS('',3,(#427776,#427777,#427778,#427779),
 .UNSPECIFIED.,.F.,.F.,(4,4),(2.16840434497101E-19,7.70025630629238E-5),
 .UNSPECIFIED.);
#26286=B_SPLINE_CURVE_WITH_KNOTS('',3,(#427783,#427784,#427785,#427786,
#427787,#427788,#427789,#427790,#427791,#427792,#427793,#427794,#427795,
#427796,#427797,#427798,#427799,#427800,#427801,#427802,#427803,#427804,
#427805,#427806,#427807,#427808,#427809,#427810,#427811,#427812,#427813,
#427814,#427815,#427816,#427817,#427818,#427819),.UNSPECIFIED.,.F.,.F.,
(4,3,3,3,3,3,3,3,3,3,3,3,4),(0.,9.59031527200811E-6,1.94769411222919E-5,
2.0240509218315E-5,3.2137413857773E-5,3.60302195070438E-5,4.42640648818379E-5,
4.53660204229443E-5,5.03633762302087E-5,5.17708036292895E-5,5.37928993851988E-5,
5.54103755460197E-5,5.64557889512956E-5),.UNSPECIFIED.);
#26287=B_SPLINE_CURVE_WITH_KNOTS('',3,(#427820,#427821,#427822,#427823,
#427824,#427825,#427826,#427827,#427828,#427829,#427830,#427831,#427832,
#427833,#427834,#427835,#427836,#427837,#427838,#427839,#427840,#427841,
#427842,#427843,#427844,#427845,#427846,#427847),.UNSPECIFIED.,.F.,.F.,
(4,3,3,3,3,3,3,3,3,4),(5.64557889512956E-5,5.98940966493751E-5,6.34214003873378E-5,
7.22241476084982E-5,7.38322796533364E-5,8.36529189331437E-5,8.80714278222499E-5,
9.8483756850066E-5,0.000108624704079128,0.000110823272382853),
 .UNSPECIFIED.);
#26288=B_SPLINE_CURVE_WITH_KNOTS('',3,(#427863,#427864,#427865,#427866,
#427867,#427868,#427869,#427870,#427871,#427872,#427873,#427874,#427875,
#427876,#427877,#427878,#427879,#427880,#427881,#427882,#427883,#427884,
#427885,#427886,#427887,#427888,#427889,#427890),.UNSPECIFIED.,.F.,.F.,
(4,3,3,3,3,3,3,3,3,4),(0.,8.66039628578402E-6,1.64707715200666E-5,2.24502894132383E-5,
2.49975961757825E-5,2.8852600369028E-5,3.10661348995017E-5,3.43053543516961E-5,
3.66410545653559E-5,4.00504537627886E-5),.UNSPECIFIED.);
#26289=B_SPLINE_CURVE_WITH_KNOTS('',3,(#427893,#427894,#427895,#427896,
#427897,#427898,#427899),.UNSPECIFIED.,.F.,.F.,(4,3,4),(0.,4.40000041065375E-5,
9.89910850773112E-5),.UNSPECIFIED.);
#26290=B_SPLINE_CURVE_WITH_KNOTS('',3,(#427920,#427921,#427922,#427923,
#427924,#427925,#427926,#427927,#427928,#427929,#427930,#427931,#427932,
#427933,#427934,#427935,#427936,#427937,#427938,#427939,#427940,#427941,
#427942,#427943,#427944,#427945,#427946,#427947,#427948,#427949,#427950,
#427951,#427952,#427953),.UNSPECIFIED.,.F.,.F.,(4,3,3,3,3,3,3,3,3,3,3,4),
(0.,4.29157837303304E-6,5.42772623795324E-6,1.00901698482347E-5,1.31279195068638E-5,
1.57383542265858E-5,1.61011507492102E-5,1.67166789291752E-5,1.95343262811359E-5,
2.29377234674647E-5,2.71556047620056E-5,3.34407099942656E-5),
 .UNSPECIFIED.);
#26291=B_SPLINE_CURVE_WITH_KNOTS('',3,(#427966,#427967,#427968,#427969,
#427970,#427971,#427972,#427973,#427974,#427975,#427976,#427977,#427978,
#427979,#427980,#427981,#427982,#427983,#427984,#427985,#427986,#427987,
#427988,#427989,#427990,#427991,#427992,#427993,#427994,#427995,#427996,
#427997,#427998,#427999),.UNSPECIFIED.,.F.,.F.,(4,3,3,3,3,3,3,3,3,3,3,4),
(0.,3.71309426656663E-6,5.39981071559434E-6,8.78933289329627E-6,9.00272357067523E-6,
1.0714398450415E-5,1.6078029967947E-5,1.65806081157688E-5,2.30369726850588E-5,
2.67819200416087E-5,3.59736924187837E-5,4.03862783807003E-5),
 .UNSPECIFIED.);
#26292=B_SPLINE_CURVE_WITH_KNOTS('',3,(#428112,#428113,#428114,#428115),
 .UNSPECIFIED.,.F.,.F.,(4,4),(0.,7.70025630629237E-5),.UNSPECIFIED.);
#26293=B_SPLINE_CURVE_WITH_KNOTS('',3,(#428125,#428126,#428127,#428128),
 .UNSPECIFIED.,.F.,.F.,(4,4),(0.,7.70025630629239E-5),.UNSPECIFIED.);
#26294=B_SPLINE_CURVE_WITH_KNOTS('',3,(#428132,#428133,#428134,#428135,
#428136,#428137,#428138,#428139,#428140,#428141,#428142,#428143,#428144,
#428145,#428146,#428147,#428148,#428149,#428150,#428151,#428152,#428153,
#428154,#428155,#428156,#428157,#428158,#428159,#428160,#428161,#428162,
#428163,#428164,#428165,#428166,#428167,#428168),.UNSPECIFIED.,.F.,.F.,
(4,3,3,3,3,3,3,3,3,3,3,3,4),(0.,9.59031527200666E-6,1.94769411223038E-5,
2.02405092183152E-5,3.21374138577607E-5,3.60302195070441E-5,4.42640648818939E-5,
4.53660204229446E-5,5.03633762302108E-5,5.177080362929E-5,5.3792899385199E-5,
5.54103755460199E-5,5.6455788950677E-5),.UNSPECIFIED.);
#26295=B_SPLINE_CURVE_WITH_KNOTS('',3,(#428169,#428170,#428171,#428172,
#428173,#428174,#428175,#428176,#428177,#428178,#428179,#428180,#428181,
#428182,#428183,#428184,#428185,#428186,#428187,#428188,#428189,#428190,
#428191,#428192,#428193,#428194,#428195,#428196),.UNSPECIFIED.,.F.,.F.,
(4,3,3,3,3,3,3,3,3,4),(5.6455788950677E-5,5.98940966493752E-5,6.34214003873382E-5,
7.2224147608401E-5,7.38322796533364E-5,8.36529189331423E-5,8.807142782225E-5,
9.84837568500578E-5,0.000108624704079111,0.000110823272382853),
 .UNSPECIFIED.);
#26296=B_SPLINE_CURVE_WITH_KNOTS('',3,(#428212,#428213,#428214,#428215,
#428216,#428217,#428218,#428219,#428220,#428221,#428222,#428223,#428224,
#428225,#428226,#428227,#428228,#428229,#428230,#428231,#428232,#428233,
#428234,#428235,#428236,#428237,#428238,#428239),.UNSPECIFIED.,.F.,.F.,
(4,3,3,3,3,3,3,3,3,4),(0.,8.66039628583575E-6,1.64707715200666E-5,2.24502894132503E-5,
2.49975961757824E-5,2.88526003690281E-5,3.10661348995017E-5,3.4305354351696E-5,
3.66410545653561E-5,4.00504537627891E-5),.UNSPECIFIED.);
#26297=B_SPLINE_CURVE_WITH_KNOTS('',3,(#428242,#428243,#428244,#428245,
#428246,#428247,#428248),.UNSPECIFIED.,.F.,.F.,(4,3,4),(0.,4.40000041065376E-5,
9.89910850773114E-5),.UNSPECIFIED.);
#26298=B_SPLINE_CURVE_WITH_KNOTS('',3,(#428269,#428270,#428271,#428272,
#428273,#428274,#428275,#428276,#428277,#428278,#428279,#428280,#428281,
#428282,#428283,#428284,#428285,#428286,#428287,#428288,#428289,#428290,
#428291,#428292,#428293,#428294,#428295,#428296,#428297,#428298,#428299,
#428300,#428301,#428302),.UNSPECIFIED.,.F.,.F.,(4,3,3,3,3,3,3,3,3,3,3,4),
(0.,4.29157837305384E-6,5.42772623795331E-6,1.00901698482348E-5,1.31279195068639E-5,
1.57383542265921E-5,1.61011507492104E-5,1.67166789291754E-5,1.95343262811356E-5,
2.29377234674648E-5,2.71556047620052E-5,3.34407099942653E-5),
 .UNSPECIFIED.);
#26299=B_SPLINE_CURVE_WITH_KNOTS('',3,(#428315,#428316,#428317,#428318,
#428319,#428320,#428321,#428322,#428323,#428324,#428325,#428326,#428327,
#428328,#428329,#428330,#428331,#428332,#428333,#428334,#428335,#428336,
#428337,#428338,#428339,#428340,#428341,#428342,#428343,#428344,#428345,
#428346,#428347,#428348),.UNSPECIFIED.,.F.,.F.,(4,3,3,3,3,3,3,3,3,3,3,4),
(2.16840434497101E-19,3.71309426656624E-6,5.39981071559413E-6,8.78933289330621E-6,
9.00272357067499E-6,1.07143984504148E-5,1.60780299679538E-5,1.65806081157682E-5,
2.30369726850502E-5,2.67819200416079E-5,3.59736924187975E-5,4.03862783806988E-5),
 .UNSPECIFIED.);
#26300=B_SPLINE_CURVE_WITH_KNOTS('',3,(#428461,#428462,#428463,#428464),
 .UNSPECIFIED.,.F.,.F.,(4,4),(0.,7.70025630629237E-5),.UNSPECIFIED.);
#26301=B_SPLINE_CURVE_WITH_KNOTS('',3,(#428474,#428475,#428476,#428477),
 .UNSPECIFIED.,.F.,.F.,(4,4),(2.16840434497101E-19,7.70025630629237E-5),
 .UNSPECIFIED.);
#26302=B_SPLINE_CURVE_WITH_KNOTS('',3,(#428481,#428482,#428483,#428484,
#428485,#428486,#428487,#428488,#428489,#428490,#428491,#428492,#428493,
#428494,#428495,#428496,#428497,#428498,#428499,#428500,#428501,#428502,
#428503,#428504,#428505,#428506,#428507,#428508,#428509,#428510,#428511,
#428512,#428513,#428514,#428515,#428516,#428517),.UNSPECIFIED.,.F.,.F.,
(4,3,3,3,3,3,3,3,3,3,3,3,4),(0.,9.59031527199202E-6,1.94769411222766E-5,
2.02405092183153E-5,3.21374138577703E-5,3.60302195070439E-5,4.42640648818995E-5,
4.53660204229444E-5,5.03633762302019E-5,5.17708036292897E-5,5.37928993851988E-5,
5.54103755460197E-5,5.64557889509303E-5),.UNSPECIFIED.);
#26303=B_SPLINE_CURVE_WITH_KNOTS('',3,(#428518,#428519,#428520,#428521,
#428522,#428523,#428524,#428525,#428526,#428527,#428528,#428529,#428530,
#428531,#428532,#428533,#428534,#428535,#428536,#428537,#428538,#428539,
#428540,#428541,#428542,#428543,#428544,#428545),.UNSPECIFIED.,.F.,.F.,
(4,3,3,3,3,3,3,3,3,4),(5.64557889509303E-5,5.98940966493749E-5,6.34214003873378E-5,
7.22241476083715E-5,7.38322796533363E-5,8.36529189331431E-5,8.80714278222498E-5,
9.84837568500731E-5,0.000108624704079147,0.000110823272382853),
 .UNSPECIFIED.);
#26304=B_SPLINE_CURVE_WITH_KNOTS('',3,(#428561,#428562,#428563,#428564,
#428565,#428566,#428567,#428568,#428569,#428570,#428571,#428572,#428573,
#428574,#428575,#428576,#428577,#428578,#428579,#428580,#428581,#428582,
#428583,#428584,#428585,#428586,#428587,#428588),.UNSPECIFIED.,.F.,.F.,
(4,3,3,3,3,3,3,3,3,4),(0.,8.66039628583168E-6,1.64707715200665E-5,2.24502894132335E-5,
2.49975961757824E-5,2.8852600369028E-5,3.10661348995016E-5,3.4305354351696E-5,
3.66410545653561E-5,4.00504537627882E-5),.UNSPECIFIED.);
#26305=B_SPLINE_CURVE_WITH_KNOTS('',3,(#428591,#428592,#428593,#428594,
#428595,#428596,#428597),.UNSPECIFIED.,.F.,.F.,(4,3,4),(0.,4.40000041065375E-5,
9.89910850773113E-5),.UNSPECIFIED.);
#26306=B_SPLINE_CURVE_WITH_KNOTS('',3,(#428618,#428619,#428620,#428621,
#428622,#428623,#428624,#428625,#428626,#428627,#428628,#428629,#428630,
#428631,#428632,#428633,#428634,#428635,#428636,#428637,#428638,#428639,
#428640,#428641,#428642,#428643,#428644,#428645,#428646,#428647,#428648,
#428649,#428650,#428651),.UNSPECIFIED.,.F.,.F.,(4,3,3,3,3,3,3,3,3,3,3,4),
(0.,4.29157837304218E-6,5.42772623795328E-6,1.00901698482345E-5,1.31279195068639E-5,
1.57383542265798E-5,1.61011507492105E-5,1.67166789291752E-5,1.9534326281136E-5,
2.29377234674652E-5,2.71556047620059E-5,3.34407099942656E-5),
 .UNSPECIFIED.);
#26307=B_SPLINE_CURVE_WITH_KNOTS('',3,(#428664,#428665,#428666,#428667,
#428668,#428669,#428670,#428671,#428672,#428673,#428674,#428675,#428676,
#428677,#428678,#428679,#428680,#428681,#428682,#428683,#428684,#428685,
#428686,#428687,#428688,#428689,#428690,#428691,#428692,#428693,#428694,
#428695,#428696,#428697),.UNSPECIFIED.,.F.,.F.,(4,3,3,3,3,3,3,3,3,3,3,4),
(0.,3.71309426656666E-6,5.39981071559459E-6,8.78933289334293E-6,9.00272357067531E-6,
1.0714398450415E-5,1.60780299679529E-5,1.65806081157687E-5,2.30369726850411E-5,
2.67819200416086E-5,3.59736924188054E-5,4.03862783806999E-5),
 .UNSPECIFIED.);
#26308=B_SPLINE_CURVE_WITH_KNOTS('',3,(#428810,#428811,#428812,#428813),
 .UNSPECIFIED.,.F.,.F.,(4,4),(0.,7.7002563062924E-5),.UNSPECIFIED.);
#26309=B_SPLINE_CURVE_WITH_KNOTS('',3,(#428823,#428824,#428825,#428826),
 .UNSPECIFIED.,.F.,.F.,(4,4),(6.1331736667335E-19,7.70025630629235E-5),
 .UNSPECIFIED.);
#26310=B_SPLINE_CURVE_WITH_KNOTS('',3,(#428830,#428831,#428832,#428833,
#428834,#428835,#428836,#428837,#428838,#428839,#428840,#428841,#428842,
#428843,#428844,#428845,#428846,#428847,#428848,#428849,#428850,#428851,
#428852,#428853,#428854,#428855,#428856,#428857,#428858,#428859,#428860,
#428861,#428862,#428863,#428864,#428865,#428866),.UNSPECIFIED.,.F.,.F.,
(4,3,3,3,3,3,3,3,3,3,3,3,4),(0.,9.59031527201265E-6,1.94769411223105E-5,
2.02405092183152E-5,3.2137413857766E-5,3.60302195070438E-5,4.42640648818916E-5,
4.53660204229442E-5,5.03633762302019E-5,5.17708036292896E-5,5.37928993851987E-5,
5.54103755460202E-5,5.64557889510335E-5),.UNSPECIFIED.);
#26311=B_SPLINE_CURVE_WITH_KNOTS('',3,(#428867,#428868,#428869,#428870,
#428871,#428872,#428873,#428874,#428875,#428876,#428877,#428878,#428879,
#428880,#428881,#428882,#428883,#428884,#428885,#428886,#428887,#428888,
#428889,#428890,#428891,#428892,#428893,#428894),.UNSPECIFIED.,.F.,.F.,
(4,3,3,3,3,3,3,3,3,4),(5.64557889510335E-5,5.98940966493751E-5,6.34214003873383E-5,
7.22241476084741E-5,7.38322796533365E-5,8.36529189331344E-5,8.80714278222503E-5,
9.8483756850067E-5,0.000108624704079123,0.000110823272382854),
 .UNSPECIFIED.);
#26312=B_SPLINE_CURVE_WITH_KNOTS('',3,(#428910,#428911,#428912,#428913,
#428914,#428915,#428916,#428917,#428918,#428919,#428920,#428921,#428922,
#428923,#428924,#428925,#428926,#428927,#428928,#428929,#428930,#428931,
#428932,#428933,#428934,#428935,#428936,#428937),.UNSPECIFIED.,.F.,.F.,
(4,3,3,3,3,3,3,3,3,4),(0.,8.66039628579893E-6,1.64707715200667E-5,2.24502894132494E-5,
2.49975961757824E-5,2.88526003690281E-5,3.10661348995014E-5,3.43053543516958E-5,
3.66410545653558E-5,4.00504537627883E-5),.UNSPECIFIED.);
#26313=B_SPLINE_CURVE_WITH_KNOTS('',3,(#428940,#428941,#428942,#428943,
#428944,#428945,#428946),.UNSPECIFIED.,.F.,.F.,(4,3,4),(0.,4.40000041065374E-5,
9.89910850773111E-5),.UNSPECIFIED.);
#26314=B_SPLINE_CURVE_WITH_KNOTS('',3,(#428967,#428968,#428969,#428970,
#428971,#428972,#428973,#428974,#428975,#428976,#428977,#428978,#428979,
#428980,#428981,#428982,#428983,#428984,#428985,#428986,#428987,#428988,
#428989,#428990,#428991,#428992,#428993,#428994,#428995,#428996,#428997,
#428998,#428999,#429000),.UNSPECIFIED.,.F.,.F.,(4,3,3,3,3,3,3,3,3,3,3,4),
(0.,4.29157837304618E-6,5.42772623795343E-6,1.0090169848235E-5,1.31279195068639E-5,
1.57383542265892E-5,1.61011507492107E-5,1.6716678929176E-5,1.95343262811359E-5,
2.29377234674647E-5,2.71556047620057E-5,3.34407099942664E-5),
 .UNSPECIFIED.);
#26315=B_SPLINE_CURVE_WITH_KNOTS('',3,(#429013,#429014,#429015,#429016,
#429017,#429018,#429019,#429020,#429021,#429022,#429023,#429024,#429025,
#429026,#429027,#429028,#429029,#429030,#429031,#429032,#429033,#429034,
#429035,#429036,#429037,#429038,#429039,#429040,#429041,#429042,#429043,
#429044,#429045,#429046),.UNSPECIFIED.,.F.,.F.,(4,3,3,3,3,3,3,3,3,3,3,4),
(0.,3.71309426656647E-6,5.39981071559407E-6,8.7893328936682E-6,9.00272357067528E-6,
1.07143984504149E-5,1.60780299679635E-5,1.65806081157687E-5,2.30369726850325E-5,
2.67819200416084E-5,3.59736924187732E-5,4.03862783806996E-5),
 .UNSPECIFIED.);
#26316=B_SPLINE_CURVE_WITH_KNOTS('',3,(#429159,#429160,#429161,#429162),
 .UNSPECIFIED.,.F.,.F.,(4,4),(0.,7.70025630629237E-5),.UNSPECIFIED.);
#26317=B_SPLINE_CURVE_WITH_KNOTS('',3,(#429172,#429173,#429174,#429175),
 .UNSPECIFIED.,.F.,.F.,(4,4),(2.16840434497101E-19,7.70025630629237E-5),
 .UNSPECIFIED.);
#26318=B_SPLINE_CURVE_WITH_KNOTS('',3,(#429179,#429180,#429181,#429182,
#429183,#429184,#429185,#429186,#429187,#429188,#429189,#429190,#429191,
#429192,#429193,#429194,#429195,#429196,#429197,#429198,#429199,#429200,
#429201,#429202,#429203,#429204,#429205,#429206,#429207,#429208,#429209,
#429210,#429211,#429212,#429213,#429214,#429215),.UNSPECIFIED.,.F.,.F.,
(4,3,3,3,3,3,3,3,3,3,3,3,4),(0.,9.59031527200831E-6,1.94769411222969E-5,
2.02405092183152E-5,3.21374138577705E-5,3.60302195070437E-5,4.4264064881883E-5,
4.53660204229444E-5,5.03633762301811E-5,5.17708036292893E-5,5.37928993851988E-5,
5.54103755460199E-5,5.64557889510115E-5),.UNSPECIFIED.);
#26319=B_SPLINE_CURVE_WITH_KNOTS('',3,(#429216,#429217,#429218,#429219,
#429220,#429221,#429222,#429223,#429224,#429225,#429226,#429227,#429228,
#429229,#429230,#429231,#429232,#429233,#429234,#429235,#429236,#429237,
#429238,#429239,#429240,#429241,#429242,#429243),.UNSPECIFIED.,.F.,.F.,
(4,3,3,3,3,3,3,3,3,4),(5.64557889510115E-5,5.98940966493751E-5,6.34214003873379E-5,
7.22241476084954E-5,7.38322796533364E-5,8.36529189331411E-5,8.80714278222498E-5,
9.84837568500968E-5,0.000108624704079193,0.000110823272382853),
 .UNSPECIFIED.);
#26320=B_SPLINE_CURVE_WITH_KNOTS('',3,(#429259,#429260,#429261,#429262,
#429263,#429264,#429265,#429266,#429267,#429268,#429269,#429270,#429271,
#429272,#429273,#429274,#429275,#429276,#429277,#429278,#429279,#429280,
#429281,#429282,#429283,#429284,#429285,#429286),.UNSPECIFIED.,.F.,.F.,
(4,3,3,3,3,3,3,3,3,4),(0.,8.66039628577601E-6,1.64707715200666E-5,2.24502894132603E-5,
2.49975961757822E-5,2.88526003690279E-5,3.10661348995017E-5,3.43053543516959E-5,
3.66410545653557E-5,4.00504537627883E-5),.UNSPECIFIED.);
#26321=B_SPLINE_CURVE_WITH_KNOTS('',3,(#429289,#429290,#429291,#429292,
#429293,#429294,#429295),.UNSPECIFIED.,.F.,.F.,(4,3,4),(0.,4.40000041065374E-5,
9.89910850773112E-5),.UNSPECIFIED.);
#26322=B_SPLINE_CURVE_WITH_KNOTS('',3,(#429316,#429317,#429318,#429319,
#429320,#429321,#429322,#429323,#429324,#429325,#429326,#429327,#429328,
#429329,#429330,#429331,#429332,#429333,#429334,#429335,#429336,#429337,
#429338,#429339,#429340,#429341,#429342,#429343,#429344,#429345,#429346,
#429347,#429348,#429349),.UNSPECIFIED.,.F.,.F.,(4,3,3,3,3,3,3,3,3,3,3,4),
(0.,4.29157837305213E-6,5.42772623795348E-6,1.0090169848235E-5,1.31279195068641E-5,
1.57383542265938E-5,1.61011507492108E-5,1.67166789291762E-5,1.95343262811361E-5,
2.29377234674651E-5,2.71556047620057E-5,3.34407099942658E-5),
 .UNSPECIFIED.);
#26323=B_SPLINE_CURVE_WITH_KNOTS('',3,(#429362,#429363,#429364,#429365,
#429366,#429367,#429368,#429369,#429370,#429371,#429372,#429373,#429374,
#429375,#429376,#429377,#429378,#429379,#429380,#429381,#429382,#429383,
#429384,#429385,#429386,#429387,#429388,#429389,#429390,#429391,#429392,
#429393,#429394,#429395),.UNSPECIFIED.,.F.,.F.,(4,3,3,3,3,3,3,3,3,3,3,4),
(2.16840434497101E-19,3.71309426656637E-6,5.39981071559423E-6,8.78933289368051E-6,
9.00272357067532E-6,1.0714398450415E-5,1.60780299679574E-5,1.65806081157687E-5,
2.30369726850297E-5,2.67819200416087E-5,3.59736924188118E-5,4.03862783807003E-5),
 .UNSPECIFIED.);
#26324=B_SPLINE_CURVE_WITH_KNOTS('',3,(#429508,#429509,#429510,#429511),
 .UNSPECIFIED.,.F.,.F.,(4,4),(0.,7.70025630629237E-5),.UNSPECIFIED.);
#26325=B_SPLINE_CURVE_WITH_KNOTS('',3,(#429521,#429522,#429523,#429524),
 .UNSPECIFIED.,.F.,.F.,(4,4),(0.,7.70025630629238E-5),.UNSPECIFIED.);
#26326=B_SPLINE_CURVE_WITH_KNOTS('',3,(#429528,#429529,#429530,#429531,
#429532,#429533,#429534,#429535,#429536,#429537,#429538,#429539,#429540,
#429541,#429542,#429543,#429544,#429545,#429546,#429547,#429548,#429549,
#429550,#429551,#429552,#429553,#429554,#429555,#429556,#429557,#429558,
#429559,#429560,#429561,#429562,#429563,#429564),.UNSPECIFIED.,.F.,.F.,
(4,3,3,3,3,3,3,3,3,3,3,3,4),(0.,9.59031527201064E-6,1.94769411223038E-5,
2.02405092183152E-5,3.21374138577706E-5,3.6030219507044E-5,4.42640648818172E-5,
4.53660204229447E-5,5.03633762302194E-5,5.17708036292895E-5,5.37928993851989E-5,
5.54103755460194E-5,5.64557889514687E-5),.UNSPECIFIED.);
#26327=B_SPLINE_CURVE_WITH_KNOTS('',3,(#429565,#429566,#429567,#429568,
#429569,#429570,#429571,#429572,#429573,#429574,#429575,#429576,#429577,
#429578,#429579,#429580,#429581,#429582,#429583,#429584,#429585,#429586,
#429587,#429588,#429589,#429590,#429591,#429592),.UNSPECIFIED.,.F.,.F.,
(4,3,3,3,3,3,3,3,3,4),(5.64557889514687E-5,5.98940966493748E-5,6.34214003873379E-5,
7.22241476084777E-5,7.38322796533365E-5,8.36529189331359E-5,8.80714278222495E-5,
9.84837568500667E-5,0.000108624704079124,0.000110823272382853),
 .UNSPECIFIED.);
#26328=B_SPLINE_CURVE_WITH_KNOTS('',3,(#429608,#429609,#429610,#429611,
#429612,#429613,#429614,#429615,#429616,#429617,#429618,#429619,#429620,
#429621,#429622,#429623,#429624,#429625,#429626,#429627,#429628,#429629,
#429630,#429631,#429632,#429633,#429634,#429635),.UNSPECIFIED.,.F.,.F.,
(4,3,3,3,3,3,3,3,3,4),(0.,8.66039628581978E-6,1.64707715200666E-5,2.24502894132339E-5,
2.49975961757823E-5,2.88526003690281E-5,3.10661348995017E-5,3.43053543516961E-5,
3.66410545653563E-5,4.00504537627894E-5),.UNSPECIFIED.);
#26329=B_SPLINE_CURVE_WITH_KNOTS('',3,(#429638,#429639,#429640,#429641,
#429642,#429643,#429644),.UNSPECIFIED.,.F.,.F.,(4,3,4),(0.,4.40000041065377E-5,
9.89910850773114E-5),.UNSPECIFIED.);
#26330=B_SPLINE_CURVE_WITH_KNOTS('',3,(#429665,#429666,#429667,#429668,
#429669,#429670,#429671,#429672,#429673,#429674,#429675,#429676,#429677,
#429678,#429679,#429680,#429681,#429682,#429683,#429684,#429685,#429686,
#429687,#429688,#429689,#429690,#429691,#429692,#429693,#429694,#429695,
#429696,#429697,#429698),.UNSPECIFIED.,.F.,.F.,(4,3,3,3,3,3,3,3,3,3,3,4),
(0.,4.29157837304062E-6,5.42772623795341E-6,1.00901698482346E-5,1.31279195068639E-5,
1.57383542265844E-5,1.61011507492103E-5,1.6716678929175E-5,1.95343262811355E-5,
2.29377234674645E-5,2.71556047620055E-5,3.34407099942655E-5),
 .UNSPECIFIED.);
#26331=B_SPLINE_CURVE_WITH_KNOTS('',3,(#429711,#429712,#429713,#429714,
#429715,#429716,#429717,#429718,#429719,#429720,#429721,#429722,#429723,
#429724,#429725,#429726,#429727,#429728,#429729,#429730,#429731,#429732,
#429733,#429734,#429735,#429736,#429737,#429738,#429739,#429740,#429741,
#429742,#429743,#429744),.UNSPECIFIED.,.F.,.F.,(4,3,3,3,3,3,3,3,3,3,3,4),
(2.16840434497101E-19,3.71309426656627E-6,5.39981071559405E-6,8.78933289328103E-6,
9.00272357067521E-6,1.0714398450415E-5,1.60780299679534E-5,1.65806081157689E-5,
2.30369726850297E-5,2.6781920041609E-5,3.59736924188219E-5,4.03862783807006E-5),
 .UNSPECIFIED.);
#26332=B_SPLINE_CURVE_WITH_KNOTS('',3,(#429857,#429858,#429859,#429860),
 .UNSPECIFIED.,.F.,.F.,(4,4),(0.,7.70025630629241E-5),.UNSPECIFIED.);
#26333=B_SPLINE_CURVE_WITH_KNOTS('',3,(#429870,#429871,#429872,#429873),
 .UNSPECIFIED.,.F.,.F.,(4,4),(4.33680868994202E-19,7.70025630629237E-5),
 .UNSPECIFIED.);
#26334=B_SPLINE_CURVE_WITH_KNOTS('',3,(#429877,#429878,#429879,#429880,
#429881,#429882,#429883,#429884,#429885,#429886,#429887,#429888,#429889,
#429890,#429891,#429892,#429893,#429894,#429895,#429896,#429897,#429898,
#429899,#429900,#429901,#429902,#429903,#429904,#429905,#429906,#429907,
#429908,#429909,#429910,#429911,#429912,#429913),.UNSPECIFIED.,.F.,.F.,
(4,3,3,3,3,3,3,3,3,3,3,3,4),(0.,9.5903152720102E-6,1.94769411223118E-5,
2.02405092183152E-5,3.21374138577704E-5,3.6030219507044E-5,4.42640648818753E-5,
4.53660204229444E-5,5.03633762302121E-5,5.17708036292897E-5,5.3792899385199E-5,
5.541037554602E-5,5.645578895115E-5),.UNSPECIFIED.);
#26335=B_SPLINE_CURVE_WITH_KNOTS('',3,(#429914,#429915,#429916,#429917,
#429918,#429919,#429920,#429921,#429922,#429923,#429924,#429925,#429926,
#429927,#429928,#429929,#429930,#429931,#429932,#429933,#429934,#429935,
#429936,#429937,#429938,#429939,#429940,#429941),.UNSPECIFIED.,.F.,.F.,
(4,3,3,3,3,3,3,3,3,4),(5.645578895115E-5,5.9894096649375E-5,6.34214003873382E-5,
7.22241476084637E-5,7.38322796533365E-5,8.36529189331475E-5,8.80714278222503E-5,
9.84837568500771E-5,0.000108624704079148,0.000110823272382854),
 .UNSPECIFIED.);
#26336=B_SPLINE_CURVE_WITH_KNOTS('',3,(#429957,#429958,#429959,#429960,
#429961,#429962,#429963,#429964,#429965,#429966,#429967,#429968,#429969,
#429970,#429971,#429972,#429973,#429974,#429975,#429976,#429977,#429978,
#429979,#429980,#429981,#429982,#429983,#429984),.UNSPECIFIED.,.F.,.F.,
(4,3,3,3,3,3,3,3,3,4),(0.,8.66039628582388E-6,1.64707715200666E-5,2.24502894132161E-5,
2.49975961757823E-5,2.8852600369028E-5,3.10661348995018E-5,3.43053543516958E-5,
3.6641054565356E-5,4.00504537627889E-5),.UNSPECIFIED.);
#26337=B_SPLINE_CURVE_WITH_KNOTS('',3,(#429987,#429988,#429989,#429990,
#429991,#429992,#429993),.UNSPECIFIED.,.F.,.F.,(4,3,4),(0.,4.40000041065375E-5,
9.89910850773112E-5),.UNSPECIFIED.);
#26338=B_SPLINE_CURVE_WITH_KNOTS('',3,(#430014,#430015,#430016,#430017,
#430018,#430019,#430020,#430021,#430022,#430023,#430024,#430025,#430026,
#430027,#430028,#430029,#430030,#430031,#430032,#430033,#430034,#430035,
#430036,#430037,#430038,#430039,#430040,#430041,#430042,#430043,#430044,
#430045,#430046,#430047),.UNSPECIFIED.,.F.,.F.,(4,3,3,3,3,3,3,3,3,3,3,4),
(0.,4.29157837304584E-6,5.42772623795323E-6,1.00901698482347E-5,1.31279195068638E-5,
1.57383542265883E-5,1.61011507492104E-5,1.67166789291758E-5,1.95343262811358E-5,
2.29377234674649E-5,2.71556047620058E-5,3.3440709994266E-5),
 .UNSPECIFIED.);
#26339=B_SPLINE_CURVE_WITH_KNOTS('',3,(#430060,#430061,#430062,#430063,
#430064,#430065,#430066,#430067,#430068,#430069,#430070,#430071,#430072,
#430073,#430074,#430075,#430076,#430077,#430078,#430079,#430080,#430081,
#430082,#430083,#430084,#430085,#430086,#430087,#430088,#430089,#430090,
#430091,#430092,#430093),.UNSPECIFIED.,.F.,.F.,(4,3,3,3,3,3,3,3,3,3,3,4),
(0.,3.71309426656669E-6,5.39981071559425E-6,8.78933289330839E-6,9.00272357067503E-6,
1.07143984504149E-5,1.6078029967955E-5,1.65806081157685E-5,2.30369726850441E-5,
2.67819200416079E-5,3.59736924187609E-5,4.03862783806989E-5),
 .UNSPECIFIED.);
#26340=B_SPLINE_CURVE_WITH_KNOTS('',3,(#430206,#430207,#430208,#430209),
 .UNSPECIFIED.,.F.,.F.,(4,4),(0.,7.70025630629237E-5),.UNSPECIFIED.);
#26341=B_SPLINE_CURVE_WITH_KNOTS('',3,(#430219,#430220,#430221,#430222),
 .UNSPECIFIED.,.F.,.F.,(4,4),(0.,7.70025630629239E-5),.UNSPECIFIED.);
#26342=B_SPLINE_CURVE_WITH_KNOTS('',3,(#430226,#430227,#430228,#430229,
#430230,#430231,#430232,#430233,#430234,#430235,#430236,#430237,#430238,
#430239,#430240,#430241,#430242,#430243,#430244,#430245,#430246,#430247,
#430248,#430249,#430250,#430251,#430252,#430253,#430254,#430255,#430256,
#430257,#430258,#430259,#430260,#430261,#430262),.UNSPECIFIED.,.F.,.F.,
(4,3,3,3,3,3,3,3,3,3,3,3,4),(0.,9.59031527199471E-6,1.94769411222829E-5,
2.02405092183151E-5,3.21374138577656E-5,3.60302195070439E-5,4.42640648818787E-5,
4.53660204229443E-5,5.03633762302059E-5,5.17708036292899E-5,5.37928993851987E-5,
5.54103755460193E-5,5.64557889511556E-5),.UNSPECIFIED.);
#26343=B_SPLINE_CURVE_WITH_KNOTS('',3,(#430263,#430264,#430265,#430266,
#430267,#430268,#430269,#430270,#430271,#430272,#430273,#430274,#430275,
#430276,#430277,#430278,#430279,#430280,#430281,#430282,#430283,#430284,
#430285,#430286,#430287,#430288,#430289,#430290),.UNSPECIFIED.,.F.,.F.,
(4,3,3,3,3,3,3,3,3,4),(5.64557889511556E-5,5.98940966493751E-5,6.34214003873379E-5,
7.22241476084211E-5,7.38322796533363E-5,8.3652918933143E-5,8.807142782225E-5,
9.84837568500654E-5,0.000108624704079118,0.000110823272382854),
 .UNSPECIFIED.);
#26344=B_SPLINE_CURVE_WITH_KNOTS('',3,(#430306,#430307,#430308,#430309,
#430310,#430311,#430312,#430313,#430314,#430315,#430316,#430317,#430318,
#430319,#430320,#430321,#430322,#430323,#430324,#430325,#430326,#430327,
#430328,#430329,#430330,#430331,#430332,#430333),.UNSPECIFIED.,.F.,.F.,
(4,3,3,3,3,3,3,3,3,4),(0.,8.660396285831E-6,1.64707715200666E-5,2.24502894132403E-5,
2.49975961757823E-5,2.8852600369028E-5,3.10661348995015E-5,3.43053543516961E-5,
3.66410545653561E-5,4.00504537627889E-5),.UNSPECIFIED.);
#26345=B_SPLINE_CURVE_WITH_KNOTS('',3,(#430336,#430337,#430338,#430339,
#430340,#430341,#430342),.UNSPECIFIED.,.F.,.F.,(4,3,4),(0.,4.40000041065374E-5,
9.89910850773116E-5),.UNSPECIFIED.);
#26346=B_SPLINE_CURVE_WITH_KNOTS('',3,(#430363,#430364,#430365,#430366,
#430367,#430368,#430369,#430370,#430371,#430372,#430373,#430374,#430375,
#430376,#430377,#430378,#430379,#430380,#430381,#430382,#430383,#430384,
#430385,#430386,#430387,#430388,#430389,#430390,#430391,#430392,#430393,
#430394,#430395,#430396),.UNSPECIFIED.,.F.,.F.,(4,3,3,3,3,3,3,3,3,3,3,4),
(0.,4.29157837303028E-6,5.42772623795317E-6,1.00901698482344E-5,1.31279195068634E-5,
1.57383542265872E-5,1.61011507492103E-5,1.67166789291751E-5,1.95343262811353E-5,
2.29377234674644E-5,2.71556047620053E-5,3.34407099942653E-5),
 .UNSPECIFIED.);
#26347=B_SPLINE_CURVE_WITH_KNOTS('',3,(#430409,#430410,#430411,#430412,
#430413,#430414,#430415,#430416,#430417,#430418,#430419,#430420,#430421,
#430422,#430423,#430424,#430425,#430426,#430427,#430428,#430429,#430430,
#430431,#430432,#430433,#430434,#430435,#430436,#430437,#430438,#430439,
#430440,#430441,#430442),.UNSPECIFIED.,.F.,.F.,(4,3,3,3,3,3,3,3,3,3,3,4),
(2.16840434497101E-19,3.71309426656678E-6,5.39981071559421E-6,8.78933289368528E-6,
9.00272357067521E-6,1.07143984504151E-5,1.60780299679553E-5,1.65806081157686E-5,
2.30369726850255E-5,2.67819200416087E-5,3.59736924188074E-5,4.03862783807002E-5),
 .UNSPECIFIED.);
#26348=B_SPLINE_CURVE_WITH_KNOTS('',3,(#430555,#430556,#430557,#430558),
 .UNSPECIFIED.,.F.,.F.,(4,4),(0.,7.7002563062924E-5),.UNSPECIFIED.);
#26349=B_SPLINE_CURVE_WITH_KNOTS('',3,(#430568,#430569,#430570,#430571),
 .UNSPECIFIED.,.F.,.F.,(4,4),(4.33680868994202E-19,7.70025630629234E-5),
 .UNSPECIFIED.);
#26350=B_SPLINE_CURVE_WITH_KNOTS('',3,(#430575,#430576,#430577,#430578,
#430579,#430580,#430581,#430582,#430583,#430584,#430585,#430586,#430587,
#430588,#430589,#430590,#430591,#430592,#430593,#430594,#430595,#430596,
#430597,#430598,#430599,#430600,#430601,#430602,#430603,#430604,#430605,
#430606,#430607,#430608,#430609,#430610,#430611),.UNSPECIFIED.,.F.,.F.,
(4,3,3,3,3,3,3,3,3,3,3,3,4),(0.,9.59031527198726E-6,1.94769411222748E-5,
2.0240509218315E-5,3.2137413857772E-5,3.60302195070436E-5,4.42640648818736E-5,
4.53660204229444E-5,5.03633762302037E-5,5.17708036292896E-5,5.3792899385199E-5,
5.54103755460196E-5,5.64557889513675E-5),.UNSPECIFIED.);
#26351=B_SPLINE_CURVE_WITH_KNOTS('',3,(#430612,#430613,#430614,#430615,
#430616,#430617,#430618,#430619,#430620,#430621,#430622,#430623,#430624,
#430625,#430626,#430627,#430628,#430629,#430630,#430631,#430632,#430633,
#430634,#430635,#430636,#430637,#430638,#430639),.UNSPECIFIED.,.F.,.F.,
(4,3,3,3,3,3,3,3,3,4),(5.64557889513675E-5,5.98940966493752E-5,6.34214003873379E-5,
7.22241476085083E-5,7.38322796533366E-5,8.36529189331453E-5,8.80714278222503E-5,
9.84837568500839E-5,0.000108624704079163,0.000110823272382854),
 .UNSPECIFIED.);
#26352=B_SPLINE_CURVE_WITH_KNOTS('',3,(#430655,#430656,#430657,#430658,
#430659,#430660,#430661,#430662,#430663,#430664,#430665,#430666,#430667,
#430668,#430669,#430670,#430671,#430672,#430673,#430674,#430675,#430676,
#430677,#430678,#430679,#430680,#430681,#430682),.UNSPECIFIED.,.F.,.F.,
(4,3,3,3,3,3,3,3,3,4),(0.,8.66039628583618E-6,1.64707715200666E-5,2.24502894132307E-5,
2.49975961757824E-5,2.88526003690281E-5,3.10661348995016E-5,3.43053543516959E-5,
3.66410545653561E-5,4.00504537627889E-5),.UNSPECIFIED.);
#26353=B_SPLINE_CURVE_WITH_KNOTS('',3,(#430685,#430686,#430687,#430688,
#430689,#430690,#430691),.UNSPECIFIED.,.F.,.F.,(4,3,4),(0.,4.40000041065375E-5,
9.89910850773113E-5),.UNSPECIFIED.);
#26354=B_SPLINE_CURVE_WITH_KNOTS('',3,(#430712,#430713,#430714,#430715,
#430716,#430717,#430718,#430719,#430720,#430721,#430722,#430723,#430724,
#430725,#430726,#430727,#430728,#430729,#430730,#430731,#430732,#430733,
#430734,#430735,#430736,#430737,#430738,#430739,#430740,#430741,#430742,
#430743,#430744,#430745),.UNSPECIFIED.,.F.,.F.,(4,3,3,3,3,3,3,3,3,3,3,4),
(0.,4.29157837303874E-6,5.42772623795334E-6,1.0090169848235E-5,1.31279195068638E-5,
1.57383542265808E-5,1.61011507492107E-5,1.67166789291761E-5,1.95343262811359E-5,
2.29377234674652E-5,2.71556047620062E-5,3.34407099942662E-5),
 .UNSPECIFIED.);
#26355=B_SPLINE_CURVE_WITH_KNOTS('',3,(#430758,#430759,#430760,#430761,
#430762,#430763,#430764,#430765,#430766,#430767,#430768,#430769,#430770,
#430771,#430772,#430773,#430774,#430775,#430776,#430777,#430778,#430779,
#430780,#430781,#430782,#430783,#430784,#430785,#430786,#430787,#430788,
#430789,#430790,#430791),.UNSPECIFIED.,.F.,.F.,(4,3,3,3,3,3,3,3,3,3,3,4),
(0.,3.71309426656648E-6,5.39981071559433E-6,8.78933289366858E-6,9.00272357067512E-6,
1.0714398450415E-5,1.60780299679577E-5,1.65806081157687E-5,2.3036972685043E-5,
2.67819200416086E-5,3.59736924187824E-5,4.03862783807001E-5),
 .UNSPECIFIED.);
#26356=B_SPLINE_CURVE_WITH_KNOTS('',3,(#430904,#430905,#430906,#430907),
 .UNSPECIFIED.,.F.,.F.,(4,4),(0.,7.70025630629237E-5),.UNSPECIFIED.);
#26357=B_SPLINE_CURVE_WITH_KNOTS('',3,(#430917,#430918,#430919,#430920),
 .UNSPECIFIED.,.F.,.F.,(4,4),(4.33680868994202E-19,7.70025630629238E-5),
 .UNSPECIFIED.);
#26358=B_SPLINE_CURVE_WITH_KNOTS('',3,(#430924,#430925,#430926,#430927,
#430928,#430929,#430930,#430931,#430932,#430933,#430934,#430935,#430936,
#430937,#430938,#430939,#430940,#430941,#430942,#430943,#430944,#430945,
#430946,#430947,#430948,#430949,#430950,#430951,#430952,#430953,#430954,
#430955,#430956,#430957,#430958,#430959,#430960),.UNSPECIFIED.,.F.,.F.,
(4,3,3,3,3,3,3,3,3,3,3,3,4),(0.,9.59031527200496E-6,1.94769411222924E-5,
2.02405092183151E-5,3.2137413857772E-5,3.6030219507044E-5,4.42640648817857E-5,
4.53660204229446E-5,5.03633762302157E-5,5.17708036292896E-5,5.37928993851989E-5,
5.54103755460198E-5,5.64557889510994E-5),.UNSPECIFIED.);
#26359=B_SPLINE_CURVE_WITH_KNOTS('',3,(#430961,#430962,#430963,#430964,
#430965,#430966,#430967,#430968,#430969,#430970,#430971,#430972,#430973,
#430974,#430975,#430976,#430977,#430978,#430979,#430980,#430981,#430982,
#430983,#430984,#430985,#430986,#430987,#430988),.UNSPECIFIED.,.F.,.F.,
(4,3,3,3,3,3,3,3,3,4),(5.64557889510994E-5,5.98940966493752E-5,6.34214003873382E-5,
7.22241476084606E-5,7.38322796533366E-5,8.36529189331425E-5,8.80714278222502E-5,
9.84837568500645E-5,0.000108624704079118,0.000110823272382854),
 .UNSPECIFIED.);
#26360=B_SPLINE_CURVE_WITH_KNOTS('',3,(#431004,#431005,#431006,#431007,
#431008,#431009,#431010,#431011,#431012,#431013,#431014,#431015,#431016,
#431017,#431018,#431019,#431020,#431021,#431022,#431023,#431024,#431025,
#431026,#431027,#431028,#431029,#431030,#431031),.UNSPECIFIED.,.F.,.F.,
(4,3,3,3,3,3,3,3,3,4),(0.,8.66039628580277E-6,1.6470771520067E-5,2.24502894132263E-5,
2.49975961757828E-5,2.88526003690287E-5,3.10661348995023E-5,3.43053543516968E-5,
3.66410545653568E-5,4.0050453762789E-5),.UNSPECIFIED.);
#26361=B_SPLINE_CURVE_WITH_KNOTS('',3,(#431034,#431035,#431036,#431037,
#431038,#431039,#431040),.UNSPECIFIED.,.F.,.F.,(4,3,4),(0.,4.40000041065373E-5,
9.89910850773113E-5),.UNSPECIFIED.);
#26362=B_SPLINE_CURVE_WITH_KNOTS('',3,(#431061,#431062,#431063,#431064,
#431065,#431066,#431067,#431068,#431069,#431070,#431071,#431072,#431073,
#431074,#431075,#431076,#431077,#431078,#431079,#431080,#431081,#431082,
#431083,#431084,#431085,#431086,#431087,#431088,#431089,#431090,#431091,
#431092,#431093,#431094),.UNSPECIFIED.,.F.,.F.,(4,3,3,3,3,3,3,3,3,3,3,4),
(0.,4.29157837304175E-6,5.42772623795323E-6,1.00901698482348E-5,1.31279195068639E-5,
1.57383542265785E-5,1.61011507492102E-5,1.67166789291755E-5,1.95343262811357E-5,
2.29377234674649E-5,2.71556047620058E-5,3.34407099942656E-5),
 .UNSPECIFIED.);
#26363=B_SPLINE_CURVE_WITH_KNOTS('',3,(#431107,#431108,#431109,#431110,
#431111,#431112,#431113,#431114,#431115,#431116,#431117,#431118,#431119,
#431120,#431121,#431122,#431123,#431124,#431125,#431126,#431127,#431128,
#431129,#431130,#431131,#431132,#431133,#431134,#431135,#431136,#431137,
#431138,#431139,#431140),.UNSPECIFIED.,.F.,.F.,(4,3,3,3,3,3,3,3,3,3,3,4),
(0.,3.71309426656655E-6,5.39981071559422E-6,8.7893328936629E-6,9.00272357067514E-6,
1.07143984504147E-5,1.60780299679635E-5,1.65806081157687E-5,2.30369726850508E-5,
2.67819200416086E-5,3.59736924187397E-5,4.03862783806999E-5),
 .UNSPECIFIED.);
#26364=B_SPLINE_CURVE_WITH_KNOTS('',3,(#431253,#431254,#431255,#431256),
 .UNSPECIFIED.,.F.,.F.,(4,4),(0.,7.70025630629239E-5),.UNSPECIFIED.);
#26365=B_SPLINE_CURVE_WITH_KNOTS('',3,(#431266,#431267,#431268,#431269),
 .UNSPECIFIED.,.F.,.F.,(4,4),(4.33680868994202E-19,7.70025630629236E-5),
 .UNSPECIFIED.);
#26366=B_SPLINE_CURVE_WITH_KNOTS('',3,(#431273,#431274,#431275,#431276,
#431277,#431278,#431279,#431280,#431281,#431282,#431283,#431284,#431285,
#431286,#431287,#431288,#431289,#431290,#431291,#431292,#431293,#431294,
#431295,#431296,#431297,#431298,#431299,#431300,#431301,#431302,#431303,
#431304,#431305,#431306,#431307,#431308,#431309),.UNSPECIFIED.,.F.,.F.,
(4,3,3,3,3,3,3,3,3,3,3,3,4),(0.,9.5903152720047E-6,1.94769411222842E-5,
2.0240509218315E-5,3.21374138577764E-5,3.6030219507044E-5,4.42640648818235E-5,
4.53660204229444E-5,5.0363376230219E-5,5.17708036292897E-5,5.37928993851989E-5,
5.54103755460197E-5,5.64557889508719E-5),.UNSPECIFIED.);
#26367=B_SPLINE_CURVE_WITH_KNOTS('',3,(#431310,#431311,#431312,#431313,
#431314,#431315,#431316,#431317,#431318,#431319,#431320,#431321,#431322,
#431323,#431324,#431325,#431326,#431327,#431328,#431329,#431330,#431331,
#431332,#431333,#431334,#431335,#431336,#431337),.UNSPECIFIED.,.F.,.F.,
(4,3,3,3,3,3,3,3,3,4),(5.64557889508719E-5,5.98940966493751E-5,6.3421400387338E-5,
7.22241476084641E-5,7.38322796533365E-5,8.36529189331414E-5,8.80714278222502E-5,
9.848375685006E-5,0.000108624704079087,0.000110823272382854),
 .UNSPECIFIED.);
#26368=B_SPLINE_CURVE_WITH_KNOTS('',3,(#431353,#431354,#431355,#431356,
#431357,#431358,#431359,#431360,#431361,#431362,#431363,#431364,#431365,
#431366,#431367,#431368,#431369,#431370,#431371,#431372,#431373,#431374,
#431375,#431376,#431377,#431378,#431379,#431380),.UNSPECIFIED.,.F.,.F.,
(4,3,3,3,3,3,3,3,3,4),(0.,8.66039628582158E-6,1.64707715200665E-5,2.24502894132426E-5,
2.49975961757824E-5,2.88526003690279E-5,3.10661348995016E-5,3.43053543516961E-5,
3.66410545653559E-5,4.00504537627885E-5),.UNSPECIFIED.);
#26369=B_SPLINE_CURVE_WITH_KNOTS('',3,(#431383,#431384,#431385,#431386,
#431387,#431388,#431389),.UNSPECIFIED.,.F.,.F.,(4,3,4),(0.,4.40000041065374E-5,
9.89910850773113E-5),.UNSPECIFIED.);
#26370=B_SPLINE_CURVE_WITH_KNOTS('',3,(#431410,#431411,#431412,#431413,
#431414,#431415,#431416,#431417,#431418,#431419,#431420,#431421,#431422,
#431423,#431424,#431425,#431426,#431427,#431428,#431429,#431430,#431431,
#431432,#431433,#431434,#431435,#431436,#431437,#431438,#431439,#431440,
#431441,#431442,#431443),.UNSPECIFIED.,.F.,.F.,(4,3,3,3,3,3,3,3,3,3,3,4),
(0.,4.29157837304048E-6,5.42772623795318E-6,1.00901698482346E-5,1.31279195068639E-5,
1.57383542265845E-5,1.61011507492104E-5,1.67166789291754E-5,1.95343262811357E-5,
2.29377234674649E-5,2.7155604762006E-5,3.34407099942659E-5),
 .UNSPECIFIED.);
#26371=B_SPLINE_CURVE_WITH_KNOTS('',3,(#431456,#431457,#431458,#431459,
#431460,#431461,#431462,#431463,#431464,#431465,#431466,#431467,#431468,
#431469,#431470,#431471,#431472,#431473,#431474,#431475,#431476,#431477,
#431478,#431479,#431480,#431481,#431482,#431483,#431484,#431485,#431486,
#431487,#431488,#431489),.UNSPECIFIED.,.F.,.F.,(4,3,3,3,3,3,3,3,3,3,3,4),
(0.,3.71309426656658E-6,5.39981071559416E-6,8.78933289367644E-6,9.00272357067511E-6,
1.07143984504147E-5,1.6078029967954E-5,1.65806081157684E-5,2.30369726850593E-5,
2.67819200416081E-5,3.59736924187712E-5,4.03862783806992E-5),
 .UNSPECIFIED.);
#26372=B_SPLINE_CURVE_WITH_KNOTS('',3,(#431602,#431603,#431604,#431605),
 .UNSPECIFIED.,.F.,.F.,(4,4),(0.,7.7002563062924E-5),.UNSPECIFIED.);
#26373=B_SPLINE_CURVE_WITH_KNOTS('',3,(#431615,#431616,#431617,#431618),
 .UNSPECIFIED.,.F.,.F.,(4,4),(4.33680868994202E-19,7.70025630629234E-5),
 .UNSPECIFIED.);
#26374=B_SPLINE_CURVE_WITH_KNOTS('',3,(#431622,#431623,#431624,#431625,
#431626,#431627,#431628,#431629,#431630,#431631,#431632,#431633,#431634,
#431635,#431636,#431637,#431638,#431639,#431640,#431641,#431642,#431643,
#431644,#431645,#431646,#431647,#431648,#431649,#431650,#431651,#431652,
#431653,#431654,#431655,#431656,#431657,#431658),.UNSPECIFIED.,.F.,.F.,
(4,3,3,3,3,3,3,3,3,3,3,3,4),(0.,9.59031527200327E-6,1.94769411222958E-5,
2.02405092183153E-5,3.21374138577732E-5,3.60302195070438E-5,4.42640648818343E-5,
4.53660204229444E-5,5.03633762302119E-5,5.17708036292895E-5,5.37928993851989E-5,
5.54103755460195E-5,5.64557889510178E-5),.UNSPECIFIED.);
#26375=B_SPLINE_CURVE_WITH_KNOTS('',3,(#431659,#431660,#431661,#431662,
#431663,#431664,#431665,#431666,#431667,#431668,#431669,#431670,#431671,
#431672,#431673,#431674,#431675,#431676,#431677,#431678,#431679,#431680,
#431681,#431682,#431683,#431684,#431685,#431686),.UNSPECIFIED.,.F.,.F.,
(4,3,3,3,3,3,3,3,3,4),(5.64557889510178E-5,5.9894096649375E-5,6.34214003873379E-5,
7.22241476083772E-5,7.38322796533363E-5,8.36529189331363E-5,8.80714278222497E-5,
9.84837568500626E-5,0.000108624704079122,0.000110823272382853),
 .UNSPECIFIED.);
#26376=B_SPLINE_CURVE_WITH_KNOTS('',3,(#431702,#431703,#431704,#431705,
#431706,#431707,#431708,#431709,#431710,#431711,#431712,#431713,#431714,
#431715,#431716,#431717,#431718,#431719,#431720,#431721,#431722,#431723,
#431724,#431725,#431726,#431727,#431728,#431729),.UNSPECIFIED.,.F.,.F.,
(4,3,3,3,3,3,3,3,3,4),(0.,8.66039628581431E-6,1.64707715200667E-5,2.24502894132164E-5,
2.49975961757824E-5,2.88526003690281E-5,3.10661348995016E-5,3.4305354351696E-5,
3.6641054565356E-5,4.00504537627885E-5),.UNSPECIFIED.);
#26377=B_SPLINE_CURVE_WITH_KNOTS('',3,(#431732,#431733,#431734,#431735,
#431736,#431737,#431738),.UNSPECIFIED.,.F.,.F.,(4,3,4),(0.,4.4000004106538E-5,
9.89910850773115E-5),.UNSPECIFIED.);
#26378=B_SPLINE_CURVE_WITH_KNOTS('',3,(#431759,#431760,#431761,#431762,
#431763,#431764,#431765,#431766,#431767,#431768,#431769,#431770,#431771,
#431772,#431773,#431774,#431775,#431776,#431777,#431778,#431779,#431780,
#431781,#431782,#431783,#431784,#431785,#431786,#431787,#431788,#431789,
#431790,#431791,#431792),.UNSPECIFIED.,.F.,.F.,(4,3,3,3,3,3,3,3,3,3,3,4),
(0.,4.29157837304129E-6,5.42772623795345E-6,1.00901698482348E-5,1.3127919506864E-5,
1.57383542265835E-5,1.61011507492105E-5,1.67166789291752E-5,1.95343262811359E-5,
2.2937723467465E-5,2.71556047620058E-5,3.34407099942656E-5),
 .UNSPECIFIED.);
#26379=B_SPLINE_CURVE_WITH_KNOTS('',3,(#431805,#431806,#431807,#431808,
#431809,#431810,#431811,#431812,#431813,#431814,#431815,#431816,#431817,
#431818,#431819,#431820,#431821,#431822,#431823,#431824,#431825,#431826,
#431827,#431828,#431829,#431830,#431831,#431832,#431833,#431834,#431835,
#431836,#431837,#431838),.UNSPECIFIED.,.F.,.F.,(4,3,3,3,3,3,3,3,3,3,3,4),
(0.,3.71309426656657E-6,5.3998107155942E-6,8.78933289368234E-6,9.00272357067517E-6,
1.07143984504149E-5,1.60780299679592E-5,1.65806081157687E-5,2.30369726850617E-5,
2.67819200416084E-5,3.59736924187323E-5,4.03862783806997E-5),
 .UNSPECIFIED.);
#26380=B_SPLINE_CURVE_WITH_KNOTS('',3,(#431951,#431952,#431953,#431954),
 .UNSPECIFIED.,.F.,.F.,(4,4),(0.,7.7002563062924E-5),.UNSPECIFIED.);
#26381=B_SPLINE_CURVE_WITH_KNOTS('',3,(#431964,#431965,#431966,#431967),
 .UNSPECIFIED.,.F.,.F.,(4,4),(4.33680868994202E-19,7.70025630629234E-5),
 .UNSPECIFIED.);
#26382=B_SPLINE_CURVE_WITH_KNOTS('',3,(#431971,#431972,#431973,#431974,
#431975,#431976,#431977,#431978,#431979,#431980,#431981,#431982,#431983,
#431984,#431985,#431986,#431987,#431988,#431989,#431990,#431991,#431992,
#431993,#431994,#431995,#431996,#431997,#431998,#431999,#432000,#432001,
#432002,#432003,#432004,#432005,#432006,#432007),.UNSPECIFIED.,.F.,.F.,
(4,3,3,3,3,3,3,3,3,3,3,3,4),(0.,9.5903152720082E-6,1.94769411223113E-5,
2.02405092183154E-5,3.21374138577727E-5,3.60302195070441E-5,4.42640648818362E-5,
4.53660204229446E-5,5.03633762302027E-5,5.17708036292899E-5,5.37928993851991E-5,
5.54103755460203E-5,5.64557889513793E-5),.UNSPECIFIED.);
#26383=B_SPLINE_CURVE_WITH_KNOTS('',3,(#432008,#432009,#432010,#432011,
#432012,#432013,#432014,#432015,#432016,#432017,#432018,#432019,#432020,
#432021,#432022,#432023,#432024,#432025,#432026,#432027,#432028,#432029,
#432030,#432031,#432032,#432033,#432034,#432035),.UNSPECIFIED.,.F.,.F.,
(4,3,3,3,3,3,3,3,3,4),(5.64557889513793E-5,5.98940966493753E-5,6.34214003873382E-5,
7.22241476083956E-5,7.38322796533367E-5,8.36529189331575E-5,8.80714278222504E-5,
9.84837568501053E-5,0.000108624704079197,0.000110823272382854),
 .UNSPECIFIED.);
#26384=B_SPLINE_CURVE_WITH_KNOTS('',3,(#432051,#432052,#432053,#432054,
#432055,#432056,#432057,#432058,#432059,#432060,#432061,#432062,#432063,
#432064,#432065,#432066,#432067,#432068,#432069,#432070,#432071,#432072,
#432073,#432074,#432075,#432076,#432077,#432078),.UNSPECIFIED.,.F.,.F.,
(4,3,3,3,3,3,3,3,3,4),(0.,8.66039628578029E-6,1.64707715200667E-5,2.24502894132172E-5,
2.49975961757824E-5,2.8852600369028E-5,3.10661348995016E-5,3.4305354351696E-5,
3.66410545653558E-5,4.00504537627886E-5),.UNSPECIFIED.);
#26385=B_SPLINE_CURVE_WITH_KNOTS('',3,(#432081,#432082,#432083,#432084,
#432085,#432086,#432087),.UNSPECIFIED.,.F.,.F.,(4,3,4),(0.,4.40000041065376E-5,
9.8991085077311E-5),.UNSPECIFIED.);
#26386=B_SPLINE_CURVE_WITH_KNOTS('',3,(#432108,#432109,#432110,#432111,
#432112,#432113,#432114,#432115,#432116,#432117,#432118,#432119,#432120,
#432121,#432122,#432123,#432124,#432125,#432126,#432127,#432128,#432129,
#432130,#432131,#432132,#432133,#432134,#432135,#432136,#432137,#432138,
#432139,#432140,#432141),.UNSPECIFIED.,.F.,.F.,(4,3,3,3,3,3,3,3,3,3,3,4),
(0.,4.29157837303255E-6,5.42772623795373E-6,1.00901698482351E-5,1.31279195068643E-5,
1.57383542265874E-5,1.61011507492108E-5,1.67166789291762E-5,1.95343262811362E-5,
2.29377234674652E-5,2.71556047620063E-5,3.34407099942663E-5),
 .UNSPECIFIED.);
#26387=B_SPLINE_CURVE_WITH_KNOTS('',3,(#432154,#432155,#432156,#432157,
#432158,#432159,#432160,#432161,#432162,#432163,#432164,#432165,#432166,
#432167,#432168,#432169,#432170,#432171,#432172,#432173,#432174,#432175,
#432176,#432177,#432178,#432179,#432180,#432181,#432182,#432183,#432184,
#432185,#432186,#432187),.UNSPECIFIED.,.F.,.F.,(4,3,3,3,3,3,3,3,3,3,3,4),
(1.0842021724855E-19,3.71309426656634E-6,5.39981071559413E-6,8.78933289367088E-6,
9.00272357067501E-6,1.07143984504148E-5,1.60780299679518E-5,1.65806081157686E-5,
2.30369726850616E-5,2.67819200416086E-5,3.59736924187708E-5,4.03862783807001E-5),
 .UNSPECIFIED.);
#26388=B_SPLINE_CURVE_WITH_KNOTS('',3,(#432300,#432301,#432302,#432303),
 .UNSPECIFIED.,.F.,.F.,(4,4),(0.,7.70025630629239E-5),.UNSPECIFIED.);
#26389=B_SPLINE_CURVE_WITH_KNOTS('',3,(#432313,#432314,#432315,#432316),
 .UNSPECIFIED.,.F.,.F.,(4,4),(4.37055868292169E-19,7.70025630629237E-5),
 .UNSPECIFIED.);
#26390=B_SPLINE_CURVE_WITH_KNOTS('',3,(#432320,#432321,#432322,#432323,
#432324,#432325,#432326,#432327,#432328,#432329,#432330,#432331,#432332,
#432333,#432334,#432335,#432336,#432337,#432338,#432339,#432340,#432341,
#432342,#432343,#432344,#432345,#432346,#432347,#432348,#432349,#432350,
#432351,#432352,#432353,#432354,#432355,#432356),.UNSPECIFIED.,.F.,.F.,
(4,3,3,3,3,3,3,3,3,3,3,3,4),(0.,9.59031527200674E-6,1.94769411222978E-5,
2.02405092183151E-5,3.21374138577751E-5,3.60302195070439E-5,4.42640648818341E-5,
4.53660204229443E-5,5.03633762302115E-5,5.17708036292897E-5,5.37928993851989E-5,
5.54103755460201E-5,5.64557889514343E-5),.UNSPECIFIED.);
#26391=B_SPLINE_CURVE_WITH_KNOTS('',3,(#432357,#432358,#432359,#432360,
#432361,#432362,#432363,#432364,#432365,#432366,#432367,#432368,#432369,
#432370,#432371,#432372,#432373,#432374,#432375,#432376,#432377,#432378,
#432379,#432380,#432381,#432382,#432383,#432384),.UNSPECIFIED.,.F.,.F.,
(4,3,3,3,3,3,3,3,3,4),(5.64557889514343E-5,5.98940966493752E-5,6.34214003873381E-5,
7.22241476084827E-5,7.38322796533365E-5,8.36529189331353E-5,8.80714278222501E-5,
9.84837568500637E-5,0.00010862470407912,0.000110823272382854),
 .UNSPECIFIED.);
#26392=B_SPLINE_CURVE_WITH_KNOTS('',3,(#432400,#432401,#432402,#432403,
#432404,#432405,#432406,#432407,#432408,#432409,#432410,#432411,#432412,
#432413,#432414,#432415,#432416,#432417,#432418,#432419,#432420,#432421,
#432422,#432423,#432424,#432425,#432426,#432427),.UNSPECIFIED.,.F.,.F.,
(4,3,3,3,3,3,3,3,3,4),(0.,8.66039628582544E-6,1.64707715200667E-5,2.24502894132273E-5,
2.49975961757824E-5,2.88526003690281E-5,3.10661348995017E-5,3.43053543516961E-5,
3.66410545653561E-5,4.0050453762789E-5),.UNSPECIFIED.);
#26393=B_SPLINE_CURVE_WITH_KNOTS('',3,(#432430,#432431,#432432,#432433,
#432434,#432435,#432436),.UNSPECIFIED.,.F.,.F.,(4,3,4),(0.,4.40000041065379E-5,
9.89910850773112E-5),.UNSPECIFIED.);
#26394=B_SPLINE_CURVE_WITH_KNOTS('',3,(#432457,#432458,#432459,#432460,
#432461,#432462,#432463,#432464,#432465,#432466,#432467,#432468,#432469,
#432470,#432471,#432472,#432473,#432474,#432475,#432476,#432477,#432478,
#432479,#432480,#432481,#432482,#432483,#432484,#432485,#432486,#432487,
#432488,#432489,#432490),.UNSPECIFIED.,.F.,.F.,(4,3,3,3,3,3,3,3,3,3,3,4),
(0.,4.29157837302454E-6,5.4277262379536E-6,1.0090169848235E-5,1.31279195068642E-5,
1.57383542265848E-5,1.61011507492107E-5,1.6716678929176E-5,1.95343262811362E-5,
2.29377234674653E-5,2.71556047620063E-5,3.34407099942665E-5),
 .UNSPECIFIED.);
#26395=B_SPLINE_CURVE_WITH_KNOTS('',3,(#432503,#432504,#432505,#432506,
#432507,#432508,#432509,#432510,#432511,#432512,#432513,#432514,#432515,
#432516,#432517,#432518,#432519,#432520,#432521,#432522,#432523,#432524,
#432525,#432526,#432527,#432528,#432529,#432530,#432531,#432532,#432533,
#432534,#432535,#432536),.UNSPECIFIED.,.F.,.F.,(4,3,3,3,3,3,3,3,3,3,3,4),
(1.0842021724855E-19,3.71309426656643E-6,5.3998107155941E-6,8.78933289366509E-6,
9.00272357067505E-6,1.07143984504149E-5,1.60780299679579E-5,1.65806081157687E-5,
2.30369726850607E-5,2.67819200416085E-5,3.59736924187652E-5,4.03862783807E-5),
 .UNSPECIFIED.);
#26396=B_SPLINE_CURVE_WITH_KNOTS('',3,(#432649,#432650,#432651,#432652),
 .UNSPECIFIED.,.F.,.F.,(4,4),(0.,7.70025630629241E-5),.UNSPECIFIED.);
#26397=B_SPLINE_CURVE_WITH_KNOTS('',3,(#432662,#432663,#432664,#432665),
 .UNSPECIFIED.,.F.,.F.,(4,4),(4.41238316394827E-19,7.70025630629235E-5),
 .UNSPECIFIED.);
#26398=B_SPLINE_CURVE_WITH_KNOTS('',3,(#432669,#432670,#432671,#432672,
#432673,#432674,#432675,#432676,#432677,#432678,#432679,#432680,#432681,
#432682,#432683,#432684,#432685,#432686,#432687,#432688,#432689,#432690,
#432691,#432692,#432693,#432694,#432695,#432696,#432697,#432698,#432699,
#432700,#432701,#432702,#432703,#432704,#432705),.UNSPECIFIED.,.F.,.F.,
(4,3,3,3,3,3,3,3,3,3,3,3,4),(0.,9.59031527197544E-6,1.94769411222578E-5,
2.02405092183153E-5,3.21374138577708E-5,3.6030219507044E-5,4.42640648818711E-5,
4.53660204229444E-5,5.03633762302043E-5,5.17708036292896E-5,5.37928993851989E-5,
5.54103755460198E-5,5.64557889511408E-5),.UNSPECIFIED.);
#26399=B_SPLINE_CURVE_WITH_KNOTS('',3,(#432706,#432707,#432708,#432709,
#432710,#432711,#432712,#432713,#432714,#432715,#432716,#432717,#432718,
#432719,#432720,#432721,#432722,#432723,#432724,#432725,#432726,#432727,
#432728,#432729,#432730,#432731,#432732,#432733),.UNSPECIFIED.,.F.,.F.,
(4,3,3,3,3,3,3,3,3,4),(5.64557889511408E-5,5.98940966493751E-5,6.3421400387338E-5,
7.22241476085115E-5,7.38322796533365E-5,8.36529189331405E-5,8.807142782225E-5,
9.84837568500711E-5,0.00010862470407914,0.000110823272382853),
 .UNSPECIFIED.);
#26400=B_SPLINE_CURVE_WITH_KNOTS('',3,(#432749,#432750,#432751,#432752,
#432753,#432754,#432755,#432756,#432757,#432758,#432759,#432760,#432761,
#432762,#432763,#432764,#432765,#432766,#432767,#432768,#432769,#432770,
#432771,#432772,#432773,#432774,#432775,#432776),.UNSPECIFIED.,.F.,.F.,
(4,3,3,3,3,3,3,3,3,4),(0.,8.66039628581856E-6,1.64707715200667E-5,2.24502894132393E-5,
2.49975961757824E-5,2.88526003690281E-5,3.10661348995016E-5,3.43053543516961E-5,
3.6641054565356E-5,4.0050453762789E-5),.UNSPECIFIED.);
#26401=B_SPLINE_CURVE_WITH_KNOTS('',3,(#432779,#432780,#432781,#432782,
#432783,#432784,#432785),.UNSPECIFIED.,.F.,.F.,(4,3,4),(0.,4.40000041065371E-5,
9.89910850773111E-5),.UNSPECIFIED.);
#26402=B_SPLINE_CURVE_WITH_KNOTS('',3,(#432806,#432807,#432808,#432809,
#432810,#432811,#432812,#432813,#432814,#432815,#432816,#432817,#432818,
#432819,#432820,#432821,#432822,#432823,#432824,#432825,#432826,#432827,
#432828,#432829,#432830,#432831,#432832,#432833,#432834,#432835,#432836,
#432837,#432838,#432839),.UNSPECIFIED.,.F.,.F.,(4,3,3,3,3,3,3,3,3,3,3,4),
(0.,4.29157837305563E-6,5.4277262379533E-6,1.00901698482349E-5,1.3127919506864E-5,
1.57383542265875E-5,1.61011507492106E-5,1.67166789291755E-5,1.9534326281136E-5,
2.29377234674649E-5,2.7155604762006E-5,3.34407099942659E-5),
 .UNSPECIFIED.);
#26403=B_SPLINE_CURVE_WITH_KNOTS('',3,(#432852,#432853,#432854,#432855,
#432856,#432857,#432858,#432859,#432860,#432861,#432862,#432863,#432864,
#432865,#432866,#432867,#432868,#432869,#432870,#432871,#432872,#432873,
#432874,#432875,#432876,#432877,#432878,#432879,#432880,#432881,#432882,
#432883,#432884,#432885),.UNSPECIFIED.,.F.,.F.,(4,3,3,3,3,3,3,3,3,3,3,4),
(1.0842021724855E-19,3.71309426656642E-6,5.39981071559414E-6,8.78933289363548E-6,
9.00272357067524E-6,1.0714398450415E-5,1.60780299679622E-5,1.65806081157688E-5,
2.30369726850369E-5,2.67819200416088E-5,3.59736924187517E-5,4.03862783807003E-5),
 .UNSPECIFIED.);
#26404=B_SPLINE_CURVE_WITH_KNOTS('',3,(#432998,#432999,#433000,#433001),
 .UNSPECIFIED.,.F.,.F.,(4,4),(0.,7.70025630629241E-5),.UNSPECIFIED.);
#26405=B_SPLINE_CURVE_WITH_KNOTS('',3,(#433011,#433012,#433013,#433014),
 .UNSPECIFIED.,.F.,.F.,(4,4),(4.42537225052217E-19,7.70025630629237E-5),
 .UNSPECIFIED.);
#26406=B_SPLINE_CURVE_WITH_KNOTS('',3,(#433018,#433019,#433020,#433021,
#433022,#433023,#433024,#433025,#433026,#433027,#433028,#433029,#433030,
#433031,#433032,#433033,#433034,#433035,#433036,#433037,#433038,#433039,
#433040,#433041,#433042,#433043,#433044,#433045,#433046,#433047,#433048,
#433049,#433050,#433051,#433052,#433053,#433054),.UNSPECIFIED.,.F.,.F.,
(4,3,3,3,3,3,3,3,3,3,3,3,4),(0.,9.59031527200432E-6,1.94769411222929E-5,
2.02405092183153E-5,3.21374138577673E-5,3.6030219507044E-5,4.42640648819217E-5,
4.53660204229445E-5,5.0363376230212E-5,5.17708036292897E-5,5.3792899385199E-5,
5.541037554602E-5,5.64557889509114E-5),.UNSPECIFIED.);
#26407=B_SPLINE_CURVE_WITH_KNOTS('',3,(#433055,#433056,#433057,#433058,
#433059,#433060,#433061,#433062,#433063,#433064,#433065,#433066,#433067,
#433068,#433069,#433070,#433071,#433072,#433073,#433074,#433075,#433076,
#433077,#433078,#433079,#433080,#433081,#433082),.UNSPECIFIED.,.F.,.F.,
(4,3,3,3,3,3,3,3,3,4),(5.64557889509114E-5,5.98940966493752E-5,6.34214003873381E-5,
7.22241476084362E-5,7.38322796533365E-5,8.36529189331371E-5,8.80714278222501E-5,
9.84837568500736E-5,0.000108624704079148,0.000110823272382854),
 .UNSPECIFIED.);
#26408=B_SPLINE_CURVE_WITH_KNOTS('',3,(#433098,#433099,#433100,#433101,
#433102,#433103,#433104,#433105,#433106,#433107,#433108,#433109,#433110,
#433111,#433112,#433113,#433114,#433115,#433116,#433117,#433118,#433119,
#433120,#433121,#433122,#433123,#433124,#433125),.UNSPECIFIED.,.F.,.F.,
(4,3,3,3,3,3,3,3,3,4),(0.,8.66039628583388E-6,1.64707715200667E-5,2.24502894132186E-5,
2.49975961757824E-5,2.88526003690281E-5,3.10661348995016E-5,3.4305354351696E-5,
3.6641054565356E-5,4.00504537627888E-5),.UNSPECIFIED.);
#26409=B_SPLINE_CURVE_WITH_KNOTS('',3,(#433128,#433129,#433130,#433131,
#433132,#433133,#433134),.UNSPECIFIED.,.F.,.F.,(4,3,4),(0.,4.40000041065376E-5,
9.89910850773113E-5),.UNSPECIFIED.);
#26410=B_SPLINE_CURVE_WITH_KNOTS('',3,(#433155,#433156,#433157,#433158,
#433159,#433160,#433161,#433162,#433163,#433164,#433165,#433166,#433167,
#433168,#433169,#433170,#433171,#433172,#433173,#433174,#433175,#433176,
#433177,#433178,#433179,#433180,#433181,#433182,#433183,#433184,#433185,
#433186,#433187,#433188),.UNSPECIFIED.,.F.,.F.,(4,3,3,3,3,3,3,3,3,3,3,4),
(0.,4.2915783730512E-6,5.42772623795345E-6,1.00901698482349E-5,1.31279195068639E-5,
1.57383542265821E-5,1.61011507492105E-5,1.67166789291757E-5,1.9534326281136E-5,
2.2937723467465E-5,2.71556047620059E-5,3.3440709994266E-5),
 .UNSPECIFIED.);
#26411=B_SPLINE_CURVE_WITH_KNOTS('',3,(#433201,#433202,#433203,#433204,
#433205,#433206,#433207,#433208,#433209,#433210,#433211,#433212,#433213,
#433214,#433215,#433216,#433217,#433218,#433219,#433220,#433221,#433222,
#433223,#433224,#433225,#433226,#433227,#433228,#433229,#433230,#433231,
#433232,#433233,#433234),.UNSPECIFIED.,.F.,.F.,(4,3,3,3,3,3,3,3,3,3,3,4),
(9.48676900924816E-20,3.71309426656646E-6,5.39981071559417E-6,8.78933289365053E-6,
9.00272357067522E-6,1.07143984504149E-5,1.60780299679672E-5,1.65806081157687E-5,
2.30369726850437E-5,2.67819200416084E-5,3.59736924187517E-5,4.03862783806997E-5),
 .UNSPECIFIED.);
#26412=B_SPLINE_CURVE_WITH_KNOTS('',3,(#433347,#433348,#433349,#433350),
 .UNSPECIFIED.,.F.,.F.,(4,4),(0.,7.70025630629241E-5),.UNSPECIFIED.);
#26413=B_SPLINE_CURVE_WITH_KNOTS('',3,(#433360,#433361,#433362,#433363),
 .UNSPECIFIED.,.F.,.F.,(4,4),(4.47028007668187E-19,7.70025630629238E-5),
 .UNSPECIFIED.);
#26414=B_SPLINE_CURVE_WITH_KNOTS('',3,(#433367,#433368,#433369,#433370,
#433371,#433372,#433373,#433374,#433375,#433376,#433377,#433378,#433379,
#433380,#433381,#433382,#433383,#433384,#433385,#433386,#433387,#433388,
#433389,#433390,#433391,#433392,#433393,#433394,#433395,#433396,#433397,
#433398,#433399,#433400,#433401,#433402,#433403),.UNSPECIFIED.,.F.,.F.,
(4,3,3,3,3,3,3,3,3,3,3,3,4),(0.,9.59031527200568E-6,1.94769411222974E-5,
2.02405092183153E-5,3.21374138577626E-5,3.60302195070439E-5,4.42640648818366E-5,
4.53660204229444E-5,5.03633762302246E-5,5.17708036292896E-5,5.37928993851989E-5,
5.54103755460199E-5,5.64557889511924E-5),.UNSPECIFIED.);
#26415=B_SPLINE_CURVE_WITH_KNOTS('',3,(#433404,#433405,#433406,#433407,
#433408,#433409,#433410,#433411,#433412,#433413,#433414,#433415,#433416,
#433417,#433418,#433419,#433420,#433421,#433422,#433423,#433424,#433425,
#433426,#433427,#433428,#433429,#433430,#433431),.UNSPECIFIED.,.F.,.F.,
(4,3,3,3,3,3,3,3,3,4),(5.64557889511924E-5,5.98940966493751E-5,6.34214003873381E-5,
7.22241476084559E-5,7.38322796533365E-5,8.36529189331304E-5,8.80714278222502E-5,
9.84837568500671E-5,0.000108624704079125,0.000110823272382854),
 .UNSPECIFIED.);
#26416=B_SPLINE_CURVE_WITH_KNOTS('',3,(#433447,#433448,#433449,#433450,
#433451,#433452,#433453,#433454,#433455,#433456,#433457,#433458,#433459,
#433460,#433461,#433462,#433463,#433464,#433465,#433466,#433467,#433468,
#433469,#433470,#433471,#433472,#433473,#433474),.UNSPECIFIED.,.F.,.F.,
(4,3,3,3,3,3,3,3,3,4),(0.,8.66039628579021E-6,1.64707715200667E-5,2.2450289413231E-5,
2.49975961757823E-5,2.8852600369028E-5,3.10661348995015E-5,3.4305354351696E-5,
3.66410545653559E-5,4.00504537627887E-5),.UNSPECIFIED.);
#26417=B_SPLINE_CURVE_WITH_KNOTS('',3,(#433477,#433478,#433479,#433480,
#433481,#433482,#433483),.UNSPECIFIED.,.F.,.F.,(4,3,4),(0.,4.40000041065377E-5,
9.89910850773116E-5),.UNSPECIFIED.);
#26418=B_SPLINE_CURVE_WITH_KNOTS('',3,(#433504,#433505,#433506,#433507,
#433508,#433509,#433510,#433511,#433512,#433513,#433514,#433515,#433516,
#433517,#433518,#433519,#433520,#433521,#433522,#433523,#433524,#433525,
#433526,#433527,#433528,#433529,#433530,#433531,#433532,#433533,#433534,
#433535,#433536,#433537),.UNSPECIFIED.,.F.,.F.,(4,3,3,3,3,3,3,3,3,3,3,4),
(0.,4.29157837303811E-6,5.42772623795339E-6,1.00901698482347E-5,1.31279195068639E-5,
1.57383542265873E-5,1.61011507492103E-5,1.67166789291758E-5,1.95343262811359E-5,
2.29377234674646E-5,2.71556047620056E-5,3.34407099942658E-5),
 .UNSPECIFIED.);
#26419=B_SPLINE_CURVE_WITH_KNOTS('',3,(#433550,#433551,#433552,#433553,
#433554,#433555,#433556,#433557,#433558,#433559,#433560,#433561,#433562,
#433563,#433564,#433565,#433566,#433567,#433568,#433569,#433570,#433571,
#433572,#433573,#433574,#433575,#433576,#433577,#433578,#433579,#433580,
#433581,#433582,#433583),.UNSPECIFIED.,.F.,.F.,(4,3,3,3,3,3,3,3,3,3,3,4),
(8.13151629364128E-20,3.71309426656637E-6,5.3998107155941E-6,8.78933289331537E-6,
9.00272357067515E-6,1.07143984504149E-5,1.60780299679551E-5,1.65806081157687E-5,
2.30369726850453E-5,2.67819200416086E-5,3.59736924188064E-5,4.03862783807001E-5),
 .UNSPECIFIED.);
#26420=B_SPLINE_CURVE_WITH_KNOTS('',3,(#433696,#433697,#433698,#433699),
 .UNSPECIFIED.,.F.,.F.,(4,4),(0.,7.7002563062924E-5),.UNSPECIFIED.);
#26421=B_SPLINE_CURVE_WITH_KNOTS('',3,(#433709,#433710,#433711,#433712),
 .UNSPECIFIED.,.F.,.F.,(4,4),(4.47028007668187E-19,7.70025630629235E-5),
 .UNSPECIFIED.);
#26422=B_SPLINE_CURVE_WITH_KNOTS('',3,(#433716,#433717,#433718,#433719,
#433720,#433721,#433722,#433723,#433724,#433725,#433726,#433727,#433728,
#433729,#433730,#433731,#433732,#433733,#433734,#433735,#433736,#433737,
#433738,#433739,#433740,#433741,#433742,#433743,#433744,#433745,#433746,
#433747,#433748,#433749,#433750,#433751,#433752),.UNSPECIFIED.,.F.,.F.,
(4,3,3,3,3,3,3,3,3,3,3,3,4),(0.,9.59031527200619E-6,1.94769411222942E-5,
2.02405092183152E-5,3.21374138577641E-5,3.60302195070439E-5,4.4264064881794E-5,
4.53660204229443E-5,5.03633762302236E-5,5.17708036292896E-5,5.37928993851988E-5,
5.54103755460197E-5,5.64557889511151E-5),.UNSPECIFIED.);
#26423=B_SPLINE_CURVE_WITH_KNOTS('',3,(#433753,#433754,#433755,#433756,
#433757,#433758,#433759,#433760,#433761,#433762,#433763,#433764,#433765,
#433766,#433767,#433768,#433769,#433770,#433771,#433772,#433773,#433774,
#433775,#433776,#433777,#433778,#433779,#433780),.UNSPECIFIED.,.F.,.F.,
(4,3,3,3,3,3,3,3,3,4),(5.64557889511151E-5,5.9894096649375E-5,6.3421400387338E-5,
7.22241476084724E-5,7.38322796533362E-5,8.36529189331358E-5,8.80714278222499E-5,
9.84837568500631E-5,0.000108624704079119,0.000110823272382853),
 .UNSPECIFIED.);
#26424=B_SPLINE_CURVE_WITH_KNOTS('',3,(#433796,#433797,#433798,#433799,
#433800,#433801,#433802,#433803,#433804,#433805,#433806,#433807,#433808,
#433809,#433810,#433811,#433812,#433813,#433814,#433815,#433816,#433817,
#433818,#433819,#433820,#433821,#433822,#433823),.UNSPECIFIED.,.F.,.F.,
(4,3,3,3,3,3,3,3,3,4),(0.,8.66039628580801E-6,1.64707715200666E-5,2.24502894132537E-5,
2.49975961757824E-5,2.88526003690281E-5,3.10661348995017E-5,3.4305354351696E-5,
3.66410545653559E-5,4.00504537627886E-5),.UNSPECIFIED.);
#26425=B_SPLINE_CURVE_WITH_KNOTS('',3,(#433826,#433827,#433828,#433829,
#433830,#433831,#433832),.UNSPECIFIED.,.F.,.F.,(4,3,4),(0.,4.40000041065374E-5,
9.89910850773113E-5),.UNSPECIFIED.);
#26426=B_SPLINE_CURVE_WITH_KNOTS('',3,(#433853,#433854,#433855,#433856,
#433857,#433858,#433859,#433860,#433861,#433862,#433863,#433864,#433865,
#433866,#433867,#433868,#433869,#433870,#433871,#433872,#433873,#433874,
#433875,#433876,#433877,#433878,#433879,#433880,#433881,#433882,#433883,
#433884,#433885,#433886),.UNSPECIFIED.,.F.,.F.,(4,3,3,3,3,3,3,3,3,3,3,4),
(0.,4.29157837303002E-6,5.42772623795338E-6,1.00901698482348E-5,1.3127919506864E-5,
1.57383542265799E-5,1.61011507492105E-5,1.67166789291756E-5,1.95343262811359E-5,
2.29377234674648E-5,2.71556047620057E-5,3.34407099942657E-5),
 .UNSPECIFIED.);
#26427=B_SPLINE_CURVE_WITH_KNOTS('',3,(#433899,#433900,#433901,#433902,
#433903,#433904,#433905,#433906,#433907,#433908,#433909,#433910,#433911,
#433912,#433913,#433914,#433915,#433916,#433917,#433918,#433919,#433920,
#433921,#433922,#433923,#433924,#433925,#433926,#433927,#433928,#433929,
#433930,#433931,#433932),.UNSPECIFIED.,.F.,.F.,(4,3,3,3,3,3,3,3,3,3,3,4),
(1.0842021724855E-19,3.71309426656652E-6,5.39981071559414E-6,8.7893328936642E-6,
9.00272357067527E-6,1.0714398450415E-5,1.60780299679545E-5,1.65806081157689E-5,
2.30369726850333E-5,2.67819200416089E-5,3.59736924188076E-5,4.03862783807005E-5),
 .UNSPECIFIED.);
#26428=B_SPLINE_CURVE_WITH_KNOTS('',3,(#434045,#434046,#434047,#434048),
 .UNSPECIFIED.,.F.,.F.,(4,4),(0.,7.70025630629239E-5),.UNSPECIFIED.);
#26429=B_SPLINE_CURVE_WITH_KNOTS('',3,(#434058,#434059,#434060,#434061),
 .UNSPECIFIED.,.F.,.F.,(4,4),(1.0842021724855E-19,7.70025630629237E-5),
 .UNSPECIFIED.);
#26430=B_SPLINE_CURVE_WITH_KNOTS('',3,(#434065,#434066,#434067,#434068,
#434069,#434070,#434071,#434072,#434073,#434074,#434075,#434076,#434077,
#434078,#434079,#434080,#434081,#434082,#434083,#434084,#434085,#434086,
#434087,#434088,#434089,#434090,#434091,#434092,#434093,#434094,#434095,
#434096,#434097,#434098,#434099,#434100,#434101),.UNSPECIFIED.,.F.,.F.,
(4,3,3,3,3,3,3,3,3,3,3,3,4),(0.,9.59031527200469E-6,1.94769411222819E-5,
2.02405092183153E-5,3.21374138577713E-5,3.60302195070438E-5,4.42640648818814E-5,
4.53660204229444E-5,5.03633762302024E-5,5.17708036292895E-5,5.37928993851988E-5,
5.54103755460199E-5,5.64557889509706E-5),.UNSPECIFIED.);
#26431=B_SPLINE_CURVE_WITH_KNOTS('',3,(#434102,#434103,#434104,#434105,
#434106,#434107,#434108,#434109,#434110,#434111,#434112,#434113,#434114,
#434115,#434116,#434117,#434118,#434119,#434120,#434121,#434122,#434123,
#434124,#434125,#434126,#434127,#434128,#434129),.UNSPECIFIED.,.F.,.F.,
(4,3,3,3,3,3,3,3,3,4),(5.64557889509706E-5,5.9894096649375E-5,6.34214003873379E-5,
7.222414760851E-5,7.38322796533364E-5,8.36529189331486E-5,8.80714278222499E-5,
9.84837568501126E-5,0.000108624704079219,0.000110823272382853),
 .UNSPECIFIED.);
#26432=B_SPLINE_CURVE_WITH_KNOTS('',3,(#434145,#434146,#434147,#434148,
#434149,#434150,#434151,#434152,#434153,#434154,#434155,#434156,#434157,
#434158,#434159,#434160,#434161,#434162,#434163,#434164,#434165,#434166,
#434167,#434168,#434169,#434170,#434171,#434172),.UNSPECIFIED.,.F.,.F.,
(4,3,3,3,3,3,3,3,3,4),(0.,8.6603962858081E-6,1.64707715200666E-5,2.24502894132384E-5,
2.49975961757823E-5,2.8852600369028E-5,3.10661348995015E-5,3.4305354351696E-5,
3.66410545653559E-5,4.00504537627885E-5),.UNSPECIFIED.);
#26433=B_SPLINE_CURVE_WITH_KNOTS('',3,(#434175,#434176,#434177,#434178,
#434179,#434180,#434181),.UNSPECIFIED.,.F.,.F.,(4,3,4),(0.,4.40000041065376E-5,
9.89910850773114E-5),.UNSPECIFIED.);
#26434=B_SPLINE_CURVE_WITH_KNOTS('',3,(#434202,#434203,#434204,#434205,
#434206,#434207,#434208,#434209,#434210,#434211,#434212,#434213,#434214,
#434215,#434216,#434217,#434218,#434219,#434220,#434221,#434222,#434223,
#434224,#434225,#434226,#434227,#434228,#434229,#434230,#434231,#434232,
#434233,#434234,#434235),.UNSPECIFIED.,.F.,.F.,(4,3,3,3,3,3,3,3,3,3,3,4),
(0.,4.29157837305019E-6,5.4277262379532E-6,1.00901698482347E-5,1.31279195068639E-5,
1.57383542265796E-5,1.61011507492104E-5,1.67166789291757E-5,1.95343262811361E-5,
2.2937723467465E-5,2.7155604762006E-5,3.34407099942661E-5),
 .UNSPECIFIED.);
#26435=B_SPLINE_CURVE_WITH_KNOTS('',3,(#434248,#434249,#434250,#434251,
#434252,#434253,#434254,#434255,#434256,#434257,#434258,#434259,#434260,
#434261,#434262,#434263,#434264,#434265,#434266,#434267,#434268,#434269,
#434270,#434271,#434272,#434273,#434274,#434275,#434276,#434277,#434278,
#434279,#434280,#434281),.UNSPECIFIED.,.F.,.F.,(4,3,3,3,3,3,3,3,3,3,3,4),
(1.0842021724855E-19,3.71309426656629E-6,5.3998107155941E-6,8.78933289329952E-6,
9.00272357067513E-6,1.07143984504149E-5,1.6078029967954E-5,1.65806081157686E-5,
2.30369726850589E-5,2.67819200416085E-5,3.59736924188033E-5,4.03862783807E-5),
 .UNSPECIFIED.);
#26436=B_SPLINE_CURVE_WITH_KNOTS('',3,(#434394,#434395,#434396,#434397),
 .UNSPECIFIED.,.F.,.F.,(4,4),(0.,7.70025630629243E-5),.UNSPECIFIED.);
#26437=B_SPLINE_CURVE_WITH_KNOTS('',3,(#434407,#434408,#434409,#434410),
 .UNSPECIFIED.,.F.,.F.,(4,4),(2.16840434497101E-19,7.70025630629238E-5),
 .UNSPECIFIED.);
#26438=B_SPLINE_CURVE_WITH_KNOTS('',3,(#434414,#434415,#434416,#434417,
#434418,#434419,#434420,#434421,#434422,#434423,#434424,#434425,#434426,
#434427,#434428,#434429,#434430,#434431,#434432,#434433,#434434,#434435,
#434436,#434437,#434438,#434439,#434440,#434441,#434442,#434443,#434444,
#434445,#434446,#434447,#434448,#434449,#434450),.UNSPECIFIED.,.F.,.F.,
(4,3,3,3,3,3,3,3,3,3,3,3,4),(0.,9.59031527197168E-6,1.94769411222557E-5,
2.02405092183152E-5,3.21374138577623E-5,3.60302195070439E-5,4.42640648819179E-5,
4.53660204229443E-5,5.03633762301952E-5,5.17708036292895E-5,5.37928993851988E-5,
5.54103755460205E-5,5.64557889511527E-5),.UNSPECIFIED.);
#26439=B_SPLINE_CURVE_WITH_KNOTS('',3,(#434451,#434452,#434453,#434454,
#434455,#434456,#434457,#434458,#434459,#434460,#434461,#434462,#434463,
#434464,#434465,#434466,#434467,#434468,#434469,#434470,#434471,#434472,
#434473,#434474,#434475,#434476,#434477,#434478),.UNSPECIFIED.,.F.,.F.,
(4,3,3,3,3,3,3,3,3,4),(5.64557889511527E-5,5.98940966493751E-5,6.3421400387338E-5,
7.22241476084597E-5,7.38322796533364E-5,8.36529189331495E-5,8.807142782225E-5,
9.84837568501151E-5,0.000108624704079247,0.000110823272382854),
 .UNSPECIFIED.);
#26440=B_SPLINE_CURVE_WITH_KNOTS('',3,(#434494,#434495,#434496,#434497,
#434498,#434499,#434500,#434501,#434502,#434503,#434504,#434505,#434506,
#434507,#434508,#434509,#434510,#434511,#434512,#434513,#434514,#434515,
#434516,#434517,#434518,#434519,#434520,#434521),.UNSPECIFIED.,.F.,.F.,
(4,3,3,3,3,3,3,3,3,4),(0.,8.6603962858347E-6,1.64707715200667E-5,2.2450289413261E-5,
2.49975961757823E-5,2.88526003690281E-5,3.10661348995018E-5,3.43053543516962E-5,
3.66410545653562E-5,4.00504537627892E-5),.UNSPECIFIED.);
#26441=B_SPLINE_CURVE_WITH_KNOTS('',3,(#434524,#434525,#434526,#434527,
#434528,#434529,#434530),.UNSPECIFIED.,.F.,.F.,(4,3,4),(0.,4.40000041065378E-5,
9.89910850773116E-5),.UNSPECIFIED.);
#26442=B_SPLINE_CURVE_WITH_KNOTS('',3,(#434551,#434552,#434553,#434554,
#434555,#434556,#434557,#434558,#434559,#434560,#434561,#434562,#434563,
#434564,#434565,#434566,#434567,#434568,#434569,#434570,#434571,#434572,
#434573,#434574,#434575,#434576,#434577,#434578,#434579,#434580,#434581,
#434582,#434583,#434584),.UNSPECIFIED.,.F.,.F.,(4,3,3,3,3,3,3,3,3,3,3,4),
(0.,4.29157837303538E-6,5.42772623795322E-6,1.00901698482348E-5,1.31279195068638E-5,
1.57383542265853E-5,1.61011507492106E-5,1.67166789291757E-5,1.95343262811361E-5,
2.2937723467465E-5,2.7155604762006E-5,3.3440709994266E-5),.UNSPECIFIED.);
#26443=B_SPLINE_CURVE_WITH_KNOTS('',3,(#434597,#434598,#434599,#434600,
#434601,#434602,#434603,#434604,#434605,#434606,#434607,#434608,#434609,
#434610,#434611,#434612,#434613,#434614,#434615,#434616,#434617,#434618,
#434619,#434620,#434621,#434622,#434623,#434624,#434625,#434626,#434627,
#434628,#434629,#434630),.UNSPECIFIED.,.F.,.F.,(4,3,3,3,3,3,3,3,3,3,3,4),
(2.16840434497101E-19,3.71309426656641E-6,5.39981071559398E-6,8.78933289365255E-6,
9.002723570675E-6,1.07143984504147E-5,1.60780299679668E-5,1.65806081157686E-5,
2.30369726850311E-5,2.67819200416086E-5,3.59736924187738E-5,4.03862783807001E-5),
 .UNSPECIFIED.);
#26444=B_SPLINE_CURVE_WITH_KNOTS('',3,(#434743,#434744,#434745,#434746),
 .UNSPECIFIED.,.F.,.F.,(4,4),(0.,7.70025630629239E-5),.UNSPECIFIED.);
#26445=B_SPLINE_CURVE_WITH_KNOTS('',3,(#434756,#434757,#434758,#434759),
 .UNSPECIFIED.,.F.,.F.,(4,4),(2.16840434497101E-19,7.7002563062924E-5),
 .UNSPECIFIED.);
#26446=B_SPLINE_CURVE_WITH_KNOTS('',3,(#434763,#434764,#434765,#434766,
#434767,#434768,#434769,#434770,#434771,#434772,#434773,#434774,#434775,
#434776,#434777,#434778,#434779,#434780,#434781,#434782,#434783,#434784,
#434785,#434786,#434787,#434788,#434789,#434790,#434791,#434792,#434793,
#434794,#434795,#434796,#434797,#434798,#434799),.UNSPECIFIED.,.F.,.F.,
(4,3,3,3,3,3,3,3,3,3,3,3,4),(0.,9.59031527200526E-6,1.94769411222901E-5,
2.02405092183153E-5,3.21374138577741E-5,3.60302195070439E-5,4.42640648818246E-5,
4.53660204229444E-5,5.03633762301999E-5,5.17708036292895E-5,5.37928993851987E-5,
5.54103755460196E-5,5.64557889512458E-5),.UNSPECIFIED.);
#26447=B_SPLINE_CURVE_WITH_KNOTS('',3,(#434800,#434801,#434802,#434803,
#434804,#434805,#434806,#434807,#434808,#434809,#434810,#434811,#434812,
#434813,#434814,#434815,#434816,#434817,#434818,#434819,#434820,#434821,
#434822,#434823,#434824,#434825,#434826,#434827),.UNSPECIFIED.,.F.,.F.,
(4,3,3,3,3,3,3,3,3,4),(5.64557889512458E-5,5.98940966493751E-5,6.34214003873378E-5,
7.22241476084449E-5,7.38322796533364E-5,8.36529189331453E-5,8.80714278222498E-5,
9.84837568500673E-5,0.000108624704079133,0.000110823272382853),
 .UNSPECIFIED.);
#26448=B_SPLINE_CURVE_WITH_KNOTS('',3,(#434843,#434844,#434845,#434846,
#434847,#434848,#434849,#434850,#434851,#434852,#434853,#434854,#434855,
#434856,#434857,#434858,#434859,#434860,#434861,#434862,#434863,#434864,
#434865,#434866,#434867,#434868,#434869,#434870),.UNSPECIFIED.,.F.,.F.,
(4,3,3,3,3,3,3,3,3,4),(0.,8.66039628585016E-6,1.64707715200665E-5,2.24502894132343E-5,
2.49975961757822E-5,2.88526003690281E-5,3.10661348995015E-5,3.4305354351696E-5,
3.66410545653557E-5,4.00504537627886E-5),.UNSPECIFIED.);
#26449=B_SPLINE_CURVE_WITH_KNOTS('',3,(#434873,#434874,#434875,#434876,
#434877,#434878,#434879),.UNSPECIFIED.,.F.,.F.,(4,3,4),(0.,4.40000041065375E-5,
9.89910850773113E-5),.UNSPECIFIED.);
#26450=B_SPLINE_CURVE_WITH_KNOTS('',3,(#434900,#434901,#434902,#434903,
#434904,#434905,#434906,#434907,#434908,#434909,#434910,#434911,#434912,
#434913,#434914,#434915,#434916,#434917,#434918,#434919,#434920,#434921,
#434922,#434923,#434924,#434925,#434926,#434927,#434928,#434929,#434930,
#434931,#434932,#434933),.UNSPECIFIED.,.F.,.F.,(4,3,3,3,3,3,3,3,3,3,3,4),
(0.,4.29157837302687E-6,5.42772623795313E-6,1.00901698482347E-5,1.31279195068639E-5,
1.57383542265806E-5,1.61011507492103E-5,1.6716678929175E-5,1.95343262811356E-5,
2.29377234674646E-5,2.71556047620055E-5,3.34407099942656E-5),
 .UNSPECIFIED.);
#26451=B_SPLINE_CURVE_WITH_KNOTS('',3,(#434946,#434947,#434948,#434949,
#434950,#434951,#434952,#434953,#434954,#434955,#434956,#434957,#434958,
#434959,#434960,#434961,#434962,#434963,#434964,#434965,#434966,#434967,
#434968,#434969,#434970,#434971,#434972,#434973,#434974,#434975,#434976,
#434977,#434978,#434979),.UNSPECIFIED.,.F.,.F.,(4,3,3,3,3,3,3,3,3,3,3,4),
(0.,3.71309426656649E-6,5.3998107155942E-6,8.78933289370609E-6,9.00272357067532E-6,
1.07143984504151E-5,1.60780299679492E-5,1.6580608115769E-5,2.3036972685064E-5,
2.6781920041609E-5,3.59736924188123E-5,4.03862783807007E-5),
 .UNSPECIFIED.);
#26452=B_SPLINE_CURVE_WITH_KNOTS('',3,(#435092,#435093,#435094,#435095),
 .UNSPECIFIED.,.F.,.F.,(4,4),(0.,7.7002563062924E-5),.UNSPECIFIED.);
#26453=B_SPLINE_CURVE_WITH_KNOTS('',3,(#435105,#435106,#435107,#435108),
 .UNSPECIFIED.,.F.,.F.,(4,4),(2.16840434497101E-19,7.70025630629234E-5),
 .UNSPECIFIED.);
#26454=B_SPLINE_CURVE_WITH_KNOTS('',3,(#435112,#435113,#435114,#435115,
#435116,#435117,#435118,#435119,#435120,#435121,#435122,#435123,#435124,
#435125,#435126,#435127,#435128,#435129,#435130,#435131,#435132,#435133,
#435134,#435135,#435136,#435137,#435138,#435139,#435140,#435141,#435142,
#435143,#435144,#435145,#435146,#435147,#435148),.UNSPECIFIED.,.F.,.F.,
(4,3,3,3,3,3,3,3,3,3,3,3,4),(0.,9.59031527199155E-6,1.94769411222748E-5,
2.02405092183152E-5,3.21374138577728E-5,3.60302195070438E-5,4.42640648818854E-5,
4.53660204229444E-5,5.036337623021E-5,5.17708036292895E-5,5.37928993851989E-5,
5.54103755460202E-5,5.64557889511684E-5),.UNSPECIFIED.);
#26455=B_SPLINE_CURVE_WITH_KNOTS('',3,(#435149,#435150,#435151,#435152,
#435153,#435154,#435155,#435156,#435157,#435158,#435159,#435160,#435161,
#435162,#435163,#435164,#435165,#435166,#435167,#435168,#435169,#435170,
#435171,#435172,#435173,#435174,#435175,#435176),.UNSPECIFIED.,.F.,.F.,
(4,3,3,3,3,3,3,3,3,4),(5.64557889511684E-5,5.9894096649375E-5,6.34214003873381E-5,
7.22241476084239E-5,7.38322796533365E-5,8.36529189331425E-5,8.807142782225E-5,
9.84837568500588E-5,0.000108624704079108,0.000110823272382854),
 .UNSPECIFIED.);
#26456=B_SPLINE_CURVE_WITH_KNOTS('',3,(#435192,#435193,#435194,#435195,
#435196,#435197,#435198,#435199,#435200,#435201,#435202,#435203,#435204,
#435205,#435206,#435207,#435208,#435209,#435210,#435211,#435212,#435213,
#435214,#435215,#435216,#435217,#435218,#435219),.UNSPECIFIED.,.F.,.F.,
(4,3,3,3,3,3,3,3,3,4),(0.,8.66039628582568E-6,1.6470771520067E-5,2.24502894132484E-5,
2.4997596175783E-5,2.88526003690286E-5,3.10661348995021E-5,3.43053543516964E-5,
3.66410545653567E-5,4.00504537627889E-5),.UNSPECIFIED.);
#26457=B_SPLINE_CURVE_WITH_KNOTS('',3,(#435222,#435223,#435224,#435225,
#435226,#435227,#435228),.UNSPECIFIED.,.F.,.F.,(4,3,4),(0.,4.40000041065377E-5,
9.89910850773115E-5),.UNSPECIFIED.);
#26458=B_SPLINE_CURVE_WITH_KNOTS('',3,(#435249,#435250,#435251,#435252,
#435253,#435254,#435255,#435256,#435257,#435258,#435259,#435260,#435261,
#435262,#435263,#435264,#435265,#435266,#435267,#435268,#435269,#435270,
#435271,#435272,#435273,#435274,#435275,#435276,#435277,#435278,#435279,
#435280,#435281,#435282),.UNSPECIFIED.,.F.,.F.,(4,3,3,3,3,3,3,3,3,3,3,4),
(0.,4.2915783730306E-6,5.42772623795349E-6,1.00901698482348E-5,1.31279195068639E-5,
1.57383542265897E-5,1.61011507492107E-5,1.6716678929176E-5,1.95343262811361E-5,
2.29377234674652E-5,2.71556047620063E-5,3.34407099942664E-5),
 .UNSPECIFIED.);
#26459=B_SPLINE_CURVE_WITH_KNOTS('',3,(#435295,#435296,#435297,#435298,
#435299,#435300,#435301,#435302,#435303,#435304,#435305,#435306,#435307,
#435308,#435309,#435310,#435311,#435312,#435313,#435314,#435315,#435316,
#435317,#435318,#435319,#435320,#435321,#435322,#435323,#435324,#435325,
#435326,#435327,#435328),.UNSPECIFIED.,.F.,.F.,(4,3,3,3,3,3,3,3,3,3,3,4),
(0.,3.71309426656607E-6,5.39981071559398E-6,8.78933289328321E-6,9.00272357067504E-6,
1.07143984504148E-5,1.60780299679388E-5,1.65806081157685E-5,2.30369726850487E-5,
2.67819200416084E-5,3.59736924188455E-5,4.03862783806998E-5),
 .UNSPECIFIED.);
#26460=B_SPLINE_CURVE_WITH_KNOTS('',3,(#435441,#435442,#435443,#435444),
 .UNSPECIFIED.,.F.,.F.,(4,4),(0.,7.70025630629241E-5),.UNSPECIFIED.);
#26461=B_SPLINE_CURVE_WITH_KNOTS('',3,(#435454,#435455,#435456,#435457),
 .UNSPECIFIED.,.F.,.F.,(4,4),(2.16840434497101E-19,7.70025630629236E-5),
 .UNSPECIFIED.);
#26462=B_SPLINE_CURVE_WITH_KNOTS('',3,(#435461,#435462,#435463,#435464,
#435465,#435466,#435467,#435468,#435469,#435470,#435471,#435472,#435473,
#435474,#435475,#435476,#435477,#435478,#435479,#435480,#435481,#435482,
#435483,#435484,#435485,#435486,#435487,#435488,#435489,#435490,#435491,
#435492,#435493,#435494,#435495,#435496,#435497),.UNSPECIFIED.,.F.,.F.,
(4,3,3,3,3,3,3,3,3,3,3,3,4),(0.,9.59031527199796E-6,1.94769411222854E-5,
2.02405092183152E-5,3.21374138577684E-5,3.60302195070438E-5,4.42640648819319E-5,
4.53660204229443E-5,5.03633762301984E-5,5.17708036292895E-5,5.37928993851986E-5,
5.54103755460199E-5,5.6455788950753E-5),.UNSPECIFIED.);
#26463=B_SPLINE_CURVE_WITH_KNOTS('',3,(#435498,#435499,#435500,#435501,
#435502,#435503,#435504,#435505,#435506,#435507,#435508,#435509,#435510,
#435511,#435512,#435513,#435514,#435515,#435516,#435517,#435518,#435519,
#435520,#435521,#435522,#435523,#435524,#435525),.UNSPECIFIED.,.F.,.F.,
(4,3,3,3,3,3,3,3,3,4),(5.6455788950753E-5,5.98940966493747E-5,6.34214003873378E-5,
7.2224147608461E-5,7.38322796533361E-5,8.36529189331474E-5,8.80714278222495E-5,
9.84837568500782E-5,0.000108624704079145,0.000110823272382853),
 .UNSPECIFIED.);
#26464=B_SPLINE_CURVE_WITH_KNOTS('',3,(#435541,#435542,#435543,#435544,
#435545,#435546,#435547,#435548,#435549,#435550,#435551,#435552,#435553,
#435554,#435555,#435556,#435557,#435558,#435559,#435560,#435561,#435562,
#435563,#435564,#435565,#435566,#435567,#435568),.UNSPECIFIED.,.F.,.F.,
(4,3,3,3,3,3,3,3,3,4),(0.,8.66039628586018E-6,1.64707715200669E-5,2.24502894132357E-5,
2.49975961757829E-5,2.88526003690289E-5,3.10661348995023E-5,3.43053543516968E-5,
3.66410545653568E-5,4.00504537627889E-5),.UNSPECIFIED.);
#26465=B_SPLINE_CURVE_WITH_KNOTS('',3,(#435571,#435572,#435573,#435574,
#435575,#435576,#435577),.UNSPECIFIED.,.F.,.F.,(4,3,4),(0.,4.40000041065378E-5,
9.89910850773116E-5),.UNSPECIFIED.);
#26466=B_SPLINE_CURVE_WITH_KNOTS('',3,(#435598,#435599,#435600,#435601,
#435602,#435603,#435604,#435605,#435606,#435607,#435608,#435609,#435610,
#435611,#435612,#435613,#435614,#435615,#435616,#435617,#435618,#435619,
#435620,#435621,#435622,#435623,#435624,#435625,#435626,#435627,#435628,
#435629,#435630,#435631),.UNSPECIFIED.,.F.,.F.,(4,3,3,3,3,3,3,3,3,3,3,4),
(0.,4.29157837302937E-6,5.42772623795306E-6,1.00901698482347E-5,1.31279195068637E-5,
1.57383542265839E-5,1.61011507492102E-5,1.67166789291754E-5,1.95343262811358E-5,
2.29377234674648E-5,2.71556047620055E-5,3.34407099942653E-5),
 .UNSPECIFIED.);
#26467=B_SPLINE_CURVE_WITH_KNOTS('',3,(#435644,#435645,#435646,#435647,
#435648,#435649,#435650,#435651,#435652,#435653,#435654,#435655,#435656,
#435657,#435658,#435659,#435660,#435661,#435662,#435663,#435664,#435665,
#435666,#435667,#435668,#435669,#435670,#435671,#435672,#435673,#435674,
#435675,#435676,#435677),.UNSPECIFIED.,.F.,.F.,(4,3,3,3,3,3,3,3,3,3,3,4),
(0.,3.71309426656662E-6,5.39981071559464E-6,8.78933289368124E-6,9.00272357067546E-6,
1.07143984504151E-5,1.60780299679529E-5,1.6580608115769E-5,2.303697268505E-5,
2.67819200416091E-5,3.59736924187716E-5,4.03862783807006E-5),
 .UNSPECIFIED.);
#26468=B_SPLINE_CURVE_WITH_KNOTS('',3,(#435790,#435791,#435792,#435793),
 .UNSPECIFIED.,.F.,.F.,(4,4),(0.,7.70025630629239E-5),.UNSPECIFIED.);
#26469=B_SPLINE_CURVE_WITH_KNOTS('',3,(#435803,#435804,#435805,#435806),
 .UNSPECIFIED.,.F.,.F.,(4,4),(0.,7.70025630629238E-5),.UNSPECIFIED.);
#26470=B_SPLINE_CURVE_WITH_KNOTS('',3,(#435810,#435811,#435812,#435813,
#435814,#435815,#435816,#435817,#435818,#435819,#435820,#435821,#435822,
#435823,#435824,#435825,#435826,#435827,#435828,#435829,#435830,#435831,
#435832,#435833,#435834,#435835,#435836,#435837,#435838,#435839,#435840,
#435841,#435842,#435843,#435844,#435845,#435846),.UNSPECIFIED.,.F.,.F.,
(4,3,3,3,3,3,3,3,3,3,3,3,4),(0.,9.59031527203606E-6,1.94769411223574E-5,
2.02405092183154E-5,3.21374138577652E-5,3.60302195070439E-5,4.42640648818479E-5,
4.53660204229445E-5,5.03633762302319E-5,5.17708036292895E-5,5.37928993851989E-5,
5.54103755460196E-5,5.64557889509337E-5),.UNSPECIFIED.);
#26471=B_SPLINE_CURVE_WITH_KNOTS('',3,(#435847,#435848,#435849,#435850,
#435851,#435852,#435853,#435854,#435855,#435856,#435857,#435858,#435859,
#435860,#435861,#435862,#435863,#435864,#435865,#435866,#435867,#435868,
#435869,#435870,#435871,#435872,#435873,#435874),.UNSPECIFIED.,.F.,.F.,
(4,3,3,3,3,3,3,3,3,4),(5.64557889509337E-5,5.98940966493753E-5,6.34214003873381E-5,
7.2224147608401E-5,7.38322796533362E-5,8.36529189331597E-5,8.80714278222501E-5,
9.84837568501059E-5,0.000108624704079191,0.000110823272382853),
 .UNSPECIFIED.);
#26472=B_SPLINE_CURVE_WITH_KNOTS('',3,(#435890,#435891,#435892,#435893,
#435894,#435895,#435896,#435897,#435898,#435899,#435900,#435901,#435902,
#435903,#435904,#435905,#435906,#435907,#435908,#435909,#435910,#435911,
#435912,#435913,#435914,#435915,#435916,#435917),.UNSPECIFIED.,.F.,.F.,
(4,3,3,3,3,3,3,3,3,4),(0.,8.66039628578931E-6,1.6470771520067E-5,2.24502894132249E-5,
2.49975961757829E-5,2.88526003690286E-5,3.10661348995018E-5,3.43053543516963E-5,
3.66410545653567E-5,4.00504537627888E-5),.UNSPECIFIED.);
#26473=B_SPLINE_CURVE_WITH_KNOTS('',3,(#435920,#435921,#435922,#435923,
#435924,#435925,#435926),.UNSPECIFIED.,.F.,.F.,(4,3,4),(0.,4.40000041065377E-5,
9.89910850773112E-5),.UNSPECIFIED.);
#26474=B_SPLINE_CURVE_WITH_KNOTS('',3,(#435947,#435948,#435949,#435950,
#435951,#435952,#435953,#435954,#435955,#435956,#435957,#435958,#435959,
#435960,#435961,#435962,#435963,#435964,#435965,#435966,#435967,#435968,
#435969,#435970,#435971,#435972,#435973,#435974,#435975,#435976,#435977,
#435978,#435979,#435980),.UNSPECIFIED.,.F.,.F.,(4,3,3,3,3,3,3,3,3,3,3,4),
(0.,4.29157837304789E-6,5.42772623795347E-6,1.0090169848235E-5,1.31279195068639E-5,
1.57383542265994E-5,1.61011507492107E-5,1.67166789291758E-5,1.95343262811364E-5,
2.29377234674653E-5,2.71556047620062E-5,3.3440709994266E-5),
 .UNSPECIFIED.);
#26475=B_SPLINE_CURVE_WITH_KNOTS('',3,(#435993,#435994,#435995,#435996,
#435997,#435998,#435999,#436000,#436001,#436002,#436003,#436004,#436005,
#436006,#436007,#436008,#436009,#436010,#436011,#436012,#436013,#436014,
#436015,#436016,#436017,#436018,#436019,#436020,#436021,#436022,#436023,
#436024,#436025,#436026),.UNSPECIFIED.,.F.,.F.,(4,3,3,3,3,3,3,3,3,3,3,4),
(2.16840434497101E-19,3.7130942665664E-6,5.39981071559413E-6,8.78933289330628E-6,
9.0027235706752E-6,1.07143984504148E-5,1.60780299679502E-5,1.65806081157688E-5,
2.30369726850799E-5,2.67819200416088E-5,3.59736924187541E-5,4.03862783807006E-5),
 .UNSPECIFIED.);
#26476=B_SPLINE_CURVE_WITH_KNOTS('',3,(#436139,#436140,#436141,#436142),
 .UNSPECIFIED.,.F.,.F.,(4,4),(0.,7.70025630629239E-5),.UNSPECIFIED.);
#26477=B_SPLINE_CURVE_WITH_KNOTS('',3,(#436152,#436153,#436154,#436155),
 .UNSPECIFIED.,.F.,.F.,(4,4),(2.16840434497101E-19,7.70025630629238E-5),
 .UNSPECIFIED.);
#26478=B_SPLINE_CURVE_WITH_KNOTS('',3,(#436159,#436160,#436161,#436162,
#436163,#436164,#436165,#436166,#436167,#436168,#436169,#436170,#436171,
#436172,#436173,#436174,#436175,#436176,#436177,#436178,#436179,#436180,
#436181,#436182,#436183,#436184,#436185,#436186,#436187,#436188,#436189,
#436190,#436191,#436192,#436193,#436194,#436195),.UNSPECIFIED.,.F.,.F.,
(4,3,3,3,3,3,3,3,3,3,3,3,4),(0.,9.5903152719825E-6,1.94769411222625E-5,
2.02405092183152E-5,3.21374138577704E-5,3.60302195070439E-5,4.42640648818249E-5,
4.53660204229442E-5,5.03633762302113E-5,5.17708036292899E-5,5.37928993851988E-5,
5.54103755460209E-5,5.64557889509965E-5),.UNSPECIFIED.);
#26479=B_SPLINE_CURVE_WITH_KNOTS('',3,(#436196,#436197,#436198,#436199,
#436200,#436201,#436202,#436203,#436204,#436205,#436206,#436207,#436208,
#436209,#436210,#436211,#436212,#436213,#436214,#436215,#436216,#436217,
#436218,#436219,#436220,#436221,#436222,#436223),.UNSPECIFIED.,.F.,.F.,
(4,3,3,3,3,3,3,3,3,4),(5.64557889509965E-5,5.98940966493753E-5,6.34214003873383E-5,
7.22241476084711E-5,7.38322796533366E-5,8.3652918933141E-5,8.80714278222504E-5,
9.84837568500915E-5,0.000108624704079173,0.000110823272382854),
 .UNSPECIFIED.);
#26480=B_SPLINE_CURVE_WITH_KNOTS('',3,(#436239,#436240,#436241,#436242,
#436243,#436244,#436245,#436246,#436247,#436248,#436249,#436250,#436251,
#436252,#436253,#436254,#436255,#436256,#436257,#436258,#436259,#436260,
#436261,#436262,#436263,#436264,#436265,#436266),.UNSPECIFIED.,.F.,.F.,
(4,3,3,3,3,3,3,3,3,4),(0.,8.66039628579659E-6,1.64707715200667E-5,2.24502894132511E-5,
2.49975961757824E-5,2.8852600369028E-5,3.10661348995018E-5,3.4305354351696E-5,
3.66410545653558E-5,4.00504537627887E-5),.UNSPECIFIED.);
#26481=B_SPLINE_CURVE_WITH_KNOTS('',3,(#436269,#436270,#436271,#436272,
#436273,#436274,#436275),.UNSPECIFIED.,.F.,.F.,(4,3,4),(0.,4.40000041065376E-5,
9.89910850773112E-5),.UNSPECIFIED.);
#26482=B_SPLINE_CURVE_WITH_KNOTS('',3,(#436296,#436297,#436298,#436299,
#436300,#436301,#436302,#436303,#436304,#436305,#436306,#436307,#436308,
#436309,#436310,#436311,#436312,#436313,#436314,#436315,#436316,#436317,
#436318,#436319,#436320,#436321,#436322,#436323,#436324,#436325,#436326,
#436327,#436328,#436329),.UNSPECIFIED.,.F.,.F.,(4,3,3,3,3,3,3,3,3,3,3,4),
(0.,4.29157837303514E-6,5.42772623795343E-6,1.00901698482349E-5,1.31279195068641E-5,
1.57383542265741E-5,1.61011507492106E-5,1.67166789291761E-5,1.95343262811359E-5,
2.29377234674652E-5,2.71556047620062E-5,3.34407099942666E-5),
 .UNSPECIFIED.);
#26483=B_SPLINE_CURVE_WITH_KNOTS('',3,(#436342,#436343,#436344,#436345,
#436346,#436347,#436348,#436349,#436350,#436351,#436352,#436353,#436354,
#436355,#436356,#436357,#436358,#436359,#436360,#436361,#436362,#436363,
#436364,#436365,#436366,#436367,#436368,#436369,#436370,#436371,#436372,
#436373,#436374,#436375),.UNSPECIFIED.,.F.,.F.,(4,3,3,3,3,3,3,3,3,3,3,4),
(0.,3.71309426656653E-6,5.39981071559412E-6,8.78933289366921E-6,9.00272357067533E-6,
1.0714398450415E-5,1.607802996795E-5,1.65806081157687E-5,2.30369726850199E-5,
2.67819200416086E-5,3.59736924188143E-5,4.03862783806999E-5),
 .UNSPECIFIED.);
#26484=B_SPLINE_CURVE_WITH_KNOTS('',3,(#436488,#436489,#436490,#436491),
 .UNSPECIFIED.,.F.,.F.,(4,4),(0.,7.70025630629239E-5),.UNSPECIFIED.);
#26485=B_SPLINE_CURVE_WITH_KNOTS('',3,(#436501,#436502,#436503,#436504),
 .UNSPECIFIED.,.F.,.F.,(4,4),(2.16840434497101E-19,7.70025630629238E-5),
 .UNSPECIFIED.);
#26486=B_SPLINE_CURVE_WITH_KNOTS('',3,(#436508,#436509,#436510,#436511,
#436512,#436513,#436514,#436515,#436516,#436517,#436518,#436519,#436520,
#436521,#436522,#436523,#436524,#436525,#436526,#436527,#436528,#436529,
#436530,#436531,#436532,#436533,#436534,#436535,#436536,#436537,#436538,
#436539,#436540,#436541,#436542,#436543,#436544),.UNSPECIFIED.,.F.,.F.,
(4,3,3,3,3,3,3,3,3,3,3,3,4),(0.,9.59031527201526E-6,1.94769411223018E-5,
2.02405092183151E-5,3.21374138577733E-5,3.6030219507044E-5,4.42640648818702E-5,
4.53660204229444E-5,5.0363376230214E-5,5.17708036292896E-5,5.37928993851991E-5,
5.54103755460203E-5,5.64557889511334E-5),.UNSPECIFIED.);
#26487=B_SPLINE_CURVE_WITH_KNOTS('',3,(#436545,#436546,#436547,#436548,
#436549,#436550,#436551,#436552,#436553,#436554,#436555,#436556,#436557,
#436558,#436559,#436560,#436561,#436562,#436563,#436564,#436565,#436566,
#436567,#436568,#436569,#436570,#436571,#436572),.UNSPECIFIED.,.F.,.F.,
(4,3,3,3,3,3,3,3,3,4),(5.64557889511334E-5,5.98940966493753E-5,6.34214003873383E-5,
7.22241476084157E-5,7.38322796533368E-5,8.36529189331239E-5,8.80714278222506E-5,
9.84837568500551E-5,0.000108624704079119,0.000110823272382854),
 .UNSPECIFIED.);
#26488=B_SPLINE_CURVE_WITH_KNOTS('',3,(#436588,#436589,#436590,#436591,
#436592,#436593,#436594,#436595,#436596,#436597,#436598,#436599,#436600,
#436601,#436602,#436603,#436604,#436605,#436606,#436607,#436608,#436609,
#436610,#436611,#436612,#436613,#436614,#436615),.UNSPECIFIED.,.F.,.F.,
(4,3,3,3,3,3,3,3,3,4),(0.,8.66039628579537E-6,1.64707715200666E-5,2.24502894132562E-5,
2.49975961757822E-5,2.8852600369028E-5,3.10661348995016E-5,3.43053543516961E-5,
3.66410545653559E-5,4.00504537627884E-5),.UNSPECIFIED.);
#26489=B_SPLINE_CURVE_WITH_KNOTS('',3,(#436618,#436619,#436620,#436621,
#436622,#436623,#436624),.UNSPECIFIED.,.F.,.F.,(4,3,4),(0.,4.40000041065378E-5,
9.89910850773114E-5),.UNSPECIFIED.);
#26490=B_SPLINE_CURVE_WITH_KNOTS('',3,(#436645,#436646,#436647,#436648,
#436649,#436650,#436651,#436652,#436653,#436654,#436655,#436656,#436657,
#436658,#436659,#436660,#436661,#436662,#436663,#436664,#436665,#436666,
#436667,#436668,#436669,#436670,#436671,#436672,#436673,#436674,#436675,
#436676,#436677,#436678),.UNSPECIFIED.,.F.,.F.,(4,3,3,3,3,3,3,3,3,3,3,4),
(0.,4.29157837302742E-6,5.42772623795344E-6,1.00901698482348E-5,1.31279195068639E-5,
1.57383542265895E-5,1.61011507492104E-5,1.6716678929176E-5,1.95343262811361E-5,
2.2937723467465E-5,2.7155604762006E-5,3.34407099942662E-5),
 .UNSPECIFIED.);
#26491=B_SPLINE_CURVE_WITH_KNOTS('',3,(#436691,#436692,#436693,#436694,
#436695,#436696,#436697,#436698,#436699,#436700,#436701,#436702,#436703,
#436704,#436705,#436706,#436707,#436708,#436709,#436710,#436711,#436712,
#436713,#436714,#436715,#436716,#436717,#436718,#436719,#436720,#436721,
#436722,#436723,#436724),.UNSPECIFIED.,.F.,.F.,(4,3,3,3,3,3,3,3,3,3,3,4),
(0.,3.71309426656648E-6,5.39981071559424E-6,8.78933289368692E-6,9.00272357067524E-6,
1.07143984504148E-5,1.60780299679589E-5,1.65806081157688E-5,2.3036972685045E-5,
2.67819200416088E-5,3.59736924188061E-5,4.03862783807006E-5),
 .UNSPECIFIED.);
#26492=B_SPLINE_CURVE_WITH_KNOTS('',3,(#436837,#436838,#436839,#436840),
 .UNSPECIFIED.,.F.,.F.,(4,4),(0.,7.70025630629238E-5),.UNSPECIFIED.);
#26493=B_SPLINE_CURVE_WITH_KNOTS('',3,(#436850,#436851,#436852,#436853),
 .UNSPECIFIED.,.F.,.F.,(4,4),(0.,7.70025630629235E-5),.UNSPECIFIED.);
#26494=B_SPLINE_CURVE_WITH_KNOTS('',3,(#436857,#436858,#436859,#436860,
#436861,#436862,#436863,#436864,#436865,#436866,#436867,#436868,#436869,
#436870,#436871,#436872,#436873,#436874,#436875,#436876,#436877,#436878,
#436879,#436880,#436881,#436882,#436883,#436884,#436885,#436886,#436887,
#436888,#436889,#436890,#436891,#436892,#436893),.UNSPECIFIED.,.F.,.F.,
(4,3,3,3,3,3,3,3,3,3,3,3,4),(0.,9.59031527202043E-6,1.94769411223311E-5,
2.02405092183154E-5,3.21374138577703E-5,3.60302195070436E-5,4.42640648819417E-5,
4.53660204229441E-5,5.03633762302143E-5,5.17708036292897E-5,5.37928993851988E-5,
5.54103755460199E-5,5.64557889509022E-5),.UNSPECIFIED.);
#26495=B_SPLINE_CURVE_WITH_KNOTS('',3,(#436894,#436895,#436896,#436897,
#436898,#436899,#436900,#436901,#436902,#436903,#436904,#436905,#436906,
#436907,#436908,#436909,#436910,#436911,#436912,#436913,#436914,#436915,
#436916,#436917,#436918,#436919,#436920,#436921),.UNSPECIFIED.,.F.,.F.,
(4,3,3,3,3,3,3,3,3,4),(5.64557889509022E-5,5.98940966493751E-5,6.34214003873379E-5,
7.22241476086138E-5,7.38322796533362E-5,8.36529189331517E-5,8.80714278222496E-5,
9.84837568501121E-5,0.000108624704079202,0.000110823272382853),
 .UNSPECIFIED.);
#26496=B_SPLINE_CURVE_WITH_KNOTS('',3,(#436937,#436938,#436939,#436940,
#436941,#436942,#436943,#436944,#436945,#436946,#436947,#436948,#436949,
#436950,#436951,#436952,#436953,#436954,#436955,#436956,#436957,#436958,
#436959,#436960,#436961,#436962,#436963,#436964),.UNSPECIFIED.,.F.,.F.,
(4,3,3,3,3,3,3,3,3,4),(0.,8.660396285838E-6,1.64707715200667E-5,2.24502894129291E-5,
2.49975961757824E-5,2.88526003690282E-5,3.10661348995017E-5,3.43053543516958E-5,
3.6641054565356E-5,4.00504537627886E-5),.UNSPECIFIED.);
#26497=B_SPLINE_CURVE_WITH_KNOTS('',3,(#436967,#436968,#436969,#436970,
#436971,#436972,#436973),.UNSPECIFIED.,.F.,.F.,(4,3,4),(0.,4.40000041065374E-5,
9.89910850773111E-5),.UNSPECIFIED.);
#26498=B_SPLINE_CURVE_WITH_KNOTS('',3,(#436994,#436995,#436996,#436997,
#436998,#436999,#437000,#437001,#437002,#437003,#437004,#437005,#437006,
#437007,#437008,#437009,#437010,#437011,#437012,#437013,#437014,#437015,
#437016,#437017,#437018,#437019,#437020,#437021,#437022,#437023,#437024,
#437025,#437026,#437027),.UNSPECIFIED.,.F.,.F.,(4,3,3,3,3,3,3,3,3,3,3,4),
(0.,4.29157837302125E-6,5.42772623795363E-6,1.00901698482349E-5,1.31279195068643E-5,
1.57383542265817E-5,1.61011507492105E-5,1.67166789291761E-5,1.95343262811362E-5,
2.29377234674653E-5,2.71556047620061E-5,3.34407099942659E-5),
 .UNSPECIFIED.);
#26499=B_SPLINE_CURVE_WITH_KNOTS('',3,(#437040,#437041,#437042,#437043,
#437044,#437045,#437046,#437047,#437048,#437049,#437050,#437051,#437052,
#437053,#437054,#437055,#437056,#437057,#437058,#437059,#437060,#437061,
#437062,#437063,#437064,#437065,#437066,#437067,#437068,#437069,#437070,
#437071,#437072,#437073),.UNSPECIFIED.,.F.,.F.,(4,3,3,3,3,3,3,3,3,3,3,4),
(2.16840434497101E-19,3.71309426656617E-6,5.39981071559392E-6,8.78933289364865E-6,
9.00272357067512E-6,1.07143984504147E-5,1.60780299679705E-5,1.65806081157687E-5,
2.30369726850335E-5,2.67819200416085E-5,3.59736924188345E-5,4.03862783806998E-5),
 .UNSPECIFIED.);
#26500=B_SPLINE_CURVE_WITH_KNOTS('',3,(#437186,#437187,#437188,#437189),
 .UNSPECIFIED.,.F.,.F.,(4,4),(0.,7.70025630629236E-5),.UNSPECIFIED.);
#26501=B_SPLINE_CURVE_WITH_KNOTS('',3,(#437199,#437200,#437201,#437202),
 .UNSPECIFIED.,.F.,.F.,(4,4),(4.33680868994202E-19,7.70025630629238E-5),
 .UNSPECIFIED.);
#26502=B_SPLINE_CURVE_WITH_KNOTS('',3,(#437206,#437207,#437208,#437209,
#437210,#437211,#437212,#437213,#437214,#437215,#437216,#437217,#437218,
#437219,#437220,#437221,#437222,#437223,#437224,#437225,#437226,#437227,
#437228,#437229,#437230,#437231,#437232,#437233,#437234,#437235,#437236,
#437237,#437238,#437239,#437240,#437241,#437242),.UNSPECIFIED.,.F.,.F.,
(4,3,3,3,3,3,3,3,3,3,3,3,4),(0.,9.5903152720398E-6,1.94769411223548E-5,
2.02405092183152E-5,3.21374138577692E-5,3.60302195070439E-5,4.42640648818201E-5,
4.53660204229444E-5,5.03633762302064E-5,5.17708036292898E-5,5.37928993851991E-5,
5.54103755460198E-5,5.64557889508151E-5),.UNSPECIFIED.);
#26503=B_SPLINE_CURVE_WITH_KNOTS('',3,(#437243,#437244,#437245,#437246,
#437247,#437248,#437249,#437250,#437251,#437252,#437253,#437254,#437255,
#437256,#437257,#437258,#437259,#437260,#437261,#437262,#437263,#437264,
#437265,#437266,#437267,#437268,#437269,#437270),.UNSPECIFIED.,.F.,.F.,
(4,3,3,3,3,3,3,3,3,4),(5.64557889508151E-5,5.98940966493754E-5,6.34214003873384E-5,
7.22241476084689E-5,7.38322796533367E-5,8.36529189331414E-5,8.80714278222504E-5,
9.84837568500745E-5,0.00010862470407914,0.000110823272382854),
 .UNSPECIFIED.);
#26504=B_SPLINE_CURVE_WITH_KNOTS('',3,(#437286,#437287,#437288,#437289,
#437290,#437291,#437292,#437293,#437294,#437295,#437296,#437297,#437298,
#437299,#437300,#437301,#437302,#437303,#437304,#437305,#437306,#437307,
#437308,#437309,#437310,#437311,#437312,#437313),.UNSPECIFIED.,.F.,.F.,
(4,3,3,3,3,3,3,3,3,4),(0.,8.6603962858034E-6,1.64707715200669E-5,2.2450289413248E-5,
2.49975961757828E-5,2.88526003690285E-5,3.1066134899502E-5,3.43053543516968E-5,
3.66410545653566E-5,4.00504537627889E-5),.UNSPECIFIED.);
#26505=B_SPLINE_CURVE_WITH_KNOTS('',3,(#437316,#437317,#437318,#437319,
#437320,#437321,#437322),.UNSPECIFIED.,.F.,.F.,(4,3,4),(0.,4.40000041065376E-5,
9.89910850773112E-5),.UNSPECIFIED.);
#26506=B_SPLINE_CURVE_WITH_KNOTS('',3,(#437343,#437344,#437345,#437346,
#437347,#437348,#437349,#437350,#437351,#437352,#437353,#437354,#437355,
#437356,#437357,#437358,#437359,#437360,#437361,#437362,#437363,#437364,
#437365,#437366,#437367,#437368,#437369,#437370,#437371,#437372,#437373,
#437374,#437375,#437376),.UNSPECIFIED.,.F.,.F.,(4,3,3,3,3,3,3,3,3,3,3,4),
(0.,4.29157837305506E-6,5.42772623795337E-6,1.00901698482351E-5,1.31279195068642E-5,
1.57383542265671E-5,1.61011507492106E-5,1.67166789291762E-5,1.95343262811363E-5,
2.29377234674653E-5,2.71556047620063E-5,3.34407099942663E-5),
 .UNSPECIFIED.);
#26507=B_SPLINE_CURVE_WITH_KNOTS('',3,(#437389,#437390,#437391,#437392,
#437393,#437394,#437395,#437396,#437397,#437398,#437399,#437400,#437401,
#437402,#437403,#437404,#437405,#437406,#437407,#437408,#437409,#437410,
#437411,#437412,#437413,#437414,#437415,#437416,#437417,#437418,#437419,
#437420,#437421,#437422),.UNSPECIFIED.,.F.,.F.,(4,3,3,3,3,3,3,3,3,3,3,4),
(0.,3.71309426656638E-6,5.3998107155941E-6,8.78933289365815E-6,9.00272357067497E-6,
1.07143984504149E-5,1.60780299679781E-5,1.65806081157684E-5,2.30369726850169E-5,
2.67819200416079E-5,3.59736924188327E-5,4.03862783806989E-5),
 .UNSPECIFIED.);
#26508=B_SPLINE_CURVE_WITH_KNOTS('',3,(#437535,#437536,#437537,#437538),
 .UNSPECIFIED.,.F.,.F.,(4,4),(0.,7.70025630629239E-5),.UNSPECIFIED.);
#26509=B_SPLINE_CURVE_WITH_KNOTS('',3,(#437548,#437549,#437550,#437551),
 .UNSPECIFIED.,.F.,.F.,(4,4),(4.33680868994202E-19,7.70025630629238E-5),
 .UNSPECIFIED.);
#26510=B_SPLINE_CURVE_WITH_KNOTS('',3,(#437555,#437556,#437557,#437558,
#437559,#437560,#437561,#437562,#437563,#437564,#437565,#437566,#437567,
#437568,#437569,#437570,#437571,#437572,#437573,#437574,#437575,#437576,
#437577,#437578,#437579,#437580,#437581,#437582,#437583,#437584,#437585,
#437586,#437587,#437588,#437589,#437590,#437591),.UNSPECIFIED.,.F.,.F.,
(4,3,3,3,3,3,3,3,3,3,3,3,4),(0.,9.59031527200714E-6,1.94769411223042E-5,
2.02405092183152E-5,3.21374138577778E-5,3.60302195070437E-5,4.42640648818082E-5,
4.53660204229444E-5,5.03633762302091E-5,5.17708036292898E-5,5.37928993851988E-5,
5.54103755460199E-5,5.64557889513718E-5),.UNSPECIFIED.);
#26511=B_SPLINE_CURVE_WITH_KNOTS('',3,(#437592,#437593,#437594,#437595,
#437596,#437597,#437598,#437599,#437600,#437601,#437602,#437603,#437604,
#437605,#437606,#437607,#437608,#437609,#437610,#437611,#437612,#437613,
#437614,#437615,#437616,#437617,#437618,#437619),.UNSPECIFIED.,.F.,.F.,
(4,3,3,3,3,3,3,3,3,4),(5.64557889513718E-5,5.98940966493751E-5,6.3421400387338E-5,
7.22241476084119E-5,7.38322796533366E-5,8.36529189331453E-5,8.80714278222501E-5,
9.84837568500711E-5,0.000108624704079126,0.000110823272382854),
 .UNSPECIFIED.);
#26512=B_SPLINE_CURVE_WITH_KNOTS('',3,(#437635,#437636,#437637,#437638,
#437639,#437640,#437641,#437642,#437643,#437644,#437645,#437646,#437647,
#437648,#437649,#437650,#437651,#437652,#437653,#437654,#437655,#437656,
#437657,#437658,#437659,#437660,#437661,#437662),.UNSPECIFIED.,.F.,.F.,
(4,3,3,3,3,3,3,3,3,4),(0.,8.66039628577752E-6,1.64707715200667E-5,2.24502894132132E-5,
2.49975961757823E-5,2.8852600369028E-5,3.10661348995015E-5,3.4305354351696E-5,
3.66410545653558E-5,4.00504537627882E-5),.UNSPECIFIED.);
#26513=B_SPLINE_CURVE_WITH_KNOTS('',3,(#437665,#437666,#437667,#437668,
#437669,#437670,#437671),.UNSPECIFIED.,.F.,.F.,(4,3,4),(0.,4.4000004106538E-5,
9.89910850773116E-5),.UNSPECIFIED.);
#26514=B_SPLINE_CURVE_WITH_KNOTS('',3,(#437692,#437693,#437694,#437695,
#437696,#437697,#437698,#437699,#437700,#437701,#437702,#437703,#437704,
#437705,#437706,#437707,#437708,#437709,#437710,#437711,#437712,#437713,
#437714,#437715,#437716,#437717,#437718,#437719,#437720,#437721,#437722,
#437723,#437724,#437725),.UNSPECIFIED.,.F.,.F.,(4,3,3,3,3,3,3,3,3,3,3,4),
(0.,4.29157837303885E-6,5.42772623795332E-6,1.00901698482349E-5,1.31279195068638E-5,
1.5738354226589E-5,1.61011507492106E-5,1.67166789291754E-5,1.95343262811361E-5,
2.29377234674651E-5,2.71556047620061E-5,3.34407099942664E-5),
 .UNSPECIFIED.);
#26515=B_SPLINE_CURVE_WITH_KNOTS('',3,(#437738,#437739,#437740,#437741,
#437742,#437743,#437744,#437745,#437746,#437747,#437748,#437749,#437750,
#437751,#437752,#437753,#437754,#437755,#437756,#437757,#437758,#437759,
#437760,#437761,#437762,#437763,#437764,#437765,#437766,#437767,#437768,
#437769,#437770,#437771),.UNSPECIFIED.,.F.,.F.,(4,3,3,3,3,3,3,3,3,3,3,4),
(0.,3.7130942665663E-6,5.39981071559403E-6,8.78933289330991E-6,9.00272357067504E-6,
1.07143984504147E-5,1.60780299679603E-5,1.65806081157687E-5,2.30369726850442E-5,
2.67819200416087E-5,3.59736924187731E-5,4.03862783807004E-5),
 .UNSPECIFIED.);
#26516=B_SPLINE_CURVE_WITH_KNOTS('',3,(#437884,#437885,#437886,#437887),
 .UNSPECIFIED.,.F.,.F.,(4,4),(0.,7.70025630629238E-5),.UNSPECIFIED.);
#26517=B_SPLINE_CURVE_WITH_KNOTS('',3,(#437897,#437898,#437899,#437900),
 .UNSPECIFIED.,.F.,.F.,(4,4),(0.,7.70025630629239E-5),.UNSPECIFIED.);
#26518=B_SPLINE_CURVE_WITH_KNOTS('',3,(#437904,#437905,#437906,#437907,
#437908,#437909,#437910,#437911,#437912,#437913,#437914,#437915,#437916,
#437917,#437918,#437919,#437920,#437921,#437922,#437923,#437924,#437925,
#437926,#437927,#437928,#437929,#437930,#437931,#437932,#437933,#437934,
#437935,#437936,#437937,#437938,#437939,#437940),.UNSPECIFIED.,.F.,.F.,
(4,3,3,3,3,3,3,3,3,3,3,3,4),(0.,9.59031527202011E-6,1.94769411223197E-5,
2.02405092183154E-5,3.21374138577635E-5,3.60302195070441E-5,4.4264064881854E-5,
4.53660204229442E-5,5.03633762302141E-5,5.17708036292897E-5,5.37928993851989E-5,
5.54103755460195E-5,5.64557889512644E-5),.UNSPECIFIED.);
#26519=B_SPLINE_CURVE_WITH_KNOTS('',3,(#437941,#437942,#437943,#437944,
#437945,#437946,#437947,#437948,#437949,#437950,#437951,#437952,#437953,
#437954,#437955,#437956,#437957,#437958,#437959,#437960,#437961,#437962,
#437963,#437964,#437965,#437966,#437967,#437968),.UNSPECIFIED.,.F.,.F.,
(4,3,3,3,3,3,3,3,3,4),(5.64557889512644E-5,5.98940966493748E-5,6.34214003873378E-5,
7.22241476084218E-5,7.38322796533363E-5,8.36529189331423E-5,8.80714278222497E-5,
9.84837568500604E-5,0.000108624704079115,0.000110823272382853),
 .UNSPECIFIED.);
#26520=B_SPLINE_CURVE_WITH_KNOTS('',3,(#437984,#437985,#437986,#437987,
#437988,#437989,#437990,#437991,#437992,#437993,#437994,#437995,#437996,
#437997,#437998,#437999,#438000,#438001,#438002,#438003,#438004,#438005,
#438006,#438007,#438008,#438009,#438010,#438011),.UNSPECIFIED.,.F.,.F.,
(4,3,3,3,3,3,3,3,3,4),(0.,8.66039628578128E-6,1.64707715200666E-5,2.24502894132383E-5,
2.49975961757824E-5,2.8852600369028E-5,3.10661348995017E-5,3.43053543516959E-5,
3.66410545653557E-5,4.00504537627889E-5),.UNSPECIFIED.);
#26521=B_SPLINE_CURVE_WITH_KNOTS('',3,(#438014,#438015,#438016,#438017,
#438018,#438019,#438020),.UNSPECIFIED.,.F.,.F.,(4,3,4),(0.,4.40000041065373E-5,
9.89910850773111E-5),.UNSPECIFIED.);
#26522=B_SPLINE_CURVE_WITH_KNOTS('',3,(#438041,#438042,#438043,#438044,
#438045,#438046,#438047,#438048,#438049,#438050,#438051,#438052,#438053,
#438054,#438055,#438056,#438057,#438058,#438059,#438060,#438061,#438062,
#438063,#438064,#438065,#438066,#438067,#438068,#438069,#438070,#438071,
#438072,#438073,#438074),.UNSPECIFIED.,.F.,.F.,(4,3,3,3,3,3,3,3,3,3,3,4),
(0.,4.2915783730307E-6,5.42772623795346E-6,1.00901698482348E-5,1.31279195068641E-5,
1.57383542265829E-5,1.61011507492106E-5,1.67166789291753E-5,1.9534326281136E-5,
2.2937723467465E-5,2.71556047620057E-5,3.34407099942656E-5),
 .UNSPECIFIED.);
#26523=B_SPLINE_CURVE_WITH_KNOTS('',3,(#438087,#438088,#438089,#438090,
#438091,#438092,#438093,#438094,#438095,#438096,#438097,#438098,#438099,
#438100,#438101,#438102,#438103,#438104,#438105,#438106,#438107,#438108,
#438109,#438110,#438111,#438112,#438113,#438114,#438115,#438116,#438117,
#438118,#438119,#438120),.UNSPECIFIED.,.F.,.F.,(4,3,3,3,3,3,3,3,3,3,3,4),
(0.,3.71309426656622E-6,5.39981071559398E-6,8.78933289327679E-6,9.00272357067504E-6,
1.07143984504148E-5,1.60780299679623E-5,1.65806081157686E-5,2.30369726850495E-5,
2.67819200416084E-5,3.5973692418755E-5,4.03862783806997E-5),
 .UNSPECIFIED.);
#26524=B_SPLINE_CURVE_WITH_KNOTS('',3,(#438233,#438234,#438235,#438236),
 .UNSPECIFIED.,.F.,.F.,(4,4),(0.,7.70025630629241E-5),.UNSPECIFIED.);
#26525=B_SPLINE_CURVE_WITH_KNOTS('',3,(#438246,#438247,#438248,#438249),
 .UNSPECIFIED.,.F.,.F.,(4,4),(4.33680868994202E-19,7.70025630629239E-5),
 .UNSPECIFIED.);
#26526=B_SPLINE_CURVE_WITH_KNOTS('',3,(#438253,#438254,#438255,#438256,
#438257,#438258,#438259,#438260,#438261,#438262,#438263,#438264,#438265,
#438266,#438267,#438268,#438269,#438270,#438271,#438272,#438273,#438274,
#438275,#438276,#438277,#438278,#438279,#438280,#438281,#438282,#438283,
#438284,#438285,#438286,#438287,#438288,#438289),.UNSPECIFIED.,.F.,.F.,
(4,3,3,3,3,3,3,3,3,3,3,3,4),(0.,9.59031527198475E-6,1.94769411222611E-5,
2.02405092183153E-5,3.21374138577742E-5,3.60302195070439E-5,4.4264064881873E-5,
4.53660204229443E-5,5.0363376230202E-5,5.17708036292894E-5,5.37928993851989E-5,
5.54103755460197E-5,5.6455788951275E-5),.UNSPECIFIED.);
#26527=B_SPLINE_CURVE_WITH_KNOTS('',3,(#438290,#438291,#438292,#438293,
#438294,#438295,#438296,#438297,#438298,#438299,#438300,#438301,#438302,
#438303,#438304,#438305,#438306,#438307,#438308,#438309,#438310,#438311,
#438312,#438313,#438314,#438315,#438316,#438317),.UNSPECIFIED.,.F.,.F.,
(4,3,3,3,3,3,3,3,3,4),(5.6455788951275E-5,5.9894096649375E-5,6.3421400387338E-5,
7.22241476084665E-5,7.38322796533363E-5,8.36529189331418E-5,8.80714278222499E-5,
9.84837568500648E-5,0.000108624704079118,0.000110823272382853),
 .UNSPECIFIED.);
#26528=B_SPLINE_CURVE_WITH_KNOTS('',3,(#438333,#438334,#438335,#438336,
#438337,#438338,#438339,#438340,#438341,#438342,#438343,#438344,#438345,
#438346,#438347,#438348,#438349,#438350,#438351,#438352,#438353,#438354,
#438355,#438356,#438357,#438358,#438359,#438360),.UNSPECIFIED.,.F.,.F.,
(4,3,3,3,3,3,3,3,3,4),(0.,8.6603962858341E-6,1.64707715200666E-5,2.24502894132345E-5,
2.49975961757823E-5,2.8852600369028E-5,3.10661348995015E-5,3.4305354351696E-5,
3.66410545653559E-5,4.00504537627888E-5),.UNSPECIFIED.);
#26529=B_SPLINE_CURVE_WITH_KNOTS('',3,(#438363,#438364,#438365,#438366,
#438367,#438368,#438369),.UNSPECIFIED.,.F.,.F.,(4,3,4),(0.,4.40000041065375E-5,
9.89910850773111E-5),.UNSPECIFIED.);
#26530=B_SPLINE_CURVE_WITH_KNOTS('',3,(#438390,#438391,#438392,#438393,
#438394,#438395,#438396,#438397,#438398,#438399,#438400,#438401,#438402,
#438403,#438404,#438405,#438406,#438407,#438408,#438409,#438410,#438411,
#438412,#438413,#438414,#438415,#438416,#438417,#438418,#438419,#438420,
#438421,#438422,#438423),.UNSPECIFIED.,.F.,.F.,(4,3,3,3,3,3,3,3,3,3,3,4),
(0.,4.29157837305459E-6,5.42772623795334E-6,1.0090169848235E-5,1.3127919506864E-5,
1.57383542265921E-5,1.61011507492108E-5,1.67166789291756E-5,1.9534326281136E-5,
2.29377234674651E-5,2.71556047620062E-5,3.34407099942664E-5),
 .UNSPECIFIED.);
#26531=B_SPLINE_CURVE_WITH_KNOTS('',3,(#438436,#438437,#438438,#438439,
#438440,#438441,#438442,#438443,#438444,#438445,#438446,#438447,#438448,
#438449,#438450,#438451,#438452,#438453,#438454,#438455,#438456,#438457,
#438458,#438459,#438460,#438461,#438462,#438463,#438464,#438465,#438466,
#438467,#438468,#438469),.UNSPECIFIED.,.F.,.F.,(4,3,3,3,3,3,3,3,3,3,3,4),
(2.16840434497101E-19,3.71309426656658E-6,5.39981071559397E-6,8.78933289368793E-6,
9.00272357067522E-6,1.0714398450415E-5,1.60780299679471E-5,1.65806081157687E-5,
2.30369726850326E-5,2.67819200416086E-5,3.59736924188203E-5,4.03862783807E-5),
 .UNSPECIFIED.);
#26532=B_SPLINE_CURVE_WITH_KNOTS('',3,(#438582,#438583,#438584,#438585),
 .UNSPECIFIED.,.F.,.F.,(4,4),(0.,7.7002563062924E-5),.UNSPECIFIED.);
#26533=B_SPLINE_CURVE_WITH_KNOTS('',3,(#438595,#438596,#438597,#438598),
 .UNSPECIFIED.,.F.,.F.,(4,4),(4.33680868994202E-19,7.70025630629233E-5),
 .UNSPECIFIED.);
#26534=B_SPLINE_CURVE_WITH_KNOTS('',3,(#438602,#438603,#438604,#438605,
#438606,#438607,#438608,#438609,#438610,#438611,#438612,#438613,#438614,
#438615,#438616,#438617,#438618,#438619,#438620,#438621,#438622,#438623,
#438624,#438625,#438626,#438627,#438628,#438629,#438630,#438631,#438632,
#438633,#438634,#438635,#438636,#438637,#438638),.UNSPECIFIED.,.F.,.F.,
(4,3,3,3,3,3,3,3,3,3,3,3,4),(0.,9.59031527199921E-6,1.94769411222901E-5,
2.02405092183154E-5,3.21374138577632E-5,3.60302195070441E-5,4.42640648818578E-5,
4.53660204229444E-5,5.03633762302122E-5,5.17708036292897E-5,5.37928993851991E-5,
5.541037554602E-5,5.64557889513533E-5),.UNSPECIFIED.);
#26535=B_SPLINE_CURVE_WITH_KNOTS('',3,(#438639,#438640,#438641,#438642,
#438643,#438644,#438645,#438646,#438647,#438648,#438649,#438650,#438651,
#438652,#438653,#438654,#438655,#438656,#438657,#438658,#438659,#438660,
#438661,#438662,#438663,#438664,#438665,#438666),.UNSPECIFIED.,.F.,.F.,
(4,3,3,3,3,3,3,3,3,4),(5.64557889513533E-5,5.98940966493752E-5,6.34214003873381E-5,
7.2224147608471E-5,7.38322796533365E-5,8.36529189331559E-5,8.807142782225E-5,
9.84837568501025E-5,0.000108624704079196,0.000110823272382853),
 .UNSPECIFIED.);
#26536=B_SPLINE_CURVE_WITH_KNOTS('',3,(#438682,#438683,#438684,#438685,
#438686,#438687,#438688,#438689,#438690,#438691,#438692,#438693,#438694,
#438695,#438696,#438697,#438698,#438699,#438700,#438701,#438702,#438703,
#438704,#438705,#438706,#438707,#438708,#438709),.UNSPECIFIED.,.F.,.F.,
(4,3,3,3,3,3,3,3,3,4),(0.,8.66039628578054E-6,1.64707715200668E-5,2.24502894132268E-5,
2.49975961757825E-5,2.88526003690282E-5,3.10661348995018E-5,3.43053543516961E-5,
3.66410545653559E-5,4.00504537627886E-5),.UNSPECIFIED.);
#26537=B_SPLINE_CURVE_WITH_KNOTS('',3,(#438712,#438713,#438714,#438715,
#438716,#438717,#438718),.UNSPECIFIED.,.F.,.F.,(4,3,4),(0.,4.4000004106538E-5,
9.89910850773115E-5),.UNSPECIFIED.);
#26538=B_SPLINE_CURVE_WITH_KNOTS('',3,(#438739,#438740,#438741,#438742,
#438743,#438744,#438745,#438746,#438747,#438748,#438749,#438750,#438751,
#438752,#438753,#438754,#438755,#438756,#438757,#438758,#438759,#438760,
#438761,#438762,#438763,#438764,#438765,#438766,#438767,#438768,#438769,
#438770,#438771,#438772),.UNSPECIFIED.,.F.,.F.,(4,3,3,3,3,3,3,3,3,3,3,4),
(0.,4.29157837304534E-6,5.42772623795311E-6,1.00901698482347E-5,1.31279195068639E-5,
1.57383542265917E-5,1.61011507492105E-5,1.67166789291755E-5,1.95343262811359E-5,
2.29377234674649E-5,2.71556047620057E-5,3.34407099942656E-5),
 .UNSPECIFIED.);
#26539=B_SPLINE_CURVE_WITH_KNOTS('',3,(#438785,#438786,#438787,#438788,
#438789,#438790,#438791,#438792,#438793,#438794,#438795,#438796,#438797,
#438798,#438799,#438800,#438801,#438802,#438803,#438804,#438805,#438806,
#438807,#438808,#438809,#438810,#438811,#438812,#438813,#438814,#438815,
#438816,#438817,#438818),.UNSPECIFIED.,.F.,.F.,(4,3,3,3,3,3,3,3,3,3,3,4),
(3.25260651745651E-19,3.71309426656627E-6,5.39981071559409E-6,8.78933289367001E-6,
9.00272357067521E-6,1.07143984504148E-5,1.60780299679545E-5,1.65806081157686E-5,
2.30369726850601E-5,2.67819200416085E-5,3.59736924187893E-5,4.03862783807E-5),
 .UNSPECIFIED.);
#26540=B_SPLINE_CURVE_WITH_KNOTS('',3,(#438931,#438932,#438933,#438934),
 .UNSPECIFIED.,.F.,.F.,(4,4),(0.,7.70025630629238E-5),.UNSPECIFIED.);
#26541=B_SPLINE_CURVE_WITH_KNOTS('',3,(#438944,#438945,#438946,#438947),
 .UNSPECIFIED.,.F.,.F.,(4,4),(4.47028007668187E-19,7.70025630629238E-5),
 .UNSPECIFIED.);
#26542=B_SPLINE_CURVE_WITH_KNOTS('',3,(#438951,#438952,#438953,#438954,
#438955,#438956,#438957,#438958,#438959,#438960,#438961,#438962,#438963,
#438964,#438965,#438966,#438967,#438968,#438969,#438970,#438971,#438972,
#438973,#438974,#438975,#438976,#438977,#438978,#438979,#438980,#438981,
#438982,#438983,#438984,#438985,#438986,#438987),.UNSPECIFIED.,.F.,.F.,
(4,3,3,3,3,3,3,3,3,3,3,3,4),(0.,9.59031527198971E-6,1.94769411222721E-5,
2.02405092183151E-5,3.2137413857768E-5,3.60302195070439E-5,4.42640648818942E-5,
4.53660204229443E-5,5.03633762302038E-5,5.17708036292894E-5,5.37928993851986E-5,
5.54103755460195E-5,5.64557889510681E-5),.UNSPECIFIED.);
#26543=B_SPLINE_CURVE_WITH_KNOTS('',3,(#438988,#438989,#438990,#438991,
#438992,#438993,#438994,#438995,#438996,#438997,#438998,#438999,#439000,
#439001,#439002,#439003,#439004,#439005,#439006,#439007,#439008,#439009,
#439010,#439011,#439012,#439013,#439014,#439015),.UNSPECIFIED.,.F.,.F.,
(4,3,3,3,3,3,3,3,3,4),(5.64557889510681E-5,5.98940966493749E-5,6.34214003873378E-5,
7.22241476084715E-5,7.38322796533362E-5,8.36529189331469E-5,8.80714278222497E-5,
9.84837568500673E-5,0.000108624704079129,0.000110823272382853),
 .UNSPECIFIED.);
#26544=B_SPLINE_CURVE_WITH_KNOTS('',3,(#439031,#439032,#439033,#439034,
#439035,#439036,#439037,#439038,#439039,#439040,#439041,#439042,#439043,
#439044,#439045,#439046,#439047,#439048,#439049,#439050,#439051,#439052,
#439053,#439054,#439055,#439056,#439057,#439058),.UNSPECIFIED.,.F.,.F.,
(4,3,3,3,3,3,3,3,3,4),(0.,8.66039628580409E-6,1.64707715200665E-5,2.24502894132433E-5,
2.49975961757824E-5,2.8852600369028E-5,3.10661348995016E-5,3.4305354351696E-5,
3.66410545653558E-5,4.00504537627886E-5),.UNSPECIFIED.);
#26545=B_SPLINE_CURVE_WITH_KNOTS('',3,(#439061,#439062,#439063,#439064,
#439065,#439066,#439067),.UNSPECIFIED.,.F.,.F.,(4,3,4),(0.,4.40000041065376E-5,
9.89910850773111E-5),.UNSPECIFIED.);
#26546=B_SPLINE_CURVE_WITH_KNOTS('',3,(#439088,#439089,#439090,#439091,
#439092,#439093,#439094,#439095,#439096,#439097,#439098,#439099,#439100,
#439101,#439102,#439103,#439104,#439105,#439106,#439107,#439108,#439109,
#439110,#439111,#439112,#439113,#439114,#439115,#439116,#439117,#439118,
#439119,#439120,#439121),.UNSPECIFIED.,.F.,.F.,(4,3,3,3,3,3,3,3,3,3,3,4),
(0.,4.2915783730258E-6,5.42772623795346E-6,1.00901698482349E-5,1.31279195068641E-5,
1.57383542265877E-5,1.61011507492107E-5,1.67166789291757E-5,1.9534326281136E-5,
2.29377234674651E-5,2.7155604762006E-5,3.34407099942659E-5),
 .UNSPECIFIED.);
#26547=B_SPLINE_CURVE_WITH_KNOTS('',3,(#439134,#439135,#439136,#439137,
#439138,#439139,#439140,#439141,#439142,#439143,#439144,#439145,#439146,
#439147,#439148,#439149,#439150,#439151,#439152,#439153,#439154,#439155,
#439156,#439157,#439158,#439159,#439160,#439161,#439162,#439163,#439164,
#439165,#439166,#439167),.UNSPECIFIED.,.F.,.F.,(4,3,3,3,3,3,3,3,3,3,3,4),
(1.0842021724855E-19,3.7130942665664E-6,5.39981071559421E-6,8.78933289366966E-6,
9.00272357067517E-6,1.07143984504149E-5,1.60780299679564E-5,1.65806081157687E-5,
2.30369726850369E-5,2.67819200416086E-5,3.59736924188085E-5,4.03862783807002E-5),
 .UNSPECIFIED.);
#26548=B_SPLINE_CURVE_WITH_KNOTS('',3,(#439280,#439281,#439282,#439283),
 .UNSPECIFIED.,.F.,.F.,(4,4),(0.,7.70025630629239E-5),.UNSPECIFIED.);
#26549=B_SPLINE_CURVE_WITH_KNOTS('',3,(#439293,#439294,#439295,#439296),
 .UNSPECIFIED.,.F.,.F.,(4,4),(4.37055868292169E-19,7.70025630629235E-5),
 .UNSPECIFIED.);
#26550=B_SPLINE_CURVE_WITH_KNOTS('',3,(#439300,#439301,#439302,#439303,
#439304,#439305,#439306,#439307,#439308,#439309,#439310,#439311,#439312,
#439313,#439314,#439315,#439316,#439317,#439318,#439319,#439320,#439321,
#439322,#439323,#439324,#439325,#439326,#439327,#439328,#439329,#439330,
#439331,#439332,#439333,#439334,#439335,#439336),.UNSPECIFIED.,.F.,.F.,
(4,3,3,3,3,3,3,3,3,3,3,3,4),(0.,9.59031527199935E-6,1.94769411222823E-5,
2.02405092183153E-5,3.21374138577703E-5,3.60302195070441E-5,4.4264064881889E-5,
4.53660204229445E-5,5.03633762302015E-5,5.17708036292898E-5,5.3792899385199E-5,
5.541037554602E-5,5.64557889510303E-5),.UNSPECIFIED.);
#26551=B_SPLINE_CURVE_WITH_KNOTS('',3,(#439337,#439338,#439339,#439340,
#439341,#439342,#439343,#439344,#439345,#439346,#439347,#439348,#439349,
#439350,#439351,#439352,#439353,#439354,#439355,#439356,#439357,#439358,
#439359,#439360,#439361,#439362,#439363,#439364),.UNSPECIFIED.,.F.,.F.,
(4,3,3,3,3,3,3,3,3,4),(5.64557889510303E-5,5.98940966493752E-5,6.34214003873382E-5,
7.22241476084422E-5,7.38322796533368E-5,8.36529189331455E-5,8.80714278222503E-5,
9.8483756850078E-5,0.000108624704079147,0.000110823272382854),
 .UNSPECIFIED.);
#26552=B_SPLINE_CURVE_WITH_KNOTS('',3,(#439380,#439381,#439382,#439383,
#439384,#439385,#439386,#439387,#439388,#439389,#439390,#439391,#439392,
#439393,#439394,#439395,#439396,#439397,#439398,#439399,#439400,#439401,
#439402,#439403,#439404,#439405,#439406,#439407),.UNSPECIFIED.,.F.,.F.,
(4,3,3,3,3,3,3,3,3,4),(0.,8.66039628584726E-6,1.64707715200667E-5,2.2450289413223E-5,
2.49975961757824E-5,2.88526003690281E-5,3.10661348995017E-5,3.43053543516961E-5,
3.66410545653559E-5,4.00504537627887E-5),.UNSPECIFIED.);
#26553=B_SPLINE_CURVE_WITH_KNOTS('',3,(#439410,#439411,#439412,#439413,
#439414,#439415,#439416),.UNSPECIFIED.,.F.,.F.,(4,3,4),(0.,4.40000041065376E-5,
9.89910850773114E-5),.UNSPECIFIED.);
#26554=B_SPLINE_CURVE_WITH_KNOTS('',3,(#439437,#439438,#439439,#439440,
#439441,#439442,#439443,#439444,#439445,#439446,#439447,#439448,#439449,
#439450,#439451,#439452,#439453,#439454,#439455,#439456,#439457,#439458,
#439459,#439460,#439461,#439462,#439463,#439464,#439465,#439466,#439467,
#439468,#439469,#439470),.UNSPECIFIED.,.F.,.F.,(4,3,3,3,3,3,3,3,3,3,3,4),
(0.,4.29157837304442E-6,5.42772623795332E-6,1.00901698482346E-5,1.31279195068639E-5,
1.57383542265886E-5,1.61011507492104E-5,1.67166789291752E-5,1.95343262811359E-5,
2.29377234674649E-5,2.71556047620057E-5,3.34407099942661E-5),
 .UNSPECIFIED.);
#26555=B_SPLINE_CURVE_WITH_KNOTS('',3,(#439483,#439484,#439485,#439486,
#439487,#439488,#439489,#439490,#439491,#439492,#439493,#439494,#439495,
#439496,#439497,#439498,#439499,#439500,#439501,#439502,#439503,#439504,
#439505,#439506,#439507,#439508,#439509,#439510,#439511,#439512,#439513,
#439514,#439515,#439516),.UNSPECIFIED.,.F.,.F.,(4,3,3,3,3,3,3,3,3,3,3,4),
(1.0842021724855E-19,3.71309426656646E-6,5.39981071559411E-6,8.78933289331216E-6,
9.00272357067517E-6,1.07143984504148E-5,1.60780299679535E-5,1.65806081157685E-5,
2.30369726850261E-5,2.67819200416085E-5,3.59736924187453E-5,4.03862783806999E-5),
 .UNSPECIFIED.);
#26556=B_SPLINE_CURVE_WITH_KNOTS('',3,(#439629,#439630,#439631,#439632),
 .UNSPECIFIED.,.F.,.F.,(4,4),(0.,7.7002563062924E-5),.UNSPECIFIED.);
#26557=B_SPLINE_CURVE_WITH_KNOTS('',3,(#439642,#439643,#439644,#439645),
 .UNSPECIFIED.,.F.,.F.,(4,4),(4.41238316394827E-19,7.70025630629232E-5),
 .UNSPECIFIED.);
#26558=B_SPLINE_CURVE_WITH_KNOTS('',3,(#439649,#439650,#439651,#439652,
#439653,#439654,#439655,#439656,#439657,#439658,#439659,#439660,#439661,
#439662,#439663,#439664,#439665,#439666,#439667,#439668,#439669,#439670,
#439671,#439672,#439673,#439674,#439675,#439676,#439677,#439678,#439679,
#439680,#439681,#439682,#439683,#439684,#439685),.UNSPECIFIED.,.F.,.F.,
(4,3,3,3,3,3,3,3,3,3,3,3,4),(0.,9.59031527201392E-6,1.94769411223066E-5,
2.02405092183155E-5,3.2137413857776E-5,3.60302195070442E-5,4.42640648817747E-5,
4.53660204229446E-5,5.03633762302201E-5,5.17708036292898E-5,5.37928993851991E-5,
5.54103755460201E-5,5.64557889513918E-5),.UNSPECIFIED.);
#26559=B_SPLINE_CURVE_WITH_KNOTS('',3,(#439686,#439687,#439688,#439689,
#439690,#439691,#439692,#439693,#439694,#439695,#439696,#439697,#439698,
#439699,#439700,#439701,#439702,#439703,#439704,#439705,#439706,#439707,
#439708,#439709,#439710,#439711,#439712,#439713),.UNSPECIFIED.,.F.,.F.,
(4,3,3,3,3,3,3,3,3,4),(5.64557889513918E-5,5.98940966493753E-5,6.34214003873382E-5,
7.22241476084647E-5,7.38322796533367E-5,8.36529189331493E-5,8.80714278222502E-5,
9.84837568500753E-5,0.000108624704079138,0.000110823272382854),
 .UNSPECIFIED.);
#26560=B_SPLINE_CURVE_WITH_KNOTS('',3,(#439729,#439730,#439731,#439732,
#439733,#439734,#439735,#439736,#439737,#439738,#439739,#439740,#439741,
#439742,#439743,#439744,#439745,#439746,#439747,#439748,#439749,#439750,
#439751,#439752,#439753,#439754,#439755,#439756),.UNSPECIFIED.,.F.,.F.,
(4,3,3,3,3,3,3,3,3,4),(0.,8.6603962857847E-6,1.64707715200667E-5,2.24502894132614E-5,
2.49975961757825E-5,2.88526003690281E-5,3.10661348995017E-5,3.43053543516961E-5,
3.66410545653559E-5,4.00504537627886E-5),.UNSPECIFIED.);
#26561=B_SPLINE_CURVE_WITH_KNOTS('',3,(#439759,#439760,#439761,#439762,
#439763,#439764,#439765),.UNSPECIFIED.,.F.,.F.,(4,3,4),(0.,4.40000041065375E-5,
9.89910850773112E-5),.UNSPECIFIED.);
#26562=B_SPLINE_CURVE_WITH_KNOTS('',3,(#439786,#439787,#439788,#439789,
#439790,#439791,#439792,#439793,#439794,#439795,#439796,#439797,#439798,
#439799,#439800,#439801,#439802,#439803,#439804,#439805,#439806,#439807,
#439808,#439809,#439810,#439811,#439812,#439813,#439814,#439815,#439816,
#439817,#439818,#439819),.UNSPECIFIED.,.F.,.F.,(4,3,3,3,3,3,3,3,3,3,3,4),
(0.,4.29157837304389E-6,5.42772623795354E-6,1.0090169848235E-5,1.31279195068641E-5,
1.57383542265878E-5,1.61011507492106E-5,1.67166789291757E-5,1.9534326281136E-5,
2.2937723467465E-5,2.71556047620059E-5,3.3440709994266E-5),
 .UNSPECIFIED.);
#26563=B_SPLINE_CURVE_WITH_KNOTS('',3,(#439832,#439833,#439834,#439835,
#439836,#439837,#439838,#439839,#439840,#439841,#439842,#439843,#439844,
#439845,#439846,#439847,#439848,#439849,#439850,#439851,#439852,#439853,
#439854,#439855,#439856,#439857,#439858,#439859,#439860,#439861,#439862,
#439863,#439864,#439865),.UNSPECIFIED.,.F.,.F.,(4,3,3,3,3,3,3,3,3,3,3,4),
(8.13151629364128E-20,3.71309426656647E-6,5.39981071559418E-6,8.78933289332817E-6,
9.0027235706752E-6,1.07143984504149E-5,1.60780299679466E-5,1.65806081157687E-5,
2.30369726850553E-5,2.67819200416087E-5,3.59736924187626E-5,4.03862783807002E-5),
 .UNSPECIFIED.);
#26564=B_SPLINE_CURVE_WITH_KNOTS('',3,(#439978,#439979,#439980,#439981),
 .UNSPECIFIED.,.F.,.F.,(4,4),(0.,7.70025630629236E-5),.UNSPECIFIED.);
#26565=B_SPLINE_CURVE_WITH_KNOTS('',3,(#439991,#439992,#439993,#439994),
 .UNSPECIFIED.,.F.,.F.,(4,4),(4.47028007668187E-19,7.70025630629236E-5),
 .UNSPECIFIED.);
#26566=B_SPLINE_CURVE_WITH_KNOTS('',3,(#439998,#439999,#440000,#440001,
#440002,#440003,#440004,#440005,#440006,#440007,#440008,#440009,#440010,
#440011,#440012,#440013,#440014,#440015,#440016,#440017,#440018,#440019,
#440020,#440021,#440022,#440023,#440024,#440025,#440026,#440027,#440028,
#440029,#440030,#440031,#440032,#440033,#440034),.UNSPECIFIED.,.F.,.F.,
(4,3,3,3,3,3,3,3,3,3,3,3,4),(0.,9.59031527201329E-6,1.94769411223138E-5,
2.02405092183152E-5,3.21374138577644E-5,3.6030219507044E-5,4.42640648818663E-5,
4.53660204229444E-5,5.03633762301941E-5,5.17708036292896E-5,5.37928993851989E-5,
5.54103755460198E-5,5.64557889511221E-5),.UNSPECIFIED.);
#26567=B_SPLINE_CURVE_WITH_KNOTS('',3,(#440035,#440036,#440037,#440038,
#440039,#440040,#440041,#440042,#440043,#440044,#440045,#440046,#440047,
#440048,#440049,#440050,#440051,#440052,#440053,#440054,#440055,#440056,
#440057,#440058,#440059,#440060,#440061,#440062),.UNSPECIFIED.,.F.,.F.,
(4,3,3,3,3,3,3,3,3,4),(5.64557889511221E-5,5.98940966493751E-5,6.34214003873381E-5,
7.22241476084529E-5,7.38322796533365E-5,8.36529189331292E-5,8.807142782225E-5,
9.84837568500623E-5,0.000108624704079134,0.000110823272382854),
 .UNSPECIFIED.);
#26568=B_SPLINE_CURVE_WITH_KNOTS('',3,(#440078,#440079,#440080,#440081,
#440082,#440083,#440084,#440085,#440086,#440087,#440088,#440089,#440090,
#440091,#440092,#440093,#440094,#440095,#440096,#440097,#440098,#440099,
#440100,#440101,#440102,#440103,#440104,#440105),.UNSPECIFIED.,.F.,.F.,
(4,3,3,3,3,3,3,3,3,4),(0.,8.66039628583239E-6,1.64707715200667E-5,2.24502894132358E-5,
2.49975961757824E-5,2.88526003690281E-5,3.10661348995017E-5,3.43053543516961E-5,
3.66410545653561E-5,4.00504537627891E-5),.UNSPECIFIED.);
#26569=B_SPLINE_CURVE_WITH_KNOTS('',3,(#440108,#440109,#440110,#440111,
#440112,#440113,#440114),.UNSPECIFIED.,.F.,.F.,(4,3,4),(0.,4.40000041065376E-5,
9.89910850773112E-5),.UNSPECIFIED.);
#26570=B_SPLINE_CURVE_WITH_KNOTS('',3,(#440135,#440136,#440137,#440138,
#440139,#440140,#440141,#440142,#440143,#440144,#440145,#440146,#440147,
#440148,#440149,#440150,#440151,#440152,#440153,#440154,#440155,#440156,
#440157,#440158,#440159,#440160,#440161,#440162,#440163,#440164,#440165,
#440166,#440167,#440168),.UNSPECIFIED.,.F.,.F.,(4,3,3,3,3,3,3,3,3,3,3,4),
(0.,4.2915783730137E-6,5.42772623795345E-6,1.00901698482348E-5,1.31279195068639E-5,
1.57383542265848E-5,1.61011507492105E-5,1.67166789291754E-5,1.95343262811359E-5,
2.29377234674649E-5,2.71556047620058E-5,3.34407099942659E-5),
 .UNSPECIFIED.);
#26571=B_SPLINE_CURVE_WITH_KNOTS('',3,(#440181,#440182,#440183,#440184,
#440185,#440186,#440187,#440188,#440189,#440190,#440191,#440192,#440193,
#440194,#440195,#440196,#440197,#440198,#440199,#440200,#440201,#440202,
#440203,#440204,#440205,#440206,#440207,#440208,#440209,#440210,#440211,
#440212,#440213,#440214),.UNSPECIFIED.,.F.,.F.,(4,3,3,3,3,3,3,3,3,3,3,4),
(8.13151629364128E-20,3.71309426656648E-6,5.39981071559416E-6,8.78933289331532E-6,
9.00272357067522E-6,1.07143984504149E-5,1.60780299679582E-5,1.65806081157687E-5,
2.30369726850442E-5,2.67819200416087E-5,3.5973692418805E-5,4.03862783807002E-5),
 .UNSPECIFIED.);
#26572=B_SPLINE_CURVE_WITH_KNOTS('',3,(#440327,#440328,#440329,#440330),
 .UNSPECIFIED.,.F.,.F.,(4,4),(0.,7.70025630629243E-5),.UNSPECIFIED.);
#26573=B_SPLINE_CURVE_WITH_KNOTS('',3,(#440340,#440341,#440342,#440343),
 .UNSPECIFIED.,.F.,.F.,(4,4),(1.0842021724855E-19,7.70025630629239E-5),
 .UNSPECIFIED.);
#26574=B_SPLINE_CURVE_WITH_KNOTS('',3,(#440347,#440348,#440349,#440350,
#440351,#440352,#440353,#440354,#440355,#440356,#440357,#440358,#440359,
#440360,#440361,#440362,#440363,#440364,#440365,#440366,#440367,#440368,
#440369,#440370,#440371,#440372,#440373,#440374,#440375,#440376,#440377,
#440378,#440379,#440380,#440381,#440382,#440383),.UNSPECIFIED.,.F.,.F.,
(4,3,3,3,3,3,3,3,3,3,3,3,4),(0.,9.59031527198821E-6,1.94769411222708E-5,
2.0240509218315E-5,3.21374138577731E-5,3.60302195070438E-5,4.42640648818033E-5,
4.53660204229442E-5,5.03633762302213E-5,5.17708036292894E-5,5.37928993851987E-5,
5.54103755460196E-5,5.64557889510612E-5),.UNSPECIFIED.);
#26575=B_SPLINE_CURVE_WITH_KNOTS('',3,(#440384,#440385,#440386,#440387,
#440388,#440389,#440390,#440391,#440392,#440393,#440394,#440395,#440396,
#440397,#440398,#440399,#440400,#440401,#440402,#440403,#440404,#440405,
#440406,#440407,#440408,#440409,#440410,#440411),.UNSPECIFIED.,.F.,.F.,
(4,3,3,3,3,3,3,3,3,4),(5.64557889510612E-5,5.9894096649375E-5,6.34214003873378E-5,
7.22241476084378E-5,7.38322796533361E-5,8.36529189331501E-5,8.80714278222497E-5,
9.84837568500782E-5,0.00010862470407915,0.000110823272382853),
 .UNSPECIFIED.);
#26576=B_SPLINE_CURVE_WITH_KNOTS('',3,(#440427,#440428,#440429,#440430,
#440431,#440432,#440433,#440434,#440435,#440436,#440437,#440438,#440439,
#440440,#440441,#440442,#440443,#440444,#440445,#440446,#440447,#440448,
#440449,#440450,#440451,#440452,#440453,#440454),.UNSPECIFIED.,.F.,.F.,
(4,3,3,3,3,3,3,3,3,4),(0.,8.66039628581255E-6,1.64707715200667E-5,2.24502894132374E-5,
2.49975961757822E-5,2.8852600369028E-5,3.10661348995016E-5,3.43053543516961E-5,
3.6641054565356E-5,4.00504537627891E-5),.UNSPECIFIED.);
#26577=B_SPLINE_CURVE_WITH_KNOTS('',3,(#440457,#440458,#440459,#440460,
#440461,#440462,#440463),.UNSPECIFIED.,.F.,.F.,(4,3,4),(0.,4.40000041065373E-5,
9.89910850773114E-5),.UNSPECIFIED.);
#26578=B_SPLINE_CURVE_WITH_KNOTS('',3,(#440484,#440485,#440486,#440487,
#440488,#440489,#440490,#440491,#440492,#440493,#440494,#440495,#440496,
#440497,#440498,#440499,#440500,#440501,#440502,#440503,#440504,#440505,
#440506,#440507,#440508,#440509,#440510,#440511,#440512,#440513,#440514,
#440515,#440516,#440517),.UNSPECIFIED.,.F.,.F.,(4,3,3,3,3,3,3,3,3,3,3,4),
(0.,4.2915783730491E-6,5.42772623795335E-6,1.00901698482346E-5,1.31279195068638E-5,
1.57383542265797E-5,1.61011507492104E-5,1.67166789291761E-5,1.95343262811359E-5,
2.2937723467465E-5,2.71556047620059E-5,3.34407099942659E-5),
 .UNSPECIFIED.);
#26579=B_SPLINE_CURVE_WITH_KNOTS('',3,(#440530,#440531,#440532,#440533,
#440534,#440535,#440536,#440537,#440538,#440539,#440540,#440541,#440542,
#440543,#440544,#440545,#440546,#440547,#440548,#440549,#440550,#440551,
#440552,#440553,#440554,#440555,#440556,#440557,#440558,#440559,#440560,
#440561,#440562,#440563),.UNSPECIFIED.,.F.,.F.,(4,3,3,3,3,3,3,3,3,3,3,4),
(1.0842021724855E-19,3.71309426656638E-6,5.39981071559417E-6,8.78933289369073E-6,
9.00272357067512E-6,1.07143984504148E-5,1.6078029967961E-5,1.65806081157686E-5,
2.30369726850332E-5,2.67819200416086E-5,3.5973692418783E-5,4.03862783806998E-5),
 .UNSPECIFIED.);
#26580=B_SPLINE_CURVE_WITH_KNOTS('',3,(#440676,#440677,#440678,#440679),
 .UNSPECIFIED.,.F.,.F.,(4,4),(0.,7.70025630629237E-5),.UNSPECIFIED.);
#26581=B_SPLINE_CURVE_WITH_KNOTS('',3,(#440689,#440690,#440691,#440692),
 .UNSPECIFIED.,.F.,.F.,(4,4),(1.0842021724855E-19,7.70025630629236E-5),
 .UNSPECIFIED.);
#26582=B_SPLINE_CURVE_WITH_KNOTS('',3,(#440696,#440697,#440698,#440699,
#440700,#440701,#440702,#440703,#440704,#440705,#440706,#440707,#440708,
#440709,#440710,#440711,#440712,#440713,#440714,#440715,#440716,#440717,
#440718,#440719,#440720,#440721,#440722,#440723,#440724,#440725,#440726,
#440727,#440728,#440729,#440730,#440731,#440732),.UNSPECIFIED.,.F.,.F.,
(4,3,3,3,3,3,3,3,3,3,3,3,4),(0.,9.59031527199807E-6,1.94769411222929E-5,
2.02405092183153E-5,3.21374138577713E-5,3.60302195070441E-5,4.42640648819238E-5,
4.53660204229445E-5,5.03633762301965E-5,5.17708036292898E-5,5.37928993851992E-5,
5.54103755460202E-5,5.64557889512322E-5),.UNSPECIFIED.);
#26583=B_SPLINE_CURVE_WITH_KNOTS('',3,(#440733,#440734,#440735,#440736,
#440737,#440738,#440739,#440740,#440741,#440742,#440743,#440744,#440745,
#440746,#440747,#440748,#440749,#440750,#440751,#440752,#440753,#440754,
#440755,#440756,#440757,#440758,#440759,#440760),.UNSPECIFIED.,.F.,.F.,
(4,3,3,3,3,3,3,3,3,4),(5.64557889512322E-5,5.98940966493754E-5,6.34214003873382E-5,
7.22241476084645E-5,7.38322796533368E-5,8.36529189331482E-5,8.80714278222504E-5,
9.84837568500693E-5,0.000108624704079132,0.000110823272382854),
 .UNSPECIFIED.);
#26584=B_SPLINE_CURVE_WITH_KNOTS('',3,(#440776,#440777,#440778,#440779,
#440780,#440781,#440782,#440783,#440784,#440785,#440786,#440787,#440788,
#440789,#440790,#440791,#440792,#440793,#440794,#440795,#440796,#440797,
#440798,#440799,#440800,#440801,#440802,#440803),.UNSPECIFIED.,.F.,.F.,
(4,3,3,3,3,3,3,3,3,4),(0.,8.66039628580622E-6,1.64707715200666E-5,2.24502894132216E-5,
2.49975961757823E-5,2.8852600369028E-5,3.10661348995015E-5,3.43053543516959E-5,
3.66410545653559E-5,4.00504537627886E-5),.UNSPECIFIED.);
#26585=B_SPLINE_CURVE_WITH_KNOTS('',3,(#440806,#440807,#440808,#440809,
#440810,#440811,#440812),.UNSPECIFIED.,.F.,.F.,(4,3,4),(0.,4.40000041065376E-5,
9.89910850773115E-5),.UNSPECIFIED.);
#26586=B_SPLINE_CURVE_WITH_KNOTS('',3,(#440833,#440834,#440835,#440836,
#440837,#440838,#440839,#440840,#440841,#440842,#440843,#440844,#440845,
#440846,#440847,#440848,#440849,#440850,#440851,#440852,#440853,#440854,
#440855,#440856,#440857,#440858,#440859,#440860,#440861,#440862,#440863,
#440864,#440865,#440866),.UNSPECIFIED.,.F.,.F.,(4,3,3,3,3,3,3,3,3,3,3,4),
(0.,4.29157837304607E-6,5.4277262379532E-6,1.00901698482346E-5,1.31279195068638E-5,
1.57383542265904E-5,1.61011507492105E-5,1.67166789291756E-5,1.95343262811358E-5,
2.29377234674647E-5,2.71556047620058E-5,3.34407099942655E-5),
 .UNSPECIFIED.);
#26587=B_SPLINE_CURVE_WITH_KNOTS('',3,(#440879,#440880,#440881,#440882,
#440883,#440884,#440885,#440886,#440887,#440888,#440889,#440890,#440891,
#440892,#440893,#440894,#440895,#440896,#440897,#440898,#440899,#440900,
#440901,#440902,#440903,#440904,#440905,#440906,#440907,#440908,#440909,
#440910,#440911,#440912),.UNSPECIFIED.,.F.,.F.,(4,3,3,3,3,3,3,3,3,3,3,4),
(1.0842021724855E-19,3.71309426656633E-6,5.39981071559412E-6,8.78933289368465E-6,
9.00272357067514E-6,1.07143984504148E-5,1.60780299679548E-5,1.65806081157686E-5,
2.30369726850478E-5,2.67819200416084E-5,3.59736924187961E-5,4.03862783806998E-5),
 .UNSPECIFIED.);
#26588=B_SPLINE_CURVE_WITH_KNOTS('',3,(#441025,#441026,#441027,#441028),
 .UNSPECIFIED.,.F.,.F.,(4,4),(0.,7.70025630629242E-5),.UNSPECIFIED.);
#26589=B_SPLINE_CURVE_WITH_KNOTS('',3,(#441038,#441039,#441040,#441041),
 .UNSPECIFIED.,.F.,.F.,(4,4),(1.0842021724855E-19,7.7002563062924E-5),
 .UNSPECIFIED.);
#26590=B_SPLINE_CURVE_WITH_KNOTS('',3,(#441045,#441046,#441047,#441048,
#441049,#441050,#441051,#441052,#441053,#441054,#441055,#441056,#441057,
#441058,#441059,#441060,#441061,#441062,#441063,#441064,#441065,#441066,
#441067,#441068,#441069,#441070,#441071,#441072,#441073,#441074,#441075,
#441076,#441077,#441078,#441079,#441080,#441081),.UNSPECIFIED.,.F.,.F.,
(4,3,3,3,3,3,3,3,3,3,3,3,4),(0.,9.59031527199008E-6,1.94769411222735E-5,
2.02405092183149E-5,3.21374138577699E-5,3.60302195070437E-5,4.42640648818485E-5,
4.53660204229443E-5,5.03633762302068E-5,5.17708036292895E-5,5.37928993851988E-5,
5.54103755460198E-5,5.64557889509075E-5),.UNSPECIFIED.);
#26591=B_SPLINE_CURVE_WITH_KNOTS('',3,(#441082,#441083,#441084,#441085,
#441086,#441087,#441088,#441089,#441090,#441091,#441092,#441093,#441094,
#441095,#441096,#441097,#441098,#441099,#441100,#441101,#441102,#441103,
#441104,#441105,#441106,#441107,#441108,#441109),.UNSPECIFIED.,.F.,.F.,
(4,3,3,3,3,3,3,3,3,4),(5.64557889509075E-5,5.98940966493748E-5,6.34214003873379E-5,
7.22241476084888E-5,7.38322796533363E-5,8.36529189331411E-5,8.807142782225E-5,
9.84837568500729E-5,0.000108624704079144,0.000110823272382854),
 .UNSPECIFIED.);
#26592=B_SPLINE_CURVE_WITH_KNOTS('',3,(#441125,#441126,#441127,#441128,
#441129,#441130,#441131,#441132,#441133,#441134,#441135,#441136,#441137,
#441138,#441139,#441140,#441141,#441142,#441143,#441144,#441145,#441146,
#441147,#441148,#441149,#441150,#441151,#441152),.UNSPECIFIED.,.F.,.F.,
(4,3,3,3,3,3,3,3,3,4),(0.,8.66039628583705E-6,1.64707715200666E-5,2.24502894132194E-5,
2.49975961757824E-5,2.8852600369028E-5,3.10661348995015E-5,3.4305354351696E-5,
3.66410545653558E-5,4.00504537627885E-5),.UNSPECIFIED.);
#26593=B_SPLINE_CURVE_WITH_KNOTS('',3,(#441155,#441156,#441157,#441158,
#441159,#441160,#441161),.UNSPECIFIED.,.F.,.F.,(4,3,4),(0.,4.40000041065375E-5,
9.89910850773112E-5),.UNSPECIFIED.);
#26594=B_SPLINE_CURVE_WITH_KNOTS('',3,(#441182,#441183,#441184,#441185,
#441186,#441187,#441188,#441189,#441190,#441191,#441192,#441193,#441194,
#441195,#441196,#441197,#441198,#441199,#441200,#441201,#441202,#441203,
#441204,#441205,#441206,#441207,#441208,#441209,#441210,#441211,#441212,
#441213,#441214,#441215),.UNSPECIFIED.,.F.,.F.,(4,3,3,3,3,3,3,3,3,3,3,4),
(0.,4.29157837302068E-6,5.42772623795361E-6,1.00901698482348E-5,1.31279195068639E-5,
1.57383542265845E-5,1.61011507492104E-5,1.67166789291762E-5,1.95343262811359E-5,
2.29377234674648E-5,2.71556047620061E-5,3.34407099942661E-5),
 .UNSPECIFIED.);
#26595=B_SPLINE_CURVE_WITH_KNOTS('',3,(#441228,#441229,#441230,#441231,
#441232,#441233,#441234,#441235,#441236,#441237,#441238,#441239,#441240,
#441241,#441242,#441243,#441244,#441245,#441246,#441247,#441248,#441249,
#441250,#441251,#441252,#441253,#441254,#441255,#441256,#441257,#441258,
#441259,#441260,#441261),.UNSPECIFIED.,.F.,.F.,(4,3,3,3,3,3,3,3,3,3,3,4),
(1.0842021724855E-19,3.71309426656657E-6,5.3998107155941E-6,8.7893328936576E-6,
9.00272357067521E-6,1.0714398450415E-5,1.60780299679475E-5,1.65806081157686E-5,
2.30369726850495E-5,2.67819200416085E-5,3.59736924187832E-5,4.03862783806998E-5),
 .UNSPECIFIED.);
#26596=B_SPLINE_CURVE_WITH_KNOTS('',3,(#441374,#441375,#441376,#441377),
 .UNSPECIFIED.,.F.,.F.,(4,4),(0.,7.70025630629242E-5),.UNSPECIFIED.);
#26597=B_SPLINE_CURVE_WITH_KNOTS('',3,(#441387,#441388,#441389,#441390),
 .UNSPECIFIED.,.F.,.F.,(4,4),(2.16840434497101E-19,7.70025630629237E-5),
 .UNSPECIFIED.);
#26598=B_SPLINE_CURVE_WITH_KNOTS('',3,(#441394,#441395,#441396,#441397,
#441398,#441399,#441400,#441401,#441402,#441403,#441404,#441405,#441406,
#441407,#441408,#441409,#441410,#441411,#441412,#441413,#441414,#441415,
#441416,#441417,#441418,#441419,#441420,#441421,#441422,#441423,#441424,
#441425,#441426,#441427,#441428,#441429,#441430),.UNSPECIFIED.,.F.,.F.,
(4,3,3,3,3,3,3,3,3,3,3,3,4),(0.,9.59031527197619E-6,1.94769411222538E-5,
2.02405092183151E-5,3.21374138577715E-5,3.60302195070438E-5,4.42640648818347E-5,
4.53660204229442E-5,5.03633762302098E-5,5.17708036292895E-5,5.37928993851989E-5,
5.54103755460198E-5,5.64557889502042E-5),.UNSPECIFIED.);
#26599=B_SPLINE_CURVE_WITH_KNOTS('',3,(#441431,#441432,#441433,#441434,
#441435,#441436,#441437,#441438,#441439,#441440,#441441,#441442,#441443,
#441444,#441445,#441446,#441447,#441448,#441449,#441450,#441451,#441452,
#441453,#441454,#441455,#441456,#441457,#441458),.UNSPECIFIED.,.F.,.F.,
(4,3,3,3,3,3,3,3,3,4),(5.64557889502042E-5,5.9894096649375E-5,6.3421400387338E-5,
7.22241476084978E-5,7.38322796533364E-5,8.36529189331515E-5,8.80714278222499E-5,
9.84837568500678E-5,0.00010862470407913,0.000110823272382853),
 .UNSPECIFIED.);
#26600=B_SPLINE_CURVE_WITH_KNOTS('',3,(#441474,#441475,#441476,#441477,
#441478,#441479,#441480,#441481,#441482,#441483,#441484,#441485,#441486,
#441487,#441488,#441489,#441490,#441491,#441492,#441493,#441494,#441495,
#441496,#441497,#441498,#441499,#441500,#441501),.UNSPECIFIED.,.F.,.F.,
(4,3,3,3,3,3,3,3,3,4),(0.,8.66039628578315E-6,1.64707715200666E-5,2.24502894132418E-5,
2.49975961757825E-5,2.88526003690282E-5,3.10661348995018E-5,3.43053543516961E-5,
3.66410545653561E-5,4.00504537627891E-5),.UNSPECIFIED.);
#26601=B_SPLINE_CURVE_WITH_KNOTS('',3,(#441504,#441505,#441506,#441507,
#441508,#441509,#441510),.UNSPECIFIED.,.F.,.F.,(4,3,4),(0.,4.40000041065374E-5,
9.89910850773113E-5),.UNSPECIFIED.);
#26602=B_SPLINE_CURVE_WITH_KNOTS('',3,(#441531,#441532,#441533,#441534,
#441535,#441536,#441537,#441538,#441539,#441540,#441541,#441542,#441543,
#441544,#441545,#441546,#441547,#441548,#441549,#441550,#441551,#441552,
#441553,#441554,#441555,#441556,#441557,#441558,#441559,#441560,#441561,
#441562,#441563,#441564),.UNSPECIFIED.,.F.,.F.,(4,3,3,3,3,3,3,3,3,3,3,4),
(0.,4.29157837302783E-6,5.42772623795327E-6,1.00901698482347E-5,1.31279195068638E-5,
1.57383542265772E-5,1.61011507492103E-5,1.67166789291755E-5,1.95343262811356E-5,
2.29377234674647E-5,2.71556047620059E-5,3.34407099942655E-5),
 .UNSPECIFIED.);
#26603=B_SPLINE_CURVE_WITH_KNOTS('',3,(#441577,#441578,#441579,#441580,
#441581,#441582,#441583,#441584,#441585,#441586,#441587,#441588,#441589,
#441590,#441591,#441592,#441593,#441594,#441595,#441596,#441597,#441598,
#441599,#441600,#441601,#441602,#441603,#441604,#441605,#441606,#441607,
#441608,#441609,#441610),.UNSPECIFIED.,.F.,.F.,(4,3,3,3,3,3,3,3,3,3,3,4),
(0.,3.71309426656659E-6,5.39981071559433E-6,8.78933289366048E-6,9.00272357067536E-6,
1.0714398450415E-5,1.60780299679548E-5,1.65806081157688E-5,2.3036972685049E-5,
2.67819200416087E-5,3.59736924187513E-5,4.03862783807003E-5),
 .UNSPECIFIED.);
#26604=B_SPLINE_CURVE_WITH_KNOTS('',3,(#441723,#441724,#441725,#441726),
 .UNSPECIFIED.,.F.,.F.,(4,4),(0.,7.70025630629239E-5),.UNSPECIFIED.);
#26605=B_SPLINE_CURVE_WITH_KNOTS('',3,(#441736,#441737,#441738,#441739),
 .UNSPECIFIED.,.F.,.F.,(4,4),(2.16840434497101E-19,7.70025630629239E-5),
 .UNSPECIFIED.);
#26606=B_SPLINE_CURVE_WITH_KNOTS('',3,(#441743,#441744,#441745,#441746,
#441747,#441748,#441749,#441750,#441751,#441752,#441753,#441754,#441755,
#441756,#441757,#441758,#441759,#441760,#441761,#441762,#441763,#441764,
#441765,#441766,#441767,#441768,#441769,#441770,#441771,#441772,#441773,
#441774,#441775,#441776,#441777,#441778,#441779),.UNSPECIFIED.,.F.,.F.,
(4,3,3,3,3,3,3,3,3,3,3,3,4),(0.,9.59031527200763E-6,1.94769411223023E-5,
2.02405092183151E-5,3.21374138577724E-5,3.60302195070439E-5,4.4264064881911E-5,
4.53660204229445E-5,5.03633762301955E-5,5.17708036292899E-5,5.37928993851988E-5,
5.541037554602E-5,5.64557889510721E-5),.UNSPECIFIED.);
#26607=B_SPLINE_CURVE_WITH_KNOTS('',3,(#441780,#441781,#441782,#441783,
#441784,#441785,#441786,#441787,#441788,#441789,#441790,#441791,#441792,
#441793,#441794,#441795,#441796,#441797,#441798,#441799,#441800,#441801,
#441802,#441803,#441804,#441805,#441806,#441807),.UNSPECIFIED.,.F.,.F.,
(4,3,3,3,3,3,3,3,3,4),(5.64557889510721E-5,5.98940966493751E-5,6.34214003873383E-5,
7.2224147608454E-5,7.38322796533366E-5,8.36529189331437E-5,8.80714278222502E-5,
9.84837568500657E-5,0.000108624704079128,0.000110823272382854),
 .UNSPECIFIED.);
#26608=B_SPLINE_CURVE_WITH_KNOTS('',3,(#441823,#441824,#441825,#441826,
#441827,#441828,#441829,#441830,#441831,#441832,#441833,#441834,#441835,
#441836,#441837,#441838,#441839,#441840,#441841,#441842,#441843,#441844,
#441845,#441846,#441847,#441848,#441849,#441850),.UNSPECIFIED.,.F.,.F.,
(4,3,3,3,3,3,3,3,3,4),(0.,8.66039628584837E-6,1.64707715200667E-5,2.24502894132287E-5,
2.49975961757824E-5,2.8852600369028E-5,3.10661348995016E-5,3.4305354351696E-5,
3.6641054565356E-5,4.00504537627888E-5),.UNSPECIFIED.);
#26609=B_SPLINE_CURVE_WITH_KNOTS('',3,(#441853,#441854,#441855,#441856,
#441857,#441858,#441859),.UNSPECIFIED.,.F.,.F.,(4,3,4),(0.,4.40000041065375E-5,
9.89910850773113E-5),.UNSPECIFIED.);
#26610=B_SPLINE_CURVE_WITH_KNOTS('',3,(#441880,#441881,#441882,#441883,
#441884,#441885,#441886,#441887,#441888,#441889,#441890,#441891,#441892,
#441893,#441894,#441895,#441896,#441897,#441898,#441899,#441900,#441901,
#441902,#441903,#441904,#441905,#441906,#441907,#441908,#441909,#441910,
#441911,#441912,#441913),.UNSPECIFIED.,.F.,.F.,(4,3,3,3,3,3,3,3,3,3,3,4),
(0.,4.29157837302178E-6,5.42772623795343E-6,1.00901698482349E-5,1.31279195068641E-5,
1.5738354226582E-5,1.61011507492108E-5,1.67166789291758E-5,1.95343262811362E-5,
2.29377234674655E-5,2.71556047620061E-5,3.34407099942666E-5),
 .UNSPECIFIED.);
#26611=B_SPLINE_CURVE_WITH_KNOTS('',3,(#441926,#441927,#441928,#441929,
#441930,#441931,#441932,#441933,#441934,#441935,#441936,#441937,#441938,
#441939,#441940,#441941,#441942,#441943,#441944,#441945,#441946,#441947,
#441948,#441949,#441950,#441951,#441952,#441953,#441954,#441955,#441956,
#441957,#441958,#441959),.UNSPECIFIED.,.F.,.F.,(4,3,3,3,3,3,3,3,3,3,3,4),
(0.,3.71309426656663E-6,5.39981071559421E-6,8.78933289334327E-6,9.00272357067522E-6,
1.07143984504149E-5,1.60780299679527E-5,1.65806081157686E-5,2.30369726850418E-5,
2.67819200416087E-5,3.59736924188099E-5,4.03862783807004E-5),
 .UNSPECIFIED.);
#26612=B_SPLINE_CURVE_WITH_KNOTS('',3,(#442072,#442073,#442074,#442075),
 .UNSPECIFIED.,.F.,.F.,(4,4),(0.,7.70025630629239E-5),.UNSPECIFIED.);
#26613=B_SPLINE_CURVE_WITH_KNOTS('',3,(#442085,#442086,#442087,#442088),
 .UNSPECIFIED.,.F.,.F.,(4,4),(2.16840434497101E-19,7.70025630629236E-5),
 .UNSPECIFIED.);
#26614=B_SPLINE_CURVE_WITH_KNOTS('',3,(#442092,#442093,#442094,#442095,
#442096,#442097,#442098,#442099,#442100,#442101,#442102,#442103,#442104,
#442105,#442106,#442107,#442108,#442109,#442110,#442111,#442112,#442113,
#442114,#442115,#442116,#442117,#442118,#442119,#442120,#442121,#442122,
#442123,#442124,#442125,#442126,#442127,#442128),.UNSPECIFIED.,.F.,.F.,
(4,3,3,3,3,3,3,3,3,3,3,3,4),(0.,9.59031527201911E-6,1.94769411223113E-5,
2.02405092183152E-5,3.21374138577674E-5,3.6030219507044E-5,4.42640648818895E-5,
4.53660204229443E-5,5.03633762302114E-5,5.17708036292897E-5,5.37928993851987E-5,
5.54103755460198E-5,5.64557889512061E-5),.UNSPECIFIED.);
#26615=B_SPLINE_CURVE_WITH_KNOTS('',3,(#442129,#442130,#442131,#442132,
#442133,#442134,#442135,#442136,#442137,#442138,#442139,#442140,#442141,
#442142,#442143,#442144,#442145,#442146,#442147,#442148,#442149,#442150,
#442151,#442152,#442153,#442154,#442155,#442156),.UNSPECIFIED.,.F.,.F.,
(4,3,3,3,3,3,3,3,3,4),(5.64557889512061E-5,5.98940966493753E-5,6.3421400387338E-5,
7.22241476084492E-5,7.38322796533364E-5,8.3652918933154E-5,8.807142782225E-5,
9.84837568500723E-5,0.000108624704079135,0.000110823272382854),
 .UNSPECIFIED.);
#26616=B_SPLINE_CURVE_WITH_KNOTS('',3,(#442172,#442173,#442174,#442175,
#442176,#442177,#442178,#442179,#442180,#442181,#442182,#442183,#442184,
#442185,#442186,#442187,#442188,#442189,#442190,#442191,#442192,#442193,
#442194,#442195,#442196,#442197,#442198,#442199),.UNSPECIFIED.,.F.,.F.,
(4,3,3,3,3,3,3,3,3,4),(0.,8.66039628581202E-6,1.64707715200667E-5,2.2450289413238E-5,
2.49975961757824E-5,2.88526003690279E-5,3.10661348995017E-5,3.43053543516958E-5,
3.66410545653558E-5,4.00504537627888E-5),.UNSPECIFIED.);
#26617=B_SPLINE_CURVE_WITH_KNOTS('',3,(#442202,#442203,#442204,#442205,
#442206,#442207,#442208),.UNSPECIFIED.,.F.,.F.,(4,3,4),(0.,4.40000041065374E-5,
9.89910850773111E-5),.UNSPECIFIED.);
#26618=B_SPLINE_CURVE_WITH_KNOTS('',3,(#442229,#442230,#442231,#442232,
#442233,#442234,#442235,#442236,#442237,#442238,#442239,#442240,#442241,
#442242,#442243,#442244,#442245,#442246,#442247,#442248,#442249,#442250,
#442251,#442252,#442253,#442254,#442255,#442256,#442257,#442258,#442259,
#442260,#442261,#442262),.UNSPECIFIED.,.F.,.F.,(4,3,3,3,3,3,3,3,3,3,3,4),
(0.,4.29157837304528E-6,5.42772623795349E-6,1.00901698482351E-5,1.31279195068643E-5,
1.5738354226576E-5,1.61011507492107E-5,1.67166789291759E-5,1.95343262811362E-5,
2.29377234674653E-5,2.71556047620063E-5,3.34407099942664E-5),
 .UNSPECIFIED.);
#26619=B_SPLINE_CURVE_WITH_KNOTS('',3,(#442275,#442276,#442277,#442278,
#442279,#442280,#442281,#442282,#442283,#442284,#442285,#442286,#442287,
#442288,#442289,#442290,#442291,#442292,#442293,#442294,#442295,#442296,
#442297,#442298,#442299,#442300,#442301,#442302,#442303,#442304,#442305,
#442306,#442307,#442308),.UNSPECIFIED.,.F.,.F.,(4,3,3,3,3,3,3,3,3,3,3,4),
(0.,3.7130942665664E-6,5.39981071559395E-6,8.78933289368984E-6,9.00272357067498E-6,
1.07143984504148E-5,1.6078029967946E-5,1.65806081157686E-5,2.30369726850543E-5,
2.67819200416085E-5,3.59736924187727E-5,4.03862783807E-5),.UNSPECIFIED.);
#26620=B_SPLINE_CURVE_WITH_KNOTS('',3,(#442421,#442422,#442423,#442424),
 .UNSPECIFIED.,.F.,.F.,(4,4),(0.,7.7002563062924E-5),.UNSPECIFIED.);
#26621=B_SPLINE_CURVE_WITH_KNOTS('',3,(#442434,#442435,#442436,#442437),
 .UNSPECIFIED.,.F.,.F.,(4,4),(2.16840434497101E-19,7.70025630629238E-5),
 .UNSPECIFIED.);
#26622=B_SPLINE_CURVE_WITH_KNOTS('',3,(#442441,#442442,#442443,#442444,
#442445,#442446,#442447,#442448,#442449,#442450,#442451,#442452,#442453,
#442454,#442455,#442456,#442457,#442458,#442459,#442460,#442461,#442462,
#442463,#442464,#442465,#442466,#442467,#442468,#442469,#442470,#442471,
#442472,#442473,#442474,#442475,#442476,#442477),.UNSPECIFIED.,.F.,.F.,
(4,3,3,3,3,3,3,3,3,3,3,3,4),(0.,9.59031527200278E-6,1.94769411222902E-5,
2.02405092183151E-5,3.21374138577676E-5,3.60302195070439E-5,4.426406488193E-5,
4.53660204229443E-5,5.03633762301989E-5,5.17708036292895E-5,5.37928993851989E-5,
5.54103755460197E-5,5.64557889509049E-5),.UNSPECIFIED.);
#26623=B_SPLINE_CURVE_WITH_KNOTS('',3,(#442478,#442479,#442480,#442481,
#442482,#442483,#442484,#442485,#442486,#442487,#442488,#442489,#442490,
#442491,#442492,#442493,#442494,#442495,#442496,#442497,#442498,#442499,
#442500,#442501,#442502,#442503,#442504,#442505),.UNSPECIFIED.,.F.,.F.,
(4,3,3,3,3,3,3,3,3,4),(5.64557889509049E-5,5.98940966493752E-5,6.3421400387338E-5,
7.22241476084301E-5,7.38322796533361E-5,8.36529189331512E-5,8.80714278222498E-5,
9.84837568500755E-5,0.000108624704079146,0.000110823272382853),
 .UNSPECIFIED.);
#26624=B_SPLINE_CURVE_WITH_KNOTS('',3,(#442521,#442522,#442523,#442524,
#442525,#442526,#442527,#442528,#442529,#442530,#442531,#442532,#442533,
#442534,#442535,#442536,#442537,#442538,#442539,#442540,#442541,#442542,
#442543,#442544,#442545,#442546,#442547,#442548),.UNSPECIFIED.,.F.,.F.,
(4,3,3,3,3,3,3,3,3,4),(0.,8.66039628582242E-6,1.6470771520067E-5,2.24502894132491E-5,
2.4997596175783E-5,2.88526003690286E-5,3.10661348995021E-5,3.43053543516965E-5,
3.66410545653568E-5,4.00504537627891E-5),.UNSPECIFIED.);
#26625=B_SPLINE_CURVE_WITH_KNOTS('',3,(#442551,#442552,#442553,#442554,
#442555,#442556,#442557),.UNSPECIFIED.,.F.,.F.,(4,3,4),(0.,4.40000041065377E-5,
9.89910850773113E-5),.UNSPECIFIED.);
#26626=B_SPLINE_CURVE_WITH_KNOTS('',3,(#442578,#442579,#442580,#442581,
#442582,#442583,#442584,#442585,#442586,#442587,#442588,#442589,#442590,
#442591,#442592,#442593,#442594,#442595,#442596,#442597,#442598,#442599,
#442600,#442601,#442602,#442603,#442604,#442605,#442606,#442607,#442608,
#442609,#442610,#442611),.UNSPECIFIED.,.F.,.F.,(4,3,3,3,3,3,3,3,3,3,3,4),
(0.,4.29157837302455E-6,5.4277262379531E-6,1.00901698482347E-5,1.31279195068636E-5,
1.57383542265912E-5,1.61011507492101E-5,1.67166789291748E-5,1.95343262811356E-5,
2.29377234674644E-5,2.7155604762005E-5,3.34407099942654E-5),
 .UNSPECIFIED.);
#26627=B_SPLINE_CURVE_WITH_KNOTS('',3,(#442624,#442625,#442626,#442627,
#442628,#442629,#442630,#442631,#442632,#442633,#442634,#442635,#442636,
#442637,#442638,#442639,#442640,#442641,#442642,#442643,#442644,#442645,
#442646,#442647,#442648,#442649,#442650,#442651,#442652,#442653,#442654,
#442655,#442656,#442657),.UNSPECIFIED.,.F.,.F.,(4,3,3,3,3,3,3,3,3,3,3,4),
(2.16840434497101E-19,3.71309426656645E-6,5.39981071559426E-6,8.78933289330928E-6,
9.00272357067514E-6,1.07143984504149E-5,1.60780299679444E-5,1.65806081157686E-5,
2.30369726850413E-5,2.67819200416083E-5,3.59736924187559E-5,4.03862783806996E-5),
 .UNSPECIFIED.);
#26628=B_SPLINE_CURVE_WITH_KNOTS('',3,(#442770,#442771,#442772,#442773),
 .UNSPECIFIED.,.F.,.F.,(4,4),(0.,7.7002563062924E-5),.UNSPECIFIED.);
#26629=B_SPLINE_CURVE_WITH_KNOTS('',3,(#442783,#442784,#442785,#442786),
 .UNSPECIFIED.,.F.,.F.,(4,4),(2.16840434497101E-19,7.70025630629236E-5),
 .UNSPECIFIED.);
#26630=B_SPLINE_CURVE_WITH_KNOTS('',3,(#442790,#442791,#442792,#442793,
#442794,#442795,#442796,#442797,#442798,#442799,#442800,#442801,#442802,
#442803,#442804,#442805,#442806,#442807,#442808,#442809,#442810,#442811,
#442812,#442813,#442814,#442815,#442816,#442817,#442818,#442819,#442820,
#442821,#442822,#442823,#442824,#442825,#442826),.UNSPECIFIED.,.F.,.F.,
(4,3,3,3,3,3,3,3,3,3,3,3,4),(0.,9.59031527199893E-6,1.94769411222929E-5,
2.02405092183152E-5,3.21374138577771E-5,3.60302195070439E-5,4.4264064881834E-5,
4.53660204229443E-5,5.03633762302013E-5,5.17708036292894E-5,5.37928993851988E-5,
5.54103755460194E-5,5.64557889511955E-5),.UNSPECIFIED.);
#26631=B_SPLINE_CURVE_WITH_KNOTS('',3,(#442827,#442828,#442829,#442830,
#442831,#442832,#442833,#442834,#442835,#442836,#442837,#442838,#442839,
#442840,#442841,#442842,#442843,#442844,#442845,#442846,#442847,#442848,
#442849,#442850,#442851,#442852,#442853,#442854),.UNSPECIFIED.,.F.,.F.,
(4,3,3,3,3,3,3,3,3,4),(5.64557889511955E-5,5.9894096649375E-5,6.34214003873381E-5,
7.22241476084563E-5,7.38322796533359E-5,8.36529189331489E-5,8.80714278222495E-5,
9.8483756850075E-5,0.000108624704079149,0.000110823272382853),
 .UNSPECIFIED.);
#26632=B_SPLINE_CURVE_WITH_KNOTS('',3,(#442870,#442871,#442872,#442873,
#442874,#442875,#442876,#442877,#442878,#442879,#442880,#442881,#442882,
#442883,#442884,#442885,#442886,#442887,#442888,#442889,#442890,#442891,
#442892,#442893,#442894,#442895,#442896,#442897),.UNSPECIFIED.,.F.,.F.,
(4,3,3,3,3,3,3,3,3,4),(0.,8.66039628581672E-6,1.64707715200666E-5,2.24502894132125E-5,
2.49975961757825E-5,2.88526003690281E-5,3.10661348995016E-5,3.43053543516959E-5,
3.66410545653562E-5,4.00504537627891E-5),.UNSPECIFIED.);
#26633=B_SPLINE_CURVE_WITH_KNOTS('',3,(#442900,#442901,#442902,#442903,
#442904,#442905,#442906),.UNSPECIFIED.,.F.,.F.,(4,3,4),(0.,4.40000041065376E-5,
9.89910850773114E-5),.UNSPECIFIED.);
#26634=B_SPLINE_CURVE_WITH_KNOTS('',3,(#442927,#442928,#442929,#442930,
#442931,#442932,#442933,#442934,#442935,#442936,#442937,#442938,#442939,
#442940,#442941,#442942,#442943,#442944,#442945,#442946,#442947,#442948,
#442949,#442950,#442951,#442952,#442953,#442954,#442955,#442956,#442957,
#442958,#442959,#442960),.UNSPECIFIED.,.F.,.F.,(4,3,3,3,3,3,3,3,3,3,3,4),
(0.,4.29157837303576E-6,5.42772623795327E-6,1.00901698482347E-5,1.31279195068638E-5,
1.57383542265823E-5,1.61011507492104E-5,1.67166789291752E-5,1.95343262811356E-5,
2.29377234674646E-5,2.71556047620055E-5,3.34407099942653E-5),
 .UNSPECIFIED.);
#26635=B_SPLINE_CURVE_WITH_KNOTS('',3,(#442973,#442974,#442975,#442976,
#442977,#442978,#442979,#442980,#442981,#442982,#442983,#442984,#442985,
#442986,#442987,#442988,#442989,#442990,#442991,#442992,#442993,#442994,
#442995,#442996,#442997,#442998,#442999,#443000,#443001,#443002,#443003,
#443004,#443005,#443006),.UNSPECIFIED.,.F.,.F.,(4,3,3,3,3,3,3,3,3,3,3,4),
(2.16840434497101E-19,3.71309426656623E-6,5.39981071559397E-6,8.78933289330331E-6,
9.00272357067499E-6,1.07143984504146E-5,1.6078029967947E-5,1.65806081157683E-5,
2.30369726850555E-5,2.6781920041608E-5,3.59736924187373E-5,4.03862783806993E-5),
 .UNSPECIFIED.);
#26636=B_SPLINE_CURVE_WITH_KNOTS('',3,(#443119,#443120,#443121,#443122),
 .UNSPECIFIED.,.F.,.F.,(4,4),(0.,7.70025630629239E-5),.UNSPECIFIED.);
#26637=B_SPLINE_CURVE_WITH_KNOTS('',3,(#443132,#443133,#443134,#443135),
 .UNSPECIFIED.,.F.,.F.,(4,4),(2.16840434497101E-19,7.70025630629237E-5),
 .UNSPECIFIED.);
#26638=B_SPLINE_CURVE_WITH_KNOTS('',3,(#443139,#443140,#443141,#443142,
#443143,#443144,#443145,#443146,#443147,#443148,#443149,#443150,#443151,
#443152,#443153,#443154,#443155,#443156,#443157,#443158,#443159,#443160,
#443161,#443162,#443163,#443164,#443165,#443166,#443167,#443168,#443169,
#443170,#443171,#443172,#443173,#443174,#443175),.UNSPECIFIED.,.F.,.F.,
(4,3,3,3,3,3,3,3,3,3,3,3,4),(0.,9.59031527200983E-6,1.94769411222978E-5,
2.02405092183153E-5,3.21374138577654E-5,3.60302195070439E-5,4.42640648818711E-5,
4.53660204229442E-5,5.03633762302079E-5,5.17708036292895E-5,5.37928993851986E-5,
5.54103755460198E-5,5.64557889512199E-5),.UNSPECIFIED.);
#26639=B_SPLINE_CURVE_WITH_KNOTS('',3,(#443176,#443177,#443178,#443179,
#443180,#443181,#443182,#443183,#443184,#443185,#443186,#443187,#443188,
#443189,#443190,#443191,#443192,#443193,#443194,#443195,#443196,#443197,
#443198,#443199,#443200,#443201,#443202,#443203),.UNSPECIFIED.,.F.,.F.,
(4,3,3,3,3,3,3,3,3,4),(5.64557889512199E-5,5.98940966493751E-5,6.34214003873378E-5,
7.22241476084778E-5,7.38322796533363E-5,8.36529189331535E-5,8.80714278222497E-5,
9.84837568501019E-5,0.000108624704079195,0.000110823272382853),
 .UNSPECIFIED.);
#26640=B_SPLINE_CURVE_WITH_KNOTS('',3,(#443219,#443220,#443221,#443222,
#443223,#443224,#443225,#443226,#443227,#443228,#443229,#443230,#443231,
#443232,#443233,#443234,#443235,#443236,#443237,#443238,#443239,#443240,
#443241,#443242,#443243,#443244,#443245,#443246),.UNSPECIFIED.,.F.,.F.,
(4,3,3,3,3,3,3,3,3,4),(0.,8.66039628582605E-6,1.64707715200667E-5,2.24502894132618E-5,
2.49975961757822E-5,2.8852600369028E-5,3.10661348995017E-5,3.43053543516961E-5,
3.66410545653558E-5,4.00504537627885E-5),.UNSPECIFIED.);
#26641=B_SPLINE_CURVE_WITH_KNOTS('',3,(#443249,#443250,#443251,#443252,
#443253,#443254,#443255),.UNSPECIFIED.,.F.,.F.,(4,3,4),(0.,4.40000041065376E-5,
9.89910850773113E-5),.UNSPECIFIED.);
#26642=B_SPLINE_CURVE_WITH_KNOTS('',3,(#443276,#443277,#443278,#443279,
#443280,#443281,#443282,#443283,#443284,#443285,#443286,#443287,#443288,
#443289,#443290,#443291,#443292,#443293,#443294,#443295,#443296,#443297,
#443298,#443299,#443300,#443301,#443302,#443303,#443304,#443305,#443306,
#443307,#443308,#443309),.UNSPECIFIED.,.F.,.F.,(4,3,3,3,3,3,3,3,3,3,3,4),
(0.,4.29157837304045E-6,5.42772623795319E-6,1.00901698482347E-5,1.31279195068639E-5,
1.57383542265809E-5,1.61011507492103E-5,1.67166789291753E-5,1.95343262811357E-5,
2.29377234674648E-5,2.71556047620057E-5,3.34407099942658E-5),
 .UNSPECIFIED.);
#26643=B_SPLINE_CURVE_WITH_KNOTS('',3,(#443322,#443323,#443324,#443325,
#443326,#443327,#443328,#443329,#443330,#443331,#443332,#443333,#443334,
#443335,#443336,#443337,#443338,#443339,#443340,#443341,#443342,#443343,
#443344,#443345,#443346,#443347,#443348,#443349,#443350,#443351,#443352,
#443353,#443354,#443355),.UNSPECIFIED.,.F.,.F.,(4,3,3,3,3,3,3,3,3,3,3,4),
(2.16840434497101E-19,3.71309426656637E-6,5.39981071559423E-6,8.78933289369147E-6,
9.00272357067518E-6,1.0714398450415E-5,1.60780299679611E-5,1.65806081157689E-5,
2.30369726850217E-5,2.6781920041609E-5,3.59736924188261E-5,4.03862783807009E-5),
 .UNSPECIFIED.);
#26644=B_SPLINE_CURVE_WITH_KNOTS('',3,(#443468,#443469,#443470,#443471),
 .UNSPECIFIED.,.F.,.F.,(4,4),(0.,7.70025630629238E-5),.UNSPECIFIED.);
#26645=B_SPLINE_CURVE_WITH_KNOTS('',3,(#443481,#443482,#443483,#443484),
 .UNSPECIFIED.,.F.,.F.,(4,4),(0.,7.7002563062924E-5),.UNSPECIFIED.);
#26646=B_SPLINE_CURVE_WITH_KNOTS('',3,(#443488,#443489,#443490,#443491,
#443492,#443493,#443494,#443495,#443496,#443497,#443498,#443499,#443500,
#443501,#443502,#443503,#443504,#443505,#443506,#443507,#443508,#443509,
#443510,#443511,#443512,#443513,#443514,#443515,#443516,#443517,#443518,
#443519,#443520,#443521,#443522,#443523,#443524),.UNSPECIFIED.,.F.,.F.,
(4,3,3,3,3,3,3,3,3,3,3,3,4),(0.,9.59031527200099E-6,1.94769411222849E-5,
2.02405092183154E-5,3.21374138577703E-5,3.60302195070439E-5,4.42640648818483E-5,
4.53660204229446E-5,5.03633762302092E-5,5.17708036292899E-5,5.37928993851989E-5,
5.54103755460196E-5,5.64557889512858E-5),.UNSPECIFIED.);
#26647=B_SPLINE_CURVE_WITH_KNOTS('',3,(#443525,#443526,#443527,#443528,
#443529,#443530,#443531,#443532,#443533,#443534,#443535,#443536,#443537,
#443538,#443539,#443540,#443541,#443542,#443543,#443544,#443545,#443546,
#443547,#443548,#443549,#443550,#443551,#443552),.UNSPECIFIED.,.F.,.F.,
(4,3,3,3,3,3,3,3,3,4),(5.64557889512858E-5,5.9894096649375E-5,6.34214003873377E-5,
7.22241476084027E-5,7.38322796533363E-5,8.36529189331388E-5,8.80714278222497E-5,
9.84837568500627E-5,0.000108624704079124,0.000110823272382853),
 .UNSPECIFIED.);
#26648=B_SPLINE_CURVE_WITH_KNOTS('',3,(#443568,#443569,#443570,#443571,
#443572,#443573,#443574,#443575,#443576,#443577,#443578,#443579,#443580,
#443581,#443582,#443583,#443584,#443585,#443586,#443587,#443588,#443589,
#443590,#443591,#443592,#443593,#443594,#443595),.UNSPECIFIED.,.F.,.F.,
(4,3,3,3,3,3,3,3,3,4),(0.,8.66039628583908E-6,1.64707715200666E-5,2.24502894132304E-5,
2.49975961757823E-5,2.88526003690279E-5,3.10661348995015E-5,3.43053543516958E-5,
3.66410545653561E-5,4.00504537627889E-5),.UNSPECIFIED.);
#26649=B_SPLINE_CURVE_WITH_KNOTS('',3,(#443598,#443599,#443600,#443601,
#443602,#443603,#443604),.UNSPECIFIED.,.F.,.F.,(4,3,4),(0.,4.40000041065374E-5,
9.89910850773112E-5),.UNSPECIFIED.);
#26650=B_SPLINE_CURVE_WITH_KNOTS('',3,(#443625,#443626,#443627,#443628,
#443629,#443630,#443631,#443632,#443633,#443634,#443635,#443636,#443637,
#443638,#443639,#443640,#443641,#443642,#443643,#443644,#443645,#443646,
#443647,#443648,#443649,#443650,#443651,#443652,#443653,#443654,#443655,
#443656,#443657,#443658),.UNSPECIFIED.,.F.,.F.,(4,3,3,3,3,3,3,3,3,3,3,4),
(0.,4.29157837303037E-6,5.42772623795304E-6,1.00901698482347E-5,1.31279195068637E-5,
1.57383542265969E-5,1.61011507492103E-5,1.67166789291754E-5,1.95343262811355E-5,
2.29377234674647E-5,2.71556047620054E-5,3.34407099942654E-5),
 .UNSPECIFIED.);
#26651=B_SPLINE_CURVE_WITH_KNOTS('',3,(#443671,#443672,#443673,#443674,
#443675,#443676,#443677,#443678,#443679,#443680,#443681,#443682,#443683,
#443684,#443685,#443686,#443687,#443688,#443689,#443690,#443691,#443692,
#443693,#443694,#443695,#443696,#443697,#443698,#443699,#443700,#443701,
#443702,#443703,#443704),.UNSPECIFIED.,.F.,.F.,(4,3,3,3,3,3,3,3,3,3,3,4),
(0.,3.71309426656671E-6,5.39981071559412E-6,8.78933289331451E-6,9.00272357067549E-6,
1.07143984504153E-5,1.60780299679558E-5,1.65806081157689E-5,2.30369726850571E-5,
2.67819200416092E-5,3.59736924187926E-5,4.0386278380701E-5),
 .UNSPECIFIED.);
#26652=B_SPLINE_CURVE_WITH_KNOTS('',3,(#443817,#443818,#443819,#443820),
 .UNSPECIFIED.,.F.,.F.,(4,4),(0.,7.70025630629237E-5),.UNSPECIFIED.);
#26653=B_SPLINE_CURVE_WITH_KNOTS('',3,(#443830,#443831,#443832,#443833),
 .UNSPECIFIED.,.F.,.F.,(4,4),(4.33680868994202E-19,7.70025630629238E-5),
 .UNSPECIFIED.);
#26654=B_SPLINE_CURVE_WITH_KNOTS('',3,(#443837,#443838,#443839,#443840,
#443841,#443842,#443843,#443844,#443845,#443846,#443847,#443848,#443849,
#443850,#443851,#443852,#443853,#443854,#443855,#443856,#443857,#443858,
#443859,#443860,#443861,#443862,#443863,#443864,#443865,#443866,#443867,
#443868,#443869,#443870,#443871,#443872,#443873),.UNSPECIFIED.,.F.,.F.,
(4,3,3,3,3,3,3,3,3,3,3,3,4),(0.,9.59031527199245E-6,1.94769411222787E-5,
2.02405092183153E-5,3.2137413857778E-5,3.60302195070441E-5,4.42640648819171E-5,
4.53660204229442E-5,5.03633762302015E-5,5.17708036292896E-5,5.37928993851988E-5,
5.54103755460206E-5,5.64557889511081E-5),.UNSPECIFIED.);
#26655=B_SPLINE_CURVE_WITH_KNOTS('',3,(#443874,#443875,#443876,#443877,
#443878,#443879,#443880,#443881,#443882,#443883,#443884,#443885,#443886,
#443887,#443888,#443889,#443890,#443891,#443892,#443893,#443894,#443895,
#443896,#443897,#443898,#443899,#443900,#443901),.UNSPECIFIED.,.F.,.F.,
(4,3,3,3,3,3,3,3,3,4),(5.64557889511081E-5,5.98940966493752E-5,6.34214003873379E-5,
7.22241476085193E-5,7.38322796533365E-5,8.36529189331587E-5,8.80714278222504E-5,
9.84837568501169E-5,0.00010862470407922,0.000110823272382854),
 .UNSPECIFIED.);
#26656=B_SPLINE_CURVE_WITH_KNOTS('',3,(#443917,#443918,#443919,#443920,
#443921,#443922,#443923,#443924,#443925,#443926,#443927,#443928,#443929,
#443930,#443931,#443932,#443933,#443934,#443935,#443936,#443937,#443938,
#443939,#443940,#443941,#443942,#443943,#443944),.UNSPECIFIED.,.F.,.F.,
(4,3,3,3,3,3,3,3,3,4),(0.,8.6603962858496E-6,1.64707715200666E-5,2.24502894132311E-5,
2.49975961757824E-5,2.8852600369028E-5,3.10661348995016E-5,3.4305354351696E-5,
3.6641054565356E-5,4.00504537627891E-5),.UNSPECIFIED.);
#26657=B_SPLINE_CURVE_WITH_KNOTS('',3,(#443947,#443948,#443949,#443950,
#443951,#443952,#443953),.UNSPECIFIED.,.F.,.F.,(4,3,4),(0.,4.40000041065375E-5,
9.89910850773112E-5),.UNSPECIFIED.);
#26658=B_SPLINE_CURVE_WITH_KNOTS('',3,(#443974,#443975,#443976,#443977,
#443978,#443979,#443980,#443981,#443982,#443983,#443984,#443985,#443986,
#443987,#443988,#443989,#443990,#443991,#443992,#443993,#443994,#443995,
#443996,#443997,#443998,#443999,#444000,#444001,#444002,#444003,#444004,
#444005,#444006,#444007),.UNSPECIFIED.,.F.,.F.,(4,3,3,3,3,3,3,3,3,3,3,4),
(0.,4.29157837301968E-6,5.42772623795346E-6,1.00901698482351E-5,1.31279195068641E-5,
1.57383542265875E-5,1.6101150749211E-5,1.67166789291759E-5,1.95343262811362E-5,
2.29377234674654E-5,2.71556047620065E-5,3.34407099942667E-5),
 .UNSPECIFIED.);
#26659=B_SPLINE_CURVE_WITH_KNOTS('',3,(#444020,#444021,#444022,#444023,
#444024,#444025,#444026,#444027,#444028,#444029,#444030,#444031,#444032,
#444033,#444034,#444035,#444036,#444037,#444038,#444039,#444040,#444041,
#444042,#444043,#444044,#444045,#444046,#444047,#444048,#444049,#444050,
#444051,#444052,#444053),.UNSPECIFIED.,.F.,.F.,(4,3,3,3,3,3,3,3,3,3,3,4),
(2.16840434497101E-19,3.71309426656662E-6,5.39981071559424E-6,8.78933289331598E-6,
9.00272357067511E-6,1.07143984504147E-5,1.60780299679598E-5,1.65806081157684E-5,
2.30369726850327E-5,2.67819200416082E-5,3.59736924188149E-5,4.03862783806993E-5),
 .UNSPECIFIED.);
#26660=B_SPLINE_CURVE_WITH_KNOTS('',3,(#444166,#444167,#444168,#444169),
 .UNSPECIFIED.,.F.,.F.,(4,4),(0.,7.70025630629239E-5),.UNSPECIFIED.);
#26661=B_SPLINE_CURVE_WITH_KNOTS('',3,(#444179,#444180,#444181,#444182),
 .UNSPECIFIED.,.F.,.F.,(4,4),(4.33680868994202E-19,7.7002563062924E-5),
 .UNSPECIFIED.);
#26662=B_SPLINE_CURVE_WITH_KNOTS('',3,(#444186,#444187,#444188,#444189,
#444190,#444191,#444192,#444193,#444194,#444195,#444196,#444197,#444198,
#444199,#444200,#444201,#444202,#444203,#444204,#444205,#444206,#444207,
#444208,#444209,#444210,#444211,#444212,#444213,#444214,#444215,#444216,
#444217,#444218,#444219,#444220,#444221,#444222),.UNSPECIFIED.,.F.,.F.,
(4,3,3,3,3,3,3,3,3,3,3,3,4),(0.,9.59031527200592E-6,1.94769411222996E-5,
2.02405092183151E-5,3.21374138577715E-5,3.60302195070437E-5,4.42640648819735E-5,
4.5366020422944E-5,5.03633762301883E-5,5.17708036292892E-5,5.37928993851985E-5,
5.5410375546019E-5,5.64557889516034E-5),.UNSPECIFIED.);
#26663=B_SPLINE_CURVE_WITH_KNOTS('',3,(#444223,#444224,#444225,#444226,
#444227,#444228,#444229,#444230,#444231,#444232,#444233,#444234,#444235,
#444236,#444237,#444238,#444239,#444240,#444241,#444242,#444243,#444244,
#444245,#444246,#444247,#444248,#444249,#444250),.UNSPECIFIED.,.F.,.F.,
(4,3,3,3,3,3,3,3,3,4),(5.64557889516034E-5,5.98940966493748E-5,6.34214003873374E-5,
7.22241476085106E-5,7.38322796533359E-5,8.36529189331493E-5,8.8071427822249E-5,
9.84837568500857E-5,0.000108624704079163,0.000110823272382852),
 .UNSPECIFIED.);
#26664=B_SPLINE_CURVE_WITH_KNOTS('',3,(#444266,#444267,#444268,#444269,
#444270,#444271,#444272,#444273,#444274,#444275,#444276,#444277,#444278,
#444279,#444280,#444281,#444282,#444283,#444284,#444285,#444286,#444287,
#444288,#444289,#444290,#444291,#444292,#444293),.UNSPECIFIED.,.F.,.F.,
(4,3,3,3,3,3,3,3,3,4),(0.,8.66039628580049E-6,1.64707715200665E-5,2.24502894132241E-5,
2.49975961757822E-5,2.8852600369028E-5,3.10661348995015E-5,3.43053543516958E-5,
3.6641054565356E-5,4.0050453762789E-5),.UNSPECIFIED.);
#26665=B_SPLINE_CURVE_WITH_KNOTS('',3,(#444296,#444297,#444298,#444299,
#444300,#444301,#444302),.UNSPECIFIED.,.F.,.F.,(4,3,4),(0.,4.40000041065373E-5,
9.89910850773112E-5),.UNSPECIFIED.);
#26666=B_SPLINE_CURVE_WITH_KNOTS('',3,(#444323,#444324,#444325,#444326,
#444327,#444328,#444329,#444330,#444331,#444332,#444333,#444334,#444335,
#444336,#444337,#444338,#444339,#444340,#444341,#444342,#444343,#444344,
#444345,#444346,#444347,#444348,#444349,#444350,#444351,#444352,#444353,
#444354,#444355,#444356),.UNSPECIFIED.,.F.,.F.,(4,3,3,3,3,3,3,3,3,3,3,4),
(0.,4.29157837306035E-6,5.42772623795318E-6,1.00901698482348E-5,1.3127919506864E-5,
1.57383542265774E-5,1.61011507492105E-5,1.67166789291753E-5,1.95343262811357E-5,
2.29377234674649E-5,2.71556047620058E-5,3.34407099942658E-5),
 .UNSPECIFIED.);
#26667=B_SPLINE_CURVE_WITH_KNOTS('',3,(#444369,#444370,#444371,#444372,
#444373,#444374,#444375,#444376,#444377,#444378,#444379,#444380,#444381,
#444382,#444383,#444384,#444385,#444386,#444387,#444388,#444389,#444390,
#444391,#444392,#444393,#444394,#444395,#444396,#444397,#444398,#444399,
#444400,#444401,#444402),.UNSPECIFIED.,.F.,.F.,(4,3,3,3,3,3,3,3,3,3,3,4),
(0.,3.71309426656633E-6,5.39981071559413E-6,8.78933289330927E-6,9.00272357067526E-6,
1.0714398450415E-5,1.60780299679556E-5,1.65806081157687E-5,2.30369726850343E-5,
2.67819200416086E-5,3.59736924187825E-5,4.03862783807002E-5),
 .UNSPECIFIED.);
#26668=B_SPLINE_CURVE_WITH_KNOTS('',3,(#444515,#444516,#444517,#444518),
 .UNSPECIFIED.,.F.,.F.,(4,4),(0.,7.70025630629237E-5),.UNSPECIFIED.);
#26669=B_SPLINE_CURVE_WITH_KNOTS('',3,(#444528,#444529,#444530,#444531),
 .UNSPECIFIED.,.F.,.F.,(4,4),(4.33680868994202E-19,7.70025630629236E-5),
 .UNSPECIFIED.);
#26670=B_SPLINE_CURVE_WITH_KNOTS('',3,(#444535,#444536,#444537,#444538,
#444539,#444540,#444541,#444542,#444543,#444544,#444545,#444546,#444547,
#444548,#444549,#444550,#444551,#444552,#444553,#444554,#444555,#444556,
#444557,#444558,#444559,#444560,#444561,#444562,#444563,#444564,#444565,
#444566,#444567,#444568,#444569,#444570,#444571),.UNSPECIFIED.,.F.,.F.,
(4,3,3,3,3,3,3,3,3,3,3,3,4),(0.,9.59031527198161E-6,1.94769411222625E-5,
2.02405092183153E-5,3.21374138577781E-5,3.60302195070436E-5,4.42640648818272E-5,
4.53660204229445E-5,5.03633762301973E-5,5.17708036292894E-5,5.37928993851988E-5,
5.54103755460195E-5,5.64557889510153E-5),.UNSPECIFIED.);
#26671=B_SPLINE_CURVE_WITH_KNOTS('',3,(#444572,#444573,#444574,#444575,
#444576,#444577,#444578,#444579,#444580,#444581,#444582,#444583,#444584,
#444585,#444586,#444587,#444588,#444589,#444590,#444591,#444592,#444593,
#444594,#444595,#444596,#444597,#444598,#444599),.UNSPECIFIED.,.F.,.F.,
(4,3,3,3,3,3,3,3,3,4),(5.64557889510153E-5,5.98940966493749E-5,6.34214003873379E-5,
7.22241476084258E-5,7.38322796533363E-5,8.36529189331488E-5,8.80714278222499E-5,
9.84837568500756E-5,0.000108624704079134,0.000110823272382853),
 .UNSPECIFIED.);
#26672=B_SPLINE_CURVE_WITH_KNOTS('',3,(#444615,#444616,#444617,#444618,
#444619,#444620,#444621,#444622,#444623,#444624,#444625,#444626,#444627,
#444628,#444629,#444630,#444631,#444632,#444633,#444634,#444635,#444636,
#444637,#444638,#444639,#444640,#444641,#444642),.UNSPECIFIED.,.F.,.F.,
(4,3,3,3,3,3,3,3,3,4),(0.,8.66039628579394E-6,1.64707715200667E-5,2.24502894132511E-5,
2.49975961757824E-5,2.88526003690281E-5,3.10661348995017E-5,3.43053543516961E-5,
3.66410545653561E-5,4.0050453762789E-5),.UNSPECIFIED.);
#26673=B_SPLINE_CURVE_WITH_KNOTS('',3,(#444645,#444646,#444647,#444648,
#444649,#444650,#444651),.UNSPECIFIED.,.F.,.F.,(4,3,4),(0.,4.40000041065371E-5,
9.89910850773111E-5),.UNSPECIFIED.);
#26674=B_SPLINE_CURVE_WITH_KNOTS('',3,(#444672,#444673,#444674,#444675,
#444676,#444677,#444678,#444679,#444680,#444681,#444682,#444683,#444684,
#444685,#444686,#444687,#444688,#444689,#444690,#444691,#444692,#444693,
#444694,#444695,#444696,#444697,#444698,#444699,#444700,#444701,#444702,
#444703,#444704,#444705),.UNSPECIFIED.,.F.,.F.,(4,3,3,3,3,3,3,3,3,3,3,4),
(0.,4.2915783730184E-6,5.42772623795351E-6,1.00901698482345E-5,1.31279195068638E-5,
1.57383542265793E-5,1.61011507492105E-5,1.67166789291754E-5,1.95343262811357E-5,
2.29377234674648E-5,2.71556047620057E-5,3.34407099942656E-5),
 .UNSPECIFIED.);
#26675=B_SPLINE_CURVE_WITH_KNOTS('',3,(#444718,#444719,#444720,#444721,
#444722,#444723,#444724,#444725,#444726,#444727,#444728,#444729,#444730,
#444731,#444732,#444733,#444734,#444735,#444736,#444737,#444738,#444739,
#444740,#444741,#444742,#444743,#444744,#444745,#444746,#444747,#444748,
#444749,#444750,#444751),.UNSPECIFIED.,.F.,.F.,(4,3,3,3,3,3,3,3,3,3,3,4),
(0.,3.71309426656649E-6,5.3998107155939E-6,8.78933289327122E-6,9.00272357067513E-6,
1.07143984504147E-5,1.60780299679589E-5,1.65806081157686E-5,2.30369726850634E-5,
2.67819200416087E-5,3.59736924187455E-5,4.03862783807006E-5),
 .UNSPECIFIED.);
#26676=B_SPLINE_CURVE_WITH_KNOTS('',3,(#444864,#444865,#444866,#444867),
 .UNSPECIFIED.,.F.,.F.,(4,4),(0.,7.70025630629237E-5),.UNSPECIFIED.);
#26677=B_SPLINE_CURVE_WITH_KNOTS('',3,(#444877,#444878,#444879,#444880),
 .UNSPECIFIED.,.F.,.F.,(4,4),(4.33680868994202E-19,7.70025630629236E-5),
 .UNSPECIFIED.);
#26678=B_SPLINE_CURVE_WITH_KNOTS('',3,(#444884,#444885,#444886,#444887,
#444888,#444889,#444890,#444891,#444892,#444893,#444894,#444895,#444896,
#444897,#444898,#444899,#444900,#444901,#444902,#444903,#444904,#444905,
#444906,#444907,#444908,#444909,#444910,#444911,#444912,#444913,#444914,
#444915,#444916,#444917,#444918,#444919,#444920),.UNSPECIFIED.,.F.,.F.,
(4,3,3,3,3,3,3,3,3,3,3,3,4),(0.,9.59031527201753E-6,1.9476941122308E-5,
2.02405092183154E-5,3.21374138577773E-5,3.60302195070444E-5,4.42640648819026E-5,
4.53660204229445E-5,5.03633762302112E-5,5.17708036292897E-5,5.37928993851987E-5,
5.54103755460199E-5,5.64557889514577E-5),.UNSPECIFIED.);
#26679=B_SPLINE_CURVE_WITH_KNOTS('',3,(#444921,#444922,#444923,#444924,
#444925,#444926,#444927,#444928,#444929,#444930,#444931,#444932,#444933,
#444934,#444935,#444936,#444937,#444938,#444939,#444940,#444941,#444942,
#444943,#444944,#444945,#444946,#444947,#444948),.UNSPECIFIED.,.F.,.F.,
(4,3,3,3,3,3,3,3,3,4),(5.64557889514577E-5,5.98940966493751E-5,6.34214003873383E-5,
7.22241476084398E-5,7.38322796533365E-5,8.36529189331448E-5,8.80714278222499E-5,
9.84837568500812E-5,0.000108624704079154,0.000110823272382853),
 .UNSPECIFIED.);
#26680=B_SPLINE_CURVE_WITH_KNOTS('',3,(#444964,#444965,#444966,#444967,
#444968,#444969,#444970,#444971,#444972,#444973,#444974,#444975,#444976,
#444977,#444978,#444979,#444980,#444981,#444982,#444983,#444984,#444985,
#444986,#444987,#444988,#444989,#444990,#444991),.UNSPECIFIED.,.F.,.F.,
(4,3,3,3,3,3,3,3,3,4),(0.,8.66039628577846E-6,1.64707715200669E-5,2.24502894132539E-5,
2.49975961757828E-5,2.88526003690286E-5,3.10661348995021E-5,3.43053543516966E-5,
3.66410545653563E-5,4.00504537627887E-5),.UNSPECIFIED.);
#26681=B_SPLINE_CURVE_WITH_KNOTS('',3,(#444994,#444995,#444996,#444997,
#444998,#444999,#445000),.UNSPECIFIED.,.F.,.F.,(4,3,4),(0.,4.40000041065374E-5,
9.89910850773111E-5),.UNSPECIFIED.);
#26682=B_SPLINE_CURVE_WITH_KNOTS('',3,(#445021,#445022,#445023,#445024,
#445025,#445026,#445027,#445028,#445029,#445030,#445031,#445032,#445033,
#445034,#445035,#445036,#445037,#445038,#445039,#445040,#445041,#445042,
#445043,#445044,#445045,#445046,#445047,#445048,#445049,#445050,#445051,
#445052,#445053,#445054),.UNSPECIFIED.,.F.,.F.,(4,3,3,3,3,3,3,3,3,3,3,4),
(0.,4.29157837305176E-6,5.42772623795343E-6,1.00901698482347E-5,1.31279195068639E-5,
1.57383542265907E-5,1.61011507492105E-5,1.67166789291758E-5,1.95343262811358E-5,
2.2937723467465E-5,2.71556047620059E-5,3.3440709994266E-5),
 .UNSPECIFIED.);
#26683=B_SPLINE_CURVE_WITH_KNOTS('',3,(#445067,#445068,#445069,#445070,
#445071,#445072,#445073,#445074,#445075,#445076,#445077,#445078,#445079,
#445080,#445081,#445082,#445083,#445084,#445085,#445086,#445087,#445088,
#445089,#445090,#445091,#445092,#445093,#445094,#445095,#445096,#445097,
#445098,#445099,#445100),.UNSPECIFIED.,.F.,.F.,(4,3,3,3,3,3,3,3,3,3,3,4),
(2.16840434497101E-19,3.7130942665665E-6,5.39981071559408E-6,8.78933289365784E-6,
9.00272357067535E-6,1.07143984504151E-5,1.60780299679626E-5,1.65806081157688E-5,
2.30369726850283E-5,2.67819200416088E-5,3.59736924187693E-5,4.03862783807004E-5),
 .UNSPECIFIED.);
#26684=B_SPLINE_CURVE_WITH_KNOTS('',3,(#445213,#445214,#445215,#445216),
 .UNSPECIFIED.,.F.,.F.,(4,4),(0.,7.70025630629241E-5),.UNSPECIFIED.);
#26685=B_SPLINE_CURVE_WITH_KNOTS('',3,(#445226,#445227,#445228,#445229),
 .UNSPECIFIED.,.F.,.F.,(4,4),(4.33680868994202E-19,7.70025630629237E-5),
 .UNSPECIFIED.);
#26686=B_SPLINE_CURVE_WITH_KNOTS('',3,(#445233,#445234,#445235,#445236,
#445237,#445238,#445239,#445240,#445241,#445242,#445243,#445244,#445245,
#445246,#445247,#445248,#445249,#445250,#445251,#445252,#445253,#445254,
#445255,#445256,#445257,#445258,#445259,#445260,#445261,#445262,#445263,
#445264,#445265,#445266,#445267,#445268,#445269),.UNSPECIFIED.,.F.,.F.,
(4,3,3,3,3,3,3,3,3,3,3,3,4),(0.,9.59031527200409E-6,1.9476941122299E-5,
2.02405092183152E-5,3.21374138577639E-5,3.60302195070437E-5,4.42640648818624E-5,
4.53660204229444E-5,5.03633762302181E-5,5.17708036292895E-5,5.37928993851987E-5,
5.54103755460196E-5,5.64557889508704E-5),.UNSPECIFIED.);
#26687=B_SPLINE_CURVE_WITH_KNOTS('',3,(#445270,#445271,#445272,#445273,
#445274,#445275,#445276,#445277,#445278,#445279,#445280,#445281,#445282,
#445283,#445284,#445285,#445286,#445287,#445288,#445289,#445290,#445291,
#445292,#445293,#445294,#445295,#445296,#445297),.UNSPECIFIED.,.F.,.F.,
(4,3,3,3,3,3,3,3,3,4),(5.64557889508704E-5,5.98940966493747E-5,6.34214003873377E-5,
7.22241476084951E-5,7.3832279653336E-5,8.36529189331591E-5,8.80714278222496E-5,
9.84837568501187E-5,0.000108624704079221,0.000110823272382853),
 .UNSPECIFIED.);
#26688=B_SPLINE_CURVE_WITH_KNOTS('',3,(#445313,#445314,#445315,#445316,
#445317,#445318,#445319,#445320,#445321,#445322,#445323,#445324,#445325,
#445326,#445327,#445328,#445329,#445330,#445331,#445332,#445333,#445334,
#445335,#445336,#445337,#445338,#445339,#445340),.UNSPECIFIED.,.F.,.F.,
(4,3,3,3,3,3,3,3,3,4),(0.,8.66039628579246E-6,1.64707715200667E-5,2.24502894129346E-5,
2.49975961757824E-5,2.88526003690281E-5,3.10661348995016E-5,3.43053543516961E-5,
3.66410545653559E-5,4.00504537627887E-5),.UNSPECIFIED.);
#26689=B_SPLINE_CURVE_WITH_KNOTS('',3,(#445343,#445344,#445345,#445346,
#445347,#445348,#445349),.UNSPECIFIED.,.F.,.F.,(4,3,4),(0.,4.40000041065373E-5,
9.89910850773112E-5),.UNSPECIFIED.);
#26690=B_SPLINE_CURVE_WITH_KNOTS('',3,(#445370,#445371,#445372,#445373,
#445374,#445375,#445376,#445377,#445378,#445379,#445380,#445381,#445382,
#445383,#445384,#445385,#445386,#445387,#445388,#445389,#445390,#445391,
#445392,#445393,#445394,#445395,#445396,#445397,#445398,#445399,#445400,
#445401,#445402,#445403),.UNSPECIFIED.,.F.,.F.,(4,3,3,3,3,3,3,3,3,3,3,4),
(0.,4.29157837305078E-6,5.4277262379532E-6,1.00901698482344E-5,1.31279195068637E-5,
1.57383542265852E-5,1.61011507492101E-5,1.67166789291755E-5,1.95343262811355E-5,
2.29377234674645E-5,2.71556047620054E-5,3.34407099942652E-5),
 .UNSPECIFIED.);
#26691=B_SPLINE_CURVE_WITH_KNOTS('',3,(#445416,#445417,#445418,#445419,
#445420,#445421,#445422,#445423,#445424,#445425,#445426,#445427,#445428,
#445429,#445430,#445431,#445432,#445433,#445434,#445435,#445436,#445437,
#445438,#445439,#445440,#445441,#445442,#445443,#445444,#445445,#445446,
#445447,#445448,#445449),.UNSPECIFIED.,.F.,.F.,(4,3,3,3,3,3,3,3,3,3,3,4),
(1.0842021724855E-19,3.71309426656644E-6,5.39981071559416E-6,8.78933289330016E-6,
9.00272357067517E-6,1.07143984504149E-5,1.60780299679582E-5,1.65806081157687E-5,
2.30369726850505E-5,2.67819200416087E-5,3.59736924187412E-5,4.03862783807004E-5),
 .UNSPECIFIED.);
#26692=B_SPLINE_CURVE_WITH_KNOTS('',3,(#445562,#445563,#445564,#445565),
 .UNSPECIFIED.,.F.,.F.,(4,4),(0.,7.70025630629238E-5),.UNSPECIFIED.);
#26693=B_SPLINE_CURVE_WITH_KNOTS('',3,(#445575,#445576,#445577,#445578),
 .UNSPECIFIED.,.F.,.F.,(4,4),(4.33680868994202E-19,7.70025630629236E-5),
 .UNSPECIFIED.);
#26694=B_SPLINE_CURVE_WITH_KNOTS('',3,(#445582,#445583,#445584,#445585,
#445586,#445587,#445588,#445589,#445590,#445591,#445592,#445593,#445594,
#445595,#445596,#445597,#445598,#445599,#445600,#445601,#445602,#445603,
#445604,#445605,#445606,#445607,#445608,#445609,#445610,#445611,#445612,
#445613,#445614,#445615,#445616,#445617,#445618),.UNSPECIFIED.,.F.,.F.,
(4,3,3,3,3,3,3,3,3,3,3,3,4),(0.,9.59031527199521E-6,1.9476941122276E-5,
2.02405092183153E-5,3.21374138577658E-5,3.6030219507044E-5,4.4264064881821E-5,
4.53660204229446E-5,5.03633762302175E-5,5.17708036292897E-5,5.37928993851991E-5,
5.54103755460206E-5,5.64557889515007E-5),.UNSPECIFIED.);
#26695=B_SPLINE_CURVE_WITH_KNOTS('',3,(#445619,#445620,#445621,#445622,
#445623,#445624,#445625,#445626,#445627,#445628,#445629,#445630,#445631,
#445632,#445633,#445634,#445635,#445636,#445637,#445638,#445639,#445640,
#445641,#445642,#445643,#445644,#445645,#445646),.UNSPECIFIED.,.F.,.F.,
(4,3,3,3,3,3,3,3,3,4),(5.64557889515007E-5,5.98940966493753E-5,6.34214003873382E-5,
7.22241476085262E-5,7.38322796533366E-5,8.365291893315E-5,8.80714278222501E-5,
9.84837568501103E-5,0.000108624704079207,0.000110823272382854),
 .UNSPECIFIED.);
#26696=B_SPLINE_CURVE_WITH_KNOTS('',3,(#445662,#445663,#445664,#445665,
#445666,#445667,#445668,#445669,#445670,#445671,#445672,#445673,#445674,
#445675,#445676,#445677,#445678,#445679,#445680,#445681,#445682,#445683,
#445684,#445685,#445686,#445687,#445688,#445689),.UNSPECIFIED.,.F.,.F.,
(4,3,3,3,3,3,3,3,3,4),(0.,8.66039628580631E-6,1.64707715200667E-5,2.24502894132641E-5,
2.49975961757823E-5,2.88526003690281E-5,3.10661348995016E-5,3.4305354351696E-5,
3.66410545653559E-5,4.00504537627885E-5),.UNSPECIFIED.);
#26697=B_SPLINE_CURVE_WITH_KNOTS('',3,(#445692,#445693,#445694,#445695,
#445696,#445697,#445698),.UNSPECIFIED.,.F.,.F.,(4,3,4),(0.,4.40000041065376E-5,
9.89910850773112E-5),.UNSPECIFIED.);
#26698=B_SPLINE_CURVE_WITH_KNOTS('',3,(#445719,#445720,#445721,#445722,
#445723,#445724,#445725,#445726,#445727,#445728,#445729,#445730,#445731,
#445732,#445733,#445734,#445735,#445736,#445737,#445738,#445739,#445740,
#445741,#445742,#445743,#445744,#445745,#445746,#445747,#445748,#445749,
#445750,#445751,#445752),.UNSPECIFIED.,.F.,.F.,(4,3,3,3,3,3,3,3,3,3,3,4),
(0.,4.29157837303616E-6,5.42772623795344E-6,1.00901698482348E-5,1.3127919506864E-5,
1.57383542265838E-5,1.61011507492106E-5,1.67166789291761E-5,1.95343262811362E-5,
2.29377234674651E-5,2.71556047620063E-5,3.34407099942663E-5),
 .UNSPECIFIED.);
#26699=B_SPLINE_CURVE_WITH_KNOTS('',3,(#445765,#445766,#445767,#445768,
#445769,#445770,#445771,#445772,#445773,#445774,#445775,#445776,#445777,
#445778,#445779,#445780,#445781,#445782,#445783,#445784,#445785,#445786,
#445787,#445788,#445789,#445790,#445791,#445792,#445793,#445794,#445795,
#445796,#445797,#445798),.UNSPECIFIED.,.F.,.F.,(4,3,3,3,3,3,3,3,3,3,3,4),
(0.,3.71309426656651E-6,5.39981071559418E-6,8.78933289368936E-6,9.00272357067521E-6,
1.0714398450415E-5,1.60780299679545E-5,1.65806081157686E-5,2.30369726850577E-5,
2.67819200416086E-5,3.59736924187482E-5,4.03862783806999E-5),
 .UNSPECIFIED.);
#26700=B_SPLINE_CURVE_WITH_KNOTS('',3,(#445911,#445912,#445913,#445914),
 .UNSPECIFIED.,.F.,.F.,(4,4),(0.,7.70025630629238E-5),.UNSPECIFIED.);
#26701=B_SPLINE_CURVE_WITH_KNOTS('',3,(#445924,#445925,#445926,#445927),
 .UNSPECIFIED.,.F.,.F.,(4,4),(4.47028007668187E-19,7.70025630629235E-5),
 .UNSPECIFIED.);
#26702=B_SPLINE_CURVE_WITH_KNOTS('',3,(#445931,#445932,#445933,#445934,
#445935,#445936,#445937,#445938,#445939,#445940,#445941,#445942,#445943,
#445944,#445945,#445946,#445947,#445948,#445949,#445950,#445951,#445952,
#445953,#445954,#445955,#445956,#445957,#445958,#445959,#445960,#445961,
#445962,#445963,#445964,#445965,#445966,#445967),.UNSPECIFIED.,.F.,.F.,
(4,3,3,3,3,3,3,3,3,3,3,3,4),(0.,9.59031527203696E-6,1.9476941122349E-5,
2.02405092183153E-5,3.21374138577552E-5,3.60302195070438E-5,4.42640648819458E-5,
4.53660204229443E-5,5.03633762301987E-5,5.17708036292895E-5,5.37928993851987E-5,
5.54103755460198E-5,5.64557889512956E-5),.UNSPECIFIED.);
#26703=B_SPLINE_CURVE_WITH_KNOTS('',3,(#445968,#445969,#445970,#445971,
#445972,#445973,#445974,#445975,#445976,#445977,#445978,#445979,#445980,
#445981,#445982,#445983,#445984,#445985,#445986,#445987,#445988,#445989,
#445990,#445991,#445992,#445993,#445994,#445995),.UNSPECIFIED.,.F.,.F.,
(4,3,3,3,3,3,3,3,3,4),(5.64557889512956E-5,5.98940966493749E-5,6.34214003873378E-5,
7.22241476084465E-5,7.38322796533362E-5,8.36529189331447E-5,8.80714278222496E-5,
9.84837568500728E-5,0.000108624704079131,0.000110823272382853),
 .UNSPECIFIED.);
#26704=B_SPLINE_CURVE_WITH_KNOTS('',3,(#446011,#446012,#446013,#446014,
#446015,#446016,#446017,#446018,#446019,#446020,#446021,#446022,#446023,
#446024,#446025,#446026,#446027,#446028,#446029,#446030,#446031,#446032,
#446033,#446034,#446035,#446036,#446037,#446038),.UNSPECIFIED.,.F.,.F.,
(4,3,3,3,3,3,3,3,3,4),(0.,8.6603962858097E-6,1.64707715200665E-5,2.24502894132422E-5,
2.49975961757823E-5,2.8852600369028E-5,3.10661348995016E-5,3.4305354351696E-5,
3.66410545653558E-5,4.00504537627886E-5),.UNSPECIFIED.);
#26705=B_SPLINE_CURVE_WITH_KNOTS('',3,(#446041,#446042,#446043,#446044,
#446045,#446046,#446047),.UNSPECIFIED.,.F.,.F.,(4,3,4),(0.,4.40000041065374E-5,
9.89910850773112E-5),.UNSPECIFIED.);
#26706=B_SPLINE_CURVE_WITH_KNOTS('',3,(#446068,#446069,#446070,#446071,
#446072,#446073,#446074,#446075,#446076,#446077,#446078,#446079,#446080,
#446081,#446082,#446083,#446084,#446085,#446086,#446087,#446088,#446089,
#446090,#446091,#446092,#446093,#446094,#446095,#446096,#446097,#446098,
#446099,#446100,#446101),.UNSPECIFIED.,.F.,.F.,(4,3,3,3,3,3,3,3,3,3,3,4),
(0.,4.29157837303425E-6,5.42772623795356E-6,1.00901698482349E-5,1.3127919506864E-5,
1.57383542265805E-5,1.61011507492106E-5,1.67166789291759E-5,1.9534326281136E-5,
2.29377234674651E-5,2.71556047620061E-5,3.34407099942661E-5),
 .UNSPECIFIED.);
#26707=B_SPLINE_CURVE_WITH_KNOTS('',3,(#446114,#446115,#446116,#446117,
#446118,#446119,#446120,#446121,#446122,#446123,#446124,#446125,#446126,
#446127,#446128,#446129,#446130,#446131,#446132,#446133,#446134,#446135,
#446136,#446137,#446138,#446139,#446140,#446141,#446142,#446143,#446144,
#446145,#446146,#446147),.UNSPECIFIED.,.F.,.F.,(4,3,3,3,3,3,3,3,3,3,3,4),
(5.42101086242752E-20,3.71309426656648E-6,5.3998107155943E-6,8.78933289365762E-6,
9.00272357067529E-6,1.0714398450415E-5,1.60780299679587E-5,1.65806081157689E-5,
2.3036972685055E-5,2.67819200416088E-5,3.59736924187735E-5,4.03862783807004E-5),
 .UNSPECIFIED.);
#26708=B_SPLINE_CURVE_WITH_KNOTS('',3,(#446260,#446261,#446262,#446263),
 .UNSPECIFIED.,.F.,.F.,(4,4),(0.,7.70025630629241E-5),.UNSPECIFIED.);
#26709=B_SPLINE_CURVE_WITH_KNOTS('',3,(#446273,#446274,#446275,#446276),
 .UNSPECIFIED.,.F.,.F.,(4,4),(4.41238316394827E-19,7.70025630629236E-5),
 .UNSPECIFIED.);
#26710=B_SPLINE_CURVE_WITH_KNOTS('',3,(#446280,#446281,#446282,#446283,
#446284,#446285,#446286,#446287,#446288,#446289,#446290,#446291,#446292,
#446293,#446294,#446295,#446296,#446297,#446298,#446299,#446300,#446301,
#446302,#446303,#446304,#446305,#446306,#446307,#446308,#446309,#446310,
#446311,#446312,#446313,#446314,#446315,#446316),.UNSPECIFIED.,.F.,.F.,
(4,3,3,3,3,3,3,3,3,3,3,3,4),(0.,9.59031527199735E-6,1.94769411222785E-5,
2.02405092183151E-5,3.2137413857779E-5,3.60302195070439E-5,4.42640648818236E-5,
4.53660204229444E-5,5.03633762302106E-5,5.17708036292896E-5,5.37928993851989E-5,
5.54103755460201E-5,5.64557889507886E-5),.UNSPECIFIED.);
#26711=B_SPLINE_CURVE_WITH_KNOTS('',3,(#446317,#446318,#446319,#446320,
#446321,#446322,#446323,#446324,#446325,#446326,#446327,#446328,#446329,
#446330,#446331,#446332,#446333,#446334,#446335,#446336,#446337,#446338,
#446339,#446340,#446341,#446342,#446343,#446344),.UNSPECIFIED.,.F.,.F.,
(4,3,3,3,3,3,3,3,3,4),(5.64557889507886E-5,5.98940966493751E-5,6.3421400387338E-5,
7.22241476084905E-5,7.38322796533365E-5,8.36529189331635E-5,8.807142782225E-5,
9.8483756850128E-5,0.000108624704079255,0.000110823272382854),
 .UNSPECIFIED.);
#26712=B_SPLINE_CURVE_WITH_KNOTS('',3,(#446360,#446361,#446362,#446363,
#446364,#446365,#446366,#446367,#446368,#446369,#446370,#446371,#446372,
#446373,#446374,#446375,#446376,#446377,#446378,#446379,#446380,#446381,
#446382,#446383,#446384,#446385,#446386,#446387),.UNSPECIFIED.,.F.,.F.,
(4,3,3,3,3,3,3,3,3,4),(0.,8.6603962857781E-6,1.64707715200667E-5,2.2450289413243E-5,
2.49975961757824E-5,2.88526003690281E-5,3.10661348995016E-5,3.43053543516961E-5,
3.66410545653559E-5,4.00504537627887E-5),.UNSPECIFIED.);
#26713=B_SPLINE_CURVE_WITH_KNOTS('',3,(#446390,#446391,#446392,#446393,
#446394,#446395,#446396),.UNSPECIFIED.,.F.,.F.,(4,3,4),(0.,4.40000041065377E-5,
9.89910850773114E-5),.UNSPECIFIED.);
#26714=B_SPLINE_CURVE_WITH_KNOTS('',3,(#446417,#446418,#446419,#446420,
#446421,#446422,#446423,#446424,#446425,#446426,#446427,#446428,#446429,
#446430,#446431,#446432,#446433,#446434,#446435,#446436,#446437,#446438,
#446439,#446440,#446441,#446442,#446443,#446444,#446445,#446446,#446447,
#446448,#446449,#446450),.UNSPECIFIED.,.F.,.F.,(4,3,3,3,3,3,3,3,3,3,3,4),
(0.,4.29157837302368E-6,5.42772623795337E-6,1.00901698482347E-5,1.31279195068638E-5,
1.57383542265853E-5,1.61011507492103E-5,1.67166789291756E-5,1.95343262811357E-5,
2.29377234674647E-5,2.71556047620056E-5,3.34407099942657E-5),
 .UNSPECIFIED.);
#26715=B_SPLINE_CURVE_WITH_KNOTS('',3,(#446463,#446464,#446465,#446466,
#446467,#446468,#446469,#446470,#446471,#446472,#446473,#446474,#446475,
#446476,#446477,#446478,#446479,#446480,#446481,#446482,#446483,#446484,
#446485,#446486,#446487,#446488,#446489,#446490,#446491,#446492,#446493,
#446494,#446495,#446496),.UNSPECIFIED.,.F.,.F.,(4,3,3,3,3,3,3,3,3,3,3,4),
(8.13151629364128E-20,3.71309426656643E-6,5.39981071559413E-6,8.78933289367591E-6,
9.00272357067522E-6,1.07143984504149E-5,1.60780299679527E-5,1.65806081157687E-5,
2.30369726850458E-5,2.67819200416086E-5,3.59736924188039E-5,4.03862783807E-5),
 .UNSPECIFIED.);
#26716=B_SPLINE_CURVE_WITH_KNOTS('',3,(#446609,#446610,#446611,#446612),
 .UNSPECIFIED.,.F.,.F.,(4,4),(4.2351647362715E-22,7.70025630629241E-5),
 .UNSPECIFIED.);
#26717=B_SPLINE_CURVE_WITH_KNOTS('',3,(#446622,#446623,#446624,#446625),
 .UNSPECIFIED.,.F.,.F.,(4,4),(4.43935777737106E-19,7.70025630629237E-5),
 .UNSPECIFIED.);
#26718=B_SPLINE_CURVE_WITH_KNOTS('',3,(#446629,#446630,#446631,#446632,
#446633,#446634,#446635,#446636,#446637,#446638,#446639,#446640,#446641,
#446642,#446643,#446644,#446645,#446646,#446647,#446648,#446649,#446650,
#446651,#446652,#446653,#446654,#446655,#446656,#446657,#446658,#446659,
#446660,#446661,#446662,#446663,#446664,#446665),.UNSPECIFIED.,.F.,.F.,
(4,3,3,3,3,3,3,3,3,3,3,3,4),(0.,9.59031527199033E-6,1.94769411222786E-5,
2.02405092183153E-5,3.21374138577756E-5,3.6030219507044E-5,4.42640648817823E-5,
4.53660204229445E-5,5.03633762302121E-5,5.17708036292897E-5,5.3792899385199E-5,
5.54103755460201E-5,5.64557889509772E-5),.UNSPECIFIED.);
#26719=B_SPLINE_CURVE_WITH_KNOTS('',3,(#446666,#446667,#446668,#446669,
#446670,#446671,#446672,#446673,#446674,#446675,#446676,#446677,#446678,
#446679,#446680,#446681,#446682,#446683,#446684,#446685,#446686,#446687,
#446688,#446689,#446690,#446691,#446692,#446693),.UNSPECIFIED.,.F.,.F.,
(4,3,3,3,3,3,3,3,3,4),(5.64557889509772E-5,5.98940966493752E-5,6.34214003873381E-5,
7.22241476084702E-5,7.38322796533365E-5,8.36529189331638E-5,8.80714278222502E-5,
9.84837568501129E-5,0.000108624704079212,0.000110823272382854),
 .UNSPECIFIED.);
#26720=B_SPLINE_CURVE_WITH_KNOTS('',3,(#446709,#446710,#446711,#446712,
#446713,#446714,#446715,#446716,#446717,#446718,#446719,#446720,#446721,
#446722,#446723,#446724,#446725,#446726,#446727,#446728,#446729,#446730,
#446731,#446732,#446733,#446734,#446735,#446736),.UNSPECIFIED.,.F.,.F.,
(4,3,3,3,3,3,3,3,3,4),(0.,8.66039628577415E-6,1.64707715200667E-5,2.24502894129709E-5,
2.49975961757824E-5,2.8852600369028E-5,3.10661348995016E-5,3.4305354351696E-5,
3.66410545653559E-5,4.00504537627886E-5),.UNSPECIFIED.);
#26721=B_SPLINE_CURVE_WITH_KNOTS('',3,(#446739,#446740,#446741,#446742,
#446743,#446744,#446745),.UNSPECIFIED.,.F.,.F.,(4,3,4),(0.,4.40000041065374E-5,
9.89910850773113E-5),.UNSPECIFIED.);
#26722=B_SPLINE_CURVE_WITH_KNOTS('',3,(#446766,#446767,#446768,#446769,
#446770,#446771,#446772,#446773,#446774,#446775,#446776,#446777,#446778,
#446779,#446780,#446781,#446782,#446783,#446784,#446785,#446786,#446787,
#446788,#446789,#446790,#446791,#446792,#446793,#446794,#446795,#446796,
#446797,#446798,#446799),.UNSPECIFIED.,.F.,.F.,(4,3,3,3,3,3,3,3,3,3,3,4),
(0.,4.29157837305466E-6,5.42772623795305E-6,1.00901698482346E-5,1.31279195068638E-5,
1.57383542265818E-5,1.61011507492103E-5,1.67166789291756E-5,1.95343262811358E-5,
2.29377234674649E-5,2.71556047620057E-5,3.34407099942656E-5),
 .UNSPECIFIED.);
#26723=B_SPLINE_CURVE_WITH_KNOTS('',3,(#446812,#446813,#446814,#446815,
#446816,#446817,#446818,#446819,#446820,#446821,#446822,#446823,#446824,
#446825,#446826,#446827,#446828,#446829,#446830,#446831,#446832,#446833,
#446834,#446835,#446836,#446837,#446838,#446839,#446840,#446841,#446842,
#446843,#446844,#446845),.UNSPECIFIED.,.F.,.F.,(4,3,3,3,3,3,3,3,3,3,3,4),
(9.14795583034644E-20,3.71309426656653E-6,5.39981071559422E-6,8.78933289365931E-6,
9.00272357067526E-6,1.07143984504149E-5,1.60780299679613E-5,1.65806081157687E-5,
2.30369726850558E-5,2.67819200416085E-5,3.5973692418903E-5,4.03862783806968E-5),
 .UNSPECIFIED.);
#26724=B_SPLINE_CURVE_WITH_KNOTS('',3,(#446958,#446959,#446960,#446961),
 .UNSPECIFIED.,.F.,.F.,(4,4),(0.,7.7002563062924E-5),.UNSPECIFIED.);
#26725=B_SPLINE_CURVE_WITH_KNOTS('',3,(#446971,#446972,#446973,#446974),
 .UNSPECIFIED.,.F.,.F.,(4,4),(4.47028007668187E-19,7.70025630629237E-5),
 .UNSPECIFIED.);
#26726=B_SPLINE_CURVE_WITH_KNOTS('',3,(#446978,#446979,#446980,#446981,
#446982,#446983,#446984,#446985,#446986,#446987,#446988,#446989,#446990,
#446991,#446992,#446993,#446994,#446995,#446996,#446997,#446998,#446999,
#447000,#447001,#447002,#447003,#447004,#447005,#447006,#447007,#447008,
#447009,#447010,#447011,#447012,#447013,#447014),.UNSPECIFIED.,.F.,.F.,
(4,3,3,3,3,3,3,3,3,3,3,3,4),(0.,9.5903152720076E-6,1.94769411223003E-5,
2.02405092183152E-5,3.21374138577718E-5,3.60302195070439E-5,4.4264064881891E-5,
4.53660204229443E-5,5.03633762301953E-5,5.17708036292895E-5,5.37928993851988E-5,
5.54103755460199E-5,5.64557889511778E-5),.UNSPECIFIED.);
#26727=B_SPLINE_CURVE_WITH_KNOTS('',3,(#447015,#447016,#447017,#447018,
#447019,#447020,#447021,#447022,#447023,#447024,#447025,#447026,#447027,
#447028,#447029,#447030,#447031,#447032,#447033,#447034,#447035,#447036,
#447037,#447038,#447039,#447040,#447041,#447042),.UNSPECIFIED.,.F.,.F.,
(4,3,3,3,3,3,3,3,3,4),(5.64557889511778E-5,5.9894096649375E-5,6.34214003873379E-5,
7.2224147608466E-5,7.38322796533362E-5,8.36529189331405E-5,8.80714278222499E-5,
9.8483756850072E-5,0.000108624704079137,0.000110823272382853),
 .UNSPECIFIED.);
#26728=B_SPLINE_CURVE_WITH_KNOTS('',3,(#447058,#447059,#447060,#447061,
#447062,#447063,#447064,#447065,#447066,#447067,#447068,#447069,#447070,
#447071,#447072,#447073,#447074,#447075,#447076,#447077,#447078,#447079,
#447080,#447081,#447082,#447083,#447084,#447085),.UNSPECIFIED.,.F.,.F.,
(4,3,3,3,3,3,3,3,3,4),(0.,8.66039628582417E-6,1.64707715200666E-5,2.24502894132344E-5,
2.49975961757823E-5,2.8852600369028E-5,3.10661348995016E-5,3.4305354351696E-5,
3.66410545653559E-5,4.00504537627888E-5),.UNSPECIFIED.);
#26729=B_SPLINE_CURVE_WITH_KNOTS('',3,(#447088,#447089,#447090,#447091,
#447092,#447093,#447094),.UNSPECIFIED.,.F.,.F.,(4,3,4),(0.,4.40000041065374E-5,
9.8991085077311E-5),.UNSPECIFIED.);
#26730=B_SPLINE_CURVE_WITH_KNOTS('',3,(#447115,#447116,#447117,#447118,
#447119,#447120,#447121,#447122,#447123,#447124,#447125,#447126,#447127,
#447128,#447129,#447130,#447131,#447132,#447133,#447134,#447135,#447136,
#447137,#447138,#447139,#447140,#447141,#447142,#447143,#447144,#447145,
#447146,#447147,#447148),.UNSPECIFIED.,.F.,.F.,(4,3,3,3,3,3,3,3,3,3,3,4),
(0.,4.29157837303296E-6,5.4277262379535E-6,1.00901698482348E-5,1.3127919506864E-5,
1.57383542265895E-5,1.61011507492105E-5,1.67166789291755E-5,1.95343262811359E-5,
2.29377234674648E-5,2.71556047620056E-5,3.34407099942656E-5),
 .UNSPECIFIED.);
#26731=B_SPLINE_CURVE_WITH_KNOTS('',3,(#447161,#447162,#447163,#447164,
#447165,#447166,#447167,#447168,#447169,#447170,#447171,#447172,#447173,
#447174,#447175,#447176,#447177,#447178,#447179,#447180,#447181,#447182,
#447183,#447184,#447185,#447186,#447187,#447188,#447189,#447190,#447191,
#447192,#447193,#447194),.UNSPECIFIED.,.F.,.F.,(4,3,3,3,3,3,3,3,3,3,3,4),
(8.13151629364128E-20,3.71309426656644E-6,5.39981071559418E-6,8.78933289368667E-6,
9.00272357067519E-6,1.07143984504149E-5,1.60780299679507E-5,1.65806081157687E-5,
2.30369726850405E-5,2.67819200416087E-5,3.59736924188187E-5,4.03862783807001E-5),
 .UNSPECIFIED.);
#26732=B_SPLINE_CURVE_WITH_KNOTS('',3,(#447307,#447308,#447309,#447310),
 .UNSPECIFIED.,.F.,.F.,(4,4),(0.,7.70025630629242E-5),.UNSPECIFIED.);
#26733=B_SPLINE_CURVE_WITH_KNOTS('',3,(#447320,#447321,#447322,#447323),
 .UNSPECIFIED.,.F.,.F.,(4,4),(4.47028007668187E-19,7.70025630629237E-5),
 .UNSPECIFIED.);
#26734=B_SPLINE_CURVE_WITH_KNOTS('',3,(#447327,#447328,#447329,#447330,
#447331,#447332,#447333,#447334,#447335,#447336,#447337,#447338,#447339,
#447340,#447341,#447342,#447343,#447344,#447345,#447346,#447347,#447348,
#447349,#447350,#447351,#447352,#447353,#447354,#447355,#447356,#447357,
#447358,#447359,#447360,#447361,#447362,#447363),.UNSPECIFIED.,.F.,.F.,
(4,3,3,3,3,3,3,3,3,3,3,3,4),(0.,9.59031527201221E-6,1.94769411223092E-5,
2.02405092183152E-5,3.21374138577726E-5,3.60302195070438E-5,4.42640648819218E-5,
4.53660204229443E-5,5.03633762302023E-5,5.17708036292896E-5,5.37928993851988E-5,
5.54103755460198E-5,5.64557889509462E-5),.UNSPECIFIED.);
#26735=B_SPLINE_CURVE_WITH_KNOTS('',3,(#447364,#447365,#447366,#447367,
#447368,#447369,#447370,#447371,#447372,#447373,#447374,#447375,#447376,
#447377,#447378,#447379,#447380,#447381,#447382,#447383,#447384,#447385,
#447386,#447387,#447388,#447389,#447390,#447391),.UNSPECIFIED.,.F.,.F.,
(4,3,3,3,3,3,3,3,3,4),(5.64557889509462E-5,5.98940966493749E-5,6.34214003873379E-5,
7.22241476084611E-5,7.38322796533362E-5,8.36529189331336E-5,8.80714278222497E-5,
9.84837568500736E-5,0.000108624704079139,0.000110823272382853),
 .UNSPECIFIED.);
#26736=B_SPLINE_CURVE_WITH_KNOTS('',3,(#447407,#447408,#447409,#447410,
#447411,#447412,#447413,#447414,#447415,#447416,#447417,#447418,#447419,
#447420,#447421,#447422,#447423,#447424,#447425,#447426,#447427,#447428,
#447429,#447430,#447431,#447432,#447433,#447434),.UNSPECIFIED.,.F.,.F.,
(4,3,3,3,3,3,3,3,3,4),(0.,8.66039628584135E-6,1.64707715200667E-5,2.24502894132571E-5,
2.49975961757824E-5,2.88526003690282E-5,3.10661348995016E-5,3.43053543516961E-5,
3.6641054565356E-5,4.00504537627888E-5),.UNSPECIFIED.);
#26737=B_SPLINE_CURVE_WITH_KNOTS('',3,(#447437,#447438,#447439,#447440,
#447441,#447442,#447443),.UNSPECIFIED.,.F.,.F.,(4,3,4),(0.,4.40000041065373E-5,
9.89910850773113E-5),.UNSPECIFIED.);
#26738=B_SPLINE_CURVE_WITH_KNOTS('',3,(#447464,#447465,#447466,#447467,
#447468,#447469,#447470,#447471,#447472,#447473,#447474,#447475,#447476,
#447477,#447478,#447479,#447480,#447481,#447482,#447483,#447484,#447485,
#447486,#447487,#447488,#447489,#447490,#447491,#447492,#447493,#447494,
#447495,#447496,#447497),.UNSPECIFIED.,.F.,.F.,(4,3,3,3,3,3,3,3,3,3,3,4),
(0.,4.29157837302508E-6,5.42772623795343E-6,1.00901698482347E-5,1.31279195068639E-5,
1.57383542265875E-5,1.61011507492105E-5,1.67166789291755E-5,1.9534326281136E-5,
2.29377234674652E-5,2.71556047620059E-5,3.3440709994266E-5),
 .UNSPECIFIED.);
#26739=B_SPLINE_CURVE_WITH_KNOTS('',3,(#447510,#447511,#447512,#447513,
#447514,#447515,#447516,#447517,#447518,#447519,#447520,#447521,#447522,
#447523,#447524,#447525,#447526,#447527,#447528,#447529,#447530,#447531,
#447532,#447533,#447534,#447535,#447536,#447537,#447538,#447539,#447540,
#447541,#447542,#447543),.UNSPECIFIED.,.F.,.F.,(4,3,3,3,3,3,3,3,3,3,3,4),
(5.42101086242752E-20,3.71309426656648E-6,5.39981071559421E-6,8.78933289331524E-6,
9.00272357067526E-6,1.0714398450415E-5,1.60780299679625E-5,1.65806081157688E-5,
2.30369726850327E-5,2.67819200416088E-5,3.59736924187896E-5,4.03862783807003E-5),
 .UNSPECIFIED.);
#26740=B_SPLINE_CURVE_WITH_KNOTS('',3,(#447656,#447657,#447658,#447659),
 .UNSPECIFIED.,.F.,.F.,(4,4),(0.,7.70025630629239E-5),.UNSPECIFIED.);
#26741=B_SPLINE_CURVE_WITH_KNOTS('',3,(#447669,#447670,#447671,#447672),
 .UNSPECIFIED.,.F.,.F.,(4,4),(1.0842021724855E-19,7.70025630629237E-5),
 .UNSPECIFIED.);
#26742=B_SPLINE_CURVE_WITH_KNOTS('',3,(#447676,#447677,#447678,#447679,
#447680,#447681,#447682,#447683,#447684,#447685,#447686,#447687,#447688,
#447689,#447690,#447691,#447692,#447693,#447694,#447695,#447696,#447697,
#447698,#447699,#447700,#447701,#447702,#447703,#447704,#447705,#447706,
#447707,#447708,#447709,#447710,#447711,#447712),.UNSPECIFIED.,.F.,.F.,
(4,3,3,3,3,3,3,3,3,3,3,3,4),(0.,9.59031527200873E-6,1.94769411223043E-5,
2.02405092183151E-5,3.21374138577679E-5,3.60302195070439E-5,4.42640648818551E-5,
4.53660204229443E-5,5.0363376230211E-5,5.17708036292896E-5,5.37928993851988E-5,
5.54103755460199E-5,5.64557889511168E-5),.UNSPECIFIED.);
#26743=B_SPLINE_CURVE_WITH_KNOTS('',3,(#447713,#447714,#447715,#447716,
#447717,#447718,#447719,#447720,#447721,#447722,#447723,#447724,#447725,
#447726,#447727,#447728,#447729,#447730,#447731,#447732,#447733,#447734,
#447735,#447736,#447737,#447738,#447739,#447740),.UNSPECIFIED.,.F.,.F.,
(4,3,3,3,3,3,3,3,3,4),(5.64557889511168E-5,5.9894096649375E-5,6.34214003873379E-5,
7.22241476083523E-5,7.38322796533361E-5,8.36529189331479E-5,8.80714278222499E-5,
9.8483756850077E-5,0.000108624704079147,0.000110823272382853),
 .UNSPECIFIED.);
#26744=B_SPLINE_CURVE_WITH_KNOTS('',3,(#447756,#447757,#447758,#447759,
#447760,#447761,#447762,#447763,#447764,#447765,#447766,#447767,#447768,
#447769,#447770,#447771,#447772,#447773,#447774,#447775,#447776,#447777,
#447778,#447779,#447780,#447781,#447782,#447783),.UNSPECIFIED.,.F.,.F.,
(4,3,3,3,3,3,3,3,3,4),(0.,8.66039628581661E-6,1.64707715200667E-5,2.24502894132545E-5,
2.49975961757824E-5,2.8852600369028E-5,3.10661348995016E-5,3.4305354351696E-5,
3.66410545653559E-5,4.00504537627887E-5),.UNSPECIFIED.);
#26745=B_SPLINE_CURVE_WITH_KNOTS('',3,(#447786,#447787,#447788,#447789,
#447790,#447791,#447792),.UNSPECIFIED.,.F.,.F.,(4,3,4),(0.,4.40000041065374E-5,
9.8991085077311E-5),.UNSPECIFIED.);
#26746=B_SPLINE_CURVE_WITH_KNOTS('',3,(#447813,#447814,#447815,#447816,
#447817,#447818,#447819,#447820,#447821,#447822,#447823,#447824,#447825,
#447826,#447827,#447828,#447829,#447830,#447831,#447832,#447833,#447834,
#447835,#447836,#447837,#447838,#447839,#447840,#447841,#447842,#447843,
#447844,#447845,#447846),.UNSPECIFIED.,.F.,.F.,(4,3,3,3,3,3,3,3,3,3,3,4),
(0.,4.2915783730183E-6,5.42772623795347E-6,1.00901698482349E-5,1.31279195068642E-5,
1.57383542265885E-5,1.61011507492107E-5,1.67166789291759E-5,1.95343262811362E-5,
2.29377234674653E-5,2.71556047620063E-5,3.34407099942661E-5),
 .UNSPECIFIED.);
#26747=B_SPLINE_CURVE_WITH_KNOTS('',3,(#447859,#447860,#447861,#447862,
#447863,#447864,#447865,#447866,#447867,#447868,#447869,#447870,#447871,
#447872,#447873,#447874,#447875,#447876,#447877,#447878,#447879,#447880,
#447881,#447882,#447883,#447884,#447885,#447886,#447887,#447888,#447889,
#447890,#447891,#447892),.UNSPECIFIED.,.F.,.F.,(4,3,3,3,3,3,3,3,3,3,3,4),
(2.16840434497101E-19,3.71309426656641E-6,5.39981071559409E-6,8.78933289329756E-6,
9.00272357067517E-6,1.07143984504149E-5,1.60780299679583E-5,1.65806081157685E-5,
2.30369726850452E-5,2.67819200416083E-5,3.59736924187826E-5,4.03862783806996E-5),
 .UNSPECIFIED.);
#26748=B_SPLINE_CURVE_WITH_KNOTS('',3,(#448005,#448006,#448007,#448008),
 .UNSPECIFIED.,.F.,.F.,(4,4),(0.,7.7002563062924E-5),.UNSPECIFIED.);
#26749=B_SPLINE_CURVE_WITH_KNOTS('',3,(#448018,#448019,#448020,#448021),
 .UNSPECIFIED.,.F.,.F.,(4,4),(2.16840434497101E-19,7.70025630629238E-5),
 .UNSPECIFIED.);
#26750=B_SPLINE_CURVE_WITH_KNOTS('',3,(#448025,#448026,#448027,#448028,
#448029,#448030,#448031,#448032,#448033,#448034,#448035,#448036,#448037,
#448038,#448039,#448040,#448041,#448042,#448043,#448044,#448045,#448046,
#448047,#448048,#448049,#448050,#448051,#448052,#448053,#448054,#448055,
#448056,#448057,#448058,#448059,#448060,#448061),.UNSPECIFIED.,.F.,.F.,
(4,3,3,3,3,3,3,3,3,3,3,3,4),(0.,9.59031527198866E-6,1.94769411222687E-5,
2.02405092183153E-5,3.21374138577716E-5,3.60302195070438E-5,4.42640648818875E-5,
4.53660204229444E-5,5.0363376230206E-5,5.17708036292895E-5,5.37928993851989E-5,
5.54103755460199E-5,5.64557889511988E-5),.UNSPECIFIED.);
#26751=B_SPLINE_CURVE_WITH_KNOTS('',3,(#448062,#448063,#448064,#448065,
#448066,#448067,#448068,#448069,#448070,#448071,#448072,#448073,#448074,
#448075,#448076,#448077,#448078,#448079,#448080,#448081,#448082,#448083,
#448084,#448085,#448086,#448087,#448088,#448089),.UNSPECIFIED.,.F.,.F.,
(4,3,3,3,3,3,3,3,3,4),(5.64557889511988E-5,5.9894096649375E-5,6.34214003873379E-5,
7.22241476083957E-5,7.38322796533361E-5,8.36529189331633E-5,8.80714278222497E-5,
9.84837568501205E-5,0.000108624704079235,0.000110823272382853),
 .UNSPECIFIED.);
#26752=B_SPLINE_CURVE_WITH_KNOTS('',3,(#448105,#448106,#448107,#448108,
#448109,#448110,#448111,#448112,#448113,#448114,#448115,#448116,#448117,
#448118,#448119,#448120,#448121,#448122,#448123,#448124,#448125,#448126,
#448127,#448128,#448129,#448130,#448131,#448132),.UNSPECIFIED.,.F.,.F.,
(4,3,3,3,3,3,3,3,3,4),(0.,8.66039628578604E-6,1.64707715200665E-5,2.24502894132191E-5,
2.49975961757823E-5,2.8852600369028E-5,3.10661348995016E-5,3.4305354351696E-5,
3.66410545653559E-5,4.00504537627889E-5),.UNSPECIFIED.);
#26753=B_SPLINE_CURVE_WITH_KNOTS('',3,(#448135,#448136,#448137,#448138,
#448139,#448140,#448141),.UNSPECIFIED.,.F.,.F.,(4,3,4),(0.,4.40000041065374E-5,
9.89910850773112E-5),.UNSPECIFIED.);
#26754=B_SPLINE_CURVE_WITH_KNOTS('',3,(#448162,#448163,#448164,#448165,
#448166,#448167,#448168,#448169,#448170,#448171,#448172,#448173,#448174,
#448175,#448176,#448177,#448178,#448179,#448180,#448181,#448182,#448183,
#448184,#448185,#448186,#448187,#448188,#448189,#448190,#448191,#448192,
#448193,#448194,#448195),.UNSPECIFIED.,.F.,.F.,(4,3,3,3,3,3,3,3,3,3,3,4),
(0.,4.29157837303585E-6,5.42772623795341E-6,1.00901698482348E-5,1.3127919506864E-5,
1.5738354226579E-5,1.61011507492105E-5,1.67166789291754E-5,1.95343262811359E-5,
2.29377234674646E-5,2.71556047620056E-5,3.34407099942653E-5),
 .UNSPECIFIED.);
#26755=B_SPLINE_CURVE_WITH_KNOTS('',3,(#448208,#448209,#448210,#448211,
#448212,#448213,#448214,#448215,#448216,#448217,#448218,#448219,#448220,
#448221,#448222,#448223,#448224,#448225,#448226,#448227,#448228,#448229,
#448230,#448231,#448232,#448233,#448234,#448235,#448236,#448237,#448238,
#448239,#448240,#448241),.UNSPECIFIED.,.F.,.F.,(4,3,3,3,3,3,3,3,3,3,3,4),
(1.0842021724855E-19,3.7130942665665E-6,5.39981071559421E-6,8.78933289329038E-6,
9.00272357067531E-6,1.0714398450415E-5,1.60780299679534E-5,1.65806081157688E-5,
2.30369726850481E-5,2.67819200416089E-5,3.59736924187636E-5,4.03862783807004E-5),
 .UNSPECIFIED.);
#26756=B_SPLINE_CURVE_WITH_KNOTS('',3,(#448354,#448355,#448356,#448357),
 .UNSPECIFIED.,.F.,.F.,(4,4),(0.,7.70025630629239E-5),.UNSPECIFIED.);
#26757=B_SPLINE_CURVE_WITH_KNOTS('',3,(#448367,#448368,#448369,#448370),
 .UNSPECIFIED.,.F.,.F.,(4,4),(0.,7.70025630629241E-5),.UNSPECIFIED.);
#26758=B_SPLINE_CURVE_WITH_KNOTS('',3,(#448374,#448375,#448376,#448377,
#448378,#448379,#448380,#448381,#448382,#448383,#448384,#448385,#448386,
#448387,#448388,#448389,#448390,#448391,#448392,#448393,#448394,#448395,
#448396,#448397,#448398,#448399,#448400,#448401,#448402,#448403,#448404,
#448405,#448406,#448407,#448408,#448409,#448410),.UNSPECIFIED.,.F.,.F.,
(4,3,3,3,3,3,3,3,3,3,3,3,4),(0.,9.59031527198869E-6,1.94769411222726E-5,
2.02405092183153E-5,3.21374138577653E-5,3.60302195070441E-5,4.42640648818868E-5,
4.53660204229444E-5,5.03633762302017E-5,5.17708036292897E-5,5.37928993851991E-5,
5.54103755460197E-5,5.64557889511107E-5),.UNSPECIFIED.);
#26759=B_SPLINE_CURVE_WITH_KNOTS('',3,(#448411,#448412,#448413,#448414,
#448415,#448416,#448417,#448418,#448419,#448420,#448421,#448422,#448423,
#448424,#448425,#448426,#448427,#448428,#448429,#448430,#448431,#448432,
#448433,#448434,#448435,#448436,#448437,#448438),.UNSPECIFIED.,.F.,.F.,
(4,3,3,3,3,3,3,3,3,4),(5.64557889511107E-5,5.98940966493752E-5,6.34214003873379E-5,
7.22241476084464E-5,7.38322796533364E-5,8.36529189331498E-5,8.807142782225E-5,
9.84837568500754E-5,0.000108624704079144,0.000110823272382853),
 .UNSPECIFIED.);
#26760=B_SPLINE_CURVE_WITH_KNOTS('',3,(#448454,#448455,#448456,#448457,
#448458,#448459,#448460,#448461,#448462,#448463,#448464,#448465,#448466,
#448467,#448468,#448469,#448470,#448471,#448472,#448473,#448474,#448475,
#448476,#448477,#448478,#448479,#448480,#448481),.UNSPECIFIED.,.F.,.F.,
(4,3,3,3,3,3,3,3,3,4),(0.,8.66039628580875E-6,1.64707715200666E-5,2.24502894132507E-5,
2.49975961757822E-5,2.8852600369028E-5,3.10661348995017E-5,3.43053543516959E-5,
3.66410545653558E-5,4.00504537627884E-5),.UNSPECIFIED.);
#26761=B_SPLINE_CURVE_WITH_KNOTS('',3,(#448484,#448485,#448486,#448487,
#448488,#448489,#448490),.UNSPECIFIED.,.F.,.F.,(4,3,4),(0.,4.40000041065377E-5,
9.89910850773113E-5),.UNSPECIFIED.);
#26762=B_SPLINE_CURVE_WITH_KNOTS('',3,(#448511,#448512,#448513,#448514,
#448515,#448516,#448517,#448518,#448519,#448520,#448521,#448522,#448523,
#448524,#448525,#448526,#448527,#448528,#448529,#448530,#448531,#448532,
#448533,#448534,#448535,#448536,#448537,#448538,#448539,#448540,#448541,
#448542,#448543,#448544),.UNSPECIFIED.,.F.,.F.,(4,3,3,3,3,3,3,3,3,3,3,4),
(0.,4.29157837305611E-6,5.42772623795344E-6,1.00901698482349E-5,1.3127919506864E-5,
1.5738354226584E-5,1.61011507492106E-5,1.6716678929175E-5,1.95343262811357E-5,
2.29377234674646E-5,2.71556047620054E-5,3.34407099942654E-5),
 .UNSPECIFIED.);
#26763=B_SPLINE_CURVE_WITH_KNOTS('',3,(#448557,#448558,#448559,#448560,
#448561,#448562,#448563,#448564,#448565,#448566,#448567,#448568,#448569,
#448570,#448571,#448572,#448573,#448574,#448575,#448576,#448577,#448578,
#448579,#448580,#448581,#448582,#448583,#448584,#448585,#448586,#448587,
#448588,#448589,#448590),.UNSPECIFIED.,.F.,.F.,(4,3,3,3,3,3,3,3,3,3,3,4),
(0.,3.71309426656648E-6,5.3998107155944E-6,8.78933289331138E-6,9.00272357067539E-6,
1.0714398450415E-5,1.60780299679542E-5,1.65806081157689E-5,2.30369726850623E-5,
2.67819200416089E-5,3.5973692418722E-5,4.03862783807005E-5),
 .UNSPECIFIED.);
#26764=B_SPLINE_CURVE_WITH_KNOTS('',3,(#448703,#448704,#448705,#448706),
 .UNSPECIFIED.,.F.,.F.,(4,4),(0.,7.70025630629239E-5),.UNSPECIFIED.);
#26765=B_SPLINE_CURVE_WITH_KNOTS('',3,(#448716,#448717,#448718,#448719),
 .UNSPECIFIED.,.F.,.F.,(4,4),(2.16840434497101E-19,7.70025630629239E-5),
 .UNSPECIFIED.);
#26766=B_SPLINE_CURVE_WITH_KNOTS('',3,(#448723,#448724,#448725,#448726,
#448727,#448728,#448729,#448730,#448731,#448732,#448733,#448734,#448735,
#448736,#448737,#448738,#448739,#448740,#448741,#448742,#448743,#448744,
#448745,#448746,#448747,#448748,#448749,#448750,#448751,#448752,#448753,
#448754,#448755,#448756,#448757,#448758,#448759),.UNSPECIFIED.,.F.,.F.,
(4,3,3,3,3,3,3,3,3,3,3,3,4),(0.,9.59031527201032E-6,1.94769411223074E-5,
2.02405092183152E-5,3.21374138577751E-5,3.60302195070438E-5,4.42640648818425E-5,
4.53660204229442E-5,5.03633762302174E-5,5.17708036292895E-5,5.37928993851987E-5,
5.54103755460198E-5,5.64557889512764E-5),.UNSPECIFIED.);
#26767=B_SPLINE_CURVE_WITH_KNOTS('',3,(#448760,#448761,#448762,#448763,
#448764,#448765,#448766,#448767,#448768,#448769,#448770,#448771,#448772,
#448773,#448774,#448775,#448776,#448777,#448778,#448779,#448780,#448781,
#448782,#448783,#448784,#448785,#448786,#448787),.UNSPECIFIED.,.F.,.F.,
(4,3,3,3,3,3,3,3,3,4),(5.64557889512764E-5,5.9894096649375E-5,6.34214003873378E-5,
7.22241476084241E-5,7.38322796533363E-5,8.36529189331436E-5,8.80714278222494E-5,
9.8483756850073E-5,0.000108624704079142,0.000110823272382853),
 .UNSPECIFIED.);
#26768=B_SPLINE_CURVE_WITH_KNOTS('',3,(#448803,#448804,#448805,#448806,
#448807,#448808,#448809,#448810,#448811,#448812,#448813,#448814,#448815,
#448816,#448817,#448818,#448819,#448820,#448821,#448822,#448823,#448824,
#448825,#448826,#448827,#448828,#448829,#448830),.UNSPECIFIED.,.F.,.F.,
(4,3,3,3,3,3,3,3,3,4),(0.,8.66039628580909E-6,1.64707715200669E-5,2.24502894132356E-5,
2.49975961757829E-5,2.88526003690284E-5,3.10661348995019E-5,3.43053543516966E-5,
3.66410545653565E-5,4.0050453762789E-5),.UNSPECIFIED.);
#26769=B_SPLINE_CURVE_WITH_KNOTS('',3,(#448833,#448834,#448835,#448836,
#448837,#448838,#448839),.UNSPECIFIED.,.F.,.F.,(4,3,4),(0.,4.40000041065376E-5,
9.89910850773114E-5),.UNSPECIFIED.);
#26770=B_SPLINE_CURVE_WITH_KNOTS('',3,(#448860,#448861,#448862,#448863,
#448864,#448865,#448866,#448867,#448868,#448869,#448870,#448871,#448872,
#448873,#448874,#448875,#448876,#448877,#448878,#448879,#448880,#448881,
#448882,#448883,#448884,#448885,#448886,#448887,#448888,#448889,#448890,
#448891,#448892,#448893),.UNSPECIFIED.,.F.,.F.,(4,3,3,3,3,3,3,3,3,3,3,4),
(0.,4.29157837305915E-6,5.42772623795332E-6,1.00901698482347E-5,1.31279195068641E-5,
1.57383542265863E-5,1.61011507492104E-5,1.67166789291754E-5,1.95343262811356E-5,
2.29377234674649E-5,2.71556047620056E-5,3.34407099942654E-5),
 .UNSPECIFIED.);
#26771=B_SPLINE_CURVE_WITH_KNOTS('',3,(#448906,#448907,#448908,#448909,
#448910,#448911,#448912,#448913,#448914,#448915,#448916,#448917,#448918,
#448919,#448920,#448921,#448922,#448923,#448924,#448925,#448926,#448927,
#448928,#448929,#448930,#448931,#448932,#448933,#448934,#448935,#448936,
#448937,#448938,#448939),.UNSPECIFIED.,.F.,.F.,(4,3,3,3,3,3,3,3,3,3,3,4),
(0.,3.71309426656643E-6,5.39981071559402E-6,8.7893328936724E-6,9.00272357067533E-6,
1.07143984504149E-5,1.60780299679559E-5,1.6580608115769E-5,2.30369726850549E-5,
2.67819200416093E-5,3.59736924187847E-5,4.03862783807012E-5),
 .UNSPECIFIED.);
#26772=B_SPLINE_CURVE_WITH_KNOTS('',3,(#449052,#449053,#449054,#449055),
 .UNSPECIFIED.,.F.,.F.,(4,4),(0.,7.70025630629241E-5),.UNSPECIFIED.);
#26773=B_SPLINE_CURVE_WITH_KNOTS('',3,(#449065,#449066,#449067,#449068),
 .UNSPECIFIED.,.F.,.F.,(4,4),(2.16840434497101E-19,7.70025630629236E-5),
 .UNSPECIFIED.);
#26774=B_SPLINE_CURVE_WITH_KNOTS('',3,(#449072,#449073,#449074,#449075,
#449076,#449077,#449078,#449079,#449080,#449081,#449082,#449083,#449084,
#449085,#449086,#449087,#449088,#449089,#449090,#449091,#449092,#449093,
#449094,#449095,#449096,#449097,#449098,#449099,#449100,#449101,#449102,
#449103,#449104,#449105,#449106,#449107,#449108),.UNSPECIFIED.,.F.,.F.,
(4,3,3,3,3,3,3,3,3,3,3,3,4),(0.,9.59031527202431E-6,1.94769411223246E-5,
2.02405092183152E-5,3.21374138577649E-5,3.6030219507044E-5,4.42640648818395E-5,
4.53660204229444E-5,5.03633762301883E-5,5.17708036292894E-5,5.37928993851986E-5,
5.54103755460197E-5,5.64557889512117E-5),.UNSPECIFIED.);
#26775=B_SPLINE_CURVE_WITH_KNOTS('',3,(#449109,#449110,#449111,#449112,
#449113,#449114,#449115,#449116,#449117,#449118,#449119,#449120,#449121,
#449122,#449123,#449124,#449125,#449126,#449127,#449128,#449129,#449130,
#449131,#449132,#449133,#449134,#449135,#449136),.UNSPECIFIED.,.F.,.F.,
(4,3,3,3,3,3,3,3,3,4),(5.64557889512117E-5,5.9894096649375E-5,6.34214003873379E-5,
7.22241476084387E-5,7.38322796533362E-5,8.36529189331548E-5,8.80714278222501E-5,
9.8483756850112E-5,0.000108624704079212,0.000110823272382853),
 .UNSPECIFIED.);
#26776=B_SPLINE_CURVE_WITH_KNOTS('',3,(#449152,#449153,#449154,#449155,
#449156,#449157,#449158,#449159,#449160,#449161,#449162,#449163,#449164,
#449165,#449166,#449167,#449168,#449169,#449170,#449171,#449172,#449173,
#449174,#449175,#449176,#449177,#449178,#449179),.UNSPECIFIED.,.F.,.F.,
(4,3,3,3,3,3,3,3,3,4),(0.,8.66039628580669E-6,1.64707715200667E-5,2.24502894132311E-5,
2.49975961757824E-5,2.88526003690281E-5,3.10661348995017E-5,3.4305354351696E-5,
3.66410545653558E-5,4.00504537627885E-5),.UNSPECIFIED.);
#26777=B_SPLINE_CURVE_WITH_KNOTS('',3,(#449182,#449183,#449184,#449185,
#449186,#449187,#449188),.UNSPECIFIED.,.F.,.F.,(4,3,4),(0.,4.40000041065373E-5,
9.89910850773112E-5),.UNSPECIFIED.);
#26778=B_SPLINE_CURVE_WITH_KNOTS('',3,(#449209,#449210,#449211,#449212,
#449213,#449214,#449215,#449216,#449217,#449218,#449219,#449220,#449221,
#449222,#449223,#449224,#449225,#449226,#449227,#449228,#449229,#449230,
#449231,#449232,#449233,#449234,#449235,#449236,#449237,#449238,#449239,
#449240,#449241,#449242),.UNSPECIFIED.,.F.,.F.,(4,3,3,3,3,3,3,3,3,3,3,4),
(0.,4.2915783730327E-6,5.42772623795325E-6,1.00901698482348E-5,1.31279195068637E-5,
1.57383542265831E-5,1.61011507492103E-5,1.67166789291759E-5,1.9534326281136E-5,
2.29377234674645E-5,2.71556047620059E-5,3.3440709994266E-5),
 .UNSPECIFIED.);
#26779=B_SPLINE_CURVE_WITH_KNOTS('',3,(#449255,#449256,#449257,#449258,
#449259,#449260,#449261,#449262,#449263,#449264,#449265,#449266,#449267,
#449268,#449269,#449270,#449271,#449272,#449273,#449274,#449275,#449276,
#449277,#449278,#449279,#449280,#449281,#449282,#449283,#449284,#449285,
#449286,#449287,#449288),.UNSPECIFIED.,.F.,.F.,(4,3,3,3,3,3,3,3,3,3,3,4),
(2.16840434497101E-19,3.71309426656647E-6,5.39981071559407E-6,8.78933289331909E-6,
9.00272357067532E-6,1.0714398450415E-5,1.60780299679462E-5,1.65806081157688E-5,
2.30369726850435E-5,2.67819200416086E-5,3.59736924187839E-5,4.03862783807001E-5),
 .UNSPECIFIED.);
#29748=LINE('',#409626,#33550);
#29749=LINE('',#409635,#33551);
#29750=LINE('',#409665,#33552);
#29751=LINE('',#409695,#33553);
#29752=LINE('',#409725,#33554);
#29753=LINE('',#409755,#33555);
#29754=LINE('',#409785,#33556);
#29755=LINE('',#409815,#33557);
#29756=LINE('',#409845,#33558);
#29757=LINE('',#409875,#33559);
#29758=LINE('',#409905,#33560);
#29759=LINE('',#409935,#33561);
#29760=LINE('',#409965,#33562);
#29761=LINE('',#409995,#33563);
#29762=LINE('',#410025,#33564);
#29763=LINE('',#410055,#33565);
#29764=LINE('',#410085,#33566);
#29765=LINE('',#410115,#33567);
#29766=LINE('',#410145,#33568);
#29767=LINE('',#410175,#33569);
#29768=LINE('',#410205,#33570);
#29769=LINE('',#410235,#33571);
#29770=LINE('',#410265,#33572);
#29771=LINE('',#410295,#33573);
#29772=LINE('',#410325,#33574);
#29773=LINE('',#410355,#33575);
#29774=LINE('',#410385,#33576);
#29775=LINE('',#410415,#33577);
#29776=LINE('',#410445,#33578);
#29777=LINE('',#410475,#33579);
#29778=LINE('',#410505,#33580);
#29779=LINE('',#410535,#33581);
#29780=LINE('',#410565,#33582);
#29781=LINE('',#410595,#33583);
#29782=LINE('',#410625,#33584);
#29783=LINE('',#410655,#33585);
#29784=LINE('',#410685,#33586);
#29785=LINE('',#410716,#33587);
#29786=LINE('',#410741,#33588);
#29787=LINE('',#410782,#33589);
#29788=LINE('',#410858,#33590);
#29789=LINE('',#410936,#33591);
#29790=LINE('',#411014,#33592);
#29791=LINE('',#411090,#33593);
#29792=LINE('',#411166,#33594);
#29793=LINE('',#411242,#33595);
#29794=LINE('',#411320,#33596);
#29795=LINE('',#411396,#33597);
#29796=LINE('',#411472,#33598);
#29797=LINE('',#411550,#33599);
#29798=LINE('',#411626,#33600);
#29799=LINE('',#411702,#33601);
#29800=LINE('',#411778,#33602);
#29801=LINE('',#411856,#33603);
#29802=LINE('',#411932,#33604);
#29803=LINE('',#412008,#33605);
#29804=LINE('',#412086,#33606);
#29805=LINE('',#412162,#33607);
#29806=LINE('',#412238,#33608);
#29807=LINE('',#412316,#33609);
#29808=LINE('',#412392,#33610);
#29809=LINE('',#412468,#33611);
#29810=LINE('',#412546,#33612);
#29811=LINE('',#412622,#33613);
#29812=LINE('',#412698,#33614);
#29813=LINE('',#412774,#33615);
#29814=LINE('',#412852,#33616);
#29815=LINE('',#412928,#33617);
#29816=LINE('',#413004,#33618);
#29817=LINE('',#413082,#33619);
#29818=LINE('',#413163,#33620);
#29819=LINE('',#413239,#33621);
#29820=LINE('',#413317,#33622);
#29821=LINE('',#413354,#33623);
#29822=LINE('',#414198,#33624);
#29823=LINE('',#414235,#33625);
#29824=LINE('',#414263,#33626);
#29825=LINE('',#414288,#33627);
#29826=LINE('',#414292,#33628);
#29827=LINE('',#414320,#33629);
#29828=LINE('',#414324,#33630);
#29829=LINE('',#414352,#33631);
#29830=LINE('',#414356,#33632);
#29831=LINE('',#414384,#33633);
#29832=LINE('',#414388,#33634);
#29833=LINE('',#414416,#33635);
#29834=LINE('',#414420,#33636);
#29835=LINE('',#414448,#33637);
#29836=LINE('',#414452,#33638);
#29837=LINE('',#414480,#33639);
#29838=LINE('',#414484,#33640);
#29839=LINE('',#414512,#33641);
#29840=LINE('',#414516,#33642);
#29841=LINE('',#414544,#33643);
#29842=LINE('',#414548,#33644);
#29843=LINE('',#414576,#33645);
#29844=LINE('',#414580,#33646);
#29845=LINE('',#414608,#33647);
#29846=LINE('',#414612,#33648);
#29847=LINE('',#414640,#33649);
#29848=LINE('',#414644,#33650);
#29849=LINE('',#414672,#33651);
#29850=LINE('',#414676,#33652);
#29851=LINE('',#414704,#33653);
#29852=LINE('',#414708,#33654);
#29853=LINE('',#414736,#33655);
#29854=LINE('',#414740,#33656);
#29855=LINE('',#414768,#33657);
#29856=LINE('',#414772,#33658);
#29857=LINE('',#414800,#33659);
#29858=LINE('',#414804,#33660);
#29859=LINE('',#414832,#33661);
#29860=LINE('',#414836,#33662);
#29861=LINE('',#414864,#33663);
#29862=LINE('',#414868,#33664);
#29863=LINE('',#414896,#33665);
#29864=LINE('',#414900,#33666);
#29865=LINE('',#414928,#33667);
#29866=LINE('',#414932,#33668);
#29867=LINE('',#414960,#33669);
#29868=LINE('',#414964,#33670);
#29869=LINE('',#414992,#33671);
#29870=LINE('',#414996,#33672);
#29871=LINE('',#415024,#33673);
#29872=LINE('',#415028,#33674);
#29873=LINE('',#415056,#33675);
#29874=LINE('',#415060,#33676);
#29875=LINE('',#415088,#33677);
#29876=LINE('',#415092,#33678);
#29877=LINE('',#415120,#33679);
#29878=LINE('',#415124,#33680);
#29879=LINE('',#415152,#33681);
#29880=LINE('',#415156,#33682);
#29881=LINE('',#415184,#33683);
#29882=LINE('',#415188,#33684);
#29883=LINE('',#415216,#33685);
#29884=LINE('',#415220,#33686);
#29885=LINE('',#415248,#33687);
#29886=LINE('',#415252,#33688);
#29887=LINE('',#415280,#33689);
#29888=LINE('',#415284,#33690);
#29889=LINE('',#415312,#33691);
#29890=LINE('',#415316,#33692);
#29891=LINE('',#415344,#33693);
#29892=LINE('',#415348,#33694);
#29893=LINE('',#415376,#33695);
#29894=LINE('',#415380,#33696);
#29895=LINE('',#415408,#33697);
#29896=LINE('',#415412,#33698);
#29897=LINE('',#415440,#33699);
#29898=LINE('',#415444,#33700);
#29899=LINE('',#415472,#33701);
#29900=LINE('',#415476,#33702);
#29901=LINE('',#415504,#33703);
#29902=LINE('',#415508,#33704);
#29903=LINE('',#415515,#33705);
#29904=LINE('',#415543,#33706);
#29905=LINE('',#415547,#33707);
#29906=LINE('',#415575,#33708);
#29907=LINE('',#415579,#33709);
#29908=LINE('',#415607,#33710);
#29909=LINE('',#415611,#33711);
#29910=LINE('',#415639,#33712);
#29911=LINE('',#415643,#33713);
#29912=LINE('',#415671,#33714);
#29913=LINE('',#415675,#33715);
#29914=LINE('',#415703,#33716);
#29915=LINE('',#415707,#33717);
#29916=LINE('',#415735,#33718);
#29917=LINE('',#415739,#33719);
#29918=LINE('',#415767,#33720);
#29919=LINE('',#415771,#33721);
#29920=LINE('',#415799,#33722);
#29921=LINE('',#415803,#33723);
#29922=LINE('',#415831,#33724);
#29923=LINE('',#415835,#33725);
#29924=LINE('',#415863,#33726);
#29925=LINE('',#415867,#33727);
#29926=LINE('',#415895,#33728);
#29927=LINE('',#415899,#33729);
#29928=LINE('',#415927,#33730);
#29929=LINE('',#415931,#33731);
#29930=LINE('',#415959,#33732);
#29931=LINE('',#415963,#33733);
#29932=LINE('',#415991,#33734);
#29933=LINE('',#415995,#33735);
#29934=LINE('',#416023,#33736);
#29935=LINE('',#416027,#33737);
#29936=LINE('',#416055,#33738);
#29937=LINE('',#416059,#33739);
#29938=LINE('',#416087,#33740);
#29939=LINE('',#416091,#33741);
#29940=LINE('',#416119,#33742);
#29941=LINE('',#416123,#33743);
#29942=LINE('',#416151,#33744);
#29943=LINE('',#416155,#33745);
#29944=LINE('',#416183,#33746);
#29945=LINE('',#416187,#33747);
#29946=LINE('',#416215,#33748);
#29947=LINE('',#416219,#33749);
#29948=LINE('',#416247,#33750);
#29949=LINE('',#416251,#33751);
#29950=LINE('',#416279,#33752);
#29951=LINE('',#416283,#33753);
#29952=LINE('',#416311,#33754);
#29953=LINE('',#416315,#33755);
#29954=LINE('',#416343,#33756);
#29955=LINE('',#416347,#33757);
#29956=LINE('',#416375,#33758);
#29957=LINE('',#416379,#33759);
#29958=LINE('',#416407,#33760);
#29959=LINE('',#416411,#33761);
#29960=LINE('',#416439,#33762);
#29961=LINE('',#416443,#33763);
#29962=LINE('',#416471,#33764);
#29963=LINE('',#416475,#33765);
#29964=LINE('',#416503,#33766);
#29965=LINE('',#416507,#33767);
#29966=LINE('',#416535,#33768);
#29967=LINE('',#416539,#33769);
#29968=LINE('',#416567,#33770);
#29969=LINE('',#416571,#33771);
#29970=LINE('',#416599,#33772);
#29971=LINE('',#416603,#33773);
#29972=LINE('',#416631,#33774);
#29973=LINE('',#416635,#33775);
#29974=LINE('',#416663,#33776);
#29975=LINE('',#416667,#33777);
#29976=LINE('',#416695,#33778);
#29977=LINE('',#416699,#33779);
#29978=LINE('',#416727,#33780);
#29979=LINE('',#416731,#33781);
#29980=LINE('',#416754,#33782);
#29981=LINE('',#416789,#33783);
#29982=LINE('',#416793,#33784);
#29983=LINE('',#416828,#33785);
#29984=LINE('',#416832,#33786);
#29985=LINE('',#416867,#33787);
#29986=LINE('',#416871,#33788);
#29987=LINE('',#416906,#33789);
#29988=LINE('',#416910,#33790);
#29989=LINE('',#416945,#33791);
#29990=LINE('',#416949,#33792);
#29991=LINE('',#416984,#33793);
#29992=LINE('',#416988,#33794);
#29993=LINE('',#417023,#33795);
#29994=LINE('',#417027,#33796);
#29995=LINE('',#417062,#33797);
#29996=LINE('',#417066,#33798);
#29997=LINE('',#417101,#33799);
#29998=LINE('',#417105,#33800);
#29999=LINE('',#417140,#33801);
#30000=LINE('',#417144,#33802);
#30001=LINE('',#417179,#33803);
#30002=LINE('',#417183,#33804);
#30003=LINE('',#417218,#33805);
#30004=LINE('',#417222,#33806);
#30005=LINE('',#417257,#33807);
#30006=LINE('',#417261,#33808);
#30007=LINE('',#417296,#33809);
#30008=LINE('',#417300,#33810);
#30009=LINE('',#417335,#33811);
#30010=LINE('',#417339,#33812);
#30011=LINE('',#417374,#33813);
#30012=LINE('',#417378,#33814);
#30013=LINE('',#417413,#33815);
#30014=LINE('',#417417,#33816);
#30015=LINE('',#417452,#33817);
#30016=LINE('',#417456,#33818);
#30017=LINE('',#417491,#33819);
#30018=LINE('',#417495,#33820);
#30019=LINE('',#417530,#33821);
#30020=LINE('',#417534,#33822);
#30021=LINE('',#417569,#33823);
#30022=LINE('',#417573,#33824);
#30023=LINE('',#417608,#33825);
#30024=LINE('',#417612,#33826);
#30025=LINE('',#417647,#33827);
#30026=LINE('',#417651,#33828);
#30027=LINE('',#417686,#33829);
#30028=LINE('',#417690,#33830);
#30029=LINE('',#417725,#33831);
#30030=LINE('',#417729,#33832);
#30031=LINE('',#417764,#33833);
#30032=LINE('',#417768,#33834);
#30033=LINE('',#417803,#33835);
#30034=LINE('',#417807,#33836);
#30035=LINE('',#417842,#33837);
#30036=LINE('',#417846,#33838);
#30037=LINE('',#417881,#33839);
#30038=LINE('',#417885,#33840);
#30039=LINE('',#417920,#33841);
#30040=LINE('',#417924,#33842);
#30041=LINE('',#417959,#33843);
#30042=LINE('',#417963,#33844);
#30043=LINE('',#417998,#33845);
#30044=LINE('',#418002,#33846);
#30045=LINE('',#418037,#33847);
#30046=LINE('',#418041,#33848);
#30047=LINE('',#418076,#33849);
#30048=LINE('',#418080,#33850);
#30049=LINE('',#418115,#33851);
#30050=LINE('',#418119,#33852);
#30051=LINE('',#418154,#33853);
#30052=LINE('',#418158,#33854);
#30053=LINE('',#418193,#33855);
#30054=LINE('',#418197,#33856);
#30055=LINE('',#418232,#33857);
#30056=LINE('',#418236,#33858);
#30057=LINE('',#418253,#33859);
#30058=LINE('',#418272,#33860);
#30059=LINE('',#418276,#33861);
#30060=LINE('',#418311,#33862);
#30061=LINE('',#418315,#33863);
#30062=LINE('',#418350,#33864);
#30063=LINE('',#418354,#33865);
#30064=LINE('',#418389,#33866);
#30065=LINE('',#418393,#33867);
#30066=LINE('',#418428,#33868);
#30067=LINE('',#418432,#33869);
#30068=LINE('',#418467,#33870);
#30069=LINE('',#418471,#33871);
#30070=LINE('',#418506,#33872);
#30071=LINE('',#418510,#33873);
#30072=LINE('',#418545,#33874);
#30073=LINE('',#418549,#33875);
#30074=LINE('',#418584,#33876);
#30075=LINE('',#418588,#33877);
#30076=LINE('',#418623,#33878);
#30077=LINE('',#418627,#33879);
#30078=LINE('',#418662,#33880);
#30079=LINE('',#418666,#33881);
#30080=LINE('',#418701,#33882);
#30081=LINE('',#418705,#33883);
#30082=LINE('',#418740,#33884);
#30083=LINE('',#418744,#33885);
#30084=LINE('',#418779,#33886);
#30085=LINE('',#418783,#33887);
#30086=LINE('',#418818,#33888);
#30087=LINE('',#418822,#33889);
#30088=LINE('',#418857,#33890);
#30089=LINE('',#418861,#33891);
#30090=LINE('',#418896,#33892);
#30091=LINE('',#418900,#33893);
#30092=LINE('',#418935,#33894);
#30093=LINE('',#418939,#33895);
#30094=LINE('',#418974,#33896);
#30095=LINE('',#418978,#33897);
#30096=LINE('',#419013,#33898);
#30097=LINE('',#419017,#33899);
#30098=LINE('',#419052,#33900);
#30099=LINE('',#419056,#33901);
#30100=LINE('',#419091,#33902);
#30101=LINE('',#419095,#33903);
#30102=LINE('',#419130,#33904);
#30103=LINE('',#419134,#33905);
#30104=LINE('',#419169,#33906);
#30105=LINE('',#419173,#33907);
#30106=LINE('',#419208,#33908);
#30107=LINE('',#419212,#33909);
#30108=LINE('',#419247,#33910);
#30109=LINE('',#419251,#33911);
#30110=LINE('',#419286,#33912);
#30111=LINE('',#419290,#33913);
#30112=LINE('',#419325,#33914);
#30113=LINE('',#419329,#33915);
#30114=LINE('',#419364,#33916);
#30115=LINE('',#419368,#33917);
#30116=LINE('',#419403,#33918);
#30117=LINE('',#419407,#33919);
#30118=LINE('',#419442,#33920);
#30119=LINE('',#419446,#33921);
#30120=LINE('',#419481,#33922);
#30121=LINE('',#419485,#33923);
#30122=LINE('',#419520,#33924);
#30123=LINE('',#419524,#33925);
#30124=LINE('',#419559,#33926);
#30125=LINE('',#419563,#33927);
#30126=LINE('',#419598,#33928);
#30127=LINE('',#419602,#33929);
#30128=LINE('',#419637,#33930);
#30129=LINE('',#419641,#33931);
#30130=LINE('',#419676,#33932);
#30131=LINE('',#419680,#33933);
#30132=LINE('',#419715,#33934);
#30133=LINE('',#419719,#33935);
#30134=LINE('',#419753,#33936);
#30135=LINE('',#419985,#33937);
#30136=LINE('',#420054,#33938);
#30137=LINE('',#420062,#33939);
#30138=LINE('',#420068,#33940);
#30139=LINE('',#420071,#33941);
#30140=LINE('',#420075,#33942);
#30141=LINE('',#420083,#33943);
#30142=LINE('',#420084,#33944);
#30143=LINE('',#420087,#33945);
#30144=LINE('',#420088,#33946);
#30145=LINE('',#420091,#33947);
#30146=LINE('',#420092,#33948);
#30147=LINE('',#420095,#33949);
#30148=LINE('',#420096,#33950);
#30149=LINE('',#420099,#33951);
#30150=LINE('',#420100,#33952);
#30151=LINE('',#420115,#33953);
#30152=LINE('',#420120,#33954);
#30153=LINE('',#420121,#33955);
#30154=LINE('',#420123,#33956);
#30155=LINE('',#420125,#33957);
#30156=LINE('',#420130,#33958);
#30157=LINE('',#420135,#33959);
#30158=LINE('',#420143,#33960);
#30159=LINE('',#422870,#33961);
#30160=LINE('',#422872,#33962);
#30161=LINE('',#422876,#33963);
#30162=LINE('',#422886,#33964);
#30163=LINE('',#422888,#33965);
#30164=LINE('',#422894,#33966);
#30165=LINE('',#423219,#33967);
#30166=LINE('',#423221,#33968);
#30167=LINE('',#423225,#33969);
#30168=LINE('',#423235,#33970);
#30169=LINE('',#423237,#33971);
#30170=LINE('',#423243,#33972);
#30171=LINE('',#423568,#33973);
#30172=LINE('',#423570,#33974);
#30173=LINE('',#423574,#33975);
#30174=LINE('',#423584,#33976);
#30175=LINE('',#423586,#33977);
#30176=LINE('',#423592,#33978);
#30177=LINE('',#423917,#33979);
#30178=LINE('',#423919,#33980);
#30179=LINE('',#423923,#33981);
#30180=LINE('',#423933,#33982);
#30181=LINE('',#423935,#33983);
#30182=LINE('',#423941,#33984);
#30183=LINE('',#424266,#33985);
#30184=LINE('',#424268,#33986);
#30185=LINE('',#424272,#33987);
#30186=LINE('',#424282,#33988);
#30187=LINE('',#424284,#33989);
#30188=LINE('',#424290,#33990);
#30189=LINE('',#424615,#33991);
#30190=LINE('',#424617,#33992);
#30191=LINE('',#424621,#33993);
#30192=LINE('',#424631,#33994);
#30193=LINE('',#424633,#33995);
#30194=LINE('',#424639,#33996);
#30195=LINE('',#424964,#33997);
#30196=LINE('',#424966,#33998);
#30197=LINE('',#424970,#33999);
#30198=LINE('',#424980,#34000);
#30199=LINE('',#424982,#34001);
#30200=LINE('',#424988,#34002);
#30201=LINE('',#425313,#34003);
#30202=LINE('',#425315,#34004);
#30203=LINE('',#425319,#34005);
#30204=LINE('',#425329,#34006);
#30205=LINE('',#425331,#34007);
#30206=LINE('',#425337,#34008);
#30207=LINE('',#425662,#34009);
#30208=LINE('',#425664,#34010);
#30209=LINE('',#425668,#34011);
#30210=LINE('',#425678,#34012);
#30211=LINE('',#425680,#34013);
#30212=LINE('',#425686,#34014);
#30213=LINE('',#426011,#34015);
#30214=LINE('',#426013,#34016);
#30215=LINE('',#426017,#34017);
#30216=LINE('',#426027,#34018);
#30217=LINE('',#426029,#34019);
#30218=LINE('',#426035,#34020);
#30219=LINE('',#426360,#34021);
#30220=LINE('',#426362,#34022);
#30221=LINE('',#426366,#34023);
#30222=LINE('',#426376,#34024);
#30223=LINE('',#426378,#34025);
#30224=LINE('',#426384,#34026);
#30225=LINE('',#426709,#34027);
#30226=LINE('',#426711,#34028);
#30227=LINE('',#426715,#34029);
#30228=LINE('',#426725,#34030);
#30229=LINE('',#426727,#34031);
#30230=LINE('',#426733,#34032);
#30231=LINE('',#427058,#34033);
#30232=LINE('',#427060,#34034);
#30233=LINE('',#427064,#34035);
#30234=LINE('',#427074,#34036);
#30235=LINE('',#427076,#34037);
#30236=LINE('',#427082,#34038);
#30237=LINE('',#427407,#34039);
#30238=LINE('',#427409,#34040);
#30239=LINE('',#427413,#34041);
#30240=LINE('',#427423,#34042);
#30241=LINE('',#427425,#34043);
#30242=LINE('',#427431,#34044);
#30243=LINE('',#427756,#34045);
#30244=LINE('',#427758,#34046);
#30245=LINE('',#427762,#34047);
#30246=LINE('',#427772,#34048);
#30247=LINE('',#427774,#34049);
#30248=LINE('',#427780,#34050);
#30249=LINE('',#428105,#34051);
#30250=LINE('',#428107,#34052);
#30251=LINE('',#428111,#34053);
#30252=LINE('',#428121,#34054);
#30253=LINE('',#428123,#34055);
#30254=LINE('',#428129,#34056);
#30255=LINE('',#428454,#34057);
#30256=LINE('',#428456,#34058);
#30257=LINE('',#428460,#34059);
#30258=LINE('',#428470,#34060);
#30259=LINE('',#428472,#34061);
#30260=LINE('',#428478,#34062);
#30261=LINE('',#428803,#34063);
#30262=LINE('',#428805,#34064);
#30263=LINE('',#428809,#34065);
#30264=LINE('',#428819,#34066);
#30265=LINE('',#428821,#34067);
#30266=LINE('',#428827,#34068);
#30267=LINE('',#429152,#34069);
#30268=LINE('',#429154,#34070);
#30269=LINE('',#429158,#34071);
#30270=LINE('',#429168,#34072);
#30271=LINE('',#429170,#34073);
#30272=LINE('',#429176,#34074);
#30273=LINE('',#429501,#34075);
#30274=LINE('',#429503,#34076);
#30275=LINE('',#429507,#34077);
#30276=LINE('',#429517,#34078);
#30277=LINE('',#429519,#34079);
#30278=LINE('',#429525,#34080);
#30279=LINE('',#429850,#34081);
#30280=LINE('',#429852,#34082);
#30281=LINE('',#429856,#34083);
#30282=LINE('',#429866,#34084);
#30283=LINE('',#429868,#34085);
#30284=LINE('',#429874,#34086);
#30285=LINE('',#430199,#34087);
#30286=LINE('',#430201,#34088);
#30287=LINE('',#430205,#34089);
#30288=LINE('',#430215,#34090);
#30289=LINE('',#430217,#34091);
#30290=LINE('',#430223,#34092);
#30291=LINE('',#430548,#34093);
#30292=LINE('',#430550,#34094);
#30293=LINE('',#430554,#34095);
#30294=LINE('',#430564,#34096);
#30295=LINE('',#430566,#34097);
#30296=LINE('',#430572,#34098);
#30297=LINE('',#430897,#34099);
#30298=LINE('',#430899,#34100);
#30299=LINE('',#430903,#34101);
#30300=LINE('',#430913,#34102);
#30301=LINE('',#430915,#34103);
#30302=LINE('',#430921,#34104);
#30303=LINE('',#431246,#34105);
#30304=LINE('',#431248,#34106);
#30305=LINE('',#431252,#34107);
#30306=LINE('',#431262,#34108);
#30307=LINE('',#431264,#34109);
#30308=LINE('',#431270,#34110);
#30309=LINE('',#431595,#34111);
#30310=LINE('',#431597,#34112);
#30311=LINE('',#431601,#34113);
#30312=LINE('',#431611,#34114);
#30313=LINE('',#431613,#34115);
#30314=LINE('',#431619,#34116);
#30315=LINE('',#431944,#34117);
#30316=LINE('',#431946,#34118);
#30317=LINE('',#431950,#34119);
#30318=LINE('',#431960,#34120);
#30319=LINE('',#431962,#34121);
#30320=LINE('',#431968,#34122);
#30321=LINE('',#432293,#34123);
#30322=LINE('',#432295,#34124);
#30323=LINE('',#432299,#34125);
#30324=LINE('',#432309,#34126);
#30325=LINE('',#432311,#34127);
#30326=LINE('',#432317,#34128);
#30327=LINE('',#432642,#34129);
#30328=LINE('',#432644,#34130);
#30329=LINE('',#432648,#34131);
#30330=LINE('',#432658,#34132);
#30331=LINE('',#432660,#34133);
#30332=LINE('',#432666,#34134);
#30333=LINE('',#432991,#34135);
#30334=LINE('',#432993,#34136);
#30335=LINE('',#432997,#34137);
#30336=LINE('',#433007,#34138);
#30337=LINE('',#433009,#34139);
#30338=LINE('',#433015,#34140);
#30339=LINE('',#433340,#34141);
#30340=LINE('',#433342,#34142);
#30341=LINE('',#433346,#34143);
#30342=LINE('',#433356,#34144);
#30343=LINE('',#433358,#34145);
#30344=LINE('',#433364,#34146);
#30345=LINE('',#433689,#34147);
#30346=LINE('',#433691,#34148);
#30347=LINE('',#433695,#34149);
#30348=LINE('',#433705,#34150);
#30349=LINE('',#433707,#34151);
#30350=LINE('',#433713,#34152);
#30351=LINE('',#434038,#34153);
#30352=LINE('',#434040,#34154);
#30353=LINE('',#434044,#34155);
#30354=LINE('',#434054,#34156);
#30355=LINE('',#434056,#34157);
#30356=LINE('',#434062,#34158);
#30357=LINE('',#434387,#34159);
#30358=LINE('',#434389,#34160);
#30359=LINE('',#434393,#34161);
#30360=LINE('',#434403,#34162);
#30361=LINE('',#434405,#34163);
#30362=LINE('',#434411,#34164);
#30363=LINE('',#434736,#34165);
#30364=LINE('',#434738,#34166);
#30365=LINE('',#434742,#34167);
#30366=LINE('',#434752,#34168);
#30367=LINE('',#434754,#34169);
#30368=LINE('',#434760,#34170);
#30369=LINE('',#435085,#34171);
#30370=LINE('',#435087,#34172);
#30371=LINE('',#435091,#34173);
#30372=LINE('',#435101,#34174);
#30373=LINE('',#435103,#34175);
#30374=LINE('',#435109,#34176);
#30375=LINE('',#435434,#34177);
#30376=LINE('',#435436,#34178);
#30377=LINE('',#435440,#34179);
#30378=LINE('',#435450,#34180);
#30379=LINE('',#435452,#34181);
#30380=LINE('',#435458,#34182);
#30381=LINE('',#435783,#34183);
#30382=LINE('',#435785,#34184);
#30383=LINE('',#435789,#34185);
#30384=LINE('',#435799,#34186);
#30385=LINE('',#435801,#34187);
#30386=LINE('',#435807,#34188);
#30387=LINE('',#436132,#34189);
#30388=LINE('',#436134,#34190);
#30389=LINE('',#436138,#34191);
#30390=LINE('',#436148,#34192);
#30391=LINE('',#436150,#34193);
#30392=LINE('',#436156,#34194);
#30393=LINE('',#436481,#34195);
#30394=LINE('',#436483,#34196);
#30395=LINE('',#436487,#34197);
#30396=LINE('',#436497,#34198);
#30397=LINE('',#436499,#34199);
#30398=LINE('',#436505,#34200);
#30399=LINE('',#436830,#34201);
#30400=LINE('',#436832,#34202);
#30401=LINE('',#436836,#34203);
#30402=LINE('',#436846,#34204);
#30403=LINE('',#436848,#34205);
#30404=LINE('',#436854,#34206);
#30405=LINE('',#437179,#34207);
#30406=LINE('',#437181,#34208);
#30407=LINE('',#437185,#34209);
#30408=LINE('',#437195,#34210);
#30409=LINE('',#437197,#34211);
#30410=LINE('',#437203,#34212);
#30411=LINE('',#437528,#34213);
#30412=LINE('',#437530,#34214);
#30413=LINE('',#437534,#34215);
#30414=LINE('',#437544,#34216);
#30415=LINE('',#437546,#34217);
#30416=LINE('',#437552,#34218);
#30417=LINE('',#437877,#34219);
#30418=LINE('',#437879,#34220);
#30419=LINE('',#437883,#34221);
#30420=LINE('',#437893,#34222);
#30421=LINE('',#437895,#34223);
#30422=LINE('',#437901,#34224);
#30423=LINE('',#438226,#34225);
#30424=LINE('',#438228,#34226);
#30425=LINE('',#438232,#34227);
#30426=LINE('',#438242,#34228);
#30427=LINE('',#438244,#34229);
#30428=LINE('',#438250,#34230);
#30429=LINE('',#438575,#34231);
#30430=LINE('',#438577,#34232);
#30431=LINE('',#438581,#34233);
#30432=LINE('',#438591,#34234);
#30433=LINE('',#438593,#34235);
#30434=LINE('',#438599,#34236);
#30435=LINE('',#438924,#34237);
#30436=LINE('',#438926,#34238);
#30437=LINE('',#438930,#34239);
#30438=LINE('',#438940,#34240);
#30439=LINE('',#438942,#34241);
#30440=LINE('',#438948,#34242);
#30441=LINE('',#439273,#34243);
#30442=LINE('',#439275,#34244);
#30443=LINE('',#439279,#34245);
#30444=LINE('',#439289,#34246);
#30445=LINE('',#439291,#34247);
#30446=LINE('',#439297,#34248);
#30447=LINE('',#439622,#34249);
#30448=LINE('',#439624,#34250);
#30449=LINE('',#439628,#34251);
#30450=LINE('',#439638,#34252);
#30451=LINE('',#439640,#34253);
#30452=LINE('',#439646,#34254);
#30453=LINE('',#439971,#34255);
#30454=LINE('',#439973,#34256);
#30455=LINE('',#439977,#34257);
#30456=LINE('',#439987,#34258);
#30457=LINE('',#439989,#34259);
#30458=LINE('',#439995,#34260);
#30459=LINE('',#440320,#34261);
#30460=LINE('',#440322,#34262);
#30461=LINE('',#440326,#34263);
#30462=LINE('',#440336,#34264);
#30463=LINE('',#440338,#34265);
#30464=LINE('',#440344,#34266);
#30465=LINE('',#440669,#34267);
#30466=LINE('',#440671,#34268);
#30467=LINE('',#440675,#34269);
#30468=LINE('',#440685,#34270);
#30469=LINE('',#440687,#34271);
#30470=LINE('',#440693,#34272);
#30471=LINE('',#441018,#34273);
#30472=LINE('',#441020,#34274);
#30473=LINE('',#441024,#34275);
#30474=LINE('',#441034,#34276);
#30475=LINE('',#441036,#34277);
#30476=LINE('',#441042,#34278);
#30477=LINE('',#441367,#34279);
#30478=LINE('',#441369,#34280);
#30479=LINE('',#441373,#34281);
#30480=LINE('',#441383,#34282);
#30481=LINE('',#441385,#34283);
#30482=LINE('',#441391,#34284);
#30483=LINE('',#441716,#34285);
#30484=LINE('',#441718,#34286);
#30485=LINE('',#441722,#34287);
#30486=LINE('',#441732,#34288);
#30487=LINE('',#441734,#34289);
#30488=LINE('',#441740,#34290);
#30489=LINE('',#442065,#34291);
#30490=LINE('',#442067,#34292);
#30491=LINE('',#442071,#34293);
#30492=LINE('',#442081,#34294);
#30493=LINE('',#442083,#34295);
#30494=LINE('',#442089,#34296);
#30495=LINE('',#442414,#34297);
#30496=LINE('',#442416,#34298);
#30497=LINE('',#442420,#34299);
#30498=LINE('',#442430,#34300);
#30499=LINE('',#442432,#34301);
#30500=LINE('',#442438,#34302);
#30501=LINE('',#442763,#34303);
#30502=LINE('',#442765,#34304);
#30503=LINE('',#442769,#34305);
#30504=LINE('',#442779,#34306);
#30505=LINE('',#442781,#34307);
#30506=LINE('',#442787,#34308);
#30507=LINE('',#443112,#34309);
#30508=LINE('',#443114,#34310);
#30509=LINE('',#443118,#34311);
#30510=LINE('',#443128,#34312);
#30511=LINE('',#443130,#34313);
#30512=LINE('',#443136,#34314);
#30513=LINE('',#443461,#34315);
#30514=LINE('',#443463,#34316);
#30515=LINE('',#443467,#34317);
#30516=LINE('',#443477,#34318);
#30517=LINE('',#443479,#34319);
#30518=LINE('',#443485,#34320);
#30519=LINE('',#443810,#34321);
#30520=LINE('',#443812,#34322);
#30521=LINE('',#443816,#34323);
#30522=LINE('',#443826,#34324);
#30523=LINE('',#443828,#34325);
#30524=LINE('',#443834,#34326);
#30525=LINE('',#444159,#34327);
#30526=LINE('',#444161,#34328);
#30527=LINE('',#444165,#34329);
#30528=LINE('',#444175,#34330);
#30529=LINE('',#444177,#34331);
#30530=LINE('',#444183,#34332);
#30531=LINE('',#444508,#34333);
#30532=LINE('',#444510,#34334);
#30533=LINE('',#444514,#34335);
#30534=LINE('',#444524,#34336);
#30535=LINE('',#444526,#34337);
#30536=LINE('',#444532,#34338);
#30537=LINE('',#444857,#34339);
#30538=LINE('',#444859,#34340);
#30539=LINE('',#444863,#34341);
#30540=LINE('',#444873,#34342);
#30541=LINE('',#444875,#34343);
#30542=LINE('',#444881,#34344);
#30543=LINE('',#445206,#34345);
#30544=LINE('',#445208,#34346);
#30545=LINE('',#445212,#34347);
#30546=LINE('',#445222,#34348);
#30547=LINE('',#445224,#34349);
#30548=LINE('',#445230,#34350);
#30549=LINE('',#445555,#34351);
#30550=LINE('',#445557,#34352);
#30551=LINE('',#445561,#34353);
#30552=LINE('',#445571,#34354);
#30553=LINE('',#445573,#34355);
#30554=LINE('',#445579,#34356);
#30555=LINE('',#445904,#34357);
#30556=LINE('',#445906,#34358);
#30557=LINE('',#445910,#34359);
#30558=LINE('',#445920,#34360);
#30559=LINE('',#445922,#34361);
#30560=LINE('',#445928,#34362);
#30561=LINE('',#446253,#34363);
#30562=LINE('',#446255,#34364);
#30563=LINE('',#446259,#34365);
#30564=LINE('',#446269,#34366);
#30565=LINE('',#446271,#34367);
#30566=LINE('',#446277,#34368);
#30567=LINE('',#446602,#34369);
#30568=LINE('',#446604,#34370);
#30569=LINE('',#446608,#34371);
#30570=LINE('',#446618,#34372);
#30571=LINE('',#446620,#34373);
#30572=LINE('',#446626,#34374);
#30573=LINE('',#446951,#34375);
#30574=LINE('',#446953,#34376);
#30575=LINE('',#446957,#34377);
#30576=LINE('',#446967,#34378);
#30577=LINE('',#446969,#34379);
#30578=LINE('',#446975,#34380);
#30579=LINE('',#447300,#34381);
#30580=LINE('',#447302,#34382);
#30581=LINE('',#447306,#34383);
#30582=LINE('',#447316,#34384);
#30583=LINE('',#447318,#34385);
#30584=LINE('',#447324,#34386);
#30585=LINE('',#447649,#34387);
#30586=LINE('',#447651,#34388);
#30587=LINE('',#447655,#34389);
#30588=LINE('',#447665,#34390);
#30589=LINE('',#447667,#34391);
#30590=LINE('',#447673,#34392);
#30591=LINE('',#447998,#34393);
#30592=LINE('',#448000,#34394);
#30593=LINE('',#448004,#34395);
#30594=LINE('',#448014,#34396);
#30595=LINE('',#448016,#34397);
#30596=LINE('',#448022,#34398);
#30597=LINE('',#448347,#34399);
#30598=LINE('',#448349,#34400);
#30599=LINE('',#448353,#34401);
#30600=LINE('',#448363,#34402);
#30601=LINE('',#448365,#34403);
#30602=LINE('',#448371,#34404);
#30603=LINE('',#448696,#34405);
#30604=LINE('',#448698,#34406);
#30605=LINE('',#448702,#34407);
#30606=LINE('',#448712,#34408);
#30607=LINE('',#448714,#34409);
#30608=LINE('',#448720,#34410);
#30609=LINE('',#449045,#34411);
#30610=LINE('',#449047,#34412);
#30611=LINE('',#449051,#34413);
#30612=LINE('',#449061,#34414);
#30613=LINE('',#449063,#34415);
#30614=LINE('',#449069,#34416);
#33550=VECTOR('',#123768,1.17524047358089);
#33551=VECTOR('',#123773,1.17524047358089);
#33552=VECTOR('',#123776,1.17524047358089);
#33553=VECTOR('',#123779,1.17524047358089);
#33554=VECTOR('',#123782,1.17524047358089);
#33555=VECTOR('',#123785,1.17524047358089);
#33556=VECTOR('',#123788,1.17524047358089);
#33557=VECTOR('',#123791,1.17524047358089);
#33558=VECTOR('',#123794,1.17524047358089);
#33559=VECTOR('',#123797,1.17524047358089);
#33560=VECTOR('',#123800,1.17524047358089);
#33561=VECTOR('',#123803,1.17524047358089);
#33562=VECTOR('',#123806,1.17524047358089);
#33563=VECTOR('',#123809,1.17524047358089);
#33564=VECTOR('',#123812,1.17524047358089);
#33565=VECTOR('',#123815,1.17524047358089);
#33566=VECTOR('',#123818,1.17524047358089);
#33567=VECTOR('',#123821,1.17524047358089);
#33568=VECTOR('',#123824,1.17524047358089);
#33569=VECTOR('',#123827,1.17524047358089);
#33570=VECTOR('',#123830,1.17524047358089);
#33571=VECTOR('',#123833,1.17524047358089);
#33572=VECTOR('',#123836,1.17524047358089);
#33573=VECTOR('',#123839,1.17524047358089);
#33574=VECTOR('',#123842,1.17524047358089);
#33575=VECTOR('',#123845,1.17524047358089);
#33576=VECTOR('',#123848,1.17524047358089);
#33577=VECTOR('',#123851,1.17524047358089);
#33578=VECTOR('',#123854,1.17524047358089);
#33579=VECTOR('',#123857,1.17524047358089);
#33580=VECTOR('',#123860,1.17524047358089);
#33581=VECTOR('',#123863,1.17524047358089);
#33582=VECTOR('',#123866,1.17524047358089);
#33583=VECTOR('',#123869,1.17524047358089);
#33584=VECTOR('',#123872,1.17524047358089);
#33585=VECTOR('',#123875,1.17524047358089);
#33586=VECTOR('',#123878,999.999999999989);
#33587=VECTOR('',#123883,1.17524047358087);
#33588=VECTOR('',#123888,1.50000000000006);
#33589=VECTOR('',#123893,1.50000000000006);
#33590=VECTOR('',#123896,1.50000000000006);
#33591=VECTOR('',#123899,1.50000000000006);
#33592=VECTOR('',#123902,1.50000000000006);
#33593=VECTOR('',#123905,1.50000000000006);
#33594=VECTOR('',#123908,1.50000000000006);
#33595=VECTOR('',#123911,1.50000000000006);
#33596=VECTOR('',#123914,1.50000000000006);
#33597=VECTOR('',#123917,1.50000000000006);
#33598=VECTOR('',#123920,1.50000000000006);
#33599=VECTOR('',#123923,1.50000000000006);
#33600=VECTOR('',#123926,1.50000000000006);
#33601=VECTOR('',#123929,1.50000000000006);
#33602=VECTOR('',#123932,1.50000000000006);
#33603=VECTOR('',#123935,1.50000000000006);
#33604=VECTOR('',#123938,1.50000000000006);
#33605=VECTOR('',#123941,1.50000000000006);
#33606=VECTOR('',#123944,1.50000000000006);
#33607=VECTOR('',#123947,1.50000000000006);
#33608=VECTOR('',#123950,1.50000000000006);
#33609=VECTOR('',#123953,1.50000000000006);
#33610=VECTOR('',#123956,1.50000000000006);
#33611=VECTOR('',#123959,1.50000000000006);
#33612=VECTOR('',#123962,1.50000000000006);
#33613=VECTOR('',#123965,1.50000000000006);
#33614=VECTOR('',#123968,1.50000000000006);
#33615=VECTOR('',#123971,1.50000000000006);
#33616=VECTOR('',#123974,1.50000000000006);
#33617=VECTOR('',#123977,1.50000000000006);
#33618=VECTOR('',#123980,1.50000000000006);
#33619=VECTOR('',#123983,1.50000000000006);
#33620=VECTOR('',#123986,1.50000000000006);
#33621=VECTOR('',#123989,1.50000000000006);
#33622=VECTOR('',#123994,1.50000000000006);
#33623=VECTOR('',#123997,1.50000000000006);
#33624=VECTOR('',#124780,1.50000000000006);
#33625=VECTOR('',#124785,1.25);
#33626=VECTOR('',#124814,2.55577460325564);
#33627=VECTOR('',#124823,10.);
#33628=VECTOR('',#124826,10.);
#33629=VECTOR('',#124827,10.);
#33630=VECTOR('',#124830,10.);
#33631=VECTOR('',#124831,10.);
#33632=VECTOR('',#124834,10.);
#33633=VECTOR('',#124835,10.);
#33634=VECTOR('',#124838,10.);
#33635=VECTOR('',#124839,10.);
#33636=VECTOR('',#124842,10.);
#33637=VECTOR('',#124843,10.);
#33638=VECTOR('',#124846,10.);
#33639=VECTOR('',#124847,10.);
#33640=VECTOR('',#124850,10.);
#33641=VECTOR('',#124851,10.);
#33642=VECTOR('',#124854,10.);
#33643=VECTOR('',#124855,10.);
#33644=VECTOR('',#124858,10.);
#33645=VECTOR('',#124859,10.);
#33646=VECTOR('',#124862,10.);
#33647=VECTOR('',#124863,10.);
#33648=VECTOR('',#124866,10.);
#33649=VECTOR('',#124867,10.);
#33650=VECTOR('',#124870,10.);
#33651=VECTOR('',#124871,10.);
#33652=VECTOR('',#124874,10.);
#33653=VECTOR('',#124875,10.);
#33654=VECTOR('',#124878,10.);
#33655=VECTOR('',#124879,10.);
#33656=VECTOR('',#124882,10.);
#33657=VECTOR('',#124883,10.);
#33658=VECTOR('',#124886,10.);
#33659=VECTOR('',#124887,10.);
#33660=VECTOR('',#124890,10.);
#33661=VECTOR('',#124891,10.);
#33662=VECTOR('',#124894,10.);
#33663=VECTOR('',#124895,10.);
#33664=VECTOR('',#124898,10.);
#33665=VECTOR('',#124899,10.);
#33666=VECTOR('',#124902,10.);
#33667=VECTOR('',#124903,10.);
#33668=VECTOR('',#124906,10.);
#33669=VECTOR('',#124907,10.);
#33670=VECTOR('',#124910,10.);
#33671=VECTOR('',#124911,10.);
#33672=VECTOR('',#124914,10.);
#33673=VECTOR('',#124915,10.);
#33674=VECTOR('',#124918,10.);
#33675=VECTOR('',#124919,10.);
#33676=VECTOR('',#124922,10.);
#33677=VECTOR('',#124923,10.);
#33678=VECTOR('',#124926,10.);
#33679=VECTOR('',#124927,10.);
#33680=VECTOR('',#124930,10.);
#33681=VECTOR('',#124931,10.);
#33682=VECTOR('',#124934,10.);
#33683=VECTOR('',#124935,10.);
#33684=VECTOR('',#124938,10.);
#33685=VECTOR('',#124939,10.);
#33686=VECTOR('',#124942,10.);
#33687=VECTOR('',#124943,10.);
#33688=VECTOR('',#124946,10.);
#33689=VECTOR('',#124947,10.);
#33690=VECTOR('',#124950,10.);
#33691=VECTOR('',#124951,10.);
#33692=VECTOR('',#124954,10.);
#33693=VECTOR('',#124955,10.);
#33694=VECTOR('',#124958,10.);
#33695=VECTOR('',#124959,10.);
#33696=VECTOR('',#124962,10.);
#33697=VECTOR('',#124963,10.);
#33698=VECTOR('',#124966,10.);
#33699=VECTOR('',#124967,10.);
#33700=VECTOR('',#124970,10.);
#33701=VECTOR('',#124971,10.);
#33702=VECTOR('',#124974,10.);
#33703=VECTOR('',#124975,10.);
#33704=VECTOR('',#124978,2.72422539674441);
#33705=VECTOR('',#124985,10.);
#33706=VECTOR('',#124986,10.);
#33707=VECTOR('',#124989,10.);
#33708=VECTOR('',#124990,10.);
#33709=VECTOR('',#124993,10.);
#33710=VECTOR('',#124994,10.);
#33711=VECTOR('',#124997,10.);
#33712=VECTOR('',#124998,10.);
#33713=VECTOR('',#125001,10.);
#33714=VECTOR('',#125002,10.);
#33715=VECTOR('',#125005,10.);
#33716=VECTOR('',#125006,10.);
#33717=VECTOR('',#125009,10.);
#33718=VECTOR('',#125010,10.);
#33719=VECTOR('',#125013,10.);
#33720=VECTOR('',#125014,10.);
#33721=VECTOR('',#125017,10.);
#33722=VECTOR('',#125018,10.);
#33723=VECTOR('',#125021,10.);
#33724=VECTOR('',#125022,10.);
#33725=VECTOR('',#125025,10.);
#33726=VECTOR('',#125026,10.);
#33727=VECTOR('',#125029,10.);
#33728=VECTOR('',#125030,10.);
#33729=VECTOR('',#125033,10.);
#33730=VECTOR('',#125034,10.);
#33731=VECTOR('',#125037,10.);
#33732=VECTOR('',#125038,10.);
#33733=VECTOR('',#125041,10.);
#33734=VECTOR('',#125042,10.);
#33735=VECTOR('',#125045,10.);
#33736=VECTOR('',#125046,10.);
#33737=VECTOR('',#125049,10.);
#33738=VECTOR('',#125050,10.);
#33739=VECTOR('',#125053,10.);
#33740=VECTOR('',#125054,10.);
#33741=VECTOR('',#125057,10.);
#33742=VECTOR('',#125058,10.);
#33743=VECTOR('',#125061,10.);
#33744=VECTOR('',#125062,10.);
#33745=VECTOR('',#125065,10.);
#33746=VECTOR('',#125066,10.);
#33747=VECTOR('',#125069,10.);
#33748=VECTOR('',#125070,10.);
#33749=VECTOR('',#125073,10.);
#33750=VECTOR('',#125074,10.);
#33751=VECTOR('',#125077,10.);
#33752=VECTOR('',#125078,10.);
#33753=VECTOR('',#125081,10.);
#33754=VECTOR('',#125082,10.);
#33755=VECTOR('',#125085,10.);
#33756=VECTOR('',#125086,10.);
#33757=VECTOR('',#125089,10.);
#33758=VECTOR('',#125090,10.);
#33759=VECTOR('',#125093,10.);
#33760=VECTOR('',#125094,10.);
#33761=VECTOR('',#125097,10.);
#33762=VECTOR('',#125098,10.);
#33763=VECTOR('',#125101,10.);
#33764=VECTOR('',#125102,10.);
#33765=VECTOR('',#125105,10.);
#33766=VECTOR('',#125106,10.);
#33767=VECTOR('',#125109,10.);
#33768=VECTOR('',#125110,10.);
#33769=VECTOR('',#125113,10.);
#33770=VECTOR('',#125114,10.);
#33771=VECTOR('',#125117,10.);
#33772=VECTOR('',#125118,10.);
#33773=VECTOR('',#125121,10.);
#33774=VECTOR('',#125122,10.);
#33775=VECTOR('',#125125,10.);
#33776=VECTOR('',#125126,10.);
#33777=VECTOR('',#125129,10.);
#33778=VECTOR('',#125130,10.);
#33779=VECTOR('',#125133,10.);
#33780=VECTOR('',#125134,10.);
#33781=VECTOR('',#125137,10.);
#33782=VECTOR('',#125148,1000.);
#33783=VECTOR('',#125149,1000.);
#33784=VECTOR('',#125152,1000.);
#33785=VECTOR('',#125153,1000.);
#33786=VECTOR('',#125156,1000.);
#33787=VECTOR('',#125157,1000.);
#33788=VECTOR('',#125160,1000.);
#33789=VECTOR('',#125161,1000.);
#33790=VECTOR('',#125164,1000.);
#33791=VECTOR('',#125165,1000.);
#33792=VECTOR('',#125168,1000.);
#33793=VECTOR('',#125169,1000.);
#33794=VECTOR('',#125172,1000.);
#33795=VECTOR('',#125173,1000.);
#33796=VECTOR('',#125176,1000.);
#33797=VECTOR('',#125177,1000.);
#33798=VECTOR('',#125180,1000.);
#33799=VECTOR('',#125181,1000.);
#33800=VECTOR('',#125184,1000.);
#33801=VECTOR('',#125185,1000.);
#33802=VECTOR('',#125188,1000.);
#33803=VECTOR('',#125189,1000.);
#33804=VECTOR('',#125192,1000.);
#33805=VECTOR('',#125193,1000.);
#33806=VECTOR('',#125196,1000.);
#33807=VECTOR('',#125197,1000.);
#33808=VECTOR('',#125200,1000.);
#33809=VECTOR('',#125201,1000.);
#33810=VECTOR('',#125204,1000.);
#33811=VECTOR('',#125205,1000.);
#33812=VECTOR('',#125208,1000.);
#33813=VECTOR('',#125209,1000.);
#33814=VECTOR('',#125212,1000.);
#33815=VECTOR('',#125213,1000.);
#33816=VECTOR('',#125216,1000.);
#33817=VECTOR('',#125217,1000.);
#33818=VECTOR('',#125220,1000.);
#33819=VECTOR('',#125221,1000.);
#33820=VECTOR('',#125224,1000.);
#33821=VECTOR('',#125225,1000.);
#33822=VECTOR('',#125228,1000.);
#33823=VECTOR('',#125229,1000.);
#33824=VECTOR('',#125232,1000.);
#33825=VECTOR('',#125233,1000.);
#33826=VECTOR('',#125236,1000.);
#33827=VECTOR('',#125237,1000.);
#33828=VECTOR('',#125240,1000.);
#33829=VECTOR('',#125241,1000.);
#33830=VECTOR('',#125244,1000.);
#33831=VECTOR('',#125245,1000.);
#33832=VECTOR('',#125248,1000.);
#33833=VECTOR('',#125249,1000.);
#33834=VECTOR('',#125252,1000.);
#33835=VECTOR('',#125253,1000.);
#33836=VECTOR('',#125256,1000.);
#33837=VECTOR('',#125257,1000.);
#33838=VECTOR('',#125260,1000.);
#33839=VECTOR('',#125261,1000.);
#33840=VECTOR('',#125264,1000.);
#33841=VECTOR('',#125265,1000.);
#33842=VECTOR('',#125268,1000.);
#33843=VECTOR('',#125269,1000.);
#33844=VECTOR('',#125272,1000.);
#33845=VECTOR('',#125273,1000.);
#33846=VECTOR('',#125276,1000.);
#33847=VECTOR('',#125277,1000.);
#33848=VECTOR('',#125280,1000.);
#33849=VECTOR('',#125281,1000.);
#33850=VECTOR('',#125284,1000.);
#33851=VECTOR('',#125285,1000.);
#33852=VECTOR('',#125288,1000.);
#33853=VECTOR('',#125289,1000.);
#33854=VECTOR('',#125292,1000.);
#33855=VECTOR('',#125293,1000.);
#33856=VECTOR('',#125296,1000.);
#33857=VECTOR('',#125297,1000.);
#33858=VECTOR('',#125300,1000.);
#33859=VECTOR('',#125301,2.75);
#33860=VECTOR('',#125302,1000.);
#33861=VECTOR('',#125305,1000.);
#33862=VECTOR('',#125306,1000.);
#33863=VECTOR('',#125309,1000.);
#33864=VECTOR('',#125310,1000.);
#33865=VECTOR('',#125313,1000.);
#33866=VECTOR('',#125314,1000.);
#33867=VECTOR('',#125317,1000.);
#33868=VECTOR('',#125318,1000.);
#33869=VECTOR('',#125321,1000.);
#33870=VECTOR('',#125322,1000.);
#33871=VECTOR('',#125325,1000.);
#33872=VECTOR('',#125326,1000.);
#33873=VECTOR('',#125329,1000.);
#33874=VECTOR('',#125330,1000.);
#33875=VECTOR('',#125333,1000.);
#33876=VECTOR('',#125334,1000.);
#33877=VECTOR('',#125337,1000.);
#33878=VECTOR('',#125338,1000.);
#33879=VECTOR('',#125341,1000.);
#33880=VECTOR('',#125342,1000.);
#33881=VECTOR('',#125345,1000.);
#33882=VECTOR('',#125346,1000.);
#33883=VECTOR('',#125349,1000.);
#33884=VECTOR('',#125350,1000.);
#33885=VECTOR('',#125353,1000.);
#33886=VECTOR('',#125354,1000.);
#33887=VECTOR('',#125357,1000.);
#33888=VECTOR('',#125358,1000.);
#33889=VECTOR('',#125361,1000.);
#33890=VECTOR('',#125362,1000.);
#33891=VECTOR('',#125365,1000.);
#33892=VECTOR('',#125366,1000.);
#33893=VECTOR('',#125369,1000.);
#33894=VECTOR('',#125370,1000.);
#33895=VECTOR('',#125373,1000.);
#33896=VECTOR('',#125374,1000.);
#33897=VECTOR('',#125377,1000.);
#33898=VECTOR('',#125378,1000.);
#33899=VECTOR('',#125381,1000.);
#33900=VECTOR('',#125382,1000.);
#33901=VECTOR('',#125385,1000.);
#33902=VECTOR('',#125386,1000.);
#33903=VECTOR('',#125389,1000.);
#33904=VECTOR('',#125390,1000.);
#33905=VECTOR('',#125393,1000.);
#33906=VECTOR('',#125394,1000.);
#33907=VECTOR('',#125397,1000.);
#33908=VECTOR('',#125398,1000.);
#33909=VECTOR('',#125401,1000.);
#33910=VECTOR('',#125402,1000.);
#33911=VECTOR('',#125405,1000.);
#33912=VECTOR('',#125406,1000.);
#33913=VECTOR('',#125409,1000.);
#33914=VECTOR('',#125410,1000.);
#33915=VECTOR('',#125413,1000.);
#33916=VECTOR('',#125414,1000.);
#33917=VECTOR('',#125417,1000.);
#33918=VECTOR('',#125418,1000.);
#33919=VECTOR('',#125421,1000.);
#33920=VECTOR('',#125422,1000.);
#33921=VECTOR('',#125425,1000.);
#33922=VECTOR('',#125426,1000.);
#33923=VECTOR('',#125429,1000.);
#33924=VECTOR('',#125430,1000.);
#33925=VECTOR('',#125433,1000.);
#33926=VECTOR('',#125434,1000.);
#33927=VECTOR('',#125437,1000.);
#33928=VECTOR('',#125438,1000.);
#33929=VECTOR('',#125441,1000.);
#33930=VECTOR('',#125442,1000.);
#33931=VECTOR('',#125445,1000.);
#33932=VECTOR('',#125446,1000.);
#33933=VECTOR('',#125449,1000.);
#33934=VECTOR('',#125450,1000.);
#33935=VECTOR('',#125453,1000.);
#33936=VECTOR('',#125454,1000.);
#33937=VECTOR('',#125913,1000.);
#33938=VECTOR('',#125914,1000.);
#33939=VECTOR('',#125923,10.);
#33940=VECTOR('',#125924,1000.);
#33941=VECTOR('',#125927,10.);
#33942=VECTOR('',#125930,1000.);
#33943=VECTOR('',#125935,1000.);
#33944=VECTOR('',#125936,1000.);
#33945=VECTOR('',#125939,1000.);
#33946=VECTOR('',#125940,1000.);
#33947=VECTOR('',#125943,1000.);
#33948=VECTOR('',#125944,1000.);
#33949=VECTOR('',#125947,1000.);
#33950=VECTOR('',#125948,1000.);
#33951=VECTOR('',#125951,1000.);
#33952=VECTOR('',#125952,1000.);
#33953=VECTOR('',#125973,1000.);
#33954=VECTOR('',#125974,1000.);
#33955=VECTOR('',#125975,1000.);
#33956=VECTOR('',#125978,1000.);
#33957=VECTOR('',#125981,1000.);
#33958=VECTOR('',#125984,1000.);
#33959=VECTOR('',#125987,1000.);
#33960=VECTOR('',#125990,1000.);
#33961=VECTOR('',#126037,1000.);
#33962=VECTOR('',#126038,10.);
#33963=VECTOR('',#126041,1000.);
#33964=VECTOR('',#126046,10.);
#33965=VECTOR('',#126047,1000.);
#33966=VECTOR('',#126048,1000.);
#33967=VECTOR('',#126085,1000.);
#33968=VECTOR('',#126086,10.);
#33969=VECTOR('',#126089,1000.);
#33970=VECTOR('',#126094,10.);
#33971=VECTOR('',#126095,1000.);
#33972=VECTOR('',#126096,1000.);
#33973=VECTOR('',#126133,1000.);
#33974=VECTOR('',#126134,10.);
#33975=VECTOR('',#126137,1000.);
#33976=VECTOR('',#126142,10.);
#33977=VECTOR('',#126143,1000.);
#33978=VECTOR('',#126144,1000.);
#33979=VECTOR('',#126181,1000.);
#33980=VECTOR('',#126182,10.);
#33981=VECTOR('',#126185,1000.);
#33982=VECTOR('',#126190,10.);
#33983=VECTOR('',#126191,1000.);
#33984=VECTOR('',#126192,1000.);
#33985=VECTOR('',#126229,1000.);
#33986=VECTOR('',#126230,10.);
#33987=VECTOR('',#126233,1000.);
#33988=VECTOR('',#126238,10.);
#33989=VECTOR('',#126239,1000.);
#33990=VECTOR('',#126240,1000.);
#33991=VECTOR('',#126277,1000.);
#33992=VECTOR('',#126278,10.);
#33993=VECTOR('',#126281,1000.);
#33994=VECTOR('',#126286,10.);
#33995=VECTOR('',#126287,1000.);
#33996=VECTOR('',#126288,1000.);
#33997=VECTOR('',#126325,1000.);
#33998=VECTOR('',#126326,10.);
#33999=VECTOR('',#126329,1000.);
#34000=VECTOR('',#126334,10.);
#34001=VECTOR('',#126335,1000.);
#34002=VECTOR('',#126336,1000.);
#34003=VECTOR('',#126373,1000.);
#34004=VECTOR('',#126374,10.);
#34005=VECTOR('',#126377,1000.);
#34006=VECTOR('',#126382,10.);
#34007=VECTOR('',#126383,1000.);
#34008=VECTOR('',#126384,1000.);
#34009=VECTOR('',#126421,1000.);
#34010=VECTOR('',#126422,10.);
#34011=VECTOR('',#126425,1000.);
#34012=VECTOR('',#126430,10.);
#34013=VECTOR('',#126431,1000.);
#34014=VECTOR('',#126432,1000.);
#34015=VECTOR('',#126469,1000.);
#34016=VECTOR('',#126470,10.);
#34017=VECTOR('',#126473,1000.);
#34018=VECTOR('',#126478,10.);
#34019=VECTOR('',#126479,1000.);
#34020=VECTOR('',#126480,1000.);
#34021=VECTOR('',#126517,1000.);
#34022=VECTOR('',#126518,10.);
#34023=VECTOR('',#126521,1000.);
#34024=VECTOR('',#126526,10.);
#34025=VECTOR('',#126527,1000.);
#34026=VECTOR('',#126528,1000.);
#34027=VECTOR('',#126565,1000.);
#34028=VECTOR('',#126566,10.);
#34029=VECTOR('',#126569,1000.);
#34030=VECTOR('',#126574,10.);
#34031=VECTOR('',#126575,1000.);
#34032=VECTOR('',#126576,1000.);
#34033=VECTOR('',#126613,1000.);
#34034=VECTOR('',#126614,10.);
#34035=VECTOR('',#126617,1000.);
#34036=VECTOR('',#126622,10.);
#34037=VECTOR('',#126623,1000.);
#34038=VECTOR('',#126624,1000.);
#34039=VECTOR('',#126661,1000.);
#34040=VECTOR('',#126662,10.);
#34041=VECTOR('',#126665,1000.);
#34042=VECTOR('',#126670,10.);
#34043=VECTOR('',#126671,1000.);
#34044=VECTOR('',#126672,1000.);
#34045=VECTOR('',#126709,1000.);
#34046=VECTOR('',#126710,10.);
#34047=VECTOR('',#126713,1000.);
#34048=VECTOR('',#126718,10.);
#34049=VECTOR('',#126719,1000.);
#34050=VECTOR('',#126720,1000.);
#34051=VECTOR('',#126757,1000.);
#34052=VECTOR('',#126758,10.);
#34053=VECTOR('',#126761,1000.);
#34054=VECTOR('',#126766,10.);
#34055=VECTOR('',#126767,1000.);
#34056=VECTOR('',#126768,1000.);
#34057=VECTOR('',#126805,1000.);
#34058=VECTOR('',#126806,10.);
#34059=VECTOR('',#126809,1000.);
#34060=VECTOR('',#126814,10.);
#34061=VECTOR('',#126815,1000.);
#34062=VECTOR('',#126816,1000.);
#34063=VECTOR('',#126853,1000.);
#34064=VECTOR('',#126854,10.);
#34065=VECTOR('',#126857,1000.);
#34066=VECTOR('',#126862,10.);
#34067=VECTOR('',#126863,1000.);
#34068=VECTOR('',#126864,1000.);
#34069=VECTOR('',#126901,1000.);
#34070=VECTOR('',#126902,10.);
#34071=VECTOR('',#126905,1000.);
#34072=VECTOR('',#126910,10.);
#34073=VECTOR('',#126911,1000.);
#34074=VECTOR('',#126912,1000.);
#34075=VECTOR('',#126949,1000.);
#34076=VECTOR('',#126950,10.);
#34077=VECTOR('',#126953,1000.);
#34078=VECTOR('',#126958,10.);
#34079=VECTOR('',#126959,1000.);
#34080=VECTOR('',#126960,1000.);
#34081=VECTOR('',#126997,1000.);
#34082=VECTOR('',#126998,10.);
#34083=VECTOR('',#127001,1000.);
#34084=VECTOR('',#127006,10.);
#34085=VECTOR('',#127007,1000.);
#34086=VECTOR('',#127008,1000.);
#34087=VECTOR('',#127045,1000.);
#34088=VECTOR('',#127046,10.);
#34089=VECTOR('',#127049,1000.);
#34090=VECTOR('',#127054,10.);
#34091=VECTOR('',#127055,1000.);
#34092=VECTOR('',#127056,1000.);
#34093=VECTOR('',#127093,1000.);
#34094=VECTOR('',#127094,10.);
#34095=VECTOR('',#127097,1000.);
#34096=VECTOR('',#127102,10.);
#34097=VECTOR('',#127103,1000.);
#34098=VECTOR('',#127104,1000.);
#34099=VECTOR('',#127141,1000.);
#34100=VECTOR('',#127142,10.);
#34101=VECTOR('',#127145,1000.);
#34102=VECTOR('',#127150,10.);
#34103=VECTOR('',#127151,1000.);
#34104=VECTOR('',#127152,1000.);
#34105=VECTOR('',#127189,1000.);
#34106=VECTOR('',#127190,10.);
#34107=VECTOR('',#127193,1000.);
#34108=VECTOR('',#127198,10.);
#34109=VECTOR('',#127199,1000.);
#34110=VECTOR('',#127200,1000.);
#34111=VECTOR('',#127237,1000.);
#34112=VECTOR('',#127238,10.);
#34113=VECTOR('',#127241,1000.);
#34114=VECTOR('',#127246,10.);
#34115=VECTOR('',#127247,1000.);
#34116=VECTOR('',#127248,1000.);
#34117=VECTOR('',#127285,1000.);
#34118=VECTOR('',#127286,10.);
#34119=VECTOR('',#127289,1000.);
#34120=VECTOR('',#127294,10.);
#34121=VECTOR('',#127295,1000.);
#34122=VECTOR('',#127296,1000.);
#34123=VECTOR('',#127333,1000.);
#34124=VECTOR('',#127334,10.);
#34125=VECTOR('',#127337,1000.);
#34126=VECTOR('',#127342,10.);
#34127=VECTOR('',#127343,1000.);
#34128=VECTOR('',#127344,1000.);
#34129=VECTOR('',#127381,1000.);
#34130=VECTOR('',#127382,10.);
#34131=VECTOR('',#127385,1000.);
#34132=VECTOR('',#127390,10.);
#34133=VECTOR('',#127391,1000.);
#34134=VECTOR('',#127392,1000.);
#34135=VECTOR('',#127429,1000.);
#34136=VECTOR('',#127430,10.);
#34137=VECTOR('',#127433,1000.);
#34138=VECTOR('',#127438,10.);
#34139=VECTOR('',#127439,1000.);
#34140=VECTOR('',#127440,1000.);
#34141=VECTOR('',#127477,1000.);
#34142=VECTOR('',#127478,10.);
#34143=VECTOR('',#127481,1000.);
#34144=VECTOR('',#127486,10.);
#34145=VECTOR('',#127487,1000.);
#34146=VECTOR('',#127488,1000.);
#34147=VECTOR('',#127525,1000.);
#34148=VECTOR('',#127526,10.);
#34149=VECTOR('',#127529,1000.);
#34150=VECTOR('',#127534,10.);
#34151=VECTOR('',#127535,1000.);
#34152=VECTOR('',#127536,1000.);
#34153=VECTOR('',#127573,1000.);
#34154=VECTOR('',#127574,10.);
#34155=VECTOR('',#127577,1000.);
#34156=VECTOR('',#127582,10.);
#34157=VECTOR('',#127583,1000.);
#34158=VECTOR('',#127584,1000.);
#34159=VECTOR('',#127621,1000.);
#34160=VECTOR('',#127622,10.);
#34161=VECTOR('',#127625,1000.);
#34162=VECTOR('',#127630,10.);
#34163=VECTOR('',#127631,1000.);
#34164=VECTOR('',#127632,1000.);
#34165=VECTOR('',#127669,1000.);
#34166=VECTOR('',#127670,10.);
#34167=VECTOR('',#127673,1000.);
#34168=VECTOR('',#127678,10.);
#34169=VECTOR('',#127679,1000.);
#34170=VECTOR('',#127680,1000.);
#34171=VECTOR('',#127717,1000.);
#34172=VECTOR('',#127718,10.);
#34173=VECTOR('',#127721,1000.);
#34174=VECTOR('',#127726,10.);
#34175=VECTOR('',#127727,1000.);
#34176=VECTOR('',#127728,1000.);
#34177=VECTOR('',#127765,1000.);
#34178=VECTOR('',#127766,10.);
#34179=VECTOR('',#127769,1000.);
#34180=VECTOR('',#127774,10.);
#34181=VECTOR('',#127775,1000.);
#34182=VECTOR('',#127776,1000.);
#34183=VECTOR('',#127813,1000.);
#34184=VECTOR('',#127814,10.);
#34185=VECTOR('',#127817,1000.);
#34186=VECTOR('',#127822,10.);
#34187=VECTOR('',#127823,1000.);
#34188=VECTOR('',#127824,1000.);
#34189=VECTOR('',#127861,1000.);
#34190=VECTOR('',#127862,10.);
#34191=VECTOR('',#127865,1000.);
#34192=VECTOR('',#127870,10.);
#34193=VECTOR('',#127871,1000.);
#34194=VECTOR('',#127872,1000.);
#34195=VECTOR('',#127909,1000.);
#34196=VECTOR('',#127910,10.);
#34197=VECTOR('',#127913,1000.);
#34198=VECTOR('',#127918,10.);
#34199=VECTOR('',#127919,1000.);
#34200=VECTOR('',#127920,1000.);
#34201=VECTOR('',#127957,1000.);
#34202=VECTOR('',#127958,10.);
#34203=VECTOR('',#127961,1000.);
#34204=VECTOR('',#127966,10.);
#34205=VECTOR('',#127967,1000.);
#34206=VECTOR('',#127968,1000.);
#34207=VECTOR('',#128005,1000.);
#34208=VECTOR('',#128006,10.);
#34209=VECTOR('',#128009,1000.);
#34210=VECTOR('',#128014,10.);
#34211=VECTOR('',#128015,1000.);
#34212=VECTOR('',#128016,1000.);
#34213=VECTOR('',#128053,1000.);
#34214=VECTOR('',#128054,10.);
#34215=VECTOR('',#128057,1000.);
#34216=VECTOR('',#128062,10.);
#34217=VECTOR('',#128063,1000.);
#34218=VECTOR('',#128064,1000.);
#34219=VECTOR('',#128101,1000.);
#34220=VECTOR('',#128102,10.);
#34221=VECTOR('',#128105,1000.);
#34222=VECTOR('',#128110,10.);
#34223=VECTOR('',#128111,1000.);
#34224=VECTOR('',#128112,1000.);
#34225=VECTOR('',#128149,1000.);
#34226=VECTOR('',#128150,10.);
#34227=VECTOR('',#128153,1000.);
#34228=VECTOR('',#128158,10.);
#34229=VECTOR('',#128159,1000.);
#34230=VECTOR('',#128160,1000.);
#34231=VECTOR('',#128197,1000.);
#34232=VECTOR('',#128198,10.);
#34233=VECTOR('',#128201,1000.);
#34234=VECTOR('',#128206,10.);
#34235=VECTOR('',#128207,1000.);
#34236=VECTOR('',#128208,1000.);
#34237=VECTOR('',#128245,1000.);
#34238=VECTOR('',#128246,10.);
#34239=VECTOR('',#128249,1000.);
#34240=VECTOR('',#128254,10.);
#34241=VECTOR('',#128255,1000.);
#34242=VECTOR('',#128256,1000.);
#34243=VECTOR('',#128293,1000.);
#34244=VECTOR('',#128294,10.);
#34245=VECTOR('',#128297,1000.);
#34246=VECTOR('',#128302,10.);
#34247=VECTOR('',#128303,1000.);
#34248=VECTOR('',#128304,1000.);
#34249=VECTOR('',#128341,1000.);
#34250=VECTOR('',#128342,10.);
#34251=VECTOR('',#128345,1000.);
#34252=VECTOR('',#128350,10.);
#34253=VECTOR('',#128351,1000.);
#34254=VECTOR('',#128352,1000.);
#34255=VECTOR('',#128389,1000.);
#34256=VECTOR('',#128390,10.);
#34257=VECTOR('',#128393,1000.);
#34258=VECTOR('',#128398,10.);
#34259=VECTOR('',#128399,1000.);
#34260=VECTOR('',#128400,1000.);
#34261=VECTOR('',#128437,1000.);
#34262=VECTOR('',#128438,10.);
#34263=VECTOR('',#128441,1000.);
#34264=VECTOR('',#128446,10.);
#34265=VECTOR('',#128447,1000.);
#34266=VECTOR('',#128448,1000.);
#34267=VECTOR('',#128485,1000.);
#34268=VECTOR('',#128486,10.);
#34269=VECTOR('',#128489,1000.);
#34270=VECTOR('',#128494,10.);
#34271=VECTOR('',#128495,1000.);
#34272=VECTOR('',#128496,1000.);
#34273=VECTOR('',#128533,1000.);
#34274=VECTOR('',#128534,10.);
#34275=VECTOR('',#128537,1000.);
#34276=VECTOR('',#128542,10.);
#34277=VECTOR('',#128543,1000.);
#34278=VECTOR('',#128544,1000.);
#34279=VECTOR('',#128581,1000.);
#34280=VECTOR('',#128582,10.);
#34281=VECTOR('',#128585,1000.);
#34282=VECTOR('',#128590,10.);
#34283=VECTOR('',#128591,1000.);
#34284=VECTOR('',#128592,1000.);
#34285=VECTOR('',#128629,1000.);
#34286=VECTOR('',#128630,10.);
#34287=VECTOR('',#128633,1000.);
#34288=VECTOR('',#128638,10.);
#34289=VECTOR('',#128639,1000.);
#34290=VECTOR('',#128640,1000.);
#34291=VECTOR('',#128677,1000.);
#34292=VECTOR('',#128678,10.);
#34293=VECTOR('',#128681,1000.);
#34294=VECTOR('',#128686,10.);
#34295=VECTOR('',#128687,1000.);
#34296=VECTOR('',#128688,1000.);
#34297=VECTOR('',#128725,1000.);
#34298=VECTOR('',#128726,10.);
#34299=VECTOR('',#128729,1000.);
#34300=VECTOR('',#128734,10.);
#34301=VECTOR('',#128735,1000.);
#34302=VECTOR('',#128736,1000.);
#34303=VECTOR('',#128773,1000.);
#34304=VECTOR('',#128774,10.);
#34305=VECTOR('',#128777,1000.);
#34306=VECTOR('',#128782,10.);
#34307=VECTOR('',#128783,1000.);
#34308=VECTOR('',#128784,1000.);
#34309=VECTOR('',#128821,1000.);
#34310=VECTOR('',#128822,10.);
#34311=VECTOR('',#128825,1000.);
#34312=VECTOR('',#128830,10.);
#34313=VECTOR('',#128831,1000.);
#34314=VECTOR('',#128832,1000.);
#34315=VECTOR('',#128869,1000.);
#34316=VECTOR('',#128870,10.);
#34317=VECTOR('',#128873,1000.);
#34318=VECTOR('',#128878,10.);
#34319=VECTOR('',#128879,1000.);
#34320=VECTOR('',#128880,1000.);
#34321=VECTOR('',#128917,1000.);
#34322=VECTOR('',#128918,10.);
#34323=VECTOR('',#128921,1000.);
#34324=VECTOR('',#128926,10.);
#34325=VECTOR('',#128927,1000.);
#34326=VECTOR('',#128928,1000.);
#34327=VECTOR('',#128965,1000.);
#34328=VECTOR('',#128966,10.);
#34329=VECTOR('',#128969,1000.);
#34330=VECTOR('',#128974,10.);
#34331=VECTOR('',#128975,1000.);
#34332=VECTOR('',#128976,1000.);
#34333=VECTOR('',#129013,1000.);
#34334=VECTOR('',#129014,10.);
#34335=VECTOR('',#129017,1000.);
#34336=VECTOR('',#129022,10.);
#34337=VECTOR('',#129023,1000.);
#34338=VECTOR('',#129024,1000.);
#34339=VECTOR('',#129061,1000.);
#34340=VECTOR('',#129062,10.);
#34341=VECTOR('',#129065,1000.);
#34342=VECTOR('',#129070,10.);
#34343=VECTOR('',#129071,1000.);
#34344=VECTOR('',#129072,1000.);
#34345=VECTOR('',#129109,1000.);
#34346=VECTOR('',#129110,10.);
#34347=VECTOR('',#129113,1000.);
#34348=VECTOR('',#129118,10.);
#34349=VECTOR('',#129119,1000.);
#34350=VECTOR('',#129120,1000.);
#34351=VECTOR('',#129157,1000.);
#34352=VECTOR('',#129158,10.);
#34353=VECTOR('',#129161,1000.);
#34354=VECTOR('',#129166,10.);
#34355=VECTOR('',#129167,1000.);
#34356=VECTOR('',#129168,1000.);
#34357=VECTOR('',#129205,1000.);
#34358=VECTOR('',#129206,10.);
#34359=VECTOR('',#129209,1000.);
#34360=VECTOR('',#129214,10.);
#34361=VECTOR('',#129215,1000.);
#34362=VECTOR('',#129216,1000.);
#34363=VECTOR('',#129253,1000.);
#34364=VECTOR('',#129254,10.);
#34365=VECTOR('',#129257,1000.);
#34366=VECTOR('',#129262,10.);
#34367=VECTOR('',#129263,1000.);
#34368=VECTOR('',#129264,1000.);
#34369=VECTOR('',#129301,1000.);
#34370=VECTOR('',#129302,10.);
#34371=VECTOR('',#129305,1000.);
#34372=VECTOR('',#129310,10.);
#34373=VECTOR('',#129311,1000.);
#34374=VECTOR('',#129312,1000.);
#34375=VECTOR('',#129349,1000.);
#34376=VECTOR('',#129350,10.);
#34377=VECTOR('',#129353,1000.);
#34378=VECTOR('',#129358,10.);
#34379=VECTOR('',#129359,1000.);
#34380=VECTOR('',#129360,1000.);
#34381=VECTOR('',#129397,1000.);
#34382=VECTOR('',#129398,10.);
#34383=VECTOR('',#129401,1000.);
#34384=VECTOR('',#129406,10.);
#34385=VECTOR('',#129407,1000.);
#34386=VECTOR('',#129408,1000.);
#34387=VECTOR('',#129445,1000.);
#34388=VECTOR('',#129446,10.);
#34389=VECTOR('',#129449,1000.);
#34390=VECTOR('',#129454,10.);
#34391=VECTOR('',#129455,1000.);
#34392=VECTOR('',#129456,1000.);
#34393=VECTOR('',#129493,1000.);
#34394=VECTOR('',#129494,10.);
#34395=VECTOR('',#129497,1000.);
#34396=VECTOR('',#129502,10.);
#34397=VECTOR('',#129503,1000.);
#34398=VECTOR('',#129504,1000.);
#34399=VECTOR('',#129541,1000.);
#34400=VECTOR('',#129542,10.);
#34401=VECTOR('',#129545,1000.);
#34402=VECTOR('',#129550,10.);
#34403=VECTOR('',#129551,1000.);
#34404=VECTOR('',#129552,1000.);
#34405=VECTOR('',#129589,1000.);
#34406=VECTOR('',#129590,10.);
#34407=VECTOR('',#129593,1000.);
#34408=VECTOR('',#129598,10.);
#34409=VECTOR('',#129599,1000.);
#34410=VECTOR('',#129600,1000.);
#34411=VECTOR('',#129637,1000.);
#34412=VECTOR('',#129638,10.);
#34413=VECTOR('',#129641,1000.);
#34414=VECTOR('',#129646,10.);
#34415=VECTOR('',#129647,1000.);
#34416=VECTOR('',#129648,1000.);
#40925=VERTEX_POINT('',#409624);
#40926=VERTEX_POINT('',#409625);
#40927=VERTEX_POINT('',#409627);
#40928=VERTEX_POINT('',#409633);
#40929=VERTEX_POINT('',#409634);
#40930=VERTEX_POINT('',#409663);
#40931=VERTEX_POINT('',#409664);
#40932=VERTEX_POINT('',#409693);
#40933=VERTEX_POINT('',#409694);
#40934=VERTEX_POINT('',#409723);
#40935=VERTEX_POINT('',#409724);
#40936=VERTEX_POINT('',#409753);
#40937=VERTEX_POINT('',#409754);
#40938=VERTEX_POINT('',#409783);
#40939=VERTEX_POINT('',#409784);
#40940=VERTEX_POINT('',#409813);
#40941=VERTEX_POINT('',#409814);
#40942=VERTEX_POINT('',#409843);
#40943=VERTEX_POINT('',#409844);
#40944=VERTEX_POINT('',#409873);
#40945=VERTEX_POINT('',#409874);
#40946=VERTEX_POINT('',#409903);
#40947=VERTEX_POINT('',#409904);
#40948=VERTEX_POINT('',#409933);
#40949=VERTEX_POINT('',#409934);
#40950=VERTEX_POINT('',#409963);
#40951=VERTEX_POINT('',#409964);
#40952=VERTEX_POINT('',#409993);
#40953=VERTEX_POINT('',#409994);
#40954=VERTEX_POINT('',#410023);
#40955=VERTEX_POINT('',#410024);
#40956=VERTEX_POINT('',#410053);
#40957=VERTEX_POINT('',#410054);
#40958=VERTEX_POINT('',#410083);
#40959=VERTEX_POINT('',#410084);
#40960=VERTEX_POINT('',#410113);
#40961=VERTEX_POINT('',#410114);
#40962=VERTEX_POINT('',#410143);
#40963=VERTEX_POINT('',#410144);
#40964=VERTEX_POINT('',#410173);
#40965=VERTEX_POINT('',#410174);
#40966=VERTEX_POINT('',#410203);
#40967=VERTEX_POINT('',#410204);
#40968=VERTEX_POINT('',#410233);
#40969=VERTEX_POINT('',#410234);
#40970=VERTEX_POINT('',#410263);
#40971=VERTEX_POINT('',#410264);
#40972=VERTEX_POINT('',#410293);
#40973=VERTEX_POINT('',#410294);
#40974=VERTEX_POINT('',#410323);
#40975=VERTEX_POINT('',#410324);
#40976=VERTEX_POINT('',#410353);
#40977=VERTEX_POINT('',#410354);
#40978=VERTEX_POINT('',#410383);
#40979=VERTEX_POINT('',#410384);
#40980=VERTEX_POINT('',#410413);
#40981=VERTEX_POINT('',#410414);
#40982=VERTEX_POINT('',#410443);
#40983=VERTEX_POINT('',#410444);
#40984=VERTEX_POINT('',#410473);
#40985=VERTEX_POINT('',#410474);
#40986=VERTEX_POINT('',#410503);
#40987=VERTEX_POINT('',#410504);
#40988=VERTEX_POINT('',#410533);
#40989=VERTEX_POINT('',#410534);
#40990=VERTEX_POINT('',#410563);
#40991=VERTEX_POINT('',#410564);
#40992=VERTEX_POINT('',#410593);
#40993=VERTEX_POINT('',#410594);
#40994=VERTEX_POINT('',#410623);
#40995=VERTEX_POINT('',#410624);
#40996=VERTEX_POINT('',#410653);
#40997=VERTEX_POINT('',#410654);
#40998=VERTEX_POINT('',#410683);
#40999=VERTEX_POINT('',#410684);
#41000=VERTEX_POINT('',#410686);
#41001=VERTEX_POINT('',#410701);
#41002=VERTEX_POINT('',#410714);
#41003=VERTEX_POINT('',#410715);
#41004=VERTEX_POINT('',#410739);
#41005=VERTEX_POINT('',#410740);
#41006=VERTEX_POINT('',#410742);
#41007=VERTEX_POINT('',#410761);
#41008=VERTEX_POINT('',#410780);
#41009=VERTEX_POINT('',#410781);
#41010=VERTEX_POINT('',#410856);
#41011=VERTEX_POINT('',#410857);
#41012=VERTEX_POINT('',#410934);
#41013=VERTEX_POINT('',#410935);
#41014=VERTEX_POINT('',#411012);
#41015=VERTEX_POINT('',#411013);
#41016=VERTEX_POINT('',#411088);
#41017=VERTEX_POINT('',#411089);
#41018=VERTEX_POINT('',#411164);
#41019=VERTEX_POINT('',#411165);
#41020=VERTEX_POINT('',#411240);
#41021=VERTEX_POINT('',#411241);
#41022=VERTEX_POINT('',#411318);
#41023=VERTEX_POINT('',#411319);
#41024=VERTEX_POINT('',#411394);
#41025=VERTEX_POINT('',#411395);
#41026=VERTEX_POINT('',#411470);
#41027=VERTEX_POINT('',#411471);
#41028=VERTEX_POINT('',#411548);
#41029=VERTEX_POINT('',#411549);
#41030=VERTEX_POINT('',#411624);
#41031=VERTEX_POINT('',#411625);
#41032=VERTEX_POINT('',#411700);
#41033=VERTEX_POINT('',#411701);
#41034=VERTEX_POINT('',#411776);
#41035=VERTEX_POINT('',#411777);
#41036=VERTEX_POINT('',#411854);
#41037=VERTEX_POINT('',#411855);
#41038=VERTEX_POINT('',#411930);
#41039=VERTEX_POINT('',#411931);
#41040=VERTEX_POINT('',#412006);
#41041=VERTEX_POINT('',#412007);
#41042=VERTEX_POINT('',#412084);
#41043=VERTEX_POINT('',#412085);
#41044=VERTEX_POINT('',#412160);
#41045=VERTEX_POINT('',#412161);
#41046=VERTEX_POINT('',#412236);
#41047=VERTEX_POINT('',#412237);
#41048=VERTEX_POINT('',#412314);
#41049=VERTEX_POINT('',#412315);
#41050=VERTEX_POINT('',#412390);
#41051=VERTEX_POINT('',#412391);
#41052=VERTEX_POINT('',#412466);
#41053=VERTEX_POINT('',#412467);
#41054=VERTEX_POINT('',#412544);
#41055=VERTEX_POINT('',#412545);
#41056=VERTEX_POINT('',#412620);
#41057=VERTEX_POINT('',#412621);
#41058=VERTEX_POINT('',#412696);
#41059=VERTEX_POINT('',#412697);
#41060=VERTEX_POINT('',#412772);
#41061=VERTEX_POINT('',#412773);
#41062=VERTEX_POINT('',#412850);
#41063=VERTEX_POINT('',#412851);
#41064=VERTEX_POINT('',#412926);
#41065=VERTEX_POINT('',#412927);
#41066=VERTEX_POINT('',#413002);
#41067=VERTEX_POINT('',#413003);
#41068=VERTEX_POINT('',#413080);
#41069=VERTEX_POINT('',#413081);
#41070=VERTEX_POINT('',#413119);
#41071=VERTEX_POINT('',#413161);
#41072=VERTEX_POINT('',#413162);
#41073=VERTEX_POINT('',#413237);
#41074=VERTEX_POINT('',#413238);
#41075=VERTEX_POINT('',#413315);
#41076=VERTEX_POINT('',#413318);
#41077=VERTEX_POINT('',#413320);
#41078=VERTEX_POINT('',#413353);
#41079=VERTEX_POINT('',#413392);
#41080=VERTEX_POINT('',#413393);
#41081=VERTEX_POINT('',#413395);
#41082=VERTEX_POINT('',#413397);
#41083=VERTEX_POINT('',#413401);
#41084=VERTEX_POINT('',#413402);
#41085=VERTEX_POINT('',#413404);
#41086=VERTEX_POINT('',#413406);
#41087=VERTEX_POINT('',#413410);
#41088=VERTEX_POINT('',#413411);
#41089=VERTEX_POINT('',#413413);
#41090=VERTEX_POINT('',#413415);
#41091=VERTEX_POINT('',#413419);
#41092=VERTEX_POINT('',#413420);
#41093=VERTEX_POINT('',#413422);
#41094=VERTEX_POINT('',#413424);
#41095=VERTEX_POINT('',#413428);
#41096=VERTEX_POINT('',#413429);
#41097=VERTEX_POINT('',#413431);
#41098=VERTEX_POINT('',#413433);
#41099=VERTEX_POINT('',#413437);
#41100=VERTEX_POINT('',#413438);
#41101=VERTEX_POINT('',#413440);
#41102=VERTEX_POINT('',#413442);
#41103=VERTEX_POINT('',#413446);
#41104=VERTEX_POINT('',#413447);
#41105=VERTEX_POINT('',#413449);
#41106=VERTEX_POINT('',#413451);
#41107=VERTEX_POINT('',#413455);
#41108=VERTEX_POINT('',#413456);
#41109=VERTEX_POINT('',#413458);
#41110=VERTEX_POINT('',#413460);
#41111=VERTEX_POINT('',#413464);
#41112=VERTEX_POINT('',#413465);
#41113=VERTEX_POINT('',#413467);
#41114=VERTEX_POINT('',#413469);
#41115=VERTEX_POINT('',#413473);
#41116=VERTEX_POINT('',#413474);
#41117=VERTEX_POINT('',#413476);
#41118=VERTEX_POINT('',#413478);
#41119=VERTEX_POINT('',#413482);
#41120=VERTEX_POINT('',#413483);
#41121=VERTEX_POINT('',#413485);
#41122=VERTEX_POINT('',#413487);
#41123=VERTEX_POINT('',#413491);
#41124=VERTEX_POINT('',#413492);
#41125=VERTEX_POINT('',#413494);
#41126=VERTEX_POINT('',#413496);
#41127=VERTEX_POINT('',#413500);
#41128=VERTEX_POINT('',#413501);
#41129=VERTEX_POINT('',#413503);
#41130=VERTEX_POINT('',#413505);
#41131=VERTEX_POINT('',#413509);
#41132=VERTEX_POINT('',#413510);
#41133=VERTEX_POINT('',#413512);
#41134=VERTEX_POINT('',#413514);
#41135=VERTEX_POINT('',#413518);
#41136=VERTEX_POINT('',#413519);
#41137=VERTEX_POINT('',#413521);
#41138=VERTEX_POINT('',#413523);
#41139=VERTEX_POINT('',#413527);
#41140=VERTEX_POINT('',#413528);
#41141=VERTEX_POINT('',#413530);
#41142=VERTEX_POINT('',#413532);
#41143=VERTEX_POINT('',#413536);
#41144=VERTEX_POINT('',#413537);
#41145=VERTEX_POINT('',#413539);
#41146=VERTEX_POINT('',#413541);
#41147=VERTEX_POINT('',#413545);
#41148=VERTEX_POINT('',#413546);
#41149=VERTEX_POINT('',#413548);
#41150=VERTEX_POINT('',#413550);
#41151=VERTEX_POINT('',#413554);
#41152=VERTEX_POINT('',#413555);
#41153=VERTEX_POINT('',#413557);
#41154=VERTEX_POINT('',#413559);
#41155=VERTEX_POINT('',#413563);
#41156=VERTEX_POINT('',#413564);
#41157=VERTEX_POINT('',#413566);
#41158=VERTEX_POINT('',#413568);
#41159=VERTEX_POINT('',#413572);
#41160=VERTEX_POINT('',#413573);
#41161=VERTEX_POINT('',#413575);
#41162=VERTEX_POINT('',#413577);
#41163=VERTEX_POINT('',#413581);
#41164=VERTEX_POINT('',#413582);
#41165=VERTEX_POINT('',#413584);
#41166=VERTEX_POINT('',#413586);
#41167=VERTEX_POINT('',#413590);
#41168=VERTEX_POINT('',#413591);
#41169=VERTEX_POINT('',#413593);
#41170=VERTEX_POINT('',#413595);
#41171=VERTEX_POINT('',#413599);
#41172=VERTEX_POINT('',#413600);
#41173=VERTEX_POINT('',#413602);
#41174=VERTEX_POINT('',#413604);
#41175=VERTEX_POINT('',#413608);
#41176=VERTEX_POINT('',#413609);
#41177=VERTEX_POINT('',#413611);
#41178=VERTEX_POINT('',#413613);
#41179=VERTEX_POINT('',#413617);
#41180=VERTEX_POINT('',#413618);
#41181=VERTEX_POINT('',#413620);
#41182=VERTEX_POINT('',#413622);
#41183=VERTEX_POINT('',#413626);
#41184=VERTEX_POINT('',#413627);
#41185=VERTEX_POINT('',#413629);
#41186=VERTEX_POINT('',#413631);
#41187=VERTEX_POINT('',#413635);
#41188=VERTEX_POINT('',#413636);
#41189=VERTEX_POINT('',#413638);
#41190=VERTEX_POINT('',#413640);
#41191=VERTEX_POINT('',#413644);
#41192=VERTEX_POINT('',#413645);
#41193=VERTEX_POINT('',#413647);
#41194=VERTEX_POINT('',#413649);
#41195=VERTEX_POINT('',#413653);
#41196=VERTEX_POINT('',#413654);
#41197=VERTEX_POINT('',#413656);
#41198=VERTEX_POINT('',#413658);
#41199=VERTEX_POINT('',#413662);
#41200=VERTEX_POINT('',#413663);
#41201=VERTEX_POINT('',#413665);
#41202=VERTEX_POINT('',#413667);
#41203=VERTEX_POINT('',#413671);
#41204=VERTEX_POINT('',#413672);
#41205=VERTEX_POINT('',#413674);
#41206=VERTEX_POINT('',#413676);
#41207=VERTEX_POINT('',#413680);
#41208=VERTEX_POINT('',#413681);
#41209=VERTEX_POINT('',#413683);
#41210=VERTEX_POINT('',#413685);
#41211=VERTEX_POINT('',#413689);
#41212=VERTEX_POINT('',#413690);
#41213=VERTEX_POINT('',#413692);
#41214=VERTEX_POINT('',#413694);
#41215=VERTEX_POINT('',#413698);
#41216=VERTEX_POINT('',#413699);
#41217=VERTEX_POINT('',#413701);
#41218=VERTEX_POINT('',#413703);
#41219=VERTEX_POINT('',#413707);
#41220=VERTEX_POINT('',#413708);
#41221=VERTEX_POINT('',#413710);
#41222=VERTEX_POINT('',#413712);
#41223=VERTEX_POINT('',#413716);
#41224=VERTEX_POINT('',#413717);
#41225=VERTEX_POINT('',#413719);
#41226=VERTEX_POINT('',#413721);
#41227=VERTEX_POINT('',#413725);
#41228=VERTEX_POINT('',#413726);
#41229=VERTEX_POINT('',#413728);
#41230=VERTEX_POINT('',#413730);
#41231=VERTEX_POINT('',#413734);
#41232=VERTEX_POINT('',#413735);
#41233=VERTEX_POINT('',#413737);
#41234=VERTEX_POINT('',#413739);
#41235=VERTEX_POINT('',#413743);
#41236=VERTEX_POINT('',#413744);
#41237=VERTEX_POINT('',#413746);
#41238=VERTEX_POINT('',#413748);
#41239=VERTEX_POINT('',#413752);
#41240=VERTEX_POINT('',#413753);
#41241=VERTEX_POINT('',#413755);
#41242=VERTEX_POINT('',#413757);
#41243=VERTEX_POINT('',#413761);
#41244=VERTEX_POINT('',#413762);
#41245=VERTEX_POINT('',#413764);
#41246=VERTEX_POINT('',#413766);
#41247=VERTEX_POINT('',#413770);
#41248=VERTEX_POINT('',#413771);
#41249=VERTEX_POINT('',#413773);
#41250=VERTEX_POINT('',#413775);
#41251=VERTEX_POINT('',#413779);
#41252=VERTEX_POINT('',#413780);
#41253=VERTEX_POINT('',#413782);
#41254=VERTEX_POINT('',#413784);
#41255=VERTEX_POINT('',#413788);
#41256=VERTEX_POINT('',#413789);
#41257=VERTEX_POINT('',#413791);
#41258=VERTEX_POINT('',#413793);
#41259=VERTEX_POINT('',#413797);
#41260=VERTEX_POINT('',#413798);
#41261=VERTEX_POINT('',#413800);
#41262=VERTEX_POINT('',#413802);
#41263=VERTEX_POINT('',#413806);
#41264=VERTEX_POINT('',#413807);
#41265=VERTEX_POINT('',#413809);
#41266=VERTEX_POINT('',#413811);
#41267=VERTEX_POINT('',#413815);
#41268=VERTEX_POINT('',#413816);
#41269=VERTEX_POINT('',#413818);
#41270=VERTEX_POINT('',#413820);
#41271=VERTEX_POINT('',#413824);
#41272=VERTEX_POINT('',#413825);
#41273=VERTEX_POINT('',#413827);
#41274=VERTEX_POINT('',#413829);
#41275=VERTEX_POINT('',#413833);
#41276=VERTEX_POINT('',#413834);
#41277=VERTEX_POINT('',#413836);
#41278=VERTEX_POINT('',#413838);
#41279=VERTEX_POINT('',#413842);
#41280=VERTEX_POINT('',#413843);
#41281=VERTEX_POINT('',#413845);
#41282=VERTEX_POINT('',#413847);
#41283=VERTEX_POINT('',#413851);
#41284=VERTEX_POINT('',#413852);
#41285=VERTEX_POINT('',#413854);
#41286=VERTEX_POINT('',#413856);
#41287=VERTEX_POINT('',#413860);
#41288=VERTEX_POINT('',#413861);
#41289=VERTEX_POINT('',#413863);
#41290=VERTEX_POINT('',#413865);
#41291=VERTEX_POINT('',#413869);
#41292=VERTEX_POINT('',#413870);
#41293=VERTEX_POINT('',#413872);
#41294=VERTEX_POINT('',#413874);
#41295=VERTEX_POINT('',#413878);
#41296=VERTEX_POINT('',#413879);
#41297=VERTEX_POINT('',#413881);
#41298=VERTEX_POINT('',#413883);
#41299=VERTEX_POINT('',#413887);
#41300=VERTEX_POINT('',#413888);
#41301=VERTEX_POINT('',#413890);
#41302=VERTEX_POINT('',#413892);
#41303=VERTEX_POINT('',#413896);
#41304=VERTEX_POINT('',#413897);
#41305=VERTEX_POINT('',#413899);
#41306=VERTEX_POINT('',#413901);
#41307=VERTEX_POINT('',#413905);
#41308=VERTEX_POINT('',#413906);
#41309=VERTEX_POINT('',#413908);
#41310=VERTEX_POINT('',#413910);
#41311=VERTEX_POINT('',#413914);
#41312=VERTEX_POINT('',#413915);
#41313=VERTEX_POINT('',#413917);
#41314=VERTEX_POINT('',#413919);
#41315=VERTEX_POINT('',#413923);
#41316=VERTEX_POINT('',#413924);
#41317=VERTEX_POINT('',#413926);
#41318=VERTEX_POINT('',#413928);
#41319=VERTEX_POINT('',#413932);
#41320=VERTEX_POINT('',#413933);
#41321=VERTEX_POINT('',#413935);
#41322=VERTEX_POINT('',#413937);
#41323=VERTEX_POINT('',#413941);
#41324=VERTEX_POINT('',#413942);
#41325=VERTEX_POINT('',#413944);
#41326=VERTEX_POINT('',#413946);
#41327=VERTEX_POINT('',#413950);
#41328=VERTEX_POINT('',#413951);
#41329=VERTEX_POINT('',#413953);
#41330=VERTEX_POINT('',#413955);
#41331=VERTEX_POINT('',#413959);
#41332=VERTEX_POINT('',#413960);
#41333=VERTEX_POINT('',#413962);
#41334=VERTEX_POINT('',#413964);
#41335=VERTEX_POINT('',#413968);
#41336=VERTEX_POINT('',#413969);
#41337=VERTEX_POINT('',#413971);
#41338=VERTEX_POINT('',#413973);
#41339=VERTEX_POINT('',#413977);
#41340=VERTEX_POINT('',#413978);
#41341=VERTEX_POINT('',#413980);
#41342=VERTEX_POINT('',#413982);
#41343=VERTEX_POINT('',#413986);
#41344=VERTEX_POINT('',#413987);
#41345=VERTEX_POINT('',#413989);
#41346=VERTEX_POINT('',#413991);
#41347=VERTEX_POINT('',#413995);
#41348=VERTEX_POINT('',#413996);
#41349=VERTEX_POINT('',#413998);
#41350=VERTEX_POINT('',#414000);
#41351=VERTEX_POINT('',#414004);
#41352=VERTEX_POINT('',#414005);
#41353=VERTEX_POINT('',#414007);
#41354=VERTEX_POINT('',#414009);
#41355=VERTEX_POINT('',#414013);
#41356=VERTEX_POINT('',#414014);
#41357=VERTEX_POINT('',#414016);
#41358=VERTEX_POINT('',#414018);
#41359=VERTEX_POINT('',#414022);
#41360=VERTEX_POINT('',#414023);
#41361=VERTEX_POINT('',#414025);
#41362=VERTEX_POINT('',#414027);
#41363=VERTEX_POINT('',#414031);
#41364=VERTEX_POINT('',#414032);
#41365=VERTEX_POINT('',#414034);
#41366=VERTEX_POINT('',#414036);
#41367=VERTEX_POINT('',#414040);
#41368=VERTEX_POINT('',#414041);
#41369=VERTEX_POINT('',#414043);
#41370=VERTEX_POINT('',#414045);
#41371=VERTEX_POINT('',#414049);
#41372=VERTEX_POINT('',#414050);
#41373=VERTEX_POINT('',#414052);
#41374=VERTEX_POINT('',#414054);
#41375=VERTEX_POINT('',#414058);
#41376=VERTEX_POINT('',#414059);
#41377=VERTEX_POINT('',#414061);
#41378=VERTEX_POINT('',#414063);
#41379=VERTEX_POINT('',#414067);
#41380=VERTEX_POINT('',#414068);
#41381=VERTEX_POINT('',#414070);
#41382=VERTEX_POINT('',#414072);
#41383=VERTEX_POINT('',#414076);
#41384=VERTEX_POINT('',#414077);
#41385=VERTEX_POINT('',#414079);
#41386=VERTEX_POINT('',#414081);
#41387=VERTEX_POINT('',#414083);
#41388=VERTEX_POINT('',#414196);
#41389=VERTEX_POINT('',#414233);
#41390=VERTEX_POINT('',#414234);
#41391=VERTEX_POINT('',#414236);
#41392=VERTEX_POINT('',#414238);
#41393=VERTEX_POINT('',#414240);
#41394=VERTEX_POINT('',#414242);
#41395=VERTEX_POINT('',#414244);
#41396=VERTEX_POINT('',#414248);
#41397=VERTEX_POINT('',#414249);
#41398=VERTEX_POINT('',#414255);
#41399=VERTEX_POINT('',#414257);
#41400=VERTEX_POINT('',#414261);
#41401=VERTEX_POINT('',#414265);
#41402=VERTEX_POINT('',#414269);
#41403=VERTEX_POINT('',#414270);
#41404=VERTEX_POINT('',#414287);
#41405=VERTEX_POINT('',#414289);
#41406=VERTEX_POINT('',#414291);
#41407=VERTEX_POINT('',#414293);
#41408=VERTEX_POINT('',#414319);
#41409=VERTEX_POINT('',#414321);
#41410=VERTEX_POINT('',#414323);
#41411=VERTEX_POINT('',#414325);
#41412=VERTEX_POINT('',#414351);
#41413=VERTEX_POINT('',#414353);
#41414=VERTEX_POINT('',#414355);
#41415=VERTEX_POINT('',#414357);
#41416=VERTEX_POINT('',#414383);
#41417=VERTEX_POINT('',#414385);
#41418=VERTEX_POINT('',#414387);
#41419=VERTEX_POINT('',#414389);
#41420=VERTEX_POINT('',#414415);
#41421=VERTEX_POINT('',#414417);
#41422=VERTEX_POINT('',#414419);
#41423=VERTEX_POINT('',#414421);
#41424=VERTEX_POINT('',#414447);
#41425=VERTEX_POINT('',#414449);
#41426=VERTEX_POINT('',#414451);
#41427=VERTEX_POINT('',#414453);
#41428=VERTEX_POINT('',#414479);
#41429=VERTEX_POINT('',#414481);
#41430=VERTEX_POINT('',#414483);
#41431=VERTEX_POINT('',#414485);
#41432=VERTEX_POINT('',#414511);
#41433=VERTEX_POINT('',#414513);
#41434=VERTEX_POINT('',#414515);
#41435=VERTEX_POINT('',#414517);
#41436=VERTEX_POINT('',#414543);
#41437=VERTEX_POINT('',#414545);
#41438=VERTEX_POINT('',#414547);
#41439=VERTEX_POINT('',#414549);
#41440=VERTEX_POINT('',#414575);
#41441=VERTEX_POINT('',#414577);
#41442=VERTEX_POINT('',#414579);
#41443=VERTEX_POINT('',#414581);
#41444=VERTEX_POINT('',#414607);
#41445=VERTEX_POINT('',#414609);
#41446=VERTEX_POINT('',#414611);
#41447=VERTEX_POINT('',#414613);
#41448=VERTEX_POINT('',#414639);
#41449=VERTEX_POINT('',#414641);
#41450=VERTEX_POINT('',#414643);
#41451=VERTEX_POINT('',#414645);
#41452=VERTEX_POINT('',#414671);
#41453=VERTEX_POINT('',#414673);
#41454=VERTEX_POINT('',#414675);
#41455=VERTEX_POINT('',#414677);
#41456=VERTEX_POINT('',#414703);
#41457=VERTEX_POINT('',#414705);
#41458=VERTEX_POINT('',#414707);
#41459=VERTEX_POINT('',#414709);
#41460=VERTEX_POINT('',#414735);
#41461=VERTEX_POINT('',#414737);
#41462=VERTEX_POINT('',#414739);
#41463=VERTEX_POINT('',#414741);
#41464=VERTEX_POINT('',#414767);
#41465=VERTEX_POINT('',#414769);
#41466=VERTEX_POINT('',#414771);
#41467=VERTEX_POINT('',#414773);
#41468=VERTEX_POINT('',#414799);
#41469=VERTEX_POINT('',#414801);
#41470=VERTEX_POINT('',#414803);
#41471=VERTEX_POINT('',#414805);
#41472=VERTEX_POINT('',#414831);
#41473=VERTEX_POINT('',#414833);
#41474=VERTEX_POINT('',#414835);
#41475=VERTEX_POINT('',#414837);
#41476=VERTEX_POINT('',#414863);
#41477=VERTEX_POINT('',#414865);
#41478=VERTEX_POINT('',#414867);
#41479=VERTEX_POINT('',#414869);
#41480=VERTEX_POINT('',#414895);
#41481=VERTEX_POINT('',#414897);
#41482=VERTEX_POINT('',#414899);
#41483=VERTEX_POINT('',#414901);
#41484=VERTEX_POINT('',#414927);
#41485=VERTEX_POINT('',#414929);
#41486=VERTEX_POINT('',#414931);
#41487=VERTEX_POINT('',#414933);
#41488=VERTEX_POINT('',#414959);
#41489=VERTEX_POINT('',#414961);
#41490=VERTEX_POINT('',#414963);
#41491=VERTEX_POINT('',#414965);
#41492=VERTEX_POINT('',#414991);
#41493=VERTEX_POINT('',#414993);
#41494=VERTEX_POINT('',#414995);
#41495=VERTEX_POINT('',#414997);
#41496=VERTEX_POINT('',#415023);
#41497=VERTEX_POINT('',#415025);
#41498=VERTEX_POINT('',#415027);
#41499=VERTEX_POINT('',#415029);
#41500=VERTEX_POINT('',#415055);
#41501=VERTEX_POINT('',#415057);
#41502=VERTEX_POINT('',#415059);
#41503=VERTEX_POINT('',#415061);
#41504=VERTEX_POINT('',#415087);
#41505=VERTEX_POINT('',#415089);
#41506=VERTEX_POINT('',#415091);
#41507=VERTEX_POINT('',#415093);
#41508=VERTEX_POINT('',#415119);
#41509=VERTEX_POINT('',#415121);
#41510=VERTEX_POINT('',#415123);
#41511=VERTEX_POINT('',#415125);
#41512=VERTEX_POINT('',#415151);
#41513=VERTEX_POINT('',#415153);
#41514=VERTEX_POINT('',#415155);
#41515=VERTEX_POINT('',#415157);
#41516=VERTEX_POINT('',#415183);
#41517=VERTEX_POINT('',#415185);
#41518=VERTEX_POINT('',#415187);
#41519=VERTEX_POINT('',#415189);
#41520=VERTEX_POINT('',#415215);
#41521=VERTEX_POINT('',#415217);
#41522=VERTEX_POINT('',#415219);
#41523=VERTEX_POINT('',#415221);
#41524=VERTEX_POINT('',#415247);
#41525=VERTEX_POINT('',#415249);
#41526=VERTEX_POINT('',#415251);
#41527=VERTEX_POINT('',#415253);
#41528=VERTEX_POINT('',#415279);
#41529=VERTEX_POINT('',#415281);
#41530=VERTEX_POINT('',#415283);
#41531=VERTEX_POINT('',#415285);
#41532=VERTEX_POINT('',#415311);
#41533=VERTEX_POINT('',#415313);
#41534=VERTEX_POINT('',#415315);
#41535=VERTEX_POINT('',#415317);
#41536=VERTEX_POINT('',#415343);
#41537=VERTEX_POINT('',#415345);
#41538=VERTEX_POINT('',#415347);
#41539=VERTEX_POINT('',#415349);
#41540=VERTEX_POINT('',#415375);
#41541=VERTEX_POINT('',#415377);
#41542=VERTEX_POINT('',#415379);
#41543=VERTEX_POINT('',#415381);
#41544=VERTEX_POINT('',#415407);
#41545=VERTEX_POINT('',#415409);
#41546=VERTEX_POINT('',#415411);
#41547=VERTEX_POINT('',#415413);
#41548=VERTEX_POINT('',#415439);
#41549=VERTEX_POINT('',#415441);
#41550=VERTEX_POINT('',#415443);
#41551=VERTEX_POINT('',#415445);
#41552=VERTEX_POINT('',#415471);
#41553=VERTEX_POINT('',#415473);
#41554=VERTEX_POINT('',#415475);
#41555=VERTEX_POINT('',#415477);
#41556=VERTEX_POINT('',#415503);
#41557=VERTEX_POINT('',#415505);
#41558=VERTEX_POINT('',#415507);
#41559=VERTEX_POINT('',#415509);
#41560=VERTEX_POINT('',#415512);
#41561=VERTEX_POINT('',#415514);
#41562=VERTEX_POINT('',#415516);
#41563=VERTEX_POINT('',#415542);
#41564=VERTEX_POINT('',#415544);
#41565=VERTEX_POINT('',#415546);
#41566=VERTEX_POINT('',#415548);
#41567=VERTEX_POINT('',#415574);
#41568=VERTEX_POINT('',#415576);
#41569=VERTEX_POINT('',#415578);
#41570=VERTEX_POINT('',#415580);
#41571=VERTEX_POINT('',#415606);
#41572=VERTEX_POINT('',#415608);
#41573=VERTEX_POINT('',#415610);
#41574=VERTEX_POINT('',#415612);
#41575=VERTEX_POINT('',#415638);
#41576=VERTEX_POINT('',#415640);
#41577=VERTEX_POINT('',#415642);
#41578=VERTEX_POINT('',#415644);
#41579=VERTEX_POINT('',#415670);
#41580=VERTEX_POINT('',#415672);
#41581=VERTEX_POINT('',#415674);
#41582=VERTEX_POINT('',#415676);
#41583=VERTEX_POINT('',#415702);
#41584=VERTEX_POINT('',#415704);
#41585=VERTEX_POINT('',#415706);
#41586=VERTEX_POINT('',#415708);
#41587=VERTEX_POINT('',#415734);
#41588=VERTEX_POINT('',#415736);
#41589=VERTEX_POINT('',#415738);
#41590=VERTEX_POINT('',#415740);
#41591=VERTEX_POINT('',#415766);
#41592=VERTEX_POINT('',#415768);
#41593=VERTEX_POINT('',#415770);
#41594=VERTEX_POINT('',#415772);
#41595=VERTEX_POINT('',#415798);
#41596=VERTEX_POINT('',#415800);
#41597=VERTEX_POINT('',#415802);
#41598=VERTEX_POINT('',#415804);
#41599=VERTEX_POINT('',#415830);
#41600=VERTEX_POINT('',#415832);
#41601=VERTEX_POINT('',#415834);
#41602=VERTEX_POINT('',#415836);
#41603=VERTEX_POINT('',#415862);
#41604=VERTEX_POINT('',#415864);
#41605=VERTEX_POINT('',#415866);
#41606=VERTEX_POINT('',#415868);
#41607=VERTEX_POINT('',#415894);
#41608=VERTEX_POINT('',#415896);
#41609=VERTEX_POINT('',#415898);
#41610=VERTEX_POINT('',#415900);
#41611=VERTEX_POINT('',#415926);
#41612=VERTEX_POINT('',#415928);
#41613=VERTEX_POINT('',#415930);
#41614=VERTEX_POINT('',#415932);
#41615=VERTEX_POINT('',#415958);
#41616=VERTEX_POINT('',#415960);
#41617=VERTEX_POINT('',#415962);
#41618=VERTEX_POINT('',#415964);
#41619=VERTEX_POINT('',#415990);
#41620=VERTEX_POINT('',#415992);
#41621=VERTEX_POINT('',#415994);
#41622=VERTEX_POINT('',#415996);
#41623=VERTEX_POINT('',#416022);
#41624=VERTEX_POINT('',#416024);
#41625=VERTEX_POINT('',#416026);
#41626=VERTEX_POINT('',#416028);
#41627=VERTEX_POINT('',#416054);
#41628=VERTEX_POINT('',#416056);
#41629=VERTEX_POINT('',#416058);
#41630=VERTEX_POINT('',#416060);
#41631=VERTEX_POINT('',#416086);
#41632=VERTEX_POINT('',#416088);
#41633=VERTEX_POINT('',#416090);
#41634=VERTEX_POINT('',#416092);
#41635=VERTEX_POINT('',#416118);
#41636=VERTEX_POINT('',#416120);
#41637=VERTEX_POINT('',#416122);
#41638=VERTEX_POINT('',#416124);
#41639=VERTEX_POINT('',#416150);
#41640=VERTEX_POINT('',#416152);
#41641=VERTEX_POINT('',#416154);
#41642=VERTEX_POINT('',#416156);
#41643=VERTEX_POINT('',#416182);
#41644=VERTEX_POINT('',#416184);
#41645=VERTEX_POINT('',#416186);
#41646=VERTEX_POINT('',#416188);
#41647=VERTEX_POINT('',#416214);
#41648=VERTEX_POINT('',#416216);
#41649=VERTEX_POINT('',#416218);
#41650=VERTEX_POINT('',#416220);
#41651=VERTEX_POINT('',#416246);
#41652=VERTEX_POINT('',#416248);
#41653=VERTEX_POINT('',#416250);
#41654=VERTEX_POINT('',#416252);
#41655=VERTEX_POINT('',#416278);
#41656=VERTEX_POINT('',#416280);
#41657=VERTEX_POINT('',#416282);
#41658=VERTEX_POINT('',#416284);
#41659=VERTEX_POINT('',#416310);
#41660=VERTEX_POINT('',#416312);
#41661=VERTEX_POINT('',#416314);
#41662=VERTEX_POINT('',#416316);
#41663=VERTEX_POINT('',#416342);
#41664=VERTEX_POINT('',#416344);
#41665=VERTEX_POINT('',#416346);
#41666=VERTEX_POINT('',#416348);
#41667=VERTEX_POINT('',#416374);
#41668=VERTEX_POINT('',#416376);
#41669=VERTEX_POINT('',#416378);
#41670=VERTEX_POINT('',#416380);
#41671=VERTEX_POINT('',#416406);
#41672=VERTEX_POINT('',#416408);
#41673=VERTEX_POINT('',#416410);
#41674=VERTEX_POINT('',#416412);
#41675=VERTEX_POINT('',#416438);
#41676=VERTEX_POINT('',#416440);
#41677=VERTEX_POINT('',#416442);
#41678=VERTEX_POINT('',#416444);
#41679=VERTEX_POINT('',#416470);
#41680=VERTEX_POINT('',#416472);
#41681=VERTEX_POINT('',#416474);
#41682=VERTEX_POINT('',#416476);
#41683=VERTEX_POINT('',#416502);
#41684=VERTEX_POINT('',#416504);
#41685=VERTEX_POINT('',#416506);
#41686=VERTEX_POINT('',#416508);
#41687=VERTEX_POINT('',#416534);
#41688=VERTEX_POINT('',#416536);
#41689=VERTEX_POINT('',#416538);
#41690=VERTEX_POINT('',#416540);
#41691=VERTEX_POINT('',#416566);
#41692=VERTEX_POINT('',#416568);
#41693=VERTEX_POINT('',#416570);
#41694=VERTEX_POINT('',#416572);
#41695=VERTEX_POINT('',#416598);
#41696=VERTEX_POINT('',#416600);
#41697=VERTEX_POINT('',#416602);
#41698=VERTEX_POINT('',#416604);
#41699=VERTEX_POINT('',#416630);
#41700=VERTEX_POINT('',#416632);
#41701=VERTEX_POINT('',#416634);
#41702=VERTEX_POINT('',#416636);
#41703=VERTEX_POINT('',#416662);
#41704=VERTEX_POINT('',#416664);
#41705=VERTEX_POINT('',#416666);
#41706=VERTEX_POINT('',#416668);
#41707=VERTEX_POINT('',#416694);
#41708=VERTEX_POINT('',#416696);
#41709=VERTEX_POINT('',#416698);
#41710=VERTEX_POINT('',#416700);
#41711=VERTEX_POINT('',#416726);
#41712=VERTEX_POINT('',#416728);
#41713=VERTEX_POINT('',#416730);
#41714=VERTEX_POINT('',#416746);
#41715=VERTEX_POINT('',#416750);
#41716=VERTEX_POINT('',#416751);
#41717=VERTEX_POINT('',#416753);
#41718=VERTEX_POINT('',#416771);
#41719=VERTEX_POINT('',#416788);
#41720=VERTEX_POINT('',#416790);
#41721=VERTEX_POINT('',#416792);
#41722=VERTEX_POINT('',#416810);
#41723=VERTEX_POINT('',#416827);
#41724=VERTEX_POINT('',#416829);
#41725=VERTEX_POINT('',#416831);
#41726=VERTEX_POINT('',#416849);
#41727=VERTEX_POINT('',#416866);
#41728=VERTEX_POINT('',#416868);
#41729=VERTEX_POINT('',#416870);
#41730=VERTEX_POINT('',#416888);
#41731=VERTEX_POINT('',#416905);
#41732=VERTEX_POINT('',#416907);
#41733=VERTEX_POINT('',#416909);
#41734=VERTEX_POINT('',#416927);
#41735=VERTEX_POINT('',#416944);
#41736=VERTEX_POINT('',#416946);
#41737=VERTEX_POINT('',#416948);
#41738=VERTEX_POINT('',#416966);
#41739=VERTEX_POINT('',#416983);
#41740=VERTEX_POINT('',#416985);
#41741=VERTEX_POINT('',#416987);
#41742=VERTEX_POINT('',#417005);
#41743=VERTEX_POINT('',#417022);
#41744=VERTEX_POINT('',#417024);
#41745=VERTEX_POINT('',#417026);
#41746=VERTEX_POINT('',#417044);
#41747=VERTEX_POINT('',#417061);
#41748=VERTEX_POINT('',#417063);
#41749=VERTEX_POINT('',#417065);
#41750=VERTEX_POINT('',#417083);
#41751=VERTEX_POINT('',#417100);
#41752=VERTEX_POINT('',#417102);
#41753=VERTEX_POINT('',#417104);
#41754=VERTEX_POINT('',#417122);
#41755=VERTEX_POINT('',#417139);
#41756=VERTEX_POINT('',#417141);
#41757=VERTEX_POINT('',#417143);
#41758=VERTEX_POINT('',#417161);
#41759=VERTEX_POINT('',#417178);
#41760=VERTEX_POINT('',#417180);
#41761=VERTEX_POINT('',#417182);
#41762=VERTEX_POINT('',#417200);
#41763=VERTEX_POINT('',#417217);
#41764=VERTEX_POINT('',#417219);
#41765=VERTEX_POINT('',#417221);
#41766=VERTEX_POINT('',#417239);
#41767=VERTEX_POINT('',#417256);
#41768=VERTEX_POINT('',#417258);
#41769=VERTEX_POINT('',#417260);
#41770=VERTEX_POINT('',#417278);
#41771=VERTEX_POINT('',#417295);
#41772=VERTEX_POINT('',#417297);
#41773=VERTEX_POINT('',#417299);
#41774=VERTEX_POINT('',#417317);
#41775=VERTEX_POINT('',#417334);
#41776=VERTEX_POINT('',#417336);
#41777=VERTEX_POINT('',#417338);
#41778=VERTEX_POINT('',#417356);
#41779=VERTEX_POINT('',#417373);
#41780=VERTEX_POINT('',#417375);
#41781=VERTEX_POINT('',#417377);
#41782=VERTEX_POINT('',#417395);
#41783=VERTEX_POINT('',#417412);
#41784=VERTEX_POINT('',#417414);
#41785=VERTEX_POINT('',#417416);
#41786=VERTEX_POINT('',#417434);
#41787=VERTEX_POINT('',#417451);
#41788=VERTEX_POINT('',#417453);
#41789=VERTEX_POINT('',#417455);
#41790=VERTEX_POINT('',#417473);
#41791=VERTEX_POINT('',#417490);
#41792=VERTEX_POINT('',#417492);
#41793=VERTEX_POINT('',#417494);
#41794=VERTEX_POINT('',#417512);
#41795=VERTEX_POINT('',#417529);
#41796=VERTEX_POINT('',#417531);
#41797=VERTEX_POINT('',#417533);
#41798=VERTEX_POINT('',#417551);
#41799=VERTEX_POINT('',#417568);
#41800=VERTEX_POINT('',#417570);
#41801=VERTEX_POINT('',#417572);
#41802=VERTEX_POINT('',#417590);
#41803=VERTEX_POINT('',#417607);
#41804=VERTEX_POINT('',#417609);
#41805=VERTEX_POINT('',#417611);
#41806=VERTEX_POINT('',#417629);
#41807=VERTEX_POINT('',#417646);
#41808=VERTEX_POINT('',#417648);
#41809=VERTEX_POINT('',#417650);
#41810=VERTEX_POINT('',#417668);
#41811=VERTEX_POINT('',#417685);
#41812=VERTEX_POINT('',#417687);
#41813=VERTEX_POINT('',#417689);
#41814=VERTEX_POINT('',#417707);
#41815=VERTEX_POINT('',#417724);
#41816=VERTEX_POINT('',#417726);
#41817=VERTEX_POINT('',#417728);
#41818=VERTEX_POINT('',#417746);
#41819=VERTEX_POINT('',#417763);
#41820=VERTEX_POINT('',#417765);
#41821=VERTEX_POINT('',#417767);
#41822=VERTEX_POINT('',#417785);
#41823=VERTEX_POINT('',#417802);
#41824=VERTEX_POINT('',#417804);
#41825=VERTEX_POINT('',#417806);
#41826=VERTEX_POINT('',#417824);
#41827=VERTEX_POINT('',#417841);
#41828=VERTEX_POINT('',#417843);
#41829=VERTEX_POINT('',#417845);
#41830=VERTEX_POINT('',#417863);
#41831=VERTEX_POINT('',#417880);
#41832=VERTEX_POINT('',#417882);
#41833=VERTEX_POINT('',#417884);
#41834=VERTEX_POINT('',#417902);
#41835=VERTEX_POINT('',#417919);
#41836=VERTEX_POINT('',#417921);
#41837=VERTEX_POINT('',#417923);
#41838=VERTEX_POINT('',#417941);
#41839=VERTEX_POINT('',#417958);
#41840=VERTEX_POINT('',#417960);
#41841=VERTEX_POINT('',#417962);
#41842=VERTEX_POINT('',#417980);
#41843=VERTEX_POINT('',#417997);
#41844=VERTEX_POINT('',#417999);
#41845=VERTEX_POINT('',#418001);
#41846=VERTEX_POINT('',#418019);
#41847=VERTEX_POINT('',#418036);
#41848=VERTEX_POINT('',#418038);
#41849=VERTEX_POINT('',#418040);
#41850=VERTEX_POINT('',#418058);
#41851=VERTEX_POINT('',#418075);
#41852=VERTEX_POINT('',#418077);
#41853=VERTEX_POINT('',#418079);
#41854=VERTEX_POINT('',#418097);
#41855=VERTEX_POINT('',#418114);
#41856=VERTEX_POINT('',#418116);
#41857=VERTEX_POINT('',#418118);
#41858=VERTEX_POINT('',#418136);
#41859=VERTEX_POINT('',#418153);
#41860=VERTEX_POINT('',#418155);
#41861=VERTEX_POINT('',#418157);
#41862=VERTEX_POINT('',#418175);
#41863=VERTEX_POINT('',#418192);
#41864=VERTEX_POINT('',#418194);
#41865=VERTEX_POINT('',#418196);
#41866=VERTEX_POINT('',#418214);
#41867=VERTEX_POINT('',#418231);
#41868=VERTEX_POINT('',#418233);
#41869=VERTEX_POINT('',#418235);
#41870=VERTEX_POINT('',#418254);
#41871=VERTEX_POINT('',#418271);
#41872=VERTEX_POINT('',#418273);
#41873=VERTEX_POINT('',#418275);
#41874=VERTEX_POINT('',#418293);
#41875=VERTEX_POINT('',#418310);
#41876=VERTEX_POINT('',#418312);
#41877=VERTEX_POINT('',#418314);
#41878=VERTEX_POINT('',#418332);
#41879=VERTEX_POINT('',#418349);
#41880=VERTEX_POINT('',#418351);
#41881=VERTEX_POINT('',#418353);
#41882=VERTEX_POINT('',#418371);
#41883=VERTEX_POINT('',#418388);
#41884=VERTEX_POINT('',#418390);
#41885=VERTEX_POINT('',#418392);
#41886=VERTEX_POINT('',#418410);
#41887=VERTEX_POINT('',#418427);
#41888=VERTEX_POINT('',#418429);
#41889=VERTEX_POINT('',#418431);
#41890=VERTEX_POINT('',#418449);
#41891=VERTEX_POINT('',#418466);
#41892=VERTEX_POINT('',#418468);
#41893=VERTEX_POINT('',#418470);
#41894=VERTEX_POINT('',#418488);
#41895=VERTEX_POINT('',#418505);
#41896=VERTEX_POINT('',#418507);
#41897=VERTEX_POINT('',#418509);
#41898=VERTEX_POINT('',#418527);
#41899=VERTEX_POINT('',#418544);
#41900=VERTEX_POINT('',#418546);
#41901=VERTEX_POINT('',#418548);
#41902=VERTEX_POINT('',#418566);
#41903=VERTEX_POINT('',#418583);
#41904=VERTEX_POINT('',#418585);
#41905=VERTEX_POINT('',#418587);
#41906=VERTEX_POINT('',#418605);
#41907=VERTEX_POINT('',#418622);
#41908=VERTEX_POINT('',#418624);
#41909=VERTEX_POINT('',#418626);
#41910=VERTEX_POINT('',#418644);
#41911=VERTEX_POINT('',#418661);
#41912=VERTEX_POINT('',#418663);
#41913=VERTEX_POINT('',#418665);
#41914=VERTEX_POINT('',#418683);
#41915=VERTEX_POINT('',#418700);
#41916=VERTEX_POINT('',#418702);
#41917=VERTEX_POINT('',#418704);
#41918=VERTEX_POINT('',#418722);
#41919=VERTEX_POINT('',#418739);
#41920=VERTEX_POINT('',#418741);
#41921=VERTEX_POINT('',#418743);
#41922=VERTEX_POINT('',#418761);
#41923=VERTEX_POINT('',#418778);
#41924=VERTEX_POINT('',#418780);
#41925=VERTEX_POINT('',#418782);
#41926=VERTEX_POINT('',#418800);
#41927=VERTEX_POINT('',#418817);
#41928=VERTEX_POINT('',#418819);
#41929=VERTEX_POINT('',#418821);
#41930=VERTEX_POINT('',#418839);
#41931=VERTEX_POINT('',#418856);
#41932=VERTEX_POINT('',#418858);
#41933=VERTEX_POINT('',#418860);
#41934=VERTEX_POINT('',#418878);
#41935=VERTEX_POINT('',#418895);
#41936=VERTEX_POINT('',#418897);
#41937=VERTEX_POINT('',#418899);
#41938=VERTEX_POINT('',#418917);
#41939=VERTEX_POINT('',#418934);
#41940=VERTEX_POINT('',#418936);
#41941=VERTEX_POINT('',#418938);
#41942=VERTEX_POINT('',#418956);
#41943=VERTEX_POINT('',#418973);
#41944=VERTEX_POINT('',#418975);
#41945=VERTEX_POINT('',#418977);
#41946=VERTEX_POINT('',#418995);
#41947=VERTEX_POINT('',#419012);
#41948=VERTEX_POINT('',#419014);
#41949=VERTEX_POINT('',#419016);
#41950=VERTEX_POINT('',#419034);
#41951=VERTEX_POINT('',#419051);
#41952=VERTEX_POINT('',#419053);
#41953=VERTEX_POINT('',#419055);
#41954=VERTEX_POINT('',#419073);
#41955=VERTEX_POINT('',#419090);
#41956=VERTEX_POINT('',#419092);
#41957=VERTEX_POINT('',#419094);
#41958=VERTEX_POINT('',#419112);
#41959=VERTEX_POINT('',#419129);
#41960=VERTEX_POINT('',#419131);
#41961=VERTEX_POINT('',#419133);
#41962=VERTEX_POINT('',#419151);
#41963=VERTEX_POINT('',#419168);
#41964=VERTEX_POINT('',#419170);
#41965=VERTEX_POINT('',#419172);
#41966=VERTEX_POINT('',#419190);
#41967=VERTEX_POINT('',#419207);
#41968=VERTEX_POINT('',#419209);
#41969=VERTEX_POINT('',#419211);
#41970=VERTEX_POINT('',#419229);
#41971=VERTEX_POINT('',#419246);
#41972=VERTEX_POINT('',#419248);
#41973=VERTEX_POINT('',#419250);
#41974=VERTEX_POINT('',#419268);
#41975=VERTEX_POINT('',#419285);
#41976=VERTEX_POINT('',#419287);
#41977=VERTEX_POINT('',#419289);
#41978=VERTEX_POINT('',#419307);
#41979=VERTEX_POINT('',#419324);
#41980=VERTEX_POINT('',#419326);
#41981=VERTEX_POINT('',#419328);
#41982=VERTEX_POINT('',#419346);
#41983=VERTEX_POINT('',#419363);
#41984=VERTEX_POINT('',#419365);
#41985=VERTEX_POINT('',#419367);
#41986=VERTEX_POINT('',#419385);
#41987=VERTEX_POINT('',#419402);
#41988=VERTEX_POINT('',#419404);
#41989=VERTEX_POINT('',#419406);
#41990=VERTEX_POINT('',#419424);
#41991=VERTEX_POINT('',#419441);
#41992=VERTEX_POINT('',#419443);
#41993=VERTEX_POINT('',#419445);
#41994=VERTEX_POINT('',#419463);
#41995=VERTEX_POINT('',#419480);
#41996=VERTEX_POINT('',#419482);
#41997=VERTEX_POINT('',#419484);
#41998=VERTEX_POINT('',#419502);
#41999=VERTEX_POINT('',#419519);
#42000=VERTEX_POINT('',#419521);
#42001=VERTEX_POINT('',#419523);
#42002=VERTEX_POINT('',#419541);
#42003=VERTEX_POINT('',#419558);
#42004=VERTEX_POINT('',#419560);
#42005=VERTEX_POINT('',#419562);
#42006=VERTEX_POINT('',#419580);
#42007=VERTEX_POINT('',#419597);
#42008=VERTEX_POINT('',#419599);
#42009=VERTEX_POINT('',#419601);
#42010=VERTEX_POINT('',#419619);
#42011=VERTEX_POINT('',#419636);
#42012=VERTEX_POINT('',#419638);
#42013=VERTEX_POINT('',#419640);
#42014=VERTEX_POINT('',#419658);
#42015=VERTEX_POINT('',#419675);
#42016=VERTEX_POINT('',#419677);
#42017=VERTEX_POINT('',#419679);
#42018=VERTEX_POINT('',#419697);
#42019=VERTEX_POINT('',#419714);
#42020=VERTEX_POINT('',#419716);
#42021=VERTEX_POINT('',#419718);
#42022=VERTEX_POINT('',#419736);
#42023=VERTEX_POINT('',#419983);
#42024=VERTEX_POINT('',#419984);
#42025=VERTEX_POINT('',#419986);
#42026=VERTEX_POINT('',#420024);
#42027=VERTEX_POINT('',#420053);
#42028=VERTEX_POINT('',#420055);
#42029=VERTEX_POINT('',#420059);
#42030=VERTEX_POINT('',#420060);
#42031=VERTEX_POINT('',#420063);
#42032=VERTEX_POINT('',#420070);
#42033=VERTEX_POINT('',#420072);
#42034=VERTEX_POINT('',#420074);
#42035=VERTEX_POINT('',#420082);
#42036=VERTEX_POINT('',#420086);
#42037=VERTEX_POINT('',#420090);
#42038=VERTEX_POINT('',#420094);
#42039=VERTEX_POINT('',#420098);
#42040=VERTEX_POINT('',#420102);
#42041=VERTEX_POINT('',#420103);
#42042=VERTEX_POINT('',#420106);
#42043=VERTEX_POINT('',#420108);
#42044=VERTEX_POINT('',#420119);
#42045=VERTEX_POINT('',#422617);
#42046=VERTEX_POINT('',#422618);
#42047=VERTEX_POINT('',#422868);
#42048=VERTEX_POINT('',#422869);
#42049=VERTEX_POINT('',#422871);
#42050=VERTEX_POINT('',#422873);
#42051=VERTEX_POINT('',#422875);
#42052=VERTEX_POINT('',#422882);
#42053=VERTEX_POINT('',#422883);
#42054=VERTEX_POINT('',#422885);
#42055=VERTEX_POINT('',#422887);
#42056=VERTEX_POINT('',#422889);
#42057=VERTEX_POINT('',#422896);
#42058=VERTEX_POINT('',#422962);
#42059=VERTEX_POINT('',#423005);
#42060=VERTEX_POINT('',#423032);
#42061=VERTEX_POINT('',#423217);
#42062=VERTEX_POINT('',#423218);
#42063=VERTEX_POINT('',#423220);
#42064=VERTEX_POINT('',#423222);
#42065=VERTEX_POINT('',#423224);
#42066=VERTEX_POINT('',#423231);
#42067=VERTEX_POINT('',#423232);
#42068=VERTEX_POINT('',#423234);
#42069=VERTEX_POINT('',#423236);
#42070=VERTEX_POINT('',#423238);
#42071=VERTEX_POINT('',#423245);
#42072=VERTEX_POINT('',#423311);
#42073=VERTEX_POINT('',#423354);
#42074=VERTEX_POINT('',#423381);
#42075=VERTEX_POINT('',#423566);
#42076=VERTEX_POINT('',#423567);
#42077=VERTEX_POINT('',#423569);
#42078=VERTEX_POINT('',#423571);
#42079=VERTEX_POINT('',#423573);
#42080=VERTEX_POINT('',#423580);
#42081=VERTEX_POINT('',#423581);
#42082=VERTEX_POINT('',#423583);
#42083=VERTEX_POINT('',#423585);
#42084=VERTEX_POINT('',#423587);
#42085=VERTEX_POINT('',#423594);
#42086=VERTEX_POINT('',#423660);
#42087=VERTEX_POINT('',#423703);
#42088=VERTEX_POINT('',#423730);
#42089=VERTEX_POINT('',#423915);
#42090=VERTEX_POINT('',#423916);
#42091=VERTEX_POINT('',#423918);
#42092=VERTEX_POINT('',#423920);
#42093=VERTEX_POINT('',#423922);
#42094=VERTEX_POINT('',#423929);
#42095=VERTEX_POINT('',#423930);
#42096=VERTEX_POINT('',#423932);
#42097=VERTEX_POINT('',#423934);
#42098=VERTEX_POINT('',#423936);
#42099=VERTEX_POINT('',#423943);
#42100=VERTEX_POINT('',#424009);
#42101=VERTEX_POINT('',#424052);
#42102=VERTEX_POINT('',#424079);
#42103=VERTEX_POINT('',#424264);
#42104=VERTEX_POINT('',#424265);
#42105=VERTEX_POINT('',#424267);
#42106=VERTEX_POINT('',#424269);
#42107=VERTEX_POINT('',#424271);
#42108=VERTEX_POINT('',#424278);
#42109=VERTEX_POINT('',#424279);
#42110=VERTEX_POINT('',#424281);
#42111=VERTEX_POINT('',#424283);
#42112=VERTEX_POINT('',#424285);
#42113=VERTEX_POINT('',#424292);
#42114=VERTEX_POINT('',#424358);
#42115=VERTEX_POINT('',#424401);
#42116=VERTEX_POINT('',#424428);
#42117=VERTEX_POINT('',#424613);
#42118=VERTEX_POINT('',#424614);
#42119=VERTEX_POINT('',#424616);
#42120=VERTEX_POINT('',#424618);
#42121=VERTEX_POINT('',#424620);
#42122=VERTEX_POINT('',#424627);
#42123=VERTEX_POINT('',#424628);
#42124=VERTEX_POINT('',#424630);
#42125=VERTEX_POINT('',#424632);
#42126=VERTEX_POINT('',#424634);
#42127=VERTEX_POINT('',#424641);
#42128=VERTEX_POINT('',#424707);
#42129=VERTEX_POINT('',#424750);
#42130=VERTEX_POINT('',#424777);
#42131=VERTEX_POINT('',#424962);
#42132=VERTEX_POINT('',#424963);
#42133=VERTEX_POINT('',#424965);
#42134=VERTEX_POINT('',#424967);
#42135=VERTEX_POINT('',#424969);
#42136=VERTEX_POINT('',#424976);
#42137=VERTEX_POINT('',#424977);
#42138=VERTEX_POINT('',#424979);
#42139=VERTEX_POINT('',#424981);
#42140=VERTEX_POINT('',#424983);
#42141=VERTEX_POINT('',#424990);
#42142=VERTEX_POINT('',#425056);
#42143=VERTEX_POINT('',#425099);
#42144=VERTEX_POINT('',#425126);
#42145=VERTEX_POINT('',#425311);
#42146=VERTEX_POINT('',#425312);
#42147=VERTEX_POINT('',#425314);
#42148=VERTEX_POINT('',#425316);
#42149=VERTEX_POINT('',#425318);
#42150=VERTEX_POINT('',#425325);
#42151=VERTEX_POINT('',#425326);
#42152=VERTEX_POINT('',#425328);
#42153=VERTEX_POINT('',#425330);
#42154=VERTEX_POINT('',#425332);
#42155=VERTEX_POINT('',#425339);
#42156=VERTEX_POINT('',#425405);
#42157=VERTEX_POINT('',#425448);
#42158=VERTEX_POINT('',#425475);
#42159=VERTEX_POINT('',#425660);
#42160=VERTEX_POINT('',#425661);
#42161=VERTEX_POINT('',#425663);
#42162=VERTEX_POINT('',#425665);
#42163=VERTEX_POINT('',#425667);
#42164=VERTEX_POINT('',#425674);
#42165=VERTEX_POINT('',#425675);
#42166=VERTEX_POINT('',#425677);
#42167=VERTEX_POINT('',#425679);
#42168=VERTEX_POINT('',#425681);
#42169=VERTEX_POINT('',#425688);
#42170=VERTEX_POINT('',#425754);
#42171=VERTEX_POINT('',#425797);
#42172=VERTEX_POINT('',#425824);
#42173=VERTEX_POINT('',#426009);
#42174=VERTEX_POINT('',#426010);
#42175=VERTEX_POINT('',#426012);
#42176=VERTEX_POINT('',#426014);
#42177=VERTEX_POINT('',#426016);
#42178=VERTEX_POINT('',#426023);
#42179=VERTEX_POINT('',#426024);
#42180=VERTEX_POINT('',#426026);
#42181=VERTEX_POINT('',#426028);
#42182=VERTEX_POINT('',#426030);
#42183=VERTEX_POINT('',#426037);
#42184=VERTEX_POINT('',#426103);
#42185=VERTEX_POINT('',#426146);
#42186=VERTEX_POINT('',#426173);
#42187=VERTEX_POINT('',#426358);
#42188=VERTEX_POINT('',#426359);
#42189=VERTEX_POINT('',#426361);
#42190=VERTEX_POINT('',#426363);
#42191=VERTEX_POINT('',#426365);
#42192=VERTEX_POINT('',#426372);
#42193=VERTEX_POINT('',#426373);
#42194=VERTEX_POINT('',#426375);
#42195=VERTEX_POINT('',#426377);
#42196=VERTEX_POINT('',#426379);
#42197=VERTEX_POINT('',#426386);
#42198=VERTEX_POINT('',#426452);
#42199=VERTEX_POINT('',#426495);
#42200=VERTEX_POINT('',#426522);
#42201=VERTEX_POINT('',#426707);
#42202=VERTEX_POINT('',#426708);
#42203=VERTEX_POINT('',#426710);
#42204=VERTEX_POINT('',#426712);
#42205=VERTEX_POINT('',#426714);
#42206=VERTEX_POINT('',#426721);
#42207=VERTEX_POINT('',#426722);
#42208=VERTEX_POINT('',#426724);
#42209=VERTEX_POINT('',#426726);
#42210=VERTEX_POINT('',#426728);
#42211=VERTEX_POINT('',#426735);
#42212=VERTEX_POINT('',#426801);
#42213=VERTEX_POINT('',#426844);
#42214=VERTEX_POINT('',#426871);
#42215=VERTEX_POINT('',#427056);
#42216=VERTEX_POINT('',#427057);
#42217=VERTEX_POINT('',#427059);
#42218=VERTEX_POINT('',#427061);
#42219=VERTEX_POINT('',#427063);
#42220=VERTEX_POINT('',#427070);
#42221=VERTEX_POINT('',#427071);
#42222=VERTEX_POINT('',#427073);
#42223=VERTEX_POINT('',#427075);
#42224=VERTEX_POINT('',#427077);
#42225=VERTEX_POINT('',#427084);
#42226=VERTEX_POINT('',#427150);
#42227=VERTEX_POINT('',#427193);
#42228=VERTEX_POINT('',#427220);
#42229=VERTEX_POINT('',#427405);
#42230=VERTEX_POINT('',#427406);
#42231=VERTEX_POINT('',#427408);
#42232=VERTEX_POINT('',#427410);
#42233=VERTEX_POINT('',#427412);
#42234=VERTEX_POINT('',#427419);
#42235=VERTEX_POINT('',#427420);
#42236=VERTEX_POINT('',#427422);
#42237=VERTEX_POINT('',#427424);
#42238=VERTEX_POINT('',#427426);
#42239=VERTEX_POINT('',#427433);
#42240=VERTEX_POINT('',#427499);
#42241=VERTEX_POINT('',#427542);
#42242=VERTEX_POINT('',#427569);
#42243=VERTEX_POINT('',#427754);
#42244=VERTEX_POINT('',#427755);
#42245=VERTEX_POINT('',#427757);
#42246=VERTEX_POINT('',#427759);
#42247=VERTEX_POINT('',#427761);
#42248=VERTEX_POINT('',#427768);
#42249=VERTEX_POINT('',#427769);
#42250=VERTEX_POINT('',#427771);
#42251=VERTEX_POINT('',#427773);
#42252=VERTEX_POINT('',#427775);
#42253=VERTEX_POINT('',#427782);
#42254=VERTEX_POINT('',#427848);
#42255=VERTEX_POINT('',#427891);
#42256=VERTEX_POINT('',#427918);
#42257=VERTEX_POINT('',#428103);
#42258=VERTEX_POINT('',#428104);
#42259=VERTEX_POINT('',#428106);
#42260=VERTEX_POINT('',#428108);
#42261=VERTEX_POINT('',#428110);
#42262=VERTEX_POINT('',#428117);
#42263=VERTEX_POINT('',#428118);
#42264=VERTEX_POINT('',#428120);
#42265=VERTEX_POINT('',#428122);
#42266=VERTEX_POINT('',#428124);
#42267=VERTEX_POINT('',#428131);
#42268=VERTEX_POINT('',#428197);
#42269=VERTEX_POINT('',#428240);
#42270=VERTEX_POINT('',#428267);
#42271=VERTEX_POINT('',#428452);
#42272=VERTEX_POINT('',#428453);
#42273=VERTEX_POINT('',#428455);
#42274=VERTEX_POINT('',#428457);
#42275=VERTEX_POINT('',#428459);
#42276=VERTEX_POINT('',#428466);
#42277=VERTEX_POINT('',#428467);
#42278=VERTEX_POINT('',#428469);
#42279=VERTEX_POINT('',#428471);
#42280=VERTEX_POINT('',#428473);
#42281=VERTEX_POINT('',#428480);
#42282=VERTEX_POINT('',#428546);
#42283=VERTEX_POINT('',#428589);
#42284=VERTEX_POINT('',#428616);
#42285=VERTEX_POINT('',#428801);
#42286=VERTEX_POINT('',#428802);
#42287=VERTEX_POINT('',#428804);
#42288=VERTEX_POINT('',#428806);
#42289=VERTEX_POINT('',#428808);
#42290=VERTEX_POINT('',#428815);
#42291=VERTEX_POINT('',#428816);
#42292=VERTEX_POINT('',#428818);
#42293=VERTEX_POINT('',#428820);
#42294=VERTEX_POINT('',#428822);
#42295=VERTEX_POINT('',#428829);
#42296=VERTEX_POINT('',#428895);
#42297=VERTEX_POINT('',#428938);
#42298=VERTEX_POINT('',#428965);
#42299=VERTEX_POINT('',#429150);
#42300=VERTEX_POINT('',#429151);
#42301=VERTEX_POINT('',#429153);
#42302=VERTEX_POINT('',#429155);
#42303=VERTEX_POINT('',#429157);
#42304=VERTEX_POINT('',#429164);
#42305=VERTEX_POINT('',#429165);
#42306=VERTEX_POINT('',#429167);
#42307=VERTEX_POINT('',#429169);
#42308=VERTEX_POINT('',#429171);
#42309=VERTEX_POINT('',#429178);
#42310=VERTEX_POINT('',#429244);
#42311=VERTEX_POINT('',#429287);
#42312=VERTEX_POINT('',#429314);
#42313=VERTEX_POINT('',#429499);
#42314=VERTEX_POINT('',#429500);
#42315=VERTEX_POINT('',#429502);
#42316=VERTEX_POINT('',#429504);
#42317=VERTEX_POINT('',#429506);
#42318=VERTEX_POINT('',#429513);
#42319=VERTEX_POINT('',#429514);
#42320=VERTEX_POINT('',#429516);
#42321=VERTEX_POINT('',#429518);
#42322=VERTEX_POINT('',#429520);
#42323=VERTEX_POINT('',#429527);
#42324=VERTEX_POINT('',#429593);
#42325=VERTEX_POINT('',#429636);
#42326=VERTEX_POINT('',#429663);
#42327=VERTEX_POINT('',#429848);
#42328=VERTEX_POINT('',#429849);
#42329=VERTEX_POINT('',#429851);
#42330=VERTEX_POINT('',#429853);
#42331=VERTEX_POINT('',#429855);
#42332=VERTEX_POINT('',#429862);
#42333=VERTEX_POINT('',#429863);
#42334=VERTEX_POINT('',#429865);
#42335=VERTEX_POINT('',#429867);
#42336=VERTEX_POINT('',#429869);
#42337=VERTEX_POINT('',#429876);
#42338=VERTEX_POINT('',#429942);
#42339=VERTEX_POINT('',#429985);
#42340=VERTEX_POINT('',#430012);
#42341=VERTEX_POINT('',#430197);
#42342=VERTEX_POINT('',#430198);
#42343=VERTEX_POINT('',#430200);
#42344=VERTEX_POINT('',#430202);
#42345=VERTEX_POINT('',#430204);
#42346=VERTEX_POINT('',#430211);
#42347=VERTEX_POINT('',#430212);
#42348=VERTEX_POINT('',#430214);
#42349=VERTEX_POINT('',#430216);
#42350=VERTEX_POINT('',#430218);
#42351=VERTEX_POINT('',#430225);
#42352=VERTEX_POINT('',#430291);
#42353=VERTEX_POINT('',#430334);
#42354=VERTEX_POINT('',#430361);
#42355=VERTEX_POINT('',#430546);
#42356=VERTEX_POINT('',#430547);
#42357=VERTEX_POINT('',#430549);
#42358=VERTEX_POINT('',#430551);
#42359=VERTEX_POINT('',#430553);
#42360=VERTEX_POINT('',#430560);
#42361=VERTEX_POINT('',#430561);
#42362=VERTEX_POINT('',#430563);
#42363=VERTEX_POINT('',#430565);
#42364=VERTEX_POINT('',#430567);
#42365=VERTEX_POINT('',#430574);
#42366=VERTEX_POINT('',#430640);
#42367=VERTEX_POINT('',#430683);
#42368=VERTEX_POINT('',#430710);
#42369=VERTEX_POINT('',#430895);
#42370=VERTEX_POINT('',#430896);
#42371=VERTEX_POINT('',#430898);
#42372=VERTEX_POINT('',#430900);
#42373=VERTEX_POINT('',#430902);
#42374=VERTEX_POINT('',#430909);
#42375=VERTEX_POINT('',#430910);
#42376=VERTEX_POINT('',#430912);
#42377=VERTEX_POINT('',#430914);
#42378=VERTEX_POINT('',#430916);
#42379=VERTEX_POINT('',#430923);
#42380=VERTEX_POINT('',#430989);
#42381=VERTEX_POINT('',#431032);
#42382=VERTEX_POINT('',#431059);
#42383=VERTEX_POINT('',#431244);
#42384=VERTEX_POINT('',#431245);
#42385=VERTEX_POINT('',#431247);
#42386=VERTEX_POINT('',#431249);
#42387=VERTEX_POINT('',#431251);
#42388=VERTEX_POINT('',#431258);
#42389=VERTEX_POINT('',#431259);
#42390=VERTEX_POINT('',#431261);
#42391=VERTEX_POINT('',#431263);
#42392=VERTEX_POINT('',#431265);
#42393=VERTEX_POINT('',#431272);
#42394=VERTEX_POINT('',#431338);
#42395=VERTEX_POINT('',#431381);
#42396=VERTEX_POINT('',#431408);
#42397=VERTEX_POINT('',#431593);
#42398=VERTEX_POINT('',#431594);
#42399=VERTEX_POINT('',#431596);
#42400=VERTEX_POINT('',#431598);
#42401=VERTEX_POINT('',#431600);
#42402=VERTEX_POINT('',#431607);
#42403=VERTEX_POINT('',#431608);
#42404=VERTEX_POINT('',#431610);
#42405=VERTEX_POINT('',#431612);
#42406=VERTEX_POINT('',#431614);
#42407=VERTEX_POINT('',#431621);
#42408=VERTEX_POINT('',#431687);
#42409=VERTEX_POINT('',#431730);
#42410=VERTEX_POINT('',#431757);
#42411=VERTEX_POINT('',#431942);
#42412=VERTEX_POINT('',#431943);
#42413=VERTEX_POINT('',#431945);
#42414=VERTEX_POINT('',#431947);
#42415=VERTEX_POINT('',#431949);
#42416=VERTEX_POINT('',#431956);
#42417=VERTEX_POINT('',#431957);
#42418=VERTEX_POINT('',#431959);
#42419=VERTEX_POINT('',#431961);
#42420=VERTEX_POINT('',#431963);
#42421=VERTEX_POINT('',#431970);
#42422=VERTEX_POINT('',#432036);
#42423=VERTEX_POINT('',#432079);
#42424=VERTEX_POINT('',#432106);
#42425=VERTEX_POINT('',#432291);
#42426=VERTEX_POINT('',#432292);
#42427=VERTEX_POINT('',#432294);
#42428=VERTEX_POINT('',#432296);
#42429=VERTEX_POINT('',#432298);
#42430=VERTEX_POINT('',#432305);
#42431=VERTEX_POINT('',#432306);
#42432=VERTEX_POINT('',#432308);
#42433=VERTEX_POINT('',#432310);
#42434=VERTEX_POINT('',#432312);
#42435=VERTEX_POINT('',#432319);
#42436=VERTEX_POINT('',#432385);
#42437=VERTEX_POINT('',#432428);
#42438=VERTEX_POINT('',#432455);
#42439=VERTEX_POINT('',#432640);
#42440=VERTEX_POINT('',#432641);
#42441=VERTEX_POINT('',#432643);
#42442=VERTEX_POINT('',#432645);
#42443=VERTEX_POINT('',#432647);
#42444=VERTEX_POINT('',#432654);
#42445=VERTEX_POINT('',#432655);
#42446=VERTEX_POINT('',#432657);
#42447=VERTEX_POINT('',#432659);
#42448=VERTEX_POINT('',#432661);
#42449=VERTEX_POINT('',#432668);
#42450=VERTEX_POINT('',#432734);
#42451=VERTEX_POINT('',#432777);
#42452=VERTEX_POINT('',#432804);
#42453=VERTEX_POINT('',#432989);
#42454=VERTEX_POINT('',#432990);
#42455=VERTEX_POINT('',#432992);
#42456=VERTEX_POINT('',#432994);
#42457=VERTEX_POINT('',#432996);
#42458=VERTEX_POINT('',#433003);
#42459=VERTEX_POINT('',#433004);
#42460=VERTEX_POINT('',#433006);
#42461=VERTEX_POINT('',#433008);
#42462=VERTEX_POINT('',#433010);
#42463=VERTEX_POINT('',#433017);
#42464=VERTEX_POINT('',#433083);
#42465=VERTEX_POINT('',#433126);
#42466=VERTEX_POINT('',#433153);
#42467=VERTEX_POINT('',#433338);
#42468=VERTEX_POINT('',#433339);
#42469=VERTEX_POINT('',#433341);
#42470=VERTEX_POINT('',#433343);
#42471=VERTEX_POINT('',#433345);
#42472=VERTEX_POINT('',#433352);
#42473=VERTEX_POINT('',#433353);
#42474=VERTEX_POINT('',#433355);
#42475=VERTEX_POINT('',#433357);
#42476=VERTEX_POINT('',#433359);
#42477=VERTEX_POINT('',#433366);
#42478=VERTEX_POINT('',#433432);
#42479=VERTEX_POINT('',#433475);
#42480=VERTEX_POINT('',#433502);
#42481=VERTEX_POINT('',#433687);
#42482=VERTEX_POINT('',#433688);
#42483=VERTEX_POINT('',#433690);
#42484=VERTEX_POINT('',#433692);
#42485=VERTEX_POINT('',#433694);
#42486=VERTEX_POINT('',#433701);
#42487=VERTEX_POINT('',#433702);
#42488=VERTEX_POINT('',#433704);
#42489=VERTEX_POINT('',#433706);
#42490=VERTEX_POINT('',#433708);
#42491=VERTEX_POINT('',#433715);
#42492=VERTEX_POINT('',#433781);
#42493=VERTEX_POINT('',#433824);
#42494=VERTEX_POINT('',#433851);
#42495=VERTEX_POINT('',#434036);
#42496=VERTEX_POINT('',#434037);
#42497=VERTEX_POINT('',#434039);
#42498=VERTEX_POINT('',#434041);
#42499=VERTEX_POINT('',#434043);
#42500=VERTEX_POINT('',#434050);
#42501=VERTEX_POINT('',#434051);
#42502=VERTEX_POINT('',#434053);
#42503=VERTEX_POINT('',#434055);
#42504=VERTEX_POINT('',#434057);
#42505=VERTEX_POINT('',#434064);
#42506=VERTEX_POINT('',#434130);
#42507=VERTEX_POINT('',#434173);
#42508=VERTEX_POINT('',#434200);
#42509=VERTEX_POINT('',#434385);
#42510=VERTEX_POINT('',#434386);
#42511=VERTEX_POINT('',#434388);
#42512=VERTEX_POINT('',#434390);
#42513=VERTEX_POINT('',#434392);
#42514=VERTEX_POINT('',#434399);
#42515=VERTEX_POINT('',#434400);
#42516=VERTEX_POINT('',#434402);
#42517=VERTEX_POINT('',#434404);
#42518=VERTEX_POINT('',#434406);
#42519=VERTEX_POINT('',#434413);
#42520=VERTEX_POINT('',#434479);
#42521=VERTEX_POINT('',#434522);
#42522=VERTEX_POINT('',#434549);
#42523=VERTEX_POINT('',#434734);
#42524=VERTEX_POINT('',#434735);
#42525=VERTEX_POINT('',#434737);
#42526=VERTEX_POINT('',#434739);
#42527=VERTEX_POINT('',#434741);
#42528=VERTEX_POINT('',#434748);
#42529=VERTEX_POINT('',#434749);
#42530=VERTEX_POINT('',#434751);
#42531=VERTEX_POINT('',#434753);
#42532=VERTEX_POINT('',#434755);
#42533=VERTEX_POINT('',#434762);
#42534=VERTEX_POINT('',#434828);
#42535=VERTEX_POINT('',#434871);
#42536=VERTEX_POINT('',#434898);
#42537=VERTEX_POINT('',#435083);
#42538=VERTEX_POINT('',#435084);
#42539=VERTEX_POINT('',#435086);
#42540=VERTEX_POINT('',#435088);
#42541=VERTEX_POINT('',#435090);
#42542=VERTEX_POINT('',#435097);
#42543=VERTEX_POINT('',#435098);
#42544=VERTEX_POINT('',#435100);
#42545=VERTEX_POINT('',#435102);
#42546=VERTEX_POINT('',#435104);
#42547=VERTEX_POINT('',#435111);
#42548=VERTEX_POINT('',#435177);
#42549=VERTEX_POINT('',#435220);
#42550=VERTEX_POINT('',#435247);
#42551=VERTEX_POINT('',#435432);
#42552=VERTEX_POINT('',#435433);
#42553=VERTEX_POINT('',#435435);
#42554=VERTEX_POINT('',#435437);
#42555=VERTEX_POINT('',#435439);
#42556=VERTEX_POINT('',#435446);
#42557=VERTEX_POINT('',#435447);
#42558=VERTEX_POINT('',#435449);
#42559=VERTEX_POINT('',#435451);
#42560=VERTEX_POINT('',#435453);
#42561=VERTEX_POINT('',#435460);
#42562=VERTEX_POINT('',#435526);
#42563=VERTEX_POINT('',#435569);
#42564=VERTEX_POINT('',#435596);
#42565=VERTEX_POINT('',#435781);
#42566=VERTEX_POINT('',#435782);
#42567=VERTEX_POINT('',#435784);
#42568=VERTEX_POINT('',#435786);
#42569=VERTEX_POINT('',#435788);
#42570=VERTEX_POINT('',#435795);
#42571=VERTEX_POINT('',#435796);
#42572=VERTEX_POINT('',#435798);
#42573=VERTEX_POINT('',#435800);
#42574=VERTEX_POINT('',#435802);
#42575=VERTEX_POINT('',#435809);
#42576=VERTEX_POINT('',#435875);
#42577=VERTEX_POINT('',#435918);
#42578=VERTEX_POINT('',#435945);
#42579=VERTEX_POINT('',#436130);
#42580=VERTEX_POINT('',#436131);
#42581=VERTEX_POINT('',#436133);
#42582=VERTEX_POINT('',#436135);
#42583=VERTEX_POINT('',#436137);
#42584=VERTEX_POINT('',#436144);
#42585=VERTEX_POINT('',#436145);
#42586=VERTEX_POINT('',#436147);
#42587=VERTEX_POINT('',#436149);
#42588=VERTEX_POINT('',#436151);
#42589=VERTEX_POINT('',#436158);
#42590=VERTEX_POINT('',#436224);
#42591=VERTEX_POINT('',#436267);
#42592=VERTEX_POINT('',#436294);
#42593=VERTEX_POINT('',#436479);
#42594=VERTEX_POINT('',#436480);
#42595=VERTEX_POINT('',#436482);
#42596=VERTEX_POINT('',#436484);
#42597=VERTEX_POINT('',#436486);
#42598=VERTEX_POINT('',#436493);
#42599=VERTEX_POINT('',#436494);
#42600=VERTEX_POINT('',#436496);
#42601=VERTEX_POINT('',#436498);
#42602=VERTEX_POINT('',#436500);
#42603=VERTEX_POINT('',#436507);
#42604=VERTEX_POINT('',#436573);
#42605=VERTEX_POINT('',#436616);
#42606=VERTEX_POINT('',#436643);
#42607=VERTEX_POINT('',#436828);
#42608=VERTEX_POINT('',#436829);
#42609=VERTEX_POINT('',#436831);
#42610=VERTEX_POINT('',#436833);
#42611=VERTEX_POINT('',#436835);
#42612=VERTEX_POINT('',#436842);
#42613=VERTEX_POINT('',#436843);
#42614=VERTEX_POINT('',#436845);
#42615=VERTEX_POINT('',#436847);
#42616=VERTEX_POINT('',#436849);
#42617=VERTEX_POINT('',#436856);
#42618=VERTEX_POINT('',#436922);
#42619=VERTEX_POINT('',#436965);
#42620=VERTEX_POINT('',#436992);
#42621=VERTEX_POINT('',#437177);
#42622=VERTEX_POINT('',#437178);
#42623=VERTEX_POINT('',#437180);
#42624=VERTEX_POINT('',#437182);
#42625=VERTEX_POINT('',#437184);
#42626=VERTEX_POINT('',#437191);
#42627=VERTEX_POINT('',#437192);
#42628=VERTEX_POINT('',#437194);
#42629=VERTEX_POINT('',#437196);
#42630=VERTEX_POINT('',#437198);
#42631=VERTEX_POINT('',#437205);
#42632=VERTEX_POINT('',#437271);
#42633=VERTEX_POINT('',#437314);
#42634=VERTEX_POINT('',#437341);
#42635=VERTEX_POINT('',#437526);
#42636=VERTEX_POINT('',#437527);
#42637=VERTEX_POINT('',#437529);
#42638=VERTEX_POINT('',#437531);
#42639=VERTEX_POINT('',#437533);
#42640=VERTEX_POINT('',#437540);
#42641=VERTEX_POINT('',#437541);
#42642=VERTEX_POINT('',#437543);
#42643=VERTEX_POINT('',#437545);
#42644=VERTEX_POINT('',#437547);
#42645=VERTEX_POINT('',#437554);
#42646=VERTEX_POINT('',#437620);
#42647=VERTEX_POINT('',#437663);
#42648=VERTEX_POINT('',#437690);
#42649=VERTEX_POINT('',#437875);
#42650=VERTEX_POINT('',#437876);
#42651=VERTEX_POINT('',#437878);
#42652=VERTEX_POINT('',#437880);
#42653=VERTEX_POINT('',#437882);
#42654=VERTEX_POINT('',#437889);
#42655=VERTEX_POINT('',#437890);
#42656=VERTEX_POINT('',#437892);
#42657=VERTEX_POINT('',#437894);
#42658=VERTEX_POINT('',#437896);
#42659=VERTEX_POINT('',#437903);
#42660=VERTEX_POINT('',#437969);
#42661=VERTEX_POINT('',#438012);
#42662=VERTEX_POINT('',#438039);
#42663=VERTEX_POINT('',#438224);
#42664=VERTEX_POINT('',#438225);
#42665=VERTEX_POINT('',#438227);
#42666=VERTEX_POINT('',#438229);
#42667=VERTEX_POINT('',#438231);
#42668=VERTEX_POINT('',#438238);
#42669=VERTEX_POINT('',#438239);
#42670=VERTEX_POINT('',#438241);
#42671=VERTEX_POINT('',#438243);
#42672=VERTEX_POINT('',#438245);
#42673=VERTEX_POINT('',#438252);
#42674=VERTEX_POINT('',#438318);
#42675=VERTEX_POINT('',#438361);
#42676=VERTEX_POINT('',#438388);
#42677=VERTEX_POINT('',#438573);
#42678=VERTEX_POINT('',#438574);
#42679=VERTEX_POINT('',#438576);
#42680=VERTEX_POINT('',#438578);
#42681=VERTEX_POINT('',#438580);
#42682=VERTEX_POINT('',#438587);
#42683=VERTEX_POINT('',#438588);
#42684=VERTEX_POINT('',#438590);
#42685=VERTEX_POINT('',#438592);
#42686=VERTEX_POINT('',#438594);
#42687=VERTEX_POINT('',#438601);
#42688=VERTEX_POINT('',#438667);
#42689=VERTEX_POINT('',#438710);
#42690=VERTEX_POINT('',#438737);
#42691=VERTEX_POINT('',#438922);
#42692=VERTEX_POINT('',#438923);
#42693=VERTEX_POINT('',#438925);
#42694=VERTEX_POINT('',#438927);
#42695=VERTEX_POINT('',#438929);
#42696=VERTEX_POINT('',#438936);
#42697=VERTEX_POINT('',#438937);
#42698=VERTEX_POINT('',#438939);
#42699=VERTEX_POINT('',#438941);
#42700=VERTEX_POINT('',#438943);
#42701=VERTEX_POINT('',#438950);
#42702=VERTEX_POINT('',#439016);
#42703=VERTEX_POINT('',#439059);
#42704=VERTEX_POINT('',#439086);
#42705=VERTEX_POINT('',#439271);
#42706=VERTEX_POINT('',#439272);
#42707=VERTEX_POINT('',#439274);
#42708=VERTEX_POINT('',#439276);
#42709=VERTEX_POINT('',#439278);
#42710=VERTEX_POINT('',#439285);
#42711=VERTEX_POINT('',#439286);
#42712=VERTEX_POINT('',#439288);
#42713=VERTEX_POINT('',#439290);
#42714=VERTEX_POINT('',#439292);
#42715=VERTEX_POINT('',#439299);
#42716=VERTEX_POINT('',#439365);
#42717=VERTEX_POINT('',#439408);
#42718=VERTEX_POINT('',#439435);
#42719=VERTEX_POINT('',#439620);
#42720=VERTEX_POINT('',#439621);
#42721=VERTEX_POINT('',#439623);
#42722=VERTEX_POINT('',#439625);
#42723=VERTEX_POINT('',#439627);
#42724=VERTEX_POINT('',#439634);
#42725=VERTEX_POINT('',#439635);
#42726=VERTEX_POINT('',#439637);
#42727=VERTEX_POINT('',#439639);
#42728=VERTEX_POINT('',#439641);
#42729=VERTEX_POINT('',#439648);
#42730=VERTEX_POINT('',#439714);
#42731=VERTEX_POINT('',#439757);
#42732=VERTEX_POINT('',#439784);
#42733=VERTEX_POINT('',#439969);
#42734=VERTEX_POINT('',#439970);
#42735=VERTEX_POINT('',#439972);
#42736=VERTEX_POINT('',#439974);
#42737=VERTEX_POINT('',#439976);
#42738=VERTEX_POINT('',#439983);
#42739=VERTEX_POINT('',#439984);
#42740=VERTEX_POINT('',#439986);
#42741=VERTEX_POINT('',#439988);
#42742=VERTEX_POINT('',#439990);
#42743=VERTEX_POINT('',#439997);
#42744=VERTEX_POINT('',#440063);
#42745=VERTEX_POINT('',#440106);
#42746=VERTEX_POINT('',#440133);
#42747=VERTEX_POINT('',#440318);
#42748=VERTEX_POINT('',#440319);
#42749=VERTEX_POINT('',#440321);
#42750=VERTEX_POINT('',#440323);
#42751=VERTEX_POINT('',#440325);
#42752=VERTEX_POINT('',#440332);
#42753=VERTEX_POINT('',#440333);
#42754=VERTEX_POINT('',#440335);
#42755=VERTEX_POINT('',#440337);
#42756=VERTEX_POINT('',#440339);
#42757=VERTEX_POINT('',#440346);
#42758=VERTEX_POINT('',#440412);
#42759=VERTEX_POINT('',#440455);
#42760=VERTEX_POINT('',#440482);
#42761=VERTEX_POINT('',#440667);
#42762=VERTEX_POINT('',#440668);
#42763=VERTEX_POINT('',#440670);
#42764=VERTEX_POINT('',#440672);
#42765=VERTEX_POINT('',#440674);
#42766=VERTEX_POINT('',#440681);
#42767=VERTEX_POINT('',#440682);
#42768=VERTEX_POINT('',#440684);
#42769=VERTEX_POINT('',#440686);
#42770=VERTEX_POINT('',#440688);
#42771=VERTEX_POINT('',#440695);
#42772=VERTEX_POINT('',#440761);
#42773=VERTEX_POINT('',#440804);
#42774=VERTEX_POINT('',#440831);
#42775=VERTEX_POINT('',#441016);
#42776=VERTEX_POINT('',#441017);
#42777=VERTEX_POINT('',#441019);
#42778=VERTEX_POINT('',#441021);
#42779=VERTEX_POINT('',#441023);
#42780=VERTEX_POINT('',#441030);
#42781=VERTEX_POINT('',#441031);
#42782=VERTEX_POINT('',#441033);
#42783=VERTEX_POINT('',#441035);
#42784=VERTEX_POINT('',#441037);
#42785=VERTEX_POINT('',#441044);
#42786=VERTEX_POINT('',#441110);
#42787=VERTEX_POINT('',#441153);
#42788=VERTEX_POINT('',#441180);
#42789=VERTEX_POINT('',#441365);
#42790=VERTEX_POINT('',#441366);
#42791=VERTEX_POINT('',#441368);
#42792=VERTEX_POINT('',#441370);
#42793=VERTEX_POINT('',#441372);
#42794=VERTEX_POINT('',#441379);
#42795=VERTEX_POINT('',#441380);
#42796=VERTEX_POINT('',#441382);
#42797=VERTEX_POINT('',#441384);
#42798=VERTEX_POINT('',#441386);
#42799=VERTEX_POINT('',#441393);
#42800=VERTEX_POINT('',#441459);
#42801=VERTEX_POINT('',#441502);
#42802=VERTEX_POINT('',#441529);
#42803=VERTEX_POINT('',#441714);
#42804=VERTEX_POINT('',#441715);
#42805=VERTEX_POINT('',#441717);
#42806=VERTEX_POINT('',#441719);
#42807=VERTEX_POINT('',#441721);
#42808=VERTEX_POINT('',#441728);
#42809=VERTEX_POINT('',#441729);
#42810=VERTEX_POINT('',#441731);
#42811=VERTEX_POINT('',#441733);
#42812=VERTEX_POINT('',#441735);
#42813=VERTEX_POINT('',#441742);
#42814=VERTEX_POINT('',#441808);
#42815=VERTEX_POINT('',#441851);
#42816=VERTEX_POINT('',#441878);
#42817=VERTEX_POINT('',#442063);
#42818=VERTEX_POINT('',#442064);
#42819=VERTEX_POINT('',#442066);
#42820=VERTEX_POINT('',#442068);
#42821=VERTEX_POINT('',#442070);
#42822=VERTEX_POINT('',#442077);
#42823=VERTEX_POINT('',#442078);
#42824=VERTEX_POINT('',#442080);
#42825=VERTEX_POINT('',#442082);
#42826=VERTEX_POINT('',#442084);
#42827=VERTEX_POINT('',#442091);
#42828=VERTEX_POINT('',#442157);
#42829=VERTEX_POINT('',#442200);
#42830=VERTEX_POINT('',#442227);
#42831=VERTEX_POINT('',#442412);
#42832=VERTEX_POINT('',#442413);
#42833=VERTEX_POINT('',#442415);
#42834=VERTEX_POINT('',#442417);
#42835=VERTEX_POINT('',#442419);
#42836=VERTEX_POINT('',#442426);
#42837=VERTEX_POINT('',#442427);
#42838=VERTEX_POINT('',#442429);
#42839=VERTEX_POINT('',#442431);
#42840=VERTEX_POINT('',#442433);
#42841=VERTEX_POINT('',#442440);
#42842=VERTEX_POINT('',#442506);
#42843=VERTEX_POINT('',#442549);
#42844=VERTEX_POINT('',#442576);
#42845=VERTEX_POINT('',#442761);
#42846=VERTEX_POINT('',#442762);
#42847=VERTEX_POINT('',#442764);
#42848=VERTEX_POINT('',#442766);
#42849=VERTEX_POINT('',#442768);
#42850=VERTEX_POINT('',#442775);
#42851=VERTEX_POINT('',#442776);
#42852=VERTEX_POINT('',#442778);
#42853=VERTEX_POINT('',#442780);
#42854=VERTEX_POINT('',#442782);
#42855=VERTEX_POINT('',#442789);
#42856=VERTEX_POINT('',#442855);
#42857=VERTEX_POINT('',#442898);
#42858=VERTEX_POINT('',#442925);
#42859=VERTEX_POINT('',#443110);
#42860=VERTEX_POINT('',#443111);
#42861=VERTEX_POINT('',#443113);
#42862=VERTEX_POINT('',#443115);
#42863=VERTEX_POINT('',#443117);
#42864=VERTEX_POINT('',#443124);
#42865=VERTEX_POINT('',#443125);
#42866=VERTEX_POINT('',#443127);
#42867=VERTEX_POINT('',#443129);
#42868=VERTEX_POINT('',#443131);
#42869=VERTEX_POINT('',#443138);
#42870=VERTEX_POINT('',#443204);
#42871=VERTEX_POINT('',#443247);
#42872=VERTEX_POINT('',#443274);
#42873=VERTEX_POINT('',#443459);
#42874=VERTEX_POINT('',#443460);
#42875=VERTEX_POINT('',#443462);
#42876=VERTEX_POINT('',#443464);
#42877=VERTEX_POINT('',#443466);
#42878=VERTEX_POINT('',#443473);
#42879=VERTEX_POINT('',#443474);
#42880=VERTEX_POINT('',#443476);
#42881=VERTEX_POINT('',#443478);
#42882=VERTEX_POINT('',#443480);
#42883=VERTEX_POINT('',#443487);
#42884=VERTEX_POINT('',#443553);
#42885=VERTEX_POINT('',#443596);
#42886=VERTEX_POINT('',#443623);
#42887=VERTEX_POINT('',#443808);
#42888=VERTEX_POINT('',#443809);
#42889=VERTEX_POINT('',#443811);
#42890=VERTEX_POINT('',#443813);
#42891=VERTEX_POINT('',#443815);
#42892=VERTEX_POINT('',#443822);
#42893=VERTEX_POINT('',#443823);
#42894=VERTEX_POINT('',#443825);
#42895=VERTEX_POINT('',#443827);
#42896=VERTEX_POINT('',#443829);
#42897=VERTEX_POINT('',#443836);
#42898=VERTEX_POINT('',#443902);
#42899=VERTEX_POINT('',#443945);
#42900=VERTEX_POINT('',#443972);
#42901=VERTEX_POINT('',#444157);
#42902=VERTEX_POINT('',#444158);
#42903=VERTEX_POINT('',#444160);
#42904=VERTEX_POINT('',#444162);
#42905=VERTEX_POINT('',#444164);
#42906=VERTEX_POINT('',#444171);
#42907=VERTEX_POINT('',#444172);
#42908=VERTEX_POINT('',#444174);
#42909=VERTEX_POINT('',#444176);
#42910=VERTEX_POINT('',#444178);
#42911=VERTEX_POINT('',#444185);
#42912=VERTEX_POINT('',#444251);
#42913=VERTEX_POINT('',#444294);
#42914=VERTEX_POINT('',#444321);
#42915=VERTEX_POINT('',#444506);
#42916=VERTEX_POINT('',#444507);
#42917=VERTEX_POINT('',#444509);
#42918=VERTEX_POINT('',#444511);
#42919=VERTEX_POINT('',#444513);
#42920=VERTEX_POINT('',#444520);
#42921=VERTEX_POINT('',#444521);
#42922=VERTEX_POINT('',#444523);
#42923=VERTEX_POINT('',#444525);
#42924=VERTEX_POINT('',#444527);
#42925=VERTEX_POINT('',#444534);
#42926=VERTEX_POINT('',#444600);
#42927=VERTEX_POINT('',#444643);
#42928=VERTEX_POINT('',#444670);
#42929=VERTEX_POINT('',#444855);
#42930=VERTEX_POINT('',#444856);
#42931=VERTEX_POINT('',#444858);
#42932=VERTEX_POINT('',#444860);
#42933=VERTEX_POINT('',#444862);
#42934=VERTEX_POINT('',#444869);
#42935=VERTEX_POINT('',#444870);
#42936=VERTEX_POINT('',#444872);
#42937=VERTEX_POINT('',#444874);
#42938=VERTEX_POINT('',#444876);
#42939=VERTEX_POINT('',#444883);
#42940=VERTEX_POINT('',#444949);
#42941=VERTEX_POINT('',#444992);
#42942=VERTEX_POINT('',#445019);
#42943=VERTEX_POINT('',#445204);
#42944=VERTEX_POINT('',#445205);
#42945=VERTEX_POINT('',#445207);
#42946=VERTEX_POINT('',#445209);
#42947=VERTEX_POINT('',#445211);
#42948=VERTEX_POINT('',#445218);
#42949=VERTEX_POINT('',#445219);
#42950=VERTEX_POINT('',#445221);
#42951=VERTEX_POINT('',#445223);
#42952=VERTEX_POINT('',#445225);
#42953=VERTEX_POINT('',#445232);
#42954=VERTEX_POINT('',#445298);
#42955=VERTEX_POINT('',#445341);
#42956=VERTEX_POINT('',#445368);
#42957=VERTEX_POINT('',#445553);
#42958=VERTEX_POINT('',#445554);
#42959=VERTEX_POINT('',#445556);
#42960=VERTEX_POINT('',#445558);
#42961=VERTEX_POINT('',#445560);
#42962=VERTEX_POINT('',#445567);
#42963=VERTEX_POINT('',#445568);
#42964=VERTEX_POINT('',#445570);
#42965=VERTEX_POINT('',#445572);
#42966=VERTEX_POINT('',#445574);
#42967=VERTEX_POINT('',#445581);
#42968=VERTEX_POINT('',#445647);
#42969=VERTEX_POINT('',#445690);
#42970=VERTEX_POINT('',#445717);
#42971=VERTEX_POINT('',#445902);
#42972=VERTEX_POINT('',#445903);
#42973=VERTEX_POINT('',#445905);
#42974=VERTEX_POINT('',#445907);
#42975=VERTEX_POINT('',#445909);
#42976=VERTEX_POINT('',#445916);
#42977=VERTEX_POINT('',#445917);
#42978=VERTEX_POINT('',#445919);
#42979=VERTEX_POINT('',#445921);
#42980=VERTEX_POINT('',#445923);
#42981=VERTEX_POINT('',#445930);
#42982=VERTEX_POINT('',#445996);
#42983=VERTEX_POINT('',#446039);
#42984=VERTEX_POINT('',#446066);
#42985=VERTEX_POINT('',#446251);
#42986=VERTEX_POINT('',#446252);
#42987=VERTEX_POINT('',#446254);
#42988=VERTEX_POINT('',#446256);
#42989=VERTEX_POINT('',#446258);
#42990=VERTEX_POINT('',#446265);
#42991=VERTEX_POINT('',#446266);
#42992=VERTEX_POINT('',#446268);
#42993=VERTEX_POINT('',#446270);
#42994=VERTEX_POINT('',#446272);
#42995=VERTEX_POINT('',#446279);
#42996=VERTEX_POINT('',#446345);
#42997=VERTEX_POINT('',#446388);
#42998=VERTEX_POINT('',#446415);
#42999=VERTEX_POINT('',#446600);
#43000=VERTEX_POINT('',#446601);
#43001=VERTEX_POINT('',#446603);
#43002=VERTEX_POINT('',#446605);
#43003=VERTEX_POINT('',#446607);
#43004=VERTEX_POINT('',#446614);
#43005=VERTEX_POINT('',#446615);
#43006=VERTEX_POINT('',#446617);
#43007=VERTEX_POINT('',#446619);
#43008=VERTEX_POINT('',#446621);
#43009=VERTEX_POINT('',#446628);
#43010=VERTEX_POINT('',#446694);
#43011=VERTEX_POINT('',#446737);
#43012=VERTEX_POINT('',#446764);
#43013=VERTEX_POINT('',#446949);
#43014=VERTEX_POINT('',#446950);
#43015=VERTEX_POINT('',#446952);
#43016=VERTEX_POINT('',#446954);
#43017=VERTEX_POINT('',#446956);
#43018=VERTEX_POINT('',#446963);
#43019=VERTEX_POINT('',#446964);
#43020=VERTEX_POINT('',#446966);
#43021=VERTEX_POINT('',#446968);
#43022=VERTEX_POINT('',#446970);
#43023=VERTEX_POINT('',#446977);
#43024=VERTEX_POINT('',#447043);
#43025=VERTEX_POINT('',#447086);
#43026=VERTEX_POINT('',#447113);
#43027=VERTEX_POINT('',#447298);
#43028=VERTEX_POINT('',#447299);
#43029=VERTEX_POINT('',#447301);
#43030=VERTEX_POINT('',#447303);
#43031=VERTEX_POINT('',#447305);
#43032=VERTEX_POINT('',#447312);
#43033=VERTEX_POINT('',#447313);
#43034=VERTEX_POINT('',#447315);
#43035=VERTEX_POINT('',#447317);
#43036=VERTEX_POINT('',#447319);
#43037=VERTEX_POINT('',#447326);
#43038=VERTEX_POINT('',#447392);
#43039=VERTEX_POINT('',#447435);
#43040=VERTEX_POINT('',#447462);
#43041=VERTEX_POINT('',#447647);
#43042=VERTEX_POINT('',#447648);
#43043=VERTEX_POINT('',#447650);
#43044=VERTEX_POINT('',#447652);
#43045=VERTEX_POINT('',#447654);
#43046=VERTEX_POINT('',#447661);
#43047=VERTEX_POINT('',#447662);
#43048=VERTEX_POINT('',#447664);
#43049=VERTEX_POINT('',#447666);
#43050=VERTEX_POINT('',#447668);
#43051=VERTEX_POINT('',#447675);
#43052=VERTEX_POINT('',#447741);
#43053=VERTEX_POINT('',#447784);
#43054=VERTEX_POINT('',#447811);
#43055=VERTEX_POINT('',#447996);
#43056=VERTEX_POINT('',#447997);
#43057=VERTEX_POINT('',#447999);
#43058=VERTEX_POINT('',#448001);
#43059=VERTEX_POINT('',#448003);
#43060=VERTEX_POINT('',#448010);
#43061=VERTEX_POINT('',#448011);
#43062=VERTEX_POINT('',#448013);
#43063=VERTEX_POINT('',#448015);
#43064=VERTEX_POINT('',#448017);
#43065=VERTEX_POINT('',#448024);
#43066=VERTEX_POINT('',#448090);
#43067=VERTEX_POINT('',#448133);
#43068=VERTEX_POINT('',#448160);
#43069=VERTEX_POINT('',#448345);
#43070=VERTEX_POINT('',#448346);
#43071=VERTEX_POINT('',#448348);
#43072=VERTEX_POINT('',#448350);
#43073=VERTEX_POINT('',#448352);
#43074=VERTEX_POINT('',#448359);
#43075=VERTEX_POINT('',#448360);
#43076=VERTEX_POINT('',#448362);
#43077=VERTEX_POINT('',#448364);
#43078=VERTEX_POINT('',#448366);
#43079=VERTEX_POINT('',#448373);
#43080=VERTEX_POINT('',#448439);
#43081=VERTEX_POINT('',#448482);
#43082=VERTEX_POINT('',#448509);
#43083=VERTEX_POINT('',#448694);
#43084=VERTEX_POINT('',#448695);
#43085=VERTEX_POINT('',#448697);
#43086=VERTEX_POINT('',#448699);
#43087=VERTEX_POINT('',#448701);
#43088=VERTEX_POINT('',#448708);
#43089=VERTEX_POINT('',#448709);
#43090=VERTEX_POINT('',#448711);
#43091=VERTEX_POINT('',#448713);
#43092=VERTEX_POINT('',#448715);
#43093=VERTEX_POINT('',#448722);
#43094=VERTEX_POINT('',#448788);
#43095=VERTEX_POINT('',#448831);
#43096=VERTEX_POINT('',#448858);
#43097=VERTEX_POINT('',#449043);
#43098=VERTEX_POINT('',#449044);
#43099=VERTEX_POINT('',#449046);
#43100=VERTEX_POINT('',#449048);
#43101=VERTEX_POINT('',#449050);
#43102=VERTEX_POINT('',#449057);
#43103=VERTEX_POINT('',#449058);
#43104=VERTEX_POINT('',#449060);
#43105=VERTEX_POINT('',#449062);
#43106=VERTEX_POINT('',#449064);
#43107=VERTEX_POINT('',#449071);
#43108=VERTEX_POINT('',#449137);
#43109=VERTEX_POINT('',#449180);
#43110=VERTEX_POINT('',#449207);
#53727=EDGE_CURVE('',#40925,#40926,#29748,.T.);
#53728=EDGE_CURVE('',#40927,#40925,#4326,.T.);
#53729=EDGE_CURVE('',#40927,#40926,#22110,.T.);
#53730=EDGE_CURVE('',#40928,#40929,#29749,.T.);
#53731=EDGE_CURVE('',#40925,#40928,#4327,.T.);
#53732=EDGE_CURVE('',#40926,#40929,#4328,.T.);
#53733=EDGE_CURVE('',#40930,#40931,#29750,.T.);
#53734=EDGE_CURVE('',#40928,#40930,#4329,.T.);
#53735=EDGE_CURVE('',#40929,#40931,#4330,.T.);
#53736=EDGE_CURVE('',#40932,#40933,#29751,.T.);
#53737=EDGE_CURVE('',#40930,#40932,#4331,.T.);
#53738=EDGE_CURVE('',#40931,#40933,#4332,.T.);
#53739=EDGE_CURVE('',#40934,#40935,#29752,.T.);
#53740=EDGE_CURVE('',#40932,#40934,#4333,.T.);
#53741=EDGE_CURVE('',#40933,#40935,#4334,.T.);
#53742=EDGE_CURVE('',#40936,#40937,#29753,.T.);
#53743=EDGE_CURVE('',#40934,#40936,#4335,.T.);
#53744=EDGE_CURVE('',#40935,#40937,#4336,.T.);
#53745=EDGE_CURVE('',#40938,#40939,#29754,.T.);
#53746=EDGE_CURVE('',#40936,#40938,#4337,.T.);
#53747=EDGE_CURVE('',#40937,#40939,#4338,.T.);
#53748=EDGE_CURVE('',#40940,#40941,#29755,.T.);
#53749=EDGE_CURVE('',#40938,#40940,#4339,.T.);
#53750=EDGE_CURVE('',#40939,#40941,#4340,.T.);
#53751=EDGE_CURVE('',#40942,#40943,#29756,.T.);
#53752=EDGE_CURVE('',#40940,#40942,#4341,.T.);
#53753=EDGE_CURVE('',#40941,#40943,#4342,.T.);
#53754=EDGE_CURVE('',#40944,#40945,#29757,.T.);
#53755=EDGE_CURVE('',#40942,#40944,#4343,.T.);
#53756=EDGE_CURVE('',#40943,#40945,#4344,.T.);
#53757=EDGE_CURVE('',#40946,#40947,#29758,.T.);
#53758=EDGE_CURVE('',#40944,#40946,#4345,.T.);
#53759=EDGE_CURVE('',#40945,#40947,#4346,.T.);
#53760=EDGE_CURVE('',#40948,#40949,#29759,.T.);
#53761=EDGE_CURVE('',#40946,#40948,#4347,.T.);
#53762=EDGE_CURVE('',#40947,#40949,#4348,.T.);
#53763=EDGE_CURVE('',#40950,#40951,#29760,.T.);
#53764=EDGE_CURVE('',#40948,#40950,#4349,.T.);
#53765=EDGE_CURVE('',#40949,#40951,#4350,.T.);
#53766=EDGE_CURVE('',#40952,#40953,#29761,.T.);
#53767=EDGE_CURVE('',#40950,#40952,#4351,.T.);
#53768=EDGE_CURVE('',#40951,#40953,#4352,.T.);
#53769=EDGE_CURVE('',#40954,#40955,#29762,.T.);
#53770=EDGE_CURVE('',#40952,#40954,#4353,.T.);
#53771=EDGE_CURVE('',#40953,#40955,#4354,.T.);
#53772=EDGE_CURVE('',#40956,#40957,#29763,.T.);
#53773=EDGE_CURVE('',#40954,#40956,#4355,.T.);
#53774=EDGE_CURVE('',#40955,#40957,#4356,.T.);
#53775=EDGE_CURVE('',#40958,#40959,#29764,.T.);
#53776=EDGE_CURVE('',#40956,#40958,#4357,.T.);
#53777=EDGE_CURVE('',#40957,#40959,#4358,.T.);
#53778=EDGE_CURVE('',#40960,#40961,#29765,.T.);
#53779=EDGE_CURVE('',#40958,#40960,#4359,.T.);
#53780=EDGE_CURVE('',#40959,#40961,#4360,.T.);
#53781=EDGE_CURVE('',#40962,#40963,#29766,.T.);
#53782=EDGE_CURVE('',#40960,#40962,#4361,.T.);
#53783=EDGE_CURVE('',#40961,#40963,#4362,.T.);
#53784=EDGE_CURVE('',#40964,#40965,#29767,.T.);
#53785=EDGE_CURVE('',#40962,#40964,#4363,.T.);
#53786=EDGE_CURVE('',#40963,#40965,#4364,.T.);
#53787=EDGE_CURVE('',#40966,#40967,#29768,.T.);
#53788=EDGE_CURVE('',#40964,#40966,#4365,.T.);
#53789=EDGE_CURVE('',#40965,#40967,#4366,.T.);
#53790=EDGE_CURVE('',#40968,#40969,#29769,.T.);
#53791=EDGE_CURVE('',#40966,#40968,#4367,.T.);
#53792=EDGE_CURVE('',#40967,#40969,#4368,.T.);
#53793=EDGE_CURVE('',#40970,#40971,#29770,.T.);
#53794=EDGE_CURVE('',#40968,#40970,#4369,.T.);
#53795=EDGE_CURVE('',#40969,#40971,#4370,.T.);
#53796=EDGE_CURVE('',#40972,#40973,#29771,.T.);
#53797=EDGE_CURVE('',#40970,#40972,#4371,.T.);
#53798=EDGE_CURVE('',#40971,#40973,#4372,.T.);
#53799=EDGE_CURVE('',#40974,#40975,#29772,.T.);
#53800=EDGE_CURVE('',#40972,#40974,#4373,.T.);
#53801=EDGE_CURVE('',#40973,#40975,#4374,.T.);
#53802=EDGE_CURVE('',#40976,#40977,#29773,.T.);
#53803=EDGE_CURVE('',#40974,#40976,#4375,.T.);
#53804=EDGE_CURVE('',#40975,#40977,#4376,.T.);
#53805=EDGE_CURVE('',#40978,#40979,#29774,.T.);
#53806=EDGE_CURVE('',#40976,#40978,#4377,.T.);
#53807=EDGE_CURVE('',#40977,#40979,#4378,.T.);
#53808=EDGE_CURVE('',#40980,#40981,#29775,.T.);
#53809=EDGE_CURVE('',#40978,#40980,#4379,.T.);
#53810=EDGE_CURVE('',#40979,#40981,#4380,.T.);
#53811=EDGE_CURVE('',#40982,#40983,#29776,.T.);
#53812=EDGE_CURVE('',#40980,#40982,#4381,.T.);
#53813=EDGE_CURVE('',#40981,#40983,#4382,.T.);
#53814=EDGE_CURVE('',#40984,#40985,#29777,.T.);
#53815=EDGE_CURVE('',#40982,#40984,#4383,.T.);
#53816=EDGE_CURVE('',#40983,#40985,#4384,.T.);
#53817=EDGE_CURVE('',#40986,#40987,#29778,.T.);
#53818=EDGE_CURVE('',#40984,#40986,#4385,.T.);
#53819=EDGE_CURVE('',#40985,#40987,#4386,.T.);
#53820=EDGE_CURVE('',#40988,#40989,#29779,.T.);
#53821=EDGE_CURVE('',#40986,#40988,#4387,.T.);
#53822=EDGE_CURVE('',#40987,#40989,#4388,.T.);
#53823=EDGE_CURVE('',#40990,#40991,#29780,.T.);
#53824=EDGE_CURVE('',#40988,#40990,#4389,.T.);
#53825=EDGE_CURVE('',#40989,#40991,#4390,.T.);
#53826=EDGE_CURVE('',#40992,#40993,#29781,.T.);
#53827=EDGE_CURVE('',#40990,#40992,#4391,.T.);
#53828=EDGE_CURVE('',#40991,#40993,#4392,.T.);
#53829=EDGE_CURVE('',#40994,#40995,#29782,.T.);
#53830=EDGE_CURVE('',#40992,#40994,#4393,.T.);
#53831=EDGE_CURVE('',#40993,#40995,#4394,.T.);
#53832=EDGE_CURVE('',#40996,#40997,#29783,.T.);
#53833=EDGE_CURVE('',#40994,#40996,#4395,.T.);
#53834=EDGE_CURVE('',#40995,#40997,#4396,.T.);
#53835=EDGE_CURVE('',#40998,#40999,#29784,.T.);
#53836=EDGE_CURVE('',#40998,#41000,#25853,.T.);
#53837=EDGE_CURVE('',#41000,#41001,#22111,.T.);
#53838=EDGE_CURVE('',#41001,#40999,#25854,.T.);
#53839=EDGE_CURVE('',#41002,#41003,#29785,.T.);
#53840=EDGE_CURVE('',#40926,#41002,#25855,.F.);
#53841=EDGE_CURVE('',#40926,#41003,#22112,.T.);
#53842=EDGE_CURVE('',#41004,#41005,#29786,.T.);
#53843=EDGE_CURVE('',#41006,#41004,#25856,.F.);
#53844=EDGE_CURVE('',#41006,#41007,#22113,.T.);
#53845=EDGE_CURVE('',#41005,#41007,#25857,.F.);
#53846=EDGE_CURVE('',#41008,#41009,#29787,.T.);
#53847=EDGE_CURVE('',#41004,#41008,#25858,.F.);
#53848=EDGE_CURVE('',#41009,#41005,#25859,.F.);
#53849=EDGE_CURVE('',#41010,#41011,#29788,.T.);
#53850=EDGE_CURVE('',#41008,#41010,#25860,.F.);
#53851=EDGE_CURVE('',#41011,#41009,#25861,.F.);
#53852=EDGE_CURVE('',#41012,#41013,#29789,.T.);
#53853=EDGE_CURVE('',#41010,#41012,#25862,.F.);
#53854=EDGE_CURVE('',#41013,#41011,#25863,.F.);
#53855=EDGE_CURVE('',#41014,#41015,#29790,.T.);
#53856=EDGE_CURVE('',#41012,#41014,#25864,.F.);
#53857=EDGE_CURVE('',#41015,#41013,#25865,.F.);
#53858=EDGE_CURVE('',#41016,#41017,#29791,.T.);
#53859=EDGE_CURVE('',#41014,#41016,#25866,.F.);
#53860=EDGE_CURVE('',#41017,#41015,#25867,.F.);
#53861=EDGE_CURVE('',#41018,#41019,#29792,.T.);
#53862=EDGE_CURVE('',#41016,#41018,#25868,.F.);
#53863=EDGE_CURVE('',#41019,#41017,#25869,.F.);
#53864=EDGE_CURVE('',#41020,#41021,#29793,.T.);
#53865=EDGE_CURVE('',#41018,#41020,#25870,.F.);
#53866=EDGE_CURVE('',#41021,#41019,#25871,.F.);
#53867=EDGE_CURVE('',#41022,#41023,#29794,.T.);
#53868=EDGE_CURVE('',#41020,#41022,#25872,.F.);
#53869=EDGE_CURVE('',#41023,#41021,#25873,.F.);
#53870=EDGE_CURVE('',#41024,#41025,#29795,.T.);
#53871=EDGE_CURVE('',#41022,#41024,#25874,.F.);
#53872=EDGE_CURVE('',#41025,#41023,#25875,.F.);
#53873=EDGE_CURVE('',#41026,#41027,#29796,.T.);
#53874=EDGE_CURVE('',#41024,#41026,#25876,.F.);
#53875=EDGE_CURVE('',#41027,#41025,#25877,.F.);
#53876=EDGE_CURVE('',#41028,#41029,#29797,.T.);
#53877=EDGE_CURVE('',#41026,#41028,#25878,.F.);
#53878=EDGE_CURVE('',#41029,#41027,#25879,.F.);
#53879=EDGE_CURVE('',#41030,#41031,#29798,.T.);
#53880=EDGE_CURVE('',#41028,#41030,#25880,.F.);
#53881=EDGE_CURVE('',#41031,#41029,#25881,.F.);
#53882=EDGE_CURVE('',#41032,#41033,#29799,.T.);
#53883=EDGE_CURVE('',#41030,#41032,#25882,.F.);
#53884=EDGE_CURVE('',#41033,#41031,#25883,.F.);
#53885=EDGE_CURVE('',#41034,#41035,#29800,.T.);
#53886=EDGE_CURVE('',#41032,#41034,#25884,.F.);
#53887=EDGE_CURVE('',#41035,#41033,#25885,.F.);
#53888=EDGE_CURVE('',#41036,#41037,#29801,.T.);
#53889=EDGE_CURVE('',#41034,#41036,#25886,.F.);
#53890=EDGE_CURVE('',#41037,#41035,#25887,.F.);
#53891=EDGE_CURVE('',#41038,#41039,#29802,.T.);
#53892=EDGE_CURVE('',#41036,#41038,#25888,.F.);
#53893=EDGE_CURVE('',#41039,#41037,#25889,.F.);
#53894=EDGE_CURVE('',#41040,#41041,#29803,.T.);
#53895=EDGE_CURVE('',#41038,#41040,#25890,.F.);
#53896=EDGE_CURVE('',#41041,#41039,#25891,.F.);
#53897=EDGE_CURVE('',#41042,#41043,#29804,.T.);
#53898=EDGE_CURVE('',#41040,#41042,#25892,.F.);
#53899=EDGE_CURVE('',#41043,#41041,#25893,.F.);
#53900=EDGE_CURVE('',#41044,#41045,#29805,.T.);
#53901=EDGE_CURVE('',#41042,#41044,#25894,.F.);
#53902=EDGE_CURVE('',#41045,#41043,#25895,.F.);
#53903=EDGE_CURVE('',#41046,#41047,#29806,.T.);
#53904=EDGE_CURVE('',#41044,#41046,#25896,.F.);
#53905=EDGE_CURVE('',#41047,#41045,#25897,.F.);
#53906=EDGE_CURVE('',#41048,#41049,#29807,.T.);
#53907=EDGE_CURVE('',#41046,#41048,#25898,.F.);
#53908=EDGE_CURVE('',#41049,#41047,#25899,.F.);
#53909=EDGE_CURVE('',#41050,#41051,#29808,.T.);
#53910=EDGE_CURVE('',#41048,#41050,#25900,.F.);
#53911=EDGE_CURVE('',#41051,#41049,#25901,.F.);
#53912=EDGE_CURVE('',#41052,#41053,#29809,.T.);
#53913=EDGE_CURVE('',#41050,#41052,#25902,.F.);
#53914=EDGE_CURVE('',#41053,#41051,#25903,.F.);
#53915=EDGE_CURVE('',#41054,#41055,#29810,.T.);
#53916=EDGE_CURVE('',#41052,#41054,#25904,.F.);
#53917=EDGE_CURVE('',#41055,#41053,#25905,.F.);
#53918=EDGE_CURVE('',#41056,#41057,#29811,.T.);
#53919=EDGE_CURVE('',#41054,#41056,#25906,.F.);
#53920=EDGE_CURVE('',#41057,#41055,#25907,.F.);
#53921=EDGE_CURVE('',#41058,#41059,#29812,.T.);
#53922=EDGE_CURVE('',#41056,#41058,#25908,.F.);
#53923=EDGE_CURVE('',#41059,#41057,#25909,.F.);
#53924=EDGE_CURVE('',#41060,#41061,#29813,.T.);
#53925=EDGE_CURVE('',#41058,#41060,#25910,.F.);
#53926=EDGE_CURVE('',#41061,#41059,#25911,.F.);
#53927=EDGE_CURVE('',#41062,#41063,#29814,.T.);
#53928=EDGE_CURVE('',#41060,#41062,#25912,.F.);
#53929=EDGE_CURVE('',#41063,#41061,#25913,.F.);
#53930=EDGE_CURVE('',#41064,#41065,#29815,.T.);
#53931=EDGE_CURVE('',#41062,#41064,#25914,.F.);
#53932=EDGE_CURVE('',#41065,#41063,#25915,.F.);
#53933=EDGE_CURVE('',#41066,#41067,#29816,.T.);
#53934=EDGE_CURVE('',#41064,#41066,#25916,.F.);
#53935=EDGE_CURVE('',#41067,#41065,#25917,.F.);
#53936=EDGE_CURVE('',#41068,#41069,#29817,.T.);
#53937=EDGE_CURVE('',#41066,#41068,#25918,.F.);
#53938=EDGE_CURVE('',#41070,#41067,#25919,.F.);
#53939=EDGE_CURVE('',#41069,#41070,#25920,.F.);
#53940=EDGE_CURVE('',#41071,#41072,#29818,.T.);
#53941=EDGE_CURVE('',#41068,#41071,#25921,.F.);
#53942=EDGE_CURVE('',#41072,#41069,#25922,.F.);
#53943=EDGE_CURVE('',#41073,#41074,#29819,.T.);
#53944=EDGE_CURVE('',#41071,#41073,#25923,.F.);
#53945=EDGE_CURVE('',#41074,#41072,#25924,.F.);
#53946=EDGE_CURVE('',#41075,#41075,#22114,.T.);
#53947=EDGE_CURVE('',#41075,#40998,#29820,.T.);
#53948=EDGE_CURVE('',#41076,#40998,#22115,.T.);
#53949=EDGE_CURVE('',#41077,#41076,#25925,.F.);
#53950=EDGE_CURVE('',#41077,#41078,#29821,.T.);
#53951=EDGE_CURVE('',#40998,#41078,#25926,.F.);
#53952=EDGE_CURVE('',#41079,#41080,#22116,.T.);
#53953=EDGE_CURVE('',#41081,#41079,#22117,.T.);
#53954=EDGE_CURVE('',#41082,#41081,#22118,.T.);
#53955=EDGE_CURVE('',#41082,#41080,#22119,.T.);
#53956=EDGE_CURVE('',#41083,#41084,#22120,.T.);
#53957=EDGE_CURVE('',#41085,#41083,#22121,.T.);
#53958=EDGE_CURVE('',#41086,#41085,#22122,.T.);
#53959=EDGE_CURVE('',#41086,#41084,#22123,.T.);
#53960=EDGE_CURVE('',#41087,#41088,#22124,.T.);
#53961=EDGE_CURVE('',#41089,#41087,#22125,.T.);
#53962=EDGE_CURVE('',#41090,#41089,#22126,.T.);
#53963=EDGE_CURVE('',#41090,#41088,#22127,.T.);
#53964=EDGE_CURVE('',#41091,#41092,#22128,.T.);
#53965=EDGE_CURVE('',#41093,#41091,#22129,.T.);
#53966=EDGE_CURVE('',#41094,#41093,#22130,.T.);
#53967=EDGE_CURVE('',#41094,#41092,#22131,.T.);
#53968=EDGE_CURVE('',#41095,#41096,#22132,.T.);
#53969=EDGE_CURVE('',#41097,#41095,#22133,.T.);
#53970=EDGE_CURVE('',#41098,#41097,#22134,.T.);
#53971=EDGE_CURVE('',#41098,#41096,#22135,.T.);
#53972=EDGE_CURVE('',#41099,#41100,#22136,.T.);
#53973=EDGE_CURVE('',#41101,#41099,#22137,.T.);
#53974=EDGE_CURVE('',#41102,#41101,#22138,.T.);
#53975=EDGE_CURVE('',#41102,#41100,#22139,.T.);
#53976=EDGE_CURVE('',#41103,#41104,#22140,.T.);
#53977=EDGE_CURVE('',#41105,#41103,#22141,.T.);
#53978=EDGE_CURVE('',#41106,#41105,#22142,.T.);
#53979=EDGE_CURVE('',#41106,#41104,#22143,.T.);
#53980=EDGE_CURVE('',#41107,#41108,#22144,.T.);
#53981=EDGE_CURVE('',#41109,#41107,#22145,.T.);
#53982=EDGE_CURVE('',#41110,#41109,#22146,.T.);
#53983=EDGE_CURVE('',#41110,#41108,#22147,.T.);
#53984=EDGE_CURVE('',#41111,#41112,#22148,.T.);
#53985=EDGE_CURVE('',#41113,#41111,#22149,.T.);
#53986=EDGE_CURVE('',#41114,#41113,#22150,.T.);
#53987=EDGE_CURVE('',#41114,#41112,#22151,.T.);
#53988=EDGE_CURVE('',#41115,#41116,#22152,.T.);
#53989=EDGE_CURVE('',#41117,#41115,#22153,.T.);
#53990=EDGE_CURVE('',#41118,#41117,#22154,.T.);
#53991=EDGE_CURVE('',#41118,#41116,#22155,.T.);
#53992=EDGE_CURVE('',#41119,#41120,#22156,.T.);
#53993=EDGE_CURVE('',#41121,#41119,#22157,.T.);
#53994=EDGE_CURVE('',#41122,#41121,#22158,.T.);
#53995=EDGE_CURVE('',#41122,#41120,#22159,.T.);
#53996=EDGE_CURVE('',#41123,#41124,#22160,.T.);
#53997=EDGE_CURVE('',#41125,#41123,#22161,.T.);
#53998=EDGE_CURVE('',#41126,#41125,#22162,.T.);
#53999=EDGE_CURVE('',#41126,#41124,#22163,.T.);
#54000=EDGE_CURVE('',#41127,#41128,#22164,.T.);
#54001=EDGE_CURVE('',#41129,#41127,#22165,.T.);
#54002=EDGE_CURVE('',#41130,#41129,#22166,.T.);
#54003=EDGE_CURVE('',#41130,#41128,#22167,.T.);
#54004=EDGE_CURVE('',#41131,#41132,#22168,.T.);
#54005=EDGE_CURVE('',#41133,#41131,#22169,.T.);
#54006=EDGE_CURVE('',#41134,#41133,#22170,.T.);
#54007=EDGE_CURVE('',#41134,#41132,#22171,.T.);
#54008=EDGE_CURVE('',#41135,#41136,#22172,.T.);
#54009=EDGE_CURVE('',#41137,#41135,#22173,.T.);
#54010=EDGE_CURVE('',#41138,#41137,#22174,.T.);
#54011=EDGE_CURVE('',#41138,#41136,#22175,.T.);
#54012=EDGE_CURVE('',#41139,#41140,#22176,.T.);
#54013=EDGE_CURVE('',#41141,#41139,#22177,.T.);
#54014=EDGE_CURVE('',#41142,#41141,#22178,.T.);
#54015=EDGE_CURVE('',#41142,#41140,#22179,.T.);
#54016=EDGE_CURVE('',#41143,#41144,#22180,.T.);
#54017=EDGE_CURVE('',#41145,#41143,#22181,.T.);
#54018=EDGE_CURVE('',#41146,#41145,#22182,.T.);
#54019=EDGE_CURVE('',#41146,#41144,#22183,.T.);
#54020=EDGE_CURVE('',#41147,#41148,#22184,.T.);
#54021=EDGE_CURVE('',#41149,#41147,#22185,.T.);
#54022=EDGE_CURVE('',#41150,#41149,#22186,.T.);
#54023=EDGE_CURVE('',#41150,#41148,#22187,.T.);
#54024=EDGE_CURVE('',#41151,#41152,#22188,.T.);
#54025=EDGE_CURVE('',#41153,#41151,#22189,.T.);
#54026=EDGE_CURVE('',#41154,#41153,#22190,.T.);
#54027=EDGE_CURVE('',#41154,#41152,#22191,.T.);
#54028=EDGE_CURVE('',#41155,#41156,#22192,.T.);
#54029=EDGE_CURVE('',#41157,#41155,#22193,.T.);
#54030=EDGE_CURVE('',#41158,#41157,#22194,.T.);
#54031=EDGE_CURVE('',#41158,#41156,#22195,.T.);
#54032=EDGE_CURVE('',#41159,#41160,#22196,.T.);
#54033=EDGE_CURVE('',#41161,#41159,#22197,.T.);
#54034=EDGE_CURVE('',#41162,#41161,#22198,.T.);
#54035=EDGE_CURVE('',#41162,#41160,#22199,.T.);
#54036=EDGE_CURVE('',#41163,#41164,#22200,.T.);
#54037=EDGE_CURVE('',#41165,#41163,#22201,.T.);
#54038=EDGE_CURVE('',#41166,#41165,#22202,.T.);
#54039=EDGE_CURVE('',#41166,#41164,#22203,.T.);
#54040=EDGE_CURVE('',#41167,#41168,#22204,.T.);
#54041=EDGE_CURVE('',#41169,#41167,#22205,.T.);
#54042=EDGE_CURVE('',#41170,#41169,#22206,.T.);
#54043=EDGE_CURVE('',#41170,#41168,#22207,.T.);
#54044=EDGE_CURVE('',#41171,#41172,#22208,.T.);
#54045=EDGE_CURVE('',#41173,#41171,#22209,.T.);
#54046=EDGE_CURVE('',#41174,#41173,#22210,.T.);
#54047=EDGE_CURVE('',#41174,#41172,#22211,.T.);
#54048=EDGE_CURVE('',#41175,#41176,#22212,.T.);
#54049=EDGE_CURVE('',#41177,#41175,#22213,.T.);
#54050=EDGE_CURVE('',#41178,#41177,#22214,.T.);
#54051=EDGE_CURVE('',#41178,#41176,#22215,.T.);
#54052=EDGE_CURVE('',#41179,#41180,#22216,.T.);
#54053=EDGE_CURVE('',#41181,#41179,#22217,.T.);
#54054=EDGE_CURVE('',#41182,#41181,#22218,.T.);
#54055=EDGE_CURVE('',#41182,#41180,#22219,.T.);
#54056=EDGE_CURVE('',#41183,#41184,#22220,.T.);
#54057=EDGE_CURVE('',#41185,#41183,#22221,.T.);
#54058=EDGE_CURVE('',#41186,#41185,#22222,.T.);
#54059=EDGE_CURVE('',#41186,#41184,#22223,.T.);
#54060=EDGE_CURVE('',#41187,#41188,#22224,.T.);
#54061=EDGE_CURVE('',#41189,#41187,#22225,.T.);
#54062=EDGE_CURVE('',#41190,#41189,#22226,.T.);
#54063=EDGE_CURVE('',#41190,#41188,#22227,.T.);
#54064=EDGE_CURVE('',#41191,#41192,#22228,.T.);
#54065=EDGE_CURVE('',#41193,#41191,#22229,.T.);
#54066=EDGE_CURVE('',#41194,#41193,#22230,.T.);
#54067=EDGE_CURVE('',#41194,#41192,#22231,.T.);
#54068=EDGE_CURVE('',#41195,#41196,#22232,.T.);
#54069=EDGE_CURVE('',#41197,#41195,#22233,.T.);
#54070=EDGE_CURVE('',#41198,#41197,#22234,.T.);
#54071=EDGE_CURVE('',#41198,#41196,#22235,.T.);
#54072=EDGE_CURVE('',#41199,#41200,#22236,.T.);
#54073=EDGE_CURVE('',#41201,#41199,#22237,.T.);
#54074=EDGE_CURVE('',#41202,#41201,#22238,.T.);
#54075=EDGE_CURVE('',#41202,#41200,#22239,.T.);
#54076=EDGE_CURVE('',#41203,#41204,#22240,.T.);
#54077=EDGE_CURVE('',#41205,#41203,#22241,.T.);
#54078=EDGE_CURVE('',#41206,#41205,#22242,.T.);
#54079=EDGE_CURVE('',#41206,#41204,#22243,.T.);
#54080=EDGE_CURVE('',#41207,#41208,#22244,.T.);
#54081=EDGE_CURVE('',#41209,#41207,#22245,.T.);
#54082=EDGE_CURVE('',#41210,#41209,#22246,.T.);
#54083=EDGE_CURVE('',#41210,#41208,#22247,.T.);
#54084=EDGE_CURVE('',#41211,#41212,#22248,.T.);
#54085=EDGE_CURVE('',#41213,#41211,#22249,.T.);
#54086=EDGE_CURVE('',#41214,#41213,#22250,.T.);
#54087=EDGE_CURVE('',#41214,#41212,#22251,.T.);
#54088=EDGE_CURVE('',#41215,#41216,#22252,.T.);
#54089=EDGE_CURVE('',#41217,#41215,#22253,.T.);
#54090=EDGE_CURVE('',#41218,#41217,#22254,.T.);
#54091=EDGE_CURVE('',#41218,#41216,#22255,.T.);
#54092=EDGE_CURVE('',#41219,#41220,#22256,.T.);
#54093=EDGE_CURVE('',#41221,#41219,#22257,.T.);
#54094=EDGE_CURVE('',#41222,#41221,#22258,.T.);
#54095=EDGE_CURVE('',#41222,#41220,#22259,.T.);
#54096=EDGE_CURVE('',#41223,#41224,#22260,.T.);
#54097=EDGE_CURVE('',#41225,#41223,#22261,.T.);
#54098=EDGE_CURVE('',#41226,#41225,#22262,.T.);
#54099=EDGE_CURVE('',#41226,#41224,#22263,.T.);
#54100=EDGE_CURVE('',#41227,#41228,#22264,.T.);
#54101=EDGE_CURVE('',#41229,#41227,#22265,.T.);
#54102=EDGE_CURVE('',#41230,#41229,#22266,.T.);
#54103=EDGE_CURVE('',#41230,#41228,#22267,.T.);
#54104=EDGE_CURVE('',#41231,#41232,#22268,.T.);
#54105=EDGE_CURVE('',#41233,#41231,#22269,.T.);
#54106=EDGE_CURVE('',#41234,#41233,#22270,.T.);
#54107=EDGE_CURVE('',#41234,#41232,#22271,.T.);
#54108=EDGE_CURVE('',#41235,#41236,#22272,.T.);
#54109=EDGE_CURVE('',#41237,#41235,#22273,.T.);
#54110=EDGE_CURVE('',#41238,#41237,#22274,.T.);
#54111=EDGE_CURVE('',#41238,#41236,#22275,.T.);
#54112=EDGE_CURVE('',#41239,#41240,#22276,.T.);
#54113=EDGE_CURVE('',#41241,#41239,#22277,.T.);
#54114=EDGE_CURVE('',#41242,#41241,#22278,.T.);
#54115=EDGE_CURVE('',#41242,#41240,#22279,.T.);
#54116=EDGE_CURVE('',#41243,#41244,#22280,.T.);
#54117=EDGE_CURVE('',#41245,#41243,#22281,.T.);
#54118=EDGE_CURVE('',#41246,#41245,#22282,.T.);
#54119=EDGE_CURVE('',#41246,#41244,#22283,.T.);
#54120=EDGE_CURVE('',#41247,#41248,#22284,.T.);
#54121=EDGE_CURVE('',#41249,#41247,#22285,.T.);
#54122=EDGE_CURVE('',#41250,#41249,#22286,.T.);
#54123=EDGE_CURVE('',#41250,#41248,#22287,.T.);
#54124=EDGE_CURVE('',#41251,#41252,#22288,.T.);
#54125=EDGE_CURVE('',#41253,#41251,#22289,.T.);
#54126=EDGE_CURVE('',#41254,#41253,#22290,.T.);
#54127=EDGE_CURVE('',#41254,#41252,#22291,.T.);
#54128=EDGE_CURVE('',#41255,#41256,#22292,.T.);
#54129=EDGE_CURVE('',#41257,#41255,#22293,.T.);
#54130=EDGE_CURVE('',#41258,#41257,#22294,.T.);
#54131=EDGE_CURVE('',#41258,#41256,#22295,.T.);
#54132=EDGE_CURVE('',#41259,#41260,#22296,.T.);
#54133=EDGE_CURVE('',#41261,#41259,#22297,.T.);
#54134=EDGE_CURVE('',#41262,#41261,#22298,.T.);
#54135=EDGE_CURVE('',#41262,#41260,#22299,.T.);
#54136=EDGE_CURVE('',#41263,#41264,#22300,.T.);
#54137=EDGE_CURVE('',#41265,#41263,#22301,.T.);
#54138=EDGE_CURVE('',#41266,#41265,#22302,.T.);
#54139=EDGE_CURVE('',#41266,#41264,#22303,.T.);
#54140=EDGE_CURVE('',#41267,#41268,#22304,.T.);
#54141=EDGE_CURVE('',#41269,#41267,#22305,.T.);
#54142=EDGE_CURVE('',#41270,#41269,#22306,.T.);
#54143=EDGE_CURVE('',#41270,#41268,#22307,.T.);
#54144=EDGE_CURVE('',#41271,#41272,#22308,.T.);
#54145=EDGE_CURVE('',#41273,#41271,#22309,.T.);
#54146=EDGE_CURVE('',#41274,#41273,#22310,.T.);
#54147=EDGE_CURVE('',#41274,#41272,#22311,.T.);
#54148=EDGE_CURVE('',#41275,#41276,#22312,.T.);
#54149=EDGE_CURVE('',#41277,#41275,#22313,.T.);
#54150=EDGE_CURVE('',#41278,#41277,#22314,.T.);
#54151=EDGE_CURVE('',#41278,#41276,#22315,.T.);
#54152=EDGE_CURVE('',#41279,#41280,#22316,.T.);
#54153=EDGE_CURVE('',#41281,#41279,#22317,.T.);
#54154=EDGE_CURVE('',#41282,#41281,#22318,.T.);
#54155=EDGE_CURVE('',#41282,#41280,#22319,.T.);
#54156=EDGE_CURVE('',#41283,#41284,#22320,.T.);
#54157=EDGE_CURVE('',#41285,#41283,#22321,.T.);
#54158=EDGE_CURVE('',#41286,#41285,#22322,.T.);
#54159=EDGE_CURVE('',#41286,#41284,#22323,.T.);
#54160=EDGE_CURVE('',#41287,#41288,#22324,.T.);
#54161=EDGE_CURVE('',#41289,#41287,#22325,.T.);
#54162=EDGE_CURVE('',#41290,#41289,#22326,.T.);
#54163=EDGE_CURVE('',#41290,#41288,#22327,.T.);
#54164=EDGE_CURVE('',#41291,#41292,#22328,.T.);
#54165=EDGE_CURVE('',#41293,#41291,#22329,.T.);
#54166=EDGE_CURVE('',#41294,#41293,#22330,.T.);
#54167=EDGE_CURVE('',#41294,#41292,#22331,.T.);
#54168=EDGE_CURVE('',#41295,#41296,#22332,.T.);
#54169=EDGE_CURVE('',#41297,#41295,#22333,.T.);
#54170=EDGE_CURVE('',#41298,#41297,#22334,.T.);
#54171=EDGE_CURVE('',#41298,#41296,#22335,.T.);
#54172=EDGE_CURVE('',#41299,#41300,#22336,.T.);
#54173=EDGE_CURVE('',#41301,#41299,#22337,.T.);
#54174=EDGE_CURVE('',#41302,#41301,#22338,.T.);
#54175=EDGE_CURVE('',#41302,#41300,#22339,.T.);
#54176=EDGE_CURVE('',#41303,#41304,#22340,.T.);
#54177=EDGE_CURVE('',#41305,#41303,#22341,.T.);
#54178=EDGE_CURVE('',#41306,#41305,#22342,.T.);
#54179=EDGE_CURVE('',#41306,#41304,#22343,.T.);
#54180=EDGE_CURVE('',#41307,#41308,#22344,.T.);
#54181=EDGE_CURVE('',#41309,#41307,#22345,.T.);
#54182=EDGE_CURVE('',#41310,#41309,#22346,.T.);
#54183=EDGE_CURVE('',#41310,#41308,#22347,.T.);
#54184=EDGE_CURVE('',#41311,#41312,#22348,.T.);
#54185=EDGE_CURVE('',#41313,#41311,#22349,.T.);
#54186=EDGE_CURVE('',#41314,#41313,#22350,.T.);
#54187=EDGE_CURVE('',#41314,#41312,#22351,.T.);
#54188=EDGE_CURVE('',#41315,#41316,#22352,.T.);
#54189=EDGE_CURVE('',#41317,#41315,#22353,.T.);
#54190=EDGE_CURVE('',#41318,#41317,#22354,.T.);
#54191=EDGE_CURVE('',#41318,#41316,#22355,.T.);
#54192=EDGE_CURVE('',#41319,#41320,#22356,.T.);
#54193=EDGE_CURVE('',#41321,#41319,#22357,.T.);
#54194=EDGE_CURVE('',#41322,#41321,#22358,.T.);
#54195=EDGE_CURVE('',#41322,#41320,#22359,.T.);
#54196=EDGE_CURVE('',#41323,#41324,#22360,.T.);
#54197=EDGE_CURVE('',#41325,#41323,#22361,.T.);
#54198=EDGE_CURVE('',#41326,#41325,#22362,.T.);
#54199=EDGE_CURVE('',#41326,#41324,#22363,.T.);
#54200=EDGE_CURVE('',#41327,#41328,#22364,.T.);
#54201=EDGE_CURVE('',#41329,#41327,#22365,.T.);
#54202=EDGE_CURVE('',#41330,#41329,#22366,.T.);
#54203=EDGE_CURVE('',#41330,#41328,#22367,.T.);
#54204=EDGE_CURVE('',#41331,#41332,#22368,.T.);
#54205=EDGE_CURVE('',#41333,#41331,#22369,.T.);
#54206=EDGE_CURVE('',#41334,#41333,#22370,.T.);
#54207=EDGE_CURVE('',#41334,#41332,#22371,.T.);
#54208=EDGE_CURVE('',#41335,#41336,#22372,.T.);
#54209=EDGE_CURVE('',#41337,#41335,#22373,.T.);
#54210=EDGE_CURVE('',#41338,#41337,#22374,.T.);
#54211=EDGE_CURVE('',#41338,#41336,#22375,.T.);
#54212=EDGE_CURVE('',#41339,#41340,#22376,.T.);
#54213=EDGE_CURVE('',#41341,#41339,#22377,.T.);
#54214=EDGE_CURVE('',#41342,#41341,#22378,.T.);
#54215=EDGE_CURVE('',#41342,#41340,#22379,.T.);
#54216=EDGE_CURVE('',#41343,#41344,#22380,.T.);
#54217=EDGE_CURVE('',#41345,#41343,#22381,.T.);
#54218=EDGE_CURVE('',#41346,#41345,#22382,.T.);
#54219=EDGE_CURVE('',#41346,#41344,#22383,.T.);
#54220=EDGE_CURVE('',#41347,#41348,#22384,.T.);
#54221=EDGE_CURVE('',#41349,#41347,#22385,.T.);
#54222=EDGE_CURVE('',#41350,#41349,#22386,.T.);
#54223=EDGE_CURVE('',#41350,#41348,#22387,.T.);
#54224=EDGE_CURVE('',#41351,#41352,#22388,.T.);
#54225=EDGE_CURVE('',#41353,#41351,#22389,.T.);
#54226=EDGE_CURVE('',#41354,#41353,#22390,.T.);
#54227=EDGE_CURVE('',#41354,#41352,#22391,.T.);
#54228=EDGE_CURVE('',#41355,#41356,#22392,.T.);
#54229=EDGE_CURVE('',#41357,#41355,#22393,.T.);
#54230=EDGE_CURVE('',#41358,#41357,#22394,.T.);
#54231=EDGE_CURVE('',#41358,#41356,#22395,.T.);
#54232=EDGE_CURVE('',#41359,#41360,#22396,.T.);
#54233=EDGE_CURVE('',#41361,#41359,#22397,.T.);
#54234=EDGE_CURVE('',#41362,#41361,#22398,.T.);
#54235=EDGE_CURVE('',#41362,#41360,#22399,.T.);
#54236=EDGE_CURVE('',#41363,#41364,#22400,.T.);
#54237=EDGE_CURVE('',#41365,#41363,#22401,.T.);
#54238=EDGE_CURVE('',#41366,#41365,#22402,.T.);
#54239=EDGE_CURVE('',#41366,#41364,#22403,.T.);
#54240=EDGE_CURVE('',#41367,#41368,#22404,.T.);
#54241=EDGE_CURVE('',#41369,#41367,#22405,.T.);
#54242=EDGE_CURVE('',#41370,#41369,#22406,.T.);
#54243=EDGE_CURVE('',#41370,#41368,#22407,.T.);
#54244=EDGE_CURVE('',#41371,#41372,#22408,.T.);
#54245=EDGE_CURVE('',#41373,#41371,#22409,.T.);
#54246=EDGE_CURVE('',#41374,#41373,#22410,.T.);
#54247=EDGE_CURVE('',#41374,#41372,#22411,.T.);
#54248=EDGE_CURVE('',#41375,#41376,#22412,.T.);
#54249=EDGE_CURVE('',#41377,#41375,#22413,.T.);
#54250=EDGE_CURVE('',#41378,#41377,#22414,.T.);
#54251=EDGE_CURVE('',#41378,#41376,#22415,.T.);
#54252=EDGE_CURVE('',#41379,#41380,#22416,.T.);
#54253=EDGE_CURVE('',#41381,#41379,#22417,.T.);
#54254=EDGE_CURVE('',#41382,#41381,#22418,.T.);
#54255=EDGE_CURVE('',#41382,#41380,#22419,.T.);
#54256=EDGE_CURVE('',#41383,#41384,#22420,.T.);
#54257=EDGE_CURVE('',#41385,#41383,#22421,.T.);
#54258=EDGE_CURVE('',#41386,#41385,#22422,.T.);
#54259=EDGE_CURVE('',#41387,#41386,#22423,.T.);
#54260=EDGE_CURVE('',#41387,#41384,#22424,.T.);
#54261=EDGE_CURVE('',#41073,#41077,#25927,.F.);
#54262=EDGE_CURVE('',#41078,#41074,#25928,.F.);
#54263=EDGE_CURVE('',#41003,#40927,#22425,.T.);
#54264=EDGE_CURVE('',#41007,#40927,#25929,.F.);
#54265=EDGE_CURVE('',#41002,#41006,#25930,.F.);
#54266=EDGE_CURVE('',#41388,#41388,#22426,.T.);
#54267=EDGE_CURVE('',#41388,#41075,#29822,.T.);
#54268=EDGE_CURVE('',#40999,#41076,#25931,.T.);
#54269=EDGE_CURVE('',#41389,#41390,#29823,.T.);
#54270=EDGE_CURVE('',#41391,#41390,#22427,.T.);
#54271=EDGE_CURVE('',#41392,#41391,#22428,.T.);
#54272=EDGE_CURVE('',#41393,#41392,#22429,.T.);
#54273=EDGE_CURVE('',#41393,#41394,#22430,.T.);
#54274=EDGE_CURVE('',#41395,#41394,#22431,.T.);
#54275=EDGE_CURVE('',#41390,#41395,#22432,.T.);
#54276=EDGE_CURVE('',#41396,#41397,#4397,.T.);
#54277=EDGE_CURVE('',#41397,#41396,#22433,.T.);
#54278=EDGE_CURVE('',#41398,#41398,#22434,.T.);
#54279=EDGE_CURVE('',#41398,#41399,#22435,.T.);
#54280=EDGE_CURVE('',#41399,#41399,#22436,.T.);
#54281=EDGE_CURVE('',#41400,#41400,#22437,.T.);
#54282=EDGE_CURVE('',#41400,#41398,#29824,.T.);
#54283=EDGE_CURVE('',#41401,#41401,#22438,.T.);
#54284=EDGE_CURVE('',#41401,#41400,#22439,.T.);
#54285=EDGE_CURVE('',#41402,#41403,#25932,.T.);
#54286=EDGE_CURVE('',#41403,#41404,#29825,.T.);
#54287=EDGE_CURVE('',#41404,#41405,#22440,.T.);
#54288=EDGE_CURVE('',#41405,#41406,#29826,.T.);
#54289=EDGE_CURVE('',#41406,#41407,#25933,.T.);
#54290=EDGE_CURVE('',#41407,#41408,#29827,.T.);
#54291=EDGE_CURVE('',#41408,#41409,#22441,.T.);
#54292=EDGE_CURVE('',#41409,#41410,#29828,.T.);
#54293=EDGE_CURVE('',#41410,#41411,#25934,.T.);
#54294=EDGE_CURVE('',#41411,#41412,#29829,.T.);
#54295=EDGE_CURVE('',#41412,#41413,#22442,.T.);
#54296=EDGE_CURVE('',#41413,#41414,#29830,.T.);
#54297=EDGE_CURVE('',#41414,#41415,#25935,.T.);
#54298=EDGE_CURVE('',#41415,#41416,#29831,.T.);
#54299=EDGE_CURVE('',#41416,#41417,#22443,.T.);
#54300=EDGE_CURVE('',#41417,#41418,#29832,.T.);
#54301=EDGE_CURVE('',#41418,#41419,#25936,.T.);
#54302=EDGE_CURVE('',#41419,#41420,#29833,.T.);
#54303=EDGE_CURVE('',#41420,#41421,#22444,.T.);
#54304=EDGE_CURVE('',#41421,#41422,#29834,.T.);
#54305=EDGE_CURVE('',#41422,#41423,#25937,.T.);
#54306=EDGE_CURVE('',#41423,#41424,#29835,.T.);
#54307=EDGE_CURVE('',#41424,#41425,#22445,.T.);
#54308=EDGE_CURVE('',#41425,#41426,#29836,.T.);
#54309=EDGE_CURVE('',#41426,#41427,#25938,.T.);
#54310=EDGE_CURVE('',#41427,#41428,#29837,.T.);
#54311=EDGE_CURVE('',#41428,#41429,#22446,.T.);
#54312=EDGE_CURVE('',#41429,#41430,#29838,.T.);
#54313=EDGE_CURVE('',#41430,#41431,#25939,.T.);
#54314=EDGE_CURVE('',#41431,#41432,#29839,.T.);
#54315=EDGE_CURVE('',#41432,#41433,#22447,.T.);
#54316=EDGE_CURVE('',#41433,#41434,#29840,.T.);
#54317=EDGE_CURVE('',#41434,#41435,#25940,.T.);
#54318=EDGE_CURVE('',#41435,#41436,#29841,.T.);
#54319=EDGE_CURVE('',#41436,#41437,#22448,.T.);
#54320=EDGE_CURVE('',#41437,#41438,#29842,.T.);
#54321=EDGE_CURVE('',#41438,#41439,#25941,.T.);
#54322=EDGE_CURVE('',#41439,#41440,#29843,.T.);
#54323=EDGE_CURVE('',#41440,#41441,#22449,.T.);
#54324=EDGE_CURVE('',#41441,#41442,#29844,.T.);
#54325=EDGE_CURVE('',#41442,#41443,#25942,.T.);
#54326=EDGE_CURVE('',#41443,#41444,#29845,.T.);
#54327=EDGE_CURVE('',#41444,#41445,#22450,.T.);
#54328=EDGE_CURVE('',#41445,#41446,#29846,.T.);
#54329=EDGE_CURVE('',#41446,#41447,#25943,.T.);
#54330=EDGE_CURVE('',#41447,#41448,#29847,.T.);
#54331=EDGE_CURVE('',#41448,#41449,#22451,.T.);
#54332=EDGE_CURVE('',#41449,#41450,#29848,.T.);
#54333=EDGE_CURVE('',#41450,#41451,#25944,.T.);
#54334=EDGE_CURVE('',#41451,#41452,#29849,.T.);
#54335=EDGE_CURVE('',#41452,#41453,#22452,.T.);
#54336=EDGE_CURVE('',#41453,#41454,#29850,.T.);
#54337=EDGE_CURVE('',#41454,#41455,#25945,.T.);
#54338=EDGE_CURVE('',#41455,#41456,#29851,.T.);
#54339=EDGE_CURVE('',#41456,#41457,#22453,.T.);
#54340=EDGE_CURVE('',#41457,#41458,#29852,.T.);
#54341=EDGE_CURVE('',#41458,#41459,#25946,.T.);
#54342=EDGE_CURVE('',#41459,#41460,#29853,.T.);
#54343=EDGE_CURVE('',#41460,#41461,#22454,.T.);
#54344=EDGE_CURVE('',#41461,#41462,#29854,.T.);
#54345=EDGE_CURVE('',#41462,#41463,#25947,.T.);
#54346=EDGE_CURVE('',#41463,#41464,#29855,.T.);
#54347=EDGE_CURVE('',#41464,#41465,#22455,.T.);
#54348=EDGE_CURVE('',#41465,#41466,#29856,.T.);
#54349=EDGE_CURVE('',#41466,#41467,#25948,.T.);
#54350=EDGE_CURVE('',#41467,#41468,#29857,.T.);
#54351=EDGE_CURVE('',#41468,#41469,#22456,.T.);
#54352=EDGE_CURVE('',#41469,#41470,#29858,.T.);
#54353=EDGE_CURVE('',#41470,#41471,#25949,.T.);
#54354=EDGE_CURVE('',#41471,#41472,#29859,.T.);
#54355=EDGE_CURVE('',#41472,#41473,#22457,.T.);
#54356=EDGE_CURVE('',#41473,#41474,#29860,.T.);
#54357=EDGE_CURVE('',#41474,#41475,#25950,.T.);
#54358=EDGE_CURVE('',#41475,#41476,#29861,.T.);
#54359=EDGE_CURVE('',#41476,#41477,#22458,.T.);
#54360=EDGE_CURVE('',#41477,#41478,#29862,.T.);
#54361=EDGE_CURVE('',#41478,#41479,#25951,.T.);
#54362=EDGE_CURVE('',#41479,#41480,#29863,.T.);
#54363=EDGE_CURVE('',#41480,#41481,#22459,.T.);
#54364=EDGE_CURVE('',#41481,#41482,#29864,.T.);
#54365=EDGE_CURVE('',#41482,#41483,#25952,.T.);
#54366=EDGE_CURVE('',#41483,#41484,#29865,.T.);
#54367=EDGE_CURVE('',#41484,#41485,#22460,.T.);
#54368=EDGE_CURVE('',#41485,#41486,#29866,.T.);
#54369=EDGE_CURVE('',#41486,#41487,#25953,.T.);
#54370=EDGE_CURVE('',#41487,#41488,#29867,.T.);
#54371=EDGE_CURVE('',#41488,#41489,#22461,.T.);
#54372=EDGE_CURVE('',#41489,#41490,#29868,.T.);
#54373=EDGE_CURVE('',#41490,#41491,#25954,.T.);
#54374=EDGE_CURVE('',#41491,#41492,#29869,.T.);
#54375=EDGE_CURVE('',#41492,#41493,#22462,.T.);
#54376=EDGE_CURVE('',#41493,#41494,#29870,.T.);
#54377=EDGE_CURVE('',#41494,#41495,#25955,.T.);
#54378=EDGE_CURVE('',#41495,#41496,#29871,.T.);
#54379=EDGE_CURVE('',#41496,#41497,#22463,.T.);
#54380=EDGE_CURVE('',#41497,#41498,#29872,.T.);
#54381=EDGE_CURVE('',#41498,#41499,#25956,.T.);
#54382=EDGE_CURVE('',#41499,#41500,#29873,.T.);
#54383=EDGE_CURVE('',#41500,#41501,#22464,.T.);
#54384=EDGE_CURVE('',#41501,#41502,#29874,.T.);
#54385=EDGE_CURVE('',#41502,#41503,#25957,.T.);
#54386=EDGE_CURVE('',#41503,#41504,#29875,.T.);
#54387=EDGE_CURVE('',#41504,#41505,#22465,.T.);
#54388=EDGE_CURVE('',#41505,#41506,#29876,.T.);
#54389=EDGE_CURVE('',#41506,#41507,#25958,.T.);
#54390=EDGE_CURVE('',#41507,#41508,#29877,.T.);
#54391=EDGE_CURVE('',#41508,#41509,#22466,.T.);
#54392=EDGE_CURVE('',#41509,#41510,#29878,.T.);
#54393=EDGE_CURVE('',#41510,#41511,#25959,.T.);
#54394=EDGE_CURVE('',#41511,#41512,#29879,.T.);
#54395=EDGE_CURVE('',#41512,#41513,#22467,.T.);
#54396=EDGE_CURVE('',#41513,#41514,#29880,.T.);
#54397=EDGE_CURVE('',#41514,#41515,#25960,.T.);
#54398=EDGE_CURVE('',#41515,#41516,#29881,.T.);
#54399=EDGE_CURVE('',#41516,#41517,#22468,.T.);
#54400=EDGE_CURVE('',#41517,#41518,#29882,.T.);
#54401=EDGE_CURVE('',#41518,#41519,#25961,.T.);
#54402=EDGE_CURVE('',#41519,#41520,#29883,.T.);
#54403=EDGE_CURVE('',#41520,#41521,#22469,.T.);
#54404=EDGE_CURVE('',#41521,#41522,#29884,.T.);
#54405=EDGE_CURVE('',#41522,#41523,#25962,.T.);
#54406=EDGE_CURVE('',#41523,#41524,#29885,.T.);
#54407=EDGE_CURVE('',#41524,#41525,#22470,.T.);
#54408=EDGE_CURVE('',#41525,#41526,#29886,.T.);
#54409=EDGE_CURVE('',#41526,#41527,#25963,.T.);
#54410=EDGE_CURVE('',#41527,#41528,#29887,.T.);
#54411=EDGE_CURVE('',#41528,#41529,#22471,.T.);
#54412=EDGE_CURVE('',#41529,#41530,#29888,.T.);
#54413=EDGE_CURVE('',#41530,#41531,#25964,.T.);
#54414=EDGE_CURVE('',#41531,#41532,#29889,.T.);
#54415=EDGE_CURVE('',#41532,#41533,#22472,.T.);
#54416=EDGE_CURVE('',#41533,#41534,#29890,.T.);
#54417=EDGE_CURVE('',#41534,#41535,#25965,.T.);
#54418=EDGE_CURVE('',#41535,#41536,#29891,.T.);
#54419=EDGE_CURVE('',#41536,#41537,#22473,.T.);
#54420=EDGE_CURVE('',#41537,#41538,#29892,.T.);
#54421=EDGE_CURVE('',#41538,#41539,#25966,.T.);
#54422=EDGE_CURVE('',#41539,#41540,#29893,.T.);
#54423=EDGE_CURVE('',#41540,#41541,#22474,.T.);
#54424=EDGE_CURVE('',#41541,#41542,#29894,.T.);
#54425=EDGE_CURVE('',#41542,#41543,#25967,.T.);
#54426=EDGE_CURVE('',#41543,#41544,#29895,.T.);
#54427=EDGE_CURVE('',#41544,#41545,#22475,.T.);
#54428=EDGE_CURVE('',#41545,#41546,#29896,.T.);
#54429=EDGE_CURVE('',#41546,#41547,#25968,.T.);
#54430=EDGE_CURVE('',#41547,#41548,#29897,.T.);
#54431=EDGE_CURVE('',#41548,#41549,#22476,.T.);
#54432=EDGE_CURVE('',#41549,#41550,#29898,.T.);
#54433=EDGE_CURVE('',#41550,#41551,#25969,.T.);
#54434=EDGE_CURVE('',#41551,#41552,#29899,.T.);
#54435=EDGE_CURVE('',#41552,#41553,#22477,.T.);
#54436=EDGE_CURVE('',#41553,#41554,#29900,.T.);
#54437=EDGE_CURVE('',#41554,#41555,#25970,.T.);
#54438=EDGE_CURVE('',#41555,#41556,#29901,.T.);
#54439=EDGE_CURVE('',#41556,#41557,#22478,.T.);
#54440=EDGE_CURVE('',#41557,#41558,#29902,.T.);
#54441=EDGE_CURVE('',#41559,#41558,#22479,.T.);
#54442=EDGE_CURVE('',#41558,#41559,#22480,.T.);
#54443=EDGE_CURVE('',#41557,#41560,#22481,.T.);
#54444=EDGE_CURVE('',#41560,#41561,#29903,.T.);
#54445=EDGE_CURVE('',#41561,#41562,#25971,.T.);
#54446=EDGE_CURVE('',#41562,#41563,#29904,.T.);
#54447=EDGE_CURVE('',#41563,#41564,#22482,.T.);
#54448=EDGE_CURVE('',#41564,#41565,#29905,.T.);
#54449=EDGE_CURVE('',#41565,#41566,#25972,.T.);
#54450=EDGE_CURVE('',#41566,#41567,#29906,.T.);
#54451=EDGE_CURVE('',#41567,#41568,#22483,.T.);
#54452=EDGE_CURVE('',#41568,#41569,#29907,.T.);
#54453=EDGE_CURVE('',#41569,#41570,#25973,.T.);
#54454=EDGE_CURVE('',#41570,#41571,#29908,.T.);
#54455=EDGE_CURVE('',#41571,#41572,#22484,.T.);
#54456=EDGE_CURVE('',#41572,#41573,#29909,.T.);
#54457=EDGE_CURVE('',#41573,#41574,#25974,.T.);
#54458=EDGE_CURVE('',#41574,#41575,#29910,.T.);
#54459=EDGE_CURVE('',#41575,#41576,#22485,.T.);
#54460=EDGE_CURVE('',#41576,#41577,#29911,.T.);
#54461=EDGE_CURVE('',#41577,#41578,#25975,.T.);
#54462=EDGE_CURVE('',#41578,#41579,#29912,.T.);
#54463=EDGE_CURVE('',#41579,#41580,#22486,.T.);
#54464=EDGE_CURVE('',#41580,#41581,#29913,.T.);
#54465=EDGE_CURVE('',#41581,#41582,#25976,.T.);
#54466=EDGE_CURVE('',#41582,#41583,#29914,.T.);
#54467=EDGE_CURVE('',#41583,#41584,#22487,.T.);
#54468=EDGE_CURVE('',#41584,#41585,#29915,.T.);
#54469=EDGE_CURVE('',#41585,#41586,#25977,.T.);
#54470=EDGE_CURVE('',#41586,#41587,#29916,.T.);
#54471=EDGE_CURVE('',#41587,#41588,#22488,.T.);
#54472=EDGE_CURVE('',#41588,#41589,#29917,.T.);
#54473=EDGE_CURVE('',#41589,#41590,#25978,.T.);
#54474=EDGE_CURVE('',#41590,#41591,#29918,.T.);
#54475=EDGE_CURVE('',#41591,#41592,#22489,.T.);
#54476=EDGE_CURVE('',#41592,#41593,#29919,.T.);
#54477=EDGE_CURVE('',#41593,#41594,#25979,.T.);
#54478=EDGE_CURVE('',#41594,#41595,#29920,.T.);
#54479=EDGE_CURVE('',#41595,#41596,#22490,.T.);
#54480=EDGE_CURVE('',#41596,#41597,#29921,.T.);
#54481=EDGE_CURVE('',#41597,#41598,#25980,.T.);
#54482=EDGE_CURVE('',#41598,#41599,#29922,.T.);
#54483=EDGE_CURVE('',#41599,#41600,#22491,.T.);
#54484=EDGE_CURVE('',#41600,#41601,#29923,.T.);
#54485=EDGE_CURVE('',#41601,#41602,#25981,.T.);
#54486=EDGE_CURVE('',#41602,#41603,#29924,.T.);
#54487=EDGE_CURVE('',#41603,#41604,#22492,.T.);
#54488=EDGE_CURVE('',#41604,#41605,#29925,.T.);
#54489=EDGE_CURVE('',#41605,#41606,#25982,.T.);
#54490=EDGE_CURVE('',#41606,#41607,#29926,.T.);
#54491=EDGE_CURVE('',#41607,#41608,#22493,.T.);
#54492=EDGE_CURVE('',#41608,#41609,#29927,.T.);
#54493=EDGE_CURVE('',#41609,#41610,#25983,.T.);
#54494=EDGE_CURVE('',#41610,#41611,#29928,.T.);
#54495=EDGE_CURVE('',#41611,#41612,#22494,.T.);
#54496=EDGE_CURVE('',#41612,#41613,#29929,.T.);
#54497=EDGE_CURVE('',#41613,#41614,#25984,.T.);
#54498=EDGE_CURVE('',#41614,#41615,#29930,.T.);
#54499=EDGE_CURVE('',#41615,#41616,#22495,.T.);
#54500=EDGE_CURVE('',#41616,#41617,#29931,.T.);
#54501=EDGE_CURVE('',#41617,#41618,#25985,.T.);
#54502=EDGE_CURVE('',#41618,#41619,#29932,.T.);
#54503=EDGE_CURVE('',#41619,#41620,#22496,.T.);
#54504=EDGE_CURVE('',#41620,#41621,#29933,.T.);
#54505=EDGE_CURVE('',#41621,#41622,#25986,.T.);
#54506=EDGE_CURVE('',#41622,#41623,#29934,.T.);
#54507=EDGE_CURVE('',#41623,#41624,#22497,.T.);
#54508=EDGE_CURVE('',#41624,#41625,#29935,.T.);
#54509=EDGE_CURVE('',#41625,#41626,#25987,.T.);
#54510=EDGE_CURVE('',#41626,#41627,#29936,.T.);
#54511=EDGE_CURVE('',#41627,#41628,#22498,.T.);
#54512=EDGE_CURVE('',#41628,#41629,#29937,.T.);
#54513=EDGE_CURVE('',#41629,#41630,#25988,.T.);
#54514=EDGE_CURVE('',#41630,#41631,#29938,.T.);
#54515=EDGE_CURVE('',#41631,#41632,#22499,.T.);
#54516=EDGE_CURVE('',#41632,#41633,#29939,.T.);
#54517=EDGE_CURVE('',#41633,#41634,#25989,.T.);
#54518=EDGE_CURVE('',#41634,#41635,#29940,.T.);
#54519=EDGE_CURVE('',#41635,#41636,#22500,.T.);
#54520=EDGE_CURVE('',#41636,#41637,#29941,.T.);
#54521=EDGE_CURVE('',#41637,#41638,#25990,.T.);
#54522=EDGE_CURVE('',#41638,#41639,#29942,.T.);
#54523=EDGE_CURVE('',#41639,#41640,#22501,.T.);
#54524=EDGE_CURVE('',#41640,#41641,#29943,.T.);
#54525=EDGE_CURVE('',#41641,#41642,#25991,.T.);
#54526=EDGE_CURVE('',#41642,#41643,#29944,.T.);
#54527=EDGE_CURVE('',#41643,#41644,#22502,.T.);
#54528=EDGE_CURVE('',#41644,#41645,#29945,.T.);
#54529=EDGE_CURVE('',#41645,#41646,#25992,.T.);
#54530=EDGE_CURVE('',#41646,#41647,#29946,.T.);
#54531=EDGE_CURVE('',#41647,#41648,#22503,.T.);
#54532=EDGE_CURVE('',#41648,#41649,#29947,.T.);
#54533=EDGE_CURVE('',#41649,#41650,#25993,.T.);
#54534=EDGE_CURVE('',#41650,#41651,#29948,.T.);
#54535=EDGE_CURVE('',#41651,#41652,#22504,.T.);
#54536=EDGE_CURVE('',#41652,#41653,#29949,.T.);
#54537=EDGE_CURVE('',#41653,#41654,#25994,.T.);
#54538=EDGE_CURVE('',#41654,#41655,#29950,.T.);
#54539=EDGE_CURVE('',#41655,#41656,#22505,.T.);
#54540=EDGE_CURVE('',#41656,#41657,#29951,.T.);
#54541=EDGE_CURVE('',#41657,#41658,#25995,.T.);
#54542=EDGE_CURVE('',#41658,#41659,#29952,.T.);
#54543=EDGE_CURVE('',#41659,#41660,#22506,.T.);
#54544=EDGE_CURVE('',#41660,#41661,#29953,.T.);
#54545=EDGE_CURVE('',#41661,#41662,#25996,.T.);
#54546=EDGE_CURVE('',#41662,#41663,#29954,.T.);
#54547=EDGE_CURVE('',#41663,#41664,#22507,.T.);
#54548=EDGE_CURVE('',#41664,#41665,#29955,.T.);
#54549=EDGE_CURVE('',#41665,#41666,#25997,.T.);
#54550=EDGE_CURVE('',#41666,#41667,#29956,.T.);
#54551=EDGE_CURVE('',#41667,#41668,#22508,.T.);
#54552=EDGE_CURVE('',#41668,#41669,#29957,.T.);
#54553=EDGE_CURVE('',#41669,#41670,#25998,.T.);
#54554=EDGE_CURVE('',#41670,#41671,#29958,.T.);
#54555=EDGE_CURVE('',#41671,#41672,#22509,.T.);
#54556=EDGE_CURVE('',#41672,#41673,#29959,.T.);
#54557=EDGE_CURVE('',#41673,#41674,#25999,.T.);
#54558=EDGE_CURVE('',#41674,#41675,#29960,.T.);
#54559=EDGE_CURVE('',#41675,#41676,#22510,.T.);
#54560=EDGE_CURVE('',#41676,#41677,#29961,.T.);
#54561=EDGE_CURVE('',#41677,#41678,#26000,.T.);
#54562=EDGE_CURVE('',#41678,#41679,#29962,.T.);
#54563=EDGE_CURVE('',#41679,#41680,#22511,.T.);
#54564=EDGE_CURVE('',#41680,#41681,#29963,.T.);
#54565=EDGE_CURVE('',#41681,#41682,#26001,.T.);
#54566=EDGE_CURVE('',#41682,#41683,#29964,.T.);
#54567=EDGE_CURVE('',#41683,#41684,#22512,.T.);
#54568=EDGE_CURVE('',#41684,#41685,#29965,.T.);
#54569=EDGE_CURVE('',#41685,#41686,#26002,.T.);
#54570=EDGE_CURVE('',#41686,#41687,#29966,.T.);
#54571=EDGE_CURVE('',#41687,#41688,#22513,.T.);
#54572=EDGE_CURVE('',#41688,#41689,#29967,.T.);
#54573=EDGE_CURVE('',#41689,#41690,#26003,.T.);
#54574=EDGE_CURVE('',#41690,#41691,#29968,.T.);
#54575=EDGE_CURVE('',#41691,#41692,#22514,.T.);
#54576=EDGE_CURVE('',#41692,#41693,#29969,.T.);
#54577=EDGE_CURVE('',#41693,#41694,#26004,.T.);
#54578=EDGE_CURVE('',#41694,#41695,#29970,.T.);
#54579=EDGE_CURVE('',#41695,#41696,#22515,.T.);
#54580=EDGE_CURVE('',#41696,#41697,#29971,.T.);
#54581=EDGE_CURVE('',#41697,#41698,#26005,.T.);
#54582=EDGE_CURVE('',#41698,#41699,#29972,.T.);
#54583=EDGE_CURVE('',#41699,#41700,#22516,.T.);
#54584=EDGE_CURVE('',#41700,#41701,#29973,.T.);
#54585=EDGE_CURVE('',#41701,#41702,#26006,.T.);
#54586=EDGE_CURVE('',#41702,#41703,#29974,.T.);
#54587=EDGE_CURVE('',#41703,#41704,#22517,.T.);
#54588=EDGE_CURVE('',#41704,#41705,#29975,.T.);
#54589=EDGE_CURVE('',#41705,#41706,#26007,.T.);
#54590=EDGE_CURVE('',#41706,#41707,#29976,.T.);
#54591=EDGE_CURVE('',#41707,#41708,#22518,.T.);
#54592=EDGE_CURVE('',#41708,#41709,#29977,.T.);
#54593=EDGE_CURVE('',#41709,#41710,#26008,.T.);
#54594=EDGE_CURVE('',#41710,#41711,#29978,.T.);
#54595=EDGE_CURVE('',#41711,#41712,#22519,.T.);
#54596=EDGE_CURVE('',#41712,#41713,#29979,.T.);
#54597=EDGE_CURVE('',#41713,#41402,#26009,.T.);
#54598=EDGE_CURVE('',#41714,#41714,#22520,.T.);
#54599=EDGE_CURVE('',#41714,#41559,#22521,.T.);
#54600=EDGE_CURVE('',#41715,#41716,#22522,.T.);
#54601=EDGE_CURVE('',#41715,#41717,#29980,.T.);
#54602=EDGE_CURVE('',#41190,#41717,#26010,.T.);
#54603=EDGE_CURVE('',#41718,#41189,#26011,.T.);
#54604=EDGE_CURVE('',#41718,#41719,#29981,.T.);
#54605=EDGE_CURVE('',#41720,#41719,#22523,.T.);
#54606=EDGE_CURVE('',#41720,#41721,#29982,.T.);
#54607=EDGE_CURVE('',#41194,#41721,#26012,.T.);
#54608=EDGE_CURVE('',#41722,#41193,#26013,.T.);
#54609=EDGE_CURVE('',#41722,#41723,#29983,.T.);
#54610=EDGE_CURVE('',#41724,#41723,#22524,.T.);
#54611=EDGE_CURVE('',#41724,#41725,#29984,.T.);
#54612=EDGE_CURVE('',#41198,#41725,#26014,.T.);
#54613=EDGE_CURVE('',#41726,#41197,#26015,.T.);
#54614=EDGE_CURVE('',#41726,#41727,#29985,.T.);
#54615=EDGE_CURVE('',#41728,#41727,#22525,.T.);
#54616=EDGE_CURVE('',#41728,#41729,#29986,.T.);
#54617=EDGE_CURVE('',#41202,#41729,#26016,.T.);
#54618=EDGE_CURVE('',#41730,#41201,#26017,.T.);
#54619=EDGE_CURVE('',#41730,#41731,#29987,.T.);
#54620=EDGE_CURVE('',#41732,#41731,#22526,.T.);
#54621=EDGE_CURVE('',#41732,#41733,#29988,.T.);
#54622=EDGE_CURVE('',#41206,#41733,#26018,.T.);
#54623=EDGE_CURVE('',#41734,#41205,#26019,.T.);
#54624=EDGE_CURVE('',#41734,#41735,#29989,.T.);
#54625=EDGE_CURVE('',#41736,#41735,#22527,.T.);
#54626=EDGE_CURVE('',#41736,#41737,#29990,.T.);
#54627=EDGE_CURVE('',#41210,#41737,#26020,.T.);
#54628=EDGE_CURVE('',#41738,#41209,#26021,.T.);
#54629=EDGE_CURVE('',#41738,#41739,#29991,.T.);
#54630=EDGE_CURVE('',#41740,#41739,#22528,.T.);
#54631=EDGE_CURVE('',#41740,#41741,#29992,.T.);
#54632=EDGE_CURVE('',#41214,#41741,#26022,.T.);
#54633=EDGE_CURVE('',#41742,#41213,#26023,.T.);
#54634=EDGE_CURVE('',#41742,#41743,#29993,.T.);
#54635=EDGE_CURVE('',#41744,#41743,#22529,.T.);
#54636=EDGE_CURVE('',#41744,#41745,#29994,.T.);
#54637=EDGE_CURVE('',#41218,#41745,#26024,.T.);
#54638=EDGE_CURVE('',#41746,#41217,#26025,.T.);
#54639=EDGE_CURVE('',#41746,#41747,#29995,.T.);
#54640=EDGE_CURVE('',#41748,#41747,#22530,.T.);
#54641=EDGE_CURVE('',#41748,#41749,#29996,.T.);
#54642=EDGE_CURVE('',#41222,#41749,#26026,.T.);
#54643=EDGE_CURVE('',#41750,#41221,#26027,.T.);
#54644=EDGE_CURVE('',#41750,#41751,#29997,.T.);
#54645=EDGE_CURVE('',#41752,#41751,#22531,.T.);
#54646=EDGE_CURVE('',#41752,#41753,#29998,.T.);
#54647=EDGE_CURVE('',#41226,#41753,#26028,.T.);
#54648=EDGE_CURVE('',#41754,#41225,#26029,.T.);
#54649=EDGE_CURVE('',#41754,#41755,#29999,.T.);
#54650=EDGE_CURVE('',#41756,#41755,#22532,.T.);
#54651=EDGE_CURVE('',#41756,#41757,#30000,.T.);
#54652=EDGE_CURVE('',#41230,#41757,#26030,.T.);
#54653=EDGE_CURVE('',#41758,#41229,#26031,.T.);
#54654=EDGE_CURVE('',#41758,#41759,#30001,.T.);
#54655=EDGE_CURVE('',#41760,#41759,#22533,.T.);
#54656=EDGE_CURVE('',#41760,#41761,#30002,.T.);
#54657=EDGE_CURVE('',#41234,#41761,#26032,.T.);
#54658=EDGE_CURVE('',#41762,#41233,#26033,.T.);
#54659=EDGE_CURVE('',#41762,#41763,#30003,.T.);
#54660=EDGE_CURVE('',#41764,#41763,#22534,.T.);
#54661=EDGE_CURVE('',#41764,#41765,#30004,.T.);
#54662=EDGE_CURVE('',#41238,#41765,#26034,.T.);
#54663=EDGE_CURVE('',#41766,#41237,#26035,.T.);
#54664=EDGE_CURVE('',#41766,#41767,#30005,.T.);
#54665=EDGE_CURVE('',#41768,#41767,#22535,.T.);
#54666=EDGE_CURVE('',#41768,#41769,#30006,.T.);
#54667=EDGE_CURVE('',#41242,#41769,#26036,.T.);
#54668=EDGE_CURVE('',#41770,#41241,#26037,.T.);
#54669=EDGE_CURVE('',#41770,#41771,#30007,.T.);
#54670=EDGE_CURVE('',#41772,#41771,#22536,.T.);
#54671=EDGE_CURVE('',#41772,#41773,#30008,.T.);
#54672=EDGE_CURVE('',#41246,#41773,#26038,.T.);
#54673=EDGE_CURVE('',#41774,#41245,#26039,.T.);
#54674=EDGE_CURVE('',#41774,#41775,#30009,.T.);
#54675=EDGE_CURVE('',#41776,#41775,#22537,.T.);
#54676=EDGE_CURVE('',#41776,#41777,#30010,.T.);
#54677=EDGE_CURVE('',#41250,#41777,#26040,.T.);
#54678=EDGE_CURVE('',#41778,#41249,#26041,.T.);
#54679=EDGE_CURVE('',#41778,#41779,#30011,.T.);
#54680=EDGE_CURVE('',#41780,#41779,#22538,.T.);
#54681=EDGE_CURVE('',#41780,#41781,#30012,.T.);
#54682=EDGE_CURVE('',#41254,#41781,#26042,.T.);
#54683=EDGE_CURVE('',#41782,#41253,#26043,.T.);
#54684=EDGE_CURVE('',#41782,#41783,#30013,.T.);
#54685=EDGE_CURVE('',#41784,#41783,#22539,.T.);
#54686=EDGE_CURVE('',#41784,#41785,#30014,.T.);
#54687=EDGE_CURVE('',#41258,#41785,#26044,.T.);
#54688=EDGE_CURVE('',#41786,#41257,#26045,.T.);
#54689=EDGE_CURVE('',#41786,#41787,#30015,.T.);
#54690=EDGE_CURVE('',#41788,#41787,#22540,.T.);
#54691=EDGE_CURVE('',#41788,#41789,#30016,.T.);
#54692=EDGE_CURVE('',#41262,#41789,#26046,.T.);
#54693=EDGE_CURVE('',#41790,#41261,#26047,.T.);
#54694=EDGE_CURVE('',#41790,#41791,#30017,.T.);
#54695=EDGE_CURVE('',#41792,#41791,#22541,.T.);
#54696=EDGE_CURVE('',#41792,#41793,#30018,.T.);
#54697=EDGE_CURVE('',#41266,#41793,#26048,.T.);
#54698=EDGE_CURVE('',#41794,#41265,#26049,.T.);
#54699=EDGE_CURVE('',#41794,#41795,#30019,.T.);
#54700=EDGE_CURVE('',#41796,#41795,#22542,.T.);
#54701=EDGE_CURVE('',#41796,#41797,#30020,.T.);
#54702=EDGE_CURVE('',#41270,#41797,#26050,.T.);
#54703=EDGE_CURVE('',#41798,#41269,#26051,.T.);
#54704=EDGE_CURVE('',#41798,#41799,#30021,.T.);
#54705=EDGE_CURVE('',#41800,#41799,#22543,.T.);
#54706=EDGE_CURVE('',#41800,#41801,#30022,.T.);
#54707=EDGE_CURVE('',#41274,#41801,#26052,.T.);
#54708=EDGE_CURVE('',#41802,#41273,#26053,.T.);
#54709=EDGE_CURVE('',#41802,#41803,#30023,.T.);
#54710=EDGE_CURVE('',#41804,#41803,#22544,.T.);
#54711=EDGE_CURVE('',#41804,#41805,#30024,.T.);
#54712=EDGE_CURVE('',#41278,#41805,#26054,.T.);
#54713=EDGE_CURVE('',#41806,#41277,#26055,.T.);
#54714=EDGE_CURVE('',#41806,#41807,#30025,.T.);
#54715=EDGE_CURVE('',#41808,#41807,#22545,.T.);
#54716=EDGE_CURVE('',#41808,#41809,#30026,.T.);
#54717=EDGE_CURVE('',#41282,#41809,#26056,.T.);
#54718=EDGE_CURVE('',#41810,#41281,#26057,.T.);
#54719=EDGE_CURVE('',#41810,#41811,#30027,.T.);
#54720=EDGE_CURVE('',#41812,#41811,#22546,.T.);
#54721=EDGE_CURVE('',#41812,#41813,#30028,.T.);
#54722=EDGE_CURVE('',#41286,#41813,#26058,.T.);
#54723=EDGE_CURVE('',#41814,#41285,#26059,.T.);
#54724=EDGE_CURVE('',#41814,#41815,#30029,.T.);
#54725=EDGE_CURVE('',#41816,#41815,#22547,.T.);
#54726=EDGE_CURVE('',#41816,#41817,#30030,.T.);
#54727=EDGE_CURVE('',#41290,#41817,#26060,.T.);
#54728=EDGE_CURVE('',#41818,#41289,#26061,.T.);
#54729=EDGE_CURVE('',#41818,#41819,#30031,.T.);
#54730=EDGE_CURVE('',#41820,#41819,#22548,.T.);
#54731=EDGE_CURVE('',#41820,#41821,#30032,.T.);
#54732=EDGE_CURVE('',#41294,#41821,#26062,.T.);
#54733=EDGE_CURVE('',#41822,#41293,#26063,.T.);
#54734=EDGE_CURVE('',#41822,#41823,#30033,.T.);
#54735=EDGE_CURVE('',#41824,#41823,#22549,.T.);
#54736=EDGE_CURVE('',#41824,#41825,#30034,.T.);
#54737=EDGE_CURVE('',#41298,#41825,#26064,.T.);
#54738=EDGE_CURVE('',#41826,#41297,#26065,.T.);
#54739=EDGE_CURVE('',#41826,#41827,#30035,.T.);
#54740=EDGE_CURVE('',#41828,#41827,#22550,.T.);
#54741=EDGE_CURVE('',#41828,#41829,#30036,.T.);
#54742=EDGE_CURVE('',#41302,#41829,#26066,.T.);
#54743=EDGE_CURVE('',#41830,#41301,#26067,.T.);
#54744=EDGE_CURVE('',#41830,#41831,#30037,.T.);
#54745=EDGE_CURVE('',#41832,#41831,#22551,.T.);
#54746=EDGE_CURVE('',#41832,#41833,#30038,.T.);
#54747=EDGE_CURVE('',#41306,#41833,#26068,.T.);
#54748=EDGE_CURVE('',#41834,#41305,#26069,.T.);
#54749=EDGE_CURVE('',#41834,#41835,#30039,.T.);
#54750=EDGE_CURVE('',#41836,#41835,#22552,.T.);
#54751=EDGE_CURVE('',#41836,#41837,#30040,.T.);
#54752=EDGE_CURVE('',#41310,#41837,#26070,.T.);
#54753=EDGE_CURVE('',#41838,#41309,#26071,.T.);
#54754=EDGE_CURVE('',#41838,#41839,#30041,.T.);
#54755=EDGE_CURVE('',#41840,#41839,#22553,.T.);
#54756=EDGE_CURVE('',#41840,#41841,#30042,.T.);
#54757=EDGE_CURVE('',#41314,#41841,#26072,.T.);
#54758=EDGE_CURVE('',#41842,#41313,#26073,.T.);
#54759=EDGE_CURVE('',#41842,#41843,#30043,.T.);
#54760=EDGE_CURVE('',#41844,#41843,#22554,.T.);
#54761=EDGE_CURVE('',#41844,#41845,#30044,.T.);
#54762=EDGE_CURVE('',#41318,#41845,#26074,.T.);
#54763=EDGE_CURVE('',#41846,#41317,#26075,.T.);
#54764=EDGE_CURVE('',#41846,#41847,#30045,.T.);
#54765=EDGE_CURVE('',#41848,#41847,#22555,.T.);
#54766=EDGE_CURVE('',#41848,#41849,#30046,.T.);
#54767=EDGE_CURVE('',#41322,#41849,#26076,.T.);
#54768=EDGE_CURVE('',#41850,#41321,#26077,.T.);
#54769=EDGE_CURVE('',#41850,#41851,#30047,.T.);
#54770=EDGE_CURVE('',#41852,#41851,#22556,.T.);
#54771=EDGE_CURVE('',#41852,#41853,#30048,.T.);
#54772=EDGE_CURVE('',#41326,#41853,#26078,.T.);
#54773=EDGE_CURVE('',#41854,#41325,#26079,.T.);
#54774=EDGE_CURVE('',#41854,#41855,#30049,.T.);
#54775=EDGE_CURVE('',#41856,#41855,#22557,.T.);
#54776=EDGE_CURVE('',#41856,#41857,#30050,.T.);
#54777=EDGE_CURVE('',#41330,#41857,#26080,.T.);
#54778=EDGE_CURVE('',#41858,#41329,#26081,.T.);
#54779=EDGE_CURVE('',#41858,#41859,#30051,.T.);
#54780=EDGE_CURVE('',#41860,#41859,#22558,.T.);
#54781=EDGE_CURVE('',#41860,#41861,#30052,.T.);
#54782=EDGE_CURVE('',#41334,#41861,#26082,.T.);
#54783=EDGE_CURVE('',#41862,#41333,#26083,.T.);
#54784=EDGE_CURVE('',#41862,#41863,#30053,.T.);
#54785=EDGE_CURVE('',#41864,#41863,#22559,.T.);
#54786=EDGE_CURVE('',#41864,#41865,#30054,.T.);
#54787=EDGE_CURVE('',#41382,#41865,#26084,.T.);
#54788=EDGE_CURVE('',#41866,#41381,#26085,.T.);
#54789=EDGE_CURVE('',#41866,#41867,#30055,.T.);
#54790=EDGE_CURVE('',#41868,#41867,#22560,.T.);
#54791=EDGE_CURVE('',#41868,#41869,#30056,.T.);
#54792=EDGE_CURVE('',#41387,#41869,#26086,.T.);
#54793=EDGE_CURVE('',#41386,#41401,#30057,.T.);
#54794=EDGE_CURVE('',#41870,#41385,#26087,.T.);
#54795=EDGE_CURVE('',#41870,#41871,#30058,.T.);
#54796=EDGE_CURVE('',#41872,#41871,#22561,.T.);
#54797=EDGE_CURVE('',#41872,#41873,#30059,.T.);
#54798=EDGE_CURVE('',#41378,#41873,#26088,.T.);
#54799=EDGE_CURVE('',#41874,#41377,#26089,.T.);
#54800=EDGE_CURVE('',#41874,#41875,#30060,.T.);
#54801=EDGE_CURVE('',#41876,#41875,#22562,.T.);
#54802=EDGE_CURVE('',#41876,#41877,#30061,.T.);
#54803=EDGE_CURVE('',#41374,#41877,#26090,.T.);
#54804=EDGE_CURVE('',#41878,#41373,#26091,.T.);
#54805=EDGE_CURVE('',#41878,#41879,#30062,.T.);
#54806=EDGE_CURVE('',#41880,#41879,#22563,.T.);
#54807=EDGE_CURVE('',#41880,#41881,#30063,.T.);
#54808=EDGE_CURVE('',#41370,#41881,#26092,.T.);
#54809=EDGE_CURVE('',#41882,#41369,#26093,.T.);
#54810=EDGE_CURVE('',#41882,#41883,#30064,.T.);
#54811=EDGE_CURVE('',#41884,#41883,#22564,.T.);
#54812=EDGE_CURVE('',#41884,#41885,#30065,.T.);
#54813=EDGE_CURVE('',#41366,#41885,#26094,.T.);
#54814=EDGE_CURVE('',#41886,#41365,#26095,.T.);
#54815=EDGE_CURVE('',#41886,#41887,#30066,.T.);
#54816=EDGE_CURVE('',#41888,#41887,#22565,.T.);
#54817=EDGE_CURVE('',#41888,#41889,#30067,.T.);
#54818=EDGE_CURVE('',#41362,#41889,#26096,.T.);
#54819=EDGE_CURVE('',#41890,#41361,#26097,.T.);
#54820=EDGE_CURVE('',#41890,#41891,#30068,.T.);
#54821=EDGE_CURVE('',#41892,#41891,#22566,.T.);
#54822=EDGE_CURVE('',#41892,#41893,#30069,.T.);
#54823=EDGE_CURVE('',#41358,#41893,#26098,.T.);
#54824=EDGE_CURVE('',#41894,#41357,#26099,.T.);
#54825=EDGE_CURVE('',#41894,#41895,#30070,.T.);
#54826=EDGE_CURVE('',#41896,#41895,#22567,.T.);
#54827=EDGE_CURVE('',#41896,#41897,#30071,.T.);
#54828=EDGE_CURVE('',#41354,#41897,#26100,.T.);
#54829=EDGE_CURVE('',#41898,#41353,#26101,.T.);
#54830=EDGE_CURVE('',#41898,#41899,#30072,.T.);
#54831=EDGE_CURVE('',#41900,#41899,#22568,.T.);
#54832=EDGE_CURVE('',#41900,#41901,#30073,.T.);
#54833=EDGE_CURVE('',#41350,#41901,#26102,.T.);
#54834=EDGE_CURVE('',#41902,#41349,#26103,.T.);
#54835=EDGE_CURVE('',#41902,#41903,#30074,.T.);
#54836=EDGE_CURVE('',#41904,#41903,#22569,.T.);
#54837=EDGE_CURVE('',#41904,#41905,#30075,.T.);
#54838=EDGE_CURVE('',#41346,#41905,#26104,.T.);
#54839=EDGE_CURVE('',#41906,#41345,#26105,.T.);
#54840=EDGE_CURVE('',#41906,#41907,#30076,.T.);
#54841=EDGE_CURVE('',#41908,#41907,#22570,.T.);
#54842=EDGE_CURVE('',#41908,#41909,#30077,.T.);
#54843=EDGE_CURVE('',#41342,#41909,#26106,.T.);
#54844=EDGE_CURVE('',#41910,#41341,#26107,.T.);
#54845=EDGE_CURVE('',#41910,#41911,#30078,.T.);
#54846=EDGE_CURVE('',#41912,#41911,#22571,.T.);
#54847=EDGE_CURVE('',#41912,#41913,#30079,.T.);
#54848=EDGE_CURVE('',#41338,#41913,#26108,.T.);
#54849=EDGE_CURVE('',#41914,#41337,#26109,.T.);
#54850=EDGE_CURVE('',#41914,#41915,#30080,.T.);
#54851=EDGE_CURVE('',#41916,#41915,#22572,.T.);
#54852=EDGE_CURVE('',#41916,#41917,#30081,.T.);
#54853=EDGE_CURVE('',#41082,#41917,#26110,.T.);
#54854=EDGE_CURVE('',#41918,#41081,#26111,.T.);
#54855=EDGE_CURVE('',#41918,#41919,#30082,.T.);
#54856=EDGE_CURVE('',#41920,#41919,#22573,.T.);
#54857=EDGE_CURVE('',#41920,#41921,#30083,.T.);
#54858=EDGE_CURVE('',#41086,#41921,#26112,.T.);
#54859=EDGE_CURVE('',#41922,#41085,#26113,.T.);
#54860=EDGE_CURVE('',#41922,#41923,#30084,.T.);
#54861=EDGE_CURVE('',#41924,#41923,#22574,.T.);
#54862=EDGE_CURVE('',#41924,#41925,#30085,.T.);
#54863=EDGE_CURVE('',#41090,#41925,#26114,.T.);
#54864=EDGE_CURVE('',#41926,#41089,#26115,.T.);
#54865=EDGE_CURVE('',#41926,#41927,#30086,.T.);
#54866=EDGE_CURVE('',#41928,#41927,#22575,.T.);
#54867=EDGE_CURVE('',#41928,#41929,#30087,.T.);
#54868=EDGE_CURVE('',#41094,#41929,#26116,.T.);
#54869=EDGE_CURVE('',#41930,#41093,#26117,.T.);
#54870=EDGE_CURVE('',#41930,#41931,#30088,.T.);
#54871=EDGE_CURVE('',#41932,#41931,#22576,.T.);
#54872=EDGE_CURVE('',#41932,#41933,#30089,.T.);
#54873=EDGE_CURVE('',#41098,#41933,#26118,.T.);
#54874=EDGE_CURVE('',#41934,#41097,#26119,.T.);
#54875=EDGE_CURVE('',#41934,#41935,#30090,.T.);
#54876=EDGE_CURVE('',#41936,#41935,#22577,.T.);
#54877=EDGE_CURVE('',#41936,#41937,#30091,.T.);
#54878=EDGE_CURVE('',#41102,#41937,#26120,.T.);
#54879=EDGE_CURVE('',#41938,#41101,#26121,.T.);
#54880=EDGE_CURVE('',#41938,#41939,#30092,.T.);
#54881=EDGE_CURVE('',#41940,#41939,#22578,.T.);
#54882=EDGE_CURVE('',#41940,#41941,#30093,.T.);
#54883=EDGE_CURVE('',#41106,#41941,#26122,.T.);
#54884=EDGE_CURVE('',#41942,#41105,#26123,.T.);
#54885=EDGE_CURVE('',#41942,#41943,#30094,.T.);
#54886=EDGE_CURVE('',#41944,#41943,#22579,.T.);
#54887=EDGE_CURVE('',#41944,#41945,#30095,.T.);
#54888=EDGE_CURVE('',#41110,#41945,#26124,.T.);
#54889=EDGE_CURVE('',#41946,#41109,#26125,.T.);
#54890=EDGE_CURVE('',#41946,#41947,#30096,.T.);
#54891=EDGE_CURVE('',#41948,#41947,#22580,.T.);
#54892=EDGE_CURVE('',#41948,#41949,#30097,.T.);
#54893=EDGE_CURVE('',#41114,#41949,#26126,.T.);
#54894=EDGE_CURVE('',#41950,#41113,#26127,.T.);
#54895=EDGE_CURVE('',#41950,#41951,#30098,.T.);
#54896=EDGE_CURVE('',#41952,#41951,#22581,.T.);
#54897=EDGE_CURVE('',#41952,#41953,#30099,.T.);
#54898=EDGE_CURVE('',#41118,#41953,#26128,.T.);
#54899=EDGE_CURVE('',#41954,#41117,#26129,.T.);
#54900=EDGE_CURVE('',#41954,#41955,#30100,.T.);
#54901=EDGE_CURVE('',#41956,#41955,#22582,.T.);
#54902=EDGE_CURVE('',#41956,#41957,#30101,.T.);
#54903=EDGE_CURVE('',#41122,#41957,#26130,.T.);
#54904=EDGE_CURVE('',#41958,#41121,#26131,.T.);
#54905=EDGE_CURVE('',#41958,#41959,#30102,.T.);
#54906=EDGE_CURVE('',#41960,#41959,#22583,.T.);
#54907=EDGE_CURVE('',#41960,#41961,#30103,.T.);
#54908=EDGE_CURVE('',#41126,#41961,#26132,.T.);
#54909=EDGE_CURVE('',#41962,#41125,#26133,.T.);
#54910=EDGE_CURVE('',#41962,#41963,#30104,.T.);
#54911=EDGE_CURVE('',#41964,#41963,#22584,.T.);
#54912=EDGE_CURVE('',#41964,#41965,#30105,.T.);
#54913=EDGE_CURVE('',#41130,#41965,#26134,.T.);
#54914=EDGE_CURVE('',#41966,#41129,#26135,.T.);
#54915=EDGE_CURVE('',#41966,#41967,#30106,.T.);
#54916=EDGE_CURVE('',#41968,#41967,#22585,.T.);
#54917=EDGE_CURVE('',#41968,#41969,#30107,.T.);
#54918=EDGE_CURVE('',#41134,#41969,#26136,.T.);
#54919=EDGE_CURVE('',#41970,#41133,#26137,.T.);
#54920=EDGE_CURVE('',#41970,#41971,#30108,.T.);
#54921=EDGE_CURVE('',#41972,#41971,#22586,.T.);
#54922=EDGE_CURVE('',#41972,#41973,#30109,.T.);
#54923=EDGE_CURVE('',#41138,#41973,#26138,.T.);
#54924=EDGE_CURVE('',#41974,#41137,#26139,.T.);
#54925=EDGE_CURVE('',#41974,#41975,#30110,.T.);
#54926=EDGE_CURVE('',#41976,#41975,#22587,.T.);
#54927=EDGE_CURVE('',#41976,#41977,#30111,.T.);
#54928=EDGE_CURVE('',#41142,#41977,#26140,.T.);
#54929=EDGE_CURVE('',#41978,#41141,#26141,.T.);
#54930=EDGE_CURVE('',#41978,#41979,#30112,.T.);
#54931=EDGE_CURVE('',#41980,#41979,#22588,.T.);
#54932=EDGE_CURVE('',#41980,#41981,#30113,.T.);
#54933=EDGE_CURVE('',#41146,#41981,#26142,.T.);
#54934=EDGE_CURVE('',#41982,#41145,#26143,.T.);
#54935=EDGE_CURVE('',#41982,#41983,#30114,.T.);
#54936=EDGE_CURVE('',#41984,#41983,#22589,.T.);
#54937=EDGE_CURVE('',#41984,#41985,#30115,.T.);
#54938=EDGE_CURVE('',#41150,#41985,#26144,.T.);
#54939=EDGE_CURVE('',#41986,#41149,#26145,.T.);
#54940=EDGE_CURVE('',#41986,#41987,#30116,.T.);
#54941=EDGE_CURVE('',#41988,#41987,#22590,.T.);
#54942=EDGE_CURVE('',#41988,#41989,#30117,.T.);
#54943=EDGE_CURVE('',#41154,#41989,#26146,.T.);
#54944=EDGE_CURVE('',#41990,#41153,#26147,.T.);
#54945=EDGE_CURVE('',#41990,#41991,#30118,.T.);
#54946=EDGE_CURVE('',#41992,#41991,#22591,.T.);
#54947=EDGE_CURVE('',#41992,#41993,#30119,.T.);
#54948=EDGE_CURVE('',#41158,#41993,#26148,.T.);
#54949=EDGE_CURVE('',#41994,#41157,#26149,.T.);
#54950=EDGE_CURVE('',#41994,#41995,#30120,.T.);
#54951=EDGE_CURVE('',#41996,#41995,#22592,.T.);
#54952=EDGE_CURVE('',#41996,#41997,#30121,.T.);
#54953=EDGE_CURVE('',#41162,#41997,#26150,.T.);
#54954=EDGE_CURVE('',#41998,#41161,#26151,.T.);
#54955=EDGE_CURVE('',#41998,#41999,#30122,.T.);
#54956=EDGE_CURVE('',#42000,#41999,#22593,.T.);
#54957=EDGE_CURVE('',#42000,#42001,#30123,.T.);
#54958=EDGE_CURVE('',#41166,#42001,#26152,.T.);
#54959=EDGE_CURVE('',#42002,#41165,#26153,.T.);
#54960=EDGE_CURVE('',#42002,#42003,#30124,.T.);
#54961=EDGE_CURVE('',#42004,#42003,#22594,.T.);
#54962=EDGE_CURVE('',#42004,#42005,#30125,.T.);
#54963=EDGE_CURVE('',#41170,#42005,#26154,.T.);
#54964=EDGE_CURVE('',#42006,#41169,#26155,.T.);
#54965=EDGE_CURVE('',#42006,#42007,#30126,.T.);
#54966=EDGE_CURVE('',#42008,#42007,#22595,.T.);
#54967=EDGE_CURVE('',#42008,#42009,#30127,.T.);
#54968=EDGE_CURVE('',#41174,#42009,#26156,.T.);
#54969=EDGE_CURVE('',#42010,#41173,#26157,.T.);
#54970=EDGE_CURVE('',#42010,#42011,#30128,.T.);
#54971=EDGE_CURVE('',#42012,#42011,#22596,.T.);
#54972=EDGE_CURVE('',#42012,#42013,#30129,.T.);
#54973=EDGE_CURVE('',#41178,#42013,#26158,.T.);
#54974=EDGE_CURVE('',#42014,#41177,#26159,.T.);
#54975=EDGE_CURVE('',#42014,#42015,#30130,.T.);
#54976=EDGE_CURVE('',#42016,#42015,#22597,.T.);
#54977=EDGE_CURVE('',#42016,#42017,#30131,.T.);
#54978=EDGE_CURVE('',#41182,#42017,#26160,.T.);
#54979=EDGE_CURVE('',#42018,#41181,#26161,.T.);
#54980=EDGE_CURVE('',#42018,#42019,#30132,.T.);
#54981=EDGE_CURVE('',#42020,#42019,#22598,.T.);
#54982=EDGE_CURVE('',#42020,#42021,#30133,.T.);
#54983=EDGE_CURVE('',#41186,#42021,#26162,.T.);
#54984=EDGE_CURVE('',#42022,#41185,#26163,.T.);
#54985=EDGE_CURVE('',#42022,#41716,#30134,.T.);
#54986=EDGE_CURVE('',#41716,#41560,#1080,.T.);
#54987=EDGE_CURVE('',#41556,#41715,#1081,.T.);
#54988=EDGE_CURVE('',#41667,#41916,#1082,.T.);
#54989=EDGE_CURVE('',#41915,#41668,#1083,.T.);
#54990=EDGE_CURVE('',#41919,#41664,#1084,.T.);
#54991=EDGE_CURVE('',#41663,#41920,#1085,.T.);
#54992=EDGE_CURVE('',#41923,#41660,#1086,.T.);
#54993=EDGE_CURVE('',#41659,#41924,#1087,.T.);
#54994=EDGE_CURVE('',#41927,#41656,#1088,.T.);
#54995=EDGE_CURVE('',#41655,#41928,#1089,.T.);
#54996=EDGE_CURVE('',#41931,#41652,#1090,.T.);
#54997=EDGE_CURVE('',#41651,#41932,#1091,.T.);
#54998=EDGE_CURVE('',#41935,#41648,#1092,.T.);
#54999=EDGE_CURVE('',#41647,#41936,#1093,.T.);
#55000=EDGE_CURVE('',#41939,#41644,#1094,.T.);
#55001=EDGE_CURVE('',#41643,#41940,#1095,.T.);
#55002=EDGE_CURVE('',#41943,#41640,#1096,.T.);
#55003=EDGE_CURVE('',#41639,#41944,#1097,.T.);
#55004=EDGE_CURVE('',#41947,#41636,#1098,.T.);
#55005=EDGE_CURVE('',#41635,#41948,#1099,.T.);
#55006=EDGE_CURVE('',#41951,#41632,#1100,.T.);
#55007=EDGE_CURVE('',#41631,#41952,#1101,.T.);
#55008=EDGE_CURVE('',#41955,#41628,#1102,.T.);
#55009=EDGE_CURVE('',#41627,#41956,#1103,.T.);
#55010=EDGE_CURVE('',#41959,#41624,#1104,.T.);
#55011=EDGE_CURVE('',#41623,#41960,#1105,.T.);
#55012=EDGE_CURVE('',#41963,#41620,#1106,.T.);
#55013=EDGE_CURVE('',#41619,#41964,#1107,.T.);
#55014=EDGE_CURVE('',#41967,#41616,#1108,.T.);
#55015=EDGE_CURVE('',#41615,#41968,#1109,.T.);
#55016=EDGE_CURVE('',#41971,#41612,#1110,.T.);
#55017=EDGE_CURVE('',#41611,#41972,#1111,.T.);
#55018=EDGE_CURVE('',#41975,#41608,#1112,.T.);
#55019=EDGE_CURVE('',#41607,#41976,#1113,.T.);
#55020=EDGE_CURVE('',#41979,#41604,#1114,.T.);
#55021=EDGE_CURVE('',#41603,#41980,#1115,.T.);
#55022=EDGE_CURVE('',#41983,#41600,#1116,.T.);
#55023=EDGE_CURVE('',#41599,#41984,#1117,.T.);
#55024=EDGE_CURVE('',#41987,#41596,#1118,.T.);
#55025=EDGE_CURVE('',#41595,#41988,#1119,.T.);
#55026=EDGE_CURVE('',#41991,#41592,#1120,.T.);
#55027=EDGE_CURVE('',#41591,#41992,#1121,.T.);
#55028=EDGE_CURVE('',#41995,#41588,#1122,.T.);
#55029=EDGE_CURVE('',#41587,#41996,#1123,.T.);
#55030=EDGE_CURVE('',#41999,#41584,#1124,.T.);
#55031=EDGE_CURVE('',#41583,#42000,#1125,.T.);
#55032=EDGE_CURVE('',#42003,#41580,#1126,.T.);
#55033=EDGE_CURVE('',#41579,#42004,#1127,.T.);
#55034=EDGE_CURVE('',#42007,#41576,#1128,.T.);
#55035=EDGE_CURVE('',#41575,#42008,#1129,.T.);
#55036=EDGE_CURVE('',#42011,#41572,#1130,.T.);
#55037=EDGE_CURVE('',#41571,#42012,#1131,.T.);
#55038=EDGE_CURVE('',#42015,#41568,#1132,.T.);
#55039=EDGE_CURVE('',#41567,#42016,#1133,.T.);
#55040=EDGE_CURVE('',#42019,#41564,#1134,.T.);
#55041=EDGE_CURVE('',#41563,#42020,#1135,.T.);
#55042=EDGE_CURVE('',#41719,#41553,#1136,.T.);
#55043=EDGE_CURVE('',#41552,#41720,#1137,.T.);
#55044=EDGE_CURVE('',#41723,#41549,#1138,.T.);
#55045=EDGE_CURVE('',#41548,#41724,#1139,.T.);
#55046=EDGE_CURVE('',#41727,#41545,#1140,.T.);
#55047=EDGE_CURVE('',#41544,#41728,#1141,.T.);
#55048=EDGE_CURVE('',#41731,#41541,#1142,.T.);
#55049=EDGE_CURVE('',#41540,#41732,#1143,.T.);
#55050=EDGE_CURVE('',#41735,#41537,#1144,.T.);
#55051=EDGE_CURVE('',#41536,#41736,#1145,.T.);
#55052=EDGE_CURVE('',#41739,#41533,#1146,.T.);
#55053=EDGE_CURVE('',#41532,#41740,#1147,.T.);
#55054=EDGE_CURVE('',#41743,#41529,#1148,.T.);
#55055=EDGE_CURVE('',#41528,#41744,#1149,.T.);
#55056=EDGE_CURVE('',#41747,#41525,#1150,.T.);
#55057=EDGE_CURVE('',#41524,#41748,#1151,.T.);
#55058=EDGE_CURVE('',#41751,#41521,#1152,.T.);
#55059=EDGE_CURVE('',#41520,#41752,#1153,.T.);
#55060=EDGE_CURVE('',#41755,#41517,#1154,.T.);
#55061=EDGE_CURVE('',#41516,#41756,#1155,.T.);
#55062=EDGE_CURVE('',#41759,#41513,#1156,.T.);
#55063=EDGE_CURVE('',#41512,#41760,#1157,.T.);
#55064=EDGE_CURVE('',#41763,#41509,#1158,.T.);
#55065=EDGE_CURVE('',#41508,#41764,#1159,.T.);
#55066=EDGE_CURVE('',#41767,#41505,#1160,.T.);
#55067=EDGE_CURVE('',#41504,#41768,#1161,.T.);
#55068=EDGE_CURVE('',#41771,#41501,#1162,.T.);
#55069=EDGE_CURVE('',#41500,#41772,#1163,.T.);
#55070=EDGE_CURVE('',#41775,#41497,#1164,.T.);
#55071=EDGE_CURVE('',#41496,#41776,#1165,.T.);
#55072=EDGE_CURVE('',#41779,#41493,#1166,.T.);
#55073=EDGE_CURVE('',#41492,#41780,#1167,.T.);
#55074=EDGE_CURVE('',#41783,#41489,#1168,.T.);
#55075=EDGE_CURVE('',#41488,#41784,#1169,.T.);
#55076=EDGE_CURVE('',#41787,#41485,#1170,.T.);
#55077=EDGE_CURVE('',#41484,#41788,#1171,.T.);
#55078=EDGE_CURVE('',#41791,#41481,#1172,.T.);
#55079=EDGE_CURVE('',#41480,#41792,#1173,.T.);
#55080=EDGE_CURVE('',#41795,#41477,#1174,.T.);
#55081=EDGE_CURVE('',#41476,#41796,#1175,.T.);
#55082=EDGE_CURVE('',#41799,#41473,#1176,.T.);
#55083=EDGE_CURVE('',#41472,#41800,#1177,.T.);
#55084=EDGE_CURVE('',#41803,#41469,#1178,.T.);
#55085=EDGE_CURVE('',#41468,#41804,#1179,.T.);
#55086=EDGE_CURVE('',#41807,#41465,#1180,.T.);
#55087=EDGE_CURVE('',#41464,#41808,#1181,.T.);
#55088=EDGE_CURVE('',#41811,#41461,#1182,.T.);
#55089=EDGE_CURVE('',#41460,#41812,#1183,.T.);
#55090=EDGE_CURVE('',#41815,#41457,#1184,.T.);
#55091=EDGE_CURVE('',#41456,#41816,#1185,.T.);
#55092=EDGE_CURVE('',#41819,#41453,#1186,.T.);
#55093=EDGE_CURVE('',#41452,#41820,#1187,.T.);
#55094=EDGE_CURVE('',#41823,#41449,#1188,.T.);
#55095=EDGE_CURVE('',#41448,#41824,#1189,.T.);
#55096=EDGE_CURVE('',#41827,#41445,#1190,.T.);
#55097=EDGE_CURVE('',#41444,#41828,#1191,.T.);
#55098=EDGE_CURVE('',#41831,#41441,#1192,.T.);
#55099=EDGE_CURVE('',#41440,#41832,#1193,.T.);
#55100=EDGE_CURVE('',#41835,#41437,#1194,.T.);
#55101=EDGE_CURVE('',#41436,#41836,#1195,.T.);
#55102=EDGE_CURVE('',#41839,#41433,#1196,.T.);
#55103=EDGE_CURVE('',#41432,#41840,#1197,.T.);
#55104=EDGE_CURVE('',#41843,#41429,#1198,.T.);
#55105=EDGE_CURVE('',#41428,#41844,#1199,.T.);
#55106=EDGE_CURVE('',#41847,#41425,#1200,.T.);
#55107=EDGE_CURVE('',#41424,#41848,#1201,.T.);
#55108=EDGE_CURVE('',#41851,#41421,#1202,.T.);
#55109=EDGE_CURVE('',#41420,#41852,#1203,.T.);
#55110=EDGE_CURVE('',#41855,#41417,#1204,.T.);
#55111=EDGE_CURVE('',#41416,#41856,#1205,.T.);
#55112=EDGE_CURVE('',#41859,#41413,#1206,.T.);
#55113=EDGE_CURVE('',#41412,#41860,#1207,.T.);
#55114=EDGE_CURVE('',#41671,#41912,#1208,.T.);
#55115=EDGE_CURVE('',#41911,#41672,#1209,.T.);
#55116=EDGE_CURVE('',#41675,#41908,#1210,.T.);
#55117=EDGE_CURVE('',#41907,#41676,#1211,.T.);
#55118=EDGE_CURVE('',#41679,#41904,#1212,.T.);
#55119=EDGE_CURVE('',#41903,#41680,#1213,.T.);
#55120=EDGE_CURVE('',#41683,#41900,#1214,.T.);
#55121=EDGE_CURVE('',#41899,#41684,#1215,.T.);
#55122=EDGE_CURVE('',#41687,#41896,#1216,.T.);
#55123=EDGE_CURVE('',#41895,#41688,#1217,.T.);
#55124=EDGE_CURVE('',#41691,#41892,#1218,.T.);
#55125=EDGE_CURVE('',#41891,#41692,#1219,.T.);
#55126=EDGE_CURVE('',#41695,#41888,#1220,.T.);
#55127=EDGE_CURVE('',#41887,#41696,#1221,.T.);
#55128=EDGE_CURVE('',#41699,#41884,#1222,.T.);
#55129=EDGE_CURVE('',#41883,#41700,#1223,.T.);
#55130=EDGE_CURVE('',#41703,#41880,#1224,.T.);
#55131=EDGE_CURVE('',#41879,#41704,#1225,.T.);
#55132=EDGE_CURVE('',#41707,#41876,#1226,.T.);
#55133=EDGE_CURVE('',#41875,#41708,#1227,.T.);
#55134=EDGE_CURVE('',#41711,#41872,#1228,.T.);
#55135=EDGE_CURVE('',#41871,#41712,#1229,.T.);
#55136=EDGE_CURVE('',#41863,#41409,#1230,.T.);
#55137=EDGE_CURVE('',#41408,#41864,#1231,.T.);
#55138=EDGE_CURVE('',#42023,#42024,#30135,.T.);
#55139=EDGE_CURVE('',#42024,#42025,#26164,.T.);
#55140=EDGE_CURVE('',#42025,#42026,#26165,.T.);
#55141=EDGE_CURVE('',#42027,#42026,#30136,.T.);
#55142=EDGE_CURVE('',#42027,#42028,#1232,.T.);
#55143=EDGE_CURVE('',#42028,#42023,#1233,.T.);
#55144=EDGE_CURVE('',#42029,#42030,#1234,.T.);
#55145=EDGE_CURVE('',#42030,#42024,#30137,.T.);
#55146=EDGE_CURVE('',#42023,#42031,#26166,.T.);
#55147=EDGE_CURVE('',#42031,#42029,#30138,.T.);
#55148=EDGE_CURVE('',#42026,#42032,#30139,.T.);
#55149=EDGE_CURVE('',#42032,#42033,#1235,.T.);
#55150=EDGE_CURVE('',#42033,#42034,#30140,.T.);
#55151=EDGE_CURVE('',#42034,#42027,#26167,.T.);
#55152=EDGE_CURVE('',#42035,#41394,#30141,.T.);
#55153=EDGE_CURVE('',#41393,#42035,#30142,.T.);
#55154=EDGE_CURVE('',#42036,#41393,#30143,.T.);
#55155=EDGE_CURVE('',#41392,#42036,#30144,.T.);
#55156=EDGE_CURVE('',#42037,#41392,#30145,.T.);
#55157=EDGE_CURVE('',#41391,#42037,#30146,.T.);
#55158=EDGE_CURVE('',#42038,#41391,#30147,.T.);
#55159=EDGE_CURVE('',#41390,#42038,#30148,.T.);
#55160=EDGE_CURVE('',#42039,#41390,#30149,.T.);
#55161=EDGE_CURVE('',#41395,#42039,#30150,.T.);
#55162=EDGE_CURVE('',#42040,#42041,#22599,.T.);
#55163=EDGE_CURVE('',#41396,#42040,#22600,.T.);
#55164=EDGE_CURVE('',#42042,#41397,#22601,.T.);
#55165=EDGE_CURVE('',#42043,#42042,#22602,.T.);
#55166=EDGE_CURVE('',#42041,#42043,#22603,.T.);
#55167=EDGE_CURVE('',#41867,#41405,#1236,.T.);
#55168=EDGE_CURVE('',#41404,#41868,#1237,.T.);
#55169=EDGE_CURVE('',#42035,#41396,#30151,.T.);
#55170=EDGE_CURVE('',#42040,#41396,#4398,.T.);
#55171=EDGE_CURVE('',#42044,#42040,#30152,.T.);
#55172=EDGE_CURVE('',#41394,#42044,#30153,.T.);
#55173=EDGE_CURVE('',#42036,#41397,#30154,.T.);
#55174=EDGE_CURVE('',#42037,#42042,#30155,.T.);
#55175=EDGE_CURVE('',#41397,#42042,#4399,.T.);
#55176=EDGE_CURVE('',#42038,#42043,#30156,.T.);
#55177=EDGE_CURVE('',#42042,#42043,#4400,.T.);
#55178=EDGE_CURVE('',#42039,#42041,#30157,.T.);
#55179=EDGE_CURVE('',#42043,#42041,#4401,.T.);
#55180=EDGE_CURVE('',#42041,#42040,#4402,.T.);
#55181=EDGE_CURVE('',#42044,#41395,#30158,.T.);
#55182=EDGE_CURVE('',#40996,#41000,#4403,.T.);
#55183=EDGE_CURVE('',#40997,#41001,#4404,.T.);
#55184=EDGE_CURVE('',#42045,#42046,#26168,.T.);
#55185=EDGE_CURVE('',#42046,#41383,#1238,.T.);
#55186=EDGE_CURVE('',#41384,#42045,#26169,.T.);
#55187=EDGE_CURVE('',#42031,#41384,#26170,.T.);
#55188=EDGE_CURVE('',#42045,#42023,#22604,.T.);
#55189=EDGE_CURVE('',#42029,#41868,#22605,.T.);
#55190=EDGE_CURVE('',#41869,#42031,#22606,.T.);
#55191=EDGE_CURVE('',#42046,#42027,#22607,.T.);
#55192=EDGE_CURVE('',#42030,#41404,#22608,.T.);
#55193=EDGE_CURVE('',#41383,#42034,#26171,.T.);
#55194=EDGE_CURVE('',#42024,#41403,#22609,.T.);
#55195=EDGE_CURVE('',#41870,#42034,#22610,.T.);
#55196=EDGE_CURVE('',#42026,#41713,#22611,.T.);
#55197=EDGE_CURVE('',#41871,#42033,#22612,.T.);
#55198=EDGE_CURVE('',#42032,#41712,#22613,.T.);
#55199=EDGE_CURVE('',#42047,#42048,#30159,.T.);
#55200=EDGE_CURVE('',#42048,#42049,#30160,.T.);
#55201=EDGE_CURVE('',#42049,#42050,#1239,.T.);
#55202=EDGE_CURVE('',#42050,#42051,#30161,.T.);
#55203=EDGE_CURVE('',#42051,#42047,#26172,.T.);
#55204=EDGE_CURVE('',#42052,#42053,#1240,.T.);
#55205=EDGE_CURVE('',#42053,#42054,#30162,.T.);
#55206=EDGE_CURVE('',#42055,#42054,#30163,.T.);
#55207=EDGE_CURVE('',#42055,#42056,#26173,.T.);
#55208=EDGE_CURVE('',#42056,#42052,#30164,.T.);
#55209=EDGE_CURVE('',#42054,#42057,#26174,.T.);
#55210=EDGE_CURVE('',#42057,#42048,#26175,.T.);
#55211=EDGE_CURVE('',#42047,#42058,#1241,.T.);
#55212=EDGE_CURVE('',#42058,#42055,#1242,.T.);
#55213=EDGE_CURVE('',#42056,#41380,#26176,.T.);
#55214=EDGE_CURVE('',#42059,#42055,#22614,.T.);
#55215=EDGE_CURVE('',#41380,#42059,#26177,.T.);
#55216=EDGE_CURVE('',#42060,#42047,#22615,.T.);
#55217=EDGE_CURVE('',#42059,#42060,#26178,.T.);
#55218=EDGE_CURVE('',#41379,#42051,#26179,.T.);
#55219=EDGE_CURVE('',#42060,#41379,#1243,.T.);
#55220=EDGE_CURVE('',#41865,#42056,#22616,.T.);
#55221=EDGE_CURVE('',#42052,#41864,#22617,.T.);
#55222=EDGE_CURVE('',#42053,#41408,#22618,.T.);
#55223=EDGE_CURVE('',#42054,#41407,#22619,.T.);
#55224=EDGE_CURVE('',#42048,#41406,#22620,.T.);
#55225=EDGE_CURVE('',#42049,#41405,#22621,.T.);
#55226=EDGE_CURVE('',#41867,#42050,#22622,.T.);
#55227=EDGE_CURVE('',#41866,#42051,#22623,.T.);
#55228=EDGE_CURVE('',#42061,#42062,#30165,.T.);
#55229=EDGE_CURVE('',#42062,#42063,#30166,.T.);
#55230=EDGE_CURVE('',#42063,#42064,#1244,.T.);
#55231=EDGE_CURVE('',#42064,#42065,#30167,.T.);
#55232=EDGE_CURVE('',#42065,#42061,#26180,.T.);
#55233=EDGE_CURVE('',#42066,#42067,#1245,.T.);
#55234=EDGE_CURVE('',#42067,#42068,#30168,.T.);
#55235=EDGE_CURVE('',#42069,#42068,#30169,.T.);
#55236=EDGE_CURVE('',#42069,#42070,#26181,.T.);
#55237=EDGE_CURVE('',#42070,#42066,#30170,.T.);
#55238=EDGE_CURVE('',#42068,#42071,#26182,.T.);
#55239=EDGE_CURVE('',#42071,#42062,#26183,.T.);
#55240=EDGE_CURVE('',#42061,#42072,#1246,.T.);
#55241=EDGE_CURVE('',#42072,#42069,#1247,.T.);
#55242=EDGE_CURVE('',#42070,#41376,#26184,.T.);
#55243=EDGE_CURVE('',#42073,#42069,#22624,.T.);
#55244=EDGE_CURVE('',#41376,#42073,#26185,.T.);
#55245=EDGE_CURVE('',#42074,#42061,#22625,.T.);
#55246=EDGE_CURVE('',#42073,#42074,#26186,.T.);
#55247=EDGE_CURVE('',#41375,#42065,#26187,.T.);
#55248=EDGE_CURVE('',#42074,#41375,#1248,.T.);
#55249=EDGE_CURVE('',#41873,#42070,#22626,.T.);
#55250=EDGE_CURVE('',#42066,#41872,#22627,.T.);
#55251=EDGE_CURVE('',#42067,#41711,#22628,.T.);
#55252=EDGE_CURVE('',#42068,#41710,#22629,.T.);
#55253=EDGE_CURVE('',#42062,#41709,#22630,.T.);
#55254=EDGE_CURVE('',#42063,#41708,#22631,.T.);
#55255=EDGE_CURVE('',#41875,#42064,#22632,.T.);
#55256=EDGE_CURVE('',#41874,#42065,#22633,.T.);
#55257=EDGE_CURVE('',#42075,#42076,#30171,.T.);
#55258=EDGE_CURVE('',#42076,#42077,#30172,.T.);
#55259=EDGE_CURVE('',#42077,#42078,#1249,.T.);
#55260=EDGE_CURVE('',#42078,#42079,#30173,.T.);
#55261=EDGE_CURVE('',#42079,#42075,#26188,.T.);
#55262=EDGE_CURVE('',#42080,#42081,#1250,.T.);
#55263=EDGE_CURVE('',#42081,#42082,#30174,.T.);
#55264=EDGE_CURVE('',#42083,#42082,#30175,.T.);
#55265=EDGE_CURVE('',#42083,#42084,#26189,.T.);
#55266=EDGE_CURVE('',#42084,#42080,#30176,.T.);
#55267=EDGE_CURVE('',#42082,#42085,#26190,.T.);
#55268=EDGE_CURVE('',#42085,#42076,#26191,.T.);
#55269=EDGE_CURVE('',#42075,#42086,#1251,.T.);
#55270=EDGE_CURVE('',#42086,#42083,#1252,.T.);
#55271=EDGE_CURVE('',#42084,#41372,#26192,.T.);
#55272=EDGE_CURVE('',#42087,#42083,#22634,.T.);
#55273=EDGE_CURVE('',#41372,#42087,#26193,.T.);
#55274=EDGE_CURVE('',#42088,#42075,#22635,.T.);
#55275=EDGE_CURVE('',#42087,#42088,#26194,.T.);
#55276=EDGE_CURVE('',#41371,#42079,#26195,.T.);
#55277=EDGE_CURVE('',#42088,#41371,#1253,.T.);
#55278=EDGE_CURVE('',#41877,#42084,#22636,.T.);
#55279=EDGE_CURVE('',#42080,#41876,#22637,.T.);
#55280=EDGE_CURVE('',#42081,#41707,#22638,.T.);
#55281=EDGE_CURVE('',#42082,#41706,#22639,.T.);
#55282=EDGE_CURVE('',#42076,#41705,#22640,.T.);
#55283=EDGE_CURVE('',#42077,#41704,#22641,.T.);
#55284=EDGE_CURVE('',#41879,#42078,#22642,.T.);
#55285=EDGE_CURVE('',#41878,#42079,#22643,.T.);
#55286=EDGE_CURVE('',#42089,#42090,#30177,.T.);
#55287=EDGE_CURVE('',#42090,#42091,#30178,.T.);
#55288=EDGE_CURVE('',#42091,#42092,#1254,.T.);
#55289=EDGE_CURVE('',#42092,#42093,#30179,.T.);
#55290=EDGE_CURVE('',#42093,#42089,#26196,.T.);
#55291=EDGE_CURVE('',#42094,#42095,#1255,.T.);
#55292=EDGE_CURVE('',#42095,#42096,#30180,.T.);
#55293=EDGE_CURVE('',#42097,#42096,#30181,.T.);
#55294=EDGE_CURVE('',#42097,#42098,#26197,.T.);
#55295=EDGE_CURVE('',#42098,#42094,#30182,.T.);
#55296=EDGE_CURVE('',#42096,#42099,#26198,.T.);
#55297=EDGE_CURVE('',#42099,#42090,#26199,.T.);
#55298=EDGE_CURVE('',#42089,#42100,#1256,.T.);
#55299=EDGE_CURVE('',#42100,#42097,#1257,.T.);
#55300=EDGE_CURVE('',#42098,#41368,#26200,.T.);
#55301=EDGE_CURVE('',#42101,#42097,#22644,.T.);
#55302=EDGE_CURVE('',#41368,#42101,#26201,.T.);
#55303=EDGE_CURVE('',#42102,#42089,#22645,.T.);
#55304=EDGE_CURVE('',#42101,#42102,#26202,.T.);
#55305=EDGE_CURVE('',#41367,#42093,#26203,.T.);
#55306=EDGE_CURVE('',#42102,#41367,#1258,.T.);
#55307=EDGE_CURVE('',#41881,#42098,#22646,.T.);
#55308=EDGE_CURVE('',#42094,#41880,#22647,.T.);
#55309=EDGE_CURVE('',#42095,#41703,#22648,.T.);
#55310=EDGE_CURVE('',#42096,#41702,#22649,.T.);
#55311=EDGE_CURVE('',#42090,#41701,#22650,.T.);
#55312=EDGE_CURVE('',#42091,#41700,#22651,.T.);
#55313=EDGE_CURVE('',#41883,#42092,#22652,.T.);
#55314=EDGE_CURVE('',#41882,#42093,#22653,.T.);
#55315=EDGE_CURVE('',#42103,#42104,#30183,.T.);
#55316=EDGE_CURVE('',#42104,#42105,#30184,.T.);
#55317=EDGE_CURVE('',#42105,#42106,#1259,.T.);
#55318=EDGE_CURVE('',#42106,#42107,#30185,.T.);
#55319=EDGE_CURVE('',#42107,#42103,#26204,.T.);
#55320=EDGE_CURVE('',#42108,#42109,#1260,.T.);
#55321=EDGE_CURVE('',#42109,#42110,#30186,.T.);
#55322=EDGE_CURVE('',#42111,#42110,#30187,.T.);
#55323=EDGE_CURVE('',#42111,#42112,#26205,.T.);
#55324=EDGE_CURVE('',#42112,#42108,#30188,.T.);
#55325=EDGE_CURVE('',#42110,#42113,#26206,.T.);
#55326=EDGE_CURVE('',#42113,#42104,#26207,.T.);
#55327=EDGE_CURVE('',#42103,#42114,#1261,.T.);
#55328=EDGE_CURVE('',#42114,#42111,#1262,.T.);
#55329=EDGE_CURVE('',#42112,#41364,#26208,.T.);
#55330=EDGE_CURVE('',#42115,#42111,#22654,.T.);
#55331=EDGE_CURVE('',#41364,#42115,#26209,.T.);
#55332=EDGE_CURVE('',#42116,#42103,#22655,.T.);
#55333=EDGE_CURVE('',#42115,#42116,#26210,.T.);
#55334=EDGE_CURVE('',#41363,#42107,#26211,.T.);
#55335=EDGE_CURVE('',#42116,#41363,#1263,.T.);
#55336=EDGE_CURVE('',#41885,#42112,#22656,.T.);
#55337=EDGE_CURVE('',#42108,#41884,#22657,.T.);
#55338=EDGE_CURVE('',#42109,#41699,#22658,.T.);
#55339=EDGE_CURVE('',#42110,#41698,#22659,.T.);
#55340=EDGE_CURVE('',#42104,#41697,#22660,.T.);
#55341=EDGE_CURVE('',#42105,#41696,#22661,.T.);
#55342=EDGE_CURVE('',#41887,#42106,#22662,.T.);
#55343=EDGE_CURVE('',#41886,#42107,#22663,.T.);
#55344=EDGE_CURVE('',#42117,#42118,#30189,.T.);
#55345=EDGE_CURVE('',#42118,#42119,#30190,.T.);
#55346=EDGE_CURVE('',#42119,#42120,#1264,.T.);
#55347=EDGE_CURVE('',#42120,#42121,#30191,.T.);
#55348=EDGE_CURVE('',#42121,#42117,#26212,.T.);
#55349=EDGE_CURVE('',#42122,#42123,#1265,.T.);
#55350=EDGE_CURVE('',#42123,#42124,#30192,.T.);
#55351=EDGE_CURVE('',#42125,#42124,#30193,.T.);
#55352=EDGE_CURVE('',#42125,#42126,#26213,.T.);
#55353=EDGE_CURVE('',#42126,#42122,#30194,.T.);
#55354=EDGE_CURVE('',#42124,#42127,#26214,.T.);
#55355=EDGE_CURVE('',#42127,#42118,#26215,.T.);
#55356=EDGE_CURVE('',#42117,#42128,#1266,.T.);
#55357=EDGE_CURVE('',#42128,#42125,#1267,.T.);
#55358=EDGE_CURVE('',#42126,#41360,#26216,.T.);
#55359=EDGE_CURVE('',#42129,#42125,#22664,.T.);
#55360=EDGE_CURVE('',#41360,#42129,#26217,.T.);
#55361=EDGE_CURVE('',#42130,#42117,#22665,.T.);
#55362=EDGE_CURVE('',#42129,#42130,#26218,.T.);
#55363=EDGE_CURVE('',#41359,#42121,#26219,.T.);
#55364=EDGE_CURVE('',#42130,#41359,#1268,.T.);
#55365=EDGE_CURVE('',#41889,#42126,#22666,.T.);
#55366=EDGE_CURVE('',#42122,#41888,#22667,.T.);
#55367=EDGE_CURVE('',#42123,#41695,#22668,.T.);
#55368=EDGE_CURVE('',#42124,#41694,#22669,.T.);
#55369=EDGE_CURVE('',#42118,#41693,#22670,.T.);
#55370=EDGE_CURVE('',#42119,#41692,#22671,.T.);
#55371=EDGE_CURVE('',#41891,#42120,#22672,.T.);
#55372=EDGE_CURVE('',#41890,#42121,#22673,.T.);
#55373=EDGE_CURVE('',#42131,#42132,#30195,.T.);
#55374=EDGE_CURVE('',#42132,#42133,#30196,.T.);
#55375=EDGE_CURVE('',#42133,#42134,#1269,.T.);
#55376=EDGE_CURVE('',#42134,#42135,#30197,.T.);
#55377=EDGE_CURVE('',#42135,#42131,#26220,.T.);
#55378=EDGE_CURVE('',#42136,#42137,#1270,.T.);
#55379=EDGE_CURVE('',#42137,#42138,#30198,.T.);
#55380=EDGE_CURVE('',#42139,#42138,#30199,.T.);
#55381=EDGE_CURVE('',#42139,#42140,#26221,.T.);
#55382=EDGE_CURVE('',#42140,#42136,#30200,.T.);
#55383=EDGE_CURVE('',#42138,#42141,#26222,.T.);
#55384=EDGE_CURVE('',#42141,#42132,#26223,.T.);
#55385=EDGE_CURVE('',#42131,#42142,#1271,.T.);
#55386=EDGE_CURVE('',#42142,#42139,#1272,.T.);
#55387=EDGE_CURVE('',#42140,#41356,#26224,.T.);
#55388=EDGE_CURVE('',#42143,#42139,#22674,.T.);
#55389=EDGE_CURVE('',#41356,#42143,#26225,.T.);
#55390=EDGE_CURVE('',#42144,#42131,#22675,.T.);
#55391=EDGE_CURVE('',#42143,#42144,#26226,.T.);
#55392=EDGE_CURVE('',#41355,#42135,#26227,.T.);
#55393=EDGE_CURVE('',#42144,#41355,#1273,.T.);
#55394=EDGE_CURVE('',#41893,#42140,#22676,.T.);
#55395=EDGE_CURVE('',#42136,#41892,#22677,.T.);
#55396=EDGE_CURVE('',#42137,#41691,#22678,.T.);
#55397=EDGE_CURVE('',#42138,#41690,#22679,.T.);
#55398=EDGE_CURVE('',#42132,#41689,#22680,.T.);
#55399=EDGE_CURVE('',#42133,#41688,#22681,.T.);
#55400=EDGE_CURVE('',#41895,#42134,#22682,.T.);
#55401=EDGE_CURVE('',#41894,#42135,#22683,.T.);
#55402=EDGE_CURVE('',#42145,#42146,#30201,.T.);
#55403=EDGE_CURVE('',#42146,#42147,#30202,.T.);
#55404=EDGE_CURVE('',#42147,#42148,#1274,.T.);
#55405=EDGE_CURVE('',#42148,#42149,#30203,.T.);
#55406=EDGE_CURVE('',#42149,#42145,#26228,.T.);
#55407=EDGE_CURVE('',#42150,#42151,#1275,.T.);
#55408=EDGE_CURVE('',#42151,#42152,#30204,.T.);
#55409=EDGE_CURVE('',#42153,#42152,#30205,.T.);
#55410=EDGE_CURVE('',#42153,#42154,#26229,.T.);
#55411=EDGE_CURVE('',#42154,#42150,#30206,.T.);
#55412=EDGE_CURVE('',#42152,#42155,#26230,.T.);
#55413=EDGE_CURVE('',#42155,#42146,#26231,.T.);
#55414=EDGE_CURVE('',#42145,#42156,#1276,.T.);
#55415=EDGE_CURVE('',#42156,#42153,#1277,.T.);
#55416=EDGE_CURVE('',#42154,#41352,#26232,.T.);
#55417=EDGE_CURVE('',#42157,#42153,#22684,.T.);
#55418=EDGE_CURVE('',#41352,#42157,#26233,.T.);
#55419=EDGE_CURVE('',#42158,#42145,#22685,.T.);
#55420=EDGE_CURVE('',#42157,#42158,#26234,.T.);
#55421=EDGE_CURVE('',#41351,#42149,#26235,.T.);
#55422=EDGE_CURVE('',#42158,#41351,#1278,.T.);
#55423=EDGE_CURVE('',#41897,#42154,#22686,.T.);
#55424=EDGE_CURVE('',#42150,#41896,#22687,.T.);
#55425=EDGE_CURVE('',#42151,#41687,#22688,.T.);
#55426=EDGE_CURVE('',#42152,#41686,#22689,.T.);
#55427=EDGE_CURVE('',#42146,#41685,#22690,.T.);
#55428=EDGE_CURVE('',#42147,#41684,#22691,.T.);
#55429=EDGE_CURVE('',#41899,#42148,#22692,.T.);
#55430=EDGE_CURVE('',#41898,#42149,#22693,.T.);
#55431=EDGE_CURVE('',#42159,#42160,#30207,.T.);
#55432=EDGE_CURVE('',#42160,#42161,#30208,.T.);
#55433=EDGE_CURVE('',#42161,#42162,#1279,.T.);
#55434=EDGE_CURVE('',#42162,#42163,#30209,.T.);
#55435=EDGE_CURVE('',#42163,#42159,#26236,.T.);
#55436=EDGE_CURVE('',#42164,#42165,#1280,.T.);
#55437=EDGE_CURVE('',#42165,#42166,#30210,.T.);
#55438=EDGE_CURVE('',#42167,#42166,#30211,.T.);
#55439=EDGE_CURVE('',#42167,#42168,#26237,.T.);
#55440=EDGE_CURVE('',#42168,#42164,#30212,.T.);
#55441=EDGE_CURVE('',#42166,#42169,#26238,.T.);
#55442=EDGE_CURVE('',#42169,#42160,#26239,.T.);
#55443=EDGE_CURVE('',#42159,#42170,#1281,.T.);
#55444=EDGE_CURVE('',#42170,#42167,#1282,.T.);
#55445=EDGE_CURVE('',#42168,#41348,#26240,.T.);
#55446=EDGE_CURVE('',#42171,#42167,#22694,.T.);
#55447=EDGE_CURVE('',#41348,#42171,#26241,.T.);
#55448=EDGE_CURVE('',#42172,#42159,#22695,.T.);
#55449=EDGE_CURVE('',#42171,#42172,#26242,.T.);
#55450=EDGE_CURVE('',#41347,#42163,#26243,.T.);
#55451=EDGE_CURVE('',#42172,#41347,#1283,.T.);
#55452=EDGE_CURVE('',#41901,#42168,#22696,.T.);
#55453=EDGE_CURVE('',#42164,#41900,#22697,.T.);
#55454=EDGE_CURVE('',#42165,#41683,#22698,.T.);
#55455=EDGE_CURVE('',#42166,#41682,#22699,.T.);
#55456=EDGE_CURVE('',#42160,#41681,#22700,.T.);
#55457=EDGE_CURVE('',#42161,#41680,#22701,.T.);
#55458=EDGE_CURVE('',#41903,#42162,#22702,.T.);
#55459=EDGE_CURVE('',#41902,#42163,#22703,.T.);
#55460=EDGE_CURVE('',#42173,#42174,#30213,.T.);
#55461=EDGE_CURVE('',#42174,#42175,#30214,.T.);
#55462=EDGE_CURVE('',#42175,#42176,#1284,.T.);
#55463=EDGE_CURVE('',#42176,#42177,#30215,.T.);
#55464=EDGE_CURVE('',#42177,#42173,#26244,.T.);
#55465=EDGE_CURVE('',#42178,#42179,#1285,.T.);
#55466=EDGE_CURVE('',#42179,#42180,#30216,.T.);
#55467=EDGE_CURVE('',#42181,#42180,#30217,.T.);
#55468=EDGE_CURVE('',#42181,#42182,#26245,.T.);
#55469=EDGE_CURVE('',#42182,#42178,#30218,.T.);
#55470=EDGE_CURVE('',#42180,#42183,#26246,.T.);
#55471=EDGE_CURVE('',#42183,#42174,#26247,.T.);
#55472=EDGE_CURVE('',#42173,#42184,#1286,.T.);
#55473=EDGE_CURVE('',#42184,#42181,#1287,.T.);
#55474=EDGE_CURVE('',#42182,#41344,#26248,.T.);
#55475=EDGE_CURVE('',#42185,#42181,#22704,.T.);
#55476=EDGE_CURVE('',#41344,#42185,#26249,.T.);
#55477=EDGE_CURVE('',#42186,#42173,#22705,.T.);
#55478=EDGE_CURVE('',#42185,#42186,#26250,.T.);
#55479=EDGE_CURVE('',#41343,#42177,#26251,.T.);
#55480=EDGE_CURVE('',#42186,#41343,#1288,.T.);
#55481=EDGE_CURVE('',#41905,#42182,#22706,.T.);
#55482=EDGE_CURVE('',#42178,#41904,#22707,.T.);
#55483=EDGE_CURVE('',#42179,#41679,#22708,.T.);
#55484=EDGE_CURVE('',#42180,#41678,#22709,.T.);
#55485=EDGE_CURVE('',#42174,#41677,#22710,.T.);
#55486=EDGE_CURVE('',#42175,#41676,#22711,.T.);
#55487=EDGE_CURVE('',#41907,#42176,#22712,.T.);
#55488=EDGE_CURVE('',#41906,#42177,#22713,.T.);
#55489=EDGE_CURVE('',#42187,#42188,#30219,.T.);
#55490=EDGE_CURVE('',#42188,#42189,#30220,.T.);
#55491=EDGE_CURVE('',#42189,#42190,#1289,.T.);
#55492=EDGE_CURVE('',#42190,#42191,#30221,.T.);
#55493=EDGE_CURVE('',#42191,#42187,#26252,.T.);
#55494=EDGE_CURVE('',#42192,#42193,#1290,.T.);
#55495=EDGE_CURVE('',#42193,#42194,#30222,.T.);
#55496=EDGE_CURVE('',#42195,#42194,#30223,.T.);
#55497=EDGE_CURVE('',#42195,#42196,#26253,.T.);
#55498=EDGE_CURVE('',#42196,#42192,#30224,.T.);
#55499=EDGE_CURVE('',#42194,#42197,#26254,.T.);
#55500=EDGE_CURVE('',#42197,#42188,#26255,.T.);
#55501=EDGE_CURVE('',#42187,#42198,#1291,.T.);
#55502=EDGE_CURVE('',#42198,#42195,#1292,.T.);
#55503=EDGE_CURVE('',#42196,#41340,#26256,.T.);
#55504=EDGE_CURVE('',#42199,#42195,#22714,.T.);
#55505=EDGE_CURVE('',#41340,#42199,#26257,.T.);
#55506=EDGE_CURVE('',#42200,#42187,#22715,.T.);
#55507=EDGE_CURVE('',#42199,#42200,#26258,.T.);
#55508=EDGE_CURVE('',#41339,#42191,#26259,.T.);
#55509=EDGE_CURVE('',#42200,#41339,#1293,.T.);
#55510=EDGE_CURVE('',#41909,#42196,#22716,.T.);
#55511=EDGE_CURVE('',#42192,#41908,#22717,.T.);
#55512=EDGE_CURVE('',#42193,#41675,#22718,.T.);
#55513=EDGE_CURVE('',#42194,#41674,#22719,.T.);
#55514=EDGE_CURVE('',#42188,#41673,#22720,.T.);
#55515=EDGE_CURVE('',#42189,#41672,#22721,.T.);
#55516=EDGE_CURVE('',#41911,#42190,#22722,.T.);
#55517=EDGE_CURVE('',#41910,#42191,#22723,.T.);
#55518=EDGE_CURVE('',#42201,#42202,#30225,.T.);
#55519=EDGE_CURVE('',#42202,#42203,#30226,.T.);
#55520=EDGE_CURVE('',#42203,#42204,#1294,.T.);
#55521=EDGE_CURVE('',#42204,#42205,#30227,.T.);
#55522=EDGE_CURVE('',#42205,#42201,#26260,.T.);
#55523=EDGE_CURVE('',#42206,#42207,#1295,.T.);
#55524=EDGE_CURVE('',#42207,#42208,#30228,.T.);
#55525=EDGE_CURVE('',#42209,#42208,#30229,.T.);
#55526=EDGE_CURVE('',#42209,#42210,#26261,.T.);
#55527=EDGE_CURVE('',#42210,#42206,#30230,.T.);
#55528=EDGE_CURVE('',#42208,#42211,#26262,.T.);
#55529=EDGE_CURVE('',#42211,#42202,#26263,.T.);
#55530=EDGE_CURVE('',#42201,#42212,#1296,.T.);
#55531=EDGE_CURVE('',#42212,#42209,#1297,.T.);
#55532=EDGE_CURVE('',#42210,#41336,#26264,.T.);
#55533=EDGE_CURVE('',#42213,#42209,#22724,.T.);
#55534=EDGE_CURVE('',#41336,#42213,#26265,.T.);
#55535=EDGE_CURVE('',#42214,#42201,#22725,.T.);
#55536=EDGE_CURVE('',#42213,#42214,#26266,.T.);
#55537=EDGE_CURVE('',#41335,#42205,#26267,.T.);
#55538=EDGE_CURVE('',#42214,#41335,#1298,.T.);
#55539=EDGE_CURVE('',#41913,#42210,#22726,.T.);
#55540=EDGE_CURVE('',#42206,#41912,#22727,.T.);
#55541=EDGE_CURVE('',#42207,#41671,#22728,.T.);
#55542=EDGE_CURVE('',#42208,#41670,#22729,.T.);
#55543=EDGE_CURVE('',#42202,#41669,#22730,.T.);
#55544=EDGE_CURVE('',#42203,#41668,#22731,.T.);
#55545=EDGE_CURVE('',#41915,#42204,#22732,.T.);
#55546=EDGE_CURVE('',#41914,#42205,#22733,.T.);
#55547=EDGE_CURVE('',#42215,#42216,#30231,.T.);
#55548=EDGE_CURVE('',#42216,#42217,#30232,.T.);
#55549=EDGE_CURVE('',#42217,#42218,#1299,.T.);
#55550=EDGE_CURVE('',#42218,#42219,#30233,.T.);
#55551=EDGE_CURVE('',#42219,#42215,#26268,.T.);
#55552=EDGE_CURVE('',#42220,#42221,#1300,.T.);
#55553=EDGE_CURVE('',#42221,#42222,#30234,.T.);
#55554=EDGE_CURVE('',#42223,#42222,#30235,.T.);
#55555=EDGE_CURVE('',#42223,#42224,#26269,.T.);
#55556=EDGE_CURVE('',#42224,#42220,#30236,.T.);
#55557=EDGE_CURVE('',#42222,#42225,#26270,.T.);
#55558=EDGE_CURVE('',#42225,#42216,#26271,.T.);
#55559=EDGE_CURVE('',#42215,#42226,#1301,.T.);
#55560=EDGE_CURVE('',#42226,#42223,#1302,.T.);
#55561=EDGE_CURVE('',#42224,#41332,#26272,.T.);
#55562=EDGE_CURVE('',#42227,#42223,#22734,.T.);
#55563=EDGE_CURVE('',#41332,#42227,#26273,.T.);
#55564=EDGE_CURVE('',#42228,#42215,#22735,.T.);
#55565=EDGE_CURVE('',#42227,#42228,#26274,.T.);
#55566=EDGE_CURVE('',#41331,#42219,#26275,.T.);
#55567=EDGE_CURVE('',#42228,#41331,#1303,.T.);
#55568=EDGE_CURVE('',#41861,#42224,#22736,.T.);
#55569=EDGE_CURVE('',#42220,#41860,#22737,.T.);
#55570=EDGE_CURVE('',#42221,#41412,#22738,.T.);
#55571=EDGE_CURVE('',#42222,#41411,#22739,.T.);
#55572=EDGE_CURVE('',#42216,#41410,#22740,.T.);
#55573=EDGE_CURVE('',#42217,#41409,#22741,.T.);
#55574=EDGE_CURVE('',#41863,#42218,#22742,.T.);
#55575=EDGE_CURVE('',#41862,#42219,#22743,.T.);
#55576=EDGE_CURVE('',#42229,#42230,#30237,.T.);
#55577=EDGE_CURVE('',#42230,#42231,#30238,.T.);
#55578=EDGE_CURVE('',#42231,#42232,#1304,.T.);
#55579=EDGE_CURVE('',#42232,#42233,#30239,.T.);
#55580=EDGE_CURVE('',#42233,#42229,#26276,.T.);
#55581=EDGE_CURVE('',#42234,#42235,#1305,.T.);
#55582=EDGE_CURVE('',#42235,#42236,#30240,.T.);
#55583=EDGE_CURVE('',#42237,#42236,#30241,.T.);
#55584=EDGE_CURVE('',#42237,#42238,#26277,.T.);
#55585=EDGE_CURVE('',#42238,#42234,#30242,.T.);
#55586=EDGE_CURVE('',#42236,#42239,#26278,.T.);
#55587=EDGE_CURVE('',#42239,#42230,#26279,.T.);
#55588=EDGE_CURVE('',#42229,#42240,#1306,.T.);
#55589=EDGE_CURVE('',#42240,#42237,#1307,.T.);
#55590=EDGE_CURVE('',#42238,#41328,#26280,.T.);
#55591=EDGE_CURVE('',#42241,#42237,#22744,.T.);
#55592=EDGE_CURVE('',#41328,#42241,#26281,.T.);
#55593=EDGE_CURVE('',#42242,#42229,#22745,.T.);
#55594=EDGE_CURVE('',#42241,#42242,#26282,.T.);
#55595=EDGE_CURVE('',#41327,#42233,#26283,.T.);
#55596=EDGE_CURVE('',#42242,#41327,#1308,.T.);
#55597=EDGE_CURVE('',#41857,#42238,#22746,.T.);
#55598=EDGE_CURVE('',#42234,#41856,#22747,.T.);
#55599=EDGE_CURVE('',#42235,#41416,#22748,.T.);
#55600=EDGE_CURVE('',#42236,#41415,#22749,.T.);
#55601=EDGE_CURVE('',#42230,#41414,#22750,.T.);
#55602=EDGE_CURVE('',#42231,#41413,#22751,.T.);
#55603=EDGE_CURVE('',#41859,#42232,#22752,.T.);
#55604=EDGE_CURVE('',#41858,#42233,#22753,.T.);
#55605=EDGE_CURVE('',#42243,#42244,#30243,.T.);
#55606=EDGE_CURVE('',#42244,#42245,#30244,.T.);
#55607=EDGE_CURVE('',#42245,#42246,#1309,.T.);
#55608=EDGE_CURVE('',#42246,#42247,#30245,.T.);
#55609=EDGE_CURVE('',#42247,#42243,#26284,.T.);
#55610=EDGE_CURVE('',#42248,#42249,#1310,.T.);
#55611=EDGE_CURVE('',#42249,#42250,#30246,.T.);
#55612=EDGE_CURVE('',#42251,#42250,#30247,.T.);
#55613=EDGE_CURVE('',#42251,#42252,#26285,.T.);
#55614=EDGE_CURVE('',#42252,#42248,#30248,.T.);
#55615=EDGE_CURVE('',#42250,#42253,#26286,.T.);
#55616=EDGE_CURVE('',#42253,#42244,#26287,.T.);
#55617=EDGE_CURVE('',#42243,#42254,#1311,.T.);
#55618=EDGE_CURVE('',#42254,#42251,#1312,.T.);
#55619=EDGE_CURVE('',#42252,#41324,#26288,.T.);
#55620=EDGE_CURVE('',#42255,#42251,#22754,.T.);
#55621=EDGE_CURVE('',#41324,#42255,#26289,.T.);
#55622=EDGE_CURVE('',#42256,#42243,#22755,.T.);
#55623=EDGE_CURVE('',#42255,#42256,#26290,.T.);
#55624=EDGE_CURVE('',#41323,#42247,#26291,.T.);
#55625=EDGE_CURVE('',#42256,#41323,#1313,.T.);
#55626=EDGE_CURVE('',#41853,#42252,#22756,.T.);
#55627=EDGE_CURVE('',#42248,#41852,#22757,.T.);
#55628=EDGE_CURVE('',#42249,#41420,#22758,.T.);
#55629=EDGE_CURVE('',#42250,#41419,#22759,.T.);
#55630=EDGE_CURVE('',#42244,#41418,#22760,.T.);
#55631=EDGE_CURVE('',#42245,#41417,#22761,.T.);
#55632=EDGE_CURVE('',#41855,#42246,#22762,.T.);
#55633=EDGE_CURVE('',#41854,#42247,#22763,.T.);
#55634=EDGE_CURVE('',#42257,#42258,#30249,.T.);
#55635=EDGE_CURVE('',#42258,#42259,#30250,.T.);
#55636=EDGE_CURVE('',#42259,#42260,#1314,.T.);
#55637=EDGE_CURVE('',#42260,#42261,#30251,.T.);
#55638=EDGE_CURVE('',#42261,#42257,#26292,.T.);
#55639=EDGE_CURVE('',#42262,#42263,#1315,.T.);
#55640=EDGE_CURVE('',#42263,#42264,#30252,.T.);
#55641=EDGE_CURVE('',#42265,#42264,#30253,.T.);
#55642=EDGE_CURVE('',#42265,#42266,#26293,.T.);
#55643=EDGE_CURVE('',#42266,#42262,#30254,.T.);
#55644=EDGE_CURVE('',#42264,#42267,#26294,.T.);
#55645=EDGE_CURVE('',#42267,#42258,#26295,.T.);
#55646=EDGE_CURVE('',#42257,#42268,#1316,.T.);
#55647=EDGE_CURVE('',#42268,#42265,#1317,.T.);
#55648=EDGE_CURVE('',#42266,#41320,#26296,.T.);
#55649=EDGE_CURVE('',#42269,#42265,#22764,.T.);
#55650=EDGE_CURVE('',#41320,#42269,#26297,.T.);
#55651=EDGE_CURVE('',#42270,#42257,#22765,.T.);
#55652=EDGE_CURVE('',#42269,#42270,#26298,.T.);
#55653=EDGE_CURVE('',#41319,#42261,#26299,.T.);
#55654=EDGE_CURVE('',#42270,#41319,#1318,.T.);
#55655=EDGE_CURVE('',#41849,#42266,#22766,.T.);
#55656=EDGE_CURVE('',#42262,#41848,#22767,.T.);
#55657=EDGE_CURVE('',#42263,#41424,#22768,.T.);
#55658=EDGE_CURVE('',#42264,#41423,#22769,.T.);
#55659=EDGE_CURVE('',#42258,#41422,#22770,.T.);
#55660=EDGE_CURVE('',#42259,#41421,#22771,.T.);
#55661=EDGE_CURVE('',#41851,#42260,#22772,.T.);
#55662=EDGE_CURVE('',#41850,#42261,#22773,.T.);
#55663=EDGE_CURVE('',#42271,#42272,#30255,.T.);
#55664=EDGE_CURVE('',#42272,#42273,#30256,.T.);
#55665=EDGE_CURVE('',#42273,#42274,#1319,.T.);
#55666=EDGE_CURVE('',#42274,#42275,#30257,.T.);
#55667=EDGE_CURVE('',#42275,#42271,#26300,.T.);
#55668=EDGE_CURVE('',#42276,#42277,#1320,.T.);
#55669=EDGE_CURVE('',#42277,#42278,#30258,.T.);
#55670=EDGE_CURVE('',#42279,#42278,#30259,.T.);
#55671=EDGE_CURVE('',#42279,#42280,#26301,.T.);
#55672=EDGE_CURVE('',#42280,#42276,#30260,.T.);
#55673=EDGE_CURVE('',#42278,#42281,#26302,.T.);
#55674=EDGE_CURVE('',#42281,#42272,#26303,.T.);
#55675=EDGE_CURVE('',#42271,#42282,#1321,.T.);
#55676=EDGE_CURVE('',#42282,#42279,#1322,.T.);
#55677=EDGE_CURVE('',#42280,#41316,#26304,.T.);
#55678=EDGE_CURVE('',#42283,#42279,#22774,.T.);
#55679=EDGE_CURVE('',#41316,#42283,#26305,.T.);
#55680=EDGE_CURVE('',#42284,#42271,#22775,.T.);
#55681=EDGE_CURVE('',#42283,#42284,#26306,.T.);
#55682=EDGE_CURVE('',#41315,#42275,#26307,.T.);
#55683=EDGE_CURVE('',#42284,#41315,#1323,.T.);
#55684=EDGE_CURVE('',#41845,#42280,#22776,.T.);
#55685=EDGE_CURVE('',#42276,#41844,#22777,.T.);
#55686=EDGE_CURVE('',#42277,#41428,#22778,.T.);
#55687=EDGE_CURVE('',#42278,#41427,#22779,.T.);
#55688=EDGE_CURVE('',#42272,#41426,#22780,.T.);
#55689=EDGE_CURVE('',#42273,#41425,#22781,.T.);
#55690=EDGE_CURVE('',#41847,#42274,#22782,.T.);
#55691=EDGE_CURVE('',#41846,#42275,#22783,.T.);
#55692=EDGE_CURVE('',#42285,#42286,#30261,.T.);
#55693=EDGE_CURVE('',#42286,#42287,#30262,.T.);
#55694=EDGE_CURVE('',#42287,#42288,#1324,.T.);
#55695=EDGE_CURVE('',#42288,#42289,#30263,.T.);
#55696=EDGE_CURVE('',#42289,#42285,#26308,.T.);
#55697=EDGE_CURVE('',#42290,#42291,#1325,.T.);
#55698=EDGE_CURVE('',#42291,#42292,#30264,.T.);
#55699=EDGE_CURVE('',#42293,#42292,#30265,.T.);
#55700=EDGE_CURVE('',#42293,#42294,#26309,.T.);
#55701=EDGE_CURVE('',#42294,#42290,#30266,.T.);
#55702=EDGE_CURVE('',#42292,#42295,#26310,.T.);
#55703=EDGE_CURVE('',#42295,#42286,#26311,.T.);
#55704=EDGE_CURVE('',#42285,#42296,#1326,.T.);
#55705=EDGE_CURVE('',#42296,#42293,#1327,.T.);
#55706=EDGE_CURVE('',#42294,#41312,#26312,.T.);
#55707=EDGE_CURVE('',#42297,#42293,#22784,.T.);
#55708=EDGE_CURVE('',#41312,#42297,#26313,.T.);
#55709=EDGE_CURVE('',#42298,#42285,#22785,.T.);
#55710=EDGE_CURVE('',#42297,#42298,#26314,.T.);
#55711=EDGE_CURVE('',#41311,#42289,#26315,.T.);
#55712=EDGE_CURVE('',#42298,#41311,#1328,.T.);
#55713=EDGE_CURVE('',#41841,#42294,#22786,.T.);
#55714=EDGE_CURVE('',#42290,#41840,#22787,.T.);
#55715=EDGE_CURVE('',#42291,#41432,#22788,.T.);
#55716=EDGE_CURVE('',#42292,#41431,#22789,.T.);
#55717=EDGE_CURVE('',#42286,#41430,#22790,.T.);
#55718=EDGE_CURVE('',#42287,#41429,#22791,.T.);
#55719=EDGE_CURVE('',#41843,#42288,#22792,.T.);
#55720=EDGE_CURVE('',#41842,#42289,#22793,.T.);
#55721=EDGE_CURVE('',#42299,#42300,#30267,.T.);
#55722=EDGE_CURVE('',#42300,#42301,#30268,.T.);
#55723=EDGE_CURVE('',#42301,#42302,#1329,.T.);
#55724=EDGE_CURVE('',#42302,#42303,#30269,.T.);
#55725=EDGE_CURVE('',#42303,#42299,#26316,.T.);
#55726=EDGE_CURVE('',#42304,#42305,#1330,.T.);
#55727=EDGE_CURVE('',#42305,#42306,#30270,.T.);
#55728=EDGE_CURVE('',#42307,#42306,#30271,.T.);
#55729=EDGE_CURVE('',#42307,#42308,#26317,.T.);
#55730=EDGE_CURVE('',#42308,#42304,#30272,.T.);
#55731=EDGE_CURVE('',#42306,#42309,#26318,.T.);
#55732=EDGE_CURVE('',#42309,#42300,#26319,.T.);
#55733=EDGE_CURVE('',#42299,#42310,#1331,.T.);
#55734=EDGE_CURVE('',#42310,#42307,#1332,.T.);
#55735=EDGE_CURVE('',#42308,#41308,#26320,.T.);
#55736=EDGE_CURVE('',#42311,#42307,#22794,.T.);
#55737=EDGE_CURVE('',#41308,#42311,#26321,.T.);
#55738=EDGE_CURVE('',#42312,#42299,#22795,.T.);
#55739=EDGE_CURVE('',#42311,#42312,#26322,.T.);
#55740=EDGE_CURVE('',#41307,#42303,#26323,.T.);
#55741=EDGE_CURVE('',#42312,#41307,#1333,.T.);
#55742=EDGE_CURVE('',#41837,#42308,#22796,.T.);
#55743=EDGE_CURVE('',#42304,#41836,#22797,.T.);
#55744=EDGE_CURVE('',#42305,#41436,#22798,.T.);
#55745=EDGE_CURVE('',#42306,#41435,#22799,.T.);
#55746=EDGE_CURVE('',#42300,#41434,#22800,.T.);
#55747=EDGE_CURVE('',#42301,#41433,#22801,.T.);
#55748=EDGE_CURVE('',#41839,#42302,#22802,.T.);
#55749=EDGE_CURVE('',#41838,#42303,#22803,.T.);
#55750=EDGE_CURVE('',#42313,#42314,#30273,.T.);
#55751=EDGE_CURVE('',#42314,#42315,#30274,.T.);
#55752=EDGE_CURVE('',#42315,#42316,#1334,.T.);
#55753=EDGE_CURVE('',#42316,#42317,#30275,.T.);
#55754=EDGE_CURVE('',#42317,#42313,#26324,.T.);
#55755=EDGE_CURVE('',#42318,#42319,#1335,.T.);
#55756=EDGE_CURVE('',#42319,#42320,#30276,.T.);
#55757=EDGE_CURVE('',#42321,#42320,#30277,.T.);
#55758=EDGE_CURVE('',#42321,#42322,#26325,.T.);
#55759=EDGE_CURVE('',#42322,#42318,#30278,.T.);
#55760=EDGE_CURVE('',#42320,#42323,#26326,.T.);
#55761=EDGE_CURVE('',#42323,#42314,#26327,.T.);
#55762=EDGE_CURVE('',#42313,#42324,#1336,.T.);
#55763=EDGE_CURVE('',#42324,#42321,#1337,.T.);
#55764=EDGE_CURVE('',#42322,#41304,#26328,.T.);
#55765=EDGE_CURVE('',#42325,#42321,#22804,.T.);
#55766=EDGE_CURVE('',#41304,#42325,#26329,.T.);
#55767=EDGE_CURVE('',#42326,#42313,#22805,.T.);
#55768=EDGE_CURVE('',#42325,#42326,#26330,.T.);
#55769=EDGE_CURVE('',#41303,#42317,#26331,.T.);
#55770=EDGE_CURVE('',#42326,#41303,#1338,.T.);
#55771=EDGE_CURVE('',#41833,#42322,#22806,.T.);
#55772=EDGE_CURVE('',#42318,#41832,#22807,.T.);
#55773=EDGE_CURVE('',#42319,#41440,#22808,.T.);
#55774=EDGE_CURVE('',#42320,#41439,#22809,.T.);
#55775=EDGE_CURVE('',#42314,#41438,#22810,.T.);
#55776=EDGE_CURVE('',#42315,#41437,#22811,.T.);
#55777=EDGE_CURVE('',#41835,#42316,#22812,.T.);
#55778=EDGE_CURVE('',#41834,#42317,#22813,.T.);
#55779=EDGE_CURVE('',#42327,#42328,#30279,.T.);
#55780=EDGE_CURVE('',#42328,#42329,#30280,.T.);
#55781=EDGE_CURVE('',#42329,#42330,#1339,.T.);
#55782=EDGE_CURVE('',#42330,#42331,#30281,.T.);
#55783=EDGE_CURVE('',#42331,#42327,#26332,.T.);
#55784=EDGE_CURVE('',#42332,#42333,#1340,.T.);
#55785=EDGE_CURVE('',#42333,#42334,#30282,.T.);
#55786=EDGE_CURVE('',#42335,#42334,#30283,.T.);
#55787=EDGE_CURVE('',#42335,#42336,#26333,.T.);
#55788=EDGE_CURVE('',#42336,#42332,#30284,.T.);
#55789=EDGE_CURVE('',#42334,#42337,#26334,.T.);
#55790=EDGE_CURVE('',#42337,#42328,#26335,.T.);
#55791=EDGE_CURVE('',#42327,#42338,#1341,.T.);
#55792=EDGE_CURVE('',#42338,#42335,#1342,.T.);
#55793=EDGE_CURVE('',#42336,#41300,#26336,.T.);
#55794=EDGE_CURVE('',#42339,#42335,#22814,.T.);
#55795=EDGE_CURVE('',#41300,#42339,#26337,.T.);
#55796=EDGE_CURVE('',#42340,#42327,#22815,.T.);
#55797=EDGE_CURVE('',#42339,#42340,#26338,.T.);
#55798=EDGE_CURVE('',#41299,#42331,#26339,.T.);
#55799=EDGE_CURVE('',#42340,#41299,#1343,.T.);
#55800=EDGE_CURVE('',#41829,#42336,#22816,.T.);
#55801=EDGE_CURVE('',#42332,#41828,#22817,.T.);
#55802=EDGE_CURVE('',#42333,#41444,#22818,.T.);
#55803=EDGE_CURVE('',#42334,#41443,#22819,.T.);
#55804=EDGE_CURVE('',#42328,#41442,#22820,.T.);
#55805=EDGE_CURVE('',#42329,#41441,#22821,.T.);
#55806=EDGE_CURVE('',#41831,#42330,#22822,.T.);
#55807=EDGE_CURVE('',#41830,#42331,#22823,.T.);
#55808=EDGE_CURVE('',#42341,#42342,#30285,.T.);
#55809=EDGE_CURVE('',#42342,#42343,#30286,.T.);
#55810=EDGE_CURVE('',#42343,#42344,#1344,.T.);
#55811=EDGE_CURVE('',#42344,#42345,#30287,.T.);
#55812=EDGE_CURVE('',#42345,#42341,#26340,.T.);
#55813=EDGE_CURVE('',#42346,#42347,#1345,.T.);
#55814=EDGE_CURVE('',#42347,#42348,#30288,.T.);
#55815=EDGE_CURVE('',#42349,#42348,#30289,.T.);
#55816=EDGE_CURVE('',#42349,#42350,#26341,.T.);
#55817=EDGE_CURVE('',#42350,#42346,#30290,.T.);
#55818=EDGE_CURVE('',#42348,#42351,#26342,.T.);
#55819=EDGE_CURVE('',#42351,#42342,#26343,.T.);
#55820=EDGE_CURVE('',#42341,#42352,#1346,.T.);
#55821=EDGE_CURVE('',#42352,#42349,#1347,.T.);
#55822=EDGE_CURVE('',#42350,#41296,#26344,.T.);
#55823=EDGE_CURVE('',#42353,#42349,#22824,.T.);
#55824=EDGE_CURVE('',#41296,#42353,#26345,.T.);
#55825=EDGE_CURVE('',#42354,#42341,#22825,.T.);
#55826=EDGE_CURVE('',#42353,#42354,#26346,.T.);
#55827=EDGE_CURVE('',#41295,#42345,#26347,.T.);
#55828=EDGE_CURVE('',#42354,#41295,#1348,.T.);
#55829=EDGE_CURVE('',#41825,#42350,#22826,.T.);
#55830=EDGE_CURVE('',#42346,#41824,#22827,.T.);
#55831=EDGE_CURVE('',#42347,#41448,#22828,.T.);
#55832=EDGE_CURVE('',#42348,#41447,#22829,.T.);
#55833=EDGE_CURVE('',#42342,#41446,#22830,.T.);
#55834=EDGE_CURVE('',#42343,#41445,#22831,.T.);
#55835=EDGE_CURVE('',#41827,#42344,#22832,.T.);
#55836=EDGE_CURVE('',#41826,#42345,#22833,.T.);
#55837=EDGE_CURVE('',#42355,#42356,#30291,.T.);
#55838=EDGE_CURVE('',#42356,#42357,#30292,.T.);
#55839=EDGE_CURVE('',#42357,#42358,#1349,.T.);
#55840=EDGE_CURVE('',#42358,#42359,#30293,.T.);
#55841=EDGE_CURVE('',#42359,#42355,#26348,.T.);
#55842=EDGE_CURVE('',#42360,#42361,#1350,.T.);
#55843=EDGE_CURVE('',#42361,#42362,#30294,.T.);
#55844=EDGE_CURVE('',#42363,#42362,#30295,.T.);
#55845=EDGE_CURVE('',#42363,#42364,#26349,.T.);
#55846=EDGE_CURVE('',#42364,#42360,#30296,.T.);
#55847=EDGE_CURVE('',#42362,#42365,#26350,.T.);
#55848=EDGE_CURVE('',#42365,#42356,#26351,.T.);
#55849=EDGE_CURVE('',#42355,#42366,#1351,.T.);
#55850=EDGE_CURVE('',#42366,#42363,#1352,.T.);
#55851=EDGE_CURVE('',#42364,#41292,#26352,.T.);
#55852=EDGE_CURVE('',#42367,#42363,#22834,.T.);
#55853=EDGE_CURVE('',#41292,#42367,#26353,.T.);
#55854=EDGE_CURVE('',#42368,#42355,#22835,.T.);
#55855=EDGE_CURVE('',#42367,#42368,#26354,.T.);
#55856=EDGE_CURVE('',#41291,#42359,#26355,.T.);
#55857=EDGE_CURVE('',#42368,#41291,#1353,.T.);
#55858=EDGE_CURVE('',#41821,#42364,#22836,.T.);
#55859=EDGE_CURVE('',#42360,#41820,#22837,.T.);
#55860=EDGE_CURVE('',#42361,#41452,#22838,.T.);
#55861=EDGE_CURVE('',#42362,#41451,#22839,.T.);
#55862=EDGE_CURVE('',#42356,#41450,#22840,.T.);
#55863=EDGE_CURVE('',#42357,#41449,#22841,.T.);
#55864=EDGE_CURVE('',#41823,#42358,#22842,.T.);
#55865=EDGE_CURVE('',#41822,#42359,#22843,.T.);
#55866=EDGE_CURVE('',#42369,#42370,#30297,.T.);
#55867=EDGE_CURVE('',#42370,#42371,#30298,.T.);
#55868=EDGE_CURVE('',#42371,#42372,#1354,.T.);
#55869=EDGE_CURVE('',#42372,#42373,#30299,.T.);
#55870=EDGE_CURVE('',#42373,#42369,#26356,.T.);
#55871=EDGE_CURVE('',#42374,#42375,#1355,.T.);
#55872=EDGE_CURVE('',#42375,#42376,#30300,.T.);
#55873=EDGE_CURVE('',#42377,#42376,#30301,.T.);
#55874=EDGE_CURVE('',#42377,#42378,#26357,.T.);
#55875=EDGE_CURVE('',#42378,#42374,#30302,.T.);
#55876=EDGE_CURVE('',#42376,#42379,#26358,.T.);
#55877=EDGE_CURVE('',#42379,#42370,#26359,.T.);
#55878=EDGE_CURVE('',#42369,#42380,#1356,.T.);
#55879=EDGE_CURVE('',#42380,#42377,#1357,.T.);
#55880=EDGE_CURVE('',#42378,#41288,#26360,.T.);
#55881=EDGE_CURVE('',#42381,#42377,#22844,.T.);
#55882=EDGE_CURVE('',#41288,#42381,#26361,.T.);
#55883=EDGE_CURVE('',#42382,#42369,#22845,.T.);
#55884=EDGE_CURVE('',#42381,#42382,#26362,.T.);
#55885=EDGE_CURVE('',#41287,#42373,#26363,.T.);
#55886=EDGE_CURVE('',#42382,#41287,#1358,.T.);
#55887=EDGE_CURVE('',#41817,#42378,#22846,.T.);
#55888=EDGE_CURVE('',#42374,#41816,#22847,.T.);
#55889=EDGE_CURVE('',#42375,#41456,#22848,.T.);
#55890=EDGE_CURVE('',#42376,#41455,#22849,.T.);
#55891=EDGE_CURVE('',#42370,#41454,#22850,.T.);
#55892=EDGE_CURVE('',#42371,#41453,#22851,.T.);
#55893=EDGE_CURVE('',#41819,#42372,#22852,.T.);
#55894=EDGE_CURVE('',#41818,#42373,#22853,.T.);
#55895=EDGE_CURVE('',#42383,#42384,#30303,.T.);
#55896=EDGE_CURVE('',#42384,#42385,#30304,.T.);
#55897=EDGE_CURVE('',#42385,#42386,#1359,.T.);
#55898=EDGE_CURVE('',#42386,#42387,#30305,.T.);
#55899=EDGE_CURVE('',#42387,#42383,#26364,.T.);
#55900=EDGE_CURVE('',#42388,#42389,#1360,.T.);
#55901=EDGE_CURVE('',#42389,#42390,#30306,.T.);
#55902=EDGE_CURVE('',#42391,#42390,#30307,.T.);
#55903=EDGE_CURVE('',#42391,#42392,#26365,.T.);
#55904=EDGE_CURVE('',#42392,#42388,#30308,.T.);
#55905=EDGE_CURVE('',#42390,#42393,#26366,.T.);
#55906=EDGE_CURVE('',#42393,#42384,#26367,.T.);
#55907=EDGE_CURVE('',#42383,#42394,#1361,.T.);
#55908=EDGE_CURVE('',#42394,#42391,#1362,.T.);
#55909=EDGE_CURVE('',#42392,#41284,#26368,.T.);
#55910=EDGE_CURVE('',#42395,#42391,#22854,.T.);
#55911=EDGE_CURVE('',#41284,#42395,#26369,.T.);
#55912=EDGE_CURVE('',#42396,#42383,#22855,.T.);
#55913=EDGE_CURVE('',#42395,#42396,#26370,.T.);
#55914=EDGE_CURVE('',#41283,#42387,#26371,.T.);
#55915=EDGE_CURVE('',#42396,#41283,#1363,.T.);
#55916=EDGE_CURVE('',#41813,#42392,#22856,.T.);
#55917=EDGE_CURVE('',#42388,#41812,#22857,.T.);
#55918=EDGE_CURVE('',#42389,#41460,#22858,.T.);
#55919=EDGE_CURVE('',#42390,#41459,#22859,.T.);
#55920=EDGE_CURVE('',#42384,#41458,#22860,.T.);
#55921=EDGE_CURVE('',#42385,#41457,#22861,.T.);
#55922=EDGE_CURVE('',#41815,#42386,#22862,.T.);
#55923=EDGE_CURVE('',#41814,#42387,#22863,.T.);
#55924=EDGE_CURVE('',#42397,#42398,#30309,.T.);
#55925=EDGE_CURVE('',#42398,#42399,#30310,.T.);
#55926=EDGE_CURVE('',#42399,#42400,#1364,.T.);
#55927=EDGE_CURVE('',#42400,#42401,#30311,.T.);
#55928=EDGE_CURVE('',#42401,#42397,#26372,.T.);
#55929=EDGE_CURVE('',#42402,#42403,#1365,.T.);
#55930=EDGE_CURVE('',#42403,#42404,#30312,.T.);
#55931=EDGE_CURVE('',#42405,#42404,#30313,.T.);
#55932=EDGE_CURVE('',#42405,#42406,#26373,.T.);
#55933=EDGE_CURVE('',#42406,#42402,#30314,.T.);
#55934=EDGE_CURVE('',#42404,#42407,#26374,.T.);
#55935=EDGE_CURVE('',#42407,#42398,#26375,.T.);
#55936=EDGE_CURVE('',#42397,#42408,#1366,.T.);
#55937=EDGE_CURVE('',#42408,#42405,#1367,.T.);
#55938=EDGE_CURVE('',#42406,#41280,#26376,.T.);
#55939=EDGE_CURVE('',#42409,#42405,#22864,.T.);
#55940=EDGE_CURVE('',#41280,#42409,#26377,.T.);
#55941=EDGE_CURVE('',#42410,#42397,#22865,.T.);
#55942=EDGE_CURVE('',#42409,#42410,#26378,.T.);
#55943=EDGE_CURVE('',#41279,#42401,#26379,.T.);
#55944=EDGE_CURVE('',#42410,#41279,#1368,.T.);
#55945=EDGE_CURVE('',#41809,#42406,#22866,.T.);
#55946=EDGE_CURVE('',#42402,#41808,#22867,.T.);
#55947=EDGE_CURVE('',#42403,#41464,#22868,.T.);
#55948=EDGE_CURVE('',#42404,#41463,#22869,.T.);
#55949=EDGE_CURVE('',#42398,#41462,#22870,.T.);
#55950=EDGE_CURVE('',#42399,#41461,#22871,.T.);
#55951=EDGE_CURVE('',#41811,#42400,#22872,.T.);
#55952=EDGE_CURVE('',#41810,#42401,#22873,.T.);
#55953=EDGE_CURVE('',#42411,#42412,#30315,.T.);
#55954=EDGE_CURVE('',#42412,#42413,#30316,.T.);
#55955=EDGE_CURVE('',#42413,#42414,#1369,.T.);
#55956=EDGE_CURVE('',#42414,#42415,#30317,.T.);
#55957=EDGE_CURVE('',#42415,#42411,#26380,.T.);
#55958=EDGE_CURVE('',#42416,#42417,#1370,.T.);
#55959=EDGE_CURVE('',#42417,#42418,#30318,.T.);
#55960=EDGE_CURVE('',#42419,#42418,#30319,.T.);
#55961=EDGE_CURVE('',#42419,#42420,#26381,.T.);
#55962=EDGE_CURVE('',#42420,#42416,#30320,.T.);
#55963=EDGE_CURVE('',#42418,#42421,#26382,.T.);
#55964=EDGE_CURVE('',#42421,#42412,#26383,.T.);
#55965=EDGE_CURVE('',#42411,#42422,#1371,.T.);
#55966=EDGE_CURVE('',#42422,#42419,#1372,.T.);
#55967=EDGE_CURVE('',#42420,#41276,#26384,.T.);
#55968=EDGE_CURVE('',#42423,#42419,#22874,.T.);
#55969=EDGE_CURVE('',#41276,#42423,#26385,.T.);
#55970=EDGE_CURVE('',#42424,#42411,#22875,.T.);
#55971=EDGE_CURVE('',#42423,#42424,#26386,.T.);
#55972=EDGE_CURVE('',#41275,#42415,#26387,.T.);
#55973=EDGE_CURVE('',#42424,#41275,#1373,.T.);
#55974=EDGE_CURVE('',#41805,#42420,#22876,.T.);
#55975=EDGE_CURVE('',#42416,#41804,#22877,.T.);
#55976=EDGE_CURVE('',#42417,#41468,#22878,.T.);
#55977=EDGE_CURVE('',#42418,#41467,#22879,.T.);
#55978=EDGE_CURVE('',#42412,#41466,#22880,.T.);
#55979=EDGE_CURVE('',#42413,#41465,#22881,.T.);
#55980=EDGE_CURVE('',#41807,#42414,#22882,.T.);
#55981=EDGE_CURVE('',#41806,#42415,#22883,.T.);
#55982=EDGE_CURVE('',#42425,#42426,#30321,.T.);
#55983=EDGE_CURVE('',#42426,#42427,#30322,.T.);
#55984=EDGE_CURVE('',#42427,#42428,#1374,.T.);
#55985=EDGE_CURVE('',#42428,#42429,#30323,.T.);
#55986=EDGE_CURVE('',#42429,#42425,#26388,.T.);
#55987=EDGE_CURVE('',#42430,#42431,#1375,.T.);
#55988=EDGE_CURVE('',#42431,#42432,#30324,.T.);
#55989=EDGE_CURVE('',#42433,#42432,#30325,.T.);
#55990=EDGE_CURVE('',#42433,#42434,#26389,.T.);
#55991=EDGE_CURVE('',#42434,#42430,#30326,.T.);
#55992=EDGE_CURVE('',#42432,#42435,#26390,.T.);
#55993=EDGE_CURVE('',#42435,#42426,#26391,.T.);
#55994=EDGE_CURVE('',#42425,#42436,#1376,.T.);
#55995=EDGE_CURVE('',#42436,#42433,#1377,.T.);
#55996=EDGE_CURVE('',#42434,#41272,#26392,.T.);
#55997=EDGE_CURVE('',#42437,#42433,#22884,.T.);
#55998=EDGE_CURVE('',#41272,#42437,#26393,.T.);
#55999=EDGE_CURVE('',#42438,#42425,#22885,.T.);
#56000=EDGE_CURVE('',#42437,#42438,#26394,.T.);
#56001=EDGE_CURVE('',#41271,#42429,#26395,.T.);
#56002=EDGE_CURVE('',#42438,#41271,#1378,.T.);
#56003=EDGE_CURVE('',#41801,#42434,#22886,.T.);
#56004=EDGE_CURVE('',#42430,#41800,#22887,.T.);
#56005=EDGE_CURVE('',#42431,#41472,#22888,.T.);
#56006=EDGE_CURVE('',#42432,#41471,#22889,.T.);
#56007=EDGE_CURVE('',#42426,#41470,#22890,.T.);
#56008=EDGE_CURVE('',#42427,#41469,#22891,.T.);
#56009=EDGE_CURVE('',#41803,#42428,#22892,.T.);
#56010=EDGE_CURVE('',#41802,#42429,#22893,.T.);
#56011=EDGE_CURVE('',#42439,#42440,#30327,.T.);
#56012=EDGE_CURVE('',#42440,#42441,#30328,.T.);
#56013=EDGE_CURVE('',#42441,#42442,#1379,.T.);
#56014=EDGE_CURVE('',#42442,#42443,#30329,.T.);
#56015=EDGE_CURVE('',#42443,#42439,#26396,.T.);
#56016=EDGE_CURVE('',#42444,#42445,#1380,.T.);
#56017=EDGE_CURVE('',#42445,#42446,#30330,.T.);
#56018=EDGE_CURVE('',#42447,#42446,#30331,.T.);
#56019=EDGE_CURVE('',#42447,#42448,#26397,.T.);
#56020=EDGE_CURVE('',#42448,#42444,#30332,.T.);
#56021=EDGE_CURVE('',#42446,#42449,#26398,.T.);
#56022=EDGE_CURVE('',#42449,#42440,#26399,.T.);
#56023=EDGE_CURVE('',#42439,#42450,#1381,.T.);
#56024=EDGE_CURVE('',#42450,#42447,#1382,.T.);
#56025=EDGE_CURVE('',#42448,#41268,#26400,.T.);
#56026=EDGE_CURVE('',#42451,#42447,#22894,.T.);
#56027=EDGE_CURVE('',#41268,#42451,#26401,.T.);
#56028=EDGE_CURVE('',#42452,#42439,#22895,.T.);
#56029=EDGE_CURVE('',#42451,#42452,#26402,.T.);
#56030=EDGE_CURVE('',#41267,#42443,#26403,.T.);
#56031=EDGE_CURVE('',#42452,#41267,#1383,.T.);
#56032=EDGE_CURVE('',#41797,#42448,#22896,.T.);
#56033=EDGE_CURVE('',#42444,#41796,#22897,.T.);
#56034=EDGE_CURVE('',#42445,#41476,#22898,.T.);
#56035=EDGE_CURVE('',#42446,#41475,#22899,.T.);
#56036=EDGE_CURVE('',#42440,#41474,#22900,.T.);
#56037=EDGE_CURVE('',#42441,#41473,#22901,.T.);
#56038=EDGE_CURVE('',#41799,#42442,#22902,.T.);
#56039=EDGE_CURVE('',#41798,#42443,#22903,.T.);
#56040=EDGE_CURVE('',#42453,#42454,#30333,.T.);
#56041=EDGE_CURVE('',#42454,#42455,#30334,.T.);
#56042=EDGE_CURVE('',#42455,#42456,#1384,.T.);
#56043=EDGE_CURVE('',#42456,#42457,#30335,.T.);
#56044=EDGE_CURVE('',#42457,#42453,#26404,.T.);
#56045=EDGE_CURVE('',#42458,#42459,#1385,.T.);
#56046=EDGE_CURVE('',#42459,#42460,#30336,.T.);
#56047=EDGE_CURVE('',#42461,#42460,#30337,.T.);
#56048=EDGE_CURVE('',#42461,#42462,#26405,.T.);
#56049=EDGE_CURVE('',#42462,#42458,#30338,.T.);
#56050=EDGE_CURVE('',#42460,#42463,#26406,.T.);
#56051=EDGE_CURVE('',#42463,#42454,#26407,.T.);
#56052=EDGE_CURVE('',#42453,#42464,#1386,.T.);
#56053=EDGE_CURVE('',#42464,#42461,#1387,.T.);
#56054=EDGE_CURVE('',#42462,#41264,#26408,.T.);
#56055=EDGE_CURVE('',#42465,#42461,#22904,.T.);
#56056=EDGE_CURVE('',#41264,#42465,#26409,.T.);
#56057=EDGE_CURVE('',#42466,#42453,#22905,.T.);
#56058=EDGE_CURVE('',#42465,#42466,#26410,.T.);
#56059=EDGE_CURVE('',#41263,#42457,#26411,.T.);
#56060=EDGE_CURVE('',#42466,#41263,#1388,.T.);
#56061=EDGE_CURVE('',#41793,#42462,#22906,.T.);
#56062=EDGE_CURVE('',#42458,#41792,#22907,.T.);
#56063=EDGE_CURVE('',#42459,#41480,#22908,.T.);
#56064=EDGE_CURVE('',#42460,#41479,#22909,.T.);
#56065=EDGE_CURVE('',#42454,#41478,#22910,.T.);
#56066=EDGE_CURVE('',#42455,#41477,#22911,.T.);
#56067=EDGE_CURVE('',#41795,#42456,#22912,.T.);
#56068=EDGE_CURVE('',#41794,#42457,#22913,.T.);
#56069=EDGE_CURVE('',#42467,#42468,#30339,.T.);
#56070=EDGE_CURVE('',#42468,#42469,#30340,.T.);
#56071=EDGE_CURVE('',#42469,#42470,#1389,.T.);
#56072=EDGE_CURVE('',#42470,#42471,#30341,.T.);
#56073=EDGE_CURVE('',#42471,#42467,#26412,.T.);
#56074=EDGE_CURVE('',#42472,#42473,#1390,.T.);
#56075=EDGE_CURVE('',#42473,#42474,#30342,.T.);
#56076=EDGE_CURVE('',#42475,#42474,#30343,.T.);
#56077=EDGE_CURVE('',#42475,#42476,#26413,.T.);
#56078=EDGE_CURVE('',#42476,#42472,#30344,.T.);
#56079=EDGE_CURVE('',#42474,#42477,#26414,.T.);
#56080=EDGE_CURVE('',#42477,#42468,#26415,.T.);
#56081=EDGE_CURVE('',#42467,#42478,#1391,.T.);
#56082=EDGE_CURVE('',#42478,#42475,#1392,.T.);
#56083=EDGE_CURVE('',#42476,#41260,#26416,.T.);
#56084=EDGE_CURVE('',#42479,#42475,#22914,.T.);
#56085=EDGE_CURVE('',#41260,#42479,#26417,.T.);
#56086=EDGE_CURVE('',#42480,#42467,#22915,.T.);
#56087=EDGE_CURVE('',#42479,#42480,#26418,.T.);
#56088=EDGE_CURVE('',#41259,#42471,#26419,.T.);
#56089=EDGE_CURVE('',#42480,#41259,#1393,.T.);
#56090=EDGE_CURVE('',#41789,#42476,#22916,.T.);
#56091=EDGE_CURVE('',#42472,#41788,#22917,.T.);
#56092=EDGE_CURVE('',#42473,#41484,#22918,.T.);
#56093=EDGE_CURVE('',#42474,#41483,#22919,.T.);
#56094=EDGE_CURVE('',#42468,#41482,#22920,.T.);
#56095=EDGE_CURVE('',#42469,#41481,#22921,.T.);
#56096=EDGE_CURVE('',#41791,#42470,#22922,.T.);
#56097=EDGE_CURVE('',#41790,#42471,#22923,.T.);
#56098=EDGE_CURVE('',#42481,#42482,#30345,.T.);
#56099=EDGE_CURVE('',#42482,#42483,#30346,.T.);
#56100=EDGE_CURVE('',#42483,#42484,#1394,.T.);
#56101=EDGE_CURVE('',#42484,#42485,#30347,.T.);
#56102=EDGE_CURVE('',#42485,#42481,#26420,.T.);
#56103=EDGE_CURVE('',#42486,#42487,#1395,.T.);
#56104=EDGE_CURVE('',#42487,#42488,#30348,.T.);
#56105=EDGE_CURVE('',#42489,#42488,#30349,.T.);
#56106=EDGE_CURVE('',#42489,#42490,#26421,.T.);
#56107=EDGE_CURVE('',#42490,#42486,#30350,.T.);
#56108=EDGE_CURVE('',#42488,#42491,#26422,.T.);
#56109=EDGE_CURVE('',#42491,#42482,#26423,.T.);
#56110=EDGE_CURVE('',#42481,#42492,#1396,.T.);
#56111=EDGE_CURVE('',#42492,#42489,#1397,.T.);
#56112=EDGE_CURVE('',#42490,#41256,#26424,.T.);
#56113=EDGE_CURVE('',#42493,#42489,#22924,.T.);
#56114=EDGE_CURVE('',#41256,#42493,#26425,.T.);
#56115=EDGE_CURVE('',#42494,#42481,#22925,.T.);
#56116=EDGE_CURVE('',#42493,#42494,#26426,.T.);
#56117=EDGE_CURVE('',#41255,#42485,#26427,.T.);
#56118=EDGE_CURVE('',#42494,#41255,#1398,.T.);
#56119=EDGE_CURVE('',#41785,#42490,#22926,.T.);
#56120=EDGE_CURVE('',#42486,#41784,#22927,.T.);
#56121=EDGE_CURVE('',#42487,#41488,#22928,.T.);
#56122=EDGE_CURVE('',#42488,#41487,#22929,.T.);
#56123=EDGE_CURVE('',#42482,#41486,#22930,.T.);
#56124=EDGE_CURVE('',#42483,#41485,#22931,.T.);
#56125=EDGE_CURVE('',#41787,#42484,#22932,.T.);
#56126=EDGE_CURVE('',#41786,#42485,#22933,.T.);
#56127=EDGE_CURVE('',#42495,#42496,#30351,.T.);
#56128=EDGE_CURVE('',#42496,#42497,#30352,.T.);
#56129=EDGE_CURVE('',#42497,#42498,#1399,.T.);
#56130=EDGE_CURVE('',#42498,#42499,#30353,.T.);
#56131=EDGE_CURVE('',#42499,#42495,#26428,.T.);
#56132=EDGE_CURVE('',#42500,#42501,#1400,.T.);
#56133=EDGE_CURVE('',#42501,#42502,#30354,.T.);
#56134=EDGE_CURVE('',#42503,#42502,#30355,.T.);
#56135=EDGE_CURVE('',#42503,#42504,#26429,.T.);
#56136=EDGE_CURVE('',#42504,#42500,#30356,.T.);
#56137=EDGE_CURVE('',#42502,#42505,#26430,.T.);
#56138=EDGE_CURVE('',#42505,#42496,#26431,.T.);
#56139=EDGE_CURVE('',#42495,#42506,#1401,.T.);
#56140=EDGE_CURVE('',#42506,#42503,#1402,.T.);
#56141=EDGE_CURVE('',#42504,#41252,#26432,.T.);
#56142=EDGE_CURVE('',#42507,#42503,#22934,.T.);
#56143=EDGE_CURVE('',#41252,#42507,#26433,.T.);
#56144=EDGE_CURVE('',#42508,#42495,#22935,.T.);
#56145=EDGE_CURVE('',#42507,#42508,#26434,.T.);
#56146=EDGE_CURVE('',#41251,#42499,#26435,.T.);
#56147=EDGE_CURVE('',#42508,#41251,#1403,.T.);
#56148=EDGE_CURVE('',#41781,#42504,#22936,.T.);
#56149=EDGE_CURVE('',#42500,#41780,#22937,.T.);
#56150=EDGE_CURVE('',#42501,#41492,#22938,.T.);
#56151=EDGE_CURVE('',#42502,#41491,#22939,.T.);
#56152=EDGE_CURVE('',#42496,#41490,#22940,.T.);
#56153=EDGE_CURVE('',#42497,#41489,#22941,.T.);
#56154=EDGE_CURVE('',#41783,#42498,#22942,.T.);
#56155=EDGE_CURVE('',#41782,#42499,#22943,.T.);
#56156=EDGE_CURVE('',#42509,#42510,#30357,.T.);
#56157=EDGE_CURVE('',#42510,#42511,#30358,.T.);
#56158=EDGE_CURVE('',#42511,#42512,#1404,.T.);
#56159=EDGE_CURVE('',#42512,#42513,#30359,.T.);
#56160=EDGE_CURVE('',#42513,#42509,#26436,.T.);
#56161=EDGE_CURVE('',#42514,#42515,#1405,.T.);
#56162=EDGE_CURVE('',#42515,#42516,#30360,.T.);
#56163=EDGE_CURVE('',#42517,#42516,#30361,.T.);
#56164=EDGE_CURVE('',#42517,#42518,#26437,.T.);
#56165=EDGE_CURVE('',#42518,#42514,#30362,.T.);
#56166=EDGE_CURVE('',#42516,#42519,#26438,.T.);
#56167=EDGE_CURVE('',#42519,#42510,#26439,.T.);
#56168=EDGE_CURVE('',#42509,#42520,#1406,.T.);
#56169=EDGE_CURVE('',#42520,#42517,#1407,.T.);
#56170=EDGE_CURVE('',#42518,#41248,#26440,.T.);
#56171=EDGE_CURVE('',#42521,#42517,#22944,.T.);
#56172=EDGE_CURVE('',#41248,#42521,#26441,.T.);
#56173=EDGE_CURVE('',#42522,#42509,#22945,.T.);
#56174=EDGE_CURVE('',#42521,#42522,#26442,.T.);
#56175=EDGE_CURVE('',#41247,#42513,#26443,.T.);
#56176=EDGE_CURVE('',#42522,#41247,#1408,.T.);
#56177=EDGE_CURVE('',#41777,#42518,#22946,.T.);
#56178=EDGE_CURVE('',#42514,#41776,#22947,.T.);
#56179=EDGE_CURVE('',#42515,#41496,#22948,.T.);
#56180=EDGE_CURVE('',#42516,#41495,#22949,.T.);
#56181=EDGE_CURVE('',#42510,#41494,#22950,.T.);
#56182=EDGE_CURVE('',#42511,#41493,#22951,.T.);
#56183=EDGE_CURVE('',#41779,#42512,#22952,.T.);
#56184=EDGE_CURVE('',#41778,#42513,#22953,.T.);
#56185=EDGE_CURVE('',#42523,#42524,#30363,.T.);
#56186=EDGE_CURVE('',#42524,#42525,#30364,.T.);
#56187=EDGE_CURVE('',#42525,#42526,#1409,.T.);
#56188=EDGE_CURVE('',#42526,#42527,#30365,.T.);
#56189=EDGE_CURVE('',#42527,#42523,#26444,.T.);
#56190=EDGE_CURVE('',#42528,#42529,#1410,.T.);
#56191=EDGE_CURVE('',#42529,#42530,#30366,.T.);
#56192=EDGE_CURVE('',#42531,#42530,#30367,.T.);
#56193=EDGE_CURVE('',#42531,#42532,#26445,.T.);
#56194=EDGE_CURVE('',#42532,#42528,#30368,.T.);
#56195=EDGE_CURVE('',#42530,#42533,#26446,.T.);
#56196=EDGE_CURVE('',#42533,#42524,#26447,.T.);
#56197=EDGE_CURVE('',#42523,#42534,#1411,.T.);
#56198=EDGE_CURVE('',#42534,#42531,#1412,.T.);
#56199=EDGE_CURVE('',#42532,#41244,#26448,.T.);
#56200=EDGE_CURVE('',#42535,#42531,#22954,.T.);
#56201=EDGE_CURVE('',#41244,#42535,#26449,.T.);
#56202=EDGE_CURVE('',#42536,#42523,#22955,.T.);
#56203=EDGE_CURVE('',#42535,#42536,#26450,.T.);
#56204=EDGE_CURVE('',#41243,#42527,#26451,.T.);
#56205=EDGE_CURVE('',#42536,#41243,#1413,.T.);
#56206=EDGE_CURVE('',#41773,#42532,#22956,.T.);
#56207=EDGE_CURVE('',#42528,#41772,#22957,.T.);
#56208=EDGE_CURVE('',#42529,#41500,#22958,.T.);
#56209=EDGE_CURVE('',#42530,#41499,#22959,.T.);
#56210=EDGE_CURVE('',#42524,#41498,#22960,.T.);
#56211=EDGE_CURVE('',#42525,#41497,#22961,.T.);
#56212=EDGE_CURVE('',#41775,#42526,#22962,.T.);
#56213=EDGE_CURVE('',#41774,#42527,#22963,.T.);
#56214=EDGE_CURVE('',#42537,#42538,#30369,.T.);
#56215=EDGE_CURVE('',#42538,#42539,#30370,.T.);
#56216=EDGE_CURVE('',#42539,#42540,#1414,.T.);
#56217=EDGE_CURVE('',#42540,#42541,#30371,.T.);
#56218=EDGE_CURVE('',#42541,#42537,#26452,.T.);
#56219=EDGE_CURVE('',#42542,#42543,#1415,.T.);
#56220=EDGE_CURVE('',#42543,#42544,#30372,.T.);
#56221=EDGE_CURVE('',#42545,#42544,#30373,.T.);
#56222=EDGE_CURVE('',#42545,#42546,#26453,.T.);
#56223=EDGE_CURVE('',#42546,#42542,#30374,.T.);
#56224=EDGE_CURVE('',#42544,#42547,#26454,.T.);
#56225=EDGE_CURVE('',#42547,#42538,#26455,.T.);
#56226=EDGE_CURVE('',#42537,#42548,#1416,.T.);
#56227=EDGE_CURVE('',#42548,#42545,#1417,.T.);
#56228=EDGE_CURVE('',#42546,#41240,#26456,.T.);
#56229=EDGE_CURVE('',#42549,#42545,#22964,.T.);
#56230=EDGE_CURVE('',#41240,#42549,#26457,.T.);
#56231=EDGE_CURVE('',#42550,#42537,#22965,.T.);
#56232=EDGE_CURVE('',#42549,#42550,#26458,.T.);
#56233=EDGE_CURVE('',#41239,#42541,#26459,.T.);
#56234=EDGE_CURVE('',#42550,#41239,#1418,.T.);
#56235=EDGE_CURVE('',#41769,#42546,#22966,.T.);
#56236=EDGE_CURVE('',#42542,#41768,#22967,.T.);
#56237=EDGE_CURVE('',#42543,#41504,#22968,.T.);
#56238=EDGE_CURVE('',#42544,#41503,#22969,.T.);
#56239=EDGE_CURVE('',#42538,#41502,#22970,.T.);
#56240=EDGE_CURVE('',#42539,#41501,#22971,.T.);
#56241=EDGE_CURVE('',#41771,#42540,#22972,.T.);
#56242=EDGE_CURVE('',#41770,#42541,#22973,.T.);
#56243=EDGE_CURVE('',#42551,#42552,#30375,.T.);
#56244=EDGE_CURVE('',#42552,#42553,#30376,.T.);
#56245=EDGE_CURVE('',#42553,#42554,#1419,.T.);
#56246=EDGE_CURVE('',#42554,#42555,#30377,.T.);
#56247=EDGE_CURVE('',#42555,#42551,#26460,.T.);
#56248=EDGE_CURVE('',#42556,#42557,#1420,.T.);
#56249=EDGE_CURVE('',#42557,#42558,#30378,.T.);
#56250=EDGE_CURVE('',#42559,#42558,#30379,.T.);
#56251=EDGE_CURVE('',#42559,#42560,#26461,.T.);
#56252=EDGE_CURVE('',#42560,#42556,#30380,.T.);
#56253=EDGE_CURVE('',#42558,#42561,#26462,.T.);
#56254=EDGE_CURVE('',#42561,#42552,#26463,.T.);
#56255=EDGE_CURVE('',#42551,#42562,#1421,.T.);
#56256=EDGE_CURVE('',#42562,#42559,#1422,.T.);
#56257=EDGE_CURVE('',#42560,#41236,#26464,.T.);
#56258=EDGE_CURVE('',#42563,#42559,#22974,.T.);
#56259=EDGE_CURVE('',#41236,#42563,#26465,.T.);
#56260=EDGE_CURVE('',#42564,#42551,#22975,.T.);
#56261=EDGE_CURVE('',#42563,#42564,#26466,.T.);
#56262=EDGE_CURVE('',#41235,#42555,#26467,.T.);
#56263=EDGE_CURVE('',#42564,#41235,#1423,.T.);
#56264=EDGE_CURVE('',#41765,#42560,#22976,.T.);
#56265=EDGE_CURVE('',#42556,#41764,#22977,.T.);
#56266=EDGE_CURVE('',#42557,#41508,#22978,.T.);
#56267=EDGE_CURVE('',#42558,#41507,#22979,.T.);
#56268=EDGE_CURVE('',#42552,#41506,#22980,.T.);
#56269=EDGE_CURVE('',#42553,#41505,#22981,.T.);
#56270=EDGE_CURVE('',#41767,#42554,#22982,.T.);
#56271=EDGE_CURVE('',#41766,#42555,#22983,.T.);
#56272=EDGE_CURVE('',#42565,#42566,#30381,.T.);
#56273=EDGE_CURVE('',#42566,#42567,#30382,.T.);
#56274=EDGE_CURVE('',#42567,#42568,#1424,.T.);
#56275=EDGE_CURVE('',#42568,#42569,#30383,.T.);
#56276=EDGE_CURVE('',#42569,#42565,#26468,.T.);
#56277=EDGE_CURVE('',#42570,#42571,#1425,.T.);
#56278=EDGE_CURVE('',#42571,#42572,#30384,.T.);
#56279=EDGE_CURVE('',#42573,#42572,#30385,.T.);
#56280=EDGE_CURVE('',#42573,#42574,#26469,.T.);
#56281=EDGE_CURVE('',#42574,#42570,#30386,.T.);
#56282=EDGE_CURVE('',#42572,#42575,#26470,.T.);
#56283=EDGE_CURVE('',#42575,#42566,#26471,.T.);
#56284=EDGE_CURVE('',#42565,#42576,#1426,.T.);
#56285=EDGE_CURVE('',#42576,#42573,#1427,.T.);
#56286=EDGE_CURVE('',#42574,#41232,#26472,.T.);
#56287=EDGE_CURVE('',#42577,#42573,#22984,.T.);
#56288=EDGE_CURVE('',#41232,#42577,#26473,.T.);
#56289=EDGE_CURVE('',#42578,#42565,#22985,.T.);
#56290=EDGE_CURVE('',#42577,#42578,#26474,.T.);
#56291=EDGE_CURVE('',#41231,#42569,#26475,.T.);
#56292=EDGE_CURVE('',#42578,#41231,#1428,.T.);
#56293=EDGE_CURVE('',#41761,#42574,#22986,.T.);
#56294=EDGE_CURVE('',#42570,#41760,#22987,.T.);
#56295=EDGE_CURVE('',#42571,#41512,#22988,.T.);
#56296=EDGE_CURVE('',#42572,#41511,#22989,.T.);
#56297=EDGE_CURVE('',#42566,#41510,#22990,.T.);
#56298=EDGE_CURVE('',#42567,#41509,#22991,.T.);
#56299=EDGE_CURVE('',#41763,#42568,#22992,.T.);
#56300=EDGE_CURVE('',#41762,#42569,#22993,.T.);
#56301=EDGE_CURVE('',#42579,#42580,#30387,.T.);
#56302=EDGE_CURVE('',#42580,#42581,#30388,.T.);
#56303=EDGE_CURVE('',#42581,#42582,#1429,.T.);
#56304=EDGE_CURVE('',#42582,#42583,#30389,.T.);
#56305=EDGE_CURVE('',#42583,#42579,#26476,.T.);
#56306=EDGE_CURVE('',#42584,#42585,#1430,.T.);
#56307=EDGE_CURVE('',#42585,#42586,#30390,.T.);
#56308=EDGE_CURVE('',#42587,#42586,#30391,.T.);
#56309=EDGE_CURVE('',#42587,#42588,#26477,.T.);
#56310=EDGE_CURVE('',#42588,#42584,#30392,.T.);
#56311=EDGE_CURVE('',#42586,#42589,#26478,.T.);
#56312=EDGE_CURVE('',#42589,#42580,#26479,.T.);
#56313=EDGE_CURVE('',#42579,#42590,#1431,.T.);
#56314=EDGE_CURVE('',#42590,#42587,#1432,.T.);
#56315=EDGE_CURVE('',#42588,#41228,#26480,.T.);
#56316=EDGE_CURVE('',#42591,#42587,#22994,.T.);
#56317=EDGE_CURVE('',#41228,#42591,#26481,.T.);
#56318=EDGE_CURVE('',#42592,#42579,#22995,.T.);
#56319=EDGE_CURVE('',#42591,#42592,#26482,.T.);
#56320=EDGE_CURVE('',#41227,#42583,#26483,.T.);
#56321=EDGE_CURVE('',#42592,#41227,#1433,.T.);
#56322=EDGE_CURVE('',#41757,#42588,#22996,.T.);
#56323=EDGE_CURVE('',#42584,#41756,#22997,.T.);
#56324=EDGE_CURVE('',#42585,#41516,#22998,.T.);
#56325=EDGE_CURVE('',#42586,#41515,#22999,.T.);
#56326=EDGE_CURVE('',#42580,#41514,#23000,.T.);
#56327=EDGE_CURVE('',#42581,#41513,#23001,.T.);
#56328=EDGE_CURVE('',#41759,#42582,#23002,.T.);
#56329=EDGE_CURVE('',#41758,#42583,#23003,.T.);
#56330=EDGE_CURVE('',#42593,#42594,#30393,.T.);
#56331=EDGE_CURVE('',#42594,#42595,#30394,.T.);
#56332=EDGE_CURVE('',#42595,#42596,#1434,.T.);
#56333=EDGE_CURVE('',#42596,#42597,#30395,.T.);
#56334=EDGE_CURVE('',#42597,#42593,#26484,.T.);
#56335=EDGE_CURVE('',#42598,#42599,#1435,.T.);
#56336=EDGE_CURVE('',#42599,#42600,#30396,.T.);
#56337=EDGE_CURVE('',#42601,#42600,#30397,.T.);
#56338=EDGE_CURVE('',#42601,#42602,#26485,.T.);
#56339=EDGE_CURVE('',#42602,#42598,#30398,.T.);
#56340=EDGE_CURVE('',#42600,#42603,#26486,.T.);
#56341=EDGE_CURVE('',#42603,#42594,#26487,.T.);
#56342=EDGE_CURVE('',#42593,#42604,#1436,.T.);
#56343=EDGE_CURVE('',#42604,#42601,#1437,.T.);
#56344=EDGE_CURVE('',#42602,#41224,#26488,.T.);
#56345=EDGE_CURVE('',#42605,#42601,#23004,.T.);
#56346=EDGE_CURVE('',#41224,#42605,#26489,.T.);
#56347=EDGE_CURVE('',#42606,#42593,#23005,.T.);
#56348=EDGE_CURVE('',#42605,#42606,#26490,.T.);
#56349=EDGE_CURVE('',#41223,#42597,#26491,.T.);
#56350=EDGE_CURVE('',#42606,#41223,#1438,.T.);
#56351=EDGE_CURVE('',#41753,#42602,#23006,.T.);
#56352=EDGE_CURVE('',#42598,#41752,#23007,.T.);
#56353=EDGE_CURVE('',#42599,#41520,#23008,.T.);
#56354=EDGE_CURVE('',#42600,#41519,#23009,.T.);
#56355=EDGE_CURVE('',#42594,#41518,#23010,.T.);
#56356=EDGE_CURVE('',#42595,#41517,#23011,.T.);
#56357=EDGE_CURVE('',#41755,#42596,#23012,.T.);
#56358=EDGE_CURVE('',#41754,#42597,#23013,.T.);
#56359=EDGE_CURVE('',#42607,#42608,#30399,.T.);
#56360=EDGE_CURVE('',#42608,#42609,#30400,.T.);
#56361=EDGE_CURVE('',#42609,#42610,#1439,.T.);
#56362=EDGE_CURVE('',#42610,#42611,#30401,.T.);
#56363=EDGE_CURVE('',#42611,#42607,#26492,.T.);
#56364=EDGE_CURVE('',#42612,#42613,#1440,.T.);
#56365=EDGE_CURVE('',#42613,#42614,#30402,.T.);
#56366=EDGE_CURVE('',#42615,#42614,#30403,.T.);
#56367=EDGE_CURVE('',#42615,#42616,#26493,.T.);
#56368=EDGE_CURVE('',#42616,#42612,#30404,.T.);
#56369=EDGE_CURVE('',#42614,#42617,#26494,.T.);
#56370=EDGE_CURVE('',#42617,#42608,#26495,.T.);
#56371=EDGE_CURVE('',#42607,#42618,#1441,.T.);
#56372=EDGE_CURVE('',#42618,#42615,#1442,.T.);
#56373=EDGE_CURVE('',#42616,#41220,#26496,.T.);
#56374=EDGE_CURVE('',#42619,#42615,#23014,.T.);
#56375=EDGE_CURVE('',#41220,#42619,#26497,.T.);
#56376=EDGE_CURVE('',#42620,#42607,#23015,.T.);
#56377=EDGE_CURVE('',#42619,#42620,#26498,.T.);
#56378=EDGE_CURVE('',#41219,#42611,#26499,.T.);
#56379=EDGE_CURVE('',#42620,#41219,#1443,.T.);
#56380=EDGE_CURVE('',#41749,#42616,#23016,.T.);
#56381=EDGE_CURVE('',#42612,#41748,#23017,.T.);
#56382=EDGE_CURVE('',#42613,#41524,#23018,.T.);
#56383=EDGE_CURVE('',#42614,#41523,#23019,.T.);
#56384=EDGE_CURVE('',#42608,#41522,#23020,.T.);
#56385=EDGE_CURVE('',#42609,#41521,#23021,.T.);
#56386=EDGE_CURVE('',#41751,#42610,#23022,.T.);
#56387=EDGE_CURVE('',#41750,#42611,#23023,.T.);
#56388=EDGE_CURVE('',#42621,#42622,#30405,.T.);
#56389=EDGE_CURVE('',#42622,#42623,#30406,.T.);
#56390=EDGE_CURVE('',#42623,#42624,#1444,.T.);
#56391=EDGE_CURVE('',#42624,#42625,#30407,.T.);
#56392=EDGE_CURVE('',#42625,#42621,#26500,.T.);
#56393=EDGE_CURVE('',#42626,#42627,#1445,.T.);
#56394=EDGE_CURVE('',#42627,#42628,#30408,.T.);
#56395=EDGE_CURVE('',#42629,#42628,#30409,.T.);
#56396=EDGE_CURVE('',#42629,#42630,#26501,.T.);
#56397=EDGE_CURVE('',#42630,#42626,#30410,.T.);
#56398=EDGE_CURVE('',#42628,#42631,#26502,.T.);
#56399=EDGE_CURVE('',#42631,#42622,#26503,.T.);
#56400=EDGE_CURVE('',#42621,#42632,#1446,.T.);
#56401=EDGE_CURVE('',#42632,#42629,#1447,.T.);
#56402=EDGE_CURVE('',#42630,#41216,#26504,.T.);
#56403=EDGE_CURVE('',#42633,#42629,#23024,.T.);
#56404=EDGE_CURVE('',#41216,#42633,#26505,.T.);
#56405=EDGE_CURVE('',#42634,#42621,#23025,.T.);
#56406=EDGE_CURVE('',#42633,#42634,#26506,.T.);
#56407=EDGE_CURVE('',#41215,#42625,#26507,.T.);
#56408=EDGE_CURVE('',#42634,#41215,#1448,.T.);
#56409=EDGE_CURVE('',#41745,#42630,#23026,.T.);
#56410=EDGE_CURVE('',#42626,#41744,#23027,.T.);
#56411=EDGE_CURVE('',#42627,#41528,#23028,.T.);
#56412=EDGE_CURVE('',#42628,#41527,#23029,.T.);
#56413=EDGE_CURVE('',#42622,#41526,#23030,.T.);
#56414=EDGE_CURVE('',#42623,#41525,#23031,.T.);
#56415=EDGE_CURVE('',#41747,#42624,#23032,.T.);
#56416=EDGE_CURVE('',#41746,#42625,#23033,.T.);
#56417=EDGE_CURVE('',#42635,#42636,#30411,.T.);
#56418=EDGE_CURVE('',#42636,#42637,#30412,.T.);
#56419=EDGE_CURVE('',#42637,#42638,#1449,.T.);
#56420=EDGE_CURVE('',#42638,#42639,#30413,.T.);
#56421=EDGE_CURVE('',#42639,#42635,#26508,.T.);
#56422=EDGE_CURVE('',#42640,#42641,#1450,.T.);
#56423=EDGE_CURVE('',#42641,#42642,#30414,.T.);
#56424=EDGE_CURVE('',#42643,#42642,#30415,.T.);
#56425=EDGE_CURVE('',#42643,#42644,#26509,.T.);
#56426=EDGE_CURVE('',#42644,#42640,#30416,.T.);
#56427=EDGE_CURVE('',#42642,#42645,#26510,.T.);
#56428=EDGE_CURVE('',#42645,#42636,#26511,.T.);
#56429=EDGE_CURVE('',#42635,#42646,#1451,.T.);
#56430=EDGE_CURVE('',#42646,#42643,#1452,.T.);
#56431=EDGE_CURVE('',#42644,#41212,#26512,.T.);
#56432=EDGE_CURVE('',#42647,#42643,#23034,.T.);
#56433=EDGE_CURVE('',#41212,#42647,#26513,.T.);
#56434=EDGE_CURVE('',#42648,#42635,#23035,.T.);
#56435=EDGE_CURVE('',#42647,#42648,#26514,.T.);
#56436=EDGE_CURVE('',#41211,#42639,#26515,.T.);
#56437=EDGE_CURVE('',#42648,#41211,#1453,.T.);
#56438=EDGE_CURVE('',#41741,#42644,#23036,.T.);
#56439=EDGE_CURVE('',#42640,#41740,#23037,.T.);
#56440=EDGE_CURVE('',#42641,#41532,#23038,.T.);
#56441=EDGE_CURVE('',#42642,#41531,#23039,.T.);
#56442=EDGE_CURVE('',#42636,#41530,#23040,.T.);
#56443=EDGE_CURVE('',#42637,#41529,#23041,.T.);
#56444=EDGE_CURVE('',#41743,#42638,#23042,.T.);
#56445=EDGE_CURVE('',#41742,#42639,#23043,.T.);
#56446=EDGE_CURVE('',#42649,#42650,#30417,.T.);
#56447=EDGE_CURVE('',#42650,#42651,#30418,.T.);
#56448=EDGE_CURVE('',#42651,#42652,#1454,.T.);
#56449=EDGE_CURVE('',#42652,#42653,#30419,.T.);
#56450=EDGE_CURVE('',#42653,#42649,#26516,.T.);
#56451=EDGE_CURVE('',#42654,#42655,#1455,.T.);
#56452=EDGE_CURVE('',#42655,#42656,#30420,.T.);
#56453=EDGE_CURVE('',#42657,#42656,#30421,.T.);
#56454=EDGE_CURVE('',#42657,#42658,#26517,.T.);
#56455=EDGE_CURVE('',#42658,#42654,#30422,.T.);
#56456=EDGE_CURVE('',#42656,#42659,#26518,.T.);
#56457=EDGE_CURVE('',#42659,#42650,#26519,.T.);
#56458=EDGE_CURVE('',#42649,#42660,#1456,.T.);
#56459=EDGE_CURVE('',#42660,#42657,#1457,.T.);
#56460=EDGE_CURVE('',#42658,#41208,#26520,.T.);
#56461=EDGE_CURVE('',#42661,#42657,#23044,.T.);
#56462=EDGE_CURVE('',#41208,#42661,#26521,.T.);
#56463=EDGE_CURVE('',#42662,#42649,#23045,.T.);
#56464=EDGE_CURVE('',#42661,#42662,#26522,.T.);
#56465=EDGE_CURVE('',#41207,#42653,#26523,.T.);
#56466=EDGE_CURVE('',#42662,#41207,#1458,.T.);
#56467=EDGE_CURVE('',#41737,#42658,#23046,.T.);
#56468=EDGE_CURVE('',#42654,#41736,#23047,.T.);
#56469=EDGE_CURVE('',#42655,#41536,#23048,.T.);
#56470=EDGE_CURVE('',#42656,#41535,#23049,.T.);
#56471=EDGE_CURVE('',#42650,#41534,#23050,.T.);
#56472=EDGE_CURVE('',#42651,#41533,#23051,.T.);
#56473=EDGE_CURVE('',#41739,#42652,#23052,.T.);
#56474=EDGE_CURVE('',#41738,#42653,#23053,.T.);
#56475=EDGE_CURVE('',#42663,#42664,#30423,.T.);
#56476=EDGE_CURVE('',#42664,#42665,#30424,.T.);
#56477=EDGE_CURVE('',#42665,#42666,#1459,.T.);
#56478=EDGE_CURVE('',#42666,#42667,#30425,.T.);
#56479=EDGE_CURVE('',#42667,#42663,#26524,.T.);
#56480=EDGE_CURVE('',#42668,#42669,#1460,.T.);
#56481=EDGE_CURVE('',#42669,#42670,#30426,.T.);
#56482=EDGE_CURVE('',#42671,#42670,#30427,.T.);
#56483=EDGE_CURVE('',#42671,#42672,#26525,.T.);
#56484=EDGE_CURVE('',#42672,#42668,#30428,.T.);
#56485=EDGE_CURVE('',#42670,#42673,#26526,.T.);
#56486=EDGE_CURVE('',#42673,#42664,#26527,.T.);
#56487=EDGE_CURVE('',#42663,#42674,#1461,.T.);
#56488=EDGE_CURVE('',#42674,#42671,#1462,.T.);
#56489=EDGE_CURVE('',#42672,#41204,#26528,.T.);
#56490=EDGE_CURVE('',#42675,#42671,#23054,.T.);
#56491=EDGE_CURVE('',#41204,#42675,#26529,.T.);
#56492=EDGE_CURVE('',#42676,#42663,#23055,.T.);
#56493=EDGE_CURVE('',#42675,#42676,#26530,.T.);
#56494=EDGE_CURVE('',#41203,#42667,#26531,.T.);
#56495=EDGE_CURVE('',#42676,#41203,#1463,.T.);
#56496=EDGE_CURVE('',#41733,#42672,#23056,.T.);
#56497=EDGE_CURVE('',#42668,#41732,#23057,.T.);
#56498=EDGE_CURVE('',#42669,#41540,#23058,.T.);
#56499=EDGE_CURVE('',#42670,#41539,#23059,.T.);
#56500=EDGE_CURVE('',#42664,#41538,#23060,.T.);
#56501=EDGE_CURVE('',#42665,#41537,#23061,.T.);
#56502=EDGE_CURVE('',#41735,#42666,#23062,.T.);
#56503=EDGE_CURVE('',#41734,#42667,#23063,.T.);
#56504=EDGE_CURVE('',#42677,#42678,#30429,.T.);
#56505=EDGE_CURVE('',#42678,#42679,#30430,.T.);
#56506=EDGE_CURVE('',#42679,#42680,#1464,.T.);
#56507=EDGE_CURVE('',#42680,#42681,#30431,.T.);
#56508=EDGE_CURVE('',#42681,#42677,#26532,.T.);
#56509=EDGE_CURVE('',#42682,#42683,#1465,.T.);
#56510=EDGE_CURVE('',#42683,#42684,#30432,.T.);
#56511=EDGE_CURVE('',#42685,#42684,#30433,.T.);
#56512=EDGE_CURVE('',#42685,#42686,#26533,.T.);
#56513=EDGE_CURVE('',#42686,#42682,#30434,.T.);
#56514=EDGE_CURVE('',#42684,#42687,#26534,.T.);
#56515=EDGE_CURVE('',#42687,#42678,#26535,.T.);
#56516=EDGE_CURVE('',#42677,#42688,#1466,.T.);
#56517=EDGE_CURVE('',#42688,#42685,#1467,.T.);
#56518=EDGE_CURVE('',#42686,#41200,#26536,.T.);
#56519=EDGE_CURVE('',#42689,#42685,#23064,.T.);
#56520=EDGE_CURVE('',#41200,#42689,#26537,.T.);
#56521=EDGE_CURVE('',#42690,#42677,#23065,.T.);
#56522=EDGE_CURVE('',#42689,#42690,#26538,.T.);
#56523=EDGE_CURVE('',#41199,#42681,#26539,.T.);
#56524=EDGE_CURVE('',#42690,#41199,#1468,.T.);
#56525=EDGE_CURVE('',#41729,#42686,#23066,.T.);
#56526=EDGE_CURVE('',#42682,#41728,#23067,.T.);
#56527=EDGE_CURVE('',#42683,#41544,#23068,.T.);
#56528=EDGE_CURVE('',#42684,#41543,#23069,.T.);
#56529=EDGE_CURVE('',#42678,#41542,#23070,.T.);
#56530=EDGE_CURVE('',#42679,#41541,#23071,.T.);
#56531=EDGE_CURVE('',#41731,#42680,#23072,.T.);
#56532=EDGE_CURVE('',#41730,#42681,#23073,.T.);
#56533=EDGE_CURVE('',#42691,#42692,#30435,.T.);
#56534=EDGE_CURVE('',#42692,#42693,#30436,.T.);
#56535=EDGE_CURVE('',#42693,#42694,#1469,.T.);
#56536=EDGE_CURVE('',#42694,#42695,#30437,.T.);
#56537=EDGE_CURVE('',#42695,#42691,#26540,.T.);
#56538=EDGE_CURVE('',#42696,#42697,#1470,.T.);
#56539=EDGE_CURVE('',#42697,#42698,#30438,.T.);
#56540=EDGE_CURVE('',#42699,#42698,#30439,.T.);
#56541=EDGE_CURVE('',#42699,#42700,#26541,.T.);
#56542=EDGE_CURVE('',#42700,#42696,#30440,.T.);
#56543=EDGE_CURVE('',#42698,#42701,#26542,.T.);
#56544=EDGE_CURVE('',#42701,#42692,#26543,.T.);
#56545=EDGE_CURVE('',#42691,#42702,#1471,.T.);
#56546=EDGE_CURVE('',#42702,#42699,#1472,.T.);
#56547=EDGE_CURVE('',#42700,#41196,#26544,.T.);
#56548=EDGE_CURVE('',#42703,#42699,#23074,.T.);
#56549=EDGE_CURVE('',#41196,#42703,#26545,.T.);
#56550=EDGE_CURVE('',#42704,#42691,#23075,.T.);
#56551=EDGE_CURVE('',#42703,#42704,#26546,.T.);
#56552=EDGE_CURVE('',#41195,#42695,#26547,.T.);
#56553=EDGE_CURVE('',#42704,#41195,#1473,.T.);
#56554=EDGE_CURVE('',#41725,#42700,#23076,.T.);
#56555=EDGE_CURVE('',#42696,#41724,#23077,.T.);
#56556=EDGE_CURVE('',#42697,#41548,#23078,.T.);
#56557=EDGE_CURVE('',#42698,#41547,#23079,.T.);
#56558=EDGE_CURVE('',#42692,#41546,#23080,.T.);
#56559=EDGE_CURVE('',#42693,#41545,#23081,.T.);
#56560=EDGE_CURVE('',#41727,#42694,#23082,.T.);
#56561=EDGE_CURVE('',#41726,#42695,#23083,.T.);
#56562=EDGE_CURVE('',#42705,#42706,#30441,.T.);
#56563=EDGE_CURVE('',#42706,#42707,#30442,.T.);
#56564=EDGE_CURVE('',#42707,#42708,#1474,.T.);
#56565=EDGE_CURVE('',#42708,#42709,#30443,.T.);
#56566=EDGE_CURVE('',#42709,#42705,#26548,.T.);
#56567=EDGE_CURVE('',#42710,#42711,#1475,.T.);
#56568=EDGE_CURVE('',#42711,#42712,#30444,.T.);
#56569=EDGE_CURVE('',#42713,#42712,#30445,.T.);
#56570=EDGE_CURVE('',#42713,#42714,#26549,.T.);
#56571=EDGE_CURVE('',#42714,#42710,#30446,.T.);
#56572=EDGE_CURVE('',#42712,#42715,#26550,.T.);
#56573=EDGE_CURVE('',#42715,#42706,#26551,.T.);
#56574=EDGE_CURVE('',#42705,#42716,#1476,.T.);
#56575=EDGE_CURVE('',#42716,#42713,#1477,.T.);
#56576=EDGE_CURVE('',#42714,#41192,#26552,.T.);
#56577=EDGE_CURVE('',#42717,#42713,#23084,.T.);
#56578=EDGE_CURVE('',#41192,#42717,#26553,.T.);
#56579=EDGE_CURVE('',#42718,#42705,#23085,.T.);
#56580=EDGE_CURVE('',#42717,#42718,#26554,.T.);
#56581=EDGE_CURVE('',#41191,#42709,#26555,.T.);
#56582=EDGE_CURVE('',#42718,#41191,#1478,.T.);
#56583=EDGE_CURVE('',#41721,#42714,#23086,.T.);
#56584=EDGE_CURVE('',#42710,#41720,#23087,.T.);
#56585=EDGE_CURVE('',#42711,#41552,#23088,.T.);
#56586=EDGE_CURVE('',#42712,#41551,#23089,.T.);
#56587=EDGE_CURVE('',#42706,#41550,#23090,.T.);
#56588=EDGE_CURVE('',#42707,#41549,#23091,.T.);
#56589=EDGE_CURVE('',#41723,#42708,#23092,.T.);
#56590=EDGE_CURVE('',#41722,#42709,#23093,.T.);
#56591=EDGE_CURVE('',#42719,#42720,#30447,.T.);
#56592=EDGE_CURVE('',#42720,#42721,#30448,.T.);
#56593=EDGE_CURVE('',#42721,#42722,#1479,.T.);
#56594=EDGE_CURVE('',#42722,#42723,#30449,.T.);
#56595=EDGE_CURVE('',#42723,#42719,#26556,.T.);
#56596=EDGE_CURVE('',#42724,#42725,#1480,.T.);
#56597=EDGE_CURVE('',#42725,#42726,#30450,.T.);
#56598=EDGE_CURVE('',#42727,#42726,#30451,.T.);
#56599=EDGE_CURVE('',#42727,#42728,#26557,.T.);
#56600=EDGE_CURVE('',#42728,#42724,#30452,.T.);
#56601=EDGE_CURVE('',#42726,#42729,#26558,.T.);
#56602=EDGE_CURVE('',#42729,#42720,#26559,.T.);
#56603=EDGE_CURVE('',#42719,#42730,#1481,.T.);
#56604=EDGE_CURVE('',#42730,#42727,#1482,.T.);
#56605=EDGE_CURVE('',#42728,#41188,#26560,.T.);
#56606=EDGE_CURVE('',#42731,#42727,#23094,.T.);
#56607=EDGE_CURVE('',#41188,#42731,#26561,.T.);
#56608=EDGE_CURVE('',#42732,#42719,#23095,.T.);
#56609=EDGE_CURVE('',#42731,#42732,#26562,.T.);
#56610=EDGE_CURVE('',#41187,#42723,#26563,.T.);
#56611=EDGE_CURVE('',#42732,#41187,#1483,.T.);
#56612=EDGE_CURVE('',#41717,#42728,#23096,.T.);
#56613=EDGE_CURVE('',#42724,#41715,#23097,.T.);
#56614=EDGE_CURVE('',#42725,#41556,#23098,.T.);
#56615=EDGE_CURVE('',#42726,#41555,#23099,.T.);
#56616=EDGE_CURVE('',#42720,#41554,#23100,.T.);
#56617=EDGE_CURVE('',#42721,#41553,#23101,.T.);
#56618=EDGE_CURVE('',#41719,#42722,#23102,.T.);
#56619=EDGE_CURVE('',#41718,#42723,#23103,.T.);
#56620=EDGE_CURVE('',#42733,#42734,#30453,.T.);
#56621=EDGE_CURVE('',#42734,#42735,#30454,.T.);
#56622=EDGE_CURVE('',#42735,#42736,#1484,.T.);
#56623=EDGE_CURVE('',#42736,#42737,#30455,.T.);
#56624=EDGE_CURVE('',#42737,#42733,#26564,.T.);
#56625=EDGE_CURVE('',#42738,#42739,#1485,.T.);
#56626=EDGE_CURVE('',#42739,#42740,#30456,.T.);
#56627=EDGE_CURVE('',#42741,#42740,#30457,.T.);
#56628=EDGE_CURVE('',#42741,#42742,#26565,.T.);
#56629=EDGE_CURVE('',#42742,#42738,#30458,.T.);
#56630=EDGE_CURVE('',#42740,#42743,#26566,.T.);
#56631=EDGE_CURVE('',#42743,#42734,#26567,.T.);
#56632=EDGE_CURVE('',#42733,#42744,#1486,.T.);
#56633=EDGE_CURVE('',#42744,#42741,#1487,.T.);
#56634=EDGE_CURVE('',#42742,#41184,#26568,.T.);
#56635=EDGE_CURVE('',#42745,#42741,#23104,.T.);
#56636=EDGE_CURVE('',#41184,#42745,#26569,.T.);
#56637=EDGE_CURVE('',#42746,#42733,#23105,.T.);
#56638=EDGE_CURVE('',#42745,#42746,#26570,.T.);
#56639=EDGE_CURVE('',#41183,#42737,#26571,.T.);
#56640=EDGE_CURVE('',#42746,#41183,#1488,.T.);
#56641=EDGE_CURVE('',#42021,#42742,#23106,.T.);
#56642=EDGE_CURVE('',#42738,#42020,#23107,.T.);
#56643=EDGE_CURVE('',#42739,#41563,#23108,.T.);
#56644=EDGE_CURVE('',#42740,#41562,#23109,.T.);
#56645=EDGE_CURVE('',#42734,#41561,#23110,.T.);
#56646=EDGE_CURVE('',#42735,#41560,#23111,.T.);
#56647=EDGE_CURVE('',#41716,#42736,#23112,.T.);
#56648=EDGE_CURVE('',#42022,#42737,#23113,.T.);
#56649=EDGE_CURVE('',#42747,#42748,#30459,.T.);
#56650=EDGE_CURVE('',#42748,#42749,#30460,.T.);
#56651=EDGE_CURVE('',#42749,#42750,#1489,.T.);
#56652=EDGE_CURVE('',#42750,#42751,#30461,.T.);
#56653=EDGE_CURVE('',#42751,#42747,#26572,.T.);
#56654=EDGE_CURVE('',#42752,#42753,#1490,.T.);
#56655=EDGE_CURVE('',#42753,#42754,#30462,.T.);
#56656=EDGE_CURVE('',#42755,#42754,#30463,.T.);
#56657=EDGE_CURVE('',#42755,#42756,#26573,.T.);
#56658=EDGE_CURVE('',#42756,#42752,#30464,.T.);
#56659=EDGE_CURVE('',#42754,#42757,#26574,.T.);
#56660=EDGE_CURVE('',#42757,#42748,#26575,.T.);
#56661=EDGE_CURVE('',#42747,#42758,#1491,.T.);
#56662=EDGE_CURVE('',#42758,#42755,#1492,.T.);
#56663=EDGE_CURVE('',#42756,#41180,#26576,.T.);
#56664=EDGE_CURVE('',#42759,#42755,#23114,.T.);
#56665=EDGE_CURVE('',#41180,#42759,#26577,.T.);
#56666=EDGE_CURVE('',#42760,#42747,#23115,.T.);
#56667=EDGE_CURVE('',#42759,#42760,#26578,.T.);
#56668=EDGE_CURVE('',#41179,#42751,#26579,.T.);
#56669=EDGE_CURVE('',#42760,#41179,#1493,.T.);
#56670=EDGE_CURVE('',#42017,#42756,#23116,.T.);
#56671=EDGE_CURVE('',#42752,#42016,#23117,.T.);
#56672=EDGE_CURVE('',#42753,#41567,#23118,.T.);
#56673=EDGE_CURVE('',#42754,#41566,#23119,.T.);
#56674=EDGE_CURVE('',#42748,#41565,#23120,.T.);
#56675=EDGE_CURVE('',#42749,#41564,#23121,.T.);
#56676=EDGE_CURVE('',#42019,#42750,#23122,.T.);
#56677=EDGE_CURVE('',#42018,#42751,#23123,.T.);
#56678=EDGE_CURVE('',#42761,#42762,#30465,.T.);
#56679=EDGE_CURVE('',#42762,#42763,#30466,.T.);
#56680=EDGE_CURVE('',#42763,#42764,#1494,.T.);
#56681=EDGE_CURVE('',#42764,#42765,#30467,.T.);
#56682=EDGE_CURVE('',#42765,#42761,#26580,.T.);
#56683=EDGE_CURVE('',#42766,#42767,#1495,.T.);
#56684=EDGE_CURVE('',#42767,#42768,#30468,.T.);
#56685=EDGE_CURVE('',#42769,#42768,#30469,.T.);
#56686=EDGE_CURVE('',#42769,#42770,#26581,.T.);
#56687=EDGE_CURVE('',#42770,#42766,#30470,.T.);
#56688=EDGE_CURVE('',#42768,#42771,#26582,.T.);
#56689=EDGE_CURVE('',#42771,#42762,#26583,.T.);
#56690=EDGE_CURVE('',#42761,#42772,#1496,.T.);
#56691=EDGE_CURVE('',#42772,#42769,#1497,.T.);
#56692=EDGE_CURVE('',#42770,#41176,#26584,.T.);
#56693=EDGE_CURVE('',#42773,#42769,#23124,.T.);
#56694=EDGE_CURVE('',#41176,#42773,#26585,.T.);
#56695=EDGE_CURVE('',#42774,#42761,#23125,.T.);
#56696=EDGE_CURVE('',#42773,#42774,#26586,.T.);
#56697=EDGE_CURVE('',#41175,#42765,#26587,.T.);
#56698=EDGE_CURVE('',#42774,#41175,#1498,.T.);
#56699=EDGE_CURVE('',#42013,#42770,#23126,.T.);
#56700=EDGE_CURVE('',#42766,#42012,#23127,.T.);
#56701=EDGE_CURVE('',#42767,#41571,#23128,.T.);
#56702=EDGE_CURVE('',#42768,#41570,#23129,.T.);
#56703=EDGE_CURVE('',#42762,#41569,#23130,.T.);
#56704=EDGE_CURVE('',#42763,#41568,#23131,.T.);
#56705=EDGE_CURVE('',#42015,#42764,#23132,.T.);
#56706=EDGE_CURVE('',#42014,#42765,#23133,.T.);
#56707=EDGE_CURVE('',#42775,#42776,#30471,.T.);
#56708=EDGE_CURVE('',#42776,#42777,#30472,.T.);
#56709=EDGE_CURVE('',#42777,#42778,#1499,.T.);
#56710=EDGE_CURVE('',#42778,#42779,#30473,.T.);
#56711=EDGE_CURVE('',#42779,#42775,#26588,.T.);
#56712=EDGE_CURVE('',#42780,#42781,#1500,.T.);
#56713=EDGE_CURVE('',#42781,#42782,#30474,.T.);
#56714=EDGE_CURVE('',#42783,#42782,#30475,.T.);
#56715=EDGE_CURVE('',#42783,#42784,#26589,.T.);
#56716=EDGE_CURVE('',#42784,#42780,#30476,.T.);
#56717=EDGE_CURVE('',#42782,#42785,#26590,.T.);
#56718=EDGE_CURVE('',#42785,#42776,#26591,.T.);
#56719=EDGE_CURVE('',#42775,#42786,#1501,.T.);
#56720=EDGE_CURVE('',#42786,#42783,#1502,.T.);
#56721=EDGE_CURVE('',#42784,#41172,#26592,.T.);
#56722=EDGE_CURVE('',#42787,#42783,#23134,.T.);
#56723=EDGE_CURVE('',#41172,#42787,#26593,.T.);
#56724=EDGE_CURVE('',#42788,#42775,#23135,.T.);
#56725=EDGE_CURVE('',#42787,#42788,#26594,.T.);
#56726=EDGE_CURVE('',#41171,#42779,#26595,.T.);
#56727=EDGE_CURVE('',#42788,#41171,#1503,.T.);
#56728=EDGE_CURVE('',#42009,#42784,#23136,.T.);
#56729=EDGE_CURVE('',#42780,#42008,#23137,.T.);
#56730=EDGE_CURVE('',#42781,#41575,#23138,.T.);
#56731=EDGE_CURVE('',#42782,#41574,#23139,.T.);
#56732=EDGE_CURVE('',#42776,#41573,#23140,.T.);
#56733=EDGE_CURVE('',#42777,#41572,#23141,.T.);
#56734=EDGE_CURVE('',#42011,#42778,#23142,.T.);
#56735=EDGE_CURVE('',#42010,#42779,#23143,.T.);
#56736=EDGE_CURVE('',#42789,#42790,#30477,.T.);
#56737=EDGE_CURVE('',#42790,#42791,#30478,.T.);
#56738=EDGE_CURVE('',#42791,#42792,#1504,.T.);
#56739=EDGE_CURVE('',#42792,#42793,#30479,.T.);
#56740=EDGE_CURVE('',#42793,#42789,#26596,.T.);
#56741=EDGE_CURVE('',#42794,#42795,#1505,.T.);
#56742=EDGE_CURVE('',#42795,#42796,#30480,.T.);
#56743=EDGE_CURVE('',#42797,#42796,#30481,.T.);
#56744=EDGE_CURVE('',#42797,#42798,#26597,.T.);
#56745=EDGE_CURVE('',#42798,#42794,#30482,.T.);
#56746=EDGE_CURVE('',#42796,#42799,#26598,.T.);
#56747=EDGE_CURVE('',#42799,#42790,#26599,.T.);
#56748=EDGE_CURVE('',#42789,#42800,#1506,.T.);
#56749=EDGE_CURVE('',#42800,#42797,#1507,.T.);
#56750=EDGE_CURVE('',#42798,#41168,#26600,.T.);
#56751=EDGE_CURVE('',#42801,#42797,#23144,.T.);
#56752=EDGE_CURVE('',#41168,#42801,#26601,.T.);
#56753=EDGE_CURVE('',#42802,#42789,#23145,.T.);
#56754=EDGE_CURVE('',#42801,#42802,#26602,.T.);
#56755=EDGE_CURVE('',#41167,#42793,#26603,.T.);
#56756=EDGE_CURVE('',#42802,#41167,#1508,.T.);
#56757=EDGE_CURVE('',#42005,#42798,#23146,.T.);
#56758=EDGE_CURVE('',#42794,#42004,#23147,.T.);
#56759=EDGE_CURVE('',#42795,#41579,#23148,.T.);
#56760=EDGE_CURVE('',#42796,#41578,#23149,.T.);
#56761=EDGE_CURVE('',#42790,#41577,#23150,.T.);
#56762=EDGE_CURVE('',#42791,#41576,#23151,.T.);
#56763=EDGE_CURVE('',#42007,#42792,#23152,.T.);
#56764=EDGE_CURVE('',#42006,#42793,#23153,.T.);
#56765=EDGE_CURVE('',#42803,#42804,#30483,.T.);
#56766=EDGE_CURVE('',#42804,#42805,#30484,.T.);
#56767=EDGE_CURVE('',#42805,#42806,#1509,.T.);
#56768=EDGE_CURVE('',#42806,#42807,#30485,.T.);
#56769=EDGE_CURVE('',#42807,#42803,#26604,.T.);
#56770=EDGE_CURVE('',#42808,#42809,#1510,.T.);
#56771=EDGE_CURVE('',#42809,#42810,#30486,.T.);
#56772=EDGE_CURVE('',#42811,#42810,#30487,.T.);
#56773=EDGE_CURVE('',#42811,#42812,#26605,.T.);
#56774=EDGE_CURVE('',#42812,#42808,#30488,.T.);
#56775=EDGE_CURVE('',#42810,#42813,#26606,.T.);
#56776=EDGE_CURVE('',#42813,#42804,#26607,.T.);
#56777=EDGE_CURVE('',#42803,#42814,#1511,.T.);
#56778=EDGE_CURVE('',#42814,#42811,#1512,.T.);
#56779=EDGE_CURVE('',#42812,#41164,#26608,.T.);
#56780=EDGE_CURVE('',#42815,#42811,#23154,.T.);
#56781=EDGE_CURVE('',#41164,#42815,#26609,.T.);
#56782=EDGE_CURVE('',#42816,#42803,#23155,.T.);
#56783=EDGE_CURVE('',#42815,#42816,#26610,.T.);
#56784=EDGE_CURVE('',#41163,#42807,#26611,.T.);
#56785=EDGE_CURVE('',#42816,#41163,#1513,.T.);
#56786=EDGE_CURVE('',#42001,#42812,#23156,.T.);
#56787=EDGE_CURVE('',#42808,#42000,#23157,.T.);
#56788=EDGE_CURVE('',#42809,#41583,#23158,.T.);
#56789=EDGE_CURVE('',#42810,#41582,#23159,.T.);
#56790=EDGE_CURVE('',#42804,#41581,#23160,.T.);
#56791=EDGE_CURVE('',#42805,#41580,#23161,.T.);
#56792=EDGE_CURVE('',#42003,#42806,#23162,.T.);
#56793=EDGE_CURVE('',#42002,#42807,#23163,.T.);
#56794=EDGE_CURVE('',#42817,#42818,#30489,.T.);
#56795=EDGE_CURVE('',#42818,#42819,#30490,.T.);
#56796=EDGE_CURVE('',#42819,#42820,#1514,.T.);
#56797=EDGE_CURVE('',#42820,#42821,#30491,.T.);
#56798=EDGE_CURVE('',#42821,#42817,#26612,.T.);
#56799=EDGE_CURVE('',#42822,#42823,#1515,.T.);
#56800=EDGE_CURVE('',#42823,#42824,#30492,.T.);
#56801=EDGE_CURVE('',#42825,#42824,#30493,.T.);
#56802=EDGE_CURVE('',#42825,#42826,#26613,.T.);
#56803=EDGE_CURVE('',#42826,#42822,#30494,.T.);
#56804=EDGE_CURVE('',#42824,#42827,#26614,.T.);
#56805=EDGE_CURVE('',#42827,#42818,#26615,.T.);
#56806=EDGE_CURVE('',#42817,#42828,#1516,.T.);
#56807=EDGE_CURVE('',#42828,#42825,#1517,.T.);
#56808=EDGE_CURVE('',#42826,#41160,#26616,.T.);
#56809=EDGE_CURVE('',#42829,#42825,#23164,.T.);
#56810=EDGE_CURVE('',#41160,#42829,#26617,.T.);
#56811=EDGE_CURVE('',#42830,#42817,#23165,.T.);
#56812=EDGE_CURVE('',#42829,#42830,#26618,.T.);
#56813=EDGE_CURVE('',#41159,#42821,#26619,.T.);
#56814=EDGE_CURVE('',#42830,#41159,#1518,.T.);
#56815=EDGE_CURVE('',#41997,#42826,#23166,.T.);
#56816=EDGE_CURVE('',#42822,#41996,#23167,.T.);
#56817=EDGE_CURVE('',#42823,#41587,#23168,.T.);
#56818=EDGE_CURVE('',#42824,#41586,#23169,.T.);
#56819=EDGE_CURVE('',#42818,#41585,#23170,.T.);
#56820=EDGE_CURVE('',#42819,#41584,#23171,.T.);
#56821=EDGE_CURVE('',#41999,#42820,#23172,.T.);
#56822=EDGE_CURVE('',#41998,#42821,#23173,.T.);
#56823=EDGE_CURVE('',#42831,#42832,#30495,.T.);
#56824=EDGE_CURVE('',#42832,#42833,#30496,.T.);
#56825=EDGE_CURVE('',#42833,#42834,#1519,.T.);
#56826=EDGE_CURVE('',#42834,#42835,#30497,.T.);
#56827=EDGE_CURVE('',#42835,#42831,#26620,.T.);
#56828=EDGE_CURVE('',#42836,#42837,#1520,.T.);
#56829=EDGE_CURVE('',#42837,#42838,#30498,.T.);
#56830=EDGE_CURVE('',#42839,#42838,#30499,.T.);
#56831=EDGE_CURVE('',#42839,#42840,#26621,.T.);
#56832=EDGE_CURVE('',#42840,#42836,#30500,.T.);
#56833=EDGE_CURVE('',#42838,#42841,#26622,.T.);
#56834=EDGE_CURVE('',#42841,#42832,#26623,.T.);
#56835=EDGE_CURVE('',#42831,#42842,#1521,.T.);
#56836=EDGE_CURVE('',#42842,#42839,#1522,.T.);
#56837=EDGE_CURVE('',#42840,#41156,#26624,.T.);
#56838=EDGE_CURVE('',#42843,#42839,#23174,.T.);
#56839=EDGE_CURVE('',#41156,#42843,#26625,.T.);
#56840=EDGE_CURVE('',#42844,#42831,#23175,.T.);
#56841=EDGE_CURVE('',#42843,#42844,#26626,.T.);
#56842=EDGE_CURVE('',#41155,#42835,#26627,.T.);
#56843=EDGE_CURVE('',#42844,#41155,#1523,.T.);
#56844=EDGE_CURVE('',#41993,#42840,#23176,.T.);
#56845=EDGE_CURVE('',#42836,#41992,#23177,.T.);
#56846=EDGE_CURVE('',#42837,#41591,#23178,.T.);
#56847=EDGE_CURVE('',#42838,#41590,#23179,.T.);
#56848=EDGE_CURVE('',#42832,#41589,#23180,.T.);
#56849=EDGE_CURVE('',#42833,#41588,#23181,.T.);
#56850=EDGE_CURVE('',#41995,#42834,#23182,.T.);
#56851=EDGE_CURVE('',#41994,#42835,#23183,.T.);
#56852=EDGE_CURVE('',#42845,#42846,#30501,.T.);
#56853=EDGE_CURVE('',#42846,#42847,#30502,.T.);
#56854=EDGE_CURVE('',#42847,#42848,#1524,.T.);
#56855=EDGE_CURVE('',#42848,#42849,#30503,.T.);
#56856=EDGE_CURVE('',#42849,#42845,#26628,.T.);
#56857=EDGE_CURVE('',#42850,#42851,#1525,.T.);
#56858=EDGE_CURVE('',#42851,#42852,#30504,.T.);
#56859=EDGE_CURVE('',#42853,#42852,#30505,.T.);
#56860=EDGE_CURVE('',#42853,#42854,#26629,.T.);
#56861=EDGE_CURVE('',#42854,#42850,#30506,.T.);
#56862=EDGE_CURVE('',#42852,#42855,#26630,.T.);
#56863=EDGE_CURVE('',#42855,#42846,#26631,.T.);
#56864=EDGE_CURVE('',#42845,#42856,#1526,.T.);
#56865=EDGE_CURVE('',#42856,#42853,#1527,.T.);
#56866=EDGE_CURVE('',#42854,#41152,#26632,.T.);
#56867=EDGE_CURVE('',#42857,#42853,#23184,.T.);
#56868=EDGE_CURVE('',#41152,#42857,#26633,.T.);
#56869=EDGE_CURVE('',#42858,#42845,#23185,.T.);
#56870=EDGE_CURVE('',#42857,#42858,#26634,.T.);
#56871=EDGE_CURVE('',#41151,#42849,#26635,.T.);
#56872=EDGE_CURVE('',#42858,#41151,#1528,.T.);
#56873=EDGE_CURVE('',#41989,#42854,#23186,.T.);
#56874=EDGE_CURVE('',#42850,#41988,#23187,.T.);
#56875=EDGE_CURVE('',#42851,#41595,#23188,.T.);
#56876=EDGE_CURVE('',#42852,#41594,#23189,.T.);
#56877=EDGE_CURVE('',#42846,#41593,#23190,.T.);
#56878=EDGE_CURVE('',#42847,#41592,#23191,.T.);
#56879=EDGE_CURVE('',#41991,#42848,#23192,.T.);
#56880=EDGE_CURVE('',#41990,#42849,#23193,.T.);
#56881=EDGE_CURVE('',#42859,#42860,#30507,.T.);
#56882=EDGE_CURVE('',#42860,#42861,#30508,.T.);
#56883=EDGE_CURVE('',#42861,#42862,#1529,.T.);
#56884=EDGE_CURVE('',#42862,#42863,#30509,.T.);
#56885=EDGE_CURVE('',#42863,#42859,#26636,.T.);
#56886=EDGE_CURVE('',#42864,#42865,#1530,.T.);
#56887=EDGE_CURVE('',#42865,#42866,#30510,.T.);
#56888=EDGE_CURVE('',#42867,#42866,#30511,.T.);
#56889=EDGE_CURVE('',#42867,#42868,#26637,.T.);
#56890=EDGE_CURVE('',#42868,#42864,#30512,.T.);
#56891=EDGE_CURVE('',#42866,#42869,#26638,.T.);
#56892=EDGE_CURVE('',#42869,#42860,#26639,.T.);
#56893=EDGE_CURVE('',#42859,#42870,#1531,.T.);
#56894=EDGE_CURVE('',#42870,#42867,#1532,.T.);
#56895=EDGE_CURVE('',#42868,#41148,#26640,.T.);
#56896=EDGE_CURVE('',#42871,#42867,#23194,.T.);
#56897=EDGE_CURVE('',#41148,#42871,#26641,.T.);
#56898=EDGE_CURVE('',#42872,#42859,#23195,.T.);
#56899=EDGE_CURVE('',#42871,#42872,#26642,.T.);
#56900=EDGE_CURVE('',#41147,#42863,#26643,.T.);
#56901=EDGE_CURVE('',#42872,#41147,#1533,.T.);
#56902=EDGE_CURVE('',#41985,#42868,#23196,.T.);
#56903=EDGE_CURVE('',#42864,#41984,#23197,.T.);
#56904=EDGE_CURVE('',#42865,#41599,#23198,.T.);
#56905=EDGE_CURVE('',#42866,#41598,#23199,.T.);
#56906=EDGE_CURVE('',#42860,#41597,#23200,.T.);
#56907=EDGE_CURVE('',#42861,#41596,#23201,.T.);
#56908=EDGE_CURVE('',#41987,#42862,#23202,.T.);
#56909=EDGE_CURVE('',#41986,#42863,#23203,.T.);
#56910=EDGE_CURVE('',#42873,#42874,#30513,.T.);
#56911=EDGE_CURVE('',#42874,#42875,#30514,.T.);
#56912=EDGE_CURVE('',#42875,#42876,#1534,.T.);
#56913=EDGE_CURVE('',#42876,#42877,#30515,.T.);
#56914=EDGE_CURVE('',#42877,#42873,#26644,.T.);
#56915=EDGE_CURVE('',#42878,#42879,#1535,.T.);
#56916=EDGE_CURVE('',#42879,#42880,#30516,.T.);
#56917=EDGE_CURVE('',#42881,#42880,#30517,.T.);
#56918=EDGE_CURVE('',#42881,#42882,#26645,.T.);
#56919=EDGE_CURVE('',#42882,#42878,#30518,.T.);
#56920=EDGE_CURVE('',#42880,#42883,#26646,.T.);
#56921=EDGE_CURVE('',#42883,#42874,#26647,.T.);
#56922=EDGE_CURVE('',#42873,#42884,#1536,.T.);
#56923=EDGE_CURVE('',#42884,#42881,#1537,.T.);
#56924=EDGE_CURVE('',#42882,#41144,#26648,.T.);
#56925=EDGE_CURVE('',#42885,#42881,#23204,.T.);
#56926=EDGE_CURVE('',#41144,#42885,#26649,.T.);
#56927=EDGE_CURVE('',#42886,#42873,#23205,.T.);
#56928=EDGE_CURVE('',#42885,#42886,#26650,.T.);
#56929=EDGE_CURVE('',#41143,#42877,#26651,.T.);
#56930=EDGE_CURVE('',#42886,#41143,#1538,.T.);
#56931=EDGE_CURVE('',#41981,#42882,#23206,.T.);
#56932=EDGE_CURVE('',#42878,#41980,#23207,.T.);
#56933=EDGE_CURVE('',#42879,#41603,#23208,.T.);
#56934=EDGE_CURVE('',#42880,#41602,#23209,.T.);
#56935=EDGE_CURVE('',#42874,#41601,#23210,.T.);
#56936=EDGE_CURVE('',#42875,#41600,#23211,.T.);
#56937=EDGE_CURVE('',#41983,#42876,#23212,.T.);
#56938=EDGE_CURVE('',#41982,#42877,#23213,.T.);
#56939=EDGE_CURVE('',#42887,#42888,#30519,.T.);
#56940=EDGE_CURVE('',#42888,#42889,#30520,.T.);
#56941=EDGE_CURVE('',#42889,#42890,#1539,.T.);
#56942=EDGE_CURVE('',#42890,#42891,#30521,.T.);
#56943=EDGE_CURVE('',#42891,#42887,#26652,.T.);
#56944=EDGE_CURVE('',#42892,#42893,#1540,.T.);
#56945=EDGE_CURVE('',#42893,#42894,#30522,.T.);
#56946=EDGE_CURVE('',#42895,#42894,#30523,.T.);
#56947=EDGE_CURVE('',#42895,#42896,#26653,.T.);
#56948=EDGE_CURVE('',#42896,#42892,#30524,.T.);
#56949=EDGE_CURVE('',#42894,#42897,#26654,.T.);
#56950=EDGE_CURVE('',#42897,#42888,#26655,.T.);
#56951=EDGE_CURVE('',#42887,#42898,#1541,.T.);
#56952=EDGE_CURVE('',#42898,#42895,#1542,.T.);
#56953=EDGE_CURVE('',#42896,#41140,#26656,.T.);
#56954=EDGE_CURVE('',#42899,#42895,#23214,.T.);
#56955=EDGE_CURVE('',#41140,#42899,#26657,.T.);
#56956=EDGE_CURVE('',#42900,#42887,#23215,.T.);
#56957=EDGE_CURVE('',#42899,#42900,#26658,.T.);
#56958=EDGE_CURVE('',#41139,#42891,#26659,.T.);
#56959=EDGE_CURVE('',#42900,#41139,#1543,.T.);
#56960=EDGE_CURVE('',#41977,#42896,#23216,.T.);
#56961=EDGE_CURVE('',#42892,#41976,#23217,.T.);
#56962=EDGE_CURVE('',#42893,#41607,#23218,.T.);
#56963=EDGE_CURVE('',#42894,#41606,#23219,.T.);
#56964=EDGE_CURVE('',#42888,#41605,#23220,.T.);
#56965=EDGE_CURVE('',#42889,#41604,#23221,.T.);
#56966=EDGE_CURVE('',#41979,#42890,#23222,.T.);
#56967=EDGE_CURVE('',#41978,#42891,#23223,.T.);
#56968=EDGE_CURVE('',#42901,#42902,#30525,.T.);
#56969=EDGE_CURVE('',#42902,#42903,#30526,.T.);
#56970=EDGE_CURVE('',#42903,#42904,#1544,.T.);
#56971=EDGE_CURVE('',#42904,#42905,#30527,.T.);
#56972=EDGE_CURVE('',#42905,#42901,#26660,.T.);
#56973=EDGE_CURVE('',#42906,#42907,#1545,.T.);
#56974=EDGE_CURVE('',#42907,#42908,#30528,.T.);
#56975=EDGE_CURVE('',#42909,#42908,#30529,.T.);
#56976=EDGE_CURVE('',#42909,#42910,#26661,.T.);
#56977=EDGE_CURVE('',#42910,#42906,#30530,.T.);
#56978=EDGE_CURVE('',#42908,#42911,#26662,.T.);
#56979=EDGE_CURVE('',#42911,#42902,#26663,.T.);
#56980=EDGE_CURVE('',#42901,#42912,#1546,.T.);
#56981=EDGE_CURVE('',#42912,#42909,#1547,.T.);
#56982=EDGE_CURVE('',#42910,#41136,#26664,.T.);
#56983=EDGE_CURVE('',#42913,#42909,#23224,.T.);
#56984=EDGE_CURVE('',#41136,#42913,#26665,.T.);
#56985=EDGE_CURVE('',#42914,#42901,#23225,.T.);
#56986=EDGE_CURVE('',#42913,#42914,#26666,.T.);
#56987=EDGE_CURVE('',#41135,#42905,#26667,.T.);
#56988=EDGE_CURVE('',#42914,#41135,#1548,.T.);
#56989=EDGE_CURVE('',#41973,#42910,#23226,.T.);
#56990=EDGE_CURVE('',#42906,#41972,#23227,.T.);
#56991=EDGE_CURVE('',#42907,#41611,#23228,.T.);
#56992=EDGE_CURVE('',#42908,#41610,#23229,.T.);
#56993=EDGE_CURVE('',#42902,#41609,#23230,.T.);
#56994=EDGE_CURVE('',#42903,#41608,#23231,.T.);
#56995=EDGE_CURVE('',#41975,#42904,#23232,.T.);
#56996=EDGE_CURVE('',#41974,#42905,#23233,.T.);
#56997=EDGE_CURVE('',#42915,#42916,#30531,.T.);
#56998=EDGE_CURVE('',#42916,#42917,#30532,.T.);
#56999=EDGE_CURVE('',#42917,#42918,#1549,.T.);
#57000=EDGE_CURVE('',#42918,#42919,#30533,.T.);
#57001=EDGE_CURVE('',#42919,#42915,#26668,.T.);
#57002=EDGE_CURVE('',#42920,#42921,#1550,.T.);
#57003=EDGE_CURVE('',#42921,#42922,#30534,.T.);
#57004=EDGE_CURVE('',#42923,#42922,#30535,.T.);
#57005=EDGE_CURVE('',#42923,#42924,#26669,.T.);
#57006=EDGE_CURVE('',#42924,#42920,#30536,.T.);
#57007=EDGE_CURVE('',#42922,#42925,#26670,.T.);
#57008=EDGE_CURVE('',#42925,#42916,#26671,.T.);
#57009=EDGE_CURVE('',#42915,#42926,#1551,.T.);
#57010=EDGE_CURVE('',#42926,#42923,#1552,.T.);
#57011=EDGE_CURVE('',#42924,#41132,#26672,.T.);
#57012=EDGE_CURVE('',#42927,#42923,#23234,.T.);
#57013=EDGE_CURVE('',#41132,#42927,#26673,.T.);
#57014=EDGE_CURVE('',#42928,#42915,#23235,.T.);
#57015=EDGE_CURVE('',#42927,#42928,#26674,.T.);
#57016=EDGE_CURVE('',#41131,#42919,#26675,.T.);
#57017=EDGE_CURVE('',#42928,#41131,#1553,.T.);
#57018=EDGE_CURVE('',#41969,#42924,#23236,.T.);
#57019=EDGE_CURVE('',#42920,#41968,#23237,.T.);
#57020=EDGE_CURVE('',#42921,#41615,#23238,.T.);
#57021=EDGE_CURVE('',#42922,#41614,#23239,.T.);
#57022=EDGE_CURVE('',#42916,#41613,#23240,.T.);
#57023=EDGE_CURVE('',#42917,#41612,#23241,.T.);
#57024=EDGE_CURVE('',#41971,#42918,#23242,.T.);
#57025=EDGE_CURVE('',#41970,#42919,#23243,.T.);
#57026=EDGE_CURVE('',#42929,#42930,#30537,.T.);
#57027=EDGE_CURVE('',#42930,#42931,#30538,.T.);
#57028=EDGE_CURVE('',#42931,#42932,#1554,.T.);
#57029=EDGE_CURVE('',#42932,#42933,#30539,.T.);
#57030=EDGE_CURVE('',#42933,#42929,#26676,.T.);
#57031=EDGE_CURVE('',#42934,#42935,#1555,.T.);
#57032=EDGE_CURVE('',#42935,#42936,#30540,.T.);
#57033=EDGE_CURVE('',#42937,#42936,#30541,.T.);
#57034=EDGE_CURVE('',#42937,#42938,#26677,.T.);
#57035=EDGE_CURVE('',#42938,#42934,#30542,.T.);
#57036=EDGE_CURVE('',#42936,#42939,#26678,.T.);
#57037=EDGE_CURVE('',#42939,#42930,#26679,.T.);
#57038=EDGE_CURVE('',#42929,#42940,#1556,.T.);
#57039=EDGE_CURVE('',#42940,#42937,#1557,.T.);
#57040=EDGE_CURVE('',#42938,#41128,#26680,.T.);
#57041=EDGE_CURVE('',#42941,#42937,#23244,.T.);
#57042=EDGE_CURVE('',#41128,#42941,#26681,.T.);
#57043=EDGE_CURVE('',#42942,#42929,#23245,.T.);
#57044=EDGE_CURVE('',#42941,#42942,#26682,.T.);
#57045=EDGE_CURVE('',#41127,#42933,#26683,.T.);
#57046=EDGE_CURVE('',#42942,#41127,#1558,.T.);
#57047=EDGE_CURVE('',#41965,#42938,#23246,.T.);
#57048=EDGE_CURVE('',#42934,#41964,#23247,.T.);
#57049=EDGE_CURVE('',#42935,#41619,#23248,.T.);
#57050=EDGE_CURVE('',#42936,#41618,#23249,.T.);
#57051=EDGE_CURVE('',#42930,#41617,#23250,.T.);
#57052=EDGE_CURVE('',#42931,#41616,#23251,.T.);
#57053=EDGE_CURVE('',#41967,#42932,#23252,.T.);
#57054=EDGE_CURVE('',#41966,#42933,#23253,.T.);
#57055=EDGE_CURVE('',#42943,#42944,#30543,.T.);
#57056=EDGE_CURVE('',#42944,#42945,#30544,.T.);
#57057=EDGE_CURVE('',#42945,#42946,#1559,.T.);
#57058=EDGE_CURVE('',#42946,#42947,#30545,.T.);
#57059=EDGE_CURVE('',#42947,#42943,#26684,.T.);
#57060=EDGE_CURVE('',#42948,#42949,#1560,.T.);
#57061=EDGE_CURVE('',#42949,#42950,#30546,.T.);
#57062=EDGE_CURVE('',#42951,#42950,#30547,.T.);
#57063=EDGE_CURVE('',#42951,#42952,#26685,.T.);
#57064=EDGE_CURVE('',#42952,#42948,#30548,.T.);
#57065=EDGE_CURVE('',#42950,#42953,#26686,.T.);
#57066=EDGE_CURVE('',#42953,#42944,#26687,.T.);
#57067=EDGE_CURVE('',#42943,#42954,#1561,.T.);
#57068=EDGE_CURVE('',#42954,#42951,#1562,.T.);
#57069=EDGE_CURVE('',#42952,#41124,#26688,.T.);
#57070=EDGE_CURVE('',#42955,#42951,#23254,.T.);
#57071=EDGE_CURVE('',#41124,#42955,#26689,.T.);
#57072=EDGE_CURVE('',#42956,#42943,#23255,.T.);
#57073=EDGE_CURVE('',#42955,#42956,#26690,.T.);
#57074=EDGE_CURVE('',#41123,#42947,#26691,.T.);
#57075=EDGE_CURVE('',#42956,#41123,#1563,.T.);
#57076=EDGE_CURVE('',#41961,#42952,#23256,.T.);
#57077=EDGE_CURVE('',#42948,#41960,#23257,.T.);
#57078=EDGE_CURVE('',#42949,#41623,#23258,.T.);
#57079=EDGE_CURVE('',#42950,#41622,#23259,.T.);
#57080=EDGE_CURVE('',#42944,#41621,#23260,.T.);
#57081=EDGE_CURVE('',#42945,#41620,#23261,.T.);
#57082=EDGE_CURVE('',#41963,#42946,#23262,.T.);
#57083=EDGE_CURVE('',#41962,#42947,#23263,.T.);
#57084=EDGE_CURVE('',#42957,#42958,#30549,.T.);
#57085=EDGE_CURVE('',#42958,#42959,#30550,.T.);
#57086=EDGE_CURVE('',#42959,#42960,#1564,.T.);
#57087=EDGE_CURVE('',#42960,#42961,#30551,.T.);
#57088=EDGE_CURVE('',#42961,#42957,#26692,.T.);
#57089=EDGE_CURVE('',#42962,#42963,#1565,.T.);
#57090=EDGE_CURVE('',#42963,#42964,#30552,.T.);
#57091=EDGE_CURVE('',#42965,#42964,#30553,.T.);
#57092=EDGE_CURVE('',#42965,#42966,#26693,.T.);
#57093=EDGE_CURVE('',#42966,#42962,#30554,.T.);
#57094=EDGE_CURVE('',#42964,#42967,#26694,.T.);
#57095=EDGE_CURVE('',#42967,#42958,#26695,.T.);
#57096=EDGE_CURVE('',#42957,#42968,#1566,.T.);
#57097=EDGE_CURVE('',#42968,#42965,#1567,.T.);
#57098=EDGE_CURVE('',#42966,#41120,#26696,.T.);
#57099=EDGE_CURVE('',#42969,#42965,#23264,.T.);
#57100=EDGE_CURVE('',#41120,#42969,#26697,.T.);
#57101=EDGE_CURVE('',#42970,#42957,#23265,.T.);
#57102=EDGE_CURVE('',#42969,#42970,#26698,.T.);
#57103=EDGE_CURVE('',#41119,#42961,#26699,.T.);
#57104=EDGE_CURVE('',#42970,#41119,#1568,.T.);
#57105=EDGE_CURVE('',#41957,#42966,#23266,.T.);
#57106=EDGE_CURVE('',#42962,#41956,#23267,.T.);
#57107=EDGE_CURVE('',#42963,#41627,#23268,.T.);
#57108=EDGE_CURVE('',#42964,#41626,#23269,.T.);
#57109=EDGE_CURVE('',#42958,#41625,#23270,.T.);
#57110=EDGE_CURVE('',#42959,#41624,#23271,.T.);
#57111=EDGE_CURVE('',#41959,#42960,#23272,.T.);
#57112=EDGE_CURVE('',#41958,#42961,#23273,.T.);
#57113=EDGE_CURVE('',#42971,#42972,#30555,.T.);
#57114=EDGE_CURVE('',#42972,#42973,#30556,.T.);
#57115=EDGE_CURVE('',#42973,#42974,#1569,.T.);
#57116=EDGE_CURVE('',#42974,#42975,#30557,.T.);
#57117=EDGE_CURVE('',#42975,#42971,#26700,.T.);
#57118=EDGE_CURVE('',#42976,#42977,#1570,.T.);
#57119=EDGE_CURVE('',#42977,#42978,#30558,.T.);
#57120=EDGE_CURVE('',#42979,#42978,#30559,.T.);
#57121=EDGE_CURVE('',#42979,#42980,#26701,.T.);
#57122=EDGE_CURVE('',#42980,#42976,#30560,.T.);
#57123=EDGE_CURVE('',#42978,#42981,#26702,.T.);
#57124=EDGE_CURVE('',#42981,#42972,#26703,.T.);
#57125=EDGE_CURVE('',#42971,#42982,#1571,.T.);
#57126=EDGE_CURVE('',#42982,#42979,#1572,.T.);
#57127=EDGE_CURVE('',#42980,#41116,#26704,.T.);
#57128=EDGE_CURVE('',#42983,#42979,#23274,.T.);
#57129=EDGE_CURVE('',#41116,#42983,#26705,.T.);
#57130=EDGE_CURVE('',#42984,#42971,#23275,.T.);
#57131=EDGE_CURVE('',#42983,#42984,#26706,.T.);
#57132=EDGE_CURVE('',#41115,#42975,#26707,.T.);
#57133=EDGE_CURVE('',#42984,#41115,#1573,.T.);
#57134=EDGE_CURVE('',#41953,#42980,#23276,.T.);
#57135=EDGE_CURVE('',#42976,#41952,#23277,.T.);
#57136=EDGE_CURVE('',#42977,#41631,#23278,.T.);
#57137=EDGE_CURVE('',#42978,#41630,#23279,.T.);
#57138=EDGE_CURVE('',#42972,#41629,#23280,.T.);
#57139=EDGE_CURVE('',#42973,#41628,#23281,.T.);
#57140=EDGE_CURVE('',#41955,#42974,#23282,.T.);
#57141=EDGE_CURVE('',#41954,#42975,#23283,.T.);
#57142=EDGE_CURVE('',#42985,#42986,#30561,.T.);
#57143=EDGE_CURVE('',#42986,#42987,#30562,.T.);
#57144=EDGE_CURVE('',#42987,#42988,#1574,.T.);
#57145=EDGE_CURVE('',#42988,#42989,#30563,.T.);
#57146=EDGE_CURVE('',#42989,#42985,#26708,.T.);
#57147=EDGE_CURVE('',#42990,#42991,#1575,.T.);
#57148=EDGE_CURVE('',#42991,#42992,#30564,.T.);
#57149=EDGE_CURVE('',#42993,#42992,#30565,.T.);
#57150=EDGE_CURVE('',#42993,#42994,#26709,.T.);
#57151=EDGE_CURVE('',#42994,#42990,#30566,.T.);
#57152=EDGE_CURVE('',#42992,#42995,#26710,.T.);
#57153=EDGE_CURVE('',#42995,#42986,#26711,.T.);
#57154=EDGE_CURVE('',#42985,#42996,#1576,.T.);
#57155=EDGE_CURVE('',#42996,#42993,#1577,.T.);
#57156=EDGE_CURVE('',#42994,#41112,#26712,.T.);
#57157=EDGE_CURVE('',#42997,#42993,#23284,.T.);
#57158=EDGE_CURVE('',#41112,#42997,#26713,.T.);
#57159=EDGE_CURVE('',#42998,#42985,#23285,.T.);
#57160=EDGE_CURVE('',#42997,#42998,#26714,.T.);
#57161=EDGE_CURVE('',#41111,#42989,#26715,.T.);
#57162=EDGE_CURVE('',#42998,#41111,#1578,.T.);
#57163=EDGE_CURVE('',#41949,#42994,#23286,.T.);
#57164=EDGE_CURVE('',#42990,#41948,#23287,.T.);
#57165=EDGE_CURVE('',#42991,#41635,#23288,.T.);
#57166=EDGE_CURVE('',#42992,#41634,#23289,.T.);
#57167=EDGE_CURVE('',#42986,#41633,#23290,.T.);
#57168=EDGE_CURVE('',#42987,#41632,#23291,.T.);
#57169=EDGE_CURVE('',#41951,#42988,#23292,.T.);
#57170=EDGE_CURVE('',#41950,#42989,#23293,.T.);
#57171=EDGE_CURVE('',#42999,#43000,#30567,.T.);
#57172=EDGE_CURVE('',#43000,#43001,#30568,.T.);
#57173=EDGE_CURVE('',#43001,#43002,#1579,.T.);
#57174=EDGE_CURVE('',#43002,#43003,#30569,.T.);
#57175=EDGE_CURVE('',#43003,#42999,#26716,.T.);
#57176=EDGE_CURVE('',#43004,#43005,#1580,.T.);
#57177=EDGE_CURVE('',#43005,#43006,#30570,.T.);
#57178=EDGE_CURVE('',#43007,#43006,#30571,.T.);
#57179=EDGE_CURVE('',#43007,#43008,#26717,.T.);
#57180=EDGE_CURVE('',#43008,#43004,#30572,.T.);
#57181=EDGE_CURVE('',#43006,#43009,#26718,.T.);
#57182=EDGE_CURVE('',#43009,#43000,#26719,.T.);
#57183=EDGE_CURVE('',#42999,#43010,#1581,.T.);
#57184=EDGE_CURVE('',#43010,#43007,#1582,.T.);
#57185=EDGE_CURVE('',#43008,#41108,#26720,.T.);
#57186=EDGE_CURVE('',#43011,#43007,#23294,.T.);
#57187=EDGE_CURVE('',#41108,#43011,#26721,.T.);
#57188=EDGE_CURVE('',#43012,#42999,#23295,.T.);
#57189=EDGE_CURVE('',#43011,#43012,#26722,.T.);
#57190=EDGE_CURVE('',#41107,#43003,#26723,.T.);
#57191=EDGE_CURVE('',#43012,#41107,#1583,.T.);
#57192=EDGE_CURVE('',#41945,#43008,#23296,.T.);
#57193=EDGE_CURVE('',#43004,#41944,#23297,.T.);
#57194=EDGE_CURVE('',#43005,#41639,#23298,.T.);
#57195=EDGE_CURVE('',#43006,#41638,#23299,.T.);
#57196=EDGE_CURVE('',#43000,#41637,#23300,.T.);
#57197=EDGE_CURVE('',#43001,#41636,#23301,.T.);
#57198=EDGE_CURVE('',#41947,#43002,#23302,.T.);
#57199=EDGE_CURVE('',#41946,#43003,#23303,.T.);
#57200=EDGE_CURVE('',#43013,#43014,#30573,.T.);
#57201=EDGE_CURVE('',#43014,#43015,#30574,.T.);
#57202=EDGE_CURVE('',#43015,#43016,#1584,.T.);
#57203=EDGE_CURVE('',#43016,#43017,#30575,.T.);
#57204=EDGE_CURVE('',#43017,#43013,#26724,.T.);
#57205=EDGE_CURVE('',#43018,#43019,#1585,.T.);
#57206=EDGE_CURVE('',#43019,#43020,#30576,.T.);
#57207=EDGE_CURVE('',#43021,#43020,#30577,.T.);
#57208=EDGE_CURVE('',#43021,#43022,#26725,.T.);
#57209=EDGE_CURVE('',#43022,#43018,#30578,.T.);
#57210=EDGE_CURVE('',#43020,#43023,#26726,.T.);
#57211=EDGE_CURVE('',#43023,#43014,#26727,.T.);
#57212=EDGE_CURVE('',#43013,#43024,#1586,.T.);
#57213=EDGE_CURVE('',#43024,#43021,#1587,.T.);
#57214=EDGE_CURVE('',#43022,#41104,#26728,.T.);
#57215=EDGE_CURVE('',#43025,#43021,#23304,.T.);
#57216=EDGE_CURVE('',#41104,#43025,#26729,.T.);
#57217=EDGE_CURVE('',#43026,#43013,#23305,.T.);
#57218=EDGE_CURVE('',#43025,#43026,#26730,.T.);
#57219=EDGE_CURVE('',#41103,#43017,#26731,.T.);
#57220=EDGE_CURVE('',#43026,#41103,#1588,.T.);
#57221=EDGE_CURVE('',#41941,#43022,#23306,.T.);
#57222=EDGE_CURVE('',#43018,#41940,#23307,.T.);
#57223=EDGE_CURVE('',#43019,#41643,#23308,.T.);
#57224=EDGE_CURVE('',#43020,#41642,#23309,.T.);
#57225=EDGE_CURVE('',#43014,#41641,#23310,.T.);
#57226=EDGE_CURVE('',#43015,#41640,#23311,.T.);
#57227=EDGE_CURVE('',#41943,#43016,#23312,.T.);
#57228=EDGE_CURVE('',#41942,#43017,#23313,.T.);
#57229=EDGE_CURVE('',#43027,#43028,#30579,.T.);
#57230=EDGE_CURVE('',#43028,#43029,#30580,.T.);
#57231=EDGE_CURVE('',#43029,#43030,#1589,.T.);
#57232=EDGE_CURVE('',#43030,#43031,#30581,.T.);
#57233=EDGE_CURVE('',#43031,#43027,#26732,.T.);
#57234=EDGE_CURVE('',#43032,#43033,#1590,.T.);
#57235=EDGE_CURVE('',#43033,#43034,#30582,.T.);
#57236=EDGE_CURVE('',#43035,#43034,#30583,.T.);
#57237=EDGE_CURVE('',#43035,#43036,#26733,.T.);
#57238=EDGE_CURVE('',#43036,#43032,#30584,.T.);
#57239=EDGE_CURVE('',#43034,#43037,#26734,.T.);
#57240=EDGE_CURVE('',#43037,#43028,#26735,.T.);
#57241=EDGE_CURVE('',#43027,#43038,#1591,.T.);
#57242=EDGE_CURVE('',#43038,#43035,#1592,.T.);
#57243=EDGE_CURVE('',#43036,#41100,#26736,.T.);
#57244=EDGE_CURVE('',#43039,#43035,#23314,.T.);
#57245=EDGE_CURVE('',#41100,#43039,#26737,.T.);
#57246=EDGE_CURVE('',#43040,#43027,#23315,.T.);
#57247=EDGE_CURVE('',#43039,#43040,#26738,.T.);
#57248=EDGE_CURVE('',#41099,#43031,#26739,.T.);
#57249=EDGE_CURVE('',#43040,#41099,#1593,.T.);
#57250=EDGE_CURVE('',#41937,#43036,#23316,.T.);
#57251=EDGE_CURVE('',#43032,#41936,#23317,.T.);
#57252=EDGE_CURVE('',#43033,#41647,#23318,.T.);
#57253=EDGE_CURVE('',#43034,#41646,#23319,.T.);
#57254=EDGE_CURVE('',#43028,#41645,#23320,.T.);
#57255=EDGE_CURVE('',#43029,#41644,#23321,.T.);
#57256=EDGE_CURVE('',#41939,#43030,#23322,.T.);
#57257=EDGE_CURVE('',#41938,#43031,#23323,.T.);
#57258=EDGE_CURVE('',#43041,#43042,#30585,.T.);
#57259=EDGE_CURVE('',#43042,#43043,#30586,.T.);
#57260=EDGE_CURVE('',#43043,#43044,#1594,.T.);
#57261=EDGE_CURVE('',#43044,#43045,#30587,.T.);
#57262=EDGE_CURVE('',#43045,#43041,#26740,.T.);
#57263=EDGE_CURVE('',#43046,#43047,#1595,.T.);
#57264=EDGE_CURVE('',#43047,#43048,#30588,.T.);
#57265=EDGE_CURVE('',#43049,#43048,#30589,.T.);
#57266=EDGE_CURVE('',#43049,#43050,#26741,.T.);
#57267=EDGE_CURVE('',#43050,#43046,#30590,.T.);
#57268=EDGE_CURVE('',#43048,#43051,#26742,.T.);
#57269=EDGE_CURVE('',#43051,#43042,#26743,.T.);
#57270=EDGE_CURVE('',#43041,#43052,#1596,.T.);
#57271=EDGE_CURVE('',#43052,#43049,#1597,.T.);
#57272=EDGE_CURVE('',#43050,#41096,#26744,.T.);
#57273=EDGE_CURVE('',#43053,#43049,#23324,.T.);
#57274=EDGE_CURVE('',#41096,#43053,#26745,.T.);
#57275=EDGE_CURVE('',#43054,#43041,#23325,.T.);
#57276=EDGE_CURVE('',#43053,#43054,#26746,.T.);
#57277=EDGE_CURVE('',#41095,#43045,#26747,.T.);
#57278=EDGE_CURVE('',#43054,#41095,#1598,.T.);
#57279=EDGE_CURVE('',#41933,#43050,#23326,.T.);
#57280=EDGE_CURVE('',#43046,#41932,#23327,.T.);
#57281=EDGE_CURVE('',#43047,#41651,#23328,.T.);
#57282=EDGE_CURVE('',#43048,#41650,#23329,.T.);
#57283=EDGE_CURVE('',#43042,#41649,#23330,.T.);
#57284=EDGE_CURVE('',#43043,#41648,#23331,.T.);
#57285=EDGE_CURVE('',#41935,#43044,#23332,.T.);
#57286=EDGE_CURVE('',#41934,#43045,#23333,.T.);
#57287=EDGE_CURVE('',#43055,#43056,#30591,.T.);
#57288=EDGE_CURVE('',#43056,#43057,#30592,.T.);
#57289=EDGE_CURVE('',#43057,#43058,#1599,.T.);
#57290=EDGE_CURVE('',#43058,#43059,#30593,.T.);
#57291=EDGE_CURVE('',#43059,#43055,#26748,.T.);
#57292=EDGE_CURVE('',#43060,#43061,#1600,.T.);
#57293=EDGE_CURVE('',#43061,#43062,#30594,.T.);
#57294=EDGE_CURVE('',#43063,#43062,#30595,.T.);
#57295=EDGE_CURVE('',#43063,#43064,#26749,.T.);
#57296=EDGE_CURVE('',#43064,#43060,#30596,.T.);
#57297=EDGE_CURVE('',#43062,#43065,#26750,.T.);
#57298=EDGE_CURVE('',#43065,#43056,#26751,.T.);
#57299=EDGE_CURVE('',#43055,#43066,#1601,.T.);
#57300=EDGE_CURVE('',#43066,#43063,#1602,.T.);
#57301=EDGE_CURVE('',#43064,#41092,#26752,.T.);
#57302=EDGE_CURVE('',#43067,#43063,#23334,.T.);
#57303=EDGE_CURVE('',#41092,#43067,#26753,.T.);
#57304=EDGE_CURVE('',#43068,#43055,#23335,.T.);
#57305=EDGE_CURVE('',#43067,#43068,#26754,.T.);
#57306=EDGE_CURVE('',#41091,#43059,#26755,.T.);
#57307=EDGE_CURVE('',#43068,#41091,#1603,.T.);
#57308=EDGE_CURVE('',#41929,#43064,#23336,.T.);
#57309=EDGE_CURVE('',#43060,#41928,#23337,.T.);
#57310=EDGE_CURVE('',#43061,#41655,#23338,.T.);
#57311=EDGE_CURVE('',#43062,#41654,#23339,.T.);
#57312=EDGE_CURVE('',#43056,#41653,#23340,.T.);
#57313=EDGE_CURVE('',#43057,#41652,#23341,.T.);
#57314=EDGE_CURVE('',#41931,#43058,#23342,.T.);
#57315=EDGE_CURVE('',#41930,#43059,#23343,.T.);
#57316=EDGE_CURVE('',#43069,#43070,#30597,.T.);
#57317=EDGE_CURVE('',#43070,#43071,#30598,.T.);
#57318=EDGE_CURVE('',#43071,#43072,#1604,.T.);
#57319=EDGE_CURVE('',#43072,#43073,#30599,.T.);
#57320=EDGE_CURVE('',#43073,#43069,#26756,.T.);
#57321=EDGE_CURVE('',#43074,#43075,#1605,.T.);
#57322=EDGE_CURVE('',#43075,#43076,#30600,.T.);
#57323=EDGE_CURVE('',#43077,#43076,#30601,.T.);
#57324=EDGE_CURVE('',#43077,#43078,#26757,.T.);
#57325=EDGE_CURVE('',#43078,#43074,#30602,.T.);
#57326=EDGE_CURVE('',#43076,#43079,#26758,.T.);
#57327=EDGE_CURVE('',#43079,#43070,#26759,.T.);
#57328=EDGE_CURVE('',#43069,#43080,#1606,.T.);
#57329=EDGE_CURVE('',#43080,#43077,#1607,.T.);
#57330=EDGE_CURVE('',#43078,#41088,#26760,.T.);
#57331=EDGE_CURVE('',#43081,#43077,#23344,.T.);
#57332=EDGE_CURVE('',#41088,#43081,#26761,.T.);
#57333=EDGE_CURVE('',#43082,#43069,#23345,.T.);
#57334=EDGE_CURVE('',#43081,#43082,#26762,.T.);
#57335=EDGE_CURVE('',#41087,#43073,#26763,.T.);
#57336=EDGE_CURVE('',#43082,#41087,#1608,.T.);
#57337=EDGE_CURVE('',#41925,#43078,#23346,.T.);
#57338=EDGE_CURVE('',#43074,#41924,#23347,.T.);
#57339=EDGE_CURVE('',#43075,#41659,#23348,.T.);
#57340=EDGE_CURVE('',#43076,#41658,#23349,.T.);
#57341=EDGE_CURVE('',#43070,#41657,#23350,.T.);
#57342=EDGE_CURVE('',#43071,#41656,#23351,.T.);
#57343=EDGE_CURVE('',#41927,#43072,#23352,.T.);
#57344=EDGE_CURVE('',#41926,#43073,#23353,.T.);
#57345=EDGE_CURVE('',#43083,#43084,#30603,.T.);
#57346=EDGE_CURVE('',#43084,#43085,#30604,.T.);
#57347=EDGE_CURVE('',#43085,#43086,#1609,.T.);
#57348=EDGE_CURVE('',#43086,#43087,#30605,.T.);
#57349=EDGE_CURVE('',#43087,#43083,#26764,.T.);
#57350=EDGE_CURVE('',#43088,#43089,#1610,.T.);
#57351=EDGE_CURVE('',#43089,#43090,#30606,.T.);
#57352=EDGE_CURVE('',#43091,#43090,#30607,.T.);
#57353=EDGE_CURVE('',#43091,#43092,#26765,.T.);
#57354=EDGE_CURVE('',#43092,#43088,#30608,.T.);
#57355=EDGE_CURVE('',#43090,#43093,#26766,.T.);
#57356=EDGE_CURVE('',#43093,#43084,#26767,.T.);
#57357=EDGE_CURVE('',#43083,#43094,#1611,.T.);
#57358=EDGE_CURVE('',#43094,#43091,#1612,.T.);
#57359=EDGE_CURVE('',#43092,#41084,#26768,.T.);
#57360=EDGE_CURVE('',#43095,#43091,#23354,.T.);
#57361=EDGE_CURVE('',#41084,#43095,#26769,.T.);
#57362=EDGE_CURVE('',#43096,#43083,#23355,.T.);
#57363=EDGE_CURVE('',#43095,#43096,#26770,.T.);
#57364=EDGE_CURVE('',#41083,#43087,#26771,.T.);
#57365=EDGE_CURVE('',#43096,#41083,#1613,.T.);
#57366=EDGE_CURVE('',#41921,#43092,#23356,.T.);
#57367=EDGE_CURVE('',#43088,#41920,#23357,.T.);
#57368=EDGE_CURVE('',#43089,#41663,#23358,.T.);
#57369=EDGE_CURVE('',#43090,#41662,#23359,.T.);
#57370=EDGE_CURVE('',#43084,#41661,#23360,.T.);
#57371=EDGE_CURVE('',#43085,#41660,#23361,.T.);
#57372=EDGE_CURVE('',#41923,#43086,#23362,.T.);
#57373=EDGE_CURVE('',#41922,#43087,#23363,.T.);
#57374=EDGE_CURVE('',#43097,#43098,#30609,.T.);
#57375=EDGE_CURVE('',#43098,#43099,#30610,.T.);
#57376=EDGE_CURVE('',#43099,#43100,#1614,.T.);
#57377=EDGE_CURVE('',#43100,#43101,#30611,.T.);
#57378=EDGE_CURVE('',#43101,#43097,#26772,.T.);
#57379=EDGE_CURVE('',#43102,#43103,#1615,.T.);
#57380=EDGE_CURVE('',#43103,#43104,#30612,.T.);
#57381=EDGE_CURVE('',#43105,#43104,#30613,.T.);
#57382=EDGE_CURVE('',#43105,#43106,#26773,.T.);
#57383=EDGE_CURVE('',#43106,#43102,#30614,.T.);
#57384=EDGE_CURVE('',#43104,#43107,#26774,.T.);
#57385=EDGE_CURVE('',#43107,#43098,#26775,.T.);
#57386=EDGE_CURVE('',#43097,#43108,#1616,.T.);
#57387=EDGE_CURVE('',#43108,#43105,#1617,.T.);
#57388=EDGE_CURVE('',#43106,#41080,#26776,.T.);
#57389=EDGE_CURVE('',#43109,#43105,#23364,.T.);
#57390=EDGE_CURVE('',#41080,#43109,#26777,.T.);
#57391=EDGE_CURVE('',#43110,#43097,#23365,.T.);
#57392=EDGE_CURVE('',#43109,#43110,#26778,.T.);
#57393=EDGE_CURVE('',#41079,#43101,#26779,.T.);
#57394=EDGE_CURVE('',#43110,#41079,#1618,.T.);
#57395=EDGE_CURVE('',#41917,#43106,#23366,.T.);
#57396=EDGE_CURVE('',#43102,#41916,#23367,.T.);
#57397=EDGE_CURVE('',#43103,#41667,#23368,.T.);
#57398=EDGE_CURVE('',#43104,#41666,#23369,.T.);
#57399=EDGE_CURVE('',#43098,#41665,#23370,.T.);
#57400=EDGE_CURVE('',#43099,#41664,#23371,.T.);
#57401=EDGE_CURVE('',#41919,#43100,#23372,.T.);
#57402=EDGE_CURVE('',#41918,#43101,#23373,.T.);
#78450=ORIENTED_EDGE('',*,*,#53727,.F.);
#78451=ORIENTED_EDGE('',*,*,#53728,.F.);
#78452=ORIENTED_EDGE('',*,*,#53729,.T.);
#78453=ORIENTED_EDGE('',*,*,#53730,.F.);
#78454=ORIENTED_EDGE('',*,*,#53731,.F.);
#78455=ORIENTED_EDGE('',*,*,#53727,.T.);
#78456=ORIENTED_EDGE('',*,*,#53732,.T.);
#78457=ORIENTED_EDGE('',*,*,#53733,.F.);
#78458=ORIENTED_EDGE('',*,*,#53734,.F.);
#78459=ORIENTED_EDGE('',*,*,#53730,.T.);
#78460=ORIENTED_EDGE('',*,*,#53735,.T.);
#78461=ORIENTED_EDGE('',*,*,#53736,.F.);
#78462=ORIENTED_EDGE('',*,*,#53737,.F.);
#78463=ORIENTED_EDGE('',*,*,#53733,.T.);
#78464=ORIENTED_EDGE('',*,*,#53738,.T.);
#78465=ORIENTED_EDGE('',*,*,#53739,.F.);
#78466=ORIENTED_EDGE('',*,*,#53740,.F.);
#78467=ORIENTED_EDGE('',*,*,#53736,.T.);
#78468=ORIENTED_EDGE('',*,*,#53741,.T.);
#78469=ORIENTED_EDGE('',*,*,#53742,.F.);
#78470=ORIENTED_EDGE('',*,*,#53743,.F.);
#78471=ORIENTED_EDGE('',*,*,#53739,.T.);
#78472=ORIENTED_EDGE('',*,*,#53744,.T.);
#78473=ORIENTED_EDGE('',*,*,#53745,.F.);
#78474=ORIENTED_EDGE('',*,*,#53746,.F.);
#78475=ORIENTED_EDGE('',*,*,#53742,.T.);
#78476=ORIENTED_EDGE('',*,*,#53747,.T.);
#78477=ORIENTED_EDGE('',*,*,#53748,.F.);
#78478=ORIENTED_EDGE('',*,*,#53749,.F.);
#78479=ORIENTED_EDGE('',*,*,#53745,.T.);
#78480=ORIENTED_EDGE('',*,*,#53750,.T.);
#78481=ORIENTED_EDGE('',*,*,#53751,.F.);
#78482=ORIENTED_EDGE('',*,*,#53752,.F.);
#78483=ORIENTED_EDGE('',*,*,#53748,.T.);
#78484=ORIENTED_EDGE('',*,*,#53753,.T.);
#78485=ORIENTED_EDGE('',*,*,#53754,.F.);
#78486=ORIENTED_EDGE('',*,*,#53755,.F.);
#78487=ORIENTED_EDGE('',*,*,#53751,.T.);
#78488=ORIENTED_EDGE('',*,*,#53756,.T.);
#78489=ORIENTED_EDGE('',*,*,#53757,.F.);
#78490=ORIENTED_EDGE('',*,*,#53758,.F.);
#78491=ORIENTED_EDGE('',*,*,#53754,.T.);
#78492=ORIENTED_EDGE('',*,*,#53759,.T.);
#78493=ORIENTED_EDGE('',*,*,#53760,.F.);
#78494=ORIENTED_EDGE('',*,*,#53761,.F.);
#78495=ORIENTED_EDGE('',*,*,#53757,.T.);
#78496=ORIENTED_EDGE('',*,*,#53762,.T.);
#78497=ORIENTED_EDGE('',*,*,#53763,.F.);
#78498=ORIENTED_EDGE('',*,*,#53764,.F.);
#78499=ORIENTED_EDGE('',*,*,#53760,.T.);
#78500=ORIENTED_EDGE('',*,*,#53765,.T.);
#78501=ORIENTED_EDGE('',*,*,#53766,.F.);
#78502=ORIENTED_EDGE('',*,*,#53767,.F.);
#78503=ORIENTED_EDGE('',*,*,#53763,.T.);
#78504=ORIENTED_EDGE('',*,*,#53768,.T.);
#78505=ORIENTED_EDGE('',*,*,#53769,.F.);
#78506=ORIENTED_EDGE('',*,*,#53770,.F.);
#78507=ORIENTED_EDGE('',*,*,#53766,.T.);
#78508=ORIENTED_EDGE('',*,*,#53771,.T.);
#78509=ORIENTED_EDGE('',*,*,#53772,.F.);
#78510=ORIENTED_EDGE('',*,*,#53773,.F.);
#78511=ORIENTED_EDGE('',*,*,#53769,.T.);
#78512=ORIENTED_EDGE('',*,*,#53774,.T.);
#78513=ORIENTED_EDGE('',*,*,#53775,.F.);
#78514=ORIENTED_EDGE('',*,*,#53776,.F.);
#78515=ORIENTED_EDGE('',*,*,#53772,.T.);
#78516=ORIENTED_EDGE('',*,*,#53777,.T.);
#78517=ORIENTED_EDGE('',*,*,#53778,.F.);
#78518=ORIENTED_EDGE('',*,*,#53779,.F.);
#78519=ORIENTED_EDGE('',*,*,#53775,.T.);
#78520=ORIENTED_EDGE('',*,*,#53780,.T.);
#78521=ORIENTED_EDGE('',*,*,#53781,.F.);
#78522=ORIENTED_EDGE('',*,*,#53782,.F.);
#78523=ORIENTED_EDGE('',*,*,#53778,.T.);
#78524=ORIENTED_EDGE('',*,*,#53783,.T.);
#78525=ORIENTED_EDGE('',*,*,#53784,.F.);
#78526=ORIENTED_EDGE('',*,*,#53785,.F.);
#78527=ORIENTED_EDGE('',*,*,#53781,.T.);
#78528=ORIENTED_EDGE('',*,*,#53786,.T.);
#78529=ORIENTED_EDGE('',*,*,#53787,.F.);
#78530=ORIENTED_EDGE('',*,*,#53788,.F.);
#78531=ORIENTED_EDGE('',*,*,#53784,.T.);
#78532=ORIENTED_EDGE('',*,*,#53789,.T.);
#78533=ORIENTED_EDGE('',*,*,#53790,.F.);
#78534=ORIENTED_EDGE('',*,*,#53791,.F.);
#78535=ORIENTED_EDGE('',*,*,#53787,.T.);
#78536=ORIENTED_EDGE('',*,*,#53792,.T.);
#78537=ORIENTED_EDGE('',*,*,#53793,.F.);
#78538=ORIENTED_EDGE('',*,*,#53794,.F.);
#78539=ORIENTED_EDGE('',*,*,#53790,.T.);
#78540=ORIENTED_EDGE('',*,*,#53795,.T.);
#78541=ORIENTED_EDGE('',*,*,#53796,.F.);
#78542=ORIENTED_EDGE('',*,*,#53797,.F.);
#78543=ORIENTED_EDGE('',*,*,#53793,.T.);
#78544=ORIENTED_EDGE('',*,*,#53798,.T.);
#78545=ORIENTED_EDGE('',*,*,#53799,.F.);
#78546=ORIENTED_EDGE('',*,*,#53800,.F.);
#78547=ORIENTED_EDGE('',*,*,#53796,.T.);
#78548=ORIENTED_EDGE('',*,*,#53801,.T.);
#78549=ORIENTED_EDGE('',*,*,#53802,.F.);
#78550=ORIENTED_EDGE('',*,*,#53803,.F.);
#78551=ORIENTED_EDGE('',*,*,#53799,.T.);
#78552=ORIENTED_EDGE('',*,*,#53804,.T.);
#78553=ORIENTED_EDGE('',*,*,#53805,.F.);
#78554=ORIENTED_EDGE('',*,*,#53806,.F.);
#78555=ORIENTED_EDGE('',*,*,#53802,.T.);
#78556=ORIENTED_EDGE('',*,*,#53807,.T.);
#78557=ORIENTED_EDGE('',*,*,#53808,.F.);
#78558=ORIENTED_EDGE('',*,*,#53809,.F.);
#78559=ORIENTED_EDGE('',*,*,#53805,.T.);
#78560=ORIENTED_EDGE('',*,*,#53810,.T.);
#78561=ORIENTED_EDGE('',*,*,#53811,.F.);
#78562=ORIENTED_EDGE('',*,*,#53812,.F.);
#78563=ORIENTED_EDGE('',*,*,#53808,.T.);
#78564=ORIENTED_EDGE('',*,*,#53813,.T.);
#78565=ORIENTED_EDGE('',*,*,#53814,.F.);
#78566=ORIENTED_EDGE('',*,*,#53815,.F.);
#78567=ORIENTED_EDGE('',*,*,#53811,.T.);
#78568=ORIENTED_EDGE('',*,*,#53816,.T.);
#78569=ORIENTED_EDGE('',*,*,#53817,.F.);
#78570=ORIENTED_EDGE('',*,*,#53818,.F.);
#78571=ORIENTED_EDGE('',*,*,#53814,.T.);
#78572=ORIENTED_EDGE('',*,*,#53819,.T.);
#78573=ORIENTED_EDGE('',*,*,#53820,.F.);
#78574=ORIENTED_EDGE('',*,*,#53821,.F.);
#78575=ORIENTED_EDGE('',*,*,#53817,.T.);
#78576=ORIENTED_EDGE('',*,*,#53822,.T.);
#78577=ORIENTED_EDGE('',*,*,#53823,.F.);
#78578=ORIENTED_EDGE('',*,*,#53824,.F.);
#78579=ORIENTED_EDGE('',*,*,#53820,.T.);
#78580=ORIENTED_EDGE('',*,*,#53825,.T.);
#78581=ORIENTED_EDGE('',*,*,#53826,.F.);
#78582=ORIENTED_EDGE('',*,*,#53827,.F.);
#78583=ORIENTED_EDGE('',*,*,#53823,.T.);
#78584=ORIENTED_EDGE('',*,*,#53828,.T.);
#78585=ORIENTED_EDGE('',*,*,#53829,.F.);
#78586=ORIENTED_EDGE('',*,*,#53830,.F.);
#78587=ORIENTED_EDGE('',*,*,#53826,.T.);
#78588=ORIENTED_EDGE('',*,*,#53831,.T.);
#78589=ORIENTED_EDGE('',*,*,#53832,.F.);
#78590=ORIENTED_EDGE('',*,*,#53833,.F.);
#78591=ORIENTED_EDGE('',*,*,#53829,.T.);
#78592=ORIENTED_EDGE('',*,*,#53834,.T.);
#78593=ORIENTED_EDGE('',*,*,#53835,.F.);
#78594=ORIENTED_EDGE('',*,*,#53836,.T.);
#78595=ORIENTED_EDGE('',*,*,#53837,.T.);
#78596=ORIENTED_EDGE('',*,*,#53838,.T.);
#78597=ORIENTED_EDGE('',*,*,#53839,.F.);
#78598=ORIENTED_EDGE('',*,*,#53840,.F.);
#78599=ORIENTED_EDGE('',*,*,#53841,.T.);
#78600=ORIENTED_EDGE('',*,*,#53842,.F.);
#78601=ORIENTED_EDGE('',*,*,#53843,.F.);
#78602=ORIENTED_EDGE('',*,*,#53844,.T.);
#78603=ORIENTED_EDGE('',*,*,#53845,.F.);
#78604=ORIENTED_EDGE('',*,*,#53846,.F.);
#78605=ORIENTED_EDGE('',*,*,#53847,.F.);
#78606=ORIENTED_EDGE('',*,*,#53842,.T.);
#78607=ORIENTED_EDGE('',*,*,#53848,.F.);
#78608=ORIENTED_EDGE('',*,*,#53849,.F.);
#78609=ORIENTED_EDGE('',*,*,#53850,.F.);
#78610=ORIENTED_EDGE('',*,*,#53846,.T.);
#78611=ORIENTED_EDGE('',*,*,#53851,.F.);
#78612=ORIENTED_EDGE('',*,*,#53852,.F.);
#78613=ORIENTED_EDGE('',*,*,#53853,.F.);
#78614=ORIENTED_EDGE('',*,*,#53849,.T.);
#78615=ORIENTED_EDGE('',*,*,#53854,.F.);
#78616=ORIENTED_EDGE('',*,*,#53855,.F.);
#78617=ORIENTED_EDGE('',*,*,#53856,.F.);
#78618=ORIENTED_EDGE('',*,*,#53852,.T.);
#78619=ORIENTED_EDGE('',*,*,#53857,.F.);
#78620=ORIENTED_EDGE('',*,*,#53858,.F.);
#78621=ORIENTED_EDGE('',*,*,#53859,.F.);
#78622=ORIENTED_EDGE('',*,*,#53855,.T.);
#78623=ORIENTED_EDGE('',*,*,#53860,.F.);
#78624=ORIENTED_EDGE('',*,*,#53861,.F.);
#78625=ORIENTED_EDGE('',*,*,#53862,.F.);
#78626=ORIENTED_EDGE('',*,*,#53858,.T.);
#78627=ORIENTED_EDGE('',*,*,#53863,.F.);
#78628=ORIENTED_EDGE('',*,*,#53864,.F.);
#78629=ORIENTED_EDGE('',*,*,#53865,.F.);
#78630=ORIENTED_EDGE('',*,*,#53861,.T.);
#78631=ORIENTED_EDGE('',*,*,#53866,.F.);
#78632=ORIENTED_EDGE('',*,*,#53867,.F.);
#78633=ORIENTED_EDGE('',*,*,#53868,.F.);
#78634=ORIENTED_EDGE('',*,*,#53864,.T.);
#78635=ORIENTED_EDGE('',*,*,#53869,.F.);
#78636=ORIENTED_EDGE('',*,*,#53870,.F.);
#78637=ORIENTED_EDGE('',*,*,#53871,.F.);
#78638=ORIENTED_EDGE('',*,*,#53867,.T.);
#78639=ORIENTED_EDGE('',*,*,#53872,.F.);
#78640=ORIENTED_EDGE('',*,*,#53873,.F.);
#78641=ORIENTED_EDGE('',*,*,#53874,.F.);
#78642=ORIENTED_EDGE('',*,*,#53870,.T.);
#78643=ORIENTED_EDGE('',*,*,#53875,.F.);
#78644=ORIENTED_EDGE('',*,*,#53876,.F.);
#78645=ORIENTED_EDGE('',*,*,#53877,.F.);
#78646=ORIENTED_EDGE('',*,*,#53873,.T.);
#78647=ORIENTED_EDGE('',*,*,#53878,.F.);
#78648=ORIENTED_EDGE('',*,*,#53879,.F.);
#78649=ORIENTED_EDGE('',*,*,#53880,.F.);
#78650=ORIENTED_EDGE('',*,*,#53876,.T.);
#78651=ORIENTED_EDGE('',*,*,#53881,.F.);
#78652=ORIENTED_EDGE('',*,*,#53882,.F.);
#78653=ORIENTED_EDGE('',*,*,#53883,.F.);
#78654=ORIENTED_EDGE('',*,*,#53879,.T.);
#78655=ORIENTED_EDGE('',*,*,#53884,.F.);
#78656=ORIENTED_EDGE('',*,*,#53885,.F.);
#78657=ORIENTED_EDGE('',*,*,#53886,.F.);
#78658=ORIENTED_EDGE('',*,*,#53882,.T.);
#78659=ORIENTED_EDGE('',*,*,#53887,.F.);
#78660=ORIENTED_EDGE('',*,*,#53888,.F.);
#78661=ORIENTED_EDGE('',*,*,#53889,.F.);
#78662=ORIENTED_EDGE('',*,*,#53885,.T.);
#78663=ORIENTED_EDGE('',*,*,#53890,.F.);
#78664=ORIENTED_EDGE('',*,*,#53891,.F.);
#78665=ORIENTED_EDGE('',*,*,#53892,.F.);
#78666=ORIENTED_EDGE('',*,*,#53888,.T.);
#78667=ORIENTED_EDGE('',*,*,#53893,.F.);
#78668=ORIENTED_EDGE('',*,*,#53894,.F.);
#78669=ORIENTED_EDGE('',*,*,#53895,.F.);
#78670=ORIENTED_EDGE('',*,*,#53891,.T.);
#78671=ORIENTED_EDGE('',*,*,#53896,.F.);
#78672=ORIENTED_EDGE('',*,*,#53897,.F.);
#78673=ORIENTED_EDGE('',*,*,#53898,.F.);
#78674=ORIENTED_EDGE('',*,*,#53894,.T.);
#78675=ORIENTED_EDGE('',*,*,#53899,.F.);
#78676=ORIENTED_EDGE('',*,*,#53900,.F.);
#78677=ORIENTED_EDGE('',*,*,#53901,.F.);
#78678=ORIENTED_EDGE('',*,*,#53897,.T.);
#78679=ORIENTED_EDGE('',*,*,#53902,.F.);
#78680=ORIENTED_EDGE('',*,*,#53903,.F.);
#78681=ORIENTED_EDGE('',*,*,#53904,.F.);
#78682=ORIENTED_EDGE('',*,*,#53900,.T.);
#78683=ORIENTED_EDGE('',*,*,#53905,.F.);
#78684=ORIENTED_EDGE('',*,*,#53906,.F.);
#78685=ORIENTED_EDGE('',*,*,#53907,.F.);
#78686=ORIENTED_EDGE('',*,*,#53903,.T.);
#78687=ORIENTED_EDGE('',*,*,#53908,.F.);
#78688=ORIENTED_EDGE('',*,*,#53909,.F.);
#78689=ORIENTED_EDGE('',*,*,#53910,.F.);
#78690=ORIENTED_EDGE('',*,*,#53906,.T.);
#78691=ORIENTED_EDGE('',*,*,#53911,.F.);
#78692=ORIENTED_EDGE('',*,*,#53912,.F.);
#78693=ORIENTED_EDGE('',*,*,#53913,.F.);
#78694=ORIENTED_EDGE('',*,*,#53909,.T.);
#78695=ORIENTED_EDGE('',*,*,#53914,.F.);
#78696=ORIENTED_EDGE('',*,*,#53915,.F.);
#78697=ORIENTED_EDGE('',*,*,#53916,.F.);
#78698=ORIENTED_EDGE('',*,*,#53912,.T.);
#78699=ORIENTED_EDGE('',*,*,#53917,.F.);
#78700=ORIENTED_EDGE('',*,*,#53918,.F.);
#78701=ORIENTED_EDGE('',*,*,#53919,.F.);
#78702=ORIENTED_EDGE('',*,*,#53915,.T.);
#78703=ORIENTED_EDGE('',*,*,#53920,.F.);
#78704=ORIENTED_EDGE('',*,*,#53921,.F.);
#78705=ORIENTED_EDGE('',*,*,#53922,.F.);
#78706=ORIENTED_EDGE('',*,*,#53918,.T.);
#78707=ORIENTED_EDGE('',*,*,#53923,.F.);
#78708=ORIENTED_EDGE('',*,*,#53924,.F.);
#78709=ORIENTED_EDGE('',*,*,#53925,.F.);
#78710=ORIENTED_EDGE('',*,*,#53921,.T.);
#78711=ORIENTED_EDGE('',*,*,#53926,.F.);
#78712=ORIENTED_EDGE('',*,*,#53927,.F.);
#78713=ORIENTED_EDGE('',*,*,#53928,.F.);
#78714=ORIENTED_EDGE('',*,*,#53924,.T.);
#78715=ORIENTED_EDGE('',*,*,#53929,.F.);
#78716=ORIENTED_EDGE('',*,*,#53930,.F.);
#78717=ORIENTED_EDGE('',*,*,#53931,.F.);
#78718=ORIENTED_EDGE('',*,*,#53927,.T.);
#78719=ORIENTED_EDGE('',*,*,#53932,.F.);
#78720=ORIENTED_EDGE('',*,*,#53933,.F.);
#78721=ORIENTED_EDGE('',*,*,#53934,.F.);
#78722=ORIENTED_EDGE('',*,*,#53930,.T.);
#78723=ORIENTED_EDGE('',*,*,#53935,.F.);
#78724=ORIENTED_EDGE('',*,*,#53936,.F.);
#78725=ORIENTED_EDGE('',*,*,#53937,.F.);
#78726=ORIENTED_EDGE('',*,*,#53933,.T.);
#78727=ORIENTED_EDGE('',*,*,#53938,.F.);
#78728=ORIENTED_EDGE('',*,*,#53939,.F.);
#78729=ORIENTED_EDGE('',*,*,#53940,.F.);
#78730=ORIENTED_EDGE('',*,*,#53941,.F.);
#78731=ORIENTED_EDGE('',*,*,#53936,.T.);
#78732=ORIENTED_EDGE('',*,*,#53942,.F.);
#78733=ORIENTED_EDGE('',*,*,#53943,.F.);
#78734=ORIENTED_EDGE('',*,*,#53944,.F.);
#78735=ORIENTED_EDGE('',*,*,#53940,.T.);
#78736=ORIENTED_EDGE('',*,*,#53945,.F.);
#78737=ORIENTED_EDGE('',*,*,#53946,.T.);
#78738=ORIENTED_EDGE('',*,*,#53947,.T.);
#78739=ORIENTED_EDGE('',*,*,#53948,.F.);
#78740=ORIENTED_EDGE('',*,*,#53949,.F.);
#78741=ORIENTED_EDGE('',*,*,#53950,.T.);
#78742=ORIENTED_EDGE('',*,*,#53951,.F.);
#78743=ORIENTED_EDGE('',*,*,#53947,.F.);
#78744=ORIENTED_EDGE('',*,*,#53952,.F.);
#78745=ORIENTED_EDGE('',*,*,#53953,.F.);
#78746=ORIENTED_EDGE('',*,*,#53954,.F.);
#78747=ORIENTED_EDGE('',*,*,#53955,.T.);
#78748=ORIENTED_EDGE('',*,*,#53956,.F.);
#78749=ORIENTED_EDGE('',*,*,#53957,.F.);
#78750=ORIENTED_EDGE('',*,*,#53958,.F.);
#78751=ORIENTED_EDGE('',*,*,#53959,.T.);
#78752=ORIENTED_EDGE('',*,*,#53960,.F.);
#78753=ORIENTED_EDGE('',*,*,#53961,.F.);
#78754=ORIENTED_EDGE('',*,*,#53962,.F.);
#78755=ORIENTED_EDGE('',*,*,#53963,.T.);
#78756=ORIENTED_EDGE('',*,*,#53964,.F.);
#78757=ORIENTED_EDGE('',*,*,#53965,.F.);
#78758=ORIENTED_EDGE('',*,*,#53966,.F.);
#78759=ORIENTED_EDGE('',*,*,#53967,.T.);
#78760=ORIENTED_EDGE('',*,*,#53968,.F.);
#78761=ORIENTED_EDGE('',*,*,#53969,.F.);
#78762=ORIENTED_EDGE('',*,*,#53970,.F.);
#78763=ORIENTED_EDGE('',*,*,#53971,.T.);
#78764=ORIENTED_EDGE('',*,*,#53972,.F.);
#78765=ORIENTED_EDGE('',*,*,#53973,.F.);
#78766=ORIENTED_EDGE('',*,*,#53974,.F.);
#78767=ORIENTED_EDGE('',*,*,#53975,.T.);
#78768=ORIENTED_EDGE('',*,*,#53976,.F.);
#78769=ORIENTED_EDGE('',*,*,#53977,.F.);
#78770=ORIENTED_EDGE('',*,*,#53978,.F.);
#78771=ORIENTED_EDGE('',*,*,#53979,.T.);
#78772=ORIENTED_EDGE('',*,*,#53980,.F.);
#78773=ORIENTED_EDGE('',*,*,#53981,.F.);
#78774=ORIENTED_EDGE('',*,*,#53982,.F.);
#78775=ORIENTED_EDGE('',*,*,#53983,.T.);
#78776=ORIENTED_EDGE('',*,*,#53984,.F.);
#78777=ORIENTED_EDGE('',*,*,#53985,.F.);
#78778=ORIENTED_EDGE('',*,*,#53986,.F.);
#78779=ORIENTED_EDGE('',*,*,#53987,.T.);
#78780=ORIENTED_EDGE('',*,*,#53988,.F.);
#78781=ORIENTED_EDGE('',*,*,#53989,.F.);
#78782=ORIENTED_EDGE('',*,*,#53990,.F.);
#78783=ORIENTED_EDGE('',*,*,#53991,.T.);
#78784=ORIENTED_EDGE('',*,*,#53992,.F.);
#78785=ORIENTED_EDGE('',*,*,#53993,.F.);
#78786=ORIENTED_EDGE('',*,*,#53994,.F.);
#78787=ORIENTED_EDGE('',*,*,#53995,.T.);
#78788=ORIENTED_EDGE('',*,*,#53996,.F.);
#78789=ORIENTED_EDGE('',*,*,#53997,.F.);
#78790=ORIENTED_EDGE('',*,*,#53998,.F.);
#78791=ORIENTED_EDGE('',*,*,#53999,.T.);
#78792=ORIENTED_EDGE('',*,*,#54000,.F.);
#78793=ORIENTED_EDGE('',*,*,#54001,.F.);
#78794=ORIENTED_EDGE('',*,*,#54002,.F.);
#78795=ORIENTED_EDGE('',*,*,#54003,.T.);
#78796=ORIENTED_EDGE('',*,*,#54004,.F.);
#78797=ORIENTED_EDGE('',*,*,#54005,.F.);
#78798=ORIENTED_EDGE('',*,*,#54006,.F.);
#78799=ORIENTED_EDGE('',*,*,#54007,.T.);
#78800=ORIENTED_EDGE('',*,*,#54008,.F.);
#78801=ORIENTED_EDGE('',*,*,#54009,.F.);
#78802=ORIENTED_EDGE('',*,*,#54010,.F.);
#78803=ORIENTED_EDGE('',*,*,#54011,.T.);
#78804=ORIENTED_EDGE('',*,*,#54012,.F.);
#78805=ORIENTED_EDGE('',*,*,#54013,.F.);
#78806=ORIENTED_EDGE('',*,*,#54014,.F.);
#78807=ORIENTED_EDGE('',*,*,#54015,.T.);
#78808=ORIENTED_EDGE('',*,*,#54016,.F.);
#78809=ORIENTED_EDGE('',*,*,#54017,.F.);
#78810=ORIENTED_EDGE('',*,*,#54018,.F.);
#78811=ORIENTED_EDGE('',*,*,#54019,.T.);
#78812=ORIENTED_EDGE('',*,*,#54020,.F.);
#78813=ORIENTED_EDGE('',*,*,#54021,.F.);
#78814=ORIENTED_EDGE('',*,*,#54022,.F.);
#78815=ORIENTED_EDGE('',*,*,#54023,.T.);
#78816=ORIENTED_EDGE('',*,*,#54024,.F.);
#78817=ORIENTED_EDGE('',*,*,#54025,.F.);
#78818=ORIENTED_EDGE('',*,*,#54026,.F.);
#78819=ORIENTED_EDGE('',*,*,#54027,.T.);
#78820=ORIENTED_EDGE('',*,*,#54028,.F.);
#78821=ORIENTED_EDGE('',*,*,#54029,.F.);
#78822=ORIENTED_EDGE('',*,*,#54030,.F.);
#78823=ORIENTED_EDGE('',*,*,#54031,.T.);
#78824=ORIENTED_EDGE('',*,*,#54032,.F.);
#78825=ORIENTED_EDGE('',*,*,#54033,.F.);
#78826=ORIENTED_EDGE('',*,*,#54034,.F.);
#78827=ORIENTED_EDGE('',*,*,#54035,.T.);
#78828=ORIENTED_EDGE('',*,*,#54036,.F.);
#78829=ORIENTED_EDGE('',*,*,#54037,.F.);
#78830=ORIENTED_EDGE('',*,*,#54038,.F.);
#78831=ORIENTED_EDGE('',*,*,#54039,.T.);
#78832=ORIENTED_EDGE('',*,*,#54040,.F.);
#78833=ORIENTED_EDGE('',*,*,#54041,.F.);
#78834=ORIENTED_EDGE('',*,*,#54042,.F.);
#78835=ORIENTED_EDGE('',*,*,#54043,.T.);
#78836=ORIENTED_EDGE('',*,*,#54044,.F.);
#78837=ORIENTED_EDGE('',*,*,#54045,.F.);
#78838=ORIENTED_EDGE('',*,*,#54046,.F.);
#78839=ORIENTED_EDGE('',*,*,#54047,.T.);
#78840=ORIENTED_EDGE('',*,*,#54048,.F.);
#78841=ORIENTED_EDGE('',*,*,#54049,.F.);
#78842=ORIENTED_EDGE('',*,*,#54050,.F.);
#78843=ORIENTED_EDGE('',*,*,#54051,.T.);
#78844=ORIENTED_EDGE('',*,*,#54052,.F.);
#78845=ORIENTED_EDGE('',*,*,#54053,.F.);
#78846=ORIENTED_EDGE('',*,*,#54054,.F.);
#78847=ORIENTED_EDGE('',*,*,#54055,.T.);
#78848=ORIENTED_EDGE('',*,*,#54056,.F.);
#78849=ORIENTED_EDGE('',*,*,#54057,.F.);
#78850=ORIENTED_EDGE('',*,*,#54058,.F.);
#78851=ORIENTED_EDGE('',*,*,#54059,.T.);
#78852=ORIENTED_EDGE('',*,*,#54060,.F.);
#78853=ORIENTED_EDGE('',*,*,#54061,.F.);
#78854=ORIENTED_EDGE('',*,*,#54062,.F.);
#78855=ORIENTED_EDGE('',*,*,#54063,.T.);
#78856=ORIENTED_EDGE('',*,*,#54064,.F.);
#78857=ORIENTED_EDGE('',*,*,#54065,.F.);
#78858=ORIENTED_EDGE('',*,*,#54066,.F.);
#78859=ORIENTED_EDGE('',*,*,#54067,.T.);
#78860=ORIENTED_EDGE('',*,*,#54068,.F.);
#78861=ORIENTED_EDGE('',*,*,#54069,.F.);
#78862=ORIENTED_EDGE('',*,*,#54070,.F.);
#78863=ORIENTED_EDGE('',*,*,#54071,.T.);
#78864=ORIENTED_EDGE('',*,*,#54072,.F.);
#78865=ORIENTED_EDGE('',*,*,#54073,.F.);
#78866=ORIENTED_EDGE('',*,*,#54074,.F.);
#78867=ORIENTED_EDGE('',*,*,#54075,.T.);
#78868=ORIENTED_EDGE('',*,*,#54076,.F.);
#78869=ORIENTED_EDGE('',*,*,#54077,.F.);
#78870=ORIENTED_EDGE('',*,*,#54078,.F.);
#78871=ORIENTED_EDGE('',*,*,#54079,.T.);
#78872=ORIENTED_EDGE('',*,*,#54080,.F.);
#78873=ORIENTED_EDGE('',*,*,#54081,.F.);
#78874=ORIENTED_EDGE('',*,*,#54082,.F.);
#78875=ORIENTED_EDGE('',*,*,#54083,.T.);
#78876=ORIENTED_EDGE('',*,*,#54084,.F.);
#78877=ORIENTED_EDGE('',*,*,#54085,.F.);
#78878=ORIENTED_EDGE('',*,*,#54086,.F.);
#78879=ORIENTED_EDGE('',*,*,#54087,.T.);
#78880=ORIENTED_EDGE('',*,*,#54088,.F.);
#78881=ORIENTED_EDGE('',*,*,#54089,.F.);
#78882=ORIENTED_EDGE('',*,*,#54090,.F.);
#78883=ORIENTED_EDGE('',*,*,#54091,.T.);
#78884=ORIENTED_EDGE('',*,*,#54092,.F.);
#78885=ORIENTED_EDGE('',*,*,#54093,.F.);
#78886=ORIENTED_EDGE('',*,*,#54094,.F.);
#78887=ORIENTED_EDGE('',*,*,#54095,.T.);
#78888=ORIENTED_EDGE('',*,*,#54096,.F.);
#78889=ORIENTED_EDGE('',*,*,#54097,.F.);
#78890=ORIENTED_EDGE('',*,*,#54098,.F.);
#78891=ORIENTED_EDGE('',*,*,#54099,.T.);
#78892=ORIENTED_EDGE('',*,*,#54100,.F.);
#78893=ORIENTED_EDGE('',*,*,#54101,.F.);
#78894=ORIENTED_EDGE('',*,*,#54102,.F.);
#78895=ORIENTED_EDGE('',*,*,#54103,.T.);
#78896=ORIENTED_EDGE('',*,*,#54104,.F.);
#78897=ORIENTED_EDGE('',*,*,#54105,.F.);
#78898=ORIENTED_EDGE('',*,*,#54106,.F.);
#78899=ORIENTED_EDGE('',*,*,#54107,.T.);
#78900=ORIENTED_EDGE('',*,*,#54108,.F.);
#78901=ORIENTED_EDGE('',*,*,#54109,.F.);
#78902=ORIENTED_EDGE('',*,*,#54110,.F.);
#78903=ORIENTED_EDGE('',*,*,#54111,.T.);
#78904=ORIENTED_EDGE('',*,*,#54112,.F.);
#78905=ORIENTED_EDGE('',*,*,#54113,.F.);
#78906=ORIENTED_EDGE('',*,*,#54114,.F.);
#78907=ORIENTED_EDGE('',*,*,#54115,.T.);
#78908=ORIENTED_EDGE('',*,*,#54116,.F.);
#78909=ORIENTED_EDGE('',*,*,#54117,.F.);
#78910=ORIENTED_EDGE('',*,*,#54118,.F.);
#78911=ORIENTED_EDGE('',*,*,#54119,.T.);
#78912=ORIENTED_EDGE('',*,*,#54120,.F.);
#78913=ORIENTED_EDGE('',*,*,#54121,.F.);
#78914=ORIENTED_EDGE('',*,*,#54122,.F.);
#78915=ORIENTED_EDGE('',*,*,#54123,.T.);
#78916=ORIENTED_EDGE('',*,*,#54124,.F.);
#78917=ORIENTED_EDGE('',*,*,#54125,.F.);
#78918=ORIENTED_EDGE('',*,*,#54126,.F.);
#78919=ORIENTED_EDGE('',*,*,#54127,.T.);
#78920=ORIENTED_EDGE('',*,*,#54128,.F.);
#78921=ORIENTED_EDGE('',*,*,#54129,.F.);
#78922=ORIENTED_EDGE('',*,*,#54130,.F.);
#78923=ORIENTED_EDGE('',*,*,#54131,.T.);
#78924=ORIENTED_EDGE('',*,*,#54132,.F.);
#78925=ORIENTED_EDGE('',*,*,#54133,.F.);
#78926=ORIENTED_EDGE('',*,*,#54134,.F.);
#78927=ORIENTED_EDGE('',*,*,#54135,.T.);
#78928=ORIENTED_EDGE('',*,*,#54136,.F.);
#78929=ORIENTED_EDGE('',*,*,#54137,.F.);
#78930=ORIENTED_EDGE('',*,*,#54138,.F.);
#78931=ORIENTED_EDGE('',*,*,#54139,.T.);
#78932=ORIENTED_EDGE('',*,*,#54140,.F.);
#78933=ORIENTED_EDGE('',*,*,#54141,.F.);
#78934=ORIENTED_EDGE('',*,*,#54142,.F.);
#78935=ORIENTED_EDGE('',*,*,#54143,.T.);
#78936=ORIENTED_EDGE('',*,*,#54144,.F.);
#78937=ORIENTED_EDGE('',*,*,#54145,.F.);
#78938=ORIENTED_EDGE('',*,*,#54146,.F.);
#78939=ORIENTED_EDGE('',*,*,#54147,.T.);
#78940=ORIENTED_EDGE('',*,*,#54148,.F.);
#78941=ORIENTED_EDGE('',*,*,#54149,.F.);
#78942=ORIENTED_EDGE('',*,*,#54150,.F.);
#78943=ORIENTED_EDGE('',*,*,#54151,.T.);
#78944=ORIENTED_EDGE('',*,*,#54152,.F.);
#78945=ORIENTED_EDGE('',*,*,#54153,.F.);
#78946=ORIENTED_EDGE('',*,*,#54154,.F.);
#78947=ORIENTED_EDGE('',*,*,#54155,.T.);
#78948=ORIENTED_EDGE('',*,*,#54156,.F.);
#78949=ORIENTED_EDGE('',*,*,#54157,.F.);
#78950=ORIENTED_EDGE('',*,*,#54158,.F.);
#78951=ORIENTED_EDGE('',*,*,#54159,.T.);
#78952=ORIENTED_EDGE('',*,*,#54160,.F.);
#78953=ORIENTED_EDGE('',*,*,#54161,.F.);
#78954=ORIENTED_EDGE('',*,*,#54162,.F.);
#78955=ORIENTED_EDGE('',*,*,#54163,.T.);
#78956=ORIENTED_EDGE('',*,*,#54164,.F.);
#78957=ORIENTED_EDGE('',*,*,#54165,.F.);
#78958=ORIENTED_EDGE('',*,*,#54166,.F.);
#78959=ORIENTED_EDGE('',*,*,#54167,.T.);
#78960=ORIENTED_EDGE('',*,*,#54168,.F.);
#78961=ORIENTED_EDGE('',*,*,#54169,.F.);
#78962=ORIENTED_EDGE('',*,*,#54170,.F.);
#78963=ORIENTED_EDGE('',*,*,#54171,.T.);
#78964=ORIENTED_EDGE('',*,*,#54172,.F.);
#78965=ORIENTED_EDGE('',*,*,#54173,.F.);
#78966=ORIENTED_EDGE('',*,*,#54174,.F.);
#78967=ORIENTED_EDGE('',*,*,#54175,.T.);
#78968=ORIENTED_EDGE('',*,*,#54176,.F.);
#78969=ORIENTED_EDGE('',*,*,#54177,.F.);
#78970=ORIENTED_EDGE('',*,*,#54178,.F.);
#78971=ORIENTED_EDGE('',*,*,#54179,.T.);
#78972=ORIENTED_EDGE('',*,*,#54180,.F.);
#78973=ORIENTED_EDGE('',*,*,#54181,.F.);
#78974=ORIENTED_EDGE('',*,*,#54182,.F.);
#78975=ORIENTED_EDGE('',*,*,#54183,.T.);
#78976=ORIENTED_EDGE('',*,*,#54184,.F.);
#78977=ORIENTED_EDGE('',*,*,#54185,.F.);
#78978=ORIENTED_EDGE('',*,*,#54186,.F.);
#78979=ORIENTED_EDGE('',*,*,#54187,.T.);
#78980=ORIENTED_EDGE('',*,*,#54188,.F.);
#78981=ORIENTED_EDGE('',*,*,#54189,.F.);
#78982=ORIENTED_EDGE('',*,*,#54190,.F.);
#78983=ORIENTED_EDGE('',*,*,#54191,.T.);
#78984=ORIENTED_EDGE('',*,*,#54192,.F.);
#78985=ORIENTED_EDGE('',*,*,#54193,.F.);
#78986=ORIENTED_EDGE('',*,*,#54194,.F.);
#78987=ORIENTED_EDGE('',*,*,#54195,.T.);
#78988=ORIENTED_EDGE('',*,*,#54196,.F.);
#78989=ORIENTED_EDGE('',*,*,#54197,.F.);
#78990=ORIENTED_EDGE('',*,*,#54198,.F.);
#78991=ORIENTED_EDGE('',*,*,#54199,.T.);
#78992=ORIENTED_EDGE('',*,*,#54200,.F.);
#78993=ORIENTED_EDGE('',*,*,#54201,.F.);
#78994=ORIENTED_EDGE('',*,*,#54202,.F.);
#78995=ORIENTED_EDGE('',*,*,#54203,.T.);
#78996=ORIENTED_EDGE('',*,*,#54204,.F.);
#78997=ORIENTED_EDGE('',*,*,#54205,.F.);
#78998=ORIENTED_EDGE('',*,*,#54206,.F.);
#78999=ORIENTED_EDGE('',*,*,#54207,.T.);
#79000=ORIENTED_EDGE('',*,*,#54208,.F.);
#79001=ORIENTED_EDGE('',*,*,#54209,.F.);
#79002=ORIENTED_EDGE('',*,*,#54210,.F.);
#79003=ORIENTED_EDGE('',*,*,#54211,.T.);
#79004=ORIENTED_EDGE('',*,*,#54212,.F.);
#79005=ORIENTED_EDGE('',*,*,#54213,.F.);
#79006=ORIENTED_EDGE('',*,*,#54214,.F.);
#79007=ORIENTED_EDGE('',*,*,#54215,.T.);
#79008=ORIENTED_EDGE('',*,*,#54216,.F.);
#79009=ORIENTED_EDGE('',*,*,#54217,.F.);
#79010=ORIENTED_EDGE('',*,*,#54218,.F.);
#79011=ORIENTED_EDGE('',*,*,#54219,.T.);
#79012=ORIENTED_EDGE('',*,*,#54220,.F.);
#79013=ORIENTED_EDGE('',*,*,#54221,.F.);
#79014=ORIENTED_EDGE('',*,*,#54222,.F.);
#79015=ORIENTED_EDGE('',*,*,#54223,.T.);
#79016=ORIENTED_EDGE('',*,*,#54224,.F.);
#79017=ORIENTED_EDGE('',*,*,#54225,.F.);
#79018=ORIENTED_EDGE('',*,*,#54226,.F.);
#79019=ORIENTED_EDGE('',*,*,#54227,.T.);
#79020=ORIENTED_EDGE('',*,*,#54228,.F.);
#79021=ORIENTED_EDGE('',*,*,#54229,.F.);
#79022=ORIENTED_EDGE('',*,*,#54230,.F.);
#79023=ORIENTED_EDGE('',*,*,#54231,.T.);
#79024=ORIENTED_EDGE('',*,*,#54232,.F.);
#79025=ORIENTED_EDGE('',*,*,#54233,.F.);
#79026=ORIENTED_EDGE('',*,*,#54234,.F.);
#79027=ORIENTED_EDGE('',*,*,#54235,.T.);
#79028=ORIENTED_EDGE('',*,*,#54236,.F.);
#79029=ORIENTED_EDGE('',*,*,#54237,.F.);
#79030=ORIENTED_EDGE('',*,*,#54238,.F.);
#79031=ORIENTED_EDGE('',*,*,#54239,.T.);
#79032=ORIENTED_EDGE('',*,*,#54240,.F.);
#79033=ORIENTED_EDGE('',*,*,#54241,.F.);
#79034=ORIENTED_EDGE('',*,*,#54242,.F.);
#79035=ORIENTED_EDGE('',*,*,#54243,.T.);
#79036=ORIENTED_EDGE('',*,*,#54244,.F.);
#79037=ORIENTED_EDGE('',*,*,#54245,.F.);
#79038=ORIENTED_EDGE('',*,*,#54246,.F.);
#79039=ORIENTED_EDGE('',*,*,#54247,.T.);
#79040=ORIENTED_EDGE('',*,*,#54248,.F.);
#79041=ORIENTED_EDGE('',*,*,#54249,.F.);
#79042=ORIENTED_EDGE('',*,*,#54250,.F.);
#79043=ORIENTED_EDGE('',*,*,#54251,.T.);
#79044=ORIENTED_EDGE('',*,*,#54252,.F.);
#79045=ORIENTED_EDGE('',*,*,#54253,.F.);
#79046=ORIENTED_EDGE('',*,*,#54254,.F.);
#79047=ORIENTED_EDGE('',*,*,#54255,.T.);
#79048=ORIENTED_EDGE('',*,*,#54256,.F.);
#79049=ORIENTED_EDGE('',*,*,#54257,.F.);
#79050=ORIENTED_EDGE('',*,*,#54258,.F.);
#79051=ORIENTED_EDGE('',*,*,#54259,.F.);
#79052=ORIENTED_EDGE('',*,*,#54260,.T.);
#79053=ORIENTED_EDGE('',*,*,#53950,.F.);
#79054=ORIENTED_EDGE('',*,*,#54261,.F.);
#79055=ORIENTED_EDGE('',*,*,#53943,.T.);
#79056=ORIENTED_EDGE('',*,*,#54262,.F.);
#79057=ORIENTED_EDGE('',*,*,#53839,.T.);
#79058=ORIENTED_EDGE('',*,*,#54263,.T.);
#79059=ORIENTED_EDGE('',*,*,#54264,.F.);
#79060=ORIENTED_EDGE('',*,*,#53844,.F.);
#79061=ORIENTED_EDGE('',*,*,#54265,.F.);
#79062=ORIENTED_EDGE('',*,*,#54266,.T.);
#79063=ORIENTED_EDGE('',*,*,#54267,.T.);
#79064=ORIENTED_EDGE('',*,*,#53946,.F.);
#79065=ORIENTED_EDGE('',*,*,#54267,.F.);
#79066=ORIENTED_EDGE('',*,*,#53835,.T.);
#79067=ORIENTED_EDGE('',*,*,#54268,.T.);
#79068=ORIENTED_EDGE('',*,*,#53948,.T.);
#79069=ORIENTED_EDGE('',*,*,#54269,.T.);
#79070=ORIENTED_EDGE('',*,*,#54270,.F.);
#79071=ORIENTED_EDGE('',*,*,#54271,.F.);
#79072=ORIENTED_EDGE('',*,*,#54272,.F.);
#79073=ORIENTED_EDGE('',*,*,#54273,.T.);
#79074=ORIENTED_EDGE('',*,*,#54274,.F.);
#79075=ORIENTED_EDGE('',*,*,#54275,.F.);
#79076=ORIENTED_EDGE('',*,*,#54269,.F.);
#79077=ORIENTED_EDGE('',*,*,#54276,.T.);
#79078=ORIENTED_EDGE('',*,*,#54277,.T.);
#79079=ORIENTED_EDGE('',*,*,#54278,.F.);
#79080=ORIENTED_EDGE('',*,*,#54279,.T.);
#79081=ORIENTED_EDGE('',*,*,#54280,.T.);
#79082=ORIENTED_EDGE('',*,*,#54279,.F.);
#79083=ORIENTED_EDGE('',*,*,#54281,.F.);
#79084=ORIENTED_EDGE('',*,*,#54282,.T.);
#79085=ORIENTED_EDGE('',*,*,#54278,.T.);
#79086=ORIENTED_EDGE('',*,*,#54282,.F.);
#79087=ORIENTED_EDGE('',*,*,#54283,.F.);
#79088=ORIENTED_EDGE('',*,*,#54284,.T.);
#79089=ORIENTED_EDGE('',*,*,#54281,.T.);
#79090=ORIENTED_EDGE('',*,*,#54284,.F.);
#79091=ORIENTED_EDGE('',*,*,#54285,.T.);
#79092=ORIENTED_EDGE('',*,*,#54286,.T.);
#79093=ORIENTED_EDGE('',*,*,#54287,.T.);
#79094=ORIENTED_EDGE('',*,*,#54288,.T.);
#79095=ORIENTED_EDGE('',*,*,#54289,.T.);
#79096=ORIENTED_EDGE('',*,*,#54290,.T.);
#79097=ORIENTED_EDGE('',*,*,#54291,.T.);
#79098=ORIENTED_EDGE('',*,*,#54292,.T.);
#79099=ORIENTED_EDGE('',*,*,#54293,.T.);
#79100=ORIENTED_EDGE('',*,*,#54294,.T.);
#79101=ORIENTED_EDGE('',*,*,#54295,.T.);
#79102=ORIENTED_EDGE('',*,*,#54296,.T.);
#79103=ORIENTED_EDGE('',*,*,#54297,.T.);
#79104=ORIENTED_EDGE('',*,*,#54298,.T.);
#79105=ORIENTED_EDGE('',*,*,#54299,.T.);
#79106=ORIENTED_EDGE('',*,*,#54300,.T.);
#79107=ORIENTED_EDGE('',*,*,#54301,.T.);
#79108=ORIENTED_EDGE('',*,*,#54302,.T.);
#79109=ORIENTED_EDGE('',*,*,#54303,.T.);
#79110=ORIENTED_EDGE('',*,*,#54304,.T.);
#79111=ORIENTED_EDGE('',*,*,#54305,.T.);
#79112=ORIENTED_EDGE('',*,*,#54306,.T.);
#79113=ORIENTED_EDGE('',*,*,#54307,.T.);
#79114=ORIENTED_EDGE('',*,*,#54308,.T.);
#79115=ORIENTED_EDGE('',*,*,#54309,.T.);
#79116=ORIENTED_EDGE('',*,*,#54310,.T.);
#79117=ORIENTED_EDGE('',*,*,#54311,.T.);
#79118=ORIENTED_EDGE('',*,*,#54312,.T.);
#79119=ORIENTED_EDGE('',*,*,#54313,.T.);
#79120=ORIENTED_EDGE('',*,*,#54314,.T.);
#79121=ORIENTED_EDGE('',*,*,#54315,.T.);
#79122=ORIENTED_EDGE('',*,*,#54316,.T.);
#79123=ORIENTED_EDGE('',*,*,#54317,.T.);
#79124=ORIENTED_EDGE('',*,*,#54318,.T.);
#79125=ORIENTED_EDGE('',*,*,#54319,.T.);
#79126=ORIENTED_EDGE('',*,*,#54320,.T.);
#79127=ORIENTED_EDGE('',*,*,#54321,.T.);
#79128=ORIENTED_EDGE('',*,*,#54322,.T.);
#79129=ORIENTED_EDGE('',*,*,#54323,.T.);
#79130=ORIENTED_EDGE('',*,*,#54324,.T.);
#79131=ORIENTED_EDGE('',*,*,#54325,.T.);
#79132=ORIENTED_EDGE('',*,*,#54326,.T.);
#79133=ORIENTED_EDGE('',*,*,#54327,.T.);
#79134=ORIENTED_EDGE('',*,*,#54328,.T.);
#79135=ORIENTED_EDGE('',*,*,#54329,.T.);
#79136=ORIENTED_EDGE('',*,*,#54330,.T.);
#79137=ORIENTED_EDGE('',*,*,#54331,.T.);
#79138=ORIENTED_EDGE('',*,*,#54332,.T.);
#79139=ORIENTED_EDGE('',*,*,#54333,.T.);
#79140=ORIENTED_EDGE('',*,*,#54334,.T.);
#79141=ORIENTED_EDGE('',*,*,#54335,.T.);
#79142=ORIENTED_EDGE('',*,*,#54336,.T.);
#79143=ORIENTED_EDGE('',*,*,#54337,.T.);
#79144=ORIENTED_EDGE('',*,*,#54338,.T.);
#79145=ORIENTED_EDGE('',*,*,#54339,.T.);
#79146=ORIENTED_EDGE('',*,*,#54340,.T.);
#79147=ORIENTED_EDGE('',*,*,#54341,.T.);
#79148=ORIENTED_EDGE('',*,*,#54342,.T.);
#79149=ORIENTED_EDGE('',*,*,#54343,.T.);
#79150=ORIENTED_EDGE('',*,*,#54344,.T.);
#79151=ORIENTED_EDGE('',*,*,#54345,.T.);
#79152=ORIENTED_EDGE('',*,*,#54346,.T.);
#79153=ORIENTED_EDGE('',*,*,#54347,.T.);
#79154=ORIENTED_EDGE('',*,*,#54348,.T.);
#79155=ORIENTED_EDGE('',*,*,#54349,.T.);
#79156=ORIENTED_EDGE('',*,*,#54350,.T.);
#79157=ORIENTED_EDGE('',*,*,#54351,.T.);
#79158=ORIENTED_EDGE('',*,*,#54352,.T.);
#79159=ORIENTED_EDGE('',*,*,#54353,.T.);
#79160=ORIENTED_EDGE('',*,*,#54354,.T.);
#79161=ORIENTED_EDGE('',*,*,#54355,.T.);
#79162=ORIENTED_EDGE('',*,*,#54356,.T.);
#79163=ORIENTED_EDGE('',*,*,#54357,.T.);
#79164=ORIENTED_EDGE('',*,*,#54358,.T.);
#79165=ORIENTED_EDGE('',*,*,#54359,.T.);
#79166=ORIENTED_EDGE('',*,*,#54360,.T.);
#79167=ORIENTED_EDGE('',*,*,#54361,.T.);
#79168=ORIENTED_EDGE('',*,*,#54362,.T.);
#79169=ORIENTED_EDGE('',*,*,#54363,.T.);
#79170=ORIENTED_EDGE('',*,*,#54364,.T.);
#79171=ORIENTED_EDGE('',*,*,#54365,.T.);
#79172=ORIENTED_EDGE('',*,*,#54366,.T.);
#79173=ORIENTED_EDGE('',*,*,#54367,.T.);
#79174=ORIENTED_EDGE('',*,*,#54368,.T.);
#79175=ORIENTED_EDGE('',*,*,#54369,.T.);
#79176=ORIENTED_EDGE('',*,*,#54370,.T.);
#79177=ORIENTED_EDGE('',*,*,#54371,.T.);
#79178=ORIENTED_EDGE('',*,*,#54372,.T.);
#79179=ORIENTED_EDGE('',*,*,#54373,.T.);
#79180=ORIENTED_EDGE('',*,*,#54374,.T.);
#79181=ORIENTED_EDGE('',*,*,#54375,.T.);
#79182=ORIENTED_EDGE('',*,*,#54376,.T.);
#79183=ORIENTED_EDGE('',*,*,#54377,.T.);
#79184=ORIENTED_EDGE('',*,*,#54378,.T.);
#79185=ORIENTED_EDGE('',*,*,#54379,.T.);
#79186=ORIENTED_EDGE('',*,*,#54380,.T.);
#79187=ORIENTED_EDGE('',*,*,#54381,.T.);
#79188=ORIENTED_EDGE('',*,*,#54382,.T.);
#79189=ORIENTED_EDGE('',*,*,#54383,.T.);
#79190=ORIENTED_EDGE('',*,*,#54384,.T.);
#79191=ORIENTED_EDGE('',*,*,#54385,.T.);
#79192=ORIENTED_EDGE('',*,*,#54386,.T.);
#79193=ORIENTED_EDGE('',*,*,#54387,.T.);
#79194=ORIENTED_EDGE('',*,*,#54388,.T.);
#79195=ORIENTED_EDGE('',*,*,#54389,.T.);
#79196=ORIENTED_EDGE('',*,*,#54390,.T.);
#79197=ORIENTED_EDGE('',*,*,#54391,.T.);
#79198=ORIENTED_EDGE('',*,*,#54392,.T.);
#79199=ORIENTED_EDGE('',*,*,#54393,.T.);
#79200=ORIENTED_EDGE('',*,*,#54394,.T.);
#79201=ORIENTED_EDGE('',*,*,#54395,.T.);
#79202=ORIENTED_EDGE('',*,*,#54396,.T.);
#79203=ORIENTED_EDGE('',*,*,#54397,.T.);
#79204=ORIENTED_EDGE('',*,*,#54398,.T.);
#79205=ORIENTED_EDGE('',*,*,#54399,.T.);
#79206=ORIENTED_EDGE('',*,*,#54400,.T.);
#79207=ORIENTED_EDGE('',*,*,#54401,.T.);
#79208=ORIENTED_EDGE('',*,*,#54402,.T.);
#79209=ORIENTED_EDGE('',*,*,#54403,.T.);
#79210=ORIENTED_EDGE('',*,*,#54404,.T.);
#79211=ORIENTED_EDGE('',*,*,#54405,.T.);
#79212=ORIENTED_EDGE('',*,*,#54406,.T.);
#79213=ORIENTED_EDGE('',*,*,#54407,.T.);
#79214=ORIENTED_EDGE('',*,*,#54408,.T.);
#79215=ORIENTED_EDGE('',*,*,#54409,.T.);
#79216=ORIENTED_EDGE('',*,*,#54410,.T.);
#79217=ORIENTED_EDGE('',*,*,#54411,.T.);
#79218=ORIENTED_EDGE('',*,*,#54412,.T.);
#79219=ORIENTED_EDGE('',*,*,#54413,.T.);
#79220=ORIENTED_EDGE('',*,*,#54414,.T.);
#79221=ORIENTED_EDGE('',*,*,#54415,.T.);
#79222=ORIENTED_EDGE('',*,*,#54416,.T.);
#79223=ORIENTED_EDGE('',*,*,#54417,.T.);
#79224=ORIENTED_EDGE('',*,*,#54418,.T.);
#79225=ORIENTED_EDGE('',*,*,#54419,.T.);
#79226=ORIENTED_EDGE('',*,*,#54420,.T.);
#79227=ORIENTED_EDGE('',*,*,#54421,.T.);
#79228=ORIENTED_EDGE('',*,*,#54422,.T.);
#79229=ORIENTED_EDGE('',*,*,#54423,.T.);
#79230=ORIENTED_EDGE('',*,*,#54424,.T.);
#79231=ORIENTED_EDGE('',*,*,#54425,.T.);
#79232=ORIENTED_EDGE('',*,*,#54426,.T.);
#79233=ORIENTED_EDGE('',*,*,#54427,.T.);
#79234=ORIENTED_EDGE('',*,*,#54428,.T.);
#79235=ORIENTED_EDGE('',*,*,#54429,.T.);
#79236=ORIENTED_EDGE('',*,*,#54430,.T.);
#79237=ORIENTED_EDGE('',*,*,#54431,.T.);
#79238=ORIENTED_EDGE('',*,*,#54432,.T.);
#79239=ORIENTED_EDGE('',*,*,#54433,.T.);
#79240=ORIENTED_EDGE('',*,*,#54434,.T.);
#79241=ORIENTED_EDGE('',*,*,#54435,.T.);
#79242=ORIENTED_EDGE('',*,*,#54436,.T.);
#79243=ORIENTED_EDGE('',*,*,#54437,.T.);
#79244=ORIENTED_EDGE('',*,*,#54438,.T.);
#79245=ORIENTED_EDGE('',*,*,#54439,.T.);
#79246=ORIENTED_EDGE('',*,*,#54440,.T.);
#79247=ORIENTED_EDGE('',*,*,#54441,.F.);
#79248=ORIENTED_EDGE('',*,*,#54442,.F.);
#79249=ORIENTED_EDGE('',*,*,#54440,.F.);
#79250=ORIENTED_EDGE('',*,*,#54443,.T.);
#79251=ORIENTED_EDGE('',*,*,#54444,.T.);
#79252=ORIENTED_EDGE('',*,*,#54445,.T.);
#79253=ORIENTED_EDGE('',*,*,#54446,.T.);
#79254=ORIENTED_EDGE('',*,*,#54447,.T.);
#79255=ORIENTED_EDGE('',*,*,#54448,.T.);
#79256=ORIENTED_EDGE('',*,*,#54449,.T.);
#79257=ORIENTED_EDGE('',*,*,#54450,.T.);
#79258=ORIENTED_EDGE('',*,*,#54451,.T.);
#79259=ORIENTED_EDGE('',*,*,#54452,.T.);
#79260=ORIENTED_EDGE('',*,*,#54453,.T.);
#79261=ORIENTED_EDGE('',*,*,#54454,.T.);
#79262=ORIENTED_EDGE('',*,*,#54455,.T.);
#79263=ORIENTED_EDGE('',*,*,#54456,.T.);
#79264=ORIENTED_EDGE('',*,*,#54457,.T.);
#79265=ORIENTED_EDGE('',*,*,#54458,.T.);
#79266=ORIENTED_EDGE('',*,*,#54459,.T.);
#79267=ORIENTED_EDGE('',*,*,#54460,.T.);
#79268=ORIENTED_EDGE('',*,*,#54461,.T.);
#79269=ORIENTED_EDGE('',*,*,#54462,.T.);
#79270=ORIENTED_EDGE('',*,*,#54463,.T.);
#79271=ORIENTED_EDGE('',*,*,#54464,.T.);
#79272=ORIENTED_EDGE('',*,*,#54465,.T.);
#79273=ORIENTED_EDGE('',*,*,#54466,.T.);
#79274=ORIENTED_EDGE('',*,*,#54467,.T.);
#79275=ORIENTED_EDGE('',*,*,#54468,.T.);
#79276=ORIENTED_EDGE('',*,*,#54469,.T.);
#79277=ORIENTED_EDGE('',*,*,#54470,.T.);
#79278=ORIENTED_EDGE('',*,*,#54471,.T.);
#79279=ORIENTED_EDGE('',*,*,#54472,.T.);
#79280=ORIENTED_EDGE('',*,*,#54473,.T.);
#79281=ORIENTED_EDGE('',*,*,#54474,.T.);
#79282=ORIENTED_EDGE('',*,*,#54475,.T.);
#79283=ORIENTED_EDGE('',*,*,#54476,.T.);
#79284=ORIENTED_EDGE('',*,*,#54477,.T.);
#79285=ORIENTED_EDGE('',*,*,#54478,.T.);
#79286=ORIENTED_EDGE('',*,*,#54479,.T.);
#79287=ORIENTED_EDGE('',*,*,#54480,.T.);
#79288=ORIENTED_EDGE('',*,*,#54481,.T.);
#79289=ORIENTED_EDGE('',*,*,#54482,.T.);
#79290=ORIENTED_EDGE('',*,*,#54483,.T.);
#79291=ORIENTED_EDGE('',*,*,#54484,.T.);
#79292=ORIENTED_EDGE('',*,*,#54485,.T.);
#79293=ORIENTED_EDGE('',*,*,#54486,.T.);
#79294=ORIENTED_EDGE('',*,*,#54487,.T.);
#79295=ORIENTED_EDGE('',*,*,#54488,.T.);
#79296=ORIENTED_EDGE('',*,*,#54489,.T.);
#79297=ORIENTED_EDGE('',*,*,#54490,.T.);
#79298=ORIENTED_EDGE('',*,*,#54491,.T.);
#79299=ORIENTED_EDGE('',*,*,#54492,.T.);
#79300=ORIENTED_EDGE('',*,*,#54493,.T.);
#79301=ORIENTED_EDGE('',*,*,#54494,.T.);
#79302=ORIENTED_EDGE('',*,*,#54495,.T.);
#79303=ORIENTED_EDGE('',*,*,#54496,.T.);
#79304=ORIENTED_EDGE('',*,*,#54497,.T.);
#79305=ORIENTED_EDGE('',*,*,#54498,.T.);
#79306=ORIENTED_EDGE('',*,*,#54499,.T.);
#79307=ORIENTED_EDGE('',*,*,#54500,.T.);
#79308=ORIENTED_EDGE('',*,*,#54501,.T.);
#79309=ORIENTED_EDGE('',*,*,#54502,.T.);
#79310=ORIENTED_EDGE('',*,*,#54503,.T.);
#79311=ORIENTED_EDGE('',*,*,#54504,.T.);
#79312=ORIENTED_EDGE('',*,*,#54505,.T.);
#79313=ORIENTED_EDGE('',*,*,#54506,.T.);
#79314=ORIENTED_EDGE('',*,*,#54507,.T.);
#79315=ORIENTED_EDGE('',*,*,#54508,.T.);
#79316=ORIENTED_EDGE('',*,*,#54509,.T.);
#79317=ORIENTED_EDGE('',*,*,#54510,.T.);
#79318=ORIENTED_EDGE('',*,*,#54511,.T.);
#79319=ORIENTED_EDGE('',*,*,#54512,.T.);
#79320=ORIENTED_EDGE('',*,*,#54513,.T.);
#79321=ORIENTED_EDGE('',*,*,#54514,.T.);
#79322=ORIENTED_EDGE('',*,*,#54515,.T.);
#79323=ORIENTED_EDGE('',*,*,#54516,.T.);
#79324=ORIENTED_EDGE('',*,*,#54517,.T.);
#79325=ORIENTED_EDGE('',*,*,#54518,.T.);
#79326=ORIENTED_EDGE('',*,*,#54519,.T.);
#79327=ORIENTED_EDGE('',*,*,#54520,.T.);
#79328=ORIENTED_EDGE('',*,*,#54521,.T.);
#79329=ORIENTED_EDGE('',*,*,#54522,.T.);
#79330=ORIENTED_EDGE('',*,*,#54523,.T.);
#79331=ORIENTED_EDGE('',*,*,#54524,.T.);
#79332=ORIENTED_EDGE('',*,*,#54525,.T.);
#79333=ORIENTED_EDGE('',*,*,#54526,.T.);
#79334=ORIENTED_EDGE('',*,*,#54527,.T.);
#79335=ORIENTED_EDGE('',*,*,#54528,.T.);
#79336=ORIENTED_EDGE('',*,*,#54529,.T.);
#79337=ORIENTED_EDGE('',*,*,#54530,.T.);
#79338=ORIENTED_EDGE('',*,*,#54531,.T.);
#79339=ORIENTED_EDGE('',*,*,#54532,.T.);
#79340=ORIENTED_EDGE('',*,*,#54533,.T.);
#79341=ORIENTED_EDGE('',*,*,#54534,.T.);
#79342=ORIENTED_EDGE('',*,*,#54535,.T.);
#79343=ORIENTED_EDGE('',*,*,#54536,.T.);
#79344=ORIENTED_EDGE('',*,*,#54537,.T.);
#79345=ORIENTED_EDGE('',*,*,#54538,.T.);
#79346=ORIENTED_EDGE('',*,*,#54539,.T.);
#79347=ORIENTED_EDGE('',*,*,#54540,.T.);
#79348=ORIENTED_EDGE('',*,*,#54541,.T.);
#79349=ORIENTED_EDGE('',*,*,#54542,.T.);
#79350=ORIENTED_EDGE('',*,*,#54543,.T.);
#79351=ORIENTED_EDGE('',*,*,#54544,.T.);
#79352=ORIENTED_EDGE('',*,*,#54545,.T.);
#79353=ORIENTED_EDGE('',*,*,#54546,.T.);
#79354=ORIENTED_EDGE('',*,*,#54547,.T.);
#79355=ORIENTED_EDGE('',*,*,#54548,.T.);
#79356=ORIENTED_EDGE('',*,*,#54549,.T.);
#79357=ORIENTED_EDGE('',*,*,#54550,.T.);
#79358=ORIENTED_EDGE('',*,*,#54551,.T.);
#79359=ORIENTED_EDGE('',*,*,#54552,.T.);
#79360=ORIENTED_EDGE('',*,*,#54553,.T.);
#79361=ORIENTED_EDGE('',*,*,#54554,.T.);
#79362=ORIENTED_EDGE('',*,*,#54555,.T.);
#79363=ORIENTED_EDGE('',*,*,#54556,.T.);
#79364=ORIENTED_EDGE('',*,*,#54557,.T.);
#79365=ORIENTED_EDGE('',*,*,#54558,.T.);
#79366=ORIENTED_EDGE('',*,*,#54559,.T.);
#79367=ORIENTED_EDGE('',*,*,#54560,.T.);
#79368=ORIENTED_EDGE('',*,*,#54561,.T.);
#79369=ORIENTED_EDGE('',*,*,#54562,.T.);
#79370=ORIENTED_EDGE('',*,*,#54563,.T.);
#79371=ORIENTED_EDGE('',*,*,#54564,.T.);
#79372=ORIENTED_EDGE('',*,*,#54565,.T.);
#79373=ORIENTED_EDGE('',*,*,#54566,.T.);
#79374=ORIENTED_EDGE('',*,*,#54567,.T.);
#79375=ORIENTED_EDGE('',*,*,#54568,.T.);
#79376=ORIENTED_EDGE('',*,*,#54569,.T.);
#79377=ORIENTED_EDGE('',*,*,#54570,.T.);
#79378=ORIENTED_EDGE('',*,*,#54571,.T.);
#79379=ORIENTED_EDGE('',*,*,#54572,.T.);
#79380=ORIENTED_EDGE('',*,*,#54573,.T.);
#79381=ORIENTED_EDGE('',*,*,#54574,.T.);
#79382=ORIENTED_EDGE('',*,*,#54575,.T.);
#79383=ORIENTED_EDGE('',*,*,#54576,.T.);
#79384=ORIENTED_EDGE('',*,*,#54577,.T.);
#79385=ORIENTED_EDGE('',*,*,#54578,.T.);
#79386=ORIENTED_EDGE('',*,*,#54579,.T.);
#79387=ORIENTED_EDGE('',*,*,#54580,.T.);
#79388=ORIENTED_EDGE('',*,*,#54581,.T.);
#79389=ORIENTED_EDGE('',*,*,#54582,.T.);
#79390=ORIENTED_EDGE('',*,*,#54583,.T.);
#79391=ORIENTED_EDGE('',*,*,#54584,.T.);
#79392=ORIENTED_EDGE('',*,*,#54585,.T.);
#79393=ORIENTED_EDGE('',*,*,#54586,.T.);
#79394=ORIENTED_EDGE('',*,*,#54587,.T.);
#79395=ORIENTED_EDGE('',*,*,#54588,.T.);
#79396=ORIENTED_EDGE('',*,*,#54589,.T.);
#79397=ORIENTED_EDGE('',*,*,#54590,.T.);
#79398=ORIENTED_EDGE('',*,*,#54591,.T.);
#79399=ORIENTED_EDGE('',*,*,#54592,.T.);
#79400=ORIENTED_EDGE('',*,*,#54593,.T.);
#79401=ORIENTED_EDGE('',*,*,#54594,.T.);
#79402=ORIENTED_EDGE('',*,*,#54595,.T.);
#79403=ORIENTED_EDGE('',*,*,#54596,.T.);
#79404=ORIENTED_EDGE('',*,*,#54597,.T.);
#79405=ORIENTED_EDGE('',*,*,#54598,.F.);
#79406=ORIENTED_EDGE('',*,*,#54599,.T.);
#79407=ORIENTED_EDGE('',*,*,#54441,.T.);
#79408=ORIENTED_EDGE('',*,*,#54442,.T.);
#79409=ORIENTED_EDGE('',*,*,#54599,.F.);
#79410=ORIENTED_EDGE('',*,*,#54600,.F.);
#79411=ORIENTED_EDGE('',*,*,#54601,.T.);
#79412=ORIENTED_EDGE('',*,*,#54602,.F.);
#79413=ORIENTED_EDGE('',*,*,#54062,.T.);
#79414=ORIENTED_EDGE('',*,*,#54603,.F.);
#79415=ORIENTED_EDGE('',*,*,#54604,.T.);
#79416=ORIENTED_EDGE('',*,*,#54605,.F.);
#79417=ORIENTED_EDGE('',*,*,#54606,.T.);
#79418=ORIENTED_EDGE('',*,*,#54607,.F.);
#79419=ORIENTED_EDGE('',*,*,#54066,.T.);
#79420=ORIENTED_EDGE('',*,*,#54608,.F.);
#79421=ORIENTED_EDGE('',*,*,#54609,.T.);
#79422=ORIENTED_EDGE('',*,*,#54610,.F.);
#79423=ORIENTED_EDGE('',*,*,#54611,.T.);
#79424=ORIENTED_EDGE('',*,*,#54612,.F.);
#79425=ORIENTED_EDGE('',*,*,#54070,.T.);
#79426=ORIENTED_EDGE('',*,*,#54613,.F.);
#79427=ORIENTED_EDGE('',*,*,#54614,.T.);
#79428=ORIENTED_EDGE('',*,*,#54615,.F.);
#79429=ORIENTED_EDGE('',*,*,#54616,.T.);
#79430=ORIENTED_EDGE('',*,*,#54617,.F.);
#79431=ORIENTED_EDGE('',*,*,#54074,.T.);
#79432=ORIENTED_EDGE('',*,*,#54618,.F.);
#79433=ORIENTED_EDGE('',*,*,#54619,.T.);
#79434=ORIENTED_EDGE('',*,*,#54620,.F.);
#79435=ORIENTED_EDGE('',*,*,#54621,.T.);
#79436=ORIENTED_EDGE('',*,*,#54622,.F.);
#79437=ORIENTED_EDGE('',*,*,#54078,.T.);
#79438=ORIENTED_EDGE('',*,*,#54623,.F.);
#79439=ORIENTED_EDGE('',*,*,#54624,.T.);
#79440=ORIENTED_EDGE('',*,*,#54625,.F.);
#79441=ORIENTED_EDGE('',*,*,#54626,.T.);
#79442=ORIENTED_EDGE('',*,*,#54627,.F.);
#79443=ORIENTED_EDGE('',*,*,#54082,.T.);
#79444=ORIENTED_EDGE('',*,*,#54628,.F.);
#79445=ORIENTED_EDGE('',*,*,#54629,.T.);
#79446=ORIENTED_EDGE('',*,*,#54630,.F.);
#79447=ORIENTED_EDGE('',*,*,#54631,.T.);
#79448=ORIENTED_EDGE('',*,*,#54632,.F.);
#79449=ORIENTED_EDGE('',*,*,#54086,.T.);
#79450=ORIENTED_EDGE('',*,*,#54633,.F.);
#79451=ORIENTED_EDGE('',*,*,#54634,.T.);
#79452=ORIENTED_EDGE('',*,*,#54635,.F.);
#79453=ORIENTED_EDGE('',*,*,#54636,.T.);
#79454=ORIENTED_EDGE('',*,*,#54637,.F.);
#79455=ORIENTED_EDGE('',*,*,#54090,.T.);
#79456=ORIENTED_EDGE('',*,*,#54638,.F.);
#79457=ORIENTED_EDGE('',*,*,#54639,.T.);
#79458=ORIENTED_EDGE('',*,*,#54640,.F.);
#79459=ORIENTED_EDGE('',*,*,#54641,.T.);
#79460=ORIENTED_EDGE('',*,*,#54642,.F.);
#79461=ORIENTED_EDGE('',*,*,#54094,.T.);
#79462=ORIENTED_EDGE('',*,*,#54643,.F.);
#79463=ORIENTED_EDGE('',*,*,#54644,.T.);
#79464=ORIENTED_EDGE('',*,*,#54645,.F.);
#79465=ORIENTED_EDGE('',*,*,#54646,.T.);
#79466=ORIENTED_EDGE('',*,*,#54647,.F.);
#79467=ORIENTED_EDGE('',*,*,#54098,.T.);
#79468=ORIENTED_EDGE('',*,*,#54648,.F.);
#79469=ORIENTED_EDGE('',*,*,#54649,.T.);
#79470=ORIENTED_EDGE('',*,*,#54650,.F.);
#79471=ORIENTED_EDGE('',*,*,#54651,.T.);
#79472=ORIENTED_EDGE('',*,*,#54652,.F.);
#79473=ORIENTED_EDGE('',*,*,#54102,.T.);
#79474=ORIENTED_EDGE('',*,*,#54653,.F.);
#79475=ORIENTED_EDGE('',*,*,#54654,.T.);
#79476=ORIENTED_EDGE('',*,*,#54655,.F.);
#79477=ORIENTED_EDGE('',*,*,#54656,.T.);
#79478=ORIENTED_EDGE('',*,*,#54657,.F.);
#79479=ORIENTED_EDGE('',*,*,#54106,.T.);
#79480=ORIENTED_EDGE('',*,*,#54658,.F.);
#79481=ORIENTED_EDGE('',*,*,#54659,.T.);
#79482=ORIENTED_EDGE('',*,*,#54660,.F.);
#79483=ORIENTED_EDGE('',*,*,#54661,.T.);
#79484=ORIENTED_EDGE('',*,*,#54662,.F.);
#79485=ORIENTED_EDGE('',*,*,#54110,.T.);
#79486=ORIENTED_EDGE('',*,*,#54663,.F.);
#79487=ORIENTED_EDGE('',*,*,#54664,.T.);
#79488=ORIENTED_EDGE('',*,*,#54665,.F.);
#79489=ORIENTED_EDGE('',*,*,#54666,.T.);
#79490=ORIENTED_EDGE('',*,*,#54667,.F.);
#79491=ORIENTED_EDGE('',*,*,#54114,.T.);
#79492=ORIENTED_EDGE('',*,*,#54668,.F.);
#79493=ORIENTED_EDGE('',*,*,#54669,.T.);
#79494=ORIENTED_EDGE('',*,*,#54670,.F.);
#79495=ORIENTED_EDGE('',*,*,#54671,.T.);
#79496=ORIENTED_EDGE('',*,*,#54672,.F.);
#79497=ORIENTED_EDGE('',*,*,#54118,.T.);
#79498=ORIENTED_EDGE('',*,*,#54673,.F.);
#79499=ORIENTED_EDGE('',*,*,#54674,.T.);
#79500=ORIENTED_EDGE('',*,*,#54675,.F.);
#79501=ORIENTED_EDGE('',*,*,#54676,.T.);
#79502=ORIENTED_EDGE('',*,*,#54677,.F.);
#79503=ORIENTED_EDGE('',*,*,#54122,.T.);
#79504=ORIENTED_EDGE('',*,*,#54678,.F.);
#79505=ORIENTED_EDGE('',*,*,#54679,.T.);
#79506=ORIENTED_EDGE('',*,*,#54680,.F.);
#79507=ORIENTED_EDGE('',*,*,#54681,.T.);
#79508=ORIENTED_EDGE('',*,*,#54682,.F.);
#79509=ORIENTED_EDGE('',*,*,#54126,.T.);
#79510=ORIENTED_EDGE('',*,*,#54683,.F.);
#79511=ORIENTED_EDGE('',*,*,#54684,.T.);
#79512=ORIENTED_EDGE('',*,*,#54685,.F.);
#79513=ORIENTED_EDGE('',*,*,#54686,.T.);
#79514=ORIENTED_EDGE('',*,*,#54687,.F.);
#79515=ORIENTED_EDGE('',*,*,#54130,.T.);
#79516=ORIENTED_EDGE('',*,*,#54688,.F.);
#79517=ORIENTED_EDGE('',*,*,#54689,.T.);
#79518=ORIENTED_EDGE('',*,*,#54690,.F.);
#79519=ORIENTED_EDGE('',*,*,#54691,.T.);
#79520=ORIENTED_EDGE('',*,*,#54692,.F.);
#79521=ORIENTED_EDGE('',*,*,#54134,.T.);
#79522=ORIENTED_EDGE('',*,*,#54693,.F.);
#79523=ORIENTED_EDGE('',*,*,#54694,.T.);
#79524=ORIENTED_EDGE('',*,*,#54695,.F.);
#79525=ORIENTED_EDGE('',*,*,#54696,.T.);
#79526=ORIENTED_EDGE('',*,*,#54697,.F.);
#79527=ORIENTED_EDGE('',*,*,#54138,.T.);
#79528=ORIENTED_EDGE('',*,*,#54698,.F.);
#79529=ORIENTED_EDGE('',*,*,#54699,.T.);
#79530=ORIENTED_EDGE('',*,*,#54700,.F.);
#79531=ORIENTED_EDGE('',*,*,#54701,.T.);
#79532=ORIENTED_EDGE('',*,*,#54702,.F.);
#79533=ORIENTED_EDGE('',*,*,#54142,.T.);
#79534=ORIENTED_EDGE('',*,*,#54703,.F.);
#79535=ORIENTED_EDGE('',*,*,#54704,.T.);
#79536=ORIENTED_EDGE('',*,*,#54705,.F.);
#79537=ORIENTED_EDGE('',*,*,#54706,.T.);
#79538=ORIENTED_EDGE('',*,*,#54707,.F.);
#79539=ORIENTED_EDGE('',*,*,#54146,.T.);
#79540=ORIENTED_EDGE('',*,*,#54708,.F.);
#79541=ORIENTED_EDGE('',*,*,#54709,.T.);
#79542=ORIENTED_EDGE('',*,*,#54710,.F.);
#79543=ORIENTED_EDGE('',*,*,#54711,.T.);
#79544=ORIENTED_EDGE('',*,*,#54712,.F.);
#79545=ORIENTED_EDGE('',*,*,#54150,.T.);
#79546=ORIENTED_EDGE('',*,*,#54713,.F.);
#79547=ORIENTED_EDGE('',*,*,#54714,.T.);
#79548=ORIENTED_EDGE('',*,*,#54715,.F.);
#79549=ORIENTED_EDGE('',*,*,#54716,.T.);
#79550=ORIENTED_EDGE('',*,*,#54717,.F.);
#79551=ORIENTED_EDGE('',*,*,#54154,.T.);
#79552=ORIENTED_EDGE('',*,*,#54718,.F.);
#79553=ORIENTED_EDGE('',*,*,#54719,.T.);
#79554=ORIENTED_EDGE('',*,*,#54720,.F.);
#79555=ORIENTED_EDGE('',*,*,#54721,.T.);
#79556=ORIENTED_EDGE('',*,*,#54722,.F.);
#79557=ORIENTED_EDGE('',*,*,#54158,.T.);
#79558=ORIENTED_EDGE('',*,*,#54723,.F.);
#79559=ORIENTED_EDGE('',*,*,#54724,.T.);
#79560=ORIENTED_EDGE('',*,*,#54725,.F.);
#79561=ORIENTED_EDGE('',*,*,#54726,.T.);
#79562=ORIENTED_EDGE('',*,*,#54727,.F.);
#79563=ORIENTED_EDGE('',*,*,#54162,.T.);
#79564=ORIENTED_EDGE('',*,*,#54728,.F.);
#79565=ORIENTED_EDGE('',*,*,#54729,.T.);
#79566=ORIENTED_EDGE('',*,*,#54730,.F.);
#79567=ORIENTED_EDGE('',*,*,#54731,.T.);
#79568=ORIENTED_EDGE('',*,*,#54732,.F.);
#79569=ORIENTED_EDGE('',*,*,#54166,.T.);
#79570=ORIENTED_EDGE('',*,*,#54733,.F.);
#79571=ORIENTED_EDGE('',*,*,#54734,.T.);
#79572=ORIENTED_EDGE('',*,*,#54735,.F.);
#79573=ORIENTED_EDGE('',*,*,#54736,.T.);
#79574=ORIENTED_EDGE('',*,*,#54737,.F.);
#79575=ORIENTED_EDGE('',*,*,#54170,.T.);
#79576=ORIENTED_EDGE('',*,*,#54738,.F.);
#79577=ORIENTED_EDGE('',*,*,#54739,.T.);
#79578=ORIENTED_EDGE('',*,*,#54740,.F.);
#79579=ORIENTED_EDGE('',*,*,#54741,.T.);
#79580=ORIENTED_EDGE('',*,*,#54742,.F.);
#79581=ORIENTED_EDGE('',*,*,#54174,.T.);
#79582=ORIENTED_EDGE('',*,*,#54743,.F.);
#79583=ORIENTED_EDGE('',*,*,#54744,.T.);
#79584=ORIENTED_EDGE('',*,*,#54745,.F.);
#79585=ORIENTED_EDGE('',*,*,#54746,.T.);
#79586=ORIENTED_EDGE('',*,*,#54747,.F.);
#79587=ORIENTED_EDGE('',*,*,#54178,.T.);
#79588=ORIENTED_EDGE('',*,*,#54748,.F.);
#79589=ORIENTED_EDGE('',*,*,#54749,.T.);
#79590=ORIENTED_EDGE('',*,*,#54750,.F.);
#79591=ORIENTED_EDGE('',*,*,#54751,.T.);
#79592=ORIENTED_EDGE('',*,*,#54752,.F.);
#79593=ORIENTED_EDGE('',*,*,#54182,.T.);
#79594=ORIENTED_EDGE('',*,*,#54753,.F.);
#79595=ORIENTED_EDGE('',*,*,#54754,.T.);
#79596=ORIENTED_EDGE('',*,*,#54755,.F.);
#79597=ORIENTED_EDGE('',*,*,#54756,.T.);
#79598=ORIENTED_EDGE('',*,*,#54757,.F.);
#79599=ORIENTED_EDGE('',*,*,#54186,.T.);
#79600=ORIENTED_EDGE('',*,*,#54758,.F.);
#79601=ORIENTED_EDGE('',*,*,#54759,.T.);
#79602=ORIENTED_EDGE('',*,*,#54760,.F.);
#79603=ORIENTED_EDGE('',*,*,#54761,.T.);
#79604=ORIENTED_EDGE('',*,*,#54762,.F.);
#79605=ORIENTED_EDGE('',*,*,#54190,.T.);
#79606=ORIENTED_EDGE('',*,*,#54763,.F.);
#79607=ORIENTED_EDGE('',*,*,#54764,.T.);
#79608=ORIENTED_EDGE('',*,*,#54765,.F.);
#79609=ORIENTED_EDGE('',*,*,#54766,.T.);
#79610=ORIENTED_EDGE('',*,*,#54767,.F.);
#79611=ORIENTED_EDGE('',*,*,#54194,.T.);
#79612=ORIENTED_EDGE('',*,*,#54768,.F.);
#79613=ORIENTED_EDGE('',*,*,#54769,.T.);
#79614=ORIENTED_EDGE('',*,*,#54770,.F.);
#79615=ORIENTED_EDGE('',*,*,#54771,.T.);
#79616=ORIENTED_EDGE('',*,*,#54772,.F.);
#79617=ORIENTED_EDGE('',*,*,#54198,.T.);
#79618=ORIENTED_EDGE('',*,*,#54773,.F.);
#79619=ORIENTED_EDGE('',*,*,#54774,.T.);
#79620=ORIENTED_EDGE('',*,*,#54775,.F.);
#79621=ORIENTED_EDGE('',*,*,#54776,.T.);
#79622=ORIENTED_EDGE('',*,*,#54777,.F.);
#79623=ORIENTED_EDGE('',*,*,#54202,.T.);
#79624=ORIENTED_EDGE('',*,*,#54778,.F.);
#79625=ORIENTED_EDGE('',*,*,#54779,.T.);
#79626=ORIENTED_EDGE('',*,*,#54780,.F.);
#79627=ORIENTED_EDGE('',*,*,#54781,.T.);
#79628=ORIENTED_EDGE('',*,*,#54782,.F.);
#79629=ORIENTED_EDGE('',*,*,#54206,.T.);
#79630=ORIENTED_EDGE('',*,*,#54783,.F.);
#79631=ORIENTED_EDGE('',*,*,#54784,.T.);
#79632=ORIENTED_EDGE('',*,*,#54785,.F.);
#79633=ORIENTED_EDGE('',*,*,#54786,.T.);
#79634=ORIENTED_EDGE('',*,*,#54787,.F.);
#79635=ORIENTED_EDGE('',*,*,#54254,.T.);
#79636=ORIENTED_EDGE('',*,*,#54788,.F.);
#79637=ORIENTED_EDGE('',*,*,#54789,.T.);
#79638=ORIENTED_EDGE('',*,*,#54790,.F.);
#79639=ORIENTED_EDGE('',*,*,#54791,.T.);
#79640=ORIENTED_EDGE('',*,*,#54792,.F.);
#79641=ORIENTED_EDGE('',*,*,#54259,.T.);
#79642=ORIENTED_EDGE('',*,*,#54793,.T.);
#79643=ORIENTED_EDGE('',*,*,#54283,.T.);
#79644=ORIENTED_EDGE('',*,*,#54793,.F.);
#79645=ORIENTED_EDGE('',*,*,#54258,.T.);
#79646=ORIENTED_EDGE('',*,*,#54794,.F.);
#79647=ORIENTED_EDGE('',*,*,#54795,.T.);
#79648=ORIENTED_EDGE('',*,*,#54796,.F.);
#79649=ORIENTED_EDGE('',*,*,#54797,.T.);
#79650=ORIENTED_EDGE('',*,*,#54798,.F.);
#79651=ORIENTED_EDGE('',*,*,#54250,.T.);
#79652=ORIENTED_EDGE('',*,*,#54799,.F.);
#79653=ORIENTED_EDGE('',*,*,#54800,.T.);
#79654=ORIENTED_EDGE('',*,*,#54801,.F.);
#79655=ORIENTED_EDGE('',*,*,#54802,.T.);
#79656=ORIENTED_EDGE('',*,*,#54803,.F.);
#79657=ORIENTED_EDGE('',*,*,#54246,.T.);
#79658=ORIENTED_EDGE('',*,*,#54804,.F.);
#79659=ORIENTED_EDGE('',*,*,#54805,.T.);
#79660=ORIENTED_EDGE('',*,*,#54806,.F.);
#79661=ORIENTED_EDGE('',*,*,#54807,.T.);
#79662=ORIENTED_EDGE('',*,*,#54808,.F.);
#79663=ORIENTED_EDGE('',*,*,#54242,.T.);
#79664=ORIENTED_EDGE('',*,*,#54809,.F.);
#79665=ORIENTED_EDGE('',*,*,#54810,.T.);
#79666=ORIENTED_EDGE('',*,*,#54811,.F.);
#79667=ORIENTED_EDGE('',*,*,#54812,.T.);
#79668=ORIENTED_EDGE('',*,*,#54813,.F.);
#79669=ORIENTED_EDGE('',*,*,#54238,.T.);
#79670=ORIENTED_EDGE('',*,*,#54814,.F.);
#79671=ORIENTED_EDGE('',*,*,#54815,.T.);
#79672=ORIENTED_EDGE('',*,*,#54816,.F.);
#79673=ORIENTED_EDGE('',*,*,#54817,.T.);
#79674=ORIENTED_EDGE('',*,*,#54818,.F.);
#79675=ORIENTED_EDGE('',*,*,#54234,.T.);
#79676=ORIENTED_EDGE('',*,*,#54819,.F.);
#79677=ORIENTED_EDGE('',*,*,#54820,.T.);
#79678=ORIENTED_EDGE('',*,*,#54821,.F.);
#79679=ORIENTED_EDGE('',*,*,#54822,.T.);
#79680=ORIENTED_EDGE('',*,*,#54823,.F.);
#79681=ORIENTED_EDGE('',*,*,#54230,.T.);
#79682=ORIENTED_EDGE('',*,*,#54824,.F.);
#79683=ORIENTED_EDGE('',*,*,#54825,.T.);
#79684=ORIENTED_EDGE('',*,*,#54826,.F.);
#79685=ORIENTED_EDGE('',*,*,#54827,.T.);
#79686=ORIENTED_EDGE('',*,*,#54828,.F.);
#79687=ORIENTED_EDGE('',*,*,#54226,.T.);
#79688=ORIENTED_EDGE('',*,*,#54829,.F.);
#79689=ORIENTED_EDGE('',*,*,#54830,.T.);
#79690=ORIENTED_EDGE('',*,*,#54831,.F.);
#79691=ORIENTED_EDGE('',*,*,#54832,.T.);
#79692=ORIENTED_EDGE('',*,*,#54833,.F.);
#79693=ORIENTED_EDGE('',*,*,#54222,.T.);
#79694=ORIENTED_EDGE('',*,*,#54834,.F.);
#79695=ORIENTED_EDGE('',*,*,#54835,.T.);
#79696=ORIENTED_EDGE('',*,*,#54836,.F.);
#79697=ORIENTED_EDGE('',*,*,#54837,.T.);
#79698=ORIENTED_EDGE('',*,*,#54838,.F.);
#79699=ORIENTED_EDGE('',*,*,#54218,.T.);
#79700=ORIENTED_EDGE('',*,*,#54839,.F.);
#79701=ORIENTED_EDGE('',*,*,#54840,.T.);
#79702=ORIENTED_EDGE('',*,*,#54841,.F.);
#79703=ORIENTED_EDGE('',*,*,#54842,.T.);
#79704=ORIENTED_EDGE('',*,*,#54843,.F.);
#79705=ORIENTED_EDGE('',*,*,#54214,.T.);
#79706=ORIENTED_EDGE('',*,*,#54844,.F.);
#79707=ORIENTED_EDGE('',*,*,#54845,.T.);
#79708=ORIENTED_EDGE('',*,*,#54846,.F.);
#79709=ORIENTED_EDGE('',*,*,#54847,.T.);
#79710=ORIENTED_EDGE('',*,*,#54848,.F.);
#79711=ORIENTED_EDGE('',*,*,#54210,.T.);
#79712=ORIENTED_EDGE('',*,*,#54849,.F.);
#79713=ORIENTED_EDGE('',*,*,#54850,.T.);
#79714=ORIENTED_EDGE('',*,*,#54851,.F.);
#79715=ORIENTED_EDGE('',*,*,#54852,.T.);
#79716=ORIENTED_EDGE('',*,*,#54853,.F.);
#79717=ORIENTED_EDGE('',*,*,#53954,.T.);
#79718=ORIENTED_EDGE('',*,*,#54854,.F.);
#79719=ORIENTED_EDGE('',*,*,#54855,.T.);
#79720=ORIENTED_EDGE('',*,*,#54856,.F.);
#79721=ORIENTED_EDGE('',*,*,#54857,.T.);
#79722=ORIENTED_EDGE('',*,*,#54858,.F.);
#79723=ORIENTED_EDGE('',*,*,#53958,.T.);
#79724=ORIENTED_EDGE('',*,*,#54859,.F.);
#79725=ORIENTED_EDGE('',*,*,#54860,.T.);
#79726=ORIENTED_EDGE('',*,*,#54861,.F.);
#79727=ORIENTED_EDGE('',*,*,#54862,.T.);
#79728=ORIENTED_EDGE('',*,*,#54863,.F.);
#79729=ORIENTED_EDGE('',*,*,#53962,.T.);
#79730=ORIENTED_EDGE('',*,*,#54864,.F.);
#79731=ORIENTED_EDGE('',*,*,#54865,.T.);
#79732=ORIENTED_EDGE('',*,*,#54866,.F.);
#79733=ORIENTED_EDGE('',*,*,#54867,.T.);
#79734=ORIENTED_EDGE('',*,*,#54868,.F.);
#79735=ORIENTED_EDGE('',*,*,#53966,.T.);
#79736=ORIENTED_EDGE('',*,*,#54869,.F.);
#79737=ORIENTED_EDGE('',*,*,#54870,.T.);
#79738=ORIENTED_EDGE('',*,*,#54871,.F.);
#79739=ORIENTED_EDGE('',*,*,#54872,.T.);
#79740=ORIENTED_EDGE('',*,*,#54873,.F.);
#79741=ORIENTED_EDGE('',*,*,#53970,.T.);
#79742=ORIENTED_EDGE('',*,*,#54874,.F.);
#79743=ORIENTED_EDGE('',*,*,#54875,.T.);
#79744=ORIENTED_EDGE('',*,*,#54876,.F.);
#79745=ORIENTED_EDGE('',*,*,#54877,.T.);
#79746=ORIENTED_EDGE('',*,*,#54878,.F.);
#79747=ORIENTED_EDGE('',*,*,#53974,.T.);
#79748=ORIENTED_EDGE('',*,*,#54879,.F.);
#79749=ORIENTED_EDGE('',*,*,#54880,.T.);
#79750=ORIENTED_EDGE('',*,*,#54881,.F.);
#79751=ORIENTED_EDGE('',*,*,#54882,.T.);
#79752=ORIENTED_EDGE('',*,*,#54883,.F.);
#79753=ORIENTED_EDGE('',*,*,#53978,.T.);
#79754=ORIENTED_EDGE('',*,*,#54884,.F.);
#79755=ORIENTED_EDGE('',*,*,#54885,.T.);
#79756=ORIENTED_EDGE('',*,*,#54886,.F.);
#79757=ORIENTED_EDGE('',*,*,#54887,.T.);
#79758=ORIENTED_EDGE('',*,*,#54888,.F.);
#79759=ORIENTED_EDGE('',*,*,#53982,.T.);
#79760=ORIENTED_EDGE('',*,*,#54889,.F.);
#79761=ORIENTED_EDGE('',*,*,#54890,.T.);
#79762=ORIENTED_EDGE('',*,*,#54891,.F.);
#79763=ORIENTED_EDGE('',*,*,#54892,.T.);
#79764=ORIENTED_EDGE('',*,*,#54893,.F.);
#79765=ORIENTED_EDGE('',*,*,#53986,.T.);
#79766=ORIENTED_EDGE('',*,*,#54894,.F.);
#79767=ORIENTED_EDGE('',*,*,#54895,.T.);
#79768=ORIENTED_EDGE('',*,*,#54896,.F.);
#79769=ORIENTED_EDGE('',*,*,#54897,.T.);
#79770=ORIENTED_EDGE('',*,*,#54898,.F.);
#79771=ORIENTED_EDGE('',*,*,#53990,.T.);
#79772=ORIENTED_EDGE('',*,*,#54899,.F.);
#79773=ORIENTED_EDGE('',*,*,#54900,.T.);
#79774=ORIENTED_EDGE('',*,*,#54901,.F.);
#79775=ORIENTED_EDGE('',*,*,#54902,.T.);
#79776=ORIENTED_EDGE('',*,*,#54903,.F.);
#79777=ORIENTED_EDGE('',*,*,#53994,.T.);
#79778=ORIENTED_EDGE('',*,*,#54904,.F.);
#79779=ORIENTED_EDGE('',*,*,#54905,.T.);
#79780=ORIENTED_EDGE('',*,*,#54906,.F.);
#79781=ORIENTED_EDGE('',*,*,#54907,.T.);
#79782=ORIENTED_EDGE('',*,*,#54908,.F.);
#79783=ORIENTED_EDGE('',*,*,#53998,.T.);
#79784=ORIENTED_EDGE('',*,*,#54909,.F.);
#79785=ORIENTED_EDGE('',*,*,#54910,.T.);
#79786=ORIENTED_EDGE('',*,*,#54911,.F.);
#79787=ORIENTED_EDGE('',*,*,#54912,.T.);
#79788=ORIENTED_EDGE('',*,*,#54913,.F.);
#79789=ORIENTED_EDGE('',*,*,#54002,.T.);
#79790=ORIENTED_EDGE('',*,*,#54914,.F.);
#79791=ORIENTED_EDGE('',*,*,#54915,.T.);
#79792=ORIENTED_EDGE('',*,*,#54916,.F.);
#79793=ORIENTED_EDGE('',*,*,#54917,.T.);
#79794=ORIENTED_EDGE('',*,*,#54918,.F.);
#79795=ORIENTED_EDGE('',*,*,#54006,.T.);
#79796=ORIENTED_EDGE('',*,*,#54919,.F.);
#79797=ORIENTED_EDGE('',*,*,#54920,.T.);
#79798=ORIENTED_EDGE('',*,*,#54921,.F.);
#79799=ORIENTED_EDGE('',*,*,#54922,.T.);
#79800=ORIENTED_EDGE('',*,*,#54923,.F.);
#79801=ORIENTED_EDGE('',*,*,#54010,.T.);
#79802=ORIENTED_EDGE('',*,*,#54924,.F.);
#79803=ORIENTED_EDGE('',*,*,#54925,.T.);
#79804=ORIENTED_EDGE('',*,*,#54926,.F.);
#79805=ORIENTED_EDGE('',*,*,#54927,.T.);
#79806=ORIENTED_EDGE('',*,*,#54928,.F.);
#79807=ORIENTED_EDGE('',*,*,#54014,.T.);
#79808=ORIENTED_EDGE('',*,*,#54929,.F.);
#79809=ORIENTED_EDGE('',*,*,#54930,.T.);
#79810=ORIENTED_EDGE('',*,*,#54931,.F.);
#79811=ORIENTED_EDGE('',*,*,#54932,.T.);
#79812=ORIENTED_EDGE('',*,*,#54933,.F.);
#79813=ORIENTED_EDGE('',*,*,#54018,.T.);
#79814=ORIENTED_EDGE('',*,*,#54934,.F.);
#79815=ORIENTED_EDGE('',*,*,#54935,.T.);
#79816=ORIENTED_EDGE('',*,*,#54936,.F.);
#79817=ORIENTED_EDGE('',*,*,#54937,.T.);
#79818=ORIENTED_EDGE('',*,*,#54938,.F.);
#79819=ORIENTED_EDGE('',*,*,#54022,.T.);
#79820=ORIENTED_EDGE('',*,*,#54939,.F.);
#79821=ORIENTED_EDGE('',*,*,#54940,.T.);
#79822=ORIENTED_EDGE('',*,*,#54941,.F.);
#79823=ORIENTED_EDGE('',*,*,#54942,.T.);
#79824=ORIENTED_EDGE('',*,*,#54943,.F.);
#79825=ORIENTED_EDGE('',*,*,#54026,.T.);
#79826=ORIENTED_EDGE('',*,*,#54944,.F.);
#79827=ORIENTED_EDGE('',*,*,#54945,.T.);
#79828=ORIENTED_EDGE('',*,*,#54946,.F.);
#79829=ORIENTED_EDGE('',*,*,#54947,.T.);
#79830=ORIENTED_EDGE('',*,*,#54948,.F.);
#79831=ORIENTED_EDGE('',*,*,#54030,.T.);
#79832=ORIENTED_EDGE('',*,*,#54949,.F.);
#79833=ORIENTED_EDGE('',*,*,#54950,.T.);
#79834=ORIENTED_EDGE('',*,*,#54951,.F.);
#79835=ORIENTED_EDGE('',*,*,#54952,.T.);
#79836=ORIENTED_EDGE('',*,*,#54953,.F.);
#79837=ORIENTED_EDGE('',*,*,#54034,.T.);
#79838=ORIENTED_EDGE('',*,*,#54954,.F.);
#79839=ORIENTED_EDGE('',*,*,#54955,.T.);
#79840=ORIENTED_EDGE('',*,*,#54956,.F.);
#79841=ORIENTED_EDGE('',*,*,#54957,.T.);
#79842=ORIENTED_EDGE('',*,*,#54958,.F.);
#79843=ORIENTED_EDGE('',*,*,#54038,.T.);
#79844=ORIENTED_EDGE('',*,*,#54959,.F.);
#79845=ORIENTED_EDGE('',*,*,#54960,.T.);
#79846=ORIENTED_EDGE('',*,*,#54961,.F.);
#79847=ORIENTED_EDGE('',*,*,#54962,.T.);
#79848=ORIENTED_EDGE('',*,*,#54963,.F.);
#79849=ORIENTED_EDGE('',*,*,#54042,.T.);
#79850=ORIENTED_EDGE('',*,*,#54964,.F.);
#79851=ORIENTED_EDGE('',*,*,#54965,.T.);
#79852=ORIENTED_EDGE('',*,*,#54966,.F.);
#79853=ORIENTED_EDGE('',*,*,#54967,.T.);
#79854=ORIENTED_EDGE('',*,*,#54968,.F.);
#79855=ORIENTED_EDGE('',*,*,#54046,.T.);
#79856=ORIENTED_EDGE('',*,*,#54969,.F.);
#79857=ORIENTED_EDGE('',*,*,#54970,.T.);
#79858=ORIENTED_EDGE('',*,*,#54971,.F.);
#79859=ORIENTED_EDGE('',*,*,#54972,.T.);
#79860=ORIENTED_EDGE('',*,*,#54973,.F.);
#79861=ORIENTED_EDGE('',*,*,#54050,.T.);
#79862=ORIENTED_EDGE('',*,*,#54974,.F.);
#79863=ORIENTED_EDGE('',*,*,#54975,.T.);
#79864=ORIENTED_EDGE('',*,*,#54976,.F.);
#79865=ORIENTED_EDGE('',*,*,#54977,.T.);
#79866=ORIENTED_EDGE('',*,*,#54978,.F.);
#79867=ORIENTED_EDGE('',*,*,#54054,.T.);
#79868=ORIENTED_EDGE('',*,*,#54979,.F.);
#79869=ORIENTED_EDGE('',*,*,#54980,.T.);
#79870=ORIENTED_EDGE('',*,*,#54981,.F.);
#79871=ORIENTED_EDGE('',*,*,#54982,.T.);
#79872=ORIENTED_EDGE('',*,*,#54983,.F.);
#79873=ORIENTED_EDGE('',*,*,#54058,.T.);
#79874=ORIENTED_EDGE('',*,*,#54984,.F.);
#79875=ORIENTED_EDGE('',*,*,#54985,.T.);
#79876=ORIENTED_EDGE('',*,*,#54600,.T.);
#79877=ORIENTED_EDGE('',*,*,#54986,.T.);
#79878=ORIENTED_EDGE('',*,*,#54443,.F.);
#79879=ORIENTED_EDGE('',*,*,#54439,.F.);
#79880=ORIENTED_EDGE('',*,*,#54987,.T.);
#79881=ORIENTED_EDGE('',*,*,#54551,.F.);
#79882=ORIENTED_EDGE('',*,*,#54988,.T.);
#79883=ORIENTED_EDGE('',*,*,#54851,.T.);
#79884=ORIENTED_EDGE('',*,*,#54989,.T.);
#79885=ORIENTED_EDGE('',*,*,#54856,.T.);
#79886=ORIENTED_EDGE('',*,*,#54990,.T.);
#79887=ORIENTED_EDGE('',*,*,#54547,.F.);
#79888=ORIENTED_EDGE('',*,*,#54991,.T.);
#79889=ORIENTED_EDGE('',*,*,#54861,.T.);
#79890=ORIENTED_EDGE('',*,*,#54992,.T.);
#79891=ORIENTED_EDGE('',*,*,#54543,.F.);
#79892=ORIENTED_EDGE('',*,*,#54993,.T.);
#79893=ORIENTED_EDGE('',*,*,#54866,.T.);
#79894=ORIENTED_EDGE('',*,*,#54994,.T.);
#79895=ORIENTED_EDGE('',*,*,#54539,.F.);
#79896=ORIENTED_EDGE('',*,*,#54995,.T.);
#79897=ORIENTED_EDGE('',*,*,#54871,.T.);
#79898=ORIENTED_EDGE('',*,*,#54996,.T.);
#79899=ORIENTED_EDGE('',*,*,#54535,.F.);
#79900=ORIENTED_EDGE('',*,*,#54997,.T.);
#79901=ORIENTED_EDGE('',*,*,#54876,.T.);
#79902=ORIENTED_EDGE('',*,*,#54998,.T.);
#79903=ORIENTED_EDGE('',*,*,#54531,.F.);
#79904=ORIENTED_EDGE('',*,*,#54999,.T.);
#79905=ORIENTED_EDGE('',*,*,#54881,.T.);
#79906=ORIENTED_EDGE('',*,*,#55000,.T.);
#79907=ORIENTED_EDGE('',*,*,#54527,.F.);
#79908=ORIENTED_EDGE('',*,*,#55001,.T.);
#79909=ORIENTED_EDGE('',*,*,#54886,.T.);
#79910=ORIENTED_EDGE('',*,*,#55002,.T.);
#79911=ORIENTED_EDGE('',*,*,#54523,.F.);
#79912=ORIENTED_EDGE('',*,*,#55003,.T.);
#79913=ORIENTED_EDGE('',*,*,#54891,.T.);
#79914=ORIENTED_EDGE('',*,*,#55004,.T.);
#79915=ORIENTED_EDGE('',*,*,#54519,.F.);
#79916=ORIENTED_EDGE('',*,*,#55005,.T.);
#79917=ORIENTED_EDGE('',*,*,#54896,.T.);
#79918=ORIENTED_EDGE('',*,*,#55006,.T.);
#79919=ORIENTED_EDGE('',*,*,#54515,.F.);
#79920=ORIENTED_EDGE('',*,*,#55007,.T.);
#79921=ORIENTED_EDGE('',*,*,#54901,.T.);
#79922=ORIENTED_EDGE('',*,*,#55008,.T.);
#79923=ORIENTED_EDGE('',*,*,#54511,.F.);
#79924=ORIENTED_EDGE('',*,*,#55009,.T.);
#79925=ORIENTED_EDGE('',*,*,#54906,.T.);
#79926=ORIENTED_EDGE('',*,*,#55010,.T.);
#79927=ORIENTED_EDGE('',*,*,#54507,.F.);
#79928=ORIENTED_EDGE('',*,*,#55011,.T.);
#79929=ORIENTED_EDGE('',*,*,#54911,.T.);
#79930=ORIENTED_EDGE('',*,*,#55012,.T.);
#79931=ORIENTED_EDGE('',*,*,#54503,.F.);
#79932=ORIENTED_EDGE('',*,*,#55013,.T.);
#79933=ORIENTED_EDGE('',*,*,#54916,.T.);
#79934=ORIENTED_EDGE('',*,*,#55014,.T.);
#79935=ORIENTED_EDGE('',*,*,#54499,.F.);
#79936=ORIENTED_EDGE('',*,*,#55015,.T.);
#79937=ORIENTED_EDGE('',*,*,#54921,.T.);
#79938=ORIENTED_EDGE('',*,*,#55016,.T.);
#79939=ORIENTED_EDGE('',*,*,#54495,.F.);
#79940=ORIENTED_EDGE('',*,*,#55017,.T.);
#79941=ORIENTED_EDGE('',*,*,#54926,.T.);
#79942=ORIENTED_EDGE('',*,*,#55018,.T.);
#79943=ORIENTED_EDGE('',*,*,#54491,.F.);
#79944=ORIENTED_EDGE('',*,*,#55019,.T.);
#79945=ORIENTED_EDGE('',*,*,#54931,.T.);
#79946=ORIENTED_EDGE('',*,*,#55020,.T.);
#79947=ORIENTED_EDGE('',*,*,#54487,.F.);
#79948=ORIENTED_EDGE('',*,*,#55021,.T.);
#79949=ORIENTED_EDGE('',*,*,#54936,.T.);
#79950=ORIENTED_EDGE('',*,*,#55022,.T.);
#79951=ORIENTED_EDGE('',*,*,#54483,.F.);
#79952=ORIENTED_EDGE('',*,*,#55023,.T.);
#79953=ORIENTED_EDGE('',*,*,#54941,.T.);
#79954=ORIENTED_EDGE('',*,*,#55024,.T.);
#79955=ORIENTED_EDGE('',*,*,#54479,.F.);
#79956=ORIENTED_EDGE('',*,*,#55025,.T.);
#79957=ORIENTED_EDGE('',*,*,#54946,.T.);
#79958=ORIENTED_EDGE('',*,*,#55026,.T.);
#79959=ORIENTED_EDGE('',*,*,#54475,.F.);
#79960=ORIENTED_EDGE('',*,*,#55027,.T.);
#79961=ORIENTED_EDGE('',*,*,#54951,.T.);
#79962=ORIENTED_EDGE('',*,*,#55028,.T.);
#79963=ORIENTED_EDGE('',*,*,#54471,.F.);
#79964=ORIENTED_EDGE('',*,*,#55029,.T.);
#79965=ORIENTED_EDGE('',*,*,#54956,.T.);
#79966=ORIENTED_EDGE('',*,*,#55030,.T.);
#79967=ORIENTED_EDGE('',*,*,#54467,.F.);
#79968=ORIENTED_EDGE('',*,*,#55031,.T.);
#79969=ORIENTED_EDGE('',*,*,#54961,.T.);
#79970=ORIENTED_EDGE('',*,*,#55032,.T.);
#79971=ORIENTED_EDGE('',*,*,#54463,.F.);
#79972=ORIENTED_EDGE('',*,*,#55033,.T.);
#79973=ORIENTED_EDGE('',*,*,#54966,.T.);
#79974=ORIENTED_EDGE('',*,*,#55034,.T.);
#79975=ORIENTED_EDGE('',*,*,#54459,.F.);
#79976=ORIENTED_EDGE('',*,*,#55035,.T.);
#79977=ORIENTED_EDGE('',*,*,#54971,.T.);
#79978=ORIENTED_EDGE('',*,*,#55036,.T.);
#79979=ORIENTED_EDGE('',*,*,#54455,.F.);
#79980=ORIENTED_EDGE('',*,*,#55037,.T.);
#79981=ORIENTED_EDGE('',*,*,#54976,.T.);
#79982=ORIENTED_EDGE('',*,*,#55038,.T.);
#79983=ORIENTED_EDGE('',*,*,#54451,.F.);
#79984=ORIENTED_EDGE('',*,*,#55039,.T.);
#79985=ORIENTED_EDGE('',*,*,#54981,.T.);
#79986=ORIENTED_EDGE('',*,*,#55040,.T.);
#79987=ORIENTED_EDGE('',*,*,#54447,.F.);
#79988=ORIENTED_EDGE('',*,*,#55041,.T.);
#79989=ORIENTED_EDGE('',*,*,#54605,.T.);
#79990=ORIENTED_EDGE('',*,*,#55042,.T.);
#79991=ORIENTED_EDGE('',*,*,#54435,.F.);
#79992=ORIENTED_EDGE('',*,*,#55043,.T.);
#79993=ORIENTED_EDGE('',*,*,#54610,.T.);
#79994=ORIENTED_EDGE('',*,*,#55044,.T.);
#79995=ORIENTED_EDGE('',*,*,#54431,.F.);
#79996=ORIENTED_EDGE('',*,*,#55045,.T.);
#79997=ORIENTED_EDGE('',*,*,#54615,.T.);
#79998=ORIENTED_EDGE('',*,*,#55046,.T.);
#79999=ORIENTED_EDGE('',*,*,#54427,.F.);
#80000=ORIENTED_EDGE('',*,*,#55047,.T.);
#80001=ORIENTED_EDGE('',*,*,#54620,.T.);
#80002=ORIENTED_EDGE('',*,*,#55048,.T.);
#80003=ORIENTED_EDGE('',*,*,#54423,.F.);
#80004=ORIENTED_EDGE('',*,*,#55049,.T.);
#80005=ORIENTED_EDGE('',*,*,#54625,.T.);
#80006=ORIENTED_EDGE('',*,*,#55050,.T.);
#80007=ORIENTED_EDGE('',*,*,#54419,.F.);
#80008=ORIENTED_EDGE('',*,*,#55051,.T.);
#80009=ORIENTED_EDGE('',*,*,#54630,.T.);
#80010=ORIENTED_EDGE('',*,*,#55052,.T.);
#80011=ORIENTED_EDGE('',*,*,#54415,.F.);
#80012=ORIENTED_EDGE('',*,*,#55053,.T.);
#80013=ORIENTED_EDGE('',*,*,#54635,.T.);
#80014=ORIENTED_EDGE('',*,*,#55054,.T.);
#80015=ORIENTED_EDGE('',*,*,#54411,.F.);
#80016=ORIENTED_EDGE('',*,*,#55055,.T.);
#80017=ORIENTED_EDGE('',*,*,#54640,.T.);
#80018=ORIENTED_EDGE('',*,*,#55056,.T.);
#80019=ORIENTED_EDGE('',*,*,#54407,.F.);
#80020=ORIENTED_EDGE('',*,*,#55057,.T.);
#80021=ORIENTED_EDGE('',*,*,#54645,.T.);
#80022=ORIENTED_EDGE('',*,*,#55058,.T.);
#80023=ORIENTED_EDGE('',*,*,#54403,.F.);
#80024=ORIENTED_EDGE('',*,*,#55059,.T.);
#80025=ORIENTED_EDGE('',*,*,#54650,.T.);
#80026=ORIENTED_EDGE('',*,*,#55060,.T.);
#80027=ORIENTED_EDGE('',*,*,#54399,.F.);
#80028=ORIENTED_EDGE('',*,*,#55061,.T.);
#80029=ORIENTED_EDGE('',*,*,#54655,.T.);
#80030=ORIENTED_EDGE('',*,*,#55062,.T.);
#80031=ORIENTED_EDGE('',*,*,#54395,.F.);
#80032=ORIENTED_EDGE('',*,*,#55063,.T.);
#80033=ORIENTED_EDGE('',*,*,#54660,.T.);
#80034=ORIENTED_EDGE('',*,*,#55064,.T.);
#80035=ORIENTED_EDGE('',*,*,#54391,.F.);
#80036=ORIENTED_EDGE('',*,*,#55065,.T.);
#80037=ORIENTED_EDGE('',*,*,#54665,.T.);
#80038=ORIENTED_EDGE('',*,*,#55066,.T.);
#80039=ORIENTED_EDGE('',*,*,#54387,.F.);
#80040=ORIENTED_EDGE('',*,*,#55067,.T.);
#80041=ORIENTED_EDGE('',*,*,#54670,.T.);
#80042=ORIENTED_EDGE('',*,*,#55068,.T.);
#80043=ORIENTED_EDGE('',*,*,#54383,.F.);
#80044=ORIENTED_EDGE('',*,*,#55069,.T.);
#80045=ORIENTED_EDGE('',*,*,#54675,.T.);
#80046=ORIENTED_EDGE('',*,*,#55070,.T.);
#80047=ORIENTED_EDGE('',*,*,#54379,.F.);
#80048=ORIENTED_EDGE('',*,*,#55071,.T.);
#80049=ORIENTED_EDGE('',*,*,#54680,.T.);
#80050=ORIENTED_EDGE('',*,*,#55072,.T.);
#80051=ORIENTED_EDGE('',*,*,#54375,.F.);
#80052=ORIENTED_EDGE('',*,*,#55073,.T.);
#80053=ORIENTED_EDGE('',*,*,#54685,.T.);
#80054=ORIENTED_EDGE('',*,*,#55074,.T.);
#80055=ORIENTED_EDGE('',*,*,#54371,.F.);
#80056=ORIENTED_EDGE('',*,*,#55075,.T.);
#80057=ORIENTED_EDGE('',*,*,#54690,.T.);
#80058=ORIENTED_EDGE('',*,*,#55076,.T.);
#80059=ORIENTED_EDGE('',*,*,#54367,.F.);
#80060=ORIENTED_EDGE('',*,*,#55077,.T.);
#80061=ORIENTED_EDGE('',*,*,#54695,.T.);
#80062=ORIENTED_EDGE('',*,*,#55078,.T.);
#80063=ORIENTED_EDGE('',*,*,#54363,.F.);
#80064=ORIENTED_EDGE('',*,*,#55079,.T.);
#80065=ORIENTED_EDGE('',*,*,#54700,.T.);
#80066=ORIENTED_EDGE('',*,*,#55080,.T.);
#80067=ORIENTED_EDGE('',*,*,#54359,.F.);
#80068=ORIENTED_EDGE('',*,*,#55081,.T.);
#80069=ORIENTED_EDGE('',*,*,#54705,.T.);
#80070=ORIENTED_EDGE('',*,*,#55082,.T.);
#80071=ORIENTED_EDGE('',*,*,#54355,.F.);
#80072=ORIENTED_EDGE('',*,*,#55083,.T.);
#80073=ORIENTED_EDGE('',*,*,#54710,.T.);
#80074=ORIENTED_EDGE('',*,*,#55084,.T.);
#80075=ORIENTED_EDGE('',*,*,#54351,.F.);
#80076=ORIENTED_EDGE('',*,*,#55085,.T.);
#80077=ORIENTED_EDGE('',*,*,#54715,.T.);
#80078=ORIENTED_EDGE('',*,*,#55086,.T.);
#80079=ORIENTED_EDGE('',*,*,#54347,.F.);
#80080=ORIENTED_EDGE('',*,*,#55087,.T.);
#80081=ORIENTED_EDGE('',*,*,#54720,.T.);
#80082=ORIENTED_EDGE('',*,*,#55088,.T.);
#80083=ORIENTED_EDGE('',*,*,#54343,.F.);
#80084=ORIENTED_EDGE('',*,*,#55089,.T.);
#80085=ORIENTED_EDGE('',*,*,#54725,.T.);
#80086=ORIENTED_EDGE('',*,*,#55090,.T.);
#80087=ORIENTED_EDGE('',*,*,#54339,.F.);
#80088=ORIENTED_EDGE('',*,*,#55091,.T.);
#80089=ORIENTED_EDGE('',*,*,#54730,.T.);
#80090=ORIENTED_EDGE('',*,*,#55092,.T.);
#80091=ORIENTED_EDGE('',*,*,#54335,.F.);
#80092=ORIENTED_EDGE('',*,*,#55093,.T.);
#80093=ORIENTED_EDGE('',*,*,#54735,.T.);
#80094=ORIENTED_EDGE('',*,*,#55094,.T.);
#80095=ORIENTED_EDGE('',*,*,#54331,.F.);
#80096=ORIENTED_EDGE('',*,*,#55095,.T.);
#80097=ORIENTED_EDGE('',*,*,#54740,.T.);
#80098=ORIENTED_EDGE('',*,*,#55096,.T.);
#80099=ORIENTED_EDGE('',*,*,#54327,.F.);
#80100=ORIENTED_EDGE('',*,*,#55097,.T.);
#80101=ORIENTED_EDGE('',*,*,#54745,.T.);
#80102=ORIENTED_EDGE('',*,*,#55098,.T.);
#80103=ORIENTED_EDGE('',*,*,#54323,.F.);
#80104=ORIENTED_EDGE('',*,*,#55099,.T.);
#80105=ORIENTED_EDGE('',*,*,#54750,.T.);
#80106=ORIENTED_EDGE('',*,*,#55100,.T.);
#80107=ORIENTED_EDGE('',*,*,#54319,.F.);
#80108=ORIENTED_EDGE('',*,*,#55101,.T.);
#80109=ORIENTED_EDGE('',*,*,#54755,.T.);
#80110=ORIENTED_EDGE('',*,*,#55102,.T.);
#80111=ORIENTED_EDGE('',*,*,#54315,.F.);
#80112=ORIENTED_EDGE('',*,*,#55103,.T.);
#80113=ORIENTED_EDGE('',*,*,#54760,.T.);
#80114=ORIENTED_EDGE('',*,*,#55104,.T.);
#80115=ORIENTED_EDGE('',*,*,#54311,.F.);
#80116=ORIENTED_EDGE('',*,*,#55105,.T.);
#80117=ORIENTED_EDGE('',*,*,#54765,.T.);
#80118=ORIENTED_EDGE('',*,*,#55106,.T.);
#80119=ORIENTED_EDGE('',*,*,#54307,.F.);
#80120=ORIENTED_EDGE('',*,*,#55107,.T.);
#80121=ORIENTED_EDGE('',*,*,#54770,.T.);
#80122=ORIENTED_EDGE('',*,*,#55108,.T.);
#80123=ORIENTED_EDGE('',*,*,#54303,.F.);
#80124=ORIENTED_EDGE('',*,*,#55109,.T.);
#80125=ORIENTED_EDGE('',*,*,#54775,.T.);
#80126=ORIENTED_EDGE('',*,*,#55110,.T.);
#80127=ORIENTED_EDGE('',*,*,#54299,.F.);
#80128=ORIENTED_EDGE('',*,*,#55111,.T.);
#80129=ORIENTED_EDGE('',*,*,#54780,.T.);
#80130=ORIENTED_EDGE('',*,*,#55112,.T.);
#80131=ORIENTED_EDGE('',*,*,#54295,.F.);
#80132=ORIENTED_EDGE('',*,*,#55113,.T.);
#80133=ORIENTED_EDGE('',*,*,#54555,.F.);
#80134=ORIENTED_EDGE('',*,*,#55114,.T.);
#80135=ORIENTED_EDGE('',*,*,#54846,.T.);
#80136=ORIENTED_EDGE('',*,*,#55115,.T.);
#80137=ORIENTED_EDGE('',*,*,#54559,.F.);
#80138=ORIENTED_EDGE('',*,*,#55116,.T.);
#80139=ORIENTED_EDGE('',*,*,#54841,.T.);
#80140=ORIENTED_EDGE('',*,*,#55117,.T.);
#80141=ORIENTED_EDGE('',*,*,#54563,.F.);
#80142=ORIENTED_EDGE('',*,*,#55118,.T.);
#80143=ORIENTED_EDGE('',*,*,#54836,.T.);
#80144=ORIENTED_EDGE('',*,*,#55119,.T.);
#80145=ORIENTED_EDGE('',*,*,#54567,.F.);
#80146=ORIENTED_EDGE('',*,*,#55120,.T.);
#80147=ORIENTED_EDGE('',*,*,#54831,.T.);
#80148=ORIENTED_EDGE('',*,*,#55121,.T.);
#80149=ORIENTED_EDGE('',*,*,#54571,.F.);
#80150=ORIENTED_EDGE('',*,*,#55122,.T.);
#80151=ORIENTED_EDGE('',*,*,#54826,.T.);
#80152=ORIENTED_EDGE('',*,*,#55123,.T.);
#80153=ORIENTED_EDGE('',*,*,#54575,.F.);
#80154=ORIENTED_EDGE('',*,*,#55124,.T.);
#80155=ORIENTED_EDGE('',*,*,#54821,.T.);
#80156=ORIENTED_EDGE('',*,*,#55125,.T.);
#80157=ORIENTED_EDGE('',*,*,#54579,.F.);
#80158=ORIENTED_EDGE('',*,*,#55126,.T.);
#80159=ORIENTED_EDGE('',*,*,#54816,.T.);
#80160=ORIENTED_EDGE('',*,*,#55127,.T.);
#80161=ORIENTED_EDGE('',*,*,#54583,.F.);
#80162=ORIENTED_EDGE('',*,*,#55128,.T.);
#80163=ORIENTED_EDGE('',*,*,#54811,.T.);
#80164=ORIENTED_EDGE('',*,*,#55129,.T.);
#80165=ORIENTED_EDGE('',*,*,#54587,.F.);
#80166=ORIENTED_EDGE('',*,*,#55130,.T.);
#80167=ORIENTED_EDGE('',*,*,#54806,.T.);
#80168=ORIENTED_EDGE('',*,*,#55131,.T.);
#80169=ORIENTED_EDGE('',*,*,#54591,.F.);
#80170=ORIENTED_EDGE('',*,*,#55132,.T.);
#80171=ORIENTED_EDGE('',*,*,#54801,.T.);
#80172=ORIENTED_EDGE('',*,*,#55133,.T.);
#80173=ORIENTED_EDGE('',*,*,#54595,.F.);
#80174=ORIENTED_EDGE('',*,*,#55134,.T.);
#80175=ORIENTED_EDGE('',*,*,#54796,.T.);
#80176=ORIENTED_EDGE('',*,*,#55135,.T.);
#80177=ORIENTED_EDGE('',*,*,#54785,.T.);
#80178=ORIENTED_EDGE('',*,*,#55136,.T.);
#80179=ORIENTED_EDGE('',*,*,#54291,.F.);
#80180=ORIENTED_EDGE('',*,*,#55137,.T.);
#80181=ORIENTED_EDGE('',*,*,#55138,.T.);
#80182=ORIENTED_EDGE('',*,*,#55139,.T.);
#80183=ORIENTED_EDGE('',*,*,#55140,.T.);
#80184=ORIENTED_EDGE('',*,*,#55141,.F.);
#80185=ORIENTED_EDGE('',*,*,#55142,.T.);
#80186=ORIENTED_EDGE('',*,*,#55143,.T.);
#80187=ORIENTED_EDGE('',*,*,#55144,.T.);
#80188=ORIENTED_EDGE('',*,*,#55145,.T.);
#80189=ORIENTED_EDGE('',*,*,#55138,.F.);
#80190=ORIENTED_EDGE('',*,*,#55146,.T.);
#80191=ORIENTED_EDGE('',*,*,#55147,.T.);
#80192=ORIENTED_EDGE('',*,*,#55141,.T.);
#80193=ORIENTED_EDGE('',*,*,#55148,.T.);
#80194=ORIENTED_EDGE('',*,*,#55149,.T.);
#80195=ORIENTED_EDGE('',*,*,#55150,.T.);
#80196=ORIENTED_EDGE('',*,*,#55151,.T.);
#80197=ORIENTED_EDGE('',*,*,#54280,.F.);
#80198=ORIENTED_EDGE('',*,*,#54266,.F.);
#80199=ORIENTED_EDGE('',*,*,#55152,.T.);
#80200=ORIENTED_EDGE('',*,*,#54273,.F.);
#80201=ORIENTED_EDGE('',*,*,#55153,.T.);
#80202=ORIENTED_EDGE('',*,*,#55154,.T.);
#80203=ORIENTED_EDGE('',*,*,#54272,.T.);
#80204=ORIENTED_EDGE('',*,*,#55155,.T.);
#80205=ORIENTED_EDGE('',*,*,#55156,.T.);
#80206=ORIENTED_EDGE('',*,*,#54271,.T.);
#80207=ORIENTED_EDGE('',*,*,#55157,.T.);
#80208=ORIENTED_EDGE('',*,*,#55158,.T.);
#80209=ORIENTED_EDGE('',*,*,#54270,.T.);
#80210=ORIENTED_EDGE('',*,*,#55159,.T.);
#80211=ORIENTED_EDGE('',*,*,#55160,.T.);
#80212=ORIENTED_EDGE('',*,*,#54275,.T.);
#80213=ORIENTED_EDGE('',*,*,#55161,.T.);
#80214=ORIENTED_EDGE('',*,*,#54598,.T.);
#80215=ORIENTED_EDGE('',*,*,#55162,.F.);
#80216=ORIENTED_EDGE('',*,*,#55163,.F.);
#80217=ORIENTED_EDGE('',*,*,#54277,.F.);
#80218=ORIENTED_EDGE('',*,*,#55164,.F.);
#80219=ORIENTED_EDGE('',*,*,#55165,.F.);
#80220=ORIENTED_EDGE('',*,*,#55166,.F.);
#80221=ORIENTED_EDGE('',*,*,#54790,.T.);
#80222=ORIENTED_EDGE('',*,*,#55167,.T.);
#80223=ORIENTED_EDGE('',*,*,#54287,.F.);
#80224=ORIENTED_EDGE('',*,*,#55168,.T.);
#80225=ORIENTED_EDGE('',*,*,#55169,.T.);
#80226=ORIENTED_EDGE('',*,*,#55170,.F.);
#80227=ORIENTED_EDGE('',*,*,#55171,.F.);
#80228=ORIENTED_EDGE('',*,*,#55172,.F.);
#80229=ORIENTED_EDGE('',*,*,#55152,.F.);
#80230=ORIENTED_EDGE('',*,*,#55173,.T.);
#80231=ORIENTED_EDGE('',*,*,#54276,.F.);
#80232=ORIENTED_EDGE('',*,*,#55169,.F.);
#80233=ORIENTED_EDGE('',*,*,#55153,.F.);
#80234=ORIENTED_EDGE('',*,*,#55154,.F.);
#80235=ORIENTED_EDGE('',*,*,#55174,.T.);
#80236=ORIENTED_EDGE('',*,*,#55175,.F.);
#80237=ORIENTED_EDGE('',*,*,#55173,.F.);
#80238=ORIENTED_EDGE('',*,*,#55155,.F.);
#80239=ORIENTED_EDGE('',*,*,#55156,.F.);
#80240=ORIENTED_EDGE('',*,*,#55176,.T.);
#80241=ORIENTED_EDGE('',*,*,#55177,.F.);
#80242=ORIENTED_EDGE('',*,*,#55174,.F.);
#80243=ORIENTED_EDGE('',*,*,#55157,.F.);
#80244=ORIENTED_EDGE('',*,*,#55158,.F.);
#80245=ORIENTED_EDGE('',*,*,#55178,.T.);
#80246=ORIENTED_EDGE('',*,*,#55179,.F.);
#80247=ORIENTED_EDGE('',*,*,#55176,.F.);
#80248=ORIENTED_EDGE('',*,*,#55159,.F.);
#80249=ORIENTED_EDGE('',*,*,#55160,.F.);
#80250=ORIENTED_EDGE('',*,*,#55171,.T.);
#80251=ORIENTED_EDGE('',*,*,#55180,.F.);
#80252=ORIENTED_EDGE('',*,*,#55178,.F.);
#80253=ORIENTED_EDGE('',*,*,#55161,.F.);
#80254=ORIENTED_EDGE('',*,*,#55181,.F.);
#80255=ORIENTED_EDGE('',*,*,#55181,.T.);
#80256=ORIENTED_EDGE('',*,*,#54274,.T.);
#80257=ORIENTED_EDGE('',*,*,#55172,.T.);
#80258=ORIENTED_EDGE('',*,*,#55180,.T.);
#80259=ORIENTED_EDGE('',*,*,#55162,.T.);
#80260=ORIENTED_EDGE('',*,*,#55177,.T.);
#80261=ORIENTED_EDGE('',*,*,#55165,.T.);
#80262=ORIENTED_EDGE('',*,*,#55175,.T.);
#80263=ORIENTED_EDGE('',*,*,#55164,.T.);
#80264=ORIENTED_EDGE('',*,*,#55179,.T.);
#80265=ORIENTED_EDGE('',*,*,#55166,.T.);
#80266=ORIENTED_EDGE('',*,*,#55170,.T.);
#80267=ORIENTED_EDGE('',*,*,#55163,.T.);
#80268=ORIENTED_EDGE('',*,*,#53841,.F.);
#80269=ORIENTED_EDGE('',*,*,#53729,.F.);
#80270=ORIENTED_EDGE('',*,*,#54263,.F.);
#80271=ORIENTED_EDGE('',*,*,#53836,.F.);
#80272=ORIENTED_EDGE('',*,*,#53951,.T.);
#80273=ORIENTED_EDGE('',*,*,#54262,.T.);
#80274=ORIENTED_EDGE('',*,*,#53945,.T.);
#80275=ORIENTED_EDGE('',*,*,#53942,.T.);
#80276=ORIENTED_EDGE('',*,*,#53939,.T.);
#80277=ORIENTED_EDGE('',*,*,#53938,.T.);
#80278=ORIENTED_EDGE('',*,*,#53935,.T.);
#80279=ORIENTED_EDGE('',*,*,#53932,.T.);
#80280=ORIENTED_EDGE('',*,*,#53929,.T.);
#80281=ORIENTED_EDGE('',*,*,#53926,.T.);
#80282=ORIENTED_EDGE('',*,*,#53923,.T.);
#80283=ORIENTED_EDGE('',*,*,#53920,.T.);
#80284=ORIENTED_EDGE('',*,*,#53917,.T.);
#80285=ORIENTED_EDGE('',*,*,#53914,.T.);
#80286=ORIENTED_EDGE('',*,*,#53911,.T.);
#80287=ORIENTED_EDGE('',*,*,#53908,.T.);
#80288=ORIENTED_EDGE('',*,*,#53905,.T.);
#80289=ORIENTED_EDGE('',*,*,#53902,.T.);
#80290=ORIENTED_EDGE('',*,*,#53899,.T.);
#80291=ORIENTED_EDGE('',*,*,#53896,.T.);
#80292=ORIENTED_EDGE('',*,*,#53893,.T.);
#80293=ORIENTED_EDGE('',*,*,#53890,.T.);
#80294=ORIENTED_EDGE('',*,*,#53887,.T.);
#80295=ORIENTED_EDGE('',*,*,#53884,.T.);
#80296=ORIENTED_EDGE('',*,*,#53881,.T.);
#80297=ORIENTED_EDGE('',*,*,#53878,.T.);
#80298=ORIENTED_EDGE('',*,*,#53875,.T.);
#80299=ORIENTED_EDGE('',*,*,#53872,.T.);
#80300=ORIENTED_EDGE('',*,*,#53869,.T.);
#80301=ORIENTED_EDGE('',*,*,#53866,.T.);
#80302=ORIENTED_EDGE('',*,*,#53863,.T.);
#80303=ORIENTED_EDGE('',*,*,#53860,.T.);
#80304=ORIENTED_EDGE('',*,*,#53857,.T.);
#80305=ORIENTED_EDGE('',*,*,#53854,.T.);
#80306=ORIENTED_EDGE('',*,*,#53851,.T.);
#80307=ORIENTED_EDGE('',*,*,#53848,.T.);
#80308=ORIENTED_EDGE('',*,*,#53845,.T.);
#80309=ORIENTED_EDGE('',*,*,#54264,.T.);
#80310=ORIENTED_EDGE('',*,*,#53728,.T.);
#80311=ORIENTED_EDGE('',*,*,#53731,.T.);
#80312=ORIENTED_EDGE('',*,*,#53734,.T.);
#80313=ORIENTED_EDGE('',*,*,#53737,.T.);
#80314=ORIENTED_EDGE('',*,*,#53740,.T.);
#80315=ORIENTED_EDGE('',*,*,#53743,.T.);
#80316=ORIENTED_EDGE('',*,*,#53746,.T.);
#80317=ORIENTED_EDGE('',*,*,#53749,.T.);
#80318=ORIENTED_EDGE('',*,*,#53752,.T.);
#80319=ORIENTED_EDGE('',*,*,#53755,.T.);
#80320=ORIENTED_EDGE('',*,*,#53758,.T.);
#80321=ORIENTED_EDGE('',*,*,#53761,.T.);
#80322=ORIENTED_EDGE('',*,*,#53764,.T.);
#80323=ORIENTED_EDGE('',*,*,#53767,.T.);
#80324=ORIENTED_EDGE('',*,*,#53770,.T.);
#80325=ORIENTED_EDGE('',*,*,#53773,.T.);
#80326=ORIENTED_EDGE('',*,*,#53776,.T.);
#80327=ORIENTED_EDGE('',*,*,#53779,.T.);
#80328=ORIENTED_EDGE('',*,*,#53782,.T.);
#80329=ORIENTED_EDGE('',*,*,#53785,.T.);
#80330=ORIENTED_EDGE('',*,*,#53788,.T.);
#80331=ORIENTED_EDGE('',*,*,#53791,.T.);
#80332=ORIENTED_EDGE('',*,*,#53794,.T.);
#80333=ORIENTED_EDGE('',*,*,#53797,.T.);
#80334=ORIENTED_EDGE('',*,*,#53800,.T.);
#80335=ORIENTED_EDGE('',*,*,#53803,.T.);
#80336=ORIENTED_EDGE('',*,*,#53806,.T.);
#80337=ORIENTED_EDGE('',*,*,#53809,.T.);
#80338=ORIENTED_EDGE('',*,*,#53812,.T.);
#80339=ORIENTED_EDGE('',*,*,#53815,.T.);
#80340=ORIENTED_EDGE('',*,*,#53818,.T.);
#80341=ORIENTED_EDGE('',*,*,#53821,.T.);
#80342=ORIENTED_EDGE('',*,*,#53824,.T.);
#80343=ORIENTED_EDGE('',*,*,#53827,.T.);
#80344=ORIENTED_EDGE('',*,*,#53830,.T.);
#80345=ORIENTED_EDGE('',*,*,#53833,.T.);
#80346=ORIENTED_EDGE('',*,*,#55182,.T.);
#80347=ORIENTED_EDGE('',*,*,#53832,.T.);
#80348=ORIENTED_EDGE('',*,*,#55183,.T.);
#80349=ORIENTED_EDGE('',*,*,#53837,.F.);
#80350=ORIENTED_EDGE('',*,*,#55182,.F.);
#80351=ORIENTED_EDGE('',*,*,#53838,.F.);
#80352=ORIENTED_EDGE('',*,*,#55183,.F.);
#80353=ORIENTED_EDGE('',*,*,#53834,.F.);
#80354=ORIENTED_EDGE('',*,*,#53831,.F.);
#80355=ORIENTED_EDGE('',*,*,#53828,.F.);
#80356=ORIENTED_EDGE('',*,*,#53825,.F.);
#80357=ORIENTED_EDGE('',*,*,#53822,.F.);
#80358=ORIENTED_EDGE('',*,*,#53819,.F.);
#80359=ORIENTED_EDGE('',*,*,#53816,.F.);
#80360=ORIENTED_EDGE('',*,*,#53813,.F.);
#80361=ORIENTED_EDGE('',*,*,#53810,.F.);
#80362=ORIENTED_EDGE('',*,*,#53807,.F.);
#80363=ORIENTED_EDGE('',*,*,#53804,.F.);
#80364=ORIENTED_EDGE('',*,*,#53801,.F.);
#80365=ORIENTED_EDGE('',*,*,#53798,.F.);
#80366=ORIENTED_EDGE('',*,*,#53795,.F.);
#80367=ORIENTED_EDGE('',*,*,#53792,.F.);
#80368=ORIENTED_EDGE('',*,*,#53789,.F.);
#80369=ORIENTED_EDGE('',*,*,#53786,.F.);
#80370=ORIENTED_EDGE('',*,*,#53783,.F.);
#80371=ORIENTED_EDGE('',*,*,#53780,.F.);
#80372=ORIENTED_EDGE('',*,*,#53777,.F.);
#80373=ORIENTED_EDGE('',*,*,#53774,.F.);
#80374=ORIENTED_EDGE('',*,*,#53771,.F.);
#80375=ORIENTED_EDGE('',*,*,#53768,.F.);
#80376=ORIENTED_EDGE('',*,*,#53765,.F.);
#80377=ORIENTED_EDGE('',*,*,#53762,.F.);
#80378=ORIENTED_EDGE('',*,*,#53759,.F.);
#80379=ORIENTED_EDGE('',*,*,#53756,.F.);
#80380=ORIENTED_EDGE('',*,*,#53753,.F.);
#80381=ORIENTED_EDGE('',*,*,#53750,.F.);
#80382=ORIENTED_EDGE('',*,*,#53747,.F.);
#80383=ORIENTED_EDGE('',*,*,#53744,.F.);
#80384=ORIENTED_EDGE('',*,*,#53741,.F.);
#80385=ORIENTED_EDGE('',*,*,#53738,.F.);
#80386=ORIENTED_EDGE('',*,*,#53735,.F.);
#80387=ORIENTED_EDGE('',*,*,#53732,.F.);
#80388=ORIENTED_EDGE('',*,*,#53840,.T.);
#80389=ORIENTED_EDGE('',*,*,#54265,.T.);
#80390=ORIENTED_EDGE('',*,*,#53843,.T.);
#80391=ORIENTED_EDGE('',*,*,#53847,.T.);
#80392=ORIENTED_EDGE('',*,*,#53850,.T.);
#80393=ORIENTED_EDGE('',*,*,#53853,.T.);
#80394=ORIENTED_EDGE('',*,*,#53856,.T.);
#80395=ORIENTED_EDGE('',*,*,#53859,.T.);
#80396=ORIENTED_EDGE('',*,*,#53862,.T.);
#80397=ORIENTED_EDGE('',*,*,#53865,.T.);
#80398=ORIENTED_EDGE('',*,*,#53868,.T.);
#80399=ORIENTED_EDGE('',*,*,#53871,.T.);
#80400=ORIENTED_EDGE('',*,*,#53874,.T.);
#80401=ORIENTED_EDGE('',*,*,#53877,.T.);
#80402=ORIENTED_EDGE('',*,*,#53880,.T.);
#80403=ORIENTED_EDGE('',*,*,#53883,.T.);
#80404=ORIENTED_EDGE('',*,*,#53886,.T.);
#80405=ORIENTED_EDGE('',*,*,#53889,.T.);
#80406=ORIENTED_EDGE('',*,*,#53892,.T.);
#80407=ORIENTED_EDGE('',*,*,#53895,.T.);
#80408=ORIENTED_EDGE('',*,*,#53898,.T.);
#80409=ORIENTED_EDGE('',*,*,#53901,.T.);
#80410=ORIENTED_EDGE('',*,*,#53904,.T.);
#80411=ORIENTED_EDGE('',*,*,#53907,.T.);
#80412=ORIENTED_EDGE('',*,*,#53910,.T.);
#80413=ORIENTED_EDGE('',*,*,#53913,.T.);
#80414=ORIENTED_EDGE('',*,*,#53916,.T.);
#80415=ORIENTED_EDGE('',*,*,#53919,.T.);
#80416=ORIENTED_EDGE('',*,*,#53922,.T.);
#80417=ORIENTED_EDGE('',*,*,#53925,.T.);
#80418=ORIENTED_EDGE('',*,*,#53928,.T.);
#80419=ORIENTED_EDGE('',*,*,#53931,.T.);
#80420=ORIENTED_EDGE('',*,*,#53934,.T.);
#80421=ORIENTED_EDGE('',*,*,#53937,.T.);
#80422=ORIENTED_EDGE('',*,*,#53941,.T.);
#80423=ORIENTED_EDGE('',*,*,#53944,.T.);
#80424=ORIENTED_EDGE('',*,*,#54261,.T.);
#80425=ORIENTED_EDGE('',*,*,#53949,.T.);
#80426=ORIENTED_EDGE('',*,*,#54268,.F.);
#80427=ORIENTED_EDGE('',*,*,#55184,.T.);
#80428=ORIENTED_EDGE('',*,*,#55185,.T.);
#80429=ORIENTED_EDGE('',*,*,#54256,.T.);
#80430=ORIENTED_EDGE('',*,*,#55186,.T.);
#80431=ORIENTED_EDGE('',*,*,#55187,.F.);
#80432=ORIENTED_EDGE('',*,*,#55146,.F.);
#80433=ORIENTED_EDGE('',*,*,#55188,.F.);
#80434=ORIENTED_EDGE('',*,*,#55186,.F.);
#80435=ORIENTED_EDGE('',*,*,#55189,.F.);
#80436=ORIENTED_EDGE('',*,*,#55147,.F.);
#80437=ORIENTED_EDGE('',*,*,#55190,.F.);
#80438=ORIENTED_EDGE('',*,*,#54791,.F.);
#80439=ORIENTED_EDGE('',*,*,#55188,.T.);
#80440=ORIENTED_EDGE('',*,*,#55143,.F.);
#80441=ORIENTED_EDGE('',*,*,#55142,.F.);
#80442=ORIENTED_EDGE('',*,*,#55191,.F.);
#80443=ORIENTED_EDGE('',*,*,#55184,.F.);
#80444=ORIENTED_EDGE('',*,*,#55190,.T.);
#80445=ORIENTED_EDGE('',*,*,#55187,.T.);
#80446=ORIENTED_EDGE('',*,*,#54260,.F.);
#80447=ORIENTED_EDGE('',*,*,#54792,.T.);
#80448=ORIENTED_EDGE('',*,*,#55189,.T.);
#80449=ORIENTED_EDGE('',*,*,#55168,.F.);
#80450=ORIENTED_EDGE('',*,*,#55192,.F.);
#80451=ORIENTED_EDGE('',*,*,#55144,.F.);
#80452=ORIENTED_EDGE('',*,*,#55191,.T.);
#80453=ORIENTED_EDGE('',*,*,#55151,.F.);
#80454=ORIENTED_EDGE('',*,*,#55193,.F.);
#80455=ORIENTED_EDGE('',*,*,#55185,.F.);
#80456=ORIENTED_EDGE('',*,*,#55192,.T.);
#80457=ORIENTED_EDGE('',*,*,#54286,.F.);
#80458=ORIENTED_EDGE('',*,*,#55194,.F.);
#80459=ORIENTED_EDGE('',*,*,#55145,.F.);
#80460=ORIENTED_EDGE('',*,*,#54257,.T.);
#80461=ORIENTED_EDGE('',*,*,#55193,.T.);
#80462=ORIENTED_EDGE('',*,*,#55195,.F.);
#80463=ORIENTED_EDGE('',*,*,#54794,.T.);
#80464=ORIENTED_EDGE('',*,*,#55194,.T.);
#80465=ORIENTED_EDGE('',*,*,#54285,.F.);
#80466=ORIENTED_EDGE('',*,*,#54597,.F.);
#80467=ORIENTED_EDGE('',*,*,#55196,.F.);
#80468=ORIENTED_EDGE('',*,*,#55140,.F.);
#80469=ORIENTED_EDGE('',*,*,#55139,.F.);
#80470=ORIENTED_EDGE('',*,*,#55195,.T.);
#80471=ORIENTED_EDGE('',*,*,#55150,.F.);
#80472=ORIENTED_EDGE('',*,*,#55197,.F.);
#80473=ORIENTED_EDGE('',*,*,#54795,.F.);
#80474=ORIENTED_EDGE('',*,*,#55196,.T.);
#80475=ORIENTED_EDGE('',*,*,#54596,.F.);
#80476=ORIENTED_EDGE('',*,*,#55198,.F.);
#80477=ORIENTED_EDGE('',*,*,#55148,.F.);
#80478=ORIENTED_EDGE('',*,*,#55197,.T.);
#80479=ORIENTED_EDGE('',*,*,#55149,.F.);
#80480=ORIENTED_EDGE('',*,*,#55198,.T.);
#80481=ORIENTED_EDGE('',*,*,#55135,.F.);
#80482=ORIENTED_EDGE('',*,*,#55199,.T.);
#80483=ORIENTED_EDGE('',*,*,#55200,.T.);
#80484=ORIENTED_EDGE('',*,*,#55201,.T.);
#80485=ORIENTED_EDGE('',*,*,#55202,.T.);
#80486=ORIENTED_EDGE('',*,*,#55203,.T.);
#80487=ORIENTED_EDGE('',*,*,#55204,.T.);
#80488=ORIENTED_EDGE('',*,*,#55205,.T.);
#80489=ORIENTED_EDGE('',*,*,#55206,.F.);
#80490=ORIENTED_EDGE('',*,*,#55207,.T.);
#80491=ORIENTED_EDGE('',*,*,#55208,.T.);
#80492=ORIENTED_EDGE('',*,*,#55206,.T.);
#80493=ORIENTED_EDGE('',*,*,#55209,.T.);
#80494=ORIENTED_EDGE('',*,*,#55210,.T.);
#80495=ORIENTED_EDGE('',*,*,#55199,.F.);
#80496=ORIENTED_EDGE('',*,*,#55211,.T.);
#80497=ORIENTED_EDGE('',*,*,#55212,.T.);
#80498=ORIENTED_EDGE('',*,*,#55213,.F.);
#80499=ORIENTED_EDGE('',*,*,#55207,.F.);
#80500=ORIENTED_EDGE('',*,*,#55214,.F.);
#80501=ORIENTED_EDGE('',*,*,#55215,.F.);
#80502=ORIENTED_EDGE('',*,*,#55214,.T.);
#80503=ORIENTED_EDGE('',*,*,#55212,.F.);
#80504=ORIENTED_EDGE('',*,*,#55211,.F.);
#80505=ORIENTED_EDGE('',*,*,#55216,.F.);
#80506=ORIENTED_EDGE('',*,*,#55217,.F.);
#80507=ORIENTED_EDGE('',*,*,#55216,.T.);
#80508=ORIENTED_EDGE('',*,*,#55203,.F.);
#80509=ORIENTED_EDGE('',*,*,#55218,.F.);
#80510=ORIENTED_EDGE('',*,*,#55219,.F.);
#80511=ORIENTED_EDGE('',*,*,#55220,.T.);
#80512=ORIENTED_EDGE('',*,*,#55213,.T.);
#80513=ORIENTED_EDGE('',*,*,#54255,.F.);
#80514=ORIENTED_EDGE('',*,*,#54787,.T.);
#80515=ORIENTED_EDGE('',*,*,#55221,.F.);
#80516=ORIENTED_EDGE('',*,*,#55208,.F.);
#80517=ORIENTED_EDGE('',*,*,#55220,.F.);
#80518=ORIENTED_EDGE('',*,*,#54786,.F.);
#80519=ORIENTED_EDGE('',*,*,#55221,.T.);
#80520=ORIENTED_EDGE('',*,*,#55137,.F.);
#80521=ORIENTED_EDGE('',*,*,#55222,.F.);
#80522=ORIENTED_EDGE('',*,*,#55204,.F.);
#80523=ORIENTED_EDGE('',*,*,#55222,.T.);
#80524=ORIENTED_EDGE('',*,*,#54290,.F.);
#80525=ORIENTED_EDGE('',*,*,#55223,.F.);
#80526=ORIENTED_EDGE('',*,*,#55205,.F.);
#80527=ORIENTED_EDGE('',*,*,#55223,.T.);
#80528=ORIENTED_EDGE('',*,*,#54289,.F.);
#80529=ORIENTED_EDGE('',*,*,#55224,.F.);
#80530=ORIENTED_EDGE('',*,*,#55210,.F.);
#80531=ORIENTED_EDGE('',*,*,#55209,.F.);
#80532=ORIENTED_EDGE('',*,*,#55224,.T.);
#80533=ORIENTED_EDGE('',*,*,#54288,.F.);
#80534=ORIENTED_EDGE('',*,*,#55225,.F.);
#80535=ORIENTED_EDGE('',*,*,#55200,.F.);
#80536=ORIENTED_EDGE('',*,*,#55226,.T.);
#80537=ORIENTED_EDGE('',*,*,#55201,.F.);
#80538=ORIENTED_EDGE('',*,*,#55225,.T.);
#80539=ORIENTED_EDGE('',*,*,#55167,.F.);
#80540=ORIENTED_EDGE('',*,*,#55227,.T.);
#80541=ORIENTED_EDGE('',*,*,#55202,.F.);
#80542=ORIENTED_EDGE('',*,*,#55226,.F.);
#80543=ORIENTED_EDGE('',*,*,#54789,.F.);
#80544=ORIENTED_EDGE('',*,*,#54253,.T.);
#80545=ORIENTED_EDGE('',*,*,#55218,.T.);
#80546=ORIENTED_EDGE('',*,*,#55227,.F.);
#80547=ORIENTED_EDGE('',*,*,#54788,.T.);
#80548=ORIENTED_EDGE('',*,*,#55217,.T.);
#80549=ORIENTED_EDGE('',*,*,#55219,.T.);
#80550=ORIENTED_EDGE('',*,*,#54252,.T.);
#80551=ORIENTED_EDGE('',*,*,#55215,.T.);
#80552=ORIENTED_EDGE('',*,*,#55228,.T.);
#80553=ORIENTED_EDGE('',*,*,#55229,.T.);
#80554=ORIENTED_EDGE('',*,*,#55230,.T.);
#80555=ORIENTED_EDGE('',*,*,#55231,.T.);
#80556=ORIENTED_EDGE('',*,*,#55232,.T.);
#80557=ORIENTED_EDGE('',*,*,#55233,.T.);
#80558=ORIENTED_EDGE('',*,*,#55234,.T.);
#80559=ORIENTED_EDGE('',*,*,#55235,.F.);
#80560=ORIENTED_EDGE('',*,*,#55236,.T.);
#80561=ORIENTED_EDGE('',*,*,#55237,.T.);
#80562=ORIENTED_EDGE('',*,*,#55235,.T.);
#80563=ORIENTED_EDGE('',*,*,#55238,.T.);
#80564=ORIENTED_EDGE('',*,*,#55239,.T.);
#80565=ORIENTED_EDGE('',*,*,#55228,.F.);
#80566=ORIENTED_EDGE('',*,*,#55240,.T.);
#80567=ORIENTED_EDGE('',*,*,#55241,.T.);
#80568=ORIENTED_EDGE('',*,*,#55242,.F.);
#80569=ORIENTED_EDGE('',*,*,#55236,.F.);
#80570=ORIENTED_EDGE('',*,*,#55243,.F.);
#80571=ORIENTED_EDGE('',*,*,#55244,.F.);
#80572=ORIENTED_EDGE('',*,*,#55243,.T.);
#80573=ORIENTED_EDGE('',*,*,#55241,.F.);
#80574=ORIENTED_EDGE('',*,*,#55240,.F.);
#80575=ORIENTED_EDGE('',*,*,#55245,.F.);
#80576=ORIENTED_EDGE('',*,*,#55246,.F.);
#80577=ORIENTED_EDGE('',*,*,#55245,.T.);
#80578=ORIENTED_EDGE('',*,*,#55232,.F.);
#80579=ORIENTED_EDGE('',*,*,#55247,.F.);
#80580=ORIENTED_EDGE('',*,*,#55248,.F.);
#80581=ORIENTED_EDGE('',*,*,#55249,.T.);
#80582=ORIENTED_EDGE('',*,*,#55242,.T.);
#80583=ORIENTED_EDGE('',*,*,#54251,.F.);
#80584=ORIENTED_EDGE('',*,*,#54798,.T.);
#80585=ORIENTED_EDGE('',*,*,#55250,.F.);
#80586=ORIENTED_EDGE('',*,*,#55237,.F.);
#80587=ORIENTED_EDGE('',*,*,#55249,.F.);
#80588=ORIENTED_EDGE('',*,*,#54797,.F.);
#80589=ORIENTED_EDGE('',*,*,#55250,.T.);
#80590=ORIENTED_EDGE('',*,*,#55134,.F.);
#80591=ORIENTED_EDGE('',*,*,#55251,.F.);
#80592=ORIENTED_EDGE('',*,*,#55233,.F.);
#80593=ORIENTED_EDGE('',*,*,#55251,.T.);
#80594=ORIENTED_EDGE('',*,*,#54594,.F.);
#80595=ORIENTED_EDGE('',*,*,#55252,.F.);
#80596=ORIENTED_EDGE('',*,*,#55234,.F.);
#80597=ORIENTED_EDGE('',*,*,#55252,.T.);
#80598=ORIENTED_EDGE('',*,*,#54593,.F.);
#80599=ORIENTED_EDGE('',*,*,#55253,.F.);
#80600=ORIENTED_EDGE('',*,*,#55239,.F.);
#80601=ORIENTED_EDGE('',*,*,#55238,.F.);
#80602=ORIENTED_EDGE('',*,*,#55253,.T.);
#80603=ORIENTED_EDGE('',*,*,#54592,.F.);
#80604=ORIENTED_EDGE('',*,*,#55254,.F.);
#80605=ORIENTED_EDGE('',*,*,#55229,.F.);
#80606=ORIENTED_EDGE('',*,*,#55255,.T.);
#80607=ORIENTED_EDGE('',*,*,#55230,.F.);
#80608=ORIENTED_EDGE('',*,*,#55254,.T.);
#80609=ORIENTED_EDGE('',*,*,#55133,.F.);
#80610=ORIENTED_EDGE('',*,*,#55256,.T.);
#80611=ORIENTED_EDGE('',*,*,#55231,.F.);
#80612=ORIENTED_EDGE('',*,*,#55255,.F.);
#80613=ORIENTED_EDGE('',*,*,#54800,.F.);
#80614=ORIENTED_EDGE('',*,*,#54249,.T.);
#80615=ORIENTED_EDGE('',*,*,#55247,.T.);
#80616=ORIENTED_EDGE('',*,*,#55256,.F.);
#80617=ORIENTED_EDGE('',*,*,#54799,.T.);
#80618=ORIENTED_EDGE('',*,*,#55246,.T.);
#80619=ORIENTED_EDGE('',*,*,#55248,.T.);
#80620=ORIENTED_EDGE('',*,*,#54248,.T.);
#80621=ORIENTED_EDGE('',*,*,#55244,.T.);
#80622=ORIENTED_EDGE('',*,*,#55257,.T.);
#80623=ORIENTED_EDGE('',*,*,#55258,.T.);
#80624=ORIENTED_EDGE('',*,*,#55259,.T.);
#80625=ORIENTED_EDGE('',*,*,#55260,.T.);
#80626=ORIENTED_EDGE('',*,*,#55261,.T.);
#80627=ORIENTED_EDGE('',*,*,#55262,.T.);
#80628=ORIENTED_EDGE('',*,*,#55263,.T.);
#80629=ORIENTED_EDGE('',*,*,#55264,.F.);
#80630=ORIENTED_EDGE('',*,*,#55265,.T.);
#80631=ORIENTED_EDGE('',*,*,#55266,.T.);
#80632=ORIENTED_EDGE('',*,*,#55264,.T.);
#80633=ORIENTED_EDGE('',*,*,#55267,.T.);
#80634=ORIENTED_EDGE('',*,*,#55268,.T.);
#80635=ORIENTED_EDGE('',*,*,#55257,.F.);
#80636=ORIENTED_EDGE('',*,*,#55269,.T.);
#80637=ORIENTED_EDGE('',*,*,#55270,.T.);
#80638=ORIENTED_EDGE('',*,*,#55271,.F.);
#80639=ORIENTED_EDGE('',*,*,#55265,.F.);
#80640=ORIENTED_EDGE('',*,*,#55272,.F.);
#80641=ORIENTED_EDGE('',*,*,#55273,.F.);
#80642=ORIENTED_EDGE('',*,*,#55272,.T.);
#80643=ORIENTED_EDGE('',*,*,#55270,.F.);
#80644=ORIENTED_EDGE('',*,*,#55269,.F.);
#80645=ORIENTED_EDGE('',*,*,#55274,.F.);
#80646=ORIENTED_EDGE('',*,*,#55275,.F.);
#80647=ORIENTED_EDGE('',*,*,#55274,.T.);
#80648=ORIENTED_EDGE('',*,*,#55261,.F.);
#80649=ORIENTED_EDGE('',*,*,#55276,.F.);
#80650=ORIENTED_EDGE('',*,*,#55277,.F.);
#80651=ORIENTED_EDGE('',*,*,#55278,.T.);
#80652=ORIENTED_EDGE('',*,*,#55271,.T.);
#80653=ORIENTED_EDGE('',*,*,#54247,.F.);
#80654=ORIENTED_EDGE('',*,*,#54803,.T.);
#80655=ORIENTED_EDGE('',*,*,#55279,.F.);
#80656=ORIENTED_EDGE('',*,*,#55266,.F.);
#80657=ORIENTED_EDGE('',*,*,#55278,.F.);
#80658=ORIENTED_EDGE('',*,*,#54802,.F.);
#80659=ORIENTED_EDGE('',*,*,#55279,.T.);
#80660=ORIENTED_EDGE('',*,*,#55132,.F.);
#80661=ORIENTED_EDGE('',*,*,#55280,.F.);
#80662=ORIENTED_EDGE('',*,*,#55262,.F.);
#80663=ORIENTED_EDGE('',*,*,#55280,.T.);
#80664=ORIENTED_EDGE('',*,*,#54590,.F.);
#80665=ORIENTED_EDGE('',*,*,#55281,.F.);
#80666=ORIENTED_EDGE('',*,*,#55263,.F.);
#80667=ORIENTED_EDGE('',*,*,#55281,.T.);
#80668=ORIENTED_EDGE('',*,*,#54589,.F.);
#80669=ORIENTED_EDGE('',*,*,#55282,.F.);
#80670=ORIENTED_EDGE('',*,*,#55268,.F.);
#80671=ORIENTED_EDGE('',*,*,#55267,.F.);
#80672=ORIENTED_EDGE('',*,*,#55282,.T.);
#80673=ORIENTED_EDGE('',*,*,#54588,.F.);
#80674=ORIENTED_EDGE('',*,*,#55283,.F.);
#80675=ORIENTED_EDGE('',*,*,#55258,.F.);
#80676=ORIENTED_EDGE('',*,*,#55284,.T.);
#80677=ORIENTED_EDGE('',*,*,#55259,.F.);
#80678=ORIENTED_EDGE('',*,*,#55283,.T.);
#80679=ORIENTED_EDGE('',*,*,#55131,.F.);
#80680=ORIENTED_EDGE('',*,*,#55285,.T.);
#80681=ORIENTED_EDGE('',*,*,#55260,.F.);
#80682=ORIENTED_EDGE('',*,*,#55284,.F.);
#80683=ORIENTED_EDGE('',*,*,#54805,.F.);
#80684=ORIENTED_EDGE('',*,*,#54245,.T.);
#80685=ORIENTED_EDGE('',*,*,#55276,.T.);
#80686=ORIENTED_EDGE('',*,*,#55285,.F.);
#80687=ORIENTED_EDGE('',*,*,#54804,.T.);
#80688=ORIENTED_EDGE('',*,*,#55275,.T.);
#80689=ORIENTED_EDGE('',*,*,#55277,.T.);
#80690=ORIENTED_EDGE('',*,*,#54244,.T.);
#80691=ORIENTED_EDGE('',*,*,#55273,.T.);
#80692=ORIENTED_EDGE('',*,*,#55286,.T.);
#80693=ORIENTED_EDGE('',*,*,#55287,.T.);
#80694=ORIENTED_EDGE('',*,*,#55288,.T.);
#80695=ORIENTED_EDGE('',*,*,#55289,.T.);
#80696=ORIENTED_EDGE('',*,*,#55290,.T.);
#80697=ORIENTED_EDGE('',*,*,#55291,.T.);
#80698=ORIENTED_EDGE('',*,*,#55292,.T.);
#80699=ORIENTED_EDGE('',*,*,#55293,.F.);
#80700=ORIENTED_EDGE('',*,*,#55294,.T.);
#80701=ORIENTED_EDGE('',*,*,#55295,.T.);
#80702=ORIENTED_EDGE('',*,*,#55293,.T.);
#80703=ORIENTED_EDGE('',*,*,#55296,.T.);
#80704=ORIENTED_EDGE('',*,*,#55297,.T.);
#80705=ORIENTED_EDGE('',*,*,#55286,.F.);
#80706=ORIENTED_EDGE('',*,*,#55298,.T.);
#80707=ORIENTED_EDGE('',*,*,#55299,.T.);
#80708=ORIENTED_EDGE('',*,*,#55300,.F.);
#80709=ORIENTED_EDGE('',*,*,#55294,.F.);
#80710=ORIENTED_EDGE('',*,*,#55301,.F.);
#80711=ORIENTED_EDGE('',*,*,#55302,.F.);
#80712=ORIENTED_EDGE('',*,*,#55301,.T.);
#80713=ORIENTED_EDGE('',*,*,#55299,.F.);
#80714=ORIENTED_EDGE('',*,*,#55298,.F.);
#80715=ORIENTED_EDGE('',*,*,#55303,.F.);
#80716=ORIENTED_EDGE('',*,*,#55304,.F.);
#80717=ORIENTED_EDGE('',*,*,#55303,.T.);
#80718=ORIENTED_EDGE('',*,*,#55290,.F.);
#80719=ORIENTED_EDGE('',*,*,#55305,.F.);
#80720=ORIENTED_EDGE('',*,*,#55306,.F.);
#80721=ORIENTED_EDGE('',*,*,#55307,.T.);
#80722=ORIENTED_EDGE('',*,*,#55300,.T.);
#80723=ORIENTED_EDGE('',*,*,#54243,.F.);
#80724=ORIENTED_EDGE('',*,*,#54808,.T.);
#80725=ORIENTED_EDGE('',*,*,#55308,.F.);
#80726=ORIENTED_EDGE('',*,*,#55295,.F.);
#80727=ORIENTED_EDGE('',*,*,#55307,.F.);
#80728=ORIENTED_EDGE('',*,*,#54807,.F.);
#80729=ORIENTED_EDGE('',*,*,#55308,.T.);
#80730=ORIENTED_EDGE('',*,*,#55130,.F.);
#80731=ORIENTED_EDGE('',*,*,#55309,.F.);
#80732=ORIENTED_EDGE('',*,*,#55291,.F.);
#80733=ORIENTED_EDGE('',*,*,#55309,.T.);
#80734=ORIENTED_EDGE('',*,*,#54586,.F.);
#80735=ORIENTED_EDGE('',*,*,#55310,.F.);
#80736=ORIENTED_EDGE('',*,*,#55292,.F.);
#80737=ORIENTED_EDGE('',*,*,#55310,.T.);
#80738=ORIENTED_EDGE('',*,*,#54585,.F.);
#80739=ORIENTED_EDGE('',*,*,#55311,.F.);
#80740=ORIENTED_EDGE('',*,*,#55297,.F.);
#80741=ORIENTED_EDGE('',*,*,#55296,.F.);
#80742=ORIENTED_EDGE('',*,*,#55311,.T.);
#80743=ORIENTED_EDGE('',*,*,#54584,.F.);
#80744=ORIENTED_EDGE('',*,*,#55312,.F.);
#80745=ORIENTED_EDGE('',*,*,#55287,.F.);
#80746=ORIENTED_EDGE('',*,*,#55313,.T.);
#80747=ORIENTED_EDGE('',*,*,#55288,.F.);
#80748=ORIENTED_EDGE('',*,*,#55312,.T.);
#80749=ORIENTED_EDGE('',*,*,#55129,.F.);
#80750=ORIENTED_EDGE('',*,*,#55314,.T.);
#80751=ORIENTED_EDGE('',*,*,#55289,.F.);
#80752=ORIENTED_EDGE('',*,*,#55313,.F.);
#80753=ORIENTED_EDGE('',*,*,#54810,.F.);
#80754=ORIENTED_EDGE('',*,*,#54241,.T.);
#80755=ORIENTED_EDGE('',*,*,#55305,.T.);
#80756=ORIENTED_EDGE('',*,*,#55314,.F.);
#80757=ORIENTED_EDGE('',*,*,#54809,.T.);
#80758=ORIENTED_EDGE('',*,*,#55304,.T.);
#80759=ORIENTED_EDGE('',*,*,#55306,.T.);
#80760=ORIENTED_EDGE('',*,*,#54240,.T.);
#80761=ORIENTED_EDGE('',*,*,#55302,.T.);
#80762=ORIENTED_EDGE('',*,*,#55315,.T.);
#80763=ORIENTED_EDGE('',*,*,#55316,.T.);
#80764=ORIENTED_EDGE('',*,*,#55317,.T.);
#80765=ORIENTED_EDGE('',*,*,#55318,.T.);
#80766=ORIENTED_EDGE('',*,*,#55319,.T.);
#80767=ORIENTED_EDGE('',*,*,#55320,.T.);
#80768=ORIENTED_EDGE('',*,*,#55321,.T.);
#80769=ORIENTED_EDGE('',*,*,#55322,.F.);
#80770=ORIENTED_EDGE('',*,*,#55323,.T.);
#80771=ORIENTED_EDGE('',*,*,#55324,.T.);
#80772=ORIENTED_EDGE('',*,*,#55322,.T.);
#80773=ORIENTED_EDGE('',*,*,#55325,.T.);
#80774=ORIENTED_EDGE('',*,*,#55326,.T.);
#80775=ORIENTED_EDGE('',*,*,#55315,.F.);
#80776=ORIENTED_EDGE('',*,*,#55327,.T.);
#80777=ORIENTED_EDGE('',*,*,#55328,.T.);
#80778=ORIENTED_EDGE('',*,*,#55329,.F.);
#80779=ORIENTED_EDGE('',*,*,#55323,.F.);
#80780=ORIENTED_EDGE('',*,*,#55330,.F.);
#80781=ORIENTED_EDGE('',*,*,#55331,.F.);
#80782=ORIENTED_EDGE('',*,*,#55330,.T.);
#80783=ORIENTED_EDGE('',*,*,#55328,.F.);
#80784=ORIENTED_EDGE('',*,*,#55327,.F.);
#80785=ORIENTED_EDGE('',*,*,#55332,.F.);
#80786=ORIENTED_EDGE('',*,*,#55333,.F.);
#80787=ORIENTED_EDGE('',*,*,#55332,.T.);
#80788=ORIENTED_EDGE('',*,*,#55319,.F.);
#80789=ORIENTED_EDGE('',*,*,#55334,.F.);
#80790=ORIENTED_EDGE('',*,*,#55335,.F.);
#80791=ORIENTED_EDGE('',*,*,#55336,.T.);
#80792=ORIENTED_EDGE('',*,*,#55329,.T.);
#80793=ORIENTED_EDGE('',*,*,#54239,.F.);
#80794=ORIENTED_EDGE('',*,*,#54813,.T.);
#80795=ORIENTED_EDGE('',*,*,#55337,.F.);
#80796=ORIENTED_EDGE('',*,*,#55324,.F.);
#80797=ORIENTED_EDGE('',*,*,#55336,.F.);
#80798=ORIENTED_EDGE('',*,*,#54812,.F.);
#80799=ORIENTED_EDGE('',*,*,#55337,.T.);
#80800=ORIENTED_EDGE('',*,*,#55128,.F.);
#80801=ORIENTED_EDGE('',*,*,#55338,.F.);
#80802=ORIENTED_EDGE('',*,*,#55320,.F.);
#80803=ORIENTED_EDGE('',*,*,#55338,.T.);
#80804=ORIENTED_EDGE('',*,*,#54582,.F.);
#80805=ORIENTED_EDGE('',*,*,#55339,.F.);
#80806=ORIENTED_EDGE('',*,*,#55321,.F.);
#80807=ORIENTED_EDGE('',*,*,#55339,.T.);
#80808=ORIENTED_EDGE('',*,*,#54581,.F.);
#80809=ORIENTED_EDGE('',*,*,#55340,.F.);
#80810=ORIENTED_EDGE('',*,*,#55326,.F.);
#80811=ORIENTED_EDGE('',*,*,#55325,.F.);
#80812=ORIENTED_EDGE('',*,*,#55340,.T.);
#80813=ORIENTED_EDGE('',*,*,#54580,.F.);
#80814=ORIENTED_EDGE('',*,*,#55341,.F.);
#80815=ORIENTED_EDGE('',*,*,#55316,.F.);
#80816=ORIENTED_EDGE('',*,*,#55342,.T.);
#80817=ORIENTED_EDGE('',*,*,#55317,.F.);
#80818=ORIENTED_EDGE('',*,*,#55341,.T.);
#80819=ORIENTED_EDGE('',*,*,#55127,.F.);
#80820=ORIENTED_EDGE('',*,*,#55343,.T.);
#80821=ORIENTED_EDGE('',*,*,#55318,.F.);
#80822=ORIENTED_EDGE('',*,*,#55342,.F.);
#80823=ORIENTED_EDGE('',*,*,#54815,.F.);
#80824=ORIENTED_EDGE('',*,*,#54237,.T.);
#80825=ORIENTED_EDGE('',*,*,#55334,.T.);
#80826=ORIENTED_EDGE('',*,*,#55343,.F.);
#80827=ORIENTED_EDGE('',*,*,#54814,.T.);
#80828=ORIENTED_EDGE('',*,*,#55333,.T.);
#80829=ORIENTED_EDGE('',*,*,#55335,.T.);
#80830=ORIENTED_EDGE('',*,*,#54236,.T.);
#80831=ORIENTED_EDGE('',*,*,#55331,.T.);
#80832=ORIENTED_EDGE('',*,*,#55344,.T.);
#80833=ORIENTED_EDGE('',*,*,#55345,.T.);
#80834=ORIENTED_EDGE('',*,*,#55346,.T.);
#80835=ORIENTED_EDGE('',*,*,#55347,.T.);
#80836=ORIENTED_EDGE('',*,*,#55348,.T.);
#80837=ORIENTED_EDGE('',*,*,#55349,.T.);
#80838=ORIENTED_EDGE('',*,*,#55350,.T.);
#80839=ORIENTED_EDGE('',*,*,#55351,.F.);
#80840=ORIENTED_EDGE('',*,*,#55352,.T.);
#80841=ORIENTED_EDGE('',*,*,#55353,.T.);
#80842=ORIENTED_EDGE('',*,*,#55351,.T.);
#80843=ORIENTED_EDGE('',*,*,#55354,.T.);
#80844=ORIENTED_EDGE('',*,*,#55355,.T.);
#80845=ORIENTED_EDGE('',*,*,#55344,.F.);
#80846=ORIENTED_EDGE('',*,*,#55356,.T.);
#80847=ORIENTED_EDGE('',*,*,#55357,.T.);
#80848=ORIENTED_EDGE('',*,*,#55358,.F.);
#80849=ORIENTED_EDGE('',*,*,#55352,.F.);
#80850=ORIENTED_EDGE('',*,*,#55359,.F.);
#80851=ORIENTED_EDGE('',*,*,#55360,.F.);
#80852=ORIENTED_EDGE('',*,*,#55359,.T.);
#80853=ORIENTED_EDGE('',*,*,#55357,.F.);
#80854=ORIENTED_EDGE('',*,*,#55356,.F.);
#80855=ORIENTED_EDGE('',*,*,#55361,.F.);
#80856=ORIENTED_EDGE('',*,*,#55362,.F.);
#80857=ORIENTED_EDGE('',*,*,#55361,.T.);
#80858=ORIENTED_EDGE('',*,*,#55348,.F.);
#80859=ORIENTED_EDGE('',*,*,#55363,.F.);
#80860=ORIENTED_EDGE('',*,*,#55364,.F.);
#80861=ORIENTED_EDGE('',*,*,#55365,.T.);
#80862=ORIENTED_EDGE('',*,*,#55358,.T.);
#80863=ORIENTED_EDGE('',*,*,#54235,.F.);
#80864=ORIENTED_EDGE('',*,*,#54818,.T.);
#80865=ORIENTED_EDGE('',*,*,#55366,.F.);
#80866=ORIENTED_EDGE('',*,*,#55353,.F.);
#80867=ORIENTED_EDGE('',*,*,#55365,.F.);
#80868=ORIENTED_EDGE('',*,*,#54817,.F.);
#80869=ORIENTED_EDGE('',*,*,#55366,.T.);
#80870=ORIENTED_EDGE('',*,*,#55126,.F.);
#80871=ORIENTED_EDGE('',*,*,#55367,.F.);
#80872=ORIENTED_EDGE('',*,*,#55349,.F.);
#80873=ORIENTED_EDGE('',*,*,#55367,.T.);
#80874=ORIENTED_EDGE('',*,*,#54578,.F.);
#80875=ORIENTED_EDGE('',*,*,#55368,.F.);
#80876=ORIENTED_EDGE('',*,*,#55350,.F.);
#80877=ORIENTED_EDGE('',*,*,#55368,.T.);
#80878=ORIENTED_EDGE('',*,*,#54577,.F.);
#80879=ORIENTED_EDGE('',*,*,#55369,.F.);
#80880=ORIENTED_EDGE('',*,*,#55355,.F.);
#80881=ORIENTED_EDGE('',*,*,#55354,.F.);
#80882=ORIENTED_EDGE('',*,*,#55369,.T.);
#80883=ORIENTED_EDGE('',*,*,#54576,.F.);
#80884=ORIENTED_EDGE('',*,*,#55370,.F.);
#80885=ORIENTED_EDGE('',*,*,#55345,.F.);
#80886=ORIENTED_EDGE('',*,*,#55371,.T.);
#80887=ORIENTED_EDGE('',*,*,#55346,.F.);
#80888=ORIENTED_EDGE('',*,*,#55370,.T.);
#80889=ORIENTED_EDGE('',*,*,#55125,.F.);
#80890=ORIENTED_EDGE('',*,*,#55372,.T.);
#80891=ORIENTED_EDGE('',*,*,#55347,.F.);
#80892=ORIENTED_EDGE('',*,*,#55371,.F.);
#80893=ORIENTED_EDGE('',*,*,#54820,.F.);
#80894=ORIENTED_EDGE('',*,*,#54233,.T.);
#80895=ORIENTED_EDGE('',*,*,#55363,.T.);
#80896=ORIENTED_EDGE('',*,*,#55372,.F.);
#80897=ORIENTED_EDGE('',*,*,#54819,.T.);
#80898=ORIENTED_EDGE('',*,*,#55362,.T.);
#80899=ORIENTED_EDGE('',*,*,#55364,.T.);
#80900=ORIENTED_EDGE('',*,*,#54232,.T.);
#80901=ORIENTED_EDGE('',*,*,#55360,.T.);
#80902=ORIENTED_EDGE('',*,*,#55373,.T.);
#80903=ORIENTED_EDGE('',*,*,#55374,.T.);
#80904=ORIENTED_EDGE('',*,*,#55375,.T.);
#80905=ORIENTED_EDGE('',*,*,#55376,.T.);
#80906=ORIENTED_EDGE('',*,*,#55377,.T.);
#80907=ORIENTED_EDGE('',*,*,#55378,.T.);
#80908=ORIENTED_EDGE('',*,*,#55379,.T.);
#80909=ORIENTED_EDGE('',*,*,#55380,.F.);
#80910=ORIENTED_EDGE('',*,*,#55381,.T.);
#80911=ORIENTED_EDGE('',*,*,#55382,.T.);
#80912=ORIENTED_EDGE('',*,*,#55380,.T.);
#80913=ORIENTED_EDGE('',*,*,#55383,.T.);
#80914=ORIENTED_EDGE('',*,*,#55384,.T.);
#80915=ORIENTED_EDGE('',*,*,#55373,.F.);
#80916=ORIENTED_EDGE('',*,*,#55385,.T.);
#80917=ORIENTED_EDGE('',*,*,#55386,.T.);
#80918=ORIENTED_EDGE('',*,*,#55387,.F.);
#80919=ORIENTED_EDGE('',*,*,#55381,.F.);
#80920=ORIENTED_EDGE('',*,*,#55388,.F.);
#80921=ORIENTED_EDGE('',*,*,#55389,.F.);
#80922=ORIENTED_EDGE('',*,*,#55388,.T.);
#80923=ORIENTED_EDGE('',*,*,#55386,.F.);
#80924=ORIENTED_EDGE('',*,*,#55385,.F.);
#80925=ORIENTED_EDGE('',*,*,#55390,.F.);
#80926=ORIENTED_EDGE('',*,*,#55391,.F.);
#80927=ORIENTED_EDGE('',*,*,#55390,.T.);
#80928=ORIENTED_EDGE('',*,*,#55377,.F.);
#80929=ORIENTED_EDGE('',*,*,#55392,.F.);
#80930=ORIENTED_EDGE('',*,*,#55393,.F.);
#80931=ORIENTED_EDGE('',*,*,#55394,.T.);
#80932=ORIENTED_EDGE('',*,*,#55387,.T.);
#80933=ORIENTED_EDGE('',*,*,#54231,.F.);
#80934=ORIENTED_EDGE('',*,*,#54823,.T.);
#80935=ORIENTED_EDGE('',*,*,#55395,.F.);
#80936=ORIENTED_EDGE('',*,*,#55382,.F.);
#80937=ORIENTED_EDGE('',*,*,#55394,.F.);
#80938=ORIENTED_EDGE('',*,*,#54822,.F.);
#80939=ORIENTED_EDGE('',*,*,#55395,.T.);
#80940=ORIENTED_EDGE('',*,*,#55124,.F.);
#80941=ORIENTED_EDGE('',*,*,#55396,.F.);
#80942=ORIENTED_EDGE('',*,*,#55378,.F.);
#80943=ORIENTED_EDGE('',*,*,#55396,.T.);
#80944=ORIENTED_EDGE('',*,*,#54574,.F.);
#80945=ORIENTED_EDGE('',*,*,#55397,.F.);
#80946=ORIENTED_EDGE('',*,*,#55379,.F.);
#80947=ORIENTED_EDGE('',*,*,#55397,.T.);
#80948=ORIENTED_EDGE('',*,*,#54573,.F.);
#80949=ORIENTED_EDGE('',*,*,#55398,.F.);
#80950=ORIENTED_EDGE('',*,*,#55384,.F.);
#80951=ORIENTED_EDGE('',*,*,#55383,.F.);
#80952=ORIENTED_EDGE('',*,*,#55398,.T.);
#80953=ORIENTED_EDGE('',*,*,#54572,.F.);
#80954=ORIENTED_EDGE('',*,*,#55399,.F.);
#80955=ORIENTED_EDGE('',*,*,#55374,.F.);
#80956=ORIENTED_EDGE('',*,*,#55400,.T.);
#80957=ORIENTED_EDGE('',*,*,#55375,.F.);
#80958=ORIENTED_EDGE('',*,*,#55399,.T.);
#80959=ORIENTED_EDGE('',*,*,#55123,.F.);
#80960=ORIENTED_EDGE('',*,*,#55401,.T.);
#80961=ORIENTED_EDGE('',*,*,#55376,.F.);
#80962=ORIENTED_EDGE('',*,*,#55400,.F.);
#80963=ORIENTED_EDGE('',*,*,#54825,.F.);
#80964=ORIENTED_EDGE('',*,*,#54229,.T.);
#80965=ORIENTED_EDGE('',*,*,#55392,.T.);
#80966=ORIENTED_EDGE('',*,*,#55401,.F.);
#80967=ORIENTED_EDGE('',*,*,#54824,.T.);
#80968=ORIENTED_EDGE('',*,*,#55391,.T.);
#80969=ORIENTED_EDGE('',*,*,#55393,.T.);
#80970=ORIENTED_EDGE('',*,*,#54228,.T.);
#80971=ORIENTED_EDGE('',*,*,#55389,.T.);
#80972=ORIENTED_EDGE('',*,*,#55402,.T.);
#80973=ORIENTED_EDGE('',*,*,#55403,.T.);
#80974=ORIENTED_EDGE('',*,*,#55404,.T.);
#80975=ORIENTED_EDGE('',*,*,#55405,.T.);
#80976=ORIENTED_EDGE('',*,*,#55406,.T.);
#80977=ORIENTED_EDGE('',*,*,#55407,.T.);
#80978=ORIENTED_EDGE('',*,*,#55408,.T.);
#80979=ORIENTED_EDGE('',*,*,#55409,.F.);
#80980=ORIENTED_EDGE('',*,*,#55410,.T.);
#80981=ORIENTED_EDGE('',*,*,#55411,.T.);
#80982=ORIENTED_EDGE('',*,*,#55409,.T.);
#80983=ORIENTED_EDGE('',*,*,#55412,.T.);
#80984=ORIENTED_EDGE('',*,*,#55413,.T.);
#80985=ORIENTED_EDGE('',*,*,#55402,.F.);
#80986=ORIENTED_EDGE('',*,*,#55414,.T.);
#80987=ORIENTED_EDGE('',*,*,#55415,.T.);
#80988=ORIENTED_EDGE('',*,*,#55416,.F.);
#80989=ORIENTED_EDGE('',*,*,#55410,.F.);
#80990=ORIENTED_EDGE('',*,*,#55417,.F.);
#80991=ORIENTED_EDGE('',*,*,#55418,.F.);
#80992=ORIENTED_EDGE('',*,*,#55417,.T.);
#80993=ORIENTED_EDGE('',*,*,#55415,.F.);
#80994=ORIENTED_EDGE('',*,*,#55414,.F.);
#80995=ORIENTED_EDGE('',*,*,#55419,.F.);
#80996=ORIENTED_EDGE('',*,*,#55420,.F.);
#80997=ORIENTED_EDGE('',*,*,#55419,.T.);
#80998=ORIENTED_EDGE('',*,*,#55406,.F.);
#80999=ORIENTED_EDGE('',*,*,#55421,.F.);
#81000=ORIENTED_EDGE('',*,*,#55422,.F.);
#81001=ORIENTED_EDGE('',*,*,#55423,.T.);
#81002=ORIENTED_EDGE('',*,*,#55416,.T.);
#81003=ORIENTED_EDGE('',*,*,#54227,.F.);
#81004=ORIENTED_EDGE('',*,*,#54828,.T.);
#81005=ORIENTED_EDGE('',*,*,#55424,.F.);
#81006=ORIENTED_EDGE('',*,*,#55411,.F.);
#81007=ORIENTED_EDGE('',*,*,#55423,.F.);
#81008=ORIENTED_EDGE('',*,*,#54827,.F.);
#81009=ORIENTED_EDGE('',*,*,#55424,.T.);
#81010=ORIENTED_EDGE('',*,*,#55122,.F.);
#81011=ORIENTED_EDGE('',*,*,#55425,.F.);
#81012=ORIENTED_EDGE('',*,*,#55407,.F.);
#81013=ORIENTED_EDGE('',*,*,#55425,.T.);
#81014=ORIENTED_EDGE('',*,*,#54570,.F.);
#81015=ORIENTED_EDGE('',*,*,#55426,.F.);
#81016=ORIENTED_EDGE('',*,*,#55408,.F.);
#81017=ORIENTED_EDGE('',*,*,#55426,.T.);
#81018=ORIENTED_EDGE('',*,*,#54569,.F.);
#81019=ORIENTED_EDGE('',*,*,#55427,.F.);
#81020=ORIENTED_EDGE('',*,*,#55413,.F.);
#81021=ORIENTED_EDGE('',*,*,#55412,.F.);
#81022=ORIENTED_EDGE('',*,*,#55427,.T.);
#81023=ORIENTED_EDGE('',*,*,#54568,.F.);
#81024=ORIENTED_EDGE('',*,*,#55428,.F.);
#81025=ORIENTED_EDGE('',*,*,#55403,.F.);
#81026=ORIENTED_EDGE('',*,*,#55429,.T.);
#81027=ORIENTED_EDGE('',*,*,#55404,.F.);
#81028=ORIENTED_EDGE('',*,*,#55428,.T.);
#81029=ORIENTED_EDGE('',*,*,#55121,.F.);
#81030=ORIENTED_EDGE('',*,*,#55430,.T.);
#81031=ORIENTED_EDGE('',*,*,#55405,.F.);
#81032=ORIENTED_EDGE('',*,*,#55429,.F.);
#81033=ORIENTED_EDGE('',*,*,#54830,.F.);
#81034=ORIENTED_EDGE('',*,*,#54225,.T.);
#81035=ORIENTED_EDGE('',*,*,#55421,.T.);
#81036=ORIENTED_EDGE('',*,*,#55430,.F.);
#81037=ORIENTED_EDGE('',*,*,#54829,.T.);
#81038=ORIENTED_EDGE('',*,*,#55420,.T.);
#81039=ORIENTED_EDGE('',*,*,#55422,.T.);
#81040=ORIENTED_EDGE('',*,*,#54224,.T.);
#81041=ORIENTED_EDGE('',*,*,#55418,.T.);
#81042=ORIENTED_EDGE('',*,*,#55431,.T.);
#81043=ORIENTED_EDGE('',*,*,#55432,.T.);
#81044=ORIENTED_EDGE('',*,*,#55433,.T.);
#81045=ORIENTED_EDGE('',*,*,#55434,.T.);
#81046=ORIENTED_EDGE('',*,*,#55435,.T.);
#81047=ORIENTED_EDGE('',*,*,#55436,.T.);
#81048=ORIENTED_EDGE('',*,*,#55437,.T.);
#81049=ORIENTED_EDGE('',*,*,#55438,.F.);
#81050=ORIENTED_EDGE('',*,*,#55439,.T.);
#81051=ORIENTED_EDGE('',*,*,#55440,.T.);
#81052=ORIENTED_EDGE('',*,*,#55438,.T.);
#81053=ORIENTED_EDGE('',*,*,#55441,.T.);
#81054=ORIENTED_EDGE('',*,*,#55442,.T.);
#81055=ORIENTED_EDGE('',*,*,#55431,.F.);
#81056=ORIENTED_EDGE('',*,*,#55443,.T.);
#81057=ORIENTED_EDGE('',*,*,#55444,.T.);
#81058=ORIENTED_EDGE('',*,*,#55445,.F.);
#81059=ORIENTED_EDGE('',*,*,#55439,.F.);
#81060=ORIENTED_EDGE('',*,*,#55446,.F.);
#81061=ORIENTED_EDGE('',*,*,#55447,.F.);
#81062=ORIENTED_EDGE('',*,*,#55446,.T.);
#81063=ORIENTED_EDGE('',*,*,#55444,.F.);
#81064=ORIENTED_EDGE('',*,*,#55443,.F.);
#81065=ORIENTED_EDGE('',*,*,#55448,.F.);
#81066=ORIENTED_EDGE('',*,*,#55449,.F.);
#81067=ORIENTED_EDGE('',*,*,#55448,.T.);
#81068=ORIENTED_EDGE('',*,*,#55435,.F.);
#81069=ORIENTED_EDGE('',*,*,#55450,.F.);
#81070=ORIENTED_EDGE('',*,*,#55451,.F.);
#81071=ORIENTED_EDGE('',*,*,#55452,.T.);
#81072=ORIENTED_EDGE('',*,*,#55445,.T.);
#81073=ORIENTED_EDGE('',*,*,#54223,.F.);
#81074=ORIENTED_EDGE('',*,*,#54833,.T.);
#81075=ORIENTED_EDGE('',*,*,#55453,.F.);
#81076=ORIENTED_EDGE('',*,*,#55440,.F.);
#81077=ORIENTED_EDGE('',*,*,#55452,.F.);
#81078=ORIENTED_EDGE('',*,*,#54832,.F.);
#81079=ORIENTED_EDGE('',*,*,#55453,.T.);
#81080=ORIENTED_EDGE('',*,*,#55120,.F.);
#81081=ORIENTED_EDGE('',*,*,#55454,.F.);
#81082=ORIENTED_EDGE('',*,*,#55436,.F.);
#81083=ORIENTED_EDGE('',*,*,#55454,.T.);
#81084=ORIENTED_EDGE('',*,*,#54566,.F.);
#81085=ORIENTED_EDGE('',*,*,#55455,.F.);
#81086=ORIENTED_EDGE('',*,*,#55437,.F.);
#81087=ORIENTED_EDGE('',*,*,#55455,.T.);
#81088=ORIENTED_EDGE('',*,*,#54565,.F.);
#81089=ORIENTED_EDGE('',*,*,#55456,.F.);
#81090=ORIENTED_EDGE('',*,*,#55442,.F.);
#81091=ORIENTED_EDGE('',*,*,#55441,.F.);
#81092=ORIENTED_EDGE('',*,*,#55456,.T.);
#81093=ORIENTED_EDGE('',*,*,#54564,.F.);
#81094=ORIENTED_EDGE('',*,*,#55457,.F.);
#81095=ORIENTED_EDGE('',*,*,#55432,.F.);
#81096=ORIENTED_EDGE('',*,*,#55458,.T.);
#81097=ORIENTED_EDGE('',*,*,#55433,.F.);
#81098=ORIENTED_EDGE('',*,*,#55457,.T.);
#81099=ORIENTED_EDGE('',*,*,#55119,.F.);
#81100=ORIENTED_EDGE('',*,*,#55459,.T.);
#81101=ORIENTED_EDGE('',*,*,#55434,.F.);
#81102=ORIENTED_EDGE('',*,*,#55458,.F.);
#81103=ORIENTED_EDGE('',*,*,#54835,.F.);
#81104=ORIENTED_EDGE('',*,*,#54221,.T.);
#81105=ORIENTED_EDGE('',*,*,#55450,.T.);
#81106=ORIENTED_EDGE('',*,*,#55459,.F.);
#81107=ORIENTED_EDGE('',*,*,#54834,.T.);
#81108=ORIENTED_EDGE('',*,*,#55449,.T.);
#81109=ORIENTED_EDGE('',*,*,#55451,.T.);
#81110=ORIENTED_EDGE('',*,*,#54220,.T.);
#81111=ORIENTED_EDGE('',*,*,#55447,.T.);
#81112=ORIENTED_EDGE('',*,*,#55460,.T.);
#81113=ORIENTED_EDGE('',*,*,#55461,.T.);
#81114=ORIENTED_EDGE('',*,*,#55462,.T.);
#81115=ORIENTED_EDGE('',*,*,#55463,.T.);
#81116=ORIENTED_EDGE('',*,*,#55464,.T.);
#81117=ORIENTED_EDGE('',*,*,#55465,.T.);
#81118=ORIENTED_EDGE('',*,*,#55466,.T.);
#81119=ORIENTED_EDGE('',*,*,#55467,.F.);
#81120=ORIENTED_EDGE('',*,*,#55468,.T.);
#81121=ORIENTED_EDGE('',*,*,#55469,.T.);
#81122=ORIENTED_EDGE('',*,*,#55467,.T.);
#81123=ORIENTED_EDGE('',*,*,#55470,.T.);
#81124=ORIENTED_EDGE('',*,*,#55471,.T.);
#81125=ORIENTED_EDGE('',*,*,#55460,.F.);
#81126=ORIENTED_EDGE('',*,*,#55472,.T.);
#81127=ORIENTED_EDGE('',*,*,#55473,.T.);
#81128=ORIENTED_EDGE('',*,*,#55474,.F.);
#81129=ORIENTED_EDGE('',*,*,#55468,.F.);
#81130=ORIENTED_EDGE('',*,*,#55475,.F.);
#81131=ORIENTED_EDGE('',*,*,#55476,.F.);
#81132=ORIENTED_EDGE('',*,*,#55475,.T.);
#81133=ORIENTED_EDGE('',*,*,#55473,.F.);
#81134=ORIENTED_EDGE('',*,*,#55472,.F.);
#81135=ORIENTED_EDGE('',*,*,#55477,.F.);
#81136=ORIENTED_EDGE('',*,*,#55478,.F.);
#81137=ORIENTED_EDGE('',*,*,#55477,.T.);
#81138=ORIENTED_EDGE('',*,*,#55464,.F.);
#81139=ORIENTED_EDGE('',*,*,#55479,.F.);
#81140=ORIENTED_EDGE('',*,*,#55480,.F.);
#81141=ORIENTED_EDGE('',*,*,#55481,.T.);
#81142=ORIENTED_EDGE('',*,*,#55474,.T.);
#81143=ORIENTED_EDGE('',*,*,#54219,.F.);
#81144=ORIENTED_EDGE('',*,*,#54838,.T.);
#81145=ORIENTED_EDGE('',*,*,#55482,.F.);
#81146=ORIENTED_EDGE('',*,*,#55469,.F.);
#81147=ORIENTED_EDGE('',*,*,#55481,.F.);
#81148=ORIENTED_EDGE('',*,*,#54837,.F.);
#81149=ORIENTED_EDGE('',*,*,#55482,.T.);
#81150=ORIENTED_EDGE('',*,*,#55118,.F.);
#81151=ORIENTED_EDGE('',*,*,#55483,.F.);
#81152=ORIENTED_EDGE('',*,*,#55465,.F.);
#81153=ORIENTED_EDGE('',*,*,#55483,.T.);
#81154=ORIENTED_EDGE('',*,*,#54562,.F.);
#81155=ORIENTED_EDGE('',*,*,#55484,.F.);
#81156=ORIENTED_EDGE('',*,*,#55466,.F.);
#81157=ORIENTED_EDGE('',*,*,#55484,.T.);
#81158=ORIENTED_EDGE('',*,*,#54561,.F.);
#81159=ORIENTED_EDGE('',*,*,#55485,.F.);
#81160=ORIENTED_EDGE('',*,*,#55471,.F.);
#81161=ORIENTED_EDGE('',*,*,#55470,.F.);
#81162=ORIENTED_EDGE('',*,*,#55485,.T.);
#81163=ORIENTED_EDGE('',*,*,#54560,.F.);
#81164=ORIENTED_EDGE('',*,*,#55486,.F.);
#81165=ORIENTED_EDGE('',*,*,#55461,.F.);
#81166=ORIENTED_EDGE('',*,*,#55487,.T.);
#81167=ORIENTED_EDGE('',*,*,#55462,.F.);
#81168=ORIENTED_EDGE('',*,*,#55486,.T.);
#81169=ORIENTED_EDGE('',*,*,#55117,.F.);
#81170=ORIENTED_EDGE('',*,*,#55488,.T.);
#81171=ORIENTED_EDGE('',*,*,#55463,.F.);
#81172=ORIENTED_EDGE('',*,*,#55487,.F.);
#81173=ORIENTED_EDGE('',*,*,#54840,.F.);
#81174=ORIENTED_EDGE('',*,*,#54217,.T.);
#81175=ORIENTED_EDGE('',*,*,#55479,.T.);
#81176=ORIENTED_EDGE('',*,*,#55488,.F.);
#81177=ORIENTED_EDGE('',*,*,#54839,.T.);
#81178=ORIENTED_EDGE('',*,*,#55478,.T.);
#81179=ORIENTED_EDGE('',*,*,#55480,.T.);
#81180=ORIENTED_EDGE('',*,*,#54216,.T.);
#81181=ORIENTED_EDGE('',*,*,#55476,.T.);
#81182=ORIENTED_EDGE('',*,*,#55489,.T.);
#81183=ORIENTED_EDGE('',*,*,#55490,.T.);
#81184=ORIENTED_EDGE('',*,*,#55491,.T.);
#81185=ORIENTED_EDGE('',*,*,#55492,.T.);
#81186=ORIENTED_EDGE('',*,*,#55493,.T.);
#81187=ORIENTED_EDGE('',*,*,#55494,.T.);
#81188=ORIENTED_EDGE('',*,*,#55495,.T.);
#81189=ORIENTED_EDGE('',*,*,#55496,.F.);
#81190=ORIENTED_EDGE('',*,*,#55497,.T.);
#81191=ORIENTED_EDGE('',*,*,#55498,.T.);
#81192=ORIENTED_EDGE('',*,*,#55496,.T.);
#81193=ORIENTED_EDGE('',*,*,#55499,.T.);
#81194=ORIENTED_EDGE('',*,*,#55500,.T.);
#81195=ORIENTED_EDGE('',*,*,#55489,.F.);
#81196=ORIENTED_EDGE('',*,*,#55501,.T.);
#81197=ORIENTED_EDGE('',*,*,#55502,.T.);
#81198=ORIENTED_EDGE('',*,*,#55503,.F.);
#81199=ORIENTED_EDGE('',*,*,#55497,.F.);
#81200=ORIENTED_EDGE('',*,*,#55504,.F.);
#81201=ORIENTED_EDGE('',*,*,#55505,.F.);
#81202=ORIENTED_EDGE('',*,*,#55504,.T.);
#81203=ORIENTED_EDGE('',*,*,#55502,.F.);
#81204=ORIENTED_EDGE('',*,*,#55501,.F.);
#81205=ORIENTED_EDGE('',*,*,#55506,.F.);
#81206=ORIENTED_EDGE('',*,*,#55507,.F.);
#81207=ORIENTED_EDGE('',*,*,#55506,.T.);
#81208=ORIENTED_EDGE('',*,*,#55493,.F.);
#81209=ORIENTED_EDGE('',*,*,#55508,.F.);
#81210=ORIENTED_EDGE('',*,*,#55509,.F.);
#81211=ORIENTED_EDGE('',*,*,#55510,.T.);
#81212=ORIENTED_EDGE('',*,*,#55503,.T.);
#81213=ORIENTED_EDGE('',*,*,#54215,.F.);
#81214=ORIENTED_EDGE('',*,*,#54843,.T.);
#81215=ORIENTED_EDGE('',*,*,#55511,.F.);
#81216=ORIENTED_EDGE('',*,*,#55498,.F.);
#81217=ORIENTED_EDGE('',*,*,#55510,.F.);
#81218=ORIENTED_EDGE('',*,*,#54842,.F.);
#81219=ORIENTED_EDGE('',*,*,#55511,.T.);
#81220=ORIENTED_EDGE('',*,*,#55116,.F.);
#81221=ORIENTED_EDGE('',*,*,#55512,.F.);
#81222=ORIENTED_EDGE('',*,*,#55494,.F.);
#81223=ORIENTED_EDGE('',*,*,#55512,.T.);
#81224=ORIENTED_EDGE('',*,*,#54558,.F.);
#81225=ORIENTED_EDGE('',*,*,#55513,.F.);
#81226=ORIENTED_EDGE('',*,*,#55495,.F.);
#81227=ORIENTED_EDGE('',*,*,#55513,.T.);
#81228=ORIENTED_EDGE('',*,*,#54557,.F.);
#81229=ORIENTED_EDGE('',*,*,#55514,.F.);
#81230=ORIENTED_EDGE('',*,*,#55500,.F.);
#81231=ORIENTED_EDGE('',*,*,#55499,.F.);
#81232=ORIENTED_EDGE('',*,*,#55514,.T.);
#81233=ORIENTED_EDGE('',*,*,#54556,.F.);
#81234=ORIENTED_EDGE('',*,*,#55515,.F.);
#81235=ORIENTED_EDGE('',*,*,#55490,.F.);
#81236=ORIENTED_EDGE('',*,*,#55516,.T.);
#81237=ORIENTED_EDGE('',*,*,#55491,.F.);
#81238=ORIENTED_EDGE('',*,*,#55515,.T.);
#81239=ORIENTED_EDGE('',*,*,#55115,.F.);
#81240=ORIENTED_EDGE('',*,*,#55517,.T.);
#81241=ORIENTED_EDGE('',*,*,#55492,.F.);
#81242=ORIENTED_EDGE('',*,*,#55516,.F.);
#81243=ORIENTED_EDGE('',*,*,#54845,.F.);
#81244=ORIENTED_EDGE('',*,*,#54213,.T.);
#81245=ORIENTED_EDGE('',*,*,#55508,.T.);
#81246=ORIENTED_EDGE('',*,*,#55517,.F.);
#81247=ORIENTED_EDGE('',*,*,#54844,.T.);
#81248=ORIENTED_EDGE('',*,*,#55507,.T.);
#81249=ORIENTED_EDGE('',*,*,#55509,.T.);
#81250=ORIENTED_EDGE('',*,*,#54212,.T.);
#81251=ORIENTED_EDGE('',*,*,#55505,.T.);
#81252=ORIENTED_EDGE('',*,*,#55518,.T.);
#81253=ORIENTED_EDGE('',*,*,#55519,.T.);
#81254=ORIENTED_EDGE('',*,*,#55520,.T.);
#81255=ORIENTED_EDGE('',*,*,#55521,.T.);
#81256=ORIENTED_EDGE('',*,*,#55522,.T.);
#81257=ORIENTED_EDGE('',*,*,#55523,.T.);
#81258=ORIENTED_EDGE('',*,*,#55524,.T.);
#81259=ORIENTED_EDGE('',*,*,#55525,.F.);
#81260=ORIENTED_EDGE('',*,*,#55526,.T.);
#81261=ORIENTED_EDGE('',*,*,#55527,.T.);
#81262=ORIENTED_EDGE('',*,*,#55525,.T.);
#81263=ORIENTED_EDGE('',*,*,#55528,.T.);
#81264=ORIENTED_EDGE('',*,*,#55529,.T.);
#81265=ORIENTED_EDGE('',*,*,#55518,.F.);
#81266=ORIENTED_EDGE('',*,*,#55530,.T.);
#81267=ORIENTED_EDGE('',*,*,#55531,.T.);
#81268=ORIENTED_EDGE('',*,*,#55532,.F.);
#81269=ORIENTED_EDGE('',*,*,#55526,.F.);
#81270=ORIENTED_EDGE('',*,*,#55533,.F.);
#81271=ORIENTED_EDGE('',*,*,#55534,.F.);
#81272=ORIENTED_EDGE('',*,*,#55533,.T.);
#81273=ORIENTED_EDGE('',*,*,#55531,.F.);
#81274=ORIENTED_EDGE('',*,*,#55530,.F.);
#81275=ORIENTED_EDGE('',*,*,#55535,.F.);
#81276=ORIENTED_EDGE('',*,*,#55536,.F.);
#81277=ORIENTED_EDGE('',*,*,#55535,.T.);
#81278=ORIENTED_EDGE('',*,*,#55522,.F.);
#81279=ORIENTED_EDGE('',*,*,#55537,.F.);
#81280=ORIENTED_EDGE('',*,*,#55538,.F.);
#81281=ORIENTED_EDGE('',*,*,#55539,.T.);
#81282=ORIENTED_EDGE('',*,*,#55532,.T.);
#81283=ORIENTED_EDGE('',*,*,#54211,.F.);
#81284=ORIENTED_EDGE('',*,*,#54848,.T.);
#81285=ORIENTED_EDGE('',*,*,#55540,.F.);
#81286=ORIENTED_EDGE('',*,*,#55527,.F.);
#81287=ORIENTED_EDGE('',*,*,#55539,.F.);
#81288=ORIENTED_EDGE('',*,*,#54847,.F.);
#81289=ORIENTED_EDGE('',*,*,#55540,.T.);
#81290=ORIENTED_EDGE('',*,*,#55114,.F.);
#81291=ORIENTED_EDGE('',*,*,#55541,.F.);
#81292=ORIENTED_EDGE('',*,*,#55523,.F.);
#81293=ORIENTED_EDGE('',*,*,#55541,.T.);
#81294=ORIENTED_EDGE('',*,*,#54554,.F.);
#81295=ORIENTED_EDGE('',*,*,#55542,.F.);
#81296=ORIENTED_EDGE('',*,*,#55524,.F.);
#81297=ORIENTED_EDGE('',*,*,#55542,.T.);
#81298=ORIENTED_EDGE('',*,*,#54553,.F.);
#81299=ORIENTED_EDGE('',*,*,#55543,.F.);
#81300=ORIENTED_EDGE('',*,*,#55529,.F.);
#81301=ORIENTED_EDGE('',*,*,#55528,.F.);
#81302=ORIENTED_EDGE('',*,*,#55543,.T.);
#81303=ORIENTED_EDGE('',*,*,#54552,.F.);
#81304=ORIENTED_EDGE('',*,*,#55544,.F.);
#81305=ORIENTED_EDGE('',*,*,#55519,.F.);
#81306=ORIENTED_EDGE('',*,*,#55545,.T.);
#81307=ORIENTED_EDGE('',*,*,#55520,.F.);
#81308=ORIENTED_EDGE('',*,*,#55544,.T.);
#81309=ORIENTED_EDGE('',*,*,#54989,.F.);
#81310=ORIENTED_EDGE('',*,*,#55546,.T.);
#81311=ORIENTED_EDGE('',*,*,#55521,.F.);
#81312=ORIENTED_EDGE('',*,*,#55545,.F.);
#81313=ORIENTED_EDGE('',*,*,#54850,.F.);
#81314=ORIENTED_EDGE('',*,*,#54209,.T.);
#81315=ORIENTED_EDGE('',*,*,#55537,.T.);
#81316=ORIENTED_EDGE('',*,*,#55546,.F.);
#81317=ORIENTED_EDGE('',*,*,#54849,.T.);
#81318=ORIENTED_EDGE('',*,*,#55536,.T.);
#81319=ORIENTED_EDGE('',*,*,#55538,.T.);
#81320=ORIENTED_EDGE('',*,*,#54208,.T.);
#81321=ORIENTED_EDGE('',*,*,#55534,.T.);
#81322=ORIENTED_EDGE('',*,*,#55547,.T.);
#81323=ORIENTED_EDGE('',*,*,#55548,.T.);
#81324=ORIENTED_EDGE('',*,*,#55549,.T.);
#81325=ORIENTED_EDGE('',*,*,#55550,.T.);
#81326=ORIENTED_EDGE('',*,*,#55551,.T.);
#81327=ORIENTED_EDGE('',*,*,#55552,.T.);
#81328=ORIENTED_EDGE('',*,*,#55553,.T.);
#81329=ORIENTED_EDGE('',*,*,#55554,.F.);
#81330=ORIENTED_EDGE('',*,*,#55555,.T.);
#81331=ORIENTED_EDGE('',*,*,#55556,.T.);
#81332=ORIENTED_EDGE('',*,*,#55554,.T.);
#81333=ORIENTED_EDGE('',*,*,#55557,.T.);
#81334=ORIENTED_EDGE('',*,*,#55558,.T.);
#81335=ORIENTED_EDGE('',*,*,#55547,.F.);
#81336=ORIENTED_EDGE('',*,*,#55559,.T.);
#81337=ORIENTED_EDGE('',*,*,#55560,.T.);
#81338=ORIENTED_EDGE('',*,*,#55561,.F.);
#81339=ORIENTED_EDGE('',*,*,#55555,.F.);
#81340=ORIENTED_EDGE('',*,*,#55562,.F.);
#81341=ORIENTED_EDGE('',*,*,#55563,.F.);
#81342=ORIENTED_EDGE('',*,*,#55562,.T.);
#81343=ORIENTED_EDGE('',*,*,#55560,.F.);
#81344=ORIENTED_EDGE('',*,*,#55559,.F.);
#81345=ORIENTED_EDGE('',*,*,#55564,.F.);
#81346=ORIENTED_EDGE('',*,*,#55565,.F.);
#81347=ORIENTED_EDGE('',*,*,#55564,.T.);
#81348=ORIENTED_EDGE('',*,*,#55551,.F.);
#81349=ORIENTED_EDGE('',*,*,#55566,.F.);
#81350=ORIENTED_EDGE('',*,*,#55567,.F.);
#81351=ORIENTED_EDGE('',*,*,#55568,.T.);
#81352=ORIENTED_EDGE('',*,*,#55561,.T.);
#81353=ORIENTED_EDGE('',*,*,#54207,.F.);
#81354=ORIENTED_EDGE('',*,*,#54782,.T.);
#81355=ORIENTED_EDGE('',*,*,#55569,.F.);
#81356=ORIENTED_EDGE('',*,*,#55556,.F.);
#81357=ORIENTED_EDGE('',*,*,#55568,.F.);
#81358=ORIENTED_EDGE('',*,*,#54781,.F.);
#81359=ORIENTED_EDGE('',*,*,#55569,.T.);
#81360=ORIENTED_EDGE('',*,*,#55113,.F.);
#81361=ORIENTED_EDGE('',*,*,#55570,.F.);
#81362=ORIENTED_EDGE('',*,*,#55552,.F.);
#81363=ORIENTED_EDGE('',*,*,#55570,.T.);
#81364=ORIENTED_EDGE('',*,*,#54294,.F.);
#81365=ORIENTED_EDGE('',*,*,#55571,.F.);
#81366=ORIENTED_EDGE('',*,*,#55553,.F.);
#81367=ORIENTED_EDGE('',*,*,#55571,.T.);
#81368=ORIENTED_EDGE('',*,*,#54293,.F.);
#81369=ORIENTED_EDGE('',*,*,#55572,.F.);
#81370=ORIENTED_EDGE('',*,*,#55558,.F.);
#81371=ORIENTED_EDGE('',*,*,#55557,.F.);
#81372=ORIENTED_EDGE('',*,*,#55572,.T.);
#81373=ORIENTED_EDGE('',*,*,#54292,.F.);
#81374=ORIENTED_EDGE('',*,*,#55573,.F.);
#81375=ORIENTED_EDGE('',*,*,#55548,.F.);
#81376=ORIENTED_EDGE('',*,*,#55574,.T.);
#81377=ORIENTED_EDGE('',*,*,#55549,.F.);
#81378=ORIENTED_EDGE('',*,*,#55573,.T.);
#81379=ORIENTED_EDGE('',*,*,#55136,.F.);
#81380=ORIENTED_EDGE('',*,*,#55575,.T.);
#81381=ORIENTED_EDGE('',*,*,#55550,.F.);
#81382=ORIENTED_EDGE('',*,*,#55574,.F.);
#81383=ORIENTED_EDGE('',*,*,#54784,.F.);
#81384=ORIENTED_EDGE('',*,*,#54205,.T.);
#81385=ORIENTED_EDGE('',*,*,#55566,.T.);
#81386=ORIENTED_EDGE('',*,*,#55575,.F.);
#81387=ORIENTED_EDGE('',*,*,#54783,.T.);
#81388=ORIENTED_EDGE('',*,*,#55565,.T.);
#81389=ORIENTED_EDGE('',*,*,#55567,.T.);
#81390=ORIENTED_EDGE('',*,*,#54204,.T.);
#81391=ORIENTED_EDGE('',*,*,#55563,.T.);
#81392=ORIENTED_EDGE('',*,*,#55576,.T.);
#81393=ORIENTED_EDGE('',*,*,#55577,.T.);
#81394=ORIENTED_EDGE('',*,*,#55578,.T.);
#81395=ORIENTED_EDGE('',*,*,#55579,.T.);
#81396=ORIENTED_EDGE('',*,*,#55580,.T.);
#81397=ORIENTED_EDGE('',*,*,#55581,.T.);
#81398=ORIENTED_EDGE('',*,*,#55582,.T.);
#81399=ORIENTED_EDGE('',*,*,#55583,.F.);
#81400=ORIENTED_EDGE('',*,*,#55584,.T.);
#81401=ORIENTED_EDGE('',*,*,#55585,.T.);
#81402=ORIENTED_EDGE('',*,*,#55583,.T.);
#81403=ORIENTED_EDGE('',*,*,#55586,.T.);
#81404=ORIENTED_EDGE('',*,*,#55587,.T.);
#81405=ORIENTED_EDGE('',*,*,#55576,.F.);
#81406=ORIENTED_EDGE('',*,*,#55588,.T.);
#81407=ORIENTED_EDGE('',*,*,#55589,.T.);
#81408=ORIENTED_EDGE('',*,*,#55590,.F.);
#81409=ORIENTED_EDGE('',*,*,#55584,.F.);
#81410=ORIENTED_EDGE('',*,*,#55591,.F.);
#81411=ORIENTED_EDGE('',*,*,#55592,.F.);
#81412=ORIENTED_EDGE('',*,*,#55591,.T.);
#81413=ORIENTED_EDGE('',*,*,#55589,.F.);
#81414=ORIENTED_EDGE('',*,*,#55588,.F.);
#81415=ORIENTED_EDGE('',*,*,#55593,.F.);
#81416=ORIENTED_EDGE('',*,*,#55594,.F.);
#81417=ORIENTED_EDGE('',*,*,#55593,.T.);
#81418=ORIENTED_EDGE('',*,*,#55580,.F.);
#81419=ORIENTED_EDGE('',*,*,#55595,.F.);
#81420=ORIENTED_EDGE('',*,*,#55596,.F.);
#81421=ORIENTED_EDGE('',*,*,#55597,.T.);
#81422=ORIENTED_EDGE('',*,*,#55590,.T.);
#81423=ORIENTED_EDGE('',*,*,#54203,.F.);
#81424=ORIENTED_EDGE('',*,*,#54777,.T.);
#81425=ORIENTED_EDGE('',*,*,#55598,.F.);
#81426=ORIENTED_EDGE('',*,*,#55585,.F.);
#81427=ORIENTED_EDGE('',*,*,#55597,.F.);
#81428=ORIENTED_EDGE('',*,*,#54776,.F.);
#81429=ORIENTED_EDGE('',*,*,#55598,.T.);
#81430=ORIENTED_EDGE('',*,*,#55111,.F.);
#81431=ORIENTED_EDGE('',*,*,#55599,.F.);
#81432=ORIENTED_EDGE('',*,*,#55581,.F.);
#81433=ORIENTED_EDGE('',*,*,#55599,.T.);
#81434=ORIENTED_EDGE('',*,*,#54298,.F.);
#81435=ORIENTED_EDGE('',*,*,#55600,.F.);
#81436=ORIENTED_EDGE('',*,*,#55582,.F.);
#81437=ORIENTED_EDGE('',*,*,#55600,.T.);
#81438=ORIENTED_EDGE('',*,*,#54297,.F.);
#81439=ORIENTED_EDGE('',*,*,#55601,.F.);
#81440=ORIENTED_EDGE('',*,*,#55587,.F.);
#81441=ORIENTED_EDGE('',*,*,#55586,.F.);
#81442=ORIENTED_EDGE('',*,*,#55601,.T.);
#81443=ORIENTED_EDGE('',*,*,#54296,.F.);
#81444=ORIENTED_EDGE('',*,*,#55602,.F.);
#81445=ORIENTED_EDGE('',*,*,#55577,.F.);
#81446=ORIENTED_EDGE('',*,*,#55603,.T.);
#81447=ORIENTED_EDGE('',*,*,#55578,.F.);
#81448=ORIENTED_EDGE('',*,*,#55602,.T.);
#81449=ORIENTED_EDGE('',*,*,#55112,.F.);
#81450=ORIENTED_EDGE('',*,*,#55604,.T.);
#81451=ORIENTED_EDGE('',*,*,#55579,.F.);
#81452=ORIENTED_EDGE('',*,*,#55603,.F.);
#81453=ORIENTED_EDGE('',*,*,#54779,.F.);
#81454=ORIENTED_EDGE('',*,*,#54201,.T.);
#81455=ORIENTED_EDGE('',*,*,#55595,.T.);
#81456=ORIENTED_EDGE('',*,*,#55604,.F.);
#81457=ORIENTED_EDGE('',*,*,#54778,.T.);
#81458=ORIENTED_EDGE('',*,*,#55594,.T.);
#81459=ORIENTED_EDGE('',*,*,#55596,.T.);
#81460=ORIENTED_EDGE('',*,*,#54200,.T.);
#81461=ORIENTED_EDGE('',*,*,#55592,.T.);
#81462=ORIENTED_EDGE('',*,*,#55605,.T.);
#81463=ORIENTED_EDGE('',*,*,#55606,.T.);
#81464=ORIENTED_EDGE('',*,*,#55607,.T.);
#81465=ORIENTED_EDGE('',*,*,#55608,.T.);
#81466=ORIENTED_EDGE('',*,*,#55609,.T.);
#81467=ORIENTED_EDGE('',*,*,#55610,.T.);
#81468=ORIENTED_EDGE('',*,*,#55611,.T.);
#81469=ORIENTED_EDGE('',*,*,#55612,.F.);
#81470=ORIENTED_EDGE('',*,*,#55613,.T.);
#81471=ORIENTED_EDGE('',*,*,#55614,.T.);
#81472=ORIENTED_EDGE('',*,*,#55612,.T.);
#81473=ORIENTED_EDGE('',*,*,#55615,.T.);
#81474=ORIENTED_EDGE('',*,*,#55616,.T.);
#81475=ORIENTED_EDGE('',*,*,#55605,.F.);
#81476=ORIENTED_EDGE('',*,*,#55617,.T.);
#81477=ORIENTED_EDGE('',*,*,#55618,.T.);
#81478=ORIENTED_EDGE('',*,*,#55619,.F.);
#81479=ORIENTED_EDGE('',*,*,#55613,.F.);
#81480=ORIENTED_EDGE('',*,*,#55620,.F.);
#81481=ORIENTED_EDGE('',*,*,#55621,.F.);
#81482=ORIENTED_EDGE('',*,*,#55620,.T.);
#81483=ORIENTED_EDGE('',*,*,#55618,.F.);
#81484=ORIENTED_EDGE('',*,*,#55617,.F.);
#81485=ORIENTED_EDGE('',*,*,#55622,.F.);
#81486=ORIENTED_EDGE('',*,*,#55623,.F.);
#81487=ORIENTED_EDGE('',*,*,#55622,.T.);
#81488=ORIENTED_EDGE('',*,*,#55609,.F.);
#81489=ORIENTED_EDGE('',*,*,#55624,.F.);
#81490=ORIENTED_EDGE('',*,*,#55625,.F.);
#81491=ORIENTED_EDGE('',*,*,#55626,.T.);
#81492=ORIENTED_EDGE('',*,*,#55619,.T.);
#81493=ORIENTED_EDGE('',*,*,#54199,.F.);
#81494=ORIENTED_EDGE('',*,*,#54772,.T.);
#81495=ORIENTED_EDGE('',*,*,#55627,.F.);
#81496=ORIENTED_EDGE('',*,*,#55614,.F.);
#81497=ORIENTED_EDGE('',*,*,#55626,.F.);
#81498=ORIENTED_EDGE('',*,*,#54771,.F.);
#81499=ORIENTED_EDGE('',*,*,#55627,.T.);
#81500=ORIENTED_EDGE('',*,*,#55109,.F.);
#81501=ORIENTED_EDGE('',*,*,#55628,.F.);
#81502=ORIENTED_EDGE('',*,*,#55610,.F.);
#81503=ORIENTED_EDGE('',*,*,#55628,.T.);
#81504=ORIENTED_EDGE('',*,*,#54302,.F.);
#81505=ORIENTED_EDGE('',*,*,#55629,.F.);
#81506=ORIENTED_EDGE('',*,*,#55611,.F.);
#81507=ORIENTED_EDGE('',*,*,#55629,.T.);
#81508=ORIENTED_EDGE('',*,*,#54301,.F.);
#81509=ORIENTED_EDGE('',*,*,#55630,.F.);
#81510=ORIENTED_EDGE('',*,*,#55616,.F.);
#81511=ORIENTED_EDGE('',*,*,#55615,.F.);
#81512=ORIENTED_EDGE('',*,*,#55630,.T.);
#81513=ORIENTED_EDGE('',*,*,#54300,.F.);
#81514=ORIENTED_EDGE('',*,*,#55631,.F.);
#81515=ORIENTED_EDGE('',*,*,#55606,.F.);
#81516=ORIENTED_EDGE('',*,*,#55632,.T.);
#81517=ORIENTED_EDGE('',*,*,#55607,.F.);
#81518=ORIENTED_EDGE('',*,*,#55631,.T.);
#81519=ORIENTED_EDGE('',*,*,#55110,.F.);
#81520=ORIENTED_EDGE('',*,*,#55633,.T.);
#81521=ORIENTED_EDGE('',*,*,#55608,.F.);
#81522=ORIENTED_EDGE('',*,*,#55632,.F.);
#81523=ORIENTED_EDGE('',*,*,#54774,.F.);
#81524=ORIENTED_EDGE('',*,*,#54197,.T.);
#81525=ORIENTED_EDGE('',*,*,#55624,.T.);
#81526=ORIENTED_EDGE('',*,*,#55633,.F.);
#81527=ORIENTED_EDGE('',*,*,#54773,.T.);
#81528=ORIENTED_EDGE('',*,*,#55623,.T.);
#81529=ORIENTED_EDGE('',*,*,#55625,.T.);
#81530=ORIENTED_EDGE('',*,*,#54196,.T.);
#81531=ORIENTED_EDGE('',*,*,#55621,.T.);
#81532=ORIENTED_EDGE('',*,*,#55634,.T.);
#81533=ORIENTED_EDGE('',*,*,#55635,.T.);
#81534=ORIENTED_EDGE('',*,*,#55636,.T.);
#81535=ORIENTED_EDGE('',*,*,#55637,.T.);
#81536=ORIENTED_EDGE('',*,*,#55638,.T.);
#81537=ORIENTED_EDGE('',*,*,#55639,.T.);
#81538=ORIENTED_EDGE('',*,*,#55640,.T.);
#81539=ORIENTED_EDGE('',*,*,#55641,.F.);
#81540=ORIENTED_EDGE('',*,*,#55642,.T.);
#81541=ORIENTED_EDGE('',*,*,#55643,.T.);
#81542=ORIENTED_EDGE('',*,*,#55641,.T.);
#81543=ORIENTED_EDGE('',*,*,#55644,.T.);
#81544=ORIENTED_EDGE('',*,*,#55645,.T.);
#81545=ORIENTED_EDGE('',*,*,#55634,.F.);
#81546=ORIENTED_EDGE('',*,*,#55646,.T.);
#81547=ORIENTED_EDGE('',*,*,#55647,.T.);
#81548=ORIENTED_EDGE('',*,*,#55648,.F.);
#81549=ORIENTED_EDGE('',*,*,#55642,.F.);
#81550=ORIENTED_EDGE('',*,*,#55649,.F.);
#81551=ORIENTED_EDGE('',*,*,#55650,.F.);
#81552=ORIENTED_EDGE('',*,*,#55649,.T.);
#81553=ORIENTED_EDGE('',*,*,#55647,.F.);
#81554=ORIENTED_EDGE('',*,*,#55646,.F.);
#81555=ORIENTED_EDGE('',*,*,#55651,.F.);
#81556=ORIENTED_EDGE('',*,*,#55652,.F.);
#81557=ORIENTED_EDGE('',*,*,#55651,.T.);
#81558=ORIENTED_EDGE('',*,*,#55638,.F.);
#81559=ORIENTED_EDGE('',*,*,#55653,.F.);
#81560=ORIENTED_EDGE('',*,*,#55654,.F.);
#81561=ORIENTED_EDGE('',*,*,#55655,.T.);
#81562=ORIENTED_EDGE('',*,*,#55648,.T.);
#81563=ORIENTED_EDGE('',*,*,#54195,.F.);
#81564=ORIENTED_EDGE('',*,*,#54767,.T.);
#81565=ORIENTED_EDGE('',*,*,#55656,.F.);
#81566=ORIENTED_EDGE('',*,*,#55643,.F.);
#81567=ORIENTED_EDGE('',*,*,#55655,.F.);
#81568=ORIENTED_EDGE('',*,*,#54766,.F.);
#81569=ORIENTED_EDGE('',*,*,#55656,.T.);
#81570=ORIENTED_EDGE('',*,*,#55107,.F.);
#81571=ORIENTED_EDGE('',*,*,#55657,.F.);
#81572=ORIENTED_EDGE('',*,*,#55639,.F.);
#81573=ORIENTED_EDGE('',*,*,#55657,.T.);
#81574=ORIENTED_EDGE('',*,*,#54306,.F.);
#81575=ORIENTED_EDGE('',*,*,#55658,.F.);
#81576=ORIENTED_EDGE('',*,*,#55640,.F.);
#81577=ORIENTED_EDGE('',*,*,#55658,.T.);
#81578=ORIENTED_EDGE('',*,*,#54305,.F.);
#81579=ORIENTED_EDGE('',*,*,#55659,.F.);
#81580=ORIENTED_EDGE('',*,*,#55645,.F.);
#81581=ORIENTED_EDGE('',*,*,#55644,.F.);
#81582=ORIENTED_EDGE('',*,*,#55659,.T.);
#81583=ORIENTED_EDGE('',*,*,#54304,.F.);
#81584=ORIENTED_EDGE('',*,*,#55660,.F.);
#81585=ORIENTED_EDGE('',*,*,#55635,.F.);
#81586=ORIENTED_EDGE('',*,*,#55661,.T.);
#81587=ORIENTED_EDGE('',*,*,#55636,.F.);
#81588=ORIENTED_EDGE('',*,*,#55660,.T.);
#81589=ORIENTED_EDGE('',*,*,#55108,.F.);
#81590=ORIENTED_EDGE('',*,*,#55662,.T.);
#81591=ORIENTED_EDGE('',*,*,#55637,.F.);
#81592=ORIENTED_EDGE('',*,*,#55661,.F.);
#81593=ORIENTED_EDGE('',*,*,#54769,.F.);
#81594=ORIENTED_EDGE('',*,*,#54193,.T.);
#81595=ORIENTED_EDGE('',*,*,#55653,.T.);
#81596=ORIENTED_EDGE('',*,*,#55662,.F.);
#81597=ORIENTED_EDGE('',*,*,#54768,.T.);
#81598=ORIENTED_EDGE('',*,*,#55652,.T.);
#81599=ORIENTED_EDGE('',*,*,#55654,.T.);
#81600=ORIENTED_EDGE('',*,*,#54192,.T.);
#81601=ORIENTED_EDGE('',*,*,#55650,.T.);
#81602=ORIENTED_EDGE('',*,*,#55663,.T.);
#81603=ORIENTED_EDGE('',*,*,#55664,.T.);
#81604=ORIENTED_EDGE('',*,*,#55665,.T.);
#81605=ORIENTED_EDGE('',*,*,#55666,.T.);
#81606=ORIENTED_EDGE('',*,*,#55667,.T.);
#81607=ORIENTED_EDGE('',*,*,#55668,.T.);
#81608=ORIENTED_EDGE('',*,*,#55669,.T.);
#81609=ORIENTED_EDGE('',*,*,#55670,.F.);
#81610=ORIENTED_EDGE('',*,*,#55671,.T.);
#81611=ORIENTED_EDGE('',*,*,#55672,.T.);
#81612=ORIENTED_EDGE('',*,*,#55670,.T.);
#81613=ORIENTED_EDGE('',*,*,#55673,.T.);
#81614=ORIENTED_EDGE('',*,*,#55674,.T.);
#81615=ORIENTED_EDGE('',*,*,#55663,.F.);
#81616=ORIENTED_EDGE('',*,*,#55675,.T.);
#81617=ORIENTED_EDGE('',*,*,#55676,.T.);
#81618=ORIENTED_EDGE('',*,*,#55677,.F.);
#81619=ORIENTED_EDGE('',*,*,#55671,.F.);
#81620=ORIENTED_EDGE('',*,*,#55678,.F.);
#81621=ORIENTED_EDGE('',*,*,#55679,.F.);
#81622=ORIENTED_EDGE('',*,*,#55678,.T.);
#81623=ORIENTED_EDGE('',*,*,#55676,.F.);
#81624=ORIENTED_EDGE('',*,*,#55675,.F.);
#81625=ORIENTED_EDGE('',*,*,#55680,.F.);
#81626=ORIENTED_EDGE('',*,*,#55681,.F.);
#81627=ORIENTED_EDGE('',*,*,#55680,.T.);
#81628=ORIENTED_EDGE('',*,*,#55667,.F.);
#81629=ORIENTED_EDGE('',*,*,#55682,.F.);
#81630=ORIENTED_EDGE('',*,*,#55683,.F.);
#81631=ORIENTED_EDGE('',*,*,#55684,.T.);
#81632=ORIENTED_EDGE('',*,*,#55677,.T.);
#81633=ORIENTED_EDGE('',*,*,#54191,.F.);
#81634=ORIENTED_EDGE('',*,*,#54762,.T.);
#81635=ORIENTED_EDGE('',*,*,#55685,.F.);
#81636=ORIENTED_EDGE('',*,*,#55672,.F.);
#81637=ORIENTED_EDGE('',*,*,#55684,.F.);
#81638=ORIENTED_EDGE('',*,*,#54761,.F.);
#81639=ORIENTED_EDGE('',*,*,#55685,.T.);
#81640=ORIENTED_EDGE('',*,*,#55105,.F.);
#81641=ORIENTED_EDGE('',*,*,#55686,.F.);
#81642=ORIENTED_EDGE('',*,*,#55668,.F.);
#81643=ORIENTED_EDGE('',*,*,#55686,.T.);
#81644=ORIENTED_EDGE('',*,*,#54310,.F.);
#81645=ORIENTED_EDGE('',*,*,#55687,.F.);
#81646=ORIENTED_EDGE('',*,*,#55669,.F.);
#81647=ORIENTED_EDGE('',*,*,#55687,.T.);
#81648=ORIENTED_EDGE('',*,*,#54309,.F.);
#81649=ORIENTED_EDGE('',*,*,#55688,.F.);
#81650=ORIENTED_EDGE('',*,*,#55674,.F.);
#81651=ORIENTED_EDGE('',*,*,#55673,.F.);
#81652=ORIENTED_EDGE('',*,*,#55688,.T.);
#81653=ORIENTED_EDGE('',*,*,#54308,.F.);
#81654=ORIENTED_EDGE('',*,*,#55689,.F.);
#81655=ORIENTED_EDGE('',*,*,#55664,.F.);
#81656=ORIENTED_EDGE('',*,*,#55690,.T.);
#81657=ORIENTED_EDGE('',*,*,#55665,.F.);
#81658=ORIENTED_EDGE('',*,*,#55689,.T.);
#81659=ORIENTED_EDGE('',*,*,#55106,.F.);
#81660=ORIENTED_EDGE('',*,*,#55691,.T.);
#81661=ORIENTED_EDGE('',*,*,#55666,.F.);
#81662=ORIENTED_EDGE('',*,*,#55690,.F.);
#81663=ORIENTED_EDGE('',*,*,#54764,.F.);
#81664=ORIENTED_EDGE('',*,*,#54189,.T.);
#81665=ORIENTED_EDGE('',*,*,#55682,.T.);
#81666=ORIENTED_EDGE('',*,*,#55691,.F.);
#81667=ORIENTED_EDGE('',*,*,#54763,.T.);
#81668=ORIENTED_EDGE('',*,*,#55681,.T.);
#81669=ORIENTED_EDGE('',*,*,#55683,.T.);
#81670=ORIENTED_EDGE('',*,*,#54188,.T.);
#81671=ORIENTED_EDGE('',*,*,#55679,.T.);
#81672=ORIENTED_EDGE('',*,*,#55692,.T.);
#81673=ORIENTED_EDGE('',*,*,#55693,.T.);
#81674=ORIENTED_EDGE('',*,*,#55694,.T.);
#81675=ORIENTED_EDGE('',*,*,#55695,.T.);
#81676=ORIENTED_EDGE('',*,*,#55696,.T.);
#81677=ORIENTED_EDGE('',*,*,#55697,.T.);
#81678=ORIENTED_EDGE('',*,*,#55698,.T.);
#81679=ORIENTED_EDGE('',*,*,#55699,.F.);
#81680=ORIENTED_EDGE('',*,*,#55700,.T.);
#81681=ORIENTED_EDGE('',*,*,#55701,.T.);
#81682=ORIENTED_EDGE('',*,*,#55699,.T.);
#81683=ORIENTED_EDGE('',*,*,#55702,.T.);
#81684=ORIENTED_EDGE('',*,*,#55703,.T.);
#81685=ORIENTED_EDGE('',*,*,#55692,.F.);
#81686=ORIENTED_EDGE('',*,*,#55704,.T.);
#81687=ORIENTED_EDGE('',*,*,#55705,.T.);
#81688=ORIENTED_EDGE('',*,*,#55706,.F.);
#81689=ORIENTED_EDGE('',*,*,#55700,.F.);
#81690=ORIENTED_EDGE('',*,*,#55707,.F.);
#81691=ORIENTED_EDGE('',*,*,#55708,.F.);
#81692=ORIENTED_EDGE('',*,*,#55707,.T.);
#81693=ORIENTED_EDGE('',*,*,#55705,.F.);
#81694=ORIENTED_EDGE('',*,*,#55704,.F.);
#81695=ORIENTED_EDGE('',*,*,#55709,.F.);
#81696=ORIENTED_EDGE('',*,*,#55710,.F.);
#81697=ORIENTED_EDGE('',*,*,#55709,.T.);
#81698=ORIENTED_EDGE('',*,*,#55696,.F.);
#81699=ORIENTED_EDGE('',*,*,#55711,.F.);
#81700=ORIENTED_EDGE('',*,*,#55712,.F.);
#81701=ORIENTED_EDGE('',*,*,#55713,.T.);
#81702=ORIENTED_EDGE('',*,*,#55706,.T.);
#81703=ORIENTED_EDGE('',*,*,#54187,.F.);
#81704=ORIENTED_EDGE('',*,*,#54757,.T.);
#81705=ORIENTED_EDGE('',*,*,#55714,.F.);
#81706=ORIENTED_EDGE('',*,*,#55701,.F.);
#81707=ORIENTED_EDGE('',*,*,#55713,.F.);
#81708=ORIENTED_EDGE('',*,*,#54756,.F.);
#81709=ORIENTED_EDGE('',*,*,#55714,.T.);
#81710=ORIENTED_EDGE('',*,*,#55103,.F.);
#81711=ORIENTED_EDGE('',*,*,#55715,.F.);
#81712=ORIENTED_EDGE('',*,*,#55697,.F.);
#81713=ORIENTED_EDGE('',*,*,#55715,.T.);
#81714=ORIENTED_EDGE('',*,*,#54314,.F.);
#81715=ORIENTED_EDGE('',*,*,#55716,.F.);
#81716=ORIENTED_EDGE('',*,*,#55698,.F.);
#81717=ORIENTED_EDGE('',*,*,#55716,.T.);
#81718=ORIENTED_EDGE('',*,*,#54313,.F.);
#81719=ORIENTED_EDGE('',*,*,#55717,.F.);
#81720=ORIENTED_EDGE('',*,*,#55703,.F.);
#81721=ORIENTED_EDGE('',*,*,#55702,.F.);
#81722=ORIENTED_EDGE('',*,*,#55717,.T.);
#81723=ORIENTED_EDGE('',*,*,#54312,.F.);
#81724=ORIENTED_EDGE('',*,*,#55718,.F.);
#81725=ORIENTED_EDGE('',*,*,#55693,.F.);
#81726=ORIENTED_EDGE('',*,*,#55719,.T.);
#81727=ORIENTED_EDGE('',*,*,#55694,.F.);
#81728=ORIENTED_EDGE('',*,*,#55718,.T.);
#81729=ORIENTED_EDGE('',*,*,#55104,.F.);
#81730=ORIENTED_EDGE('',*,*,#55720,.T.);
#81731=ORIENTED_EDGE('',*,*,#55695,.F.);
#81732=ORIENTED_EDGE('',*,*,#55719,.F.);
#81733=ORIENTED_EDGE('',*,*,#54759,.F.);
#81734=ORIENTED_EDGE('',*,*,#54185,.T.);
#81735=ORIENTED_EDGE('',*,*,#55711,.T.);
#81736=ORIENTED_EDGE('',*,*,#55720,.F.);
#81737=ORIENTED_EDGE('',*,*,#54758,.T.);
#81738=ORIENTED_EDGE('',*,*,#55710,.T.);
#81739=ORIENTED_EDGE('',*,*,#55712,.T.);
#81740=ORIENTED_EDGE('',*,*,#54184,.T.);
#81741=ORIENTED_EDGE('',*,*,#55708,.T.);
#81742=ORIENTED_EDGE('',*,*,#55721,.T.);
#81743=ORIENTED_EDGE('',*,*,#55722,.T.);
#81744=ORIENTED_EDGE('',*,*,#55723,.T.);
#81745=ORIENTED_EDGE('',*,*,#55724,.T.);
#81746=ORIENTED_EDGE('',*,*,#55725,.T.);
#81747=ORIENTED_EDGE('',*,*,#55726,.T.);
#81748=ORIENTED_EDGE('',*,*,#55727,.T.);
#81749=ORIENTED_EDGE('',*,*,#55728,.F.);
#81750=ORIENTED_EDGE('',*,*,#55729,.T.);
#81751=ORIENTED_EDGE('',*,*,#55730,.T.);
#81752=ORIENTED_EDGE('',*,*,#55728,.T.);
#81753=ORIENTED_EDGE('',*,*,#55731,.T.);
#81754=ORIENTED_EDGE('',*,*,#55732,.T.);
#81755=ORIENTED_EDGE('',*,*,#55721,.F.);
#81756=ORIENTED_EDGE('',*,*,#55733,.T.);
#81757=ORIENTED_EDGE('',*,*,#55734,.T.);
#81758=ORIENTED_EDGE('',*,*,#55735,.F.);
#81759=ORIENTED_EDGE('',*,*,#55729,.F.);
#81760=ORIENTED_EDGE('',*,*,#55736,.F.);
#81761=ORIENTED_EDGE('',*,*,#55737,.F.);
#81762=ORIENTED_EDGE('',*,*,#55736,.T.);
#81763=ORIENTED_EDGE('',*,*,#55734,.F.);
#81764=ORIENTED_EDGE('',*,*,#55733,.F.);
#81765=ORIENTED_EDGE('',*,*,#55738,.F.);
#81766=ORIENTED_EDGE('',*,*,#55739,.F.);
#81767=ORIENTED_EDGE('',*,*,#55738,.T.);
#81768=ORIENTED_EDGE('',*,*,#55725,.F.);
#81769=ORIENTED_EDGE('',*,*,#55740,.F.);
#81770=ORIENTED_EDGE('',*,*,#55741,.F.);
#81771=ORIENTED_EDGE('',*,*,#55742,.T.);
#81772=ORIENTED_EDGE('',*,*,#55735,.T.);
#81773=ORIENTED_EDGE('',*,*,#54183,.F.);
#81774=ORIENTED_EDGE('',*,*,#54752,.T.);
#81775=ORIENTED_EDGE('',*,*,#55743,.F.);
#81776=ORIENTED_EDGE('',*,*,#55730,.F.);
#81777=ORIENTED_EDGE('',*,*,#55742,.F.);
#81778=ORIENTED_EDGE('',*,*,#54751,.F.);
#81779=ORIENTED_EDGE('',*,*,#55743,.T.);
#81780=ORIENTED_EDGE('',*,*,#55101,.F.);
#81781=ORIENTED_EDGE('',*,*,#55744,.F.);
#81782=ORIENTED_EDGE('',*,*,#55726,.F.);
#81783=ORIENTED_EDGE('',*,*,#55744,.T.);
#81784=ORIENTED_EDGE('',*,*,#54318,.F.);
#81785=ORIENTED_EDGE('',*,*,#55745,.F.);
#81786=ORIENTED_EDGE('',*,*,#55727,.F.);
#81787=ORIENTED_EDGE('',*,*,#55745,.T.);
#81788=ORIENTED_EDGE('',*,*,#54317,.F.);
#81789=ORIENTED_EDGE('',*,*,#55746,.F.);
#81790=ORIENTED_EDGE('',*,*,#55732,.F.);
#81791=ORIENTED_EDGE('',*,*,#55731,.F.);
#81792=ORIENTED_EDGE('',*,*,#55746,.T.);
#81793=ORIENTED_EDGE('',*,*,#54316,.F.);
#81794=ORIENTED_EDGE('',*,*,#55747,.F.);
#81795=ORIENTED_EDGE('',*,*,#55722,.F.);
#81796=ORIENTED_EDGE('',*,*,#55748,.T.);
#81797=ORIENTED_EDGE('',*,*,#55723,.F.);
#81798=ORIENTED_EDGE('',*,*,#55747,.T.);
#81799=ORIENTED_EDGE('',*,*,#55102,.F.);
#81800=ORIENTED_EDGE('',*,*,#55749,.T.);
#81801=ORIENTED_EDGE('',*,*,#55724,.F.);
#81802=ORIENTED_EDGE('',*,*,#55748,.F.);
#81803=ORIENTED_EDGE('',*,*,#54754,.F.);
#81804=ORIENTED_EDGE('',*,*,#54181,.T.);
#81805=ORIENTED_EDGE('',*,*,#55740,.T.);
#81806=ORIENTED_EDGE('',*,*,#55749,.F.);
#81807=ORIENTED_EDGE('',*,*,#54753,.T.);
#81808=ORIENTED_EDGE('',*,*,#55739,.T.);
#81809=ORIENTED_EDGE('',*,*,#55741,.T.);
#81810=ORIENTED_EDGE('',*,*,#54180,.T.);
#81811=ORIENTED_EDGE('',*,*,#55737,.T.);
#81812=ORIENTED_EDGE('',*,*,#55750,.T.);
#81813=ORIENTED_EDGE('',*,*,#55751,.T.);
#81814=ORIENTED_EDGE('',*,*,#55752,.T.);
#81815=ORIENTED_EDGE('',*,*,#55753,.T.);
#81816=ORIENTED_EDGE('',*,*,#55754,.T.);
#81817=ORIENTED_EDGE('',*,*,#55755,.T.);
#81818=ORIENTED_EDGE('',*,*,#55756,.T.);
#81819=ORIENTED_EDGE('',*,*,#55757,.F.);
#81820=ORIENTED_EDGE('',*,*,#55758,.T.);
#81821=ORIENTED_EDGE('',*,*,#55759,.T.);
#81822=ORIENTED_EDGE('',*,*,#55757,.T.);
#81823=ORIENTED_EDGE('',*,*,#55760,.T.);
#81824=ORIENTED_EDGE('',*,*,#55761,.T.);
#81825=ORIENTED_EDGE('',*,*,#55750,.F.);
#81826=ORIENTED_EDGE('',*,*,#55762,.T.);
#81827=ORIENTED_EDGE('',*,*,#55763,.T.);
#81828=ORIENTED_EDGE('',*,*,#55764,.F.);
#81829=ORIENTED_EDGE('',*,*,#55758,.F.);
#81830=ORIENTED_EDGE('',*,*,#55765,.F.);
#81831=ORIENTED_EDGE('',*,*,#55766,.F.);
#81832=ORIENTED_EDGE('',*,*,#55765,.T.);
#81833=ORIENTED_EDGE('',*,*,#55763,.F.);
#81834=ORIENTED_EDGE('',*,*,#55762,.F.);
#81835=ORIENTED_EDGE('',*,*,#55767,.F.);
#81836=ORIENTED_EDGE('',*,*,#55768,.F.);
#81837=ORIENTED_EDGE('',*,*,#55767,.T.);
#81838=ORIENTED_EDGE('',*,*,#55754,.F.);
#81839=ORIENTED_EDGE('',*,*,#55769,.F.);
#81840=ORIENTED_EDGE('',*,*,#55770,.F.);
#81841=ORIENTED_EDGE('',*,*,#55771,.T.);
#81842=ORIENTED_EDGE('',*,*,#55764,.T.);
#81843=ORIENTED_EDGE('',*,*,#54179,.F.);
#81844=ORIENTED_EDGE('',*,*,#54747,.T.);
#81845=ORIENTED_EDGE('',*,*,#55772,.F.);
#81846=ORIENTED_EDGE('',*,*,#55759,.F.);
#81847=ORIENTED_EDGE('',*,*,#55771,.F.);
#81848=ORIENTED_EDGE('',*,*,#54746,.F.);
#81849=ORIENTED_EDGE('',*,*,#55772,.T.);
#81850=ORIENTED_EDGE('',*,*,#55099,.F.);
#81851=ORIENTED_EDGE('',*,*,#55773,.F.);
#81852=ORIENTED_EDGE('',*,*,#55755,.F.);
#81853=ORIENTED_EDGE('',*,*,#55773,.T.);
#81854=ORIENTED_EDGE('',*,*,#54322,.F.);
#81855=ORIENTED_EDGE('',*,*,#55774,.F.);
#81856=ORIENTED_EDGE('',*,*,#55756,.F.);
#81857=ORIENTED_EDGE('',*,*,#55774,.T.);
#81858=ORIENTED_EDGE('',*,*,#54321,.F.);
#81859=ORIENTED_EDGE('',*,*,#55775,.F.);
#81860=ORIENTED_EDGE('',*,*,#55761,.F.);
#81861=ORIENTED_EDGE('',*,*,#55760,.F.);
#81862=ORIENTED_EDGE('',*,*,#55775,.T.);
#81863=ORIENTED_EDGE('',*,*,#54320,.F.);
#81864=ORIENTED_EDGE('',*,*,#55776,.F.);
#81865=ORIENTED_EDGE('',*,*,#55751,.F.);
#81866=ORIENTED_EDGE('',*,*,#55777,.T.);
#81867=ORIENTED_EDGE('',*,*,#55752,.F.);
#81868=ORIENTED_EDGE('',*,*,#55776,.T.);
#81869=ORIENTED_EDGE('',*,*,#55100,.F.);
#81870=ORIENTED_EDGE('',*,*,#55778,.T.);
#81871=ORIENTED_EDGE('',*,*,#55753,.F.);
#81872=ORIENTED_EDGE('',*,*,#55777,.F.);
#81873=ORIENTED_EDGE('',*,*,#54749,.F.);
#81874=ORIENTED_EDGE('',*,*,#54177,.T.);
#81875=ORIENTED_EDGE('',*,*,#55769,.T.);
#81876=ORIENTED_EDGE('',*,*,#55778,.F.);
#81877=ORIENTED_EDGE('',*,*,#54748,.T.);
#81878=ORIENTED_EDGE('',*,*,#55768,.T.);
#81879=ORIENTED_EDGE('',*,*,#55770,.T.);
#81880=ORIENTED_EDGE('',*,*,#54176,.T.);
#81881=ORIENTED_EDGE('',*,*,#55766,.T.);
#81882=ORIENTED_EDGE('',*,*,#55779,.T.);
#81883=ORIENTED_EDGE('',*,*,#55780,.T.);
#81884=ORIENTED_EDGE('',*,*,#55781,.T.);
#81885=ORIENTED_EDGE('',*,*,#55782,.T.);
#81886=ORIENTED_EDGE('',*,*,#55783,.T.);
#81887=ORIENTED_EDGE('',*,*,#55784,.T.);
#81888=ORIENTED_EDGE('',*,*,#55785,.T.);
#81889=ORIENTED_EDGE('',*,*,#55786,.F.);
#81890=ORIENTED_EDGE('',*,*,#55787,.T.);
#81891=ORIENTED_EDGE('',*,*,#55788,.T.);
#81892=ORIENTED_EDGE('',*,*,#55786,.T.);
#81893=ORIENTED_EDGE('',*,*,#55789,.T.);
#81894=ORIENTED_EDGE('',*,*,#55790,.T.);
#81895=ORIENTED_EDGE('',*,*,#55779,.F.);
#81896=ORIENTED_EDGE('',*,*,#55791,.T.);
#81897=ORIENTED_EDGE('',*,*,#55792,.T.);
#81898=ORIENTED_EDGE('',*,*,#55793,.F.);
#81899=ORIENTED_EDGE('',*,*,#55787,.F.);
#81900=ORIENTED_EDGE('',*,*,#55794,.F.);
#81901=ORIENTED_EDGE('',*,*,#55795,.F.);
#81902=ORIENTED_EDGE('',*,*,#55794,.T.);
#81903=ORIENTED_EDGE('',*,*,#55792,.F.);
#81904=ORIENTED_EDGE('',*,*,#55791,.F.);
#81905=ORIENTED_EDGE('',*,*,#55796,.F.);
#81906=ORIENTED_EDGE('',*,*,#55797,.F.);
#81907=ORIENTED_EDGE('',*,*,#55796,.T.);
#81908=ORIENTED_EDGE('',*,*,#55783,.F.);
#81909=ORIENTED_EDGE('',*,*,#55798,.F.);
#81910=ORIENTED_EDGE('',*,*,#55799,.F.);
#81911=ORIENTED_EDGE('',*,*,#55800,.T.);
#81912=ORIENTED_EDGE('',*,*,#55793,.T.);
#81913=ORIENTED_EDGE('',*,*,#54175,.F.);
#81914=ORIENTED_EDGE('',*,*,#54742,.T.);
#81915=ORIENTED_EDGE('',*,*,#55801,.F.);
#81916=ORIENTED_EDGE('',*,*,#55788,.F.);
#81917=ORIENTED_EDGE('',*,*,#55800,.F.);
#81918=ORIENTED_EDGE('',*,*,#54741,.F.);
#81919=ORIENTED_EDGE('',*,*,#55801,.T.);
#81920=ORIENTED_EDGE('',*,*,#55097,.F.);
#81921=ORIENTED_EDGE('',*,*,#55802,.F.);
#81922=ORIENTED_EDGE('',*,*,#55784,.F.);
#81923=ORIENTED_EDGE('',*,*,#55802,.T.);
#81924=ORIENTED_EDGE('',*,*,#54326,.F.);
#81925=ORIENTED_EDGE('',*,*,#55803,.F.);
#81926=ORIENTED_EDGE('',*,*,#55785,.F.);
#81927=ORIENTED_EDGE('',*,*,#55803,.T.);
#81928=ORIENTED_EDGE('',*,*,#54325,.F.);
#81929=ORIENTED_EDGE('',*,*,#55804,.F.);
#81930=ORIENTED_EDGE('',*,*,#55790,.F.);
#81931=ORIENTED_EDGE('',*,*,#55789,.F.);
#81932=ORIENTED_EDGE('',*,*,#55804,.T.);
#81933=ORIENTED_EDGE('',*,*,#54324,.F.);
#81934=ORIENTED_EDGE('',*,*,#55805,.F.);
#81935=ORIENTED_EDGE('',*,*,#55780,.F.);
#81936=ORIENTED_EDGE('',*,*,#55806,.T.);
#81937=ORIENTED_EDGE('',*,*,#55781,.F.);
#81938=ORIENTED_EDGE('',*,*,#55805,.T.);
#81939=ORIENTED_EDGE('',*,*,#55098,.F.);
#81940=ORIENTED_EDGE('',*,*,#55807,.T.);
#81941=ORIENTED_EDGE('',*,*,#55782,.F.);
#81942=ORIENTED_EDGE('',*,*,#55806,.F.);
#81943=ORIENTED_EDGE('',*,*,#54744,.F.);
#81944=ORIENTED_EDGE('',*,*,#54173,.T.);
#81945=ORIENTED_EDGE('',*,*,#55798,.T.);
#81946=ORIENTED_EDGE('',*,*,#55807,.F.);
#81947=ORIENTED_EDGE('',*,*,#54743,.T.);
#81948=ORIENTED_EDGE('',*,*,#55797,.T.);
#81949=ORIENTED_EDGE('',*,*,#55799,.T.);
#81950=ORIENTED_EDGE('',*,*,#54172,.T.);
#81951=ORIENTED_EDGE('',*,*,#55795,.T.);
#81952=ORIENTED_EDGE('',*,*,#55808,.T.);
#81953=ORIENTED_EDGE('',*,*,#55809,.T.);
#81954=ORIENTED_EDGE('',*,*,#55810,.T.);
#81955=ORIENTED_EDGE('',*,*,#55811,.T.);
#81956=ORIENTED_EDGE('',*,*,#55812,.T.);
#81957=ORIENTED_EDGE('',*,*,#55813,.T.);
#81958=ORIENTED_EDGE('',*,*,#55814,.T.);
#81959=ORIENTED_EDGE('',*,*,#55815,.F.);
#81960=ORIENTED_EDGE('',*,*,#55816,.T.);
#81961=ORIENTED_EDGE('',*,*,#55817,.T.);
#81962=ORIENTED_EDGE('',*,*,#55815,.T.);
#81963=ORIENTED_EDGE('',*,*,#55818,.T.);
#81964=ORIENTED_EDGE('',*,*,#55819,.T.);
#81965=ORIENTED_EDGE('',*,*,#55808,.F.);
#81966=ORIENTED_EDGE('',*,*,#55820,.T.);
#81967=ORIENTED_EDGE('',*,*,#55821,.T.);
#81968=ORIENTED_EDGE('',*,*,#55822,.F.);
#81969=ORIENTED_EDGE('',*,*,#55816,.F.);
#81970=ORIENTED_EDGE('',*,*,#55823,.F.);
#81971=ORIENTED_EDGE('',*,*,#55824,.F.);
#81972=ORIENTED_EDGE('',*,*,#55823,.T.);
#81973=ORIENTED_EDGE('',*,*,#55821,.F.);
#81974=ORIENTED_EDGE('',*,*,#55820,.F.);
#81975=ORIENTED_EDGE('',*,*,#55825,.F.);
#81976=ORIENTED_EDGE('',*,*,#55826,.F.);
#81977=ORIENTED_EDGE('',*,*,#55825,.T.);
#81978=ORIENTED_EDGE('',*,*,#55812,.F.);
#81979=ORIENTED_EDGE('',*,*,#55827,.F.);
#81980=ORIENTED_EDGE('',*,*,#55828,.F.);
#81981=ORIENTED_EDGE('',*,*,#55829,.T.);
#81982=ORIENTED_EDGE('',*,*,#55822,.T.);
#81983=ORIENTED_EDGE('',*,*,#54171,.F.);
#81984=ORIENTED_EDGE('',*,*,#54737,.T.);
#81985=ORIENTED_EDGE('',*,*,#55830,.F.);
#81986=ORIENTED_EDGE('',*,*,#55817,.F.);
#81987=ORIENTED_EDGE('',*,*,#55829,.F.);
#81988=ORIENTED_EDGE('',*,*,#54736,.F.);
#81989=ORIENTED_EDGE('',*,*,#55830,.T.);
#81990=ORIENTED_EDGE('',*,*,#55095,.F.);
#81991=ORIENTED_EDGE('',*,*,#55831,.F.);
#81992=ORIENTED_EDGE('',*,*,#55813,.F.);
#81993=ORIENTED_EDGE('',*,*,#55831,.T.);
#81994=ORIENTED_EDGE('',*,*,#54330,.F.);
#81995=ORIENTED_EDGE('',*,*,#55832,.F.);
#81996=ORIENTED_EDGE('',*,*,#55814,.F.);
#81997=ORIENTED_EDGE('',*,*,#55832,.T.);
#81998=ORIENTED_EDGE('',*,*,#54329,.F.);
#81999=ORIENTED_EDGE('',*,*,#55833,.F.);
#82000=ORIENTED_EDGE('',*,*,#55819,.F.);
#82001=ORIENTED_EDGE('',*,*,#55818,.F.);
#82002=ORIENTED_EDGE('',*,*,#55833,.T.);
#82003=ORIENTED_EDGE('',*,*,#54328,.F.);
#82004=ORIENTED_EDGE('',*,*,#55834,.F.);
#82005=ORIENTED_EDGE('',*,*,#55809,.F.);
#82006=ORIENTED_EDGE('',*,*,#55835,.T.);
#82007=ORIENTED_EDGE('',*,*,#55810,.F.);
#82008=ORIENTED_EDGE('',*,*,#55834,.T.);
#82009=ORIENTED_EDGE('',*,*,#55096,.F.);
#82010=ORIENTED_EDGE('',*,*,#55836,.T.);
#82011=ORIENTED_EDGE('',*,*,#55811,.F.);
#82012=ORIENTED_EDGE('',*,*,#55835,.F.);
#82013=ORIENTED_EDGE('',*,*,#54739,.F.);
#82014=ORIENTED_EDGE('',*,*,#54169,.T.);
#82015=ORIENTED_EDGE('',*,*,#55827,.T.);
#82016=ORIENTED_EDGE('',*,*,#55836,.F.);
#82017=ORIENTED_EDGE('',*,*,#54738,.T.);
#82018=ORIENTED_EDGE('',*,*,#55826,.T.);
#82019=ORIENTED_EDGE('',*,*,#55828,.T.);
#82020=ORIENTED_EDGE('',*,*,#54168,.T.);
#82021=ORIENTED_EDGE('',*,*,#55824,.T.);
#82022=ORIENTED_EDGE('',*,*,#55837,.T.);
#82023=ORIENTED_EDGE('',*,*,#55838,.T.);
#82024=ORIENTED_EDGE('',*,*,#55839,.T.);
#82025=ORIENTED_EDGE('',*,*,#55840,.T.);
#82026=ORIENTED_EDGE('',*,*,#55841,.T.);
#82027=ORIENTED_EDGE('',*,*,#55842,.T.);
#82028=ORIENTED_EDGE('',*,*,#55843,.T.);
#82029=ORIENTED_EDGE('',*,*,#55844,.F.);
#82030=ORIENTED_EDGE('',*,*,#55845,.T.);
#82031=ORIENTED_EDGE('',*,*,#55846,.T.);
#82032=ORIENTED_EDGE('',*,*,#55844,.T.);
#82033=ORIENTED_EDGE('',*,*,#55847,.T.);
#82034=ORIENTED_EDGE('',*,*,#55848,.T.);
#82035=ORIENTED_EDGE('',*,*,#55837,.F.);
#82036=ORIENTED_EDGE('',*,*,#55849,.T.);
#82037=ORIENTED_EDGE('',*,*,#55850,.T.);
#82038=ORIENTED_EDGE('',*,*,#55851,.F.);
#82039=ORIENTED_EDGE('',*,*,#55845,.F.);
#82040=ORIENTED_EDGE('',*,*,#55852,.F.);
#82041=ORIENTED_EDGE('',*,*,#55853,.F.);
#82042=ORIENTED_EDGE('',*,*,#55852,.T.);
#82043=ORIENTED_EDGE('',*,*,#55850,.F.);
#82044=ORIENTED_EDGE('',*,*,#55849,.F.);
#82045=ORIENTED_EDGE('',*,*,#55854,.F.);
#82046=ORIENTED_EDGE('',*,*,#55855,.F.);
#82047=ORIENTED_EDGE('',*,*,#55854,.T.);
#82048=ORIENTED_EDGE('',*,*,#55841,.F.);
#82049=ORIENTED_EDGE('',*,*,#55856,.F.);
#82050=ORIENTED_EDGE('',*,*,#55857,.F.);
#82051=ORIENTED_EDGE('',*,*,#55858,.T.);
#82052=ORIENTED_EDGE('',*,*,#55851,.T.);
#82053=ORIENTED_EDGE('',*,*,#54167,.F.);
#82054=ORIENTED_EDGE('',*,*,#54732,.T.);
#82055=ORIENTED_EDGE('',*,*,#55859,.F.);
#82056=ORIENTED_EDGE('',*,*,#55846,.F.);
#82057=ORIENTED_EDGE('',*,*,#55858,.F.);
#82058=ORIENTED_EDGE('',*,*,#54731,.F.);
#82059=ORIENTED_EDGE('',*,*,#55859,.T.);
#82060=ORIENTED_EDGE('',*,*,#55093,.F.);
#82061=ORIENTED_EDGE('',*,*,#55860,.F.);
#82062=ORIENTED_EDGE('',*,*,#55842,.F.);
#82063=ORIENTED_EDGE('',*,*,#55860,.T.);
#82064=ORIENTED_EDGE('',*,*,#54334,.F.);
#82065=ORIENTED_EDGE('',*,*,#55861,.F.);
#82066=ORIENTED_EDGE('',*,*,#55843,.F.);
#82067=ORIENTED_EDGE('',*,*,#55861,.T.);
#82068=ORIENTED_EDGE('',*,*,#54333,.F.);
#82069=ORIENTED_EDGE('',*,*,#55862,.F.);
#82070=ORIENTED_EDGE('',*,*,#55848,.F.);
#82071=ORIENTED_EDGE('',*,*,#55847,.F.);
#82072=ORIENTED_EDGE('',*,*,#55862,.T.);
#82073=ORIENTED_EDGE('',*,*,#54332,.F.);
#82074=ORIENTED_EDGE('',*,*,#55863,.F.);
#82075=ORIENTED_EDGE('',*,*,#55838,.F.);
#82076=ORIENTED_EDGE('',*,*,#55864,.T.);
#82077=ORIENTED_EDGE('',*,*,#55839,.F.);
#82078=ORIENTED_EDGE('',*,*,#55863,.T.);
#82079=ORIENTED_EDGE('',*,*,#55094,.F.);
#82080=ORIENTED_EDGE('',*,*,#55865,.T.);
#82081=ORIENTED_EDGE('',*,*,#55840,.F.);
#82082=ORIENTED_EDGE('',*,*,#55864,.F.);
#82083=ORIENTED_EDGE('',*,*,#54734,.F.);
#82084=ORIENTED_EDGE('',*,*,#54165,.T.);
#82085=ORIENTED_EDGE('',*,*,#55856,.T.);
#82086=ORIENTED_EDGE('',*,*,#55865,.F.);
#82087=ORIENTED_EDGE('',*,*,#54733,.T.);
#82088=ORIENTED_EDGE('',*,*,#55855,.T.);
#82089=ORIENTED_EDGE('',*,*,#55857,.T.);
#82090=ORIENTED_EDGE('',*,*,#54164,.T.);
#82091=ORIENTED_EDGE('',*,*,#55853,.T.);
#82092=ORIENTED_EDGE('',*,*,#55866,.T.);
#82093=ORIENTED_EDGE('',*,*,#55867,.T.);
#82094=ORIENTED_EDGE('',*,*,#55868,.T.);
#82095=ORIENTED_EDGE('',*,*,#55869,.T.);
#82096=ORIENTED_EDGE('',*,*,#55870,.T.);
#82097=ORIENTED_EDGE('',*,*,#55871,.T.);
#82098=ORIENTED_EDGE('',*,*,#55872,.T.);
#82099=ORIENTED_EDGE('',*,*,#55873,.F.);
#82100=ORIENTED_EDGE('',*,*,#55874,.T.);
#82101=ORIENTED_EDGE('',*,*,#55875,.T.);
#82102=ORIENTED_EDGE('',*,*,#55873,.T.);
#82103=ORIENTED_EDGE('',*,*,#55876,.T.);
#82104=ORIENTED_EDGE('',*,*,#55877,.T.);
#82105=ORIENTED_EDGE('',*,*,#55866,.F.);
#82106=ORIENTED_EDGE('',*,*,#55878,.T.);
#82107=ORIENTED_EDGE('',*,*,#55879,.T.);
#82108=ORIENTED_EDGE('',*,*,#55880,.F.);
#82109=ORIENTED_EDGE('',*,*,#55874,.F.);
#82110=ORIENTED_EDGE('',*,*,#55881,.F.);
#82111=ORIENTED_EDGE('',*,*,#55882,.F.);
#82112=ORIENTED_EDGE('',*,*,#55881,.T.);
#82113=ORIENTED_EDGE('',*,*,#55879,.F.);
#82114=ORIENTED_EDGE('',*,*,#55878,.F.);
#82115=ORIENTED_EDGE('',*,*,#55883,.F.);
#82116=ORIENTED_EDGE('',*,*,#55884,.F.);
#82117=ORIENTED_EDGE('',*,*,#55883,.T.);
#82118=ORIENTED_EDGE('',*,*,#55870,.F.);
#82119=ORIENTED_EDGE('',*,*,#55885,.F.);
#82120=ORIENTED_EDGE('',*,*,#55886,.F.);
#82121=ORIENTED_EDGE('',*,*,#55887,.T.);
#82122=ORIENTED_EDGE('',*,*,#55880,.T.);
#82123=ORIENTED_EDGE('',*,*,#54163,.F.);
#82124=ORIENTED_EDGE('',*,*,#54727,.T.);
#82125=ORIENTED_EDGE('',*,*,#55888,.F.);
#82126=ORIENTED_EDGE('',*,*,#55875,.F.);
#82127=ORIENTED_EDGE('',*,*,#55887,.F.);
#82128=ORIENTED_EDGE('',*,*,#54726,.F.);
#82129=ORIENTED_EDGE('',*,*,#55888,.T.);
#82130=ORIENTED_EDGE('',*,*,#55091,.F.);
#82131=ORIENTED_EDGE('',*,*,#55889,.F.);
#82132=ORIENTED_EDGE('',*,*,#55871,.F.);
#82133=ORIENTED_EDGE('',*,*,#55889,.T.);
#82134=ORIENTED_EDGE('',*,*,#54338,.F.);
#82135=ORIENTED_EDGE('',*,*,#55890,.F.);
#82136=ORIENTED_EDGE('',*,*,#55872,.F.);
#82137=ORIENTED_EDGE('',*,*,#55890,.T.);
#82138=ORIENTED_EDGE('',*,*,#54337,.F.);
#82139=ORIENTED_EDGE('',*,*,#55891,.F.);
#82140=ORIENTED_EDGE('',*,*,#55877,.F.);
#82141=ORIENTED_EDGE('',*,*,#55876,.F.);
#82142=ORIENTED_EDGE('',*,*,#55891,.T.);
#82143=ORIENTED_EDGE('',*,*,#54336,.F.);
#82144=ORIENTED_EDGE('',*,*,#55892,.F.);
#82145=ORIENTED_EDGE('',*,*,#55867,.F.);
#82146=ORIENTED_EDGE('',*,*,#55893,.T.);
#82147=ORIENTED_EDGE('',*,*,#55868,.F.);
#82148=ORIENTED_EDGE('',*,*,#55892,.T.);
#82149=ORIENTED_EDGE('',*,*,#55092,.F.);
#82150=ORIENTED_EDGE('',*,*,#55894,.T.);
#82151=ORIENTED_EDGE('',*,*,#55869,.F.);
#82152=ORIENTED_EDGE('',*,*,#55893,.F.);
#82153=ORIENTED_EDGE('',*,*,#54729,.F.);
#82154=ORIENTED_EDGE('',*,*,#54161,.T.);
#82155=ORIENTED_EDGE('',*,*,#55885,.T.);
#82156=ORIENTED_EDGE('',*,*,#55894,.F.);
#82157=ORIENTED_EDGE('',*,*,#54728,.T.);
#82158=ORIENTED_EDGE('',*,*,#55884,.T.);
#82159=ORIENTED_EDGE('',*,*,#55886,.T.);
#82160=ORIENTED_EDGE('',*,*,#54160,.T.);
#82161=ORIENTED_EDGE('',*,*,#55882,.T.);
#82162=ORIENTED_EDGE('',*,*,#55895,.T.);
#82163=ORIENTED_EDGE('',*,*,#55896,.T.);
#82164=ORIENTED_EDGE('',*,*,#55897,.T.);
#82165=ORIENTED_EDGE('',*,*,#55898,.T.);
#82166=ORIENTED_EDGE('',*,*,#55899,.T.);
#82167=ORIENTED_EDGE('',*,*,#55900,.T.);
#82168=ORIENTED_EDGE('',*,*,#55901,.T.);
#82169=ORIENTED_EDGE('',*,*,#55902,.F.);
#82170=ORIENTED_EDGE('',*,*,#55903,.T.);
#82171=ORIENTED_EDGE('',*,*,#55904,.T.);
#82172=ORIENTED_EDGE('',*,*,#55902,.T.);
#82173=ORIENTED_EDGE('',*,*,#55905,.T.);
#82174=ORIENTED_EDGE('',*,*,#55906,.T.);
#82175=ORIENTED_EDGE('',*,*,#55895,.F.);
#82176=ORIENTED_EDGE('',*,*,#55907,.T.);
#82177=ORIENTED_EDGE('',*,*,#55908,.T.);
#82178=ORIENTED_EDGE('',*,*,#55909,.F.);
#82179=ORIENTED_EDGE('',*,*,#55903,.F.);
#82180=ORIENTED_EDGE('',*,*,#55910,.F.);
#82181=ORIENTED_EDGE('',*,*,#55911,.F.);
#82182=ORIENTED_EDGE('',*,*,#55910,.T.);
#82183=ORIENTED_EDGE('',*,*,#55908,.F.);
#82184=ORIENTED_EDGE('',*,*,#55907,.F.);
#82185=ORIENTED_EDGE('',*,*,#55912,.F.);
#82186=ORIENTED_EDGE('',*,*,#55913,.F.);
#82187=ORIENTED_EDGE('',*,*,#55912,.T.);
#82188=ORIENTED_EDGE('',*,*,#55899,.F.);
#82189=ORIENTED_EDGE('',*,*,#55914,.F.);
#82190=ORIENTED_EDGE('',*,*,#55915,.F.);
#82191=ORIENTED_EDGE('',*,*,#55916,.T.);
#82192=ORIENTED_EDGE('',*,*,#55909,.T.);
#82193=ORIENTED_EDGE('',*,*,#54159,.F.);
#82194=ORIENTED_EDGE('',*,*,#54722,.T.);
#82195=ORIENTED_EDGE('',*,*,#55917,.F.);
#82196=ORIENTED_EDGE('',*,*,#55904,.F.);
#82197=ORIENTED_EDGE('',*,*,#55916,.F.);
#82198=ORIENTED_EDGE('',*,*,#54721,.F.);
#82199=ORIENTED_EDGE('',*,*,#55917,.T.);
#82200=ORIENTED_EDGE('',*,*,#55089,.F.);
#82201=ORIENTED_EDGE('',*,*,#55918,.F.);
#82202=ORIENTED_EDGE('',*,*,#55900,.F.);
#82203=ORIENTED_EDGE('',*,*,#55918,.T.);
#82204=ORIENTED_EDGE('',*,*,#54342,.F.);
#82205=ORIENTED_EDGE('',*,*,#55919,.F.);
#82206=ORIENTED_EDGE('',*,*,#55901,.F.);
#82207=ORIENTED_EDGE('',*,*,#55919,.T.);
#82208=ORIENTED_EDGE('',*,*,#54341,.F.);
#82209=ORIENTED_EDGE('',*,*,#55920,.F.);
#82210=ORIENTED_EDGE('',*,*,#55906,.F.);
#82211=ORIENTED_EDGE('',*,*,#55905,.F.);
#82212=ORIENTED_EDGE('',*,*,#55920,.T.);
#82213=ORIENTED_EDGE('',*,*,#54340,.F.);
#82214=ORIENTED_EDGE('',*,*,#55921,.F.);
#82215=ORIENTED_EDGE('',*,*,#55896,.F.);
#82216=ORIENTED_EDGE('',*,*,#55922,.T.);
#82217=ORIENTED_EDGE('',*,*,#55897,.F.);
#82218=ORIENTED_EDGE('',*,*,#55921,.T.);
#82219=ORIENTED_EDGE('',*,*,#55090,.F.);
#82220=ORIENTED_EDGE('',*,*,#55923,.T.);
#82221=ORIENTED_EDGE('',*,*,#55898,.F.);
#82222=ORIENTED_EDGE('',*,*,#55922,.F.);
#82223=ORIENTED_EDGE('',*,*,#54724,.F.);
#82224=ORIENTED_EDGE('',*,*,#54157,.T.);
#82225=ORIENTED_EDGE('',*,*,#55914,.T.);
#82226=ORIENTED_EDGE('',*,*,#55923,.F.);
#82227=ORIENTED_EDGE('',*,*,#54723,.T.);
#82228=ORIENTED_EDGE('',*,*,#55913,.T.);
#82229=ORIENTED_EDGE('',*,*,#55915,.T.);
#82230=ORIENTED_EDGE('',*,*,#54156,.T.);
#82231=ORIENTED_EDGE('',*,*,#55911,.T.);
#82232=ORIENTED_EDGE('',*,*,#55924,.T.);
#82233=ORIENTED_EDGE('',*,*,#55925,.T.);
#82234=ORIENTED_EDGE('',*,*,#55926,.T.);
#82235=ORIENTED_EDGE('',*,*,#55927,.T.);
#82236=ORIENTED_EDGE('',*,*,#55928,.T.);
#82237=ORIENTED_EDGE('',*,*,#55929,.T.);
#82238=ORIENTED_EDGE('',*,*,#55930,.T.);
#82239=ORIENTED_EDGE('',*,*,#55931,.F.);
#82240=ORIENTED_EDGE('',*,*,#55932,.T.);
#82241=ORIENTED_EDGE('',*,*,#55933,.T.);
#82242=ORIENTED_EDGE('',*,*,#55931,.T.);
#82243=ORIENTED_EDGE('',*,*,#55934,.T.);
#82244=ORIENTED_EDGE('',*,*,#55935,.T.);
#82245=ORIENTED_EDGE('',*,*,#55924,.F.);
#82246=ORIENTED_EDGE('',*,*,#55936,.T.);
#82247=ORIENTED_EDGE('',*,*,#55937,.T.);
#82248=ORIENTED_EDGE('',*,*,#55938,.F.);
#82249=ORIENTED_EDGE('',*,*,#55932,.F.);
#82250=ORIENTED_EDGE('',*,*,#55939,.F.);
#82251=ORIENTED_EDGE('',*,*,#55940,.F.);
#82252=ORIENTED_EDGE('',*,*,#55939,.T.);
#82253=ORIENTED_EDGE('',*,*,#55937,.F.);
#82254=ORIENTED_EDGE('',*,*,#55936,.F.);
#82255=ORIENTED_EDGE('',*,*,#55941,.F.);
#82256=ORIENTED_EDGE('',*,*,#55942,.F.);
#82257=ORIENTED_EDGE('',*,*,#55941,.T.);
#82258=ORIENTED_EDGE('',*,*,#55928,.F.);
#82259=ORIENTED_EDGE('',*,*,#55943,.F.);
#82260=ORIENTED_EDGE('',*,*,#55944,.F.);
#82261=ORIENTED_EDGE('',*,*,#55945,.T.);
#82262=ORIENTED_EDGE('',*,*,#55938,.T.);
#82263=ORIENTED_EDGE('',*,*,#54155,.F.);
#82264=ORIENTED_EDGE('',*,*,#54717,.T.);
#82265=ORIENTED_EDGE('',*,*,#55946,.F.);
#82266=ORIENTED_EDGE('',*,*,#55933,.F.);
#82267=ORIENTED_EDGE('',*,*,#55945,.F.);
#82268=ORIENTED_EDGE('',*,*,#54716,.F.);
#82269=ORIENTED_EDGE('',*,*,#55946,.T.);
#82270=ORIENTED_EDGE('',*,*,#55087,.F.);
#82271=ORIENTED_EDGE('',*,*,#55947,.F.);
#82272=ORIENTED_EDGE('',*,*,#55929,.F.);
#82273=ORIENTED_EDGE('',*,*,#55947,.T.);
#82274=ORIENTED_EDGE('',*,*,#54346,.F.);
#82275=ORIENTED_EDGE('',*,*,#55948,.F.);
#82276=ORIENTED_EDGE('',*,*,#55930,.F.);
#82277=ORIENTED_EDGE('',*,*,#55948,.T.);
#82278=ORIENTED_EDGE('',*,*,#54345,.F.);
#82279=ORIENTED_EDGE('',*,*,#55949,.F.);
#82280=ORIENTED_EDGE('',*,*,#55935,.F.);
#82281=ORIENTED_EDGE('',*,*,#55934,.F.);
#82282=ORIENTED_EDGE('',*,*,#55949,.T.);
#82283=ORIENTED_EDGE('',*,*,#54344,.F.);
#82284=ORIENTED_EDGE('',*,*,#55950,.F.);
#82285=ORIENTED_EDGE('',*,*,#55925,.F.);
#82286=ORIENTED_EDGE('',*,*,#55951,.T.);
#82287=ORIENTED_EDGE('',*,*,#55926,.F.);
#82288=ORIENTED_EDGE('',*,*,#55950,.T.);
#82289=ORIENTED_EDGE('',*,*,#55088,.F.);
#82290=ORIENTED_EDGE('',*,*,#55952,.T.);
#82291=ORIENTED_EDGE('',*,*,#55927,.F.);
#82292=ORIENTED_EDGE('',*,*,#55951,.F.);
#82293=ORIENTED_EDGE('',*,*,#54719,.F.);
#82294=ORIENTED_EDGE('',*,*,#54153,.T.);
#82295=ORIENTED_EDGE('',*,*,#55943,.T.);
#82296=ORIENTED_EDGE('',*,*,#55952,.F.);
#82297=ORIENTED_EDGE('',*,*,#54718,.T.);
#82298=ORIENTED_EDGE('',*,*,#55942,.T.);
#82299=ORIENTED_EDGE('',*,*,#55944,.T.);
#82300=ORIENTED_EDGE('',*,*,#54152,.T.);
#82301=ORIENTED_EDGE('',*,*,#55940,.T.);
#82302=ORIENTED_EDGE('',*,*,#55953,.T.);
#82303=ORIENTED_EDGE('',*,*,#55954,.T.);
#82304=ORIENTED_EDGE('',*,*,#55955,.T.);
#82305=ORIENTED_EDGE('',*,*,#55956,.T.);
#82306=ORIENTED_EDGE('',*,*,#55957,.T.);
#82307=ORIENTED_EDGE('',*,*,#55958,.T.);
#82308=ORIENTED_EDGE('',*,*,#55959,.T.);
#82309=ORIENTED_EDGE('',*,*,#55960,.F.);
#82310=ORIENTED_EDGE('',*,*,#55961,.T.);
#82311=ORIENTED_EDGE('',*,*,#55962,.T.);
#82312=ORIENTED_EDGE('',*,*,#55960,.T.);
#82313=ORIENTED_EDGE('',*,*,#55963,.T.);
#82314=ORIENTED_EDGE('',*,*,#55964,.T.);
#82315=ORIENTED_EDGE('',*,*,#55953,.F.);
#82316=ORIENTED_EDGE('',*,*,#55965,.T.);
#82317=ORIENTED_EDGE('',*,*,#55966,.T.);
#82318=ORIENTED_EDGE('',*,*,#55967,.F.);
#82319=ORIENTED_EDGE('',*,*,#55961,.F.);
#82320=ORIENTED_EDGE('',*,*,#55968,.F.);
#82321=ORIENTED_EDGE('',*,*,#55969,.F.);
#82322=ORIENTED_EDGE('',*,*,#55968,.T.);
#82323=ORIENTED_EDGE('',*,*,#55966,.F.);
#82324=ORIENTED_EDGE('',*,*,#55965,.F.);
#82325=ORIENTED_EDGE('',*,*,#55970,.F.);
#82326=ORIENTED_EDGE('',*,*,#55971,.F.);
#82327=ORIENTED_EDGE('',*,*,#55970,.T.);
#82328=ORIENTED_EDGE('',*,*,#55957,.F.);
#82329=ORIENTED_EDGE('',*,*,#55972,.F.);
#82330=ORIENTED_EDGE('',*,*,#55973,.F.);
#82331=ORIENTED_EDGE('',*,*,#55974,.T.);
#82332=ORIENTED_EDGE('',*,*,#55967,.T.);
#82333=ORIENTED_EDGE('',*,*,#54151,.F.);
#82334=ORIENTED_EDGE('',*,*,#54712,.T.);
#82335=ORIENTED_EDGE('',*,*,#55975,.F.);
#82336=ORIENTED_EDGE('',*,*,#55962,.F.);
#82337=ORIENTED_EDGE('',*,*,#55974,.F.);
#82338=ORIENTED_EDGE('',*,*,#54711,.F.);
#82339=ORIENTED_EDGE('',*,*,#55975,.T.);
#82340=ORIENTED_EDGE('',*,*,#55085,.F.);
#82341=ORIENTED_EDGE('',*,*,#55976,.F.);
#82342=ORIENTED_EDGE('',*,*,#55958,.F.);
#82343=ORIENTED_EDGE('',*,*,#55976,.T.);
#82344=ORIENTED_EDGE('',*,*,#54350,.F.);
#82345=ORIENTED_EDGE('',*,*,#55977,.F.);
#82346=ORIENTED_EDGE('',*,*,#55959,.F.);
#82347=ORIENTED_EDGE('',*,*,#55977,.T.);
#82348=ORIENTED_EDGE('',*,*,#54349,.F.);
#82349=ORIENTED_EDGE('',*,*,#55978,.F.);
#82350=ORIENTED_EDGE('',*,*,#55964,.F.);
#82351=ORIENTED_EDGE('',*,*,#55963,.F.);
#82352=ORIENTED_EDGE('',*,*,#55978,.T.);
#82353=ORIENTED_EDGE('',*,*,#54348,.F.);
#82354=ORIENTED_EDGE('',*,*,#55979,.F.);
#82355=ORIENTED_EDGE('',*,*,#55954,.F.);
#82356=ORIENTED_EDGE('',*,*,#55980,.T.);
#82357=ORIENTED_EDGE('',*,*,#55955,.F.);
#82358=ORIENTED_EDGE('',*,*,#55979,.T.);
#82359=ORIENTED_EDGE('',*,*,#55086,.F.);
#82360=ORIENTED_EDGE('',*,*,#55981,.T.);
#82361=ORIENTED_EDGE('',*,*,#55956,.F.);
#82362=ORIENTED_EDGE('',*,*,#55980,.F.);
#82363=ORIENTED_EDGE('',*,*,#54714,.F.);
#82364=ORIENTED_EDGE('',*,*,#54149,.T.);
#82365=ORIENTED_EDGE('',*,*,#55972,.T.);
#82366=ORIENTED_EDGE('',*,*,#55981,.F.);
#82367=ORIENTED_EDGE('',*,*,#54713,.T.);
#82368=ORIENTED_EDGE('',*,*,#55971,.T.);
#82369=ORIENTED_EDGE('',*,*,#55973,.T.);
#82370=ORIENTED_EDGE('',*,*,#54148,.T.);
#82371=ORIENTED_EDGE('',*,*,#55969,.T.);
#82372=ORIENTED_EDGE('',*,*,#55982,.T.);
#82373=ORIENTED_EDGE('',*,*,#55983,.T.);
#82374=ORIENTED_EDGE('',*,*,#55984,.T.);
#82375=ORIENTED_EDGE('',*,*,#55985,.T.);
#82376=ORIENTED_EDGE('',*,*,#55986,.T.);
#82377=ORIENTED_EDGE('',*,*,#55987,.T.);
#82378=ORIENTED_EDGE('',*,*,#55988,.T.);
#82379=ORIENTED_EDGE('',*,*,#55989,.F.);
#82380=ORIENTED_EDGE('',*,*,#55990,.T.);
#82381=ORIENTED_EDGE('',*,*,#55991,.T.);
#82382=ORIENTED_EDGE('',*,*,#55989,.T.);
#82383=ORIENTED_EDGE('',*,*,#55992,.T.);
#82384=ORIENTED_EDGE('',*,*,#55993,.T.);
#82385=ORIENTED_EDGE('',*,*,#55982,.F.);
#82386=ORIENTED_EDGE('',*,*,#55994,.T.);
#82387=ORIENTED_EDGE('',*,*,#55995,.T.);
#82388=ORIENTED_EDGE('',*,*,#55996,.F.);
#82389=ORIENTED_EDGE('',*,*,#55990,.F.);
#82390=ORIENTED_EDGE('',*,*,#55997,.F.);
#82391=ORIENTED_EDGE('',*,*,#55998,.F.);
#82392=ORIENTED_EDGE('',*,*,#55997,.T.);
#82393=ORIENTED_EDGE('',*,*,#55995,.F.);
#82394=ORIENTED_EDGE('',*,*,#55994,.F.);
#82395=ORIENTED_EDGE('',*,*,#55999,.F.);
#82396=ORIENTED_EDGE('',*,*,#56000,.F.);
#82397=ORIENTED_EDGE('',*,*,#55999,.T.);
#82398=ORIENTED_EDGE('',*,*,#55986,.F.);
#82399=ORIENTED_EDGE('',*,*,#56001,.F.);
#82400=ORIENTED_EDGE('',*,*,#56002,.F.);
#82401=ORIENTED_EDGE('',*,*,#56003,.T.);
#82402=ORIENTED_EDGE('',*,*,#55996,.T.);
#82403=ORIENTED_EDGE('',*,*,#54147,.F.);
#82404=ORIENTED_EDGE('',*,*,#54707,.T.);
#82405=ORIENTED_EDGE('',*,*,#56004,.F.);
#82406=ORIENTED_EDGE('',*,*,#55991,.F.);
#82407=ORIENTED_EDGE('',*,*,#56003,.F.);
#82408=ORIENTED_EDGE('',*,*,#54706,.F.);
#82409=ORIENTED_EDGE('',*,*,#56004,.T.);
#82410=ORIENTED_EDGE('',*,*,#55083,.F.);
#82411=ORIENTED_EDGE('',*,*,#56005,.F.);
#82412=ORIENTED_EDGE('',*,*,#55987,.F.);
#82413=ORIENTED_EDGE('',*,*,#56005,.T.);
#82414=ORIENTED_EDGE('',*,*,#54354,.F.);
#82415=ORIENTED_EDGE('',*,*,#56006,.F.);
#82416=ORIENTED_EDGE('',*,*,#55988,.F.);
#82417=ORIENTED_EDGE('',*,*,#56006,.T.);
#82418=ORIENTED_EDGE('',*,*,#54353,.F.);
#82419=ORIENTED_EDGE('',*,*,#56007,.F.);
#82420=ORIENTED_EDGE('',*,*,#55993,.F.);
#82421=ORIENTED_EDGE('',*,*,#55992,.F.);
#82422=ORIENTED_EDGE('',*,*,#56007,.T.);
#82423=ORIENTED_EDGE('',*,*,#54352,.F.);
#82424=ORIENTED_EDGE('',*,*,#56008,.F.);
#82425=ORIENTED_EDGE('',*,*,#55983,.F.);
#82426=ORIENTED_EDGE('',*,*,#56009,.T.);
#82427=ORIENTED_EDGE('',*,*,#55984,.F.);
#82428=ORIENTED_EDGE('',*,*,#56008,.T.);
#82429=ORIENTED_EDGE('',*,*,#55084,.F.);
#82430=ORIENTED_EDGE('',*,*,#56010,.T.);
#82431=ORIENTED_EDGE('',*,*,#55985,.F.);
#82432=ORIENTED_EDGE('',*,*,#56009,.F.);
#82433=ORIENTED_EDGE('',*,*,#54709,.F.);
#82434=ORIENTED_EDGE('',*,*,#54145,.T.);
#82435=ORIENTED_EDGE('',*,*,#56001,.T.);
#82436=ORIENTED_EDGE('',*,*,#56010,.F.);
#82437=ORIENTED_EDGE('',*,*,#54708,.T.);
#82438=ORIENTED_EDGE('',*,*,#56000,.T.);
#82439=ORIENTED_EDGE('',*,*,#56002,.T.);
#82440=ORIENTED_EDGE('',*,*,#54144,.T.);
#82441=ORIENTED_EDGE('',*,*,#55998,.T.);
#82442=ORIENTED_EDGE('',*,*,#56011,.T.);
#82443=ORIENTED_EDGE('',*,*,#56012,.T.);
#82444=ORIENTED_EDGE('',*,*,#56013,.T.);
#82445=ORIENTED_EDGE('',*,*,#56014,.T.);
#82446=ORIENTED_EDGE('',*,*,#56015,.T.);
#82447=ORIENTED_EDGE('',*,*,#56016,.T.);
#82448=ORIENTED_EDGE('',*,*,#56017,.T.);
#82449=ORIENTED_EDGE('',*,*,#56018,.F.);
#82450=ORIENTED_EDGE('',*,*,#56019,.T.);
#82451=ORIENTED_EDGE('',*,*,#56020,.T.);
#82452=ORIENTED_EDGE('',*,*,#56018,.T.);
#82453=ORIENTED_EDGE('',*,*,#56021,.T.);
#82454=ORIENTED_EDGE('',*,*,#56022,.T.);
#82455=ORIENTED_EDGE('',*,*,#56011,.F.);
#82456=ORIENTED_EDGE('',*,*,#56023,.T.);
#82457=ORIENTED_EDGE('',*,*,#56024,.T.);
#82458=ORIENTED_EDGE('',*,*,#56025,.F.);
#82459=ORIENTED_EDGE('',*,*,#56019,.F.);
#82460=ORIENTED_EDGE('',*,*,#56026,.F.);
#82461=ORIENTED_EDGE('',*,*,#56027,.F.);
#82462=ORIENTED_EDGE('',*,*,#56026,.T.);
#82463=ORIENTED_EDGE('',*,*,#56024,.F.);
#82464=ORIENTED_EDGE('',*,*,#56023,.F.);
#82465=ORIENTED_EDGE('',*,*,#56028,.F.);
#82466=ORIENTED_EDGE('',*,*,#56029,.F.);
#82467=ORIENTED_EDGE('',*,*,#56028,.T.);
#82468=ORIENTED_EDGE('',*,*,#56015,.F.);
#82469=ORIENTED_EDGE('',*,*,#56030,.F.);
#82470=ORIENTED_EDGE('',*,*,#56031,.F.);
#82471=ORIENTED_EDGE('',*,*,#56032,.T.);
#82472=ORIENTED_EDGE('',*,*,#56025,.T.);
#82473=ORIENTED_EDGE('',*,*,#54143,.F.);
#82474=ORIENTED_EDGE('',*,*,#54702,.T.);
#82475=ORIENTED_EDGE('',*,*,#56033,.F.);
#82476=ORIENTED_EDGE('',*,*,#56020,.F.);
#82477=ORIENTED_EDGE('',*,*,#56032,.F.);
#82478=ORIENTED_EDGE('',*,*,#54701,.F.);
#82479=ORIENTED_EDGE('',*,*,#56033,.T.);
#82480=ORIENTED_EDGE('',*,*,#55081,.F.);
#82481=ORIENTED_EDGE('',*,*,#56034,.F.);
#82482=ORIENTED_EDGE('',*,*,#56016,.F.);
#82483=ORIENTED_EDGE('',*,*,#56034,.T.);
#82484=ORIENTED_EDGE('',*,*,#54358,.F.);
#82485=ORIENTED_EDGE('',*,*,#56035,.F.);
#82486=ORIENTED_EDGE('',*,*,#56017,.F.);
#82487=ORIENTED_EDGE('',*,*,#56035,.T.);
#82488=ORIENTED_EDGE('',*,*,#54357,.F.);
#82489=ORIENTED_EDGE('',*,*,#56036,.F.);
#82490=ORIENTED_EDGE('',*,*,#56022,.F.);
#82491=ORIENTED_EDGE('',*,*,#56021,.F.);
#82492=ORIENTED_EDGE('',*,*,#56036,.T.);
#82493=ORIENTED_EDGE('',*,*,#54356,.F.);
#82494=ORIENTED_EDGE('',*,*,#56037,.F.);
#82495=ORIENTED_EDGE('',*,*,#56012,.F.);
#82496=ORIENTED_EDGE('',*,*,#56038,.T.);
#82497=ORIENTED_EDGE('',*,*,#56013,.F.);
#82498=ORIENTED_EDGE('',*,*,#56037,.T.);
#82499=ORIENTED_EDGE('',*,*,#55082,.F.);
#82500=ORIENTED_EDGE('',*,*,#56039,.T.);
#82501=ORIENTED_EDGE('',*,*,#56014,.F.);
#82502=ORIENTED_EDGE('',*,*,#56038,.F.);
#82503=ORIENTED_EDGE('',*,*,#54704,.F.);
#82504=ORIENTED_EDGE('',*,*,#54141,.T.);
#82505=ORIENTED_EDGE('',*,*,#56030,.T.);
#82506=ORIENTED_EDGE('',*,*,#56039,.F.);
#82507=ORIENTED_EDGE('',*,*,#54703,.T.);
#82508=ORIENTED_EDGE('',*,*,#56029,.T.);
#82509=ORIENTED_EDGE('',*,*,#56031,.T.);
#82510=ORIENTED_EDGE('',*,*,#54140,.T.);
#82511=ORIENTED_EDGE('',*,*,#56027,.T.);
#82512=ORIENTED_EDGE('',*,*,#56040,.T.);
#82513=ORIENTED_EDGE('',*,*,#56041,.T.);
#82514=ORIENTED_EDGE('',*,*,#56042,.T.);
#82515=ORIENTED_EDGE('',*,*,#56043,.T.);
#82516=ORIENTED_EDGE('',*,*,#56044,.T.);
#82517=ORIENTED_EDGE('',*,*,#56045,.T.);
#82518=ORIENTED_EDGE('',*,*,#56046,.T.);
#82519=ORIENTED_EDGE('',*,*,#56047,.F.);
#82520=ORIENTED_EDGE('',*,*,#56048,.T.);
#82521=ORIENTED_EDGE('',*,*,#56049,.T.);
#82522=ORIENTED_EDGE('',*,*,#56047,.T.);
#82523=ORIENTED_EDGE('',*,*,#56050,.T.);
#82524=ORIENTED_EDGE('',*,*,#56051,.T.);
#82525=ORIENTED_EDGE('',*,*,#56040,.F.);
#82526=ORIENTED_EDGE('',*,*,#56052,.T.);
#82527=ORIENTED_EDGE('',*,*,#56053,.T.);
#82528=ORIENTED_EDGE('',*,*,#56054,.F.);
#82529=ORIENTED_EDGE('',*,*,#56048,.F.);
#82530=ORIENTED_EDGE('',*,*,#56055,.F.);
#82531=ORIENTED_EDGE('',*,*,#56056,.F.);
#82532=ORIENTED_EDGE('',*,*,#56055,.T.);
#82533=ORIENTED_EDGE('',*,*,#56053,.F.);
#82534=ORIENTED_EDGE('',*,*,#56052,.F.);
#82535=ORIENTED_EDGE('',*,*,#56057,.F.);
#82536=ORIENTED_EDGE('',*,*,#56058,.F.);
#82537=ORIENTED_EDGE('',*,*,#56057,.T.);
#82538=ORIENTED_EDGE('',*,*,#56044,.F.);
#82539=ORIENTED_EDGE('',*,*,#56059,.F.);
#82540=ORIENTED_EDGE('',*,*,#56060,.F.);
#82541=ORIENTED_EDGE('',*,*,#56061,.T.);
#82542=ORIENTED_EDGE('',*,*,#56054,.T.);
#82543=ORIENTED_EDGE('',*,*,#54139,.F.);
#82544=ORIENTED_EDGE('',*,*,#54697,.T.);
#82545=ORIENTED_EDGE('',*,*,#56062,.F.);
#82546=ORIENTED_EDGE('',*,*,#56049,.F.);
#82547=ORIENTED_EDGE('',*,*,#56061,.F.);
#82548=ORIENTED_EDGE('',*,*,#54696,.F.);
#82549=ORIENTED_EDGE('',*,*,#56062,.T.);
#82550=ORIENTED_EDGE('',*,*,#55079,.F.);
#82551=ORIENTED_EDGE('',*,*,#56063,.F.);
#82552=ORIENTED_EDGE('',*,*,#56045,.F.);
#82553=ORIENTED_EDGE('',*,*,#56063,.T.);
#82554=ORIENTED_EDGE('',*,*,#54362,.F.);
#82555=ORIENTED_EDGE('',*,*,#56064,.F.);
#82556=ORIENTED_EDGE('',*,*,#56046,.F.);
#82557=ORIENTED_EDGE('',*,*,#56064,.T.);
#82558=ORIENTED_EDGE('',*,*,#54361,.F.);
#82559=ORIENTED_EDGE('',*,*,#56065,.F.);
#82560=ORIENTED_EDGE('',*,*,#56051,.F.);
#82561=ORIENTED_EDGE('',*,*,#56050,.F.);
#82562=ORIENTED_EDGE('',*,*,#56065,.T.);
#82563=ORIENTED_EDGE('',*,*,#54360,.F.);
#82564=ORIENTED_EDGE('',*,*,#56066,.F.);
#82565=ORIENTED_EDGE('',*,*,#56041,.F.);
#82566=ORIENTED_EDGE('',*,*,#56067,.T.);
#82567=ORIENTED_EDGE('',*,*,#56042,.F.);
#82568=ORIENTED_EDGE('',*,*,#56066,.T.);
#82569=ORIENTED_EDGE('',*,*,#55080,.F.);
#82570=ORIENTED_EDGE('',*,*,#56068,.T.);
#82571=ORIENTED_EDGE('',*,*,#56043,.F.);
#82572=ORIENTED_EDGE('',*,*,#56067,.F.);
#82573=ORIENTED_EDGE('',*,*,#54699,.F.);
#82574=ORIENTED_EDGE('',*,*,#54137,.T.);
#82575=ORIENTED_EDGE('',*,*,#56059,.T.);
#82576=ORIENTED_EDGE('',*,*,#56068,.F.);
#82577=ORIENTED_EDGE('',*,*,#54698,.T.);
#82578=ORIENTED_EDGE('',*,*,#56058,.T.);
#82579=ORIENTED_EDGE('',*,*,#56060,.T.);
#82580=ORIENTED_EDGE('',*,*,#54136,.T.);
#82581=ORIENTED_EDGE('',*,*,#56056,.T.);
#82582=ORIENTED_EDGE('',*,*,#56069,.T.);
#82583=ORIENTED_EDGE('',*,*,#56070,.T.);
#82584=ORIENTED_EDGE('',*,*,#56071,.T.);
#82585=ORIENTED_EDGE('',*,*,#56072,.T.);
#82586=ORIENTED_EDGE('',*,*,#56073,.T.);
#82587=ORIENTED_EDGE('',*,*,#56074,.T.);
#82588=ORIENTED_EDGE('',*,*,#56075,.T.);
#82589=ORIENTED_EDGE('',*,*,#56076,.F.);
#82590=ORIENTED_EDGE('',*,*,#56077,.T.);
#82591=ORIENTED_EDGE('',*,*,#56078,.T.);
#82592=ORIENTED_EDGE('',*,*,#56076,.T.);
#82593=ORIENTED_EDGE('',*,*,#56079,.T.);
#82594=ORIENTED_EDGE('',*,*,#56080,.T.);
#82595=ORIENTED_EDGE('',*,*,#56069,.F.);
#82596=ORIENTED_EDGE('',*,*,#56081,.T.);
#82597=ORIENTED_EDGE('',*,*,#56082,.T.);
#82598=ORIENTED_EDGE('',*,*,#56083,.F.);
#82599=ORIENTED_EDGE('',*,*,#56077,.F.);
#82600=ORIENTED_EDGE('',*,*,#56084,.F.);
#82601=ORIENTED_EDGE('',*,*,#56085,.F.);
#82602=ORIENTED_EDGE('',*,*,#56084,.T.);
#82603=ORIENTED_EDGE('',*,*,#56082,.F.);
#82604=ORIENTED_EDGE('',*,*,#56081,.F.);
#82605=ORIENTED_EDGE('',*,*,#56086,.F.);
#82606=ORIENTED_EDGE('',*,*,#56087,.F.);
#82607=ORIENTED_EDGE('',*,*,#56086,.T.);
#82608=ORIENTED_EDGE('',*,*,#56073,.F.);
#82609=ORIENTED_EDGE('',*,*,#56088,.F.);
#82610=ORIENTED_EDGE('',*,*,#56089,.F.);
#82611=ORIENTED_EDGE('',*,*,#56090,.T.);
#82612=ORIENTED_EDGE('',*,*,#56083,.T.);
#82613=ORIENTED_EDGE('',*,*,#54135,.F.);
#82614=ORIENTED_EDGE('',*,*,#54692,.T.);
#82615=ORIENTED_EDGE('',*,*,#56091,.F.);
#82616=ORIENTED_EDGE('',*,*,#56078,.F.);
#82617=ORIENTED_EDGE('',*,*,#56090,.F.);
#82618=ORIENTED_EDGE('',*,*,#54691,.F.);
#82619=ORIENTED_EDGE('',*,*,#56091,.T.);
#82620=ORIENTED_EDGE('',*,*,#55077,.F.);
#82621=ORIENTED_EDGE('',*,*,#56092,.F.);
#82622=ORIENTED_EDGE('',*,*,#56074,.F.);
#82623=ORIENTED_EDGE('',*,*,#56092,.T.);
#82624=ORIENTED_EDGE('',*,*,#54366,.F.);
#82625=ORIENTED_EDGE('',*,*,#56093,.F.);
#82626=ORIENTED_EDGE('',*,*,#56075,.F.);
#82627=ORIENTED_EDGE('',*,*,#56093,.T.);
#82628=ORIENTED_EDGE('',*,*,#54365,.F.);
#82629=ORIENTED_EDGE('',*,*,#56094,.F.);
#82630=ORIENTED_EDGE('',*,*,#56080,.F.);
#82631=ORIENTED_EDGE('',*,*,#56079,.F.);
#82632=ORIENTED_EDGE('',*,*,#56094,.T.);
#82633=ORIENTED_EDGE('',*,*,#54364,.F.);
#82634=ORIENTED_EDGE('',*,*,#56095,.F.);
#82635=ORIENTED_EDGE('',*,*,#56070,.F.);
#82636=ORIENTED_EDGE('',*,*,#56096,.T.);
#82637=ORIENTED_EDGE('',*,*,#56071,.F.);
#82638=ORIENTED_EDGE('',*,*,#56095,.T.);
#82639=ORIENTED_EDGE('',*,*,#55078,.F.);
#82640=ORIENTED_EDGE('',*,*,#56097,.T.);
#82641=ORIENTED_EDGE('',*,*,#56072,.F.);
#82642=ORIENTED_EDGE('',*,*,#56096,.F.);
#82643=ORIENTED_EDGE('',*,*,#54694,.F.);
#82644=ORIENTED_EDGE('',*,*,#54133,.T.);
#82645=ORIENTED_EDGE('',*,*,#56088,.T.);
#82646=ORIENTED_EDGE('',*,*,#56097,.F.);
#82647=ORIENTED_EDGE('',*,*,#54693,.T.);
#82648=ORIENTED_EDGE('',*,*,#56087,.T.);
#82649=ORIENTED_EDGE('',*,*,#56089,.T.);
#82650=ORIENTED_EDGE('',*,*,#54132,.T.);
#82651=ORIENTED_EDGE('',*,*,#56085,.T.);
#82652=ORIENTED_EDGE('',*,*,#56098,.T.);
#82653=ORIENTED_EDGE('',*,*,#56099,.T.);
#82654=ORIENTED_EDGE('',*,*,#56100,.T.);
#82655=ORIENTED_EDGE('',*,*,#56101,.T.);
#82656=ORIENTED_EDGE('',*,*,#56102,.T.);
#82657=ORIENTED_EDGE('',*,*,#56103,.T.);
#82658=ORIENTED_EDGE('',*,*,#56104,.T.);
#82659=ORIENTED_EDGE('',*,*,#56105,.F.);
#82660=ORIENTED_EDGE('',*,*,#56106,.T.);
#82661=ORIENTED_EDGE('',*,*,#56107,.T.);
#82662=ORIENTED_EDGE('',*,*,#56105,.T.);
#82663=ORIENTED_EDGE('',*,*,#56108,.T.);
#82664=ORIENTED_EDGE('',*,*,#56109,.T.);
#82665=ORIENTED_EDGE('',*,*,#56098,.F.);
#82666=ORIENTED_EDGE('',*,*,#56110,.T.);
#82667=ORIENTED_EDGE('',*,*,#56111,.T.);
#82668=ORIENTED_EDGE('',*,*,#56112,.F.);
#82669=ORIENTED_EDGE('',*,*,#56106,.F.);
#82670=ORIENTED_EDGE('',*,*,#56113,.F.);
#82671=ORIENTED_EDGE('',*,*,#56114,.F.);
#82672=ORIENTED_EDGE('',*,*,#56113,.T.);
#82673=ORIENTED_EDGE('',*,*,#56111,.F.);
#82674=ORIENTED_EDGE('',*,*,#56110,.F.);
#82675=ORIENTED_EDGE('',*,*,#56115,.F.);
#82676=ORIENTED_EDGE('',*,*,#56116,.F.);
#82677=ORIENTED_EDGE('',*,*,#56115,.T.);
#82678=ORIENTED_EDGE('',*,*,#56102,.F.);
#82679=ORIENTED_EDGE('',*,*,#56117,.F.);
#82680=ORIENTED_EDGE('',*,*,#56118,.F.);
#82681=ORIENTED_EDGE('',*,*,#56119,.T.);
#82682=ORIENTED_EDGE('',*,*,#56112,.T.);
#82683=ORIENTED_EDGE('',*,*,#54131,.F.);
#82684=ORIENTED_EDGE('',*,*,#54687,.T.);
#82685=ORIENTED_EDGE('',*,*,#56120,.F.);
#82686=ORIENTED_EDGE('',*,*,#56107,.F.);
#82687=ORIENTED_EDGE('',*,*,#56119,.F.);
#82688=ORIENTED_EDGE('',*,*,#54686,.F.);
#82689=ORIENTED_EDGE('',*,*,#56120,.T.);
#82690=ORIENTED_EDGE('',*,*,#55075,.F.);
#82691=ORIENTED_EDGE('',*,*,#56121,.F.);
#82692=ORIENTED_EDGE('',*,*,#56103,.F.);
#82693=ORIENTED_EDGE('',*,*,#56121,.T.);
#82694=ORIENTED_EDGE('',*,*,#54370,.F.);
#82695=ORIENTED_EDGE('',*,*,#56122,.F.);
#82696=ORIENTED_EDGE('',*,*,#56104,.F.);
#82697=ORIENTED_EDGE('',*,*,#56122,.T.);
#82698=ORIENTED_EDGE('',*,*,#54369,.F.);
#82699=ORIENTED_EDGE('',*,*,#56123,.F.);
#82700=ORIENTED_EDGE('',*,*,#56109,.F.);
#82701=ORIENTED_EDGE('',*,*,#56108,.F.);
#82702=ORIENTED_EDGE('',*,*,#56123,.T.);
#82703=ORIENTED_EDGE('',*,*,#54368,.F.);
#82704=ORIENTED_EDGE('',*,*,#56124,.F.);
#82705=ORIENTED_EDGE('',*,*,#56099,.F.);
#82706=ORIENTED_EDGE('',*,*,#56125,.T.);
#82707=ORIENTED_EDGE('',*,*,#56100,.F.);
#82708=ORIENTED_EDGE('',*,*,#56124,.T.);
#82709=ORIENTED_EDGE('',*,*,#55076,.F.);
#82710=ORIENTED_EDGE('',*,*,#56126,.T.);
#82711=ORIENTED_EDGE('',*,*,#56101,.F.);
#82712=ORIENTED_EDGE('',*,*,#56125,.F.);
#82713=ORIENTED_EDGE('',*,*,#54689,.F.);
#82714=ORIENTED_EDGE('',*,*,#54129,.T.);
#82715=ORIENTED_EDGE('',*,*,#56117,.T.);
#82716=ORIENTED_EDGE('',*,*,#56126,.F.);
#82717=ORIENTED_EDGE('',*,*,#54688,.T.);
#82718=ORIENTED_EDGE('',*,*,#56116,.T.);
#82719=ORIENTED_EDGE('',*,*,#56118,.T.);
#82720=ORIENTED_EDGE('',*,*,#54128,.T.);
#82721=ORIENTED_EDGE('',*,*,#56114,.T.);
#82722=ORIENTED_EDGE('',*,*,#56127,.T.);
#82723=ORIENTED_EDGE('',*,*,#56128,.T.);
#82724=ORIENTED_EDGE('',*,*,#56129,.T.);
#82725=ORIENTED_EDGE('',*,*,#56130,.T.);
#82726=ORIENTED_EDGE('',*,*,#56131,.T.);
#82727=ORIENTED_EDGE('',*,*,#56132,.T.);
#82728=ORIENTED_EDGE('',*,*,#56133,.T.);
#82729=ORIENTED_EDGE('',*,*,#56134,.F.);
#82730=ORIENTED_EDGE('',*,*,#56135,.T.);
#82731=ORIENTED_EDGE('',*,*,#56136,.T.);
#82732=ORIENTED_EDGE('',*,*,#56134,.T.);
#82733=ORIENTED_EDGE('',*,*,#56137,.T.);
#82734=ORIENTED_EDGE('',*,*,#56138,.T.);
#82735=ORIENTED_EDGE('',*,*,#56127,.F.);
#82736=ORIENTED_EDGE('',*,*,#56139,.T.);
#82737=ORIENTED_EDGE('',*,*,#56140,.T.);
#82738=ORIENTED_EDGE('',*,*,#56141,.F.);
#82739=ORIENTED_EDGE('',*,*,#56135,.F.);
#82740=ORIENTED_EDGE('',*,*,#56142,.F.);
#82741=ORIENTED_EDGE('',*,*,#56143,.F.);
#82742=ORIENTED_EDGE('',*,*,#56142,.T.);
#82743=ORIENTED_EDGE('',*,*,#56140,.F.);
#82744=ORIENTED_EDGE('',*,*,#56139,.F.);
#82745=ORIENTED_EDGE('',*,*,#56144,.F.);
#82746=ORIENTED_EDGE('',*,*,#56145,.F.);
#82747=ORIENTED_EDGE('',*,*,#56144,.T.);
#82748=ORIENTED_EDGE('',*,*,#56131,.F.);
#82749=ORIENTED_EDGE('',*,*,#56146,.F.);
#82750=ORIENTED_EDGE('',*,*,#56147,.F.);
#82751=ORIENTED_EDGE('',*,*,#56148,.T.);
#82752=ORIENTED_EDGE('',*,*,#56141,.T.);
#82753=ORIENTED_EDGE('',*,*,#54127,.F.);
#82754=ORIENTED_EDGE('',*,*,#54682,.T.);
#82755=ORIENTED_EDGE('',*,*,#56149,.F.);
#82756=ORIENTED_EDGE('',*,*,#56136,.F.);
#82757=ORIENTED_EDGE('',*,*,#56148,.F.);
#82758=ORIENTED_EDGE('',*,*,#54681,.F.);
#82759=ORIENTED_EDGE('',*,*,#56149,.T.);
#82760=ORIENTED_EDGE('',*,*,#55073,.F.);
#82761=ORIENTED_EDGE('',*,*,#56150,.F.);
#82762=ORIENTED_EDGE('',*,*,#56132,.F.);
#82763=ORIENTED_EDGE('',*,*,#56150,.T.);
#82764=ORIENTED_EDGE('',*,*,#54374,.F.);
#82765=ORIENTED_EDGE('',*,*,#56151,.F.);
#82766=ORIENTED_EDGE('',*,*,#56133,.F.);
#82767=ORIENTED_EDGE('',*,*,#56151,.T.);
#82768=ORIENTED_EDGE('',*,*,#54373,.F.);
#82769=ORIENTED_EDGE('',*,*,#56152,.F.);
#82770=ORIENTED_EDGE('',*,*,#56138,.F.);
#82771=ORIENTED_EDGE('',*,*,#56137,.F.);
#82772=ORIENTED_EDGE('',*,*,#56152,.T.);
#82773=ORIENTED_EDGE('',*,*,#54372,.F.);
#82774=ORIENTED_EDGE('',*,*,#56153,.F.);
#82775=ORIENTED_EDGE('',*,*,#56128,.F.);
#82776=ORIENTED_EDGE('',*,*,#56154,.T.);
#82777=ORIENTED_EDGE('',*,*,#56129,.F.);
#82778=ORIENTED_EDGE('',*,*,#56153,.T.);
#82779=ORIENTED_EDGE('',*,*,#55074,.F.);
#82780=ORIENTED_EDGE('',*,*,#56155,.T.);
#82781=ORIENTED_EDGE('',*,*,#56130,.F.);
#82782=ORIENTED_EDGE('',*,*,#56154,.F.);
#82783=ORIENTED_EDGE('',*,*,#54684,.F.);
#82784=ORIENTED_EDGE('',*,*,#54125,.T.);
#82785=ORIENTED_EDGE('',*,*,#56146,.T.);
#82786=ORIENTED_EDGE('',*,*,#56155,.F.);
#82787=ORIENTED_EDGE('',*,*,#54683,.T.);
#82788=ORIENTED_EDGE('',*,*,#56145,.T.);
#82789=ORIENTED_EDGE('',*,*,#56147,.T.);
#82790=ORIENTED_EDGE('',*,*,#54124,.T.);
#82791=ORIENTED_EDGE('',*,*,#56143,.T.);
#82792=ORIENTED_EDGE('',*,*,#56156,.T.);
#82793=ORIENTED_EDGE('',*,*,#56157,.T.);
#82794=ORIENTED_EDGE('',*,*,#56158,.T.);
#82795=ORIENTED_EDGE('',*,*,#56159,.T.);
#82796=ORIENTED_EDGE('',*,*,#56160,.T.);
#82797=ORIENTED_EDGE('',*,*,#56161,.T.);
#82798=ORIENTED_EDGE('',*,*,#56162,.T.);
#82799=ORIENTED_EDGE('',*,*,#56163,.F.);
#82800=ORIENTED_EDGE('',*,*,#56164,.T.);
#82801=ORIENTED_EDGE('',*,*,#56165,.T.);
#82802=ORIENTED_EDGE('',*,*,#56163,.T.);
#82803=ORIENTED_EDGE('',*,*,#56166,.T.);
#82804=ORIENTED_EDGE('',*,*,#56167,.T.);
#82805=ORIENTED_EDGE('',*,*,#56156,.F.);
#82806=ORIENTED_EDGE('',*,*,#56168,.T.);
#82807=ORIENTED_EDGE('',*,*,#56169,.T.);
#82808=ORIENTED_EDGE('',*,*,#56170,.F.);
#82809=ORIENTED_EDGE('',*,*,#56164,.F.);
#82810=ORIENTED_EDGE('',*,*,#56171,.F.);
#82811=ORIENTED_EDGE('',*,*,#56172,.F.);
#82812=ORIENTED_EDGE('',*,*,#56171,.T.);
#82813=ORIENTED_EDGE('',*,*,#56169,.F.);
#82814=ORIENTED_EDGE('',*,*,#56168,.F.);
#82815=ORIENTED_EDGE('',*,*,#56173,.F.);
#82816=ORIENTED_EDGE('',*,*,#56174,.F.);
#82817=ORIENTED_EDGE('',*,*,#56173,.T.);
#82818=ORIENTED_EDGE('',*,*,#56160,.F.);
#82819=ORIENTED_EDGE('',*,*,#56175,.F.);
#82820=ORIENTED_EDGE('',*,*,#56176,.F.);
#82821=ORIENTED_EDGE('',*,*,#56177,.T.);
#82822=ORIENTED_EDGE('',*,*,#56170,.T.);
#82823=ORIENTED_EDGE('',*,*,#54123,.F.);
#82824=ORIENTED_EDGE('',*,*,#54677,.T.);
#82825=ORIENTED_EDGE('',*,*,#56178,.F.);
#82826=ORIENTED_EDGE('',*,*,#56165,.F.);
#82827=ORIENTED_EDGE('',*,*,#56177,.F.);
#82828=ORIENTED_EDGE('',*,*,#54676,.F.);
#82829=ORIENTED_EDGE('',*,*,#56178,.T.);
#82830=ORIENTED_EDGE('',*,*,#55071,.F.);
#82831=ORIENTED_EDGE('',*,*,#56179,.F.);
#82832=ORIENTED_EDGE('',*,*,#56161,.F.);
#82833=ORIENTED_EDGE('',*,*,#56179,.T.);
#82834=ORIENTED_EDGE('',*,*,#54378,.F.);
#82835=ORIENTED_EDGE('',*,*,#56180,.F.);
#82836=ORIENTED_EDGE('',*,*,#56162,.F.);
#82837=ORIENTED_EDGE('',*,*,#56180,.T.);
#82838=ORIENTED_EDGE('',*,*,#54377,.F.);
#82839=ORIENTED_EDGE('',*,*,#56181,.F.);
#82840=ORIENTED_EDGE('',*,*,#56167,.F.);
#82841=ORIENTED_EDGE('',*,*,#56166,.F.);
#82842=ORIENTED_EDGE('',*,*,#56181,.T.);
#82843=ORIENTED_EDGE('',*,*,#54376,.F.);
#82844=ORIENTED_EDGE('',*,*,#56182,.F.);
#82845=ORIENTED_EDGE('',*,*,#56157,.F.);
#82846=ORIENTED_EDGE('',*,*,#56183,.T.);
#82847=ORIENTED_EDGE('',*,*,#56158,.F.);
#82848=ORIENTED_EDGE('',*,*,#56182,.T.);
#82849=ORIENTED_EDGE('',*,*,#55072,.F.);
#82850=ORIENTED_EDGE('',*,*,#56184,.T.);
#82851=ORIENTED_EDGE('',*,*,#56159,.F.);
#82852=ORIENTED_EDGE('',*,*,#56183,.F.);
#82853=ORIENTED_EDGE('',*,*,#54679,.F.);
#82854=ORIENTED_EDGE('',*,*,#54121,.T.);
#82855=ORIENTED_EDGE('',*,*,#56175,.T.);
#82856=ORIENTED_EDGE('',*,*,#56184,.F.);
#82857=ORIENTED_EDGE('',*,*,#54678,.T.);
#82858=ORIENTED_EDGE('',*,*,#56174,.T.);
#82859=ORIENTED_EDGE('',*,*,#56176,.T.);
#82860=ORIENTED_EDGE('',*,*,#54120,.T.);
#82861=ORIENTED_EDGE('',*,*,#56172,.T.);
#82862=ORIENTED_EDGE('',*,*,#56185,.T.);
#82863=ORIENTED_EDGE('',*,*,#56186,.T.);
#82864=ORIENTED_EDGE('',*,*,#56187,.T.);
#82865=ORIENTED_EDGE('',*,*,#56188,.T.);
#82866=ORIENTED_EDGE('',*,*,#56189,.T.);
#82867=ORIENTED_EDGE('',*,*,#56190,.T.);
#82868=ORIENTED_EDGE('',*,*,#56191,.T.);
#82869=ORIENTED_EDGE('',*,*,#56192,.F.);
#82870=ORIENTED_EDGE('',*,*,#56193,.T.);
#82871=ORIENTED_EDGE('',*,*,#56194,.T.);
#82872=ORIENTED_EDGE('',*,*,#56192,.T.);
#82873=ORIENTED_EDGE('',*,*,#56195,.T.);
#82874=ORIENTED_EDGE('',*,*,#56196,.T.);
#82875=ORIENTED_EDGE('',*,*,#56185,.F.);
#82876=ORIENTED_EDGE('',*,*,#56197,.T.);
#82877=ORIENTED_EDGE('',*,*,#56198,.T.);
#82878=ORIENTED_EDGE('',*,*,#56199,.F.);
#82879=ORIENTED_EDGE('',*,*,#56193,.F.);
#82880=ORIENTED_EDGE('',*,*,#56200,.F.);
#82881=ORIENTED_EDGE('',*,*,#56201,.F.);
#82882=ORIENTED_EDGE('',*,*,#56200,.T.);
#82883=ORIENTED_EDGE('',*,*,#56198,.F.);
#82884=ORIENTED_EDGE('',*,*,#56197,.F.);
#82885=ORIENTED_EDGE('',*,*,#56202,.F.);
#82886=ORIENTED_EDGE('',*,*,#56203,.F.);
#82887=ORIENTED_EDGE('',*,*,#56202,.T.);
#82888=ORIENTED_EDGE('',*,*,#56189,.F.);
#82889=ORIENTED_EDGE('',*,*,#56204,.F.);
#82890=ORIENTED_EDGE('',*,*,#56205,.F.);
#82891=ORIENTED_EDGE('',*,*,#56206,.T.);
#82892=ORIENTED_EDGE('',*,*,#56199,.T.);
#82893=ORIENTED_EDGE('',*,*,#54119,.F.);
#82894=ORIENTED_EDGE('',*,*,#54672,.T.);
#82895=ORIENTED_EDGE('',*,*,#56207,.F.);
#82896=ORIENTED_EDGE('',*,*,#56194,.F.);
#82897=ORIENTED_EDGE('',*,*,#56206,.F.);
#82898=ORIENTED_EDGE('',*,*,#54671,.F.);
#82899=ORIENTED_EDGE('',*,*,#56207,.T.);
#82900=ORIENTED_EDGE('',*,*,#55069,.F.);
#82901=ORIENTED_EDGE('',*,*,#56208,.F.);
#82902=ORIENTED_EDGE('',*,*,#56190,.F.);
#82903=ORIENTED_EDGE('',*,*,#56208,.T.);
#82904=ORIENTED_EDGE('',*,*,#54382,.F.);
#82905=ORIENTED_EDGE('',*,*,#56209,.F.);
#82906=ORIENTED_EDGE('',*,*,#56191,.F.);
#82907=ORIENTED_EDGE('',*,*,#56209,.T.);
#82908=ORIENTED_EDGE('',*,*,#54381,.F.);
#82909=ORIENTED_EDGE('',*,*,#56210,.F.);
#82910=ORIENTED_EDGE('',*,*,#56196,.F.);
#82911=ORIENTED_EDGE('',*,*,#56195,.F.);
#82912=ORIENTED_EDGE('',*,*,#56210,.T.);
#82913=ORIENTED_EDGE('',*,*,#54380,.F.);
#82914=ORIENTED_EDGE('',*,*,#56211,.F.);
#82915=ORIENTED_EDGE('',*,*,#56186,.F.);
#82916=ORIENTED_EDGE('',*,*,#56212,.T.);
#82917=ORIENTED_EDGE('',*,*,#56187,.F.);
#82918=ORIENTED_EDGE('',*,*,#56211,.T.);
#82919=ORIENTED_EDGE('',*,*,#55070,.F.);
#82920=ORIENTED_EDGE('',*,*,#56213,.T.);
#82921=ORIENTED_EDGE('',*,*,#56188,.F.);
#82922=ORIENTED_EDGE('',*,*,#56212,.F.);
#82923=ORIENTED_EDGE('',*,*,#54674,.F.);
#82924=ORIENTED_EDGE('',*,*,#54117,.T.);
#82925=ORIENTED_EDGE('',*,*,#56204,.T.);
#82926=ORIENTED_EDGE('',*,*,#56213,.F.);
#82927=ORIENTED_EDGE('',*,*,#54673,.T.);
#82928=ORIENTED_EDGE('',*,*,#56203,.T.);
#82929=ORIENTED_EDGE('',*,*,#56205,.T.);
#82930=ORIENTED_EDGE('',*,*,#54116,.T.);
#82931=ORIENTED_EDGE('',*,*,#56201,.T.);
#82932=ORIENTED_EDGE('',*,*,#56214,.T.);
#82933=ORIENTED_EDGE('',*,*,#56215,.T.);
#82934=ORIENTED_EDGE('',*,*,#56216,.T.);
#82935=ORIENTED_EDGE('',*,*,#56217,.T.);
#82936=ORIENTED_EDGE('',*,*,#56218,.T.);
#82937=ORIENTED_EDGE('',*,*,#56219,.T.);
#82938=ORIENTED_EDGE('',*,*,#56220,.T.);
#82939=ORIENTED_EDGE('',*,*,#56221,.F.);
#82940=ORIENTED_EDGE('',*,*,#56222,.T.);
#82941=ORIENTED_EDGE('',*,*,#56223,.T.);
#82942=ORIENTED_EDGE('',*,*,#56221,.T.);
#82943=ORIENTED_EDGE('',*,*,#56224,.T.);
#82944=ORIENTED_EDGE('',*,*,#56225,.T.);
#82945=ORIENTED_EDGE('',*,*,#56214,.F.);
#82946=ORIENTED_EDGE('',*,*,#56226,.T.);
#82947=ORIENTED_EDGE('',*,*,#56227,.T.);
#82948=ORIENTED_EDGE('',*,*,#56228,.F.);
#82949=ORIENTED_EDGE('',*,*,#56222,.F.);
#82950=ORIENTED_EDGE('',*,*,#56229,.F.);
#82951=ORIENTED_EDGE('',*,*,#56230,.F.);
#82952=ORIENTED_EDGE('',*,*,#56229,.T.);
#82953=ORIENTED_EDGE('',*,*,#56227,.F.);
#82954=ORIENTED_EDGE('',*,*,#56226,.F.);
#82955=ORIENTED_EDGE('',*,*,#56231,.F.);
#82956=ORIENTED_EDGE('',*,*,#56232,.F.);
#82957=ORIENTED_EDGE('',*,*,#56231,.T.);
#82958=ORIENTED_EDGE('',*,*,#56218,.F.);
#82959=ORIENTED_EDGE('',*,*,#56233,.F.);
#82960=ORIENTED_EDGE('',*,*,#56234,.F.);
#82961=ORIENTED_EDGE('',*,*,#56235,.T.);
#82962=ORIENTED_EDGE('',*,*,#56228,.T.);
#82963=ORIENTED_EDGE('',*,*,#54115,.F.);
#82964=ORIENTED_EDGE('',*,*,#54667,.T.);
#82965=ORIENTED_EDGE('',*,*,#56236,.F.);
#82966=ORIENTED_EDGE('',*,*,#56223,.F.);
#82967=ORIENTED_EDGE('',*,*,#56235,.F.);
#82968=ORIENTED_EDGE('',*,*,#54666,.F.);
#82969=ORIENTED_EDGE('',*,*,#56236,.T.);
#82970=ORIENTED_EDGE('',*,*,#55067,.F.);
#82971=ORIENTED_EDGE('',*,*,#56237,.F.);
#82972=ORIENTED_EDGE('',*,*,#56219,.F.);
#82973=ORIENTED_EDGE('',*,*,#56237,.T.);
#82974=ORIENTED_EDGE('',*,*,#54386,.F.);
#82975=ORIENTED_EDGE('',*,*,#56238,.F.);
#82976=ORIENTED_EDGE('',*,*,#56220,.F.);
#82977=ORIENTED_EDGE('',*,*,#56238,.T.);
#82978=ORIENTED_EDGE('',*,*,#54385,.F.);
#82979=ORIENTED_EDGE('',*,*,#56239,.F.);
#82980=ORIENTED_EDGE('',*,*,#56225,.F.);
#82981=ORIENTED_EDGE('',*,*,#56224,.F.);
#82982=ORIENTED_EDGE('',*,*,#56239,.T.);
#82983=ORIENTED_EDGE('',*,*,#54384,.F.);
#82984=ORIENTED_EDGE('',*,*,#56240,.F.);
#82985=ORIENTED_EDGE('',*,*,#56215,.F.);
#82986=ORIENTED_EDGE('',*,*,#56241,.T.);
#82987=ORIENTED_EDGE('',*,*,#56216,.F.);
#82988=ORIENTED_EDGE('',*,*,#56240,.T.);
#82989=ORIENTED_EDGE('',*,*,#55068,.F.);
#82990=ORIENTED_EDGE('',*,*,#56242,.T.);
#82991=ORIENTED_EDGE('',*,*,#56217,.F.);
#82992=ORIENTED_EDGE('',*,*,#56241,.F.);
#82993=ORIENTED_EDGE('',*,*,#54669,.F.);
#82994=ORIENTED_EDGE('',*,*,#54113,.T.);
#82995=ORIENTED_EDGE('',*,*,#56233,.T.);
#82996=ORIENTED_EDGE('',*,*,#56242,.F.);
#82997=ORIENTED_EDGE('',*,*,#54668,.T.);
#82998=ORIENTED_EDGE('',*,*,#56232,.T.);
#82999=ORIENTED_EDGE('',*,*,#56234,.T.);
#83000=ORIENTED_EDGE('',*,*,#54112,.T.);
#83001=ORIENTED_EDGE('',*,*,#56230,.T.);
#83002=ORIENTED_EDGE('',*,*,#56243,.T.);
#83003=ORIENTED_EDGE('',*,*,#56244,.T.);
#83004=ORIENTED_EDGE('',*,*,#56245,.T.);
#83005=ORIENTED_EDGE('',*,*,#56246,.T.);
#83006=ORIENTED_EDGE('',*,*,#56247,.T.);
#83007=ORIENTED_EDGE('',*,*,#56248,.T.);
#83008=ORIENTED_EDGE('',*,*,#56249,.T.);
#83009=ORIENTED_EDGE('',*,*,#56250,.F.);
#83010=ORIENTED_EDGE('',*,*,#56251,.T.);
#83011=ORIENTED_EDGE('',*,*,#56252,.T.);
#83012=ORIENTED_EDGE('',*,*,#56250,.T.);
#83013=ORIENTED_EDGE('',*,*,#56253,.T.);
#83014=ORIENTED_EDGE('',*,*,#56254,.T.);
#83015=ORIENTED_EDGE('',*,*,#56243,.F.);
#83016=ORIENTED_EDGE('',*,*,#56255,.T.);
#83017=ORIENTED_EDGE('',*,*,#56256,.T.);
#83018=ORIENTED_EDGE('',*,*,#56257,.F.);
#83019=ORIENTED_EDGE('',*,*,#56251,.F.);
#83020=ORIENTED_EDGE('',*,*,#56258,.F.);
#83021=ORIENTED_EDGE('',*,*,#56259,.F.);
#83022=ORIENTED_EDGE('',*,*,#56258,.T.);
#83023=ORIENTED_EDGE('',*,*,#56256,.F.);
#83024=ORIENTED_EDGE('',*,*,#56255,.F.);
#83025=ORIENTED_EDGE('',*,*,#56260,.F.);
#83026=ORIENTED_EDGE('',*,*,#56261,.F.);
#83027=ORIENTED_EDGE('',*,*,#56260,.T.);
#83028=ORIENTED_EDGE('',*,*,#56247,.F.);
#83029=ORIENTED_EDGE('',*,*,#56262,.F.);
#83030=ORIENTED_EDGE('',*,*,#56263,.F.);
#83031=ORIENTED_EDGE('',*,*,#56264,.T.);
#83032=ORIENTED_EDGE('',*,*,#56257,.T.);
#83033=ORIENTED_EDGE('',*,*,#54111,.F.);
#83034=ORIENTED_EDGE('',*,*,#54662,.T.);
#83035=ORIENTED_EDGE('',*,*,#56265,.F.);
#83036=ORIENTED_EDGE('',*,*,#56252,.F.);
#83037=ORIENTED_EDGE('',*,*,#56264,.F.);
#83038=ORIENTED_EDGE('',*,*,#54661,.F.);
#83039=ORIENTED_EDGE('',*,*,#56265,.T.);
#83040=ORIENTED_EDGE('',*,*,#55065,.F.);
#83041=ORIENTED_EDGE('',*,*,#56266,.F.);
#83042=ORIENTED_EDGE('',*,*,#56248,.F.);
#83043=ORIENTED_EDGE('',*,*,#56266,.T.);
#83044=ORIENTED_EDGE('',*,*,#54390,.F.);
#83045=ORIENTED_EDGE('',*,*,#56267,.F.);
#83046=ORIENTED_EDGE('',*,*,#56249,.F.);
#83047=ORIENTED_EDGE('',*,*,#56267,.T.);
#83048=ORIENTED_EDGE('',*,*,#54389,.F.);
#83049=ORIENTED_EDGE('',*,*,#56268,.F.);
#83050=ORIENTED_EDGE('',*,*,#56254,.F.);
#83051=ORIENTED_EDGE('',*,*,#56253,.F.);
#83052=ORIENTED_EDGE('',*,*,#56268,.T.);
#83053=ORIENTED_EDGE('',*,*,#54388,.F.);
#83054=ORIENTED_EDGE('',*,*,#56269,.F.);
#83055=ORIENTED_EDGE('',*,*,#56244,.F.);
#83056=ORIENTED_EDGE('',*,*,#56270,.T.);
#83057=ORIENTED_EDGE('',*,*,#56245,.F.);
#83058=ORIENTED_EDGE('',*,*,#56269,.T.);
#83059=ORIENTED_EDGE('',*,*,#55066,.F.);
#83060=ORIENTED_EDGE('',*,*,#56271,.T.);
#83061=ORIENTED_EDGE('',*,*,#56246,.F.);
#83062=ORIENTED_EDGE('',*,*,#56270,.F.);
#83063=ORIENTED_EDGE('',*,*,#54664,.F.);
#83064=ORIENTED_EDGE('',*,*,#54109,.T.);
#83065=ORIENTED_EDGE('',*,*,#56262,.T.);
#83066=ORIENTED_EDGE('',*,*,#56271,.F.);
#83067=ORIENTED_EDGE('',*,*,#54663,.T.);
#83068=ORIENTED_EDGE('',*,*,#56261,.T.);
#83069=ORIENTED_EDGE('',*,*,#56263,.T.);
#83070=ORIENTED_EDGE('',*,*,#54108,.T.);
#83071=ORIENTED_EDGE('',*,*,#56259,.T.);
#83072=ORIENTED_EDGE('',*,*,#56272,.T.);
#83073=ORIENTED_EDGE('',*,*,#56273,.T.);
#83074=ORIENTED_EDGE('',*,*,#56274,.T.);
#83075=ORIENTED_EDGE('',*,*,#56275,.T.);
#83076=ORIENTED_EDGE('',*,*,#56276,.T.);
#83077=ORIENTED_EDGE('',*,*,#56277,.T.);
#83078=ORIENTED_EDGE('',*,*,#56278,.T.);
#83079=ORIENTED_EDGE('',*,*,#56279,.F.);
#83080=ORIENTED_EDGE('',*,*,#56280,.T.);
#83081=ORIENTED_EDGE('',*,*,#56281,.T.);
#83082=ORIENTED_EDGE('',*,*,#56279,.T.);
#83083=ORIENTED_EDGE('',*,*,#56282,.T.);
#83084=ORIENTED_EDGE('',*,*,#56283,.T.);
#83085=ORIENTED_EDGE('',*,*,#56272,.F.);
#83086=ORIENTED_EDGE('',*,*,#56284,.T.);
#83087=ORIENTED_EDGE('',*,*,#56285,.T.);
#83088=ORIENTED_EDGE('',*,*,#56286,.F.);
#83089=ORIENTED_EDGE('',*,*,#56280,.F.);
#83090=ORIENTED_EDGE('',*,*,#56287,.F.);
#83091=ORIENTED_EDGE('',*,*,#56288,.F.);
#83092=ORIENTED_EDGE('',*,*,#56287,.T.);
#83093=ORIENTED_EDGE('',*,*,#56285,.F.);
#83094=ORIENTED_EDGE('',*,*,#56284,.F.);
#83095=ORIENTED_EDGE('',*,*,#56289,.F.);
#83096=ORIENTED_EDGE('',*,*,#56290,.F.);
#83097=ORIENTED_EDGE('',*,*,#56289,.T.);
#83098=ORIENTED_EDGE('',*,*,#56276,.F.);
#83099=ORIENTED_EDGE('',*,*,#56291,.F.);
#83100=ORIENTED_EDGE('',*,*,#56292,.F.);
#83101=ORIENTED_EDGE('',*,*,#56293,.T.);
#83102=ORIENTED_EDGE('',*,*,#56286,.T.);
#83103=ORIENTED_EDGE('',*,*,#54107,.F.);
#83104=ORIENTED_EDGE('',*,*,#54657,.T.);
#83105=ORIENTED_EDGE('',*,*,#56294,.F.);
#83106=ORIENTED_EDGE('',*,*,#56281,.F.);
#83107=ORIENTED_EDGE('',*,*,#56293,.F.);
#83108=ORIENTED_EDGE('',*,*,#54656,.F.);
#83109=ORIENTED_EDGE('',*,*,#56294,.T.);
#83110=ORIENTED_EDGE('',*,*,#55063,.F.);
#83111=ORIENTED_EDGE('',*,*,#56295,.F.);
#83112=ORIENTED_EDGE('',*,*,#56277,.F.);
#83113=ORIENTED_EDGE('',*,*,#56295,.T.);
#83114=ORIENTED_EDGE('',*,*,#54394,.F.);
#83115=ORIENTED_EDGE('',*,*,#56296,.F.);
#83116=ORIENTED_EDGE('',*,*,#56278,.F.);
#83117=ORIENTED_EDGE('',*,*,#56296,.T.);
#83118=ORIENTED_EDGE('',*,*,#54393,.F.);
#83119=ORIENTED_EDGE('',*,*,#56297,.F.);
#83120=ORIENTED_EDGE('',*,*,#56283,.F.);
#83121=ORIENTED_EDGE('',*,*,#56282,.F.);
#83122=ORIENTED_EDGE('',*,*,#56297,.T.);
#83123=ORIENTED_EDGE('',*,*,#54392,.F.);
#83124=ORIENTED_EDGE('',*,*,#56298,.F.);
#83125=ORIENTED_EDGE('',*,*,#56273,.F.);
#83126=ORIENTED_EDGE('',*,*,#56299,.T.);
#83127=ORIENTED_EDGE('',*,*,#56274,.F.);
#83128=ORIENTED_EDGE('',*,*,#56298,.T.);
#83129=ORIENTED_EDGE('',*,*,#55064,.F.);
#83130=ORIENTED_EDGE('',*,*,#56300,.T.);
#83131=ORIENTED_EDGE('',*,*,#56275,.F.);
#83132=ORIENTED_EDGE('',*,*,#56299,.F.);
#83133=ORIENTED_EDGE('',*,*,#54659,.F.);
#83134=ORIENTED_EDGE('',*,*,#54105,.T.);
#83135=ORIENTED_EDGE('',*,*,#56291,.T.);
#83136=ORIENTED_EDGE('',*,*,#56300,.F.);
#83137=ORIENTED_EDGE('',*,*,#54658,.T.);
#83138=ORIENTED_EDGE('',*,*,#56290,.T.);
#83139=ORIENTED_EDGE('',*,*,#56292,.T.);
#83140=ORIENTED_EDGE('',*,*,#54104,.T.);
#83141=ORIENTED_EDGE('',*,*,#56288,.T.);
#83142=ORIENTED_EDGE('',*,*,#56301,.T.);
#83143=ORIENTED_EDGE('',*,*,#56302,.T.);
#83144=ORIENTED_EDGE('',*,*,#56303,.T.);
#83145=ORIENTED_EDGE('',*,*,#56304,.T.);
#83146=ORIENTED_EDGE('',*,*,#56305,.T.);
#83147=ORIENTED_EDGE('',*,*,#56306,.T.);
#83148=ORIENTED_EDGE('',*,*,#56307,.T.);
#83149=ORIENTED_EDGE('',*,*,#56308,.F.);
#83150=ORIENTED_EDGE('',*,*,#56309,.T.);
#83151=ORIENTED_EDGE('',*,*,#56310,.T.);
#83152=ORIENTED_EDGE('',*,*,#56308,.T.);
#83153=ORIENTED_EDGE('',*,*,#56311,.T.);
#83154=ORIENTED_EDGE('',*,*,#56312,.T.);
#83155=ORIENTED_EDGE('',*,*,#56301,.F.);
#83156=ORIENTED_EDGE('',*,*,#56313,.T.);
#83157=ORIENTED_EDGE('',*,*,#56314,.T.);
#83158=ORIENTED_EDGE('',*,*,#56315,.F.);
#83159=ORIENTED_EDGE('',*,*,#56309,.F.);
#83160=ORIENTED_EDGE('',*,*,#56316,.F.);
#83161=ORIENTED_EDGE('',*,*,#56317,.F.);
#83162=ORIENTED_EDGE('',*,*,#56316,.T.);
#83163=ORIENTED_EDGE('',*,*,#56314,.F.);
#83164=ORIENTED_EDGE('',*,*,#56313,.F.);
#83165=ORIENTED_EDGE('',*,*,#56318,.F.);
#83166=ORIENTED_EDGE('',*,*,#56319,.F.);
#83167=ORIENTED_EDGE('',*,*,#56318,.T.);
#83168=ORIENTED_EDGE('',*,*,#56305,.F.);
#83169=ORIENTED_EDGE('',*,*,#56320,.F.);
#83170=ORIENTED_EDGE('',*,*,#56321,.F.);
#83171=ORIENTED_EDGE('',*,*,#56322,.T.);
#83172=ORIENTED_EDGE('',*,*,#56315,.T.);
#83173=ORIENTED_EDGE('',*,*,#54103,.F.);
#83174=ORIENTED_EDGE('',*,*,#54652,.T.);
#83175=ORIENTED_EDGE('',*,*,#56323,.F.);
#83176=ORIENTED_EDGE('',*,*,#56310,.F.);
#83177=ORIENTED_EDGE('',*,*,#56322,.F.);
#83178=ORIENTED_EDGE('',*,*,#54651,.F.);
#83179=ORIENTED_EDGE('',*,*,#56323,.T.);
#83180=ORIENTED_EDGE('',*,*,#55061,.F.);
#83181=ORIENTED_EDGE('',*,*,#56324,.F.);
#83182=ORIENTED_EDGE('',*,*,#56306,.F.);
#83183=ORIENTED_EDGE('',*,*,#56324,.T.);
#83184=ORIENTED_EDGE('',*,*,#54398,.F.);
#83185=ORIENTED_EDGE('',*,*,#56325,.F.);
#83186=ORIENTED_EDGE('',*,*,#56307,.F.);
#83187=ORIENTED_EDGE('',*,*,#56325,.T.);
#83188=ORIENTED_EDGE('',*,*,#54397,.F.);
#83189=ORIENTED_EDGE('',*,*,#56326,.F.);
#83190=ORIENTED_EDGE('',*,*,#56312,.F.);
#83191=ORIENTED_EDGE('',*,*,#56311,.F.);
#83192=ORIENTED_EDGE('',*,*,#56326,.T.);
#83193=ORIENTED_EDGE('',*,*,#54396,.F.);
#83194=ORIENTED_EDGE('',*,*,#56327,.F.);
#83195=ORIENTED_EDGE('',*,*,#56302,.F.);
#83196=ORIENTED_EDGE('',*,*,#56328,.T.);
#83197=ORIENTED_EDGE('',*,*,#56303,.F.);
#83198=ORIENTED_EDGE('',*,*,#56327,.T.);
#83199=ORIENTED_EDGE('',*,*,#55062,.F.);
#83200=ORIENTED_EDGE('',*,*,#56329,.T.);
#83201=ORIENTED_EDGE('',*,*,#56304,.F.);
#83202=ORIENTED_EDGE('',*,*,#56328,.F.);
#83203=ORIENTED_EDGE('',*,*,#54654,.F.);
#83204=ORIENTED_EDGE('',*,*,#54101,.T.);
#83205=ORIENTED_EDGE('',*,*,#56320,.T.);
#83206=ORIENTED_EDGE('',*,*,#56329,.F.);
#83207=ORIENTED_EDGE('',*,*,#54653,.T.);
#83208=ORIENTED_EDGE('',*,*,#56319,.T.);
#83209=ORIENTED_EDGE('',*,*,#56321,.T.);
#83210=ORIENTED_EDGE('',*,*,#54100,.T.);
#83211=ORIENTED_EDGE('',*,*,#56317,.T.);
#83212=ORIENTED_EDGE('',*,*,#56330,.T.);
#83213=ORIENTED_EDGE('',*,*,#56331,.T.);
#83214=ORIENTED_EDGE('',*,*,#56332,.T.);
#83215=ORIENTED_EDGE('',*,*,#56333,.T.);
#83216=ORIENTED_EDGE('',*,*,#56334,.T.);
#83217=ORIENTED_EDGE('',*,*,#56335,.T.);
#83218=ORIENTED_EDGE('',*,*,#56336,.T.);
#83219=ORIENTED_EDGE('',*,*,#56337,.F.);
#83220=ORIENTED_EDGE('',*,*,#56338,.T.);
#83221=ORIENTED_EDGE('',*,*,#56339,.T.);
#83222=ORIENTED_EDGE('',*,*,#56337,.T.);
#83223=ORIENTED_EDGE('',*,*,#56340,.T.);
#83224=ORIENTED_EDGE('',*,*,#56341,.T.);
#83225=ORIENTED_EDGE('',*,*,#56330,.F.);
#83226=ORIENTED_EDGE('',*,*,#56342,.T.);
#83227=ORIENTED_EDGE('',*,*,#56343,.T.);
#83228=ORIENTED_EDGE('',*,*,#56344,.F.);
#83229=ORIENTED_EDGE('',*,*,#56338,.F.);
#83230=ORIENTED_EDGE('',*,*,#56345,.F.);
#83231=ORIENTED_EDGE('',*,*,#56346,.F.);
#83232=ORIENTED_EDGE('',*,*,#56345,.T.);
#83233=ORIENTED_EDGE('',*,*,#56343,.F.);
#83234=ORIENTED_EDGE('',*,*,#56342,.F.);
#83235=ORIENTED_EDGE('',*,*,#56347,.F.);
#83236=ORIENTED_EDGE('',*,*,#56348,.F.);
#83237=ORIENTED_EDGE('',*,*,#56347,.T.);
#83238=ORIENTED_EDGE('',*,*,#56334,.F.);
#83239=ORIENTED_EDGE('',*,*,#56349,.F.);
#83240=ORIENTED_EDGE('',*,*,#56350,.F.);
#83241=ORIENTED_EDGE('',*,*,#56351,.T.);
#83242=ORIENTED_EDGE('',*,*,#56344,.T.);
#83243=ORIENTED_EDGE('',*,*,#54099,.F.);
#83244=ORIENTED_EDGE('',*,*,#54647,.T.);
#83245=ORIENTED_EDGE('',*,*,#56352,.F.);
#83246=ORIENTED_EDGE('',*,*,#56339,.F.);
#83247=ORIENTED_EDGE('',*,*,#56351,.F.);
#83248=ORIENTED_EDGE('',*,*,#54646,.F.);
#83249=ORIENTED_EDGE('',*,*,#56352,.T.);
#83250=ORIENTED_EDGE('',*,*,#55059,.F.);
#83251=ORIENTED_EDGE('',*,*,#56353,.F.);
#83252=ORIENTED_EDGE('',*,*,#56335,.F.);
#83253=ORIENTED_EDGE('',*,*,#56353,.T.);
#83254=ORIENTED_EDGE('',*,*,#54402,.F.);
#83255=ORIENTED_EDGE('',*,*,#56354,.F.);
#83256=ORIENTED_EDGE('',*,*,#56336,.F.);
#83257=ORIENTED_EDGE('',*,*,#56354,.T.);
#83258=ORIENTED_EDGE('',*,*,#54401,.F.);
#83259=ORIENTED_EDGE('',*,*,#56355,.F.);
#83260=ORIENTED_EDGE('',*,*,#56341,.F.);
#83261=ORIENTED_EDGE('',*,*,#56340,.F.);
#83262=ORIENTED_EDGE('',*,*,#56355,.T.);
#83263=ORIENTED_EDGE('',*,*,#54400,.F.);
#83264=ORIENTED_EDGE('',*,*,#56356,.F.);
#83265=ORIENTED_EDGE('',*,*,#56331,.F.);
#83266=ORIENTED_EDGE('',*,*,#56357,.T.);
#83267=ORIENTED_EDGE('',*,*,#56332,.F.);
#83268=ORIENTED_EDGE('',*,*,#56356,.T.);
#83269=ORIENTED_EDGE('',*,*,#55060,.F.);
#83270=ORIENTED_EDGE('',*,*,#56358,.T.);
#83271=ORIENTED_EDGE('',*,*,#56333,.F.);
#83272=ORIENTED_EDGE('',*,*,#56357,.F.);
#83273=ORIENTED_EDGE('',*,*,#54649,.F.);
#83274=ORIENTED_EDGE('',*,*,#54097,.T.);
#83275=ORIENTED_EDGE('',*,*,#56349,.T.);
#83276=ORIENTED_EDGE('',*,*,#56358,.F.);
#83277=ORIENTED_EDGE('',*,*,#54648,.T.);
#83278=ORIENTED_EDGE('',*,*,#56348,.T.);
#83279=ORIENTED_EDGE('',*,*,#56350,.T.);
#83280=ORIENTED_EDGE('',*,*,#54096,.T.);
#83281=ORIENTED_EDGE('',*,*,#56346,.T.);
#83282=ORIENTED_EDGE('',*,*,#56359,.T.);
#83283=ORIENTED_EDGE('',*,*,#56360,.T.);
#83284=ORIENTED_EDGE('',*,*,#56361,.T.);
#83285=ORIENTED_EDGE('',*,*,#56362,.T.);
#83286=ORIENTED_EDGE('',*,*,#56363,.T.);
#83287=ORIENTED_EDGE('',*,*,#56364,.T.);
#83288=ORIENTED_EDGE('',*,*,#56365,.T.);
#83289=ORIENTED_EDGE('',*,*,#56366,.F.);
#83290=ORIENTED_EDGE('',*,*,#56367,.T.);
#83291=ORIENTED_EDGE('',*,*,#56368,.T.);
#83292=ORIENTED_EDGE('',*,*,#56366,.T.);
#83293=ORIENTED_EDGE('',*,*,#56369,.T.);
#83294=ORIENTED_EDGE('',*,*,#56370,.T.);
#83295=ORIENTED_EDGE('',*,*,#56359,.F.);
#83296=ORIENTED_EDGE('',*,*,#56371,.T.);
#83297=ORIENTED_EDGE('',*,*,#56372,.T.);
#83298=ORIENTED_EDGE('',*,*,#56373,.F.);
#83299=ORIENTED_EDGE('',*,*,#56367,.F.);
#83300=ORIENTED_EDGE('',*,*,#56374,.F.);
#83301=ORIENTED_EDGE('',*,*,#56375,.F.);
#83302=ORIENTED_EDGE('',*,*,#56374,.T.);
#83303=ORIENTED_EDGE('',*,*,#56372,.F.);
#83304=ORIENTED_EDGE('',*,*,#56371,.F.);
#83305=ORIENTED_EDGE('',*,*,#56376,.F.);
#83306=ORIENTED_EDGE('',*,*,#56377,.F.);
#83307=ORIENTED_EDGE('',*,*,#56376,.T.);
#83308=ORIENTED_EDGE('',*,*,#56363,.F.);
#83309=ORIENTED_EDGE('',*,*,#56378,.F.);
#83310=ORIENTED_EDGE('',*,*,#56379,.F.);
#83311=ORIENTED_EDGE('',*,*,#56380,.T.);
#83312=ORIENTED_EDGE('',*,*,#56373,.T.);
#83313=ORIENTED_EDGE('',*,*,#54095,.F.);
#83314=ORIENTED_EDGE('',*,*,#54642,.T.);
#83315=ORIENTED_EDGE('',*,*,#56381,.F.);
#83316=ORIENTED_EDGE('',*,*,#56368,.F.);
#83317=ORIENTED_EDGE('',*,*,#56380,.F.);
#83318=ORIENTED_EDGE('',*,*,#54641,.F.);
#83319=ORIENTED_EDGE('',*,*,#56381,.T.);
#83320=ORIENTED_EDGE('',*,*,#55057,.F.);
#83321=ORIENTED_EDGE('',*,*,#56382,.F.);
#83322=ORIENTED_EDGE('',*,*,#56364,.F.);
#83323=ORIENTED_EDGE('',*,*,#56382,.T.);
#83324=ORIENTED_EDGE('',*,*,#54406,.F.);
#83325=ORIENTED_EDGE('',*,*,#56383,.F.);
#83326=ORIENTED_EDGE('',*,*,#56365,.F.);
#83327=ORIENTED_EDGE('',*,*,#56383,.T.);
#83328=ORIENTED_EDGE('',*,*,#54405,.F.);
#83329=ORIENTED_EDGE('',*,*,#56384,.F.);
#83330=ORIENTED_EDGE('',*,*,#56370,.F.);
#83331=ORIENTED_EDGE('',*,*,#56369,.F.);
#83332=ORIENTED_EDGE('',*,*,#56384,.T.);
#83333=ORIENTED_EDGE('',*,*,#54404,.F.);
#83334=ORIENTED_EDGE('',*,*,#56385,.F.);
#83335=ORIENTED_EDGE('',*,*,#56360,.F.);
#83336=ORIENTED_EDGE('',*,*,#56386,.T.);
#83337=ORIENTED_EDGE('',*,*,#56361,.F.);
#83338=ORIENTED_EDGE('',*,*,#56385,.T.);
#83339=ORIENTED_EDGE('',*,*,#55058,.F.);
#83340=ORIENTED_EDGE('',*,*,#56387,.T.);
#83341=ORIENTED_EDGE('',*,*,#56362,.F.);
#83342=ORIENTED_EDGE('',*,*,#56386,.F.);
#83343=ORIENTED_EDGE('',*,*,#54644,.F.);
#83344=ORIENTED_EDGE('',*,*,#54093,.T.);
#83345=ORIENTED_EDGE('',*,*,#56378,.T.);
#83346=ORIENTED_EDGE('',*,*,#56387,.F.);
#83347=ORIENTED_EDGE('',*,*,#54643,.T.);
#83348=ORIENTED_EDGE('',*,*,#56377,.T.);
#83349=ORIENTED_EDGE('',*,*,#56379,.T.);
#83350=ORIENTED_EDGE('',*,*,#54092,.T.);
#83351=ORIENTED_EDGE('',*,*,#56375,.T.);
#83352=ORIENTED_EDGE('',*,*,#56388,.T.);
#83353=ORIENTED_EDGE('',*,*,#56389,.T.);
#83354=ORIENTED_EDGE('',*,*,#56390,.T.);
#83355=ORIENTED_EDGE('',*,*,#56391,.T.);
#83356=ORIENTED_EDGE('',*,*,#56392,.T.);
#83357=ORIENTED_EDGE('',*,*,#56393,.T.);
#83358=ORIENTED_EDGE('',*,*,#56394,.T.);
#83359=ORIENTED_EDGE('',*,*,#56395,.F.);
#83360=ORIENTED_EDGE('',*,*,#56396,.T.);
#83361=ORIENTED_EDGE('',*,*,#56397,.T.);
#83362=ORIENTED_EDGE('',*,*,#56395,.T.);
#83363=ORIENTED_EDGE('',*,*,#56398,.T.);
#83364=ORIENTED_EDGE('',*,*,#56399,.T.);
#83365=ORIENTED_EDGE('',*,*,#56388,.F.);
#83366=ORIENTED_EDGE('',*,*,#56400,.T.);
#83367=ORIENTED_EDGE('',*,*,#56401,.T.);
#83368=ORIENTED_EDGE('',*,*,#56402,.F.);
#83369=ORIENTED_EDGE('',*,*,#56396,.F.);
#83370=ORIENTED_EDGE('',*,*,#56403,.F.);
#83371=ORIENTED_EDGE('',*,*,#56404,.F.);
#83372=ORIENTED_EDGE('',*,*,#56403,.T.);
#83373=ORIENTED_EDGE('',*,*,#56401,.F.);
#83374=ORIENTED_EDGE('',*,*,#56400,.F.);
#83375=ORIENTED_EDGE('',*,*,#56405,.F.);
#83376=ORIENTED_EDGE('',*,*,#56406,.F.);
#83377=ORIENTED_EDGE('',*,*,#56405,.T.);
#83378=ORIENTED_EDGE('',*,*,#56392,.F.);
#83379=ORIENTED_EDGE('',*,*,#56407,.F.);
#83380=ORIENTED_EDGE('',*,*,#56408,.F.);
#83381=ORIENTED_EDGE('',*,*,#56409,.T.);
#83382=ORIENTED_EDGE('',*,*,#56402,.T.);
#83383=ORIENTED_EDGE('',*,*,#54091,.F.);
#83384=ORIENTED_EDGE('',*,*,#54637,.T.);
#83385=ORIENTED_EDGE('',*,*,#56410,.F.);
#83386=ORIENTED_EDGE('',*,*,#56397,.F.);
#83387=ORIENTED_EDGE('',*,*,#56409,.F.);
#83388=ORIENTED_EDGE('',*,*,#54636,.F.);
#83389=ORIENTED_EDGE('',*,*,#56410,.T.);
#83390=ORIENTED_EDGE('',*,*,#55055,.F.);
#83391=ORIENTED_EDGE('',*,*,#56411,.F.);
#83392=ORIENTED_EDGE('',*,*,#56393,.F.);
#83393=ORIENTED_EDGE('',*,*,#56411,.T.);
#83394=ORIENTED_EDGE('',*,*,#54410,.F.);
#83395=ORIENTED_EDGE('',*,*,#56412,.F.);
#83396=ORIENTED_EDGE('',*,*,#56394,.F.);
#83397=ORIENTED_EDGE('',*,*,#56412,.T.);
#83398=ORIENTED_EDGE('',*,*,#54409,.F.);
#83399=ORIENTED_EDGE('',*,*,#56413,.F.);
#83400=ORIENTED_EDGE('',*,*,#56399,.F.);
#83401=ORIENTED_EDGE('',*,*,#56398,.F.);
#83402=ORIENTED_EDGE('',*,*,#56413,.T.);
#83403=ORIENTED_EDGE('',*,*,#54408,.F.);
#83404=ORIENTED_EDGE('',*,*,#56414,.F.);
#83405=ORIENTED_EDGE('',*,*,#56389,.F.);
#83406=ORIENTED_EDGE('',*,*,#56415,.T.);
#83407=ORIENTED_EDGE('',*,*,#56390,.F.);
#83408=ORIENTED_EDGE('',*,*,#56414,.T.);
#83409=ORIENTED_EDGE('',*,*,#55056,.F.);
#83410=ORIENTED_EDGE('',*,*,#56416,.T.);
#83411=ORIENTED_EDGE('',*,*,#56391,.F.);
#83412=ORIENTED_EDGE('',*,*,#56415,.F.);
#83413=ORIENTED_EDGE('',*,*,#54639,.F.);
#83414=ORIENTED_EDGE('',*,*,#54089,.T.);
#83415=ORIENTED_EDGE('',*,*,#56407,.T.);
#83416=ORIENTED_EDGE('',*,*,#56416,.F.);
#83417=ORIENTED_EDGE('',*,*,#54638,.T.);
#83418=ORIENTED_EDGE('',*,*,#56406,.T.);
#83419=ORIENTED_EDGE('',*,*,#56408,.T.);
#83420=ORIENTED_EDGE('',*,*,#54088,.T.);
#83421=ORIENTED_EDGE('',*,*,#56404,.T.);
#83422=ORIENTED_EDGE('',*,*,#56417,.T.);
#83423=ORIENTED_EDGE('',*,*,#56418,.T.);
#83424=ORIENTED_EDGE('',*,*,#56419,.T.);
#83425=ORIENTED_EDGE('',*,*,#56420,.T.);
#83426=ORIENTED_EDGE('',*,*,#56421,.T.);
#83427=ORIENTED_EDGE('',*,*,#56422,.T.);
#83428=ORIENTED_EDGE('',*,*,#56423,.T.);
#83429=ORIENTED_EDGE('',*,*,#56424,.F.);
#83430=ORIENTED_EDGE('',*,*,#56425,.T.);
#83431=ORIENTED_EDGE('',*,*,#56426,.T.);
#83432=ORIENTED_EDGE('',*,*,#56424,.T.);
#83433=ORIENTED_EDGE('',*,*,#56427,.T.);
#83434=ORIENTED_EDGE('',*,*,#56428,.T.);
#83435=ORIENTED_EDGE('',*,*,#56417,.F.);
#83436=ORIENTED_EDGE('',*,*,#56429,.T.);
#83437=ORIENTED_EDGE('',*,*,#56430,.T.);
#83438=ORIENTED_EDGE('',*,*,#56431,.F.);
#83439=ORIENTED_EDGE('',*,*,#56425,.F.);
#83440=ORIENTED_EDGE('',*,*,#56432,.F.);
#83441=ORIENTED_EDGE('',*,*,#56433,.F.);
#83442=ORIENTED_EDGE('',*,*,#56432,.T.);
#83443=ORIENTED_EDGE('',*,*,#56430,.F.);
#83444=ORIENTED_EDGE('',*,*,#56429,.F.);
#83445=ORIENTED_EDGE('',*,*,#56434,.F.);
#83446=ORIENTED_EDGE('',*,*,#56435,.F.);
#83447=ORIENTED_EDGE('',*,*,#56434,.T.);
#83448=ORIENTED_EDGE('',*,*,#56421,.F.);
#83449=ORIENTED_EDGE('',*,*,#56436,.F.);
#83450=ORIENTED_EDGE('',*,*,#56437,.F.);
#83451=ORIENTED_EDGE('',*,*,#56438,.T.);
#83452=ORIENTED_EDGE('',*,*,#56431,.T.);
#83453=ORIENTED_EDGE('',*,*,#54087,.F.);
#83454=ORIENTED_EDGE('',*,*,#54632,.T.);
#83455=ORIENTED_EDGE('',*,*,#56439,.F.);
#83456=ORIENTED_EDGE('',*,*,#56426,.F.);
#83457=ORIENTED_EDGE('',*,*,#56438,.F.);
#83458=ORIENTED_EDGE('',*,*,#54631,.F.);
#83459=ORIENTED_EDGE('',*,*,#56439,.T.);
#83460=ORIENTED_EDGE('',*,*,#55053,.F.);
#83461=ORIENTED_EDGE('',*,*,#56440,.F.);
#83462=ORIENTED_EDGE('',*,*,#56422,.F.);
#83463=ORIENTED_EDGE('',*,*,#56440,.T.);
#83464=ORIENTED_EDGE('',*,*,#54414,.F.);
#83465=ORIENTED_EDGE('',*,*,#56441,.F.);
#83466=ORIENTED_EDGE('',*,*,#56423,.F.);
#83467=ORIENTED_EDGE('',*,*,#56441,.T.);
#83468=ORIENTED_EDGE('',*,*,#54413,.F.);
#83469=ORIENTED_EDGE('',*,*,#56442,.F.);
#83470=ORIENTED_EDGE('',*,*,#56428,.F.);
#83471=ORIENTED_EDGE('',*,*,#56427,.F.);
#83472=ORIENTED_EDGE('',*,*,#56442,.T.);
#83473=ORIENTED_EDGE('',*,*,#54412,.F.);
#83474=ORIENTED_EDGE('',*,*,#56443,.F.);
#83475=ORIENTED_EDGE('',*,*,#56418,.F.);
#83476=ORIENTED_EDGE('',*,*,#56444,.T.);
#83477=ORIENTED_EDGE('',*,*,#56419,.F.);
#83478=ORIENTED_EDGE('',*,*,#56443,.T.);
#83479=ORIENTED_EDGE('',*,*,#55054,.F.);
#83480=ORIENTED_EDGE('',*,*,#56445,.T.);
#83481=ORIENTED_EDGE('',*,*,#56420,.F.);
#83482=ORIENTED_EDGE('',*,*,#56444,.F.);
#83483=ORIENTED_EDGE('',*,*,#54634,.F.);
#83484=ORIENTED_EDGE('',*,*,#54085,.T.);
#83485=ORIENTED_EDGE('',*,*,#56436,.T.);
#83486=ORIENTED_EDGE('',*,*,#56445,.F.);
#83487=ORIENTED_EDGE('',*,*,#54633,.T.);
#83488=ORIENTED_EDGE('',*,*,#56435,.T.);
#83489=ORIENTED_EDGE('',*,*,#56437,.T.);
#83490=ORIENTED_EDGE('',*,*,#54084,.T.);
#83491=ORIENTED_EDGE('',*,*,#56433,.T.);
#83492=ORIENTED_EDGE('',*,*,#56446,.T.);
#83493=ORIENTED_EDGE('',*,*,#56447,.T.);
#83494=ORIENTED_EDGE('',*,*,#56448,.T.);
#83495=ORIENTED_EDGE('',*,*,#56449,.T.);
#83496=ORIENTED_EDGE('',*,*,#56450,.T.);
#83497=ORIENTED_EDGE('',*,*,#56451,.T.);
#83498=ORIENTED_EDGE('',*,*,#56452,.T.);
#83499=ORIENTED_EDGE('',*,*,#56453,.F.);
#83500=ORIENTED_EDGE('',*,*,#56454,.T.);
#83501=ORIENTED_EDGE('',*,*,#56455,.T.);
#83502=ORIENTED_EDGE('',*,*,#56453,.T.);
#83503=ORIENTED_EDGE('',*,*,#56456,.T.);
#83504=ORIENTED_EDGE('',*,*,#56457,.T.);
#83505=ORIENTED_EDGE('',*,*,#56446,.F.);
#83506=ORIENTED_EDGE('',*,*,#56458,.T.);
#83507=ORIENTED_EDGE('',*,*,#56459,.T.);
#83508=ORIENTED_EDGE('',*,*,#56460,.F.);
#83509=ORIENTED_EDGE('',*,*,#56454,.F.);
#83510=ORIENTED_EDGE('',*,*,#56461,.F.);
#83511=ORIENTED_EDGE('',*,*,#56462,.F.);
#83512=ORIENTED_EDGE('',*,*,#56461,.T.);
#83513=ORIENTED_EDGE('',*,*,#56459,.F.);
#83514=ORIENTED_EDGE('',*,*,#56458,.F.);
#83515=ORIENTED_EDGE('',*,*,#56463,.F.);
#83516=ORIENTED_EDGE('',*,*,#56464,.F.);
#83517=ORIENTED_EDGE('',*,*,#56463,.T.);
#83518=ORIENTED_EDGE('',*,*,#56450,.F.);
#83519=ORIENTED_EDGE('',*,*,#56465,.F.);
#83520=ORIENTED_EDGE('',*,*,#56466,.F.);
#83521=ORIENTED_EDGE('',*,*,#56467,.T.);
#83522=ORIENTED_EDGE('',*,*,#56460,.T.);
#83523=ORIENTED_EDGE('',*,*,#54083,.F.);
#83524=ORIENTED_EDGE('',*,*,#54627,.T.);
#83525=ORIENTED_EDGE('',*,*,#56468,.F.);
#83526=ORIENTED_EDGE('',*,*,#56455,.F.);
#83527=ORIENTED_EDGE('',*,*,#56467,.F.);
#83528=ORIENTED_EDGE('',*,*,#54626,.F.);
#83529=ORIENTED_EDGE('',*,*,#56468,.T.);
#83530=ORIENTED_EDGE('',*,*,#55051,.F.);
#83531=ORIENTED_EDGE('',*,*,#56469,.F.);
#83532=ORIENTED_EDGE('',*,*,#56451,.F.);
#83533=ORIENTED_EDGE('',*,*,#56469,.T.);
#83534=ORIENTED_EDGE('',*,*,#54418,.F.);
#83535=ORIENTED_EDGE('',*,*,#56470,.F.);
#83536=ORIENTED_EDGE('',*,*,#56452,.F.);
#83537=ORIENTED_EDGE('',*,*,#56470,.T.);
#83538=ORIENTED_EDGE('',*,*,#54417,.F.);
#83539=ORIENTED_EDGE('',*,*,#56471,.F.);
#83540=ORIENTED_EDGE('',*,*,#56457,.F.);
#83541=ORIENTED_EDGE('',*,*,#56456,.F.);
#83542=ORIENTED_EDGE('',*,*,#56471,.T.);
#83543=ORIENTED_EDGE('',*,*,#54416,.F.);
#83544=ORIENTED_EDGE('',*,*,#56472,.F.);
#83545=ORIENTED_EDGE('',*,*,#56447,.F.);
#83546=ORIENTED_EDGE('',*,*,#56473,.T.);
#83547=ORIENTED_EDGE('',*,*,#56448,.F.);
#83548=ORIENTED_EDGE('',*,*,#56472,.T.);
#83549=ORIENTED_EDGE('',*,*,#55052,.F.);
#83550=ORIENTED_EDGE('',*,*,#56474,.T.);
#83551=ORIENTED_EDGE('',*,*,#56449,.F.);
#83552=ORIENTED_EDGE('',*,*,#56473,.F.);
#83553=ORIENTED_EDGE('',*,*,#54629,.F.);
#83554=ORIENTED_EDGE('',*,*,#54081,.T.);
#83555=ORIENTED_EDGE('',*,*,#56465,.T.);
#83556=ORIENTED_EDGE('',*,*,#56474,.F.);
#83557=ORIENTED_EDGE('',*,*,#54628,.T.);
#83558=ORIENTED_EDGE('',*,*,#56464,.T.);
#83559=ORIENTED_EDGE('',*,*,#56466,.T.);
#83560=ORIENTED_EDGE('',*,*,#54080,.T.);
#83561=ORIENTED_EDGE('',*,*,#56462,.T.);
#83562=ORIENTED_EDGE('',*,*,#56475,.T.);
#83563=ORIENTED_EDGE('',*,*,#56476,.T.);
#83564=ORIENTED_EDGE('',*,*,#56477,.T.);
#83565=ORIENTED_EDGE('',*,*,#56478,.T.);
#83566=ORIENTED_EDGE('',*,*,#56479,.T.);
#83567=ORIENTED_EDGE('',*,*,#56480,.T.);
#83568=ORIENTED_EDGE('',*,*,#56481,.T.);
#83569=ORIENTED_EDGE('',*,*,#56482,.F.);
#83570=ORIENTED_EDGE('',*,*,#56483,.T.);
#83571=ORIENTED_EDGE('',*,*,#56484,.T.);
#83572=ORIENTED_EDGE('',*,*,#56482,.T.);
#83573=ORIENTED_EDGE('',*,*,#56485,.T.);
#83574=ORIENTED_EDGE('',*,*,#56486,.T.);
#83575=ORIENTED_EDGE('',*,*,#56475,.F.);
#83576=ORIENTED_EDGE('',*,*,#56487,.T.);
#83577=ORIENTED_EDGE('',*,*,#56488,.T.);
#83578=ORIENTED_EDGE('',*,*,#56489,.F.);
#83579=ORIENTED_EDGE('',*,*,#56483,.F.);
#83580=ORIENTED_EDGE('',*,*,#56490,.F.);
#83581=ORIENTED_EDGE('',*,*,#56491,.F.);
#83582=ORIENTED_EDGE('',*,*,#56490,.T.);
#83583=ORIENTED_EDGE('',*,*,#56488,.F.);
#83584=ORIENTED_EDGE('',*,*,#56487,.F.);
#83585=ORIENTED_EDGE('',*,*,#56492,.F.);
#83586=ORIENTED_EDGE('',*,*,#56493,.F.);
#83587=ORIENTED_EDGE('',*,*,#56492,.T.);
#83588=ORIENTED_EDGE('',*,*,#56479,.F.);
#83589=ORIENTED_EDGE('',*,*,#56494,.F.);
#83590=ORIENTED_EDGE('',*,*,#56495,.F.);
#83591=ORIENTED_EDGE('',*,*,#56496,.T.);
#83592=ORIENTED_EDGE('',*,*,#56489,.T.);
#83593=ORIENTED_EDGE('',*,*,#54079,.F.);
#83594=ORIENTED_EDGE('',*,*,#54622,.T.);
#83595=ORIENTED_EDGE('',*,*,#56497,.F.);
#83596=ORIENTED_EDGE('',*,*,#56484,.F.);
#83597=ORIENTED_EDGE('',*,*,#56496,.F.);
#83598=ORIENTED_EDGE('',*,*,#54621,.F.);
#83599=ORIENTED_EDGE('',*,*,#56497,.T.);
#83600=ORIENTED_EDGE('',*,*,#55049,.F.);
#83601=ORIENTED_EDGE('',*,*,#56498,.F.);
#83602=ORIENTED_EDGE('',*,*,#56480,.F.);
#83603=ORIENTED_EDGE('',*,*,#56498,.T.);
#83604=ORIENTED_EDGE('',*,*,#54422,.F.);
#83605=ORIENTED_EDGE('',*,*,#56499,.F.);
#83606=ORIENTED_EDGE('',*,*,#56481,.F.);
#83607=ORIENTED_EDGE('',*,*,#56499,.T.);
#83608=ORIENTED_EDGE('',*,*,#54421,.F.);
#83609=ORIENTED_EDGE('',*,*,#56500,.F.);
#83610=ORIENTED_EDGE('',*,*,#56486,.F.);
#83611=ORIENTED_EDGE('',*,*,#56485,.F.);
#83612=ORIENTED_EDGE('',*,*,#56500,.T.);
#83613=ORIENTED_EDGE('',*,*,#54420,.F.);
#83614=ORIENTED_EDGE('',*,*,#56501,.F.);
#83615=ORIENTED_EDGE('',*,*,#56476,.F.);
#83616=ORIENTED_EDGE('',*,*,#56502,.T.);
#83617=ORIENTED_EDGE('',*,*,#56477,.F.);
#83618=ORIENTED_EDGE('',*,*,#56501,.T.);
#83619=ORIENTED_EDGE('',*,*,#55050,.F.);
#83620=ORIENTED_EDGE('',*,*,#56503,.T.);
#83621=ORIENTED_EDGE('',*,*,#56478,.F.);
#83622=ORIENTED_EDGE('',*,*,#56502,.F.);
#83623=ORIENTED_EDGE('',*,*,#54624,.F.);
#83624=ORIENTED_EDGE('',*,*,#54077,.T.);
#83625=ORIENTED_EDGE('',*,*,#56494,.T.);
#83626=ORIENTED_EDGE('',*,*,#56503,.F.);
#83627=ORIENTED_EDGE('',*,*,#54623,.T.);
#83628=ORIENTED_EDGE('',*,*,#56493,.T.);
#83629=ORIENTED_EDGE('',*,*,#56495,.T.);
#83630=ORIENTED_EDGE('',*,*,#54076,.T.);
#83631=ORIENTED_EDGE('',*,*,#56491,.T.);
#83632=ORIENTED_EDGE('',*,*,#56504,.T.);
#83633=ORIENTED_EDGE('',*,*,#56505,.T.);
#83634=ORIENTED_EDGE('',*,*,#56506,.T.);
#83635=ORIENTED_EDGE('',*,*,#56507,.T.);
#83636=ORIENTED_EDGE('',*,*,#56508,.T.);
#83637=ORIENTED_EDGE('',*,*,#56509,.T.);
#83638=ORIENTED_EDGE('',*,*,#56510,.T.);
#83639=ORIENTED_EDGE('',*,*,#56511,.F.);
#83640=ORIENTED_EDGE('',*,*,#56512,.T.);
#83641=ORIENTED_EDGE('',*,*,#56513,.T.);
#83642=ORIENTED_EDGE('',*,*,#56511,.T.);
#83643=ORIENTED_EDGE('',*,*,#56514,.T.);
#83644=ORIENTED_EDGE('',*,*,#56515,.T.);
#83645=ORIENTED_EDGE('',*,*,#56504,.F.);
#83646=ORIENTED_EDGE('',*,*,#56516,.T.);
#83647=ORIENTED_EDGE('',*,*,#56517,.T.);
#83648=ORIENTED_EDGE('',*,*,#56518,.F.);
#83649=ORIENTED_EDGE('',*,*,#56512,.F.);
#83650=ORIENTED_EDGE('',*,*,#56519,.F.);
#83651=ORIENTED_EDGE('',*,*,#56520,.F.);
#83652=ORIENTED_EDGE('',*,*,#56519,.T.);
#83653=ORIENTED_EDGE('',*,*,#56517,.F.);
#83654=ORIENTED_EDGE('',*,*,#56516,.F.);
#83655=ORIENTED_EDGE('',*,*,#56521,.F.);
#83656=ORIENTED_EDGE('',*,*,#56522,.F.);
#83657=ORIENTED_EDGE('',*,*,#56521,.T.);
#83658=ORIENTED_EDGE('',*,*,#56508,.F.);
#83659=ORIENTED_EDGE('',*,*,#56523,.F.);
#83660=ORIENTED_EDGE('',*,*,#56524,.F.);
#83661=ORIENTED_EDGE('',*,*,#56525,.T.);
#83662=ORIENTED_EDGE('',*,*,#56518,.T.);
#83663=ORIENTED_EDGE('',*,*,#54075,.F.);
#83664=ORIENTED_EDGE('',*,*,#54617,.T.);
#83665=ORIENTED_EDGE('',*,*,#56526,.F.);
#83666=ORIENTED_EDGE('',*,*,#56513,.F.);
#83667=ORIENTED_EDGE('',*,*,#56525,.F.);
#83668=ORIENTED_EDGE('',*,*,#54616,.F.);
#83669=ORIENTED_EDGE('',*,*,#56526,.T.);
#83670=ORIENTED_EDGE('',*,*,#55047,.F.);
#83671=ORIENTED_EDGE('',*,*,#56527,.F.);
#83672=ORIENTED_EDGE('',*,*,#56509,.F.);
#83673=ORIENTED_EDGE('',*,*,#56527,.T.);
#83674=ORIENTED_EDGE('',*,*,#54426,.F.);
#83675=ORIENTED_EDGE('',*,*,#56528,.F.);
#83676=ORIENTED_EDGE('',*,*,#56510,.F.);
#83677=ORIENTED_EDGE('',*,*,#56528,.T.);
#83678=ORIENTED_EDGE('',*,*,#54425,.F.);
#83679=ORIENTED_EDGE('',*,*,#56529,.F.);
#83680=ORIENTED_EDGE('',*,*,#56515,.F.);
#83681=ORIENTED_EDGE('',*,*,#56514,.F.);
#83682=ORIENTED_EDGE('',*,*,#56529,.T.);
#83683=ORIENTED_EDGE('',*,*,#54424,.F.);
#83684=ORIENTED_EDGE('',*,*,#56530,.F.);
#83685=ORIENTED_EDGE('',*,*,#56505,.F.);
#83686=ORIENTED_EDGE('',*,*,#56531,.T.);
#83687=ORIENTED_EDGE('',*,*,#56506,.F.);
#83688=ORIENTED_EDGE('',*,*,#56530,.T.);
#83689=ORIENTED_EDGE('',*,*,#55048,.F.);
#83690=ORIENTED_EDGE('',*,*,#56532,.T.);
#83691=ORIENTED_EDGE('',*,*,#56507,.F.);
#83692=ORIENTED_EDGE('',*,*,#56531,.F.);
#83693=ORIENTED_EDGE('',*,*,#54619,.F.);
#83694=ORIENTED_EDGE('',*,*,#54073,.T.);
#83695=ORIENTED_EDGE('',*,*,#56523,.T.);
#83696=ORIENTED_EDGE('',*,*,#56532,.F.);
#83697=ORIENTED_EDGE('',*,*,#54618,.T.);
#83698=ORIENTED_EDGE('',*,*,#56522,.T.);
#83699=ORIENTED_EDGE('',*,*,#56524,.T.);
#83700=ORIENTED_EDGE('',*,*,#54072,.T.);
#83701=ORIENTED_EDGE('',*,*,#56520,.T.);
#83702=ORIENTED_EDGE('',*,*,#56533,.T.);
#83703=ORIENTED_EDGE('',*,*,#56534,.T.);
#83704=ORIENTED_EDGE('',*,*,#56535,.T.);
#83705=ORIENTED_EDGE('',*,*,#56536,.T.);
#83706=ORIENTED_EDGE('',*,*,#56537,.T.);
#83707=ORIENTED_EDGE('',*,*,#56538,.T.);
#83708=ORIENTED_EDGE('',*,*,#56539,.T.);
#83709=ORIENTED_EDGE('',*,*,#56540,.F.);
#83710=ORIENTED_EDGE('',*,*,#56541,.T.);
#83711=ORIENTED_EDGE('',*,*,#56542,.T.);
#83712=ORIENTED_EDGE('',*,*,#56540,.T.);
#83713=ORIENTED_EDGE('',*,*,#56543,.T.);
#83714=ORIENTED_EDGE('',*,*,#56544,.T.);
#83715=ORIENTED_EDGE('',*,*,#56533,.F.);
#83716=ORIENTED_EDGE('',*,*,#56545,.T.);
#83717=ORIENTED_EDGE('',*,*,#56546,.T.);
#83718=ORIENTED_EDGE('',*,*,#56547,.F.);
#83719=ORIENTED_EDGE('',*,*,#56541,.F.);
#83720=ORIENTED_EDGE('',*,*,#56548,.F.);
#83721=ORIENTED_EDGE('',*,*,#56549,.F.);
#83722=ORIENTED_EDGE('',*,*,#56548,.T.);
#83723=ORIENTED_EDGE('',*,*,#56546,.F.);
#83724=ORIENTED_EDGE('',*,*,#56545,.F.);
#83725=ORIENTED_EDGE('',*,*,#56550,.F.);
#83726=ORIENTED_EDGE('',*,*,#56551,.F.);
#83727=ORIENTED_EDGE('',*,*,#56550,.T.);
#83728=ORIENTED_EDGE('',*,*,#56537,.F.);
#83729=ORIENTED_EDGE('',*,*,#56552,.F.);
#83730=ORIENTED_EDGE('',*,*,#56553,.F.);
#83731=ORIENTED_EDGE('',*,*,#56554,.T.);
#83732=ORIENTED_EDGE('',*,*,#56547,.T.);
#83733=ORIENTED_EDGE('',*,*,#54071,.F.);
#83734=ORIENTED_EDGE('',*,*,#54612,.T.);
#83735=ORIENTED_EDGE('',*,*,#56555,.F.);
#83736=ORIENTED_EDGE('',*,*,#56542,.F.);
#83737=ORIENTED_EDGE('',*,*,#56554,.F.);
#83738=ORIENTED_EDGE('',*,*,#54611,.F.);
#83739=ORIENTED_EDGE('',*,*,#56555,.T.);
#83740=ORIENTED_EDGE('',*,*,#55045,.F.);
#83741=ORIENTED_EDGE('',*,*,#56556,.F.);
#83742=ORIENTED_EDGE('',*,*,#56538,.F.);
#83743=ORIENTED_EDGE('',*,*,#56556,.T.);
#83744=ORIENTED_EDGE('',*,*,#54430,.F.);
#83745=ORIENTED_EDGE('',*,*,#56557,.F.);
#83746=ORIENTED_EDGE('',*,*,#56539,.F.);
#83747=ORIENTED_EDGE('',*,*,#56557,.T.);
#83748=ORIENTED_EDGE('',*,*,#54429,.F.);
#83749=ORIENTED_EDGE('',*,*,#56558,.F.);
#83750=ORIENTED_EDGE('',*,*,#56544,.F.);
#83751=ORIENTED_EDGE('',*,*,#56543,.F.);
#83752=ORIENTED_EDGE('',*,*,#56558,.T.);
#83753=ORIENTED_EDGE('',*,*,#54428,.F.);
#83754=ORIENTED_EDGE('',*,*,#56559,.F.);
#83755=ORIENTED_EDGE('',*,*,#56534,.F.);
#83756=ORIENTED_EDGE('',*,*,#56560,.T.);
#83757=ORIENTED_EDGE('',*,*,#56535,.F.);
#83758=ORIENTED_EDGE('',*,*,#56559,.T.);
#83759=ORIENTED_EDGE('',*,*,#55046,.F.);
#83760=ORIENTED_EDGE('',*,*,#56561,.T.);
#83761=ORIENTED_EDGE('',*,*,#56536,.F.);
#83762=ORIENTED_EDGE('',*,*,#56560,.F.);
#83763=ORIENTED_EDGE('',*,*,#54614,.F.);
#83764=ORIENTED_EDGE('',*,*,#54069,.T.);
#83765=ORIENTED_EDGE('',*,*,#56552,.T.);
#83766=ORIENTED_EDGE('',*,*,#56561,.F.);
#83767=ORIENTED_EDGE('',*,*,#54613,.T.);
#83768=ORIENTED_EDGE('',*,*,#56551,.T.);
#83769=ORIENTED_EDGE('',*,*,#56553,.T.);
#83770=ORIENTED_EDGE('',*,*,#54068,.T.);
#83771=ORIENTED_EDGE('',*,*,#56549,.T.);
#83772=ORIENTED_EDGE('',*,*,#56562,.T.);
#83773=ORIENTED_EDGE('',*,*,#56563,.T.);
#83774=ORIENTED_EDGE('',*,*,#56564,.T.);
#83775=ORIENTED_EDGE('',*,*,#56565,.T.);
#83776=ORIENTED_EDGE('',*,*,#56566,.T.);
#83777=ORIENTED_EDGE('',*,*,#56567,.T.);
#83778=ORIENTED_EDGE('',*,*,#56568,.T.);
#83779=ORIENTED_EDGE('',*,*,#56569,.F.);
#83780=ORIENTED_EDGE('',*,*,#56570,.T.);
#83781=ORIENTED_EDGE('',*,*,#56571,.T.);
#83782=ORIENTED_EDGE('',*,*,#56569,.T.);
#83783=ORIENTED_EDGE('',*,*,#56572,.T.);
#83784=ORIENTED_EDGE('',*,*,#56573,.T.);
#83785=ORIENTED_EDGE('',*,*,#56562,.F.);
#83786=ORIENTED_EDGE('',*,*,#56574,.T.);
#83787=ORIENTED_EDGE('',*,*,#56575,.T.);
#83788=ORIENTED_EDGE('',*,*,#56576,.F.);
#83789=ORIENTED_EDGE('',*,*,#56570,.F.);
#83790=ORIENTED_EDGE('',*,*,#56577,.F.);
#83791=ORIENTED_EDGE('',*,*,#56578,.F.);
#83792=ORIENTED_EDGE('',*,*,#56577,.T.);
#83793=ORIENTED_EDGE('',*,*,#56575,.F.);
#83794=ORIENTED_EDGE('',*,*,#56574,.F.);
#83795=ORIENTED_EDGE('',*,*,#56579,.F.);
#83796=ORIENTED_EDGE('',*,*,#56580,.F.);
#83797=ORIENTED_EDGE('',*,*,#56579,.T.);
#83798=ORIENTED_EDGE('',*,*,#56566,.F.);
#83799=ORIENTED_EDGE('',*,*,#56581,.F.);
#83800=ORIENTED_EDGE('',*,*,#56582,.F.);
#83801=ORIENTED_EDGE('',*,*,#56583,.T.);
#83802=ORIENTED_EDGE('',*,*,#56576,.T.);
#83803=ORIENTED_EDGE('',*,*,#54067,.F.);
#83804=ORIENTED_EDGE('',*,*,#54607,.T.);
#83805=ORIENTED_EDGE('',*,*,#56584,.F.);
#83806=ORIENTED_EDGE('',*,*,#56571,.F.);
#83807=ORIENTED_EDGE('',*,*,#56583,.F.);
#83808=ORIENTED_EDGE('',*,*,#54606,.F.);
#83809=ORIENTED_EDGE('',*,*,#56584,.T.);
#83810=ORIENTED_EDGE('',*,*,#55043,.F.);
#83811=ORIENTED_EDGE('',*,*,#56585,.F.);
#83812=ORIENTED_EDGE('',*,*,#56567,.F.);
#83813=ORIENTED_EDGE('',*,*,#56585,.T.);
#83814=ORIENTED_EDGE('',*,*,#54434,.F.);
#83815=ORIENTED_EDGE('',*,*,#56586,.F.);
#83816=ORIENTED_EDGE('',*,*,#56568,.F.);
#83817=ORIENTED_EDGE('',*,*,#56586,.T.);
#83818=ORIENTED_EDGE('',*,*,#54433,.F.);
#83819=ORIENTED_EDGE('',*,*,#56587,.F.);
#83820=ORIENTED_EDGE('',*,*,#56573,.F.);
#83821=ORIENTED_EDGE('',*,*,#56572,.F.);
#83822=ORIENTED_EDGE('',*,*,#56587,.T.);
#83823=ORIENTED_EDGE('',*,*,#54432,.F.);
#83824=ORIENTED_EDGE('',*,*,#56588,.F.);
#83825=ORIENTED_EDGE('',*,*,#56563,.F.);
#83826=ORIENTED_EDGE('',*,*,#56589,.T.);
#83827=ORIENTED_EDGE('',*,*,#56564,.F.);
#83828=ORIENTED_EDGE('',*,*,#56588,.T.);
#83829=ORIENTED_EDGE('',*,*,#55044,.F.);
#83830=ORIENTED_EDGE('',*,*,#56590,.T.);
#83831=ORIENTED_EDGE('',*,*,#56565,.F.);
#83832=ORIENTED_EDGE('',*,*,#56589,.F.);
#83833=ORIENTED_EDGE('',*,*,#54609,.F.);
#83834=ORIENTED_EDGE('',*,*,#54065,.T.);
#83835=ORIENTED_EDGE('',*,*,#56581,.T.);
#83836=ORIENTED_EDGE('',*,*,#56590,.F.);
#83837=ORIENTED_EDGE('',*,*,#54608,.T.);
#83838=ORIENTED_EDGE('',*,*,#56580,.T.);
#83839=ORIENTED_EDGE('',*,*,#56582,.T.);
#83840=ORIENTED_EDGE('',*,*,#54064,.T.);
#83841=ORIENTED_EDGE('',*,*,#56578,.T.);
#83842=ORIENTED_EDGE('',*,*,#56591,.T.);
#83843=ORIENTED_EDGE('',*,*,#56592,.T.);
#83844=ORIENTED_EDGE('',*,*,#56593,.T.);
#83845=ORIENTED_EDGE('',*,*,#56594,.T.);
#83846=ORIENTED_EDGE('',*,*,#56595,.T.);
#83847=ORIENTED_EDGE('',*,*,#56596,.T.);
#83848=ORIENTED_EDGE('',*,*,#56597,.T.);
#83849=ORIENTED_EDGE('',*,*,#56598,.F.);
#83850=ORIENTED_EDGE('',*,*,#56599,.T.);
#83851=ORIENTED_EDGE('',*,*,#56600,.T.);
#83852=ORIENTED_EDGE('',*,*,#56598,.T.);
#83853=ORIENTED_EDGE('',*,*,#56601,.T.);
#83854=ORIENTED_EDGE('',*,*,#56602,.T.);
#83855=ORIENTED_EDGE('',*,*,#56591,.F.);
#83856=ORIENTED_EDGE('',*,*,#56603,.T.);
#83857=ORIENTED_EDGE('',*,*,#56604,.T.);
#83858=ORIENTED_EDGE('',*,*,#56605,.F.);
#83859=ORIENTED_EDGE('',*,*,#56599,.F.);
#83860=ORIENTED_EDGE('',*,*,#56606,.F.);
#83861=ORIENTED_EDGE('',*,*,#56607,.F.);
#83862=ORIENTED_EDGE('',*,*,#56606,.T.);
#83863=ORIENTED_EDGE('',*,*,#56604,.F.);
#83864=ORIENTED_EDGE('',*,*,#56603,.F.);
#83865=ORIENTED_EDGE('',*,*,#56608,.F.);
#83866=ORIENTED_EDGE('',*,*,#56609,.F.);
#83867=ORIENTED_EDGE('',*,*,#56608,.T.);
#83868=ORIENTED_EDGE('',*,*,#56595,.F.);
#83869=ORIENTED_EDGE('',*,*,#56610,.F.);
#83870=ORIENTED_EDGE('',*,*,#56611,.F.);
#83871=ORIENTED_EDGE('',*,*,#56612,.T.);
#83872=ORIENTED_EDGE('',*,*,#56605,.T.);
#83873=ORIENTED_EDGE('',*,*,#54063,.F.);
#83874=ORIENTED_EDGE('',*,*,#54602,.T.);
#83875=ORIENTED_EDGE('',*,*,#56613,.F.);
#83876=ORIENTED_EDGE('',*,*,#56600,.F.);
#83877=ORIENTED_EDGE('',*,*,#56612,.F.);
#83878=ORIENTED_EDGE('',*,*,#54601,.F.);
#83879=ORIENTED_EDGE('',*,*,#56613,.T.);
#83880=ORIENTED_EDGE('',*,*,#54987,.F.);
#83881=ORIENTED_EDGE('',*,*,#56614,.F.);
#83882=ORIENTED_EDGE('',*,*,#56596,.F.);
#83883=ORIENTED_EDGE('',*,*,#56614,.T.);
#83884=ORIENTED_EDGE('',*,*,#54438,.F.);
#83885=ORIENTED_EDGE('',*,*,#56615,.F.);
#83886=ORIENTED_EDGE('',*,*,#56597,.F.);
#83887=ORIENTED_EDGE('',*,*,#56615,.T.);
#83888=ORIENTED_EDGE('',*,*,#54437,.F.);
#83889=ORIENTED_EDGE('',*,*,#56616,.F.);
#83890=ORIENTED_EDGE('',*,*,#56602,.F.);
#83891=ORIENTED_EDGE('',*,*,#56601,.F.);
#83892=ORIENTED_EDGE('',*,*,#56616,.T.);
#83893=ORIENTED_EDGE('',*,*,#54436,.F.);
#83894=ORIENTED_EDGE('',*,*,#56617,.F.);
#83895=ORIENTED_EDGE('',*,*,#56592,.F.);
#83896=ORIENTED_EDGE('',*,*,#56618,.T.);
#83897=ORIENTED_EDGE('',*,*,#56593,.F.);
#83898=ORIENTED_EDGE('',*,*,#56617,.T.);
#83899=ORIENTED_EDGE('',*,*,#55042,.F.);
#83900=ORIENTED_EDGE('',*,*,#56619,.T.);
#83901=ORIENTED_EDGE('',*,*,#56594,.F.);
#83902=ORIENTED_EDGE('',*,*,#56618,.F.);
#83903=ORIENTED_EDGE('',*,*,#54604,.F.);
#83904=ORIENTED_EDGE('',*,*,#54061,.T.);
#83905=ORIENTED_EDGE('',*,*,#56610,.T.);
#83906=ORIENTED_EDGE('',*,*,#56619,.F.);
#83907=ORIENTED_EDGE('',*,*,#54603,.T.);
#83908=ORIENTED_EDGE('',*,*,#56609,.T.);
#83909=ORIENTED_EDGE('',*,*,#56611,.T.);
#83910=ORIENTED_EDGE('',*,*,#54060,.T.);
#83911=ORIENTED_EDGE('',*,*,#56607,.T.);
#83912=ORIENTED_EDGE('',*,*,#56620,.T.);
#83913=ORIENTED_EDGE('',*,*,#56621,.T.);
#83914=ORIENTED_EDGE('',*,*,#56622,.T.);
#83915=ORIENTED_EDGE('',*,*,#56623,.T.);
#83916=ORIENTED_EDGE('',*,*,#56624,.T.);
#83917=ORIENTED_EDGE('',*,*,#56625,.T.);
#83918=ORIENTED_EDGE('',*,*,#56626,.T.);
#83919=ORIENTED_EDGE('',*,*,#56627,.F.);
#83920=ORIENTED_EDGE('',*,*,#56628,.T.);
#83921=ORIENTED_EDGE('',*,*,#56629,.T.);
#83922=ORIENTED_EDGE('',*,*,#56627,.T.);
#83923=ORIENTED_EDGE('',*,*,#56630,.T.);
#83924=ORIENTED_EDGE('',*,*,#56631,.T.);
#83925=ORIENTED_EDGE('',*,*,#56620,.F.);
#83926=ORIENTED_EDGE('',*,*,#56632,.T.);
#83927=ORIENTED_EDGE('',*,*,#56633,.T.);
#83928=ORIENTED_EDGE('',*,*,#56634,.F.);
#83929=ORIENTED_EDGE('',*,*,#56628,.F.);
#83930=ORIENTED_EDGE('',*,*,#56635,.F.);
#83931=ORIENTED_EDGE('',*,*,#56636,.F.);
#83932=ORIENTED_EDGE('',*,*,#56635,.T.);
#83933=ORIENTED_EDGE('',*,*,#56633,.F.);
#83934=ORIENTED_EDGE('',*,*,#56632,.F.);
#83935=ORIENTED_EDGE('',*,*,#56637,.F.);
#83936=ORIENTED_EDGE('',*,*,#56638,.F.);
#83937=ORIENTED_EDGE('',*,*,#56637,.T.);
#83938=ORIENTED_EDGE('',*,*,#56624,.F.);
#83939=ORIENTED_EDGE('',*,*,#56639,.F.);
#83940=ORIENTED_EDGE('',*,*,#56640,.F.);
#83941=ORIENTED_EDGE('',*,*,#56641,.T.);
#83942=ORIENTED_EDGE('',*,*,#56634,.T.);
#83943=ORIENTED_EDGE('',*,*,#54059,.F.);
#83944=ORIENTED_EDGE('',*,*,#54983,.T.);
#83945=ORIENTED_EDGE('',*,*,#56642,.F.);
#83946=ORIENTED_EDGE('',*,*,#56629,.F.);
#83947=ORIENTED_EDGE('',*,*,#56641,.F.);
#83948=ORIENTED_EDGE('',*,*,#54982,.F.);
#83949=ORIENTED_EDGE('',*,*,#56642,.T.);
#83950=ORIENTED_EDGE('',*,*,#55041,.F.);
#83951=ORIENTED_EDGE('',*,*,#56643,.F.);
#83952=ORIENTED_EDGE('',*,*,#56625,.F.);
#83953=ORIENTED_EDGE('',*,*,#56643,.T.);
#83954=ORIENTED_EDGE('',*,*,#54446,.F.);
#83955=ORIENTED_EDGE('',*,*,#56644,.F.);
#83956=ORIENTED_EDGE('',*,*,#56626,.F.);
#83957=ORIENTED_EDGE('',*,*,#56644,.T.);
#83958=ORIENTED_EDGE('',*,*,#54445,.F.);
#83959=ORIENTED_EDGE('',*,*,#56645,.F.);
#83960=ORIENTED_EDGE('',*,*,#56631,.F.);
#83961=ORIENTED_EDGE('',*,*,#56630,.F.);
#83962=ORIENTED_EDGE('',*,*,#56645,.T.);
#83963=ORIENTED_EDGE('',*,*,#54444,.F.);
#83964=ORIENTED_EDGE('',*,*,#56646,.F.);
#83965=ORIENTED_EDGE('',*,*,#56621,.F.);
#83966=ORIENTED_EDGE('',*,*,#56647,.T.);
#83967=ORIENTED_EDGE('',*,*,#56622,.F.);
#83968=ORIENTED_EDGE('',*,*,#56646,.T.);
#83969=ORIENTED_EDGE('',*,*,#54986,.F.);
#83970=ORIENTED_EDGE('',*,*,#56648,.T.);
#83971=ORIENTED_EDGE('',*,*,#56623,.F.);
#83972=ORIENTED_EDGE('',*,*,#56647,.F.);
#83973=ORIENTED_EDGE('',*,*,#54985,.F.);
#83974=ORIENTED_EDGE('',*,*,#54057,.T.);
#83975=ORIENTED_EDGE('',*,*,#56639,.T.);
#83976=ORIENTED_EDGE('',*,*,#56648,.F.);
#83977=ORIENTED_EDGE('',*,*,#54984,.T.);
#83978=ORIENTED_EDGE('',*,*,#56638,.T.);
#83979=ORIENTED_EDGE('',*,*,#56640,.T.);
#83980=ORIENTED_EDGE('',*,*,#54056,.T.);
#83981=ORIENTED_EDGE('',*,*,#56636,.T.);
#83982=ORIENTED_EDGE('',*,*,#56649,.T.);
#83983=ORIENTED_EDGE('',*,*,#56650,.T.);
#83984=ORIENTED_EDGE('',*,*,#56651,.T.);
#83985=ORIENTED_EDGE('',*,*,#56652,.T.);
#83986=ORIENTED_EDGE('',*,*,#56653,.T.);
#83987=ORIENTED_EDGE('',*,*,#56654,.T.);
#83988=ORIENTED_EDGE('',*,*,#56655,.T.);
#83989=ORIENTED_EDGE('',*,*,#56656,.F.);
#83990=ORIENTED_EDGE('',*,*,#56657,.T.);
#83991=ORIENTED_EDGE('',*,*,#56658,.T.);
#83992=ORIENTED_EDGE('',*,*,#56656,.T.);
#83993=ORIENTED_EDGE('',*,*,#56659,.T.);
#83994=ORIENTED_EDGE('',*,*,#56660,.T.);
#83995=ORIENTED_EDGE('',*,*,#56649,.F.);
#83996=ORIENTED_EDGE('',*,*,#56661,.T.);
#83997=ORIENTED_EDGE('',*,*,#56662,.T.);
#83998=ORIENTED_EDGE('',*,*,#56663,.F.);
#83999=ORIENTED_EDGE('',*,*,#56657,.F.);
#84000=ORIENTED_EDGE('',*,*,#56664,.F.);
#84001=ORIENTED_EDGE('',*,*,#56665,.F.);
#84002=ORIENTED_EDGE('',*,*,#56664,.T.);
#84003=ORIENTED_EDGE('',*,*,#56662,.F.);
#84004=ORIENTED_EDGE('',*,*,#56661,.F.);
#84005=ORIENTED_EDGE('',*,*,#56666,.F.);
#84006=ORIENTED_EDGE('',*,*,#56667,.F.);
#84007=ORIENTED_EDGE('',*,*,#56666,.T.);
#84008=ORIENTED_EDGE('',*,*,#56653,.F.);
#84009=ORIENTED_EDGE('',*,*,#56668,.F.);
#84010=ORIENTED_EDGE('',*,*,#56669,.F.);
#84011=ORIENTED_EDGE('',*,*,#56670,.T.);
#84012=ORIENTED_EDGE('',*,*,#56663,.T.);
#84013=ORIENTED_EDGE('',*,*,#54055,.F.);
#84014=ORIENTED_EDGE('',*,*,#54978,.T.);
#84015=ORIENTED_EDGE('',*,*,#56671,.F.);
#84016=ORIENTED_EDGE('',*,*,#56658,.F.);
#84017=ORIENTED_EDGE('',*,*,#56670,.F.);
#84018=ORIENTED_EDGE('',*,*,#54977,.F.);
#84019=ORIENTED_EDGE('',*,*,#56671,.T.);
#84020=ORIENTED_EDGE('',*,*,#55039,.F.);
#84021=ORIENTED_EDGE('',*,*,#56672,.F.);
#84022=ORIENTED_EDGE('',*,*,#56654,.F.);
#84023=ORIENTED_EDGE('',*,*,#56672,.T.);
#84024=ORIENTED_EDGE('',*,*,#54450,.F.);
#84025=ORIENTED_EDGE('',*,*,#56673,.F.);
#84026=ORIENTED_EDGE('',*,*,#56655,.F.);
#84027=ORIENTED_EDGE('',*,*,#56673,.T.);
#84028=ORIENTED_EDGE('',*,*,#54449,.F.);
#84029=ORIENTED_EDGE('',*,*,#56674,.F.);
#84030=ORIENTED_EDGE('',*,*,#56660,.F.);
#84031=ORIENTED_EDGE('',*,*,#56659,.F.);
#84032=ORIENTED_EDGE('',*,*,#56674,.T.);
#84033=ORIENTED_EDGE('',*,*,#54448,.F.);
#84034=ORIENTED_EDGE('',*,*,#56675,.F.);
#84035=ORIENTED_EDGE('',*,*,#56650,.F.);
#84036=ORIENTED_EDGE('',*,*,#56676,.T.);
#84037=ORIENTED_EDGE('',*,*,#56651,.F.);
#84038=ORIENTED_EDGE('',*,*,#56675,.T.);
#84039=ORIENTED_EDGE('',*,*,#55040,.F.);
#84040=ORIENTED_EDGE('',*,*,#56677,.T.);
#84041=ORIENTED_EDGE('',*,*,#56652,.F.);
#84042=ORIENTED_EDGE('',*,*,#56676,.F.);
#84043=ORIENTED_EDGE('',*,*,#54980,.F.);
#84044=ORIENTED_EDGE('',*,*,#54053,.T.);
#84045=ORIENTED_EDGE('',*,*,#56668,.T.);
#84046=ORIENTED_EDGE('',*,*,#56677,.F.);
#84047=ORIENTED_EDGE('',*,*,#54979,.T.);
#84048=ORIENTED_EDGE('',*,*,#56667,.T.);
#84049=ORIENTED_EDGE('',*,*,#56669,.T.);
#84050=ORIENTED_EDGE('',*,*,#54052,.T.);
#84051=ORIENTED_EDGE('',*,*,#56665,.T.);
#84052=ORIENTED_EDGE('',*,*,#56678,.T.);
#84053=ORIENTED_EDGE('',*,*,#56679,.T.);
#84054=ORIENTED_EDGE('',*,*,#56680,.T.);
#84055=ORIENTED_EDGE('',*,*,#56681,.T.);
#84056=ORIENTED_EDGE('',*,*,#56682,.T.);
#84057=ORIENTED_EDGE('',*,*,#56683,.T.);
#84058=ORIENTED_EDGE('',*,*,#56684,.T.);
#84059=ORIENTED_EDGE('',*,*,#56685,.F.);
#84060=ORIENTED_EDGE('',*,*,#56686,.T.);
#84061=ORIENTED_EDGE('',*,*,#56687,.T.);
#84062=ORIENTED_EDGE('',*,*,#56685,.T.);
#84063=ORIENTED_EDGE('',*,*,#56688,.T.);
#84064=ORIENTED_EDGE('',*,*,#56689,.T.);
#84065=ORIENTED_EDGE('',*,*,#56678,.F.);
#84066=ORIENTED_EDGE('',*,*,#56690,.T.);
#84067=ORIENTED_EDGE('',*,*,#56691,.T.);
#84068=ORIENTED_EDGE('',*,*,#56692,.F.);
#84069=ORIENTED_EDGE('',*,*,#56686,.F.);
#84070=ORIENTED_EDGE('',*,*,#56693,.F.);
#84071=ORIENTED_EDGE('',*,*,#56694,.F.);
#84072=ORIENTED_EDGE('',*,*,#56693,.T.);
#84073=ORIENTED_EDGE('',*,*,#56691,.F.);
#84074=ORIENTED_EDGE('',*,*,#56690,.F.);
#84075=ORIENTED_EDGE('',*,*,#56695,.F.);
#84076=ORIENTED_EDGE('',*,*,#56696,.F.);
#84077=ORIENTED_EDGE('',*,*,#56695,.T.);
#84078=ORIENTED_EDGE('',*,*,#56682,.F.);
#84079=ORIENTED_EDGE('',*,*,#56697,.F.);
#84080=ORIENTED_EDGE('',*,*,#56698,.F.);
#84081=ORIENTED_EDGE('',*,*,#56699,.T.);
#84082=ORIENTED_EDGE('',*,*,#56692,.T.);
#84083=ORIENTED_EDGE('',*,*,#54051,.F.);
#84084=ORIENTED_EDGE('',*,*,#54973,.T.);
#84085=ORIENTED_EDGE('',*,*,#56700,.F.);
#84086=ORIENTED_EDGE('',*,*,#56687,.F.);
#84087=ORIENTED_EDGE('',*,*,#56699,.F.);
#84088=ORIENTED_EDGE('',*,*,#54972,.F.);
#84089=ORIENTED_EDGE('',*,*,#56700,.T.);
#84090=ORIENTED_EDGE('',*,*,#55037,.F.);
#84091=ORIENTED_EDGE('',*,*,#56701,.F.);
#84092=ORIENTED_EDGE('',*,*,#56683,.F.);
#84093=ORIENTED_EDGE('',*,*,#56701,.T.);
#84094=ORIENTED_EDGE('',*,*,#54454,.F.);
#84095=ORIENTED_EDGE('',*,*,#56702,.F.);
#84096=ORIENTED_EDGE('',*,*,#56684,.F.);
#84097=ORIENTED_EDGE('',*,*,#56702,.T.);
#84098=ORIENTED_EDGE('',*,*,#54453,.F.);
#84099=ORIENTED_EDGE('',*,*,#56703,.F.);
#84100=ORIENTED_EDGE('',*,*,#56689,.F.);
#84101=ORIENTED_EDGE('',*,*,#56688,.F.);
#84102=ORIENTED_EDGE('',*,*,#56703,.T.);
#84103=ORIENTED_EDGE('',*,*,#54452,.F.);
#84104=ORIENTED_EDGE('',*,*,#56704,.F.);
#84105=ORIENTED_EDGE('',*,*,#56679,.F.);
#84106=ORIENTED_EDGE('',*,*,#56705,.T.);
#84107=ORIENTED_EDGE('',*,*,#56680,.F.);
#84108=ORIENTED_EDGE('',*,*,#56704,.T.);
#84109=ORIENTED_EDGE('',*,*,#55038,.F.);
#84110=ORIENTED_EDGE('',*,*,#56706,.T.);
#84111=ORIENTED_EDGE('',*,*,#56681,.F.);
#84112=ORIENTED_EDGE('',*,*,#56705,.F.);
#84113=ORIENTED_EDGE('',*,*,#54975,.F.);
#84114=ORIENTED_EDGE('',*,*,#54049,.T.);
#84115=ORIENTED_EDGE('',*,*,#56697,.T.);
#84116=ORIENTED_EDGE('',*,*,#56706,.F.);
#84117=ORIENTED_EDGE('',*,*,#54974,.T.);
#84118=ORIENTED_EDGE('',*,*,#56696,.T.);
#84119=ORIENTED_EDGE('',*,*,#56698,.T.);
#84120=ORIENTED_EDGE('',*,*,#54048,.T.);
#84121=ORIENTED_EDGE('',*,*,#56694,.T.);
#84122=ORIENTED_EDGE('',*,*,#56707,.T.);
#84123=ORIENTED_EDGE('',*,*,#56708,.T.);
#84124=ORIENTED_EDGE('',*,*,#56709,.T.);
#84125=ORIENTED_EDGE('',*,*,#56710,.T.);
#84126=ORIENTED_EDGE('',*,*,#56711,.T.);
#84127=ORIENTED_EDGE('',*,*,#56712,.T.);
#84128=ORIENTED_EDGE('',*,*,#56713,.T.);
#84129=ORIENTED_EDGE('',*,*,#56714,.F.);
#84130=ORIENTED_EDGE('',*,*,#56715,.T.);
#84131=ORIENTED_EDGE('',*,*,#56716,.T.);
#84132=ORIENTED_EDGE('',*,*,#56714,.T.);
#84133=ORIENTED_EDGE('',*,*,#56717,.T.);
#84134=ORIENTED_EDGE('',*,*,#56718,.T.);
#84135=ORIENTED_EDGE('',*,*,#56707,.F.);
#84136=ORIENTED_EDGE('',*,*,#56719,.T.);
#84137=ORIENTED_EDGE('',*,*,#56720,.T.);
#84138=ORIENTED_EDGE('',*,*,#56721,.F.);
#84139=ORIENTED_EDGE('',*,*,#56715,.F.);
#84140=ORIENTED_EDGE('',*,*,#56722,.F.);
#84141=ORIENTED_EDGE('',*,*,#56723,.F.);
#84142=ORIENTED_EDGE('',*,*,#56722,.T.);
#84143=ORIENTED_EDGE('',*,*,#56720,.F.);
#84144=ORIENTED_EDGE('',*,*,#56719,.F.);
#84145=ORIENTED_EDGE('',*,*,#56724,.F.);
#84146=ORIENTED_EDGE('',*,*,#56725,.F.);
#84147=ORIENTED_EDGE('',*,*,#56724,.T.);
#84148=ORIENTED_EDGE('',*,*,#56711,.F.);
#84149=ORIENTED_EDGE('',*,*,#56726,.F.);
#84150=ORIENTED_EDGE('',*,*,#56727,.F.);
#84151=ORIENTED_EDGE('',*,*,#56728,.T.);
#84152=ORIENTED_EDGE('',*,*,#56721,.T.);
#84153=ORIENTED_EDGE('',*,*,#54047,.F.);
#84154=ORIENTED_EDGE('',*,*,#54968,.T.);
#84155=ORIENTED_EDGE('',*,*,#56729,.F.);
#84156=ORIENTED_EDGE('',*,*,#56716,.F.);
#84157=ORIENTED_EDGE('',*,*,#56728,.F.);
#84158=ORIENTED_EDGE('',*,*,#54967,.F.);
#84159=ORIENTED_EDGE('',*,*,#56729,.T.);
#84160=ORIENTED_EDGE('',*,*,#55035,.F.);
#84161=ORIENTED_EDGE('',*,*,#56730,.F.);
#84162=ORIENTED_EDGE('',*,*,#56712,.F.);
#84163=ORIENTED_EDGE('',*,*,#56730,.T.);
#84164=ORIENTED_EDGE('',*,*,#54458,.F.);
#84165=ORIENTED_EDGE('',*,*,#56731,.F.);
#84166=ORIENTED_EDGE('',*,*,#56713,.F.);
#84167=ORIENTED_EDGE('',*,*,#56731,.T.);
#84168=ORIENTED_EDGE('',*,*,#54457,.F.);
#84169=ORIENTED_EDGE('',*,*,#56732,.F.);
#84170=ORIENTED_EDGE('',*,*,#56718,.F.);
#84171=ORIENTED_EDGE('',*,*,#56717,.F.);
#84172=ORIENTED_EDGE('',*,*,#56732,.T.);
#84173=ORIENTED_EDGE('',*,*,#54456,.F.);
#84174=ORIENTED_EDGE('',*,*,#56733,.F.);
#84175=ORIENTED_EDGE('',*,*,#56708,.F.);
#84176=ORIENTED_EDGE('',*,*,#56734,.T.);
#84177=ORIENTED_EDGE('',*,*,#56709,.F.);
#84178=ORIENTED_EDGE('',*,*,#56733,.T.);
#84179=ORIENTED_EDGE('',*,*,#55036,.F.);
#84180=ORIENTED_EDGE('',*,*,#56735,.T.);
#84181=ORIENTED_EDGE('',*,*,#56710,.F.);
#84182=ORIENTED_EDGE('',*,*,#56734,.F.);
#84183=ORIENTED_EDGE('',*,*,#54970,.F.);
#84184=ORIENTED_EDGE('',*,*,#54045,.T.);
#84185=ORIENTED_EDGE('',*,*,#56726,.T.);
#84186=ORIENTED_EDGE('',*,*,#56735,.F.);
#84187=ORIENTED_EDGE('',*,*,#54969,.T.);
#84188=ORIENTED_EDGE('',*,*,#56725,.T.);
#84189=ORIENTED_EDGE('',*,*,#56727,.T.);
#84190=ORIENTED_EDGE('',*,*,#54044,.T.);
#84191=ORIENTED_EDGE('',*,*,#56723,.T.);
#84192=ORIENTED_EDGE('',*,*,#56736,.T.);
#84193=ORIENTED_EDGE('',*,*,#56737,.T.);
#84194=ORIENTED_EDGE('',*,*,#56738,.T.);
#84195=ORIENTED_EDGE('',*,*,#56739,.T.);
#84196=ORIENTED_EDGE('',*,*,#56740,.T.);
#84197=ORIENTED_EDGE('',*,*,#56741,.T.);
#84198=ORIENTED_EDGE('',*,*,#56742,.T.);
#84199=ORIENTED_EDGE('',*,*,#56743,.F.);
#84200=ORIENTED_EDGE('',*,*,#56744,.T.);
#84201=ORIENTED_EDGE('',*,*,#56745,.T.);
#84202=ORIENTED_EDGE('',*,*,#56743,.T.);
#84203=ORIENTED_EDGE('',*,*,#56746,.T.);
#84204=ORIENTED_EDGE('',*,*,#56747,.T.);
#84205=ORIENTED_EDGE('',*,*,#56736,.F.);
#84206=ORIENTED_EDGE('',*,*,#56748,.T.);
#84207=ORIENTED_EDGE('',*,*,#56749,.T.);
#84208=ORIENTED_EDGE('',*,*,#56750,.F.);
#84209=ORIENTED_EDGE('',*,*,#56744,.F.);
#84210=ORIENTED_EDGE('',*,*,#56751,.F.);
#84211=ORIENTED_EDGE('',*,*,#56752,.F.);
#84212=ORIENTED_EDGE('',*,*,#56751,.T.);
#84213=ORIENTED_EDGE('',*,*,#56749,.F.);
#84214=ORIENTED_EDGE('',*,*,#56748,.F.);
#84215=ORIENTED_EDGE('',*,*,#56753,.F.);
#84216=ORIENTED_EDGE('',*,*,#56754,.F.);
#84217=ORIENTED_EDGE('',*,*,#56753,.T.);
#84218=ORIENTED_EDGE('',*,*,#56740,.F.);
#84219=ORIENTED_EDGE('',*,*,#56755,.F.);
#84220=ORIENTED_EDGE('',*,*,#56756,.F.);
#84221=ORIENTED_EDGE('',*,*,#56757,.T.);
#84222=ORIENTED_EDGE('',*,*,#56750,.T.);
#84223=ORIENTED_EDGE('',*,*,#54043,.F.);
#84224=ORIENTED_EDGE('',*,*,#54963,.T.);
#84225=ORIENTED_EDGE('',*,*,#56758,.F.);
#84226=ORIENTED_EDGE('',*,*,#56745,.F.);
#84227=ORIENTED_EDGE('',*,*,#56757,.F.);
#84228=ORIENTED_EDGE('',*,*,#54962,.F.);
#84229=ORIENTED_EDGE('',*,*,#56758,.T.);
#84230=ORIENTED_EDGE('',*,*,#55033,.F.);
#84231=ORIENTED_EDGE('',*,*,#56759,.F.);
#84232=ORIENTED_EDGE('',*,*,#56741,.F.);
#84233=ORIENTED_EDGE('',*,*,#56759,.T.);
#84234=ORIENTED_EDGE('',*,*,#54462,.F.);
#84235=ORIENTED_EDGE('',*,*,#56760,.F.);
#84236=ORIENTED_EDGE('',*,*,#56742,.F.);
#84237=ORIENTED_EDGE('',*,*,#56760,.T.);
#84238=ORIENTED_EDGE('',*,*,#54461,.F.);
#84239=ORIENTED_EDGE('',*,*,#56761,.F.);
#84240=ORIENTED_EDGE('',*,*,#56747,.F.);
#84241=ORIENTED_EDGE('',*,*,#56746,.F.);
#84242=ORIENTED_EDGE('',*,*,#56761,.T.);
#84243=ORIENTED_EDGE('',*,*,#54460,.F.);
#84244=ORIENTED_EDGE('',*,*,#56762,.F.);
#84245=ORIENTED_EDGE('',*,*,#56737,.F.);
#84246=ORIENTED_EDGE('',*,*,#56763,.T.);
#84247=ORIENTED_EDGE('',*,*,#56738,.F.);
#84248=ORIENTED_EDGE('',*,*,#56762,.T.);
#84249=ORIENTED_EDGE('',*,*,#55034,.F.);
#84250=ORIENTED_EDGE('',*,*,#56764,.T.);
#84251=ORIENTED_EDGE('',*,*,#56739,.F.);
#84252=ORIENTED_EDGE('',*,*,#56763,.F.);
#84253=ORIENTED_EDGE('',*,*,#54965,.F.);
#84254=ORIENTED_EDGE('',*,*,#54041,.T.);
#84255=ORIENTED_EDGE('',*,*,#56755,.T.);
#84256=ORIENTED_EDGE('',*,*,#56764,.F.);
#84257=ORIENTED_EDGE('',*,*,#54964,.T.);
#84258=ORIENTED_EDGE('',*,*,#56754,.T.);
#84259=ORIENTED_EDGE('',*,*,#56756,.T.);
#84260=ORIENTED_EDGE('',*,*,#54040,.T.);
#84261=ORIENTED_EDGE('',*,*,#56752,.T.);
#84262=ORIENTED_EDGE('',*,*,#56765,.T.);
#84263=ORIENTED_EDGE('',*,*,#56766,.T.);
#84264=ORIENTED_EDGE('',*,*,#56767,.T.);
#84265=ORIENTED_EDGE('',*,*,#56768,.T.);
#84266=ORIENTED_EDGE('',*,*,#56769,.T.);
#84267=ORIENTED_EDGE('',*,*,#56770,.T.);
#84268=ORIENTED_EDGE('',*,*,#56771,.T.);
#84269=ORIENTED_EDGE('',*,*,#56772,.F.);
#84270=ORIENTED_EDGE('',*,*,#56773,.T.);
#84271=ORIENTED_EDGE('',*,*,#56774,.T.);
#84272=ORIENTED_EDGE('',*,*,#56772,.T.);
#84273=ORIENTED_EDGE('',*,*,#56775,.T.);
#84274=ORIENTED_EDGE('',*,*,#56776,.T.);
#84275=ORIENTED_EDGE('',*,*,#56765,.F.);
#84276=ORIENTED_EDGE('',*,*,#56777,.T.);
#84277=ORIENTED_EDGE('',*,*,#56778,.T.);
#84278=ORIENTED_EDGE('',*,*,#56779,.F.);
#84279=ORIENTED_EDGE('',*,*,#56773,.F.);
#84280=ORIENTED_EDGE('',*,*,#56780,.F.);
#84281=ORIENTED_EDGE('',*,*,#56781,.F.);
#84282=ORIENTED_EDGE('',*,*,#56780,.T.);
#84283=ORIENTED_EDGE('',*,*,#56778,.F.);
#84284=ORIENTED_EDGE('',*,*,#56777,.F.);
#84285=ORIENTED_EDGE('',*,*,#56782,.F.);
#84286=ORIENTED_EDGE('',*,*,#56783,.F.);
#84287=ORIENTED_EDGE('',*,*,#56782,.T.);
#84288=ORIENTED_EDGE('',*,*,#56769,.F.);
#84289=ORIENTED_EDGE('',*,*,#56784,.F.);
#84290=ORIENTED_EDGE('',*,*,#56785,.F.);
#84291=ORIENTED_EDGE('',*,*,#56786,.T.);
#84292=ORIENTED_EDGE('',*,*,#56779,.T.);
#84293=ORIENTED_EDGE('',*,*,#54039,.F.);
#84294=ORIENTED_EDGE('',*,*,#54958,.T.);
#84295=ORIENTED_EDGE('',*,*,#56787,.F.);
#84296=ORIENTED_EDGE('',*,*,#56774,.F.);
#84297=ORIENTED_EDGE('',*,*,#56786,.F.);
#84298=ORIENTED_EDGE('',*,*,#54957,.F.);
#84299=ORIENTED_EDGE('',*,*,#56787,.T.);
#84300=ORIENTED_EDGE('',*,*,#55031,.F.);
#84301=ORIENTED_EDGE('',*,*,#56788,.F.);
#84302=ORIENTED_EDGE('',*,*,#56770,.F.);
#84303=ORIENTED_EDGE('',*,*,#56788,.T.);
#84304=ORIENTED_EDGE('',*,*,#54466,.F.);
#84305=ORIENTED_EDGE('',*,*,#56789,.F.);
#84306=ORIENTED_EDGE('',*,*,#56771,.F.);
#84307=ORIENTED_EDGE('',*,*,#56789,.T.);
#84308=ORIENTED_EDGE('',*,*,#54465,.F.);
#84309=ORIENTED_EDGE('',*,*,#56790,.F.);
#84310=ORIENTED_EDGE('',*,*,#56776,.F.);
#84311=ORIENTED_EDGE('',*,*,#56775,.F.);
#84312=ORIENTED_EDGE('',*,*,#56790,.T.);
#84313=ORIENTED_EDGE('',*,*,#54464,.F.);
#84314=ORIENTED_EDGE('',*,*,#56791,.F.);
#84315=ORIENTED_EDGE('',*,*,#56766,.F.);
#84316=ORIENTED_EDGE('',*,*,#56792,.T.);
#84317=ORIENTED_EDGE('',*,*,#56767,.F.);
#84318=ORIENTED_EDGE('',*,*,#56791,.T.);
#84319=ORIENTED_EDGE('',*,*,#55032,.F.);
#84320=ORIENTED_EDGE('',*,*,#56793,.T.);
#84321=ORIENTED_EDGE('',*,*,#56768,.F.);
#84322=ORIENTED_EDGE('',*,*,#56792,.F.);
#84323=ORIENTED_EDGE('',*,*,#54960,.F.);
#84324=ORIENTED_EDGE('',*,*,#54037,.T.);
#84325=ORIENTED_EDGE('',*,*,#56784,.T.);
#84326=ORIENTED_EDGE('',*,*,#56793,.F.);
#84327=ORIENTED_EDGE('',*,*,#54959,.T.);
#84328=ORIENTED_EDGE('',*,*,#56783,.T.);
#84329=ORIENTED_EDGE('',*,*,#56785,.T.);
#84330=ORIENTED_EDGE('',*,*,#54036,.T.);
#84331=ORIENTED_EDGE('',*,*,#56781,.T.);
#84332=ORIENTED_EDGE('',*,*,#56794,.T.);
#84333=ORIENTED_EDGE('',*,*,#56795,.T.);
#84334=ORIENTED_EDGE('',*,*,#56796,.T.);
#84335=ORIENTED_EDGE('',*,*,#56797,.T.);
#84336=ORIENTED_EDGE('',*,*,#56798,.T.);
#84337=ORIENTED_EDGE('',*,*,#56799,.T.);
#84338=ORIENTED_EDGE('',*,*,#56800,.T.);
#84339=ORIENTED_EDGE('',*,*,#56801,.F.);
#84340=ORIENTED_EDGE('',*,*,#56802,.T.);
#84341=ORIENTED_EDGE('',*,*,#56803,.T.);
#84342=ORIENTED_EDGE('',*,*,#56801,.T.);
#84343=ORIENTED_EDGE('',*,*,#56804,.T.);
#84344=ORIENTED_EDGE('',*,*,#56805,.T.);
#84345=ORIENTED_EDGE('',*,*,#56794,.F.);
#84346=ORIENTED_EDGE('',*,*,#56806,.T.);
#84347=ORIENTED_EDGE('',*,*,#56807,.T.);
#84348=ORIENTED_EDGE('',*,*,#56808,.F.);
#84349=ORIENTED_EDGE('',*,*,#56802,.F.);
#84350=ORIENTED_EDGE('',*,*,#56809,.F.);
#84351=ORIENTED_EDGE('',*,*,#56810,.F.);
#84352=ORIENTED_EDGE('',*,*,#56809,.T.);
#84353=ORIENTED_EDGE('',*,*,#56807,.F.);
#84354=ORIENTED_EDGE('',*,*,#56806,.F.);
#84355=ORIENTED_EDGE('',*,*,#56811,.F.);
#84356=ORIENTED_EDGE('',*,*,#56812,.F.);
#84357=ORIENTED_EDGE('',*,*,#56811,.T.);
#84358=ORIENTED_EDGE('',*,*,#56798,.F.);
#84359=ORIENTED_EDGE('',*,*,#56813,.F.);
#84360=ORIENTED_EDGE('',*,*,#56814,.F.);
#84361=ORIENTED_EDGE('',*,*,#56815,.T.);
#84362=ORIENTED_EDGE('',*,*,#56808,.T.);
#84363=ORIENTED_EDGE('',*,*,#54035,.F.);
#84364=ORIENTED_EDGE('',*,*,#54953,.T.);
#84365=ORIENTED_EDGE('',*,*,#56816,.F.);
#84366=ORIENTED_EDGE('',*,*,#56803,.F.);
#84367=ORIENTED_EDGE('',*,*,#56815,.F.);
#84368=ORIENTED_EDGE('',*,*,#54952,.F.);
#84369=ORIENTED_EDGE('',*,*,#56816,.T.);
#84370=ORIENTED_EDGE('',*,*,#55029,.F.);
#84371=ORIENTED_EDGE('',*,*,#56817,.F.);
#84372=ORIENTED_EDGE('',*,*,#56799,.F.);
#84373=ORIENTED_EDGE('',*,*,#56817,.T.);
#84374=ORIENTED_EDGE('',*,*,#54470,.F.);
#84375=ORIENTED_EDGE('',*,*,#56818,.F.);
#84376=ORIENTED_EDGE('',*,*,#56800,.F.);
#84377=ORIENTED_EDGE('',*,*,#56818,.T.);
#84378=ORIENTED_EDGE('',*,*,#54469,.F.);
#84379=ORIENTED_EDGE('',*,*,#56819,.F.);
#84380=ORIENTED_EDGE('',*,*,#56805,.F.);
#84381=ORIENTED_EDGE('',*,*,#56804,.F.);
#84382=ORIENTED_EDGE('',*,*,#56819,.T.);
#84383=ORIENTED_EDGE('',*,*,#54468,.F.);
#84384=ORIENTED_EDGE('',*,*,#56820,.F.);
#84385=ORIENTED_EDGE('',*,*,#56795,.F.);
#84386=ORIENTED_EDGE('',*,*,#56821,.T.);
#84387=ORIENTED_EDGE('',*,*,#56796,.F.);
#84388=ORIENTED_EDGE('',*,*,#56820,.T.);
#84389=ORIENTED_EDGE('',*,*,#55030,.F.);
#84390=ORIENTED_EDGE('',*,*,#56822,.T.);
#84391=ORIENTED_EDGE('',*,*,#56797,.F.);
#84392=ORIENTED_EDGE('',*,*,#56821,.F.);
#84393=ORIENTED_EDGE('',*,*,#54955,.F.);
#84394=ORIENTED_EDGE('',*,*,#54033,.T.);
#84395=ORIENTED_EDGE('',*,*,#56813,.T.);
#84396=ORIENTED_EDGE('',*,*,#56822,.F.);
#84397=ORIENTED_EDGE('',*,*,#54954,.T.);
#84398=ORIENTED_EDGE('',*,*,#56812,.T.);
#84399=ORIENTED_EDGE('',*,*,#56814,.T.);
#84400=ORIENTED_EDGE('',*,*,#54032,.T.);
#84401=ORIENTED_EDGE('',*,*,#56810,.T.);
#84402=ORIENTED_EDGE('',*,*,#56823,.T.);
#84403=ORIENTED_EDGE('',*,*,#56824,.T.);
#84404=ORIENTED_EDGE('',*,*,#56825,.T.);
#84405=ORIENTED_EDGE('',*,*,#56826,.T.);
#84406=ORIENTED_EDGE('',*,*,#56827,.T.);
#84407=ORIENTED_EDGE('',*,*,#56828,.T.);
#84408=ORIENTED_EDGE('',*,*,#56829,.T.);
#84409=ORIENTED_EDGE('',*,*,#56830,.F.);
#84410=ORIENTED_EDGE('',*,*,#56831,.T.);
#84411=ORIENTED_EDGE('',*,*,#56832,.T.);
#84412=ORIENTED_EDGE('',*,*,#56830,.T.);
#84413=ORIENTED_EDGE('',*,*,#56833,.T.);
#84414=ORIENTED_EDGE('',*,*,#56834,.T.);
#84415=ORIENTED_EDGE('',*,*,#56823,.F.);
#84416=ORIENTED_EDGE('',*,*,#56835,.T.);
#84417=ORIENTED_EDGE('',*,*,#56836,.T.);
#84418=ORIENTED_EDGE('',*,*,#56837,.F.);
#84419=ORIENTED_EDGE('',*,*,#56831,.F.);
#84420=ORIENTED_EDGE('',*,*,#56838,.F.);
#84421=ORIENTED_EDGE('',*,*,#56839,.F.);
#84422=ORIENTED_EDGE('',*,*,#56838,.T.);
#84423=ORIENTED_EDGE('',*,*,#56836,.F.);
#84424=ORIENTED_EDGE('',*,*,#56835,.F.);
#84425=ORIENTED_EDGE('',*,*,#56840,.F.);
#84426=ORIENTED_EDGE('',*,*,#56841,.F.);
#84427=ORIENTED_EDGE('',*,*,#56840,.T.);
#84428=ORIENTED_EDGE('',*,*,#56827,.F.);
#84429=ORIENTED_EDGE('',*,*,#56842,.F.);
#84430=ORIENTED_EDGE('',*,*,#56843,.F.);
#84431=ORIENTED_EDGE('',*,*,#56844,.T.);
#84432=ORIENTED_EDGE('',*,*,#56837,.T.);
#84433=ORIENTED_EDGE('',*,*,#54031,.F.);
#84434=ORIENTED_EDGE('',*,*,#54948,.T.);
#84435=ORIENTED_EDGE('',*,*,#56845,.F.);
#84436=ORIENTED_EDGE('',*,*,#56832,.F.);
#84437=ORIENTED_EDGE('',*,*,#56844,.F.);
#84438=ORIENTED_EDGE('',*,*,#54947,.F.);
#84439=ORIENTED_EDGE('',*,*,#56845,.T.);
#84440=ORIENTED_EDGE('',*,*,#55027,.F.);
#84441=ORIENTED_EDGE('',*,*,#56846,.F.);
#84442=ORIENTED_EDGE('',*,*,#56828,.F.);
#84443=ORIENTED_EDGE('',*,*,#56846,.T.);
#84444=ORIENTED_EDGE('',*,*,#54474,.F.);
#84445=ORIENTED_EDGE('',*,*,#56847,.F.);
#84446=ORIENTED_EDGE('',*,*,#56829,.F.);
#84447=ORIENTED_EDGE('',*,*,#56847,.T.);
#84448=ORIENTED_EDGE('',*,*,#54473,.F.);
#84449=ORIENTED_EDGE('',*,*,#56848,.F.);
#84450=ORIENTED_EDGE('',*,*,#56834,.F.);
#84451=ORIENTED_EDGE('',*,*,#56833,.F.);
#84452=ORIENTED_EDGE('',*,*,#56848,.T.);
#84453=ORIENTED_EDGE('',*,*,#54472,.F.);
#84454=ORIENTED_EDGE('',*,*,#56849,.F.);
#84455=ORIENTED_EDGE('',*,*,#56824,.F.);
#84456=ORIENTED_EDGE('',*,*,#56850,.T.);
#84457=ORIENTED_EDGE('',*,*,#56825,.F.);
#84458=ORIENTED_EDGE('',*,*,#56849,.T.);
#84459=ORIENTED_EDGE('',*,*,#55028,.F.);
#84460=ORIENTED_EDGE('',*,*,#56851,.T.);
#84461=ORIENTED_EDGE('',*,*,#56826,.F.);
#84462=ORIENTED_EDGE('',*,*,#56850,.F.);
#84463=ORIENTED_EDGE('',*,*,#54950,.F.);
#84464=ORIENTED_EDGE('',*,*,#54029,.T.);
#84465=ORIENTED_EDGE('',*,*,#56842,.T.);
#84466=ORIENTED_EDGE('',*,*,#56851,.F.);
#84467=ORIENTED_EDGE('',*,*,#54949,.T.);
#84468=ORIENTED_EDGE('',*,*,#56841,.T.);
#84469=ORIENTED_EDGE('',*,*,#56843,.T.);
#84470=ORIENTED_EDGE('',*,*,#54028,.T.);
#84471=ORIENTED_EDGE('',*,*,#56839,.T.);
#84472=ORIENTED_EDGE('',*,*,#56852,.T.);
#84473=ORIENTED_EDGE('',*,*,#56853,.T.);
#84474=ORIENTED_EDGE('',*,*,#56854,.T.);
#84475=ORIENTED_EDGE('',*,*,#56855,.T.);
#84476=ORIENTED_EDGE('',*,*,#56856,.T.);
#84477=ORIENTED_EDGE('',*,*,#56857,.T.);
#84478=ORIENTED_EDGE('',*,*,#56858,.T.);
#84479=ORIENTED_EDGE('',*,*,#56859,.F.);
#84480=ORIENTED_EDGE('',*,*,#56860,.T.);
#84481=ORIENTED_EDGE('',*,*,#56861,.T.);
#84482=ORIENTED_EDGE('',*,*,#56859,.T.);
#84483=ORIENTED_EDGE('',*,*,#56862,.T.);
#84484=ORIENTED_EDGE('',*,*,#56863,.T.);
#84485=ORIENTED_EDGE('',*,*,#56852,.F.);
#84486=ORIENTED_EDGE('',*,*,#56864,.T.);
#84487=ORIENTED_EDGE('',*,*,#56865,.T.);
#84488=ORIENTED_EDGE('',*,*,#56866,.F.);
#84489=ORIENTED_EDGE('',*,*,#56860,.F.);
#84490=ORIENTED_EDGE('',*,*,#56867,.F.);
#84491=ORIENTED_EDGE('',*,*,#56868,.F.);
#84492=ORIENTED_EDGE('',*,*,#56867,.T.);
#84493=ORIENTED_EDGE('',*,*,#56865,.F.);
#84494=ORIENTED_EDGE('',*,*,#56864,.F.);
#84495=ORIENTED_EDGE('',*,*,#56869,.F.);
#84496=ORIENTED_EDGE('',*,*,#56870,.F.);
#84497=ORIENTED_EDGE('',*,*,#56869,.T.);
#84498=ORIENTED_EDGE('',*,*,#56856,.F.);
#84499=ORIENTED_EDGE('',*,*,#56871,.F.);
#84500=ORIENTED_EDGE('',*,*,#56872,.F.);
#84501=ORIENTED_EDGE('',*,*,#56873,.T.);
#84502=ORIENTED_EDGE('',*,*,#56866,.T.);
#84503=ORIENTED_EDGE('',*,*,#54027,.F.);
#84504=ORIENTED_EDGE('',*,*,#54943,.T.);
#84505=ORIENTED_EDGE('',*,*,#56874,.F.);
#84506=ORIENTED_EDGE('',*,*,#56861,.F.);
#84507=ORIENTED_EDGE('',*,*,#56873,.F.);
#84508=ORIENTED_EDGE('',*,*,#54942,.F.);
#84509=ORIENTED_EDGE('',*,*,#56874,.T.);
#84510=ORIENTED_EDGE('',*,*,#55025,.F.);
#84511=ORIENTED_EDGE('',*,*,#56875,.F.);
#84512=ORIENTED_EDGE('',*,*,#56857,.F.);
#84513=ORIENTED_EDGE('',*,*,#56875,.T.);
#84514=ORIENTED_EDGE('',*,*,#54478,.F.);
#84515=ORIENTED_EDGE('',*,*,#56876,.F.);
#84516=ORIENTED_EDGE('',*,*,#56858,.F.);
#84517=ORIENTED_EDGE('',*,*,#56876,.T.);
#84518=ORIENTED_EDGE('',*,*,#54477,.F.);
#84519=ORIENTED_EDGE('',*,*,#56877,.F.);
#84520=ORIENTED_EDGE('',*,*,#56863,.F.);
#84521=ORIENTED_EDGE('',*,*,#56862,.F.);
#84522=ORIENTED_EDGE('',*,*,#56877,.T.);
#84523=ORIENTED_EDGE('',*,*,#54476,.F.);
#84524=ORIENTED_EDGE('',*,*,#56878,.F.);
#84525=ORIENTED_EDGE('',*,*,#56853,.F.);
#84526=ORIENTED_EDGE('',*,*,#56879,.T.);
#84527=ORIENTED_EDGE('',*,*,#56854,.F.);
#84528=ORIENTED_EDGE('',*,*,#56878,.T.);
#84529=ORIENTED_EDGE('',*,*,#55026,.F.);
#84530=ORIENTED_EDGE('',*,*,#56880,.T.);
#84531=ORIENTED_EDGE('',*,*,#56855,.F.);
#84532=ORIENTED_EDGE('',*,*,#56879,.F.);
#84533=ORIENTED_EDGE('',*,*,#54945,.F.);
#84534=ORIENTED_EDGE('',*,*,#54025,.T.);
#84535=ORIENTED_EDGE('',*,*,#56871,.T.);
#84536=ORIENTED_EDGE('',*,*,#56880,.F.);
#84537=ORIENTED_EDGE('',*,*,#54944,.T.);
#84538=ORIENTED_EDGE('',*,*,#56870,.T.);
#84539=ORIENTED_EDGE('',*,*,#56872,.T.);
#84540=ORIENTED_EDGE('',*,*,#54024,.T.);
#84541=ORIENTED_EDGE('',*,*,#56868,.T.);
#84542=ORIENTED_EDGE('',*,*,#56881,.T.);
#84543=ORIENTED_EDGE('',*,*,#56882,.T.);
#84544=ORIENTED_EDGE('',*,*,#56883,.T.);
#84545=ORIENTED_EDGE('',*,*,#56884,.T.);
#84546=ORIENTED_EDGE('',*,*,#56885,.T.);
#84547=ORIENTED_EDGE('',*,*,#56886,.T.);
#84548=ORIENTED_EDGE('',*,*,#56887,.T.);
#84549=ORIENTED_EDGE('',*,*,#56888,.F.);
#84550=ORIENTED_EDGE('',*,*,#56889,.T.);
#84551=ORIENTED_EDGE('',*,*,#56890,.T.);
#84552=ORIENTED_EDGE('',*,*,#56888,.T.);
#84553=ORIENTED_EDGE('',*,*,#56891,.T.);
#84554=ORIENTED_EDGE('',*,*,#56892,.T.);
#84555=ORIENTED_EDGE('',*,*,#56881,.F.);
#84556=ORIENTED_EDGE('',*,*,#56893,.T.);
#84557=ORIENTED_EDGE('',*,*,#56894,.T.);
#84558=ORIENTED_EDGE('',*,*,#56895,.F.);
#84559=ORIENTED_EDGE('',*,*,#56889,.F.);
#84560=ORIENTED_EDGE('',*,*,#56896,.F.);
#84561=ORIENTED_EDGE('',*,*,#56897,.F.);
#84562=ORIENTED_EDGE('',*,*,#56896,.T.);
#84563=ORIENTED_EDGE('',*,*,#56894,.F.);
#84564=ORIENTED_EDGE('',*,*,#56893,.F.);
#84565=ORIENTED_EDGE('',*,*,#56898,.F.);
#84566=ORIENTED_EDGE('',*,*,#56899,.F.);
#84567=ORIENTED_EDGE('',*,*,#56898,.T.);
#84568=ORIENTED_EDGE('',*,*,#56885,.F.);
#84569=ORIENTED_EDGE('',*,*,#56900,.F.);
#84570=ORIENTED_EDGE('',*,*,#56901,.F.);
#84571=ORIENTED_EDGE('',*,*,#56902,.T.);
#84572=ORIENTED_EDGE('',*,*,#56895,.T.);
#84573=ORIENTED_EDGE('',*,*,#54023,.F.);
#84574=ORIENTED_EDGE('',*,*,#54938,.T.);
#84575=ORIENTED_EDGE('',*,*,#56903,.F.);
#84576=ORIENTED_EDGE('',*,*,#56890,.F.);
#84577=ORIENTED_EDGE('',*,*,#56902,.F.);
#84578=ORIENTED_EDGE('',*,*,#54937,.F.);
#84579=ORIENTED_EDGE('',*,*,#56903,.T.);
#84580=ORIENTED_EDGE('',*,*,#55023,.F.);
#84581=ORIENTED_EDGE('',*,*,#56904,.F.);
#84582=ORIENTED_EDGE('',*,*,#56886,.F.);
#84583=ORIENTED_EDGE('',*,*,#56904,.T.);
#84584=ORIENTED_EDGE('',*,*,#54482,.F.);
#84585=ORIENTED_EDGE('',*,*,#56905,.F.);
#84586=ORIENTED_EDGE('',*,*,#56887,.F.);
#84587=ORIENTED_EDGE('',*,*,#56905,.T.);
#84588=ORIENTED_EDGE('',*,*,#54481,.F.);
#84589=ORIENTED_EDGE('',*,*,#56906,.F.);
#84590=ORIENTED_EDGE('',*,*,#56892,.F.);
#84591=ORIENTED_EDGE('',*,*,#56891,.F.);
#84592=ORIENTED_EDGE('',*,*,#56906,.T.);
#84593=ORIENTED_EDGE('',*,*,#54480,.F.);
#84594=ORIENTED_EDGE('',*,*,#56907,.F.);
#84595=ORIENTED_EDGE('',*,*,#56882,.F.);
#84596=ORIENTED_EDGE('',*,*,#56908,.T.);
#84597=ORIENTED_EDGE('',*,*,#56883,.F.);
#84598=ORIENTED_EDGE('',*,*,#56907,.T.);
#84599=ORIENTED_EDGE('',*,*,#55024,.F.);
#84600=ORIENTED_EDGE('',*,*,#56909,.T.);
#84601=ORIENTED_EDGE('',*,*,#56884,.F.);
#84602=ORIENTED_EDGE('',*,*,#56908,.F.);
#84603=ORIENTED_EDGE('',*,*,#54940,.F.);
#84604=ORIENTED_EDGE('',*,*,#54021,.T.);
#84605=ORIENTED_EDGE('',*,*,#56900,.T.);
#84606=ORIENTED_EDGE('',*,*,#56909,.F.);
#84607=ORIENTED_EDGE('',*,*,#54939,.T.);
#84608=ORIENTED_EDGE('',*,*,#56899,.T.);
#84609=ORIENTED_EDGE('',*,*,#56901,.T.);
#84610=ORIENTED_EDGE('',*,*,#54020,.T.);
#84611=ORIENTED_EDGE('',*,*,#56897,.T.);
#84612=ORIENTED_EDGE('',*,*,#56910,.T.);
#84613=ORIENTED_EDGE('',*,*,#56911,.T.);
#84614=ORIENTED_EDGE('',*,*,#56912,.T.);
#84615=ORIENTED_EDGE('',*,*,#56913,.T.);
#84616=ORIENTED_EDGE('',*,*,#56914,.T.);
#84617=ORIENTED_EDGE('',*,*,#56915,.T.);
#84618=ORIENTED_EDGE('',*,*,#56916,.T.);
#84619=ORIENTED_EDGE('',*,*,#56917,.F.);
#84620=ORIENTED_EDGE('',*,*,#56918,.T.);
#84621=ORIENTED_EDGE('',*,*,#56919,.T.);
#84622=ORIENTED_EDGE('',*,*,#56917,.T.);
#84623=ORIENTED_EDGE('',*,*,#56920,.T.);
#84624=ORIENTED_EDGE('',*,*,#56921,.T.);
#84625=ORIENTED_EDGE('',*,*,#56910,.F.);
#84626=ORIENTED_EDGE('',*,*,#56922,.T.);
#84627=ORIENTED_EDGE('',*,*,#56923,.T.);
#84628=ORIENTED_EDGE('',*,*,#56924,.F.);
#84629=ORIENTED_EDGE('',*,*,#56918,.F.);
#84630=ORIENTED_EDGE('',*,*,#56925,.F.);
#84631=ORIENTED_EDGE('',*,*,#56926,.F.);
#84632=ORIENTED_EDGE('',*,*,#56925,.T.);
#84633=ORIENTED_EDGE('',*,*,#56923,.F.);
#84634=ORIENTED_EDGE('',*,*,#56922,.F.);
#84635=ORIENTED_EDGE('',*,*,#56927,.F.);
#84636=ORIENTED_EDGE('',*,*,#56928,.F.);
#84637=ORIENTED_EDGE('',*,*,#56927,.T.);
#84638=ORIENTED_EDGE('',*,*,#56914,.F.);
#84639=ORIENTED_EDGE('',*,*,#56929,.F.);
#84640=ORIENTED_EDGE('',*,*,#56930,.F.);
#84641=ORIENTED_EDGE('',*,*,#56931,.T.);
#84642=ORIENTED_EDGE('',*,*,#56924,.T.);
#84643=ORIENTED_EDGE('',*,*,#54019,.F.);
#84644=ORIENTED_EDGE('',*,*,#54933,.T.);
#84645=ORIENTED_EDGE('',*,*,#56932,.F.);
#84646=ORIENTED_EDGE('',*,*,#56919,.F.);
#84647=ORIENTED_EDGE('',*,*,#56931,.F.);
#84648=ORIENTED_EDGE('',*,*,#54932,.F.);
#84649=ORIENTED_EDGE('',*,*,#56932,.T.);
#84650=ORIENTED_EDGE('',*,*,#55021,.F.);
#84651=ORIENTED_EDGE('',*,*,#56933,.F.);
#84652=ORIENTED_EDGE('',*,*,#56915,.F.);
#84653=ORIENTED_EDGE('',*,*,#56933,.T.);
#84654=ORIENTED_EDGE('',*,*,#54486,.F.);
#84655=ORIENTED_EDGE('',*,*,#56934,.F.);
#84656=ORIENTED_EDGE('',*,*,#56916,.F.);
#84657=ORIENTED_EDGE('',*,*,#56934,.T.);
#84658=ORIENTED_EDGE('',*,*,#54485,.F.);
#84659=ORIENTED_EDGE('',*,*,#56935,.F.);
#84660=ORIENTED_EDGE('',*,*,#56921,.F.);
#84661=ORIENTED_EDGE('',*,*,#56920,.F.);
#84662=ORIENTED_EDGE('',*,*,#56935,.T.);
#84663=ORIENTED_EDGE('',*,*,#54484,.F.);
#84664=ORIENTED_EDGE('',*,*,#56936,.F.);
#84665=ORIENTED_EDGE('',*,*,#56911,.F.);
#84666=ORIENTED_EDGE('',*,*,#56937,.T.);
#84667=ORIENTED_EDGE('',*,*,#56912,.F.);
#84668=ORIENTED_EDGE('',*,*,#56936,.T.);
#84669=ORIENTED_EDGE('',*,*,#55022,.F.);
#84670=ORIENTED_EDGE('',*,*,#56938,.T.);
#84671=ORIENTED_EDGE('',*,*,#56913,.F.);
#84672=ORIENTED_EDGE('',*,*,#56937,.F.);
#84673=ORIENTED_EDGE('',*,*,#54935,.F.);
#84674=ORIENTED_EDGE('',*,*,#54017,.T.);
#84675=ORIENTED_EDGE('',*,*,#56929,.T.);
#84676=ORIENTED_EDGE('',*,*,#56938,.F.);
#84677=ORIENTED_EDGE('',*,*,#54934,.T.);
#84678=ORIENTED_EDGE('',*,*,#56928,.T.);
#84679=ORIENTED_EDGE('',*,*,#56930,.T.);
#84680=ORIENTED_EDGE('',*,*,#54016,.T.);
#84681=ORIENTED_EDGE('',*,*,#56926,.T.);
#84682=ORIENTED_EDGE('',*,*,#56939,.T.);
#84683=ORIENTED_EDGE('',*,*,#56940,.T.);
#84684=ORIENTED_EDGE('',*,*,#56941,.T.);
#84685=ORIENTED_EDGE('',*,*,#56942,.T.);
#84686=ORIENTED_EDGE('',*,*,#56943,.T.);
#84687=ORIENTED_EDGE('',*,*,#56944,.T.);
#84688=ORIENTED_EDGE('',*,*,#56945,.T.);
#84689=ORIENTED_EDGE('',*,*,#56946,.F.);
#84690=ORIENTED_EDGE('',*,*,#56947,.T.);
#84691=ORIENTED_EDGE('',*,*,#56948,.T.);
#84692=ORIENTED_EDGE('',*,*,#56946,.T.);
#84693=ORIENTED_EDGE('',*,*,#56949,.T.);
#84694=ORIENTED_EDGE('',*,*,#56950,.T.);
#84695=ORIENTED_EDGE('',*,*,#56939,.F.);
#84696=ORIENTED_EDGE('',*,*,#56951,.T.);
#84697=ORIENTED_EDGE('',*,*,#56952,.T.);
#84698=ORIENTED_EDGE('',*,*,#56953,.F.);
#84699=ORIENTED_EDGE('',*,*,#56947,.F.);
#84700=ORIENTED_EDGE('',*,*,#56954,.F.);
#84701=ORIENTED_EDGE('',*,*,#56955,.F.);
#84702=ORIENTED_EDGE('',*,*,#56954,.T.);
#84703=ORIENTED_EDGE('',*,*,#56952,.F.);
#84704=ORIENTED_EDGE('',*,*,#56951,.F.);
#84705=ORIENTED_EDGE('',*,*,#56956,.F.);
#84706=ORIENTED_EDGE('',*,*,#56957,.F.);
#84707=ORIENTED_EDGE('',*,*,#56956,.T.);
#84708=ORIENTED_EDGE('',*,*,#56943,.F.);
#84709=ORIENTED_EDGE('',*,*,#56958,.F.);
#84710=ORIENTED_EDGE('',*,*,#56959,.F.);
#84711=ORIENTED_EDGE('',*,*,#56960,.T.);
#84712=ORIENTED_EDGE('',*,*,#56953,.T.);
#84713=ORIENTED_EDGE('',*,*,#54015,.F.);
#84714=ORIENTED_EDGE('',*,*,#54928,.T.);
#84715=ORIENTED_EDGE('',*,*,#56961,.F.);
#84716=ORIENTED_EDGE('',*,*,#56948,.F.);
#84717=ORIENTED_EDGE('',*,*,#56960,.F.);
#84718=ORIENTED_EDGE('',*,*,#54927,.F.);
#84719=ORIENTED_EDGE('',*,*,#56961,.T.);
#84720=ORIENTED_EDGE('',*,*,#55019,.F.);
#84721=ORIENTED_EDGE('',*,*,#56962,.F.);
#84722=ORIENTED_EDGE('',*,*,#56944,.F.);
#84723=ORIENTED_EDGE('',*,*,#56962,.T.);
#84724=ORIENTED_EDGE('',*,*,#54490,.F.);
#84725=ORIENTED_EDGE('',*,*,#56963,.F.);
#84726=ORIENTED_EDGE('',*,*,#56945,.F.);
#84727=ORIENTED_EDGE('',*,*,#56963,.T.);
#84728=ORIENTED_EDGE('',*,*,#54489,.F.);
#84729=ORIENTED_EDGE('',*,*,#56964,.F.);
#84730=ORIENTED_EDGE('',*,*,#56950,.F.);
#84731=ORIENTED_EDGE('',*,*,#56949,.F.);
#84732=ORIENTED_EDGE('',*,*,#56964,.T.);
#84733=ORIENTED_EDGE('',*,*,#54488,.F.);
#84734=ORIENTED_EDGE('',*,*,#56965,.F.);
#84735=ORIENTED_EDGE('',*,*,#56940,.F.);
#84736=ORIENTED_EDGE('',*,*,#56966,.T.);
#84737=ORIENTED_EDGE('',*,*,#56941,.F.);
#84738=ORIENTED_EDGE('',*,*,#56965,.T.);
#84739=ORIENTED_EDGE('',*,*,#55020,.F.);
#84740=ORIENTED_EDGE('',*,*,#56967,.T.);
#84741=ORIENTED_EDGE('',*,*,#56942,.F.);
#84742=ORIENTED_EDGE('',*,*,#56966,.F.);
#84743=ORIENTED_EDGE('',*,*,#54930,.F.);
#84744=ORIENTED_EDGE('',*,*,#54013,.T.);
#84745=ORIENTED_EDGE('',*,*,#56958,.T.);
#84746=ORIENTED_EDGE('',*,*,#56967,.F.);
#84747=ORIENTED_EDGE('',*,*,#54929,.T.);
#84748=ORIENTED_EDGE('',*,*,#56957,.T.);
#84749=ORIENTED_EDGE('',*,*,#56959,.T.);
#84750=ORIENTED_EDGE('',*,*,#54012,.T.);
#84751=ORIENTED_EDGE('',*,*,#56955,.T.);
#84752=ORIENTED_EDGE('',*,*,#56968,.T.);
#84753=ORIENTED_EDGE('',*,*,#56969,.T.);
#84754=ORIENTED_EDGE('',*,*,#56970,.T.);
#84755=ORIENTED_EDGE('',*,*,#56971,.T.);
#84756=ORIENTED_EDGE('',*,*,#56972,.T.);
#84757=ORIENTED_EDGE('',*,*,#56973,.T.);
#84758=ORIENTED_EDGE('',*,*,#56974,.T.);
#84759=ORIENTED_EDGE('',*,*,#56975,.F.);
#84760=ORIENTED_EDGE('',*,*,#56976,.T.);
#84761=ORIENTED_EDGE('',*,*,#56977,.T.);
#84762=ORIENTED_EDGE('',*,*,#56975,.T.);
#84763=ORIENTED_EDGE('',*,*,#56978,.T.);
#84764=ORIENTED_EDGE('',*,*,#56979,.T.);
#84765=ORIENTED_EDGE('',*,*,#56968,.F.);
#84766=ORIENTED_EDGE('',*,*,#56980,.T.);
#84767=ORIENTED_EDGE('',*,*,#56981,.T.);
#84768=ORIENTED_EDGE('',*,*,#56982,.F.);
#84769=ORIENTED_EDGE('',*,*,#56976,.F.);
#84770=ORIENTED_EDGE('',*,*,#56983,.F.);
#84771=ORIENTED_EDGE('',*,*,#56984,.F.);
#84772=ORIENTED_EDGE('',*,*,#56983,.T.);
#84773=ORIENTED_EDGE('',*,*,#56981,.F.);
#84774=ORIENTED_EDGE('',*,*,#56980,.F.);
#84775=ORIENTED_EDGE('',*,*,#56985,.F.);
#84776=ORIENTED_EDGE('',*,*,#56986,.F.);
#84777=ORIENTED_EDGE('',*,*,#56985,.T.);
#84778=ORIENTED_EDGE('',*,*,#56972,.F.);
#84779=ORIENTED_EDGE('',*,*,#56987,.F.);
#84780=ORIENTED_EDGE('',*,*,#56988,.F.);
#84781=ORIENTED_EDGE('',*,*,#56989,.T.);
#84782=ORIENTED_EDGE('',*,*,#56982,.T.);
#84783=ORIENTED_EDGE('',*,*,#54011,.F.);
#84784=ORIENTED_EDGE('',*,*,#54923,.T.);
#84785=ORIENTED_EDGE('',*,*,#56990,.F.);
#84786=ORIENTED_EDGE('',*,*,#56977,.F.);
#84787=ORIENTED_EDGE('',*,*,#56989,.F.);
#84788=ORIENTED_EDGE('',*,*,#54922,.F.);
#84789=ORIENTED_EDGE('',*,*,#56990,.T.);
#84790=ORIENTED_EDGE('',*,*,#55017,.F.);
#84791=ORIENTED_EDGE('',*,*,#56991,.F.);
#84792=ORIENTED_EDGE('',*,*,#56973,.F.);
#84793=ORIENTED_EDGE('',*,*,#56991,.T.);
#84794=ORIENTED_EDGE('',*,*,#54494,.F.);
#84795=ORIENTED_EDGE('',*,*,#56992,.F.);
#84796=ORIENTED_EDGE('',*,*,#56974,.F.);
#84797=ORIENTED_EDGE('',*,*,#56992,.T.);
#84798=ORIENTED_EDGE('',*,*,#54493,.F.);
#84799=ORIENTED_EDGE('',*,*,#56993,.F.);
#84800=ORIENTED_EDGE('',*,*,#56979,.F.);
#84801=ORIENTED_EDGE('',*,*,#56978,.F.);
#84802=ORIENTED_EDGE('',*,*,#56993,.T.);
#84803=ORIENTED_EDGE('',*,*,#54492,.F.);
#84804=ORIENTED_EDGE('',*,*,#56994,.F.);
#84805=ORIENTED_EDGE('',*,*,#56969,.F.);
#84806=ORIENTED_EDGE('',*,*,#56995,.T.);
#84807=ORIENTED_EDGE('',*,*,#56970,.F.);
#84808=ORIENTED_EDGE('',*,*,#56994,.T.);
#84809=ORIENTED_EDGE('',*,*,#55018,.F.);
#84810=ORIENTED_EDGE('',*,*,#56996,.T.);
#84811=ORIENTED_EDGE('',*,*,#56971,.F.);
#84812=ORIENTED_EDGE('',*,*,#56995,.F.);
#84813=ORIENTED_EDGE('',*,*,#54925,.F.);
#84814=ORIENTED_EDGE('',*,*,#54009,.T.);
#84815=ORIENTED_EDGE('',*,*,#56987,.T.);
#84816=ORIENTED_EDGE('',*,*,#56996,.F.);
#84817=ORIENTED_EDGE('',*,*,#54924,.T.);
#84818=ORIENTED_EDGE('',*,*,#56986,.T.);
#84819=ORIENTED_EDGE('',*,*,#56988,.T.);
#84820=ORIENTED_EDGE('',*,*,#54008,.T.);
#84821=ORIENTED_EDGE('',*,*,#56984,.T.);
#84822=ORIENTED_EDGE('',*,*,#56997,.T.);
#84823=ORIENTED_EDGE('',*,*,#56998,.T.);
#84824=ORIENTED_EDGE('',*,*,#56999,.T.);
#84825=ORIENTED_EDGE('',*,*,#57000,.T.);
#84826=ORIENTED_EDGE('',*,*,#57001,.T.);
#84827=ORIENTED_EDGE('',*,*,#57002,.T.);
#84828=ORIENTED_EDGE('',*,*,#57003,.T.);
#84829=ORIENTED_EDGE('',*,*,#57004,.F.);
#84830=ORIENTED_EDGE('',*,*,#57005,.T.);
#84831=ORIENTED_EDGE('',*,*,#57006,.T.);
#84832=ORIENTED_EDGE('',*,*,#57004,.T.);
#84833=ORIENTED_EDGE('',*,*,#57007,.T.);
#84834=ORIENTED_EDGE('',*,*,#57008,.T.);
#84835=ORIENTED_EDGE('',*,*,#56997,.F.);
#84836=ORIENTED_EDGE('',*,*,#57009,.T.);
#84837=ORIENTED_EDGE('',*,*,#57010,.T.);
#84838=ORIENTED_EDGE('',*,*,#57011,.F.);
#84839=ORIENTED_EDGE('',*,*,#57005,.F.);
#84840=ORIENTED_EDGE('',*,*,#57012,.F.);
#84841=ORIENTED_EDGE('',*,*,#57013,.F.);
#84842=ORIENTED_EDGE('',*,*,#57012,.T.);
#84843=ORIENTED_EDGE('',*,*,#57010,.F.);
#84844=ORIENTED_EDGE('',*,*,#57009,.F.);
#84845=ORIENTED_EDGE('',*,*,#57014,.F.);
#84846=ORIENTED_EDGE('',*,*,#57015,.F.);
#84847=ORIENTED_EDGE('',*,*,#57014,.T.);
#84848=ORIENTED_EDGE('',*,*,#57001,.F.);
#84849=ORIENTED_EDGE('',*,*,#57016,.F.);
#84850=ORIENTED_EDGE('',*,*,#57017,.F.);
#84851=ORIENTED_EDGE('',*,*,#57018,.T.);
#84852=ORIENTED_EDGE('',*,*,#57011,.T.);
#84853=ORIENTED_EDGE('',*,*,#54007,.F.);
#84854=ORIENTED_EDGE('',*,*,#54918,.T.);
#84855=ORIENTED_EDGE('',*,*,#57019,.F.);
#84856=ORIENTED_EDGE('',*,*,#57006,.F.);
#84857=ORIENTED_EDGE('',*,*,#57018,.F.);
#84858=ORIENTED_EDGE('',*,*,#54917,.F.);
#84859=ORIENTED_EDGE('',*,*,#57019,.T.);
#84860=ORIENTED_EDGE('',*,*,#55015,.F.);
#84861=ORIENTED_EDGE('',*,*,#57020,.F.);
#84862=ORIENTED_EDGE('',*,*,#57002,.F.);
#84863=ORIENTED_EDGE('',*,*,#57020,.T.);
#84864=ORIENTED_EDGE('',*,*,#54498,.F.);
#84865=ORIENTED_EDGE('',*,*,#57021,.F.);
#84866=ORIENTED_EDGE('',*,*,#57003,.F.);
#84867=ORIENTED_EDGE('',*,*,#57021,.T.);
#84868=ORIENTED_EDGE('',*,*,#54497,.F.);
#84869=ORIENTED_EDGE('',*,*,#57022,.F.);
#84870=ORIENTED_EDGE('',*,*,#57008,.F.);
#84871=ORIENTED_EDGE('',*,*,#57007,.F.);
#84872=ORIENTED_EDGE('',*,*,#57022,.T.);
#84873=ORIENTED_EDGE('',*,*,#54496,.F.);
#84874=ORIENTED_EDGE('',*,*,#57023,.F.);
#84875=ORIENTED_EDGE('',*,*,#56998,.F.);
#84876=ORIENTED_EDGE('',*,*,#57024,.T.);
#84877=ORIENTED_EDGE('',*,*,#56999,.F.);
#84878=ORIENTED_EDGE('',*,*,#57023,.T.);
#84879=ORIENTED_EDGE('',*,*,#55016,.F.);
#84880=ORIENTED_EDGE('',*,*,#57025,.T.);
#84881=ORIENTED_EDGE('',*,*,#57000,.F.);
#84882=ORIENTED_EDGE('',*,*,#57024,.F.);
#84883=ORIENTED_EDGE('',*,*,#54920,.F.);
#84884=ORIENTED_EDGE('',*,*,#54005,.T.);
#84885=ORIENTED_EDGE('',*,*,#57016,.T.);
#84886=ORIENTED_EDGE('',*,*,#57025,.F.);
#84887=ORIENTED_EDGE('',*,*,#54919,.T.);
#84888=ORIENTED_EDGE('',*,*,#57015,.T.);
#84889=ORIENTED_EDGE('',*,*,#57017,.T.);
#84890=ORIENTED_EDGE('',*,*,#54004,.T.);
#84891=ORIENTED_EDGE('',*,*,#57013,.T.);
#84892=ORIENTED_EDGE('',*,*,#57026,.T.);
#84893=ORIENTED_EDGE('',*,*,#57027,.T.);
#84894=ORIENTED_EDGE('',*,*,#57028,.T.);
#84895=ORIENTED_EDGE('',*,*,#57029,.T.);
#84896=ORIENTED_EDGE('',*,*,#57030,.T.);
#84897=ORIENTED_EDGE('',*,*,#57031,.T.);
#84898=ORIENTED_EDGE('',*,*,#57032,.T.);
#84899=ORIENTED_EDGE('',*,*,#57033,.F.);
#84900=ORIENTED_EDGE('',*,*,#57034,.T.);
#84901=ORIENTED_EDGE('',*,*,#57035,.T.);
#84902=ORIENTED_EDGE('',*,*,#57033,.T.);
#84903=ORIENTED_EDGE('',*,*,#57036,.T.);
#84904=ORIENTED_EDGE('',*,*,#57037,.T.);
#84905=ORIENTED_EDGE('',*,*,#57026,.F.);
#84906=ORIENTED_EDGE('',*,*,#57038,.T.);
#84907=ORIENTED_EDGE('',*,*,#57039,.T.);
#84908=ORIENTED_EDGE('',*,*,#57040,.F.);
#84909=ORIENTED_EDGE('',*,*,#57034,.F.);
#84910=ORIENTED_EDGE('',*,*,#57041,.F.);
#84911=ORIENTED_EDGE('',*,*,#57042,.F.);
#84912=ORIENTED_EDGE('',*,*,#57041,.T.);
#84913=ORIENTED_EDGE('',*,*,#57039,.F.);
#84914=ORIENTED_EDGE('',*,*,#57038,.F.);
#84915=ORIENTED_EDGE('',*,*,#57043,.F.);
#84916=ORIENTED_EDGE('',*,*,#57044,.F.);
#84917=ORIENTED_EDGE('',*,*,#57043,.T.);
#84918=ORIENTED_EDGE('',*,*,#57030,.F.);
#84919=ORIENTED_EDGE('',*,*,#57045,.F.);
#84920=ORIENTED_EDGE('',*,*,#57046,.F.);
#84921=ORIENTED_EDGE('',*,*,#57047,.T.);
#84922=ORIENTED_EDGE('',*,*,#57040,.T.);
#84923=ORIENTED_EDGE('',*,*,#54003,.F.);
#84924=ORIENTED_EDGE('',*,*,#54913,.T.);
#84925=ORIENTED_EDGE('',*,*,#57048,.F.);
#84926=ORIENTED_EDGE('',*,*,#57035,.F.);
#84927=ORIENTED_EDGE('',*,*,#57047,.F.);
#84928=ORIENTED_EDGE('',*,*,#54912,.F.);
#84929=ORIENTED_EDGE('',*,*,#57048,.T.);
#84930=ORIENTED_EDGE('',*,*,#55013,.F.);
#84931=ORIENTED_EDGE('',*,*,#57049,.F.);
#84932=ORIENTED_EDGE('',*,*,#57031,.F.);
#84933=ORIENTED_EDGE('',*,*,#57049,.T.);
#84934=ORIENTED_EDGE('',*,*,#54502,.F.);
#84935=ORIENTED_EDGE('',*,*,#57050,.F.);
#84936=ORIENTED_EDGE('',*,*,#57032,.F.);
#84937=ORIENTED_EDGE('',*,*,#57050,.T.);
#84938=ORIENTED_EDGE('',*,*,#54501,.F.);
#84939=ORIENTED_EDGE('',*,*,#57051,.F.);
#84940=ORIENTED_EDGE('',*,*,#57037,.F.);
#84941=ORIENTED_EDGE('',*,*,#57036,.F.);
#84942=ORIENTED_EDGE('',*,*,#57051,.T.);
#84943=ORIENTED_EDGE('',*,*,#54500,.F.);
#84944=ORIENTED_EDGE('',*,*,#57052,.F.);
#84945=ORIENTED_EDGE('',*,*,#57027,.F.);
#84946=ORIENTED_EDGE('',*,*,#57053,.T.);
#84947=ORIENTED_EDGE('',*,*,#57028,.F.);
#84948=ORIENTED_EDGE('',*,*,#57052,.T.);
#84949=ORIENTED_EDGE('',*,*,#55014,.F.);
#84950=ORIENTED_EDGE('',*,*,#57054,.T.);
#84951=ORIENTED_EDGE('',*,*,#57029,.F.);
#84952=ORIENTED_EDGE('',*,*,#57053,.F.);
#84953=ORIENTED_EDGE('',*,*,#54915,.F.);
#84954=ORIENTED_EDGE('',*,*,#54001,.T.);
#84955=ORIENTED_EDGE('',*,*,#57045,.T.);
#84956=ORIENTED_EDGE('',*,*,#57054,.F.);
#84957=ORIENTED_EDGE('',*,*,#54914,.T.);
#84958=ORIENTED_EDGE('',*,*,#57044,.T.);
#84959=ORIENTED_EDGE('',*,*,#57046,.T.);
#84960=ORIENTED_EDGE('',*,*,#54000,.T.);
#84961=ORIENTED_EDGE('',*,*,#57042,.T.);
#84962=ORIENTED_EDGE('',*,*,#57055,.T.);
#84963=ORIENTED_EDGE('',*,*,#57056,.T.);
#84964=ORIENTED_EDGE('',*,*,#57057,.T.);
#84965=ORIENTED_EDGE('',*,*,#57058,.T.);
#84966=ORIENTED_EDGE('',*,*,#57059,.T.);
#84967=ORIENTED_EDGE('',*,*,#57060,.T.);
#84968=ORIENTED_EDGE('',*,*,#57061,.T.);
#84969=ORIENTED_EDGE('',*,*,#57062,.F.);
#84970=ORIENTED_EDGE('',*,*,#57063,.T.);
#84971=ORIENTED_EDGE('',*,*,#57064,.T.);
#84972=ORIENTED_EDGE('',*,*,#57062,.T.);
#84973=ORIENTED_EDGE('',*,*,#57065,.T.);
#84974=ORIENTED_EDGE('',*,*,#57066,.T.);
#84975=ORIENTED_EDGE('',*,*,#57055,.F.);
#84976=ORIENTED_EDGE('',*,*,#57067,.T.);
#84977=ORIENTED_EDGE('',*,*,#57068,.T.);
#84978=ORIENTED_EDGE('',*,*,#57069,.F.);
#84979=ORIENTED_EDGE('',*,*,#57063,.F.);
#84980=ORIENTED_EDGE('',*,*,#57070,.F.);
#84981=ORIENTED_EDGE('',*,*,#57071,.F.);
#84982=ORIENTED_EDGE('',*,*,#57070,.T.);
#84983=ORIENTED_EDGE('',*,*,#57068,.F.);
#84984=ORIENTED_EDGE('',*,*,#57067,.F.);
#84985=ORIENTED_EDGE('',*,*,#57072,.F.);
#84986=ORIENTED_EDGE('',*,*,#57073,.F.);
#84987=ORIENTED_EDGE('',*,*,#57072,.T.);
#84988=ORIENTED_EDGE('',*,*,#57059,.F.);
#84989=ORIENTED_EDGE('',*,*,#57074,.F.);
#84990=ORIENTED_EDGE('',*,*,#57075,.F.);
#84991=ORIENTED_EDGE('',*,*,#57076,.T.);
#84992=ORIENTED_EDGE('',*,*,#57069,.T.);
#84993=ORIENTED_EDGE('',*,*,#53999,.F.);
#84994=ORIENTED_EDGE('',*,*,#54908,.T.);
#84995=ORIENTED_EDGE('',*,*,#57077,.F.);
#84996=ORIENTED_EDGE('',*,*,#57064,.F.);
#84997=ORIENTED_EDGE('',*,*,#57076,.F.);
#84998=ORIENTED_EDGE('',*,*,#54907,.F.);
#84999=ORIENTED_EDGE('',*,*,#57077,.T.);
#85000=ORIENTED_EDGE('',*,*,#55011,.F.);
#85001=ORIENTED_EDGE('',*,*,#57078,.F.);
#85002=ORIENTED_EDGE('',*,*,#57060,.F.);
#85003=ORIENTED_EDGE('',*,*,#57078,.T.);
#85004=ORIENTED_EDGE('',*,*,#54506,.F.);
#85005=ORIENTED_EDGE('',*,*,#57079,.F.);
#85006=ORIENTED_EDGE('',*,*,#57061,.F.);
#85007=ORIENTED_EDGE('',*,*,#57079,.T.);
#85008=ORIENTED_EDGE('',*,*,#54505,.F.);
#85009=ORIENTED_EDGE('',*,*,#57080,.F.);
#85010=ORIENTED_EDGE('',*,*,#57066,.F.);
#85011=ORIENTED_EDGE('',*,*,#57065,.F.);
#85012=ORIENTED_EDGE('',*,*,#57080,.T.);
#85013=ORIENTED_EDGE('',*,*,#54504,.F.);
#85014=ORIENTED_EDGE('',*,*,#57081,.F.);
#85015=ORIENTED_EDGE('',*,*,#57056,.F.);
#85016=ORIENTED_EDGE('',*,*,#57082,.T.);
#85017=ORIENTED_EDGE('',*,*,#57057,.F.);
#85018=ORIENTED_EDGE('',*,*,#57081,.T.);
#85019=ORIENTED_EDGE('',*,*,#55012,.F.);
#85020=ORIENTED_EDGE('',*,*,#57083,.T.);
#85021=ORIENTED_EDGE('',*,*,#57058,.F.);
#85022=ORIENTED_EDGE('',*,*,#57082,.F.);
#85023=ORIENTED_EDGE('',*,*,#54910,.F.);
#85024=ORIENTED_EDGE('',*,*,#53997,.T.);
#85025=ORIENTED_EDGE('',*,*,#57074,.T.);
#85026=ORIENTED_EDGE('',*,*,#57083,.F.);
#85027=ORIENTED_EDGE('',*,*,#54909,.T.);
#85028=ORIENTED_EDGE('',*,*,#57073,.T.);
#85029=ORIENTED_EDGE('',*,*,#57075,.T.);
#85030=ORIENTED_EDGE('',*,*,#53996,.T.);
#85031=ORIENTED_EDGE('',*,*,#57071,.T.);
#85032=ORIENTED_EDGE('',*,*,#57084,.T.);
#85033=ORIENTED_EDGE('',*,*,#57085,.T.);
#85034=ORIENTED_EDGE('',*,*,#57086,.T.);
#85035=ORIENTED_EDGE('',*,*,#57087,.T.);
#85036=ORIENTED_EDGE('',*,*,#57088,.T.);
#85037=ORIENTED_EDGE('',*,*,#57089,.T.);
#85038=ORIENTED_EDGE('',*,*,#57090,.T.);
#85039=ORIENTED_EDGE('',*,*,#57091,.F.);
#85040=ORIENTED_EDGE('',*,*,#57092,.T.);
#85041=ORIENTED_EDGE('',*,*,#57093,.T.);
#85042=ORIENTED_EDGE('',*,*,#57091,.T.);
#85043=ORIENTED_EDGE('',*,*,#57094,.T.);
#85044=ORIENTED_EDGE('',*,*,#57095,.T.);
#85045=ORIENTED_EDGE('',*,*,#57084,.F.);
#85046=ORIENTED_EDGE('',*,*,#57096,.T.);
#85047=ORIENTED_EDGE('',*,*,#57097,.T.);
#85048=ORIENTED_EDGE('',*,*,#57098,.F.);
#85049=ORIENTED_EDGE('',*,*,#57092,.F.);
#85050=ORIENTED_EDGE('',*,*,#57099,.F.);
#85051=ORIENTED_EDGE('',*,*,#57100,.F.);
#85052=ORIENTED_EDGE('',*,*,#57099,.T.);
#85053=ORIENTED_EDGE('',*,*,#57097,.F.);
#85054=ORIENTED_EDGE('',*,*,#57096,.F.);
#85055=ORIENTED_EDGE('',*,*,#57101,.F.);
#85056=ORIENTED_EDGE('',*,*,#57102,.F.);
#85057=ORIENTED_EDGE('',*,*,#57101,.T.);
#85058=ORIENTED_EDGE('',*,*,#57088,.F.);
#85059=ORIENTED_EDGE('',*,*,#57103,.F.);
#85060=ORIENTED_EDGE('',*,*,#57104,.F.);
#85061=ORIENTED_EDGE('',*,*,#57105,.T.);
#85062=ORIENTED_EDGE('',*,*,#57098,.T.);
#85063=ORIENTED_EDGE('',*,*,#53995,.F.);
#85064=ORIENTED_EDGE('',*,*,#54903,.T.);
#85065=ORIENTED_EDGE('',*,*,#57106,.F.);
#85066=ORIENTED_EDGE('',*,*,#57093,.F.);
#85067=ORIENTED_EDGE('',*,*,#57105,.F.);
#85068=ORIENTED_EDGE('',*,*,#54902,.F.);
#85069=ORIENTED_EDGE('',*,*,#57106,.T.);
#85070=ORIENTED_EDGE('',*,*,#55009,.F.);
#85071=ORIENTED_EDGE('',*,*,#57107,.F.);
#85072=ORIENTED_EDGE('',*,*,#57089,.F.);
#85073=ORIENTED_EDGE('',*,*,#57107,.T.);
#85074=ORIENTED_EDGE('',*,*,#54510,.F.);
#85075=ORIENTED_EDGE('',*,*,#57108,.F.);
#85076=ORIENTED_EDGE('',*,*,#57090,.F.);
#85077=ORIENTED_EDGE('',*,*,#57108,.T.);
#85078=ORIENTED_EDGE('',*,*,#54509,.F.);
#85079=ORIENTED_EDGE('',*,*,#57109,.F.);
#85080=ORIENTED_EDGE('',*,*,#57095,.F.);
#85081=ORIENTED_EDGE('',*,*,#57094,.F.);
#85082=ORIENTED_EDGE('',*,*,#57109,.T.);
#85083=ORIENTED_EDGE('',*,*,#54508,.F.);
#85084=ORIENTED_EDGE('',*,*,#57110,.F.);
#85085=ORIENTED_EDGE('',*,*,#57085,.F.);
#85086=ORIENTED_EDGE('',*,*,#57111,.T.);
#85087=ORIENTED_EDGE('',*,*,#57086,.F.);
#85088=ORIENTED_EDGE('',*,*,#57110,.T.);
#85089=ORIENTED_EDGE('',*,*,#55010,.F.);
#85090=ORIENTED_EDGE('',*,*,#57112,.T.);
#85091=ORIENTED_EDGE('',*,*,#57087,.F.);
#85092=ORIENTED_EDGE('',*,*,#57111,.F.);
#85093=ORIENTED_EDGE('',*,*,#54905,.F.);
#85094=ORIENTED_EDGE('',*,*,#53993,.T.);
#85095=ORIENTED_EDGE('',*,*,#57103,.T.);
#85096=ORIENTED_EDGE('',*,*,#57112,.F.);
#85097=ORIENTED_EDGE('',*,*,#54904,.T.);
#85098=ORIENTED_EDGE('',*,*,#57102,.T.);
#85099=ORIENTED_EDGE('',*,*,#57104,.T.);
#85100=ORIENTED_EDGE('',*,*,#53992,.T.);
#85101=ORIENTED_EDGE('',*,*,#57100,.T.);
#85102=ORIENTED_EDGE('',*,*,#57113,.T.);
#85103=ORIENTED_EDGE('',*,*,#57114,.T.);
#85104=ORIENTED_EDGE('',*,*,#57115,.T.);
#85105=ORIENTED_EDGE('',*,*,#57116,.T.);
#85106=ORIENTED_EDGE('',*,*,#57117,.T.);
#85107=ORIENTED_EDGE('',*,*,#57118,.T.);
#85108=ORIENTED_EDGE('',*,*,#57119,.T.);
#85109=ORIENTED_EDGE('',*,*,#57120,.F.);
#85110=ORIENTED_EDGE('',*,*,#57121,.T.);
#85111=ORIENTED_EDGE('',*,*,#57122,.T.);
#85112=ORIENTED_EDGE('',*,*,#57120,.T.);
#85113=ORIENTED_EDGE('',*,*,#57123,.T.);
#85114=ORIENTED_EDGE('',*,*,#57124,.T.);
#85115=ORIENTED_EDGE('',*,*,#57113,.F.);
#85116=ORIENTED_EDGE('',*,*,#57125,.T.);
#85117=ORIENTED_EDGE('',*,*,#57126,.T.);
#85118=ORIENTED_EDGE('',*,*,#57127,.F.);
#85119=ORIENTED_EDGE('',*,*,#57121,.F.);
#85120=ORIENTED_EDGE('',*,*,#57128,.F.);
#85121=ORIENTED_EDGE('',*,*,#57129,.F.);
#85122=ORIENTED_EDGE('',*,*,#57128,.T.);
#85123=ORIENTED_EDGE('',*,*,#57126,.F.);
#85124=ORIENTED_EDGE('',*,*,#57125,.F.);
#85125=ORIENTED_EDGE('',*,*,#57130,.F.);
#85126=ORIENTED_EDGE('',*,*,#57131,.F.);
#85127=ORIENTED_EDGE('',*,*,#57130,.T.);
#85128=ORIENTED_EDGE('',*,*,#57117,.F.);
#85129=ORIENTED_EDGE('',*,*,#57132,.F.);
#85130=ORIENTED_EDGE('',*,*,#57133,.F.);
#85131=ORIENTED_EDGE('',*,*,#57134,.T.);
#85132=ORIENTED_EDGE('',*,*,#57127,.T.);
#85133=ORIENTED_EDGE('',*,*,#53991,.F.);
#85134=ORIENTED_EDGE('',*,*,#54898,.T.);
#85135=ORIENTED_EDGE('',*,*,#57135,.F.);
#85136=ORIENTED_EDGE('',*,*,#57122,.F.);
#85137=ORIENTED_EDGE('',*,*,#57134,.F.);
#85138=ORIENTED_EDGE('',*,*,#54897,.F.);
#85139=ORIENTED_EDGE('',*,*,#57135,.T.);
#85140=ORIENTED_EDGE('',*,*,#55007,.F.);
#85141=ORIENTED_EDGE('',*,*,#57136,.F.);
#85142=ORIENTED_EDGE('',*,*,#57118,.F.);
#85143=ORIENTED_EDGE('',*,*,#57136,.T.);
#85144=ORIENTED_EDGE('',*,*,#54514,.F.);
#85145=ORIENTED_EDGE('',*,*,#57137,.F.);
#85146=ORIENTED_EDGE('',*,*,#57119,.F.);
#85147=ORIENTED_EDGE('',*,*,#57137,.T.);
#85148=ORIENTED_EDGE('',*,*,#54513,.F.);
#85149=ORIENTED_EDGE('',*,*,#57138,.F.);
#85150=ORIENTED_EDGE('',*,*,#57124,.F.);
#85151=ORIENTED_EDGE('',*,*,#57123,.F.);
#85152=ORIENTED_EDGE('',*,*,#57138,.T.);
#85153=ORIENTED_EDGE('',*,*,#54512,.F.);
#85154=ORIENTED_EDGE('',*,*,#57139,.F.);
#85155=ORIENTED_EDGE('',*,*,#57114,.F.);
#85156=ORIENTED_EDGE('',*,*,#57140,.T.);
#85157=ORIENTED_EDGE('',*,*,#57115,.F.);
#85158=ORIENTED_EDGE('',*,*,#57139,.T.);
#85159=ORIENTED_EDGE('',*,*,#55008,.F.);
#85160=ORIENTED_EDGE('',*,*,#57141,.T.);
#85161=ORIENTED_EDGE('',*,*,#57116,.F.);
#85162=ORIENTED_EDGE('',*,*,#57140,.F.);
#85163=ORIENTED_EDGE('',*,*,#54900,.F.);
#85164=ORIENTED_EDGE('',*,*,#53989,.T.);
#85165=ORIENTED_EDGE('',*,*,#57132,.T.);
#85166=ORIENTED_EDGE('',*,*,#57141,.F.);
#85167=ORIENTED_EDGE('',*,*,#54899,.T.);
#85168=ORIENTED_EDGE('',*,*,#57131,.T.);
#85169=ORIENTED_EDGE('',*,*,#57133,.T.);
#85170=ORIENTED_EDGE('',*,*,#53988,.T.);
#85171=ORIENTED_EDGE('',*,*,#57129,.T.);
#85172=ORIENTED_EDGE('',*,*,#57142,.T.);
#85173=ORIENTED_EDGE('',*,*,#57143,.T.);
#85174=ORIENTED_EDGE('',*,*,#57144,.T.);
#85175=ORIENTED_EDGE('',*,*,#57145,.T.);
#85176=ORIENTED_EDGE('',*,*,#57146,.T.);
#85177=ORIENTED_EDGE('',*,*,#57147,.T.);
#85178=ORIENTED_EDGE('',*,*,#57148,.T.);
#85179=ORIENTED_EDGE('',*,*,#57149,.F.);
#85180=ORIENTED_EDGE('',*,*,#57150,.T.);
#85181=ORIENTED_EDGE('',*,*,#57151,.T.);
#85182=ORIENTED_EDGE('',*,*,#57149,.T.);
#85183=ORIENTED_EDGE('',*,*,#57152,.T.);
#85184=ORIENTED_EDGE('',*,*,#57153,.T.);
#85185=ORIENTED_EDGE('',*,*,#57142,.F.);
#85186=ORIENTED_EDGE('',*,*,#57154,.T.);
#85187=ORIENTED_EDGE('',*,*,#57155,.T.);
#85188=ORIENTED_EDGE('',*,*,#57156,.F.);
#85189=ORIENTED_EDGE('',*,*,#57150,.F.);
#85190=ORIENTED_EDGE('',*,*,#57157,.F.);
#85191=ORIENTED_EDGE('',*,*,#57158,.F.);
#85192=ORIENTED_EDGE('',*,*,#57157,.T.);
#85193=ORIENTED_EDGE('',*,*,#57155,.F.);
#85194=ORIENTED_EDGE('',*,*,#57154,.F.);
#85195=ORIENTED_EDGE('',*,*,#57159,.F.);
#85196=ORIENTED_EDGE('',*,*,#57160,.F.);
#85197=ORIENTED_EDGE('',*,*,#57159,.T.);
#85198=ORIENTED_EDGE('',*,*,#57146,.F.);
#85199=ORIENTED_EDGE('',*,*,#57161,.F.);
#85200=ORIENTED_EDGE('',*,*,#57162,.F.);
#85201=ORIENTED_EDGE('',*,*,#57163,.T.);
#85202=ORIENTED_EDGE('',*,*,#57156,.T.);
#85203=ORIENTED_EDGE('',*,*,#53987,.F.);
#85204=ORIENTED_EDGE('',*,*,#54893,.T.);
#85205=ORIENTED_EDGE('',*,*,#57164,.F.);
#85206=ORIENTED_EDGE('',*,*,#57151,.F.);
#85207=ORIENTED_EDGE('',*,*,#57163,.F.);
#85208=ORIENTED_EDGE('',*,*,#54892,.F.);
#85209=ORIENTED_EDGE('',*,*,#57164,.T.);
#85210=ORIENTED_EDGE('',*,*,#55005,.F.);
#85211=ORIENTED_EDGE('',*,*,#57165,.F.);
#85212=ORIENTED_EDGE('',*,*,#57147,.F.);
#85213=ORIENTED_EDGE('',*,*,#57165,.T.);
#85214=ORIENTED_EDGE('',*,*,#54518,.F.);
#85215=ORIENTED_EDGE('',*,*,#57166,.F.);
#85216=ORIENTED_EDGE('',*,*,#57148,.F.);
#85217=ORIENTED_EDGE('',*,*,#57166,.T.);
#85218=ORIENTED_EDGE('',*,*,#54517,.F.);
#85219=ORIENTED_EDGE('',*,*,#57167,.F.);
#85220=ORIENTED_EDGE('',*,*,#57153,.F.);
#85221=ORIENTED_EDGE('',*,*,#57152,.F.);
#85222=ORIENTED_EDGE('',*,*,#57167,.T.);
#85223=ORIENTED_EDGE('',*,*,#54516,.F.);
#85224=ORIENTED_EDGE('',*,*,#57168,.F.);
#85225=ORIENTED_EDGE('',*,*,#57143,.F.);
#85226=ORIENTED_EDGE('',*,*,#57169,.T.);
#85227=ORIENTED_EDGE('',*,*,#57144,.F.);
#85228=ORIENTED_EDGE('',*,*,#57168,.T.);
#85229=ORIENTED_EDGE('',*,*,#55006,.F.);
#85230=ORIENTED_EDGE('',*,*,#57170,.T.);
#85231=ORIENTED_EDGE('',*,*,#57145,.F.);
#85232=ORIENTED_EDGE('',*,*,#57169,.F.);
#85233=ORIENTED_EDGE('',*,*,#54895,.F.);
#85234=ORIENTED_EDGE('',*,*,#53985,.T.);
#85235=ORIENTED_EDGE('',*,*,#57161,.T.);
#85236=ORIENTED_EDGE('',*,*,#57170,.F.);
#85237=ORIENTED_EDGE('',*,*,#54894,.T.);
#85238=ORIENTED_EDGE('',*,*,#57160,.T.);
#85239=ORIENTED_EDGE('',*,*,#57162,.T.);
#85240=ORIENTED_EDGE('',*,*,#53984,.T.);
#85241=ORIENTED_EDGE('',*,*,#57158,.T.);
#85242=ORIENTED_EDGE('',*,*,#57171,.T.);
#85243=ORIENTED_EDGE('',*,*,#57172,.T.);
#85244=ORIENTED_EDGE('',*,*,#57173,.T.);
#85245=ORIENTED_EDGE('',*,*,#57174,.T.);
#85246=ORIENTED_EDGE('',*,*,#57175,.T.);
#85247=ORIENTED_EDGE('',*,*,#57176,.T.);
#85248=ORIENTED_EDGE('',*,*,#57177,.T.);
#85249=ORIENTED_EDGE('',*,*,#57178,.F.);
#85250=ORIENTED_EDGE('',*,*,#57179,.T.);
#85251=ORIENTED_EDGE('',*,*,#57180,.T.);
#85252=ORIENTED_EDGE('',*,*,#57178,.T.);
#85253=ORIENTED_EDGE('',*,*,#57181,.T.);
#85254=ORIENTED_EDGE('',*,*,#57182,.T.);
#85255=ORIENTED_EDGE('',*,*,#57171,.F.);
#85256=ORIENTED_EDGE('',*,*,#57183,.T.);
#85257=ORIENTED_EDGE('',*,*,#57184,.T.);
#85258=ORIENTED_EDGE('',*,*,#57185,.F.);
#85259=ORIENTED_EDGE('',*,*,#57179,.F.);
#85260=ORIENTED_EDGE('',*,*,#57186,.F.);
#85261=ORIENTED_EDGE('',*,*,#57187,.F.);
#85262=ORIENTED_EDGE('',*,*,#57186,.T.);
#85263=ORIENTED_EDGE('',*,*,#57184,.F.);
#85264=ORIENTED_EDGE('',*,*,#57183,.F.);
#85265=ORIENTED_EDGE('',*,*,#57188,.F.);
#85266=ORIENTED_EDGE('',*,*,#57189,.F.);
#85267=ORIENTED_EDGE('',*,*,#57188,.T.);
#85268=ORIENTED_EDGE('',*,*,#57175,.F.);
#85269=ORIENTED_EDGE('',*,*,#57190,.F.);
#85270=ORIENTED_EDGE('',*,*,#57191,.F.);
#85271=ORIENTED_EDGE('',*,*,#57192,.T.);
#85272=ORIENTED_EDGE('',*,*,#57185,.T.);
#85273=ORIENTED_EDGE('',*,*,#53983,.F.);
#85274=ORIENTED_EDGE('',*,*,#54888,.T.);
#85275=ORIENTED_EDGE('',*,*,#57193,.F.);
#85276=ORIENTED_EDGE('',*,*,#57180,.F.);
#85277=ORIENTED_EDGE('',*,*,#57192,.F.);
#85278=ORIENTED_EDGE('',*,*,#54887,.F.);
#85279=ORIENTED_EDGE('',*,*,#57193,.T.);
#85280=ORIENTED_EDGE('',*,*,#55003,.F.);
#85281=ORIENTED_EDGE('',*,*,#57194,.F.);
#85282=ORIENTED_EDGE('',*,*,#57176,.F.);
#85283=ORIENTED_EDGE('',*,*,#57194,.T.);
#85284=ORIENTED_EDGE('',*,*,#54522,.F.);
#85285=ORIENTED_EDGE('',*,*,#57195,.F.);
#85286=ORIENTED_EDGE('',*,*,#57177,.F.);
#85287=ORIENTED_EDGE('',*,*,#57195,.T.);
#85288=ORIENTED_EDGE('',*,*,#54521,.F.);
#85289=ORIENTED_EDGE('',*,*,#57196,.F.);
#85290=ORIENTED_EDGE('',*,*,#57182,.F.);
#85291=ORIENTED_EDGE('',*,*,#57181,.F.);
#85292=ORIENTED_EDGE('',*,*,#57196,.T.);
#85293=ORIENTED_EDGE('',*,*,#54520,.F.);
#85294=ORIENTED_EDGE('',*,*,#57197,.F.);
#85295=ORIENTED_EDGE('',*,*,#57172,.F.);
#85296=ORIENTED_EDGE('',*,*,#57198,.T.);
#85297=ORIENTED_EDGE('',*,*,#57173,.F.);
#85298=ORIENTED_EDGE('',*,*,#57197,.T.);
#85299=ORIENTED_EDGE('',*,*,#55004,.F.);
#85300=ORIENTED_EDGE('',*,*,#57199,.T.);
#85301=ORIENTED_EDGE('',*,*,#57174,.F.);
#85302=ORIENTED_EDGE('',*,*,#57198,.F.);
#85303=ORIENTED_EDGE('',*,*,#54890,.F.);
#85304=ORIENTED_EDGE('',*,*,#53981,.T.);
#85305=ORIENTED_EDGE('',*,*,#57190,.T.);
#85306=ORIENTED_EDGE('',*,*,#57199,.F.);
#85307=ORIENTED_EDGE('',*,*,#54889,.T.);
#85308=ORIENTED_EDGE('',*,*,#57189,.T.);
#85309=ORIENTED_EDGE('',*,*,#57191,.T.);
#85310=ORIENTED_EDGE('',*,*,#53980,.T.);
#85311=ORIENTED_EDGE('',*,*,#57187,.T.);
#85312=ORIENTED_EDGE('',*,*,#57200,.T.);
#85313=ORIENTED_EDGE('',*,*,#57201,.T.);
#85314=ORIENTED_EDGE('',*,*,#57202,.T.);
#85315=ORIENTED_EDGE('',*,*,#57203,.T.);
#85316=ORIENTED_EDGE('',*,*,#57204,.T.);
#85317=ORIENTED_EDGE('',*,*,#57205,.T.);
#85318=ORIENTED_EDGE('',*,*,#57206,.T.);
#85319=ORIENTED_EDGE('',*,*,#57207,.F.);
#85320=ORIENTED_EDGE('',*,*,#57208,.T.);
#85321=ORIENTED_EDGE('',*,*,#57209,.T.);
#85322=ORIENTED_EDGE('',*,*,#57207,.T.);
#85323=ORIENTED_EDGE('',*,*,#57210,.T.);
#85324=ORIENTED_EDGE('',*,*,#57211,.T.);
#85325=ORIENTED_EDGE('',*,*,#57200,.F.);
#85326=ORIENTED_EDGE('',*,*,#57212,.T.);
#85327=ORIENTED_EDGE('',*,*,#57213,.T.);
#85328=ORIENTED_EDGE('',*,*,#57214,.F.);
#85329=ORIENTED_EDGE('',*,*,#57208,.F.);
#85330=ORIENTED_EDGE('',*,*,#57215,.F.);
#85331=ORIENTED_EDGE('',*,*,#57216,.F.);
#85332=ORIENTED_EDGE('',*,*,#57215,.T.);
#85333=ORIENTED_EDGE('',*,*,#57213,.F.);
#85334=ORIENTED_EDGE('',*,*,#57212,.F.);
#85335=ORIENTED_EDGE('',*,*,#57217,.F.);
#85336=ORIENTED_EDGE('',*,*,#57218,.F.);
#85337=ORIENTED_EDGE('',*,*,#57217,.T.);
#85338=ORIENTED_EDGE('',*,*,#57204,.F.);
#85339=ORIENTED_EDGE('',*,*,#57219,.F.);
#85340=ORIENTED_EDGE('',*,*,#57220,.F.);
#85341=ORIENTED_EDGE('',*,*,#57221,.T.);
#85342=ORIENTED_EDGE('',*,*,#57214,.T.);
#85343=ORIENTED_EDGE('',*,*,#53979,.F.);
#85344=ORIENTED_EDGE('',*,*,#54883,.T.);
#85345=ORIENTED_EDGE('',*,*,#57222,.F.);
#85346=ORIENTED_EDGE('',*,*,#57209,.F.);
#85347=ORIENTED_EDGE('',*,*,#57221,.F.);
#85348=ORIENTED_EDGE('',*,*,#54882,.F.);
#85349=ORIENTED_EDGE('',*,*,#57222,.T.);
#85350=ORIENTED_EDGE('',*,*,#55001,.F.);
#85351=ORIENTED_EDGE('',*,*,#57223,.F.);
#85352=ORIENTED_EDGE('',*,*,#57205,.F.);
#85353=ORIENTED_EDGE('',*,*,#57223,.T.);
#85354=ORIENTED_EDGE('',*,*,#54526,.F.);
#85355=ORIENTED_EDGE('',*,*,#57224,.F.);
#85356=ORIENTED_EDGE('',*,*,#57206,.F.);
#85357=ORIENTED_EDGE('',*,*,#57224,.T.);
#85358=ORIENTED_EDGE('',*,*,#54525,.F.);
#85359=ORIENTED_EDGE('',*,*,#57225,.F.);
#85360=ORIENTED_EDGE('',*,*,#57211,.F.);
#85361=ORIENTED_EDGE('',*,*,#57210,.F.);
#85362=ORIENTED_EDGE('',*,*,#57225,.T.);
#85363=ORIENTED_EDGE('',*,*,#54524,.F.);
#85364=ORIENTED_EDGE('',*,*,#57226,.F.);
#85365=ORIENTED_EDGE('',*,*,#57201,.F.);
#85366=ORIENTED_EDGE('',*,*,#57227,.T.);
#85367=ORIENTED_EDGE('',*,*,#57202,.F.);
#85368=ORIENTED_EDGE('',*,*,#57226,.T.);
#85369=ORIENTED_EDGE('',*,*,#55002,.F.);
#85370=ORIENTED_EDGE('',*,*,#57228,.T.);
#85371=ORIENTED_EDGE('',*,*,#57203,.F.);
#85372=ORIENTED_EDGE('',*,*,#57227,.F.);
#85373=ORIENTED_EDGE('',*,*,#54885,.F.);
#85374=ORIENTED_EDGE('',*,*,#53977,.T.);
#85375=ORIENTED_EDGE('',*,*,#57219,.T.);
#85376=ORIENTED_EDGE('',*,*,#57228,.F.);
#85377=ORIENTED_EDGE('',*,*,#54884,.T.);
#85378=ORIENTED_EDGE('',*,*,#57218,.T.);
#85379=ORIENTED_EDGE('',*,*,#57220,.T.);
#85380=ORIENTED_EDGE('',*,*,#53976,.T.);
#85381=ORIENTED_EDGE('',*,*,#57216,.T.);
#85382=ORIENTED_EDGE('',*,*,#57229,.T.);
#85383=ORIENTED_EDGE('',*,*,#57230,.T.);
#85384=ORIENTED_EDGE('',*,*,#57231,.T.);
#85385=ORIENTED_EDGE('',*,*,#57232,.T.);
#85386=ORIENTED_EDGE('',*,*,#57233,.T.);
#85387=ORIENTED_EDGE('',*,*,#57234,.T.);
#85388=ORIENTED_EDGE('',*,*,#57235,.T.);
#85389=ORIENTED_EDGE('',*,*,#57236,.F.);
#85390=ORIENTED_EDGE('',*,*,#57237,.T.);
#85391=ORIENTED_EDGE('',*,*,#57238,.T.);
#85392=ORIENTED_EDGE('',*,*,#57236,.T.);
#85393=ORIENTED_EDGE('',*,*,#57239,.T.);
#85394=ORIENTED_EDGE('',*,*,#57240,.T.);
#85395=ORIENTED_EDGE('',*,*,#57229,.F.);
#85396=ORIENTED_EDGE('',*,*,#57241,.T.);
#85397=ORIENTED_EDGE('',*,*,#57242,.T.);
#85398=ORIENTED_EDGE('',*,*,#57243,.F.);
#85399=ORIENTED_EDGE('',*,*,#57237,.F.);
#85400=ORIENTED_EDGE('',*,*,#57244,.F.);
#85401=ORIENTED_EDGE('',*,*,#57245,.F.);
#85402=ORIENTED_EDGE('',*,*,#57244,.T.);
#85403=ORIENTED_EDGE('',*,*,#57242,.F.);
#85404=ORIENTED_EDGE('',*,*,#57241,.F.);
#85405=ORIENTED_EDGE('',*,*,#57246,.F.);
#85406=ORIENTED_EDGE('',*,*,#57247,.F.);
#85407=ORIENTED_EDGE('',*,*,#57246,.T.);
#85408=ORIENTED_EDGE('',*,*,#57233,.F.);
#85409=ORIENTED_EDGE('',*,*,#57248,.F.);
#85410=ORIENTED_EDGE('',*,*,#57249,.F.);
#85411=ORIENTED_EDGE('',*,*,#57250,.T.);
#85412=ORIENTED_EDGE('',*,*,#57243,.T.);
#85413=ORIENTED_EDGE('',*,*,#53975,.F.);
#85414=ORIENTED_EDGE('',*,*,#54878,.T.);
#85415=ORIENTED_EDGE('',*,*,#57251,.F.);
#85416=ORIENTED_EDGE('',*,*,#57238,.F.);
#85417=ORIENTED_EDGE('',*,*,#57250,.F.);
#85418=ORIENTED_EDGE('',*,*,#54877,.F.);
#85419=ORIENTED_EDGE('',*,*,#57251,.T.);
#85420=ORIENTED_EDGE('',*,*,#54999,.F.);
#85421=ORIENTED_EDGE('',*,*,#57252,.F.);
#85422=ORIENTED_EDGE('',*,*,#57234,.F.);
#85423=ORIENTED_EDGE('',*,*,#57252,.T.);
#85424=ORIENTED_EDGE('',*,*,#54530,.F.);
#85425=ORIENTED_EDGE('',*,*,#57253,.F.);
#85426=ORIENTED_EDGE('',*,*,#57235,.F.);
#85427=ORIENTED_EDGE('',*,*,#57253,.T.);
#85428=ORIENTED_EDGE('',*,*,#54529,.F.);
#85429=ORIENTED_EDGE('',*,*,#57254,.F.);
#85430=ORIENTED_EDGE('',*,*,#57240,.F.);
#85431=ORIENTED_EDGE('',*,*,#57239,.F.);
#85432=ORIENTED_EDGE('',*,*,#57254,.T.);
#85433=ORIENTED_EDGE('',*,*,#54528,.F.);
#85434=ORIENTED_EDGE('',*,*,#57255,.F.);
#85435=ORIENTED_EDGE('',*,*,#57230,.F.);
#85436=ORIENTED_EDGE('',*,*,#57256,.T.);
#85437=ORIENTED_EDGE('',*,*,#57231,.F.);
#85438=ORIENTED_EDGE('',*,*,#57255,.T.);
#85439=ORIENTED_EDGE('',*,*,#55000,.F.);
#85440=ORIENTED_EDGE('',*,*,#57257,.T.);
#85441=ORIENTED_EDGE('',*,*,#57232,.F.);
#85442=ORIENTED_EDGE('',*,*,#57256,.F.);
#85443=ORIENTED_EDGE('',*,*,#54880,.F.);
#85444=ORIENTED_EDGE('',*,*,#53973,.T.);
#85445=ORIENTED_EDGE('',*,*,#57248,.T.);
#85446=ORIENTED_EDGE('',*,*,#57257,.F.);
#85447=ORIENTED_EDGE('',*,*,#54879,.T.);
#85448=ORIENTED_EDGE('',*,*,#57247,.T.);
#85449=ORIENTED_EDGE('',*,*,#57249,.T.);
#85450=ORIENTED_EDGE('',*,*,#53972,.T.);
#85451=ORIENTED_EDGE('',*,*,#57245,.T.);
#85452=ORIENTED_EDGE('',*,*,#57258,.T.);
#85453=ORIENTED_EDGE('',*,*,#57259,.T.);
#85454=ORIENTED_EDGE('',*,*,#57260,.T.);
#85455=ORIENTED_EDGE('',*,*,#57261,.T.);
#85456=ORIENTED_EDGE('',*,*,#57262,.T.);
#85457=ORIENTED_EDGE('',*,*,#57263,.T.);
#85458=ORIENTED_EDGE('',*,*,#57264,.T.);
#85459=ORIENTED_EDGE('',*,*,#57265,.F.);
#85460=ORIENTED_EDGE('',*,*,#57266,.T.);
#85461=ORIENTED_EDGE('',*,*,#57267,.T.);
#85462=ORIENTED_EDGE('',*,*,#57265,.T.);
#85463=ORIENTED_EDGE('',*,*,#57268,.T.);
#85464=ORIENTED_EDGE('',*,*,#57269,.T.);
#85465=ORIENTED_EDGE('',*,*,#57258,.F.);
#85466=ORIENTED_EDGE('',*,*,#57270,.T.);
#85467=ORIENTED_EDGE('',*,*,#57271,.T.);
#85468=ORIENTED_EDGE('',*,*,#57272,.F.);
#85469=ORIENTED_EDGE('',*,*,#57266,.F.);
#85470=ORIENTED_EDGE('',*,*,#57273,.F.);
#85471=ORIENTED_EDGE('',*,*,#57274,.F.);
#85472=ORIENTED_EDGE('',*,*,#57273,.T.);
#85473=ORIENTED_EDGE('',*,*,#57271,.F.);
#85474=ORIENTED_EDGE('',*,*,#57270,.F.);
#85475=ORIENTED_EDGE('',*,*,#57275,.F.);
#85476=ORIENTED_EDGE('',*,*,#57276,.F.);
#85477=ORIENTED_EDGE('',*,*,#57275,.T.);
#85478=ORIENTED_EDGE('',*,*,#57262,.F.);
#85479=ORIENTED_EDGE('',*,*,#57277,.F.);
#85480=ORIENTED_EDGE('',*,*,#57278,.F.);
#85481=ORIENTED_EDGE('',*,*,#57279,.T.);
#85482=ORIENTED_EDGE('',*,*,#57272,.T.);
#85483=ORIENTED_EDGE('',*,*,#53971,.F.);
#85484=ORIENTED_EDGE('',*,*,#54873,.T.);
#85485=ORIENTED_EDGE('',*,*,#57280,.F.);
#85486=ORIENTED_EDGE('',*,*,#57267,.F.);
#85487=ORIENTED_EDGE('',*,*,#57279,.F.);
#85488=ORIENTED_EDGE('',*,*,#54872,.F.);
#85489=ORIENTED_EDGE('',*,*,#57280,.T.);
#85490=ORIENTED_EDGE('',*,*,#54997,.F.);
#85491=ORIENTED_EDGE('',*,*,#57281,.F.);
#85492=ORIENTED_EDGE('',*,*,#57263,.F.);
#85493=ORIENTED_EDGE('',*,*,#57281,.T.);
#85494=ORIENTED_EDGE('',*,*,#54534,.F.);
#85495=ORIENTED_EDGE('',*,*,#57282,.F.);
#85496=ORIENTED_EDGE('',*,*,#57264,.F.);
#85497=ORIENTED_EDGE('',*,*,#57282,.T.);
#85498=ORIENTED_EDGE('',*,*,#54533,.F.);
#85499=ORIENTED_EDGE('',*,*,#57283,.F.);
#85500=ORIENTED_EDGE('',*,*,#57269,.F.);
#85501=ORIENTED_EDGE('',*,*,#57268,.F.);
#85502=ORIENTED_EDGE('',*,*,#57283,.T.);
#85503=ORIENTED_EDGE('',*,*,#54532,.F.);
#85504=ORIENTED_EDGE('',*,*,#57284,.F.);
#85505=ORIENTED_EDGE('',*,*,#57259,.F.);
#85506=ORIENTED_EDGE('',*,*,#57285,.T.);
#85507=ORIENTED_EDGE('',*,*,#57260,.F.);
#85508=ORIENTED_EDGE('',*,*,#57284,.T.);
#85509=ORIENTED_EDGE('',*,*,#54998,.F.);
#85510=ORIENTED_EDGE('',*,*,#57286,.T.);
#85511=ORIENTED_EDGE('',*,*,#57261,.F.);
#85512=ORIENTED_EDGE('',*,*,#57285,.F.);
#85513=ORIENTED_EDGE('',*,*,#54875,.F.);
#85514=ORIENTED_EDGE('',*,*,#53969,.T.);
#85515=ORIENTED_EDGE('',*,*,#57277,.T.);
#85516=ORIENTED_EDGE('',*,*,#57286,.F.);
#85517=ORIENTED_EDGE('',*,*,#54874,.T.);
#85518=ORIENTED_EDGE('',*,*,#57276,.T.);
#85519=ORIENTED_EDGE('',*,*,#57278,.T.);
#85520=ORIENTED_EDGE('',*,*,#53968,.T.);
#85521=ORIENTED_EDGE('',*,*,#57274,.T.);
#85522=ORIENTED_EDGE('',*,*,#57287,.T.);
#85523=ORIENTED_EDGE('',*,*,#57288,.T.);
#85524=ORIENTED_EDGE('',*,*,#57289,.T.);
#85525=ORIENTED_EDGE('',*,*,#57290,.T.);
#85526=ORIENTED_EDGE('',*,*,#57291,.T.);
#85527=ORIENTED_EDGE('',*,*,#57292,.T.);
#85528=ORIENTED_EDGE('',*,*,#57293,.T.);
#85529=ORIENTED_EDGE('',*,*,#57294,.F.);
#85530=ORIENTED_EDGE('',*,*,#57295,.T.);
#85531=ORIENTED_EDGE('',*,*,#57296,.T.);
#85532=ORIENTED_EDGE('',*,*,#57294,.T.);
#85533=ORIENTED_EDGE('',*,*,#57297,.T.);
#85534=ORIENTED_EDGE('',*,*,#57298,.T.);
#85535=ORIENTED_EDGE('',*,*,#57287,.F.);
#85536=ORIENTED_EDGE('',*,*,#57299,.T.);
#85537=ORIENTED_EDGE('',*,*,#57300,.T.);
#85538=ORIENTED_EDGE('',*,*,#57301,.F.);
#85539=ORIENTED_EDGE('',*,*,#57295,.F.);
#85540=ORIENTED_EDGE('',*,*,#57302,.F.);
#85541=ORIENTED_EDGE('',*,*,#57303,.F.);
#85542=ORIENTED_EDGE('',*,*,#57302,.T.);
#85543=ORIENTED_EDGE('',*,*,#57300,.F.);
#85544=ORIENTED_EDGE('',*,*,#57299,.F.);
#85545=ORIENTED_EDGE('',*,*,#57304,.F.);
#85546=ORIENTED_EDGE('',*,*,#57305,.F.);
#85547=ORIENTED_EDGE('',*,*,#57304,.T.);
#85548=ORIENTED_EDGE('',*,*,#57291,.F.);
#85549=ORIENTED_EDGE('',*,*,#57306,.F.);
#85550=ORIENTED_EDGE('',*,*,#57307,.F.);
#85551=ORIENTED_EDGE('',*,*,#57308,.T.);
#85552=ORIENTED_EDGE('',*,*,#57301,.T.);
#85553=ORIENTED_EDGE('',*,*,#53967,.F.);
#85554=ORIENTED_EDGE('',*,*,#54868,.T.);
#85555=ORIENTED_EDGE('',*,*,#57309,.F.);
#85556=ORIENTED_EDGE('',*,*,#57296,.F.);
#85557=ORIENTED_EDGE('',*,*,#57308,.F.);
#85558=ORIENTED_EDGE('',*,*,#54867,.F.);
#85559=ORIENTED_EDGE('',*,*,#57309,.T.);
#85560=ORIENTED_EDGE('',*,*,#54995,.F.);
#85561=ORIENTED_EDGE('',*,*,#57310,.F.);
#85562=ORIENTED_EDGE('',*,*,#57292,.F.);
#85563=ORIENTED_EDGE('',*,*,#57310,.T.);
#85564=ORIENTED_EDGE('',*,*,#54538,.F.);
#85565=ORIENTED_EDGE('',*,*,#57311,.F.);
#85566=ORIENTED_EDGE('',*,*,#57293,.F.);
#85567=ORIENTED_EDGE('',*,*,#57311,.T.);
#85568=ORIENTED_EDGE('',*,*,#54537,.F.);
#85569=ORIENTED_EDGE('',*,*,#57312,.F.);
#85570=ORIENTED_EDGE('',*,*,#57298,.F.);
#85571=ORIENTED_EDGE('',*,*,#57297,.F.);
#85572=ORIENTED_EDGE('',*,*,#57312,.T.);
#85573=ORIENTED_EDGE('',*,*,#54536,.F.);
#85574=ORIENTED_EDGE('',*,*,#57313,.F.);
#85575=ORIENTED_EDGE('',*,*,#57288,.F.);
#85576=ORIENTED_EDGE('',*,*,#57314,.T.);
#85577=ORIENTED_EDGE('',*,*,#57289,.F.);
#85578=ORIENTED_EDGE('',*,*,#57313,.T.);
#85579=ORIENTED_EDGE('',*,*,#54996,.F.);
#85580=ORIENTED_EDGE('',*,*,#57315,.T.);
#85581=ORIENTED_EDGE('',*,*,#57290,.F.);
#85582=ORIENTED_EDGE('',*,*,#57314,.F.);
#85583=ORIENTED_EDGE('',*,*,#54870,.F.);
#85584=ORIENTED_EDGE('',*,*,#53965,.T.);
#85585=ORIENTED_EDGE('',*,*,#57306,.T.);
#85586=ORIENTED_EDGE('',*,*,#57315,.F.);
#85587=ORIENTED_EDGE('',*,*,#54869,.T.);
#85588=ORIENTED_EDGE('',*,*,#57305,.T.);
#85589=ORIENTED_EDGE('',*,*,#57307,.T.);
#85590=ORIENTED_EDGE('',*,*,#53964,.T.);
#85591=ORIENTED_EDGE('',*,*,#57303,.T.);
#85592=ORIENTED_EDGE('',*,*,#57316,.T.);
#85593=ORIENTED_EDGE('',*,*,#57317,.T.);
#85594=ORIENTED_EDGE('',*,*,#57318,.T.);
#85595=ORIENTED_EDGE('',*,*,#57319,.T.);
#85596=ORIENTED_EDGE('',*,*,#57320,.T.);
#85597=ORIENTED_EDGE('',*,*,#57321,.T.);
#85598=ORIENTED_EDGE('',*,*,#57322,.T.);
#85599=ORIENTED_EDGE('',*,*,#57323,.F.);
#85600=ORIENTED_EDGE('',*,*,#57324,.T.);
#85601=ORIENTED_EDGE('',*,*,#57325,.T.);
#85602=ORIENTED_EDGE('',*,*,#57323,.T.);
#85603=ORIENTED_EDGE('',*,*,#57326,.T.);
#85604=ORIENTED_EDGE('',*,*,#57327,.T.);
#85605=ORIENTED_EDGE('',*,*,#57316,.F.);
#85606=ORIENTED_EDGE('',*,*,#57328,.T.);
#85607=ORIENTED_EDGE('',*,*,#57329,.T.);
#85608=ORIENTED_EDGE('',*,*,#57330,.F.);
#85609=ORIENTED_EDGE('',*,*,#57324,.F.);
#85610=ORIENTED_EDGE('',*,*,#57331,.F.);
#85611=ORIENTED_EDGE('',*,*,#57332,.F.);
#85612=ORIENTED_EDGE('',*,*,#57331,.T.);
#85613=ORIENTED_EDGE('',*,*,#57329,.F.);
#85614=ORIENTED_EDGE('',*,*,#57328,.F.);
#85615=ORIENTED_EDGE('',*,*,#57333,.F.);
#85616=ORIENTED_EDGE('',*,*,#57334,.F.);
#85617=ORIENTED_EDGE('',*,*,#57333,.T.);
#85618=ORIENTED_EDGE('',*,*,#57320,.F.);
#85619=ORIENTED_EDGE('',*,*,#57335,.F.);
#85620=ORIENTED_EDGE('',*,*,#57336,.F.);
#85621=ORIENTED_EDGE('',*,*,#57337,.T.);
#85622=ORIENTED_EDGE('',*,*,#57330,.T.);
#85623=ORIENTED_EDGE('',*,*,#53963,.F.);
#85624=ORIENTED_EDGE('',*,*,#54863,.T.);
#85625=ORIENTED_EDGE('',*,*,#57338,.F.);
#85626=ORIENTED_EDGE('',*,*,#57325,.F.);
#85627=ORIENTED_EDGE('',*,*,#57337,.F.);
#85628=ORIENTED_EDGE('',*,*,#54862,.F.);
#85629=ORIENTED_EDGE('',*,*,#57338,.T.);
#85630=ORIENTED_EDGE('',*,*,#54993,.F.);
#85631=ORIENTED_EDGE('',*,*,#57339,.F.);
#85632=ORIENTED_EDGE('',*,*,#57321,.F.);
#85633=ORIENTED_EDGE('',*,*,#57339,.T.);
#85634=ORIENTED_EDGE('',*,*,#54542,.F.);
#85635=ORIENTED_EDGE('',*,*,#57340,.F.);
#85636=ORIENTED_EDGE('',*,*,#57322,.F.);
#85637=ORIENTED_EDGE('',*,*,#57340,.T.);
#85638=ORIENTED_EDGE('',*,*,#54541,.F.);
#85639=ORIENTED_EDGE('',*,*,#57341,.F.);
#85640=ORIENTED_EDGE('',*,*,#57327,.F.);
#85641=ORIENTED_EDGE('',*,*,#57326,.F.);
#85642=ORIENTED_EDGE('',*,*,#57341,.T.);
#85643=ORIENTED_EDGE('',*,*,#54540,.F.);
#85644=ORIENTED_EDGE('',*,*,#57342,.F.);
#85645=ORIENTED_EDGE('',*,*,#57317,.F.);
#85646=ORIENTED_EDGE('',*,*,#57343,.T.);
#85647=ORIENTED_EDGE('',*,*,#57318,.F.);
#85648=ORIENTED_EDGE('',*,*,#57342,.T.);
#85649=ORIENTED_EDGE('',*,*,#54994,.F.);
#85650=ORIENTED_EDGE('',*,*,#57344,.T.);
#85651=ORIENTED_EDGE('',*,*,#57319,.F.);
#85652=ORIENTED_EDGE('',*,*,#57343,.F.);
#85653=ORIENTED_EDGE('',*,*,#54865,.F.);
#85654=ORIENTED_EDGE('',*,*,#53961,.T.);
#85655=ORIENTED_EDGE('',*,*,#57335,.T.);
#85656=ORIENTED_EDGE('',*,*,#57344,.F.);
#85657=ORIENTED_EDGE('',*,*,#54864,.T.);
#85658=ORIENTED_EDGE('',*,*,#57334,.T.);
#85659=ORIENTED_EDGE('',*,*,#57336,.T.);
#85660=ORIENTED_EDGE('',*,*,#53960,.T.);
#85661=ORIENTED_EDGE('',*,*,#57332,.T.);
#85662=ORIENTED_EDGE('',*,*,#57345,.T.);
#85663=ORIENTED_EDGE('',*,*,#57346,.T.);
#85664=ORIENTED_EDGE('',*,*,#57347,.T.);
#85665=ORIENTED_EDGE('',*,*,#57348,.T.);
#85666=ORIENTED_EDGE('',*,*,#57349,.T.);
#85667=ORIENTED_EDGE('',*,*,#57350,.T.);
#85668=ORIENTED_EDGE('',*,*,#57351,.T.);
#85669=ORIENTED_EDGE('',*,*,#57352,.F.);
#85670=ORIENTED_EDGE('',*,*,#57353,.T.);
#85671=ORIENTED_EDGE('',*,*,#57354,.T.);
#85672=ORIENTED_EDGE('',*,*,#57352,.T.);
#85673=ORIENTED_EDGE('',*,*,#57355,.T.);
#85674=ORIENTED_EDGE('',*,*,#57356,.T.);
#85675=ORIENTED_EDGE('',*,*,#57345,.F.);
#85676=ORIENTED_EDGE('',*,*,#57357,.T.);
#85677=ORIENTED_EDGE('',*,*,#57358,.T.);
#85678=ORIENTED_EDGE('',*,*,#57359,.F.);
#85679=ORIENTED_EDGE('',*,*,#57353,.F.);
#85680=ORIENTED_EDGE('',*,*,#57360,.F.);
#85681=ORIENTED_EDGE('',*,*,#57361,.F.);
#85682=ORIENTED_EDGE('',*,*,#57360,.T.);
#85683=ORIENTED_EDGE('',*,*,#57358,.F.);
#85684=ORIENTED_EDGE('',*,*,#57357,.F.);
#85685=ORIENTED_EDGE('',*,*,#57362,.F.);
#85686=ORIENTED_EDGE('',*,*,#57363,.F.);
#85687=ORIENTED_EDGE('',*,*,#57362,.T.);
#85688=ORIENTED_EDGE('',*,*,#57349,.F.);
#85689=ORIENTED_EDGE('',*,*,#57364,.F.);
#85690=ORIENTED_EDGE('',*,*,#57365,.F.);
#85691=ORIENTED_EDGE('',*,*,#57366,.T.);
#85692=ORIENTED_EDGE('',*,*,#57359,.T.);
#85693=ORIENTED_EDGE('',*,*,#53959,.F.);
#85694=ORIENTED_EDGE('',*,*,#54858,.T.);
#85695=ORIENTED_EDGE('',*,*,#57367,.F.);
#85696=ORIENTED_EDGE('',*,*,#57354,.F.);
#85697=ORIENTED_EDGE('',*,*,#57366,.F.);
#85698=ORIENTED_EDGE('',*,*,#54857,.F.);
#85699=ORIENTED_EDGE('',*,*,#57367,.T.);
#85700=ORIENTED_EDGE('',*,*,#54991,.F.);
#85701=ORIENTED_EDGE('',*,*,#57368,.F.);
#85702=ORIENTED_EDGE('',*,*,#57350,.F.);
#85703=ORIENTED_EDGE('',*,*,#57368,.T.);
#85704=ORIENTED_EDGE('',*,*,#54546,.F.);
#85705=ORIENTED_EDGE('',*,*,#57369,.F.);
#85706=ORIENTED_EDGE('',*,*,#57351,.F.);
#85707=ORIENTED_EDGE('',*,*,#57369,.T.);
#85708=ORIENTED_EDGE('',*,*,#54545,.F.);
#85709=ORIENTED_EDGE('',*,*,#57370,.F.);
#85710=ORIENTED_EDGE('',*,*,#57356,.F.);
#85711=ORIENTED_EDGE('',*,*,#57355,.F.);
#85712=ORIENTED_EDGE('',*,*,#57370,.T.);
#85713=ORIENTED_EDGE('',*,*,#54544,.F.);
#85714=ORIENTED_EDGE('',*,*,#57371,.F.);
#85715=ORIENTED_EDGE('',*,*,#57346,.F.);
#85716=ORIENTED_EDGE('',*,*,#57372,.T.);
#85717=ORIENTED_EDGE('',*,*,#57347,.F.);
#85718=ORIENTED_EDGE('',*,*,#57371,.T.);
#85719=ORIENTED_EDGE('',*,*,#54992,.F.);
#85720=ORIENTED_EDGE('',*,*,#57373,.T.);
#85721=ORIENTED_EDGE('',*,*,#57348,.F.);
#85722=ORIENTED_EDGE('',*,*,#57372,.F.);
#85723=ORIENTED_EDGE('',*,*,#54860,.F.);
#85724=ORIENTED_EDGE('',*,*,#53957,.T.);
#85725=ORIENTED_EDGE('',*,*,#57364,.T.);
#85726=ORIENTED_EDGE('',*,*,#57373,.F.);
#85727=ORIENTED_EDGE('',*,*,#54859,.T.);
#85728=ORIENTED_EDGE('',*,*,#57363,.T.);
#85729=ORIENTED_EDGE('',*,*,#57365,.T.);
#85730=ORIENTED_EDGE('',*,*,#53956,.T.);
#85731=ORIENTED_EDGE('',*,*,#57361,.T.);
#85732=ORIENTED_EDGE('',*,*,#57374,.T.);
#85733=ORIENTED_EDGE('',*,*,#57375,.T.);
#85734=ORIENTED_EDGE('',*,*,#57376,.T.);
#85735=ORIENTED_EDGE('',*,*,#57377,.T.);
#85736=ORIENTED_EDGE('',*,*,#57378,.T.);
#85737=ORIENTED_EDGE('',*,*,#57379,.T.);
#85738=ORIENTED_EDGE('',*,*,#57380,.T.);
#85739=ORIENTED_EDGE('',*,*,#57381,.F.);
#85740=ORIENTED_EDGE('',*,*,#57382,.T.);
#85741=ORIENTED_EDGE('',*,*,#57383,.T.);
#85742=ORIENTED_EDGE('',*,*,#57381,.T.);
#85743=ORIENTED_EDGE('',*,*,#57384,.T.);
#85744=ORIENTED_EDGE('',*,*,#57385,.T.);
#85745=ORIENTED_EDGE('',*,*,#57374,.F.);
#85746=ORIENTED_EDGE('',*,*,#57386,.T.);
#85747=ORIENTED_EDGE('',*,*,#57387,.T.);
#85748=ORIENTED_EDGE('',*,*,#57388,.F.);
#85749=ORIENTED_EDGE('',*,*,#57382,.F.);
#85750=ORIENTED_EDGE('',*,*,#57389,.F.);
#85751=ORIENTED_EDGE('',*,*,#57390,.F.);
#85752=ORIENTED_EDGE('',*,*,#57389,.T.);
#85753=ORIENTED_EDGE('',*,*,#57387,.F.);
#85754=ORIENTED_EDGE('',*,*,#57386,.F.);
#85755=ORIENTED_EDGE('',*,*,#57391,.F.);
#85756=ORIENTED_EDGE('',*,*,#57392,.F.);
#85757=ORIENTED_EDGE('',*,*,#57391,.T.);
#85758=ORIENTED_EDGE('',*,*,#57378,.F.);
#85759=ORIENTED_EDGE('',*,*,#57393,.F.);
#85760=ORIENTED_EDGE('',*,*,#57394,.F.);
#85761=ORIENTED_EDGE('',*,*,#57395,.T.);
#85762=ORIENTED_EDGE('',*,*,#57388,.T.);
#85763=ORIENTED_EDGE('',*,*,#53955,.F.);
#85764=ORIENTED_EDGE('',*,*,#54853,.T.);
#85765=ORIENTED_EDGE('',*,*,#57396,.F.);
#85766=ORIENTED_EDGE('',*,*,#57383,.F.);
#85767=ORIENTED_EDGE('',*,*,#57395,.F.);
#85768=ORIENTED_EDGE('',*,*,#54852,.F.);
#85769=ORIENTED_EDGE('',*,*,#57396,.T.);
#85770=ORIENTED_EDGE('',*,*,#54988,.F.);
#85771=ORIENTED_EDGE('',*,*,#57397,.F.);
#85772=ORIENTED_EDGE('',*,*,#57379,.F.);
#85773=ORIENTED_EDGE('',*,*,#57397,.T.);
#85774=ORIENTED_EDGE('',*,*,#54550,.F.);
#85775=ORIENTED_EDGE('',*,*,#57398,.F.);
#85776=ORIENTED_EDGE('',*,*,#57380,.F.);
#85777=ORIENTED_EDGE('',*,*,#57398,.T.);
#85778=ORIENTED_EDGE('',*,*,#54549,.F.);
#85779=ORIENTED_EDGE('',*,*,#57399,.F.);
#85780=ORIENTED_EDGE('',*,*,#57385,.F.);
#85781=ORIENTED_EDGE('',*,*,#57384,.F.);
#85782=ORIENTED_EDGE('',*,*,#57399,.T.);
#85783=ORIENTED_EDGE('',*,*,#54548,.F.);
#85784=ORIENTED_EDGE('',*,*,#57400,.F.);
#85785=ORIENTED_EDGE('',*,*,#57375,.F.);
#85786=ORIENTED_EDGE('',*,*,#57401,.T.);
#85787=ORIENTED_EDGE('',*,*,#57376,.F.);
#85788=ORIENTED_EDGE('',*,*,#57400,.T.);
#85789=ORIENTED_EDGE('',*,*,#54990,.F.);
#85790=ORIENTED_EDGE('',*,*,#57402,.T.);
#85791=ORIENTED_EDGE('',*,*,#57377,.F.);
#85792=ORIENTED_EDGE('',*,*,#57401,.F.);
#85793=ORIENTED_EDGE('',*,*,#54855,.F.);
#85794=ORIENTED_EDGE('',*,*,#53953,.T.);
#85795=ORIENTED_EDGE('',*,*,#57393,.T.);
#85796=ORIENTED_EDGE('',*,*,#57402,.F.);
#85797=ORIENTED_EDGE('',*,*,#54854,.T.);
#85798=ORIENTED_EDGE('',*,*,#57392,.T.);
#85799=ORIENTED_EDGE('',*,*,#57394,.T.);
#85800=ORIENTED_EDGE('',*,*,#53952,.T.);
#85801=ORIENTED_EDGE('',*,*,#57390,.T.);
#88351=CYLINDRICAL_SURFACE('',#102649,1.17524047358089);
#88352=CYLINDRICAL_SURFACE('',#102651,1.17524047358089);
#88353=CYLINDRICAL_SURFACE('',#102652,1.17524047358089);
#88354=CYLINDRICAL_SURFACE('',#102653,1.17524047358089);
#88355=CYLINDRICAL_SURFACE('',#102654,1.17524047358089);
#88356=CYLINDRICAL_SURFACE('',#102655,1.17524047358089);
#88357=CYLINDRICAL_SURFACE('',#102656,1.17524047358089);
#88358=CYLINDRICAL_SURFACE('',#102657,1.17524047358089);
#88359=CYLINDRICAL_SURFACE('',#102658,1.17524047358089);
#88360=CYLINDRICAL_SURFACE('',#102659,1.17524047358089);
#88361=CYLINDRICAL_SURFACE('',#102660,1.17524047358089);
#88362=CYLINDRICAL_SURFACE('',#102661,1.17524047358089);
#88363=CYLINDRICAL_SURFACE('',#102662,1.17524047358089);
#88364=CYLINDRICAL_SURFACE('',#102663,1.17524047358089);
#88365=CYLINDRICAL_SURFACE('',#102664,1.17524047358089);
#88366=CYLINDRICAL_SURFACE('',#102665,1.17524047358089);
#88367=CYLINDRICAL_SURFACE('',#102666,1.17524047358089);
#88368=CYLINDRICAL_SURFACE('',#102667,1.17524047358089);
#88369=CYLINDRICAL_SURFACE('',#102668,1.17524047358089);
#88370=CYLINDRICAL_SURFACE('',#102669,1.17524047358089);
#88371=CYLINDRICAL_SURFACE('',#102670,1.17524047358089);
#88372=CYLINDRICAL_SURFACE('',#102671,1.17524047358089);
#88373=CYLINDRICAL_SURFACE('',#102672,1.17524047358089);
#88374=CYLINDRICAL_SURFACE('',#102673,1.17524047358089);
#88375=CYLINDRICAL_SURFACE('',#102674,1.17524047358089);
#88376=CYLINDRICAL_SURFACE('',#102675,1.17524047358089);
#88377=CYLINDRICAL_SURFACE('',#102676,1.17524047358089);
#88378=CYLINDRICAL_SURFACE('',#102677,1.17524047358089);
#88379=CYLINDRICAL_SURFACE('',#102678,1.17524047358089);
#88380=CYLINDRICAL_SURFACE('',#102679,1.17524047358089);
#88381=CYLINDRICAL_SURFACE('',#102680,1.17524047358089);
#88382=CYLINDRICAL_SURFACE('',#102681,1.17524047358089);
#88383=CYLINDRICAL_SURFACE('',#102682,1.17524047358089);
#88384=CYLINDRICAL_SURFACE('',#102683,1.17524047358089);
#88385=CYLINDRICAL_SURFACE('',#102684,1.17524047358089);
#88386=CYLINDRICAL_SURFACE('',#102685,1.17524047358089);
#88387=CYLINDRICAL_SURFACE('',#102690,1.50000000000006);
#88388=CYLINDRICAL_SURFACE('',#102692,1.50000000000006);
#88389=CYLINDRICAL_SURFACE('',#102693,1.50000000000006);
#88390=CYLINDRICAL_SURFACE('',#102694,1.50000000000006);
#88391=CYLINDRICAL_SURFACE('',#102695,1.50000000000006);
#88392=CYLINDRICAL_SURFACE('',#102696,1.50000000000006);
#88393=CYLINDRICAL_SURFACE('',#102697,1.50000000000006);
#88394=CYLINDRICAL_SURFACE('',#102698,1.50000000000006);
#88395=CYLINDRICAL_SURFACE('',#102699,1.50000000000006);
#88396=CYLINDRICAL_SURFACE('',#102700,1.50000000000006);
#88397=CYLINDRICAL_SURFACE('',#102701,1.50000000000006);
#88398=CYLINDRICAL_SURFACE('',#102702,1.50000000000006);
#88399=CYLINDRICAL_SURFACE('',#102703,1.50000000000006);
#88400=CYLINDRICAL_SURFACE('',#102704,1.50000000000006);
#88401=CYLINDRICAL_SURFACE('',#102705,1.50000000000006);
#88402=CYLINDRICAL_SURFACE('',#102706,1.50000000000006);
#88403=CYLINDRICAL_SURFACE('',#102707,1.50000000000006);
#88404=CYLINDRICAL_SURFACE('',#102708,1.50000000000006);
#88405=CYLINDRICAL_SURFACE('',#102709,1.50000000000006);
#88406=CYLINDRICAL_SURFACE('',#102710,1.50000000000006);
#88407=CYLINDRICAL_SURFACE('',#102711,1.50000000000006);
#88408=CYLINDRICAL_SURFACE('',#102712,1.50000000000006);
#88409=CYLINDRICAL_SURFACE('',#102713,1.50000000000006);
#88410=CYLINDRICAL_SURFACE('',#102714,1.50000000000006);
#88411=CYLINDRICAL_SURFACE('',#102715,1.50000000000006);
#88412=CYLINDRICAL_SURFACE('',#102716,1.50000000000006);
#88413=CYLINDRICAL_SURFACE('',#102717,1.50000000000006);
#88414=CYLINDRICAL_SURFACE('',#102718,1.50000000000006);
#88415=CYLINDRICAL_SURFACE('',#102719,1.50000000000006);
#88416=CYLINDRICAL_SURFACE('',#102720,1.50000000000006);
#88417=CYLINDRICAL_SURFACE('',#102721,1.50000000000006);
#88418=CYLINDRICAL_SURFACE('',#102722,1.50000000000006);
#88419=CYLINDRICAL_SURFACE('',#102723,1.50000000000006);
#88420=CYLINDRICAL_SURFACE('',#102724,1.50000000000006);
#88421=CYLINDRICAL_SURFACE('',#102725,1.50000000000006);
#88422=CYLINDRICAL_SURFACE('',#103114,1.50000000000006);
#88423=CYLINDRICAL_SURFACE('',#103222,2.75);
#88424=CYLINDRICAL_SURFACE('',#103528,0.0343750000000002);
#88425=CYLINDRICAL_SURFACE('',#103563,1.17524047358089);
#88426=CYLINDRICAL_SURFACE('',#103567,0.0219999999999999);
#88427=CYLINDRICAL_SURFACE('',#103575,0.0219999999999999);
#88428=CYLINDRICAL_SURFACE('',#103582,0.0343750000000002);
#88429=CYLINDRICAL_SURFACE('',#103589,0.0219999999999999);
#88430=CYLINDRICAL_SURFACE('',#103596,0.0219999999999999);
#88431=CYLINDRICAL_SURFACE('',#103603,0.0343750000000002);
#88432=CYLINDRICAL_SURFACE('',#103610,0.0219999999999999);
#88433=CYLINDRICAL_SURFACE('',#103617,0.0219999999999999);
#88434=CYLINDRICAL_SURFACE('',#103624,0.0343750000000002);
#88435=CYLINDRICAL_SURFACE('',#103631,0.0220000000000001);
#88436=CYLINDRICAL_SURFACE('',#103638,0.0220000000000001);
#88437=CYLINDRICAL_SURFACE('',#103645,0.0343750000000002);
#88438=CYLINDRICAL_SURFACE('',#103652,0.022);
#88439=CYLINDRICAL_SURFACE('',#103659,0.022);
#88440=CYLINDRICAL_SURFACE('',#103666,0.0343750000000002);
#88441=CYLINDRICAL_SURFACE('',#103673,0.022);
#88442=CYLINDRICAL_SURFACE('',#103680,0.022);
#88443=CYLINDRICAL_SURFACE('',#103687,0.0343750000000003);
#88444=CYLINDRICAL_SURFACE('',#103694,0.0219999999999999);
#88445=CYLINDRICAL_SURFACE('',#103701,0.0219999999999999);
#88446=CYLINDRICAL_SURFACE('',#103708,0.0343750000000004);
#88447=CYLINDRICAL_SURFACE('',#103715,0.022);
#88448=CYLINDRICAL_SURFACE('',#103722,0.022);
#88449=CYLINDRICAL_SURFACE('',#103729,0.0343750000000001);
#88450=CYLINDRICAL_SURFACE('',#103736,0.0220000000000002);
#88451=CYLINDRICAL_SURFACE('',#103743,0.0220000000000002);
#88452=CYLINDRICAL_SURFACE('',#103750,0.0343750000000003);
#88453=CYLINDRICAL_SURFACE('',#103757,0.0220000000000001);
#88454=CYLINDRICAL_SURFACE('',#103764,0.0220000000000001);
#88455=CYLINDRICAL_SURFACE('',#103771,0.0343750000000003);
#88456=CYLINDRICAL_SURFACE('',#103778,0.022);
#88457=CYLINDRICAL_SURFACE('',#103785,0.022);
#88458=CYLINDRICAL_SURFACE('',#103792,0.0343750000000002);
#88459=CYLINDRICAL_SURFACE('',#103799,0.022);
#88460=CYLINDRICAL_SURFACE('',#103806,0.0219999999999998);
#88461=CYLINDRICAL_SURFACE('',#103813,0.0343750000000002);
#88462=CYLINDRICAL_SURFACE('',#103820,0.0220000000000002);
#88463=CYLINDRICAL_SURFACE('',#103827,0.0220000000000002);
#88464=CYLINDRICAL_SURFACE('',#103834,0.0343750000000002);
#88465=CYLINDRICAL_SURFACE('',#103841,0.0220000000000002);
#88466=CYLINDRICAL_SURFACE('',#103848,0.0220000000000002);
#88467=CYLINDRICAL_SURFACE('',#103855,0.0343750000000002);
#88468=CYLINDRICAL_SURFACE('',#103862,0.0220000000000001);
#88469=CYLINDRICAL_SURFACE('',#103869,0.0220000000000001);
#88470=CYLINDRICAL_SURFACE('',#103876,0.0343750000000002);
#88471=CYLINDRICAL_SURFACE('',#103883,0.0220000000000001);
#88472=CYLINDRICAL_SURFACE('',#103890,0.0220000000000001);
#88473=CYLINDRICAL_SURFACE('',#103897,0.0343750000000002);
#88474=CYLINDRICAL_SURFACE('',#103904,0.022);
#88475=CYLINDRICAL_SURFACE('',#103911,0.022);
#88476=CYLINDRICAL_SURFACE('',#103918,0.0343750000000004);
#88477=CYLINDRICAL_SURFACE('',#103925,0.0220000000000001);
#88478=CYLINDRICAL_SURFACE('',#103932,0.0220000000000001);
#88479=CYLINDRICAL_SURFACE('',#103939,0.0343750000000002);
#88480=CYLINDRICAL_SURFACE('',#103946,0.0219999999999999);
#88481=CYLINDRICAL_SURFACE('',#103953,0.0219999999999999);
#88482=CYLINDRICAL_SURFACE('',#103960,0.0343750000000001);
#88483=CYLINDRICAL_SURFACE('',#103967,0.0220000000000002);
#88484=CYLINDRICAL_SURFACE('',#103974,0.0220000000000002);
#88485=CYLINDRICAL_SURFACE('',#103981,0.0343750000000004);
#88486=CYLINDRICAL_SURFACE('',#103988,0.0220000000000002);
#88487=CYLINDRICAL_SURFACE('',#103995,0.0220000000000002);
#88488=CYLINDRICAL_SURFACE('',#104002,0.0343750000000002);
#88489=CYLINDRICAL_SURFACE('',#104009,0.022);
#88490=CYLINDRICAL_SURFACE('',#104016,0.022);
#88491=CYLINDRICAL_SURFACE('',#104023,0.0343750000000001);
#88492=CYLINDRICAL_SURFACE('',#104030,0.022);
#88493=CYLINDRICAL_SURFACE('',#104037,0.022);
#88494=CYLINDRICAL_SURFACE('',#104044,0.0343750000000002);
#88495=CYLINDRICAL_SURFACE('',#104051,0.0220000000000001);
#88496=CYLINDRICAL_SURFACE('',#104058,0.0220000000000001);
#88497=CYLINDRICAL_SURFACE('',#104065,0.0343750000000001);
#88498=CYLINDRICAL_SURFACE('',#104072,0.0220000000000002);
#88499=CYLINDRICAL_SURFACE('',#104079,0.0220000000000002);
#88500=CYLINDRICAL_SURFACE('',#104086,0.0343750000000003);
#88501=CYLINDRICAL_SURFACE('',#104093,0.022);
#88502=CYLINDRICAL_SURFACE('',#104100,0.022);
#88503=CYLINDRICAL_SURFACE('',#104107,0.0343750000000003);
#88504=CYLINDRICAL_SURFACE('',#104114,0.022);
#88505=CYLINDRICAL_SURFACE('',#104121,0.022);
#88506=CYLINDRICAL_SURFACE('',#104128,0.0343750000000003);
#88507=CYLINDRICAL_SURFACE('',#104135,0.022);
#88508=CYLINDRICAL_SURFACE('',#104142,0.022);
#88509=CYLINDRICAL_SURFACE('',#104149,0.0343750000000003);
#88510=CYLINDRICAL_SURFACE('',#104156,0.022);
#88511=CYLINDRICAL_SURFACE('',#104163,0.022);
#88512=CYLINDRICAL_SURFACE('',#104170,0.0343750000000002);
#88513=CYLINDRICAL_SURFACE('',#104177,0.0220000000000001);
#88514=CYLINDRICAL_SURFACE('',#104184,0.0220000000000001);
#88515=CYLINDRICAL_SURFACE('',#104191,0.0343750000000002);
#88516=CYLINDRICAL_SURFACE('',#104198,0.022);
#88517=CYLINDRICAL_SURFACE('',#104205,0.022);
#88518=CYLINDRICAL_SURFACE('',#104212,0.0343750000000002);
#88519=CYLINDRICAL_SURFACE('',#104219,0.0220000000000002);
#88520=CYLINDRICAL_SURFACE('',#104226,0.0220000000000001);
#88521=CYLINDRICAL_SURFACE('',#104233,0.0343750000000002);
#88522=CYLINDRICAL_SURFACE('',#104240,0.0219999999999999);
#88523=CYLINDRICAL_SURFACE('',#104247,0.0219999999999999);
#88524=CYLINDRICAL_SURFACE('',#104254,0.0343750000000003);
#88525=CYLINDRICAL_SURFACE('',#104261,0.0220000000000001);
#88526=CYLINDRICAL_SURFACE('',#104268,0.0220000000000001);
#88527=CYLINDRICAL_SURFACE('',#104275,0.0343750000000003);
#88528=CYLINDRICAL_SURFACE('',#104282,0.0219999999999999);
#88529=CYLINDRICAL_SURFACE('',#104289,0.0219999999999999);
#88530=CYLINDRICAL_SURFACE('',#104296,0.0343750000000002);
#88531=CYLINDRICAL_SURFACE('',#104303,0.0220000000000002);
#88532=CYLINDRICAL_SURFACE('',#104310,0.0220000000000002);
#88533=CYLINDRICAL_SURFACE('',#104317,0.0343750000000003);
#88534=CYLINDRICAL_SURFACE('',#104324,0.0219999999999999);
#88535=CYLINDRICAL_SURFACE('',#104331,0.0219999999999999);
#88536=CYLINDRICAL_SURFACE('',#104338,0.0343750000000003);
#88537=CYLINDRICAL_SURFACE('',#104345,0.0219999999999999);
#88538=CYLINDRICAL_SURFACE('',#104352,0.0219999999999999);
#88539=CYLINDRICAL_SURFACE('',#104359,0.0343750000000004);
#88540=CYLINDRICAL_SURFACE('',#104366,0.0219999999999999);
#88541=CYLINDRICAL_SURFACE('',#104373,0.0219999999999999);
#88542=CYLINDRICAL_SURFACE('',#104380,0.034375);
#88543=CYLINDRICAL_SURFACE('',#104387,0.0220000000000001);
#88544=CYLINDRICAL_SURFACE('',#104394,0.0220000000000001);
#88545=CYLINDRICAL_SURFACE('',#104401,0.0343750000000003);
#88546=CYLINDRICAL_SURFACE('',#104408,0.0219999999999999);
#88547=CYLINDRICAL_SURFACE('',#104415,0.022);
#88548=CYLINDRICAL_SURFACE('',#104422,0.0343750000000004);
#88549=CYLINDRICAL_SURFACE('',#104429,0.0219999999999999);
#88550=CYLINDRICAL_SURFACE('',#104436,0.0219999999999999);
#88551=CYLINDRICAL_SURFACE('',#104443,0.0343750000000002);
#88552=CYLINDRICAL_SURFACE('',#104450,0.022);
#88553=CYLINDRICAL_SURFACE('',#104457,0.022);
#88554=CYLINDRICAL_SURFACE('',#104464,0.0343750000000003);
#88555=CYLINDRICAL_SURFACE('',#104471,0.022);
#88556=CYLINDRICAL_SURFACE('',#104478,0.022);
#88557=CYLINDRICAL_SURFACE('',#104485,0.0343750000000001);
#88558=CYLINDRICAL_SURFACE('',#104492,0.0219999999999998);
#88559=CYLINDRICAL_SURFACE('',#104499,0.0219999999999998);
#88560=CYLINDRICAL_SURFACE('',#104506,0.0343750000000001);
#88561=CYLINDRICAL_SURFACE('',#104513,0.0220000000000002);
#88562=CYLINDRICAL_SURFACE('',#104520,0.0220000000000001);
#88563=CYLINDRICAL_SURFACE('',#104527,0.0343750000000003);
#88564=CYLINDRICAL_SURFACE('',#104534,0.0219999999999998);
#88565=CYLINDRICAL_SURFACE('',#104541,0.0219999999999998);
#88566=CYLINDRICAL_SURFACE('',#104548,0.0343750000000001);
#88567=CYLINDRICAL_SURFACE('',#104555,0.0219999999999999);
#88568=CYLINDRICAL_SURFACE('',#104562,0.0219999999999999);
#88569=CYLINDRICAL_SURFACE('',#104569,0.0343750000000002);
#88570=CYLINDRICAL_SURFACE('',#104576,0.022);
#88571=CYLINDRICAL_SURFACE('',#104583,0.022);
#88572=CYLINDRICAL_SURFACE('',#104590,0.0343750000000002);
#88573=CYLINDRICAL_SURFACE('',#104597,0.022);
#88574=CYLINDRICAL_SURFACE('',#104604,0.022);
#88575=CYLINDRICAL_SURFACE('',#104611,0.0343750000000002);
#88576=CYLINDRICAL_SURFACE('',#104618,0.022);
#88577=CYLINDRICAL_SURFACE('',#104625,0.022);
#88578=CYLINDRICAL_SURFACE('',#104632,0.0343750000000002);
#88579=CYLINDRICAL_SURFACE('',#104639,0.022);
#88580=CYLINDRICAL_SURFACE('',#104646,0.022);
#88581=CYLINDRICAL_SURFACE('',#104653,0.0343750000000002);
#88582=CYLINDRICAL_SURFACE('',#104660,0.0219999999999999);
#88583=CYLINDRICAL_SURFACE('',#104667,0.0219999999999999);
#88584=CYLINDRICAL_SURFACE('',#104674,0.0343750000000002);
#88585=CYLINDRICAL_SURFACE('',#104681,0.0219999999999999);
#88586=CYLINDRICAL_SURFACE('',#104688,0.0219999999999999);
#88587=CYLINDRICAL_SURFACE('',#104695,0.0343750000000002);
#88588=CYLINDRICAL_SURFACE('',#104702,0.0219999999999999);
#88589=CYLINDRICAL_SURFACE('',#104709,0.0219999999999998);
#88590=CYLINDRICAL_SURFACE('',#104716,0.0343750000000001);
#88591=CYLINDRICAL_SURFACE('',#104723,0.0219999999999999);
#88592=CYLINDRICAL_SURFACE('',#104730,0.0219999999999999);
#88593=CYLINDRICAL_SURFACE('',#104737,0.0343750000000001);
#88594=CYLINDRICAL_SURFACE('',#104744,0.0219999999999999);
#88595=CYLINDRICAL_SURFACE('',#104751,0.0219999999999999);
#88596=CYLINDRICAL_SURFACE('',#104758,0.0343750000000003);
#88597=CYLINDRICAL_SURFACE('',#104765,0.0220000000000001);
#88598=CYLINDRICAL_SURFACE('',#104772,0.0220000000000001);
#88599=CYLINDRICAL_SURFACE('',#104779,0.034375);
#88600=CYLINDRICAL_SURFACE('',#104786,0.0220000000000001);
#88601=CYLINDRICAL_SURFACE('',#104793,0.022);
#88602=CYLINDRICAL_SURFACE('',#104800,0.0343750000000002);
#88603=CYLINDRICAL_SURFACE('',#104807,0.022);
#88604=CYLINDRICAL_SURFACE('',#104814,0.022);
#88605=CYLINDRICAL_SURFACE('',#104821,0.0343750000000004);
#88606=CYLINDRICAL_SURFACE('',#104828,0.022);
#88607=CYLINDRICAL_SURFACE('',#104835,0.022);
#88608=CYLINDRICAL_SURFACE('',#104842,0.0343750000000003);
#88609=CYLINDRICAL_SURFACE('',#104849,0.0220000000000001);
#88610=CYLINDRICAL_SURFACE('',#104856,0.0220000000000001);
#88611=CYLINDRICAL_SURFACE('',#104863,0.0343750000000002);
#88612=CYLINDRICAL_SURFACE('',#104870,0.0220000000000002);
#88613=CYLINDRICAL_SURFACE('',#104877,0.0220000000000002);
#88614=CYLINDRICAL_SURFACE('',#104884,0.0343750000000003);
#88615=CYLINDRICAL_SURFACE('',#104891,0.0220000000000002);
#88616=CYLINDRICAL_SURFACE('',#104898,0.0220000000000002);
#88617=CYLINDRICAL_SURFACE('',#104905,0.0343750000000003);
#88618=CYLINDRICAL_SURFACE('',#104912,0.0220000000000001);
#88619=CYLINDRICAL_SURFACE('',#104919,0.0220000000000001);
#88620=CYLINDRICAL_SURFACE('',#104926,0.0343750000000002);
#88621=CYLINDRICAL_SURFACE('',#104933,0.0219999999999998);
#88622=CYLINDRICAL_SURFACE('',#104940,0.0219999999999998);
#88623=CYLINDRICAL_SURFACE('',#104947,0.0343750000000003);
#88624=CYLINDRICAL_SURFACE('',#104954,0.0220000000000001);
#88625=CYLINDRICAL_SURFACE('',#104961,0.0220000000000001);
#88626=CYLINDRICAL_SURFACE('',#104968,0.0343750000000002);
#88627=CYLINDRICAL_SURFACE('',#104975,0.0219999999999998);
#88628=CYLINDRICAL_SURFACE('',#104982,0.0219999999999998);
#88629=CYLINDRICAL_SURFACE('',#104989,0.0343750000000002);
#88630=CYLINDRICAL_SURFACE('',#104996,0.0220000000000001);
#88631=CYLINDRICAL_SURFACE('',#105003,0.0220000000000001);
#88632=CYLINDRICAL_SURFACE('',#105010,0.0343750000000002);
#88633=CYLINDRICAL_SURFACE('',#105017,0.022);
#88634=CYLINDRICAL_SURFACE('',#105024,0.022);
#88635=CYLINDRICAL_SURFACE('',#105031,0.0343750000000002);
#88636=CYLINDRICAL_SURFACE('',#105038,0.0220000000000001);
#88637=CYLINDRICAL_SURFACE('',#105045,0.0220000000000001);
#88638=CYLINDRICAL_SURFACE('',#105052,0.0343750000000002);
#88639=CYLINDRICAL_SURFACE('',#105059,0.022);
#88640=CYLINDRICAL_SURFACE('',#105066,0.022);
#88641=CYLINDRICAL_SURFACE('',#105073,0.0343750000000003);
#88642=CYLINDRICAL_SURFACE('',#105080,0.0220000000000001);
#88643=CYLINDRICAL_SURFACE('',#105087,0.0220000000000001);
#88644=CYLINDRICAL_SURFACE('',#105094,0.0343750000000002);
#88645=CYLINDRICAL_SURFACE('',#105101,0.0220000000000001);
#88646=CYLINDRICAL_SURFACE('',#105108,0.0220000000000001);
#88647=CYLINDRICAL_SURFACE('',#105115,0.0343750000000003);
#88648=CYLINDRICAL_SURFACE('',#105122,0.0220000000000001);
#88649=CYLINDRICAL_SURFACE('',#105129,0.0220000000000001);
#88650=CYLINDRICAL_SURFACE('',#105136,0.0343750000000001);
#88651=CYLINDRICAL_SURFACE('',#105143,0.0219999999999999);
#88652=CYLINDRICAL_SURFACE('',#105150,0.0219999999999999);
#88653=CYLINDRICAL_SURFACE('',#105157,0.0343750000000003);
#88654=CYLINDRICAL_SURFACE('',#105164,0.0219999999999999);
#88655=CYLINDRICAL_SURFACE('',#105171,0.0219999999999999);
#92873=ADVANCED_FACE('',(#10409),#88351,.T.);
#92874=ADVANCED_FACE('',(#10410),#88352,.T.);
#92875=ADVANCED_FACE('',(#10411),#88353,.T.);
#92876=ADVANCED_FACE('',(#10412),#88354,.T.);
#92877=ADVANCED_FACE('',(#10413),#88355,.T.);
#92878=ADVANCED_FACE('',(#10414),#88356,.T.);
#92879=ADVANCED_FACE('',(#10415),#88357,.T.);
#92880=ADVANCED_FACE('',(#10416),#88358,.T.);
#92881=ADVANCED_FACE('',(#10417),#88359,.T.);
#92882=ADVANCED_FACE('',(#10418),#88360,.T.);
#92883=ADVANCED_FACE('',(#10419),#88361,.T.);
#92884=ADVANCED_FACE('',(#10420),#88362,.T.);
#92885=ADVANCED_FACE('',(#10421),#88363,.T.);
#92886=ADVANCED_FACE('',(#10422),#88364,.T.);
#92887=ADVANCED_FACE('',(#10423),#88365,.T.);
#92888=ADVANCED_FACE('',(#10424),#88366,.T.);
#92889=ADVANCED_FACE('',(#10425),#88367,.T.);
#92890=ADVANCED_FACE('',(#10426),#88368,.T.);
#92891=ADVANCED_FACE('',(#10427),#88369,.T.);
#92892=ADVANCED_FACE('',(#10428),#88370,.T.);
#92893=ADVANCED_FACE('',(#10429),#88371,.T.);
#92894=ADVANCED_FACE('',(#10430),#88372,.T.);
#92895=ADVANCED_FACE('',(#10431),#88373,.T.);
#92896=ADVANCED_FACE('',(#10432),#88374,.T.);
#92897=ADVANCED_FACE('',(#10433),#88375,.T.);
#92898=ADVANCED_FACE('',(#10434),#88376,.T.);
#92899=ADVANCED_FACE('',(#10435),#88377,.T.);
#92900=ADVANCED_FACE('',(#10436),#88378,.T.);
#92901=ADVANCED_FACE('',(#10437),#88379,.T.);
#92902=ADVANCED_FACE('',(#10438),#88380,.T.);
#92903=ADVANCED_FACE('',(#10439),#88381,.T.);
#92904=ADVANCED_FACE('',(#10440),#88382,.T.);
#92905=ADVANCED_FACE('',(#10441),#88383,.T.);
#92906=ADVANCED_FACE('',(#10442),#88384,.T.);
#92907=ADVANCED_FACE('',(#10443),#88385,.T.);
#92908=ADVANCED_FACE('',(#10444),#88386,.T.);
#92909=ADVANCED_FACE('',(#10445),#5014,.T.);
#92910=ADVANCED_FACE('',(#10446),#5015,.T.);
#92911=ADVANCED_FACE('',(#10447),#88387,.T.);
#92912=ADVANCED_FACE('',(#10448),#88388,.T.);
#92913=ADVANCED_FACE('',(#10449),#88389,.T.);
#92914=ADVANCED_FACE('',(#10450),#88390,.T.);
#92915=ADVANCED_FACE('',(#10451),#88391,.T.);
#92916=ADVANCED_FACE('',(#10452),#88392,.T.);
#92917=ADVANCED_FACE('',(#10453),#88393,.T.);
#92918=ADVANCED_FACE('',(#10454),#88394,.T.);
#92919=ADVANCED_FACE('',(#10455),#88395,.T.);
#92920=ADVANCED_FACE('',(#10456),#88396,.T.);
#92921=ADVANCED_FACE('',(#10457),#88397,.T.);
#92922=ADVANCED_FACE('',(#10458),#88398,.T.);
#92923=ADVANCED_FACE('',(#10459),#88399,.T.);
#92924=ADVANCED_FACE('',(#10460),#88400,.T.);
#92925=ADVANCED_FACE('',(#10461),#88401,.T.);
#92926=ADVANCED_FACE('',(#10462),#88402,.T.);
#92927=ADVANCED_FACE('',(#10463),#88403,.T.);
#92928=ADVANCED_FACE('',(#10464),#88404,.T.);
#92929=ADVANCED_FACE('',(#10465),#88405,.T.);
#92930=ADVANCED_FACE('',(#10466),#88406,.T.);
#92931=ADVANCED_FACE('',(#10467),#88407,.T.);
#92932=ADVANCED_FACE('',(#10468),#88408,.T.);
#92933=ADVANCED_FACE('',(#10469),#88409,.T.);
#92934=ADVANCED_FACE('',(#10470),#88410,.T.);
#92935=ADVANCED_FACE('',(#10471),#88411,.T.);
#92936=ADVANCED_FACE('',(#10472),#88412,.T.);
#92937=ADVANCED_FACE('',(#10473),#88413,.T.);
#92938=ADVANCED_FACE('',(#10474),#88414,.T.);
#92939=ADVANCED_FACE('',(#10475),#88415,.T.);
#92940=ADVANCED_FACE('',(#10476),#88416,.T.);
#92941=ADVANCED_FACE('',(#10477),#88417,.T.);
#92942=ADVANCED_FACE('',(#10478),#88418,.T.);
#92943=ADVANCED_FACE('',(#10479),#88419,.T.);
#92944=ADVANCED_FACE('',(#10480),#88420,.T.);
#92945=ADVANCED_FACE('',(#10481),#88421,.T.);
#92946=ADVANCED_FACE('',(#10482),#2064,.T.);
#92947=ADVANCED_FACE('',(#10483),#2065,.T.);
#92948=ADVANCED_FACE('',(#10484),#2066,.T.);
#92949=ADVANCED_FACE('',(#10485),#2067,.T.);
#92950=ADVANCED_FACE('',(#10486),#2068,.T.);
#92951=ADVANCED_FACE('',(#10487),#2069,.T.);
#92952=ADVANCED_FACE('',(#10488),#2070,.T.);
#92953=ADVANCED_FACE('',(#10489),#2071,.T.);
#92954=ADVANCED_FACE('',(#10490),#2072,.T.);
#92955=ADVANCED_FACE('',(#10491),#2073,.T.);
#92956=ADVANCED_FACE('',(#10492),#2074,.T.);
#92957=ADVANCED_FACE('',(#10493),#2075,.T.);
#92958=ADVANCED_FACE('',(#10494),#2076,.T.);
#92959=ADVANCED_FACE('',(#10495),#2077,.T.);
#92960=ADVANCED_FACE('',(#10496),#2078,.T.);
#92961=ADVANCED_FACE('',(#10497),#2079,.T.);
#92962=ADVANCED_FACE('',(#10498),#2080,.T.);
#92963=ADVANCED_FACE('',(#10499),#2081,.T.);
#92964=ADVANCED_FACE('',(#10500),#2082,.T.);
#92965=ADVANCED_FACE('',(#10501),#2083,.T.);
#92966=ADVANCED_FACE('',(#10502),#2084,.T.);
#92967=ADVANCED_FACE('',(#10503),#2085,.T.);
#92968=ADVANCED_FACE('',(#10504),#2086,.T.);
#92969=ADVANCED_FACE('',(#10505),#2087,.T.);
#92970=ADVANCED_FACE('',(#10506),#2088,.T.);
#92971=ADVANCED_FACE('',(#10507),#2089,.T.);
#92972=ADVANCED_FACE('',(#10508),#2090,.T.);
#92973=ADVANCED_FACE('',(#10509),#2091,.T.);
#92974=ADVANCED_FACE('',(#10510),#2092,.T.);
#92975=ADVANCED_FACE('',(#10511),#2093,.T.);
#92976=ADVANCED_FACE('',(#10512),#2094,.T.);
#92977=ADVANCED_FACE('',(#10513),#2095,.T.);
#92978=ADVANCED_FACE('',(#10514),#2096,.T.);
#92979=ADVANCED_FACE('',(#10515),#2097,.T.);
#92980=ADVANCED_FACE('',(#10516),#2098,.T.);
#92981=ADVANCED_FACE('',(#10517),#2099,.T.);
#92982=ADVANCED_FACE('',(#10518),#2100,.T.);
#92983=ADVANCED_FACE('',(#10519),#2101,.T.);
#92984=ADVANCED_FACE('',(#10520),#2102,.T.);
#92985=ADVANCED_FACE('',(#10521),#2103,.T.);
#92986=ADVANCED_FACE('',(#10522),#2104,.T.);
#92987=ADVANCED_FACE('',(#10523),#2105,.T.);
#92988=ADVANCED_FACE('',(#10524),#2106,.T.);
#92989=ADVANCED_FACE('',(#10525),#2107,.T.);
#92990=ADVANCED_FACE('',(#10526),#2108,.T.);
#92991=ADVANCED_FACE('',(#10527),#2109,.T.);
#92992=ADVANCED_FACE('',(#10528),#2110,.T.);
#92993=ADVANCED_FACE('',(#10529),#2111,.T.);
#92994=ADVANCED_FACE('',(#10530),#2112,.T.);
#92995=ADVANCED_FACE('',(#10531),#2113,.T.);
#92996=ADVANCED_FACE('',(#10532),#2114,.T.);
#92997=ADVANCED_FACE('',(#10533),#2115,.T.);
#92998=ADVANCED_FACE('',(#10534),#2116,.T.);
#92999=ADVANCED_FACE('',(#10535),#2117,.T.);
#93000=ADVANCED_FACE('',(#10536),#2118,.T.);
#93001=ADVANCED_FACE('',(#10537),#2119,.T.);
#93002=ADVANCED_FACE('',(#10538),#2120,.T.);
#93003=ADVANCED_FACE('',(#10539),#2121,.T.);
#93004=ADVANCED_FACE('',(#10540),#2122,.T.);
#93005=ADVANCED_FACE('',(#10541),#2123,.T.);
#93006=ADVANCED_FACE('',(#10542),#2124,.T.);
#93007=ADVANCED_FACE('',(#10543),#2125,.T.);
#93008=ADVANCED_FACE('',(#10544),#2126,.T.);
#93009=ADVANCED_FACE('',(#10545),#2127,.T.);
#93010=ADVANCED_FACE('',(#10546),#2128,.T.);
#93011=ADVANCED_FACE('',(#10547),#2129,.T.);
#93012=ADVANCED_FACE('',(#10548),#2130,.T.);
#93013=ADVANCED_FACE('',(#10549),#2131,.T.);
#93014=ADVANCED_FACE('',(#10550),#2132,.T.);
#93015=ADVANCED_FACE('',(#10551),#2133,.T.);
#93016=ADVANCED_FACE('',(#10552),#2134,.T.);
#93017=ADVANCED_FACE('',(#10553),#2135,.T.);
#93018=ADVANCED_FACE('',(#10554),#2136,.T.);
#93019=ADVANCED_FACE('',(#10555),#2137,.T.);
#93020=ADVANCED_FACE('',(#10556),#2138,.T.);
#93021=ADVANCED_FACE('',(#10557),#2139,.T.);
#93022=ADVANCED_FACE('',(#10558),#2140,.T.);
#93023=ADVANCED_FACE('',(#10559),#88422,.T.);
#93024=ADVANCED_FACE('',(#10560),#5016,.T.);
#93025=ADVANCED_FACE('',(#10561),#5017,.T.);
#93026=ADVANCED_FACE('',(#10562),#5018,.T.);
#93027=ADVANCED_FACE('',(#10563),#5019,.F.);
#93028=ADVANCED_FACE('',(#10564),#5020,.F.);
#93029=ADVANCED_FACE('',(#10565),#2141,.T.);
#93030=ADVANCED_FACE('',(#10566),#5021,.T.);
#93031=ADVANCED_FACE('',(#10567),#2142,.T.);
#93032=ADVANCED_FACE('',(#10568),#5022,.T.);
#93033=ADVANCED_FACE('',(#10569),#2143,.T.);
#93034=ADVANCED_FACE('',(#10570),#88423,.T.);
#93035=ADVANCED_FACE('',(#10571),#2144,.T.);
#93036=ADVANCED_FACE('',(#10572),#2145,.T.);
#93037=ADVANCED_FACE('',(#10573),#2146,.T.);
#93038=ADVANCED_FACE('',(#10574),#2147,.T.);
#93039=ADVANCED_FACE('',(#10575),#2148,.T.);
#93040=ADVANCED_FACE('',(#10576),#2149,.T.);
#93041=ADVANCED_FACE('',(#10577),#2150,.T.);
#93042=ADVANCED_FACE('',(#10578),#2151,.T.);
#93043=ADVANCED_FACE('',(#10579),#2152,.T.);
#93044=ADVANCED_FACE('',(#10580),#2153,.T.);
#93045=ADVANCED_FACE('',(#10581),#2154,.T.);
#93046=ADVANCED_FACE('',(#10582),#2155,.T.);
#93047=ADVANCED_FACE('',(#10583),#2156,.T.);
#93048=ADVANCED_FACE('',(#10584),#2157,.T.);
#93049=ADVANCED_FACE('',(#10585),#2158,.T.);
#93050=ADVANCED_FACE('',(#10586),#2159,.T.);
#93051=ADVANCED_FACE('',(#10587),#2160,.T.);
#93052=ADVANCED_FACE('',(#10588),#2161,.T.);
#93053=ADVANCED_FACE('',(#10589),#2162,.T.);
#93054=ADVANCED_FACE('',(#10590),#2163,.T.);
#93055=ADVANCED_FACE('',(#10591),#2164,.T.);
#93056=ADVANCED_FACE('',(#10592),#2165,.T.);
#93057=ADVANCED_FACE('',(#10593),#2166,.T.);
#93058=ADVANCED_FACE('',(#10594),#2167,.T.);
#93059=ADVANCED_FACE('',(#10595),#2168,.T.);
#93060=ADVANCED_FACE('',(#10596),#2169,.T.);
#93061=ADVANCED_FACE('',(#10597),#2170,.T.);
#93062=ADVANCED_FACE('',(#10598),#2171,.T.);
#93063=ADVANCED_FACE('',(#10599),#2172,.T.);
#93064=ADVANCED_FACE('',(#10600),#2173,.T.);
#93065=ADVANCED_FACE('',(#10601),#2174,.T.);
#93066=ADVANCED_FACE('',(#10602),#2175,.T.);
#93067=ADVANCED_FACE('',(#10603),#2176,.T.);
#93068=ADVANCED_FACE('',(#10604),#2177,.T.);
#93069=ADVANCED_FACE('',(#10605),#2178,.T.);
#93070=ADVANCED_FACE('',(#10606),#2179,.T.);
#93071=ADVANCED_FACE('',(#10607),#2180,.T.);
#93072=ADVANCED_FACE('',(#10608),#2181,.T.);
#93073=ADVANCED_FACE('',(#10609),#2182,.T.);
#93074=ADVANCED_FACE('',(#10610),#2183,.T.);
#93075=ADVANCED_FACE('',(#10611),#2184,.T.);
#93076=ADVANCED_FACE('',(#10612),#2185,.T.);
#93077=ADVANCED_FACE('',(#10613),#2186,.T.);
#93078=ADVANCED_FACE('',(#10614),#2187,.T.);
#93079=ADVANCED_FACE('',(#10615),#2188,.T.);
#93080=ADVANCED_FACE('',(#10616),#2189,.T.);
#93081=ADVANCED_FACE('',(#10617),#2190,.T.);
#93082=ADVANCED_FACE('',(#10618),#2191,.T.);
#93083=ADVANCED_FACE('',(#10619),#2192,.T.);
#93084=ADVANCED_FACE('',(#10620),#2193,.T.);
#93085=ADVANCED_FACE('',(#10621),#2194,.T.);
#93086=ADVANCED_FACE('',(#10622),#2195,.T.);
#93087=ADVANCED_FACE('',(#10623),#2196,.T.);
#93088=ADVANCED_FACE('',(#10624),#2197,.T.);
#93089=ADVANCED_FACE('',(#10625),#2198,.T.);
#93090=ADVANCED_FACE('',(#10626),#2199,.T.);
#93091=ADVANCED_FACE('',(#10627),#2200,.T.);
#93092=ADVANCED_FACE('',(#10628),#2201,.T.);
#93093=ADVANCED_FACE('',(#10629),#2202,.T.);
#93094=ADVANCED_FACE('',(#10630),#2203,.T.);
#93095=ADVANCED_FACE('',(#10631),#2204,.T.);
#93096=ADVANCED_FACE('',(#10632),#2205,.T.);
#93097=ADVANCED_FACE('',(#10633),#2206,.T.);
#93098=ADVANCED_FACE('',(#10634),#2207,.T.);
#93099=ADVANCED_FACE('',(#10635),#2208,.T.);
#93100=ADVANCED_FACE('',(#10636),#2209,.T.);
#93101=ADVANCED_FACE('',(#10637),#2210,.T.);
#93102=ADVANCED_FACE('',(#10638),#2211,.T.);
#93103=ADVANCED_FACE('',(#10639),#2212,.T.);
#93104=ADVANCED_FACE('',(#10640),#2213,.T.);
#93105=ADVANCED_FACE('',(#10641),#2214,.T.);
#93106=ADVANCED_FACE('',(#10642),#2215,.T.);
#93107=ADVANCED_FACE('',(#10643),#2216,.T.);
#93108=ADVANCED_FACE('',(#10644),#2217,.T.);
#93109=ADVANCED_FACE('',(#10645),#2218,.T.);
#93110=ADVANCED_FACE('',(#10646),#2219,.T.);
#93111=ADVANCED_FACE('',(#10647),#88424,.F.);
#93112=ADVANCED_FACE('',(#10648),#5937,.F.);
#93113=ADVANCED_FACE('',(#10649),#5938,.F.);
#93114=ADVANCED_FACE('',(#10650,#5228),#5939,.F.);
#93115=ADVANCED_FACE('',(#10651),#5940,.F.);
#93116=ADVANCED_FACE('',(#10652),#5941,.F.);
#93117=ADVANCED_FACE('',(#10653),#5942,.F.);
#93118=ADVANCED_FACE('',(#10654),#5943,.F.);
#93119=ADVANCED_FACE('',(#10655),#5944,.F.);
#93120=ADVANCED_FACE('',(#10656,#5229),#5945,.F.);
#93121=ADVANCED_FACE('',(#10657),#2220,.T.);
#93122=ADVANCED_FACE('',(#10658),#5946,.F.);
#93123=ADVANCED_FACE('',(#10659),#5947,.F.);
#93124=ADVANCED_FACE('',(#10660),#5948,.F.);
#93125=ADVANCED_FACE('',(#10661),#5949,.F.);
#93126=ADVANCED_FACE('',(#10662),#5950,.F.);
#93127=ADVANCED_FACE('',(#10663),#5951,.F.);
#93128=ADVANCED_FACE('',(#10664),#5952,.F.);
#93129=ADVANCED_FACE('',(#10665),#5023,.F.);
#93130=ADVANCED_FACE('',(#10666),#5024,.F.);
#93131=ADVANCED_FACE('',(#10667),#5025,.F.);
#93132=ADVANCED_FACE('',(#10668),#5026,.F.);
#93133=ADVANCED_FACE('',(#10669),#5027,.F.);
#93134=ADVANCED_FACE('',(#10670),#5953,.F.);
#93135=ADVANCED_FACE('',(#10671),#3301,.T.);
#93136=ADVANCED_FACE('',(#10672),#88425,.T.);
#93137=ADVANCED_FACE('',(#10673),#3302,.T.);
#93138=ADVANCED_FACE('',(#10674),#5028,.T.);
#93139=ADVANCED_FACE('',(#10675),#3303,.F.);
#93140=ADVANCED_FACE('',(#10676),#88426,.T.);
#93141=ADVANCED_FACE('',(#10677),#3304,.F.);
#93142=ADVANCED_FACE('',(#10678),#3305,.T.);
#93143=ADVANCED_FACE('',(#10679),#3306,.T.);
#93144=ADVANCED_FACE('',(#10680),#3307,.F.);
#93145=ADVANCED_FACE('',(#10681),#3308,.T.);
#93146=ADVANCED_FACE('',(#10682),#3309,.T.);
#93147=ADVANCED_FACE('',(#10683),#3310,.T.);
#93148=ADVANCED_FACE('',(#10684),#88427,.T.);
#93149=ADVANCED_FACE('',(#10685),#3311,.T.);
#93150=ADVANCED_FACE('',(#10686),#3312,.T.);
#93151=ADVANCED_FACE('',(#10687),#5954,.F.);
#93152=ADVANCED_FACE('',(#10688),#5955,.F.);
#93153=ADVANCED_FACE('',(#10689),#88428,.F.);
#93154=ADVANCED_FACE('',(#10690),#3313,.F.);
#93155=ADVANCED_FACE('',(#10691),#3314,.F.);
#93156=ADVANCED_FACE('',(#10692),#3315,.F.);
#93157=ADVANCED_FACE('',(#10693),#3316,.T.);
#93158=ADVANCED_FACE('',(#10694),#88429,.T.);
#93159=ADVANCED_FACE('',(#10695),#3317,.T.);
#93160=ADVANCED_FACE('',(#10696),#3318,.T.);
#93161=ADVANCED_FACE('',(#10697),#3319,.T.);
#93162=ADVANCED_FACE('',(#10698),#3320,.T.);
#93163=ADVANCED_FACE('',(#10699),#3321,.T.);
#93164=ADVANCED_FACE('',(#10700),#88430,.T.);
#93165=ADVANCED_FACE('',(#10701),#3322,.T.);
#93166=ADVANCED_FACE('',(#10702),#5029,.T.);
#93167=ADVANCED_FACE('',(#10703),#5956,.F.);
#93168=ADVANCED_FACE('',(#10704),#5957,.F.);
#93169=ADVANCED_FACE('',(#10705),#88431,.F.);
#93170=ADVANCED_FACE('',(#10706),#3323,.F.);
#93171=ADVANCED_FACE('',(#10707),#3324,.F.);
#93172=ADVANCED_FACE('',(#10708),#3325,.F.);
#93173=ADVANCED_FACE('',(#10709),#3326,.T.);
#93174=ADVANCED_FACE('',(#10710),#88432,.T.);
#93175=ADVANCED_FACE('',(#10711),#3327,.T.);
#93176=ADVANCED_FACE('',(#10712),#3328,.T.);
#93177=ADVANCED_FACE('',(#10713),#3329,.T.);
#93178=ADVANCED_FACE('',(#10714),#3330,.T.);
#93179=ADVANCED_FACE('',(#10715),#3331,.T.);
#93180=ADVANCED_FACE('',(#10716),#88433,.T.);
#93181=ADVANCED_FACE('',(#10717),#3332,.T.);
#93182=ADVANCED_FACE('',(#10718),#5030,.T.);
#93183=ADVANCED_FACE('',(#10719),#5958,.F.);
#93184=ADVANCED_FACE('',(#10720),#5959,.F.);
#93185=ADVANCED_FACE('',(#10721),#88434,.F.);
#93186=ADVANCED_FACE('',(#10722),#3333,.F.);
#93187=ADVANCED_FACE('',(#10723),#3334,.F.);
#93188=ADVANCED_FACE('',(#10724),#3335,.F.);
#93189=ADVANCED_FACE('',(#10725),#3336,.T.);
#93190=ADVANCED_FACE('',(#10726),#88435,.T.);
#93191=ADVANCED_FACE('',(#10727),#3337,.T.);
#93192=ADVANCED_FACE('',(#10728),#3338,.T.);
#93193=ADVANCED_FACE('',(#10729),#3339,.T.);
#93194=ADVANCED_FACE('',(#10730),#3340,.T.);
#93195=ADVANCED_FACE('',(#10731),#3341,.T.);
#93196=ADVANCED_FACE('',(#10732),#88436,.T.);
#93197=ADVANCED_FACE('',(#10733),#3342,.T.);
#93198=ADVANCED_FACE('',(#10734),#5031,.T.);
#93199=ADVANCED_FACE('',(#10735),#5960,.F.);
#93200=ADVANCED_FACE('',(#10736),#5961,.F.);
#93201=ADVANCED_FACE('',(#10737),#88437,.F.);
#93202=ADVANCED_FACE('',(#10738),#3343,.F.);
#93203=ADVANCED_FACE('',(#10739),#3344,.F.);
#93204=ADVANCED_FACE('',(#10740),#3345,.F.);
#93205=ADVANCED_FACE('',(#10741),#3346,.T.);
#93206=ADVANCED_FACE('',(#10742),#88438,.T.);
#93207=ADVANCED_FACE('',(#10743),#3347,.T.);
#93208=ADVANCED_FACE('',(#10744),#3348,.T.);
#93209=ADVANCED_FACE('',(#10745),#3349,.T.);
#93210=ADVANCED_FACE('',(#10746),#3350,.T.);
#93211=ADVANCED_FACE('',(#10747),#3351,.T.);
#93212=ADVANCED_FACE('',(#10748),#88439,.T.);
#93213=ADVANCED_FACE('',(#10749),#3352,.T.);
#93214=ADVANCED_FACE('',(#10750),#5032,.T.);
#93215=ADVANCED_FACE('',(#10751),#5962,.F.);
#93216=ADVANCED_FACE('',(#10752),#5963,.F.);
#93217=ADVANCED_FACE('',(#10753),#88440,.F.);
#93218=ADVANCED_FACE('',(#10754),#3353,.F.);
#93219=ADVANCED_FACE('',(#10755),#3354,.F.);
#93220=ADVANCED_FACE('',(#10756),#3355,.F.);
#93221=ADVANCED_FACE('',(#10757),#3356,.T.);
#93222=ADVANCED_FACE('',(#10758),#88441,.T.);
#93223=ADVANCED_FACE('',(#10759),#3357,.T.);
#93224=ADVANCED_FACE('',(#10760),#3358,.T.);
#93225=ADVANCED_FACE('',(#10761),#3359,.T.);
#93226=ADVANCED_FACE('',(#10762),#3360,.T.);
#93227=ADVANCED_FACE('',(#10763),#3361,.T.);
#93228=ADVANCED_FACE('',(#10764),#88442,.T.);
#93229=ADVANCED_FACE('',(#10765),#3362,.T.);
#93230=ADVANCED_FACE('',(#10766),#5033,.T.);
#93231=ADVANCED_FACE('',(#10767),#5964,.F.);
#93232=ADVANCED_FACE('',(#10768),#5965,.F.);
#93233=ADVANCED_FACE('',(#10769),#88443,.F.);
#93234=ADVANCED_FACE('',(#10770),#3363,.F.);
#93235=ADVANCED_FACE('',(#10771),#3364,.F.);
#93236=ADVANCED_FACE('',(#10772),#3365,.F.);
#93237=ADVANCED_FACE('',(#10773),#3366,.T.);
#93238=ADVANCED_FACE('',(#10774),#88444,.T.);
#93239=ADVANCED_FACE('',(#10775),#3367,.T.);
#93240=ADVANCED_FACE('',(#10776),#3368,.T.);
#93241=ADVANCED_FACE('',(#10777),#3369,.T.);
#93242=ADVANCED_FACE('',(#10778),#3370,.T.);
#93243=ADVANCED_FACE('',(#10779),#3371,.T.);
#93244=ADVANCED_FACE('',(#10780),#88445,.T.);
#93245=ADVANCED_FACE('',(#10781),#3372,.T.);
#93246=ADVANCED_FACE('',(#10782),#5034,.T.);
#93247=ADVANCED_FACE('',(#10783),#5966,.F.);
#93248=ADVANCED_FACE('',(#10784),#5967,.F.);
#93249=ADVANCED_FACE('',(#10785),#88446,.F.);
#93250=ADVANCED_FACE('',(#10786),#3373,.F.);
#93251=ADVANCED_FACE('',(#10787),#3374,.F.);
#93252=ADVANCED_FACE('',(#10788),#3375,.F.);
#93253=ADVANCED_FACE('',(#10789),#3376,.T.);
#93254=ADVANCED_FACE('',(#10790),#88447,.T.);
#93255=ADVANCED_FACE('',(#10791),#3377,.T.);
#93256=ADVANCED_FACE('',(#10792),#3378,.T.);
#93257=ADVANCED_FACE('',(#10793),#3379,.T.);
#93258=ADVANCED_FACE('',(#10794),#3380,.T.);
#93259=ADVANCED_FACE('',(#10795),#3381,.T.);
#93260=ADVANCED_FACE('',(#10796),#88448,.T.);
#93261=ADVANCED_FACE('',(#10797),#3382,.T.);
#93262=ADVANCED_FACE('',(#10798),#5035,.T.);
#93263=ADVANCED_FACE('',(#10799),#5968,.F.);
#93264=ADVANCED_FACE('',(#10800),#5969,.F.);
#93265=ADVANCED_FACE('',(#10801),#88449,.F.);
#93266=ADVANCED_FACE('',(#10802),#3383,.F.);
#93267=ADVANCED_FACE('',(#10803),#3384,.F.);
#93268=ADVANCED_FACE('',(#10804),#3385,.F.);
#93269=ADVANCED_FACE('',(#10805),#3386,.T.);
#93270=ADVANCED_FACE('',(#10806),#88450,.T.);
#93271=ADVANCED_FACE('',(#10807),#3387,.T.);
#93272=ADVANCED_FACE('',(#10808),#3388,.T.);
#93273=ADVANCED_FACE('',(#10809),#3389,.T.);
#93274=ADVANCED_FACE('',(#10810),#3390,.T.);
#93275=ADVANCED_FACE('',(#10811),#3391,.T.);
#93276=ADVANCED_FACE('',(#10812),#88451,.T.);
#93277=ADVANCED_FACE('',(#10813),#3392,.T.);
#93278=ADVANCED_FACE('',(#10814),#5036,.T.);
#93279=ADVANCED_FACE('',(#10815),#5970,.F.);
#93280=ADVANCED_FACE('',(#10816),#5971,.F.);
#93281=ADVANCED_FACE('',(#10817),#88452,.F.);
#93282=ADVANCED_FACE('',(#10818),#3393,.F.);
#93283=ADVANCED_FACE('',(#10819),#3394,.F.);
#93284=ADVANCED_FACE('',(#10820),#3395,.F.);
#93285=ADVANCED_FACE('',(#10821),#3396,.T.);
#93286=ADVANCED_FACE('',(#10822),#88453,.T.);
#93287=ADVANCED_FACE('',(#10823),#3397,.T.);
#93288=ADVANCED_FACE('',(#10824),#3398,.T.);
#93289=ADVANCED_FACE('',(#10825),#3399,.T.);
#93290=ADVANCED_FACE('',(#10826),#3400,.T.);
#93291=ADVANCED_FACE('',(#10827),#3401,.T.);
#93292=ADVANCED_FACE('',(#10828),#88454,.T.);
#93293=ADVANCED_FACE('',(#10829),#3402,.T.);
#93294=ADVANCED_FACE('',(#10830),#5037,.T.);
#93295=ADVANCED_FACE('',(#10831),#5972,.F.);
#93296=ADVANCED_FACE('',(#10832),#5973,.F.);
#93297=ADVANCED_FACE('',(#10833),#88455,.F.);
#93298=ADVANCED_FACE('',(#10834),#3403,.F.);
#93299=ADVANCED_FACE('',(#10835),#3404,.F.);
#93300=ADVANCED_FACE('',(#10836),#3405,.F.);
#93301=ADVANCED_FACE('',(#10837),#3406,.T.);
#93302=ADVANCED_FACE('',(#10838),#88456,.T.);
#93303=ADVANCED_FACE('',(#10839),#3407,.T.);
#93304=ADVANCED_FACE('',(#10840),#3408,.T.);
#93305=ADVANCED_FACE('',(#10841),#3409,.T.);
#93306=ADVANCED_FACE('',(#10842),#3410,.T.);
#93307=ADVANCED_FACE('',(#10843),#3411,.T.);
#93308=ADVANCED_FACE('',(#10844),#88457,.T.);
#93309=ADVANCED_FACE('',(#10845),#3412,.T.);
#93310=ADVANCED_FACE('',(#10846),#5038,.T.);
#93311=ADVANCED_FACE('',(#10847),#5974,.F.);
#93312=ADVANCED_FACE('',(#10848),#5975,.F.);
#93313=ADVANCED_FACE('',(#10849),#88458,.F.);
#93314=ADVANCED_FACE('',(#10850),#3413,.F.);
#93315=ADVANCED_FACE('',(#10851),#3414,.F.);
#93316=ADVANCED_FACE('',(#10852),#3415,.F.);
#93317=ADVANCED_FACE('',(#10853),#3416,.T.);
#93318=ADVANCED_FACE('',(#10854),#88459,.T.);
#93319=ADVANCED_FACE('',(#10855),#3417,.T.);
#93320=ADVANCED_FACE('',(#10856),#3418,.T.);
#93321=ADVANCED_FACE('',(#10857),#3419,.T.);
#93322=ADVANCED_FACE('',(#10858),#3420,.T.);
#93323=ADVANCED_FACE('',(#10859),#3421,.T.);
#93324=ADVANCED_FACE('',(#10860),#88460,.T.);
#93325=ADVANCED_FACE('',(#10861),#3422,.T.);
#93326=ADVANCED_FACE('',(#10862),#5039,.T.);
#93327=ADVANCED_FACE('',(#10863),#5976,.F.);
#93328=ADVANCED_FACE('',(#10864),#5977,.F.);
#93329=ADVANCED_FACE('',(#10865),#88461,.F.);
#93330=ADVANCED_FACE('',(#10866),#3423,.F.);
#93331=ADVANCED_FACE('',(#10867),#3424,.F.);
#93332=ADVANCED_FACE('',(#10868),#3425,.F.);
#93333=ADVANCED_FACE('',(#10869),#3426,.T.);
#93334=ADVANCED_FACE('',(#10870),#88462,.T.);
#93335=ADVANCED_FACE('',(#10871),#3427,.T.);
#93336=ADVANCED_FACE('',(#10872),#3428,.T.);
#93337=ADVANCED_FACE('',(#10873),#3429,.T.);
#93338=ADVANCED_FACE('',(#10874),#3430,.T.);
#93339=ADVANCED_FACE('',(#10875),#3431,.T.);
#93340=ADVANCED_FACE('',(#10876),#88463,.T.);
#93341=ADVANCED_FACE('',(#10877),#3432,.T.);
#93342=ADVANCED_FACE('',(#10878),#5040,.T.);
#93343=ADVANCED_FACE('',(#10879),#5978,.F.);
#93344=ADVANCED_FACE('',(#10880),#5979,.F.);
#93345=ADVANCED_FACE('',(#10881),#88464,.F.);
#93346=ADVANCED_FACE('',(#10882),#3433,.F.);
#93347=ADVANCED_FACE('',(#10883),#3434,.F.);
#93348=ADVANCED_FACE('',(#10884),#3435,.F.);
#93349=ADVANCED_FACE('',(#10885),#3436,.T.);
#93350=ADVANCED_FACE('',(#10886),#88465,.T.);
#93351=ADVANCED_FACE('',(#10887),#3437,.T.);
#93352=ADVANCED_FACE('',(#10888),#3438,.T.);
#93353=ADVANCED_FACE('',(#10889),#3439,.T.);
#93354=ADVANCED_FACE('',(#10890),#3440,.T.);
#93355=ADVANCED_FACE('',(#10891),#3441,.T.);
#93356=ADVANCED_FACE('',(#10892),#88466,.T.);
#93357=ADVANCED_FACE('',(#10893),#3442,.T.);
#93358=ADVANCED_FACE('',(#10894),#5041,.T.);
#93359=ADVANCED_FACE('',(#10895),#5980,.F.);
#93360=ADVANCED_FACE('',(#10896),#5981,.F.);
#93361=ADVANCED_FACE('',(#10897),#88467,.F.);
#93362=ADVANCED_FACE('',(#10898),#3443,.F.);
#93363=ADVANCED_FACE('',(#10899),#3444,.F.);
#93364=ADVANCED_FACE('',(#10900),#3445,.F.);
#93365=ADVANCED_FACE('',(#10901),#3446,.T.);
#93366=ADVANCED_FACE('',(#10902),#88468,.T.);
#93367=ADVANCED_FACE('',(#10903),#3447,.T.);
#93368=ADVANCED_FACE('',(#10904),#3448,.T.);
#93369=ADVANCED_FACE('',(#10905),#3449,.T.);
#93370=ADVANCED_FACE('',(#10906),#3450,.T.);
#93371=ADVANCED_FACE('',(#10907),#3451,.T.);
#93372=ADVANCED_FACE('',(#10908),#88469,.T.);
#93373=ADVANCED_FACE('',(#10909),#3452,.T.);
#93374=ADVANCED_FACE('',(#10910),#5042,.T.);
#93375=ADVANCED_FACE('',(#10911),#5982,.F.);
#93376=ADVANCED_FACE('',(#10912),#5983,.F.);
#93377=ADVANCED_FACE('',(#10913),#88470,.F.);
#93378=ADVANCED_FACE('',(#10914),#3453,.F.);
#93379=ADVANCED_FACE('',(#10915),#3454,.F.);
#93380=ADVANCED_FACE('',(#10916),#3455,.F.);
#93381=ADVANCED_FACE('',(#10917),#3456,.T.);
#93382=ADVANCED_FACE('',(#10918),#88471,.T.);
#93383=ADVANCED_FACE('',(#10919),#3457,.T.);
#93384=ADVANCED_FACE('',(#10920),#3458,.T.);
#93385=ADVANCED_FACE('',(#10921),#3459,.T.);
#93386=ADVANCED_FACE('',(#10922),#3460,.T.);
#93387=ADVANCED_FACE('',(#10923),#3461,.T.);
#93388=ADVANCED_FACE('',(#10924),#88472,.T.);
#93389=ADVANCED_FACE('',(#10925),#3462,.T.);
#93390=ADVANCED_FACE('',(#10926),#5043,.T.);
#93391=ADVANCED_FACE('',(#10927),#5984,.F.);
#93392=ADVANCED_FACE('',(#10928),#5985,.F.);
#93393=ADVANCED_FACE('',(#10929),#88473,.F.);
#93394=ADVANCED_FACE('',(#10930),#3463,.F.);
#93395=ADVANCED_FACE('',(#10931),#3464,.F.);
#93396=ADVANCED_FACE('',(#10932),#3465,.F.);
#93397=ADVANCED_FACE('',(#10933),#3466,.T.);
#93398=ADVANCED_FACE('',(#10934),#88474,.T.);
#93399=ADVANCED_FACE('',(#10935),#3467,.T.);
#93400=ADVANCED_FACE('',(#10936),#3468,.T.);
#93401=ADVANCED_FACE('',(#10937),#3469,.T.);
#93402=ADVANCED_FACE('',(#10938),#3470,.T.);
#93403=ADVANCED_FACE('',(#10939),#3471,.T.);
#93404=ADVANCED_FACE('',(#10940),#88475,.T.);
#93405=ADVANCED_FACE('',(#10941),#3472,.T.);
#93406=ADVANCED_FACE('',(#10942),#5044,.T.);
#93407=ADVANCED_FACE('',(#10943),#5986,.F.);
#93408=ADVANCED_FACE('',(#10944),#5987,.F.);
#93409=ADVANCED_FACE('',(#10945),#88476,.F.);
#93410=ADVANCED_FACE('',(#10946),#3473,.F.);
#93411=ADVANCED_FACE('',(#10947),#3474,.F.);
#93412=ADVANCED_FACE('',(#10948),#3475,.F.);
#93413=ADVANCED_FACE('',(#10949),#3476,.T.);
#93414=ADVANCED_FACE('',(#10950),#88477,.T.);
#93415=ADVANCED_FACE('',(#10951),#3477,.T.);
#93416=ADVANCED_FACE('',(#10952),#3478,.T.);
#93417=ADVANCED_FACE('',(#10953),#3479,.T.);
#93418=ADVANCED_FACE('',(#10954),#3480,.T.);
#93419=ADVANCED_FACE('',(#10955),#3481,.T.);
#93420=ADVANCED_FACE('',(#10956),#88478,.T.);
#93421=ADVANCED_FACE('',(#10957),#3482,.T.);
#93422=ADVANCED_FACE('',(#10958),#5045,.T.);
#93423=ADVANCED_FACE('',(#10959),#5988,.F.);
#93424=ADVANCED_FACE('',(#10960),#5989,.F.);
#93425=ADVANCED_FACE('',(#10961),#88479,.F.);
#93426=ADVANCED_FACE('',(#10962),#3483,.F.);
#93427=ADVANCED_FACE('',(#10963),#3484,.F.);
#93428=ADVANCED_FACE('',(#10964),#3485,.F.);
#93429=ADVANCED_FACE('',(#10965),#3486,.T.);
#93430=ADVANCED_FACE('',(#10966),#88480,.T.);
#93431=ADVANCED_FACE('',(#10967),#3487,.T.);
#93432=ADVANCED_FACE('',(#10968),#3488,.T.);
#93433=ADVANCED_FACE('',(#10969),#3489,.T.);
#93434=ADVANCED_FACE('',(#10970),#3490,.T.);
#93435=ADVANCED_FACE('',(#10971),#3491,.T.);
#93436=ADVANCED_FACE('',(#10972),#88481,.T.);
#93437=ADVANCED_FACE('',(#10973),#3492,.T.);
#93438=ADVANCED_FACE('',(#10974),#5046,.T.);
#93439=ADVANCED_FACE('',(#10975),#5990,.F.);
#93440=ADVANCED_FACE('',(#10976),#5991,.F.);
#93441=ADVANCED_FACE('',(#10977),#88482,.F.);
#93442=ADVANCED_FACE('',(#10978),#3493,.F.);
#93443=ADVANCED_FACE('',(#10979),#3494,.F.);
#93444=ADVANCED_FACE('',(#10980),#3495,.F.);
#93445=ADVANCED_FACE('',(#10981),#3496,.T.);
#93446=ADVANCED_FACE('',(#10982),#88483,.T.);
#93447=ADVANCED_FACE('',(#10983),#3497,.T.);
#93448=ADVANCED_FACE('',(#10984),#3498,.T.);
#93449=ADVANCED_FACE('',(#10985),#3499,.T.);
#93450=ADVANCED_FACE('',(#10986),#3500,.T.);
#93451=ADVANCED_FACE('',(#10987),#3501,.T.);
#93452=ADVANCED_FACE('',(#10988),#88484,.T.);
#93453=ADVANCED_FACE('',(#10989),#3502,.T.);
#93454=ADVANCED_FACE('',(#10990),#5047,.T.);
#93455=ADVANCED_FACE('',(#10991),#5992,.F.);
#93456=ADVANCED_FACE('',(#10992),#5993,.F.);
#93457=ADVANCED_FACE('',(#10993),#88485,.F.);
#93458=ADVANCED_FACE('',(#10994),#3503,.F.);
#93459=ADVANCED_FACE('',(#10995),#3504,.F.);
#93460=ADVANCED_FACE('',(#10996),#3505,.F.);
#93461=ADVANCED_FACE('',(#10997),#3506,.T.);
#93462=ADVANCED_FACE('',(#10998),#88486,.T.);
#93463=ADVANCED_FACE('',(#10999),#3507,.T.);
#93464=ADVANCED_FACE('',(#11000),#3508,.T.);
#93465=ADVANCED_FACE('',(#11001),#3509,.T.);
#93466=ADVANCED_FACE('',(#11002),#3510,.T.);
#93467=ADVANCED_FACE('',(#11003),#3511,.T.);
#93468=ADVANCED_FACE('',(#11004),#88487,.T.);
#93469=ADVANCED_FACE('',(#11005),#3512,.T.);
#93470=ADVANCED_FACE('',(#11006),#5048,.T.);
#93471=ADVANCED_FACE('',(#11007),#5994,.F.);
#93472=ADVANCED_FACE('',(#11008),#5995,.F.);
#93473=ADVANCED_FACE('',(#11009),#88488,.F.);
#93474=ADVANCED_FACE('',(#11010),#3513,.F.);
#93475=ADVANCED_FACE('',(#11011),#3514,.F.);
#93476=ADVANCED_FACE('',(#11012),#3515,.F.);
#93477=ADVANCED_FACE('',(#11013),#3516,.T.);
#93478=ADVANCED_FACE('',(#11014),#88489,.T.);
#93479=ADVANCED_FACE('',(#11015),#3517,.T.);
#93480=ADVANCED_FACE('',(#11016),#3518,.T.);
#93481=ADVANCED_FACE('',(#11017),#3519,.T.);
#93482=ADVANCED_FACE('',(#11018),#3520,.T.);
#93483=ADVANCED_FACE('',(#11019),#3521,.T.);
#93484=ADVANCED_FACE('',(#11020),#88490,.T.);
#93485=ADVANCED_FACE('',(#11021),#3522,.T.);
#93486=ADVANCED_FACE('',(#11022),#5049,.T.);
#93487=ADVANCED_FACE('',(#11023),#5996,.F.);
#93488=ADVANCED_FACE('',(#11024),#5997,.F.);
#93489=ADVANCED_FACE('',(#11025),#88491,.F.);
#93490=ADVANCED_FACE('',(#11026),#3523,.F.);
#93491=ADVANCED_FACE('',(#11027),#3524,.F.);
#93492=ADVANCED_FACE('',(#11028),#3525,.F.);
#93493=ADVANCED_FACE('',(#11029),#3526,.T.);
#93494=ADVANCED_FACE('',(#11030),#88492,.T.);
#93495=ADVANCED_FACE('',(#11031),#3527,.T.);
#93496=ADVANCED_FACE('',(#11032),#3528,.T.);
#93497=ADVANCED_FACE('',(#11033),#3529,.T.);
#93498=ADVANCED_FACE('',(#11034),#3530,.T.);
#93499=ADVANCED_FACE('',(#11035),#3531,.T.);
#93500=ADVANCED_FACE('',(#11036),#88493,.T.);
#93501=ADVANCED_FACE('',(#11037),#3532,.T.);
#93502=ADVANCED_FACE('',(#11038),#5050,.T.);
#93503=ADVANCED_FACE('',(#11039),#5998,.F.);
#93504=ADVANCED_FACE('',(#11040),#5999,.F.);
#93505=ADVANCED_FACE('',(#11041),#88494,.F.);
#93506=ADVANCED_FACE('',(#11042),#3533,.F.);
#93507=ADVANCED_FACE('',(#11043),#3534,.F.);
#93508=ADVANCED_FACE('',(#11044),#3535,.F.);
#93509=ADVANCED_FACE('',(#11045),#3536,.T.);
#93510=ADVANCED_FACE('',(#11046),#88495,.T.);
#93511=ADVANCED_FACE('',(#11047),#3537,.T.);
#93512=ADVANCED_FACE('',(#11048),#3538,.T.);
#93513=ADVANCED_FACE('',(#11049),#3539,.T.);
#93514=ADVANCED_FACE('',(#11050),#3540,.T.);
#93515=ADVANCED_FACE('',(#11051),#3541,.T.);
#93516=ADVANCED_FACE('',(#11052),#88496,.T.);
#93517=ADVANCED_FACE('',(#11053),#3542,.T.);
#93518=ADVANCED_FACE('',(#11054),#5051,.T.);
#93519=ADVANCED_FACE('',(#11055),#6000,.F.);
#93520=ADVANCED_FACE('',(#11056),#6001,.F.);
#93521=ADVANCED_FACE('',(#11057),#88497,.F.);
#93522=ADVANCED_FACE('',(#11058),#3543,.F.);
#93523=ADVANCED_FACE('',(#11059),#3544,.F.);
#93524=ADVANCED_FACE('',(#11060),#3545,.F.);
#93525=ADVANCED_FACE('',(#11061),#3546,.T.);
#93526=ADVANCED_FACE('',(#11062),#88498,.T.);
#93527=ADVANCED_FACE('',(#11063),#3547,.T.);
#93528=ADVANCED_FACE('',(#11064),#3548,.T.);
#93529=ADVANCED_FACE('',(#11065),#3549,.T.);
#93530=ADVANCED_FACE('',(#11066),#3550,.T.);
#93531=ADVANCED_FACE('',(#11067),#3551,.T.);
#93532=ADVANCED_FACE('',(#11068),#88499,.T.);
#93533=ADVANCED_FACE('',(#11069),#3552,.T.);
#93534=ADVANCED_FACE('',(#11070),#5052,.T.);
#93535=ADVANCED_FACE('',(#11071),#6002,.F.);
#93536=ADVANCED_FACE('',(#11072),#6003,.F.);
#93537=ADVANCED_FACE('',(#11073),#88500,.F.);
#93538=ADVANCED_FACE('',(#11074),#3553,.F.);
#93539=ADVANCED_FACE('',(#11075),#3554,.F.);
#93540=ADVANCED_FACE('',(#11076),#3555,.F.);
#93541=ADVANCED_FACE('',(#11077),#3556,.T.);
#93542=ADVANCED_FACE('',(#11078),#88501,.T.);
#93543=ADVANCED_FACE('',(#11079),#3557,.T.);
#93544=ADVANCED_FACE('',(#11080),#3558,.T.);
#93545=ADVANCED_FACE('',(#11081),#3559,.T.);
#93546=ADVANCED_FACE('',(#11082),#3560,.T.);
#93547=ADVANCED_FACE('',(#11083),#3561,.T.);
#93548=ADVANCED_FACE('',(#11084),#88502,.T.);
#93549=ADVANCED_FACE('',(#11085),#3562,.T.);
#93550=ADVANCED_FACE('',(#11086),#5053,.T.);
#93551=ADVANCED_FACE('',(#11087),#6004,.F.);
#93552=ADVANCED_FACE('',(#11088),#6005,.F.);
#93553=ADVANCED_FACE('',(#11089),#88503,.F.);
#93554=ADVANCED_FACE('',(#11090),#3563,.F.);
#93555=ADVANCED_FACE('',(#11091),#3564,.F.);
#93556=ADVANCED_FACE('',(#11092),#3565,.F.);
#93557=ADVANCED_FACE('',(#11093),#3566,.T.);
#93558=ADVANCED_FACE('',(#11094),#88504,.T.);
#93559=ADVANCED_FACE('',(#11095),#3567,.T.);
#93560=ADVANCED_FACE('',(#11096),#3568,.T.);
#93561=ADVANCED_FACE('',(#11097),#3569,.T.);
#93562=ADVANCED_FACE('',(#11098),#3570,.T.);
#93563=ADVANCED_FACE('',(#11099),#3571,.T.);
#93564=ADVANCED_FACE('',(#11100),#88505,.T.);
#93565=ADVANCED_FACE('',(#11101),#3572,.T.);
#93566=ADVANCED_FACE('',(#11102),#5054,.T.);
#93567=ADVANCED_FACE('',(#11103),#6006,.F.);
#93568=ADVANCED_FACE('',(#11104),#6007,.F.);
#93569=ADVANCED_FACE('',(#11105),#88506,.F.);
#93570=ADVANCED_FACE('',(#11106),#3573,.F.);
#93571=ADVANCED_FACE('',(#11107),#3574,.F.);
#93572=ADVANCED_FACE('',(#11108),#3575,.F.);
#93573=ADVANCED_FACE('',(#11109),#3576,.T.);
#93574=ADVANCED_FACE('',(#11110),#88507,.T.);
#93575=ADVANCED_FACE('',(#11111),#3577,.T.);
#93576=ADVANCED_FACE('',(#11112),#3578,.T.);
#93577=ADVANCED_FACE('',(#11113),#3579,.T.);
#93578=ADVANCED_FACE('',(#11114),#3580,.T.);
#93579=ADVANCED_FACE('',(#11115),#3581,.T.);
#93580=ADVANCED_FACE('',(#11116),#88508,.T.);
#93581=ADVANCED_FACE('',(#11117),#3582,.T.);
#93582=ADVANCED_FACE('',(#11118),#5055,.T.);
#93583=ADVANCED_FACE('',(#11119),#6008,.F.);
#93584=ADVANCED_FACE('',(#11120),#6009,.F.);
#93585=ADVANCED_FACE('',(#11121),#88509,.F.);
#93586=ADVANCED_FACE('',(#11122),#3583,.F.);
#93587=ADVANCED_FACE('',(#11123),#3584,.F.);
#93588=ADVANCED_FACE('',(#11124),#3585,.F.);
#93589=ADVANCED_FACE('',(#11125),#3586,.T.);
#93590=ADVANCED_FACE('',(#11126),#88510,.T.);
#93591=ADVANCED_FACE('',(#11127),#3587,.T.);
#93592=ADVANCED_FACE('',(#11128),#3588,.T.);
#93593=ADVANCED_FACE('',(#11129),#3589,.T.);
#93594=ADVANCED_FACE('',(#11130),#3590,.T.);
#93595=ADVANCED_FACE('',(#11131),#3591,.T.);
#93596=ADVANCED_FACE('',(#11132),#88511,.T.);
#93597=ADVANCED_FACE('',(#11133),#3592,.T.);
#93598=ADVANCED_FACE('',(#11134),#5056,.T.);
#93599=ADVANCED_FACE('',(#11135),#6010,.F.);
#93600=ADVANCED_FACE('',(#11136),#6011,.F.);
#93601=ADVANCED_FACE('',(#11137),#88512,.F.);
#93602=ADVANCED_FACE('',(#11138),#3593,.F.);
#93603=ADVANCED_FACE('',(#11139),#3594,.F.);
#93604=ADVANCED_FACE('',(#11140),#3595,.F.);
#93605=ADVANCED_FACE('',(#11141),#3596,.T.);
#93606=ADVANCED_FACE('',(#11142),#88513,.T.);
#93607=ADVANCED_FACE('',(#11143),#3597,.T.);
#93608=ADVANCED_FACE('',(#11144),#3598,.T.);
#93609=ADVANCED_FACE('',(#11145),#3599,.T.);
#93610=ADVANCED_FACE('',(#11146),#3600,.T.);
#93611=ADVANCED_FACE('',(#11147),#3601,.T.);
#93612=ADVANCED_FACE('',(#11148),#88514,.T.);
#93613=ADVANCED_FACE('',(#11149),#3602,.T.);
#93614=ADVANCED_FACE('',(#11150),#5057,.T.);
#93615=ADVANCED_FACE('',(#11151),#6012,.F.);
#93616=ADVANCED_FACE('',(#11152),#6013,.F.);
#93617=ADVANCED_FACE('',(#11153),#88515,.F.);
#93618=ADVANCED_FACE('',(#11154),#3603,.F.);
#93619=ADVANCED_FACE('',(#11155),#3604,.F.);
#93620=ADVANCED_FACE('',(#11156),#3605,.F.);
#93621=ADVANCED_FACE('',(#11157),#3606,.T.);
#93622=ADVANCED_FACE('',(#11158),#88516,.T.);
#93623=ADVANCED_FACE('',(#11159),#3607,.T.);
#93624=ADVANCED_FACE('',(#11160),#3608,.T.);
#93625=ADVANCED_FACE('',(#11161),#3609,.T.);
#93626=ADVANCED_FACE('',(#11162),#3610,.T.);
#93627=ADVANCED_FACE('',(#11163),#3611,.T.);
#93628=ADVANCED_FACE('',(#11164),#88517,.T.);
#93629=ADVANCED_FACE('',(#11165),#3612,.T.);
#93630=ADVANCED_FACE('',(#11166),#5058,.T.);
#93631=ADVANCED_FACE('',(#11167),#6014,.F.);
#93632=ADVANCED_FACE('',(#11168),#6015,.F.);
#93633=ADVANCED_FACE('',(#11169),#88518,.F.);
#93634=ADVANCED_FACE('',(#11170),#3613,.F.);
#93635=ADVANCED_FACE('',(#11171),#3614,.F.);
#93636=ADVANCED_FACE('',(#11172),#3615,.F.);
#93637=ADVANCED_FACE('',(#11173),#3616,.T.);
#93638=ADVANCED_FACE('',(#11174),#88519,.T.);
#93639=ADVANCED_FACE('',(#11175),#3617,.T.);
#93640=ADVANCED_FACE('',(#11176),#3618,.T.);
#93641=ADVANCED_FACE('',(#11177),#3619,.T.);
#93642=ADVANCED_FACE('',(#11178),#3620,.T.);
#93643=ADVANCED_FACE('',(#11179),#3621,.T.);
#93644=ADVANCED_FACE('',(#11180),#88520,.T.);
#93645=ADVANCED_FACE('',(#11181),#3622,.T.);
#93646=ADVANCED_FACE('',(#11182),#5059,.T.);
#93647=ADVANCED_FACE('',(#11183),#6016,.F.);
#93648=ADVANCED_FACE('',(#11184),#6017,.F.);
#93649=ADVANCED_FACE('',(#11185),#88521,.F.);
#93650=ADVANCED_FACE('',(#11186),#3623,.F.);
#93651=ADVANCED_FACE('',(#11187),#3624,.F.);
#93652=ADVANCED_FACE('',(#11188),#3625,.F.);
#93653=ADVANCED_FACE('',(#11189),#3626,.T.);
#93654=ADVANCED_FACE('',(#11190),#88522,.T.);
#93655=ADVANCED_FACE('',(#11191),#3627,.T.);
#93656=ADVANCED_FACE('',(#11192),#3628,.T.);
#93657=ADVANCED_FACE('',(#11193),#3629,.T.);
#93658=ADVANCED_FACE('',(#11194),#3630,.T.);
#93659=ADVANCED_FACE('',(#11195),#3631,.T.);
#93660=ADVANCED_FACE('',(#11196),#88523,.T.);
#93661=ADVANCED_FACE('',(#11197),#3632,.T.);
#93662=ADVANCED_FACE('',(#11198),#5060,.T.);
#93663=ADVANCED_FACE('',(#11199),#6018,.F.);
#93664=ADVANCED_FACE('',(#11200),#6019,.F.);
#93665=ADVANCED_FACE('',(#11201),#88524,.F.);
#93666=ADVANCED_FACE('',(#11202),#3633,.F.);
#93667=ADVANCED_FACE('',(#11203),#3634,.F.);
#93668=ADVANCED_FACE('',(#11204),#3635,.F.);
#93669=ADVANCED_FACE('',(#11205),#3636,.T.);
#93670=ADVANCED_FACE('',(#11206),#88525,.T.);
#93671=ADVANCED_FACE('',(#11207),#3637,.T.);
#93672=ADVANCED_FACE('',(#11208),#3638,.T.);
#93673=ADVANCED_FACE('',(#11209),#3639,.T.);
#93674=ADVANCED_FACE('',(#11210),#3640,.T.);
#93675=ADVANCED_FACE('',(#11211),#3641,.T.);
#93676=ADVANCED_FACE('',(#11212),#88526,.T.);
#93677=ADVANCED_FACE('',(#11213),#3642,.T.);
#93678=ADVANCED_FACE('',(#11214),#5061,.T.);
#93679=ADVANCED_FACE('',(#11215),#6020,.F.);
#93680=ADVANCED_FACE('',(#11216),#6021,.F.);
#93681=ADVANCED_FACE('',(#11217),#88527,.F.);
#93682=ADVANCED_FACE('',(#11218),#3643,.F.);
#93683=ADVANCED_FACE('',(#11219),#3644,.F.);
#93684=ADVANCED_FACE('',(#11220),#3645,.F.);
#93685=ADVANCED_FACE('',(#11221),#3646,.T.);
#93686=ADVANCED_FACE('',(#11222),#88528,.T.);
#93687=ADVANCED_FACE('',(#11223),#3647,.T.);
#93688=ADVANCED_FACE('',(#11224),#3648,.T.);
#93689=ADVANCED_FACE('',(#11225),#3649,.T.);
#93690=ADVANCED_FACE('',(#11226),#3650,.T.);
#93691=ADVANCED_FACE('',(#11227),#3651,.T.);
#93692=ADVANCED_FACE('',(#11228),#88529,.T.);
#93693=ADVANCED_FACE('',(#11229),#3652,.T.);
#93694=ADVANCED_FACE('',(#11230),#5062,.T.);
#93695=ADVANCED_FACE('',(#11231),#6022,.F.);
#93696=ADVANCED_FACE('',(#11232),#6023,.F.);
#93697=ADVANCED_FACE('',(#11233),#88530,.F.);
#93698=ADVANCED_FACE('',(#11234),#3653,.F.);
#93699=ADVANCED_FACE('',(#11235),#3654,.F.);
#93700=ADVANCED_FACE('',(#11236),#3655,.F.);
#93701=ADVANCED_FACE('',(#11237),#3656,.T.);
#93702=ADVANCED_FACE('',(#11238),#88531,.T.);
#93703=ADVANCED_FACE('',(#11239),#3657,.T.);
#93704=ADVANCED_FACE('',(#11240),#3658,.T.);
#93705=ADVANCED_FACE('',(#11241),#3659,.T.);
#93706=ADVANCED_FACE('',(#11242),#3660,.T.);
#93707=ADVANCED_FACE('',(#11243),#3661,.T.);
#93708=ADVANCED_FACE('',(#11244),#88532,.T.);
#93709=ADVANCED_FACE('',(#11245),#3662,.T.);
#93710=ADVANCED_FACE('',(#11246),#5063,.T.);
#93711=ADVANCED_FACE('',(#11247),#6024,.F.);
#93712=ADVANCED_FACE('',(#11248),#6025,.F.);
#93713=ADVANCED_FACE('',(#11249),#88533,.F.);
#93714=ADVANCED_FACE('',(#11250),#3663,.F.);
#93715=ADVANCED_FACE('',(#11251),#3664,.F.);
#93716=ADVANCED_FACE('',(#11252),#3665,.F.);
#93717=ADVANCED_FACE('',(#11253),#3666,.T.);
#93718=ADVANCED_FACE('',(#11254),#88534,.T.);
#93719=ADVANCED_FACE('',(#11255),#3667,.T.);
#93720=ADVANCED_FACE('',(#11256),#3668,.T.);
#93721=ADVANCED_FACE('',(#11257),#3669,.T.);
#93722=ADVANCED_FACE('',(#11258),#3670,.T.);
#93723=ADVANCED_FACE('',(#11259),#3671,.T.);
#93724=ADVANCED_FACE('',(#11260),#88535,.T.);
#93725=ADVANCED_FACE('',(#11261),#3672,.T.);
#93726=ADVANCED_FACE('',(#11262),#5064,.T.);
#93727=ADVANCED_FACE('',(#11263),#6026,.F.);
#93728=ADVANCED_FACE('',(#11264),#6027,.F.);
#93729=ADVANCED_FACE('',(#11265),#88536,.F.);
#93730=ADVANCED_FACE('',(#11266),#3673,.F.);
#93731=ADVANCED_FACE('',(#11267),#3674,.F.);
#93732=ADVANCED_FACE('',(#11268),#3675,.F.);
#93733=ADVANCED_FACE('',(#11269),#3676,.T.);
#93734=ADVANCED_FACE('',(#11270),#88537,.T.);
#93735=ADVANCED_FACE('',(#11271),#3677,.T.);
#93736=ADVANCED_FACE('',(#11272),#3678,.T.);
#93737=ADVANCED_FACE('',(#11273),#3679,.T.);
#93738=ADVANCED_FACE('',(#11274),#3680,.T.);
#93739=ADVANCED_FACE('',(#11275),#3681,.T.);
#93740=ADVANCED_FACE('',(#11276),#88538,.T.);
#93741=ADVANCED_FACE('',(#11277),#3682,.T.);
#93742=ADVANCED_FACE('',(#11278),#5065,.T.);
#93743=ADVANCED_FACE('',(#11279),#6028,.F.);
#93744=ADVANCED_FACE('',(#11280),#6029,.F.);
#93745=ADVANCED_FACE('',(#11281),#88539,.F.);
#93746=ADVANCED_FACE('',(#11282),#3683,.F.);
#93747=ADVANCED_FACE('',(#11283),#3684,.F.);
#93748=ADVANCED_FACE('',(#11284),#3685,.F.);
#93749=ADVANCED_FACE('',(#11285),#3686,.T.);
#93750=ADVANCED_FACE('',(#11286),#88540,.T.);
#93751=ADVANCED_FACE('',(#11287),#3687,.T.);
#93752=ADVANCED_FACE('',(#11288),#3688,.T.);
#93753=ADVANCED_FACE('',(#11289),#3689,.T.);
#93754=ADVANCED_FACE('',(#11290),#3690,.T.);
#93755=ADVANCED_FACE('',(#11291),#3691,.T.);
#93756=ADVANCED_FACE('',(#11292),#88541,.T.);
#93757=ADVANCED_FACE('',(#11293),#3692,.T.);
#93758=ADVANCED_FACE('',(#11294),#5066,.T.);
#93759=ADVANCED_FACE('',(#11295),#6030,.F.);
#93760=ADVANCED_FACE('',(#11296),#6031,.F.);
#93761=ADVANCED_FACE('',(#11297),#88542,.F.);
#93762=ADVANCED_FACE('',(#11298),#3693,.F.);
#93763=ADVANCED_FACE('',(#11299),#3694,.F.);
#93764=ADVANCED_FACE('',(#11300),#3695,.F.);
#93765=ADVANCED_FACE('',(#11301),#3696,.T.);
#93766=ADVANCED_FACE('',(#11302),#88543,.T.);
#93767=ADVANCED_FACE('',(#11303),#3697,.T.);
#93768=ADVANCED_FACE('',(#11304),#3698,.T.);
#93769=ADVANCED_FACE('',(#11305),#3699,.T.);
#93770=ADVANCED_FACE('',(#11306),#3700,.T.);
#93771=ADVANCED_FACE('',(#11307),#3701,.T.);
#93772=ADVANCED_FACE('',(#11308),#88544,.T.);
#93773=ADVANCED_FACE('',(#11309),#3702,.T.);
#93774=ADVANCED_FACE('',(#11310),#5067,.T.);
#93775=ADVANCED_FACE('',(#11311),#6032,.F.);
#93776=ADVANCED_FACE('',(#11312),#6033,.F.);
#93777=ADVANCED_FACE('',(#11313),#88545,.F.);
#93778=ADVANCED_FACE('',(#11314),#3703,.F.);
#93779=ADVANCED_FACE('',(#11315),#3704,.F.);
#93780=ADVANCED_FACE('',(#11316),#3705,.F.);
#93781=ADVANCED_FACE('',(#11317),#3706,.T.);
#93782=ADVANCED_FACE('',(#11318),#88546,.T.);
#93783=ADVANCED_FACE('',(#11319),#3707,.T.);
#93784=ADVANCED_FACE('',(#11320),#3708,.T.);
#93785=ADVANCED_FACE('',(#11321),#3709,.T.);
#93786=ADVANCED_FACE('',(#11322),#3710,.T.);
#93787=ADVANCED_FACE('',(#11323),#3711,.T.);
#93788=ADVANCED_FACE('',(#11324),#88547,.T.);
#93789=ADVANCED_FACE('',(#11325),#3712,.T.);
#93790=ADVANCED_FACE('',(#11326),#5068,.T.);
#93791=ADVANCED_FACE('',(#11327),#6034,.F.);
#93792=ADVANCED_FACE('',(#11328),#6035,.F.);
#93793=ADVANCED_FACE('',(#11329),#88548,.F.);
#93794=ADVANCED_FACE('',(#11330),#3713,.F.);
#93795=ADVANCED_FACE('',(#11331),#3714,.F.);
#93796=ADVANCED_FACE('',(#11332),#3715,.F.);
#93797=ADVANCED_FACE('',(#11333),#3716,.T.);
#93798=ADVANCED_FACE('',(#11334),#88549,.T.);
#93799=ADVANCED_FACE('',(#11335),#3717,.T.);
#93800=ADVANCED_FACE('',(#11336),#3718,.T.);
#93801=ADVANCED_FACE('',(#11337),#3719,.T.);
#93802=ADVANCED_FACE('',(#11338),#3720,.T.);
#93803=ADVANCED_FACE('',(#11339),#3721,.T.);
#93804=ADVANCED_FACE('',(#11340),#88550,.T.);
#93805=ADVANCED_FACE('',(#11341),#3722,.T.);
#93806=ADVANCED_FACE('',(#11342),#5069,.T.);
#93807=ADVANCED_FACE('',(#11343),#6036,.F.);
#93808=ADVANCED_FACE('',(#11344),#6037,.F.);
#93809=ADVANCED_FACE('',(#11345),#88551,.F.);
#93810=ADVANCED_FACE('',(#11346),#3723,.F.);
#93811=ADVANCED_FACE('',(#11347),#3724,.F.);
#93812=ADVANCED_FACE('',(#11348),#3725,.F.);
#93813=ADVANCED_FACE('',(#11349),#3726,.T.);
#93814=ADVANCED_FACE('',(#11350),#88552,.T.);
#93815=ADVANCED_FACE('',(#11351),#3727,.T.);
#93816=ADVANCED_FACE('',(#11352),#3728,.T.);
#93817=ADVANCED_FACE('',(#11353),#3729,.T.);
#93818=ADVANCED_FACE('',(#11354),#3730,.T.);
#93819=ADVANCED_FACE('',(#11355),#3731,.T.);
#93820=ADVANCED_FACE('',(#11356),#88553,.T.);
#93821=ADVANCED_FACE('',(#11357),#3732,.T.);
#93822=ADVANCED_FACE('',(#11358),#5070,.T.);
#93823=ADVANCED_FACE('',(#11359),#6038,.F.);
#93824=ADVANCED_FACE('',(#11360),#6039,.F.);
#93825=ADVANCED_FACE('',(#11361),#88554,.F.);
#93826=ADVANCED_FACE('',(#11362),#3733,.F.);
#93827=ADVANCED_FACE('',(#11363),#3734,.F.);
#93828=ADVANCED_FACE('',(#11364),#3735,.F.);
#93829=ADVANCED_FACE('',(#11365),#3736,.T.);
#93830=ADVANCED_FACE('',(#11366),#88555,.T.);
#93831=ADVANCED_FACE('',(#11367),#3737,.T.);
#93832=ADVANCED_FACE('',(#11368),#3738,.T.);
#93833=ADVANCED_FACE('',(#11369),#3739,.T.);
#93834=ADVANCED_FACE('',(#11370),#3740,.T.);
#93835=ADVANCED_FACE('',(#11371),#3741,.T.);
#93836=ADVANCED_FACE('',(#11372),#88556,.T.);
#93837=ADVANCED_FACE('',(#11373),#3742,.T.);
#93838=ADVANCED_FACE('',(#11374),#5071,.T.);
#93839=ADVANCED_FACE('',(#11375),#6040,.F.);
#93840=ADVANCED_FACE('',(#11376),#6041,.F.);
#93841=ADVANCED_FACE('',(#11377),#88557,.F.);
#93842=ADVANCED_FACE('',(#11378),#3743,.F.);
#93843=ADVANCED_FACE('',(#11379),#3744,.F.);
#93844=ADVANCED_FACE('',(#11380),#3745,.F.);
#93845=ADVANCED_FACE('',(#11381),#3746,.T.);
#93846=ADVANCED_FACE('',(#11382),#88558,.T.);
#93847=ADVANCED_FACE('',(#11383),#3747,.T.);
#93848=ADVANCED_FACE('',(#11384),#3748,.T.);
#93849=ADVANCED_FACE('',(#11385),#3749,.T.);
#93850=ADVANCED_FACE('',(#11386),#3750,.T.);
#93851=ADVANCED_FACE('',(#11387),#3751,.T.);
#93852=ADVANCED_FACE('',(#11388),#88559,.T.);
#93853=ADVANCED_FACE('',(#11389),#3752,.T.);
#93854=ADVANCED_FACE('',(#11390),#5072,.T.);
#93855=ADVANCED_FACE('',(#11391),#6042,.F.);
#93856=ADVANCED_FACE('',(#11392),#6043,.F.);
#93857=ADVANCED_FACE('',(#11393),#88560,.F.);
#93858=ADVANCED_FACE('',(#11394),#3753,.F.);
#93859=ADVANCED_FACE('',(#11395),#3754,.F.);
#93860=ADVANCED_FACE('',(#11396),#3755,.F.);
#93861=ADVANCED_FACE('',(#11397),#3756,.T.);
#93862=ADVANCED_FACE('',(#11398),#88561,.T.);
#93863=ADVANCED_FACE('',(#11399),#3757,.T.);
#93864=ADVANCED_FACE('',(#11400),#3758,.T.);
#93865=ADVANCED_FACE('',(#11401),#3759,.T.);
#93866=ADVANCED_FACE('',(#11402),#3760,.T.);
#93867=ADVANCED_FACE('',(#11403),#3761,.T.);
#93868=ADVANCED_FACE('',(#11404),#88562,.T.);
#93869=ADVANCED_FACE('',(#11405),#3762,.T.);
#93870=ADVANCED_FACE('',(#11406),#5073,.T.);
#93871=ADVANCED_FACE('',(#11407),#6044,.F.);
#93872=ADVANCED_FACE('',(#11408),#6045,.F.);
#93873=ADVANCED_FACE('',(#11409),#88563,.F.);
#93874=ADVANCED_FACE('',(#11410),#3763,.F.);
#93875=ADVANCED_FACE('',(#11411),#3764,.F.);
#93876=ADVANCED_FACE('',(#11412),#3765,.F.);
#93877=ADVANCED_FACE('',(#11413),#3766,.T.);
#93878=ADVANCED_FACE('',(#11414),#88564,.T.);
#93879=ADVANCED_FACE('',(#11415),#3767,.T.);
#93880=ADVANCED_FACE('',(#11416),#3768,.T.);
#93881=ADVANCED_FACE('',(#11417),#3769,.T.);
#93882=ADVANCED_FACE('',(#11418),#3770,.T.);
#93883=ADVANCED_FACE('',(#11419),#3771,.T.);
#93884=ADVANCED_FACE('',(#11420),#88565,.T.);
#93885=ADVANCED_FACE('',(#11421),#3772,.T.);
#93886=ADVANCED_FACE('',(#11422),#5074,.T.);
#93887=ADVANCED_FACE('',(#11423),#6046,.F.);
#93888=ADVANCED_FACE('',(#11424),#6047,.F.);
#93889=ADVANCED_FACE('',(#11425),#88566,.F.);
#93890=ADVANCED_FACE('',(#11426),#3773,.F.);
#93891=ADVANCED_FACE('',(#11427),#3774,.F.);
#93892=ADVANCED_FACE('',(#11428),#3775,.F.);
#93893=ADVANCED_FACE('',(#11429),#3776,.T.);
#93894=ADVANCED_FACE('',(#11430),#88567,.T.);
#93895=ADVANCED_FACE('',(#11431),#3777,.T.);
#93896=ADVANCED_FACE('',(#11432),#3778,.T.);
#93897=ADVANCED_FACE('',(#11433),#3779,.T.);
#93898=ADVANCED_FACE('',(#11434),#3780,.T.);
#93899=ADVANCED_FACE('',(#11435),#3781,.T.);
#93900=ADVANCED_FACE('',(#11436),#88568,.T.);
#93901=ADVANCED_FACE('',(#11437),#3782,.T.);
#93902=ADVANCED_FACE('',(#11438),#5075,.T.);
#93903=ADVANCED_FACE('',(#11439),#6048,.F.);
#93904=ADVANCED_FACE('',(#11440),#6049,.F.);
#93905=ADVANCED_FACE('',(#11441),#88569,.F.);
#93906=ADVANCED_FACE('',(#11442),#3783,.F.);
#93907=ADVANCED_FACE('',(#11443),#3784,.F.);
#93908=ADVANCED_FACE('',(#11444),#3785,.F.);
#93909=ADVANCED_FACE('',(#11445),#3786,.T.);
#93910=ADVANCED_FACE('',(#11446),#88570,.T.);
#93911=ADVANCED_FACE('',(#11447),#3787,.T.);
#93912=ADVANCED_FACE('',(#11448),#3788,.T.);
#93913=ADVANCED_FACE('',(#11449),#3789,.T.);
#93914=ADVANCED_FACE('',(#11450),#3790,.T.);
#93915=ADVANCED_FACE('',(#11451),#3791,.T.);
#93916=ADVANCED_FACE('',(#11452),#88571,.T.);
#93917=ADVANCED_FACE('',(#11453),#3792,.T.);
#93918=ADVANCED_FACE('',(#11454),#5076,.T.);
#93919=ADVANCED_FACE('',(#11455),#6050,.F.);
#93920=ADVANCED_FACE('',(#11456),#6051,.F.);
#93921=ADVANCED_FACE('',(#11457),#88572,.F.);
#93922=ADVANCED_FACE('',(#11458),#3793,.F.);
#93923=ADVANCED_FACE('',(#11459),#3794,.F.);
#93924=ADVANCED_FACE('',(#11460),#3795,.F.);
#93925=ADVANCED_FACE('',(#11461),#3796,.T.);
#93926=ADVANCED_FACE('',(#11462),#88573,.T.);
#93927=ADVANCED_FACE('',(#11463),#3797,.T.);
#93928=ADVANCED_FACE('',(#11464),#3798,.T.);
#93929=ADVANCED_FACE('',(#11465),#3799,.T.);
#93930=ADVANCED_FACE('',(#11466),#3800,.T.);
#93931=ADVANCED_FACE('',(#11467),#3801,.T.);
#93932=ADVANCED_FACE('',(#11468),#88574,.T.);
#93933=ADVANCED_FACE('',(#11469),#3802,.T.);
#93934=ADVANCED_FACE('',(#11470),#5077,.T.);
#93935=ADVANCED_FACE('',(#11471),#6052,.F.);
#93936=ADVANCED_FACE('',(#11472),#6053,.F.);
#93937=ADVANCED_FACE('',(#11473),#88575,.F.);
#93938=ADVANCED_FACE('',(#11474),#3803,.F.);
#93939=ADVANCED_FACE('',(#11475),#3804,.F.);
#93940=ADVANCED_FACE('',(#11476),#3805,.F.);
#93941=ADVANCED_FACE('',(#11477),#3806,.T.);
#93942=ADVANCED_FACE('',(#11478),#88576,.T.);
#93943=ADVANCED_FACE('',(#11479),#3807,.T.);
#93944=ADVANCED_FACE('',(#11480),#3808,.T.);
#93945=ADVANCED_FACE('',(#11481),#3809,.T.);
#93946=ADVANCED_FACE('',(#11482),#3810,.T.);
#93947=ADVANCED_FACE('',(#11483),#3811,.T.);
#93948=ADVANCED_FACE('',(#11484),#88577,.T.);
#93949=ADVANCED_FACE('',(#11485),#3812,.T.);
#93950=ADVANCED_FACE('',(#11486),#5078,.T.);
#93951=ADVANCED_FACE('',(#11487),#6054,.F.);
#93952=ADVANCED_FACE('',(#11488),#6055,.F.);
#93953=ADVANCED_FACE('',(#11489),#88578,.F.);
#93954=ADVANCED_FACE('',(#11490),#3813,.F.);
#93955=ADVANCED_FACE('',(#11491),#3814,.F.);
#93956=ADVANCED_FACE('',(#11492),#3815,.F.);
#93957=ADVANCED_FACE('',(#11493),#3816,.T.);
#93958=ADVANCED_FACE('',(#11494),#88579,.T.);
#93959=ADVANCED_FACE('',(#11495),#3817,.T.);
#93960=ADVANCED_FACE('',(#11496),#3818,.T.);
#93961=ADVANCED_FACE('',(#11497),#3819,.T.);
#93962=ADVANCED_FACE('',(#11498),#3820,.T.);
#93963=ADVANCED_FACE('',(#11499),#3821,.T.);
#93964=ADVANCED_FACE('',(#11500),#88580,.T.);
#93965=ADVANCED_FACE('',(#11501),#3822,.T.);
#93966=ADVANCED_FACE('',(#11502),#5079,.T.);
#93967=ADVANCED_FACE('',(#11503),#6056,.F.);
#93968=ADVANCED_FACE('',(#11504),#6057,.F.);
#93969=ADVANCED_FACE('',(#11505),#88581,.F.);
#93970=ADVANCED_FACE('',(#11506),#3823,.F.);
#93971=ADVANCED_FACE('',(#11507),#3824,.F.);
#93972=ADVANCED_FACE('',(#11508),#3825,.F.);
#93973=ADVANCED_FACE('',(#11509),#3826,.T.);
#93974=ADVANCED_FACE('',(#11510),#88582,.T.);
#93975=ADVANCED_FACE('',(#11511),#3827,.T.);
#93976=ADVANCED_FACE('',(#11512),#3828,.T.);
#93977=ADVANCED_FACE('',(#11513),#3829,.T.);
#93978=ADVANCED_FACE('',(#11514),#3830,.T.);
#93979=ADVANCED_FACE('',(#11515),#3831,.T.);
#93980=ADVANCED_FACE('',(#11516),#88583,.T.);
#93981=ADVANCED_FACE('',(#11517),#3832,.T.);
#93982=ADVANCED_FACE('',(#11518),#5080,.T.);
#93983=ADVANCED_FACE('',(#11519),#6058,.F.);
#93984=ADVANCED_FACE('',(#11520),#6059,.F.);
#93985=ADVANCED_FACE('',(#11521),#88584,.F.);
#93986=ADVANCED_FACE('',(#11522),#3833,.F.);
#93987=ADVANCED_FACE('',(#11523),#3834,.F.);
#93988=ADVANCED_FACE('',(#11524),#3835,.F.);
#93989=ADVANCED_FACE('',(#11525),#3836,.T.);
#93990=ADVANCED_FACE('',(#11526),#88585,.T.);
#93991=ADVANCED_FACE('',(#11527),#3837,.T.);
#93992=ADVANCED_FACE('',(#11528),#3838,.T.);
#93993=ADVANCED_FACE('',(#11529),#3839,.T.);
#93994=ADVANCED_FACE('',(#11530),#3840,.T.);
#93995=ADVANCED_FACE('',(#11531),#3841,.T.);
#93996=ADVANCED_FACE('',(#11532),#88586,.T.);
#93997=ADVANCED_FACE('',(#11533),#3842,.T.);
#93998=ADVANCED_FACE('',(#11534),#5081,.T.);
#93999=ADVANCED_FACE('',(#11535),#6060,.F.);
#94000=ADVANCED_FACE('',(#11536),#6061,.F.);
#94001=ADVANCED_FACE('',(#11537),#88587,.F.);
#94002=ADVANCED_FACE('',(#11538),#3843,.F.);
#94003=ADVANCED_FACE('',(#11539),#3844,.F.);
#94004=ADVANCED_FACE('',(#11540),#3845,.F.);
#94005=ADVANCED_FACE('',(#11541),#3846,.T.);
#94006=ADVANCED_FACE('',(#11542),#88588,.T.);
#94007=ADVANCED_FACE('',(#11543),#3847,.T.);
#94008=ADVANCED_FACE('',(#11544),#3848,.T.);
#94009=ADVANCED_FACE('',(#11545),#3849,.T.);
#94010=ADVANCED_FACE('',(#11546),#3850,.T.);
#94011=ADVANCED_FACE('',(#11547),#3851,.T.);
#94012=ADVANCED_FACE('',(#11548),#88589,.T.);
#94013=ADVANCED_FACE('',(#11549),#3852,.T.);
#94014=ADVANCED_FACE('',(#11550),#5082,.T.);
#94015=ADVANCED_FACE('',(#11551),#6062,.F.);
#94016=ADVANCED_FACE('',(#11552),#6063,.F.);
#94017=ADVANCED_FACE('',(#11553),#88590,.F.);
#94018=ADVANCED_FACE('',(#11554),#3853,.F.);
#94019=ADVANCED_FACE('',(#11555),#3854,.F.);
#94020=ADVANCED_FACE('',(#11556),#3855,.F.);
#94021=ADVANCED_FACE('',(#11557),#3856,.T.);
#94022=ADVANCED_FACE('',(#11558),#88591,.T.);
#94023=ADVANCED_FACE('',(#11559),#3857,.T.);
#94024=ADVANCED_FACE('',(#11560),#3858,.T.);
#94025=ADVANCED_FACE('',(#11561),#3859,.T.);
#94026=ADVANCED_FACE('',(#11562),#3860,.T.);
#94027=ADVANCED_FACE('',(#11563),#3861,.T.);
#94028=ADVANCED_FACE('',(#11564),#88592,.T.);
#94029=ADVANCED_FACE('',(#11565),#3862,.T.);
#94030=ADVANCED_FACE('',(#11566),#5083,.T.);
#94031=ADVANCED_FACE('',(#11567),#6064,.F.);
#94032=ADVANCED_FACE('',(#11568),#6065,.F.);
#94033=ADVANCED_FACE('',(#11569),#88593,.F.);
#94034=ADVANCED_FACE('',(#11570),#3863,.F.);
#94035=ADVANCED_FACE('',(#11571),#3864,.F.);
#94036=ADVANCED_FACE('',(#11572),#3865,.F.);
#94037=ADVANCED_FACE('',(#11573),#3866,.T.);
#94038=ADVANCED_FACE('',(#11574),#88594,.T.);
#94039=ADVANCED_FACE('',(#11575),#3867,.T.);
#94040=ADVANCED_FACE('',(#11576),#3868,.T.);
#94041=ADVANCED_FACE('',(#11577),#3869,.T.);
#94042=ADVANCED_FACE('',(#11578),#3870,.T.);
#94043=ADVANCED_FACE('',(#11579),#3871,.T.);
#94044=ADVANCED_FACE('',(#11580),#88595,.T.);
#94045=ADVANCED_FACE('',(#11581),#3872,.T.);
#94046=ADVANCED_FACE('',(#11582),#5084,.T.);
#94047=ADVANCED_FACE('',(#11583),#6066,.F.);
#94048=ADVANCED_FACE('',(#11584),#6067,.F.);
#94049=ADVANCED_FACE('',(#11585),#88596,.F.);
#94050=ADVANCED_FACE('',(#11586),#3873,.F.);
#94051=ADVANCED_FACE('',(#11587),#3874,.F.);
#94052=ADVANCED_FACE('',(#11588),#3875,.F.);
#94053=ADVANCED_FACE('',(#11589),#3876,.T.);
#94054=ADVANCED_FACE('',(#11590),#88597,.T.);
#94055=ADVANCED_FACE('',(#11591),#3877,.T.);
#94056=ADVANCED_FACE('',(#11592),#3878,.T.);
#94057=ADVANCED_FACE('',(#11593),#3879,.T.);
#94058=ADVANCED_FACE('',(#11594),#3880,.T.);
#94059=ADVANCED_FACE('',(#11595),#3881,.T.);
#94060=ADVANCED_FACE('',(#11596),#88598,.T.);
#94061=ADVANCED_FACE('',(#11597),#3882,.T.);
#94062=ADVANCED_FACE('',(#11598),#5085,.T.);
#94063=ADVANCED_FACE('',(#11599),#6068,.F.);
#94064=ADVANCED_FACE('',(#11600),#6069,.F.);
#94065=ADVANCED_FACE('',(#11601),#88599,.F.);
#94066=ADVANCED_FACE('',(#11602),#3883,.F.);
#94067=ADVANCED_FACE('',(#11603),#3884,.F.);
#94068=ADVANCED_FACE('',(#11604),#3885,.F.);
#94069=ADVANCED_FACE('',(#11605),#3886,.T.);
#94070=ADVANCED_FACE('',(#11606),#88600,.T.);
#94071=ADVANCED_FACE('',(#11607),#3887,.T.);
#94072=ADVANCED_FACE('',(#11608),#3888,.T.);
#94073=ADVANCED_FACE('',(#11609),#3889,.T.);
#94074=ADVANCED_FACE('',(#11610),#3890,.T.);
#94075=ADVANCED_FACE('',(#11611),#3891,.T.);
#94076=ADVANCED_FACE('',(#11612),#88601,.T.);
#94077=ADVANCED_FACE('',(#11613),#3892,.T.);
#94078=ADVANCED_FACE('',(#11614),#5086,.T.);
#94079=ADVANCED_FACE('',(#11615),#6070,.F.);
#94080=ADVANCED_FACE('',(#11616),#6071,.F.);
#94081=ADVANCED_FACE('',(#11617),#88602,.F.);
#94082=ADVANCED_FACE('',(#11618),#3893,.F.);
#94083=ADVANCED_FACE('',(#11619),#3894,.F.);
#94084=ADVANCED_FACE('',(#11620),#3895,.F.);
#94085=ADVANCED_FACE('',(#11621),#3896,.T.);
#94086=ADVANCED_FACE('',(#11622),#88603,.T.);
#94087=ADVANCED_FACE('',(#11623),#3897,.T.);
#94088=ADVANCED_FACE('',(#11624),#3898,.T.);
#94089=ADVANCED_FACE('',(#11625),#3899,.T.);
#94090=ADVANCED_FACE('',(#11626),#3900,.T.);
#94091=ADVANCED_FACE('',(#11627),#3901,.T.);
#94092=ADVANCED_FACE('',(#11628),#88604,.T.);
#94093=ADVANCED_FACE('',(#11629),#3902,.T.);
#94094=ADVANCED_FACE('',(#11630),#5087,.T.);
#94095=ADVANCED_FACE('',(#11631),#6072,.F.);
#94096=ADVANCED_FACE('',(#11632),#6073,.F.);
#94097=ADVANCED_FACE('',(#11633),#88605,.F.);
#94098=ADVANCED_FACE('',(#11634),#3903,.F.);
#94099=ADVANCED_FACE('',(#11635),#3904,.F.);
#94100=ADVANCED_FACE('',(#11636),#3905,.F.);
#94101=ADVANCED_FACE('',(#11637),#3906,.T.);
#94102=ADVANCED_FACE('',(#11638),#88606,.T.);
#94103=ADVANCED_FACE('',(#11639),#3907,.T.);
#94104=ADVANCED_FACE('',(#11640),#3908,.T.);
#94105=ADVANCED_FACE('',(#11641),#3909,.T.);
#94106=ADVANCED_FACE('',(#11642),#3910,.T.);
#94107=ADVANCED_FACE('',(#11643),#3911,.T.);
#94108=ADVANCED_FACE('',(#11644),#88607,.T.);
#94109=ADVANCED_FACE('',(#11645),#3912,.T.);
#94110=ADVANCED_FACE('',(#11646),#5088,.T.);
#94111=ADVANCED_FACE('',(#11647),#6074,.F.);
#94112=ADVANCED_FACE('',(#11648),#6075,.F.);
#94113=ADVANCED_FACE('',(#11649),#88608,.F.);
#94114=ADVANCED_FACE('',(#11650),#3913,.F.);
#94115=ADVANCED_FACE('',(#11651),#3914,.F.);
#94116=ADVANCED_FACE('',(#11652),#3915,.F.);
#94117=ADVANCED_FACE('',(#11653),#3916,.T.);
#94118=ADVANCED_FACE('',(#11654),#88609,.T.);
#94119=ADVANCED_FACE('',(#11655),#3917,.T.);
#94120=ADVANCED_FACE('',(#11656),#3918,.T.);
#94121=ADVANCED_FACE('',(#11657),#3919,.T.);
#94122=ADVANCED_FACE('',(#11658),#3920,.T.);
#94123=ADVANCED_FACE('',(#11659),#3921,.T.);
#94124=ADVANCED_FACE('',(#11660),#88610,.T.);
#94125=ADVANCED_FACE('',(#11661),#3922,.T.);
#94126=ADVANCED_FACE('',(#11662),#5089,.T.);
#94127=ADVANCED_FACE('',(#11663),#6076,.F.);
#94128=ADVANCED_FACE('',(#11664),#6077,.F.);
#94129=ADVANCED_FACE('',(#11665),#88611,.F.);
#94130=ADVANCED_FACE('',(#11666),#3923,.F.);
#94131=ADVANCED_FACE('',(#11667),#3924,.F.);
#94132=ADVANCED_FACE('',(#11668),#3925,.F.);
#94133=ADVANCED_FACE('',(#11669),#3926,.T.);
#94134=ADVANCED_FACE('',(#11670),#88612,.T.);
#94135=ADVANCED_FACE('',(#11671),#3927,.T.);
#94136=ADVANCED_FACE('',(#11672),#3928,.T.);
#94137=ADVANCED_FACE('',(#11673),#3929,.T.);
#94138=ADVANCED_FACE('',(#11674),#3930,.T.);
#94139=ADVANCED_FACE('',(#11675),#3931,.T.);
#94140=ADVANCED_FACE('',(#11676),#88613,.T.);
#94141=ADVANCED_FACE('',(#11677),#3932,.T.);
#94142=ADVANCED_FACE('',(#11678),#5090,.T.);
#94143=ADVANCED_FACE('',(#11679),#6078,.F.);
#94144=ADVANCED_FACE('',(#11680),#6079,.F.);
#94145=ADVANCED_FACE('',(#11681),#88614,.F.);
#94146=ADVANCED_FACE('',(#11682),#3933,.F.);
#94147=ADVANCED_FACE('',(#11683),#3934,.F.);
#94148=ADVANCED_FACE('',(#11684),#3935,.F.);
#94149=ADVANCED_FACE('',(#11685),#3936,.T.);
#94150=ADVANCED_FACE('',(#11686),#88615,.T.);
#94151=ADVANCED_FACE('',(#11687),#3937,.T.);
#94152=ADVANCED_FACE('',(#11688),#3938,.T.);
#94153=ADVANCED_FACE('',(#11689),#3939,.T.);
#94154=ADVANCED_FACE('',(#11690),#3940,.T.);
#94155=ADVANCED_FACE('',(#11691),#3941,.T.);
#94156=ADVANCED_FACE('',(#11692),#88616,.T.);
#94157=ADVANCED_FACE('',(#11693),#3942,.T.);
#94158=ADVANCED_FACE('',(#11694),#5091,.T.);
#94159=ADVANCED_FACE('',(#11695),#6080,.F.);
#94160=ADVANCED_FACE('',(#11696),#6081,.F.);
#94161=ADVANCED_FACE('',(#11697),#88617,.F.);
#94162=ADVANCED_FACE('',(#11698),#3943,.F.);
#94163=ADVANCED_FACE('',(#11699),#3944,.F.);
#94164=ADVANCED_FACE('',(#11700),#3945,.F.);
#94165=ADVANCED_FACE('',(#11701),#3946,.T.);
#94166=ADVANCED_FACE('',(#11702),#88618,.T.);
#94167=ADVANCED_FACE('',(#11703),#3947,.T.);
#94168=ADVANCED_FACE('',(#11704),#3948,.T.);
#94169=ADVANCED_FACE('',(#11705),#3949,.T.);
#94170=ADVANCED_FACE('',(#11706),#3950,.T.);
#94171=ADVANCED_FACE('',(#11707),#3951,.T.);
#94172=ADVANCED_FACE('',(#11708),#88619,.T.);
#94173=ADVANCED_FACE('',(#11709),#3952,.T.);
#94174=ADVANCED_FACE('',(#11710),#5092,.T.);
#94175=ADVANCED_FACE('',(#11711),#6082,.F.);
#94176=ADVANCED_FACE('',(#11712),#6083,.F.);
#94177=ADVANCED_FACE('',(#11713),#88620,.F.);
#94178=ADVANCED_FACE('',(#11714),#3953,.F.);
#94179=ADVANCED_FACE('',(#11715),#3954,.F.);
#94180=ADVANCED_FACE('',(#11716),#3955,.F.);
#94181=ADVANCED_FACE('',(#11717),#3956,.T.);
#94182=ADVANCED_FACE('',(#11718),#88621,.T.);
#94183=ADVANCED_FACE('',(#11719),#3957,.T.);
#94184=ADVANCED_FACE('',(#11720),#3958,.T.);
#94185=ADVANCED_FACE('',(#11721),#3959,.T.);
#94186=ADVANCED_FACE('',(#11722),#3960,.T.);
#94187=ADVANCED_FACE('',(#11723),#3961,.T.);
#94188=ADVANCED_FACE('',(#11724),#88622,.T.);
#94189=ADVANCED_FACE('',(#11725),#3962,.T.);
#94190=ADVANCED_FACE('',(#11726),#5093,.T.);
#94191=ADVANCED_FACE('',(#11727),#6084,.F.);
#94192=ADVANCED_FACE('',(#11728),#6085,.F.);
#94193=ADVANCED_FACE('',(#11729),#88623,.F.);
#94194=ADVANCED_FACE('',(#11730),#3963,.F.);
#94195=ADVANCED_FACE('',(#11731),#3964,.F.);
#94196=ADVANCED_FACE('',(#11732),#3965,.F.);
#94197=ADVANCED_FACE('',(#11733),#3966,.T.);
#94198=ADVANCED_FACE('',(#11734),#88624,.T.);
#94199=ADVANCED_FACE('',(#11735),#3967,.T.);
#94200=ADVANCED_FACE('',(#11736),#3968,.T.);
#94201=ADVANCED_FACE('',(#11737),#3969,.T.);
#94202=ADVANCED_FACE('',(#11738),#3970,.T.);
#94203=ADVANCED_FACE('',(#11739),#3971,.T.);
#94204=ADVANCED_FACE('',(#11740),#88625,.T.);
#94205=ADVANCED_FACE('',(#11741),#3972,.T.);
#94206=ADVANCED_FACE('',(#11742),#5094,.T.);
#94207=ADVANCED_FACE('',(#11743),#6086,.F.);
#94208=ADVANCED_FACE('',(#11744),#6087,.F.);
#94209=ADVANCED_FACE('',(#11745),#88626,.F.);
#94210=ADVANCED_FACE('',(#11746),#3973,.F.);
#94211=ADVANCED_FACE('',(#11747),#3974,.F.);
#94212=ADVANCED_FACE('',(#11748),#3975,.F.);
#94213=ADVANCED_FACE('',(#11749),#3976,.T.);
#94214=ADVANCED_FACE('',(#11750),#88627,.T.);
#94215=ADVANCED_FACE('',(#11751),#3977,.T.);
#94216=ADVANCED_FACE('',(#11752),#3978,.T.);
#94217=ADVANCED_FACE('',(#11753),#3979,.T.);
#94218=ADVANCED_FACE('',(#11754),#3980,.T.);
#94219=ADVANCED_FACE('',(#11755),#3981,.T.);
#94220=ADVANCED_FACE('',(#11756),#88628,.T.);
#94221=ADVANCED_FACE('',(#11757),#3982,.T.);
#94222=ADVANCED_FACE('',(#11758),#5095,.T.);
#94223=ADVANCED_FACE('',(#11759),#6088,.F.);
#94224=ADVANCED_FACE('',(#11760),#6089,.F.);
#94225=ADVANCED_FACE('',(#11761),#88629,.F.);
#94226=ADVANCED_FACE('',(#11762),#3983,.F.);
#94227=ADVANCED_FACE('',(#11763),#3984,.F.);
#94228=ADVANCED_FACE('',(#11764),#3985,.F.);
#94229=ADVANCED_FACE('',(#11765),#3986,.T.);
#94230=ADVANCED_FACE('',(#11766),#88630,.T.);
#94231=ADVANCED_FACE('',(#11767),#3987,.T.);
#94232=ADVANCED_FACE('',(#11768),#3988,.T.);
#94233=ADVANCED_FACE('',(#11769),#3989,.T.);
#94234=ADVANCED_FACE('',(#11770),#3990,.T.);
#94235=ADVANCED_FACE('',(#11771),#3991,.T.);
#94236=ADVANCED_FACE('',(#11772),#88631,.T.);
#94237=ADVANCED_FACE('',(#11773),#3992,.T.);
#94238=ADVANCED_FACE('',(#11774),#5096,.T.);
#94239=ADVANCED_FACE('',(#11775),#6090,.F.);
#94240=ADVANCED_FACE('',(#11776),#6091,.F.);
#94241=ADVANCED_FACE('',(#11777),#88632,.F.);
#94242=ADVANCED_FACE('',(#11778),#3993,.F.);
#94243=ADVANCED_FACE('',(#11779),#3994,.F.);
#94244=ADVANCED_FACE('',(#11780),#3995,.F.);
#94245=ADVANCED_FACE('',(#11781),#3996,.T.);
#94246=ADVANCED_FACE('',(#11782),#88633,.T.);
#94247=ADVANCED_FACE('',(#11783),#3997,.T.);
#94248=ADVANCED_FACE('',(#11784),#3998,.T.);
#94249=ADVANCED_FACE('',(#11785),#3999,.T.);
#94250=ADVANCED_FACE('',(#11786),#4000,.T.);
#94251=ADVANCED_FACE('',(#11787),#4001,.T.);
#94252=ADVANCED_FACE('',(#11788),#88634,.T.);
#94253=ADVANCED_FACE('',(#11789),#4002,.T.);
#94254=ADVANCED_FACE('',(#11790),#5097,.T.);
#94255=ADVANCED_FACE('',(#11791),#6092,.F.);
#94256=ADVANCED_FACE('',(#11792),#6093,.F.);
#94257=ADVANCED_FACE('',(#11793),#88635,.F.);
#94258=ADVANCED_FACE('',(#11794),#4003,.F.);
#94259=ADVANCED_FACE('',(#11795),#4004,.F.);
#94260=ADVANCED_FACE('',(#11796),#4005,.F.);
#94261=ADVANCED_FACE('',(#11797),#4006,.T.);
#94262=ADVANCED_FACE('',(#11798),#88636,.T.);
#94263=ADVANCED_FACE('',(#11799),#4007,.T.);
#94264=ADVANCED_FACE('',(#11800),#4008,.T.);
#94265=ADVANCED_FACE('',(#11801),#4009,.T.);
#94266=ADVANCED_FACE('',(#11802),#4010,.T.);
#94267=ADVANCED_FACE('',(#11803),#4011,.T.);
#94268=ADVANCED_FACE('',(#11804),#88637,.T.);
#94269=ADVANCED_FACE('',(#11805),#4012,.T.);
#94270=ADVANCED_FACE('',(#11806),#5098,.T.);
#94271=ADVANCED_FACE('',(#11807),#6094,.F.);
#94272=ADVANCED_FACE('',(#11808),#6095,.F.);
#94273=ADVANCED_FACE('',(#11809),#88638,.F.);
#94274=ADVANCED_FACE('',(#11810),#4013,.F.);
#94275=ADVANCED_FACE('',(#11811),#4014,.F.);
#94276=ADVANCED_FACE('',(#11812),#4015,.F.);
#94277=ADVANCED_FACE('',(#11813),#4016,.T.);
#94278=ADVANCED_FACE('',(#11814),#88639,.T.);
#94279=ADVANCED_FACE('',(#11815),#4017,.T.);
#94280=ADVANCED_FACE('',(#11816),#4018,.T.);
#94281=ADVANCED_FACE('',(#11817),#4019,.T.);
#94282=ADVANCED_FACE('',(#11818),#4020,.T.);
#94283=ADVANCED_FACE('',(#11819),#4021,.T.);
#94284=ADVANCED_FACE('',(#11820),#88640,.T.);
#94285=ADVANCED_FACE('',(#11821),#4022,.T.);
#94286=ADVANCED_FACE('',(#11822),#5099,.T.);
#94287=ADVANCED_FACE('',(#11823),#6096,.F.);
#94288=ADVANCED_FACE('',(#11824),#6097,.F.);
#94289=ADVANCED_FACE('',(#11825),#88641,.F.);
#94290=ADVANCED_FACE('',(#11826),#4023,.F.);
#94291=ADVANCED_FACE('',(#11827),#4024,.F.);
#94292=ADVANCED_FACE('',(#11828),#4025,.F.);
#94293=ADVANCED_FACE('',(#11829),#4026,.T.);
#94294=ADVANCED_FACE('',(#11830),#88642,.T.);
#94295=ADVANCED_FACE('',(#11831),#4027,.T.);
#94296=ADVANCED_FACE('',(#11832),#4028,.T.);
#94297=ADVANCED_FACE('',(#11833),#4029,.T.);
#94298=ADVANCED_FACE('',(#11834),#4030,.T.);
#94299=ADVANCED_FACE('',(#11835),#4031,.T.);
#94300=ADVANCED_FACE('',(#11836),#88643,.T.);
#94301=ADVANCED_FACE('',(#11837),#4032,.T.);
#94302=ADVANCED_FACE('',(#11838),#5100,.T.);
#94303=ADVANCED_FACE('',(#11839),#6098,.F.);
#94304=ADVANCED_FACE('',(#11840),#6099,.F.);
#94305=ADVANCED_FACE('',(#11841),#88644,.F.);
#94306=ADVANCED_FACE('',(#11842),#4033,.F.);
#94307=ADVANCED_FACE('',(#11843),#4034,.F.);
#94308=ADVANCED_FACE('',(#11844),#4035,.F.);
#94309=ADVANCED_FACE('',(#11845),#4036,.T.);
#94310=ADVANCED_FACE('',(#11846),#88645,.T.);
#94311=ADVANCED_FACE('',(#11847),#4037,.T.);
#94312=ADVANCED_FACE('',(#11848),#4038,.T.);
#94313=ADVANCED_FACE('',(#11849),#4039,.T.);
#94314=ADVANCED_FACE('',(#11850),#4040,.T.);
#94315=ADVANCED_FACE('',(#11851),#4041,.T.);
#94316=ADVANCED_FACE('',(#11852),#88646,.T.);
#94317=ADVANCED_FACE('',(#11853),#4042,.T.);
#94318=ADVANCED_FACE('',(#11854),#5101,.T.);
#94319=ADVANCED_FACE('',(#11855),#6100,.F.);
#94320=ADVANCED_FACE('',(#11856),#6101,.F.);
#94321=ADVANCED_FACE('',(#11857),#88647,.F.);
#94322=ADVANCED_FACE('',(#11858),#4043,.F.);
#94323=ADVANCED_FACE('',(#11859),#4044,.F.);
#94324=ADVANCED_FACE('',(#11860),#4045,.F.);
#94325=ADVANCED_FACE('',(#11861),#4046,.T.);
#94326=ADVANCED_FACE('',(#11862),#88648,.T.);
#94327=ADVANCED_FACE('',(#11863),#4047,.T.);
#94328=ADVANCED_FACE('',(#11864),#4048,.T.);
#94329=ADVANCED_FACE('',(#11865),#4049,.T.);
#94330=ADVANCED_FACE('',(#11866),#4050,.T.);
#94331=ADVANCED_FACE('',(#11867),#4051,.T.);
#94332=ADVANCED_FACE('',(#11868),#88649,.T.);
#94333=ADVANCED_FACE('',(#11869),#4052,.T.);
#94334=ADVANCED_FACE('',(#11870),#5102,.T.);
#94335=ADVANCED_FACE('',(#11871),#6102,.F.);
#94336=ADVANCED_FACE('',(#11872),#6103,.F.);
#94337=ADVANCED_FACE('',(#11873),#88650,.F.);
#94338=ADVANCED_FACE('',(#11874),#4053,.F.);
#94339=ADVANCED_FACE('',(#11875),#4054,.F.);
#94340=ADVANCED_FACE('',(#11876),#4055,.F.);
#94341=ADVANCED_FACE('',(#11877),#4056,.T.);
#94342=ADVANCED_FACE('',(#11878),#88651,.T.);
#94343=ADVANCED_FACE('',(#11879),#4057,.T.);
#94344=ADVANCED_FACE('',(#11880),#4058,.T.);
#94345=ADVANCED_FACE('',(#11881),#4059,.T.);
#94346=ADVANCED_FACE('',(#11882),#4060,.T.);
#94347=ADVANCED_FACE('',(#11883),#4061,.T.);
#94348=ADVANCED_FACE('',(#11884),#88652,.T.);
#94349=ADVANCED_FACE('',(#11885),#4062,.T.);
#94350=ADVANCED_FACE('',(#11886),#5103,.T.);
#94351=ADVANCED_FACE('',(#11887),#6104,.F.);
#94352=ADVANCED_FACE('',(#11888),#6105,.F.);
#94353=ADVANCED_FACE('',(#11889),#88653,.F.);
#94354=ADVANCED_FACE('',(#11890),#4063,.F.);
#94355=ADVANCED_FACE('',(#11891),#4064,.F.);
#94356=ADVANCED_FACE('',(#11892),#4065,.F.);
#94357=ADVANCED_FACE('',(#11893),#4066,.T.);
#94358=ADVANCED_FACE('',(#11894),#88654,.T.);
#94359=ADVANCED_FACE('',(#11895),#4067,.T.);
#94360=ADVANCED_FACE('',(#11896),#4068,.T.);
#94361=ADVANCED_FACE('',(#11897),#4069,.T.);
#94362=ADVANCED_FACE('',(#11898),#4070,.T.);
#94363=ADVANCED_FACE('',(#11899),#4071,.T.);
#94364=ADVANCED_FACE('',(#11900),#88655,.T.);
#94365=ADVANCED_FACE('',(#11901),#4072,.T.);
#94366=ADVANCED_FACE('',(#11902),#5104,.T.);
#94666=CLOSED_SHELL('',(#92873,#92874,#92875,#92876,#92877,#92878,#92879,
#92880,#92881,#92882,#92883,#92884,#92885,#92886,#92887,#92888,#92889,#92890,
#92891,#92892,#92893,#92894,#92895,#92896,#92897,#92898,#92899,#92900,#92901,
#92902,#92903,#92904,#92905,#92906,#92907,#92908,#92909,#92910,#92911,#92912,
#92913,#92914,#92915,#92916,#92917,#92918,#92919,#92920,#92921,#92922,#92923,
#92924,#92925,#92926,#92927,#92928,#92929,#92930,#92931,#92932,#92933,#92934,
#92935,#92936,#92937,#92938,#92939,#92940,#92941,#92942,#92943,#92944,#92945,
#92946,#92947,#92948,#92949,#92950,#92951,#92952,#92953,#92954,#92955,#92956,
#92957,#92958,#92959,#92960,#92961,#92962,#92963,#92964,#92965,#92966,#92967,
#92968,#92969,#92970,#92971,#92972,#92973,#92974,#92975,#92976,#92977,#92978,
#92979,#92980,#92981,#92982,#92983,#92984,#92985,#92986,#92987,#92988,#92989,
#92990,#92991,#92992,#92993,#92994,#92995,#92996,#92997,#92998,#92999,#93000,
#93001,#93002,#93003,#93004,#93005,#93006,#93007,#93008,#93009,#93010,#93011,
#93012,#93013,#93014,#93015,#93016,#93017,#93018,#93019,#93020,#93021,#93022,
#93023,#93024,#93025,#93026,#93027,#93028,#93029,#93030,#93031,#93032,#93033,
#93034,#93035,#93036,#93037,#93038,#93039,#93040,#93041,#93042,#93043,#93044,
#93045,#93046,#93047,#93048,#93049,#93050,#93051,#93052,#93053,#93054,#93055,
#93056,#93057,#93058,#93059,#93060,#93061,#93062,#93063,#93064,#93065,#93066,
#93067,#93068,#93069,#93070,#93071,#93072,#93073,#93074,#93075,#93076,#93077,
#93078,#93079,#93080,#93081,#93082,#93083,#93084,#93085,#93086,#93087,#93088,
#93089,#93090,#93091,#93092,#93093,#93094,#93095,#93096,#93097,#93098,#93099,
#93100,#93101,#93102,#93103,#93104,#93105,#93106,#93107,#93108,#93109,#93110,
#93111,#93112,#93113,#93114,#93115,#93116,#93117,#93118,#93119,#93120,#93121,
#93122,#93123,#93124,#93125,#93126,#93127,#93128,#93129,#93130,#93131,#93132,
#93133,#93134,#93135,#93136,#93137,#93138,#93139,#93140,#93141,#93142,#93143,
#93144,#93145,#93146,#93147,#93148,#93149,#93150,#93151,#93152,#93153,#93154,
#93155,#93156,#93157,#93158,#93159,#93160,#93161,#93162,#93163,#93164,#93165,
#93166,#93167,#93168,#93169,#93170,#93171,#93172,#93173,#93174,#93175,#93176,
#93177,#93178,#93179,#93180,#93181,#93182,#93183,#93184,#93185,#93186,#93187,
#93188,#93189,#93190,#93191,#93192,#93193,#93194,#93195,#93196,#93197,#93198,
#93199,#93200,#93201,#93202,#93203,#93204,#93205,#93206,#93207,#93208,#93209,
#93210,#93211,#93212,#93213,#93214,#93215,#93216,#93217,#93218,#93219,#93220,
#93221,#93222,#93223,#93224,#93225,#93226,#93227,#93228,#93229,#93230,#93231,
#93232,#93233,#93234,#93235,#93236,#93237,#93238,#93239,#93240,#93241,#93242,
#93243,#93244,#93245,#93246,#93247,#93248,#93249,#93250,#93251,#93252,#93253,
#93254,#93255,#93256,#93257,#93258,#93259,#93260,#93261,#93262,#93263,#93264,
#93265,#93266,#93267,#93268,#93269,#93270,#93271,#93272,#93273,#93274,#93275,
#93276,#93277,#93278,#93279,#93280,#93281,#93282,#93283,#93284,#93285,#93286,
#93287,#93288,#93289,#93290,#93291,#93292,#93293,#93294,#93295,#93296,#93297,
#93298,#93299,#93300,#93301,#93302,#93303,#93304,#93305,#93306,#93307,#93308,
#93309,#93310,#93311,#93312,#93313,#93314,#93315,#93316,#93317,#93318,#93319,
#93320,#93321,#93322,#93323,#93324,#93325,#93326,#93327,#93328,#93329,#93330,
#93331,#93332,#93333,#93334,#93335,#93336,#93337,#93338,#93339,#93340,#93341,
#93342,#93343,#93344,#93345,#93346,#93347,#93348,#93349,#93350,#93351,#93352,
#93353,#93354,#93355,#93356,#93357,#93358,#93359,#93360,#93361,#93362,#93363,
#93364,#93365,#93366,#93367,#93368,#93369,#93370,#93371,#93372,#93373,#93374,
#93375,#93376,#93377,#93378,#93379,#93380,#93381,#93382,#93383,#93384,#93385,
#93386,#93387,#93388,#93389,#93390,#93391,#93392,#93393,#93394,#93395,#93396,
#93397,#93398,#93399,#93400,#93401,#93402,#93403,#93404,#93405,#93406,#93407,
#93408,#93409,#93410,#93411,#93412,#93413,#93414,#93415,#93416,#93417,#93418,
#93419,#93420,#93421,#93422,#93423,#93424,#93425,#93426,#93427,#93428,#93429,
#93430,#93431,#93432,#93433,#93434,#93435,#93436,#93437,#93438,#93439,#93440,
#93441,#93442,#93443,#93444,#93445,#93446,#93447,#93448,#93449,#93450,#93451,
#93452,#93453,#93454,#93455,#93456,#93457,#93458,#93459,#93460,#93461,#93462,
#93463,#93464,#93465,#93466,#93467,#93468,#93469,#93470,#93471,#93472,#93473,
#93474,#93475,#93476,#93477,#93478,#93479,#93480,#93481,#93482,#93483,#93484,
#93485,#93486,#93487,#93488,#93489,#93490,#93491,#93492,#93493,#93494,#93495,
#93496,#93497,#93498,#93499,#93500,#93501,#93502,#93503,#93504,#93505,#93506,
#93507,#93508,#93509,#93510,#93511,#93512,#93513,#93514,#93515,#93516,#93517,
#93518,#93519,#93520,#93521,#93522,#93523,#93524,#93525,#93526,#93527,#93528,
#93529,#93530,#93531,#93532,#93533,#93534,#93535,#93536,#93537,#93538,#93539,
#93540,#93541,#93542,#93543,#93544,#93545,#93546,#93547,#93548,#93549,#93550,
#93551,#93552,#93553,#93554,#93555,#93556,#93557,#93558,#93559,#93560,#93561,
#93562,#93563,#93564,#93565,#93566,#93567,#93568,#93569,#93570,#93571,#93572,
#93573,#93574,#93575,#93576,#93577,#93578,#93579,#93580,#93581,#93582,#93583,
#93584,#93585,#93586,#93587,#93588,#93589,#93590,#93591,#93592,#93593,#93594,
#93595,#93596,#93597,#93598,#93599,#93600,#93601,#93602,#93603,#93604,#93605,
#93606,#93607,#93608,#93609,#93610,#93611,#93612,#93613,#93614,#93615,#93616,
#93617,#93618,#93619,#93620,#93621,#93622,#93623,#93624,#93625,#93626,#93627,
#93628,#93629,#93630,#93631,#93632,#93633,#93634,#93635,#93636,#93637,#93638,
#93639,#93640,#93641,#93642,#93643,#93644,#93645,#93646,#93647,#93648,#93649,
#93650,#93651,#93652,#93653,#93654,#93655,#93656,#93657,#93658,#93659,#93660,
#93661,#93662,#93663,#93664,#93665,#93666,#93667,#93668,#93669,#93670,#93671,
#93672,#93673,#93674,#93675,#93676,#93677,#93678,#93679,#93680,#93681,#93682,
#93683,#93684,#93685,#93686,#93687,#93688,#93689,#93690,#93691,#93692,#93693,
#93694,#93695,#93696,#93697,#93698,#93699,#93700,#93701,#93702,#93703,#93704,
#93705,#93706,#93707,#93708,#93709,#93710,#93711,#93712,#93713,#93714,#93715,
#93716,#93717,#93718,#93719,#93720,#93721,#93722,#93723,#93724,#93725,#93726,
#93727,#93728,#93729,#93730,#93731,#93732,#93733,#93734,#93735,#93736,#93737,
#93738,#93739,#93740,#93741,#93742,#93743,#93744,#93745,#93746,#93747,#93748,
#93749,#93750,#93751,#93752,#93753,#93754,#93755,#93756,#93757,#93758,#93759,
#93760,#93761,#93762,#93763,#93764,#93765,#93766,#93767,#93768,#93769,#93770,
#93771,#93772,#93773,#93774,#93775,#93776,#93777,#93778,#93779,#93780,#93781,
#93782,#93783,#93784,#93785,#93786,#93787,#93788,#93789,#93790,#93791,#93792,
#93793,#93794,#93795,#93796,#93797,#93798,#93799,#93800,#93801,#93802,#93803,
#93804,#93805,#93806,#93807,#93808,#93809,#93810,#93811,#93812,#93813,#93814,
#93815,#93816,#93817,#93818,#93819,#93820,#93821,#93822,#93823,#93824,#93825,
#93826,#93827,#93828,#93829,#93830,#93831,#93832,#93833,#93834,#93835,#93836,
#93837,#93838,#93839,#93840,#93841,#93842,#93843,#93844,#93845,#93846,#93847,
#93848,#93849,#93850,#93851,#93852,#93853,#93854,#93855,#93856,#93857,#93858,
#93859,#93860,#93861,#93862,#93863,#93864,#93865,#93866,#93867,#93868,#93869,
#93870,#93871,#93872,#93873,#93874,#93875,#93876,#93877,#93878,#93879,#93880,
#93881,#93882,#93883,#93884,#93885,#93886,#93887,#93888,#93889,#93890,#93891,
#93892,#93893,#93894,#93895,#93896,#93897,#93898,#93899,#93900,#93901,#93902,
#93903,#93904,#93905,#93906,#93907,#93908,#93909,#93910,#93911,#93912,#93913,
#93914,#93915,#93916,#93917,#93918,#93919,#93920,#93921,#93922,#93923,#93924,
#93925,#93926,#93927,#93928,#93929,#93930,#93931,#93932,#93933,#93934,#93935,
#93936,#93937,#93938,#93939,#93940,#93941,#93942,#93943,#93944,#93945,#93946,
#93947,#93948,#93949,#93950,#93951,#93952,#93953,#93954,#93955,#93956,#93957,
#93958,#93959,#93960,#93961,#93962,#93963,#93964,#93965,#93966,#93967,#93968,
#93969,#93970,#93971,#93972,#93973,#93974,#93975,#93976,#93977,#93978,#93979,
#93980,#93981,#93982,#93983,#93984,#93985,#93986,#93987,#93988,#93989,#93990,
#93991,#93992,#93993,#93994,#93995,#93996,#93997,#93998,#93999,#94000,#94001,
#94002,#94003,#94004,#94005,#94006,#94007,#94008,#94009,#94010,#94011,#94012,
#94013,#94014,#94015,#94016,#94017,#94018,#94019,#94020,#94021,#94022,#94023,
#94024,#94025,#94026,#94027,#94028,#94029,#94030,#94031,#94032,#94033,#94034,
#94035,#94036,#94037,#94038,#94039,#94040,#94041,#94042,#94043,#94044,#94045,
#94046,#94047,#94048,#94049,#94050,#94051,#94052,#94053,#94054,#94055,#94056,
#94057,#94058,#94059,#94060,#94061,#94062,#94063,#94064,#94065,#94066,#94067,
#94068,#94069,#94070,#94071,#94072,#94073,#94074,#94075,#94076,#94077,#94078,
#94079,#94080,#94081,#94082,#94083,#94084,#94085,#94086,#94087,#94088,#94089,
#94090,#94091,#94092,#94093,#94094,#94095,#94096,#94097,#94098,#94099,#94100,
#94101,#94102,#94103,#94104,#94105,#94106,#94107,#94108,#94109,#94110,#94111,
#94112,#94113,#94114,#94115,#94116,#94117,#94118,#94119,#94120,#94121,#94122,
#94123,#94124,#94125,#94126,#94127,#94128,#94129,#94130,#94131,#94132,#94133,
#94134,#94135,#94136,#94137,#94138,#94139,#94140,#94141,#94142,#94143,#94144,
#94145,#94146,#94147,#94148,#94149,#94150,#94151,#94152,#94153,#94154,#94155,
#94156,#94157,#94158,#94159,#94160,#94161,#94162,#94163,#94164,#94165,#94166,
#94167,#94168,#94169,#94170,#94171,#94172,#94173,#94174,#94175,#94176,#94177,
#94178,#94179,#94180,#94181,#94182,#94183,#94184,#94185,#94186,#94187,#94188,
#94189,#94190,#94191,#94192,#94193,#94194,#94195,#94196,#94197,#94198,#94199,
#94200,#94201,#94202,#94203,#94204,#94205,#94206,#94207,#94208,#94209,#94210,
#94211,#94212,#94213,#94214,#94215,#94216,#94217,#94218,#94219,#94220,#94221,
#94222,#94223,#94224,#94225,#94226,#94227,#94228,#94229,#94230,#94231,#94232,
#94233,#94234,#94235,#94236,#94237,#94238,#94239,#94240,#94241,#94242,#94243,
#94244,#94245,#94246,#94247,#94248,#94249,#94250,#94251,#94252,#94253,#94254,
#94255,#94256,#94257,#94258,#94259,#94260,#94261,#94262,#94263,#94264,#94265,
#94266,#94267,#94268,#94269,#94270,#94271,#94272,#94273,#94274,#94275,#94276,
#94277,#94278,#94279,#94280,#94281,#94282,#94283,#94284,#94285,#94286,#94287,
#94288,#94289,#94290,#94291,#94292,#94293,#94294,#94295,#94296,#94297,#94298,
#94299,#94300,#94301,#94302,#94303,#94304,#94305,#94306,#94307,#94308,#94309,
#94310,#94311,#94312,#94313,#94314,#94315,#94316,#94317,#94318,#94319,#94320,
#94321,#94322,#94323,#94324,#94325,#94326,#94327,#94328,#94329,#94330,#94331,
#94332,#94333,#94334,#94335,#94336,#94337,#94338,#94339,#94340,#94341,#94342,
#94343,#94344,#94345,#94346,#94347,#94348,#94349,#94350,#94351,#94352,#94353,
#94354,#94355,#94356,#94357,#94358,#94359,#94360,#94361,#94362,#94363,#94364,
#94365,#94366));
#102648=AXIS2_PLACEMENT_3D('',#409622,#123764,#123765);
#102649=AXIS2_PLACEMENT_3D('',#409623,#123766,#123767);
#102650=AXIS2_PLACEMENT_3D('',#409631,#123769,#123770);
#102651=AXIS2_PLACEMENT_3D('',#409632,#123771,#123772);
#102652=AXIS2_PLACEMENT_3D('',#409662,#123774,#123775);
#102653=AXIS2_PLACEMENT_3D('',#409692,#123777,#123778);
#102654=AXIS2_PLACEMENT_3D('',#409722,#123780,#123781);
#102655=AXIS2_PLACEMENT_3D('',#409752,#123783,#123784);
#102656=AXIS2_PLACEMENT_3D('',#409782,#123786,#123787);
#102657=AXIS2_PLACEMENT_3D('',#409812,#123789,#123790);
#102658=AXIS2_PLACEMENT_3D('',#409842,#123792,#123793);
#102659=AXIS2_PLACEMENT_3D('',#409872,#123795,#123796);
#102660=AXIS2_PLACEMENT_3D('',#409902,#123798,#123799);
#102661=AXIS2_PLACEMENT_3D('',#409932,#123801,#123802);
#102662=AXIS2_PLACEMENT_3D('',#409962,#123804,#123805);
#102663=AXIS2_PLACEMENT_3D('',#409992,#123807,#123808);
#102664=AXIS2_PLACEMENT_3D('',#410022,#123810,#123811);
#102665=AXIS2_PLACEMENT_3D('',#410052,#123813,#123814);
#102666=AXIS2_PLACEMENT_3D('',#410082,#123816,#123817);
#102667=AXIS2_PLACEMENT_3D('',#410112,#123819,#123820);
#102668=AXIS2_PLACEMENT_3D('',#410142,#123822,#123823);
#102669=AXIS2_PLACEMENT_3D('',#410172,#123825,#123826);
#102670=AXIS2_PLACEMENT_3D('',#410202,#123828,#123829);
#102671=AXIS2_PLACEMENT_3D('',#410232,#123831,#123832);
#102672=AXIS2_PLACEMENT_3D('',#410262,#123834,#123835);
#102673=AXIS2_PLACEMENT_3D('',#410292,#123837,#123838);
#102674=AXIS2_PLACEMENT_3D('',#410322,#123840,#123841);
#102675=AXIS2_PLACEMENT_3D('',#410352,#123843,#123844);
#102676=AXIS2_PLACEMENT_3D('',#410382,#123846,#123847);
#102677=AXIS2_PLACEMENT_3D('',#410412,#123849,#123850);
#102678=AXIS2_PLACEMENT_3D('',#410442,#123852,#123853);
#102679=AXIS2_PLACEMENT_3D('',#410472,#123855,#123856);
#102680=AXIS2_PLACEMENT_3D('',#410502,#123858,#123859);
#102681=AXIS2_PLACEMENT_3D('',#410532,#123861,#123862);
#102682=AXIS2_PLACEMENT_3D('',#410562,#123864,#123865);
#102683=AXIS2_PLACEMENT_3D('',#410592,#123867,#123868);
#102684=AXIS2_PLACEMENT_3D('',#410622,#123870,#123871);
#102685=AXIS2_PLACEMENT_3D('',#410652,#123873,#123874);
#102686=AXIS2_PLACEMENT_3D('',#410682,#123876,#123877);
#102687=AXIS2_PLACEMENT_3D('',#410702,#123879,#123880);
#102688=AXIS2_PLACEMENT_3D('',#410713,#123881,#123882);
#102689=AXIS2_PLACEMENT_3D('',#410737,#123884,#123885);
#102690=AXIS2_PLACEMENT_3D('',#410738,#123886,#123887);
#102691=AXIS2_PLACEMENT_3D('',#410762,#123889,#123890);
#102692=AXIS2_PLACEMENT_3D('',#410779,#123891,#123892);
#102693=AXIS2_PLACEMENT_3D('',#410855,#123894,#123895);
#102694=AXIS2_PLACEMENT_3D('',#410933,#123897,#123898);
#102695=AXIS2_PLACEMENT_3D('',#411011,#123900,#123901);
#102696=AXIS2_PLACEMENT_3D('',#411087,#123903,#123904);
#102697=AXIS2_PLACEMENT_3D('',#411163,#123906,#123907);
#102698=AXIS2_PLACEMENT_3D('',#411239,#123909,#123910);
#102699=AXIS2_PLACEMENT_3D('',#411317,#123912,#123913);
#102700=AXIS2_PLACEMENT_3D('',#411393,#123915,#123916);
#102701=AXIS2_PLACEMENT_3D('',#411469,#123918,#123919);
#102702=AXIS2_PLACEMENT_3D('',#411547,#123921,#123922);
#102703=AXIS2_PLACEMENT_3D('',#411623,#123924,#123925);
#102704=AXIS2_PLACEMENT_3D('',#411699,#123927,#123928);
#102705=AXIS2_PLACEMENT_3D('',#411775,#123930,#123931);
#102706=AXIS2_PLACEMENT_3D('',#411853,#123933,#123934);
#102707=AXIS2_PLACEMENT_3D('',#411929,#123936,#123937);
#102708=AXIS2_PLACEMENT_3D('',#412005,#123939,#123940);
#102709=AXIS2_PLACEMENT_3D('',#412083,#123942,#123943);
#102710=AXIS2_PLACEMENT_3D('',#412159,#123945,#123946);
#102711=AXIS2_PLACEMENT_3D('',#412235,#123948,#123949);
#102712=AXIS2_PLACEMENT_3D('',#412313,#123951,#123952);
#102713=AXIS2_PLACEMENT_3D('',#412389,#123954,#123955);
#102714=AXIS2_PLACEMENT_3D('',#412465,#123957,#123958);
#102715=AXIS2_PLACEMENT_3D('',#412543,#123960,#123961);
#102716=AXIS2_PLACEMENT_3D('',#412619,#123963,#123964);
#102717=AXIS2_PLACEMENT_3D('',#412695,#123966,#123967);
#102718=AXIS2_PLACEMENT_3D('',#412771,#123969,#123970);
#102719=AXIS2_PLACEMENT_3D('',#412849,#123972,#123973);
#102720=AXIS2_PLACEMENT_3D('',#412925,#123975,#123976);
#102721=AXIS2_PLACEMENT_3D('',#413001,#123978,#123979);
#102722=AXIS2_PLACEMENT_3D('',#413079,#123981,#123982);
#102723=AXIS2_PLACEMENT_3D('',#413160,#123984,#123985);
#102724=AXIS2_PLACEMENT_3D('',#413236,#123987,#123988);
#102725=AXIS2_PLACEMENT_3D('',#413314,#123990,#123991);
#102726=AXIS2_PLACEMENT_3D('',#413316,#123992,#123993);
#102727=AXIS2_PLACEMENT_3D('',#413319,#123995,#123996);
#102728=AXIS2_PLACEMENT_3D('',#413391,#123998,#123999);
#102729=AXIS2_PLACEMENT_3D('',#413394,#124000,#124001);
#102730=AXIS2_PLACEMENT_3D('',#413396,#124002,#124003);
#102731=AXIS2_PLACEMENT_3D('',#413398,#124004,#124005);
#102732=AXIS2_PLACEMENT_3D('',#413399,#124006,#124007);
#102733=AXIS2_PLACEMENT_3D('',#413400,#124008,#124009);
#102734=AXIS2_PLACEMENT_3D('',#413403,#124010,#124011);
#102735=AXIS2_PLACEMENT_3D('',#413405,#124012,#124013);
#102736=AXIS2_PLACEMENT_3D('',#413407,#124014,#124015);
#102737=AXIS2_PLACEMENT_3D('',#413408,#124016,#124017);
#102738=AXIS2_PLACEMENT_3D('',#413409,#124018,#124019);
#102739=AXIS2_PLACEMENT_3D('',#413412,#124020,#124021);
#102740=AXIS2_PLACEMENT_3D('',#413414,#124022,#124023);
#102741=AXIS2_PLACEMENT_3D('',#413416,#124024,#124025);
#102742=AXIS2_PLACEMENT_3D('',#413417,#124026,#124027);
#102743=AXIS2_PLACEMENT_3D('',#413418,#124028,#124029);
#102744=AXIS2_PLACEMENT_3D('',#413421,#124030,#124031);
#102745=AXIS2_PLACEMENT_3D('',#413423,#124032,#124033);
#102746=AXIS2_PLACEMENT_3D('',#413425,#124034,#124035);
#102747=AXIS2_PLACEMENT_3D('',#413426,#124036,#124037);
#102748=AXIS2_PLACEMENT_3D('',#413427,#124038,#124039);
#102749=AXIS2_PLACEMENT_3D('',#413430,#124040,#124041);
#102750=AXIS2_PLACEMENT_3D('',#413432,#124042,#124043);
#102751=AXIS2_PLACEMENT_3D('',#413434,#124044,#124045);
#102752=AXIS2_PLACEMENT_3D('',#413435,#124046,#124047);
#102753=AXIS2_PLACEMENT_3D('',#413436,#124048,#124049);
#102754=AXIS2_PLACEMENT_3D('',#413439,#124050,#124051);
#102755=AXIS2_PLACEMENT_3D('',#413441,#124052,#124053);
#102756=AXIS2_PLACEMENT_3D('',#413443,#124054,#124055);
#102757=AXIS2_PLACEMENT_3D('',#413444,#124056,#124057);
#102758=AXIS2_PLACEMENT_3D('',#413445,#124058,#124059);
#102759=AXIS2_PLACEMENT_3D('',#413448,#124060,#124061);
#102760=AXIS2_PLACEMENT_3D('',#413450,#124062,#124063);
#102761=AXIS2_PLACEMENT_3D('',#413452,#124064,#124065);
#102762=AXIS2_PLACEMENT_3D('',#413453,#124066,#124067);
#102763=AXIS2_PLACEMENT_3D('',#413454,#124068,#124069);
#102764=AXIS2_PLACEMENT_3D('',#413457,#124070,#124071);
#102765=AXIS2_PLACEMENT_3D('',#413459,#124072,#124073);
#102766=AXIS2_PLACEMENT_3D('',#413461,#124074,#124075);
#102767=AXIS2_PLACEMENT_3D('',#413462,#124076,#124077);
#102768=AXIS2_PLACEMENT_3D('',#413463,#124078,#124079);
#102769=AXIS2_PLACEMENT_3D('',#413466,#124080,#124081);
#102770=AXIS2_PLACEMENT_3D('',#413468,#124082,#124083);
#102771=AXIS2_PLACEMENT_3D('',#413470,#124084,#124085);
#102772=AXIS2_PLACEMENT_3D('',#413471,#124086,#124087);
#102773=AXIS2_PLACEMENT_3D('',#413472,#124088,#124089);
#102774=AXIS2_PLACEMENT_3D('',#413475,#124090,#124091);
#102775=AXIS2_PLACEMENT_3D('',#413477,#124092,#124093);
#102776=AXIS2_PLACEMENT_3D('',#413479,#124094,#124095);
#102777=AXIS2_PLACEMENT_3D('',#413480,#124096,#124097);
#102778=AXIS2_PLACEMENT_3D('',#413481,#124098,#124099);
#102779=AXIS2_PLACEMENT_3D('',#413484,#124100,#124101);
#102780=AXIS2_PLACEMENT_3D('',#413486,#124102,#124103);
#102781=AXIS2_PLACEMENT_3D('',#413488,#124104,#124105);
#102782=AXIS2_PLACEMENT_3D('',#413489,#124106,#124107);
#102783=AXIS2_PLACEMENT_3D('',#413490,#124108,#124109);
#102784=AXIS2_PLACEMENT_3D('',#413493,#124110,#124111);
#102785=AXIS2_PLACEMENT_3D('',#413495,#124112,#124113);
#102786=AXIS2_PLACEMENT_3D('',#413497,#124114,#124115);
#102787=AXIS2_PLACEMENT_3D('',#413498,#124116,#124117);
#102788=AXIS2_PLACEMENT_3D('',#413499,#124118,#124119);
#102789=AXIS2_PLACEMENT_3D('',#413502,#124120,#124121);
#102790=AXIS2_PLACEMENT_3D('',#413504,#124122,#124123);
#102791=AXIS2_PLACEMENT_3D('',#413506,#124124,#124125);
#102792=AXIS2_PLACEMENT_3D('',#413507,#124126,#124127);
#102793=AXIS2_PLACEMENT_3D('',#413508,#124128,#124129);
#102794=AXIS2_PLACEMENT_3D('',#413511,#124130,#124131);
#102795=AXIS2_PLACEMENT_3D('',#413513,#124132,#124133);
#102796=AXIS2_PLACEMENT_3D('',#413515,#124134,#124135);
#102797=AXIS2_PLACEMENT_3D('',#413516,#124136,#124137);
#102798=AXIS2_PLACEMENT_3D('',#413517,#124138,#124139);
#102799=AXIS2_PLACEMENT_3D('',#413520,#124140,#124141);
#102800=AXIS2_PLACEMENT_3D('',#413522,#124142,#124143);
#102801=AXIS2_PLACEMENT_3D('',#413524,#124144,#124145);
#102802=AXIS2_PLACEMENT_3D('',#413525,#124146,#124147);
#102803=AXIS2_PLACEMENT_3D('',#413526,#124148,#124149);
#102804=AXIS2_PLACEMENT_3D('',#413529,#124150,#124151);
#102805=AXIS2_PLACEMENT_3D('',#413531,#124152,#124153);
#102806=AXIS2_PLACEMENT_3D('',#413533,#124154,#124155);
#102807=AXIS2_PLACEMENT_3D('',#413534,#124156,#124157);
#102808=AXIS2_PLACEMENT_3D('',#413535,#124158,#124159);
#102809=AXIS2_PLACEMENT_3D('',#413538,#124160,#124161);
#102810=AXIS2_PLACEMENT_3D('',#413540,#124162,#124163);
#102811=AXIS2_PLACEMENT_3D('',#413542,#124164,#124165);
#102812=AXIS2_PLACEMENT_3D('',#413543,#124166,#124167);
#102813=AXIS2_PLACEMENT_3D('',#413544,#124168,#124169);
#102814=AXIS2_PLACEMENT_3D('',#413547,#124170,#124171);
#102815=AXIS2_PLACEMENT_3D('',#413549,#124172,#124173);
#102816=AXIS2_PLACEMENT_3D('',#413551,#124174,#124175);
#102817=AXIS2_PLACEMENT_3D('',#413552,#124176,#124177);
#102818=AXIS2_PLACEMENT_3D('',#413553,#124178,#124179);
#102819=AXIS2_PLACEMENT_3D('',#413556,#124180,#124181);
#102820=AXIS2_PLACEMENT_3D('',#413558,#124182,#124183);
#102821=AXIS2_PLACEMENT_3D('',#413560,#124184,#124185);
#102822=AXIS2_PLACEMENT_3D('',#413561,#124186,#124187);
#102823=AXIS2_PLACEMENT_3D('',#413562,#124188,#124189);
#102824=AXIS2_PLACEMENT_3D('',#413565,#124190,#124191);
#102825=AXIS2_PLACEMENT_3D('',#413567,#124192,#124193);
#102826=AXIS2_PLACEMENT_3D('',#413569,#124194,#124195);
#102827=AXIS2_PLACEMENT_3D('',#413570,#124196,#124197);
#102828=AXIS2_PLACEMENT_3D('',#413571,#124198,#124199);
#102829=AXIS2_PLACEMENT_3D('',#413574,#124200,#124201);
#102830=AXIS2_PLACEMENT_3D('',#413576,#124202,#124203);
#102831=AXIS2_PLACEMENT_3D('',#413578,#124204,#124205);
#102832=AXIS2_PLACEMENT_3D('',#413579,#124206,#124207);
#102833=AXIS2_PLACEMENT_3D('',#413580,#124208,#124209);
#102834=AXIS2_PLACEMENT_3D('',#413583,#124210,#124211);
#102835=AXIS2_PLACEMENT_3D('',#413585,#124212,#124213);
#102836=AXIS2_PLACEMENT_3D('',#413587,#124214,#124215);
#102837=AXIS2_PLACEMENT_3D('',#413588,#124216,#124217);
#102838=AXIS2_PLACEMENT_3D('',#413589,#124218,#124219);
#102839=AXIS2_PLACEMENT_3D('',#413592,#124220,#124221);
#102840=AXIS2_PLACEMENT_3D('',#413594,#124222,#124223);
#102841=AXIS2_PLACEMENT_3D('',#413596,#124224,#124225);
#102842=AXIS2_PLACEMENT_3D('',#413597,#124226,#124227);
#102843=AXIS2_PLACEMENT_3D('',#413598,#124228,#124229);
#102844=AXIS2_PLACEMENT_3D('',#413601,#124230,#124231);
#102845=AXIS2_PLACEMENT_3D('',#413603,#124232,#124233);
#102846=AXIS2_PLACEMENT_3D('',#413605,#124234,#124235);
#102847=AXIS2_PLACEMENT_3D('',#413606,#124236,#124237);
#102848=AXIS2_PLACEMENT_3D('',#413607,#124238,#124239);
#102849=AXIS2_PLACEMENT_3D('',#413610,#124240,#124241);
#102850=AXIS2_PLACEMENT_3D('',#413612,#124242,#124243);
#102851=AXIS2_PLACEMENT_3D('',#413614,#124244,#124245);
#102852=AXIS2_PLACEMENT_3D('',#413615,#124246,#124247);
#102853=AXIS2_PLACEMENT_3D('',#413616,#124248,#124249);
#102854=AXIS2_PLACEMENT_3D('',#413619,#124250,#124251);
#102855=AXIS2_PLACEMENT_3D('',#413621,#124252,#124253);
#102856=AXIS2_PLACEMENT_3D('',#413623,#124254,#124255);
#102857=AXIS2_PLACEMENT_3D('',#413624,#124256,#124257);
#102858=AXIS2_PLACEMENT_3D('',#413625,#124258,#124259);
#102859=AXIS2_PLACEMENT_3D('',#413628,#124260,#124261);
#102860=AXIS2_PLACEMENT_3D('',#413630,#124262,#124263);
#102861=AXIS2_PLACEMENT_3D('',#413632,#124264,#124265);
#102862=AXIS2_PLACEMENT_3D('',#413633,#124266,#124267);
#102863=AXIS2_PLACEMENT_3D('',#413634,#124268,#124269);
#102864=AXIS2_PLACEMENT_3D('',#413637,#124270,#124271);
#102865=AXIS2_PLACEMENT_3D('',#413639,#124272,#124273);
#102866=AXIS2_PLACEMENT_3D('',#413641,#124274,#124275);
#102867=AXIS2_PLACEMENT_3D('',#413642,#124276,#124277);
#102868=AXIS2_PLACEMENT_3D('',#413643,#124278,#124279);
#102869=AXIS2_PLACEMENT_3D('',#413646,#124280,#124281);
#102870=AXIS2_PLACEMENT_3D('',#413648,#124282,#124283);
#102871=AXIS2_PLACEMENT_3D('',#413650,#124284,#124285);
#102872=AXIS2_PLACEMENT_3D('',#413651,#124286,#124287);
#102873=AXIS2_PLACEMENT_3D('',#413652,#124288,#124289);
#102874=AXIS2_PLACEMENT_3D('',#413655,#124290,#124291);
#102875=AXIS2_PLACEMENT_3D('',#413657,#124292,#124293);
#102876=AXIS2_PLACEMENT_3D('',#413659,#124294,#124295);
#102877=AXIS2_PLACEMENT_3D('',#413660,#124296,#124297);
#102878=AXIS2_PLACEMENT_3D('',#413661,#124298,#124299);
#102879=AXIS2_PLACEMENT_3D('',#413664,#124300,#124301);
#102880=AXIS2_PLACEMENT_3D('',#413666,#124302,#124303);
#102881=AXIS2_PLACEMENT_3D('',#413668,#124304,#124305);
#102882=AXIS2_PLACEMENT_3D('',#413669,#124306,#124307);
#102883=AXIS2_PLACEMENT_3D('',#413670,#124308,#124309);
#102884=AXIS2_PLACEMENT_3D('',#413673,#124310,#124311);
#102885=AXIS2_PLACEMENT_3D('',#413675,#124312,#124313);
#102886=AXIS2_PLACEMENT_3D('',#413677,#124314,#124315);
#102887=AXIS2_PLACEMENT_3D('',#413678,#124316,#124317);
#102888=AXIS2_PLACEMENT_3D('',#413679,#124318,#124319);
#102889=AXIS2_PLACEMENT_3D('',#413682,#124320,#124321);
#102890=AXIS2_PLACEMENT_3D('',#413684,#124322,#124323);
#102891=AXIS2_PLACEMENT_3D('',#413686,#124324,#124325);
#102892=AXIS2_PLACEMENT_3D('',#413687,#124326,#124327);
#102893=AXIS2_PLACEMENT_3D('',#413688,#124328,#124329);
#102894=AXIS2_PLACEMENT_3D('',#413691,#124330,#124331);
#102895=AXIS2_PLACEMENT_3D('',#413693,#124332,#124333);
#102896=AXIS2_PLACEMENT_3D('',#413695,#124334,#124335);
#102897=AXIS2_PLACEMENT_3D('',#413696,#124336,#124337);
#102898=AXIS2_PLACEMENT_3D('',#413697,#124338,#124339);
#102899=AXIS2_PLACEMENT_3D('',#413700,#124340,#124341);
#102900=AXIS2_PLACEMENT_3D('',#413702,#124342,#124343);
#102901=AXIS2_PLACEMENT_3D('',#413704,#124344,#124345);
#102902=AXIS2_PLACEMENT_3D('',#413705,#124346,#124347);
#102903=AXIS2_PLACEMENT_3D('',#413706,#124348,#124349);
#102904=AXIS2_PLACEMENT_3D('',#413709,#124350,#124351);
#102905=AXIS2_PLACEMENT_3D('',#413711,#124352,#124353);
#102906=AXIS2_PLACEMENT_3D('',#413713,#124354,#124355);
#102907=AXIS2_PLACEMENT_3D('',#413714,#124356,#124357);
#102908=AXIS2_PLACEMENT_3D('',#413715,#124358,#124359);
#102909=AXIS2_PLACEMENT_3D('',#413718,#124360,#124361);
#102910=AXIS2_PLACEMENT_3D('',#413720,#124362,#124363);
#102911=AXIS2_PLACEMENT_3D('',#413722,#124364,#124365);
#102912=AXIS2_PLACEMENT_3D('',#413723,#124366,#124367);
#102913=AXIS2_PLACEMENT_3D('',#413724,#124368,#124369);
#102914=AXIS2_PLACEMENT_3D('',#413727,#124370,#124371);
#102915=AXIS2_PLACEMENT_3D('',#413729,#124372,#124373);
#102916=AXIS2_PLACEMENT_3D('',#413731,#124374,#124375);
#102917=AXIS2_PLACEMENT_3D('',#413732,#124376,#124377);
#102918=AXIS2_PLACEMENT_3D('',#413733,#124378,#124379);
#102919=AXIS2_PLACEMENT_3D('',#413736,#124380,#124381);
#102920=AXIS2_PLACEMENT_3D('',#413738,#124382,#124383);
#102921=AXIS2_PLACEMENT_3D('',#413740,#124384,#124385);
#102922=AXIS2_PLACEMENT_3D('',#413741,#124386,#124387);
#102923=AXIS2_PLACEMENT_3D('',#413742,#124388,#124389);
#102924=AXIS2_PLACEMENT_3D('',#413745,#124390,#124391);
#102925=AXIS2_PLACEMENT_3D('',#413747,#124392,#124393);
#102926=AXIS2_PLACEMENT_3D('',#413749,#124394,#124395);
#102927=AXIS2_PLACEMENT_3D('',#413750,#124396,#124397);
#102928=AXIS2_PLACEMENT_3D('',#413751,#124398,#124399);
#102929=AXIS2_PLACEMENT_3D('',#413754,#124400,#124401);
#102930=AXIS2_PLACEMENT_3D('',#413756,#124402,#124403);
#102931=AXIS2_PLACEMENT_3D('',#413758,#124404,#124405);
#102932=AXIS2_PLACEMENT_3D('',#413759,#124406,#124407);
#102933=AXIS2_PLACEMENT_3D('',#413760,#124408,#124409);
#102934=AXIS2_PLACEMENT_3D('',#413763,#124410,#124411);
#102935=AXIS2_PLACEMENT_3D('',#413765,#124412,#124413);
#102936=AXIS2_PLACEMENT_3D('',#413767,#124414,#124415);
#102937=AXIS2_PLACEMENT_3D('',#413768,#124416,#124417);
#102938=AXIS2_PLACEMENT_3D('',#413769,#124418,#124419);
#102939=AXIS2_PLACEMENT_3D('',#413772,#124420,#124421);
#102940=AXIS2_PLACEMENT_3D('',#413774,#124422,#124423);
#102941=AXIS2_PLACEMENT_3D('',#413776,#124424,#124425);
#102942=AXIS2_PLACEMENT_3D('',#413777,#124426,#124427);
#102943=AXIS2_PLACEMENT_3D('',#413778,#124428,#124429);
#102944=AXIS2_PLACEMENT_3D('',#413781,#124430,#124431);
#102945=AXIS2_PLACEMENT_3D('',#413783,#124432,#124433);
#102946=AXIS2_PLACEMENT_3D('',#413785,#124434,#124435);
#102947=AXIS2_PLACEMENT_3D('',#413786,#124436,#124437);
#102948=AXIS2_PLACEMENT_3D('',#413787,#124438,#124439);
#102949=AXIS2_PLACEMENT_3D('',#413790,#124440,#124441);
#102950=AXIS2_PLACEMENT_3D('',#413792,#124442,#124443);
#102951=AXIS2_PLACEMENT_3D('',#413794,#124444,#124445);
#102952=AXIS2_PLACEMENT_3D('',#413795,#124446,#124447);
#102953=AXIS2_PLACEMENT_3D('',#413796,#124448,#124449);
#102954=AXIS2_PLACEMENT_3D('',#413799,#124450,#124451);
#102955=AXIS2_PLACEMENT_3D('',#413801,#124452,#124453);
#102956=AXIS2_PLACEMENT_3D('',#413803,#124454,#124455);
#102957=AXIS2_PLACEMENT_3D('',#413804,#124456,#124457);
#102958=AXIS2_PLACEMENT_3D('',#413805,#124458,#124459);
#102959=AXIS2_PLACEMENT_3D('',#413808,#124460,#124461);
#102960=AXIS2_PLACEMENT_3D('',#413810,#124462,#124463);
#102961=AXIS2_PLACEMENT_3D('',#413812,#124464,#124465);
#102962=AXIS2_PLACEMENT_3D('',#413813,#124466,#124467);
#102963=AXIS2_PLACEMENT_3D('',#413814,#124468,#124469);
#102964=AXIS2_PLACEMENT_3D('',#413817,#124470,#124471);
#102965=AXIS2_PLACEMENT_3D('',#413819,#124472,#124473);
#102966=AXIS2_PLACEMENT_3D('',#413821,#124474,#124475);
#102967=AXIS2_PLACEMENT_3D('',#413822,#124476,#124477);
#102968=AXIS2_PLACEMENT_3D('',#413823,#124478,#124479);
#102969=AXIS2_PLACEMENT_3D('',#413826,#124480,#124481);
#102970=AXIS2_PLACEMENT_3D('',#413828,#124482,#124483);
#102971=AXIS2_PLACEMENT_3D('',#413830,#124484,#124485);
#102972=AXIS2_PLACEMENT_3D('',#413831,#124486,#124487);
#102973=AXIS2_PLACEMENT_3D('',#413832,#124488,#124489);
#102974=AXIS2_PLACEMENT_3D('',#413835,#124490,#124491);
#102975=AXIS2_PLACEMENT_3D('',#413837,#124492,#124493);
#102976=AXIS2_PLACEMENT_3D('',#413839,#124494,#124495);
#102977=AXIS2_PLACEMENT_3D('',#413840,#124496,#124497);
#102978=AXIS2_PLACEMENT_3D('',#413841,#124498,#124499);
#102979=AXIS2_PLACEMENT_3D('',#413844,#124500,#124501);
#102980=AXIS2_PLACEMENT_3D('',#413846,#124502,#124503);
#102981=AXIS2_PLACEMENT_3D('',#413848,#124504,#124505);
#102982=AXIS2_PLACEMENT_3D('',#413849,#124506,#124507);
#102983=AXIS2_PLACEMENT_3D('',#413850,#124508,#124509);
#102984=AXIS2_PLACEMENT_3D('',#413853,#124510,#124511);
#102985=AXIS2_PLACEMENT_3D('',#413855,#124512,#124513);
#102986=AXIS2_PLACEMENT_3D('',#413857,#124514,#124515);
#102987=AXIS2_PLACEMENT_3D('',#413858,#124516,#124517);
#102988=AXIS2_PLACEMENT_3D('',#413859,#124518,#124519);
#102989=AXIS2_PLACEMENT_3D('',#413862,#124520,#124521);
#102990=AXIS2_PLACEMENT_3D('',#413864,#124522,#124523);
#102991=AXIS2_PLACEMENT_3D('',#413866,#124524,#124525);
#102992=AXIS2_PLACEMENT_3D('',#413867,#124526,#124527);
#102993=AXIS2_PLACEMENT_3D('',#413868,#124528,#124529);
#102994=AXIS2_PLACEMENT_3D('',#413871,#124530,#124531);
#102995=AXIS2_PLACEMENT_3D('',#413873,#124532,#124533);
#102996=AXIS2_PLACEMENT_3D('',#413875,#124534,#124535);
#102997=AXIS2_PLACEMENT_3D('',#413876,#124536,#124537);
#102998=AXIS2_PLACEMENT_3D('',#413877,#124538,#124539);
#102999=AXIS2_PLACEMENT_3D('',#413880,#124540,#124541);
#103000=AXIS2_PLACEMENT_3D('',#413882,#124542,#124543);
#103001=AXIS2_PLACEMENT_3D('',#413884,#124544,#124545);
#103002=AXIS2_PLACEMENT_3D('',#413885,#124546,#124547);
#103003=AXIS2_PLACEMENT_3D('',#413886,#124548,#124549);
#103004=AXIS2_PLACEMENT_3D('',#413889,#124550,#124551);
#103005=AXIS2_PLACEMENT_3D('',#413891,#124552,#124553);
#103006=AXIS2_PLACEMENT_3D('',#413893,#124554,#124555);
#103007=AXIS2_PLACEMENT_3D('',#413894,#124556,#124557);
#103008=AXIS2_PLACEMENT_3D('',#413895,#124558,#124559);
#103009=AXIS2_PLACEMENT_3D('',#413898,#124560,#124561);
#103010=AXIS2_PLACEMENT_3D('',#413900,#124562,#124563);
#103011=AXIS2_PLACEMENT_3D('',#413902,#124564,#124565);
#103012=AXIS2_PLACEMENT_3D('',#413903,#124566,#124567);
#103013=AXIS2_PLACEMENT_3D('',#413904,#124568,#124569);
#103014=AXIS2_PLACEMENT_3D('',#413907,#124570,#124571);
#103015=AXIS2_PLACEMENT_3D('',#413909,#124572,#124573);
#103016=AXIS2_PLACEMENT_3D('',#413911,#124574,#124575);
#103017=AXIS2_PLACEMENT_3D('',#413912,#124576,#124577);
#103018=AXIS2_PLACEMENT_3D('',#413913,#124578,#124579);
#103019=AXIS2_PLACEMENT_3D('',#413916,#124580,#124581);
#103020=AXIS2_PLACEMENT_3D('',#413918,#124582,#124583);
#103021=AXIS2_PLACEMENT_3D('',#413920,#124584,#124585);
#103022=AXIS2_PLACEMENT_3D('',#413921,#124586,#124587);
#103023=AXIS2_PLACEMENT_3D('',#413922,#124588,#124589);
#103024=AXIS2_PLACEMENT_3D('',#413925,#124590,#124591);
#103025=AXIS2_PLACEMENT_3D('',#413927,#124592,#124593);
#103026=AXIS2_PLACEMENT_3D('',#413929,#124594,#124595);
#103027=AXIS2_PLACEMENT_3D('',#413930,#124596,#124597);
#103028=AXIS2_PLACEMENT_3D('',#413931,#124598,#124599);
#103029=AXIS2_PLACEMENT_3D('',#413934,#124600,#124601);
#103030=AXIS2_PLACEMENT_3D('',#413936,#124602,#124603);
#103031=AXIS2_PLACEMENT_3D('',#413938,#124604,#124605);
#103032=AXIS2_PLACEMENT_3D('',#413939,#124606,#124607);
#103033=AXIS2_PLACEMENT_3D('',#413940,#124608,#124609);
#103034=AXIS2_PLACEMENT_3D('',#413943,#124610,#124611);
#103035=AXIS2_PLACEMENT_3D('',#413945,#124612,#124613);
#103036=AXIS2_PLACEMENT_3D('',#413947,#124614,#124615);
#103037=AXIS2_PLACEMENT_3D('',#413948,#124616,#124617);
#103038=AXIS2_PLACEMENT_3D('',#413949,#124618,#124619);
#103039=AXIS2_PLACEMENT_3D('',#413952,#124620,#124621);
#103040=AXIS2_PLACEMENT_3D('',#413954,#124622,#124623);
#103041=AXIS2_PLACEMENT_3D('',#413956,#124624,#124625);
#103042=AXIS2_PLACEMENT_3D('',#413957,#124626,#124627);
#103043=AXIS2_PLACEMENT_3D('',#413958,#124628,#124629);
#103044=AXIS2_PLACEMENT_3D('',#413961,#124630,#124631);
#103045=AXIS2_PLACEMENT_3D('',#413963,#124632,#124633);
#103046=AXIS2_PLACEMENT_3D('',#413965,#124634,#124635);
#103047=AXIS2_PLACEMENT_3D('',#413966,#124636,#124637);
#103048=AXIS2_PLACEMENT_3D('',#413967,#124638,#124639);
#103049=AXIS2_PLACEMENT_3D('',#413970,#124640,#124641);
#103050=AXIS2_PLACEMENT_3D('',#413972,#124642,#124643);
#103051=AXIS2_PLACEMENT_3D('',#413974,#124644,#124645);
#103052=AXIS2_PLACEMENT_3D('',#413975,#124646,#124647);
#103053=AXIS2_PLACEMENT_3D('',#413976,#124648,#124649);
#103054=AXIS2_PLACEMENT_3D('',#413979,#124650,#124651);
#103055=AXIS2_PLACEMENT_3D('',#413981,#124652,#124653);
#103056=AXIS2_PLACEMENT_3D('',#413983,#124654,#124655);
#103057=AXIS2_PLACEMENT_3D('',#413984,#124656,#124657);
#103058=AXIS2_PLACEMENT_3D('',#413985,#124658,#124659);
#103059=AXIS2_PLACEMENT_3D('',#413988,#124660,#124661);
#103060=AXIS2_PLACEMENT_3D('',#413990,#124662,#124663);
#103061=AXIS2_PLACEMENT_3D('',#413992,#124664,#124665);
#103062=AXIS2_PLACEMENT_3D('',#413993,#124666,#124667);
#103063=AXIS2_PLACEMENT_3D('',#413994,#124668,#124669);
#103064=AXIS2_PLACEMENT_3D('',#413997,#124670,#124671);
#103065=AXIS2_PLACEMENT_3D('',#413999,#124672,#124673);
#103066=AXIS2_PLACEMENT_3D('',#414001,#124674,#124675);
#103067=AXIS2_PLACEMENT_3D('',#414002,#124676,#124677);
#103068=AXIS2_PLACEMENT_3D('',#414003,#124678,#124679);
#103069=AXIS2_PLACEMENT_3D('',#414006,#124680,#124681);
#103070=AXIS2_PLACEMENT_3D('',#414008,#124682,#124683);
#103071=AXIS2_PLACEMENT_3D('',#414010,#124684,#124685);
#103072=AXIS2_PLACEMENT_3D('',#414011,#124686,#124687);
#103073=AXIS2_PLACEMENT_3D('',#414012,#124688,#124689);
#103074=AXIS2_PLACEMENT_3D('',#414015,#124690,#124691);
#103075=AXIS2_PLACEMENT_3D('',#414017,#124692,#124693);
#103076=AXIS2_PLACEMENT_3D('',#414019,#124694,#124695);
#103077=AXIS2_PLACEMENT_3D('',#414020,#124696,#124697);
#103078=AXIS2_PLACEMENT_3D('',#414021,#124698,#124699);
#103079=AXIS2_PLACEMENT_3D('',#414024,#124700,#124701);
#103080=AXIS2_PLACEMENT_3D('',#414026,#124702,#124703);
#103081=AXIS2_PLACEMENT_3D('',#414028,#124704,#124705);
#103082=AXIS2_PLACEMENT_3D('',#414029,#124706,#124707);
#103083=AXIS2_PLACEMENT_3D('',#414030,#124708,#124709);
#103084=AXIS2_PLACEMENT_3D('',#414033,#124710,#124711);
#103085=AXIS2_PLACEMENT_3D('',#414035,#124712,#124713);
#103086=AXIS2_PLACEMENT_3D('',#414037,#124714,#124715);
#103087=AXIS2_PLACEMENT_3D('',#414038,#124716,#124717);
#103088=AXIS2_PLACEMENT_3D('',#414039,#124718,#124719);
#103089=AXIS2_PLACEMENT_3D('',#414042,#124720,#124721);
#103090=AXIS2_PLACEMENT_3D('',#414044,#124722,#124723);
#103091=AXIS2_PLACEMENT_3D('',#414046,#124724,#124725);
#103092=AXIS2_PLACEMENT_3D('',#414047,#124726,#124727);
#103093=AXIS2_PLACEMENT_3D('',#414048,#124728,#124729);
#103094=AXIS2_PLACEMENT_3D('',#414051,#124730,#124731);
#103095=AXIS2_PLACEMENT_3D('',#414053,#124732,#124733);
#103096=AXIS2_PLACEMENT_3D('',#414055,#124734,#124735);
#103097=AXIS2_PLACEMENT_3D('',#414056,#124736,#124737);
#103098=AXIS2_PLACEMENT_3D('',#414057,#124738,#124739);
#103099=AXIS2_PLACEMENT_3D('',#414060,#124740,#124741);
#103100=AXIS2_PLACEMENT_3D('',#414062,#124742,#124743);
#103101=AXIS2_PLACEMENT_3D('',#414064,#124744,#124745);
#103102=AXIS2_PLACEMENT_3D('',#414065,#124746,#124747);
#103103=AXIS2_PLACEMENT_3D('',#414066,#124748,#124749);
#103104=AXIS2_PLACEMENT_3D('',#414069,#124750,#124751);
#103105=AXIS2_PLACEMENT_3D('',#414071,#124752,#124753);
#103106=AXIS2_PLACEMENT_3D('',#414073,#124754,#124755);
#103107=AXIS2_PLACEMENT_3D('',#414074,#124756,#124757);
#103108=AXIS2_PLACEMENT_3D('',#414075,#124758,#124759);
#103109=AXIS2_PLACEMENT_3D('',#414078,#124760,#124761);
#103110=AXIS2_PLACEMENT_3D('',#414080,#124762,#124763);
#103111=AXIS2_PLACEMENT_3D('',#414082,#124764,#124765);
#103112=AXIS2_PLACEMENT_3D('',#414084,#124766,#124767);
#103113=AXIS2_PLACEMENT_3D('',#414085,#124768,#124769);
#103114=AXIS2_PLACEMENT_3D('',#414086,#124770,#124771);
#103115=AXIS2_PLACEMENT_3D('',#414161,#124772,#124773);
#103116=AXIS2_PLACEMENT_3D('',#414162,#124774,#124775);
#103117=AXIS2_PLACEMENT_3D('',#414195,#124776,#124777);
#103118=AXIS2_PLACEMENT_3D('',#414197,#124778,#124779);
#103119=AXIS2_PLACEMENT_3D('',#414199,#124781,#124782);
#103120=AXIS2_PLACEMENT_3D('',#414232,#124783,#124784);
#103121=AXIS2_PLACEMENT_3D('',#414237,#124786,#124787);
#103122=AXIS2_PLACEMENT_3D('',#414239,#124788,#124789);
#103123=AXIS2_PLACEMENT_3D('',#414241,#124790,#124791);
#103124=AXIS2_PLACEMENT_3D('',#414243,#124792,#124793);
#103125=AXIS2_PLACEMENT_3D('',#414245,#124794,#124795);
#103126=AXIS2_PLACEMENT_3D('',#414246,#124796,#124797);
#103127=AXIS2_PLACEMENT_3D('',#414247,#124798,#124799);
#103128=AXIS2_PLACEMENT_3D('',#414253,#124800,#124801);
#103129=AXIS2_PLACEMENT_3D('',#414254,#124802,#124803);
#103130=AXIS2_PLACEMENT_3D('',#414256,#124804,#124805);
#103131=AXIS2_PLACEMENT_3D('',#414258,#124806,#124807);
#103132=AXIS2_PLACEMENT_3D('',#414259,#124808,#124809);
#103133=AXIS2_PLACEMENT_3D('',#414260,#124810,#124811);
#103134=AXIS2_PLACEMENT_3D('',#414262,#124812,#124813);
#103135=AXIS2_PLACEMENT_3D('',#414264,#124815,#124816);
#103136=AXIS2_PLACEMENT_3D('',#414266,#124817,#124818);
#103137=AXIS2_PLACEMENT_3D('',#414267,#124819,#124820);
#103138=AXIS2_PLACEMENT_3D('',#414268,#124821,#124822);
#103139=AXIS2_PLACEMENT_3D('',#414290,#124824,#124825);
#103140=AXIS2_PLACEMENT_3D('',#414322,#124828,#124829);
#103141=AXIS2_PLACEMENT_3D('',#414354,#124832,#124833);
#103142=AXIS2_PLACEMENT_3D('',#414386,#124836,#124837);
#103143=AXIS2_PLACEMENT_3D('',#414418,#124840,#124841);
#103144=AXIS2_PLACEMENT_3D('',#414450,#124844,#124845);
#103145=AXIS2_PLACEMENT_3D('',#414482,#124848,#124849);
#103146=AXIS2_PLACEMENT_3D('',#414514,#124852,#124853);
#103147=AXIS2_PLACEMENT_3D('',#414546,#124856,#124857);
#103148=AXIS2_PLACEMENT_3D('',#414578,#124860,#124861);
#103149=AXIS2_PLACEMENT_3D('',#414610,#124864,#124865);
#103150=AXIS2_PLACEMENT_3D('',#414642,#124868,#124869);
#103151=AXIS2_PLACEMENT_3D('',#414674,#124872,#124873);
#103152=AXIS2_PLACEMENT_3D('',#414706,#124876,#124877);
#103153=AXIS2_PLACEMENT_3D('',#414738,#124880,#124881);
#103154=AXIS2_PLACEMENT_3D('',#414770,#124884,#124885);
#103155=AXIS2_PLACEMENT_3D('',#414802,#124888,#124889);
#103156=AXIS2_PLACEMENT_3D('',#414834,#124892,#124893);
#103157=AXIS2_PLACEMENT_3D('',#414866,#124896,#124897);
#103158=AXIS2_PLACEMENT_3D('',#414898,#124900,#124901);
#103159=AXIS2_PLACEMENT_3D('',#414930,#124904,#124905);
#103160=AXIS2_PLACEMENT_3D('',#414962,#124908,#124909);
#103161=AXIS2_PLACEMENT_3D('',#414994,#124912,#124913);
#103162=AXIS2_PLACEMENT_3D('',#415026,#124916,#124917);
#103163=AXIS2_PLACEMENT_3D('',#415058,#124920,#124921);
#103164=AXIS2_PLACEMENT_3D('',#415090,#124924,#124925);
#103165=AXIS2_PLACEMENT_3D('',#415122,#124928,#124929);
#103166=AXIS2_PLACEMENT_3D('',#415154,#124932,#124933);
#103167=AXIS2_PLACEMENT_3D('',#415186,#124936,#124937);
#103168=AXIS2_PLACEMENT_3D('',#415218,#124940,#124941);
#103169=AXIS2_PLACEMENT_3D('',#415250,#124944,#124945);
#103170=AXIS2_PLACEMENT_3D('',#415282,#124948,#124949);
#103171=AXIS2_PLACEMENT_3D('',#415314,#124952,#124953);
#103172=AXIS2_PLACEMENT_3D('',#415346,#124956,#124957);
#103173=AXIS2_PLACEMENT_3D('',#415378,#124960,#124961);
#103174=AXIS2_PLACEMENT_3D('',#415410,#124964,#124965);
#103175=AXIS2_PLACEMENT_3D('',#415442,#124968,#124969);
#103176=AXIS2_PLACEMENT_3D('',#415474,#124972,#124973);
#103177=AXIS2_PLACEMENT_3D('',#415506,#124976,#124977);
#103178=AXIS2_PLACEMENT_3D('',#415510,#124979,#124980);
#103179=AXIS2_PLACEMENT_3D('',#415511,#124981,#124982);
#103180=AXIS2_PLACEMENT_3D('',#415513,#124983,#124984);
#103181=AXIS2_PLACEMENT_3D('',#415545,#124987,#124988);
#103182=AXIS2_PLACEMENT_3D('',#415577,#124991,#124992);
#103183=AXIS2_PLACEMENT_3D('',#415609,#124995,#124996);
#103184=AXIS2_PLACEMENT_3D('',#415641,#124999,#125000);
#103185=AXIS2_PLACEMENT_3D('',#415673,#125003,#125004);
#103186=AXIS2_PLACEMENT_3D('',#415705,#125007,#125008);
#103187=AXIS2_PLACEMENT_3D('',#415737,#125011,#125012);
#103188=AXIS2_PLACEMENT_3D('',#415769,#125015,#125016);
#103189=AXIS2_PLACEMENT_3D('',#415801,#125019,#125020);
#103190=AXIS2_PLACEMENT_3D('',#415833,#125023,#125024);
#103191=AXIS2_PLACEMENT_3D('',#415865,#125027,#125028);
#103192=AXIS2_PLACEMENT_3D('',#415897,#125031,#125032);
#103193=AXIS2_PLACEMENT_3D('',#415929,#125035,#125036);
#103194=AXIS2_PLACEMENT_3D('',#415961,#125039,#125040);
#103195=AXIS2_PLACEMENT_3D('',#415993,#125043,#125044);
#103196=AXIS2_PLACEMENT_3D('',#416025,#125047,#125048);
#103197=AXIS2_PLACEMENT_3D('',#416057,#125051,#125052);
#103198=AXIS2_PLACEMENT_3D('',#416089,#125055,#125056);
#103199=AXIS2_PLACEMENT_3D('',#416121,#125059,#125060);
#103200=AXIS2_PLACEMENT_3D('',#416153,#125063,#125064);
#103201=AXIS2_PLACEMENT_3D('',#416185,#125067,#125068);
#103202=AXIS2_PLACEMENT_3D('',#416217,#125071,#125072);
#103203=AXIS2_PLACEMENT_3D('',#416249,#125075,#125076);
#103204=AXIS2_PLACEMENT_3D('',#416281,#125079,#125080);
#103205=AXIS2_PLACEMENT_3D('',#416313,#125083,#125084);
#103206=AXIS2_PLACEMENT_3D('',#416345,#125087,#125088);
#103207=AXIS2_PLACEMENT_3D('',#416377,#125091,#125092);
#103208=AXIS2_PLACEMENT_3D('',#416409,#125095,#125096);
#103209=AXIS2_PLACEMENT_3D('',#416441,#125099,#125100);
#103210=AXIS2_PLACEMENT_3D('',#416473,#125103,#125104);
#103211=AXIS2_PLACEMENT_3D('',#416505,#125107,#125108);
#103212=AXIS2_PLACEMENT_3D('',#416537,#125111,#125112);
#103213=AXIS2_PLACEMENT_3D('',#416569,#125115,#125116);
#103214=AXIS2_PLACEMENT_3D('',#416601,#125119,#125120);
#103215=AXIS2_PLACEMENT_3D('',#416633,#125123,#125124);
#103216=AXIS2_PLACEMENT_3D('',#416665,#125127,#125128);
#103217=AXIS2_PLACEMENT_3D('',#416697,#125131,#125132);
#103218=AXIS2_PLACEMENT_3D('',#416729,#125135,#125136);
#103219=AXIS2_PLACEMENT_3D('',#416745,#125138,#125139);
#103220=AXIS2_PLACEMENT_3D('',#416747,#125140,#125141);
#103221=AXIS2_PLACEMENT_3D('',#416748,#125142,#125143);
#103222=AXIS2_PLACEMENT_3D('',#416749,#125144,#125145);
#103223=AXIS2_PLACEMENT_3D('',#416752,#125146,#125147);
#103224=AXIS2_PLACEMENT_3D('',#416791,#125150,#125151);
#103225=AXIS2_PLACEMENT_3D('',#416830,#125154,#125155);
#103226=AXIS2_PLACEMENT_3D('',#416869,#125158,#125159);
#103227=AXIS2_PLACEMENT_3D('',#416908,#125162,#125163);
#103228=AXIS2_PLACEMENT_3D('',#416947,#125166,#125167);
#103229=AXIS2_PLACEMENT_3D('',#416986,#125170,#125171);
#103230=AXIS2_PLACEMENT_3D('',#417025,#125174,#125175);
#103231=AXIS2_PLACEMENT_3D('',#417064,#125178,#125179);
#103232=AXIS2_PLACEMENT_3D('',#417103,#125182,#125183);
#103233=AXIS2_PLACEMENT_3D('',#417142,#125186,#125187);
#103234=AXIS2_PLACEMENT_3D('',#417181,#125190,#125191);
#103235=AXIS2_PLACEMENT_3D('',#417220,#125194,#125195);
#103236=AXIS2_PLACEMENT_3D('',#417259,#125198,#125199);
#103237=AXIS2_PLACEMENT_3D('',#417298,#125202,#125203);
#103238=AXIS2_PLACEMENT_3D('',#417337,#125206,#125207);
#103239=AXIS2_PLACEMENT_3D('',#417376,#125210,#125211);
#103240=AXIS2_PLACEMENT_3D('',#417415,#125214,#125215);
#103241=AXIS2_PLACEMENT_3D('',#417454,#125218,#125219);
#103242=AXIS2_PLACEMENT_3D('',#417493,#125222,#125223);
#103243=AXIS2_PLACEMENT_3D('',#417532,#125226,#125227);
#103244=AXIS2_PLACEMENT_3D('',#417571,#125230,#125231);
#103245=AXIS2_PLACEMENT_3D('',#417610,#125234,#125235);
#103246=AXIS2_PLACEMENT_3D('',#417649,#125238,#125239);
#103247=AXIS2_PLACEMENT_3D('',#417688,#125242,#125243);
#103248=AXIS2_PLACEMENT_3D('',#417727,#125246,#125247);
#103249=AXIS2_PLACEMENT_3D('',#417766,#125250,#125251);
#103250=AXIS2_PLACEMENT_3D('',#417805,#125254,#125255);
#103251=AXIS2_PLACEMENT_3D('',#417844,#125258,#125259);
#103252=AXIS2_PLACEMENT_3D('',#417883,#125262,#125263);
#103253=AXIS2_PLACEMENT_3D('',#417922,#125266,#125267);
#103254=AXIS2_PLACEMENT_3D('',#417961,#125270,#125271);
#103255=AXIS2_PLACEMENT_3D('',#418000,#125274,#125275);
#103256=AXIS2_PLACEMENT_3D('',#418039,#125278,#125279);
#103257=AXIS2_PLACEMENT_3D('',#418078,#125282,#125283);
#103258=AXIS2_PLACEMENT_3D('',#418117,#125286,#125287);
#103259=AXIS2_PLACEMENT_3D('',#418156,#125290,#125291);
#103260=AXIS2_PLACEMENT_3D('',#418195,#125294,#125295);
#103261=AXIS2_PLACEMENT_3D('',#418234,#125298,#125299);
#103262=AXIS2_PLACEMENT_3D('',#418274,#125303,#125304);
#103263=AXIS2_PLACEMENT_3D('',#418313,#125307,#125308);
#103264=AXIS2_PLACEMENT_3D('',#418352,#125311,#125312);
#103265=AXIS2_PLACEMENT_3D('',#418391,#125315,#125316);
#103266=AXIS2_PLACEMENT_3D('',#418430,#125319,#125320);
#103267=AXIS2_PLACEMENT_3D('',#418469,#125323,#125324);
#103268=AXIS2_PLACEMENT_3D('',#418508,#125327,#125328);
#103269=AXIS2_PLACEMENT_3D('',#418547,#125331,#125332);
#103270=AXIS2_PLACEMENT_3D('',#418586,#125335,#125336);
#103271=AXIS2_PLACEMENT_3D('',#418625,#125339,#125340);
#103272=AXIS2_PLACEMENT_3D('',#418664,#125343,#125344);
#103273=AXIS2_PLACEMENT_3D('',#418703,#125347,#125348);
#103274=AXIS2_PLACEMENT_3D('',#418742,#125351,#125352);
#103275=AXIS2_PLACEMENT_3D('',#418781,#125355,#125356);
#103276=AXIS2_PLACEMENT_3D('',#418820,#125359,#125360);
#103277=AXIS2_PLACEMENT_3D('',#418859,#125363,#125364);
#103278=AXIS2_PLACEMENT_3D('',#418898,#125367,#125368);
#103279=AXIS2_PLACEMENT_3D('',#418937,#125371,#125372);
#103280=AXIS2_PLACEMENT_3D('',#418976,#125375,#125376);
#103281=AXIS2_PLACEMENT_3D('',#419015,#125379,#125380);
#103282=AXIS2_PLACEMENT_3D('',#419054,#125383,#125384);
#103283=AXIS2_PLACEMENT_3D('',#419093,#125387,#125388);
#103284=AXIS2_PLACEMENT_3D('',#419132,#125391,#125392);
#103285=AXIS2_PLACEMENT_3D('',#419171,#125395,#125396);
#103286=AXIS2_PLACEMENT_3D('',#419210,#125399,#125400);
#103287=AXIS2_PLACEMENT_3D('',#419249,#125403,#125404);
#103288=AXIS2_PLACEMENT_3D('',#419288,#125407,#125408);
#103289=AXIS2_PLACEMENT_3D('',#419327,#125411,#125412);
#103290=AXIS2_PLACEMENT_3D('',#419366,#125415,#125416);
#103291=AXIS2_PLACEMENT_3D('',#419405,#125419,#125420);
#103292=AXIS2_PLACEMENT_3D('',#419444,#125423,#125424);
#103293=AXIS2_PLACEMENT_3D('',#419483,#125427,#125428);
#103294=AXIS2_PLACEMENT_3D('',#419522,#125431,#125432);
#103295=AXIS2_PLACEMENT_3D('',#419561,#125435,#125436);
#103296=AXIS2_PLACEMENT_3D('',#419600,#125439,#125440);
#103297=AXIS2_PLACEMENT_3D('',#419639,#125443,#125444);
#103298=AXIS2_PLACEMENT_3D('',#419678,#125447,#125448);
#103299=AXIS2_PLACEMENT_3D('',#419717,#125451,#125452);
#103300=AXIS2_PLACEMENT_3D('',#419754,#125455,#125456);
#103301=AXIS2_PLACEMENT_3D('',#419755,#125457,#125458);
#103302=AXIS2_PLACEMENT_3D('',#419756,#125459,#125460);
#103303=AXIS2_PLACEMENT_3D('',#419757,#125461,#125462);
#103304=AXIS2_PLACEMENT_3D('',#419758,#125463,#125464);
#103305=AXIS2_PLACEMENT_3D('',#419759,#125465,#125466);
#103306=AXIS2_PLACEMENT_3D('',#419760,#125467,#125468);
#103307=AXIS2_PLACEMENT_3D('',#419761,#125469,#125470);
#103308=AXIS2_PLACEMENT_3D('',#419762,#125471,#125472);
#103309=AXIS2_PLACEMENT_3D('',#419763,#125473,#125474);
#103310=AXIS2_PLACEMENT_3D('',#419764,#125475,#125476);
#103311=AXIS2_PLACEMENT_3D('',#419765,#125477,#125478);
#103312=AXIS2_PLACEMENT_3D('',#419766,#125479,#125480);
#103313=AXIS2_PLACEMENT_3D('',#419767,#125481,#125482);
#103314=AXIS2_PLACEMENT_3D('',#419768,#125483,#125484);
#103315=AXIS2_PLACEMENT_3D('',#419769,#125485,#125486);
#103316=AXIS2_PLACEMENT_3D('',#419770,#125487,#125488);
#103317=AXIS2_PLACEMENT_3D('',#419771,#125489,#125490);
#103318=AXIS2_PLACEMENT_3D('',#419772,#125491,#125492);
#103319=AXIS2_PLACEMENT_3D('',#419773,#125493,#125494);
#103320=AXIS2_PLACEMENT_3D('',#419774,#125495,#125496);
#103321=AXIS2_PLACEMENT_3D('',#419775,#125497,#125498);
#103322=AXIS2_PLACEMENT_3D('',#419776,#125499,#125500);
#103323=AXIS2_PLACEMENT_3D('',#419777,#125501,#125502);
#103324=AXIS2_PLACEMENT_3D('',#419778,#125503,#125504);
#103325=AXIS2_PLACEMENT_3D('',#419779,#125505,#125506);
#103326=AXIS2_PLACEMENT_3D('',#419780,#125507,#125508);
#103327=AXIS2_PLACEMENT_3D('',#419781,#125509,#125510);
#103328=AXIS2_PLACEMENT_3D('',#419782,#125511,#125512);
#103329=AXIS2_PLACEMENT_3D('',#419783,#125513,#125514);
#103330=AXIS2_PLACEMENT_3D('',#419784,#125515,#125516);
#103331=AXIS2_PLACEMENT_3D('',#419785,#125517,#125518);
#103332=AXIS2_PLACEMENT_3D('',#419786,#125519,#125520);
#103333=AXIS2_PLACEMENT_3D('',#419787,#125521,#125522);
#103334=AXIS2_PLACEMENT_3D('',#419788,#125523,#125524);
#103335=AXIS2_PLACEMENT_3D('',#419789,#125525,#125526);
#103336=AXIS2_PLACEMENT_3D('',#419790,#125527,#125528);
#103337=AXIS2_PLACEMENT_3D('',#419791,#125529,#125530);
#103338=AXIS2_PLACEMENT_3D('',#419792,#125531,#125532);
#103339=AXIS2_PLACEMENT_3D('',#419793,#125533,#125534);
#103340=AXIS2_PLACEMENT_3D('',#419794,#125535,#125536);
#103341=AXIS2_PLACEMENT_3D('',#419795,#125537,#125538);
#103342=AXIS2_PLACEMENT_3D('',#419796,#125539,#125540);
#103343=AXIS2_PLACEMENT_3D('',#419797,#125541,#125542);
#103344=AXIS2_PLACEMENT_3D('',#419798,#125543,#125544);
#103345=AXIS2_PLACEMENT_3D('',#419799,#125545,#125546);
#103346=AXIS2_PLACEMENT_3D('',#419800,#125547,#125548);
#103347=AXIS2_PLACEMENT_3D('',#419801,#125549,#125550);
#103348=AXIS2_PLACEMENT_3D('',#419802,#125551,#125552);
#103349=AXIS2_PLACEMENT_3D('',#419803,#125553,#125554);
#103350=AXIS2_PLACEMENT_3D('',#419804,#125555,#125556);
#103351=AXIS2_PLACEMENT_3D('',#419805,#125557,#125558);
#103352=AXIS2_PLACEMENT_3D('',#419806,#125559,#125560);
#103353=AXIS2_PLACEMENT_3D('',#419807,#125561,#125562);
#103354=AXIS2_PLACEMENT_3D('',#419808,#125563,#125564);
#103355=AXIS2_PLACEMENT_3D('',#419809,#125565,#125566);
#103356=AXIS2_PLACEMENT_3D('',#419810,#125567,#125568);
#103357=AXIS2_PLACEMENT_3D('',#419811,#125569,#125570);
#103358=AXIS2_PLACEMENT_3D('',#419812,#125571,#125572);
#103359=AXIS2_PLACEMENT_3D('',#419813,#125573,#125574);
#103360=AXIS2_PLACEMENT_3D('',#419814,#125575,#125576);
#103361=AXIS2_PLACEMENT_3D('',#419815,#125577,#125578);
#103362=AXIS2_PLACEMENT_3D('',#419816,#125579,#125580);
#103363=AXIS2_PLACEMENT_3D('',#419817,#125581,#125582);
#103364=AXIS2_PLACEMENT_3D('',#419818,#125583,#125584);
#103365=AXIS2_PLACEMENT_3D('',#419819,#125585,#125586);
#103366=AXIS2_PLACEMENT_3D('',#419820,#125587,#125588);
#103367=AXIS2_PLACEMENT_3D('',#419821,#125589,#125590);
#103368=AXIS2_PLACEMENT_3D('',#419822,#125591,#125592);
#103369=AXIS2_PLACEMENT_3D('',#419823,#125593,#125594);
#103370=AXIS2_PLACEMENT_3D('',#419824,#125595,#125596);
#103371=AXIS2_PLACEMENT_3D('',#419825,#125597,#125598);
#103372=AXIS2_PLACEMENT_3D('',#419826,#125599,#125600);
#103373=AXIS2_PLACEMENT_3D('',#419827,#125601,#125602);
#103374=AXIS2_PLACEMENT_3D('',#419828,#125603,#125604);
#103375=AXIS2_PLACEMENT_3D('',#419829,#125605,#125606);
#103376=AXIS2_PLACEMENT_3D('',#419830,#125607,#125608);
#103377=AXIS2_PLACEMENT_3D('',#419831,#125609,#125610);
#103378=AXIS2_PLACEMENT_3D('',#419832,#125611,#125612);
#103379=AXIS2_PLACEMENT_3D('',#419833,#125613,#125614);
#103380=AXIS2_PLACEMENT_3D('',#419834,#125615,#125616);
#103381=AXIS2_PLACEMENT_3D('',#419835,#125617,#125618);
#103382=AXIS2_PLACEMENT_3D('',#419836,#125619,#125620);
#103383=AXIS2_PLACEMENT_3D('',#419837,#125621,#125622);
#103384=AXIS2_PLACEMENT_3D('',#419838,#125623,#125624);
#103385=AXIS2_PLACEMENT_3D('',#419839,#125625,#125626);
#103386=AXIS2_PLACEMENT_3D('',#419840,#125627,#125628);
#103387=AXIS2_PLACEMENT_3D('',#419841,#125629,#125630);
#103388=AXIS2_PLACEMENT_3D('',#419842,#125631,#125632);
#103389=AXIS2_PLACEMENT_3D('',#419843,#125633,#125634);
#103390=AXIS2_PLACEMENT_3D('',#419844,#125635,#125636);
#103391=AXIS2_PLACEMENT_3D('',#419845,#125637,#125638);
#103392=AXIS2_PLACEMENT_3D('',#419846,#125639,#125640);
#103393=AXIS2_PLACEMENT_3D('',#419847,#125641,#125642);
#103394=AXIS2_PLACEMENT_3D('',#419848,#125643,#125644);
#103395=AXIS2_PLACEMENT_3D('',#419849,#125645,#125646);
#103396=AXIS2_PLACEMENT_3D('',#419850,#125647,#125648);
#103397=AXIS2_PLACEMENT_3D('',#419851,#125649,#125650);
#103398=AXIS2_PLACEMENT_3D('',#419852,#125651,#125652);
#103399=AXIS2_PLACEMENT_3D('',#419853,#125653,#125654);
#103400=AXIS2_PLACEMENT_3D('',#419854,#125655,#125656);
#103401=AXIS2_PLACEMENT_3D('',#419855,#125657,#125658);
#103402=AXIS2_PLACEMENT_3D('',#419856,#125659,#125660);
#103403=AXIS2_PLACEMENT_3D('',#419857,#125661,#125662);
#103404=AXIS2_PLACEMENT_3D('',#419858,#125663,#125664);
#103405=AXIS2_PLACEMENT_3D('',#419859,#125665,#125666);
#103406=AXIS2_PLACEMENT_3D('',#419860,#125667,#125668);
#103407=AXIS2_PLACEMENT_3D('',#419861,#125669,#125670);
#103408=AXIS2_PLACEMENT_3D('',#419862,#125671,#125672);
#103409=AXIS2_PLACEMENT_3D('',#419863,#125673,#125674);
#103410=AXIS2_PLACEMENT_3D('',#419864,#125675,#125676);
#103411=AXIS2_PLACEMENT_3D('',#419865,#125677,#125678);
#103412=AXIS2_PLACEMENT_3D('',#419866,#125679,#125680);
#103413=AXIS2_PLACEMENT_3D('',#419867,#125681,#125682);
#103414=AXIS2_PLACEMENT_3D('',#419868,#125683,#125684);
#103415=AXIS2_PLACEMENT_3D('',#419869,#125685,#125686);
#103416=AXIS2_PLACEMENT_3D('',#419870,#125687,#125688);
#103417=AXIS2_PLACEMENT_3D('',#419871,#125689,#125690);
#103418=AXIS2_PLACEMENT_3D('',#419872,#125691,#125692);
#103419=AXIS2_PLACEMENT_3D('',#419873,#125693,#125694);
#103420=AXIS2_PLACEMENT_3D('',#419874,#125695,#125696);
#103421=AXIS2_PLACEMENT_3D('',#419875,#125697,#125698);
#103422=AXIS2_PLACEMENT_3D('',#419876,#125699,#125700);
#103423=AXIS2_PLACEMENT_3D('',#419877,#125701,#125702);
#103424=AXIS2_PLACEMENT_3D('',#419878,#125703,#125704);
#103425=AXIS2_PLACEMENT_3D('',#419879,#125705,#125706);
#103426=AXIS2_PLACEMENT_3D('',#419880,#125707,#125708);
#103427=AXIS2_PLACEMENT_3D('',#419881,#125709,#125710);
#103428=AXIS2_PLACEMENT_3D('',#419882,#125711,#125712);
#103429=AXIS2_PLACEMENT_3D('',#419883,#125713,#125714);
#103430=AXIS2_PLACEMENT_3D('',#419884,#125715,#125716);
#103431=AXIS2_PLACEMENT_3D('',#419885,#125717,#125718);
#103432=AXIS2_PLACEMENT_3D('',#419886,#125719,#125720);
#103433=AXIS2_PLACEMENT_3D('',#419887,#125721,#125722);
#103434=AXIS2_PLACEMENT_3D('',#419888,#125723,#125724);
#103435=AXIS2_PLACEMENT_3D('',#419889,#125725,#125726);
#103436=AXIS2_PLACEMENT_3D('',#419890,#125727,#125728);
#103437=AXIS2_PLACEMENT_3D('',#419891,#125729,#125730);
#103438=AXIS2_PLACEMENT_3D('',#419892,#125731,#125732);
#103439=AXIS2_PLACEMENT_3D('',#419893,#125733,#125734);
#103440=AXIS2_PLACEMENT_3D('',#419894,#125735,#125736);
#103441=AXIS2_PLACEMENT_3D('',#419895,#125737,#125738);
#103442=AXIS2_PLACEMENT_3D('',#419896,#125739,#125740);
#103443=AXIS2_PLACEMENT_3D('',#419897,#125741,#125742);
#103444=AXIS2_PLACEMENT_3D('',#419898,#125743,#125744);
#103445=AXIS2_PLACEMENT_3D('',#419899,#125745,#125746);
#103446=AXIS2_PLACEMENT_3D('',#419900,#125747,#125748);
#103447=AXIS2_PLACEMENT_3D('',#419901,#125749,#125750);
#103448=AXIS2_PLACEMENT_3D('',#419902,#125751,#125752);
#103449=AXIS2_PLACEMENT_3D('',#419903,#125753,#125754);
#103450=AXIS2_PLACEMENT_3D('',#419904,#125755,#125756);
#103451=AXIS2_PLACEMENT_3D('',#419905,#125757,#125758);
#103452=AXIS2_PLACEMENT_3D('',#419906,#125759,#125760);
#103453=AXIS2_PLACEMENT_3D('',#419907,#125761,#125762);
#103454=AXIS2_PLACEMENT_3D('',#419908,#125763,#125764);
#103455=AXIS2_PLACEMENT_3D('',#419909,#125765,#125766);
#103456=AXIS2_PLACEMENT_3D('',#419910,#125767,#125768);
#103457=AXIS2_PLACEMENT_3D('',#419911,#125769,#125770);
#103458=AXIS2_PLACEMENT_3D('',#419912,#125771,#125772);
#103459=AXIS2_PLACEMENT_3D('',#419913,#125773,#125774);
#103460=AXIS2_PLACEMENT_3D('',#419914,#125775,#125776);
#103461=AXIS2_PLACEMENT_3D('',#419915,#125777,#125778);
#103462=AXIS2_PLACEMENT_3D('',#419916,#125779,#125780);
#103463=AXIS2_PLACEMENT_3D('',#419917,#125781,#125782);
#103464=AXIS2_PLACEMENT_3D('',#419918,#125783,#125784);
#103465=AXIS2_PLACEMENT_3D('',#419919,#125785,#125786);
#103466=AXIS2_PLACEMENT_3D('',#419920,#125787,#125788);
#103467=AXIS2_PLACEMENT_3D('',#419921,#125789,#125790);
#103468=AXIS2_PLACEMENT_3D('',#419922,#125791,#125792);
#103469=AXIS2_PLACEMENT_3D('',#419923,#125793,#125794);
#103470=AXIS2_PLACEMENT_3D('',#419924,#125795,#125796);
#103471=AXIS2_PLACEMENT_3D('',#419925,#125797,#125798);
#103472=AXIS2_PLACEMENT_3D('',#419926,#125799,#125800);
#103473=AXIS2_PLACEMENT_3D('',#419927,#125801,#125802);
#103474=AXIS2_PLACEMENT_3D('',#419928,#125803,#125804);
#103475=AXIS2_PLACEMENT_3D('',#419929,#125805,#125806);
#103476=AXIS2_PLACEMENT_3D('',#419930,#125807,#125808);
#103477=AXIS2_PLACEMENT_3D('',#419931,#125809,#125810);
#103478=AXIS2_PLACEMENT_3D('',#419932,#125811,#125812);
#103479=AXIS2_PLACEMENT_3D('',#419933,#125813,#125814);
#103480=AXIS2_PLACEMENT_3D('',#419934,#125815,#125816);
#103481=AXIS2_PLACEMENT_3D('',#419935,#125817,#125818);
#103482=AXIS2_PLACEMENT_3D('',#419936,#125819,#125820);
#103483=AXIS2_PLACEMENT_3D('',#419937,#125821,#125822);
#103484=AXIS2_PLACEMENT_3D('',#419938,#125823,#125824);
#103485=AXIS2_PLACEMENT_3D('',#419939,#125825,#125826);
#103486=AXIS2_PLACEMENT_3D('',#419940,#125827,#125828);
#103487=AXIS2_PLACEMENT_3D('',#419941,#125829,#125830);
#103488=AXIS2_PLACEMENT_3D('',#419942,#125831,#125832);
#103489=AXIS2_PLACEMENT_3D('',#419943,#125833,#125834);
#103490=AXIS2_PLACEMENT_3D('',#419944,#125835,#125836);
#103491=AXIS2_PLACEMENT_3D('',#419945,#125837,#125838);
#103492=AXIS2_PLACEMENT_3D('',#419946,#125839,#125840);
#103493=AXIS2_PLACEMENT_3D('',#419947,#125841,#125842);
#103494=AXIS2_PLACEMENT_3D('',#419948,#125843,#125844);
#103495=AXIS2_PLACEMENT_3D('',#419949,#125845,#125846);
#103496=AXIS2_PLACEMENT_3D('',#419950,#125847,#125848);
#103497=AXIS2_PLACEMENT_3D('',#419951,#125849,#125850);
#103498=AXIS2_PLACEMENT_3D('',#419952,#125851,#125852);
#103499=AXIS2_PLACEMENT_3D('',#419953,#125853,#125854);
#103500=AXIS2_PLACEMENT_3D('',#419954,#125855,#125856);
#103501=AXIS2_PLACEMENT_3D('',#419955,#125857,#125858);
#103502=AXIS2_PLACEMENT_3D('',#419956,#125859,#125860);
#103503=AXIS2_PLACEMENT_3D('',#419957,#125861,#125862);
#103504=AXIS2_PLACEMENT_3D('',#419958,#125863,#125864);
#103505=AXIS2_PLACEMENT_3D('',#419959,#125865,#125866);
#103506=AXIS2_PLACEMENT_3D('',#419960,#125867,#125868);
#103507=AXIS2_PLACEMENT_3D('',#419961,#125869,#125870);
#103508=AXIS2_PLACEMENT_3D('',#419962,#125871,#125872);
#103509=AXIS2_PLACEMENT_3D('',#419963,#125873,#125874);
#103510=AXIS2_PLACEMENT_3D('',#419964,#125875,#125876);
#103511=AXIS2_PLACEMENT_3D('',#419965,#125877,#125878);
#103512=AXIS2_PLACEMENT_3D('',#419966,#125879,#125880);
#103513=AXIS2_PLACEMENT_3D('',#419967,#125881,#125882);
#103514=AXIS2_PLACEMENT_3D('',#419968,#125883,#125884);
#103515=AXIS2_PLACEMENT_3D('',#419969,#125885,#125886);
#103516=AXIS2_PLACEMENT_3D('',#419970,#125887,#125888);
#103517=AXIS2_PLACEMENT_3D('',#419971,#125889,#125890);
#103518=AXIS2_PLACEMENT_3D('',#419972,#125891,#125892);
#103519=AXIS2_PLACEMENT_3D('',#419973,#125893,#125894);
#103520=AXIS2_PLACEMENT_3D('',#419974,#125895,#125896);
#103521=AXIS2_PLACEMENT_3D('',#419975,#125897,#125898);
#103522=AXIS2_PLACEMENT_3D('',#419976,#125899,#125900);
#103523=AXIS2_PLACEMENT_3D('',#419977,#125901,#125902);
#103524=AXIS2_PLACEMENT_3D('',#419978,#125903,#125904);
#103525=AXIS2_PLACEMENT_3D('',#419979,#125905,#125906);
#103526=AXIS2_PLACEMENT_3D('',#419980,#125907,#125908);
#103527=AXIS2_PLACEMENT_3D('',#419981,#125909,#125910);
#103528=AXIS2_PLACEMENT_3D('',#419982,#125911,#125912);
#103529=AXIS2_PLACEMENT_3D('',#420056,#125915,#125916);
#103530=AXIS2_PLACEMENT_3D('',#420057,#125917,#125918);
#103531=AXIS2_PLACEMENT_3D('',#420058,#125919,#125920);
#103532=AXIS2_PLACEMENT_3D('',#420061,#125921,#125922);
#103533=AXIS2_PLACEMENT_3D('',#420069,#125925,#125926);
#103534=AXIS2_PLACEMENT_3D('',#420073,#125928,#125929);
#103535=AXIS2_PLACEMENT_3D('',#420080,#125931,#125932);
#103536=AXIS2_PLACEMENT_3D('',#420081,#125933,#125934);
#103537=AXIS2_PLACEMENT_3D('',#420085,#125937,#125938);
#103538=AXIS2_PLACEMENT_3D('',#420089,#125941,#125942);
#103539=AXIS2_PLACEMENT_3D('',#420093,#125945,#125946);
#103540=AXIS2_PLACEMENT_3D('',#420097,#125949,#125950);
#103541=AXIS2_PLACEMENT_3D('',#420101,#125953,#125954);
#103542=AXIS2_PLACEMENT_3D('',#420104,#125955,#125956);
#103543=AXIS2_PLACEMENT_3D('',#420105,#125957,#125958);
#103544=AXIS2_PLACEMENT_3D('',#420107,#125959,#125960);
#103545=AXIS2_PLACEMENT_3D('',#420109,#125961,#125962);
#103546=AXIS2_PLACEMENT_3D('',#420110,#125963,#125964);
#103547=AXIS2_PLACEMENT_3D('',#420111,#125965,#125966);
#103548=AXIS2_PLACEMENT_3D('',#420112,#125967,#125968);
#103549=AXIS2_PLACEMENT_3D('',#420113,#125969,#125970);
#103550=AXIS2_PLACEMENT_3D('',#420114,#125971,#125972);
#103551=AXIS2_PLACEMENT_3D('',#420122,#125976,#125977);
#103552=AXIS2_PLACEMENT_3D('',#420124,#125979,#125980);
#103553=AXIS2_PLACEMENT_3D('',#420129,#125982,#125983);
#103554=AXIS2_PLACEMENT_3D('',#420134,#125985,#125986);
#103555=AXIS2_PLACEMENT_3D('',#420139,#125988,#125989);
#103556=AXIS2_PLACEMENT_3D('',#420144,#125991,#125992);
#103557=AXIS2_PLACEMENT_3D('',#420145,#125993,#125994);
#103558=AXIS2_PLACEMENT_3D('',#420146,#125995,#125996);
#103559=AXIS2_PLACEMENT_3D('',#420147,#125997,#125998);
#103560=AXIS2_PLACEMENT_3D('',#420148,#125999,#126000);
#103561=AXIS2_PLACEMENT_3D('',#420149,#126001,#126002);
#103562=AXIS2_PLACEMENT_3D('',#420150,#126003,#126004);
#103563=AXIS2_PLACEMENT_3D('',#421382,#126005,#126006);
#103564=AXIS2_PLACEMENT_3D('',#422616,#126007,#126008);
#103565=AXIS2_PLACEMENT_3D('',#422653,#126009,#126010);
#103566=AXIS2_PLACEMENT_3D('',#422701,#126011,#126012);
#103567=AXIS2_PLACEMENT_3D('',#422702,#126013,#126014);
#103568=AXIS2_PLACEMENT_3D('',#422703,#126015,#126016);
#103569=AXIS2_PLACEMENT_3D('',#422704,#126017,#126018);
#103570=AXIS2_PLACEMENT_3D('',#422723,#126019,#126020);
#103571=AXIS2_PLACEMENT_3D('',#422748,#126021,#126022);
#103572=AXIS2_PLACEMENT_3D('',#422807,#126023,#126024);
#103573=AXIS2_PLACEMENT_3D('',#422820,#126025,#126026);
#103574=AXIS2_PLACEMENT_3D('',#422839,#126027,#126028);
#103575=AXIS2_PLACEMENT_3D('',#422840,#126029,#126030);
#103576=AXIS2_PLACEMENT_3D('',#422841,#126031,#126032);
#103577=AXIS2_PLACEMENT_3D('',#422854,#126033,#126034);
#103578=AXIS2_PLACEMENT_3D('',#422867,#126035,#126036);
#103579=AXIS2_PLACEMENT_3D('',#422874,#126039,#126040);
#103580=AXIS2_PLACEMENT_3D('',#422881,#126042,#126043);
#103581=AXIS2_PLACEMENT_3D('',#422884,#126044,#126045);
#103582=AXIS2_PLACEMENT_3D('',#422895,#126049,#126050);
#103583=AXIS2_PLACEMENT_3D('',#422963,#126051,#126052);
#103584=AXIS2_PLACEMENT_3D('',#422964,#126053,#126054);
#103585=AXIS2_PLACEMENT_3D('',#423006,#126055,#126056);
#103586=AXIS2_PLACEMENT_3D('',#423033,#126057,#126058);
#103587=AXIS2_PLACEMENT_3D('',#423114,#126059,#126060);
#103588=AXIS2_PLACEMENT_3D('',#423127,#126061,#126062);
#103589=AXIS2_PLACEMENT_3D('',#423128,#126063,#126064);
#103590=AXIS2_PLACEMENT_3D('',#423129,#126065,#126066);
#103591=AXIS2_PLACEMENT_3D('',#423142,#126067,#126068);
#103592=AXIS2_PLACEMENT_3D('',#423155,#126069,#126070);
#103593=AXIS2_PLACEMENT_3D('',#423174,#126071,#126072);
#103594=AXIS2_PLACEMENT_3D('',#423187,#126073,#126074);
#103595=AXIS2_PLACEMENT_3D('',#423200,#126075,#126076);
#103596=AXIS2_PLACEMENT_3D('',#423201,#126077,#126078);
#103597=AXIS2_PLACEMENT_3D('',#423202,#126079,#126080);
#103598=AXIS2_PLACEMENT_3D('',#423215,#126081,#126082);
#103599=AXIS2_PLACEMENT_3D('',#423216,#126083,#126084);
#103600=AXIS2_PLACEMENT_3D('',#423223,#126087,#126088);
#103601=AXIS2_PLACEMENT_3D('',#423230,#126090,#126091);
#103602=AXIS2_PLACEMENT_3D('',#423233,#126092,#126093);
#103603=AXIS2_PLACEMENT_3D('',#423244,#126097,#126098);
#103604=AXIS2_PLACEMENT_3D('',#423312,#126099,#126100);
#103605=AXIS2_PLACEMENT_3D('',#423313,#126101,#126102);
#103606=AXIS2_PLACEMENT_3D('',#423355,#126103,#126104);
#103607=AXIS2_PLACEMENT_3D('',#423382,#126105,#126106);
#103608=AXIS2_PLACEMENT_3D('',#423463,#126107,#126108);
#103609=AXIS2_PLACEMENT_3D('',#423476,#126109,#126110);
#103610=AXIS2_PLACEMENT_3D('',#423477,#126111,#126112);
#103611=AXIS2_PLACEMENT_3D('',#423478,#126113,#126114);
#103612=AXIS2_PLACEMENT_3D('',#423491,#126115,#126116);
#103613=AXIS2_PLACEMENT_3D('',#423504,#126117,#126118);
#103614=AXIS2_PLACEMENT_3D('',#423523,#126119,#126120);
#103615=AXIS2_PLACEMENT_3D('',#423536,#126121,#126122);
#103616=AXIS2_PLACEMENT_3D('',#423549,#126123,#126124);
#103617=AXIS2_PLACEMENT_3D('',#423550,#126125,#126126);
#103618=AXIS2_PLACEMENT_3D('',#423551,#126127,#126128);
#103619=AXIS2_PLACEMENT_3D('',#423564,#126129,#126130);
#103620=AXIS2_PLACEMENT_3D('',#423565,#126131,#126132);
#103621=AXIS2_PLACEMENT_3D('',#423572,#126135,#126136);
#103622=AXIS2_PLACEMENT_3D('',#423579,#126138,#126139);
#103623=AXIS2_PLACEMENT_3D('',#423582,#126140,#126141);
#103624=AXIS2_PLACEMENT_3D('',#423593,#126145,#126146);
#103625=AXIS2_PLACEMENT_3D('',#423661,#126147,#126148);
#103626=AXIS2_PLACEMENT_3D('',#423662,#126149,#126150);
#103627=AXIS2_PLACEMENT_3D('',#423704,#126151,#126152);
#103628=AXIS2_PLACEMENT_3D('',#423731,#126153,#126154);
#103629=AXIS2_PLACEMENT_3D('',#423812,#126155,#126156);
#103630=AXIS2_PLACEMENT_3D('',#423825,#126157,#126158);
#103631=AXIS2_PLACEMENT_3D('',#423826,#126159,#126160);
#103632=AXIS2_PLACEMENT_3D('',#423827,#126161,#126162);
#103633=AXIS2_PLACEMENT_3D('',#423840,#126163,#126164);
#103634=AXIS2_PLACEMENT_3D('',#423853,#126165,#126166);
#103635=AXIS2_PLACEMENT_3D('',#423872,#126167,#126168);
#103636=AXIS2_PLACEMENT_3D('',#423885,#126169,#126170);
#103637=AXIS2_PLACEMENT_3D('',#423898,#126171,#126172);
#103638=AXIS2_PLACEMENT_3D('',#423899,#126173,#126174);
#103639=AXIS2_PLACEMENT_3D('',#423900,#126175,#126176);
#103640=AXIS2_PLACEMENT_3D('',#423913,#126177,#126178);
#103641=AXIS2_PLACEMENT_3D('',#423914,#126179,#126180);
#103642=AXIS2_PLACEMENT_3D('',#423921,#126183,#126184);
#103643=AXIS2_PLACEMENT_3D('',#423928,#126186,#126187);
#103644=AXIS2_PLACEMENT_3D('',#423931,#126188,#126189);
#103645=AXIS2_PLACEMENT_3D('',#423942,#126193,#126194);
#103646=AXIS2_PLACEMENT_3D('',#424010,#126195,#126196);
#103647=AXIS2_PLACEMENT_3D('',#424011,#126197,#126198);
#103648=AXIS2_PLACEMENT_3D('',#424053,#126199,#126200);
#103649=AXIS2_PLACEMENT_3D('',#424080,#126201,#126202);
#103650=AXIS2_PLACEMENT_3D('',#424161,#126203,#126204);
#103651=AXIS2_PLACEMENT_3D('',#424174,#126205,#126206);
#103652=AXIS2_PLACEMENT_3D('',#424175,#126207,#126208);
#103653=AXIS2_PLACEMENT_3D('',#424176,#126209,#126210);
#103654=AXIS2_PLACEMENT_3D('',#424189,#126211,#126212);
#103655=AXIS2_PLACEMENT_3D('',#424202,#126213,#126214);
#103656=AXIS2_PLACEMENT_3D('',#424221,#126215,#126216);
#103657=AXIS2_PLACEMENT_3D('',#424234,#126217,#126218);
#103658=AXIS2_PLACEMENT_3D('',#424247,#126219,#126220);
#103659=AXIS2_PLACEMENT_3D('',#424248,#126221,#126222);
#103660=AXIS2_PLACEMENT_3D('',#424249,#126223,#126224);
#103661=AXIS2_PLACEMENT_3D('',#424262,#126225,#126226);
#103662=AXIS2_PLACEMENT_3D('',#424263,#126227,#126228);
#103663=AXIS2_PLACEMENT_3D('',#424270,#126231,#126232);
#103664=AXIS2_PLACEMENT_3D('',#424277,#126234,#126235);
#103665=AXIS2_PLACEMENT_3D('',#424280,#126236,#126237);
#103666=AXIS2_PLACEMENT_3D('',#424291,#126241,#126242);
#103667=AXIS2_PLACEMENT_3D('',#424359,#126243,#126244);
#103668=AXIS2_PLACEMENT_3D('',#424360,#126245,#126246);
#103669=AXIS2_PLACEMENT_3D('',#424402,#126247,#126248);
#103670=AXIS2_PLACEMENT_3D('',#424429,#126249,#126250);
#103671=AXIS2_PLACEMENT_3D('',#424510,#126251,#126252);
#103672=AXIS2_PLACEMENT_3D('',#424523,#126253,#126254);
#103673=AXIS2_PLACEMENT_3D('',#424524,#126255,#126256);
#103674=AXIS2_PLACEMENT_3D('',#424525,#126257,#126258);
#103675=AXIS2_PLACEMENT_3D('',#424538,#126259,#126260);
#103676=AXIS2_PLACEMENT_3D('',#424551,#126261,#126262);
#103677=AXIS2_PLACEMENT_3D('',#424570,#126263,#126264);
#103678=AXIS2_PLACEMENT_3D('',#424583,#126265,#126266);
#103679=AXIS2_PLACEMENT_3D('',#424596,#126267,#126268);
#103680=AXIS2_PLACEMENT_3D('',#424597,#126269,#126270);
#103681=AXIS2_PLACEMENT_3D('',#424598,#126271,#126272);
#103682=AXIS2_PLACEMENT_3D('',#424611,#126273,#126274);
#103683=AXIS2_PLACEMENT_3D('',#424612,#126275,#126276);
#103684=AXIS2_PLACEMENT_3D('',#424619,#126279,#126280);
#103685=AXIS2_PLACEMENT_3D('',#424626,#126282,#126283);
#103686=AXIS2_PLACEMENT_3D('',#424629,#126284,#126285);
#103687=AXIS2_PLACEMENT_3D('',#424640,#126289,#126290);
#103688=AXIS2_PLACEMENT_3D('',#424708,#126291,#126292);
#103689=AXIS2_PLACEMENT_3D('',#424709,#126293,#126294);
#103690=AXIS2_PLACEMENT_3D('',#424751,#126295,#126296);
#103691=AXIS2_PLACEMENT_3D('',#424778,#126297,#126298);
#103692=AXIS2_PLACEMENT_3D('',#424859,#126299,#126300);
#103693=AXIS2_PLACEMENT_3D('',#424872,#126301,#126302);
#103694=AXIS2_PLACEMENT_3D('',#424873,#126303,#126304);
#103695=AXIS2_PLACEMENT_3D('',#424874,#126305,#126306);
#103696=AXIS2_PLACEMENT_3D('',#424887,#126307,#126308);
#103697=AXIS2_PLACEMENT_3D('',#424900,#126309,#126310);
#103698=AXIS2_PLACEMENT_3D('',#424919,#126311,#126312);
#103699=AXIS2_PLACEMENT_3D('',#424932,#126313,#126314);
#103700=AXIS2_PLACEMENT_3D('',#424945,#126315,#126316);
#103701=AXIS2_PLACEMENT_3D('',#424946,#126317,#126318);
#103702=AXIS2_PLACEMENT_3D('',#424947,#126319,#126320);
#103703=AXIS2_PLACEMENT_3D('',#424960,#126321,#126322);
#103704=AXIS2_PLACEMENT_3D('',#424961,#126323,#126324);
#103705=AXIS2_PLACEMENT_3D('',#424968,#126327,#126328);
#103706=AXIS2_PLACEMENT_3D('',#424975,#126330,#126331);
#103707=AXIS2_PLACEMENT_3D('',#424978,#126332,#126333);
#103708=AXIS2_PLACEMENT_3D('',#424989,#126337,#126338);
#103709=AXIS2_PLACEMENT_3D('',#425057,#126339,#126340);
#103710=AXIS2_PLACEMENT_3D('',#425058,#126341,#126342);
#103711=AXIS2_PLACEMENT_3D('',#425100,#126343,#126344);
#103712=AXIS2_PLACEMENT_3D('',#425127,#126345,#126346);
#103713=AXIS2_PLACEMENT_3D('',#425208,#126347,#126348);
#103714=AXIS2_PLACEMENT_3D('',#425221,#126349,#126350);
#103715=AXIS2_PLACEMENT_3D('',#425222,#126351,#126352);
#103716=AXIS2_PLACEMENT_3D('',#425223,#126353,#126354);
#103717=AXIS2_PLACEMENT_3D('',#425236,#126355,#126356);
#103718=AXIS2_PLACEMENT_3D('',#425249,#126357,#126358);
#103719=AXIS2_PLACEMENT_3D('',#425268,#126359,#126360);
#103720=AXIS2_PLACEMENT_3D('',#425281,#126361,#126362);
#103721=AXIS2_PLACEMENT_3D('',#425294,#126363,#126364);
#103722=AXIS2_PLACEMENT_3D('',#425295,#126365,#126366);
#103723=AXIS2_PLACEMENT_3D('',#425296,#126367,#126368);
#103724=AXIS2_PLACEMENT_3D('',#425309,#126369,#126370);
#103725=AXIS2_PLACEMENT_3D('',#425310,#126371,#126372);
#103726=AXIS2_PLACEMENT_3D('',#425317,#126375,#126376);
#103727=AXIS2_PLACEMENT_3D('',#425324,#126378,#126379);
#103728=AXIS2_PLACEMENT_3D('',#425327,#126380,#126381);
#103729=AXIS2_PLACEMENT_3D('',#425338,#126385,#126386);
#103730=AXIS2_PLACEMENT_3D('',#425406,#126387,#126388);
#103731=AXIS2_PLACEMENT_3D('',#425407,#126389,#126390);
#103732=AXIS2_PLACEMENT_3D('',#425449,#126391,#126392);
#103733=AXIS2_PLACEMENT_3D('',#425476,#126393,#126394);
#103734=AXIS2_PLACEMENT_3D('',#425557,#126395,#126396);
#103735=AXIS2_PLACEMENT_3D('',#425570,#126397,#126398);
#103736=AXIS2_PLACEMENT_3D('',#425571,#126399,#126400);
#103737=AXIS2_PLACEMENT_3D('',#425572,#126401,#126402);
#103738=AXIS2_PLACEMENT_3D('',#425585,#126403,#126404);
#103739=AXIS2_PLACEMENT_3D('',#425598,#126405,#126406);
#103740=AXIS2_PLACEMENT_3D('',#425617,#126407,#126408);
#103741=AXIS2_PLACEMENT_3D('',#425630,#126409,#126410);
#103742=AXIS2_PLACEMENT_3D('',#425643,#126411,#126412);
#103743=AXIS2_PLACEMENT_3D('',#425644,#126413,#126414);
#103744=AXIS2_PLACEMENT_3D('',#425645,#126415,#126416);
#103745=AXIS2_PLACEMENT_3D('',#425658,#126417,#126418);
#103746=AXIS2_PLACEMENT_3D('',#425659,#126419,#126420);
#103747=AXIS2_PLACEMENT_3D('',#425666,#126423,#126424);
#103748=AXIS2_PLACEMENT_3D('',#425673,#126426,#126427);
#103749=AXIS2_PLACEMENT_3D('',#425676,#126428,#126429);
#103750=AXIS2_PLACEMENT_3D('',#425687,#126433,#126434);
#103751=AXIS2_PLACEMENT_3D('',#425755,#126435,#126436);
#103752=AXIS2_PLACEMENT_3D('',#425756,#126437,#126438);
#103753=AXIS2_PLACEMENT_3D('',#425798,#126439,#126440);
#103754=AXIS2_PLACEMENT_3D('',#425825,#126441,#126442);
#103755=AXIS2_PLACEMENT_3D('',#425906,#126443,#126444);
#103756=AXIS2_PLACEMENT_3D('',#425919,#126445,#126446);
#103757=AXIS2_PLACEMENT_3D('',#425920,#126447,#126448);
#103758=AXIS2_PLACEMENT_3D('',#425921,#126449,#126450);
#103759=AXIS2_PLACEMENT_3D('',#425934,#126451,#126452);
#103760=AXIS2_PLACEMENT_3D('',#425947,#126453,#126454);
#103761=AXIS2_PLACEMENT_3D('',#425966,#126455,#126456);
#103762=AXIS2_PLACEMENT_3D('',#425979,#126457,#126458);
#103763=AXIS2_PLACEMENT_3D('',#425992,#126459,#126460);
#103764=AXIS2_PLACEMENT_3D('',#425993,#126461,#126462);
#103765=AXIS2_PLACEMENT_3D('',#425994,#126463,#126464);
#103766=AXIS2_PLACEMENT_3D('',#426007,#126465,#126466);
#103767=AXIS2_PLACEMENT_3D('',#426008,#126467,#126468);
#103768=AXIS2_PLACEMENT_3D('',#426015,#126471,#126472);
#103769=AXIS2_PLACEMENT_3D('',#426022,#126474,#126475);
#103770=AXIS2_PLACEMENT_3D('',#426025,#126476,#126477);
#103771=AXIS2_PLACEMENT_3D('',#426036,#126481,#126482);
#103772=AXIS2_PLACEMENT_3D('',#426104,#126483,#126484);
#103773=AXIS2_PLACEMENT_3D('',#426105,#126485,#126486);
#103774=AXIS2_PLACEMENT_3D('',#426147,#126487,#126488);
#103775=AXIS2_PLACEMENT_3D('',#426174,#126489,#126490);
#103776=AXIS2_PLACEMENT_3D('',#426255,#126491,#126492);
#103777=AXIS2_PLACEMENT_3D('',#426268,#126493,#126494);
#103778=AXIS2_PLACEMENT_3D('',#426269,#126495,#126496);
#103779=AXIS2_PLACEMENT_3D('',#426270,#126497,#126498);
#103780=AXIS2_PLACEMENT_3D('',#426283,#126499,#126500);
#103781=AXIS2_PLACEMENT_3D('',#426296,#126501,#126502);
#103782=AXIS2_PLACEMENT_3D('',#426315,#126503,#126504);
#103783=AXIS2_PLACEMENT_3D('',#426328,#126505,#126506);
#103784=AXIS2_PLACEMENT_3D('',#426341,#126507,#126508);
#103785=AXIS2_PLACEMENT_3D('',#426342,#126509,#126510);
#103786=AXIS2_PLACEMENT_3D('',#426343,#126511,#126512);
#103787=AXIS2_PLACEMENT_3D('',#426356,#126513,#126514);
#103788=AXIS2_PLACEMENT_3D('',#426357,#126515,#126516);
#103789=AXIS2_PLACEMENT_3D('',#426364,#126519,#126520);
#103790=AXIS2_PLACEMENT_3D('',#426371,#126522,#126523);
#103791=AXIS2_PLACEMENT_3D('',#426374,#126524,#126525);
#103792=AXIS2_PLACEMENT_3D('',#426385,#126529,#126530);
#103793=AXIS2_PLACEMENT_3D('',#426453,#126531,#126532);
#103794=AXIS2_PLACEMENT_3D('',#426454,#126533,#126534);
#103795=AXIS2_PLACEMENT_3D('',#426496,#126535,#126536);
#103796=AXIS2_PLACEMENT_3D('',#426523,#126537,#126538);
#103797=AXIS2_PLACEMENT_3D('',#426604,#126539,#126540);
#103798=AXIS2_PLACEMENT_3D('',#426617,#126541,#126542);
#103799=AXIS2_PLACEMENT_3D('',#426618,#126543,#126544);
#103800=AXIS2_PLACEMENT_3D('',#426619,#126545,#126546);
#103801=AXIS2_PLACEMENT_3D('',#426632,#126547,#126548);
#103802=AXIS2_PLACEMENT_3D('',#426645,#126549,#126550);
#103803=AXIS2_PLACEMENT_3D('',#426664,#126551,#126552);
#103804=AXIS2_PLACEMENT_3D('',#426677,#126553,#126554);
#103805=AXIS2_PLACEMENT_3D('',#426690,#126555,#126556);
#103806=AXIS2_PLACEMENT_3D('',#426691,#126557,#126558);
#103807=AXIS2_PLACEMENT_3D('',#426692,#126559,#126560);
#103808=AXIS2_PLACEMENT_3D('',#426705,#126561,#126562);
#103809=AXIS2_PLACEMENT_3D('',#426706,#126563,#126564);
#103810=AXIS2_PLACEMENT_3D('',#426713,#126567,#126568);
#103811=AXIS2_PLACEMENT_3D('',#426720,#126570,#126571);
#103812=AXIS2_PLACEMENT_3D('',#426723,#126572,#126573);
#103813=AXIS2_PLACEMENT_3D('',#426734,#126577,#126578);
#103814=AXIS2_PLACEMENT_3D('',#426802,#126579,#126580);
#103815=AXIS2_PLACEMENT_3D('',#426803,#126581,#126582);
#103816=AXIS2_PLACEMENT_3D('',#426845,#126583,#126584);
#103817=AXIS2_PLACEMENT_3D('',#426872,#126585,#126586);
#103818=AXIS2_PLACEMENT_3D('',#426953,#126587,#126588);
#103819=AXIS2_PLACEMENT_3D('',#426966,#126589,#126590);
#103820=AXIS2_PLACEMENT_3D('',#426967,#126591,#126592);
#103821=AXIS2_PLACEMENT_3D('',#426968,#126593,#126594);
#103822=AXIS2_PLACEMENT_3D('',#426981,#126595,#126596);
#103823=AXIS2_PLACEMENT_3D('',#426994,#126597,#126598);
#103824=AXIS2_PLACEMENT_3D('',#427013,#126599,#126600);
#103825=AXIS2_PLACEMENT_3D('',#427026,#126601,#126602);
#103826=AXIS2_PLACEMENT_3D('',#427039,#126603,#126604);
#103827=AXIS2_PLACEMENT_3D('',#427040,#126605,#126606);
#103828=AXIS2_PLACEMENT_3D('',#427041,#126607,#126608);
#103829=AXIS2_PLACEMENT_3D('',#427054,#126609,#126610);
#103830=AXIS2_PLACEMENT_3D('',#427055,#126611,#126612);
#103831=AXIS2_PLACEMENT_3D('',#427062,#126615,#126616);
#103832=AXIS2_PLACEMENT_3D('',#427069,#126618,#126619);
#103833=AXIS2_PLACEMENT_3D('',#427072,#126620,#126621);
#103834=AXIS2_PLACEMENT_3D('',#427083,#126625,#126626);
#103835=AXIS2_PLACEMENT_3D('',#427151,#126627,#126628);
#103836=AXIS2_PLACEMENT_3D('',#427152,#126629,#126630);
#103837=AXIS2_PLACEMENT_3D('',#427194,#126631,#126632);
#103838=AXIS2_PLACEMENT_3D('',#427221,#126633,#126634);
#103839=AXIS2_PLACEMENT_3D('',#427302,#126635,#126636);
#103840=AXIS2_PLACEMENT_3D('',#427315,#126637,#126638);
#103841=AXIS2_PLACEMENT_3D('',#427316,#126639,#126640);
#103842=AXIS2_PLACEMENT_3D('',#427317,#126641,#126642);
#103843=AXIS2_PLACEMENT_3D('',#427330,#126643,#126644);
#103844=AXIS2_PLACEMENT_3D('',#427343,#126645,#126646);
#103845=AXIS2_PLACEMENT_3D('',#427362,#126647,#126648);
#103846=AXIS2_PLACEMENT_3D('',#427375,#126649,#126650);
#103847=AXIS2_PLACEMENT_3D('',#427388,#126651,#126652);
#103848=AXIS2_PLACEMENT_3D('',#427389,#126653,#126654);
#103849=AXIS2_PLACEMENT_3D('',#427390,#126655,#126656);
#103850=AXIS2_PLACEMENT_3D('',#427403,#126657,#126658);
#103851=AXIS2_PLACEMENT_3D('',#427404,#126659,#126660);
#103852=AXIS2_PLACEMENT_3D('',#427411,#126663,#126664);
#103853=AXIS2_PLACEMENT_3D('',#427418,#126666,#126667);
#103854=AXIS2_PLACEMENT_3D('',#427421,#126668,#126669);
#103855=AXIS2_PLACEMENT_3D('',#427432,#126673,#126674);
#103856=AXIS2_PLACEMENT_3D('',#427500,#126675,#126676);
#103857=AXIS2_PLACEMENT_3D('',#427501,#126677,#126678);
#103858=AXIS2_PLACEMENT_3D('',#427543,#126679,#126680);
#103859=AXIS2_PLACEMENT_3D('',#427570,#126681,#126682);
#103860=AXIS2_PLACEMENT_3D('',#427651,#126683,#126684);
#103861=AXIS2_PLACEMENT_3D('',#427664,#126685,#126686);
#103862=AXIS2_PLACEMENT_3D('',#427665,#126687,#126688);
#103863=AXIS2_PLACEMENT_3D('',#427666,#126689,#126690);
#103864=AXIS2_PLACEMENT_3D('',#427679,#126691,#126692);
#103865=AXIS2_PLACEMENT_3D('',#427692,#126693,#126694);
#103866=AXIS2_PLACEMENT_3D('',#427711,#126695,#126696);
#103867=AXIS2_PLACEMENT_3D('',#427724,#126697,#126698);
#103868=AXIS2_PLACEMENT_3D('',#427737,#126699,#126700);
#103869=AXIS2_PLACEMENT_3D('',#427738,#126701,#126702);
#103870=AXIS2_PLACEMENT_3D('',#427739,#126703,#126704);
#103871=AXIS2_PLACEMENT_3D('',#427752,#126705,#126706);
#103872=AXIS2_PLACEMENT_3D('',#427753,#126707,#126708);
#103873=AXIS2_PLACEMENT_3D('',#427760,#126711,#126712);
#103874=AXIS2_PLACEMENT_3D('',#427767,#126714,#126715);
#103875=AXIS2_PLACEMENT_3D('',#427770,#126716,#126717);
#103876=AXIS2_PLACEMENT_3D('',#427781,#126721,#126722);
#103877=AXIS2_PLACEMENT_3D('',#427849,#126723,#126724);
#103878=AXIS2_PLACEMENT_3D('',#427850,#126725,#126726);
#103879=AXIS2_PLACEMENT_3D('',#427892,#126727,#126728);
#103880=AXIS2_PLACEMENT_3D('',#427919,#126729,#126730);
#103881=AXIS2_PLACEMENT_3D('',#428000,#126731,#126732);
#103882=AXIS2_PLACEMENT_3D('',#428013,#126733,#126734);
#103883=AXIS2_PLACEMENT_3D('',#428014,#126735,#126736);
#103884=AXIS2_PLACEMENT_3D('',#428015,#126737,#126738);
#103885=AXIS2_PLACEMENT_3D('',#428028,#126739,#126740);
#103886=AXIS2_PLACEMENT_3D('',#428041,#126741,#126742);
#103887=AXIS2_PLACEMENT_3D('',#428060,#126743,#126744);
#103888=AXIS2_PLACEMENT_3D('',#428073,#126745,#126746);
#103889=AXIS2_PLACEMENT_3D('',#428086,#126747,#126748);
#103890=AXIS2_PLACEMENT_3D('',#428087,#126749,#126750);
#103891=AXIS2_PLACEMENT_3D('',#428088,#126751,#126752);
#103892=AXIS2_PLACEMENT_3D('',#428101,#126753,#126754);
#103893=AXIS2_PLACEMENT_3D('',#428102,#126755,#126756);
#103894=AXIS2_PLACEMENT_3D('',#428109,#126759,#126760);
#103895=AXIS2_PLACEMENT_3D('',#428116,#126762,#126763);
#103896=AXIS2_PLACEMENT_3D('',#428119,#126764,#126765);
#103897=AXIS2_PLACEMENT_3D('',#428130,#126769,#126770);
#103898=AXIS2_PLACEMENT_3D('',#428198,#126771,#126772);
#103899=AXIS2_PLACEMENT_3D('',#428199,#126773,#126774);
#103900=AXIS2_PLACEMENT_3D('',#428241,#126775,#126776);
#103901=AXIS2_PLACEMENT_3D('',#428268,#126777,#126778);
#103902=AXIS2_PLACEMENT_3D('',#428349,#126779,#126780);
#103903=AXIS2_PLACEMENT_3D('',#428362,#126781,#126782);
#103904=AXIS2_PLACEMENT_3D('',#428363,#126783,#126784);
#103905=AXIS2_PLACEMENT_3D('',#428364,#126785,#126786);
#103906=AXIS2_PLACEMENT_3D('',#428377,#126787,#126788);
#103907=AXIS2_PLACEMENT_3D('',#428390,#126789,#126790);
#103908=AXIS2_PLACEMENT_3D('',#428409,#126791,#126792);
#103909=AXIS2_PLACEMENT_3D('',#428422,#126793,#126794);
#103910=AXIS2_PLACEMENT_3D('',#428435,#126795,#126796);
#103911=AXIS2_PLACEMENT_3D('',#428436,#126797,#126798);
#103912=AXIS2_PLACEMENT_3D('',#428437,#126799,#126800);
#103913=AXIS2_PLACEMENT_3D('',#428450,#126801,#126802);
#103914=AXIS2_PLACEMENT_3D('',#428451,#126803,#126804);
#103915=AXIS2_PLACEMENT_3D('',#428458,#126807,#126808);
#103916=AXIS2_PLACEMENT_3D('',#428465,#126810,#126811);
#103917=AXIS2_PLACEMENT_3D('',#428468,#126812,#126813);
#103918=AXIS2_PLACEMENT_3D('',#428479,#126817,#126818);
#103919=AXIS2_PLACEMENT_3D('',#428547,#126819,#126820);
#103920=AXIS2_PLACEMENT_3D('',#428548,#126821,#126822);
#103921=AXIS2_PLACEMENT_3D('',#428590,#126823,#126824);
#103922=AXIS2_PLACEMENT_3D('',#428617,#126825,#126826);
#103923=AXIS2_PLACEMENT_3D('',#428698,#126827,#126828);
#103924=AXIS2_PLACEMENT_3D('',#428711,#126829,#126830);
#103925=AXIS2_PLACEMENT_3D('',#428712,#126831,#126832);
#103926=AXIS2_PLACEMENT_3D('',#428713,#126833,#126834);
#103927=AXIS2_PLACEMENT_3D('',#428726,#126835,#126836);
#103928=AXIS2_PLACEMENT_3D('',#428739,#126837,#126838);
#103929=AXIS2_PLACEMENT_3D('',#428758,#126839,#126840);
#103930=AXIS2_PLACEMENT_3D('',#428771,#126841,#126842);
#103931=AXIS2_PLACEMENT_3D('',#428784,#126843,#126844);
#103932=AXIS2_PLACEMENT_3D('',#428785,#126845,#126846);
#103933=AXIS2_PLACEMENT_3D('',#428786,#126847,#126848);
#103934=AXIS2_PLACEMENT_3D('',#428799,#126849,#126850);
#103935=AXIS2_PLACEMENT_3D('',#428800,#126851,#126852);
#103936=AXIS2_PLACEMENT_3D('',#428807,#126855,#126856);
#103937=AXIS2_PLACEMENT_3D('',#428814,#126858,#126859);
#103938=AXIS2_PLACEMENT_3D('',#428817,#126860,#126861);
#103939=AXIS2_PLACEMENT_3D('',#428828,#126865,#126866);
#103940=AXIS2_PLACEMENT_3D('',#428896,#126867,#126868);
#103941=AXIS2_PLACEMENT_3D('',#428897,#126869,#126870);
#103942=AXIS2_PLACEMENT_3D('',#428939,#126871,#126872);
#103943=AXIS2_PLACEMENT_3D('',#428966,#126873,#126874);
#103944=AXIS2_PLACEMENT_3D('',#429047,#126875,#126876);
#103945=AXIS2_PLACEMENT_3D('',#429060,#126877,#126878);
#103946=AXIS2_PLACEMENT_3D('',#429061,#126879,#126880);
#103947=AXIS2_PLACEMENT_3D('',#429062,#126881,#126882);
#103948=AXIS2_PLACEMENT_3D('',#429075,#126883,#126884);
#103949=AXIS2_PLACEMENT_3D('',#429088,#126885,#126886);
#103950=AXIS2_PLACEMENT_3D('',#429107,#126887,#126888);
#103951=AXIS2_PLACEMENT_3D('',#429120,#126889,#126890);
#103952=AXIS2_PLACEMENT_3D('',#429133,#126891,#126892);
#103953=AXIS2_PLACEMENT_3D('',#429134,#126893,#126894);
#103954=AXIS2_PLACEMENT_3D('',#429135,#126895,#126896);
#103955=AXIS2_PLACEMENT_3D('',#429148,#126897,#126898);
#103956=AXIS2_PLACEMENT_3D('',#429149,#126899,#126900);
#103957=AXIS2_PLACEMENT_3D('',#429156,#126903,#126904);
#103958=AXIS2_PLACEMENT_3D('',#429163,#126906,#126907);
#103959=AXIS2_PLACEMENT_3D('',#429166,#126908,#126909);
#103960=AXIS2_PLACEMENT_3D('',#429177,#126913,#126914);
#103961=AXIS2_PLACEMENT_3D('',#429245,#126915,#126916);
#103962=AXIS2_PLACEMENT_3D('',#429246,#126917,#126918);
#103963=AXIS2_PLACEMENT_3D('',#429288,#126919,#126920);
#103964=AXIS2_PLACEMENT_3D('',#429315,#126921,#126922);
#103965=AXIS2_PLACEMENT_3D('',#429396,#126923,#126924);
#103966=AXIS2_PLACEMENT_3D('',#429409,#126925,#126926);
#103967=AXIS2_PLACEMENT_3D('',#429410,#126927,#126928);
#103968=AXIS2_PLACEMENT_3D('',#429411,#126929,#126930);
#103969=AXIS2_PLACEMENT_3D('',#429424,#126931,#126932);
#103970=AXIS2_PLACEMENT_3D('',#429437,#126933,#126934);
#103971=AXIS2_PLACEMENT_3D('',#429456,#126935,#126936);
#103972=AXIS2_PLACEMENT_3D('',#429469,#126937,#126938);
#103973=AXIS2_PLACEMENT_3D('',#429482,#126939,#126940);
#103974=AXIS2_PLACEMENT_3D('',#429483,#126941,#126942);
#103975=AXIS2_PLACEMENT_3D('',#429484,#126943,#126944);
#103976=AXIS2_PLACEMENT_3D('',#429497,#126945,#126946);
#103977=AXIS2_PLACEMENT_3D('',#429498,#126947,#126948);
#103978=AXIS2_PLACEMENT_3D('',#429505,#126951,#126952);
#103979=AXIS2_PLACEMENT_3D('',#429512,#126954,#126955);
#103980=AXIS2_PLACEMENT_3D('',#429515,#126956,#126957);
#103981=AXIS2_PLACEMENT_3D('',#429526,#126961,#126962);
#103982=AXIS2_PLACEMENT_3D('',#429594,#126963,#126964);
#103983=AXIS2_PLACEMENT_3D('',#429595,#126965,#126966);
#103984=AXIS2_PLACEMENT_3D('',#429637,#126967,#126968);
#103985=AXIS2_PLACEMENT_3D('',#429664,#126969,#126970);
#103986=AXIS2_PLACEMENT_3D('',#429745,#126971,#126972);
#103987=AXIS2_PLACEMENT_3D('',#429758,#126973,#126974);
#103988=AXIS2_PLACEMENT_3D('',#429759,#126975,#126976);
#103989=AXIS2_PLACEMENT_3D('',#429760,#126977,#126978);
#103990=AXIS2_PLACEMENT_3D('',#429773,#126979,#126980);
#103991=AXIS2_PLACEMENT_3D('',#429786,#126981,#126982);
#103992=AXIS2_PLACEMENT_3D('',#429805,#126983,#126984);
#103993=AXIS2_PLACEMENT_3D('',#429818,#126985,#126986);
#103994=AXIS2_PLACEMENT_3D('',#429831,#126987,#126988);
#103995=AXIS2_PLACEMENT_3D('',#429832,#126989,#126990);
#103996=AXIS2_PLACEMENT_3D('',#429833,#126991,#126992);
#103997=AXIS2_PLACEMENT_3D('',#429846,#126993,#126994);
#103998=AXIS2_PLACEMENT_3D('',#429847,#126995,#126996);
#103999=AXIS2_PLACEMENT_3D('',#429854,#126999,#127000);
#104000=AXIS2_PLACEMENT_3D('',#429861,#127002,#127003);
#104001=AXIS2_PLACEMENT_3D('',#429864,#127004,#127005);
#104002=AXIS2_PLACEMENT_3D('',#429875,#127009,#127010);
#104003=AXIS2_PLACEMENT_3D('',#429943,#127011,#127012);
#104004=AXIS2_PLACEMENT_3D('',#429944,#127013,#127014);
#104005=AXIS2_PLACEMENT_3D('',#429986,#127015,#127016);
#104006=AXIS2_PLACEMENT_3D('',#430013,#127017,#127018);
#104007=AXIS2_PLACEMENT_3D('',#430094,#127019,#127020);
#104008=AXIS2_PLACEMENT_3D('',#430107,#127021,#127022);
#104009=AXIS2_PLACEMENT_3D('',#430108,#127023,#127024);
#104010=AXIS2_PLACEMENT_3D('',#430109,#127025,#127026);
#104011=AXIS2_PLACEMENT_3D('',#430122,#127027,#127028);
#104012=AXIS2_PLACEMENT_3D('',#430135,#127029,#127030);
#104013=AXIS2_PLACEMENT_3D('',#430154,#127031,#127032);
#104014=AXIS2_PLACEMENT_3D('',#430167,#127033,#127034);
#104015=AXIS2_PLACEMENT_3D('',#430180,#127035,#127036);
#104016=AXIS2_PLACEMENT_3D('',#430181,#127037,#127038);
#104017=AXIS2_PLACEMENT_3D('',#430182,#127039,#127040);
#104018=AXIS2_PLACEMENT_3D('',#430195,#127041,#127042);
#104019=AXIS2_PLACEMENT_3D('',#430196,#127043,#127044);
#104020=AXIS2_PLACEMENT_3D('',#430203,#127047,#127048);
#104021=AXIS2_PLACEMENT_3D('',#430210,#127050,#127051);
#104022=AXIS2_PLACEMENT_3D('',#430213,#127052,#127053);
#104023=AXIS2_PLACEMENT_3D('',#430224,#127057,#127058);
#104024=AXIS2_PLACEMENT_3D('',#430292,#127059,#127060);
#104025=AXIS2_PLACEMENT_3D('',#430293,#127061,#127062);
#104026=AXIS2_PLACEMENT_3D('',#430335,#127063,#127064);
#104027=AXIS2_PLACEMENT_3D('',#430362,#127065,#127066);
#104028=AXIS2_PLACEMENT_3D('',#430443,#127067,#127068);
#104029=AXIS2_PLACEMENT_3D('',#430456,#127069,#127070);
#104030=AXIS2_PLACEMENT_3D('',#430457,#127071,#127072);
#104031=AXIS2_PLACEMENT_3D('',#430458,#127073,#127074);
#104032=AXIS2_PLACEMENT_3D('',#430471,#127075,#127076);
#104033=AXIS2_PLACEMENT_3D('',#430484,#127077,#127078);
#104034=AXIS2_PLACEMENT_3D('',#430503,#127079,#127080);
#104035=AXIS2_PLACEMENT_3D('',#430516,#127081,#127082);
#104036=AXIS2_PLACEMENT_3D('',#430529,#127083,#127084);
#104037=AXIS2_PLACEMENT_3D('',#430530,#127085,#127086);
#104038=AXIS2_PLACEMENT_3D('',#430531,#127087,#127088);
#104039=AXIS2_PLACEMENT_3D('',#430544,#127089,#127090);
#104040=AXIS2_PLACEMENT_3D('',#430545,#127091,#127092);
#104041=AXIS2_PLACEMENT_3D('',#430552,#127095,#127096);
#104042=AXIS2_PLACEMENT_3D('',#430559,#127098,#127099);
#104043=AXIS2_PLACEMENT_3D('',#430562,#127100,#127101);
#104044=AXIS2_PLACEMENT_3D('',#430573,#127105,#127106);
#104045=AXIS2_PLACEMENT_3D('',#430641,#127107,#127108);
#104046=AXIS2_PLACEMENT_3D('',#430642,#127109,#127110);
#104047=AXIS2_PLACEMENT_3D('',#430684,#127111,#127112);
#104048=AXIS2_PLACEMENT_3D('',#430711,#127113,#127114);
#104049=AXIS2_PLACEMENT_3D('',#430792,#127115,#127116);
#104050=AXIS2_PLACEMENT_3D('',#430805,#127117,#127118);
#104051=AXIS2_PLACEMENT_3D('',#430806,#127119,#127120);
#104052=AXIS2_PLACEMENT_3D('',#430807,#127121,#127122);
#104053=AXIS2_PLACEMENT_3D('',#430820,#127123,#127124);
#104054=AXIS2_PLACEMENT_3D('',#430833,#127125,#127126);
#104055=AXIS2_PLACEMENT_3D('',#430852,#127127,#127128);
#104056=AXIS2_PLACEMENT_3D('',#430865,#127129,#127130);
#104057=AXIS2_PLACEMENT_3D('',#430878,#127131,#127132);
#104058=AXIS2_PLACEMENT_3D('',#430879,#127133,#127134);
#104059=AXIS2_PLACEMENT_3D('',#430880,#127135,#127136);
#104060=AXIS2_PLACEMENT_3D('',#430893,#127137,#127138);
#104061=AXIS2_PLACEMENT_3D('',#430894,#127139,#127140);
#104062=AXIS2_PLACEMENT_3D('',#430901,#127143,#127144);
#104063=AXIS2_PLACEMENT_3D('',#430908,#127146,#127147);
#104064=AXIS2_PLACEMENT_3D('',#430911,#127148,#127149);
#104065=AXIS2_PLACEMENT_3D('',#430922,#127153,#127154);
#104066=AXIS2_PLACEMENT_3D('',#430990,#127155,#127156);
#104067=AXIS2_PLACEMENT_3D('',#430991,#127157,#127158);
#104068=AXIS2_PLACEMENT_3D('',#431033,#127159,#127160);
#104069=AXIS2_PLACEMENT_3D('',#431060,#127161,#127162);
#104070=AXIS2_PLACEMENT_3D('',#431141,#127163,#127164);
#104071=AXIS2_PLACEMENT_3D('',#431154,#127165,#127166);
#104072=AXIS2_PLACEMENT_3D('',#431155,#127167,#127168);
#104073=AXIS2_PLACEMENT_3D('',#431156,#127169,#127170);
#104074=AXIS2_PLACEMENT_3D('',#431169,#127171,#127172);
#104075=AXIS2_PLACEMENT_3D('',#431182,#127173,#127174);
#104076=AXIS2_PLACEMENT_3D('',#431201,#127175,#127176);
#104077=AXIS2_PLACEMENT_3D('',#431214,#127177,#127178);
#104078=AXIS2_PLACEMENT_3D('',#431227,#127179,#127180);
#104079=AXIS2_PLACEMENT_3D('',#431228,#127181,#127182);
#104080=AXIS2_PLACEMENT_3D('',#431229,#127183,#127184);
#104081=AXIS2_PLACEMENT_3D('',#431242,#127185,#127186);
#104082=AXIS2_PLACEMENT_3D('',#431243,#127187,#127188);
#104083=AXIS2_PLACEMENT_3D('',#431250,#127191,#127192);
#104084=AXIS2_PLACEMENT_3D('',#431257,#127194,#127195);
#104085=AXIS2_PLACEMENT_3D('',#431260,#127196,#127197);
#104086=AXIS2_PLACEMENT_3D('',#431271,#127201,#127202);
#104087=AXIS2_PLACEMENT_3D('',#431339,#127203,#127204);
#104088=AXIS2_PLACEMENT_3D('',#431340,#127205,#127206);
#104089=AXIS2_PLACEMENT_3D('',#431382,#127207,#127208);
#104090=AXIS2_PLACEMENT_3D('',#431409,#127209,#127210);
#104091=AXIS2_PLACEMENT_3D('',#431490,#127211,#127212);
#104092=AXIS2_PLACEMENT_3D('',#431503,#127213,#127214);
#104093=AXIS2_PLACEMENT_3D('',#431504,#127215,#127216);
#104094=AXIS2_PLACEMENT_3D('',#431505,#127217,#127218);
#104095=AXIS2_PLACEMENT_3D('',#431518,#127219,#127220);
#104096=AXIS2_PLACEMENT_3D('',#431531,#127221,#127222);
#104097=AXIS2_PLACEMENT_3D('',#431550,#127223,#127224);
#104098=AXIS2_PLACEMENT_3D('',#431563,#127225,#127226);
#104099=AXIS2_PLACEMENT_3D('',#431576,#127227,#127228);
#104100=AXIS2_PLACEMENT_3D('',#431577,#127229,#127230);
#104101=AXIS2_PLACEMENT_3D('',#431578,#127231,#127232);
#104102=AXIS2_PLACEMENT_3D('',#431591,#127233,#127234);
#104103=AXIS2_PLACEMENT_3D('',#431592,#127235,#127236);
#104104=AXIS2_PLACEMENT_3D('',#431599,#127239,#127240);
#104105=AXIS2_PLACEMENT_3D('',#431606,#127242,#127243);
#104106=AXIS2_PLACEMENT_3D('',#431609,#127244,#127245);
#104107=AXIS2_PLACEMENT_3D('',#431620,#127249,#127250);
#104108=AXIS2_PLACEMENT_3D('',#431688,#127251,#127252);
#104109=AXIS2_PLACEMENT_3D('',#431689,#127253,#127254);
#104110=AXIS2_PLACEMENT_3D('',#431731,#127255,#127256);
#104111=AXIS2_PLACEMENT_3D('',#431758,#127257,#127258);
#104112=AXIS2_PLACEMENT_3D('',#431839,#127259,#127260);
#104113=AXIS2_PLACEMENT_3D('',#431852,#127261,#127262);
#104114=AXIS2_PLACEMENT_3D('',#431853,#127263,#127264);
#104115=AXIS2_PLACEMENT_3D('',#431854,#127265,#127266);
#104116=AXIS2_PLACEMENT_3D('',#431867,#127267,#127268);
#104117=AXIS2_PLACEMENT_3D('',#431880,#127269,#127270);
#104118=AXIS2_PLACEMENT_3D('',#431899,#127271,#127272);
#104119=AXIS2_PLACEMENT_3D('',#431912,#127273,#127274);
#104120=AXIS2_PLACEMENT_3D('',#431925,#127275,#127276);
#104121=AXIS2_PLACEMENT_3D('',#431926,#127277,#127278);
#104122=AXIS2_PLACEMENT_3D('',#431927,#127279,#127280);
#104123=AXIS2_PLACEMENT_3D('',#431940,#127281,#127282);
#104124=AXIS2_PLACEMENT_3D('',#431941,#127283,#127284);
#104125=AXIS2_PLACEMENT_3D('',#431948,#127287,#127288);
#104126=AXIS2_PLACEMENT_3D('',#431955,#127290,#127291);
#104127=AXIS2_PLACEMENT_3D('',#431958,#127292,#127293);
#104128=AXIS2_PLACEMENT_3D('',#431969,#127297,#127298);
#104129=AXIS2_PLACEMENT_3D('',#432037,#127299,#127300);
#104130=AXIS2_PLACEMENT_3D('',#432038,#127301,#127302);
#104131=AXIS2_PLACEMENT_3D('',#432080,#127303,#127304);
#104132=AXIS2_PLACEMENT_3D('',#432107,#127305,#127306);
#104133=AXIS2_PLACEMENT_3D('',#432188,#127307,#127308);
#104134=AXIS2_PLACEMENT_3D('',#432201,#127309,#127310);
#104135=AXIS2_PLACEMENT_3D('',#432202,#127311,#127312);
#104136=AXIS2_PLACEMENT_3D('',#432203,#127313,#127314);
#104137=AXIS2_PLACEMENT_3D('',#432216,#127315,#127316);
#104138=AXIS2_PLACEMENT_3D('',#432229,#127317,#127318);
#104139=AXIS2_PLACEMENT_3D('',#432248,#127319,#127320);
#104140=AXIS2_PLACEMENT_3D('',#432261,#127321,#127322);
#104141=AXIS2_PLACEMENT_3D('',#432274,#127323,#127324);
#104142=AXIS2_PLACEMENT_3D('',#432275,#127325,#127326);
#104143=AXIS2_PLACEMENT_3D('',#432276,#127327,#127328);
#104144=AXIS2_PLACEMENT_3D('',#432289,#127329,#127330);
#104145=AXIS2_PLACEMENT_3D('',#432290,#127331,#127332);
#104146=AXIS2_PLACEMENT_3D('',#432297,#127335,#127336);
#104147=AXIS2_PLACEMENT_3D('',#432304,#127338,#127339);
#104148=AXIS2_PLACEMENT_3D('',#432307,#127340,#127341);
#104149=AXIS2_PLACEMENT_3D('',#432318,#127345,#127346);
#104150=AXIS2_PLACEMENT_3D('',#432386,#127347,#127348);
#104151=AXIS2_PLACEMENT_3D('',#432387,#127349,#127350);
#104152=AXIS2_PLACEMENT_3D('',#432429,#127351,#127352);
#104153=AXIS2_PLACEMENT_3D('',#432456,#127353,#127354);
#104154=AXIS2_PLACEMENT_3D('',#432537,#127355,#127356);
#104155=AXIS2_PLACEMENT_3D('',#432550,#127357,#127358);
#104156=AXIS2_PLACEMENT_3D('',#432551,#127359,#127360);
#104157=AXIS2_PLACEMENT_3D('',#432552,#127361,#127362);
#104158=AXIS2_PLACEMENT_3D('',#432565,#127363,#127364);
#104159=AXIS2_PLACEMENT_3D('',#432578,#127365,#127366);
#104160=AXIS2_PLACEMENT_3D('',#432597,#127367,#127368);
#104161=AXIS2_PLACEMENT_3D('',#432610,#127369,#127370);
#104162=AXIS2_PLACEMENT_3D('',#432623,#127371,#127372);
#104163=AXIS2_PLACEMENT_3D('',#432624,#127373,#127374);
#104164=AXIS2_PLACEMENT_3D('',#432625,#127375,#127376);
#104165=AXIS2_PLACEMENT_3D('',#432638,#127377,#127378);
#104166=AXIS2_PLACEMENT_3D('',#432639,#127379,#127380);
#104167=AXIS2_PLACEMENT_3D('',#432646,#127383,#127384);
#104168=AXIS2_PLACEMENT_3D('',#432653,#127386,#127387);
#104169=AXIS2_PLACEMENT_3D('',#432656,#127388,#127389);
#104170=AXIS2_PLACEMENT_3D('',#432667,#127393,#127394);
#104171=AXIS2_PLACEMENT_3D('',#432735,#127395,#127396);
#104172=AXIS2_PLACEMENT_3D('',#432736,#127397,#127398);
#104173=AXIS2_PLACEMENT_3D('',#432778,#127399,#127400);
#104174=AXIS2_PLACEMENT_3D('',#432805,#127401,#127402);
#104175=AXIS2_PLACEMENT_3D('',#432886,#127403,#127404);
#104176=AXIS2_PLACEMENT_3D('',#432899,#127405,#127406);
#104177=AXIS2_PLACEMENT_3D('',#432900,#127407,#127408);
#104178=AXIS2_PLACEMENT_3D('',#432901,#127409,#127410);
#104179=AXIS2_PLACEMENT_3D('',#432914,#127411,#127412);
#104180=AXIS2_PLACEMENT_3D('',#432927,#127413,#127414);
#104181=AXIS2_PLACEMENT_3D('',#432946,#127415,#127416);
#104182=AXIS2_PLACEMENT_3D('',#432959,#127417,#127418);
#104183=AXIS2_PLACEMENT_3D('',#432972,#127419,#127420);
#104184=AXIS2_PLACEMENT_3D('',#432973,#127421,#127422);
#104185=AXIS2_PLACEMENT_3D('',#432974,#127423,#127424);
#104186=AXIS2_PLACEMENT_3D('',#432987,#127425,#127426);
#104187=AXIS2_PLACEMENT_3D('',#432988,#127427,#127428);
#104188=AXIS2_PLACEMENT_3D('',#432995,#127431,#127432);
#104189=AXIS2_PLACEMENT_3D('',#433002,#127434,#127435);
#104190=AXIS2_PLACEMENT_3D('',#433005,#127436,#127437);
#104191=AXIS2_PLACEMENT_3D('',#433016,#127441,#127442);
#104192=AXIS2_PLACEMENT_3D('',#433084,#127443,#127444);
#104193=AXIS2_PLACEMENT_3D('',#433085,#127445,#127446);
#104194=AXIS2_PLACEMENT_3D('',#433127,#127447,#127448);
#104195=AXIS2_PLACEMENT_3D('',#433154,#127449,#127450);
#104196=AXIS2_PLACEMENT_3D('',#433235,#127451,#127452);
#104197=AXIS2_PLACEMENT_3D('',#433248,#127453,#127454);
#104198=AXIS2_PLACEMENT_3D('',#433249,#127455,#127456);
#104199=AXIS2_PLACEMENT_3D('',#433250,#127457,#127458);
#104200=AXIS2_PLACEMENT_3D('',#433263,#127459,#127460);
#104201=AXIS2_PLACEMENT_3D('',#433276,#127461,#127462);
#104202=AXIS2_PLACEMENT_3D('',#433295,#127463,#127464);
#104203=AXIS2_PLACEMENT_3D('',#433308,#127465,#127466);
#104204=AXIS2_PLACEMENT_3D('',#433321,#127467,#127468);
#104205=AXIS2_PLACEMENT_3D('',#433322,#127469,#127470);
#104206=AXIS2_PLACEMENT_3D('',#433323,#127471,#127472);
#104207=AXIS2_PLACEMENT_3D('',#433336,#127473,#127474);
#104208=AXIS2_PLACEMENT_3D('',#433337,#127475,#127476);
#104209=AXIS2_PLACEMENT_3D('',#433344,#127479,#127480);
#104210=AXIS2_PLACEMENT_3D('',#433351,#127482,#127483);
#104211=AXIS2_PLACEMENT_3D('',#433354,#127484,#127485);
#104212=AXIS2_PLACEMENT_3D('',#433365,#127489,#127490);
#104213=AXIS2_PLACEMENT_3D('',#433433,#127491,#127492);
#104214=AXIS2_PLACEMENT_3D('',#433434,#127493,#127494);
#104215=AXIS2_PLACEMENT_3D('',#433476,#127495,#127496);
#104216=AXIS2_PLACEMENT_3D('',#433503,#127497,#127498);
#104217=AXIS2_PLACEMENT_3D('',#433584,#127499,#127500);
#104218=AXIS2_PLACEMENT_3D('',#433597,#127501,#127502);
#104219=AXIS2_PLACEMENT_3D('',#433598,#127503,#127504);
#104220=AXIS2_PLACEMENT_3D('',#433599,#127505,#127506);
#104221=AXIS2_PLACEMENT_3D('',#433612,#127507,#127508);
#104222=AXIS2_PLACEMENT_3D('',#433625,#127509,#127510);
#104223=AXIS2_PLACEMENT_3D('',#433644,#127511,#127512);
#104224=AXIS2_PLACEMENT_3D('',#433657,#127513,#127514);
#104225=AXIS2_PLACEMENT_3D('',#433670,#127515,#127516);
#104226=AXIS2_PLACEMENT_3D('',#433671,#127517,#127518);
#104227=AXIS2_PLACEMENT_3D('',#433672,#127519,#127520);
#104228=AXIS2_PLACEMENT_3D('',#433685,#127521,#127522);
#104229=AXIS2_PLACEMENT_3D('',#433686,#127523,#127524);
#104230=AXIS2_PLACEMENT_3D('',#433693,#127527,#127528);
#104231=AXIS2_PLACEMENT_3D('',#433700,#127530,#127531);
#104232=AXIS2_PLACEMENT_3D('',#433703,#127532,#127533);
#104233=AXIS2_PLACEMENT_3D('',#433714,#127537,#127538);
#104234=AXIS2_PLACEMENT_3D('',#433782,#127539,#127540);
#104235=AXIS2_PLACEMENT_3D('',#433783,#127541,#127542);
#104236=AXIS2_PLACEMENT_3D('',#433825,#127543,#127544);
#104237=AXIS2_PLACEMENT_3D('',#433852,#127545,#127546);
#104238=AXIS2_PLACEMENT_3D('',#433933,#127547,#127548);
#104239=AXIS2_PLACEMENT_3D('',#433946,#127549,#127550);
#104240=AXIS2_PLACEMENT_3D('',#433947,#127551,#127552);
#104241=AXIS2_PLACEMENT_3D('',#433948,#127553,#127554);
#104242=AXIS2_PLACEMENT_3D('',#433961,#127555,#127556);
#104243=AXIS2_PLACEMENT_3D('',#433974,#127557,#127558);
#104244=AXIS2_PLACEMENT_3D('',#433993,#127559,#127560);
#104245=AXIS2_PLACEMENT_3D('',#434006,#127561,#127562);
#104246=AXIS2_PLACEMENT_3D('',#434019,#127563,#127564);
#104247=AXIS2_PLACEMENT_3D('',#434020,#127565,#127566);
#104248=AXIS2_PLACEMENT_3D('',#434021,#127567,#127568);
#104249=AXIS2_PLACEMENT_3D('',#434034,#127569,#127570);
#104250=AXIS2_PLACEMENT_3D('',#434035,#127571,#127572);
#104251=AXIS2_PLACEMENT_3D('',#434042,#127575,#127576);
#104252=AXIS2_PLACEMENT_3D('',#434049,#127578,#127579);
#104253=AXIS2_PLACEMENT_3D('',#434052,#127580,#127581);
#104254=AXIS2_PLACEMENT_3D('',#434063,#127585,#127586);
#104255=AXIS2_PLACEMENT_3D('',#434131,#127587,#127588);
#104256=AXIS2_PLACEMENT_3D('',#434132,#127589,#127590);
#104257=AXIS2_PLACEMENT_3D('',#434174,#127591,#127592);
#104258=AXIS2_PLACEMENT_3D('',#434201,#127593,#127594);
#104259=AXIS2_PLACEMENT_3D('',#434282,#127595,#127596);
#104260=AXIS2_PLACEMENT_3D('',#434295,#127597,#127598);
#104261=AXIS2_PLACEMENT_3D('',#434296,#127599,#127600);
#104262=AXIS2_PLACEMENT_3D('',#434297,#127601,#127602);
#104263=AXIS2_PLACEMENT_3D('',#434310,#127603,#127604);
#104264=AXIS2_PLACEMENT_3D('',#434323,#127605,#127606);
#104265=AXIS2_PLACEMENT_3D('',#434342,#127607,#127608);
#104266=AXIS2_PLACEMENT_3D('',#434355,#127609,#127610);
#104267=AXIS2_PLACEMENT_3D('',#434368,#127611,#127612);
#104268=AXIS2_PLACEMENT_3D('',#434369,#127613,#127614);
#104269=AXIS2_PLACEMENT_3D('',#434370,#127615,#127616);
#104270=AXIS2_PLACEMENT_3D('',#434383,#127617,#127618);
#104271=AXIS2_PLACEMENT_3D('',#434384,#127619,#127620);
#104272=AXIS2_PLACEMENT_3D('',#434391,#127623,#127624);
#104273=AXIS2_PLACEMENT_3D('',#434398,#127626,#127627);
#104274=AXIS2_PLACEMENT_3D('',#434401,#127628,#127629);
#104275=AXIS2_PLACEMENT_3D('',#434412,#127633,#127634);
#104276=AXIS2_PLACEMENT_3D('',#434480,#127635,#127636);
#104277=AXIS2_PLACEMENT_3D('',#434481,#127637,#127638);
#104278=AXIS2_PLACEMENT_3D('',#434523,#127639,#127640);
#104279=AXIS2_PLACEMENT_3D('',#434550,#127641,#127642);
#104280=AXIS2_PLACEMENT_3D('',#434631,#127643,#127644);
#104281=AXIS2_PLACEMENT_3D('',#434644,#127645,#127646);
#104282=AXIS2_PLACEMENT_3D('',#434645,#127647,#127648);
#104283=AXIS2_PLACEMENT_3D('',#434646,#127649,#127650);
#104284=AXIS2_PLACEMENT_3D('',#434659,#127651,#127652);
#104285=AXIS2_PLACEMENT_3D('',#434672,#127653,#127654);
#104286=AXIS2_PLACEMENT_3D('',#434691,#127655,#127656);
#104287=AXIS2_PLACEMENT_3D('',#434704,#127657,#127658);
#104288=AXIS2_PLACEMENT_3D('',#434717,#127659,#127660);
#104289=AXIS2_PLACEMENT_3D('',#434718,#127661,#127662);
#104290=AXIS2_PLACEMENT_3D('',#434719,#127663,#127664);
#104291=AXIS2_PLACEMENT_3D('',#434732,#127665,#127666);
#104292=AXIS2_PLACEMENT_3D('',#434733,#127667,#127668);
#104293=AXIS2_PLACEMENT_3D('',#434740,#127671,#127672);
#104294=AXIS2_PLACEMENT_3D('',#434747,#127674,#127675);
#104295=AXIS2_PLACEMENT_3D('',#434750,#127676,#127677);
#104296=AXIS2_PLACEMENT_3D('',#434761,#127681,#127682);
#104297=AXIS2_PLACEMENT_3D('',#434829,#127683,#127684);
#104298=AXIS2_PLACEMENT_3D('',#434830,#127685,#127686);
#104299=AXIS2_PLACEMENT_3D('',#434872,#127687,#127688);
#104300=AXIS2_PLACEMENT_3D('',#434899,#127689,#127690);
#104301=AXIS2_PLACEMENT_3D('',#434980,#127691,#127692);
#104302=AXIS2_PLACEMENT_3D('',#434993,#127693,#127694);
#104303=AXIS2_PLACEMENT_3D('',#434994,#127695,#127696);
#104304=AXIS2_PLACEMENT_3D('',#434995,#127697,#127698);
#104305=AXIS2_PLACEMENT_3D('',#435008,#127699,#127700);
#104306=AXIS2_PLACEMENT_3D('',#435021,#127701,#127702);
#104307=AXIS2_PLACEMENT_3D('',#435040,#127703,#127704);
#104308=AXIS2_PLACEMENT_3D('',#435053,#127705,#127706);
#104309=AXIS2_PLACEMENT_3D('',#435066,#127707,#127708);
#104310=AXIS2_PLACEMENT_3D('',#435067,#127709,#127710);
#104311=AXIS2_PLACEMENT_3D('',#435068,#127711,#127712);
#104312=AXIS2_PLACEMENT_3D('',#435081,#127713,#127714);
#104313=AXIS2_PLACEMENT_3D('',#435082,#127715,#127716);
#104314=AXIS2_PLACEMENT_3D('',#435089,#127719,#127720);
#104315=AXIS2_PLACEMENT_3D('',#435096,#127722,#127723);
#104316=AXIS2_PLACEMENT_3D('',#435099,#127724,#127725);
#104317=AXIS2_PLACEMENT_3D('',#435110,#127729,#127730);
#104318=AXIS2_PLACEMENT_3D('',#435178,#127731,#127732);
#104319=AXIS2_PLACEMENT_3D('',#435179,#127733,#127734);
#104320=AXIS2_PLACEMENT_3D('',#435221,#127735,#127736);
#104321=AXIS2_PLACEMENT_3D('',#435248,#127737,#127738);
#104322=AXIS2_PLACEMENT_3D('',#435329,#127739,#127740);
#104323=AXIS2_PLACEMENT_3D('',#435342,#127741,#127742);
#104324=AXIS2_PLACEMENT_3D('',#435343,#127743,#127744);
#104325=AXIS2_PLACEMENT_3D('',#435344,#127745,#127746);
#104326=AXIS2_PLACEMENT_3D('',#435357,#127747,#127748);
#104327=AXIS2_PLACEMENT_3D('',#435370,#127749,#127750);
#104328=AXIS2_PLACEMENT_3D('',#435389,#127751,#127752);
#104329=AXIS2_PLACEMENT_3D('',#435402,#127753,#127754);
#104330=AXIS2_PLACEMENT_3D('',#435415,#127755,#127756);
#104331=AXIS2_PLACEMENT_3D('',#435416,#127757,#127758);
#104332=AXIS2_PLACEMENT_3D('',#435417,#127759,#127760);
#104333=AXIS2_PLACEMENT_3D('',#435430,#127761,#127762);
#104334=AXIS2_PLACEMENT_3D('',#435431,#127763,#127764);
#104335=AXIS2_PLACEMENT_3D('',#435438,#127767,#127768);
#104336=AXIS2_PLACEMENT_3D('',#435445,#127770,#127771);
#104337=AXIS2_PLACEMENT_3D('',#435448,#127772,#127773);
#104338=AXIS2_PLACEMENT_3D('',#435459,#127777,#127778);
#104339=AXIS2_PLACEMENT_3D('',#435527,#127779,#127780);
#104340=AXIS2_PLACEMENT_3D('',#435528,#127781,#127782);
#104341=AXIS2_PLACEMENT_3D('',#435570,#127783,#127784);
#104342=AXIS2_PLACEMENT_3D('',#435597,#127785,#127786);
#104343=AXIS2_PLACEMENT_3D('',#435678,#127787,#127788);
#104344=AXIS2_PLACEMENT_3D('',#435691,#127789,#127790);
#104345=AXIS2_PLACEMENT_3D('',#435692,#127791,#127792);
#104346=AXIS2_PLACEMENT_3D('',#435693,#127793,#127794);
#104347=AXIS2_PLACEMENT_3D('',#435706,#127795,#127796);
#104348=AXIS2_PLACEMENT_3D('',#435719,#127797,#127798);
#104349=AXIS2_PLACEMENT_3D('',#435738,#127799,#127800);
#104350=AXIS2_PLACEMENT_3D('',#435751,#127801,#127802);
#104351=AXIS2_PLACEMENT_3D('',#435764,#127803,#127804);
#104352=AXIS2_PLACEMENT_3D('',#435765,#127805,#127806);
#104353=AXIS2_PLACEMENT_3D('',#435766,#127807,#127808);
#104354=AXIS2_PLACEMENT_3D('',#435779,#127809,#127810);
#104355=AXIS2_PLACEMENT_3D('',#435780,#127811,#127812);
#104356=AXIS2_PLACEMENT_3D('',#435787,#127815,#127816);
#104357=AXIS2_PLACEMENT_3D('',#435794,#127818,#127819);
#104358=AXIS2_PLACEMENT_3D('',#435797,#127820,#127821);
#104359=AXIS2_PLACEMENT_3D('',#435808,#127825,#127826);
#104360=AXIS2_PLACEMENT_3D('',#435876,#127827,#127828);
#104361=AXIS2_PLACEMENT_3D('',#435877,#127829,#127830);
#104362=AXIS2_PLACEMENT_3D('',#435919,#127831,#127832);
#104363=AXIS2_PLACEMENT_3D('',#435946,#127833,#127834);
#104364=AXIS2_PLACEMENT_3D('',#436027,#127835,#127836);
#104365=AXIS2_PLACEMENT_3D('',#436040,#127837,#127838);
#104366=AXIS2_PLACEMENT_3D('',#436041,#127839,#127840);
#104367=AXIS2_PLACEMENT_3D('',#436042,#127841,#127842);
#104368=AXIS2_PLACEMENT_3D('',#436055,#127843,#127844);
#104369=AXIS2_PLACEMENT_3D('',#436068,#127845,#127846);
#104370=AXIS2_PLACEMENT_3D('',#436087,#127847,#127848);
#104371=AXIS2_PLACEMENT_3D('',#436100,#127849,#127850);
#104372=AXIS2_PLACEMENT_3D('',#436113,#127851,#127852);
#104373=AXIS2_PLACEMENT_3D('',#436114,#127853,#127854);
#104374=AXIS2_PLACEMENT_3D('',#436115,#127855,#127856);
#104375=AXIS2_PLACEMENT_3D('',#436128,#127857,#127858);
#104376=AXIS2_PLACEMENT_3D('',#436129,#127859,#127860);
#104377=AXIS2_PLACEMENT_3D('',#436136,#127863,#127864);
#104378=AXIS2_PLACEMENT_3D('',#436143,#127866,#127867);
#104379=AXIS2_PLACEMENT_3D('',#436146,#127868,#127869);
#104380=AXIS2_PLACEMENT_3D('',#436157,#127873,#127874);
#104381=AXIS2_PLACEMENT_3D('',#436225,#127875,#127876);
#104382=AXIS2_PLACEMENT_3D('',#436226,#127877,#127878);
#104383=AXIS2_PLACEMENT_3D('',#436268,#127879,#127880);
#104384=AXIS2_PLACEMENT_3D('',#436295,#127881,#127882);
#104385=AXIS2_PLACEMENT_3D('',#436376,#127883,#127884);
#104386=AXIS2_PLACEMENT_3D('',#436389,#127885,#127886);
#104387=AXIS2_PLACEMENT_3D('',#436390,#127887,#127888);
#104388=AXIS2_PLACEMENT_3D('',#436391,#127889,#127890);
#104389=AXIS2_PLACEMENT_3D('',#436404,#127891,#127892);
#104390=AXIS2_PLACEMENT_3D('',#436417,#127893,#127894);
#104391=AXIS2_PLACEMENT_3D('',#436436,#127895,#127896);
#104392=AXIS2_PLACEMENT_3D('',#436449,#127897,#127898);
#104393=AXIS2_PLACEMENT_3D('',#436462,#127899,#127900);
#104394=AXIS2_PLACEMENT_3D('',#436463,#127901,#127902);
#104395=AXIS2_PLACEMENT_3D('',#436464,#127903,#127904);
#104396=AXIS2_PLACEMENT_3D('',#436477,#127905,#127906);
#104397=AXIS2_PLACEMENT_3D('',#436478,#127907,#127908);
#104398=AXIS2_PLACEMENT_3D('',#436485,#127911,#127912);
#104399=AXIS2_PLACEMENT_3D('',#436492,#127914,#127915);
#104400=AXIS2_PLACEMENT_3D('',#436495,#127916,#127917);
#104401=AXIS2_PLACEMENT_3D('',#436506,#127921,#127922);
#104402=AXIS2_PLACEMENT_3D('',#436574,#127923,#127924);
#104403=AXIS2_PLACEMENT_3D('',#436575,#127925,#127926);
#104404=AXIS2_PLACEMENT_3D('',#436617,#127927,#127928);
#104405=AXIS2_PLACEMENT_3D('',#436644,#127929,#127930);
#104406=AXIS2_PLACEMENT_3D('',#436725,#127931,#127932);
#104407=AXIS2_PLACEMENT_3D('',#436738,#127933,#127934);
#104408=AXIS2_PLACEMENT_3D('',#436739,#127935,#127936);
#104409=AXIS2_PLACEMENT_3D('',#436740,#127937,#127938);
#104410=AXIS2_PLACEMENT_3D('',#436753,#127939,#127940);
#104411=AXIS2_PLACEMENT_3D('',#436766,#127941,#127942);
#104412=AXIS2_PLACEMENT_3D('',#436785,#127943,#127944);
#104413=AXIS2_PLACEMENT_3D('',#436798,#127945,#127946);
#104414=AXIS2_PLACEMENT_3D('',#436811,#127947,#127948);
#104415=AXIS2_PLACEMENT_3D('',#436812,#127949,#127950);
#104416=AXIS2_PLACEMENT_3D('',#436813,#127951,#127952);
#104417=AXIS2_PLACEMENT_3D('',#436826,#127953,#127954);
#104418=AXIS2_PLACEMENT_3D('',#436827,#127955,#127956);
#104419=AXIS2_PLACEMENT_3D('',#436834,#127959,#127960);
#104420=AXIS2_PLACEMENT_3D('',#436841,#127962,#127963);
#104421=AXIS2_PLACEMENT_3D('',#436844,#127964,#127965);
#104422=AXIS2_PLACEMENT_3D('',#436855,#127969,#127970);
#104423=AXIS2_PLACEMENT_3D('',#436923,#127971,#127972);
#104424=AXIS2_PLACEMENT_3D('',#436924,#127973,#127974);
#104425=AXIS2_PLACEMENT_3D('',#436966,#127975,#127976);
#104426=AXIS2_PLACEMENT_3D('',#436993,#127977,#127978);
#104427=AXIS2_PLACEMENT_3D('',#437074,#127979,#127980);
#104428=AXIS2_PLACEMENT_3D('',#437087,#127981,#127982);
#104429=AXIS2_PLACEMENT_3D('',#437088,#127983,#127984);
#104430=AXIS2_PLACEMENT_3D('',#437089,#127985,#127986);
#104431=AXIS2_PLACEMENT_3D('',#437102,#127987,#127988);
#104432=AXIS2_PLACEMENT_3D('',#437115,#127989,#127990);
#104433=AXIS2_PLACEMENT_3D('',#437134,#127991,#127992);
#104434=AXIS2_PLACEMENT_3D('',#437147,#127993,#127994);
#104435=AXIS2_PLACEMENT_3D('',#437160,#127995,#127996);
#104436=AXIS2_PLACEMENT_3D('',#437161,#127997,#127998);
#104437=AXIS2_PLACEMENT_3D('',#437162,#127999,#128000);
#104438=AXIS2_PLACEMENT_3D('',#437175,#128001,#128002);
#104439=AXIS2_PLACEMENT_3D('',#437176,#128003,#128004);
#104440=AXIS2_PLACEMENT_3D('',#437183,#128007,#128008);
#104441=AXIS2_PLACEMENT_3D('',#437190,#128010,#128011);
#104442=AXIS2_PLACEMENT_3D('',#437193,#128012,#128013);
#104443=AXIS2_PLACEMENT_3D('',#437204,#128017,#128018);
#104444=AXIS2_PLACEMENT_3D('',#437272,#128019,#128020);
#104445=AXIS2_PLACEMENT_3D('',#437273,#128021,#128022);
#104446=AXIS2_PLACEMENT_3D('',#437315,#128023,#128024);
#104447=AXIS2_PLACEMENT_3D('',#437342,#128025,#128026);
#104448=AXIS2_PLACEMENT_3D('',#437423,#128027,#128028);
#104449=AXIS2_PLACEMENT_3D('',#437436,#128029,#128030);
#104450=AXIS2_PLACEMENT_3D('',#437437,#128031,#128032);
#104451=AXIS2_PLACEMENT_3D('',#437438,#128033,#128034);
#104452=AXIS2_PLACEMENT_3D('',#437451,#128035,#128036);
#104453=AXIS2_PLACEMENT_3D('',#437464,#128037,#128038);
#104454=AXIS2_PLACEMENT_3D('',#437483,#128039,#128040);
#104455=AXIS2_PLACEMENT_3D('',#437496,#128041,#128042);
#104456=AXIS2_PLACEMENT_3D('',#437509,#128043,#128044);
#104457=AXIS2_PLACEMENT_3D('',#437510,#128045,#128046);
#104458=AXIS2_PLACEMENT_3D('',#437511,#128047,#128048);
#104459=AXIS2_PLACEMENT_3D('',#437524,#128049,#128050);
#104460=AXIS2_PLACEMENT_3D('',#437525,#128051,#128052);
#104461=AXIS2_PLACEMENT_3D('',#437532,#128055,#128056);
#104462=AXIS2_PLACEMENT_3D('',#437539,#128058,#128059);
#104463=AXIS2_PLACEMENT_3D('',#437542,#128060,#128061);
#104464=AXIS2_PLACEMENT_3D('',#437553,#128065,#128066);
#104465=AXIS2_PLACEMENT_3D('',#437621,#128067,#128068);
#104466=AXIS2_PLACEMENT_3D('',#437622,#128069,#128070);
#104467=AXIS2_PLACEMENT_3D('',#437664,#128071,#128072);
#104468=AXIS2_PLACEMENT_3D('',#437691,#128073,#128074);
#104469=AXIS2_PLACEMENT_3D('',#437772,#128075,#128076);
#104470=AXIS2_PLACEMENT_3D('',#437785,#128077,#128078);
#104471=AXIS2_PLACEMENT_3D('',#437786,#128079,#128080);
#104472=AXIS2_PLACEMENT_3D('',#437787,#128081,#128082);
#104473=AXIS2_PLACEMENT_3D('',#437800,#128083,#128084);
#104474=AXIS2_PLACEMENT_3D('',#437813,#128085,#128086);
#104475=AXIS2_PLACEMENT_3D('',#437832,#128087,#128088);
#104476=AXIS2_PLACEMENT_3D('',#437845,#128089,#128090);
#104477=AXIS2_PLACEMENT_3D('',#437858,#128091,#128092);
#104478=AXIS2_PLACEMENT_3D('',#437859,#128093,#128094);
#104479=AXIS2_PLACEMENT_3D('',#437860,#128095,#128096);
#104480=AXIS2_PLACEMENT_3D('',#437873,#128097,#128098);
#104481=AXIS2_PLACEMENT_3D('',#437874,#128099,#128100);
#104482=AXIS2_PLACEMENT_3D('',#437881,#128103,#128104);
#104483=AXIS2_PLACEMENT_3D('',#437888,#128106,#128107);
#104484=AXIS2_PLACEMENT_3D('',#437891,#128108,#128109);
#104485=AXIS2_PLACEMENT_3D('',#437902,#128113,#128114);
#104486=AXIS2_PLACEMENT_3D('',#437970,#128115,#128116);
#104487=AXIS2_PLACEMENT_3D('',#437971,#128117,#128118);
#104488=AXIS2_PLACEMENT_3D('',#438013,#128119,#128120);
#104489=AXIS2_PLACEMENT_3D('',#438040,#128121,#128122);
#104490=AXIS2_PLACEMENT_3D('',#438121,#128123,#128124);
#104491=AXIS2_PLACEMENT_3D('',#438134,#128125,#128126);
#104492=AXIS2_PLACEMENT_3D('',#438135,#128127,#128128);
#104493=AXIS2_PLACEMENT_3D('',#438136,#128129,#128130);
#104494=AXIS2_PLACEMENT_3D('',#438149,#128131,#128132);
#104495=AXIS2_PLACEMENT_3D('',#438162,#128133,#128134);
#104496=AXIS2_PLACEMENT_3D('',#438181,#128135,#128136);
#104497=AXIS2_PLACEMENT_3D('',#438194,#128137,#128138);
#104498=AXIS2_PLACEMENT_3D('',#438207,#128139,#128140);
#104499=AXIS2_PLACEMENT_3D('',#438208,#128141,#128142);
#104500=AXIS2_PLACEMENT_3D('',#438209,#128143,#128144);
#104501=AXIS2_PLACEMENT_3D('',#438222,#128145,#128146);
#104502=AXIS2_PLACEMENT_3D('',#438223,#128147,#128148);
#104503=AXIS2_PLACEMENT_3D('',#438230,#128151,#128152);
#104504=AXIS2_PLACEMENT_3D('',#438237,#128154,#128155);
#104505=AXIS2_PLACEMENT_3D('',#438240,#128156,#128157);
#104506=AXIS2_PLACEMENT_3D('',#438251,#128161,#128162);
#104507=AXIS2_PLACEMENT_3D('',#438319,#128163,#128164);
#104508=AXIS2_PLACEMENT_3D('',#438320,#128165,#128166);
#104509=AXIS2_PLACEMENT_3D('',#438362,#128167,#128168);
#104510=AXIS2_PLACEMENT_3D('',#438389,#128169,#128170);
#104511=AXIS2_PLACEMENT_3D('',#438470,#128171,#128172);
#104512=AXIS2_PLACEMENT_3D('',#438483,#128173,#128174);
#104513=AXIS2_PLACEMENT_3D('',#438484,#128175,#128176);
#104514=AXIS2_PLACEMENT_3D('',#438485,#128177,#128178);
#104515=AXIS2_PLACEMENT_3D('',#438498,#128179,#128180);
#104516=AXIS2_PLACEMENT_3D('',#438511,#128181,#128182);
#104517=AXIS2_PLACEMENT_3D('',#438530,#128183,#128184);
#104518=AXIS2_PLACEMENT_3D('',#438543,#128185,#128186);
#104519=AXIS2_PLACEMENT_3D('',#438556,#128187,#128188);
#104520=AXIS2_PLACEMENT_3D('',#438557,#128189,#128190);
#104521=AXIS2_PLACEMENT_3D('',#438558,#128191,#128192);
#104522=AXIS2_PLACEMENT_3D('',#438571,#128193,#128194);
#104523=AXIS2_PLACEMENT_3D('',#438572,#128195,#128196);
#104524=AXIS2_PLACEMENT_3D('',#438579,#128199,#128200);
#104525=AXIS2_PLACEMENT_3D('',#438586,#128202,#128203);
#104526=AXIS2_PLACEMENT_3D('',#438589,#128204,#128205);
#104527=AXIS2_PLACEMENT_3D('',#438600,#128209,#128210);
#104528=AXIS2_PLACEMENT_3D('',#438668,#128211,#128212);
#104529=AXIS2_PLACEMENT_3D('',#438669,#128213,#128214);
#104530=AXIS2_PLACEMENT_3D('',#438711,#128215,#128216);
#104531=AXIS2_PLACEMENT_3D('',#438738,#128217,#128218);
#104532=AXIS2_PLACEMENT_3D('',#438819,#128219,#128220);
#104533=AXIS2_PLACEMENT_3D('',#438832,#128221,#128222);
#104534=AXIS2_PLACEMENT_3D('',#438833,#128223,#128224);
#104535=AXIS2_PLACEMENT_3D('',#438834,#128225,#128226);
#104536=AXIS2_PLACEMENT_3D('',#438847,#128227,#128228);
#104537=AXIS2_PLACEMENT_3D('',#438860,#128229,#128230);
#104538=AXIS2_PLACEMENT_3D('',#438879,#128231,#128232);
#104539=AXIS2_PLACEMENT_3D('',#438892,#128233,#128234);
#104540=AXIS2_PLACEMENT_3D('',#438905,#128235,#128236);
#104541=AXIS2_PLACEMENT_3D('',#438906,#128237,#128238);
#104542=AXIS2_PLACEMENT_3D('',#438907,#128239,#128240);
#104543=AXIS2_PLACEMENT_3D('',#438920,#128241,#128242);
#104544=AXIS2_PLACEMENT_3D('',#438921,#128243,#128244);
#104545=AXIS2_PLACEMENT_3D('',#438928,#128247,#128248);
#104546=AXIS2_PLACEMENT_3D('',#438935,#128250,#128251);
#104547=AXIS2_PLACEMENT_3D('',#438938,#128252,#128253);
#104548=AXIS2_PLACEMENT_3D('',#438949,#128257,#128258);
#104549=AXIS2_PLACEMENT_3D('',#439017,#128259,#128260);
#104550=AXIS2_PLACEMENT_3D('',#439018,#128261,#128262);
#104551=AXIS2_PLACEMENT_3D('',#439060,#128263,#128264);
#104552=AXIS2_PLACEMENT_3D('',#439087,#128265,#128266);
#104553=AXIS2_PLACEMENT_3D('',#439168,#128267,#128268);
#104554=AXIS2_PLACEMENT_3D('',#439181,#128269,#128270);
#104555=AXIS2_PLACEMENT_3D('',#439182,#128271,#128272);
#104556=AXIS2_PLACEMENT_3D('',#439183,#128273,#128274);
#104557=AXIS2_PLACEMENT_3D('',#439196,#128275,#128276);
#104558=AXIS2_PLACEMENT_3D('',#439209,#128277,#128278);
#104559=AXIS2_PLACEMENT_3D('',#439228,#128279,#128280);
#104560=AXIS2_PLACEMENT_3D('',#439241,#128281,#128282);
#104561=AXIS2_PLACEMENT_3D('',#439254,#128283,#128284);
#104562=AXIS2_PLACEMENT_3D('',#439255,#128285,#128286);
#104563=AXIS2_PLACEMENT_3D('',#439256,#128287,#128288);
#104564=AXIS2_PLACEMENT_3D('',#439269,#128289,#128290);
#104565=AXIS2_PLACEMENT_3D('',#439270,#128291,#128292);
#104566=AXIS2_PLACEMENT_3D('',#439277,#128295,#128296);
#104567=AXIS2_PLACEMENT_3D('',#439284,#128298,#128299);
#104568=AXIS2_PLACEMENT_3D('',#439287,#128300,#128301);
#104569=AXIS2_PLACEMENT_3D('',#439298,#128305,#128306);
#104570=AXIS2_PLACEMENT_3D('',#439366,#128307,#128308);
#104571=AXIS2_PLACEMENT_3D('',#439367,#128309,#128310);
#104572=AXIS2_PLACEMENT_3D('',#439409,#128311,#128312);
#104573=AXIS2_PLACEMENT_3D('',#439436,#128313,#128314);
#104574=AXIS2_PLACEMENT_3D('',#439517,#128315,#128316);
#104575=AXIS2_PLACEMENT_3D('',#439530,#128317,#128318);
#104576=AXIS2_PLACEMENT_3D('',#439531,#128319,#128320);
#104577=AXIS2_PLACEMENT_3D('',#439532,#128321,#128322);
#104578=AXIS2_PLACEMENT_3D('',#439545,#128323,#128324);
#104579=AXIS2_PLACEMENT_3D('',#439558,#128325,#128326);
#104580=AXIS2_PLACEMENT_3D('',#439577,#128327,#128328);
#104581=AXIS2_PLACEMENT_3D('',#439590,#128329,#128330);
#104582=AXIS2_PLACEMENT_3D('',#439603,#128331,#128332);
#104583=AXIS2_PLACEMENT_3D('',#439604,#128333,#128334);
#104584=AXIS2_PLACEMENT_3D('',#439605,#128335,#128336);
#104585=AXIS2_PLACEMENT_3D('',#439618,#128337,#128338);
#104586=AXIS2_PLACEMENT_3D('',#439619,#128339,#128340);
#104587=AXIS2_PLACEMENT_3D('',#439626,#128343,#128344);
#104588=AXIS2_PLACEMENT_3D('',#439633,#128346,#128347);
#104589=AXIS2_PLACEMENT_3D('',#439636,#128348,#128349);
#104590=AXIS2_PLACEMENT_3D('',#439647,#128353,#128354);
#104591=AXIS2_PLACEMENT_3D('',#439715,#128355,#128356);
#104592=AXIS2_PLACEMENT_3D('',#439716,#128357,#128358);
#104593=AXIS2_PLACEMENT_3D('',#439758,#128359,#128360);
#104594=AXIS2_PLACEMENT_3D('',#439785,#128361,#128362);
#104595=AXIS2_PLACEMENT_3D('',#439866,#128363,#128364);
#104596=AXIS2_PLACEMENT_3D('',#439879,#128365,#128366);
#104597=AXIS2_PLACEMENT_3D('',#439880,#128367,#128368);
#104598=AXIS2_PLACEMENT_3D('',#439881,#128369,#128370);
#104599=AXIS2_PLACEMENT_3D('',#439894,#128371,#128372);
#104600=AXIS2_PLACEMENT_3D('',#439907,#128373,#128374);
#104601=AXIS2_PLACEMENT_3D('',#439926,#128375,#128376);
#104602=AXIS2_PLACEMENT_3D('',#439939,#128377,#128378);
#104603=AXIS2_PLACEMENT_3D('',#439952,#128379,#128380);
#104604=AXIS2_PLACEMENT_3D('',#439953,#128381,#128382);
#104605=AXIS2_PLACEMENT_3D('',#439954,#128383,#128384);
#104606=AXIS2_PLACEMENT_3D('',#439967,#128385,#128386);
#104607=AXIS2_PLACEMENT_3D('',#439968,#128387,#128388);
#104608=AXIS2_PLACEMENT_3D('',#439975,#128391,#128392);
#104609=AXIS2_PLACEMENT_3D('',#439982,#128394,#128395);
#104610=AXIS2_PLACEMENT_3D('',#439985,#128396,#128397);
#104611=AXIS2_PLACEMENT_3D('',#439996,#128401,#128402);
#104612=AXIS2_PLACEMENT_3D('',#440064,#128403,#128404);
#104613=AXIS2_PLACEMENT_3D('',#440065,#128405,#128406);
#104614=AXIS2_PLACEMENT_3D('',#440107,#128407,#128408);
#104615=AXIS2_PLACEMENT_3D('',#440134,#128409,#128410);
#104616=AXIS2_PLACEMENT_3D('',#440215,#128411,#128412);
#104617=AXIS2_PLACEMENT_3D('',#440228,#128413,#128414);
#104618=AXIS2_PLACEMENT_3D('',#440229,#128415,#128416);
#104619=AXIS2_PLACEMENT_3D('',#440230,#128417,#128418);
#104620=AXIS2_PLACEMENT_3D('',#440243,#128419,#128420);
#104621=AXIS2_PLACEMENT_3D('',#440256,#128421,#128422);
#104622=AXIS2_PLACEMENT_3D('',#440275,#128423,#128424);
#104623=AXIS2_PLACEMENT_3D('',#440288,#128425,#128426);
#104624=AXIS2_PLACEMENT_3D('',#440301,#128427,#128428);
#104625=AXIS2_PLACEMENT_3D('',#440302,#128429,#128430);
#104626=AXIS2_PLACEMENT_3D('',#440303,#128431,#128432);
#104627=AXIS2_PLACEMENT_3D('',#440316,#128433,#128434);
#104628=AXIS2_PLACEMENT_3D('',#440317,#128435,#128436);
#104629=AXIS2_PLACEMENT_3D('',#440324,#128439,#128440);
#104630=AXIS2_PLACEMENT_3D('',#440331,#128442,#128443);
#104631=AXIS2_PLACEMENT_3D('',#440334,#128444,#128445);
#104632=AXIS2_PLACEMENT_3D('',#440345,#128449,#128450);
#104633=AXIS2_PLACEMENT_3D('',#440413,#128451,#128452);
#104634=AXIS2_PLACEMENT_3D('',#440414,#128453,#128454);
#104635=AXIS2_PLACEMENT_3D('',#440456,#128455,#128456);
#104636=AXIS2_PLACEMENT_3D('',#440483,#128457,#128458);
#104637=AXIS2_PLACEMENT_3D('',#440564,#128459,#128460);
#104638=AXIS2_PLACEMENT_3D('',#440577,#128461,#128462);
#104639=AXIS2_PLACEMENT_3D('',#440578,#128463,#128464);
#104640=AXIS2_PLACEMENT_3D('',#440579,#128465,#128466);
#104641=AXIS2_PLACEMENT_3D('',#440592,#128467,#128468);
#104642=AXIS2_PLACEMENT_3D('',#440605,#128469,#128470);
#104643=AXIS2_PLACEMENT_3D('',#440624,#128471,#128472);
#104644=AXIS2_PLACEMENT_3D('',#440637,#128473,#128474);
#104645=AXIS2_PLACEMENT_3D('',#440650,#128475,#128476);
#104646=AXIS2_PLACEMENT_3D('',#440651,#128477,#128478);
#104647=AXIS2_PLACEMENT_3D('',#440652,#128479,#128480);
#104648=AXIS2_PLACEMENT_3D('',#440665,#128481,#128482);
#104649=AXIS2_PLACEMENT_3D('',#440666,#128483,#128484);
#104650=AXIS2_PLACEMENT_3D('',#440673,#128487,#128488);
#104651=AXIS2_PLACEMENT_3D('',#440680,#128490,#128491);
#104652=AXIS2_PLACEMENT_3D('',#440683,#128492,#128493);
#104653=AXIS2_PLACEMENT_3D('',#440694,#128497,#128498);
#104654=AXIS2_PLACEMENT_3D('',#440762,#128499,#128500);
#104655=AXIS2_PLACEMENT_3D('',#440763,#128501,#128502);
#104656=AXIS2_PLACEMENT_3D('',#440805,#128503,#128504);
#104657=AXIS2_PLACEMENT_3D('',#440832,#128505,#128506);
#104658=AXIS2_PLACEMENT_3D('',#440913,#128507,#128508);
#104659=AXIS2_PLACEMENT_3D('',#440926,#128509,#128510);
#104660=AXIS2_PLACEMENT_3D('',#440927,#128511,#128512);
#104661=AXIS2_PLACEMENT_3D('',#440928,#128513,#128514);
#104662=AXIS2_PLACEMENT_3D('',#440941,#128515,#128516);
#104663=AXIS2_PLACEMENT_3D('',#440954,#128517,#128518);
#104664=AXIS2_PLACEMENT_3D('',#440973,#128519,#128520);
#104665=AXIS2_PLACEMENT_3D('',#440986,#128521,#128522);
#104666=AXIS2_PLACEMENT_3D('',#440999,#128523,#128524);
#104667=AXIS2_PLACEMENT_3D('',#441000,#128525,#128526);
#104668=AXIS2_PLACEMENT_3D('',#441001,#128527,#128528);
#104669=AXIS2_PLACEMENT_3D('',#441014,#128529,#128530);
#104670=AXIS2_PLACEMENT_3D('',#441015,#128531,#128532);
#104671=AXIS2_PLACEMENT_3D('',#441022,#128535,#128536);
#104672=AXIS2_PLACEMENT_3D('',#441029,#128538,#128539);
#104673=AXIS2_PLACEMENT_3D('',#441032,#128540,#128541);
#104674=AXIS2_PLACEMENT_3D('',#441043,#128545,#128546);
#104675=AXIS2_PLACEMENT_3D('',#441111,#128547,#128548);
#104676=AXIS2_PLACEMENT_3D('',#441112,#128549,#128550);
#104677=AXIS2_PLACEMENT_3D('',#441154,#128551,#128552);
#104678=AXIS2_PLACEMENT_3D('',#441181,#128553,#128554);
#104679=AXIS2_PLACEMENT_3D('',#441262,#128555,#128556);
#104680=AXIS2_PLACEMENT_3D('',#441275,#128557,#128558);
#104681=AXIS2_PLACEMENT_3D('',#441276,#128559,#128560);
#104682=AXIS2_PLACEMENT_3D('',#441277,#128561,#128562);
#104683=AXIS2_PLACEMENT_3D('',#441290,#128563,#128564);
#104684=AXIS2_PLACEMENT_3D('',#441303,#128565,#128566);
#104685=AXIS2_PLACEMENT_3D('',#441322,#128567,#128568);
#104686=AXIS2_PLACEMENT_3D('',#441335,#128569,#128570);
#104687=AXIS2_PLACEMENT_3D('',#441348,#128571,#128572);
#104688=AXIS2_PLACEMENT_3D('',#441349,#128573,#128574);
#104689=AXIS2_PLACEMENT_3D('',#441350,#128575,#128576);
#104690=AXIS2_PLACEMENT_3D('',#441363,#128577,#128578);
#104691=AXIS2_PLACEMENT_3D('',#441364,#128579,#128580);
#104692=AXIS2_PLACEMENT_3D('',#441371,#128583,#128584);
#104693=AXIS2_PLACEMENT_3D('',#441378,#128586,#128587);
#104694=AXIS2_PLACEMENT_3D('',#441381,#128588,#128589);
#104695=AXIS2_PLACEMENT_3D('',#441392,#128593,#128594);
#104696=AXIS2_PLACEMENT_3D('',#441460,#128595,#128596);
#104697=AXIS2_PLACEMENT_3D('',#441461,#128597,#128598);
#104698=AXIS2_PLACEMENT_3D('',#441503,#128599,#128600);
#104699=AXIS2_PLACEMENT_3D('',#441530,#128601,#128602);
#104700=AXIS2_PLACEMENT_3D('',#441611,#128603,#128604);
#104701=AXIS2_PLACEMENT_3D('',#441624,#128605,#128606);
#104702=AXIS2_PLACEMENT_3D('',#441625,#128607,#128608);
#104703=AXIS2_PLACEMENT_3D('',#441626,#128609,#128610);
#104704=AXIS2_PLACEMENT_3D('',#441639,#128611,#128612);
#104705=AXIS2_PLACEMENT_3D('',#441652,#128613,#128614);
#104706=AXIS2_PLACEMENT_3D('',#441671,#128615,#128616);
#104707=AXIS2_PLACEMENT_3D('',#441684,#128617,#128618);
#104708=AXIS2_PLACEMENT_3D('',#441697,#128619,#128620);
#104709=AXIS2_PLACEMENT_3D('',#441698,#128621,#128622);
#104710=AXIS2_PLACEMENT_3D('',#441699,#128623,#128624);
#104711=AXIS2_PLACEMENT_3D('',#441712,#128625,#128626);
#104712=AXIS2_PLACEMENT_3D('',#441713,#128627,#128628);
#104713=AXIS2_PLACEMENT_3D('',#441720,#128631,#128632);
#104714=AXIS2_PLACEMENT_3D('',#441727,#128634,#128635);
#104715=AXIS2_PLACEMENT_3D('',#441730,#128636,#128637);
#104716=AXIS2_PLACEMENT_3D('',#441741,#128641,#128642);
#104717=AXIS2_PLACEMENT_3D('',#441809,#128643,#128644);
#104718=AXIS2_PLACEMENT_3D('',#441810,#128645,#128646);
#104719=AXIS2_PLACEMENT_3D('',#441852,#128647,#128648);
#104720=AXIS2_PLACEMENT_3D('',#441879,#128649,#128650);
#104721=AXIS2_PLACEMENT_3D('',#441960,#128651,#128652);
#104722=AXIS2_PLACEMENT_3D('',#441973,#128653,#128654);
#104723=AXIS2_PLACEMENT_3D('',#441974,#128655,#128656);
#104724=AXIS2_PLACEMENT_3D('',#441975,#128657,#128658);
#104725=AXIS2_PLACEMENT_3D('',#441988,#128659,#128660);
#104726=AXIS2_PLACEMENT_3D('',#442001,#128661,#128662);
#104727=AXIS2_PLACEMENT_3D('',#442020,#128663,#128664);
#104728=AXIS2_PLACEMENT_3D('',#442033,#128665,#128666);
#104729=AXIS2_PLACEMENT_3D('',#442046,#128667,#128668);
#104730=AXIS2_PLACEMENT_3D('',#442047,#128669,#128670);
#104731=AXIS2_PLACEMENT_3D('',#442048,#128671,#128672);
#104732=AXIS2_PLACEMENT_3D('',#442061,#128673,#128674);
#104733=AXIS2_PLACEMENT_3D('',#442062,#128675,#128676);
#104734=AXIS2_PLACEMENT_3D('',#442069,#128679,#128680);
#104735=AXIS2_PLACEMENT_3D('',#442076,#128682,#128683);
#104736=AXIS2_PLACEMENT_3D('',#442079,#128684,#128685);
#104737=AXIS2_PLACEMENT_3D('',#442090,#128689,#128690);
#104738=AXIS2_PLACEMENT_3D('',#442158,#128691,#128692);
#104739=AXIS2_PLACEMENT_3D('',#442159,#128693,#128694);
#104740=AXIS2_PLACEMENT_3D('',#442201,#128695,#128696);
#104741=AXIS2_PLACEMENT_3D('',#442228,#128697,#128698);
#104742=AXIS2_PLACEMENT_3D('',#442309,#128699,#128700);
#104743=AXIS2_PLACEMENT_3D('',#442322,#128701,#128702);
#104744=AXIS2_PLACEMENT_3D('',#442323,#128703,#128704);
#104745=AXIS2_PLACEMENT_3D('',#442324,#128705,#128706);
#104746=AXIS2_PLACEMENT_3D('',#442337,#128707,#128708);
#104747=AXIS2_PLACEMENT_3D('',#442350,#128709,#128710);
#104748=AXIS2_PLACEMENT_3D('',#442369,#128711,#128712);
#104749=AXIS2_PLACEMENT_3D('',#442382,#128713,#128714);
#104750=AXIS2_PLACEMENT_3D('',#442395,#128715,#128716);
#104751=AXIS2_PLACEMENT_3D('',#442396,#128717,#128718);
#104752=AXIS2_PLACEMENT_3D('',#442397,#128719,#128720);
#104753=AXIS2_PLACEMENT_3D('',#442410,#128721,#128722);
#104754=AXIS2_PLACEMENT_3D('',#442411,#128723,#128724);
#104755=AXIS2_PLACEMENT_3D('',#442418,#128727,#128728);
#104756=AXIS2_PLACEMENT_3D('',#442425,#128730,#128731);
#104757=AXIS2_PLACEMENT_3D('',#442428,#128732,#128733);
#104758=AXIS2_PLACEMENT_3D('',#442439,#128737,#128738);
#104759=AXIS2_PLACEMENT_3D('',#442507,#128739,#128740);
#104760=AXIS2_PLACEMENT_3D('',#442508,#128741,#128742);
#104761=AXIS2_PLACEMENT_3D('',#442550,#128743,#128744);
#104762=AXIS2_PLACEMENT_3D('',#442577,#128745,#128746);
#104763=AXIS2_PLACEMENT_3D('',#442658,#128747,#128748);
#104764=AXIS2_PLACEMENT_3D('',#442671,#128749,#128750);
#104765=AXIS2_PLACEMENT_3D('',#442672,#128751,#128752);
#104766=AXIS2_PLACEMENT_3D('',#442673,#128753,#128754);
#104767=AXIS2_PLACEMENT_3D('',#442686,#128755,#128756);
#104768=AXIS2_PLACEMENT_3D('',#442699,#128757,#128758);
#104769=AXIS2_PLACEMENT_3D('',#442718,#128759,#128760);
#104770=AXIS2_PLACEMENT_3D('',#442731,#128761,#128762);
#104771=AXIS2_PLACEMENT_3D('',#442744,#128763,#128764);
#104772=AXIS2_PLACEMENT_3D('',#442745,#128765,#128766);
#104773=AXIS2_PLACEMENT_3D('',#442746,#128767,#128768);
#104774=AXIS2_PLACEMENT_3D('',#442759,#128769,#128770);
#104775=AXIS2_PLACEMENT_3D('',#442760,#128771,#128772);
#104776=AXIS2_PLACEMENT_3D('',#442767,#128775,#128776);
#104777=AXIS2_PLACEMENT_3D('',#442774,#128778,#128779);
#104778=AXIS2_PLACEMENT_3D('',#442777,#128780,#128781);
#104779=AXIS2_PLACEMENT_3D('',#442788,#128785,#128786);
#104780=AXIS2_PLACEMENT_3D('',#442856,#128787,#128788);
#104781=AXIS2_PLACEMENT_3D('',#442857,#128789,#128790);
#104782=AXIS2_PLACEMENT_3D('',#442899,#128791,#128792);
#104783=AXIS2_PLACEMENT_3D('',#442926,#128793,#128794);
#104784=AXIS2_PLACEMENT_3D('',#443007,#128795,#128796);
#104785=AXIS2_PLACEMENT_3D('',#443020,#128797,#128798);
#104786=AXIS2_PLACEMENT_3D('',#443021,#128799,#128800);
#104787=AXIS2_PLACEMENT_3D('',#443022,#128801,#128802);
#104788=AXIS2_PLACEMENT_3D('',#443035,#128803,#128804);
#104789=AXIS2_PLACEMENT_3D('',#443048,#128805,#128806);
#104790=AXIS2_PLACEMENT_3D('',#443067,#128807,#128808);
#104791=AXIS2_PLACEMENT_3D('',#443080,#128809,#128810);
#104792=AXIS2_PLACEMENT_3D('',#443093,#128811,#128812);
#104793=AXIS2_PLACEMENT_3D('',#443094,#128813,#128814);
#104794=AXIS2_PLACEMENT_3D('',#443095,#128815,#128816);
#104795=AXIS2_PLACEMENT_3D('',#443108,#128817,#128818);
#104796=AXIS2_PLACEMENT_3D('',#443109,#128819,#128820);
#104797=AXIS2_PLACEMENT_3D('',#443116,#128823,#128824);
#104798=AXIS2_PLACEMENT_3D('',#443123,#128826,#128827);
#104799=AXIS2_PLACEMENT_3D('',#443126,#128828,#128829);
#104800=AXIS2_PLACEMENT_3D('',#443137,#128833,#128834);
#104801=AXIS2_PLACEMENT_3D('',#443205,#128835,#128836);
#104802=AXIS2_PLACEMENT_3D('',#443206,#128837,#128838);
#104803=AXIS2_PLACEMENT_3D('',#443248,#128839,#128840);
#104804=AXIS2_PLACEMENT_3D('',#443275,#128841,#128842);
#104805=AXIS2_PLACEMENT_3D('',#443356,#128843,#128844);
#104806=AXIS2_PLACEMENT_3D('',#443369,#128845,#128846);
#104807=AXIS2_PLACEMENT_3D('',#443370,#128847,#128848);
#104808=AXIS2_PLACEMENT_3D('',#443371,#128849,#128850);
#104809=AXIS2_PLACEMENT_3D('',#443384,#128851,#128852);
#104810=AXIS2_PLACEMENT_3D('',#443397,#128853,#128854);
#104811=AXIS2_PLACEMENT_3D('',#443416,#128855,#128856);
#104812=AXIS2_PLACEMENT_3D('',#443429,#128857,#128858);
#104813=AXIS2_PLACEMENT_3D('',#443442,#128859,#128860);
#104814=AXIS2_PLACEMENT_3D('',#443443,#128861,#128862);
#104815=AXIS2_PLACEMENT_3D('',#443444,#128863,#128864);
#104816=AXIS2_PLACEMENT_3D('',#443457,#128865,#128866);
#104817=AXIS2_PLACEMENT_3D('',#443458,#128867,#128868);
#104818=AXIS2_PLACEMENT_3D('',#443465,#128871,#128872);
#104819=AXIS2_PLACEMENT_3D('',#443472,#128874,#128875);
#104820=AXIS2_PLACEMENT_3D('',#443475,#128876,#128877);
#104821=AXIS2_PLACEMENT_3D('',#443486,#128881,#128882);
#104822=AXIS2_PLACEMENT_3D('',#443554,#128883,#128884);
#104823=AXIS2_PLACEMENT_3D('',#443555,#128885,#128886);
#104824=AXIS2_PLACEMENT_3D('',#443597,#128887,#128888);
#104825=AXIS2_PLACEMENT_3D('',#443624,#128889,#128890);
#104826=AXIS2_PLACEMENT_3D('',#443705,#128891,#128892);
#104827=AXIS2_PLACEMENT_3D('',#443718,#128893,#128894);
#104828=AXIS2_PLACEMENT_3D('',#443719,#128895,#128896);
#104829=AXIS2_PLACEMENT_3D('',#443720,#128897,#128898);
#104830=AXIS2_PLACEMENT_3D('',#443733,#128899,#128900);
#104831=AXIS2_PLACEMENT_3D('',#443746,#128901,#128902);
#104832=AXIS2_PLACEMENT_3D('',#443765,#128903,#128904);
#104833=AXIS2_PLACEMENT_3D('',#443778,#128905,#128906);
#104834=AXIS2_PLACEMENT_3D('',#443791,#128907,#128908);
#104835=AXIS2_PLACEMENT_3D('',#443792,#128909,#128910);
#104836=AXIS2_PLACEMENT_3D('',#443793,#128911,#128912);
#104837=AXIS2_PLACEMENT_3D('',#443806,#128913,#128914);
#104838=AXIS2_PLACEMENT_3D('',#443807,#128915,#128916);
#104839=AXIS2_PLACEMENT_3D('',#443814,#128919,#128920);
#104840=AXIS2_PLACEMENT_3D('',#443821,#128922,#128923);
#104841=AXIS2_PLACEMENT_3D('',#443824,#128924,#128925);
#104842=AXIS2_PLACEMENT_3D('',#443835,#128929,#128930);
#104843=AXIS2_PLACEMENT_3D('',#443903,#128931,#128932);
#104844=AXIS2_PLACEMENT_3D('',#443904,#128933,#128934);
#104845=AXIS2_PLACEMENT_3D('',#443946,#128935,#128936);
#104846=AXIS2_PLACEMENT_3D('',#443973,#128937,#128938);
#104847=AXIS2_PLACEMENT_3D('',#444054,#128939,#128940);
#104848=AXIS2_PLACEMENT_3D('',#444067,#128941,#128942);
#104849=AXIS2_PLACEMENT_3D('',#444068,#128943,#128944);
#104850=AXIS2_PLACEMENT_3D('',#444069,#128945,#128946);
#104851=AXIS2_PLACEMENT_3D('',#444082,#128947,#128948);
#104852=AXIS2_PLACEMENT_3D('',#444095,#128949,#128950);
#104853=AXIS2_PLACEMENT_3D('',#444114,#128951,#128952);
#104854=AXIS2_PLACEMENT_3D('',#444127,#128953,#128954);
#104855=AXIS2_PLACEMENT_3D('',#444140,#128955,#128956);
#104856=AXIS2_PLACEMENT_3D('',#444141,#128957,#128958);
#104857=AXIS2_PLACEMENT_3D('',#444142,#128959,#128960);
#104858=AXIS2_PLACEMENT_3D('',#444155,#128961,#128962);
#104859=AXIS2_PLACEMENT_3D('',#444156,#128963,#128964);
#104860=AXIS2_PLACEMENT_3D('',#444163,#128967,#128968);
#104861=AXIS2_PLACEMENT_3D('',#444170,#128970,#128971);
#104862=AXIS2_PLACEMENT_3D('',#444173,#128972,#128973);
#104863=AXIS2_PLACEMENT_3D('',#444184,#128977,#128978);
#104864=AXIS2_PLACEMENT_3D('',#444252,#128979,#128980);
#104865=AXIS2_PLACEMENT_3D('',#444253,#128981,#128982);
#104866=AXIS2_PLACEMENT_3D('',#444295,#128983,#128984);
#104867=AXIS2_PLACEMENT_3D('',#444322,#128985,#128986);
#104868=AXIS2_PLACEMENT_3D('',#444403,#128987,#128988);
#104869=AXIS2_PLACEMENT_3D('',#444416,#128989,#128990);
#104870=AXIS2_PLACEMENT_3D('',#444417,#128991,#128992);
#104871=AXIS2_PLACEMENT_3D('',#444418,#128993,#128994);
#104872=AXIS2_PLACEMENT_3D('',#444431,#128995,#128996);
#104873=AXIS2_PLACEMENT_3D('',#444444,#128997,#128998);
#104874=AXIS2_PLACEMENT_3D('',#444463,#128999,#129000);
#104875=AXIS2_PLACEMENT_3D('',#444476,#129001,#129002);
#104876=AXIS2_PLACEMENT_3D('',#444489,#129003,#129004);
#104877=AXIS2_PLACEMENT_3D('',#444490,#129005,#129006);
#104878=AXIS2_PLACEMENT_3D('',#444491,#129007,#129008);
#104879=AXIS2_PLACEMENT_3D('',#444504,#129009,#129010);
#104880=AXIS2_PLACEMENT_3D('',#444505,#129011,#129012);
#104881=AXIS2_PLACEMENT_3D('',#444512,#129015,#129016);
#104882=AXIS2_PLACEMENT_3D('',#444519,#129018,#129019);
#104883=AXIS2_PLACEMENT_3D('',#444522,#129020,#129021);
#104884=AXIS2_PLACEMENT_3D('',#444533,#129025,#129026);
#104885=AXIS2_PLACEMENT_3D('',#444601,#129027,#129028);
#104886=AXIS2_PLACEMENT_3D('',#444602,#129029,#129030);
#104887=AXIS2_PLACEMENT_3D('',#444644,#129031,#129032);
#104888=AXIS2_PLACEMENT_3D('',#444671,#129033,#129034);
#104889=AXIS2_PLACEMENT_3D('',#444752,#129035,#129036);
#104890=AXIS2_PLACEMENT_3D('',#444765,#129037,#129038);
#104891=AXIS2_PLACEMENT_3D('',#444766,#129039,#129040);
#104892=AXIS2_PLACEMENT_3D('',#444767,#129041,#129042);
#104893=AXIS2_PLACEMENT_3D('',#444780,#129043,#129044);
#104894=AXIS2_PLACEMENT_3D('',#444793,#129045,#129046);
#104895=AXIS2_PLACEMENT_3D('',#444812,#129047,#129048);
#104896=AXIS2_PLACEMENT_3D('',#444825,#129049,#129050);
#104897=AXIS2_PLACEMENT_3D('',#444838,#129051,#129052);
#104898=AXIS2_PLACEMENT_3D('',#444839,#129053,#129054);
#104899=AXIS2_PLACEMENT_3D('',#444840,#129055,#129056);
#104900=AXIS2_PLACEMENT_3D('',#444853,#129057,#129058);
#104901=AXIS2_PLACEMENT_3D('',#444854,#129059,#129060);
#104902=AXIS2_PLACEMENT_3D('',#444861,#129063,#129064);
#104903=AXIS2_PLACEMENT_3D('',#444868,#129066,#129067);
#104904=AXIS2_PLACEMENT_3D('',#444871,#129068,#129069);
#104905=AXIS2_PLACEMENT_3D('',#444882,#129073,#129074);
#104906=AXIS2_PLACEMENT_3D('',#444950,#129075,#129076);
#104907=AXIS2_PLACEMENT_3D('',#444951,#129077,#129078);
#104908=AXIS2_PLACEMENT_3D('',#444993,#129079,#129080);
#104909=AXIS2_PLACEMENT_3D('',#445020,#129081,#129082);
#104910=AXIS2_PLACEMENT_3D('',#445101,#129083,#129084);
#104911=AXIS2_PLACEMENT_3D('',#445114,#129085,#129086);
#104912=AXIS2_PLACEMENT_3D('',#445115,#129087,#129088);
#104913=AXIS2_PLACEMENT_3D('',#445116,#129089,#129090);
#104914=AXIS2_PLACEMENT_3D('',#445129,#129091,#129092);
#104915=AXIS2_PLACEMENT_3D('',#445142,#129093,#129094);
#104916=AXIS2_PLACEMENT_3D('',#445161,#129095,#129096);
#104917=AXIS2_PLACEMENT_3D('',#445174,#129097,#129098);
#104918=AXIS2_PLACEMENT_3D('',#445187,#129099,#129100);
#104919=AXIS2_PLACEMENT_3D('',#445188,#129101,#129102);
#104920=AXIS2_PLACEMENT_3D('',#445189,#129103,#129104);
#104921=AXIS2_PLACEMENT_3D('',#445202,#129105,#129106);
#104922=AXIS2_PLACEMENT_3D('',#445203,#129107,#129108);
#104923=AXIS2_PLACEMENT_3D('',#445210,#129111,#129112);
#104924=AXIS2_PLACEMENT_3D('',#445217,#129114,#129115);
#104925=AXIS2_PLACEMENT_3D('',#445220,#129116,#129117);
#104926=AXIS2_PLACEMENT_3D('',#445231,#129121,#129122);
#104927=AXIS2_PLACEMENT_3D('',#445299,#129123,#129124);
#104928=AXIS2_PLACEMENT_3D('',#445300,#129125,#129126);
#104929=AXIS2_PLACEMENT_3D('',#445342,#129127,#129128);
#104930=AXIS2_PLACEMENT_3D('',#445369,#129129,#129130);
#104931=AXIS2_PLACEMENT_3D('',#445450,#129131,#129132);
#104932=AXIS2_PLACEMENT_3D('',#445463,#129133,#129134);
#104933=AXIS2_PLACEMENT_3D('',#445464,#129135,#129136);
#104934=AXIS2_PLACEMENT_3D('',#445465,#129137,#129138);
#104935=AXIS2_PLACEMENT_3D('',#445478,#129139,#129140);
#104936=AXIS2_PLACEMENT_3D('',#445491,#129141,#129142);
#104937=AXIS2_PLACEMENT_3D('',#445510,#129143,#129144);
#104938=AXIS2_PLACEMENT_3D('',#445523,#129145,#129146);
#104939=AXIS2_PLACEMENT_3D('',#445536,#129147,#129148);
#104940=AXIS2_PLACEMENT_3D('',#445537,#129149,#129150);
#104941=AXIS2_PLACEMENT_3D('',#445538,#129151,#129152);
#104942=AXIS2_PLACEMENT_3D('',#445551,#129153,#129154);
#104943=AXIS2_PLACEMENT_3D('',#445552,#129155,#129156);
#104944=AXIS2_PLACEMENT_3D('',#445559,#129159,#129160);
#104945=AXIS2_PLACEMENT_3D('',#445566,#129162,#129163);
#104946=AXIS2_PLACEMENT_3D('',#445569,#129164,#129165);
#104947=AXIS2_PLACEMENT_3D('',#445580,#129169,#129170);
#104948=AXIS2_PLACEMENT_3D('',#445648,#129171,#129172);
#104949=AXIS2_PLACEMENT_3D('',#445649,#129173,#129174);
#104950=AXIS2_PLACEMENT_3D('',#445691,#129175,#129176);
#104951=AXIS2_PLACEMENT_3D('',#445718,#129177,#129178);
#104952=AXIS2_PLACEMENT_3D('',#445799,#129179,#129180);
#104953=AXIS2_PLACEMENT_3D('',#445812,#129181,#129182);
#104954=AXIS2_PLACEMENT_3D('',#445813,#129183,#129184);
#104955=AXIS2_PLACEMENT_3D('',#445814,#129185,#129186);
#104956=AXIS2_PLACEMENT_3D('',#445827,#129187,#129188);
#104957=AXIS2_PLACEMENT_3D('',#445840,#129189,#129190);
#104958=AXIS2_PLACEMENT_3D('',#445859,#129191,#129192);
#104959=AXIS2_PLACEMENT_3D('',#445872,#129193,#129194);
#104960=AXIS2_PLACEMENT_3D('',#445885,#129195,#129196);
#104961=AXIS2_PLACEMENT_3D('',#445886,#129197,#129198);
#104962=AXIS2_PLACEMENT_3D('',#445887,#129199,#129200);
#104963=AXIS2_PLACEMENT_3D('',#445900,#129201,#129202);
#104964=AXIS2_PLACEMENT_3D('',#445901,#129203,#129204);
#104965=AXIS2_PLACEMENT_3D('',#445908,#129207,#129208);
#104966=AXIS2_PLACEMENT_3D('',#445915,#129210,#129211);
#104967=AXIS2_PLACEMENT_3D('',#445918,#129212,#129213);
#104968=AXIS2_PLACEMENT_3D('',#445929,#129217,#129218);
#104969=AXIS2_PLACEMENT_3D('',#445997,#129219,#129220);
#104970=AXIS2_PLACEMENT_3D('',#445998,#129221,#129222);
#104971=AXIS2_PLACEMENT_3D('',#446040,#129223,#129224);
#104972=AXIS2_PLACEMENT_3D('',#446067,#129225,#129226);
#104973=AXIS2_PLACEMENT_3D('',#446148,#129227,#129228);
#104974=AXIS2_PLACEMENT_3D('',#446161,#129229,#129230);
#104975=AXIS2_PLACEMENT_3D('',#446162,#129231,#129232);
#104976=AXIS2_PLACEMENT_3D('',#446163,#129233,#129234);
#104977=AXIS2_PLACEMENT_3D('',#446176,#129235,#129236);
#104978=AXIS2_PLACEMENT_3D('',#446189,#129237,#129238);
#104979=AXIS2_PLACEMENT_3D('',#446208,#129239,#129240);
#104980=AXIS2_PLACEMENT_3D('',#446221,#129241,#129242);
#104981=AXIS2_PLACEMENT_3D('',#446234,#129243,#129244);
#104982=AXIS2_PLACEMENT_3D('',#446235,#129245,#129246);
#104983=AXIS2_PLACEMENT_3D('',#446236,#129247,#129248);
#104984=AXIS2_PLACEMENT_3D('',#446249,#129249,#129250);
#104985=AXIS2_PLACEMENT_3D('',#446250,#129251,#129252);
#104986=AXIS2_PLACEMENT_3D('',#446257,#129255,#129256);
#104987=AXIS2_PLACEMENT_3D('',#446264,#129258,#129259);
#104988=AXIS2_PLACEMENT_3D('',#446267,#129260,#129261);
#104989=AXIS2_PLACEMENT_3D('',#446278,#129265,#129266);
#104990=AXIS2_PLACEMENT_3D('',#446346,#129267,#129268);
#104991=AXIS2_PLACEMENT_3D('',#446347,#129269,#129270);
#104992=AXIS2_PLACEMENT_3D('',#446389,#129271,#129272);
#104993=AXIS2_PLACEMENT_3D('',#446416,#129273,#129274);
#104994=AXIS2_PLACEMENT_3D('',#446497,#129275,#129276);
#104995=AXIS2_PLACEMENT_3D('',#446510,#129277,#129278);
#104996=AXIS2_PLACEMENT_3D('',#446511,#129279,#129280);
#104997=AXIS2_PLACEMENT_3D('',#446512,#129281,#129282);
#104998=AXIS2_PLACEMENT_3D('',#446525,#129283,#129284);
#104999=AXIS2_PLACEMENT_3D('',#446538,#129285,#129286);
#105000=AXIS2_PLACEMENT_3D('',#446557,#129287,#129288);
#105001=AXIS2_PLACEMENT_3D('',#446570,#129289,#129290);
#105002=AXIS2_PLACEMENT_3D('',#446583,#129291,#129292);
#105003=AXIS2_PLACEMENT_3D('',#446584,#129293,#129294);
#105004=AXIS2_PLACEMENT_3D('',#446585,#129295,#129296);
#105005=AXIS2_PLACEMENT_3D('',#446598,#129297,#129298);
#105006=AXIS2_PLACEMENT_3D('',#446599,#129299,#129300);
#105007=AXIS2_PLACEMENT_3D('',#446606,#129303,#129304);
#105008=AXIS2_PLACEMENT_3D('',#446613,#129306,#129307);
#105009=AXIS2_PLACEMENT_3D('',#446616,#129308,#129309);
#105010=AXIS2_PLACEMENT_3D('',#446627,#129313,#129314);
#105011=AXIS2_PLACEMENT_3D('',#446695,#129315,#129316);
#105012=AXIS2_PLACEMENT_3D('',#446696,#129317,#129318);
#105013=AXIS2_PLACEMENT_3D('',#446738,#129319,#129320);
#105014=AXIS2_PLACEMENT_3D('',#446765,#129321,#129322);
#105015=AXIS2_PLACEMENT_3D('',#446846,#129323,#129324);
#105016=AXIS2_PLACEMENT_3D('',#446859,#129325,#129326);
#105017=AXIS2_PLACEMENT_3D('',#446860,#129327,#129328);
#105018=AXIS2_PLACEMENT_3D('',#446861,#129329,#129330);
#105019=AXIS2_PLACEMENT_3D('',#446874,#129331,#129332);
#105020=AXIS2_PLACEMENT_3D('',#446887,#129333,#129334);
#105021=AXIS2_PLACEMENT_3D('',#446906,#129335,#129336);
#105022=AXIS2_PLACEMENT_3D('',#446919,#129337,#129338);
#105023=AXIS2_PLACEMENT_3D('',#446932,#129339,#129340);
#105024=AXIS2_PLACEMENT_3D('',#446933,#129341,#129342);
#105025=AXIS2_PLACEMENT_3D('',#446934,#129343,#129344);
#105026=AXIS2_PLACEMENT_3D('',#446947,#129345,#129346);
#105027=AXIS2_PLACEMENT_3D('',#446948,#129347,#129348);
#105028=AXIS2_PLACEMENT_3D('',#446955,#129351,#129352);
#105029=AXIS2_PLACEMENT_3D('',#446962,#129354,#129355);
#105030=AXIS2_PLACEMENT_3D('',#446965,#129356,#129357);
#105031=AXIS2_PLACEMENT_3D('',#446976,#129361,#129362);
#105032=AXIS2_PLACEMENT_3D('',#447044,#129363,#129364);
#105033=AXIS2_PLACEMENT_3D('',#447045,#129365,#129366);
#105034=AXIS2_PLACEMENT_3D('',#447087,#129367,#129368);
#105035=AXIS2_PLACEMENT_3D('',#447114,#129369,#129370);
#105036=AXIS2_PLACEMENT_3D('',#447195,#129371,#129372);
#105037=AXIS2_PLACEMENT_3D('',#447208,#129373,#129374);
#105038=AXIS2_PLACEMENT_3D('',#447209,#129375,#129376);
#105039=AXIS2_PLACEMENT_3D('',#447210,#129377,#129378);
#105040=AXIS2_PLACEMENT_3D('',#447223,#129379,#129380);
#105041=AXIS2_PLACEMENT_3D('',#447236,#129381,#129382);
#105042=AXIS2_PLACEMENT_3D('',#447255,#129383,#129384);
#105043=AXIS2_PLACEMENT_3D('',#447268,#129385,#129386);
#105044=AXIS2_PLACEMENT_3D('',#447281,#129387,#129388);
#105045=AXIS2_PLACEMENT_3D('',#447282,#129389,#129390);
#105046=AXIS2_PLACEMENT_3D('',#447283,#129391,#129392);
#105047=AXIS2_PLACEMENT_3D('',#447296,#129393,#129394);
#105048=AXIS2_PLACEMENT_3D('',#447297,#129395,#129396);
#105049=AXIS2_PLACEMENT_3D('',#447304,#129399,#129400);
#105050=AXIS2_PLACEMENT_3D('',#447311,#129402,#129403);
#105051=AXIS2_PLACEMENT_3D('',#447314,#129404,#129405);
#105052=AXIS2_PLACEMENT_3D('',#447325,#129409,#129410);
#105053=AXIS2_PLACEMENT_3D('',#447393,#129411,#129412);
#105054=AXIS2_PLACEMENT_3D('',#447394,#129413,#129414);
#105055=AXIS2_PLACEMENT_3D('',#447436,#129415,#129416);
#105056=AXIS2_PLACEMENT_3D('',#447463,#129417,#129418);
#105057=AXIS2_PLACEMENT_3D('',#447544,#129419,#129420);
#105058=AXIS2_PLACEMENT_3D('',#447557,#129421,#129422);
#105059=AXIS2_PLACEMENT_3D('',#447558,#129423,#129424);
#105060=AXIS2_PLACEMENT_3D('',#447559,#129425,#129426);
#105061=AXIS2_PLACEMENT_3D('',#447572,#129427,#129428);
#105062=AXIS2_PLACEMENT_3D('',#447585,#129429,#129430);
#105063=AXIS2_PLACEMENT_3D('',#447604,#129431,#129432);
#105064=AXIS2_PLACEMENT_3D('',#447617,#129433,#129434);
#105065=AXIS2_PLACEMENT_3D('',#447630,#129435,#129436);
#105066=AXIS2_PLACEMENT_3D('',#447631,#129437,#129438);
#105067=AXIS2_PLACEMENT_3D('',#447632,#129439,#129440);
#105068=AXIS2_PLACEMENT_3D('',#447645,#129441,#129442);
#105069=AXIS2_PLACEMENT_3D('',#447646,#129443,#129444);
#105070=AXIS2_PLACEMENT_3D('',#447653,#129447,#129448);
#105071=AXIS2_PLACEMENT_3D('',#447660,#129450,#129451);
#105072=AXIS2_PLACEMENT_3D('',#447663,#129452,#129453);
#105073=AXIS2_PLACEMENT_3D('',#447674,#129457,#129458);
#105074=AXIS2_PLACEMENT_3D('',#447742,#129459,#129460);
#105075=AXIS2_PLACEMENT_3D('',#447743,#129461,#129462);
#105076=AXIS2_PLACEMENT_3D('',#447785,#129463,#129464);
#105077=AXIS2_PLACEMENT_3D('',#447812,#129465,#129466);
#105078=AXIS2_PLACEMENT_3D('',#447893,#129467,#129468);
#105079=AXIS2_PLACEMENT_3D('',#447906,#129469,#129470);
#105080=AXIS2_PLACEMENT_3D('',#447907,#129471,#129472);
#105081=AXIS2_PLACEMENT_3D('',#447908,#129473,#129474);
#105082=AXIS2_PLACEMENT_3D('',#447921,#129475,#129476);
#105083=AXIS2_PLACEMENT_3D('',#447934,#129477,#129478);
#105084=AXIS2_PLACEMENT_3D('',#447953,#129479,#129480);
#105085=AXIS2_PLACEMENT_3D('',#447966,#129481,#129482);
#105086=AXIS2_PLACEMENT_3D('',#447979,#129483,#129484);
#105087=AXIS2_PLACEMENT_3D('',#447980,#129485,#129486);
#105088=AXIS2_PLACEMENT_3D('',#447981,#129487,#129488);
#105089=AXIS2_PLACEMENT_3D('',#447994,#129489,#129490);
#105090=AXIS2_PLACEMENT_3D('',#447995,#129491,#129492);
#105091=AXIS2_PLACEMENT_3D('',#448002,#129495,#129496);
#105092=AXIS2_PLACEMENT_3D('',#448009,#129498,#129499);
#105093=AXIS2_PLACEMENT_3D('',#448012,#129500,#129501);
#105094=AXIS2_PLACEMENT_3D('',#448023,#129505,#129506);
#105095=AXIS2_PLACEMENT_3D('',#448091,#129507,#129508);
#105096=AXIS2_PLACEMENT_3D('',#448092,#129509,#129510);
#105097=AXIS2_PLACEMENT_3D('',#448134,#129511,#129512);
#105098=AXIS2_PLACEMENT_3D('',#448161,#129513,#129514);
#105099=AXIS2_PLACEMENT_3D('',#448242,#129515,#129516);
#105100=AXIS2_PLACEMENT_3D('',#448255,#129517,#129518);
#105101=AXIS2_PLACEMENT_3D('',#448256,#129519,#129520);
#105102=AXIS2_PLACEMENT_3D('',#448257,#129521,#129522);
#105103=AXIS2_PLACEMENT_3D('',#448270,#129523,#129524);
#105104=AXIS2_PLACEMENT_3D('',#448283,#129525,#129526);
#105105=AXIS2_PLACEMENT_3D('',#448302,#129527,#129528);
#105106=AXIS2_PLACEMENT_3D('',#448315,#129529,#129530);
#105107=AXIS2_PLACEMENT_3D('',#448328,#129531,#129532);
#105108=AXIS2_PLACEMENT_3D('',#448329,#129533,#129534);
#105109=AXIS2_PLACEMENT_3D('',#448330,#129535,#129536);
#105110=AXIS2_PLACEMENT_3D('',#448343,#129537,#129538);
#105111=AXIS2_PLACEMENT_3D('',#448344,#129539,#129540);
#105112=AXIS2_PLACEMENT_3D('',#448351,#129543,#129544);
#105113=AXIS2_PLACEMENT_3D('',#448358,#129546,#129547);
#105114=AXIS2_PLACEMENT_3D('',#448361,#129548,#129549);
#105115=AXIS2_PLACEMENT_3D('',#448372,#129553,#129554);
#105116=AXIS2_PLACEMENT_3D('',#448440,#129555,#129556);
#105117=AXIS2_PLACEMENT_3D('',#448441,#129557,#129558);
#105118=AXIS2_PLACEMENT_3D('',#448483,#129559,#129560);
#105119=AXIS2_PLACEMENT_3D('',#448510,#129561,#129562);
#105120=AXIS2_PLACEMENT_3D('',#448591,#129563,#129564);
#105121=AXIS2_PLACEMENT_3D('',#448604,#129565,#129566);
#105122=AXIS2_PLACEMENT_3D('',#448605,#129567,#129568);
#105123=AXIS2_PLACEMENT_3D('',#448606,#129569,#129570);
#105124=AXIS2_PLACEMENT_3D('',#448619,#129571,#129572);
#105125=AXIS2_PLACEMENT_3D('',#448632,#129573,#129574);
#105126=AXIS2_PLACEMENT_3D('',#448651,#129575,#129576);
#105127=AXIS2_PLACEMENT_3D('',#448664,#129577,#129578);
#105128=AXIS2_PLACEMENT_3D('',#448677,#129579,#129580);
#105129=AXIS2_PLACEMENT_3D('',#448678,#129581,#129582);
#105130=AXIS2_PLACEMENT_3D('',#448679,#129583,#129584);
#105131=AXIS2_PLACEMENT_3D('',#448692,#129585,#129586);
#105132=AXIS2_PLACEMENT_3D('',#448693,#129587,#129588);
#105133=AXIS2_PLACEMENT_3D('',#448700,#129591,#129592);
#105134=AXIS2_PLACEMENT_3D('',#448707,#129594,#129595);
#105135=AXIS2_PLACEMENT_3D('',#448710,#129596,#129597);
#105136=AXIS2_PLACEMENT_3D('',#448721,#129601,#129602);
#105137=AXIS2_PLACEMENT_3D('',#448789,#129603,#129604);
#105138=AXIS2_PLACEMENT_3D('',#448790,#129605,#129606);
#105139=AXIS2_PLACEMENT_3D('',#448832,#129607,#129608);
#105140=AXIS2_PLACEMENT_3D('',#448859,#129609,#129610);
#105141=AXIS2_PLACEMENT_3D('',#448940,#129611,#129612);
#105142=AXIS2_PLACEMENT_3D('',#448953,#129613,#129614);
#105143=AXIS2_PLACEMENT_3D('',#448954,#129615,#129616);
#105144=AXIS2_PLACEMENT_3D('',#448955,#129617,#129618);
#105145=AXIS2_PLACEMENT_3D('',#448968,#129619,#129620);
#105146=AXIS2_PLACEMENT_3D('',#448981,#129621,#129622);
#105147=AXIS2_PLACEMENT_3D('',#449000,#129623,#129624);
#105148=AXIS2_PLACEMENT_3D('',#449013,#129625,#129626);
#105149=AXIS2_PLACEMENT_3D('',#449026,#129627,#129628);
#105150=AXIS2_PLACEMENT_3D('',#449027,#129629,#129630);
#105151=AXIS2_PLACEMENT_3D('',#449028,#129631,#129632);
#105152=AXIS2_PLACEMENT_3D('',#449041,#129633,#129634);
#105153=AXIS2_PLACEMENT_3D('',#449042,#129635,#129636);
#105154=AXIS2_PLACEMENT_3D('',#449049,#129639,#129640);
#105155=AXIS2_PLACEMENT_3D('',#449056,#129642,#129643);
#105156=AXIS2_PLACEMENT_3D('',#449059,#129644,#129645);
#105157=AXIS2_PLACEMENT_3D('',#449070,#129649,#129650);
#105158=AXIS2_PLACEMENT_3D('',#449138,#129651,#129652);
#105159=AXIS2_PLACEMENT_3D('',#449139,#129653,#129654);
#105160=AXIS2_PLACEMENT_3D('',#449181,#129655,#129656);
#105161=AXIS2_PLACEMENT_3D('',#449208,#129657,#129658);
#105162=AXIS2_PLACEMENT_3D('',#449289,#129659,#129660);
#105163=AXIS2_PLACEMENT_3D('',#449302,#129661,#129662);
#105164=AXIS2_PLACEMENT_3D('',#449303,#129663,#129664);
#105165=AXIS2_PLACEMENT_3D('',#449304,#129665,#129666);
#105166=AXIS2_PLACEMENT_3D('',#449317,#129667,#129668);
#105167=AXIS2_PLACEMENT_3D('',#449330,#129669,#129670);
#105168=AXIS2_PLACEMENT_3D('',#449349,#129671,#129672);
#105169=AXIS2_PLACEMENT_3D('',#449362,#129673,#129674);
#105170=AXIS2_PLACEMENT_3D('',#449375,#129675,#129676);
#105171=AXIS2_PLACEMENT_3D('',#449376,#129677,#129678);
#105172=AXIS2_PLACEMENT_3D('',#449377,#129679,#129680);
#105173=AXIS2_PLACEMENT_3D('',#449390,#129681,#129682);
#123764=DIRECTION('axis',(0.,0.,1.));
#123765=DIRECTION('refdir',(1.,0.,0.));
#123766=DIRECTION('center_axis',(0.,0.,1.));
#123767=DIRECTION('ref_axis',(0.,1.,0.));
#123768=DIRECTION('',(0.,0.,-1.));
#123769=DIRECTION('center_axis',(0.,-4.12699273797265E-32,1.));
#123770=DIRECTION('ref_axis',(0.,-1.,-4.12699273797265E-32));
#123771=DIRECTION('center_axis',(0.,0.,1.));
#123772=DIRECTION('ref_axis',(0.,1.,0.));
#123773=DIRECTION('',(0.,0.,-1.));
#123774=DIRECTION('center_axis',(0.,0.,1.));
#123775=DIRECTION('ref_axis',(0.,1.,0.));
#123776=DIRECTION('',(0.,0.,-1.));
#123777=DIRECTION('center_axis',(0.,0.,1.));
#123778=DIRECTION('ref_axis',(0.,1.,0.));
#123779=DIRECTION('',(0.,0.,-1.));
#123780=DIRECTION('center_axis',(0.,0.,1.));
#123781=DIRECTION('ref_axis',(0.,1.,0.));
#123782=DIRECTION('',(0.,0.,-1.));
#123783=DIRECTION('center_axis',(0.,0.,1.));
#123784=DIRECTION('ref_axis',(0.,1.,0.));
#123785=DIRECTION('',(0.,0.,-1.));
#123786=DIRECTION('center_axis',(0.,0.,1.));
#123787=DIRECTION('ref_axis',(0.,1.,0.));
#123788=DIRECTION('',(0.,0.,-1.));
#123789=DIRECTION('center_axis',(0.,0.,1.));
#123790=DIRECTION('ref_axis',(0.,1.,0.));
#123791=DIRECTION('',(0.,0.,-1.));
#123792=DIRECTION('center_axis',(0.,0.,1.));
#123793=DIRECTION('ref_axis',(0.,1.,0.));
#123794=DIRECTION('',(0.,0.,-1.));
#123795=DIRECTION('center_axis',(0.,0.,1.));
#123796=DIRECTION('ref_axis',(0.,1.,0.));
#123797=DIRECTION('',(0.,0.,-1.));
#123798=DIRECTION('center_axis',(0.,0.,1.));
#123799=DIRECTION('ref_axis',(0.,1.,0.));
#123800=DIRECTION('',(0.,0.,-1.));
#123801=DIRECTION('center_axis',(0.,0.,1.));
#123802=DIRECTION('ref_axis',(0.,1.,0.));
#123803=DIRECTION('',(0.,0.,-1.));
#123804=DIRECTION('center_axis',(0.,0.,1.));
#123805=DIRECTION('ref_axis',(0.,1.,0.));
#123806=DIRECTION('',(0.,0.,-1.));
#123807=DIRECTION('center_axis',(0.,0.,1.));
#123808=DIRECTION('ref_axis',(0.,1.,0.));
#123809=DIRECTION('',(0.,0.,-1.));
#123810=DIRECTION('center_axis',(0.,0.,1.));
#123811=DIRECTION('ref_axis',(0.,1.,0.));
#123812=DIRECTION('',(0.,0.,-1.));
#123813=DIRECTION('center_axis',(0.,0.,1.));
#123814=DIRECTION('ref_axis',(0.,1.,0.));
#123815=DIRECTION('',(0.,0.,-1.));
#123816=DIRECTION('center_axis',(0.,0.,1.));
#123817=DIRECTION('ref_axis',(0.,1.,0.));
#123818=DIRECTION('',(0.,0.,-1.));
#123819=DIRECTION('center_axis',(0.,0.,1.));
#123820=DIRECTION('ref_axis',(0.,1.,0.));
#123821=DIRECTION('',(0.,0.,-1.));
#123822=DIRECTION('center_axis',(0.,0.,1.));
#123823=DIRECTION('ref_axis',(0.,1.,0.));
#123824=DIRECTION('',(0.,0.,-1.));
#123825=DIRECTION('center_axis',(0.,0.,1.));
#123826=DIRECTION('ref_axis',(0.,1.,0.));
#123827=DIRECTION('',(0.,0.,-1.));
#123828=DIRECTION('center_axis',(0.,0.,1.));
#123829=DIRECTION('ref_axis',(0.,1.,0.));
#123830=DIRECTION('',(0.,0.,-1.));
#123831=DIRECTION('center_axis',(0.,0.,1.));
#123832=DIRECTION('ref_axis',(0.,1.,0.));
#123833=DIRECTION('',(0.,0.,-1.));
#123834=DIRECTION('center_axis',(0.,0.,1.));
#123835=DIRECTION('ref_axis',(0.,1.,0.));
#123836=DIRECTION('',(0.,0.,-1.));
#123837=DIRECTION('center_axis',(0.,0.,1.));
#123838=DIRECTION('ref_axis',(0.,1.,0.));
#123839=DIRECTION('',(0.,0.,-1.));
#123840=DIRECTION('center_axis',(0.,0.,1.));
#123841=DIRECTION('ref_axis',(0.,1.,0.));
#123842=DIRECTION('',(0.,0.,-1.));
#123843=DIRECTION('center_axis',(0.,0.,1.));
#123844=DIRECTION('ref_axis',(0.,1.,0.));
#123845=DIRECTION('',(0.,0.,-1.));
#123846=DIRECTION('center_axis',(0.,0.,1.));
#123847=DIRECTION('ref_axis',(0.,1.,0.));
#123848=DIRECTION('',(0.,0.,-1.));
#123849=DIRECTION('center_axis',(0.,0.,1.));
#123850=DIRECTION('ref_axis',(0.,1.,0.));
#123851=DIRECTION('',(0.,0.,-1.));
#123852=DIRECTION('center_axis',(0.,0.,1.));
#123853=DIRECTION('ref_axis',(0.,1.,0.));
#123854=DIRECTION('',(0.,0.,-1.));
#123855=DIRECTION('center_axis',(0.,0.,1.));
#123856=DIRECTION('ref_axis',(0.,1.,0.));
#123857=DIRECTION('',(0.,0.,-1.));
#123858=DIRECTION('center_axis',(0.,0.,1.));
#123859=DIRECTION('ref_axis',(0.,1.,0.));
#123860=DIRECTION('',(0.,0.,-1.));
#123861=DIRECTION('center_axis',(0.,0.,1.));
#123862=DIRECTION('ref_axis',(0.,1.,0.));
#123863=DIRECTION('',(0.,0.,-1.));
#123864=DIRECTION('center_axis',(0.,0.,1.));
#123865=DIRECTION('ref_axis',(0.,1.,0.));
#123866=DIRECTION('',(0.,0.,-1.));
#123867=DIRECTION('center_axis',(0.,0.,1.));
#123868=DIRECTION('ref_axis',(0.,1.,0.));
#123869=DIRECTION('',(0.,0.,-1.));
#123870=DIRECTION('center_axis',(0.,0.,1.));
#123871=DIRECTION('ref_axis',(0.,1.,0.));
#123872=DIRECTION('',(0.,0.,-1.));
#123873=DIRECTION('center_axis',(0.,0.,1.));
#123874=DIRECTION('ref_axis',(0.,1.,0.));
#123875=DIRECTION('',(0.,0.,-1.));
#123876=DIRECTION('center_axis',(0.,-1.22464679914735E-16,1.));
#123877=DIRECTION('ref_axis',(0.,-1.,-1.22464679914735E-16));
#123878=DIRECTION('',(8.65956056235489E-17,-0.707106781186543,-0.707106781186552));
#123879=DIRECTION('center_axis',(0.,0.,1.));
#123880=DIRECTION('ref_axis',(0.802795663530306,0.596254243269543,0.));
#123881=DIRECTION('center_axis',(0.,-4.12699273797265E-32,1.));
#123882=DIRECTION('ref_axis',(0.,-1.,-4.12699273797265E-32));
#123883=DIRECTION('',(8.65956056235498E-17,-0.707106781186552,-0.707106781186544));
#123884=DIRECTION('center_axis',(0.,-4.12699273797265E-32,1.));
#123885=DIRECTION('ref_axis',(0.,-1.,-4.12699273797265E-32));
#123886=DIRECTION('center_axis',(0.,-4.12699273797265E-32,1.));
#123887=DIRECTION('ref_axis',(0.,-1.,-4.12699273797265E-32));
#123888=DIRECTION('',(0.,4.12699273797265E-32,-1.));
#123889=DIRECTION('center_axis',(0.,-4.12699273797265E-32,1.));
#123890=DIRECTION('ref_axis',(0.,-1.,-4.12699273797265E-32));
#123891=DIRECTION('center_axis',(0.,-4.12699273797265E-32,1.));
#123892=DIRECTION('ref_axis',(0.,-1.,-4.12699273797265E-32));
#123893=DIRECTION('',(0.,4.12699273797265E-32,-1.));
#123894=DIRECTION('center_axis',(0.,-4.12699273797265E-32,1.));
#123895=DIRECTION('ref_axis',(0.,-1.,-4.12699273797265E-32));
#123896=DIRECTION('',(0.,4.12699273797265E-32,-1.));
#123897=DIRECTION('center_axis',(0.,-4.12699273797265E-32,1.));
#123898=DIRECTION('ref_axis',(0.,-1.,-4.12699273797265E-32));
#123899=DIRECTION('',(0.,4.12699273797265E-32,-1.));
#123900=DIRECTION('center_axis',(0.,-4.12699273797265E-32,1.));
#123901=DIRECTION('ref_axis',(0.,-1.,-4.12699273797265E-32));
#123902=DIRECTION('',(0.,4.12699273797265E-32,-1.));
#123903=DIRECTION('center_axis',(0.,-4.12699273797265E-32,1.));
#123904=DIRECTION('ref_axis',(0.,-1.,-4.12699273797265E-32));
#123905=DIRECTION('',(0.,4.12699273797265E-32,-1.));
#123906=DIRECTION('center_axis',(0.,-4.12699273797265E-32,1.));
#123907=DIRECTION('ref_axis',(0.,-1.,-4.12699273797265E-32));
#123908=DIRECTION('',(0.,4.12699273797265E-32,-1.));
#123909=DIRECTION('center_axis',(0.,-4.12699273797265E-32,1.));
#123910=DIRECTION('ref_axis',(0.,-1.,-4.12699273797265E-32));
#123911=DIRECTION('',(0.,4.12699273797265E-32,-1.));
#123912=DIRECTION('center_axis',(0.,-4.12699273797265E-32,1.));
#123913=DIRECTION('ref_axis',(0.,-1.,-4.12699273797265E-32));
#123914=DIRECTION('',(0.,4.12699273797265E-32,-1.));
#123915=DIRECTION('center_axis',(0.,-4.12699273797265E-32,1.));
#123916=DIRECTION('ref_axis',(0.,-1.,-4.12699273797265E-32));
#123917=DIRECTION('',(0.,4.12699273797265E-32,-1.));
#123918=DIRECTION('center_axis',(0.,-4.12699273797265E-32,1.));
#123919=DIRECTION('ref_axis',(0.,-1.,-4.12699273797265E-32));
#123920=DIRECTION('',(0.,4.12699273797265E-32,-1.));
#123921=DIRECTION('center_axis',(0.,-4.12699273797265E-32,1.));
#123922=DIRECTION('ref_axis',(0.,-1.,-4.12699273797265E-32));
#123923=DIRECTION('',(0.,4.12699273797265E-32,-1.));
#123924=DIRECTION('center_axis',(0.,-4.12699273797265E-32,1.));
#123925=DIRECTION('ref_axis',(0.,-1.,-4.12699273797265E-32));
#123926=DIRECTION('',(0.,4.12699273797265E-32,-1.));
#123927=DIRECTION('center_axis',(0.,-4.12699273797265E-32,1.));
#123928=DIRECTION('ref_axis',(0.,-1.,-4.12699273797265E-32));
#123929=DIRECTION('',(0.,4.12699273797265E-32,-1.));
#123930=DIRECTION('center_axis',(0.,-4.12699273797265E-32,1.));
#123931=DIRECTION('ref_axis',(0.,-1.,-4.12699273797265E-32));
#123932=DIRECTION('',(0.,4.12699273797265E-32,-1.));
#123933=DIRECTION('center_axis',(0.,-4.12699273797265E-32,1.));
#123934=DIRECTION('ref_axis',(0.,-1.,-4.12699273797265E-32));
#123935=DIRECTION('',(0.,4.12699273797265E-32,-1.));
#123936=DIRECTION('center_axis',(0.,-4.12699273797265E-32,1.));
#123937=DIRECTION('ref_axis',(0.,-1.,-4.12699273797265E-32));
#123938=DIRECTION('',(0.,4.12699273797265E-32,-1.));
#123939=DIRECTION('center_axis',(0.,-4.12699273797265E-32,1.));
#123940=DIRECTION('ref_axis',(0.,-1.,-4.12699273797265E-32));
#123941=DIRECTION('',(0.,4.12699273797265E-32,-1.));
#123942=DIRECTION('center_axis',(0.,-4.12699273797265E-32,1.));
#123943=DIRECTION('ref_axis',(0.,-1.,-4.12699273797265E-32));
#123944=DIRECTION('',(0.,4.12699273797265E-32,-1.));
#123945=DIRECTION('center_axis',(0.,-4.12699273797265E-32,1.));
#123946=DIRECTION('ref_axis',(0.,-1.,-4.12699273797265E-32));
#123947=DIRECTION('',(0.,4.12699273797265E-32,-1.));
#123948=DIRECTION('center_axis',(0.,-4.12699273797265E-32,1.));
#123949=DIRECTION('ref_axis',(0.,-1.,-4.12699273797265E-32));
#123950=DIRECTION('',(0.,4.12699273797265E-32,-1.));
#123951=DIRECTION('center_axis',(0.,-4.12699273797265E-32,1.));
#123952=DIRECTION('ref_axis',(0.,-1.,-4.12699273797265E-32));
#123953=DIRECTION('',(0.,4.12699273797265E-32,-1.));
#123954=DIRECTION('center_axis',(0.,-4.12699273797265E-32,1.));
#123955=DIRECTION('ref_axis',(0.,-1.,-4.12699273797265E-32));
#123956=DIRECTION('',(0.,4.12699273797265E-32,-1.));
#123957=DIRECTION('center_axis',(0.,-4.12699273797265E-32,1.));
#123958=DIRECTION('ref_axis',(0.,-1.,-4.12699273797265E-32));
#123959=DIRECTION('',(0.,4.12699273797265E-32,-1.));
#123960=DIRECTION('center_axis',(0.,-4.12699273797265E-32,1.));
#123961=DIRECTION('ref_axis',(0.,-1.,-4.12699273797265E-32));
#123962=DIRECTION('',(0.,4.12699273797265E-32,-1.));
#123963=DIRECTION('center_axis',(0.,-4.12699273797265E-32,1.));
#123964=DIRECTION('ref_axis',(0.,-1.,-4.12699273797265E-32));
#123965=DIRECTION('',(0.,4.12699273797265E-32,-1.));
#123966=DIRECTION('center_axis',(0.,-4.12699273797265E-32,1.));
#123967=DIRECTION('ref_axis',(0.,-1.,-4.12699273797265E-32));
#123968=DIRECTION('',(0.,4.12699273797265E-32,-1.));
#123969=DIRECTION('center_axis',(0.,-4.12699273797265E-32,1.));
#123970=DIRECTION('ref_axis',(0.,-1.,-4.12699273797265E-32));
#123971=DIRECTION('',(0.,4.12699273797265E-32,-1.));
#123972=DIRECTION('center_axis',(0.,-4.12699273797265E-32,1.));
#123973=DIRECTION('ref_axis',(0.,-1.,-4.12699273797265E-32));
#123974=DIRECTION('',(0.,4.12699273797265E-32,-1.));
#123975=DIRECTION('center_axis',(0.,-4.12699273797265E-32,1.));
#123976=DIRECTION('ref_axis',(0.,-1.,-4.12699273797265E-32));
#123977=DIRECTION('',(0.,4.12699273797265E-32,-1.));
#123978=DIRECTION('center_axis',(0.,-4.12699273797265E-32,1.));
#123979=DIRECTION('ref_axis',(0.,-1.,-4.12699273797265E-32));
#123980=DIRECTION('',(0.,4.12699273797265E-32,-1.));
#123981=DIRECTION('center_axis',(0.,-4.12699273797265E-32,1.));
#123982=DIRECTION('ref_axis',(0.,-1.,-4.12699273797265E-32));
#123983=DIRECTION('',(0.,4.12699273797265E-32,-1.));
#123984=DIRECTION('center_axis',(0.,-4.12699273797265E-32,1.));
#123985=DIRECTION('ref_axis',(0.,-1.,-4.12699273797265E-32));
#123986=DIRECTION('',(0.,4.12699273797265E-32,-1.));
#123987=DIRECTION('center_axis',(0.,-4.12699273797265E-32,1.));
#123988=DIRECTION('ref_axis',(0.,-1.,-4.12699273797265E-32));
#123989=DIRECTION('',(0.,4.12699273797265E-32,-1.));
#123990=DIRECTION('center_axis',(0.,-4.12699273797265E-32,1.));
#123991=DIRECTION('ref_axis',(0.,-1.,-4.12699273797265E-32));
#123992=DIRECTION('center_axis',(0.,1.22464679914735E-16,-1.));
#123993=DIRECTION('ref_axis',(0.,1.,1.22464679914735E-16));
#123994=DIRECTION('',(0.,4.12699273797265E-32,-1.));
#123995=DIRECTION('center_axis',(0.,1.22464679914735E-16,-1.));
#123996=DIRECTION('ref_axis',(0.,1.,1.22464679914735E-16));
#123997=DIRECTION('',(0.,4.12699273797265E-32,-1.));
#123998=DIRECTION('center_axis',(-1.70823811232218E-32,2.97377031107479E-32,
-1.));
#123999=DIRECTION('ref_axis',(0.830050209755074,0.557688666986839,0.));
#124000=DIRECTION('center_axis',(1.70823811232218E-32,-2.97377031107479E-32,
1.));
#124001=DIRECTION('ref_axis',(-0.830050209755074,-0.557688666986839,-2.40514597263697E-33));
#124002=DIRECTION('center_axis',(0.545790114644076,-0.837921924022045,6.13681984861663E-17));
#124003=DIRECTION('ref_axis',(0.837921924022045,0.545790114644076,-3.6361557350031E-31));
#124004=DIRECTION('center_axis',(-1.70823811232218E-32,2.97377031107479E-32,
-1.));
#124005=DIRECTION('ref_axis',(0.830050209755074,0.557688666986839,2.40514597263697E-33));
#124006=DIRECTION('center_axis',(0.569473707694335,-0.822009547538754,-3.46966352979465E-16));
#124007=DIRECTION('ref_axis',(-0.822009547538754,-0.569473707694335,7.88510670898553E-14));
#124008=DIRECTION('center_axis',(-1.79610390708164E-32,3.11682651859213E-32,
-1.));
#124009=DIRECTION('ref_axis',(0.872745089844851,0.488176206048291,0.));
#124010=DIRECTION('center_axis',(1.79610390708164E-32,-3.11682651859213E-32,
1.));
#124011=DIRECTION('ref_axis',(-0.872745089844851,-0.488176206048291,4.59803209996414E-34));
#124012=DIRECTION('center_axis',(0.4756756273667,-0.879620769155263,6.13681984861663E-17));
#124013=DIRECTION('ref_axis',(0.879620769155263,0.4756756273667,1.87970762572194E-31));
#124014=DIRECTION('center_axis',(-1.79610390708164E-32,3.11682651859213E-32,
-1.));
#124015=DIRECTION('ref_axis',(0.872745089844851,0.488176206048291,-4.59803209996414E-34));
#124016=DIRECTION('center_axis',(0.500577421621527,-0.865691772493388,-3.46966352979465E-16));
#124017=DIRECTION('ref_axis',(-0.865691772493388,-0.500577421621527,7.88510670898553E-14));
#124018=DIRECTION('center_axis',(-1.87201692667575E-32,3.2665685963594E-32,
-1.));
#124019=DIRECTION('ref_axis',(0.909631995354514,0.415415013001897,0.));
#124020=DIRECTION('center_axis',(1.87201692667575E-32,-3.2665685963594E-32,
1.));
#124021=DIRECTION('ref_axis',(-0.909631995354514,-0.415415013001896,3.45864856421259E-33));
#124022=DIRECTION('center_axis',(0.402395597270152,-0.915465883196964,6.13681984861663E-17));
#124023=DIRECTION('ref_axis',(0.915465883196964,0.402395597270152,-6.16297582203915E-33));
#124024=DIRECTION('center_axis',(-1.87201692667575E-32,3.2665685963594E-32,
-1.));
#124025=DIRECTION('ref_axis',(0.909631995354514,0.415415013001897,-3.45864856421259E-33));
#124026=DIRECTION('center_axis',(0.428349875397288,-0.903612961531168,-3.46966352979465E-16));
#124027=DIRECTION('ref_axis',(-0.903612961531168,-0.428349875397288,7.88510670898543E-14));
#124028=DIRECTION('center_axis',(-1.93547198248389E-32,3.42200003555476E-32,
-1.));
#124029=DIRECTION('ref_axis',(0.940465450013808,0.339889301582627,0.));
#124030=DIRECTION('center_axis',(1.93547198248389E-32,-3.42200003555476E-32,
1.));
#124031=DIRECTION('ref_axis',(-0.940465450013808,-0.339889301582627,6.57143326895392E-33));
#124032=DIRECTION('center_axis',(0.326437690864372,-0.945218722827229,6.13681984861663E-17));
#124033=DIRECTION('ref_axis',(0.945218722827228,0.326437690864372,2.65007960347684E-31));
#124034=DIRECTION('center_axis',(-1.93547198248389E-32,3.42200003555476E-32,
-1.));
#124035=DIRECTION('ref_axis',(0.940465450013808,0.339889301582627,-6.57143326895392E-33));
#124036=DIRECTION('center_axis',(0.353271731425036,-0.935520755395602,-3.46966352979465E-16));
#124037=DIRECTION('ref_axis',(-0.935520755395602,-0.353271731425036,7.88510670898545E-14));
#124038=DIRECTION('center_axis',(-1.98604679157899E-32,3.58208646559475E-32,
-1.));
#124039=DIRECTION('ref_axis',(0.965040262269137,0.262101682939113,0.));
#124040=DIRECTION('center_axis',(1.98604679157899E-32,-3.58208646559475E-32,
1.));
#124041=DIRECTION('ref_axis',(-0.965040262269137,-0.262101682939113,9.77744225558367E-33));
#124042=DIRECTION('center_axis',(0.248307395484317,-0.96868128780719,6.13681984861663E-17));
#124043=DIRECTION('ref_axis',(0.968681287807189,0.248307395484317,-4.00593428432545E-32));
#124044=DIRECTION('center_axis',(-1.98604679157899E-32,3.58208646559475E-32,
-1.));
#124045=DIRECTION('ref_axis',(0.965040262269137,0.262101682939113,-9.77744225558366E-33));
#124046=DIRECTION('center_axis',(0.275842622365882,-0.961202812982938,-3.46966352979465E-16));
#124047=DIRECTION('ref_axis',(-0.961202812982938,-0.275842622365882,7.88510670898555E-14));
#124048=DIRECTION('center_axis',(-2.0234047869508E-32,3.74576253769986E-32,
-1.));
#124049=DIRECTION('ref_axis',(0.983192890799501,0.182569820839372,0.));
#124050=DIRECTION('center_axis',(2.0234047869508E-32,-3.74576253769986E-32,
1.));
#124051=DIRECTION('ref_axis',(-0.983192890799501,-0.182569820839372,1.30553400632501E-32));
#124052=DIRECTION('center_axis',(0.16852465535515,-0.985697438637956,6.13681984861663E-17));
#124053=DIRECTION('ref_axis',(0.985697438637956,0.16852465535515,-9.24446373305873E-32));
#124054=DIRECTION('center_axis',(-2.0234047869508E-32,3.74576253769986E-32,
-1.));
#124055=DIRECTION('ref_axis',(0.983192890799501,0.182569820839372,-1.30553400632501E-32));
#124056=DIRECTION('center_axis',(0.196577826165713,-0.980488224437174,-3.46966352979465E-16));
#124057=DIRECTION('ref_axis',(-0.980488224437174,-0.196577826165713,7.88510670898544E-14));
#124058=DIRECTION('center_axis',(-2.04729735730373E-32,3.91193901461487E-32,
-1.));
#124059=DIRECTION('ref_axis',(0.994802532857003,0.101822986703845,0.));
#124060=DIRECTION('center_axis',(2.04729735730373E-32,-3.91193901461487E-32,
1.));
#124061=DIRECTION('ref_axis',(-0.994802532857003,-0.101822986703845,1.63833128228582E-32));
#124062=DIRECTION('center_axis',(0.0876204114492056,-0.996153935643218,
6.13681984861663E-17));
#124063=DIRECTION('ref_axis',(0.996153935643218,0.0876204114492056,7.70371977754894E-34));
#124064=DIRECTION('center_axis',(-2.04729735730373E-32,3.91193901461487E-32,
-1.));
#124065=DIRECTION('ref_axis',(0.994802532857003,0.101822986703845,-1.63833128228582E-32));
#124066=DIRECTION('center_axis',(0.116004836965469,-0.993248648526951,-3.46966352979465E-16));
#124067=DIRECTION('ref_axis',(-0.993248648526951,-0.116004836965469,7.88510670898549E-14));
#124068=DIRECTION('center_axis',(-2.0575655015241E-32,4.07951001930311E-32,
-1.));
#124069=DIRECTION('ref_axis',(0.999791928189206,0.0203985373914152,0.));
#124070=DIRECTION('center_axis',(2.0575655015241E-32,-4.07951001930311E-32,
1.));
#124071=DIRECTION('ref_axis',(-0.999791928189206,-0.0203985373914152,1.97392134247697E-32));
#124072=DIRECTION('center_axis',(0.00613306816141749,-0.999981192560604,
6.13681984861663E-17));
#124073=DIRECTION('ref_axis',(0.999981192560604,0.0061330681614175,-3.37037740267766E-33));
#124074=DIRECTION('center_axis',(-2.0575655015241E-32,4.07951001930311E-32,
-1.));
#124075=DIRECTION('ref_axis',(0.999791928189206,0.0203985373914152,-1.97392134247697E-32));
#124076=DIRECTION('center_axis',(0.0346598547146713,-0.999399166735273,
-3.46966352979465E-16));
#124077=DIRECTION('ref_axis',(-0.999399166735273,-0.0346598547146713,7.88510670898555E-14));
#124078=DIRECTION('center_axis',(-2.05414088680624E-32,4.24736039437564E-32,
-1.));
#124079=DIRECTION('ref_axis',(0.998127873193367,-0.061161660821833,0.));
#124080=DIRECTION('center_axis',(2.05414088680624E-32,-4.24736039437564E-32,
1.));
#124081=DIRECTION('ref_axis',(-0.998127873193367,0.061161660821833,2.31007089041634E-32));
#124082=DIRECTION('center_axis',(-0.0753950896830998,-0.997153739626783,
6.13681984861663E-17));
#124083=DIRECTION('ref_axis',(0.997153739626783,-0.0753950896830998,3.38963670212153E-32));
#124084=DIRECTION('center_axis',(-2.05414088680624E-32,4.24736039437564E-32,
-1.));
#124085=DIRECTION('ref_axis',(0.998127873193367,-0.061161660821833,-2.31007089041634E-32));
#124086=DIRECTION('center_axis',(-0.0469157831507791,-0.998898848378228,
-3.46966352979465E-16));
#124087=DIRECTION('ref_axis',(-0.998898848378228,0.0469157831507791,7.88510670898549E-14));
#124088=DIRECTION('center_axis',(-2.03704630339607E-32,4.41437312327972E-32,
-1.));
#124089=DIRECTION('ref_axis',(0.989821441880934,-0.142314838273276,0.));
#124090=DIRECTION('center_axis',(2.03704630339607E-32,-4.41437312327972E-32,
1.));
#124091=DIRECTION('ref_axis',(-0.989821441880934,0.142314838273276,2.64454290632317E-32));
#124092=DIRECTION('center_axis',(-0.15642150564509,-0.987690393074532,6.13681984861663E-17));
#124093=DIRECTION('ref_axis',(0.987690393074532,-0.15642150564509,1.55615139506489E-31));
#124094=DIRECTION('center_axis',(-2.03704630339607E-32,4.41437312327972E-32,
-1.));
#124095=DIRECTION('ref_axis',(0.989821441880934,-0.142314838273276,-2.64454290632317E-32));
#124096=DIRECTION('center_axis',(-0.12817920421992,-0.991751022991934,-3.46966352979465E-16));
#124097=DIRECTION('ref_axis',(-0.991751022991934,0.12817920421992,7.88510670898542E-14));
#124098=DIRECTION('center_axis',(-2.00639551292579E-32,4.57943676385965E-32,
-1.));
#124099=DIRECTION('ref_axis',(0.974927912181826,-0.222520933956305,0.));
#124100=DIRECTION('center_axis',(2.00639551292579E-32,-4.57943676385965E-32,
1.));
#124101=DIRECTION('ref_axis',(-0.974927912181826,0.222520933956305,2.97511153411561E-32));
#124102=DIRECTION('center_axis',(-0.236406962294745,-0.971654129913814,
6.13681984861663E-17));
#124103=DIRECTION('ref_axis',(0.971654129913814,-0.236406962294745,-1.72563323017096E-31));
#124104=DIRECTION('center_axis',(-2.00639551292579E-32,4.57943676385965E-32,
-1.));
#124105=DIRECTION('ref_axis',(0.974927912181826,-0.222520933956305,-2.97511153411561E-32));
#124106=DIRECTION('center_axis',(-0.208589613833058,-0.978003258175031,
-3.46966352979465E-16));
#124107=DIRECTION('ref_axis',(-0.978003258175031,0.208589613833058,7.88510670898555E-14));
#124108=DIRECTION('center_axis',(-1.96239249134894E-32,4.74145284482097E-32,
-1.));
#124109=DIRECTION('ref_axis',(0.953546398078931,-0.301246189537225,0.));
#124110=DIRECTION('center_axis',(1.96239249134894E-32,-4.74145284482097E-32,
1.));
#124111=DIRECTION('ref_axis',(-0.95354639807893,0.301246189537225,3.29957689411567E-32));
#124112=DIRECTION('center_axis',(-0.31481916961473,-0.949151668830167,6.13681984861663E-17));
#124113=DIRECTION('ref_axis',(0.949151668830167,-0.31481916961473,-1.72563323017096E-31));
#124114=DIRECTION('center_axis',(-1.96239249134894E-32,4.74145284482097E-32,
-1.));
#124115=DIRECTION('ref_axis',(0.953546398078931,-0.301246189537225,-3.29957689411567E-32));
#124116=DIRECTION('center_axis',(-0.287611893981001,-0.957747043034152,
-3.46966352979465E-16));
#124117=DIRECTION('ref_axis',(-0.957747043034152,0.287611893981001,7.88510670898555E-14));
#124118=DIRECTION('center_axis',(-1.90533007151413E-32,4.89934317587563E-32,
-1.));
#124119=DIRECTION('ref_axis',(0.925819190020902,-0.377966701428898,0.));
#124120=DIRECTION('center_axis',(1.90533007151413E-32,-4.89934317587563E-32,
1.));
#124121=DIRECTION('ref_axis',(-0.925819190020902,0.377966701428898,3.61577972288558E-32));
#124122=DIRECTION('center_axis',(-0.391136307302437,-0.920332759989458,
6.13681984861663E-17));
#124123=DIRECTION('ref_axis',(0.920332759989458,-0.391136307302437,2.61926472436664E-31));
#124124=DIRECTION('center_axis',(-1.90533007151413E-32,4.89934317587563E-32,
-1.));
#124125=DIRECTION('ref_axis',(0.925819190020902,-0.377966701428898,-3.61577972288558E-32));
#124126=DIRECTION('center_axis',(-0.364720164427122,-0.93111717933902,-3.46966352979465E-16));
#124127=DIRECTION('ref_axis',(-0.93111717933902,0.364720164427122,7.88510670898555E-14));
#124128=DIRECTION('center_axis',(-1.83558799441074E-32,5.05205702292055E-32,
-1.));
#124129=DIRECTION('ref_axis',(0.891930808002698,-0.452171907282677,0.));
#124130=DIRECTION('center_axis',(1.83558799441074E-32,-5.05205702292055E-32,
1.));
#124131=DIRECTION('ref_axis',(-0.891930808002698,0.452171907282677,3.92161574276965E-32));
#124132=DIRECTION('center_axis',(-0.464850497397995,-0.885389188475236,
6.13681984861663E-17));
#124133=DIRECTION('ref_axis',(0.885389188475236,-0.464850497397995,-2.8965986363584E-31));
#124134=DIRECTION('center_axis',(-1.83558799441074E-32,5.05205702292055E-32,
-1.));
#124135=DIRECTION('ref_axis',(0.891930808002698,-0.452171907282677,-3.92161574276965E-32));
#124136=DIRECTION('center_axis',(-0.439401282353573,-0.898290884438908,
-3.46966352979465E-16));
#124137=DIRECTION('ref_axis',(-0.898290884438908,0.439401282353573,1.57702134179708E-13));
#124138=DIRECTION('center_axis',(-1.75363038205524E-32,5.19857810049965E-32,
-1.));
#124139=DIRECTION('ref_axis',(0.852106773615461,-0.523367983696604,0.));
#124140=DIRECTION('center_axis',(1.75363038205524E-32,-5.19857810049965E-32,
1.));
#124141=DIRECTION('ref_axis',(-0.852106773615461,0.523367983696604,4.21504966551496E-32));
#124142=DIRECTION('center_axis',(-0.535471184128302,-0.844553497990645,
6.13681984861663E-17));
#124143=DIRECTION('ref_axis',(0.844553497990645,-0.535471184128302,-4.93038065763132E-32));
#124144=DIRECTION('center_axis',(-1.75363038205524E-32,5.19857810049965E-32,
-1.));
#124145=DIRECTION('ref_axis',(0.852106773615461,-0.523367983696604,-4.21504966551496E-32));
#124146=DIRECTION('center_axis',(-0.511158257242069,-0.859486611910419,
-3.46966352979465E-16));
#124147=DIRECTION('ref_axis',(-0.859486611910419,0.511158257242069,7.88510670898547E-14));
#124148=DIRECTION('center_axis',(-1.66000264883581E-32,5.33793133501592E-32,
-1.));
#124149=DIRECTION('ref_axis',(0.806612109237535,-0.59108113252867,0.));
#124150=DIRECTION('center_axis',(1.66000264883581E-32,-5.33793133501592E-32,
1.));
#124151=DIRECTION('ref_axis',(-0.806612109237535,0.59108113252867,4.49412873677883E-32));
#124152=DIRECTION('center_axis',(-0.602528398474762,-0.798097443318445,
6.13681984861663E-17));
#124153=DIRECTION('ref_axis',(0.798097443318445,-0.602528398474762,-2.65007960347684E-31));
#124154=DIRECTION('center_axis',(-1.66000264883581E-32,5.33793133501592E-32,
-1.));
#124155=DIRECTION('ref_axis',(0.806612109237535,-0.59108113252867,-4.49412873677883E-32));
#124156=DIRECTION('center_axis',(-0.579513558263796,-0.814962597784975,
-3.46966352979465E-16));
#124157=DIRECTION('ref_axis',(-0.814962597784975,0.579513558263796,7.88510670898541E-14));
#124158=DIRECTION('center_axis',(-1.55532787186954E-32,5.46918935368532E-32,
-1.));
#124159=DIRECTION('ref_axis',(0.755749574354264,-0.654860733945279,0.));
#124160=DIRECTION('center_axis',(1.55532787186954E-32,-5.46918935368532E-32,
1.));
#124161=DIRECTION('ref_axis',(-0.755749574354264,0.654860733945279,4.7569957313868E-32));
#124162=DIRECTION('center_axis',(-0.665575885739561,-0.74633018183777,6.13681984861663E-17));
#124163=DIRECTION('ref_axis',(0.74633018183777,-0.665575885739561,3.14311766923997E-31));
#124164=DIRECTION('center_axis',(-1.55532787186954E-32,5.46918935368532E-32,
-1.));
#124165=DIRECTION('ref_axis',(0.755749574354264,-0.654860733945279,-4.7569957313868E-32));
#124166=DIRECTION('center_axis',(-0.644012292168283,-0.765015142030636,
-3.46966352979465E-16));
#124167=DIRECTION('ref_axis',(-0.765015142030636,0.644012292168283,7.88510670898549E-14));
#124168=DIRECTION('center_axis',(-1.44030264452701E-32,5.59147865604965E-32,
-1.));
#124169=DIRECTION('ref_axis',(0.699857650743568,-0.714282345221898,0.));
#124170=DIRECTION('center_axis',(1.44030264452701E-32,-5.59147865604965E-32,
1.));
#124171=DIRECTION('ref_axis',(-0.699857650743568,0.714282345221898,5.00190131285975E-32));
#124172=DIRECTION('center_axis',(-0.724194075297055,-0.689596216132777,
6.13681984861663E-17));
#124173=DIRECTION('ref_axis',(0.689596216132777,-0.724194075297054,7.39557098644698E-32));
#124174=DIRECTION('center_axis',(-1.44030264452701E-32,5.59147865604965E-32,
-1.));
#124175=DIRECTION('ref_axis',(0.699857650743568,-0.714282345221898,-5.00190131285975E-32));
#124176=DIRECTION('center_axis',(-0.70422523052294,-0.709976636724697,-3.46966352979465E-16));
#124177=DIRECTION('ref_axis',(-0.709976636724697,0.704225230522939,7.88510670898545E-14));
#124178=DIRECTION('center_axis',(-1.31569244071836E-32,5.70398542697799E-32,
-1.));
#124179=DIRECTION('ref_axis',(0.639308289935558,-0.768950525339357,0.));
#124180=DIRECTION('center_axis',(1.31569244071836E-32,-5.70398542697799E-32,
1.));
#124181=DIRECTION('ref_axis',(-0.639308289935558,0.768950525339357,5.22721567495956E-32));
#124182=DIRECTION('center_axis',(-0.777992872767058,-0.628273101384788,
6.13681984861663E-17));
#124183=DIRECTION('ref_axis',(0.628273101384788,-0.777992872767058,-1.41748443906901E-31));
#124184=DIRECTION('center_axis',(-1.31569244071836E-32,5.70398542697799E-32,
-1.));
#124185=DIRECTION('ref_axis',(0.639308289935558,-0.768950525339357,-5.22721567495956E-32));
#124186=DIRECTION('center_axis',(-0.75975166615745,-0.650213354039255,-3.46966352979465E-16));
#124187=DIRECTION('ref_axis',(-0.650213354039255,0.75975166615745,7.88510670898545E-14));
#124188=DIRECTION('center_axis',(-1.18232652079071E-32,5.80596095247213E-32,
-1.));
#124189=DIRECTION('ref_axis',(0.57450443793647,-0.818501466578589,0.));
#124190=DIRECTION('center_axis',(1.18232652079071E-32,-5.80596095247213E-32,
1.));
#124191=DIRECTION('ref_axis',(-0.57450443793647,0.818501466578589,5.43143938778071E-32));
#124192=DIRECTION('center_axis',(-0.826614256028586,-0.562768932804849,
6.13681984861663E-17));
#124193=DIRECTION('ref_axis',(0.562768932804848,-0.826614256028586,-3.82104500966428E-31));
#124194=DIRECTION('center_axis',(-1.18232652079071E-32,5.80596095247213E-32,
-1.));
#124195=DIRECTION('ref_axis',(0.57450443793647,-0.818501466578589,-5.43143938778071E-32));
#124196=DIRECTION('center_axis',(-0.810222079803885,-0.586123008760335,
-3.46966352979465E-16));
#124197=DIRECTION('ref_axis',(-0.586123008760335,0.810222079803885,1.5770213417971E-13));
#124198=DIRECTION('center_axis',(-1.04109241293733E-32,5.89672660223468E-32,
-1.));
#124199=DIRECTION('ref_axis',(0.505877353689475,-0.862605415600977,0.));
#124200=DIRECTION('center_axis',(1.04109241293733E-32,-5.89672660223468E-32,
1.));
#124201=DIRECTION('ref_axis',(-0.505877353689475,0.862605415600977,5.61321337620891E-32));
#124202=DIRECTION('center_axis',(-0.869734657797995,-0.493519629827431,
6.13681984861663E-17));
#124203=DIRECTION('ref_axis',(0.493519629827431,-0.869734657797995,2.65007960347684E-31));
#124204=DIRECTION('center_axis',(-1.04109241293733E-32,5.89672660223468E-32,
-1.));
#124205=DIRECTION('ref_axis',(0.505877353689475,-0.862605415600977,-5.61321337620891E-32));
#124206=DIRECTION('center_axis',(-0.855300599186458,-0.518132111561603,
-3.46966352979465E-16));
#124207=DIRECTION('ref_axis',(-0.518132111561603,0.855300599186458,7.88510670898553E-14));
#124208=DIRECTION('center_axis',(-8.92930006844022E-33,5.97567834584174E-32,
-1.));
#124209=DIRECTION('ref_axis',(0.433883739117565,-0.900968867902416,0.));
#124210=DIRECTION('center_axis',(8.92930006844022E-33,-5.97567834584174E-32,
1.));
#124211=DIRECTION('ref_axis',(-0.433883739117565,0.900968867902416,5.77132796434177E-32));
#124212=DIRECTION('center_axis',(-0.907067118915877,-0.420986035138519,
6.13681984861663E-17));
#124213=DIRECTION('ref_axis',(0.420986035138519,-0.907067118915877,2.40356057059527E-31));
#124214=DIRECTION('center_axis',(-8.92930006844022E-33,5.97567834584174E-32,
-1.));
#124215=DIRECTION('ref_axis',(0.433883739117565,-0.900968867902416,-5.77132796434177E-32));
#124216=DIRECTION('center_axis',(-0.894687234196112,-0.44669313064621,-3.46966352979465E-16));
#124217=DIRECTION('ref_axis',(-0.44669313064621,0.894687234196112,7.88510670898555E-14));
#124218=DIRECTION('center_axis',(-7.38825298878243E-33,6.04229077246574E-32,
-1.));
#124219=DIRECTION('ref_axis',(0.359002699847606,-0.933336521037364,0.));
#124220=DIRECTION('center_axis',(7.38825298878243E-33,-6.04229077246574E-32,
1.));
#124221=DIRECTION('ref_axis',(-0.359002699847605,0.933336521037364,5.90473092568234E-32));
#124222=DIRECTION('center_axis',(-0.938363198012914,-0.345650847843566,
6.13681984861663E-17));
#124223=DIRECTION('ref_axis',(0.345650847843566,-0.938363198012914,-1.14015052707724E-31));
#124224=DIRECTION('center_axis',(-7.38825298878243E-33,6.04229077246574E-32,
-1.));
#124225=DIRECTION('ref_axis',(0.359002699847606,-0.933336521037364,-5.90473092568234E-32));
#124226=DIRECTION('center_axis',(-0.928119873275193,-0.372281480645545,
-3.46966352979465E-16));
#124227=DIRECTION('ref_axis',(-0.372281480645545,0.928119873275193,7.88510670898547E-14));
#124228=DIRECTION('center_axis',(-5.79803830446025E-33,6.09612058739776E-32,
-1.));
#124229=DIRECTION('ref_axis',(0.281732556841437,-0.959492973614495,0.));
#124230=DIRECTION('center_axis',(5.79803830446025E-33,-6.09612058739776E-32,
1.));
#124231=DIRECTION('ref_axis',(-0.281732556841437,0.959492973614495,6.01253448553284E-32));
#124232=DIRECTION('center_axis',(-0.963414624846205,-0.268015411184591,
6.13681984861663E-17));
#124233=DIRECTION('ref_axis',(0.268015411184591,-0.963414624846205,-6.16297582203915E-32));
#124234=DIRECTION('center_axis',(-5.79803830446025E-33,6.09612058739776E-32,
-1.));
#124235=DIRECTION('ref_axis',(0.281732556841437,-0.959492973614495,-6.01253448553284E-32));
#124236=DIRECTION('center_axis',(-0.955376027726628,-0.295392358813306,
-3.46966352979465E-16));
#124237=DIRECTION('ref_axis',(-0.295392358813306,0.955376027726628,1.35585468084861E-30));
#124238=DIRECTION('center_axis',(-4.16923863183086E-33,6.13680956210074E-32,
-1.));
#124239=DIRECTION('ref_axis',(0.202587530152088,-0.97926415875742,0.));
#124240=DIRECTION('center_axis',(4.16923863183086E-33,-6.13680956210074E-32,
1.));
#124241=DIRECTION('ref_axis',(-0.202587530152088,0.97926415875742,6.0940212289888E-32));
#124242=DIRECTION('center_axis',(-0.982054686303369,-0.188596376183613,
6.13681984861663E-17));
#124243=DIRECTION('ref_axis',(0.188596376183613,-0.982054686303369,4.62223186652937E-32));
#124244=DIRECTION('center_axis',(-4.16923863183086E-33,6.13680956210074E-32,
-1.));
#124245=DIRECTION('ref_axis',(0.202587530152088,-0.97926415875742,-6.0940212289888E-32));
#124246=DIRECTION('center_axis',(-0.976274312339492,-0.216537449569472,
-3.46966352979465E-16));
#124247=DIRECTION('ref_axis',(-0.216537449569472,0.976274312339492,7.88510670898554E-14));
#124248=DIRECTION('center_axis',(-2.51269336398259E-33,6.16408691816122E-32,
-1.));
#124249=DIRECTION('ref_axis',(0.122094316874167,-0.992518502491027,0.));
#124250=DIRECTION('center_axis',(2.51269336398259E-33,-6.16408691816122E-32,
1.));
#124251=DIRECTION('ref_axis',(-0.122094316874167,0.992518502491027,6.14864887521687E-32));
#124252=DIRECTION('center_axis',(-0.994159335850803,-0.107922263415344,
6.13681984861663E-17));
#124253=DIRECTION('ref_axis',(0.107922263415344,-0.994159335850803,4.16000867987643E-32));
#124254=DIRECTION('center_axis',(-2.51269336398259E-33,6.16408691816122E-32,
-1.));
#124255=DIRECTION('ref_axis',(0.122094316874167,-0.992518502491027,-6.14864887521687E-32));
#124256=DIRECTION('center_axis',(-0.99067565247766,-0.136241519324918,-3.46966352979465E-16));
#124257=DIRECTION('ref_axis',(-0.136241519324918,0.99067565247766,1.5770213417971E-13));
#124258=DIRECTION('center_axis',(-8.39426536362247E-34,6.17777112927507E-32,
-1.));
#124259=DIRECTION('ref_axis',(0.0407885860615926,-0.999167799344583,0.));
#124260=DIRECTION('center_axis',(8.39426536362247E-34,-6.17777112927507E-32,
1.));
#124261=DIRECTION('ref_axis',(-0.0407885860615926,0.999167799344583,6.17605388624435E-32));
#124262=DIRECTION('center_axis',(-0.999648019042894,-0.0265299457899662,
6.13681984861663E-17));
#124263=DIRECTION('ref_axis',(0.0265299457899662,-0.999648019042894,1.63704045272915E-32));
#124264=DIRECTION('center_axis',(-8.39426536362247E-34,6.17777112927507E-32,
-1.));
#124265=DIRECTION('ref_axis',(0.0407885860615926,-0.999167799344583,-6.17605388624435E-32));
#124266=DIRECTION('center_axis',(-0.998484209598567,-0.055038924247525,
-3.46966352979465E-16));
#124267=DIRECTION('ref_axis',(-0.055038924247525,0.998484209598567,7.88510670898542E-14));
#124268=DIRECTION('center_axis',(8.39426536361969E-34,6.17777112927507E-32,
-1.));
#124269=DIRECTION('ref_axis',(-0.0407885860615791,-0.999167799344583,0.));
#124270=DIRECTION('center_axis',(-8.39426536361969E-34,-6.17777112927507E-32,
1.));
#124271=DIRECTION('ref_axis',(0.0407885860615791,0.999167799344583,6.17605388624435E-32));
#124272=DIRECTION('center_axis',(-0.998484209598568,0.0550389242475112,
6.13681984861663E-17));
#124273=DIRECTION('ref_axis',(-0.0550389242475112,-0.998484209598568,-1.00148357108136E-32));
#124274=DIRECTION('center_axis',(8.39426536361969E-34,6.17777112927507E-32,
-1.));
#124275=DIRECTION('ref_axis',(-0.0407885860615791,-0.999167799344583,-6.17605388624435E-32));
#124276=DIRECTION('center_axis',(-0.999648019042894,0.0265299457899523,
-3.46966352979465E-16));
#124277=DIRECTION('ref_axis',(0.0265299457899523,0.999648019042894,7.88510670898553E-14));
#124278=DIRECTION('center_axis',(2.51269336398232E-33,6.16408691816122E-32,
-1.));
#124279=DIRECTION('ref_axis',(-0.122094316874153,-0.992518502491029,0.));
#124280=DIRECTION('center_axis',(-2.51269336398232E-33,-6.16408691816122E-32,
1.));
#124281=DIRECTION('ref_axis',(0.122094316874153,0.992518502491029,6.14864887521688E-32));
#124282=DIRECTION('center_axis',(-0.990675652477662,0.136241519324904,6.13681984861664E-17));
#124283=DIRECTION('ref_axis',(-0.136241519324904,-0.990675652477662,-5.54667823983524E-32));
#124284=DIRECTION('center_axis',(2.51269336398232E-33,6.16408691816122E-32,
-1.));
#124285=DIRECTION('ref_axis',(-0.122094316874153,-0.992518502491028,-6.14864887521688E-32));
#124286=DIRECTION('center_axis',(-0.994159335850804,0.10792226341533,-3.46966352979465E-16));
#124287=DIRECTION('ref_axis',(0.10792226341533,0.994159335850804,7.88510670898554E-14));
#124288=DIRECTION('center_axis',(4.16923863183059E-33,6.13680956210074E-32,
-1.));
#124289=DIRECTION('ref_axis',(-0.202587530152075,-0.979264158757422,0.));
#124290=DIRECTION('center_axis',(-4.16923863183059E-33,-6.13680956210074E-32,
1.));
#124291=DIRECTION('ref_axis',(0.202587530152075,0.979264158757422,6.09402122898881E-32));
#124292=DIRECTION('center_axis',(-0.976274312339495,0.216537449569458,6.13681984861664E-17));
#124293=DIRECTION('ref_axis',(-0.216537449569458,-0.976274312339495,1.38666955995881E-32));
#124294=DIRECTION('center_axis',(4.16923863183059E-33,6.13680956210074E-32,
-1.));
#124295=DIRECTION('ref_axis',(-0.202587530152075,-0.979264158757422,-6.09402122898881E-32));
#124296=DIRECTION('center_axis',(-0.982054686303372,0.188596376183599,-3.46966352979465E-16));
#124297=DIRECTION('ref_axis',(0.188596376183599,0.982054686303372,7.88510670898547E-14));
#124298=DIRECTION('center_axis',(5.79803830445998E-33,6.09612058739777E-32,
-1.));
#124299=DIRECTION('ref_axis',(-0.281732556841424,-0.959492973614499,0.));
#124300=DIRECTION('center_axis',(-5.79803830445998E-33,-6.09612058739777E-32,
1.));
#124301=DIRECTION('ref_axis',(0.281732556841424,0.959492973614499,6.01253448553286E-32));
#124302=DIRECTION('center_axis',(-0.955376027726632,0.295392358813292,6.13681984861664E-17));
#124303=DIRECTION('ref_axis',(-0.295392358813292,-0.955376027726632,1.32503980173842E-31));
#124304=DIRECTION('center_axis',(5.79803830445998E-33,6.09612058739777E-32,
-1.));
#124305=DIRECTION('ref_axis',(-0.281732556841424,-0.959492973614499,-6.01253448553286E-32));
#124306=DIRECTION('center_axis',(-0.963414624846209,0.268015411184578,-3.46966352979465E-16));
#124307=DIRECTION('ref_axis',(0.268015411184578,0.963414624846209,7.88510670898549E-14));
#124308=DIRECTION('center_axis',(7.38825298878218E-33,6.04229077246575E-32,
-1.));
#124309=DIRECTION('ref_axis',(-0.359002699847593,-0.933336521037369,0.));
#124310=DIRECTION('center_axis',(-7.38825298878218E-33,-6.04229077246575E-32,
1.));
#124311=DIRECTION('ref_axis',(0.359002699847593,0.933336521037369,5.90473092568236E-32));
#124312=DIRECTION('center_axis',(-0.928119873275198,0.372281480645533,6.13681984861664E-17));
#124313=DIRECTION('ref_axis',(-0.372281480645533,-0.928119873275198,-1.14015052707724E-31));
#124314=DIRECTION('center_axis',(7.38825298878218E-33,6.04229077246575E-32,
-1.));
#124315=DIRECTION('ref_axis',(-0.359002699847593,-0.933336521037369,-5.90473092568236E-32));
#124316=DIRECTION('center_axis',(-0.938363198012919,0.345650847843554,-3.46966352979465E-16));
#124317=DIRECTION('ref_axis',(0.345650847843554,0.938363198012919,7.88510670898547E-14));
#124318=DIRECTION('center_axis',(8.92930006843997E-33,5.97567834584175E-32,
-1.));
#124319=DIRECTION('ref_axis',(-0.433883739117553,-0.900968867902422,0.));
#124320=DIRECTION('center_axis',(-8.92930006843997E-33,-5.97567834584175E-32,
1.));
#124321=DIRECTION('ref_axis',(0.433883739117553,0.900968867902422,5.7713279643418E-32));
#124322=DIRECTION('center_axis',(-0.894687234196118,0.446693130646198,6.13681984861664E-17));
#124323=DIRECTION('ref_axis',(-0.446693130646198,-0.894687234196118,4.00593428432545E-32));
#124324=DIRECTION('center_axis',(8.92930006843997E-33,5.97567834584175E-32,
-1.));
#124325=DIRECTION('ref_axis',(-0.433883739117553,-0.900968867902422,-5.7713279643418E-32));
#124326=DIRECTION('center_axis',(-0.907067118915883,0.420986035138506,-3.46966352979465E-16));
#124327=DIRECTION('ref_axis',(0.420986035138506,0.907067118915883,7.88510670898557E-14));
#124328=DIRECTION('center_axis',(1.04109241293731E-32,5.89672660223469E-32,
-1.));
#124329=DIRECTION('ref_axis',(-0.505877353689464,-0.862605415600984,0.));
#124330=DIRECTION('center_axis',(-1.04109241293731E-32,-5.89672660223469E-32,
1.));
#124331=DIRECTION('ref_axis',(0.505877353689463,0.862605415600983,5.61321337620894E-32));
#124332=DIRECTION('center_axis',(-0.855300599186466,0.518132111561591,6.13681984861664E-17));
#124333=DIRECTION('ref_axis',(-0.518132111561591,-0.855300599186465,4.00593428432545E-32));
#124334=DIRECTION('center_axis',(1.04109241293731E-32,5.89672660223469E-32,
-1.));
#124335=DIRECTION('ref_axis',(-0.505877353689463,-0.862605415600984,-5.61321337620894E-32));
#124336=DIRECTION('center_axis',(-0.869734657798002,0.493519629827419,-3.46966352979465E-16));
#124337=DIRECTION('ref_axis',(0.493519629827419,0.869734657798002,2.95822839457879E-30));
#124338=DIRECTION('center_axis',(1.18232652079068E-32,5.80596095247215E-32,
-1.));
#124339=DIRECTION('ref_axis',(-0.574504437936459,-0.818501466578597,0.));
#124340=DIRECTION('center_axis',(-1.18232652079068E-32,-5.80596095247215E-32,
1.));
#124341=DIRECTION('ref_axis',(0.574504437936459,0.818501466578597,5.43143938778074E-32));
#124342=DIRECTION('center_axis',(-0.810222079803893,0.586123008760323,6.13681984861664E-17));
#124343=DIRECTION('ref_axis',(-0.586123008760323,-0.810222079803893,1.91052250483214E-31));
#124344=DIRECTION('center_axis',(1.18232652079068E-32,5.80596095247215E-32,
-1.));
#124345=DIRECTION('ref_axis',(-0.574504437936459,-0.818501466578597,-5.43143938778074E-32));
#124346=DIRECTION('center_axis',(-0.826614256028593,0.562768932804837,-3.46966352979465E-16));
#124347=DIRECTION('ref_axis',(0.562768932804837,0.826614256028593,7.8851067089855E-14));
#124348=DIRECTION('center_axis',(1.31569244071834E-32,5.70398542697801E-32,
-1.));
#124349=DIRECTION('ref_axis',(-0.639308289935547,-0.768950525339365,0.));
#124350=DIRECTION('center_axis',(-1.31569244071834E-32,-5.70398542697801E-32,
1.));
#124351=DIRECTION('ref_axis',(0.639308289935547,0.768950525339365,5.22721567495959E-32));
#124352=DIRECTION('center_axis',(-0.759751666157459,0.650213354039245,6.13681984861664E-17));
#124353=DIRECTION('ref_axis',(-0.650213354039245,-0.759751666157459,2.1570415377137E-31));
#124354=DIRECTION('center_axis',(1.31569244071834E-32,5.70398542697801E-32,
-1.));
#124355=DIRECTION('ref_axis',(-0.639308289935547,-0.768950525339365,-5.22721567495959E-32));
#124356=DIRECTION('center_axis',(-0.777992872767067,0.628273101384777,-3.46966352979465E-16));
#124357=DIRECTION('ref_axis',(0.628273101384777,0.777992872767067,7.88510670898555E-14));
#124358=DIRECTION('center_axis',(1.44030264452699E-32,5.59147865604967E-32,
-1.));
#124359=DIRECTION('ref_axis',(-0.699857650743558,-0.714282345221907,0.));
#124360=DIRECTION('center_axis',(-1.44030264452699E-32,-5.59147865604967E-32,
1.));
#124361=DIRECTION('ref_axis',(0.699857650743558,0.714282345221907,5.00190131285979E-32));
#124362=DIRECTION('center_axis',(-0.704225230522949,0.709976636724688,6.13681984861664E-17));
#124363=DIRECTION('ref_axis',(-0.709976636724688,-0.704225230522949,-8.0118685686509E-32));
#124364=DIRECTION('center_axis',(1.44030264452699E-32,5.59147865604967E-32,
-1.));
#124365=DIRECTION('ref_axis',(-0.699857650743558,-0.714282345221907,-5.00190131285979E-32));
#124366=DIRECTION('center_axis',(-0.724194075297064,0.689596216132768,-3.46966352979465E-16));
#124367=DIRECTION('ref_axis',(0.689596216132768,0.724194075297064,2.12006368278147E-30));
#124368=DIRECTION('center_axis',(1.55532787186952E-32,5.46918935368534E-32,
-1.));
#124369=DIRECTION('ref_axis',(-0.755749574354255,-0.654860733945289,0.));
#124370=DIRECTION('center_axis',(-1.55532787186952E-32,-5.46918935368534E-32,
1.));
#124371=DIRECTION('ref_axis',(0.755749574354255,0.654860733945289,4.75699573138684E-32));
#124372=DIRECTION('center_axis',(-0.644012292168293,0.765015142030627,6.13681984861664E-17));
#124373=DIRECTION('ref_axis',(-0.765015142030627,-0.644012292168293,-2.46519032881566E-32));
#124374=DIRECTION('center_axis',(1.55532787186952E-32,5.46918935368534E-32,
-1.));
#124375=DIRECTION('ref_axis',(-0.755749574354255,-0.654860733945289,-4.75699573138684E-32));
#124376=DIRECTION('center_axis',(-0.665575885739571,0.746330181837761,-3.46966352979465E-16));
#124377=DIRECTION('ref_axis',(0.746330181837761,0.665575885739571,7.88510670898554E-14));
#124378=DIRECTION('center_axis',(1.66000264883579E-32,5.33793133501594E-32,
-1.));
#124379=DIRECTION('ref_axis',(-0.806612109237527,-0.59108113252868,0.));
#124380=DIRECTION('center_axis',(-1.66000264883579E-32,-5.33793133501594E-32,
1.));
#124381=DIRECTION('ref_axis',(0.806612109237527,0.59108113252868,4.49412873677887E-32));
#124382=DIRECTION('center_axis',(-0.579513558263807,0.814962597784967,6.13681984861664E-17));
#124383=DIRECTION('ref_axis',(-0.814962597784967,-0.579513558263806,2.77333911991762E-31));
#124384=DIRECTION('center_axis',(1.66000264883579E-32,5.33793133501594E-32,
-1.));
#124385=DIRECTION('ref_axis',(-0.806612109237527,-0.59108113252868,-4.49412873677888E-32));
#124386=DIRECTION('center_axis',(-0.602528398474773,0.798097443318436,-3.46966352979465E-16));
#124387=DIRECTION('ref_axis',(0.798097443318437,0.602528398474773,7.88510670898551E-14));
#124388=DIRECTION('center_axis',(1.75363038205522E-32,5.19857810049967E-32,
-1.));
#124389=DIRECTION('ref_axis',(-0.852106773615454,-0.523367983696616,0.));
#124390=DIRECTION('center_axis',(-1.75363038205522E-32,-5.19857810049967E-32,
1.));
#124391=DIRECTION('ref_axis',(0.852106773615454,0.523367983696616,4.21504966551501E-32));
#124392=DIRECTION('center_axis',(-0.511158257242081,0.859486611910412,6.13681984861664E-17));
#124393=DIRECTION('ref_axis',(-0.859486611910412,-0.511158257242081,1.26341004351803E-31));
#124394=DIRECTION('center_axis',(1.75363038205522E-32,5.19857810049967E-32,
-1.));
#124395=DIRECTION('ref_axis',(-0.852106773615454,-0.523367983696616,-4.21504966551501E-32));
#124396=DIRECTION('center_axis',(-0.535471184128314,0.844553497990637,-3.46966352979465E-16));
#124397=DIRECTION('ref_axis',(0.844553497990637,0.535471184128314,7.88510670898547E-14));
#124398=DIRECTION('center_axis',(1.83558799441073E-32,5.05205702292057E-32,
-1.));
#124399=DIRECTION('ref_axis',(-0.891930808002692,-0.452171907282689,0.));
#124400=DIRECTION('center_axis',(-1.83558799441073E-32,-5.05205702292057E-32,
1.));
#124401=DIRECTION('ref_axis',(0.891930808002692,0.452171907282689,3.9216157427697E-32));
#124402=DIRECTION('center_axis',(-0.439401282353585,0.898290884438902,6.13681984861664E-17));
#124403=DIRECTION('ref_axis',(-0.898290884438902,-0.439401282353585,8.32001735975286E-32));
#124404=DIRECTION('center_axis',(1.83558799441073E-32,5.05205702292057E-32,
-1.));
#124405=DIRECTION('ref_axis',(-0.891930808002692,-0.452171907282689,-3.9216157427697E-32));
#124406=DIRECTION('center_axis',(-0.464850497398007,0.88538918847523,-3.46966352979465E-16));
#124407=DIRECTION('ref_axis',(0.88538918847523,0.464850497398007,-1.97215226305253E-31));
#124408=DIRECTION('center_axis',(1.90533007151412E-32,4.89934317587566E-32,
-1.));
#124409=DIRECTION('ref_axis',(-0.925819190020897,-0.37796670142891,0.));
#124410=DIRECTION('center_axis',(-1.90533007151412E-32,-4.89934317587566E-32,
1.));
#124411=DIRECTION('ref_axis',(0.925819190020897,0.37796670142891,3.61577972288563E-32));
#124412=DIRECTION('center_axis',(-0.364720164427135,0.931117179339015,6.13681984861664E-17));
#124413=DIRECTION('ref_axis',(-0.931117179339015,-0.364720164427135,-2.24948617504429E-31));
#124414=DIRECTION('center_axis',(1.90533007151412E-32,4.89934317587566E-32,
-1.));
#124415=DIRECTION('ref_axis',(-0.925819190020897,-0.37796670142891,-3.61577972288563E-32));
#124416=DIRECTION('center_axis',(-0.39113630730245,0.920332759989453,-3.46966352979465E-16));
#124417=DIRECTION('ref_axis',(0.920332759989453,0.39113630730245,7.8851067089854E-14));
#124418=DIRECTION('center_axis',(1.96239249134893E-32,4.74145284482099E-32,
-1.));
#124419=DIRECTION('ref_axis',(-0.953546398078926,-0.301246189537238,0.));
#124420=DIRECTION('center_axis',(-1.96239249134893E-32,-4.74145284482099E-32,
1.));
#124421=DIRECTION('ref_axis',(0.953546398078926,0.301246189537238,3.29957689411572E-32));
#124422=DIRECTION('center_axis',(-0.287611893981014,0.957747043034148,6.13681984861664E-17));
#124423=DIRECTION('ref_axis',(-0.957747043034148,-0.287611893981014,3.69778549322349E-32));
#124424=DIRECTION('center_axis',(1.96239249134893E-32,4.74145284482099E-32,
-1.));
#124425=DIRECTION('ref_axis',(-0.953546398078926,-0.301246189537238,-3.29957689411572E-32));
#124426=DIRECTION('center_axis',(-0.314819169614744,0.949151668830163,-3.46966352979465E-16));
#124427=DIRECTION('ref_axis',(0.949151668830163,0.314819169614744,7.88510670898548E-14));
#124428=DIRECTION('center_axis',(2.00639551292578E-32,4.57943676385968E-32,
-1.));
#124429=DIRECTION('ref_axis',(-0.974927912181823,-0.222520933956318,0.));
#124430=DIRECTION('center_axis',(-2.00639551292578E-32,-4.57943676385968E-32,
1.));
#124431=DIRECTION('ref_axis',(0.974927912181823,0.222520933956318,2.97511153411567E-32));
#124432=DIRECTION('center_axis',(-0.208589613833072,0.978003258175028,6.13681984861664E-17));
#124433=DIRECTION('ref_axis',(-0.978003258175028,-0.208589613833072,-5.0844550531823E-32));
#124434=DIRECTION('center_axis',(2.00639551292578E-32,4.57943676385968E-32,
-1.));
#124435=DIRECTION('ref_axis',(-0.974927912181823,-0.222520933956318,-2.97511153411566E-32));
#124436=DIRECTION('center_axis',(-0.236406962294758,0.971654129913811,-3.46966352979465E-16));
#124437=DIRECTION('ref_axis',(0.971654129913811,0.236406962294758,1.5770213417971E-13));
#124438=DIRECTION('center_axis',(2.03704630339607E-32,4.41437312327975E-32,
-1.));
#124439=DIRECTION('ref_axis',(-0.989821441880932,-0.142314838273289,0.));
#124440=DIRECTION('center_axis',(-2.03704630339607E-32,-4.41437312327975E-32,
1.));
#124441=DIRECTION('ref_axis',(0.989821441880932,0.142314838273289,2.64454290632323E-32));
#124442=DIRECTION('center_axis',(-0.128179204219934,0.991751022991933,6.13681984861664E-17));
#124443=DIRECTION('ref_axis',(-0.991751022991932,-0.128179204219934,4.16000867987643E-32));
#124444=DIRECTION('center_axis',(2.03704630339607E-32,4.41437312327975E-32,
-1.));
#124445=DIRECTION('ref_axis',(-0.989821441880932,-0.142314838273289,-2.64454290632323E-32));
#124446=DIRECTION('center_axis',(-0.156421505645104,0.98769039307453,-3.46966352979465E-16));
#124447=DIRECTION('ref_axis',(0.98769039307453,0.156421505645104,7.88510670898555E-14));
#124448=DIRECTION('center_axis',(2.05414088680624E-32,4.24736039437567E-32,
-1.));
#124449=DIRECTION('ref_axis',(-0.998127873193367,-0.0611616608218463,0.));
#124450=DIRECTION('center_axis',(-2.05414088680624E-32,-4.24736039437567E-32,
1.));
#124451=DIRECTION('ref_axis',(0.998127873193367,0.0611616608218462,2.3100708904164E-32));
#124452=DIRECTION('center_axis',(-0.0469157831507927,0.998898848378227,
6.13681984861664E-17));
#124453=DIRECTION('ref_axis',(-0.998898848378227,-0.0469157831507927,-3.58222969656026E-32));
#124454=DIRECTION('center_axis',(2.05414088680624E-32,4.24736039437567E-32,
-1.));
#124455=DIRECTION('ref_axis',(-0.998127873193367,-0.0611616608218463,-2.3100708904164E-32));
#124456=DIRECTION('center_axis',(-0.0753950896831134,0.997153739626782,
-3.46966352979465E-16));
#124457=DIRECTION('ref_axis',(0.997153739626782,0.0753950896831134,7.88510670898542E-14));
#124458=DIRECTION('center_axis',(2.0575655015241E-32,4.07951001930313E-32,
-1.));
#124459=DIRECTION('ref_axis',(-0.999791928189207,0.0203985373914021,0.));
#124460=DIRECTION('center_axis',(-2.0575655015241E-32,-4.07951001930313E-32,
1.));
#124461=DIRECTION('ref_axis',(0.999791928189207,-0.0203985373914021,1.97392134247702E-32));
#124462=DIRECTION('center_axis',(0.0346598547146579,0.999399166735274,6.13681984861664E-17));
#124463=DIRECTION('ref_axis',(-0.999399166735273,0.0346598547146579,-2.1570415377137E-32));
#124464=DIRECTION('center_axis',(2.0575655015241E-32,4.07951001930313E-32,
-1.));
#124465=DIRECTION('ref_axis',(-0.999791928189207,0.0203985373914021,-1.97392134247702E-32));
#124466=DIRECTION('center_axis',(0.00613306816140406,0.999981192560604,
-3.46966352979465E-16));
#124467=DIRECTION('ref_axis',(0.999981192560604,-0.00613306816140406,7.88510670898547E-14));
#124468=DIRECTION('center_axis',(2.04729735730374E-32,3.9119390146149E-32,
-1.));
#124469=DIRECTION('ref_axis',(-0.994802532857004,0.101822986703832,0.));
#124470=DIRECTION('center_axis',(-2.04729735730374E-32,-3.9119390146149E-32,
1.));
#124471=DIRECTION('ref_axis',(0.994802532857004,-0.101822986703832,1.63833128228587E-32));
#124472=DIRECTION('center_axis',(0.116004836965456,0.993248648526953,6.13681984861664E-17));
#124473=DIRECTION('ref_axis',(-0.993248648526953,0.116004836965456,-7.39557098644699E-32));
#124474=DIRECTION('center_axis',(2.04729735730374E-32,3.9119390146149E-32,
-1.));
#124475=DIRECTION('ref_axis',(-0.994802532857004,0.101822986703832,-1.63833128228587E-32));
#124476=DIRECTION('center_axis',(0.0876204114491922,0.996153935643219,-3.46966352979465E-16));
#124477=DIRECTION('ref_axis',(0.996153935643219,-0.0876204114491922,7.88510670898545E-14));
#124478=DIRECTION('center_axis',(2.0234047869508E-32,3.74576253769989E-32,
-1.));
#124479=DIRECTION('ref_axis',(-0.983192890799504,0.182569820839359,0.));
#124480=DIRECTION('center_axis',(-2.0234047869508E-32,-3.74576253769989E-32,
1.));
#124481=DIRECTION('ref_axis',(0.983192890799504,-0.182569820839359,1.30553400632506E-32));
#124482=DIRECTION('center_axis',(0.1965778261657,0.980488224437177,6.13681984861664E-17));
#124483=DIRECTION('ref_axis',(-0.980488224437177,0.1965778261657,5.54667823983524E-32));
#124484=DIRECTION('center_axis',(2.0234047869508E-32,3.74576253769989E-32,
-1.));
#124485=DIRECTION('ref_axis',(-0.983192890799503,0.182569820839359,-1.30553400632506E-32));
#124486=DIRECTION('center_axis',(0.168524655355137,0.985697438637959,-3.46966352979465E-16));
#124487=DIRECTION('ref_axis',(0.985697438637959,-0.168524655355137,7.88510670898548E-14));
#124488=DIRECTION('center_axis',(1.986046791579E-32,3.58208646559478E-32,
-1.));
#124489=DIRECTION('ref_axis',(-0.965040262269141,0.262101682939099,0.));
#124490=DIRECTION('center_axis',(-1.986046791579E-32,-3.58208646559478E-32,
1.));
#124491=DIRECTION('ref_axis',(0.965040262269141,-0.262101682939099,9.77744225558421E-33));
#124492=DIRECTION('center_axis',(0.275842622365869,0.961202812982942,6.13681984861664E-17));
#124493=DIRECTION('ref_axis',(-0.961202812982942,0.275842622365869,1.41748443906901E-31));
#124494=DIRECTION('center_axis',(1.986046791579E-32,3.58208646559478E-32,
-1.));
#124495=DIRECTION('ref_axis',(-0.965040262269141,0.2621016829391,-9.77744225558421E-33));
#124496=DIRECTION('center_axis',(0.248307395484303,0.968681287807193,-3.46966352979465E-16));
#124497=DIRECTION('ref_axis',(0.968681287807193,-0.248307395484303,1.57702134179711E-13));
#124498=DIRECTION('center_axis',(1.9354719824839E-32,3.42200003555479E-32,
-1.));
#124499=DIRECTION('ref_axis',(-0.940465450013813,0.339889301582614,0.));
#124500=DIRECTION('center_axis',(-1.9354719824839E-32,-3.42200003555479E-32,
1.));
#124501=DIRECTION('ref_axis',(0.940465450013812,-0.339889301582614,6.57143326895444E-33));
#124502=DIRECTION('center_axis',(0.353271731425022,0.935520755395607,6.13681984861664E-17));
#124503=DIRECTION('ref_axis',(-0.935520755395607,0.353271731425022,9.24446373305873E-33));
#124504=DIRECTION('center_axis',(1.9354719824839E-32,3.42200003555479E-32,
-1.));
#124505=DIRECTION('ref_axis',(-0.940465450013812,0.339889301582614,-6.57143326895444E-33));
#124506=DIRECTION('center_axis',(0.326437690864358,0.945218722827233,-3.46966352979465E-16));
#124507=DIRECTION('ref_axis',(0.945218722827233,-0.326437690864358,7.88510670898542E-14));
#124508=DIRECTION('center_axis',(1.87201692667576E-32,3.26656859635943E-32,
-1.));
#124509=DIRECTION('ref_axis',(-0.909631995354519,0.415415013001884,0.));
#124510=DIRECTION('center_axis',(-1.87201692667576E-32,-3.26656859635943E-32,
1.));
#124511=DIRECTION('ref_axis',(0.909631995354519,-0.415415013001884,3.45864856421308E-33));
#124512=DIRECTION('center_axis',(0.428349875397276,0.903612961531174,6.13681984861664E-17));
#124513=DIRECTION('ref_axis',(-0.903612961531174,0.428349875397276,9.55261252416069E-32));
#124514=DIRECTION('center_axis',(1.87201692667576E-32,3.26656859635943E-32,
-1.));
#124515=DIRECTION('ref_axis',(-0.909631995354519,0.415415013001884,-3.45864856421309E-33));
#124516=DIRECTION('center_axis',(0.402395597270139,0.91546588319697,-3.46966352979465E-16));
#124517=DIRECTION('ref_axis',(0.91546588319697,-0.402395597270139,7.88510670898551E-14));
#124518=DIRECTION('center_axis',(1.79610390708165E-32,3.11682651859216E-32,
-1.));
#124519=DIRECTION('ref_axis',(-0.872745089844857,0.488176206048279,0.));
#124520=DIRECTION('center_axis',(-1.79610390708165E-32,-3.11682651859216E-32,
1.));
#124521=DIRECTION('ref_axis',(0.872745089844857,-0.488176206048279,4.59803209996904E-34));
#124522=DIRECTION('center_axis',(0.500577421621515,0.865691772493395,6.13681984861664E-17));
#124523=DIRECTION('ref_axis',(-0.865691772493395,0.500577421621515,3.57452597678271E-31));
#124524=DIRECTION('center_axis',(1.79610390708165E-32,3.11682651859216E-32,
-1.));
#124525=DIRECTION('ref_axis',(-0.872745089844857,0.488176206048279,-4.59803209996901E-34));
#124526=DIRECTION('center_axis',(0.475675627366687,0.87962076915527,-3.46966352979465E-16));
#124527=DIRECTION('ref_axis',(0.87962076915527,-0.475675627366688,1.57702134179709E-13));
#124528=DIRECTION('center_axis',(1.7082381123222E-32,2.97377031107481E-32,
-1.));
#124529=DIRECTION('ref_axis',(-0.830050209755082,0.557688666986828,0.));
#124530=DIRECTION('center_axis',(-1.7082381123222E-32,-2.97377031107481E-32,
1.));
#124531=DIRECTION('ref_axis',(0.830050209755082,-0.557688666986828,-2.40514597263651E-33));
#124532=DIRECTION('center_axis',(0.569473707694324,0.822009547538762,6.13681984861664E-17));
#124533=DIRECTION('ref_axis',(-0.822009547538762,0.569473707694324,3.38963670212154E-31));
#124534=DIRECTION('center_axis',(1.7082381123222E-32,2.97377031107481E-32,
-1.));
#124535=DIRECTION('ref_axis',(-0.830050209755082,0.557688666986828,2.40514597263651E-33));
#124536=DIRECTION('center_axis',(0.545790114644065,0.837921924022053,-3.46966352979465E-16));
#124537=DIRECTION('ref_axis',(0.837921924022053,-0.545790114644065,7.8851067089855E-14));
#124538=DIRECTION('center_axis',(1.60900427476469E-32,2.83835198926582E-32,
-1.));
#124539=DIRECTION('ref_axis',(-0.781831482468031,0.623489801858732,0.));
#124540=DIRECTION('center_axis',(-1.60900427476469E-32,-2.83835198926582E-32,
1.));
#124541=DIRECTION('ref_axis',(0.781831482468031,-0.623489801858732,-5.11713321956004E-33));
#124542=DIRECTION('center_axis',(0.634580240198975,0.772856984667287,6.13681984861664E-17));
#124543=DIRECTION('ref_axis',(-0.772856984667287,0.634580240198975,9.24446373305873E-32));
#124544=DIRECTION('center_axis',(1.60900427476469E-32,2.83835198926582E-32,
-1.));
#124545=DIRECTION('ref_axis',(-0.781831482468031,0.623489801858732,5.11713321956004E-33));
#124546=DIRECTION('center_axis',(0.612272458757516,0.790646846731855,-3.46966352979465E-16));
#124547=DIRECTION('ref_axis',(0.790646846731855,-0.612272458757516,7.8851067089855E-14));
#124548=DIRECTION('center_axis',(1.49906277922564E-32,2.71147273975435E-32,
-1.));
#124549=DIRECTION('ref_axis',(-0.72840979565827,0.685141714967843,0.));
#124550=DIRECTION('center_axis',(-1.49906277922564E-32,-2.71147273975435E-32,
1.));
#124551=DIRECTION('ref_axis',(0.72840979565827,-0.685141714967843,-7.6581107030918E-33));
#124552=DIRECTION('center_axis',(0.695463745903472,0.718561186075278,6.13681984861664E-17));
#124553=DIRECTION('ref_axis',(-0.718561186075278,0.695463745903472,3.45126646034192E-31));
#124554=DIRECTION('center_axis',(1.49906277922564E-32,2.71147273975435E-32,
-1.));
#124555=DIRECTION('ref_axis',(-0.72840979565827,0.685141714967843,7.6581107030918E-33));
#124556=DIRECTION('center_axis',(0.674680230675781,0.738110145124205,-3.46966352979465E-16));
#124557=DIRECTION('ref_axis',(0.738110145124205,-0.674680230675781,7.88510670898546E-14));
#124558=DIRECTION('center_axis',(1.3791452682188E-32,2.59397692301231E-32,
-1.));
#124559=DIRECTION('ref_axis',(-0.670140661837561,0.742234123004269,0.));
#124560=DIRECTION('center_axis',(-1.3791452682188E-32,-2.59397692301231E-32,
1.));
#124561=DIRECTION('ref_axis',(0.670140661837561,-0.742234123004269,-1.00111686373107E-32));
#124562=DIRECTION('center_axis',(0.751719055122423,0.659483481344189,6.13681984861664E-17));
#124563=DIRECTION('ref_axis',(-0.659483481344189,0.751719055122423,-1.66400347195057E-31));
#124564=DIRECTION('center_axis',(1.3791452682188E-32,2.59397692301231E-32,
-1.));
#124565=DIRECTION('ref_axis',(-0.670140661837561,0.742234123004269,1.00111686373107E-32));
#124566=DIRECTION('center_axis',(0.732598116973302,0.680661442280354,-3.46966352979465E-16));
#124567=DIRECTION('ref_axis',(0.680661442280354,-0.732598116973302,-7.64209001932855E-31));
#124568=DIRECTION('center_axis',(1.25004977299491E-32,2.48664645431468E-32,
-1.));
#124569=DIRECTION('ref_axis',(-0.607411852477749,0.794387085412112,0.));
#124570=DIRECTION('center_axis',(-1.25004977299491E-32,-2.48664645431468E-32,
1.));
#124571=DIRECTION('ref_axis',(0.607411852477749,-0.794387085412112,-1.21606478098917E-32));
#124572=DIRECTION('center_axis',(0.802971798054448,0.59601702285187,6.13681984861664E-17));
#124573=DIRECTION('ref_axis',(-0.59601702285187,0.802971798054448,8.0118685686509E-32));
#124574=DIRECTION('center_axis',(1.25004977299491E-32,2.48664645431468E-32,
-1.));
#124575=DIRECTION('ref_axis',(-0.607411852477749,0.794387085412112,1.21606478098917E-32));
#124576=DIRECTION('center_axis',(0.785640683672546,0.618683049839362,-3.46966352979465E-16));
#124577=DIRECTION('ref_axis',(0.618683049839362,-0.785640683672546,7.88510670898545E-14));
#124578=DIRECTION('center_axis',(1.11263540277544E-32,2.39019560022234E-32,
-1.));
#124579=DIRECTION('ref_axis',(-0.540640817455599,0.841253532831181,0.));
#124580=DIRECTION('center_axis',(-1.11263540277544E-32,-2.39019560022234E-32,
1.));
#124581=DIRECTION('ref_axis',(0.540640817455599,-0.841253532831181,-1.40922437915804E-32));
#124582=DIRECTION('center_axis',(0.848880896151442,0.528584169408359,6.13681984861664E-17));
#124583=DIRECTION('ref_axis',(-0.528584169408359,0.848880896151442,4.62223186652936E-32));
#124584=DIRECTION('center_axis',(1.11263540277544E-32,2.39019560022234E-32,
-1.));
#124585=DIRECTION('ref_axis',(-0.540640817455599,0.841253532831181,1.40922437915804E-32));
#124586=DIRECTION('center_axis',(0.833454941243539,0.552587423777206,-3.46966352979465E-16));
#124587=DIRECTION('ref_axis',(0.552587423777206,-0.833454941243539,1.57702134179709E-13));
#124588=DIRECTION('center_axis',(9.67816627522413E-33,2.30526622525603E-32,
-1.));
#124589=DIRECTION('ref_axis',(-0.470271906992738,0.882521576786321,0.));
#124590=DIRECTION('center_axis',(-9.67816627522413E-33,-2.30526622525603E-32,
1.));
#124591=DIRECTION('ref_axis',(0.470271906992738,-0.882521576786321,-1.57931021298095E-32));
#124592=DIRECTION('center_axis',(0.889140831940038,0.457633675527684,6.13681984861664E-17));
#124593=DIRECTION('ref_axis',(-0.457633675527684,0.889140831940038,1.4791141972894E-31));
#124594=DIRECTION('center_axis',(9.67816627522413E-33,2.30526622525603E-32,
-1.));
#124595=DIRECTION('ref_axis',(-0.470271906992738,0.882521576786321,1.57931021298095E-32));
#124596=DIRECTION('center_axis',(0.875722693690941,0.48281441958032,-3.46966352979465E-16));
#124597=DIRECTION('ref_axis',(0.48281441958032,-0.875722693690941,7.88510670898549E-14));
#124598=DIRECTION('center_axis',(8.1655719229173E-33,2.23242352039377E-32,
-1.));
#124599=DIRECTION('ref_axis',(-0.396773414578243,0.917916585253759,0.));
#124600=DIRECTION('center_axis',(-8.1655719229173E-33,-2.23242352039377E-32,
1.));
#124601=DIRECTION('ref_axis',(0.396773414578243,-0.917916585253759,-1.72519038929601E-32));
#124602=DIRECTION('center_axis',(0.923483682189984,0.383637705040614,6.13681984861663E-17));
#124603=DIRECTION('ref_axis',(-0.383637705040614,0.923483682189984,5.54667823983524E-32));
#124604=DIRECTION('center_axis',(8.1655719229173E-33,2.23242352039377E-32,
-1.));
#124605=DIRECTION('ref_axis',(-0.396773414578243,0.917916585253759,1.72519038929601E-32));
#124606=DIRECTION('center_axis',(0.912162656095905,0.4098283650799,-3.46966352979465E-16));
#124607=DIRECTION('ref_axis',(0.4098283650799,-0.912162656095905,7.88510670898547E-14));
#124608=DIRECTION('center_axis',(6.598637036688E-33,2.17215224181823E-32,
-1.));
#124609=DIRECTION('ref_axis',(-0.320634460552736,0.94720301029191,0.));
#124610=DIRECTION('center_axis',(-6.598637036688E-33,-2.17215224181823E-32,
1.));
#124611=DIRECTION('ref_axis',(0.320634460552736,-0.94720301029191,-1.84589409959837E-32));
#124612=DIRECTION('center_axis',(0.951680900899038,0.307088688922265,6.13681984861664E-17));
#124613=DIRECTION('ref_axis',(-0.307088688922265,0.951680900899038,9.24446373305873E-33));
#124614=DIRECTION('center_axis',(6.598637036688E-33,2.17215224181823E-32,
-1.));
#124615=DIRECTION('ref_axis',(-0.320634460552736,0.94720301029191,1.84589409959837E-32));
#124616=DIRECTION('center_axis',(0.942532326520795,0.334114970426793,-3.46966352979465E-16));
#124617=DIRECTION('ref_axis',(0.334114970426793,-0.942532326520795,7.88510670898544E-14));
#124618=DIRECTION('center_axis',(4.98778930967801E-33,2.12485348494426E-32,
-1.));
#124619=DIRECTION('ref_axis',(-0.242361737093213,0.970185955574064,0.));
#124620=DIRECTION('center_axis',(-4.98778930967801E-33,-2.12485348494426E-32,
1.));
#124621=DIRECTION('ref_axis',(0.242361737093213,-0.970185955574064,-1.94061808061067E-32));
#124622=DIRECTION('center_axis',(0.973544840228905,0.228496048245205,6.13681984861664E-17));
#124623=DIRECTION('ref_axis',(-0.228496048245205,0.973544840228905,7.08742219534502E-32));
#124624=DIRECTION('center_axis',(4.98778930967801E-33,2.12485348494426E-32,
-1.));
#124625=DIRECTION('ref_axis',(-0.242361737093213,0.970185955574064,1.94061808061067E-32));
#124626=DIRECTION('center_axis',(0.966629599819577,0.256178095770586,-3.46966352979465E-16));
#124627=DIRECTION('ref_axis',(0.256178095770586,-0.966629599819577,7.88510670898549E-14));
#124628=DIRECTION('center_axis',(3.34374866773943E-33,2.09084201519512E-32,
-1.));
#124629=DIRECTION('ref_axis',(-0.162476136260206,0.986712473391289,0.));
#124630=DIRECTION('center_axis',(-3.34374866773943E-33,-2.09084201519512E-32,
1.));
#124631=DIRECTION('ref_axis',(0.162476136260206,-0.986712473391289,-2.00873195986765E-32));
#124632=DIRECTION('center_axis',(0.988929999270642,0.148382804066268,6.13681984861664E-17));
#124633=DIRECTION('ref_axis',(-0.148382804066268,0.988929999270642,-4.46815747097839E-32));
#124634=DIRECTION('center_axis',(3.34374866773943E-33,2.09084201519512E-32,
-1.));
#124635=DIRECTION('ref_axis',(-0.162476136260206,0.986712473391289,2.00873195986765E-32));
#124636=DIRECTION('center_axis',(0.984294112614218,0.176536398153437,-3.46966352979465E-16));
#124637=DIRECTION('ref_axis',(0.176536398153437,-0.984294112614218,7.88510670898552E-14));
#124638=DIRECTION('center_axis',(-1.60900427476467E-32,2.8383519892658E-32,
-1.));
#124639=DIRECTION('ref_axis',(0.781831482468023,0.623489801858742,0.));
#124640=DIRECTION('center_axis',(1.60900427476467E-32,-2.8383519892658E-32,
1.));
#124641=DIRECTION('ref_axis',(-0.781831482468023,-0.623489801858742,-5.11713321956047E-33));
#124642=DIRECTION('center_axis',(0.612272458757527,-0.790646846731847,6.13681984861663E-17));
#124643=DIRECTION('ref_axis',(0.790646846731847,0.612272458757527,-5.23852944873328E-31));
#124644=DIRECTION('center_axis',(-1.60900427476467E-32,2.8383519892658E-32,
-1.));
#124645=DIRECTION('ref_axis',(0.781831482468023,0.623489801858742,5.11713321956047E-33));
#124646=DIRECTION('center_axis',(0.634580240198986,-0.772856984667278,-3.46966352979465E-16));
#124647=DIRECTION('ref_axis',(-0.772856984667278,-0.634580240198986,7.88510670898554E-14));
#124648=DIRECTION('center_axis',(-1.49906277922563E-32,2.71147273975433E-32,
-1.));
#124649=DIRECTION('ref_axis',(0.728409795658261,0.685141714967852,0.));
#124650=DIRECTION('center_axis',(1.49906277922563E-32,-2.71147273975433E-32,
1.));
#124651=DIRECTION('ref_axis',(-0.728409795658261,-0.685141714967852,-7.6581107030922E-33));
#124652=DIRECTION('center_axis',(0.674680230675791,-0.738110145124195,6.13681984861663E-17));
#124653=DIRECTION('ref_axis',(0.738110145124195,0.674680230675791,2.09541177949331E-31));
#124654=DIRECTION('center_axis',(-1.49906277922563E-32,2.71147273975433E-32,
-1.));
#124655=DIRECTION('ref_axis',(0.728409795658261,0.685141714967853,7.65811070309221E-33));
#124656=DIRECTION('center_axis',(0.695463745903482,-0.718561186075269,-3.46966352979465E-16));
#124657=DIRECTION('ref_axis',(-0.718561186075269,-0.695463745903482,7.8851067089855E-14));
#124658=DIRECTION('center_axis',(-1.37914526821878E-32,2.59397692301229E-32,
-1.));
#124659=DIRECTION('ref_axis',(0.670140661837551,0.742234123004278,0.));
#124660=DIRECTION('center_axis',(1.37914526821878E-32,-2.59397692301229E-32,
1.));
#124661=DIRECTION('ref_axis',(-0.670140661837551,-0.742234123004278,-1.0011168637311E-32));
#124662=DIRECTION('center_axis',(0.732598116973311,-0.680661442280345,6.13681984861663E-17));
#124663=DIRECTION('ref_axis',(0.680661442280345,0.732598116973311,5.79319727271681E-31));
#124664=DIRECTION('center_axis',(-1.37914526821878E-32,2.59397692301229E-32,
-1.));
#124665=DIRECTION('ref_axis',(0.670140661837551,0.742234123004278,1.00111686373111E-32));
#124666=DIRECTION('center_axis',(0.751719055122432,-0.659483481344179,-3.46966352979465E-16));
#124667=DIRECTION('ref_axis',(-0.659483481344179,-0.751719055122432,7.88510670898551E-14));
#124668=DIRECTION('center_axis',(-1.25004977299489E-32,2.48664645431466E-32,
-1.));
#124669=DIRECTION('ref_axis',(0.607411852477738,0.79438708541212,0.));
#124670=DIRECTION('center_axis',(1.25004977299489E-32,-2.48664645431466E-32,
1.));
#124671=DIRECTION('ref_axis',(-0.607411852477738,-0.79438708541212,-1.2160647809892E-32));
#124672=DIRECTION('center_axis',(0.785640683672555,-0.61868304983935,6.13681984861663E-17));
#124673=DIRECTION('ref_axis',(0.61868304983935,0.785640683672555,9.24446373305873E-32));
#124674=DIRECTION('center_axis',(-1.25004977299489E-32,2.48664645431466E-32,
-1.));
#124675=DIRECTION('ref_axis',(0.607411852477738,0.79438708541212,1.2160647809892E-32));
#124676=DIRECTION('center_axis',(0.802971798054457,-0.596017022851859,-3.46966352979465E-16));
#124677=DIRECTION('ref_axis',(-0.596017022851859,-0.802971798054457,7.88510670898544E-14));
#124678=DIRECTION('center_axis',(-1.11263540277541E-32,2.39019560022233E-32,
-1.));
#124679=DIRECTION('ref_axis',(0.540640817455587,0.841253532831188,0.));
#124680=DIRECTION('center_axis',(1.11263540277541E-32,-2.39019560022233E-32,
1.));
#124681=DIRECTION('ref_axis',(-0.540640817455587,-0.841253532831188,-1.40922437915807E-32));
#124682=DIRECTION('center_axis',(0.833454941243547,-0.552587423777194,6.13681984861663E-17));
#124683=DIRECTION('ref_axis',(0.552587423777194,0.833454941243547,9.86076131526265E-32));
#124684=DIRECTION('center_axis',(-1.11263540277541E-32,2.39019560022233E-32,
-1.));
#124685=DIRECTION('ref_axis',(0.540640817455587,0.841253532831188,1.40922437915807E-32));
#124686=DIRECTION('center_axis',(0.84888089615145,-0.528584169408347,-3.46966352979465E-16));
#124687=DIRECTION('ref_axis',(-0.528584169408346,-0.84888089615145,7.8851067089855E-14));
#124688=DIRECTION('center_axis',(-9.67816627522388E-33,2.30526622525602E-32,
-1.));
#124689=DIRECTION('ref_axis',(0.470271906992726,0.882521576786327,0.));
#124690=DIRECTION('center_axis',(9.67816627522388E-33,-2.30526622525602E-32,
1.));
#124691=DIRECTION('ref_axis',(-0.470271906992726,-0.882521576786327,-1.57931021298098E-32));
#124692=DIRECTION('center_axis',(0.875722693690948,-0.482814419580308,6.13681984861663E-17));
#124693=DIRECTION('ref_axis',(0.482814419580308,0.875722693690948,-1.07852076885685E-31));
#124694=DIRECTION('center_axis',(-9.67816627522388E-33,2.30526622525602E-32,
-1.));
#124695=DIRECTION('ref_axis',(0.470271906992726,0.882521576786327,1.57931021298098E-32));
#124696=DIRECTION('center_axis',(0.889140831940044,-0.457633675527671,-3.46966352979465E-16));
#124697=DIRECTION('ref_axis',(-0.457633675527671,-0.889140831940044,7.88510670898546E-14));
#124698=DIRECTION('center_axis',(-8.16557192291705E-33,2.23242352039376E-32,
-1.));
#124699=DIRECTION('ref_axis',(0.396773414578231,0.917916585253765,0.));
#124700=DIRECTION('center_axis',(8.16557192291705E-33,-2.23242352039376E-32,
1.));
#124701=DIRECTION('ref_axis',(-0.396773414578231,-0.917916585253764,-1.72519038929603E-32));
#124702=DIRECTION('center_axis',(0.912162656095911,-0.409828365079887,6.13681984861663E-17));
#124703=DIRECTION('ref_axis',(0.409828365079887,0.912162656095911,2.46519032881566E-32));
#124704=DIRECTION('center_axis',(-8.16557192291705E-33,2.23242352039376E-32,
-1.));
#124705=DIRECTION('ref_axis',(0.396773414578231,0.917916585253764,1.72519038929603E-32));
#124706=DIRECTION('center_axis',(0.923483682189989,-0.383637705040601,-3.46966352979465E-16));
#124707=DIRECTION('ref_axis',(-0.383637705040601,-0.923483682189989,7.88510670898542E-14));
#124708=DIRECTION('center_axis',(-6.59863703668774E-33,2.17215224181822E-32,
-1.));
#124709=DIRECTION('ref_axis',(0.320634460552723,0.947203010291914,0.));
#124710=DIRECTION('center_axis',(6.59863703668774E-33,-2.17215224181822E-32,
1.));
#124711=DIRECTION('ref_axis',(-0.320634460552723,-0.947203010291914,-1.84589409959839E-32));
#124712=DIRECTION('center_axis',(0.9425323265208,-0.33411497042678,6.13681984861663E-17));
#124713=DIRECTION('ref_axis',(0.33411497042678,0.9425323265208,1.29422492262822E-31));
#124714=DIRECTION('center_axis',(-6.59863703668774E-33,2.17215224181822E-32,
-1.));
#124715=DIRECTION('ref_axis',(0.320634460552723,0.947203010291914,1.84589409959839E-32));
#124716=DIRECTION('center_axis',(0.951680900899042,-0.307088688922252,-3.46966352979465E-16));
#124717=DIRECTION('ref_axis',(-0.307088688922252,-0.951680900899042,1.57702134179711E-13));
#124718=DIRECTION('center_axis',(-4.98778930967775E-33,2.12485348494425E-32,
-1.));
#124719=DIRECTION('ref_axis',(0.2423617370932,0.970185955574068,0.));
#124720=DIRECTION('center_axis',(4.98778930967775E-33,-2.12485348494425E-32,
1.));
#124721=DIRECTION('ref_axis',(-0.2423617370932,-0.970185955574068,-1.94061808061069E-32));
#124722=DIRECTION('center_axis',(0.966629599819581,-0.256178095770573,6.13681984861663E-17));
#124723=DIRECTION('ref_axis',(0.256178095770573,0.966629599819581,-3.08148791101958E-32));
#124724=DIRECTION('center_axis',(-4.98778930967775E-33,2.12485348494425E-32,
-1.));
#124725=DIRECTION('ref_axis',(0.2423617370932,0.970185955574068,1.94061808061069E-32));
#124726=DIRECTION('center_axis',(0.973544840228909,-0.228496048245192,-3.46966352979465E-16));
#124727=DIRECTION('ref_axis',(-0.228496048245192,-0.973544840228909,1.57702134179709E-13));
#124728=DIRECTION('center_axis',(-3.34374866773916E-33,2.09084201519511E-32,
-1.));
#124729=DIRECTION('ref_axis',(0.162476136260193,0.986712473391291,0.));
#124730=DIRECTION('center_axis',(3.34374866773916E-33,-2.09084201519511E-32,
1.));
#124731=DIRECTION('ref_axis',(-0.162476136260193,-0.986712473391291,-2.00873195986766E-32));
#124732=DIRECTION('center_axis',(0.984294112614221,-0.176536398153423,6.13681984861663E-17));
#124733=DIRECTION('ref_axis',(0.176536398153423,0.984294112614221,-4.93038065763132E-32));
#124734=DIRECTION('center_axis',(-3.34374866773916E-33,2.09084201519511E-32,
-1.));
#124735=DIRECTION('ref_axis',(0.162476136260193,0.986712473391291,2.00873195986766E-32));
#124736=DIRECTION('center_axis',(0.988929999270644,-0.148382804066255,-3.46966352979465E-16));
#124737=DIRECTION('ref_axis',(-0.148382804066255,-0.988929999270644,7.88510670898552E-14));
#124738=DIRECTION('center_axis',(-1.67745593009647E-33,2.07034417329048E-32,
-1.));
#124739=DIRECTION('ref_axis',(0.0815092835470502,0.996672582494194,0.));
#124740=DIRECTION('center_axis',(1.67745593009647E-33,-2.07034417329048E-32,
1.));
#124741=DIRECTION('ref_axis',(-0.0815092835470502,-0.996672582494194,-2.04978245074084E-32));
#124742=DIRECTION('center_axis',(0.99540831048651,-0.0957198799330179,6.13681984861663E-17));
#124743=DIRECTION('ref_axis',(0.0957198799330179,0.99540831048651,1.92592994438724E-32));
#124744=DIRECTION('center_axis',(-1.67745593009647E-33,2.07034417329048E-32,
-1.));
#124745=DIRECTION('ref_axis',(0.0815092835470502,0.996672582494194,2.04978245074084E-32));
#124746=DIRECTION('center_axis',(0.997733992329198,-0.0672820968076959,
-3.46966352979465E-16));
#124747=DIRECTION('ref_axis',(-0.0672820968076959,-0.997733992329198,7.88510670898553E-14));
#124748=DIRECTION('center_axis',(1.67745593009674E-33,2.07034417329048E-32,
-1.));
#124749=DIRECTION('ref_axis',(-0.0815092835470633,0.996672582494193,0.));
#124750=DIRECTION('center_axis',(-1.67745593009674E-33,-2.07034417329048E-32,
1.));
#124751=DIRECTION('ref_axis',(0.0815092835470634,-0.996672582494193,-2.04978245074083E-32));
#124752=DIRECTION('center_axis',(0.997733992329197,0.0672820968077094,6.13681984861663E-17));
#124753=DIRECTION('ref_axis',(-0.0672820968077094,0.997733992329197,1.4637067577343E-32));
#124754=DIRECTION('center_axis',(1.67745593009674E-33,2.07034417329048E-32,
-1.));
#124755=DIRECTION('ref_axis',(-0.0815092835470634,0.996672582494193,2.04978245074083E-32));
#124756=DIRECTION('center_axis',(0.995408310486509,0.0957198799330314,-3.46966352979465E-16));
#124757=DIRECTION('ref_axis',(0.0957198799330314,-0.995408310486509,7.88510670898544E-14));
#124758=DIRECTION('center_axis',(0.,2.06349636898632E-32,-1.));
#124759=DIRECTION('ref_axis',(0.,1.,0.));
#124760=DIRECTION('center_axis',(0.,-2.06349636898632E-32,1.));
#124761=DIRECTION('ref_axis',(0.,-1.,-2.06349636898632E-32));
#124762=DIRECTION('center_axis',(0.999898230283323,-0.01426636170434,6.13681984861663E-17));
#124763=DIRECTION('ref_axis',(0.01426636170434,0.999898230283323,0.));
#124764=DIRECTION('center_axis',(0.,2.06349636898632E-32,-1.));
#124765=DIRECTION('ref_axis',(0.,1.,2.06349636898632E-32));
#124766=DIRECTION('center_axis',(0.,2.06349636898632E-32,-1.));
#124767=DIRECTION('ref_axis',(0.,1.,2.06349636898632E-32));
#124768=DIRECTION('center_axis',(0.999898230283323,0.0142663617043404,-3.46966352979465E-16));
#124769=DIRECTION('ref_axis',(0.0142663617043404,-0.999898230283323,7.88510670898545E-14));
#124770=DIRECTION('center_axis',(0.,-4.12699273797265E-32,1.));
#124771=DIRECTION('ref_axis',(0.,-1.,-4.12699273797265E-32));
#124772=DIRECTION('center_axis',(0.,-4.12699273797265E-32,1.));
#124773=DIRECTION('ref_axis',(0.,-1.,-4.12699273797265E-32));
#124774=DIRECTION('center_axis',(0.,-4.12699273797265E-32,1.));
#124775=DIRECTION('ref_axis',(0.,-1.,-4.12699273797265E-32));
#124776=DIRECTION('center_axis',(0.,-1.22464679914735E-16,1.));
#124777=DIRECTION('ref_axis',(0.,-1.,-1.22464679914735E-16));
#124778=DIRECTION('center_axis',(0.,1.22464679914735E-16,-1.));
#124779=DIRECTION('ref_axis',(0.,1.,1.22464679914735E-16));
#124780=DIRECTION('',(8.65956056235493E-17,-0.707106781186547,-0.707106781186548));
#124781=DIRECTION('center_axis',(0.,-1.22464679914735E-16,1.));
#124782=DIRECTION('ref_axis',(0.,-1.,-1.22464679914735E-16));
#124783=DIRECTION('center_axis',(0.,0.,1.));
#124784=DIRECTION('ref_axis',(1.,0.,0.));
#124785=DIRECTION('',(-0.86602540378444,-1.06057523872491E-16,0.499999999999998));
#124786=DIRECTION('center_axis',(0.,4.12699273797265E-32,-1.));
#124787=DIRECTION('ref_axis',(0.,1.,4.12699273797265E-32));
#124788=DIRECTION('center_axis',(0.,4.12699273797265E-32,-1.));
#124789=DIRECTION('ref_axis',(0.,1.,4.12699273797265E-32));
#124790=DIRECTION('center_axis',(0.,4.12699273797265E-32,-1.));
#124791=DIRECTION('ref_axis',(0.,1.,4.12699273797265E-32));
#124792=DIRECTION('center_axis',(0.,0.,1.));
#124793=DIRECTION('ref_axis',(1.,0.,0.));
#124794=DIRECTION('center_axis',(0.,4.12699273797265E-32,-1.));
#124795=DIRECTION('ref_axis',(0.,1.,4.12699273797265E-32));
#124796=DIRECTION('center_axis',(0.,4.12699273797265E-32,-1.));
#124797=DIRECTION('ref_axis',(0.,1.,4.12699273797265E-32));
#124798=DIRECTION('center_axis',(0.,0.,1.));
#124799=DIRECTION('ref_axis',(1.,0.,0.));
#124800=DIRECTION('center_axis',(0.,0.,1.));
#124801=DIRECTION('ref_axis',(1.,0.,0.));
#124802=DIRECTION('center_axis',(0.,-4.12699273797265E-32,1.));
#124803=DIRECTION('ref_axis',(0.,-1.,0.));
#124804=DIRECTION('center_axis',(0.,-4.12699273797265E-32,1.));
#124805=DIRECTION('ref_axis',(0.,-1.,-4.12699273797265E-32));
#124806=DIRECTION('center_axis',(-1.,-1.22464679914735E-16,-5.05410844666257E-48));
#124807=DIRECTION('ref_axis',(-1.22464679914735E-16,1.,0.));
#124808=DIRECTION('center_axis',(0.,-4.12699273797265E-32,1.));
#124809=DIRECTION('ref_axis',(0.,-1.,-4.12699273797265E-32));
#124810=DIRECTION('center_axis',(0.,-4.12699273797265E-32,1.));
#124811=DIRECTION('ref_axis',(0.,-1.,-4.12699273797265E-32));
#124812=DIRECTION('center_axis',(0.,-4.12699273797265E-32,1.));
#124813=DIRECTION('ref_axis',(0.,-1.,-4.12699273797265E-32));
#124814=DIRECTION('',(8.6595605623543E-17,-0.707106781186496,-0.707106781186599));
#124815=DIRECTION('center_axis',(0.,-4.12699273797265E-32,1.));
#124816=DIRECTION('ref_axis',(0.,-1.,0.));
#124817=DIRECTION('center_axis',(0.,-4.12699273797265E-32,1.));
#124818=DIRECTION('ref_axis',(0.,-1.,-4.12699273797265E-32));
#124819=DIRECTION('center_axis',(-1.,-1.22464679914735E-16,-5.05410844666257E-48));
#124820=DIRECTION('ref_axis',(-1.22464679914735E-16,1.,0.));
#124821=DIRECTION('center_axis',(0.,4.12699273797265E-32,-1.));
#124822=DIRECTION('ref_axis',(0.,1.,4.12699273797265E-32));
#124823=DIRECTION('',(-0.282888365662603,0.675203035852198,-0.681230528491433));
#124824=DIRECTION('center_axis',(0.,-4.12699273797265E-32,1.));
#124825=DIRECTION('ref_axis',(0.,-1.,-4.12699273797265E-32));
#124826=DIRECTION('',(-0.226911762261394,-0.696014381459685,0.681230528491435));
#124827=DIRECTION('',(-0.336982393663624,0.649898325441773,-0.681230528491431));
#124828=DIRECTION('center_axis',(0.,-4.12699273797265E-32,1.));
#124829=DIRECTION('ref_axis',(0.,-1.,-4.12699273797265E-32));
#124830=DIRECTION('',(-0.169425098520137,-0.712193866192861,0.681230528491426));
#124831=DIRECTION('',(-0.388833859432995,0.620268648901205,-0.681230528491432));
#124832=DIRECTION('center_axis',(0.,-4.12699273797265E-32,1.));
#124833=DIRECTION('ref_axis',(0.,-1.,-4.12699273797265E-32));
#124834=DIRECTION('',(-0.110810938701405,-0.723633818250228,0.681230528491427));
#124835=DIRECTION('',(-0.438097700020906,0.586511186839332,-0.681230528491428));
#124836=DIRECTION('center_axis',(0.,-4.12699273797265E-32,1.));
#124837=DIRECTION('ref_axis',(0.,-1.,-4.12699273797265E-32));
#124838=DIRECTION('',(-0.0514593503681312,-0.730258106638318,0.681230528491426));
#124839=DIRECTION('',(-0.484446072696218,0.548850589596559,-0.681230528491436));
#124840=DIRECTION('center_axis',(0.,-4.12699273797265E-32,1.));
#124841=DIRECTION('ref_axis',(0.,-1.,-4.12699273797265E-32));
#124842=DIRECTION('',(0.00823469145164575,-0.73202264781083,0.681230528491434));
#124843=DIRECTION('',(-0.527570536685703,0.507537482234015,-0.681230528491432));
#124844=DIRECTION('center_axis',(0.,-4.12699273797265E-32,1.));
#124845=DIRECTION('ref_axis',(0.,-1.,-4.12699273797265E-32));
#124846=DIRECTION('',(0.0678739327584426,-0.728915699037407,0.681230528491429));
#124847=DIRECTION('',(-0.567184105796568,0.462846796664981,-0.68123052849143));
#124848=DIRECTION('center_axis',(0.,-4.12699273797265E-32,1.));
#124849=DIRECTION('ref_axis',(0.,-1.,-4.12699273797265E-32));
#124850=DIRECTION('',(0.127061484241137,-0.720957936549514,0.681230528491425));
#124851=DIRECTION('',(-0.603023158262138,0.415075942028502,-0.681230528491426));
#124852=DIRECTION('center_axis',(0.,-4.12699273797265E-32,1.));
#124853=DIRECTION('ref_axis',(0.,-1.,-4.12699273797265E-32));
#124854=DIRECTION('',(0.185403462509881,-0.708202317943565,0.681230528491427));
#124855=DIRECTION('',(-0.634849191101295,0.364542825480514,-0.681230528491432));
#124856=DIRECTION('center_axis',(0.,-4.12699273797265E-32,1.));
#124857=DIRECTION('ref_axis',(0.,-1.,-4.12699273797265E-32));
#124858=DIRECTION('',(0.242511611325033,-0.690733729756857,0.681230528491433));
#124859=DIRECTION('',(-0.662450407316416,0.311583736574296,-0.681230528491431));
#124860=DIRECTION('center_axis',(0.,-4.12699273797265E-32,1.));
#124861=DIRECTION('ref_axis',(0.,-1.,-4.12699273797265E-32));
#124862=DIRECTION('',(0.298005885378429,-0.668668422561666,0.681230528491429));
#124863=DIRECTION('',(-0.685643125367474,0.256551109308882,-0.681230528491424));
#124864=DIRECTION('center_axis',(0.,-4.12699273797265E-32,1.));
#124865=DIRECTION('ref_axis',(0.,-1.,-4.12699273797265E-32));
#124866=DIRECTION('',(0.351516979432132,-0.642153237336854,0.681230528491427));
#124867=DIRECTION('',(-0.704273001542363,0.199811176738953,-0.681230528491424));
#124868=DIRECTION('center_axis',(0.,-4.12699273797265E-32,1.));
#124869=DIRECTION('ref_axis',(0.,-1.,-4.12699273797265E-32));
#124870=DIRECTION('',(0.402688785983932,-0.611364628265391,0.681230528491425));
#124871=DIRECTION('',(-0.718216057088846,0.14174153375436,-0.68123052849143));
#124872=DIRECTION('center_axis',(0.,-4.12699273797265E-32,1.));
#124873=DIRECTION('ref_axis',(0.,-1.,-4.12699273797265E-32));
#124874=DIRECTION('',(0.451180765103993,-0.57650748846088,0.681230528491423));
#124875=DIRECTION('',(-0.72737950327272,0.0827286242483378,-0.681230528491427));
#124876=DIRECTION('center_axis',(0.,-4.12699273797265E-32,1.));
#124877=DIRECTION('ref_axis',(0.,-1.,-4.12699273797265E-32));
#124878=DIRECTION('',(0.496670210671858,-0.537813786437704,0.681230528491429));
#124879=DIRECTION('',(-0.731702358871481,0.023165169397201,-0.681230528491428));
#124880=DIRECTION('center_axis',(0.,-4.12699273797265E-32,1.));
#124881=DIRECTION('ref_axis',(0.,-1.,-4.12699273797265E-32));
#124882=DIRECTION('',(0.538854397932528,-0.495541022398817,0.681230528491426));
#124883=DIRECTION('',(-0.731155855994348,-0.0365524458342823,-0.681230528491423));
#124884=DIRECTION('center_axis',(0.,-4.12699273797265E-32,1.));
#124885=DIRECTION('ref_axis',(0.,-1.,-4.12699273797265E-32));
#124886=DIRECTION('',(0.577452598079667,-0.449970514614377,0.681230528491431));
#124887=DIRECTION('',(-0.725743631527792,-0.0960268105694711,-0.681230528491426));
#124888=DIRECTION('center_axis',(0.,-4.12699273797265E-32,1.));
#124889=DIRECTION('ref_axis',(0.,-1.,-4.12699273797265E-32));
#124890=DIRECTION('',(0.612207946459573,-0.401405527295087,0.681230528491425));
#124891=DIRECTION('',(-0.715501702932691,-0.154862132723631,-0.681230528491426));
#124892=DIRECTION('center_axis',(0.,-4.12699273797265E-32,1.));
#124893=DIRECTION('ref_axis',(0.,-1.,-4.12699273797265E-32));
#124894=DIRECTION('',(0.642889151962973,-0.350169252418901,0.681230528491433));
#124895=DIRECTION('',(-0.700498228554037,-0.212666872934969,-0.681230528491433));
#124896=DIRECTION('center_axis',(0.,-4.12699273797265E-32,1.));
#124897=DIRECTION('ref_axis',(0.,-1.,-4.12699273797265E-32));
#124898=DIRECTION('',(0.669292036229316,-0.296602658941726,0.681230528491431));
#124899=DIRECTION('',(-0.680833054038443,-0.269056350194485,-0.681230528491427));
#124900=DIRECTION('center_axis',(0.,-4.12699273797265E-32,1.));
#124901=DIRECTION('ref_axis',(0.,-1.,-4.12699273797265E-32));
#124902=DIRECTION('',(0.691240892419964,-0.241062223705287,0.68123052849143));
#124903=DIRECTION('',(-0.656637047877763,-0.323655301834632,-0.681230528491428));
#124904=DIRECTION('center_axis',(0.,-4.12699273797265E-32,1.));
#124905=DIRECTION('ref_axis',(0.,-1.,-4.12699273797265E-32));
#124906=DIRECTION('',(0.708589654518281,-0.183917559142556,0.681230528491427));
#124907=DIRECTION('',(-0.628071230500937,-0.376100380840438,-0.681230528491432));
#124908=DIRECTION('center_axis',(0.,-4.12699273797265E-32,1.));
#124909=DIRECTION('ref_axis',(0.,-1.,-4.12699273797265E-32));
#124910=DIRECTION('',(0.721222869374837,-0.125548953567995,0.681230528491427));
#124911=DIRECTION('',(-0.595325702709604,-0.426042573863937,-0.681230528491426));
#124912=DIRECTION('center_axis',(0.,-4.12699273797265E-32,1.));
#124913=DIRECTION('ref_axis',(0.,-1.,-4.12699273797265E-32));
#124914=DIRECTION('',(0.7290564650291,-0.0663448404215596,0.681230528491428));
#124915=DIRECTION('',(-0.558618380588551,-0.473149523850459,-0.681230528491427));
#124916=DIRECTION('center_axis',(0.,-4.12699273797265E-32,1.));
#124917=DIRECTION('ref_axis',(0.,-1.,-4.12699273797265E-32));
#124918=DIRECTION('',(0.732038310194444,-0.00669921330824207,0.68123052849143));
#124919=DIRECTION('',(-0.518193545310225,-0.517107741819927,-0.681230528491432));
#124920=DIRECTION('center_axis',(0.,-4.12699273797265E-32,1.));
#124921=DIRECTION('ref_axis',(0.,-1.,-4.12699273797265E-32));
#124922=DIRECTION('',(0.730148561183267,0.052990995964345,0.681230528491429));
#124923=DIRECTION('',(-0.474320217483789,-0.557624693084355,-0.681230528491428));
#124924=DIRECTION('center_axis',(0.,-4.12699273797265E-32,1.));
#124925=DIRECTION('ref_axis',(0.,-1.,-4.12699273797265E-32));
#124926=DIRECTION('',(0.72339979396345,0.112328558901694,0.681230528491425));
#124927=DIRECTION('',(-0.427290366867324,-0.594430744017905,-0.681230528491426));
#124928=DIRECTION('center_axis',(0.,-4.12699273797265E-32,1.));
#124929=DIRECTION('ref_axis',(0.,-1.,-4.12699273797265E-32));
#124930=DIRECTION('',(0.711836920467365,0.170918593812461,0.681230528491427));
#124931=DIRECTION('',(-0.377416969357283,-0.627280956424197,-0.681230528491426));
#124932=DIRECTION('center_axis',(0.,-4.12699273797265E-32,1.));
#124933=DIRECTION('ref_axis',(0.,-1.,-4.12699273797265E-32));
#124934=DIRECTION('',(0.695536889710404,0.228371193680976,0.681230528491423));
#124935=DIRECTION('',(-0.325031924185611,-0.655956717559541,-0.681230528491429));
#124936=DIRECTION('center_axis',(0.,-4.12699273797265E-32,1.));
#124937=DIRECTION('ref_axis',(0.,-1.,-4.12699273797265E-32));
#124938=DIRECTION('',(0.67460817570792,0.284304020934146,0.681230528491427));
#124939=DIRECTION('',(-0.27048384518497,-0.680267194964773,-0.68123052849143));
#124940=DIRECTION('center_axis',(0.,-4.12699273797265E-32,1.));
#124941=DIRECTION('ref_axis',(0.,-1.,-4.12699273797265E-32));
#124942=DIRECTION('',(0.649190055598613,0.338344851834863,0.681230528491431));
#124943=DIRECTION('',(-0.21413574082131,-0.700050606423701,-0.681230528491433));
#124944=DIRECTION('center_axis',(0.,-4.12699273797265E-32,1.));
#124945=DIRECTION('ref_axis',(0.,-1.,-4.12699273797265E-32));
#124946=DIRECTION('',(0.619451682778123,0.39013405356959,0.681230528491429));
#124947=DIRECTION('',(-0.156362598432402,-0.715175296597104,-0.681230528491429));
#124948=DIRECTION('center_axis',(0.,-4.12699273797265E-32,1.));
#124949=DIRECTION('ref_axis',(0.,-1.,-4.12699273797265E-32));
#124950=DIRECTION('',(0.585590961211076,0.439326977545395,0.681230528491432));
#124951=DIRECTION('',(-0.0975488887489323,-0.725540613167269,-0.681230528491429));
#124952=DIRECTION('center_axis',(0.,-4.12699273797265E-32,1.));
#124953=DIRECTION('ref_axis',(0.,-1.,-4.12699273797265E-32));
#124954=DIRECTION('',(0.547833228412878,0.485596252969493,0.681230528491429));
#124955=DIRECTION('',(-0.0380860073052719,-0.731077576662577,-0.681230528491432));
#124956=DIRECTION('center_axis',(0.,-4.12699273797265E-32,1.));
#124957=DIRECTION('ref_axis',(0.,-1.,-4.12699273797265E-32));
#124958=DIRECTION('',(0.506429755865707,0.528633965447829,0.681230528491423));
#124959=DIRECTION('',(0.0216303302332448,-0.731749339504516,-0.681230528491425));
#124960=DIRECTION('center_axis',(0.,-4.12699273797265E-32,1.));
#124961=DIRECTION('ref_axis',(0.,-1.,-4.12699273797265E-32));
#124962=DIRECTION('',(0.461656076848288,0.568153706104551,0.681230528491429));
#124963=DIRECTION('',(0.0812027214928242,-0.727551431222185,-0.681230528491427));
#124964=DIRECTION('center_axis',(0.,-4.12699273797265E-32,1.));
#124965=DIRECTION('ref_axis',(0.,-1.,-4.12699273797265E-32));
#124966=DIRECTION('',(0.413810152807329,0.603892477585927,0.681230528491425));
#124967=DIRECTION('',(0.140234722038368,-0.718511788202607,-0.68123052849143));
#124968=DIRECTION('center_axis',(0.,-4.12699273797265E-32,1.));
#124969=DIRECTION('ref_axis',(0.,-1.,-4.12699273797265E-32));
#124970=DIRECTION('',(0.363210390473304,0.635612444264213,0.681230528491422));
#124971=DIRECTION('',(0.19833348364585,-0.704690567778647,-0.681230528491427));
#124972=DIRECTION('center_axis',(0.,-4.12699273797265E-32,1.));
#124973=DIRECTION('ref_axis',(0.,-1.,-4.12699273797265E-32));
#124974=DIRECTION('',(0.310193522916185,0.663102514994576,0.681230528491431));
#124975=DIRECTION('',(0.25511236864239,-0.686179747891876,-0.681230528491428));
#124976=DIRECTION('center_axis',(0.,-4.12699273797265E-32,1.));
#124977=DIRECTION('ref_axis',(0.,-1.,-4.12699273797265E-32));
#124978=DIRECTION('',(8.65956056235492E-17,0.707106781186547,0.707106781186548));
#124979=DIRECTION('center_axis',(0.,-4.12699273797265E-32,1.));
#124980=DIRECTION('ref_axis',(0.,-1.,-4.12699273797265E-32));
#124981=DIRECTION('center_axis',(0.,-4.12699273797265E-32,1.));
#124982=DIRECTION('ref_axis',(0.,-1.,-4.12699273797265E-32));
#124983=DIRECTION('center_axis',(0.,-4.12699273797265E-32,1.));
#124984=DIRECTION('ref_axis',(0.,-1.,-4.12699273797265E-32));
#124985=DIRECTION('',(0.255112368642381,0.686179747891878,0.68123052849143));
#124986=DIRECTION('',(0.310193522916193,-0.663102514994574,-0.68123052849143));
#124987=DIRECTION('center_axis',(0.,-4.12699273797265E-32,1.));
#124988=DIRECTION('ref_axis',(0.,-1.,-4.12699273797265E-32));
#124989=DIRECTION('',(0.198333483645841,0.704690567778648,0.681230528491429));
#124990=DIRECTION('',(0.363210390473318,-0.635612444264197,-0.68123052849143));
#124991=DIRECTION('center_axis',(0.,-4.12699273797265E-32,1.));
#124992=DIRECTION('ref_axis',(0.,-1.,-4.12699273797265E-32));
#124993=DIRECTION('',(0.140234722038358,0.718511788202608,0.681230528491431));
#124994=DIRECTION('',(0.413810152807337,-0.603892477585918,-0.681230528491428));
#124995=DIRECTION('center_axis',(0.,-4.12699273797265E-32,1.));
#124996=DIRECTION('ref_axis',(0.,-1.,-4.12699273797265E-32));
#124997=DIRECTION('',(0.0812027214928108,0.727551431222181,0.681230528491433));
#124998=DIRECTION('',(0.461656076848292,-0.568153706104549,-0.681230528491427));
#124999=DIRECTION('center_axis',(0.,-4.12699273797265E-32,1.));
#125000=DIRECTION('ref_axis',(0.,-1.,-4.12699273797265E-32));
#125001=DIRECTION('',(0.0216303302332394,0.731749339504505,0.681230528491436));
#125002=DIRECTION('',(0.506429755865719,-0.528633965447818,-0.681230528491424));
#125003=DIRECTION('center_axis',(0.,-4.12699273797265E-32,1.));
#125004=DIRECTION('ref_axis',(0.,-1.,-4.12699273797265E-32));
#125005=DIRECTION('',(-0.0380860073052859,0.73107757666258,0.681230528491429));
#125006=DIRECTION('',(0.547833228412883,-0.485596252969484,-0.681230528491432));
#125007=DIRECTION('center_axis',(0.,-4.12699273797265E-32,1.));
#125008=DIRECTION('ref_axis',(0.,-1.,-4.12699273797265E-32));
#125009=DIRECTION('',(-0.0975488887489436,0.725540613167269,0.681230528491428));
#125010=DIRECTION('',(0.585590961211085,-0.439326977545388,-0.681230528491429));
#125011=DIRECTION('center_axis',(0.,-4.12699273797265E-32,1.));
#125012=DIRECTION('ref_axis',(0.,-1.,-4.12699273797265E-32));
#125013=DIRECTION('',(-0.156362598432407,0.715175296597106,0.681230528491426));
#125014=DIRECTION('',(0.619451682778131,-0.390134053569583,-0.681230528491426));
#125015=DIRECTION('center_axis',(0.,-4.12699273797265E-32,1.));
#125016=DIRECTION('ref_axis',(0.,-1.,-4.12699273797265E-32));
#125017=DIRECTION('',(-0.214135740821315,0.7000506064237,0.681230528491432));
#125018=DIRECTION('',(0.649190055598621,-0.338344851834856,-0.681230528491427));
#125019=DIRECTION('center_axis',(0.,-4.12699273797265E-32,1.));
#125020=DIRECTION('ref_axis',(0.,-1.,-4.12699273797265E-32));
#125021=DIRECTION('',(-0.270483845184975,0.680267194964772,0.681230528491429));
#125022=DIRECTION('',(0.674608175707922,-0.284304020934136,-0.681230528491429));
#125023=DIRECTION('center_axis',(0.,-4.12699273797265E-32,1.));
#125024=DIRECTION('ref_axis',(0.,-1.,-4.12699273797265E-32));
#125025=DIRECTION('',(-0.325031924185617,0.65595671755954,0.681230528491428));
#125026=DIRECTION('',(0.695536889710403,-0.228371193680966,-0.681230528491428));
#125027=DIRECTION('center_axis',(0.,-4.12699273797265E-32,1.));
#125028=DIRECTION('ref_axis',(0.,-1.,-4.12699273797265E-32));
#125029=DIRECTION('',(-0.377416969357297,0.627280956424184,0.681230528491431));
#125030=DIRECTION('',(0.711836920467366,-0.17091859381245,-0.681230528491429));
#125031=DIRECTION('center_axis',(0.,-4.12699273797265E-32,1.));
#125032=DIRECTION('ref_axis',(0.,-1.,-4.12699273797265E-32));
#125033=DIRECTION('',(-0.427290366867324,0.594430744017905,0.681230528491426));
#125034=DIRECTION('',(0.723399793963449,-0.112328558901684,-0.681230528491429));
#125035=DIRECTION('center_axis',(0.,-4.12699273797265E-32,1.));
#125036=DIRECTION('ref_axis',(0.,-1.,-4.12699273797265E-32));
#125037=DIRECTION('',(-0.474320217483799,0.557624693084348,0.681230528491426));
#125038=DIRECTION('',(0.730148561183259,-0.0529909959643429,-0.681230528491438));
#125039=DIRECTION('center_axis',(0.,-4.12699273797265E-32,1.));
#125040=DIRECTION('ref_axis',(0.,-1.,-4.12699273797265E-32));
#125041=DIRECTION('',(-0.518193545310239,0.517107741819918,0.681230528491428));
#125042=DIRECTION('',(0.732038310194444,0.00669921330825058,-0.68123052849143));
#125043=DIRECTION('center_axis',(0.,-4.12699273797265E-32,1.));
#125044=DIRECTION('ref_axis',(0.,-1.,-4.12699273797265E-32));
#125045=DIRECTION('',(-0.558618380588554,0.47314952385045,0.681230528491431));
#125046=DIRECTION('',(0.729056465029095,0.0663448404215658,-0.681230528491433));
#125047=DIRECTION('center_axis',(0.,-4.12699273797265E-32,1.));
#125048=DIRECTION('ref_axis',(0.,-1.,-4.12699273797265E-32));
#125049=DIRECTION('',(-0.595325702709605,0.426042573863934,0.681230528491427));
#125050=DIRECTION('',(0.72122286937483,0.125548953568005,-0.681230528491432));
#125051=DIRECTION('center_axis',(0.,-4.12699273797265E-32,1.));
#125052=DIRECTION('ref_axis',(0.,-1.,-4.12699273797265E-32));
#125053=DIRECTION('',(-0.628071230500946,0.376100380840428,0.681230528491429));
#125054=DIRECTION('',(0.70858965451828,0.183917559142564,-0.681230528491425));
#125055=DIRECTION('center_axis',(0.,-4.12699273797265E-32,1.));
#125056=DIRECTION('ref_axis',(0.,-1.,-4.12699273797265E-32));
#125057=DIRECTION('',(-0.656637047877765,0.323655301834624,0.681230528491429));
#125058=DIRECTION('',(0.691240892419969,0.241062223705293,-0.681230528491424));
#125059=DIRECTION('center_axis',(0.,-4.12699273797265E-32,1.));
#125060=DIRECTION('ref_axis',(0.,-1.,-4.12699273797265E-32));
#125061=DIRECTION('',(-0.680833054038444,0.269056350194477,0.681230528491429));
#125062=DIRECTION('',(0.669292036229309,0.296602658941735,-0.681230528491434));
#125063=DIRECTION('center_axis',(0.,-4.12699273797265E-32,1.));
#125064=DIRECTION('ref_axis',(0.,-1.,-4.12699273797265E-32));
#125065=DIRECTION('',(-0.700498228554044,0.212666872934959,0.681230528491429));
#125066=DIRECTION('',(0.642889151962971,0.350169252418909,-0.681230528491431));
#125067=DIRECTION('center_axis',(0.,-4.12699273797265E-32,1.));
#125068=DIRECTION('ref_axis',(0.,-1.,-4.12699273797265E-32));
#125069=DIRECTION('',(-0.715501702932687,0.154862132723623,0.681230528491433));
#125070=DIRECTION('',(0.612207946459557,0.401405527295097,-0.681230528491433));
#125071=DIRECTION('center_axis',(0.,-4.12699273797265E-32,1.));
#125072=DIRECTION('ref_axis',(0.,-1.,-4.12699273797265E-32));
#125073=DIRECTION('',(-0.725743631527792,0.0960268105694655,0.681230528491427));
#125074=DIRECTION('',(0.577452598079657,0.449970514614387,-0.681230528491433));
#125075=DIRECTION('center_axis',(0.,-4.12699273797265E-32,1.));
#125076=DIRECTION('ref_axis',(0.,-1.,-4.12699273797265E-32));
#125077=DIRECTION('',(-0.731155855994343,0.0365524458342741,0.681230528491429));
#125078=DIRECTION('',(0.538854397932528,0.495541022398819,-0.681230528491425));
#125079=DIRECTION('center_axis',(0.,-4.12699273797265E-32,1.));
#125080=DIRECTION('ref_axis',(0.,-1.,-4.12699273797265E-32));
#125081=DIRECTION('',(-0.731702358871478,-0.0231651693972153,0.68123052849143));
#125082=DIRECTION('',(0.496670210671855,0.53781378643771,-0.681230528491426));
#125083=DIRECTION('center_axis',(0.,-4.12699273797265E-32,1.));
#125084=DIRECTION('ref_axis',(0.,-1.,-4.12699273797265E-32));
#125085=DIRECTION('',(-0.72737950327272,-0.0827286242483435,0.681230528491426));
#125086=DIRECTION('',(0.451180765103981,0.576507488460881,-0.681230528491431));
#125087=DIRECTION('center_axis',(0.,-4.12699273797265E-32,1.));
#125088=DIRECTION('ref_axis',(0.,-1.,-4.12699273797265E-32));
#125089=DIRECTION('',(-0.718216057088845,-0.141741533754371,0.681230528491429));
#125090=DIRECTION('',(0.402688785983913,0.611364628265397,-0.681230528491432));
#125091=DIRECTION('center_axis',(0.,-4.12699273797265E-32,1.));
#125092=DIRECTION('ref_axis',(0.,-1.,-4.12699273797265E-32));
#125093=DIRECTION('',(-0.70427300154235,-0.199811176738967,0.681230528491434));
#125094=DIRECTION('',(0.351516979432122,0.642153237336857,-0.681230528491429));
#125095=DIRECTION('center_axis',(0.,-4.12699273797265E-32,1.));
#125096=DIRECTION('ref_axis',(0.,-1.,-4.12699273797265E-32));
#125097=DIRECTION('',(-0.685643125367468,-0.256551109308884,0.68123052849143));
#125098=DIRECTION('',(0.298005885378418,0.668668422561672,-0.681230528491428));
#125099=DIRECTION('center_axis',(0.,-4.12699273797265E-32,1.));
#125100=DIRECTION('ref_axis',(0.,-1.,-4.12699273797265E-32));
#125101=DIRECTION('',(-0.662450407316412,-0.311583736574311,0.681230528491427));
#125102=DIRECTION('',(0.242511611325018,0.690733729756874,-0.681230528491421));
#125103=DIRECTION('center_axis',(0.,-4.12699273797265E-32,1.));
#125104=DIRECTION('ref_axis',(0.,-1.,-4.12699273797265E-32));
#125105=DIRECTION('',(-0.634849191101292,-0.364542825480524,0.681230528491429));
#125106=DIRECTION('',(0.185403462509872,0.708202317943561,-0.681230528491434));
#125107=DIRECTION('center_axis',(0.,-4.12699273797265E-32,1.));
#125108=DIRECTION('ref_axis',(0.,-1.,-4.12699273797265E-32));
#125109=DIRECTION('',(-0.603023158262138,-0.415075942028502,0.681230528491426));
#125110=DIRECTION('',(0.127061484241121,0.720957936549513,-0.681230528491429));
#125111=DIRECTION('center_axis',(0.,-4.12699273797265E-32,1.));
#125112=DIRECTION('ref_axis',(0.,-1.,-4.12699273797265E-32));
#125113=DIRECTION('',(-0.567184105796557,-0.462846796664993,0.681230528491431));
#125114=DIRECTION('',(0.0678739327584265,0.728915699037399,-0.681230528491438));
#125115=DIRECTION('center_axis',(0.,-4.12699273797265E-32,1.));
#125116=DIRECTION('ref_axis',(0.,-1.,-4.12699273797265E-32));
#125117=DIRECTION('',(-0.527570536685702,-0.507537482234019,0.68123052849143));
#125118=DIRECTION('',(0.00823469145162862,0.732022647810838,-0.681230528491425));
#125119=DIRECTION('center_axis',(0.,-4.12699273797265E-32,1.));
#125120=DIRECTION('ref_axis',(0.,-1.,-4.12699273797265E-32));
#125121=DIRECTION('',(-0.48444607269621,-0.548850589596576,0.681230528491428));
#125122=DIRECTION('',(-0.0514593503681429,0.730258106638313,-0.681230528491432));
#125123=DIRECTION('center_axis',(0.,-4.12699273797265E-32,1.));
#125124=DIRECTION('ref_axis',(0.,-1.,-4.12699273797265E-32));
#125125=DIRECTION('',(-0.438097700020894,-0.586511186839349,0.681230528491422));
#125126=DIRECTION('',(-0.110810938701414,0.723633818250228,-0.681230528491426));
#125127=DIRECTION('center_axis',(0.,-4.12699273797265E-32,1.));
#125128=DIRECTION('ref_axis',(0.,-1.,-4.12699273797265E-32));
#125129=DIRECTION('',(-0.388833859432984,-0.620268648901214,0.68123052849143));
#125130=DIRECTION('',(-0.16942509852015,0.712193866192848,-0.681230528491436));
#125131=DIRECTION('center_axis',(0.,-4.12699273797265E-32,1.));
#125132=DIRECTION('ref_axis',(0.,-1.,-4.12699273797265E-32));
#125133=DIRECTION('',(-0.336982393663615,-0.649898325441775,0.681230528491433));
#125134=DIRECTION('',(-0.226911762261403,0.696014381459684,-0.681230528491434));
#125135=DIRECTION('center_axis',(0.,-4.12699273797265E-32,1.));
#125136=DIRECTION('ref_axis',(0.,-1.,-4.12699273797265E-32));
#125137=DIRECTION('',(-0.282888365662603,-0.675203035852198,0.681230528491433));
#125138=DIRECTION('center_axis',(0.,-4.12699273797265E-32,1.));
#125139=DIRECTION('ref_axis',(0.,-1.,0.));
#125140=DIRECTION('center_axis',(0.,-4.12699273797265E-32,1.));
#125141=DIRECTION('ref_axis',(0.,-1.,-4.12699273797265E-32));
#125142=DIRECTION('center_axis',(-1.,-1.22464679914735E-16,-5.05410844666257E-48));
#125143=DIRECTION('ref_axis',(-1.22464679914735E-16,1.,0.));
#125144=DIRECTION('center_axis',(0.,-4.12699273797265E-32,1.));
#125145=DIRECTION('ref_axis',(0.,-1.,-4.12699273797265E-32));
#125146=DIRECTION('center_axis',(0.,-4.12699273797265E-32,1.));
#125147=DIRECTION('ref_axis',(0.,-1.,-4.12699273797265E-32));
#125148=DIRECTION('',(-2.24445597957705E-36,4.11599200331947E-32,-1.));
#125149=DIRECTION('',(2.24445597957705E-36,-4.11599200331947E-32,1.));
#125150=DIRECTION('center_axis',(0.,-4.12699273797265E-32,1.));
#125151=DIRECTION('ref_axis',(0.,-1.,-4.12699273797265E-32));
#125152=DIRECTION('',(-6.71843145449713E-36,4.11602859211924E-32,-1.));
#125153=DIRECTION('',(6.71843145449713E-36,-4.11602859211924E-32,1.));
#125154=DIRECTION('center_axis',(0.,-4.12699273797265E-32,1.));
#125155=DIRECTION('ref_axis',(0.,-1.,-4.12699273797265E-32));
#125156=DIRECTION('',(-1.11476968765511E-35,4.11610152622635E-32,-1.));
#125157=DIRECTION('',(1.11476968765511E-35,-4.11610152622635E-32,1.));
#125158=DIRECTION('center_axis',(0.,-4.12699273797265E-32,1.));
#125159=DIRECTION('ref_axis',(0.,-1.,-4.12699273797265E-32));
#125160=DIRECTION('',(-1.5502776215132E-35,4.11621032027636E-32,-1.));
#125161=DIRECTION('',(1.5502776215132E-35,-4.11621032027636E-32,1.));
#125162=DIRECTION('center_axis',(0.,-4.12699273797265E-32,1.));
#125163=DIRECTION('ref_axis',(0.,-1.,-4.12699273797265E-32));
#125164=DIRECTION('',(-1.97546871357812E-35,4.11635425026281E-32,-1.));
#125165=DIRECTION('',(1.97546871357812E-35,-4.11635425026281E-32,1.));
#125166=DIRECTION('center_axis',(0.,-4.12699273797265E-32,1.));
#125167=DIRECTION('ref_axis',(0.,-1.,-4.12699273797265E-32));
#125168=DIRECTION('',(-2.3875133872833E-35,4.11653235835539E-32,-1.));
#125169=DIRECTION('',(2.3875133872833E-35,-4.11653235835539E-32,1.));
#125170=DIRECTION('center_axis',(0.,-4.12699273797265E-32,1.));
#125171=DIRECTION('ref_axis',(0.,-1.,-4.12699273797265E-32));
#125172=DIRECTION('',(-2.78366955330785E-35,4.11674345927413E-32,-1.));
#125173=DIRECTION('',(2.78366955330785E-35,-4.11674345927413E-32,1.));
#125174=DIRECTION('center_axis',(0.,-4.12699273797265E-32,1.));
#125175=DIRECTION('ref_axis',(0.,-1.,-4.12699273797265E-32));
#125176=DIRECTION('',(-3.1613008577281E-35,4.11698614817723E-32,-1.));
#125177=DIRECTION('',(3.1613008577281E-35,-4.11698614817723E-32,1.));
#125178=DIRECTION('center_axis',(0.,-4.12699273797265E-32,1.));
#125179=DIRECTION('ref_axis',(0.,-1.,-4.12699273797265E-32));
#125180=DIRECTION('',(-3.51789422651897E-35,4.1172588100101E-32,-1.));
#125181=DIRECTION('',(3.51789422651897E-35,-4.1172588100101E-32,1.));
#125182=DIRECTION('center_axis',(0.,-4.12699273797265E-32,1.));
#125183=DIRECTION('ref_axis',(0.,-1.,-4.12699273797265E-32));
#125184=DIRECTION('',(-3.85107658964331E-35,4.11755963025323E-32,-1.));
#125185=DIRECTION('',(3.85107658964331E-35,-4.11755963025323E-32,1.));
#125186=DIRECTION('center_axis',(0.,-4.12699273797265E-32,1.));
#125187=DIRECTION('ref_axis',(0.,-1.,-4.12699273797265E-32));
#125188=DIRECTION('',(-4.1586306734472E-35,4.11788660699752E-32,-1.));
#125189=DIRECTION('',(4.1586306734472E-35,-4.11788660699752E-32,1.));
#125190=DIRECTION('center_axis',(0.,-4.12699273797265E-32,1.));
#125191=DIRECTION('ref_axis',(0.,-1.,-4.12699273797265E-32));
#125192=DIRECTION('',(-4.43850975624469E-35,4.11823756426669E-32,-1.));
#125193=DIRECTION('',(4.43850975624469E-35,-4.11823756426669E-32,1.));
#125194=DIRECTION('center_axis',(0.,-4.12699273797265E-32,1.));
#125195=DIRECTION('ref_axis',(0.,-1.,-4.12699273797265E-32));
#125196=DIRECTION('',(-4.6888512889172E-35,4.11861016649801E-32,-1.));
#125197=DIRECTION('',(4.6888512889172E-35,-4.11861016649801E-32,1.));
#125198=DIRECTION('center_axis',(0.,-4.12699273797265E-32,1.));
#125199=DIRECTION('ref_axis',(0.,-1.,-4.12699273797265E-32));
#125200=DIRECTION('',(-4.90798928986703E-35,4.11900193408512E-32,-1.));
#125201=DIRECTION('',(4.90798928986703E-35,-4.11900193408512E-32,1.));
#125202=DIRECTION('center_axis',(0.,-4.12699273797265E-32,1.));
#125203=DIRECTION('ref_axis',(0.,-1.,-4.12699273797265E-32));
#125204=DIRECTION('',(-5.09446543185543E-35,4.11941025987936E-32,-1.));
#125205=DIRECTION('',(5.09446543185543E-35,-4.11941025987936E-32,1.));
#125206=DIRECTION('center_axis',(0.,-4.12699273797265E-32,1.));
#125207=DIRECTION('ref_axis',(0.,-1.,-4.12699273797265E-32));
#125208=DIRECTION('',(-5.24703874692283E-35,4.11983242653994E-32,-1.));
#125209=DIRECTION('',(5.24703874692283E-35,-4.11983242653994E-32,1.));
#125210=DIRECTION('center_axis',(0.,-4.12699273797265E-32,1.));
#125211=DIRECTION('ref_axis',(0.,-1.,-4.12699273797265E-32));
#125212=DIRECTION('',(-5.36469388482745E-35,4.12026562461737E-32,-1.));
#125213=DIRECTION('',(5.36469388482745E-35,-4.12026562461737E-32,1.));
#125214=DIRECTION('center_axis',(0.,-4.12699273797265E-32,1.));
#125215=DIRECTION('ref_axis',(0.,-1.,-4.12699273797265E-32));
#125216=DIRECTION('',(-5.44664787004251E-35,4.12070697124994E-32,-1.));
#125217=DIRECTION('',(5.44664787004251E-35,-4.12070697124994E-32,1.));
#125218=DIRECTION('center_axis',(0.,-4.12699273797265E-32,1.));
#125219=DIRECTION('ref_axis',(0.,-1.,-4.12699273797265E-32));
#125220=DIRECTION('',(-5.49235531231428E-35,4.12115352934861E-32,-1.));
#125221=DIRECTION('',(5.49235531231428E-35,-4.12115352934861E-32,1.));
#125222=DIRECTION('center_axis',(0.,-4.12699273797265E-32,1.));
#125223=DIRECTION('ref_axis',(0.,-1.,-4.12699273797265E-32));
#125224=DIRECTION('',(-5.50151203616034E-35,4.12160232714293E-32,-1.));
#125225=DIRECTION('',(5.50151203616034E-35,-4.12160232714293E-32,1.));
#125226=DIRECTION('center_axis',(0.,-4.12699273797265E-32,1.));
#125227=DIRECTION('ref_axis',(0.,-1.,-4.12699273797265E-32));
#125228=DIRECTION('',(-5.47405710508952E-35,4.1220503779576E-32,-1.));
#125229=DIRECTION('',(5.47405710508952E-35,-4.1220503779576E-32,1.));
#125230=DIRECTION('center_axis',(0.,-4.12699273797265E-32,1.));
#125231=DIRECTION('ref_axis',(0.,-1.,-4.12699273797265E-32));
#125232=DIRECTION('',(-5.41017322714156E-35,4.12249470008839E-32,-1.));
#125233=DIRECTION('',(5.41017322714156E-35,-4.12249470008839E-32,1.));
#125234=DIRECTION('center_axis',(0.,-4.12699273797265E-32,1.));
#125235=DIRECTION('ref_axis',(0.,-1.,-4.12699273797265E-32));
#125236=DIRECTION('',(-5.3102855389809E-35,4.12293233664482E-32,-1.));
#125237=DIRECTION('',(5.3102855389809E-35,-4.12293233664482E-32,1.));
#125238=DIRECTION('center_axis',(0.,-4.12699273797265E-32,1.));
#125239=DIRECTION('ref_axis',(0.,-1.,-4.12699273797265E-32));
#125240=DIRECTION('',(-5.17505877669541E-35,4.12336037522781E-32,-1.));
#125241=DIRECTION('',(5.17505877669541E-35,-4.12336037522781E-32,1.));
#125242=DIRECTION('center_axis',(0.,-4.12699273797265E-32,1.));
#125243=DIRECTION('ref_axis',(0.,-1.,-4.12699273797265E-32));
#125244=DIRECTION('',(-5.00539285207499E-35,4.12377596731122E-32,-1.));
#125245=DIRECTION('',(5.00539285207499E-35,-4.12377596731122E-32,1.));
#125246=DIRECTION('center_axis',(0.,-4.12699273797265E-32,1.));
#125247=DIRECTION('ref_axis',(0.,-1.,-4.12699273797265E-32));
#125248=DIRECTION('',(-4.80241686385389E-35,4.1241763471983E-32,-1.));
#125249=DIRECTION('',(4.80241686385389E-35,-4.1241763471983E-32,1.));
#125250=DIRECTION('center_axis',(0.,-4.12699273797265E-32,1.));
#125251=DIRECTION('ref_axis',(0.,-1.,-4.12699273797265E-32));
#125252=DIRECTION('',(-4.56748158374851E-35,4.12455885042696E-32,-1.));
#125253=DIRECTION('',(4.56748158374851E-35,-4.12455885042696E-32,1.));
#125254=DIRECTION('center_axis',(0.,-4.12699273797265E-32,1.));
#125255=DIRECTION('ref_axis',(0.,-1.,-4.12699273797265E-32));
#125256=DIRECTION('',(-4.30215046728491E-35,4.12492093150131E-32,-1.));
#125257=DIRECTION('',(4.30215046728491E-35,-4.12492093150131E-32,1.));
#125258=DIRECTION('center_axis',(0.,-4.12699273797265E-32,1.));
#125259=DIRECTION('ref_axis',(0.,-1.,-4.12699273797265E-32));
#125260=DIRECTION('',(-4.00818924926601E-35,4.12526018083156E-32,-1.));
#125261=DIRECTION('',(4.00818924926601E-35,-4.12526018083156E-32,1.));
#125262=DIRECTION('center_axis',(0.,-4.12699273797265E-32,1.));
#125263=DIRECTION('ref_axis',(0.,-1.,-4.12699273797265E-32));
#125264=DIRECTION('',(-3.68755419309802E-35,4.12557434076937E-32,-1.));
#125265=DIRECTION('',(3.68755419309802E-35,-4.12557434076937E-32,1.));
#125266=DIRECTION('center_axis',(0.,-4.12699273797265E-32,1.));
#125267=DIRECTION('ref_axis',(0.,-1.,-4.12699273797265E-32));
#125268=DIRECTION('',(-3.34237907217807E-35,4.1258613206322E-32,-1.));
#125269=DIRECTION('',(3.34237907217807E-35,-4.1258613206322E-32,1.));
#125270=DIRECTION('center_axis',(0.,-4.12699273797265E-32,1.));
#125271=DIRECTION('ref_axis',(0.,-1.,-4.12699273797265E-32));
#125272=DIRECTION('',(-2.97496096998759E-35,4.1261192106164E-32,-1.));
#125273=DIRECTION('',(2.97496096998759E-35,-4.1261192106164E-32,1.));
#125274=DIRECTION('center_axis',(0.,-4.12699273797265E-32,1.));
#125275=DIRECTION('ref_axis',(0.,-1.,-4.12699273797265E-32));
#125276=DIRECTION('',(-2.58774499337527E-35,4.12634629450669E-32,-1.));
#125277=DIRECTION('',(2.58774499337527E-35,-4.12634629450669E-32,1.));
#125278=DIRECTION('center_axis',(0.,-4.12699273797265E-32,1.));
#125279=DIRECTION('ref_axis',(0.,-1.,-4.12699273797265E-32));
#125280=DIRECTION('',(-2.18330800078025E-35,4.12654106109723E-32,-1.));
#125281=DIRECTION('',(2.18330800078025E-35,-4.12654106109723E-32,1.));
#125282=DIRECTION('center_axis',(0.,-4.12699273797265E-32,1.));
#125283=DIRECTION('ref_axis',(0.,-1.,-4.12699273797265E-32));
#125284=DIRECTION('',(-1.76434145365967E-35,4.1267022142485E-32,-1.));
#125285=DIRECTION('',(1.76434145365967E-35,-4.1267022142485E-32,1.));
#125286=DIRECTION('center_axis',(0.,-4.12699273797265E-32,1.));
#125287=DIRECTION('ref_axis',(0.,-1.,-4.12699273797265E-32));
#125288=DIRECTION('',(-1.3336335052612E-35,4.12682868151287E-32,-1.));
#125289=DIRECTION('',(1.3336335052612E-35,-4.12682868151287E-32,1.));
#125290=DIRECTION('center_axis',(0.,-4.12699273797265E-32,1.));
#125291=DIRECTION('ref_axis',(0.,-1.,-4.12699273797265E-32));
#125292=DIRECTION('',(-8.94050445919518E-36,4.12691962127155E-32,-1.));
#125293=DIRECTION('',(8.94050445919518E-36,-4.12691962127155E-32,1.));
#125294=DIRECTION('center_axis',(0.,-4.12699273797265E-32,1.));
#125295=DIRECTION('ref_axis',(0.,-1.,-4.12699273797265E-32));
#125296=DIRECTION('',(-4.48517628368065E-36,4.12697442833547E-32,-1.));
#125297=DIRECTION('',(4.48517628368065E-36,-4.12697442833547E-32,1.));
#125298=DIRECTION('center_axis',(0.,-4.12699273797265E-32,1.));
#125299=DIRECTION('ref_axis',(0.,-1.,-4.12699273797265E-32));
#125300=DIRECTION('',(0.,4.12699273797265E-32,-1.));
#125301=DIRECTION('',(0.,4.12699273797265E-32,-1.));
#125302=DIRECTION('',(0.,-4.12699273797265E-32,1.));
#125303=DIRECTION('center_axis',(0.,-4.12699273797265E-32,1.));
#125304=DIRECTION('ref_axis',(0.,-1.,-4.12699273797265E-32));
#125305=DIRECTION('',(4.48517628367996E-36,4.12697442833547E-32,-1.));
#125306=DIRECTION('',(-4.48517628367996E-36,-4.12697442833547E-32,1.));
#125307=DIRECTION('center_axis',(0.,-4.12699273797265E-32,1.));
#125308=DIRECTION('ref_axis',(0.,-1.,-4.12699273797265E-32));
#125309=DIRECTION('',(8.94050445919518E-36,4.12691962127156E-32,-1.));
#125310=DIRECTION('',(-8.94050445919518E-36,-4.12691962127156E-32,1.));
#125311=DIRECTION('center_axis',(0.,-4.12699273797265E-32,1.));
#125312=DIRECTION('ref_axis',(0.,-1.,-4.12699273797265E-32));
#125313=DIRECTION('',(1.3336335052612E-35,4.12682868151287E-32,-1.));
#125314=DIRECTION('',(-1.3336335052612E-35,-4.12682868151287E-32,1.));
#125315=DIRECTION('center_axis',(0.,-4.12699273797265E-32,1.));
#125316=DIRECTION('ref_axis',(0.,-1.,-4.12699273797265E-32));
#125317=DIRECTION('',(1.76434145365967E-35,4.1267022142485E-32,-1.));
#125318=DIRECTION('',(-1.76434145365967E-35,-4.1267022142485E-32,1.));
#125319=DIRECTION('center_axis',(0.,-4.12699273797265E-32,1.));
#125320=DIRECTION('ref_axis',(0.,-1.,-4.12699273797265E-32));
#125321=DIRECTION('',(2.18330800077971E-35,4.12654106109723E-32,-1.));
#125322=DIRECTION('',(-2.18330800077971E-35,-4.12654106109723E-32,1.));
#125323=DIRECTION('center_axis',(0.,-4.12699273797265E-32,1.));
#125324=DIRECTION('ref_axis',(0.,-1.,-4.12699273797265E-32));
#125325=DIRECTION('',(2.58774499337554E-35,4.12634629450669E-32,-1.));
#125326=DIRECTION('',(-2.58774499337554E-35,-4.12634629450669E-32,1.));
#125327=DIRECTION('center_axis',(0.,-4.12699273797265E-32,1.));
#125328=DIRECTION('ref_axis',(0.,-1.,-4.12699273797265E-32));
#125329=DIRECTION('',(2.97496096998732E-35,4.1261192106164E-32,-1.));
#125330=DIRECTION('',(-2.97496096998732E-35,-4.1261192106164E-32,1.));
#125331=DIRECTION('center_axis',(0.,-4.12699273797265E-32,1.));
#125332=DIRECTION('ref_axis',(0.,-1.,-4.12699273797265E-32));
#125333=DIRECTION('',(3.34237907217862E-35,4.1258613206322E-32,-1.));
#125334=DIRECTION('',(-3.34237907217862E-35,-4.1258613206322E-32,1.));
#125335=DIRECTION('center_axis',(0.,-4.12699273797265E-32,1.));
#125336=DIRECTION('ref_axis',(0.,-1.,-4.12699273797265E-32));
#125337=DIRECTION('',(3.68755419309748E-35,4.12557434076937E-32,-1.));
#125338=DIRECTION('',(-3.68755419309748E-35,-4.12557434076937E-32,1.));
#125339=DIRECTION('center_axis',(0.,-4.12699273797265E-32,1.));
#125340=DIRECTION('ref_axis',(0.,-1.,-4.12699273797265E-32));
#125341=DIRECTION('',(4.00818924926656E-35,4.12526018083156E-32,-1.));
#125342=DIRECTION('',(-4.00818924926656E-35,-4.12526018083156E-32,1.));
#125343=DIRECTION('center_axis',(0.,-4.12699273797265E-32,1.));
#125344=DIRECTION('ref_axis',(0.,-1.,-4.12699273797265E-32));
#125345=DIRECTION('',(4.30215046728545E-35,4.12492093150131E-32,-1.));
#125346=DIRECTION('',(-4.30215046728545E-35,-4.12492093150131E-32,1.));
#125347=DIRECTION('center_axis',(0.,-4.12699273797265E-32,1.));
#125348=DIRECTION('ref_axis',(0.,-1.,-4.12699273797265E-32));
#125349=DIRECTION('',(4.56748158374851E-35,4.12455885042696E-32,-1.));
#125350=DIRECTION('',(-4.56748158374851E-35,-4.12455885042696E-32,1.));
#125351=DIRECTION('center_axis',(0.,-4.12699273797265E-32,1.));
#125352=DIRECTION('ref_axis',(0.,-1.,-4.12699273797265E-32));
#125353=DIRECTION('',(4.80241686385389E-35,4.1241763471983E-32,-1.));
#125354=DIRECTION('',(-4.80241686385389E-35,-4.1241763471983E-32,1.));
#125355=DIRECTION('center_axis',(0.,-4.12699273797265E-32,1.));
#125356=DIRECTION('ref_axis',(0.,-1.,-4.12699273797265E-32));
#125357=DIRECTION('',(5.00539285207335E-35,4.12377596731122E-32,-1.));
#125358=DIRECTION('',(-5.00539285207335E-35,-4.12377596731122E-32,1.));
#125359=DIRECTION('center_axis',(0.,-4.12699273797265E-32,1.));
#125360=DIRECTION('ref_axis',(0.,-1.,-4.12699273797265E-32));
#125361=DIRECTION('',(5.17505877669431E-35,4.12336037522781E-32,-1.));
#125362=DIRECTION('',(-5.17505877669431E-35,-4.12336037522781E-32,1.));
#125363=DIRECTION('center_axis',(0.,-4.12699273797265E-32,1.));
#125364=DIRECTION('ref_axis',(0.,-1.,-4.12699273797265E-32));
#125365=DIRECTION('',(5.31028553898035E-35,4.12293233664482E-32,-1.));
#125366=DIRECTION('',(-5.31028553898035E-35,-4.12293233664482E-32,1.));
#125367=DIRECTION('center_axis',(0.,-4.12699273797265E-32,1.));
#125368=DIRECTION('ref_axis',(0.,-1.,-4.12699273797265E-32));
#125369=DIRECTION('',(5.41017322714046E-35,4.12249470008839E-32,-1.));
#125370=DIRECTION('',(-5.41017322714046E-35,-4.12249470008839E-32,1.));
#125371=DIRECTION('center_axis',(0.,-4.12699273797265E-32,1.));
#125372=DIRECTION('ref_axis',(0.,-1.,-4.12699273797265E-32));
#125373=DIRECTION('',(5.47405710508952E-35,4.1220503779576E-32,-1.));
#125374=DIRECTION('',(-5.47405710508952E-35,-4.1220503779576E-32,1.));
#125375=DIRECTION('center_axis',(0.,-4.12699273797265E-32,1.));
#125376=DIRECTION('ref_axis',(0.,-1.,-4.12699273797265E-32));
#125377=DIRECTION('',(5.50151203615979E-35,4.12160232714292E-32,-1.));
#125378=DIRECTION('',(-5.50151203615979E-35,-4.12160232714292E-32,1.));
#125379=DIRECTION('center_axis',(0.,-4.12699273797265E-32,1.));
#125380=DIRECTION('ref_axis',(0.,-1.,-4.12699273797265E-32));
#125381=DIRECTION('',(5.49235531231592E-35,4.12115352934861E-32,-1.));
#125382=DIRECTION('',(-5.49235531231592E-35,-4.12115352934861E-32,1.));
#125383=DIRECTION('center_axis',(0.,-4.12699273797265E-32,1.));
#125384=DIRECTION('ref_axis',(0.,-1.,-4.12699273797265E-32));
#125385=DIRECTION('',(5.44664787004196E-35,4.12070697124994E-32,-1.));
#125386=DIRECTION('',(-5.44664787004196E-35,-4.12070697124994E-32,1.));
#125387=DIRECTION('center_axis',(0.,-4.12699273797265E-32,1.));
#125388=DIRECTION('ref_axis',(0.,-1.,-4.12699273797265E-32));
#125389=DIRECTION('',(5.36469388482745E-35,4.12026562461737E-32,-1.));
#125390=DIRECTION('',(-5.36469388482745E-35,-4.12026562461737E-32,1.));
#125391=DIRECTION('center_axis',(0.,-4.12699273797265E-32,1.));
#125392=DIRECTION('ref_axis',(0.,-1.,-4.12699273797265E-32));
#125393=DIRECTION('',(5.24703874692173E-35,4.11983242653994E-32,-1.));
#125394=DIRECTION('',(-5.24703874692173E-35,-4.11983242653994E-32,1.));
#125395=DIRECTION('center_axis',(0.,-4.12699273797265E-32,1.));
#125396=DIRECTION('ref_axis',(0.,-1.,-4.12699273797265E-32));
#125397=DIRECTION('',(5.09446543185489E-35,4.11941025987936E-32,-1.));
#125398=DIRECTION('',(-5.09446543185489E-35,-4.11941025987936E-32,1.));
#125399=DIRECTION('center_axis',(0.,-4.12699273797265E-32,1.));
#125400=DIRECTION('ref_axis',(0.,-1.,-4.12699273797265E-32));
#125401=DIRECTION('',(4.90798928986758E-35,4.11900193408512E-32,-1.));
#125402=DIRECTION('',(-4.90798928986758E-35,-4.11900193408512E-32,1.));
#125403=DIRECTION('center_axis',(0.,-4.12699273797265E-32,1.));
#125404=DIRECTION('ref_axis',(0.,-1.,-4.12699273797265E-32));
#125405=DIRECTION('',(4.6888512889172E-35,4.11861016649801E-32,-1.));
#125406=DIRECTION('',(-4.6888512889172E-35,-4.11861016649801E-32,1.));
#125407=DIRECTION('center_axis',(0.,-4.12699273797265E-32,1.));
#125408=DIRECTION('ref_axis',(0.,-1.,-4.12699273797265E-32));
#125409=DIRECTION('',(4.43850975624469E-35,4.11823756426669E-32,-1.));
#125410=DIRECTION('',(-4.43850975624469E-35,-4.11823756426669E-32,1.));
#125411=DIRECTION('center_axis',(0.,-4.12699273797265E-32,1.));
#125412=DIRECTION('ref_axis',(0.,-1.,-4.12699273797265E-32));
#125413=DIRECTION('',(4.15863067344775E-35,4.11788660699752E-32,-1.));
#125414=DIRECTION('',(-4.15863067344775E-35,-4.11788660699752E-32,1.));
#125415=DIRECTION('center_axis',(0.,-4.12699273797265E-32,1.));
#125416=DIRECTION('ref_axis',(0.,-1.,-4.12699273797265E-32));
#125417=DIRECTION('',(3.85107658964385E-35,4.11755963025323E-32,-1.));
#125418=DIRECTION('',(-3.85107658964385E-35,-4.11755963025323E-32,1.));
#125419=DIRECTION('center_axis',(0.,-4.12699273797265E-32,1.));
#125420=DIRECTION('ref_axis',(0.,-1.,-4.12699273797265E-32));
#125421=DIRECTION('',(3.51789422651897E-35,4.1172588100101E-32,-1.));
#125422=DIRECTION('',(-3.51789422651897E-35,-4.1172588100101E-32,1.));
#125423=DIRECTION('center_axis',(0.,-4.12699273797265E-32,1.));
#125424=DIRECTION('ref_axis',(0.,-1.,-4.12699273797265E-32));
#125425=DIRECTION('',(3.16130085772864E-35,4.11698614817723E-32,-1.));
#125426=DIRECTION('',(-3.16130085772864E-35,-4.11698614817723E-32,1.));
#125427=DIRECTION('center_axis',(0.,-4.12699273797265E-32,1.));
#125428=DIRECTION('ref_axis',(0.,-1.,-4.12699273797265E-32));
#125429=DIRECTION('',(2.7836695533073E-35,4.11674345927413E-32,-1.));
#125430=DIRECTION('',(-2.7836695533073E-35,-4.11674345927413E-32,1.));
#125431=DIRECTION('center_axis',(0.,-4.12699273797265E-32,1.));
#125432=DIRECTION('ref_axis',(0.,-1.,-4.12699273797265E-32));
#125433=DIRECTION('',(2.38751338728303E-35,4.11653235835539E-32,-1.));
#125434=DIRECTION('',(-2.38751338728303E-35,-4.11653235835539E-32,1.));
#125435=DIRECTION('center_axis',(0.,-4.12699273797265E-32,1.));
#125436=DIRECTION('ref_axis',(0.,-1.,-4.12699273797265E-32));
#125437=DIRECTION('',(1.9754687135784E-35,4.11635425026281E-32,-1.));
#125438=DIRECTION('',(-1.9754687135784E-35,-4.11635425026281E-32,1.));
#125439=DIRECTION('center_axis',(0.,-4.12699273797265E-32,1.));
#125440=DIRECTION('ref_axis',(0.,-1.,-4.12699273797265E-32));
#125441=DIRECTION('',(1.55027762151293E-35,4.11621032027636E-32,-1.));
#125442=DIRECTION('',(-1.55027762151293E-35,-4.11621032027636E-32,1.));
#125443=DIRECTION('center_axis',(0.,-4.12699273797265E-32,1.));
#125444=DIRECTION('ref_axis',(0.,-1.,-4.12699273797265E-32));
#125445=DIRECTION('',(1.11476968765511E-35,4.11610152622635E-32,-1.));
#125446=DIRECTION('',(-1.11476968765511E-35,-4.11610152622635E-32,1.));
#125447=DIRECTION('center_axis',(0.,-4.12699273797265E-32,1.));
#125448=DIRECTION('ref_axis',(0.,-1.,-4.12699273797265E-32));
#125449=DIRECTION('',(6.7184314544985E-36,4.11602859211924E-32,-1.));
#125450=DIRECTION('',(-6.7184314544985E-36,-4.11602859211924E-32,1.));
#125451=DIRECTION('center_axis',(0.,-4.12699273797265E-32,1.));
#125452=DIRECTION('ref_axis',(0.,-1.,-4.12699273797265E-32));
#125453=DIRECTION('',(2.24445597957774E-36,4.11599200331947E-32,-1.));
#125454=DIRECTION('',(-2.24445597957774E-36,-4.11599200331947E-32,1.));
#125455=DIRECTION('center_axis',(0.,-4.12699273797265E-32,1.));
#125456=DIRECTION('ref_axis',(0.,-1.,0.));
#125457=DIRECTION('center_axis',(-0.964116593759479,0.265479120587077,0.000173694938042578));
#125458=DIRECTION('ref_axis',(0.262650981856607,0.953940735958569,-0.14495355810943));
#125459=DIRECTION('center_axis',(0.964117203276892,0.265476906397448,0.000174685963057186));
#125460=DIRECTION('ref_axis',(0.261983001398329,-0.951534581673234,0.161080249746099));
#125461=DIRECTION('center_axis',(0.,-4.12699273797265E-32,1.));
#125462=DIRECTION('ref_axis',(0.,-1.,0.));
#125463=DIRECTION('center_axis',(-0.784008375826398,0.620750220393733,0.000174685963051847));
#125464=DIRECTION('ref_axis',(0.612666106769434,0.77375279952214,0.161080249713102));
#125465=DIRECTION('center_axis',(0.355732454713716,-0.934587818502586,0.000173694938015866));
#125466=DIRECTION('ref_axis',(0.924708188924584,0.351998908103049,0.14495355818357));
#125467=DIRECTION('center_axis',(0.,-4.12699273797265E-32,1.));
#125468=DIRECTION('ref_axis',(0.,-1.,0.));
#125469=DIRECTION('center_axis',(0.278371200818614,-0.960473552152724,0.000173694938036704));
#125470=DIRECTION('ref_axis',(0.950322477522101,0.275455358806153,0.144953558153051));
#125471=DIRECTION('center_axis',(-0.730802746906005,0.682588686252162,0.000174685963045779));
#125472=DIRECTION('ref_axis',(0.67369554717971,0.721240225503635,0.161080249645006));
#125473=DIRECTION('center_axis',(0.,-4.12699273797265E-32,1.));
#125474=DIRECTION('ref_axis',(0.,-1.,0.));
#125475=DIRECTION('center_axis',(0.199157432510043,-0.979967492780284,0.000173694938040826));
#125476=DIRECTION('ref_axis',(0.969612526830206,0.197078699543833,0.144953558080011));
#125477=DIRECTION('center_axis',(-0.672733746278912,0.739884637022796,0.000174685963050579));
#125478=DIRECTION('ref_axis',(0.730241654858009,0.663927916762316,0.161080249732511));
#125479=DIRECTION('center_axis',(0.,-4.12699273797265E-32,1.));
#125480=DIRECTION('ref_axis',(0.,-1.,0.));
#125481=DIRECTION('center_axis',(0.118618304346775,-0.992939911426651,0.00017369493805128));
#125482=DIRECTION('ref_axis',(0.98244996474591,0.117390514049851,0.14495355801729));
#125483=DIRECTION('center_axis',(-0.610187813563555,0.792256777606442,0.000174685963065682));
#125484=DIRECTION('ref_axis',(0.781928124821259,0.602197277291061,0.161080249679293));
#125485=DIRECTION('center_axis',(0.,-4.12699273797265E-32,1.));
#125486=DIRECTION('ref_axis',(0.,-1.,0.));
#125487=DIRECTION('center_axis',(0.0372897909386947,-0.999304478786029,
0.000173694938041732));
#125488=DIRECTION('ref_axis',(0.988749360215715,0.0369211140505736,0.144953558115277));
#125489=DIRECTION('center_axis',(-0.54358118162286,0.83935658004826,0.000174685963067228));
#125490=DIRECTION('ref_axis',(0.828410992105546,0.536459114282095,0.161080249758856));
#125491=DIRECTION('center_axis',(0.,-4.12699273797265E-32,1.));
#125492=DIRECTION('ref_axis',(0.,-1.,0.));
#125493=DIRECTION('center_axis',(-0.0442868798756908,-0.999018839712718,
0.000173694938034547));
#125494=DIRECTION('ref_axis',(0.988468791846664,-0.0437939898697778,0.144953558067689));
#125495=DIRECTION('center_axis',(-0.473357106603132,0.880870602933896,0.000174685963033159));
#125496=DIRECTION('ref_axis',(0.869380920935805,0.467150904390525,0.161080249689174));
#125497=DIRECTION('center_axis',(0.,-4.12699273797265E-32,1.));
#125498=DIRECTION('ref_axis',(0.,-1.,0.));
#125499=DIRECTION('center_axis',(-0.125568828811331,-0.992084895087623,
0.000173694938030051));
#125500=DIRECTION('ref_axis',(0.981610126752954,-0.124217652014093,0.144953558025165));
#125501=DIRECTION('center_axis',(-0.399982918137251,0.916522577290502,0.000174685963062819));
#125502=DIRECTION('ref_axis',(0.904565263167025,0.394733882299028,0.161080249679181));
#125503=DIRECTION('center_axis',(0.,-4.12699273797265E-32,1.));
#125504=DIRECTION('ref_axis',(0.,-1.,0.));
#125505=DIRECTION('center_axis',(-0.206015137908635,-0.978548789168202,
0.000173694938025831));
#125506=DIRECTION('ref_axis',(0.968219008221905,-0.203814666180172,0.144953557968256));
#125507=DIRECTION('center_axis',(-0.323946909343764,0.946075245110788,0.000174685963058239));
#125508=DIRECTION('ref_axis',(0.933729872804219,0.319689971343558,0.16108024973712));
#125509=DIRECTION('center_axis',(0.,-4.12699273797265E-32,1.));
#125510=DIRECTION('ref_axis',(0.,-1.,0.));
#125511=DIRECTION('center_axis',(-0.285090450253219,-0.958500602506063,
0.000173694938036217));
#125512=DIRECTION('ref_axis',(0.948384551914434,-0.282055327364791,0.144953558063258));
#125513=DIRECTION('center_axis',(-0.245755087316061,0.969331938266294,0.000174685963067071));
#125514=DIRECTION('ref_axis',(0.956680664197139,0.242518576376685,0.161080249762494));
#125515=DIRECTION('center_axis',(0.,-4.12699273797265E-32,1.));
#125516=DIRECTION('ref_axis',(0.,-1.,0.));
#125517=DIRECTION('center_axis',(-0.362268532688063,-0.932073752475686,
0.000173694938007782));
#125518=DIRECTION('ref_axis',(0.922238752915758,-0.358418956890768,0.144953557947781));
#125519=DIRECTION('center_axis',(-0.165927805729023,0.986137887301145,0.000174685963059481));
#125520=DIRECTION('ref_axis',(0.973264903614975,0.163733260298146,0.161080249762262));
#125521=DIRECTION('center_axis',(0.,-4.12699273797265E-32,1.));
#125522=DIRECTION('ref_axis',(0.,-1.,0.));
#125523=DIRECTION('center_axis',(-0.437035777807844,-0.899444105403978,
0.000173694938040317));
#125524=DIRECTION('ref_axis',(0.889955607146088,-0.432397367382357,0.144953558045479));
#125525=DIRECTION('center_axis',(-0.0849963019710254,0.996381251397308,
0.000174685963051347));
#125526=DIRECTION('ref_axis',(0.983372225679145,0.0838583263866241,0.16108024974676));
#125527=DIRECTION('center_axis',(0.,-4.12699273797265E-32,1.));
#125528=DIRECTION('ref_axis',(0.,-1.,0.));
#125529=DIRECTION('center_axis',(-0.50889462193225,-0.860828806208587,0.000173694938014614));
#125530=DIRECTION('ref_axis',(0.851749953658509,-0.503498244741079,0.144953558029389));
#125531=DIRECTION('center_axis',(-0.00349916184678272,0.999993862656759,
0.000174685963057099));
#125532=DIRECTION('ref_axis',(0.98693536782401,0.00342532914819454,0.161080249746247));
#125533=DIRECTION('center_axis',(0.,-4.12699273797265E-32,1.));
#125534=DIRECTION('ref_axis',(0.,-1.,0.));
#125535=DIRECTION('center_axis',(-0.577366856309305,-0.816484833334691,
0.000173694938048078));
#125536=DIRECTION('ref_axis',(0.807876044753958,-0.571248424349741,0.144953558047536));
#125537=DIRECTION('center_axis',(0.0780212646221935,0.996951679747603,0.00017468596304852));
#125538=DIRECTION('ref_axis',(0.9839306179374,-0.0770304630912104,0.161080249693373));
#125539=DIRECTION('center_axis',(0.,-4.12699273797265E-32,1.));
#125540=DIRECTION('ref_axis',(0.,-1.,0.));
#125541=DIRECTION('center_axis',(-0.641996809516522,-0.76670728860542,0.000173694938037895));
#125542=DIRECTION('ref_axis',(0.758625854057432,-0.635197039939658,0.14495355810579));
#125543=DIRECTION('center_axis',(0.159022472447753,0.987274947895174,0.000174685963063276));
#125544=DIRECTION('ref_axis',(0.974377972117496,-0.156973630308053,0.161080249689733));
#125545=DIRECTION('center_axis',(0.,-4.12699273797265E-32,1.));
#125546=DIRECTION('ref_axis',(0.,-1.,0.));
#125547=DIRECTION('center_axis',(-0.702354379878435,-0.711827433368262,
0.000173694938018697));
#125548=DIRECTION('ref_axis',(0.704327133475682,-0.694918524035963,0.144953558085365));
#125549=DIRECTION('center_axis',(0.238965411956016,0.971028064153403,0.000174685963061851));
#125550=DIRECTION('ref_axis',(0.958341001655361,-0.235872163914385,0.16108024967868));
#125551=DIRECTION('center_axis',(0.,-4.12699273797265E-32,1.));
#125552=DIRECTION('ref_axis',(0.,-1.,0.));
#125553=DIRECTION('center_axis',(-0.758037897722513,-0.652210484005357,
0.000173694938036324));
#125554=DIRECTION('ref_axis',(0.645341232020346,-0.750015440001797,0.144953558125948));
#125555=DIRECTION('center_axis',(0.317318076074206,0.948319148853053,0.000174685963053342));
#125556=DIRECTION('ref_axis',(0.935926429926839,-0.313201007181146,0.161080249767366));
#125557=DIRECTION('center_axis',(0.,-4.12699273797265E-32,1.));
#125558=DIRECTION('ref_axis',(0.,-1.,0.));
#125559=DIRECTION('center_axis',(-0.808676798424737,-0.588253181478508,
0.000173694938024896));
#125560=DIRECTION('ref_axis',(0.582060691151914,-0.800121126973516,0.144953558032864));
#125561=DIRECTION('center_axis',(0.393559040749975,0.919299326078712,0.000174685963059358));
#125562=DIRECTION('ref_axis',(0.90728342224558,-0.388445549426304,0.161080249718102));
#125563=DIRECTION('center_axis',(0.,-4.12699273797265E-32,1.));
#125564=DIRECTION('ref_axis',(0.,-1.,0.));
#125565=DIRECTION('center_axis',(-0.853934088455684,-0.520381151083923,
0.000173694938054823));
#125566=DIRECTION('ref_axis',(0.514906632408805,-0.844902139846358,0.144953558026248));
#125567=DIRECTION('center_axis',(0.467180934942176,0.884161717963048,0.000174685963059081));
#125568=DIRECTION('ref_axis',(0.872602593079875,-0.461105050630121,0.161080249669756));
#125569=DIRECTION('center_axis',(0.,-4.12699273797265E-32,1.));
#125570=DIRECTION('ref_axis',(0.,-1.,0.));
#125571=DIRECTION('center_axis',(-0.89350858801721,-0.449046069985654,0.000173694938035765));
#125572=DIRECTION('ref_axis',(0.44432595497643,-0.88406046836972,0.144953558080494));
#125573=DIRECTION('center_axis',(0.53769381709176,0.843140159490762,0.000174685963044948));
#125574=DIRECTION('ref_axis',(0.832114737608997,-0.530695973789334,0.161080249744345));
#125575=DIRECTION('center_axis',(0.,-4.12699273797265E-32,1.));
#125576=DIRECTION('ref_axis',(0.,-1.,0.));
#125577=DIRECTION('center_axis',(-0.927136935344019,-0.37472266137901,0.000173694938021475));
#125578=DIRECTION('ref_axis',(0.370788361633148,-0.91733552035926,0.144953557957756));
#125579=DIRECTION('center_axis',(0.604628435601924,0.796507642365335,0.000174685963076138));
#125580=DIRECTION('ref_axis',(0.786089295859101,-0.596755202807269,0.161080249745889));
#125581=DIRECTION('center_axis',(0.,-4.12699273797265E-32,1.));
#125582=DIRECTION('ref_axis',(0.,-1.,0.));
#125583=DIRECTION('center_axis',(-0.95459533933292,-0.297905535285827,0.000173694938038584));
#125584=DIRECTION('ref_axis',(0.294783232905703,-0.944505855777472,0.144953558078881));
#125585=DIRECTION('center_axis',(0.667539351629772,0.744574498294508,0.000174685963094329));
#125586=DIRECTION('ref_axis',(0.734832559538327,-0.658843124405789,0.16108024976877));
#125587=DIRECTION('center_axis',(0.,-4.12699273797265E-32,1.));
#125588=DIRECTION('ref_axis',(0.,-1.,0.));
#125589=DIRECTION('center_axis',(-0.975701068835708,-0.219105897006276,
0.000173694938047038));
#125590=DIRECTION('ref_axis',(0.216816370407067,-0.965390660580497,0.144953558036552));
#125591=DIRECTION('center_axis',(0.726007903408699,0.687686333783738,0.000174685963071939));
#125592=DIRECTION('ref_axis',(0.678685633776137,-0.716546553715493,0.161080249764932));
#125593=DIRECTION('center_axis',(0.,-4.12699273797265E-32,1.));
#125594=DIRECTION('ref_axis',(0.,-1.,0.));
#125595=DIRECTION('center_axis',(-0.990313668704752,-0.138848145132025,
0.000173694938038594));
#125596=DIRECTION('ref_axis',(0.137406630733052,-0.979850949805316,0.144953558066752));
#125597=DIRECTION('center_axis',(0.779644992373389,0.62622173018182,0.000174685963098564));
#125598=DIRECTION('ref_axis',(0.618022167103482,-0.7694814839412,0.161080249690531));
#125599=DIRECTION('center_axis',(0.,-4.12699273797265E-32,1.));
#125600=DIRECTION('ref_axis',(0.,-1.,0.));
#125601=DIRECTION('center_axis',(-0.998335894498814,-0.05766638176027,0.000173694938032902));
#125602=DIRECTION('ref_axis',(0.0570824726036373,-0.987790492638966,0.144953557988494));
#125603=DIRECTION('center_axis',(0.828093672546161,0.560589724284905,0.000174685963077943));
#125604=DIRECTION('ref_axis',(0.553245864863052,-0.817295641832221,0.161080249732829));
#125605=DIRECTION('center_axis',(0.,-4.12699273797265E-32,1.));
#125606=DIRECTION('ref_axis',(0.,-1.,0.));
#125607=DIRECTION('center_axis',(-0.999714359628814,0.0238991418678133,
0.000173694938034033));
#125608=DIRECTION('ref_axis',(0.0236215599645613,0.989156452705798,-0.144953557994702));
#125609=DIRECTION('center_axis',(0.871031525953977,0.491227086263675,0.000174685963068119));
#125610=DIRECTION('ref_axis',(0.484787802678601,-0.859670832082115,0.161080249693429));
#125611=DIRECTION('center_axis',(0.,-4.12699273797265E-32,1.));
#125612=DIRECTION('ref_axis',(0.,-1.,0.));
#125613=DIRECTION('center_axis',(-0.994439890636744,0.105305620649848,0.000173694938035152));
#125614=DIRECTION('ref_axis',(0.104168394946778,0.983939739764692,-0.144953558100528));
#125615=DIRECTION('center_axis',(0.908172808266673,0.4185954130301,0.000174685963064905));
#125616=DIRECTION('ref_axis',(0.413103557643788,-0.896325054765691,0.161080249755599));
#125617=DIRECTION('center_axis',(0.,-4.12699273797265E-32,1.));
#125618=DIRECTION('ref_axis',(0.,-1.,0.));
#125619=DIRECTION('center_axis',(-0.982547588243519,0.186011307900658,0.000173694938032103));
#125620=DIRECTION('ref_axis',(0.184022006446546,0.972175070204138,-0.144953558138347));
#125621=DIRECTION('center_axis',(0.939270350378314,0.343178056386206,0.000174685963062408));
#125622=DIRECTION('ref_axis',(0.338670176597351,-0.927014382107848,0.161080249716481));
#125623=DIRECTION('center_axis',(0.,-4.12699273797265E-32,1.));
#125624=DIRECTION('ref_axis',(0.,-1.,0.));
#125625=DIRECTION('center_axis',(-0.939269562412001,0.343180213526999,0.000173694938031579));
#125626=DIRECTION('ref_axis',(0.339532058317171,0.929358083503298,-0.144953558086661));
#125627=DIRECTION('center_axis',(0.982548015255807,0.186009051397209,0.000174685963063537));
#125628=DIRECTION('ref_axis',(0.183552372552309,-0.969722475602179,0.161080249696849));
#125629=DIRECTION('center_axis',(0.,-4.12699273797265E-32,1.));
#125630=DIRECTION('ref_axis',(0.,-1.,0.));
#125631=DIRECTION('center_axis',(-0.908171847095246,0.418597498766629,0.000173694938032065));
#125632=DIRECTION('ref_axis',(0.414153604942779,0.898590706322032,-0.144953558164584));
#125633=DIRECTION('center_axis',(0.994440132302203,0.105303336849277,0.000174685963054474));
#125634=DIRECTION('ref_axis',(0.103900232948935,-0.981457026442032,0.161080249691642));
#125635=DIRECTION('center_axis',(0.,-4.12699273797265E-32,1.));
#125636=DIRECTION('ref_axis',(0.,-1.,0.));
#125637=DIRECTION('center_axis',(-0.871030397973873,0.491229086715704,0.000173694938031785));
#125638=DIRECTION('ref_axis',(0.48601902766875,0.861843356269927,-0.144953558070544));
#125639=DIRECTION('center_axis',(0.999714414339203,0.0238968459684036,0.000174685963064245));
#125640=DIRECTION('ref_axis',(0.0235566544373952,-0.986660142698139,0.161080249697491));
#125641=DIRECTION('center_axis',(0.,-4.12699273797265E-32,1.));
#125642=DIRECTION('ref_axis',(0.,-1.,0.));
#125643=DIRECTION('center_axis',(-0.828092385263878,0.560591626139786,0.000173694938011966));
#125644=DIRECTION('ref_axis',(0.554650073944248,0.81936058085897,-0.144953558107731));
#125645=DIRECTION('center_axis',(0.998335761890044,-0.0576686744796514,
0.000174685963059713));
#125646=DIRECTION('ref_axis',(0.0569436897224966,0.985297198489207,-0.161080249720776));
#125647=DIRECTION('center_axis',(0.,-4.12699273797265E-32,1.));
#125648=DIRECTION('ref_axis',(0.,-1.,0.));
#125649=DIRECTION('center_axis',(-0.779643554355606,0.626223520782975,0.000173694938038147));
#125650=DIRECTION('ref_axis',(0.619590015495319,0.771425095977384,-0.144953558061866));
#125651=DIRECTION('center_axis',(0.990313349659314,-0.138850419413709,0.000174685963050317));
#125652=DIRECTION('ref_axis',(0.137065083024103,0.977377264004113,-0.161080249637969));
#125653=DIRECTION('center_axis',(0.,-4.12699273797265E-32,1.));
#125654=DIRECTION('ref_axis',(0.,-1.,0.));
#125655=DIRECTION('center_axis',(-0.726006324225229,0.68768800121497,0.000173694938033376));
#125656=DIRECTION('ref_axis',(0.68040668771909,0.718355904357349,-0.144953558017983));
#125657=DIRECTION('center_axis',(0.9757005654768,-0.219108137715302,0.000174685963060536));
#125658=DIRECTION('ref_axis',(0.216274330807799,0.962953045052486,-0.1610802497446));
#125659=DIRECTION('center_axis',(0.,-4.12699273797265E-32,1.));
#125660=DIRECTION('ref_axis',(0.,-1.,0.));
#125661=DIRECTION('center_axis',(-0.66753764178975,0.744576031459413,0.000173694938049494));
#125662=DIRECTION('ref_axis',(0.736695365690809,0.660506172708796,-0.144953558022086));
#125663=DIRECTION('center_axis',(0.954594655010301,-0.297907727510681,0.000174685963056511));
#125664=DIRECTION('ref_axis',(0.294044308610184,0.942120532495689,-0.161080249639732));
#125665=DIRECTION('center_axis',(0.,-4.12699273797265E-32,1.));
#125666=DIRECTION('ref_axis',(0.,-1.,0.));
#125667=DIRECTION('center_axis',(-0.604626606484044,0.796509031060953,0.000173694938017039));
#125668=DIRECTION('ref_axis',(0.788081457547906,0.598260881455095,-0.144953558044432));
#125669=DIRECTION('center_axis',(0.927136074611733,-0.374724790530812,0.000174685963067698));
#125670=DIRECTION('ref_axis',(0.369857470042992,0.915018363202569,-0.161080249737478));
#125671=DIRECTION('center_axis',(0.,-4.12699273797265E-32,1.));
#125672=DIRECTION('ref_axis',(0.,-1.,0.));
#125673=DIRECTION('center_axis',(-0.53769188086865,0.843141394475448,0.000173694938039761));
#125674=DIRECTION('ref_axis',(0.834222997314027,0.532034262732468,-0.144953558187165));
#125675=DIRECTION('center_axis',(0.893507556603344,-0.449048121895122,0.000174685963043604));
#125676=DIRECTION('ref_axis',(0.443209291040966,0.881826897687926,-0.161080249717502));
#125677=DIRECTION('center_axis',(0.,-4.12699273797265E-32,1.));
#125678=DIRECTION('ref_axis',(0.,-1.,0.));
#125679=DIRECTION('center_axis',(-0.467178904498963,0.88416279101827,0.000173694938045996));
#125680=DIRECTION('ref_axis',(0.874812920690553,0.462267043785389,-0.144953558158402));
#125681=DIRECTION('center_axis',(0.853932893224105,-0.520383112096006,0.000174685963043952));
#125682=DIRECTION('ref_axis',(0.513611627330155,0.842767019657086,-0.161080249719146));
#125683=DIRECTION('center_axis',(0.,-4.12699273797265E-32,1.));
#125684=DIRECTION('ref_axis',(0.,-1.,0.));
#125685=DIRECTION('center_axis',(-0.393556929598893,0.919300230063476,0.000173694938030032));
#125686=DIRECTION('ref_axis',(0.909581108427159,0.389423513935497,-0.144953558033427));
#125687=DIRECTION('center_axis',(0.808675447329435,-0.588255038543107,0.000174685963058817));
#125688=DIRECTION('ref_axis',(0.580595962980463,0.798098666158617,-0.161080249709967));
#125689=DIRECTION('center_axis',(0.,-4.12699273797265E-32,1.));
#125690=DIRECTION('ref_axis',(0.,-1.,0.));
#125691=DIRECTION('center_axis',(-0.317315898264684,0.948319877751461,0.000173694938030787));
#125692=DIRECTION('ref_axis',(0.938296183923317,0.313988434836218,-0.144953558162752));
#125693=DIRECTION('center_axis',(0.758036399754929,-0.652212224763841,0.000174685963032238));
#125694=DIRECTION('ref_axis',(0.643716528291106,0.748119097716493,-0.161080249679177));
#125695=DIRECTION('center_axis',(0.,-4.12699273797265E-32,1.));
#125696=DIRECTION('ref_axis',(0.,-1.,0.));
#125697=DIRECTION('center_axis',(-0.238963181980971,0.971028613114772,0.000173694938030256));
#125698=DIRECTION('ref_axis',(0.960767053149991,0.236463814517229,-0.1449535580986));
#125699=DIRECTION('center_axis',(0.702352745007179,-0.71182904623631,0.000174685963053707));
#125700=DIRECTION('ref_axis',(0.702553266302939,0.693160920100014,-0.161080249730294));
#125701=DIRECTION('center_axis',(0.,-4.12699273797265E-32,1.));
#125702=DIRECTION('ref_axis',(0.,-1.,0.));
#125703=DIRECTION('center_axis',(-0.159020205147339,0.987275313266247,0.000173694938038525));
#125704=DIRECTION('ref_axis',(0.976844176148955,0.157365566524177,-0.144953558067387));
#125705=DIRECTION('center_axis',(0.641995048621441,-0.766708762849602,0.000174685963078827));
#125706=DIRECTION('ref_axis',(0.756714628244622,0.633589870928856,-0.16108024974204));
#125707=DIRECTION('center_axis',(0.,-4.12699273797265E-32,1.));
#125708=DIRECTION('ref_axis',(0.,-1.,0.));
#125709=DIRECTION('center_axis',(-0.0780189750849014,0.996951859096902,
0.000173694938032577));
#125710=DIRECTION('ref_axis',(0.986420562298587,0.0772200766466855,-0.144953558208202));
#125711=DIRECTION('center_axis',(0.577364981108916,-0.816486159144119,0.000174685963063083));
#125712=DIRECTION('ref_axis',(0.80584017919105,0.569802385706794,-0.161080249702384));
#125713=DIRECTION('center_axis',(0.,-4.12699273797265E-32,1.));
#125714=DIRECTION('ref_axis',(0.,-1.,0.));
#125715=DIRECTION('center_axis',(0.00350145838446337,0.999993854790743,
0.000173694938039412));
#125716=DIRECTION('ref_axis',(0.989432482391681,-0.00343930009725844,-0.144953558090438));
#125717=DIRECTION('center_axis',(0.508892644905654,-0.860829974760256,0.000174685963037557));
#125718=DIRECTION('ref_axis',(0.849602996695427,0.502222959615186,-0.161080249694099));
#125719=DIRECTION('center_axis',(0.,-4.12699273797265E-32,1.));
#125720=DIRECTION('ref_axis',(0.,-1.,0.));
#125721=DIRECTION('center_axis',(0.0849985902259986,0.996381056368326,0.000173694938038034));
#125722=DIRECTION('ref_axis',(0.98585989253223,-0.0840757888669896,-0.144953558158235));
#125723=DIRECTION('center_axis',(0.437033712111826,-0.899445108921368,0.000174685963056523));
#125724=DIRECTION('ref_axis',(0.887711846418836,0.431301322581788,-0.161080249772778));
#125725=DIRECTION('center_axis',(0.,-4.12699273797265E-32,1.));
#125726=DIRECTION('ref_axis',(0.,-1.,0.));
#125727=DIRECTION('center_axis',(0.165930070473371,0.986137506407078,0.000173694938036312));
#125728=DIRECTION('ref_axis',(0.975726567763563,-0.164152767135129,-0.144953558087466));
#125729=DIRECTION('center_axis',(0.362266392069445,-0.932074584280572,0.000174685963047641));
#125730=DIRECTION('ref_axis',(0.919913120284889,0.357509446415818,-0.161080249724085));
#125731=DIRECTION('center_axis',(0.,-4.12699273797265E-32,1.));
#125732=DIRECTION('ref_axis',(0.,-1.,0.));
#125733=DIRECTION('center_axis',(0.245757313478258,0.969331374041931,0.000173694938041656));
#125734=DIRECTION('ref_axis',(0.95909994365823,-0.243137335820007,-0.144953558097514));
#125735=DIRECTION('center_axis',(0.28508824895752,-0.958501257062895,0.000174685963072556));
#125736=DIRECTION('ref_axis',(0.945992524106419,0.281338403866232,-0.161080249704198));
#125737=DIRECTION('center_axis',(0.,-4.12699273797265E-32,1.));
#125738=DIRECTION('ref_axis',(0.,-1.,0.));
#125739=DIRECTION('center_axis',(0.323949082109054,0.946074501310954,0.000173694938040627));
#125740=DIRECTION('ref_axis',(0.936090667680424,-0.320503865653793,-0.144953558019777));
#125741=DIRECTION('center_axis',(0.206012890585117,-0.978549262121013,0.000174685963054924));
#125742=DIRECTION('ref_axis',(0.965776503747655,0.203295100653895,-0.161080249748623));
#125743=DIRECTION('center_axis',(0.,-4.12699273797265E-32,1.));
#125744=DIRECTION('ref_axis',(0.,-1.,0.));
#125745=DIRECTION('center_axis',(0.399985023046293,0.91652165886504,0.000173694938024144));
#125746=DIRECTION('ref_axis',(0.906851862735966,-0.395737495135554,-0.144953558066528));
#125747=DIRECTION('center_axis',(0.125566550415584,-0.992085183288988,0.000174685963050411));
#125748=DIRECTION('ref_axis',(0.979133400098864,0.123898902089266,-0.161080249788461));
#125749=DIRECTION('center_axis',(0.,-4.12699273797265E-32,1.));
#125750=DIRECTION('ref_axis',(0.,-1.,0.));
#125751=DIRECTION('center_axis',(0.473359129647977,0.880869515994837,0.000173694938041029));
#125752=DIRECTION('ref_axis',(0.871578108263211,-0.468337556876952,-0.144953558131046));
#125753=DIRECTION('center_axis',(0.044284585570049,-0.999018941244711,0.000174685963050208));
#125754=DIRECTION('ref_axis',(0.985974325245433,0.0436781767754032,-0.161080249659572));
#125755=DIRECTION('center_axis',(0.,-4.12699273797265E-32,1.));
#125756=DIRECTION('ref_axis',(0.,-1.,0.));
#125757=DIRECTION('center_axis',(0.543583109340639,0.839355331828917,0.00017369493803777));
#125758=DIRECTION('ref_axis',(0.830504145292599,-0.537820909453829,-0.144953558100746));
#125759=DIRECTION('center_axis',(-0.0372920858860229,-0.999304392972974,
0.00017468596305223));
#125760=DIRECTION('ref_axis',(0.986253753914206,-0.0368332196013007,-0.16108024963955));
#125761=DIRECTION('center_axis',(0.,-4.12699273797265E-32,1.));
#125762=DIRECTION('ref_axis',(0.,-1.,0.));
#125763=DIRECTION('center_axis',(0.610189633125563,0.79225537641354,0.000173694938026845));
#125764=DIRECTION('ref_axis',(0.783903314256242,-0.603725152611619,-0.14495355808726));
#125765=DIRECTION('center_axis',(-0.118620584663302,-0.992939638839618,
0.000174685963056815));
#125766=DIRECTION('ref_axis',(0.979969826540933,-0.117099496975594,-0.161080249805483));
#125767=DIRECTION('center_axis',(0.,-4.12699273797265E-32,1.));
#125768=DIRECTION('ref_axis',(0.,-1.,0.));
#125769=DIRECTION('center_axis',(0.672735445576227,0.739883092181072,0.000173694938022371));
#125770=DIRECTION('ref_axis',(0.732085735994742,-0.665611704483453,-0.144953558106277));
#125771=DIRECTION('center_axis',(-0.199159683020644,-0.979967035233293,
0.000174685963060404));
#125772=DIRECTION('ref_axis',(0.967164361690274,-0.196586496520054,-0.161080249758361));
#125773=DIRECTION('center_axis',(0.,-4.12699273797265E-32,1.));
#125774=DIRECTION('ref_axis',(0.,-1.,0.));
#125775=DIRECTION('center_axis',(0.730804314630066,0.682587008042307,0.000173694938039999));
#125776=DIRECTION('ref_axis',(0.675396247952083,-0.723068720286077,-0.144953558066381));
#125777=DIRECTION('center_axis',(-0.278373406546575,-0.960472912690654,
0.000174685963093089));
#125778=DIRECTION('ref_axis',(0.947922577585518,-0.274765245366625,-0.161080249696373));
#125779=DIRECTION('center_axis',(0.,-4.12699273797265E-32,1.));
#125780=DIRECTION('ref_axis',(0.,-1.,0.));
#125781=DIRECTION('center_axis',(0.784009801544307,0.620748419983913,0.000173694938043742));
#125782=DIRECTION('ref_axis',(0.614212109297605,-0.775713833036737,-0.144953558175163));
#125783=DIRECTION('center_axis',(-0.355734600980206,-0.934587001380967,
0.000174685963059907));
#125784=DIRECTION('ref_axis',(0.922372525104978,-0.351115476833086,-0.161080249750679));
#125785=DIRECTION('center_axis',(0.,-4.12699273797265E-32,1.));
#125786=DIRECTION('ref_axis',(0.,-1.,0.));
#125787=DIRECTION('center_axis',(0.831997832581782,0.554778853606809,0.000173694938052519));
#125788=DIRECTION('ref_axis',(0.548940490414457,-0.823196698238963,-0.14495355805224));
#125789=DIRECTION('center_axis',(-0.430728440336455,-0.902481567773071,
0.000174685963073157));
#125790=DIRECTION('ref_axis',(0.890684235670549,-0.42512909273917,-0.161080249673074));
#125791=DIRECTION('center_axis',(0.,-4.12699273797265E-32,1.));
#125792=DIRECTION('ref_axis',(0.,-1.,0.));
#125793=DIRECTION('center_axis',(0.874449055313417,0.485117325491,0.000173694938044398));
#125794=DIRECTION('ref_axis',(0.480015763116306,-0.865201325202067,-0.144953558177983));
#125795=DIRECTION('center_axis',(-0.502855852987447,-0.864370268230624,
0.000174685963069477));
#125796=DIRECTION('ref_axis',(0.853068589594169,-0.496313544673254,-0.161080249632552));
#125797=DIRECTION('center_axis',(0.,-4.12699273797265E-32,1.));
#125798=DIRECTION('ref_axis',(0.,-1.,0.));
#125799=DIRECTION('center_axis',(0.911080963855876,0.412227421612775,0.000173694938031732));
#125800=DIRECTION('ref_axis',(0.407896610121612,-0.901448180108941,-0.144953558181837));
#125801=DIRECTION('center_axis',(-0.57163684290217,-0.820506727164168,0.000174685963066123));
#125802=DIRECTION('ref_axis',(0.809775912776532,-0.564195111838173,-0.161080249766526));
#125803=DIRECTION('center_axis',(0.,-4.12699273797265E-32,1.));
#125804=DIRECTION('ref_axis',(0.,-1.,0.));
#125805=DIRECTION('center_axis',(0.941649778901648,0.336594212256459,0.00017369493803296));
#125806=DIRECTION('ref_axis',(0.333062972491066,-0.931696046123075,-0.144953558059274));
#125807=DIRECTION('center_axis',(-0.63661368394079,-0.771182849202542,0.00017468596305796));
#125808=DIRECTION('ref_axis',(0.761094310895386,-0.628322053641482,-0.16108024965969));
#125809=DIRECTION('center_axis',(0.,-4.12699273797265E-32,1.));
#125810=DIRECTION('ref_axis',(0.,-1.,0.));
#125811=DIRECTION('center_axis',(0.965952070030099,0.258721023951739,0.000173694938034315));
#125812=DIRECTION('ref_axis',(0.256012855721305,-0.955743628647454,-0.144953558097827));
#125813=DIRECTION('center_axis',(-0.697353965946701,-0.716726876615648,
0.000174685963046821));
#125814=DIRECTION('ref_axis',(0.707347751921464,-0.688267615822936,-0.161080249754778));
#125815=DIRECTION('center_axis',(0.,-4.12699273797265E-32,1.));
#125816=DIRECTION('ref_axis',(0.,-1.,0.));
#125817=DIRECTION('center_axis',(0.983826109503387,0.179126089918523,0.000173694938024096));
#125818=DIRECTION('ref_axis',(0.177259015639969,-0.973430895027676,-0.144953558010722));
#125819=DIRECTION('center_axis',(-0.753453472364535,-0.657501204916493,
0.000174685963058063));
#125820=DIRECTION('ref_axis',(0.648893910389724,-0.743632870604353,-0.161080249614477));
#125821=DIRECTION('center_axis',(0.,-4.12699273797265E-32,1.));
#125822=DIRECTION('ref_axis',(0.,-1.,0.));
#125823=DIRECTION('center_axis',(0.995152948537796,0.0983391013107115,0.000173694938042572));
#125824=DIRECTION('ref_axis',(0.0973255460498904,-0.984640139371994,-0.144953558161193));
#125825=DIRECTION('center_axis',(-0.804538870234896,-0.593899971178624,
0.000174685963083651));
#125826=DIRECTION('ref_axis',(0.586121786917812,-0.794049371293258,-0.161080249717499));
#125827=DIRECTION('center_axis',(0.,-4.12699273797265E-32,1.));
#125828=DIRECTION('ref_axis',(0.,-1.,0.));
#125829=DIRECTION('center_axis',(0.999857208888375,0.0168976822084356,0.000173694938038329));
#125830=DIRECTION('ref_axis',(0.0167443910123756,-0.989296766069278,-0.144953558129814));
#125831=DIRECTION('center_axis',(-0.850270194663315,-0.526346431119299,
0.00017468596304367));
#125832=DIRECTION('ref_axis',(0.519449119674191,-0.839181604446911,-0.161080249650962));
#125833=DIRECTION('center_axis',(0.,-4.12699273797265E-32,1.));
#125834=DIRECTION('ref_axis',(0.,-1.,0.));
#125835=DIRECTION('center_axis',(0.997907584478628,-0.0646561881810041,
0.00017369493803715));
#125836=DIRECTION('ref_axis',(0.0639481951858162,0.98736978601666,0.144953558058749));
#125837=DIRECTION('center_axis',(-0.890343111231032,-0.455290142401809,
0.000174685963060243));
#125838=DIRECTION('ref_axis',(0.449319604233089,-0.878729222464582,-0.16108024968509));
#125839=DIRECTION('center_axis',(0.,-4.12699273797265E-32,1.));
#125840=DIRECTION('ref_axis',(0.,-1.,0.));
#125841=DIRECTION('center_axis',(-0.831996558357966,0.554780764235129,0.000174685963036686));
#125842=DIRECTION('ref_axis',(0.547559474507209,0.8211161763256,0.161080249732285));
#125843=DIRECTION('center_axis',(0.430726367814519,-0.902482557116413,0.00017369493803426));
#125844=DIRECTION('ref_axis',(0.892940119914814,0.426199962750572,0.144953558072679));
#125845=DIRECTION('center_axis',(0.,-4.12699273797265E-32,1.));
#125846=DIRECTION('ref_axis',(0.,-1.,0.));
#125847=DIRECTION('center_axis',(-0.874447941063388,0.485119333622992,0.00017468596306053));
#125848=DIRECTION('ref_axis',(0.47880892428474,0.863015160451995,0.161080249736917));
#125849=DIRECTION('center_axis',(0.502853868002302,-0.8643714232118,0.000173694938021085));
#125850=DIRECTION('ref_axis',(0.855229681726789,0.497564726964118,0.144953557992271));
#125851=DIRECTION('center_axis',(0.,-4.12699273797265E-32,1.));
#125852=DIRECTION('ref_axis',(0.,-1.,0.));
#125853=DIRECTION('center_axis',(-0.911080016994841,0.412229513884554,0.000174685963026989));
#125854=DIRECTION('ref_axis',(0.406871979675512,0.89917092108733,0.161080249645609));
#125855=DIRECTION('center_axis',(0.571634958663587,-0.820508040096956,0.000173694938017433));
#125856=DIRECTION('ref_axis',(0.811827831091178,0.565618280001494,0.144953558058938));
#125857=DIRECTION('center_axis',(0.,-4.12699273797265E-32,1.));
#125858=DIRECTION('ref_axis',(0.,-1.,0.));
#125859=DIRECTION('center_axis',(-0.941649005730778,0.33659637474437,0.000174685963048853));
#125860=DIRECTION('ref_axis',(0.332227369159855,0.929342847572107,0.16108024971327));
#125861=DIRECTION('center_axis',(0.636611912988104,-0.77118431134956,0.000173694938013388));
#125862=DIRECTION('ref_axis',(0.763023400189289,0.629907736710017,0.144953558067543));
#125863=DIRECTION('center_axis',(0.,-4.12699273797265E-32,1.));
#125864=DIRECTION('ref_axis',(0.,-1.,0.));
#125865=DIRECTION('center_axis',(-0.965951475694722,0.258723242264785,0.000174685963070544));
#125866=DIRECTION('ref_axis',(0.255371840321265,0.953330150749369,0.161080249699075));
#125867=DIRECTION('center_axis',(0.697352320065293,-0.716728478246555,0.00017369493803279));
#125868=DIRECTION('ref_axis',(0.70914117443807,0.690005261347236,0.144953558182362));
#125869=DIRECTION('center_axis',(0.,-4.12699273797265E-32,1.));
#125870=DIRECTION('ref_axis',(0.,-1.,0.));
#125871=DIRECTION('center_axis',(-0.983825697958711,0.179128349294213,0.000174685963070963));
#125872=DIRECTION('ref_axis',(0.176816854017924,0.970973199059766,0.161080249698242));
#125873=DIRECTION('center_axis',(0.753451962507452,-0.657502935372716,0.000173694938036256));
#125874=DIRECTION('ref_axis',(0.650539731194123,0.745510914835243,0.14495355807774));
#125875=DIRECTION('center_axis',(0.,-4.12699273797265E-32,1.));
#125876=DIRECTION('ref_axis',(0.,-1.,0.));
#125877=DIRECTION('center_axis',(-0.9951527225226,0.0983413867131789,0.000174685963064377));
#125878=DIRECTION('ref_axis',(0.0970851807228342,0.982154580919935,0.161080249757698));
#125879=DIRECTION('center_axis',(0.804537506449909,-0.59390181894437,0.000173694938015236));
#125880=DIRECTION('ref_axis',(0.58760905336439,0.796055316181374,0.144953558023174));
#125881=DIRECTION('center_axis',(0.,-4.12699273797265E-32,1.));
#125882=DIRECTION('ref_axis',(0.,-1.,0.));
#125883=DIRECTION('center_axis',(-0.999857169906744,0.0168999784287159,
0.000174685963049014));
#125884=DIRECTION('ref_axis',(0.0167074215697249,0.98679988610253,0.161080249728283));
#125885=DIRECTION('center_axis',(0.85026898602633,-0.526348383897799,0.000173694938027909));
#125886=DIRECTION('ref_axis',(0.520767934225771,0.841302100728855,0.144953558050291));
#125887=DIRECTION('center_axis',(0.,-4.12699273797265E-32,1.));
#125888=DIRECTION('ref_axis',(0.,-1.,0.));
#125889=DIRECTION('center_axis',(-0.997907732789978,-0.0646538964238091,
0.0001746859630669));
#125890=DIRECTION('ref_axis',(0.0637815227177578,-0.984878200848485,-0.161080249730545));
#125891=DIRECTION('center_axis',(0.890342065785251,-0.455292187197761,0.000173694938023638));
#125892=DIRECTION('ref_axis',(0.450461190401379,0.880950158591516,0.144953558147968));
#125893=DIRECTION('center_axis',(0.,-4.12699273797265E-32,1.));
#125894=DIRECTION('ref_axis',(0.,-1.,0.));
#125895=DIRECTION('center_axis',(-0.989317384354678,-0.145777510262838,
0.000174685963054987));
#125896=DIRECTION('ref_axis',(0.143846011496079,-0.976402313670072,-0.161080249678226));
#125897=DIRECTION('center_axis',(0.924490065992462,-0.381206096109862,0.000173694938023807));
#125898=DIRECTION('ref_axis',(0.37715670168693,0.914735638516238,0.144953558083019));
#125899=DIRECTION('center_axis',(0.,-4.12699273797265E-32,1.));
#125900=DIRECTION('ref_axis',(0.,-1.,0.));
#125901=DIRECTION('center_axis',(-0.974143291952382,-0.225930998822629,
0.00017468596306252));
#125902=DIRECTION('ref_axis',(0.222953228798234,-0.961428630172209,-0.161080249731719));
#125903=DIRECTION('center_axis',(0.952485737340632,-0.304583141346891,0.000173694938041347));
#125904=DIRECTION('ref_axis',(0.301342297345122,0.942433703679797,0.144953558076867));
#125905=DIRECTION('center_axis',(0.,-4.12699273797265E-32,1.));
#125906=DIRECTION('ref_axis',(0.,-1.,0.));
#125907=DIRECTION('center_axis',(0.989317049737339,-0.145779782305628,0.000173694938037687));
#125908=DIRECTION('ref_axis',(0.144215216694403,0.97887202292198,0.144953558129552));
#125909=DIRECTION('center_axis',(-0.92449094128977,-0.38120397290423,0.000174685963069724));
#125910=DIRECTION('ref_axis',(0.376199940957144,-0.912429042481591,-0.161080249751384));
#125911=DIRECTION('center_axis',(0.,0.,1.));
#125912=DIRECTION('ref_axis',(1.,0.,0.));
#125913=DIRECTION('',(0.,0.,1.));
#125914=DIRECTION('',(0.,0.,1.));
#125915=DIRECTION('center_axis',(0.,-0.3396732719682,-0.940543496235245));
#125916=DIRECTION('ref_axis',(0.000119202233163679,0.940543489553072,-0.339673269554962));
#125917=DIRECTION('center_axis',(0.,-0.3396732719682,-0.940543496235245));
#125918=DIRECTION('ref_axis',(0.000119202233163679,0.940543489553072,-0.339673269554962));
#125919=DIRECTION('center_axis',(-0.923076923076923,-0.384615384615384,
0.));
#125920=DIRECTION('ref_axis',(0.384615384615384,-0.923076923076923,0.));
#125921=DIRECTION('center_axis',(0.923076923076904,0.384615384615431,2.59253294309151E-14));
#125922=DIRECTION('ref_axis',(0.381730136921527,-0.916152328611528,-0.122257978658025));
#125923=DIRECTION('',(0.281464519857291,-0.675514847657501,0.68151112584885));
#125924=DIRECTION('',(1.46520452235715E-32,-3.51649085365717E-32,1.));
#125925=DIRECTION('center_axis',(0.923076923076923,-0.384615384615384,0.));
#125926=DIRECTION('ref_axis',(0.384615384615384,0.923076923076923,0.));
#125927=DIRECTION('',(0.281464519857292,0.675514847657501,-0.68151112584885));
#125928=DIRECTION('center_axis',(-0.92307507402904,0.384619822294333,2.13514021449077E-6));
#125929=DIRECTION('ref_axis',(0.381364544927114,0.915263234831132,-0.129824091905111));
#125930=DIRECTION('',(1.46520452235715E-32,3.51649085365717E-32,-1.));
#125931=DIRECTION('center_axis',(0.,-4.12699273797265E-32,1.));
#125932=DIRECTION('ref_axis',(0.,-1.,-4.12699273797265E-32));
#125933=DIRECTION('center_axis',(0.,4.12699273797265E-32,-1.));
#125934=DIRECTION('ref_axis',(0.,1.,4.12699273797265E-32));
#125935=DIRECTION('',(-0.866025403784439,0.5,0.));
#125936=DIRECTION('',(4.50694379621149E-16,1.,0.));
#125937=DIRECTION('center_axis',(0.,4.12699273797265E-32,-1.));
#125938=DIRECTION('ref_axis',(0.,1.,4.12699273797265E-32));
#125939=DIRECTION('',(4.50694379621149E-16,1.,0.));
#125940=DIRECTION('',(0.866025403784439,0.5,0.));
#125941=DIRECTION('center_axis',(0.,4.12699273797265E-32,-1.));
#125942=DIRECTION('ref_axis',(0.,1.,4.12699273797265E-32));
#125943=DIRECTION('',(0.866025403784439,0.5,0.));
#125944=DIRECTION('',(0.866025403784439,-0.5,0.));
#125945=DIRECTION('center_axis',(0.,4.12699273797265E-32,-1.));
#125946=DIRECTION('ref_axis',(0.,1.,4.12699273797265E-32));
#125947=DIRECTION('',(0.866025403784439,-0.5,0.));
#125948=DIRECTION('',(0.,-1.,0.));
#125949=DIRECTION('center_axis',(0.,4.12699273797265E-32,-1.));
#125950=DIRECTION('ref_axis',(0.,1.,4.12699273797265E-32));
#125951=DIRECTION('',(0.,-1.,0.));
#125952=DIRECTION('',(-0.866025403784439,-0.5,0.));
#125953=DIRECTION('center_axis',(0.,4.12699273797265E-32,-1.));
#125954=DIRECTION('ref_axis',(0.,1.,4.12699273797265E-32));
#125955=DIRECTION('center_axis',(0.,0.,1.));
#125956=DIRECTION('ref_axis',(1.,0.,0.));
#125957=DIRECTION('center_axis',(0.,0.,1.));
#125958=DIRECTION('ref_axis',(1.,0.,0.));
#125959=DIRECTION('center_axis',(0.,0.,1.));
#125960=DIRECTION('ref_axis',(1.,0.,0.));
#125961=DIRECTION('center_axis',(0.,0.,1.));
#125962=DIRECTION('ref_axis',(1.,0.,0.));
#125963=DIRECTION('center_axis',(0.,0.,1.));
#125964=DIRECTION('ref_axis',(1.,0.,0.));
#125965=DIRECTION('center_axis',(0.,-4.12699273797265E-32,1.));
#125966=DIRECTION('ref_axis',(0.,-1.,0.));
#125967=DIRECTION('center_axis',(0.974142773255869,-0.225933236030987,0.000173694938032367));
#125968=DIRECTION('ref_axis',(0.223522509730735,0.963860028028979,0.144953558120001));
#125969=DIRECTION('center_axis',(-0.952486436664481,-0.304580953861225,
0.000174685963071088));
#125970=DIRECTION('ref_axis',(0.300576729150183,-0.940056797778399,-0.161080249701816));
#125971=DIRECTION('center_axis',(0.5,0.866025403784439,0.));
#125972=DIRECTION('ref_axis',(-0.866025403784439,0.5,0.));
#125973=DIRECTION('',(0.,0.,1.));
#125974=DIRECTION('',(0.,0.,1.));
#125975=DIRECTION('',(-0.866025403784439,0.5,0.));
#125976=DIRECTION('center_axis',(1.,-4.50694379621149E-16,0.));
#125977=DIRECTION('ref_axis',(4.50694379621149E-16,1.,0.));
#125978=DIRECTION('',(0.,0.,1.));
#125979=DIRECTION('center_axis',(0.5,-0.866025403784439,0.));
#125980=DIRECTION('ref_axis',(0.866025403784439,0.5,0.));
#125981=DIRECTION('',(0.,0.,1.));
#125982=DIRECTION('center_axis',(-0.5,-0.866025403784439,0.));
#125983=DIRECTION('ref_axis',(0.866025403784439,-0.5,0.));
#125984=DIRECTION('',(0.,0.,1.));
#125985=DIRECTION('center_axis',(-1.,0.,0.));
#125986=DIRECTION('ref_axis',(0.,0.,1.));
#125987=DIRECTION('',(0.,0.,1.));
#125988=DIRECTION('center_axis',(-0.5,0.866025403784439,0.));
#125989=DIRECTION('ref_axis',(-0.866025403784439,-0.5,0.));
#125990=DIRECTION('',(-0.866025403784439,-0.5,0.));
#125991=DIRECTION('center_axis',(0.,4.12699273797265E-32,-1.));
#125992=DIRECTION('ref_axis',(0.,1.,4.12699273797265E-32));
#125993=DIRECTION('center_axis',(0.,0.,1.));
#125994=DIRECTION('ref_axis',(1.,0.,0.));
#125995=DIRECTION('center_axis',(0.,0.,1.));
#125996=DIRECTION('ref_axis',(1.,0.,0.));
#125997=DIRECTION('center_axis',(0.,0.,1.));
#125998=DIRECTION('ref_axis',(1.,0.,0.));
#125999=DIRECTION('center_axis',(0.,0.,1.));
#126000=DIRECTION('ref_axis',(-1.,-1.22464679914735E-16,0.));
#126001=DIRECTION('center_axis',(0.,0.,1.));
#126002=DIRECTION('ref_axis',(1.,0.,0.));
#126003=DIRECTION('center_axis',(0.,-4.12699273797265E-32,1.));
#126004=DIRECTION('ref_axis',(0.,-1.,-4.12699273797265E-32));
#126005=DIRECTION('center_axis',(0.,0.,1.));
#126006=DIRECTION('ref_axis',(0.,1.,0.));
#126007=DIRECTION('center_axis',(0.,0.,-1.));
#126008=DIRECTION('ref_axis',(1.,0.,0.));
#126009=DIRECTION('center_axis',(-0.931957757426395,0.361751902433362,-0.0242960790789018));
#126010=DIRECTION('ref_axis',(0.265681371836198,0.635785003161866,-0.724700516360863));
#126011=DIRECTION('center_axis',(-0.282388053744349,0.677731328986489,-0.678923583927297));
#126012=DIRECTION('ref_axis',(-5.21804821573824E-15,0.707727927194326,0.706485089063614));
#126013=DIRECTION('center_axis',(0.,-4.12699273797265E-32,1.));
#126014=DIRECTION('ref_axis',(0.543398865272314,0.839474641201723,3.4645057479517E-32));
#126015=DIRECTION('center_axis',(0.,0.,1.));
#126016=DIRECTION('ref_axis',(1.,0.,0.));
#126017=DIRECTION('center_axis',(0.,0.,-1.));
#126018=DIRECTION('ref_axis',(-1.,0.,0.));
#126019=DIRECTION('center_axis',(-0.28238805374435,-0.677731328986489,0.678923583927297));
#126020=DIRECTION('ref_axis',(-5.19029264012261E-15,-0.707727927194326,
-0.706485089063614));
#126021=DIRECTION('center_axis',(0.281341523064402,-0.675219655354574,0.681854357192688));
#126022=DIRECTION('ref_axis',(-4.6074255521944E-15,-0.71055531721483,-0.703641344136153));
#126023=DIRECTION('center_axis',(0.281589094373317,-0.675813826495969,0.681163162426516));
#126024=DIRECTION('ref_axis',(2.41473507855972E-15,-0.709888749373493,-0.704313824593084));
#126025=DIRECTION('center_axis',(0.,0.,1.));
#126026=DIRECTION('ref_axis',(-1.,0.,0.));
#126027=DIRECTION('center_axis',(0.281589094373317,0.675813826495969,-0.681163162426516));
#126028=DIRECTION('ref_axis',(2.52575738102223E-15,0.709888749373494,0.704313824593084));
#126029=DIRECTION('center_axis',(0.,-4.12699273797265E-32,1.));
#126030=DIRECTION('ref_axis',(-0.543398865272315,0.839474641201722,3.4645057479517E-32));
#126031=DIRECTION('center_axis',(0.,0.,1.));
#126032=DIRECTION('ref_axis',(1.,0.,0.));
#126033=DIRECTION('center_axis',(0.281341523064402,0.675219655354575,-0.681854357192686));
#126034=DIRECTION('ref_axis',(-5.19029264012261E-15,0.710555317214828,0.703641344136155));
#126035=DIRECTION('center_axis',(0.951355185205049,-0.308096269992785,3.1537277192308E-33));
#126036=DIRECTION('ref_axis',(0.308096269992785,0.951355185205049,1.16548576868668E-33));
#126037=DIRECTION('',(-3.35939703647716E-33,-1.37139182454908E-34,1.));
#126038=DIRECTION('',(0.225467238628688,0.696209099085459,-0.68151112584885));
#126039=DIRECTION('center_axis',(-0.951353704021749,0.308100843620298,2.13514021596686E-6));
#126040=DIRECTION('ref_axis',(0.305493135327841,0.943302522722636,-0.129824092111888));
#126041=DIRECTION('',(1.50964222874619E-32,3.63793170954444E-32,-1.));
#126042=DIRECTION('center_axis',(-0.888655736322693,-0.45857494731044,-3.04823604041934E-33));
#126043=DIRECTION('ref_axis',(0.45857494731044,-0.888655736322693,1.4186657978342E-33));
#126044=DIRECTION('center_axis',(0.888655736322668,0.458574947310488,2.22108072553328E-14));
#126045=DIRECTION('ref_axis',(0.45513488130679,-0.881989357347002,-0.122257978653648));
#126046=DIRECTION('',(0.335588701144621,-0.650325156370489,0.681511125848849));
#126047=DIRECTION('',(-3.35939703647716E-33,-1.37139182454908E-34,1.));
#126048=DIRECTION('',(1.41101612161355E-32,-3.39907616780994E-32,1.));
#126049=DIRECTION('center_axis',(-3.35939703647716E-33,-1.37139182454908E-34,
1.));
#126050=DIRECTION('ref_axis',(0.996672582494194,0.0815092835470589,3.35939703647716E-33));
#126051=DIRECTION('center_axis',(0.027686525038222,-0.338543037176896,-0.940543496235209));
#126052=DIRECTION('ref_axis',(-0.0765442203803849,0.937423624769578,-0.33967326955506));
#126053=DIRECTION('center_axis',(0.027686525038222,-0.338543037176896,-0.940543496235209));
#126054=DIRECTION('ref_axis',(-0.0765442203803849,0.937423624769578,-0.33967326955506));
#126055=DIRECTION('center_axis',(-0.336689825853977,0.652458985955234,-0.678923583927297));
#126056=DIRECTION('ref_axis',(-0.0576863962918622,0.705373020900031,0.706485089063614));
#126057=DIRECTION('center_axis',(-0.226207035727802,-0.698493481841137,
0.678923583927297));
#126058=DIRECTION('ref_axis',(0.0576863962918529,-0.705373020900032,-0.706485089063614));
#126059=DIRECTION('center_axis',(-0.958342883256615,0.284584993724602,-0.0242960790698013));
#126060=DIRECTION('ref_axis',(0.212974880022829,0.655324689333347,-0.724700801730903));
#126061=DIRECTION('center_axis',(3.35939703647716E-33,1.37139182454908E-34,
-1.));
#126062=DIRECTION('ref_axis',(-0.996672582494194,-0.0815092835470579,-3.35939703647716E-33));
#126063=DIRECTION('center_axis',(4.48517628368065E-36,-4.12697442833547E-32,
1.));
#126064=DIRECTION('ref_axis',(0.473165773815097,0.880973410773538,3.63554251511517E-32));
#126065=DIRECTION('center_axis',(-3.35939703647716E-33,-1.37139182454908E-34,
1.));
#126066=DIRECTION('ref_axis',(0.996672582494194,0.0815092835470579,3.35939703647716E-33));
#126067=DIRECTION('center_axis',(0.335442052700293,-0.650040971676063,0.681854357192688));
#126068=DIRECTION('ref_axis',(0.0579168548267297,-0.708191003013486,-0.703641344136153));
#126069=DIRECTION('center_axis',(0.33573723070014,-0.650612986401985,0.681163162426516));
#126070=DIRECTION('ref_axis',(0.0578625233595577,-0.707526653121652,-0.704313824593084));
#126071=DIRECTION('center_axis',(0.225567029082369,0.696517237076055,-0.681163162426516));
#126072=DIRECTION('ref_axis',(-0.0578625233595519,0.707526653121653,0.704313824593084));
#126073=DIRECTION('center_axis',(0.225368712010601,0.695904863630102,-0.681854357192686));
#126074=DIRECTION('ref_axis',(-0.0579168548267439,0.708191003013484,0.703641344136154));
#126075=DIRECTION('center_axis',(-3.35939703647716E-33,-1.37139182454908E-34,
1.));
#126076=DIRECTION('ref_axis',(0.996672582494194,0.0815092835470579,3.35939703647716E-33));
#126077=DIRECTION('center_axis',(4.48517628368065E-36,-4.12697442833547E-32,
1.));
#126078=DIRECTION('ref_axis',(-0.610015726935623,0.792389306396296,3.27044400759111E-32));
#126079=DIRECTION('center_axis',(-3.35939703647716E-33,-1.37139182454908E-34,
1.));
#126080=DIRECTION('ref_axis',(-0.996672582494194,-0.0815092835470579,-3.35939703647716E-33));
#126081=DIRECTION('center_axis',(3.35939703647716E-33,1.37139182454908E-34,
-1.));
#126082=DIRECTION('ref_axis',(0.996672582494193,0.0815092835470633,3.35939703647716E-33));
#126083=DIRECTION('center_axis',(0.888655736322699,-0.458574947310428,-3.04823604041885E-33));
#126084=DIRECTION('ref_axis',(0.458574947310428,0.888655736322699,-1.41866579783395E-33));
#126085=DIRECTION('',(3.35939703647662E-33,-1.37139182454862E-34,1.));
#126086=DIRECTION('',(0.335588701144614,0.65032515637049,-0.681511125848851));
#126087=DIRECTION('center_axis',(-0.888653531715357,0.458579219508761,2.13514018757357E-6));
#126088=DIRECTION('ref_axis',(0.454698036374906,0.881133021060312,-0.129824092193755));
#126089=DIRECTION('',(1.41101612161356E-32,3.39907616780996E-32,-1.));
#126090=DIRECTION('center_axis',(-0.951355185205045,-0.308096269992797,
3.15372771923029E-33));
#126091=DIRECTION('ref_axis',(0.308096269992797,-0.951355185205045,-1.16548576868652E-33));
#126092=DIRECTION('center_axis',(0.951355185205055,0.308096269992766,-1.17032890463339E-14));
#126093=DIRECTION('ref_axis',(0.305785041452959,-0.944218457273914,-0.122257978745287));
#126094=DIRECTION('',(0.225467238628697,-0.696209099085458,0.681511125848849));
#126095=DIRECTION('',(3.35939703647662E-33,-1.37139182454862E-34,1.));
#126096=DIRECTION('',(1.50964222874619E-32,-3.63793170954442E-32,1.));
#126097=DIRECTION('center_axis',(3.35939703647662E-33,-1.37139182454862E-34,
1.));
#126098=DIRECTION('ref_axis',(0.996672582494195,-0.0815092835470462,-3.35939703647662E-33));
#126099=DIRECTION('center_axis',(-0.0276865250382154,-0.338543037176888,
-0.940543496235212));
#126100=DIRECTION('ref_axis',(0.0767818315756177,0.937404192592328,-0.339673269555052));
#126101=DIRECTION('center_axis',(-0.0276865250382154,-0.338543037176888,
-0.940543496235212));
#126102=DIRECTION('ref_axis',(0.0767818315756177,0.937404192592328,-0.339673269555052));
#126103=DIRECTION('center_axis',(-0.226207035727811,0.698493481841134,-0.678923583927297));
#126104=DIRECTION('ref_axis',(0.0576863962918442,0.705373020900032,0.706485089063614));
#126105=DIRECTION('center_axis',(-0.336689825853969,-0.652458985955238,
0.678923583927297));
#126106=DIRECTION('ref_axis',(-0.0576863962918536,-0.705373020900031,-0.706485089063614));
#126107=DIRECTION('center_axis',(-0.899370606478019,0.436511411929941,-0.0242960790723403));
#126108=DIRECTION('ref_axis',(0.316619608623823,0.612013741106922,-0.724700768684018));
#126109=DIRECTION('center_axis',(-3.35939703647662E-33,1.37139182454862E-34,
-1.));
#126110=DIRECTION('ref_axis',(-0.996672582494194,0.0815092835470578,3.35939703647662E-33));
#126111=DIRECTION('center_axis',(-4.48517628367996E-36,-4.12697442833547E-32,
1.));
#126112=DIRECTION('ref_axis',(0.610015726935643,0.792389306396281,3.27044400759104E-32));
#126113=DIRECTION('center_axis',(3.35939703647662E-33,-1.37139182454862E-34,
1.));
#126114=DIRECTION('ref_axis',(0.996672582494194,-0.0815092835470578,-3.35939703647662E-33));
#126115=DIRECTION('center_axis',(0.22536871201061,-0.695904863630098,0.681854357192688));
#126116=DIRECTION('ref_axis',(-0.0579168548267348,-0.708191003013486,-0.703641344136153));
#126117=DIRECTION('center_axis',(0.225567029082378,-0.696517237076053,0.681163162426516));
#126118=DIRECTION('ref_axis',(-0.057862523359542,-0.707526653121654,-0.704313824593084));
#126119=DIRECTION('center_axis',(0.335737230700132,0.650612986401989,-0.681163162426516));
#126120=DIRECTION('ref_axis',(0.0578625233595482,0.707526653121653,0.704313824593084));
#126121=DIRECTION('center_axis',(0.335442052700285,0.650040971676069,-0.681854357192686));
#126122=DIRECTION('ref_axis',(0.0579168548267194,0.708191003013486,0.703641344136154));
#126123=DIRECTION('center_axis',(3.35939703647662E-33,-1.37139182454862E-34,
1.));
#126124=DIRECTION('ref_axis',(0.996672582494194,-0.0815092835470577,-3.35939703647662E-33));
#126125=DIRECTION('center_axis',(-4.48517628367996E-36,-4.12697442833547E-32,
1.));
#126126=DIRECTION('ref_axis',(-0.473165773815079,0.880973410773547,3.63554251511521E-32));
#126127=DIRECTION('center_axis',(3.35939703647662E-33,-1.37139182454862E-34,
1.));
#126128=DIRECTION('ref_axis',(-0.996672582494195,0.0815092835470381,3.35939703647662E-33));
#126129=DIRECTION('center_axis',(-3.35939703647662E-33,1.37139182454862E-34,
-1.));
#126130=DIRECTION('ref_axis',(0.996672582494194,-0.0815092835470502,-3.35939703647662E-33));
#126131=DIRECTION('center_axis',(0.848320692261118,-0.529482769390674,-5.9706948941013E-33));
#126132=DIRECTION('ref_axis',(0.529482769390674,0.848320692261118,-3.08107063799443E-33));
#126133=DIRECTION('',(6.69643783993752E-33,-5.47644091186675E-34,1.));
#126134=DIRECTION('',(0.387479594994063,0.620807658463935,-0.681511125848847));
#126135=DIRECTION('center_axis',(-0.848318146765595,0.529486847677661,2.13514020029428E-6));
#126136=DIRECTION('ref_axis',(0.525005587425765,0.841139012446968,-0.12982409218426));
#126137=DIRECTION('',(1.3474376413819E-32,3.28646902736504E-32,-1.));
#126138=DIRECTION('center_axis',(-0.973302335538189,-0.229526825525702,
6.39195957962951E-33));
#126139=DIRECTION('ref_axis',(0.229526825525702,-0.973302335538189,-2.07003539272673E-33));
#126140=DIRECTION('center_axis',(0.973302335538189,0.229526825525702,-1.99719171769005E-15));
#126141=DIRECTION('ref_axis',(0.227804996989923,-0.966000967903135,-0.122257978703341));
#126142=DIRECTION('',(0.167969510126494,-0.712270193825424,0.681511125848844));
#126143=DIRECTION('',(6.69643783993752E-33,-5.47644091186675E-34,1.));
#126144=DIRECTION('',(1.54403351517636E-32,-3.76259056661214E-32,1.));
#126145=DIRECTION('center_axis',(6.69643783993752E-33,-5.47644091186674E-34,
1.));
#126146=DIRECTION('ref_axis',(0.986712473391291,-0.162476136260194,-6.69643783993752E-33));
#126147=DIRECTION('center_axis',(-0.0551888008202638,-0.335159854328745,
-0.940543496235212));
#126148=DIRECTION('ref_axis',(0.152933490497652,0.928026625390665,-0.339673269555052));
#126149=DIRECTION('center_axis',(-0.0551888008202638,-0.335159854328745,
-0.940543496235212));
#126150=DIRECTION('ref_axis',(0.152933490497652,0.928026625390665,-0.339673269555052));
#126151=DIRECTION('center_axis',(-0.168520647210029,0.714607275817443,-0.678923583927297));
#126152=DIRECTION('ref_axis',(0.114988899133967,0.698323973530006,0.706485089063614));
#126153=DIRECTION('center_axis',(-0.388750982722451,-0.622844636020608,
0.678923583927297));
#126154=DIRECTION('ref_axis',(-0.114988899133973,-0.698323973530004,-0.706485089063614));
#126155=DIRECTION('center_axis',(-0.86079829254277,0.508366009973053,-0.0242960790978609));
#126156=DIRECTION('ref_axis',(0.365450838207706,0.584169795627829,-0.724700858788939));
#126157=DIRECTION('center_axis',(-6.69643783993752E-33,5.47644091186674E-34,
-1.));
#126158=DIRECTION('ref_axis',(-0.98671247339129,0.162476136260201,6.69643783993751E-33));
#126159=DIRECTION('center_axis',(-8.94050445919518E-36,-4.12691962127156E-32,
1.));
#126160=DIRECTION('ref_axis',(0.672573034581739,0.740030751491795,3.05464874289731E-32));
#126161=DIRECTION('center_axis',(6.69643783993752E-33,-5.47644091186674E-34,
1.));
#126162=DIRECTION('ref_axis',(0.98671247339129,-0.162476136260201,-6.69643783993751E-33));
#126163=DIRECTION('center_axis',(0.167896109361599,-0.711958939854388,0.681854357192688));
#126164=DIRECTION('ref_axis',(-0.115448282540208,-0.701113794530378,-0.703641344136153));
#126165=DIRECTION('center_axis',(0.168043852428827,-0.712585440360654,0.681163162426516));
#126166=DIRECTION('ref_axis',(-0.115339981172784,-0.70045608372697,-0.704313824593084));
#126167=DIRECTION('center_axis',(0.387651091149391,0.621082424227087,-0.681163162426516));
#126168=DIRECTION('ref_axis',(0.115339981172785,0.700456083726971,0.704313824593083));
#126169=DIRECTION('center_axis',(0.3873102708195,0.620536372580266,-0.681854357192686));
#126170=DIRECTION('ref_axis',(0.115448282540195,0.701113794530378,0.703641344136155));
#126171=DIRECTION('center_axis',(6.69643783993752E-33,-5.47644091186674E-34,
1.));
#126172=DIRECTION('ref_axis',(0.98671247339129,-0.162476136260201,-6.69643783993751E-33));
#126173=DIRECTION('center_axis',(-8.94050445919518E-36,-4.12691962127156E-32,
1.));
#126174=DIRECTION('ref_axis',(-0.399783842199965,0.916609447647052,3.78241608761511E-32));
#126175=DIRECTION('center_axis',(6.69643783993752E-33,-5.47644091186674E-34,
1.));
#126176=DIRECTION('ref_axis',(-0.986712473391296,0.162476136260162,6.69643783993754E-33));
#126177=DIRECTION('center_axis',(-6.69643783993752E-33,5.47644091186674E-34,
-1.));
#126178=DIRECTION('ref_axis',(0.986712473391291,-0.162476136260193,-6.69643783993752E-33));
#126179=DIRECTION('center_axis',(0.802340213955601,-0.596866970999133,-8.74792807954735E-33));
#126180=DIRECTION('ref_axis',(0.596866970999133,0.802340213955601,-4.97615149054745E-33));
#126181=DIRECTION('',(9.98891495440811E-33,-1.22878288375636E-33,1.));
#126182=DIRECTION('',(0.436791876068461,0.587158788016352,-0.681511125848847));
#126183=DIRECTION('center_axis',(-0.802337344511779,0.596870828234408,2.13514018553818E-6));
#126184=DIRECTION('ref_axis',(0.591819312914846,0.795547362487343,-0.129824092141757));
#126185=DIRECTION('',(1.27489218595841E-32,3.17941881426319E-32,-1.));
#126186=DIRECTION('center_axis',(-0.988772319411909,-0.149429917903995,
9.69314568243686E-33));
#126187=DIRECTION('ref_axis',(0.149429917903995,-0.988772319411909,-2.70762924361262E-33));
#126188=DIRECTION('center_axis',(0.988772319411903,0.14942991790403,1.57485563471379E-14));
#126189=DIRECTION('ref_axis',(0.148308947855242,-0.981354901463211,-0.122257978717968));
#126190=DIRECTION('',(0.109353972247421,-0.723591247941779,0.681511125848852));
#126191=DIRECTION('',(9.98891495440811E-33,-1.22878288375636E-33,1.));
#126192=DIRECTION('',(1.56814951331063E-32,-3.88963784073378E-32,1.));
#126193=DIRECTION('center_axis',(9.98891495440811E-33,-1.22878288375636E-33,
1.));
#126194=DIRECTION('ref_axis',(0.970185955574067,-0.242361737093202,-9.9889149544081E-33));
#126195=DIRECTION('center_axis',(-0.0823238042383858,-0.329546237947602,
-0.940543496235183));
#126196=DIRECTION('ref_axis',(0.228067402272856,0.912473194110511,-0.339673269555131));
#126197=DIRECTION('center_axis',(-0.0823238042383858,-0.329546237947602,
-0.940543496235183));
#126198=DIRECTION('ref_axis',(0.228067402272856,0.912473194110511,-0.339673269555131));
#126199=DIRECTION('center_axis',(-0.109712781589014,0.725965476275088,-0.678923583927297));
#126200=DIRECTION('ref_axis',(0.171526169824185,0.686627695331482,0.706485089063614));
#126201=DIRECTION('center_axis',(-0.438225065940312,-0.589085357795391,
0.678923583927297));
#126202=DIRECTION('ref_axis',(-0.171526169824195,-0.686627695331478,-0.706485089063615));
#126203=DIRECTION('center_axis',(-0.816497507979672,0.576837516120213,-0.0242960790920933));
#126204=DIRECTION('ref_axis',(0.411849783893902,0.552437924326749,-0.724701383517445));
#126205=DIRECTION('center_axis',(-9.98891495440811E-33,1.22878288375636E-33,
-1.));
#126206=DIRECTION('ref_axis',(-0.970185955574069,0.242361737093194,9.98891495440811E-33));
#126207=DIRECTION('center_axis',(-1.3336335052612E-35,-4.12682868151287E-32,
1.));
#126208=DIRECTION('ref_axis',(0.730654479649428,0.682747414032615,2.81855603575337E-32));
#126209=DIRECTION('center_axis',(9.98891495440811E-33,-1.22878288375636E-33,
1.));
#126210=DIRECTION('ref_axis',(0.970185955574069,-0.242361737093194,-9.98891495440811E-33));
#126211=DIRECTION('center_axis',(0.109306185805694,-0.723275046798904,0.681854357192688));
#126212=DIRECTION('ref_axis',(-0.172211420981001,-0.689370789420303,-0.703641344136153));
#126213=DIRECTION('center_axis',(0.109402371662647,-0.723911505107977,0.681163162426516));
#126214=DIRECTION('ref_axis',(-0.172049870441076,-0.688724094662203,-0.704313824593084));
#126215=DIRECTION('center_axis',(0.436985197544978,0.58741866099034,-0.681163162426516));
#126216=DIRECTION('ref_axis',(0.172049870441082,0.688724094662202,0.704313824593084));
#126217=DIRECTION('center_axis',(0.436601002988107,0.586902206306236,-0.681854357192686));
#126218=DIRECTION('ref_axis',(0.172211420980992,0.689370789420304,0.703641344136155));
#126219=DIRECTION('center_axis',(9.98891495440811E-33,-1.22878288375636E-33,
1.));
#126220=DIRECTION('ref_axis',(0.970185955574069,-0.242361737093194,-9.98891495440811E-33));
#126221=DIRECTION('center_axis',(-1.3336335052612E-35,-4.12682868151287E-32,
1.));
#126222=DIRECTION('ref_axis',(-0.323741415074715,0.946145599876373,3.90414904605883E-32));
#126223=DIRECTION('center_axis',(9.98891495440811E-33,-1.22878288375636E-33,
1.));
#126224=DIRECTION('ref_axis',(-0.970185955574059,0.242361737093233,9.98891495440806E-33));
#126225=DIRECTION('center_axis',(-9.98891495440811E-33,1.22878288375636E-33,
-1.));
#126226=DIRECTION('ref_axis',(0.970185955574068,-0.2423617370932,-9.98891495440811E-33));
#126227=DIRECTION('center_axis',(0.751020293903028,-0.660279121391711,-1.13614535681191E-32));
#126228=DIRECTION('ref_axis',(0.660279121391711,0.751020293903028,-7.0912969050856E-33));
#126229=DIRECTION('',(1.32149174879121E-32,-2.17602269387938E-33,1.));
#126230=DIRECTION('',(0.483197379273213,0.549602472708897,-0.681511125848848));
#126231=DIRECTION('center_axis',(-0.751017119606567,0.660282731906035,2.13514017760057E-6));
#126232=DIRECTION('ref_axis',(0.654694578522591,0.744661476088215,-0.129824092075573));
#126233=DIRECTION('',(1.19386253337977E-32,3.0786379300106E-32,-1.));
#126234=DIRECTION('center_axis',(-0.997662186635891,-0.0683385788328371,
1.30353171787955E-32));
#126235=DIRECTION('ref_axis',(0.0683385788328371,-0.997662186635891,-3.07402423946213E-33));
#126236=DIRECTION('center_axis',(0.997662186635891,0.0683385788328493,8.00466807870197E-15));
#126237=DIRECTION('ref_axis',(0.0678259271421216,-0.99017808006695,-0.122257978726304));
#126238=DIRECTION('',(0.0500107017251773,-0.73009692168724,0.681511125848853));
#126239=DIRECTION('',(1.32149174879121E-32,-2.17602269387938E-33,1.));
#126240=DIRECTION('',(1.58182973516027E-32,-4.01822805326139E-32,1.));
#126241=DIRECTION('center_axis',(1.32149174879121E-32,-2.17602269387938E-33,
1.));
#126242=DIRECTION('ref_axis',(0.947203010291915,-0.320634460552722,-1.32149174879121E-32));
#126243=DIRECTION('center_axis',(-0.108910956321728,-0.321739545724065,
-0.940543496235213));
#126244=DIRECTION('ref_axis',(0.301683563113628,0.890847404271264,-0.339673269555048));
#126245=DIRECTION('center_axis',(-0.108910956321728,-0.321739545724065,
-0.940543496235213));
#126246=DIRECTION('ref_axis',(0.301683563113628,0.890847404271264,-0.339673269555048));
#126247=DIRECTION('center_axis',(-0.0501747955078592,0.732492496263995,
-0.678923583927297));
#126248=DIRECTION('ref_axis',(0.226921962154045,0.670362023106124,0.706485089063615));
#126249=DIRECTION('center_axis',(-0.484782833646386,-0.551405813706289,
0.678923583927297));
#126250=DIRECTION('ref_axis',(-0.226921962154054,-0.670362023106121,-0.706485089063614));
#126251=DIRECTION('center_axis',(-0.766763067216207,0.641470263764373,-0.0242960790923158));
#126252=DIRECTION('ref_axis',(0.455508349976982,0.517030330878251,-0.724701166035472));
#126253=DIRECTION('center_axis',(-1.32149174879121E-32,2.17602269387938E-33,
-1.));
#126254=DIRECTION('ref_axis',(-0.947203010291914,0.320634460552723,1.32149174879121E-32));
#126255=DIRECTION('center_axis',(-1.76434145365967E-35,-4.1267022142485E-32,
1.));
#126256=DIRECTION('ref_axis',(0.783873539704558,0.620920505178438,2.56373704417269E-32));
#126257=DIRECTION('center_axis',(1.32149174879121E-32,-2.17602269387938E-33,
1.));
#126258=DIRECTION('ref_axis',(0.947203010291914,-0.320634460552723,-1.32149174879121E-32));
#126259=DIRECTION('center_axis',(0.0499888476175039,-0.729777877638957,
0.681854357192688));
#126260=DIRECTION('ref_axis',(-0.227828520828051,-0.673040135444811,-0.703641344136153));
#126261=DIRECTION('center_axis',(0.0500328361631726,-0.730420058225798,
0.681163162426516));
#126262=DIRECTION('ref_axis',(-0.227614796207816,-0.672408760378936,-0.704313824593084));
#126263=DIRECTION('center_axis',(0.483411239548387,0.549845723481961,-0.681163162426516));
#126264=DIRECTION('ref_axis',(0.227614796207819,0.672408760378935,0.704313824593084));
#126265=DIRECTION('center_axis',(0.482986227515924,0.549362302681286,-0.681854357192686));
#126266=DIRECTION('ref_axis',(0.227828520828041,0.673040135444813,0.703641344136155));
#126267=DIRECTION('center_axis',(1.32149174879121E-32,-2.17602269387938E-33,
1.));
#126268=DIRECTION('ref_axis',(0.947203010291914,-0.320634460552723,-1.32149174879121E-32));
#126269=DIRECTION('center_axis',(-1.76434145365967E-35,-4.1267022142485E-32,
1.));
#126270=DIRECTION('ref_axis',(-0.24554454224571,0.969385309241555,3.99993127769249E-32));
#126271=DIRECTION('center_axis',(1.32149174879121E-32,-2.17602269387938E-33,
1.));
#126272=DIRECTION('ref_axis',(-0.947203010291915,0.320634460552722,1.32149174879121E-32));
#126273=DIRECTION('center_axis',(-1.32149174879121E-32,2.17602269387938E-33,
-1.));
#126274=DIRECTION('ref_axis',(0.947203010291914,-0.320634460552723,-1.32149174879121E-32));
#126275=DIRECTION('center_axis',(0.694702457704156,-0.719297223169814,-1.37938787788914E-32));
#126276=DIRECTION('ref_axis',(0.719297223169814,0.694702457704156,-9.41243093784955E-33));
#126277=DIRECTION('',(1.63529769258419E-32,-3.3830597969029E-33,1.));
#126278=DIRECTION('',(0.526387283640853,0.508388643623594,-0.68151112584885));
#126279=DIRECTION('center_axis',(-0.694698999679441,0.719300562935846,2.13514020416028E-6));
#126280=DIRECTION('ref_axis',(0.713212959724422,0.688819990421442,-0.129824092051258));
#126281=DIRECTION('',(1.10488792261493E-32,2.98479705476426E-32,-1.));
#126282=DIRECTION('center_axis',(-0.999912776610487,0.0132075422053813,
1.63962324688167E-32));
#126283=DIRECTION('ref_axis',(-0.0132075422053813,-0.999912776610487,-3.16678208202881E-33));
#126284=DIRECTION('center_axis',(0.999912776610487,-0.0132075422053234,
2.36411209098337E-14));
#126285=DIRECTION('ref_axis',(0.013108463925482,0.992411786921792,0.122257978685276));
#126286=DIRECTION('',(-0.00966538176586899,-0.73174392087639,0.68151112584885));
#126287=DIRECTION('',(1.63529769258419E-32,-3.3830597969029E-33,1.));
#126288=DIRECTION('',(1.58498314110597E-32,-4.14750545754649E-32,1.));
#126289=DIRECTION('center_axis',(1.63529769258419E-32,-3.3830597969029E-33,
1.));
#126290=DIRECTION('ref_axis',(0.917916585253764,-0.396773414578232,-1.63529769258419E-32));
#126291=DIRECTION('center_axis',(-0.134773323959819,-0.311791729907105,
-0.940543496235212));
#126292=DIRECTION('ref_axis',(0.373292069616715,0.863293171935844,-0.339673269555051));
#126293=DIRECTION('center_axis',(-0.134773323959819,-0.311791729907105,
-0.940543496235212));
#126294=DIRECTION('ref_axis',(0.373292069616715,0.863293171935844,-0.339673269555051));
#126295=DIRECTION('center_axis',(0.009697095559142,0.73414489954302,-0.678923583927297));
#126296=DIRECTION('ref_axis',(0.280807626265263,0.649635202218942,0.706485089063614));
#126297=DIRECTION('center_axis',(-0.528114451578082,-0.510056754902527,
0.678923583927297));
#126298=DIRECTION('ref_axis',(-0.280807626265268,-0.64963520221894,-0.706485089063614));
#126299=DIRECTION('center_axis',(-0.711925944736631,0.701834132649891,-0.0242960790752475));
#126300=DIRECTION('ref_axis',(-0.496135854106694,-0.478182219455507,0.72470061354081));
#126301=DIRECTION('center_axis',(-1.63529769258419E-32,3.3830597969029E-33,
-1.));
#126302=DIRECTION('ref_axis',(-0.917916585253767,0.396773414578224,1.63529769258419E-32));
#126303=DIRECTION('center_axis',(-2.18330800077971E-35,-4.12654106109723E-32,
1.));
#126304=DIRECTION('ref_axis',(0.831876050682982,0.554961472806973,2.29188754650208E-32));
#126305=DIRECTION('center_axis',(1.63529769258419E-32,-3.3830597969029E-33,
1.));
#126306=DIRECTION('ref_axis',(0.917916585253767,-0.396773414578224,-1.63529769258419E-32));
#126307=DIRECTION('center_axis',(-0.00966115810400148,-0.731424157108197,
0.681854357192688));
#126308=DIRECTION('ref_axis',(-0.281929459458053,-0.65223051041174,-0.703641344136153));
#126309=DIRECTION('center_axis',(-0.00966965960613086,-0.732067786366952,
0.681163162426516));
#126310=DIRECTION('ref_axis',(-0.281664983059587,-0.651618656734984,-0.704313824593084));
#126311=DIRECTION('center_axis',(0.526620259509841,0.508613653401967,-0.681163162426516));
#126312=DIRECTION('ref_axis',(0.28166498305959,0.651618656734984,0.704313824593083));
#126313=DIRECTION('center_axis',(0.52615725838674,0.508166483570392,-0.681854357192686));
#126314=DIRECTION('ref_axis',(0.281929459458042,0.652230510411742,0.703641344136155));
#126315=DIRECTION('center_axis',(1.63529769258419E-32,-3.3830597969029E-33,
1.));
#126316=DIRECTION('ref_axis',(0.917916585253767,-0.396773414578224,-1.63529769258419E-32));
#126317=DIRECTION('center_axis',(-2.18330800077971E-35,-4.12654106109723E-32,
1.));
#126318=DIRECTION('ref_axis',(-0.165713611000076,0.986173919311049,4.06912536756749E-32));
#126319=DIRECTION('center_axis',(1.63529769258419E-32,-3.3830597969029E-33,
1.));
#126320=DIRECTION('ref_axis',(-0.917916585253776,0.396773414578204,1.6352976925842E-32));
#126321=DIRECTION('center_axis',(-1.63529769258419E-32,3.3830597969029E-33,
-1.));
#126322=DIRECTION('ref_axis',(0.917916585253764,-0.396773414578231,-1.63529769258419E-32));
#126323=DIRECTION('center_axis',(0.6337614912671,-0.773528520603411,-1.60290163234086E-32));
#126324=DIRECTION('ref_axis',(0.773528520603411,0.6337614912671,-1.19241068248114E-32));
#126325=DIRECTION('',(1.93822100003815E-32,-4.84186156005344E-33,1.));
#126326=DIRECTION('',(0.566074167483658,0.463791571993196,-0.681511125848847));
#126327=DIRECTION('center_axis',(-0.633757772526766,0.773531567395509,2.13514017139377E-6));
#126328=DIRECTION('ref_axis',(0.766985026313205,0.628394521334046,-0.129824092404638));
#126329=DIRECTION('',(1.00856046501877E-32,2.8985206840663E-32,-1.));
#126330=DIRECTION('center_axis',(-0.995509112030735,0.0946657692293139,
1.97535252157573E-32));
#126331=DIRECTION('ref_axis',(-0.0946657692293139,-0.995509112030735,-2.98528548317433E-33));
#126332=DIRECTION('center_axis',(0.995509112030737,-0.0946657692292906,
9.50256186696977E-15));
#126333=DIRECTION('ref_axis',(0.0939556203289657,0.988041157067433,0.122257978673981));
#126334=DIRECTION('',(-0.0692771437359349,-0.728521285001353,0.681511125848851));
#126335=DIRECTION('',(1.93822100003815E-32,-4.84186156005344E-33,1.));
#126336=DIRECTION('',(1.57758874575141E-32,-4.27660973379283E-32,1.));
#126337=DIRECTION('center_axis',(1.93822100003815E-32,-4.84186156005343E-33,
1.));
#126338=DIRECTION('ref_axis',(0.882521576786326,-0.470271906992728,-1.93822100003815E-32));
#126339=DIRECTION('center_axis',(-0.159738797363072,-0.299768991569782,
-0.940543496235148));
#126340=DIRECTION('ref_axis',(0.4424163789848,0.829993865974706,-0.33967326955523));
#126341=DIRECTION('center_axis',(-0.159738797363072,-0.299768991569782,
-0.940543496235148));
#126342=DIRECTION('ref_axis',(0.4424163789848,0.829993865974706,-0.33967326955523));
#126343=DIRECTION('center_axis',(0.0695044540551054,0.730911689640969,-0.678923583927297));
#126344=DIRECTION('ref_axis',(0.332824561953684,0.624585166243257,0.706485089063614));
#126345=DIRECTION('center_axis',(-0.567931554967276,-0.46531335254833,0.678923583927297));
#126346=DIRECTION('ref_axis',(-0.332824561953689,-0.624585166243253,-0.706485089063614));
#126347=DIRECTION('center_axis',(-0.652351072554589,0.757527411173429,-0.0242960790614626));
#126348=DIRECTION('ref_axis',(-0.533461682387404,-0.436151780773054,0.724700115601546));
#126349=DIRECTION('center_axis',(-1.93822100003815E-32,4.84186156005343E-33,
-1.));
#126350=DIRECTION('ref_axis',(-0.882521576786327,0.470271906992727,1.93822100003815E-32));
#126351=DIRECTION('center_axis',(-2.58774499337554E-35,-4.12634629450669E-32,
1.));
#126352=DIRECTION('ref_axis',(0.874342563793993,0.485309263396185,2.00481665629657E-32));
#126353=DIRECTION('center_axis',(1.93822100003815E-32,-4.84186156005344E-33,
1.));
#126354=DIRECTION('ref_axis',(0.882521576786327,-0.470271906992727,-1.93822100003815E-32));
#126355=DIRECTION('center_axis',(-0.0692468704123036,-0.728202929488373,
0.681854357192688));
#126356=DIRECTION('ref_axis',(-0.334154204050443,-0.627080398942338,-0.703641344136153));
#126357=DIRECTION('center_axis',(-0.0693078053861371,-0.728843724172518,
0.681163162426516));
#126358=DIRECTION('ref_axis',(-0.333840735920551,-0.626492138439971,-0.704313824593084));
#126359=DIRECTION('center_axis',(0.566324708530484,0.463996843373929,-0.681163162426516));
#126360=DIRECTION('ref_axis',(0.333840735920556,0.626492138439969,0.704313824593084));
#126361=DIRECTION('center_axis',(0.56582679951283,0.463588900352905,-0.681854357192686));
#126362=DIRECTION('ref_axis',(0.33415420405043,0.627080398942345,0.703641344136154));
#126363=DIRECTION('center_axis',(1.93822100003815E-32,-4.84186156005343E-33,
1.));
#126364=DIRECTION('ref_axis',(0.882521576786327,-0.470271906992727,-1.93822100003815E-32));
#126365=DIRECTION('center_axis',(-2.58774499337554E-35,-4.12634629450669E-32,
1.));
#126366=DIRECTION('ref_axis',(-0.0847798830140404,0.996399704654776,4.11127084043199E-32));
#126367=DIRECTION('center_axis',(1.93822100003815E-32,-4.84186156005344E-33,
1.));
#126368=DIRECTION('ref_axis',(-0.882521576786316,0.470271906992746,1.93822100003814E-32));
#126369=DIRECTION('center_axis',(-1.93822100003815E-32,4.84186156005343E-33,
-1.));
#126370=DIRECTION('ref_axis',(0.882521576786327,-0.470271906992726,-1.93822100003815E-32));
#126371=DIRECTION('center_axis',(0.568602946668948,-0.822612113355614,-1.80519917300835E-32));
#126372=DIRECTION('ref_axis',(0.822612113355614,0.568602946668948,-1.46096097773409E-32));
#126373=DIRECTION('',(2.22824576652082E-32,-6.54271989828255E-33,1.));
#126374=DIRECTION('',(0.601993921137519,0.416108043971408,-0.681511125848848));
#126375=DIRECTION('center_axis',(-0.568598991960532,0.822614846897932,2.13514021179288E-6));
#126376=DIRECTION('ref_axis',(0.815652934166245,0.563787190442918,-0.129824092057199));
#126377=DIRECTION('',(9.05521203928678E-33,2.82038297292912E-32,-1.));
#126378=DIRECTION('center_axis',(-0.984480498557861,0.175494011177778,2.30848531903008E-32));
#126379=DIRECTION('ref_axis',(-0.175494011177778,-0.984480498557861,-2.53074227281923E-33));
#126380=DIRECTION('center_axis',(0.98448049855786,-0.17549401117778,-2.26433201113865E-15));
#126381=DIRECTION('ref_axis',(0.174177517580498,0.977095276325475,0.122257978684169));
#126382=DIRECTION('',(-0.128427877744355,-0.720450460172188,0.681511125848848));
#126383=DIRECTION('',(2.22824576652082E-32,-6.54271989828255E-33,1.));
#126384=DIRECTION('',(1.5596957575777E-32,-4.4046817143427E-32,1.));
#126385=DIRECTION('center_axis',(2.22824576652082E-32,-6.54271989828255E-33,
1.));
#126386=DIRECTION('ref_axis',(0.841253532831189,-0.540640817455585,-2.22824576652082E-32));
#126387=DIRECTION('center_axis',(-0.183641235424748,-0.28575134005165,-0.940543496235213));
#126388=DIRECTION('ref_axis',(0.508596480344212,0.791171087775118,-0.339673269555049));
#126389=DIRECTION('center_axis',(-0.183641235424748,-0.28575134005165,-0.940543496235213));
#126390=DIRECTION('ref_axis',(0.508596480344212,0.791171087775118,-0.339673269555049));
#126391=DIRECTION('center_axis',(0.12884927187676,0.722814383036297,-0.678923583927297));
#126392=DIRECTION('ref_axis',(0.382626605094485,0.595378619035523,0.706485089063614));
#126393=DIRECTION('center_axis',(-0.603969167560274,-0.417473366604222,
0.678923583927297));
#126394=DIRECTION('ref_axis',(-0.382626605094491,-0.595378619035519,-0.706485089063614));
#126395=DIRECTION('center_axis',(-0.588434911639695,0.808179469737246,-0.0242960790830131));
#126396=DIRECTION('ref_axis',(-0.567236981821274,-0.39121838869147,0.724700199257556));
#126397=DIRECTION('center_axis',(-2.22824576652082E-32,6.54271989828255E-33,
-1.));
#126398=DIRECTION('ref_axis',(-0.841253532831187,0.540640817455589,2.22824576652081E-32));
#126399=DIRECTION('center_axis',(-2.97496096998732E-35,-4.1261192106164E-32,
1.));
#126400=DIRECTION('ref_axis',(0.91099047139933,0.412427400907876,1.70443478296702E-32));
#126401=DIRECTION('center_axis',(2.22824576652082E-32,-6.54271989828255E-33,
1.));
#126402=DIRECTION('ref_axis',(0.841253532831187,-0.540640817455589,-2.22824576652081E-32));
#126403=DIRECTION('center_axis',(-0.128371756222941,-0.72013563151783,0.681854357192688));
#126404=DIRECTION('ref_axis',(-0.38415520754645,-0.597757170878956,-0.703641344136152));
#126405=DIRECTION('center_axis',(-0.128484719156282,-0.720769327244466,
0.681163162426516));
#126406=DIRECTION('ref_axis',(-0.383794833763806,-0.597196418327567,-0.704313824593084));
#126407=DIRECTION('center_axis',(0.602260360052857,0.416292210907329,-0.681163162426516));
#126408=DIRECTION('ref_axis',(0.383794833763808,0.597196418327568,0.704313824593083));
#126409=DIRECTION('center_axis',(0.601730856643013,0.415926209490355,-0.681854357192686));
#126410=DIRECTION('ref_axis',(0.384155207546438,0.597757170878959,0.703641344136156));
#126411=DIRECTION('center_axis',(2.22824576652082E-32,-6.54271989828255E-33,
1.));
#126412=DIRECTION('ref_axis',(0.841253532831187,-0.540640817455589,-2.22824576652081E-32));
#126413=DIRECTION('center_axis',(-2.97496096998732E-35,-4.1261192106164E-32,
1.));
#126414=DIRECTION('ref_axis',(-0.00328195889422331,0.999994614358406,4.12608722511754E-32));
#126415=DIRECTION('center_axis',(2.22824576652082E-32,-6.54271989828255E-33,
1.));
#126416=DIRECTION('ref_axis',(-0.841253532831199,0.54064081745557,2.22824576652083E-32));
#126417=DIRECTION('center_axis',(-2.22824576652082E-32,6.54271989828255E-33,
-1.));
#126418=DIRECTION('ref_axis',(0.841253532831188,-0.540640817455587,-2.22824576652082E-32));
#126419=DIRECTION('center_axis',(0.499660443273597,-0.866221358214881,-1.98493424313522E-32));
#126420=DIRECTION('ref_axis',(0.866221358214881,0.499660443273597,-1.74510682163656E-32));
#126421=DIRECTION('',(2.50344192506196E-32,-8.47431587997121E-33,1.));
#126422=DIRECTION('',(0.633907504568215,0.365655385569985,-0.681511125848848));
#126423=DIRECTION('center_axis',(-0.499656278915068,0.866223760316114,2.13514019205242E-6));
#126424=DIRECTION('ref_axis',(0.858892806234444,0.495427948762394,-0.129824092462874));
#126425=DIRECTION('',(7.96455848626919E-33,2.7509039149285E-32,-1.));
#126426=DIRECTION('center_axis',(-0.966900329794933,0.255154369436328,2.6368046954407E-32));
#126427=DIRECTION('ref_axis',(-0.255154369436328,-0.966900329794933,-1.80617736103409E-33));
#126428=DIRECTION('center_axis',(0.966900329794936,-0.255154369436314,1.27209663547126E-17));
#126429=DIRECTION('ref_axis',(0.253240292188925,0.959646987726596,0.122257978714434));
#126430=DIRECTION('',(-0.186723945415513,-0.70758515639653,0.681511125848847));
#126431=DIRECTION('',(2.50344192506196E-32,-8.47431587997121E-33,1.));
#126432=DIRECTION('',(1.53142325146899E-32,-4.53086910129593E-32,1.));
#126433=DIRECTION('center_axis',(2.50344192506196E-32,-8.47431587997121E-33,
1.));
#126434=DIRECTION('ref_axis',(0.794387085412117,-0.607411852477742,-2.50344192506195E-32));
#126435=DIRECTION('center_axis',(-0.206321571363482,-0.269832060511356,
-0.940543496235182));
#126436=DIRECTION('ref_axis',(0.571391956039873,0.747083196520074,-0.339673269555135));
#126437=DIRECTION('center_axis',(-0.206321571363482,-0.269832060511356,
-0.940543496235182));
#126438=DIRECTION('ref_axis',(0.571391956039873,0.747083196520074,-0.339673269555135));
#126439=DIRECTION('center_axis',(0.187336619052708,0.709906865968498,-0.678923583927297));
#126440=DIRECTION('ref_axis',(0.42988233130733,0.562209925348665,0.706485089063615));
#126441=DIRECTION('center_axis',(-0.635987464991058,-0.366855164283621,
0.678923583927297));
#126442=DIRECTION('ref_axis',(-0.429882331307336,-0.562209925348662,-0.706485089063613));
#126443=DIRECTION('center_axis',(-0.520602813447602,0.853453227290336,-0.0242960790695151));
#126444=DIRECTION('ref_axis',(-0.597236896350991,-0.343681188212525,0.724700855874934));
#126445=DIRECTION('center_axis',(-2.50344192506196E-32,8.47431587997121E-33,
-1.));
#126446=DIRECTION('ref_axis',(-0.794387085412123,0.607411852477734,2.50344192506196E-32));
#126447=DIRECTION('center_axis',(-3.34237907217862E-35,-4.1258613206322E-32,
1.));
#126448=DIRECTION('ref_axis',(0.941575887720349,0.336800902112267,1.39274091832102E-32));
#126449=DIRECTION('center_axis',(2.50344192506196E-32,-8.47431587997121E-33,
1.));
#126450=DIRECTION('ref_axis',(0.794387085412123,-0.607411852477734,-2.50344192506196E-32));
#126451=DIRECTION('center_axis',(-0.186642349175764,-0.707275949733552,
0.681854357192688));
#126452=DIRECTION('ref_axis',(-0.431599721517371,-0.56445596746637,-0.703641344136153));
#126453=DIRECTION('center_axis',(-0.186806588318928,-0.70789832936217,0.681163162426516));
#126454=DIRECTION('ref_axis',(-0.43119484031005,-0.563926454581669,-0.704313824593085));
#126455=DIRECTION('center_axis',(0.634188068245042,0.36581722246052,-0.681163162426516));
#126456=DIRECTION('ref_axis',(0.431194840310054,0.563926454581671,0.704313824593082));
#126457=DIRECTION('center_axis',(0.633630494200839,0.36549559832664,-0.681854357192686));
#126458=DIRECTION('ref_axis',(0.431599721517362,0.564455967466375,0.703641344136155));
#126459=DIRECTION('center_axis',(2.50344192506196E-32,-8.47431587997121E-33,
1.));
#126460=DIRECTION('ref_axis',(0.794387085412123,-0.607411852477734,-2.50344192506196E-32));
#126461=DIRECTION('center_axis',(-3.34237907217862E-35,-4.1258613206322E-32,
1.));
#126462=DIRECTION('ref_axis',(0.0782378061205324,0.996934724890976,4.11347592102861E-32));
#126463=DIRECTION('center_axis',(2.50344192506196E-32,-8.47431587997121E-33,
1.));
#126464=DIRECTION('ref_axis',(-0.79438708541211,0.607411852477751,2.50344192506194E-32));
#126465=DIRECTION('center_axis',(-2.50344192506196E-32,8.47431587997121E-33,
-1.));
#126466=DIRECTION('ref_axis',(0.79438708541212,-0.607411852477738,-2.50344192506196E-32));
#126467=DIRECTION('center_axis',(0.42739278206643,-0.904066042851692,-2.14091073548399E-32));
#126468=DIRECTION('ref_axis',(0.904066042851692,0.427392782066429,-2.04295727047815E-32));
#126469=DIRECTION('',(2.76197809063066E-32,-1.06237950525522E-32,1.));
#126470=DIRECTION('',(0.661602538143388,0.312769350906479,-0.68151112584885));
#126471=DIRECTION('center_axis',(-0.42738843577091,0.904068097526252,2.13514020324528E-6));
#126472=DIRECTION('ref_axis',(0.896416888448679,0.423771715862612,-0.129824092289708));
#126473=DIRECTION('',(6.82090211058513E-33,2.69054588173222E-32,-1.));
#126474=DIRECTION('center_axis',(-0.942885598864545,0.333116717463787,2.95812573952646E-32));
#126475=DIRECTION('ref_axis',(-0.333116717463787,-0.942885598864545,-8.16412607762027E-34));
#126476=DIRECTION('center_axis',(0.942885598864544,-0.33311671746379,-8.77746678475083E-15));
#126477=DIRECTION('ref_axis',(0.330617794436068,0.935812406761036,0.122257978694019));
#126478=DIRECTION('',(-0.243777396037202,-0.690010990148384,0.681511125848851));
#126479=DIRECTION('',(2.76197809063066E-32,-1.06237950525522E-32,1.));
#126480=DIRECTION('',(1.49295937628881E-32,-4.65433213841181E-32,1.));
#126481=DIRECTION('center_axis',(2.76197809063066E-32,-1.06237950525522E-32,
1.));
#126482=DIRECTION('ref_axis',(0.742234123004276,-0.670140661837553,-2.76197809063066E-32));
#126483=DIRECTION('center_axis',(-0.22762887128535,-0.25211709312737,-0.940543496235215));
#126484=DIRECTION('ref_axis',(0.630384912541233,0.698023589852212,-0.339673269555043));
#126485=DIRECTION('center_axis',(-0.22762887128535,-0.25211709312737,-0.940543496235215));
#126486=DIRECTION('ref_axis',(0.630384912541233,0.698023589852212,-0.339673269555043));
#126487=DIRECTION('center_axis',(0.244577271937227,0.692275035834066,-0.678923583927297));
#126488=DIRECTION('ref_axis',(0.474277261530919,0.525299817366719,0.706485089063614));
#126489=DIRECTION('center_axis',(-0.663773370772871,-0.313795601371554,
0.678923583927297));
#126490=DIRECTION('ref_axis',(-0.474277261530926,-0.525299817366714,-0.706485089063614));
#126491=DIRECTION('center_axis',(-0.449306189438012,0.893047394416651,-0.0242960790730498));
#126492=DIRECTION('ref_axis',(-0.623262680235246,-0.29385717695526,0.724701035584925));
#126493=DIRECTION('center_axis',(-2.76197809063066E-32,1.06237950525522E-32,
-1.));
#126494=DIRECTION('ref_axis',(-0.742234123004278,0.67014066183755,2.76197809063066E-32));
#126495=DIRECTION('center_axis',(-3.68755419309748E-35,-4.12557434076937E-32,
1.));
#126496=DIRECTION('ref_axis',(0.965895271857685,0.258933048881306,1.07180933360173E-32));
#126497=DIRECTION('center_axis',(2.76197809063066E-32,-1.06237950525522E-32,
1.));
#126498=DIRECTION('ref_axis',(0.742234123004278,-0.67014066183755,-2.76197809063066E-32));
#126499=DIRECTION('center_axis',(-0.243670868088643,-0.689709463196115,
0.681854357192688));
#126500=DIRECTION('ref_axis',(-0.476172010550545,-0.52739840271897,-0.703641344136152));
#126501=DIRECTION('center_axis',(-0.243885290457229,-0.690316384892972,
0.681163162426516));
#126502=DIRECTION('ref_axis',(-0.475725316336185,-0.526903653321838,-0.704313824593083));
#126503=DIRECTION('center_axis',(0.661895359476724,0.312907780753829,-0.681163162426516));
#126504=DIRECTION('ref_axis',(0.475725316336192,0.52690365332183,0.704313824593086));
#126505=DIRECTION('center_axis',(0.661313425361432,0.31263267425859,-0.681854357192686));
#126506=DIRECTION('ref_axis',(0.476172010550534,0.527398402718976,0.703641344136155));
#126507=DIRECTION('center_axis',(2.76197809063066E-32,-1.06237950525522E-32,
1.));
#126508=DIRECTION('ref_axis',(0.742234123004278,-0.67014066183755,-2.76197809063066E-32));
#126509=DIRECTION('center_axis',(-3.68755419309748E-35,-4.12557434076937E-32,
1.));
#126510=DIRECTION('ref_axis',(0.159236911443873,0.98724039931205,4.07352085431319E-32));
#126511=DIRECTION('center_axis',(2.76197809063066E-32,-1.06237950525522E-32,
1.));
#126512=DIRECTION('ref_axis',(-0.742234123004274,0.670140661837555,2.76197809063065E-32));
#126513=DIRECTION('center_axis',(-2.76197809063066E-32,1.06237950525522E-32,
-1.));
#126514=DIRECTION('ref_axis',(0.742234123004278,-0.670140661837551,-2.76197809063066E-32));
#126515=DIRECTION('center_axis',(0.352280892409456,-0.935894317133723,-2.27209065223236E-32));
#126516=DIRECTION('ref_axis',(0.935894317133723,0.352280892409456,-2.35253017866368E-32));
#126517=DIRECTION('',(3.00213374770052E-32,-1.2976852986771E-32,1.));
#126518=DIRECTION('',(0.68489471598395,0.257801887816007,-0.68151112584885));
#126519=DIRECTION('center_axis',(-0.352276393100843,0.935896010708081,2.13514019485086E-6));
#126520=DIRECTION('ref_axis',(0.927975464140372,0.349295352096607,-0.129824092360271));
#126521=DIRECTION('',(5.63185375672478E-33,2.63971054609281E-32,-1.));
#126522=DIRECTION('center_axis',(-0.912596119838887,0.408862228696914,3.27031011275321E-32));
#126523=DIRECTION('ref_axis',(-0.408862228696914,-0.912596119838887,4.31965265863604E-34));
#126524=DIRECTION('center_axis',(0.912596119838905,-0.408862228696875,2.54164907767165E-14));
#126525=DIRECTION('ref_axis',(0.40579508981168,0.905750148631062,0.122257978633466));
#126526=DIRECTION('',(-0.299208548308696,-0.66784491460461,0.681511125848847));
#126527=DIRECTION('',(3.00213374770052E-32,-1.2976852986771E-32,1.));
#126528=DIRECTION('',(1.44456010278039E-32,-4.77424919954828E-32,1.));
#126529=DIRECTION('center_axis',(3.00213374770052E-32,-1.2976852986771E-32,
1.));
#126530=DIRECTION('ref_axis',(0.685141714967854,-0.72840979565826,-3.00213374770052E-32));
#126531=DIRECTION('center_axis',(-0.247421338625061,-0.232724328085158,
-0.94054349623518));
#126532=DIRECTION('ref_axis',(0.685182761455578,0.644318751359782,-0.339673269555142));
#126533=DIRECTION('center_axis',(-0.247421338625061,-0.232724328085158,
-0.94054349623518));
#126534=DIRECTION('ref_axis',(0.685182761455578,0.644318751359782,-0.339673269555142));
#126535=DIRECTION('center_axis',(0.300190303429413,0.670036229553501,-0.678923583927297));
#126536=DIRECTION('ref_axis',(0.51551595482926,0.484893925768568,0.706485089063615));
#126537=DIRECTION('center_axis',(-0.687141974287088,-0.258647780504989,
0.678923583927297));
#126538=DIRECTION('ref_axis',(-0.515515954829265,-0.484893925768564,-0.706485089063614));
#126539=DIRECTION('center_axis',(-0.375019506858782,0.926698478480159,-0.0242960790654331));
#126540=DIRECTION('ref_axis',(-0.645140812230435,-0.242077653382994,0.724701139868869));
#126541=DIRECTION('center_axis',(-3.00213374770052E-32,1.2976852986771E-32,
-1.));
#126542=DIRECTION('ref_axis',(-0.685141714967848,0.728409795658265,3.00213374770051E-32));
#126543=DIRECTION('center_axis',(-4.00818924926656E-35,-4.12526018083156E-32,
1.));
#126544=DIRECTION('ref_axis',(0.983786782322298,0.179342038931033,7.43775775555807E-33));
#126545=DIRECTION('center_axis',(3.00213374770052E-32,-1.2976852986771E-32,
1.));
#126546=DIRECTION('ref_axis',(0.685141714967848,-0.728409795658265,-3.00213374770051E-32));
#126547=DIRECTION('center_axis',(-0.299077797577255,-0.66755307397516,0.681854357192688));
#126548=DIRECTION('ref_axis',(-0.517575453416348,-0.486831088616092,-0.703641344136154));
#126549=DIRECTION('center_axis',(-0.299340976225778,-0.668140498776498,
0.681163162426516));
#126550=DIRECTION('ref_axis',(-0.517089918871244,-0.486374395182141,-0.704313824593084));
#126551=DIRECTION('center_axis',(0.685197846296135,0.257915989392372,-0.681163162426516));
#126552=DIRECTION('ref_axis',(0.517089918871247,0.486374395182137,0.704313824593084));
#126553=DIRECTION('center_axis',(0.68459542478528,0.25768923132411,-0.681854357192686));
#126554=DIRECTION('ref_axis',(0.517575453416338,0.486831088616102,0.703641344136154));
#126555=DIRECTION('center_axis',(3.00213374770052E-32,-1.2976852986771E-32,
1.));
#126556=DIRECTION('ref_axis',(0.685141714967854,-0.72840979565826,-3.00213374770052E-32));
#126557=DIRECTION('center_axis',(-4.00818924926656E-35,-4.12526018083156E-32,
1.));
#126558=DIRECTION('ref_axis',(0.239176321393792,0.970976151758906,4.00648791934816E-32));
#126559=DIRECTION('center_axis',(3.00213374770052E-32,-1.2976852986771E-32,
1.));
#126560=DIRECTION('ref_axis',(-0.685141714967843,0.72840979565827,3.0021337477005E-32));
#126561=DIRECTION('center_axis',(-3.00213374770052E-32,1.2976852986771E-32,
-1.));
#126562=DIRECTION('ref_axis',(0.685141714967852,-0.728409795658261,-3.00213374770052E-32));
#126563=DIRECTION('center_axis',(0.274824631535754,-0.961494369146922,-2.37760101267756E-32));
#126564=DIRECTION('ref_axis',(0.961494369146922,0.274824631535754,-2.67176538956511E-32));
#126565=DIRECTION('',(3.22231069999663E-32,-1.55178304703028E-32,1.));
#126566=DIRECTION('',(0.703629032489313,0.201118795696443,-0.681511125848849));
#126567=DIRECTION('center_axis',(-0.274820009156125,0.961495690350648,2.13514022130774E-6));
#126568=DIRECTION('ref_axis',(0.953358516276989,0.272494485408876,-0.129824092001024));
#126569=DIRECTION('',(4.40532634530388E-33,2.59873620878172E-32,-1.));
#126570=DIRECTION('center_axis',(-0.876233464203463,0.481886829255582,3.57128027962392E-32));
#126571=DIRECTION('ref_axis',(-0.481886829255582,-0.876233464203463,1.93064851106168E-33));
#126572=DIRECTION('center_axis',(0.876233464203449,-0.481886829255608,-1.7249630376986E-14));
#126573=DIRECTION('ref_axis',(0.478271885807456,0.86966027268176,0.122257978738674));
#126574=DIRECTION('',(-0.352648517057147,-0.641234441340787,0.681511125848848));
#126575=DIRECTION('',(3.22231069999663E-32,-1.55178304703028E-32,1.));
#126576=DIRECTION('',(1.3865475201236E-32,-4.88982225644841E-32,1.));
#126577=DIRECTION('center_axis',(3.22231069999663E-32,-1.55178304703028E-32,
1.));
#126578=DIRECTION('ref_axis',(0.623489801858739,-0.781831482468025,-3.22231069999663E-32));
#126579=DIRECTION('center_axis',(-0.265567257777731,-0.211782821036219,
-0.940543496235213));
#126580=DIRECTION('ref_axis',(0.735420832139579,0.586326077882361,-0.33967326955505));
#126581=DIRECTION('center_axis',(-0.265567257777731,-0.211782821036219,
-0.940543496235213));
#126582=DIRECTION('ref_axis',(0.735420832139579,0.586326077882361,-0.33967326955505));
#126583=DIRECTION('center_axis',(0.35380561798019,0.643338442713452,-0.678923583927297));
#126584=DIRECTION('ref_axis',(0.553323974502355,0.441261145096295,0.706485089063615));
#126585=DIRECTION('center_axis',(-0.70593776133287,-0.201778701333043,0.678923583927297));
#126586=DIRECTION('ref_axis',(-0.553323974502362,-0.441261145096289,-0.706485089063613));
#126587=DIRECTION('center_axis',(-0.298237131350729,0.954182537057364,-0.0242960790758392));
#126588=DIRECTION('ref_axis',(-0.662725964726312,-0.188687272070395,0.72470091005615));
#126589=DIRECTION('center_axis',(-3.22231069999663E-32,1.55178304703028E-32,
-1.));
#126590=DIRECTION('ref_axis',(-0.623489801858739,0.781831482468025,3.22231069999663E-32));
#126591=DIRECTION('center_axis',(-4.30215046728545E-35,-4.12492093150131E-32,
1.));
#126592=DIRECTION('ref_axis',(0.995131354063957,0.0985575373009913,4.10823253389977E-33));
#126593=DIRECTION('center_axis',(3.22231069999663E-32,-1.55178304703028E-32,
1.));
#126594=DIRECTION('ref_axis',(0.623489801858739,-0.781831482468025,-3.22231069999663E-32));
#126595=DIRECTION('center_axis',(-0.352494413667353,-0.640954229185404,
0.681854357192688));
#126596=DIRECTION('ref_axis',(-0.555534517033615,-0.443023993939942,-0.703641344136152));
#126597=DIRECTION('center_axis',(-0.352804597185329,-0.641518247876089,
0.681163162426516));
#126598=DIRECTION('ref_axis',(-0.55501337331005,-0.442608395688629,-0.704313824593083));
#126599=DIRECTION('center_axis',(0.703940454498133,0.201207809674652,-0.681163162426516));
#126600=DIRECTION('ref_axis',(0.555013373310052,0.442608395688626,0.704313824593084));
#126601=DIRECTION('center_axis',(0.703321554607476,0.201030909070899,-0.681854357192686));
#126602=DIRECTION('ref_axis',(0.555534517033603,0.443023993939952,0.703641344136155));
#126603=DIRECTION('center_axis',(3.22231069999663E-32,-1.55178304703028E-32,
1.));
#126604=DIRECTION('ref_axis',(0.623489801858739,-0.781831482468025,-3.22231069999663E-32));
#126605=DIRECTION('center_axis',(-4.30215046728545E-35,-4.12492093150131E-32,
1.));
#126606=DIRECTION('ref_axis',(0.317524052386177,0.948250218115588,3.91282320925602E-32));
#126607=DIRECTION('center_axis',(3.22231069999663E-32,-1.55178304703028E-32,
1.));
#126608=DIRECTION('ref_axis',(-0.623489801858734,0.781831482468029,3.22231069999662E-32));
#126609=DIRECTION('center_axis',(-3.22231069999663E-32,1.55178304703028E-32,
-1.));
#126610=DIRECTION('ref_axis',(0.623489801858742,-0.781831482468023,-3.22231069999663E-32));
#126611=DIRECTION('center_axis',(0.973302335538192,-0.229526825525689,6.39195957963004E-33));
#126612=DIRECTION('ref_axis',(0.229526825525689,0.973302335538192,2.07003539272685E-33));
#126613=DIRECTION('',(-6.69643783993806E-33,-5.47644091186761E-34,1.));
#126614=DIRECTION('',(0.167969510126485,0.712270193825419,-0.681511125848851));
#126615=DIRECTION('center_axis',(-0.973301232076518,0.229531504664986,2.13514020350011E-6));
#126616=DIRECTION('ref_axis',(0.227588719328633,0.965064287994901,-0.129824092029358));
#126617=DIRECTION('',(1.54403351517636E-32,3.76259056661216E-32,-1.));
#126618=DIRECTION('center_axis',(-0.848320692261111,-0.529482769390685,
-5.97069489410176E-33));
#126619=DIRECTION('ref_axis',(0.529482769390685,-0.848320692261111,3.08107063799472E-33));
#126620=DIRECTION('center_axis',(0.848320692261124,0.529482769390664,-1.61810692031897E-14));
#126621=DIRECTION('ref_axis',(0.525510778145861,-0.84195689242242,-0.122257978696332));
#126622=DIRECTION('',(0.387479594994073,-0.620807658463926,0.681511125848849));
#126623=DIRECTION('',(-6.69643783993806E-33,-5.47644091186761E-34,1.));
#126624=DIRECTION('',(1.34743764138189E-32,-3.28646902736502E-32,1.));
#126625=DIRECTION('center_axis',(-6.69643783993806E-33,-5.47644091186761E-34,
1.));
#126626=DIRECTION('ref_axis',(0.986712473391289,0.162476136260207,6.69643783993806E-33));
#126627=DIRECTION('center_axis',(0.0551888008202831,-0.335159854328824,
-0.940543496235182));
#126628=DIRECTION('ref_axis',(-0.152698253836419,0.928065360427289,-0.339673269555134));
#126629=DIRECTION('center_axis',(0.0551888008202831,-0.335159854328824,
-0.940543496235182));
#126630=DIRECTION('ref_axis',(-0.152698253836419,0.928065360427289,-0.339673269555134));
#126631=DIRECTION('center_axis',(-0.388750982722458,0.622844636020603,-0.678923583927297));
#126632=DIRECTION('ref_axis',(-0.11498889913398,0.698323973530004,0.706485089063614));
#126633=DIRECTION('center_axis',(-0.16852064721002,-0.714607275817445,0.678923583927297));
#126634=DIRECTION('ref_axis',(0.114988899133974,-0.698323973530004,-0.706485089063614));
#126635=DIRECTION('center_axis',(-0.978350395317852,0.205524218823469,-0.02429607907475));
#126636=DIRECTION('ref_axis',(0.15885123442695,0.670503884894633,-0.724700507563116));
#126637=DIRECTION('center_axis',(6.69643783993806E-33,5.47644091186761E-34,
-1.));
#126638=DIRECTION('ref_axis',(-0.98671247339129,-0.162476136260201,-6.69643783993806E-33));
#126639=DIRECTION('center_axis',(8.94050445919518E-36,-4.12691962127155E-32,
1.));
#126640=DIRECTION('ref_axis',(0.399783842199988,0.916609447647042,3.78241608761507E-32));
#126641=DIRECTION('center_axis',(-6.69643783993806E-33,-5.47644091186761E-34,
1.));
#126642=DIRECTION('ref_axis',(0.98671247339129,0.162476136260201,6.69643783993806E-33));
#126643=DIRECTION('center_axis',(0.387310270819507,-0.620536372580259,0.681854357192688));
#126644=DIRECTION('ref_axis',(0.115448282540205,-0.701113794530378,-0.703641344136153));
#126645=DIRECTION('center_axis',(0.387651091149399,-0.621082424227082,0.681163162426516));
#126646=DIRECTION('ref_axis',(0.115339981172796,-0.700456083726969,-0.704313824593084));
#126647=DIRECTION('center_axis',(0.168043852428818,0.712585440360656,-0.681163162426516));
#126648=DIRECTION('ref_axis',(-0.115339981172794,0.700456083726969,0.704313824593084));
#126649=DIRECTION('center_axis',(0.16789610936159,0.711958939854392,-0.681854357192686));
#126650=DIRECTION('ref_axis',(-0.115448282540218,0.701113794530375,0.703641344136154));
#126651=DIRECTION('center_axis',(-6.69643783993806E-33,-5.47644091186761E-34,
1.));
#126652=DIRECTION('ref_axis',(0.98671247339129,0.162476136260201,6.69643783993806E-33));
#126653=DIRECTION('center_axis',(8.94050445919518E-36,-4.12691962127155E-32,
1.));
#126654=DIRECTION('ref_axis',(-0.67257303458172,0.740030751491812,3.05464874289737E-32));
#126655=DIRECTION('center_axis',(-6.69643783993806E-33,-5.47644091186761E-34,
1.));
#126656=DIRECTION('ref_axis',(-0.98671247339129,-0.162476136260201,-6.69643783993806E-33));
#126657=DIRECTION('center_axis',(6.69643783993806E-33,5.47644091186761E-34,
-1.));
#126658=DIRECTION('ref_axis',(0.986712473391289,0.162476136260206,6.69643783993805E-33));
#126659=DIRECTION('center_axis',(0.988772319411911,-0.149429917903982,9.6931456824374E-33));
#126660=DIRECTION('ref_axis',(0.149429917903982,0.988772319411911,2.70762924361271E-33));
#126661=DIRECTION('',(-9.98891495440864E-33,-1.2287828837565E-33,1.));
#126662=DIRECTION('',(0.109353972247411,0.72359124794178,-0.681511125848853));
#126663=DIRECTION('center_axis',(-0.988771601015213,0.149434671416156,2.1351401804249E-6));
#126664=DIRECTION('ref_axis',(0.148169737941467,0.980403709598452,-0.129824092386398));
#126665=DIRECTION('',(1.56814951331063E-32,3.8896378407338E-32,-1.));
#126666=DIRECTION('center_axis',(-0.802340213955593,-0.596866970999144,
-8.74792807954779E-33));
#126667=DIRECTION('ref_axis',(0.596866970999144,-0.802340213955593,4.97615149054778E-33));
#126668=DIRECTION('center_axis',(0.802340213955602,0.596866970999133,-1.20340341715621E-14));
#126669=DIRECTION('ref_axis',(0.59238948746369,-0.79632134329872,-0.122257978673905));
#126670=DIRECTION('',(0.436791876068471,-0.587158788016343,0.681511125848849));
#126671=DIRECTION('',(-9.98891495440864E-33,-1.2287828837565E-33,1.));
#126672=DIRECTION('',(1.2748921859584E-32,-3.17941881426318E-32,1.));
#126673=DIRECTION('center_axis',(-9.98891495440864E-33,-1.2287828837565E-33,
1.));
#126674=DIRECTION('ref_axis',(0.970185955574064,0.242361737093215,9.98891495440864E-33));
#126675=DIRECTION('center_axis',(0.0823238042383934,-0.329546237947607,
-0.940543496235181));
#126676=DIRECTION('ref_axis',(-0.227836105607519,0.912530974231188,-0.339673269555138));
#126677=DIRECTION('center_axis',(0.0823238042383934,-0.329546237947607,
-0.940543496235181));
#126678=DIRECTION('ref_axis',(-0.227836105607519,0.912530974231188,-0.339673269555138));
#126679=DIRECTION('center_axis',(-0.438225065940319,0.589085357795385,-0.678923583927297));
#126680=DIRECTION('ref_axis',(-0.1715261698242,0.686627695331478,0.706485089063614));
#126681=DIRECTION('center_axis',(-0.109712781589005,-0.725965476275089,
0.678923583927297));
#126682=DIRECTION('ref_axis',(0.17152616982419,-0.68662769533148,-0.706485089063615));
#126683=DIRECTION('center_axis',(-0.991847146913457,0.125095714160269,-0.0242960790739686));
#126684=DIRECTION('ref_axis',(0.103670414118919,0.681221032856078,-0.724700179129901));
#126685=DIRECTION('center_axis',(9.98891495440864E-33,1.2287828837565E-33,
-1.));
#126686=DIRECTION('ref_axis',(-0.970185955574064,-0.242361737093213,-9.98891495440864E-33));
#126687=DIRECTION('center_axis',(1.3336335052612E-35,-4.12682868151287E-32,
1.));
#126688=DIRECTION('ref_axis',(0.323741415074756,0.946145599876359,3.90414904605877E-32));
#126689=DIRECTION('center_axis',(-9.98891495440864E-33,-1.2287828837565E-33,
1.));
#126690=DIRECTION('ref_axis',(0.970185955574064,0.242361737093213,9.98891495440864E-33));
#126691=DIRECTION('center_axis',(0.436601002988114,-0.586902206306229,0.681854357192688));
#126692=DIRECTION('ref_axis',(0.172211420981002,-0.689370789420303,-0.703641344136154));
#126693=DIRECTION('center_axis',(0.436985197544986,-0.587418660990335,0.681163162426516));
#126694=DIRECTION('ref_axis',(0.17204987044109,-0.6887240946622,-0.704313824593084));
#126695=DIRECTION('center_axis',(0.109402371662638,0.723911505107978,-0.681163162426516));
#126696=DIRECTION('ref_axis',(-0.172049870441086,0.688724094662201,0.704313824593084));
#126697=DIRECTION('center_axis',(0.109306185805685,0.723275046798907,-0.681854357192686));
#126698=DIRECTION('ref_axis',(-0.172211420981012,0.689370789420299,0.703641344136154));
#126699=DIRECTION('center_axis',(-9.98891495440864E-33,-1.2287828837565E-33,
1.));
#126700=DIRECTION('ref_axis',(0.970185955574064,0.242361737093213,9.98891495440864E-33));
#126701=DIRECTION('center_axis',(1.3336335052612E-35,-4.12682868151287E-32,
1.));
#126702=DIRECTION('ref_axis',(-0.730654479649412,0.682747414032633,2.81855603575344E-32));
#126703=DIRECTION('center_axis',(-9.98891495440864E-33,-1.2287828837565E-33,
1.));
#126704=DIRECTION('ref_axis',(-0.970185955574069,-0.242361737093194,-9.98891495440866E-33));
#126705=DIRECTION('center_axis',(9.98891495440864E-33,1.2287828837565E-33,
-1.));
#126706=DIRECTION('ref_axis',(0.970185955574064,0.242361737093213,9.98891495440864E-33));
#126707=DIRECTION('center_axis',(0.997662186635892,-0.0683385788328237,
1.30353171787961E-32));
#126708=DIRECTION('ref_axis',(0.0683385788328237,0.997662186635892,3.07402423946217E-33));
#126709=DIRECTION('',(-1.32149174879126E-32,-2.17602269387955E-33,1.));
#126710=DIRECTION('',(0.0500107017251656,0.730096921687246,-0.681511125848848));
#126711=DIRECTION('center_axis',(-0.99766185808497,0.0683433750840998,2.13514018679782E-6));
#126712=DIRECTION('ref_axis',(0.0677647114083837,0.989218706359218,-0.129824092050492));
#126713=DIRECTION('',(1.58182973516028E-32,4.01822805326141E-32,-1.));
#126714=DIRECTION('center_axis',(-0.751020293903019,-0.660279121391721,
-1.13614535681195E-32));
#126715=DIRECTION('ref_axis',(0.660279121391721,-0.751020293903019,7.09129690508596E-33));
#126716=DIRECTION('center_axis',(0.751020293903004,0.660279121391738,4.604989820407E-15));
#126717=DIRECTION('ref_axis',(0.655325942479862,-0.745386407018453,-0.122257978655797));
#126718=DIRECTION('',(0.483197379273218,-0.549602472708896,0.681511125848846));
#126719=DIRECTION('',(-1.32149174879126E-32,-2.17602269387955E-33,1.));
#126720=DIRECTION('',(1.19386253337975E-32,-3.07863793001058E-32,1.));
#126721=DIRECTION('center_axis',(-1.32149174879126E-32,-2.17602269387955E-33,
1.));
#126722=DIRECTION('ref_axis',(0.94720301029191,0.320634460552734,1.32149174879126E-32));
#126723=DIRECTION('center_axis',(0.108910956321738,-0.321739545724076,-0.940543496235208));
#126724=DIRECTION('ref_axis',(-0.301457745685325,0.890923844958758,-0.339673269555061));
#126725=DIRECTION('center_axis',(0.108910956321738,-0.321739545724076,-0.940543496235208));
#126726=DIRECTION('ref_axis',(-0.301457745685325,0.890923844958758,-0.339673269555061));
#126727=DIRECTION('center_axis',(-0.484782833646393,0.551405813706283,-0.678923583927297));
#126728=DIRECTION('ref_axis',(-0.226921962154062,0.670362023106118,0.706485089063614));
#126729=DIRECTION('center_axis',(-0.05017479550785,-0.732492496263996,0.678923583927297));
#126730=DIRECTION('ref_axis',(0.226921962154054,-0.670362023106121,-0.706485089063614));
#126731=DIRECTION('center_axis',(-0.998743319389926,0.0438347181477059,
-0.0242960790849923));
#126732=DIRECTION('ref_axis',(0.0477996139550044,0.687404086140894,-0.724700503147718));
#126733=DIRECTION('center_axis',(1.32149174879126E-32,2.17602269387955E-33,
-1.));
#126734=DIRECTION('ref_axis',(-0.947203010291908,-0.320634460552743,-1.32149174879126E-32));
#126735=DIRECTION('center_axis',(1.76434145365967E-35,-4.1267022142485E-32,
1.));
#126736=DIRECTION('ref_axis',(0.245544542245741,0.969385309241547,3.99993127769245E-32));
#126737=DIRECTION('center_axis',(-1.32149174879126E-32,-2.17602269387955E-33,
1.));
#126738=DIRECTION('ref_axis',(0.947203010291908,0.320634460552741,1.32149174879126E-32));
#126739=DIRECTION('center_axis',(0.48298622751593,-0.549362302681278,0.681854357192688));
#126740=DIRECTION('ref_axis',(0.227828520828051,-0.673040135444811,-0.703641344136153));
#126741=DIRECTION('center_axis',(0.483411239548394,-0.549845723481955,0.681163162426516));
#126742=DIRECTION('ref_axis',(0.227614796207828,-0.672408760378932,-0.704313824593084));
#126743=DIRECTION('center_axis',(0.0500328361631631,0.730420058225798,-0.681163162426516));
#126744=DIRECTION('ref_axis',(-0.227614796207826,0.672408760378933,0.704313824593083));
#126745=DIRECTION('center_axis',(0.0499888476174943,0.729777877638959,-0.681854357192686));
#126746=DIRECTION('ref_axis',(-0.227828520828061,0.673040135444807,0.703641344136154));
#126747=DIRECTION('center_axis',(-1.32149174879126E-32,-2.17602269387955E-33,
1.));
#126748=DIRECTION('ref_axis',(0.947203010291908,0.320634460552741,1.32149174879126E-32));
#126749=DIRECTION('center_axis',(1.76434145365967E-35,-4.1267022142485E-32,
1.));
#126750=DIRECTION('ref_axis',(-0.783873539704543,0.620920505178457,2.56373704417276E-32));
#126751=DIRECTION('center_axis',(-1.32149174879126E-32,-2.17602269387955E-33,
1.));
#126752=DIRECTION('ref_axis',(-0.947203010291908,-0.320634460552741,-1.32149174879126E-32));
#126753=DIRECTION('center_axis',(1.32149174879126E-32,2.17602269387955E-33,
-1.));
#126754=DIRECTION('ref_axis',(0.94720301029191,0.320634460552736,1.32149174879126E-32));
#126755=DIRECTION('center_axis',(0.999912776610487,0.0132075422053949,1.63962324688173E-32));
#126756=DIRECTION('ref_axis',(-0.0132075422053949,0.999912776610487,3.1667820820288E-33));
#126757=DIRECTION('',(-1.63529769258424E-32,-3.38305979690313E-33,1.));
#126758=DIRECTION('',(-0.00966538176587747,0.731743920876393,-0.681511125848848));
#126759=DIRECTION('center_axis',(-0.999912840091796,-0.013202735133283,
2.13514020082165E-6));
#126760=DIRECTION('ref_axis',(0.0130912781053972,-0.991450615801791,0.129824092000736));
#126761=DIRECTION('',(1.58498314110597E-32,4.14750545754651E-32,-1.));
#126762=DIRECTION('center_axis',(-0.694702457704146,-0.719297223169824,
-1.37938787788918E-32));
#126763=DIRECTION('ref_axis',(0.719297223169824,-0.694702457704146,9.41243093784996E-33));
#126764=DIRECTION('center_axis',(0.694702457704154,0.719297223169816,-1.24411050949079E-14));
#126765=DIRECTION('ref_axis',(0.71390131146342,-0.68949104717282,-0.122257978714422));
#126766=DIRECTION('',(0.52638728364086,-0.508388643623588,0.681511125848848));
#126767=DIRECTION('',(-1.63529769258424E-32,-3.38305979690313E-33,1.));
#126768=DIRECTION('',(1.10488792261492E-32,-2.98479705476425E-32,1.));
#126769=DIRECTION('center_axis',(-1.63529769258424E-32,-3.38305979690313E-33,
1.));
#126770=DIRECTION('ref_axis',(0.917916585253758,0.396773414578245,1.63529769258424E-32));
#126771=DIRECTION('center_axis',(0.134773323959819,-0.311791729907097,-0.940543496235215));
#126772=DIRECTION('ref_axis',(-0.373073234202291,0.863387764490341,-0.339673269555044));
#126773=DIRECTION('center_axis',(0.134773323959819,-0.311791729907097,-0.940543496235215));
#126774=DIRECTION('ref_axis',(-0.373073234202291,0.863387764490341,-0.339673269555044));
#126775=DIRECTION('center_axis',(-0.528114451578088,0.51005675490252,-0.678923583927297));
#126776=DIRECTION('ref_axis',(-0.280807626265276,0.649635202218937,0.706485089063614));
#126777=DIRECTION('center_axis',(0.00969709555915143,-0.73414489954302,
0.678923583927297));
#126778=DIRECTION('ref_axis',(0.280807626265272,-0.649635202218938,-0.706485089063614));
#126779=DIRECTION('center_axis',(-0.998993019856255,-0.0377179906659659,
-0.024296079078787));
#126780=DIRECTION('ref_axis',(-0.0083891685448101,0.689011582292177,-0.724701774054927));
#126781=DIRECTION('center_axis',(1.63529769258424E-32,3.38305979690313E-33,
-1.));
#126782=DIRECTION('ref_axis',(-0.917916585253758,-0.396773414578245,-1.63529769258424E-32));
#126783=DIRECTION('center_axis',(2.18330800078025E-35,-4.12654106109723E-32,
1.));
#126784=DIRECTION('ref_axis',(0.16571361100008,0.986173919311048,4.06912536756749E-32));
#126785=DIRECTION('center_axis',(-1.63529769258424E-32,-3.38305979690313E-33,
1.));
#126786=DIRECTION('ref_axis',(0.917916585253758,0.396773414578245,1.63529769258424E-32));
#126787=DIRECTION('center_axis',(0.526157258386746,-0.508166483570384,0.681854357192688));
#126788=DIRECTION('ref_axis',(0.281929459458051,-0.65223051041174,-0.703641344136154));
#126789=DIRECTION('center_axis',(0.526620259509848,-0.50861365340196,0.681163162426515));
#126790=DIRECTION('ref_axis',(0.281664983059597,-0.651618656734981,-0.704313824593083));
#126791=DIRECTION('center_axis',(-0.00966965960614047,0.732067786366952,
-0.681163162426516));
#126792=DIRECTION('ref_axis',(-0.281664983059596,0.65161865673498,0.704313824593084));
#126793=DIRECTION('center_axis',(-0.00966115810401136,0.731424157108198,
-0.681854357192686));
#126794=DIRECTION('ref_axis',(-0.281929459458062,0.652230510411734,0.703641344136154));
#126795=DIRECTION('center_axis',(-1.63529769258424E-32,-3.38305979690313E-33,
1.));
#126796=DIRECTION('ref_axis',(0.917916585253758,0.396773414578245,1.63529769258424E-32));
#126797=DIRECTION('center_axis',(2.18330800078025E-35,-4.12654106109723E-32,
1.));
#126798=DIRECTION('ref_axis',(-0.831876050682975,0.554961472806984,2.29188754650213E-32));
#126799=DIRECTION('center_axis',(-1.63529769258424E-32,-3.38305979690313E-33,
1.));
#126800=DIRECTION('ref_axis',(-0.917916585253758,-0.396773414578245,-1.63529769258424E-32));
#126801=DIRECTION('center_axis',(1.63529769258424E-32,3.38305979690313E-33,
-1.));
#126802=DIRECTION('ref_axis',(0.917916585253759,0.396773414578243,1.63529769258424E-32));
#126803=DIRECTION('center_axis',(0.995509112030734,0.0946657692293274,1.97535252157579E-32));
#126804=DIRECTION('ref_axis',(-0.0946657692293274,0.995509112030734,2.98528548317427E-33));
#126805=DIRECTION('',(-1.9382210000382E-32,-4.8418615600537E-33,1.));
#126806=DIRECTION('',(-0.0692771437359437,0.72852128500135,-0.681511125848853));
#126807=DIRECTION('center_axis',(-0.995509567121819,-0.0946609833266599,
2.13514020730258E-6));
#126808=DIRECTION('ref_axis',(0.0938601473240115,-0.987084584970317,0.129824091979465));
#126809=DIRECTION('',(1.57758874575141E-32,4.27660973379285E-32,-1.));
#126810=DIRECTION('center_axis',(-0.63376149126709,-0.773528520603419,-1.60290163234089E-32));
#126811=DIRECTION('ref_axis',(0.773528520603419,-0.63376149126709,1.19241068248119E-32));
#126812=DIRECTION('center_axis',(0.633761491266992,0.773528520603499,5.86436548952487E-14));
#126813=DIRECTION('ref_axis',(0.76772578501665,-0.629007238177413,-0.122257978639401));
#126814=DIRECTION('',(0.566074167483661,-0.463791571993187,0.681511125848851));
#126815=DIRECTION('',(-1.9382210000382E-32,-4.8418615600537E-33,1.));
#126816=DIRECTION('',(1.00856046501876E-32,-2.89852068406629E-32,1.));
#126817=DIRECTION('center_axis',(-1.9382210000382E-32,-4.8418615600537E-33,
1.));
#126818=DIRECTION('ref_axis',(0.882521576786319,0.47027190699274,1.9382210000382E-32));
#126819=DIRECTION('center_axis',(0.159738797363031,-0.2997689915697,-0.940543496235181));
#126820=DIRECTION('ref_axis',(-0.442205981897974,0.830105980898446,-0.339673269555138));
#126821=DIRECTION('center_axis',(0.159738797363031,-0.2997689915697,-0.940543496235181));
#126822=DIRECTION('ref_axis',(-0.442205981897974,0.830105980898446,-0.339673269555138));
#126823=DIRECTION('center_axis',(-0.567931554967282,0.465313352548322,-0.678923583927297));
#126824=DIRECTION('ref_axis',(-0.332824561953696,0.62458516624325,0.706485089063614));
#126825=DIRECTION('center_axis',(0.0695044540551147,-0.730911689640968,
0.678923583927297));
#126826=DIRECTION('ref_axis',(0.332824561953692,-0.624585166243252,-0.706485089063614));
#126827=DIRECTION('center_axis',(-0.9925945865974,-0.119019692483191,-0.0242960790816824));
#126828=DIRECTION('ref_axis',(-0.0645222095089911,0.686035958596192,-0.724701005928018));
#126829=DIRECTION('center_axis',(1.9382210000382E-32,4.8418615600537E-33,
-1.));
#126830=DIRECTION('ref_axis',(-0.882521576786316,-0.470271906992746,-1.9382210000382E-32));
#126831=DIRECTION('center_axis',(2.58774499337527E-35,-4.12634629450669E-32,
1.));
#126832=DIRECTION('ref_axis',(0.0847798830140602,0.996399704654775,4.11127084043198E-32));
#126833=DIRECTION('center_axis',(-1.9382210000382E-32,-4.8418615600537E-33,
1.));
#126834=DIRECTION('ref_axis',(0.882521576786316,0.470271906992746,1.9382210000382E-32));
#126835=DIRECTION('center_axis',(0.565826799512835,-0.463588900352897,0.681854357192688));
#126836=DIRECTION('ref_axis',(0.334154204050439,-0.627080398942342,-0.703641344136152));
#126837=DIRECTION('center_axis',(0.56632470853049,-0.463996843373922,0.681163162426516));
#126838=DIRECTION('ref_axis',(0.333840735920563,-0.626492138439965,-0.704313824593083));
#126839=DIRECTION('center_axis',(-0.0693078053861466,0.728843724172517,
-0.681163162426516));
#126840=DIRECTION('ref_axis',(-0.333840735920559,0.626492138439966,0.704313824593084));
#126841=DIRECTION('center_axis',(-0.0692468704123135,0.728202929488373,
-0.681854357192686));
#126842=DIRECTION('ref_axis',(-0.334154204050452,0.627080398942332,0.703641344136155));
#126843=DIRECTION('center_axis',(-1.9382210000382E-32,-4.8418615600537E-33,
1.));
#126844=DIRECTION('ref_axis',(0.882521576786316,0.470271906992746,1.9382210000382E-32));
#126845=DIRECTION('center_axis',(2.58774499337527E-35,-4.12634629450669E-32,
1.));
#126846=DIRECTION('ref_axis',(-0.874342563793985,0.485309263396199,2.00481665629663E-32));
#126847=DIRECTION('center_axis',(-1.9382210000382E-32,-4.8418615600537E-33,
1.));
#126848=DIRECTION('ref_axis',(-0.882521576786316,-0.470271906992746,-1.9382210000382E-32));
#126849=DIRECTION('center_axis',(1.9382210000382E-32,4.8418615600537E-33,
-1.));
#126850=DIRECTION('ref_axis',(0.882521576786321,0.470271906992738,1.9382210000382E-32));
#126851=DIRECTION('center_axis',(0.984480498557858,0.175494011177791,2.30848531903014E-32));
#126852=DIRECTION('ref_axis',(-0.175494011177791,0.984480498557858,2.53074227281913E-33));
#126853=DIRECTION('',(-2.22824576652086E-32,-6.54271989828285E-33,1.));
#126854=DIRECTION('',(-0.128427877744372,0.720450460172186,-0.681511125848846));
#126855=DIRECTION('center_axis',(-0.984481342230153,-0.175489278294025,
2.13514017808401E-6));
#126856=DIRECTION('ref_axis',(0.174004392741512,-0.976149669043933,0.129824092263641));
#126857=DIRECTION('',(1.55969575757769E-32,4.40468171434272E-32,-1.));
#126858=DIRECTION('center_axis',(-0.568602946668937,-0.822612113355622,
-1.80519917300838E-32));
#126859=DIRECTION('ref_axis',(0.822612113355622,-0.568602946668937,1.46096097773413E-32));
#126860=DIRECTION('center_axis',(0.568602946668932,0.822612113355625,-5.82620259045788E-15));
#126861=DIRECTION('ref_axis',(0.816441170119489,-0.564337489777616,-0.122257978739302));
#126862=DIRECTION('',(0.601993921137532,-0.416108043971394,0.681511125848844));
#126863=DIRECTION('',(-2.22824576652086E-32,-6.54271989828285E-33,1.));
#126864=DIRECTION('',(9.0552120392866E-33,-2.8203829729291E-32,1.));
#126865=DIRECTION('center_axis',(-2.22824576652086E-32,-6.54271989828285E-33,
1.));
#126866=DIRECTION('ref_axis',(0.841253532831182,0.540640817455597,2.22824576652086E-32));
#126867=DIRECTION('center_axis',(0.183641235424755,-0.285751340051653,-0.940543496235211));
#126868=DIRECTION('ref_axis',(-0.508395921744393,0.791299978960854,-0.339673269555054));
#126869=DIRECTION('center_axis',(0.183641235424755,-0.285751340051653,-0.940543496235211));
#126870=DIRECTION('ref_axis',(-0.508395921744393,0.791299978960854,-0.339673269555054));
#126871=DIRECTION('center_axis',(-0.60396916756028,0.417473366604215,-0.678923583927297));
#126872=DIRECTION('ref_axis',(-0.382626605094497,0.595378619035516,0.706485089063613));
#126873=DIRECTION('center_axis',(0.128849271876769,-0.722814383036296,0.678923583927297));
#126874=DIRECTION('ref_axis',(0.382626605094492,-0.595378619035518,-0.706485089063614));
#126875=DIRECTION('center_axis',(-0.979590600131391,-0.199529337881564,
-0.0242960790821469));
#126876=DIRECTION('ref_axis',(-0.120225842285555,0.678494183971453,-0.724700896345272));
#126877=DIRECTION('center_axis',(2.22824576652086E-32,6.54271989828285E-33,
-1.));
#126878=DIRECTION('ref_axis',(-0.841253532831175,-0.540640817455607,-2.22824576652086E-32));
#126879=DIRECTION('center_axis',(2.97496096998759E-35,-4.1261192106164E-32,
1.));
#126880=DIRECTION('ref_axis',(0.00328195889423764,0.999994614358406,4.12608722511754E-32));
#126881=DIRECTION('center_axis',(-2.22824576652086E-32,-6.54271989828285E-33,
1.));
#126882=DIRECTION('ref_axis',(0.841253532831175,0.540640817455607,2.22824576652086E-32));
#126883=DIRECTION('center_axis',(0.601730856643017,-0.415926209490346,0.681854357192688));
#126884=DIRECTION('ref_axis',(0.384155207546441,-0.597757170878961,-0.703641344136152));
#126885=DIRECTION('center_axis',(0.602260360052862,-0.416292210907321,0.681163162426516));
#126886=DIRECTION('ref_axis',(0.383794833763824,-0.597196418327555,-0.704313824593085));
#126887=DIRECTION('center_axis',(-0.128484719156291,0.720769327244464,-0.681163162426516));
#126888=DIRECTION('ref_axis',(-0.38379483376382,0.59719641832756,0.704313824593083));
#126889=DIRECTION('center_axis',(-0.128371756222951,0.72013563151783,-0.681854357192686));
#126890=DIRECTION('ref_axis',(-0.384155207546449,0.597757170878953,0.703641344136155));
#126891=DIRECTION('center_axis',(-2.22824576652086E-32,-6.54271989828285E-33,
1.));
#126892=DIRECTION('ref_axis',(0.841253532831175,0.540640817455607,2.22824576652086E-32));
#126893=DIRECTION('center_axis',(2.97496096998759E-35,-4.1261192106164E-32,
1.));
#126894=DIRECTION('ref_axis',(-0.91099047139932,0.412427400907898,1.70443478296712E-32));
#126895=DIRECTION('center_axis',(-2.22824576652086E-32,-6.54271989828285E-33,
1.));
#126896=DIRECTION('ref_axis',(-0.841253532831175,-0.540640817455607,-2.22824576652086E-32));
#126897=DIRECTION('center_axis',(2.22824576652086E-32,6.54271989828285E-33,
-1.));
#126898=DIRECTION('ref_axis',(0.841253532831181,0.540640817455599,2.22824576652086E-32));
#126899=DIRECTION('center_axis',(0.966900329794929,0.255154369436341,2.63680469544076E-32));
#126900=DIRECTION('ref_axis',(-0.255154369436341,0.966900329794929,1.80617736103395E-33));
#126901=DIRECTION('',(-2.503441925062E-32,-8.47431587997155E-33,1.));
#126902=DIRECTION('',(-0.186723945415519,0.707585156396526,-0.681511125848849));
#126903=DIRECTION('center_axis',(-0.966901556433968,-0.255149721067868,
2.13514022410592E-6));
#126904=DIRECTION('ref_axis',(0.252990667638338,-0.958718638164101,0.129824092235145));
#126905=DIRECTION('',(1.53142325146899E-32,4.53086910129595E-32,-1.));
#126906=DIRECTION('center_axis',(-0.499660443273585,-0.866221358214888,
-1.98493424313525E-32));
#126907=DIRECTION('ref_axis',(0.866221358214888,-0.499660443273585,1.7451068216366E-32));
#126908=DIRECTION('center_axis',(0.499660443273578,0.866221358214892,8.62481518849798E-15));
#126909=DIRECTION('ref_axis',(0.859723273961663,-0.495912168508003,-0.122257978612151));
#126910=DIRECTION('',(0.633907504568221,-0.365655385569965,0.681511125848853));
#126911=DIRECTION('',(-2.503441925062E-32,-8.47431587997155E-33,1.));
#126912=DIRECTION('',(7.964558486269E-33,-2.75090391492849E-32,1.));
#126913=DIRECTION('center_axis',(-2.503441925062E-32,-8.47431587997155E-33,
1.));
#126914=DIRECTION('ref_axis',(0.794387085412114,0.607411852477745,2.50344192506201E-32));
#126915=DIRECTION('center_axis',(0.206321571363439,-0.269832060511291,-0.94054349623521));
#126916=DIRECTION('ref_axis',(-0.571202570610379,0.7472280062189,-0.339673269555058));
#126917=DIRECTION('center_axis',(0.206321571363439,-0.269832060511291,-0.94054349623521));
#126918=DIRECTION('ref_axis',(-0.571202570610379,0.7472280062189,-0.339673269555058));
#126919=DIRECTION('center_axis',(-0.635987464991062,0.366855164283613,-0.678923583927297));
#126920=DIRECTION('ref_axis',(-0.429882331307342,0.562209925348658,0.706485089063613));
#126921=DIRECTION('center_axis',(0.187336619052717,-0.709906865968496,0.678923583927297));
#126922=DIRECTION('ref_axis',(0.429882331307337,-0.56220992534866,-0.706485089063615));
#126923=DIRECTION('center_axis',(-0.960067599843407,-0.278711148453534,
-0.0242960790793859));
#126924=DIRECTION('ref_axis',(-0.175129429493246,0.666437199283665,-0.724700726049254));
#126925=DIRECTION('center_axis',(2.503441925062E-32,8.47431587997155E-33,
-1.));
#126926=DIRECTION('ref_axis',(-0.79438708541211,-0.607411852477751,-2.503441925062E-32));
#126927=DIRECTION('center_axis',(3.34237907217807E-35,-4.1258613206322E-32,
1.));
#126928=DIRECTION('ref_axis',(-0.0782378061205037,0.996934724890978,4.11347592102862E-32));
#126929=DIRECTION('center_axis',(-2.503441925062E-32,-8.47431587997155E-33,
1.));
#126930=DIRECTION('ref_axis',(0.79438708541211,0.607411852477751,2.503441925062E-32));
#126931=DIRECTION('center_axis',(0.633630494200843,-0.365495598326631,0.681854357192688));
#126932=DIRECTION('ref_axis',(0.431599721517369,-0.564455967466372,-0.703641344136153));
#126933=DIRECTION('center_axis',(0.634188068245048,-0.365817222460512,0.681163162426516));
#126934=DIRECTION('ref_axis',(0.431194840310069,-0.563926454581656,-0.704313824593084));
#126935=DIRECTION('center_axis',(-0.186806588318937,0.707898329362167,-0.681163162426516));
#126936=DIRECTION('ref_axis',(-0.431194840310065,0.56392645458166,0.704313824593084));
#126937=DIRECTION('center_axis',(-0.186642349175774,0.707275949733551,-0.681854357192686));
#126938=DIRECTION('ref_axis',(-0.431599721517378,0.564455967466363,0.703641344136155));
#126939=DIRECTION('center_axis',(-2.503441925062E-32,-8.47431587997155E-33,
1.));
#126940=DIRECTION('ref_axis',(0.79438708541211,0.607411852477751,2.503441925062E-32));
#126941=DIRECTION('center_axis',(3.34237907217807E-35,-4.1258613206322E-32,
1.));
#126942=DIRECTION('ref_axis',(-0.941575887720347,0.336800902112274,1.39274091832105E-32));
#126943=DIRECTION('center_axis',(-2.503441925062E-32,-8.47431587997155E-33,
1.));
#126944=DIRECTION('ref_axis',(-0.794387085412093,-0.607411852477773,-2.50344192506198E-32));
#126945=DIRECTION('center_axis',(2.503441925062E-32,8.47431587997155E-33,
-1.));
#126946=DIRECTION('ref_axis',(0.794387085412112,0.607411852477749,2.503441925062E-32));
#126947=DIRECTION('center_axis',(0.942885598864541,0.333116717463799,2.95812573952651E-32));
#126948=DIRECTION('ref_axis',(-0.333116717463799,0.942885598864541,8.16412607761849E-34));
#126949=DIRECTION('',(-2.7619780906307E-32,-1.06237950525526E-32,1.));
#126950=DIRECTION('',(-0.243777396037203,0.690010990148381,-0.681511125848853));
#126951=DIRECTION('center_axis',(-0.942887200307189,-0.333112184544956,
2.13514018502994E-6));
#126952=DIRECTION('ref_axis',(0.330293331385506,-0.934907492930652,0.12982409215699));
#126953=DIRECTION('',(1.4929593762888E-32,4.65433213841183E-32,-1.));
#126954=DIRECTION('center_axis',(-0.427392782066418,-0.904066042851698,
-2.14091073548401E-32));
#126955=DIRECTION('ref_axis',(0.904066042851698,-0.427392782066418,2.0429572704782E-32));
#126956=DIRECTION('center_axis',(0.427392782066393,0.904066042851709,6.1569477156822E-15));
#126957=DIRECTION('ref_axis',(0.897284061240695,-0.424186633564772,-0.122257978669661));
#126958=DIRECTION('',(0.661602538143392,-0.312769350906473,0.681511125848849));
#126959=DIRECTION('',(-2.7619780906307E-32,-1.06237950525526E-32,1.));
#126960=DIRECTION('',(6.82090211058494E-33,-2.69054588173221E-32,1.));
#126961=DIRECTION('center_axis',(-2.7619780906307E-32,-1.06237950525526E-32,
1.));
#126962=DIRECTION('ref_axis',(0.742234123004267,0.670140661837563,2.7619780906307E-32));
#126963=DIRECTION('center_axis',(0.227628871285482,-0.252117093127508,-0.940543496235147));
#126964=DIRECTION('ref_axis',(-0.630207960610639,0.698183354379519,-0.339673269555233));
#126965=DIRECTION('center_axis',(0.227628871285482,-0.252117093127508,-0.940543496235147));
#126966=DIRECTION('ref_axis',(-0.630207960610639,0.698183354379519,-0.339673269555233));
#126967=DIRECTION('center_axis',(-0.663773370772875,0.313795601371545,-0.678923583927297));
#126968=DIRECTION('ref_axis',(-0.474277261530931,0.525299817366711,0.706485089063613));
#126969=DIRECTION('center_axis',(0.244577271937235,-0.692275035834063,0.678923583927297));
#126970=DIRECTION('ref_axis',(0.474277261530926,-0.525299817366713,-0.706485089063615));
#126971=DIRECTION('center_axis',(-0.934155508074011,-0.356038182328548,
-0.0242960790904556));
#126972=DIRECTION('ref_axis',(-0.228867508979934,0.649944984589603,-0.724700752269611));
#126973=DIRECTION('center_axis',(2.7619780906307E-32,1.06237950525526E-32,
-1.));
#126974=DIRECTION('ref_axis',(-0.742234123004264,-0.670140661837566,-2.76197809063069E-32));
#126975=DIRECTION('center_axis',(3.68755419309802E-35,-4.12557434076937E-32,
1.));
#126976=DIRECTION('ref_axis',(-0.159236911443844,0.987240399312055,4.07352085431321E-32));
#126977=DIRECTION('center_axis',(-2.7619780906307E-32,-1.06237950525526E-32,
1.));
#126978=DIRECTION('ref_axis',(0.742234123004264,0.670140661837566,2.76197809063069E-32));
#126979=DIRECTION('center_axis',(0.661313425361435,-0.312632674258581,0.681854357192688));
#126980=DIRECTION('ref_axis',(0.476172010550541,-0.527398402718972,-0.703641344136153));
#126981=DIRECTION('center_axis',(0.661895359476728,-0.312907780753821,0.681163162426516));
#126982=DIRECTION('ref_axis',(0.475725316336193,-0.52690365332183,-0.704313824593084));
#126983=DIRECTION('center_axis',(-0.243885290457238,0.690316384892969,-0.681163162426516));
#126984=DIRECTION('ref_axis',(-0.475725316336185,0.526903653321837,0.704313824593085));
#126985=DIRECTION('center_axis',(-0.243670868088652,0.689709463196114,-0.681854357192686));
#126986=DIRECTION('ref_axis',(-0.476172010550551,0.527398402718963,0.703641344136154));
#126987=DIRECTION('center_axis',(-2.7619780906307E-32,-1.06237950525526E-32,
1.));
#126988=DIRECTION('ref_axis',(0.742234123004264,0.670140661837566,2.76197809063069E-32));
#126989=DIRECTION('center_axis',(3.68755419309802E-35,-4.12557434076937E-32,
1.));
#126990=DIRECTION('ref_axis',(-0.965895271857674,0.258933048881347,1.0718093336019E-32));
#126991=DIRECTION('center_axis',(-2.7619780906307E-32,-1.06237950525526E-32,
1.));
#126992=DIRECTION('ref_axis',(-0.74223412300426,-0.670140661837571,-2.76197809063068E-32));
#126993=DIRECTION('center_axis',(2.7619780906307E-32,1.06237950525526E-32,
-1.));
#126994=DIRECTION('ref_axis',(0.742234123004269,0.670140661837561,2.7619780906307E-32));
#126995=DIRECTION('center_axis',(0.912596119838882,0.408862228696926,3.27031011275326E-32));
#126996=DIRECTION('ref_axis',(-0.408862228696926,0.912596119838882,-4.31965265863823E-34));
#126997=DIRECTION('',(-3.00213374770056E-32,-1.29768529867714E-32,1.));
#126998=DIRECTION('',(-0.299208548308713,0.667844914604604,-0.681511125848846));
#126999=DIRECTION('center_axis',(-0.91259808542786,-0.40885784139337,2.13514020802859E-6));
#127000=DIRECTION('ref_axis',(0.405397947498362,-0.904874692557993,0.129824092264084));
#127001=DIRECTION('',(1.44456010278038E-32,4.7742491995483E-32,-1.));
#127002=DIRECTION('center_axis',(-0.352280892409444,-0.935894317133727,
-2.27209065223238E-32));
#127003=DIRECTION('ref_axis',(0.935894317133727,-0.352280892409444,2.35253017866373E-32));
#127004=DIRECTION('center_axis',(0.352280892409472,0.935894317133717,-2.12694557450725E-14));
#127005=DIRECTION('ref_axis',(0.928873571132182,-0.349638206561809,-0.122257978735087));
#127006=DIRECTION('',(0.684894715983951,-0.257801887816002,0.681511125848851));
#127007=DIRECTION('',(-3.00213374770056E-32,-1.29768529867714E-32,1.));
#127008=DIRECTION('',(5.63185375672457E-33,-2.6397105460928E-32,1.));
#127009=DIRECTION('center_axis',(-3.00213374770056E-32,-1.29768529867714E-32,
1.));
#127010=DIRECTION('ref_axis',(0.685141714967841,0.728409795658272,3.00213374770055E-32));
#127011=DIRECTION('center_axis',(0.247421338625064,-0.232724328085156,-0.940543496235179));
#127012=DIRECTION('ref_axis',(-0.685019420610463,0.644492407508595,-0.339673269555143));
#127013=DIRECTION('center_axis',(0.247421338625064,-0.232724328085156,-0.940543496235179));
#127014=DIRECTION('ref_axis',(-0.685019420610463,0.644492407508595,-0.339673269555143));
#127015=DIRECTION('center_axis',(-0.687141974287091,0.25864778050498,-0.678923583927297));
#127016=DIRECTION('ref_axis',(-0.515515954829271,0.484893925768558,0.706485089063613));
#127017=DIRECTION('center_axis',(0.300190303429421,-0.670036229553497,0.678923583927297));
#127018=DIRECTION('ref_axis',(0.51551595482927,-0.484893925768558,-0.706485089063614));
#127019=DIRECTION('center_axis',(-0.90202676553384,-0.430995840817816,-0.0242960790726165));
#127020=DIRECTION('ref_axis',(-0.281082723153935,0.629127918196647,-0.72470032792177));
#127021=DIRECTION('center_axis',(3.00213374770056E-32,1.29768529867714E-32,
-1.));
#127022=DIRECTION('ref_axis',(-0.685141714967838,-0.728409795658274,-3.00213374770055E-32));
#127023=DIRECTION('center_axis',(4.00818924926601E-35,-4.12526018083156E-32,
1.));
#127024=DIRECTION('ref_axis',(-0.239176321393795,0.970976151758905,4.00648791934816E-32));
#127025=DIRECTION('center_axis',(-3.00213374770056E-32,-1.29768529867714E-32,
1.));
#127026=DIRECTION('ref_axis',(0.685141714967838,0.728409795658274,3.00213374770055E-32));
#127027=DIRECTION('center_axis',(0.684595424785282,-0.257689231324101,0.681854357192688));
#127028=DIRECTION('ref_axis',(0.517575453416346,-0.486831088616096,-0.703641344136152));
#127029=DIRECTION('center_axis',(0.685197846296139,-0.257915989392363,0.681163162426516));
#127030=DIRECTION('ref_axis',(0.517089918871253,-0.486374395182131,-0.704313824593084));
#127031=DIRECTION('center_axis',(-0.299340976225786,0.668140498776494,-0.681163162426516));
#127032=DIRECTION('ref_axis',(-0.517089918871254,0.486374395182132,0.704313824593083));
#127033=DIRECTION('center_axis',(-0.299077797577264,0.667553073975157,-0.681854357192686));
#127034=DIRECTION('ref_axis',(-0.517575453416357,0.486831088616081,0.703641344136154));
#127035=DIRECTION('center_axis',(-3.00213374770056E-32,-1.29768529867714E-32,
1.));
#127036=DIRECTION('ref_axis',(0.685141714967838,0.728409795658274,3.00213374770055E-32));
#127037=DIRECTION('center_axis',(4.00818924926601E-35,-4.12526018083156E-32,
1.));
#127038=DIRECTION('ref_axis',(-0.983786782322297,0.179342038931035,7.43775775555815E-33));
#127039=DIRECTION('center_axis',(-3.00213374770056E-32,-1.29768529867714E-32,
1.));
#127040=DIRECTION('ref_axis',(-0.685141714967838,-0.728409795658274,-3.00213374770055E-32));
#127041=DIRECTION('center_axis',(3.00213374770056E-32,1.29768529867714E-32,
-1.));
#127042=DIRECTION('ref_axis',(0.685141714967843,0.72840979565827,3.00213374770056E-32));
#127043=DIRECTION('center_axis',(0.876233464203457,0.481886829255594,3.57128027962397E-32));
#127044=DIRECTION('ref_axis',(-0.481886829255594,0.876233464203457,-1.93064851106194E-33));
#127045=DIRECTION('',(-3.22231069999667E-32,-1.55178304703032E-32,1.));
#127046=DIRECTION('',(-0.352648517057139,0.641234441340786,-0.681511125848853));
#127047=DIRECTION('center_axis',(-0.876235780858048,-0.481882616764217,
2.13514019795421E-6));
#127048=DIRECTION('ref_axis',(0.477804707150802,-0.868820100394176,0.12982409243122));
#127049=DIRECTION('',(1.38654752012359E-32,4.88982225644843E-32,-1.));
#127050=DIRECTION('center_axis',(-0.274824631535741,-0.961494369146925,
-2.37760101267757E-32));
#127051=DIRECTION('ref_axis',(0.961494369146926,-0.274824631535741,2.67176538956517E-32));
#127052=DIRECTION('center_axis',(0.274824631535787,0.961494369146912,-2.06334074273449E-14));
#127053=DIRECTION('ref_axis',(0.954281580675183,-0.272762994985753,-0.122257978678188));
#127054=DIRECTION('',(0.703629032489319,-0.201118795696426,0.681511125848848));
#127055=DIRECTION('',(-3.22231069999667E-32,-1.55178304703032E-32,1.));
#127056=DIRECTION('',(4.40532634530366E-33,-2.59873620878172E-32,1.));
#127057=DIRECTION('center_axis',(-3.22231069999667E-32,-1.55178304703032E-32,
1.));
#127058=DIRECTION('ref_axis',(0.623489801858728,0.781831482468034,3.22231069999666E-32));
#127059=DIRECTION('center_axis',(0.2655672577778,-0.211782821036267,-0.940543496235182));
#127060=DIRECTION('ref_axis',(0.735272189385988,-0.586512469999794,0.339673269555135));
#127061=DIRECTION('center_axis',(0.2655672577778,-0.211782821036267,-0.940543496235182));
#127062=DIRECTION('ref_axis',(0.735272189385988,-0.586512469999794,0.339673269555135));
#127063=DIRECTION('center_axis',(-0.705937761332873,0.201778701333035,-0.678923583927297));
#127064=DIRECTION('ref_axis',(-0.553323974502371,0.441261145096274,0.706485089063615));
#127065=DIRECTION('center_axis',(0.353805617980198,-0.643338442713448,0.678923583927297));
#127066=DIRECTION('ref_axis',(0.553323974502369,-0.44126114509628,-0.706485089063613));
#127067=DIRECTION('center_axis',(-0.863895183680872,-0.503085293120479,
-0.0242960790843667));
#127068=DIRECTION('ref_axis',(-0.331427070555256,0.604123469235223,-0.724700580117306));
#127069=DIRECTION('center_axis',(3.22231069999667E-32,1.55178304703032E-32,
-1.));
#127070=DIRECTION('ref_axis',(-0.623489801858734,-0.781831482468029,-3.22231069999667E-32));
#127071=DIRECTION('center_axis',(4.30215046728491E-35,-4.12492093150131E-32,
1.));
#127072=DIRECTION('ref_axis',(-0.317524052386152,0.948250218115597,3.91282320925606E-32));
#127073=DIRECTION('center_axis',(-3.22231069999667E-32,-1.55178304703032E-32,
1.));
#127074=DIRECTION('ref_axis',(0.623489801858734,0.781831482468029,3.22231069999667E-32));
#127075=DIRECTION('center_axis',(0.703321554607477,-0.201030909070889,0.681854357192688));
#127076=DIRECTION('ref_axis',(0.55553451703361,-0.443023993939946,-0.703641344136153));
#127077=DIRECTION('center_axis',(0.703940454498135,-0.201207809674643,0.681163162426516));
#127078=DIRECTION('ref_axis',(0.555013373310054,-0.442608395688626,-0.704313824593083));
#127079=DIRECTION('center_axis',(-0.352804597185337,0.641518247876084,-0.681163162426516));
#127080=DIRECTION('ref_axis',(-0.555013373310049,0.442608395688628,0.704313824593085));
#127081=DIRECTION('center_axis',(-0.352494413667362,0.640954229185401,-0.681854357192686));
#127082=DIRECTION('ref_axis',(-0.555534517033618,0.443023993939935,0.703641344136154));
#127083=DIRECTION('center_axis',(-3.22231069999667E-32,-1.55178304703032E-32,
1.));
#127084=DIRECTION('ref_axis',(0.623489801858734,0.781831482468029,3.22231069999667E-32));
#127085=DIRECTION('center_axis',(4.30215046728491E-35,-4.12492093150131E-32,
1.));
#127086=DIRECTION('ref_axis',(-0.995131354063954,0.0985575373010178,4.10823253390086E-33));
#127087=DIRECTION('center_axis',(-3.22231069999667E-32,-1.55178304703032E-32,
1.));
#127088=DIRECTION('ref_axis',(-0.623489801858718,-0.781831482468042,-3.22231069999664E-32));
#127089=DIRECTION('center_axis',(3.22231069999667E-32,1.55178304703032E-32,
-1.));
#127090=DIRECTION('ref_axis',(0.623489801858732,0.781831482468031,3.22231069999667E-32));
#127091=DIRECTION('center_axis',(0.834039619432103,0.551704552471296,3.8590333333347E-32));
#127092=DIRECTION('ref_axis',(-0.551704552471296,0.834039619432103,-3.66966363810105E-33));
#127093=DIRECTION('',(-3.42104370622815E-32,-1.82298177172267E-32,1.));
#127094=DIRECTION('',(-0.403741668107477,0.610356658666085,-0.681511125848848));
#127095=DIRECTION('center_axis',(-0.834042271735419,-0.55170054282542,2.13514023031498E-6));
#127096=DIRECTION('ref_axis',(0.547031755324907,-0.826983653837606,0.129824092338646));
#127097=DIRECTION('',(1.31930769248462E-32,5.00028218948676E-32,-1.));
#127098=DIRECTION('center_axis',(-0.195539458082041,-0.980695834768855,
-2.4567396627788E-32));
#127099=DIRECTION('ref_axis',(0.980695834768855,-0.195539458082041,2.99853844552406E-32));
#127100=DIRECTION('center_axis',(0.195539458081979,0.980695834768868,2.63196793879087E-14));
#127101=DIRECTION('ref_axis',(0.973339003741128,-0.194072590678889,-0.122257978649298));
#127102=DIRECTION('',(0.71768081387408,-0.143097291173766,0.681511125848851));
#127103=DIRECTION('',(-3.42104370622815E-32,-1.82298177172267E-32,1.));
#127104=DIRECTION('',(3.14948221388244E-33,-2.56789554725346E-32,1.));
#127105=DIRECTION('center_axis',(-3.42104370622815E-32,-1.82298177172267E-32,
1.));
#127106=DIRECTION('ref_axis',(0.557688666986824,0.830050209755084,3.42104370622814E-32));
#127107=DIRECTION('center_axis',(0.281945870645546,-0.189431934255097,-0.940543496235181));
#127108=DIRECTION('ref_axis',(0.780631843052823,-0.524629388770469,0.339673269555138));
#127109=DIRECTION('center_axis',(0.281945870645546,-0.189431934255097,-0.940543496235181));
#127110=DIRECTION('ref_axis',(0.780631843052823,-0.524629388770469,0.339673269555138));
#127111=DIRECTION('center_axis',(-0.720035649048516,0.14356681819486,-0.678923583927297));
#127112=DIRECTION('ref_axis',(-0.587449714417181,0.394691844306352,0.706485089063614));
#127113=DIRECTION('center_axis',(0.405066414517134,-0.612359344680513,0.678923583927297));
#127114=DIRECTION('ref_axis',(0.58744971441718,-0.394691844306355,-0.706485089063614));
#127115=DIRECTION('center_axis',(-0.820014521923814,-0.571826795783192,
-0.0242960790743142));
#127116=DIRECTION('ref_axis',(-0.379566263881805,0.575099350020013,-0.72470006825539));
#127117=DIRECTION('center_axis',(3.42104370622815E-32,1.82298177172267E-32,
-1.));
#127118=DIRECTION('ref_axis',(-0.557688666986826,-0.830050209755083,-3.42104370622814E-32));
#127119=DIRECTION('center_axis',(4.56748158374851E-35,-4.12455885042696E-32,
1.));
#127120=DIRECTION('ref_axis',(-0.393758713197673,0.919213835721,3.79315004722893E-32));
#127121=DIRECTION('center_axis',(-3.42104370622815E-32,-1.82298177172267E-32,
1.));
#127122=DIRECTION('ref_axis',(0.557688666986826,0.830050209755083,3.42104370622814E-32));
#127123=DIRECTION('center_axis',(0.717367195523648,-0.143034759285577,0.681854357192688));
#127124=DIRECTION('ref_axis',(0.589796590096754,-0.396268647677949,-0.703641344136152));
#127125=DIRECTION('center_axis',(0.717998455117447,-0.143160625180489,0.681163162426516));
#127126=DIRECTION('ref_axis',(0.589243305320241,-0.39589691034705,-0.704313824593083));
#127127=DIRECTION('center_axis',(-0.40392036175928,0.610626798879119,-0.681163162426516));
#127128=DIRECTION('ref_axis',(-0.589243305320237,0.395896910347054,0.704313824593084));
#127129=DIRECTION('center_axis',(-0.403565237591988,0.61008993975042,-0.681854357192686));
#127130=DIRECTION('ref_axis',(-0.58979659009676,0.396268647677936,0.703641344136155));
#127131=DIRECTION('center_axis',(-3.42104370622815E-32,-1.82298177172267E-32,
1.));
#127132=DIRECTION('ref_axis',(0.557688666986826,0.830050209755083,3.42104370622814E-32));
#127133=DIRECTION('center_axis',(4.56748158374851E-35,-4.12455885042696E-32,
1.));
#127134=DIRECTION('ref_axis',(-0.999853490829433,0.0171171515211064,7.5167511206289E-34));
#127135=DIRECTION('center_axis',(-3.42104370622815E-32,-1.82298177172267E-32,
1.));
#127136=DIRECTION('ref_axis',(-0.557688666986844,-0.830050209755071,-3.42104370622818E-32));
#127137=DIRECTION('center_axis',(3.42104370622815E-32,1.82298177172267E-32,
-1.));
#127138=DIRECTION('ref_axis',(0.557688666986828,0.830050209755082,3.42104370622815E-32));
#127139=DIRECTION('center_axis',(0.786295378600279,0.617850772915146,4.13165432478892E-32));
#127140=DIRECTION('ref_axis',(-0.617850772915146,0.78629537860028,-5.63743778822801E-33));
#127141=DIRECTION('',(-3.59701023102716E-32,-2.10947668998601E-32,1.));
#127142=DIRECTION('',(-0.452147984969248,0.575417053129711,-0.68151112584885));
#127143=DIRECTION('center_axis',(-0.786298348901551,-0.617846992798489,
2.13514017688966E-6));
#127144=DIRECTION('ref_axis',(0.612618397399368,-0.779643767476114,0.129824092538636));
#127145=DIRECTION('',(1.24328808982261E-32,5.10489390603353E-32,-1.));
#127146=DIRECTION('center_axis',(-0.114953001796544,-0.993370931413822,
-2.5089799478766E-32));
#127147=DIRECTION('ref_axis',(0.993370931413822,-0.114953001796544,3.33067472576676E-32));
#127148=DIRECTION('center_axis',(0.114953001796478,0.993370931413829,1.98701494460553E-14));
#127149=DIRECTION('ref_axis',(0.985919016308877,-0.114090665298237,-0.122257978767613));
#127150=DIRECTION('',(0.726956547851517,-0.0841234977877295,0.681511125848846));
#127151=DIRECTION('',(-3.59701023102716E-32,-2.10947668998601E-32,1.));
#127152=DIRECTION('',(1.87267879795583E-33,-2.54739380102216E-32,1.));
#127153=DIRECTION('center_axis',(-3.59701023102716E-32,-2.10947668998601E-32,
1.));
#127154=DIRECTION('ref_axis',(0.488176206048277,0.872745089844858,3.59701023102715E-32));
#127155=DIRECTION('center_axis',(0.296448180261865,-0.165820409205486,-0.940543496235211));
#127156=DIRECTION('ref_axis',(0.820796520599088,-0.459254985516989,0.339673269555055));
#127157=DIRECTION('center_axis',(0.296448180261865,-0.165820409205486,-0.940543496235211));
#127158=DIRECTION('ref_axis',(0.820796520599088,-0.459254985516989,0.339673269555055));
#127159=DIRECTION('center_axis',(-0.729341818317262,0.084399521568456,-0.678923583927297));
#127160=DIRECTION('ref_axis',(-0.617666073404929,0.345495934412133,0.706485089063615));
#127161=DIRECTION('center_axis',(0.453631560896713,-0.577305096240909,0.678923583927297));
#127162=DIRECTION('ref_axis',(0.617666073404927,-0.34549593441214,-0.706485089063614));
#127163=DIRECTION('center_axis',(-0.770676798808639,-0.636762885475809,
-0.0242960790785247));
#127164=DIRECTION('ref_axis',(-0.425178902774582,0.542247208642873,-0.724700534948344));
#127165=DIRECTION('center_axis',(3.59701023102716E-32,2.10947668998601E-32,
-1.));
#127166=DIRECTION('ref_axis',(-0.488176206048286,-0.872745089844853,-3.59701023102717E-32));
#127167=DIRECTION('center_axis',(4.80241686385389E-35,-4.1241763471983E-32,
1.));
#127168=DIRECTION('ref_axis',(-0.467372974738498,0.884060236909277,3.64826483841536E-32));
#127169=DIRECTION('center_axis',(-3.59701023102716E-32,-2.10947668998601E-32,
1.));
#127170=DIRECTION('ref_axis',(0.488176206048286,0.872745089844853,3.59701023102717E-32));
#127171=DIRECTION('center_axis',(0.726638876110865,-0.0840867367762921,
0.681854357192688));
#127172=DIRECTION('ref_axis',(0.620133664162395,-0.346876198945372,-0.703641344136153));
#127173=DIRECTION('center_axis',(0.727278294479358,-0.0841607303456,0.681163162426516));
#127174=DIRECTION('ref_axis',(0.619551920351823,-0.346550796385511,-0.704313824593083));
#127175=DIRECTION('center_axis',(-0.452348102967884,0.575671729281945,-0.681163162426516));
#127176=DIRECTION('ref_axis',(-0.619551920351822,0.346550796385512,0.704313824593084));
#127177=DIRECTION('center_axis',(-0.451950401444018,0.575165602424154,-0.681854357192686));
#127178=DIRECTION('ref_axis',(-0.620133664162403,0.346876198945357,0.703641344136154));
#127179=DIRECTION('center_axis',(-3.59701023102716E-32,-2.10947668998601E-32,
1.));
#127180=DIRECTION('ref_axis',(0.488176206048286,0.872745089844853,3.59701023102717E-32));
#127181=DIRECTION('center_axis',(4.80241686385389E-35,-4.1241763471983E-32,
1.));
#127182=DIRECTION('ref_axis',(-0.997921767577657,-0.06443714607805,-2.60957717410633E-33));
#127183=DIRECTION('center_axis',(-3.59701023102716E-32,-2.10947668998601E-32,
1.));
#127184=DIRECTION('ref_axis',(-0.488176206048267,-0.872745089844864,-3.59701023102713E-32));
#127185=DIRECTION('center_axis',(3.59701023102716E-32,2.10947668998601E-32,
-1.));
#127186=DIRECTION('ref_axis',(0.488176206048279,0.872745089844857,3.59701023102716E-32));
#127187=DIRECTION('center_axis',(0.733318471753477,0.679885298403447,4.38732900626779E-32));
#127188=DIRECTION('ref_axis',(-0.679885298403447,0.733318471753477,-7.82087574913358E-33));
#127189=DIRECTION('',(-3.7490392462036E-32,-2.40936122540763E-32,1.));
#127190=DIRECTION('',(-0.497545331590198,0.536648142041903,-0.681511125848855));
#127191=DIRECTION('center_axis',(-0.733321740285969,-0.67988177297189,2.13514019561374E-6));
#127192=DIRECTION('ref_axis',(0.674128165144339,-0.727115480513455,0.129824092358906));
#127193=DIRECTION('',(1.15899461005092E-32,5.20296123237483E-32,-1.));
#127194=DIRECTION('center_axis',(-0.0336015522500017,-0.999435308404896,
-2.53397421749269E-32));
#127195=DIRECTION('ref_axis',(0.999435308404897,-0.0336015522500017,3.66596391814689E-32));
#127196=DIRECTION('center_axis',(0.0336015522499427,0.999435308404898,2.27466779630292E-14));
#127197=DIRECTION('ref_axis',(0.991937900519573,-0.0333494853670919,-0.122257978629503));
#127198=DIRECTION('',(0.731394505942389,-0.0245898764033206,0.681511125848843));
#127199=DIRECTION('',(-3.7490392462036E-32,-2.40936122540763E-32,1.));
#127200=DIRECTION('',(5.83413013599077E-34,-2.53736740582643E-32,1.));
#127201=DIRECTION('center_axis',(-3.7490392462036E-32,-2.40936122540763E-32,
1.));
#127202=DIRECTION('ref_axis',(0.415415013001888,0.909631995354517,3.74903924620361E-32));
#127203=DIRECTION('center_axis',(0.308977676149196,-0.141105376691133,-0.94054349623518));
#127204=DIRECTION('ref_axis',(0.855498932722574,-0.390824316106684,0.339673269555141));
#127205=DIRECTION('center_axis',(0.308977676149196,-0.141105376691133,-0.94054349623518));
#127206=DIRECTION('ref_axis',(0.855498932722574,-0.390824316106684,0.339673269555141));
#127207=DIRECTION('center_axis',(-0.733794338118036,0.024670560050955,-0.678923583927297));
#127208=DIRECTION('ref_axis',(-0.643771966581894,0.294000806077225,0.706485089063614));
#127209=DIRECTION('center_axis',(0.499177864082464,-0.538408977634459,0.678923583927297));
#127210=DIRECTION('ref_axis',(0.643771966581889,-0.294000806077234,-0.706485089063615));
#127211=DIRECTION('center_axis',(-0.716210348753134,-0.697461423220216,
-0.0242960790775933));
#127212=DIRECTION('ref_axis',(-0.46796256549965,0.505787122557392,-0.724700230402957));
#127213=DIRECTION('center_axis',(3.7490392462036E-32,2.40936122540763E-32,
-1.));
#127214=DIRECTION('ref_axis',(-0.415415013001888,-0.909631995354518,-3.74903924620361E-32));
#127215=DIRECTION('center_axis',(5.00539285207499E-35,-4.12377596731122E-32,
1.));
#127216=DIRECTION('ref_axis',(-0.537876946243531,0.843023363080605,3.47913176997571E-32));
#127217=DIRECTION('center_axis',(-3.7490392462036E-32,-2.40936122540763E-32,
1.));
#127218=DIRECTION('ref_axis',(0.415415013001888,0.909631995354518,3.74903924620361E-32));
#127219=DIRECTION('center_axis',(0.73107489486454,-0.0245791309070966,0.681854357192688));
#127220=DIRECTION('ref_axis',(0.646343851007887,-0.295175346339363,-0.703641344136153));
#127221=DIRECTION('center_axis',(0.731718216783982,-0.0246007597358041,
0.681163162426516));
#127222=DIRECTION('ref_axis',(0.645737519572335,-0.294898444050882,-0.704313824593083));
#127223=DIRECTION('center_axis',(-0.497765542183421,0.536885659305548,-0.681163162426516));
#127224=DIRECTION('ref_axis',(-0.645737519572333,0.294898444050884,0.704313824593084));
#127225=DIRECTION('center_axis',(-0.497327909941004,0.5364136329094,-0.681854357192686));
#127226=DIRECTION('ref_axis',(-0.646343851007887,0.295175346339356,0.703641344136156));
#127227=DIRECTION('center_axis',(-3.7490392462036E-32,-2.40936122540763E-32,
1.));
#127228=DIRECTION('ref_axis',(0.415415013001888,0.909631995354518,3.74903924620361E-32));
#127229=DIRECTION('center_axis',(5.00539285207499E-35,-4.12377596731122E-32,
1.));
#127230=DIRECTION('ref_axis',(-0.989349039608151,-0.145562625101462,-5.95315574521082E-33));
#127231=DIRECTION('center_axis',(-3.7490392462036E-32,-2.40936122540763E-32,
1.));
#127232=DIRECTION('ref_axis',(-0.415415013001908,-0.909631995354509,-3.74903924620366E-32));
#127233=DIRECTION('center_axis',(3.7490392462036E-32,2.40936122540763E-32,
-1.));
#127234=DIRECTION('ref_axis',(0.415415013001884,0.909631995354519,3.7490392462036E-32));
#127235=DIRECTION('center_axis',(0.675461451466187,0.737395299404053,4.62435590494944E-32));
#127236=DIRECTION('ref_axis',(-0.737395299404053,0.675461451466187,-1.02054471014299E-32));
#127237=DIRECTION('',(-3.87611902374449E-32,-2.72063969588177E-32,1.));
#127238=DIRECTION('',(-0.539631596118643,0.494307926109506,-0.681511125848849));
#127239=DIRECTION('center_axis',(-0.675464996478299,-0.737392052118826,
2.13514020039549E-6));
#127240=DIRECTION('ref_axis',(0.731151721197705,-0.669748360010381,0.12982409195923));
#127241=DIRECTION('',(1.06698821237E-32,5.29383154663385E-32,-1.));
#127242=DIRECTION('center_axis',(0.0479735100828988,-0.998848608313755,
-2.53155613888654E-32));
#127243=DIRECTION('ref_axis',(0.998848608313755,0.0479735100828988,4.00217472840797E-32));
#127244=DIRECTION('center_axis',(-0.0479735100828819,0.998848608313756,
-9.89055134078661E-15));
#127245=DIRECTION('ref_axis',(0.991355601632822,0.0476136298882577,-0.122257978717502));
#127246=DIRECTION('',(0.730965154267811,0.0351073865515132,0.681511125848843));
#127247=DIRECTION('',(-3.87611902374449E-32,-2.72063969588177E-32,1.));
#127248=DIRECTION('',(-7.09735288106811E-34,-2.53788308567206E-32,1.));
#127249=DIRECTION('center_axis',(-3.87611902374449E-32,-2.72063969588177E-32,
1.));
#127250=DIRECTION('ref_axis',(0.339889301582619,0.940465450013811,3.8761190237445E-32));
#127251=DIRECTION('center_axis',(0.319450976579402,-0.115451311175611,-0.940543496235182));
#127252=DIRECTION('ref_axis',(0.884508140596374,-0.319792775353774,0.339673269555136));
#127253=DIRECTION('center_axis',(0.319450976579402,-0.115451311175611,-0.940543496235182));
#127254=DIRECTION('ref_axis',(0.884508140596374,-0.319792775353774,0.339673269555136));
#127255=DIRECTION('center_axis',(-0.733363577666178,-0.0352225799733294,
-0.678923583927297));
#127256=DIRECTION('ref_axis',(-0.665593663536156,0.240549150884587,0.706485089063614));
#127257=DIRECTION('center_axis',(0.541402220941297,-0.495929836113079,0.678923583927297));
#127258=DIRECTION('ref_axis',(0.665593663536153,-0.240549150884594,-0.706485089063614));
#127259=DIRECTION('center_axis',(-0.656977636984026,-0.753518470273803,
-0.0242960790892854));
#127260=DIRECTION('ref_axis',(-0.50763101857097,0.465960210135762,-0.724701201568506));
#127261=DIRECTION('center_axis',(3.87611902374449E-32,2.72063969588177E-32,
-1.));
#127262=DIRECTION('ref_axis',(-0.339889301582622,-0.94046545001381,-3.87611902374451E-32));
#127263=DIRECTION('center_axis',(5.17505877669541E-35,-4.12336037522781E-32,
1.));
#127264=DIRECTION('ref_axis',(-0.604801435414764,0.796376307859696,3.2868763945754E-32));
#127265=DIRECTION('center_axis',(-3.87611902374449E-32,-2.72063969588177E-32,
1.));
#127266=DIRECTION('ref_axis',(0.339889301582622,0.94046545001381,3.87611902374451E-32));
#127267=DIRECTION('center_axis',(0.730645730811759,0.0350920450230146,0.681854357192688));
#127268=DIRECTION('ref_axis',(0.66825272616415,-0.241510150503968,-0.703641344136153));
#127269=DIRECTION('center_axis',(0.731288675080916,0.0351229248711943,0.681163162426515));
#127270=DIRECTION('ref_axis',(0.667625842139285,-0.241283591225913,-0.704313824593084));
#127271=DIRECTION('center_axis',(-0.53987043384126,0.494526703846372,-0.681163162426516));
#127272=DIRECTION('ref_axis',(-0.667625842139283,0.241283591225916,0.704313824593084));
#127273=DIRECTION('center_axis',(-0.539395783250663,0.494091919169655,-0.681854357192686));
#127274=DIRECTION('ref_axis',(-0.668252726164153,0.241510150503956,0.703641344136155));
#127275=DIRECTION('center_axis',(-3.87611902374449E-32,-2.72063969588177E-32,
1.));
#127276=DIRECTION('ref_axis',(0.339889301582622,0.94046545001381,3.87611902374451E-32));
#127277=DIRECTION('center_axis',(5.17505877669541E-35,-4.12336037522781E-32,
1.));
#127278=DIRECTION('ref_axis',(-0.97419235701116,-0.225719408870926,-9.25680963750882E-33));
#127279=DIRECTION('center_axis',(-3.87611902374449E-32,-2.72063969588177E-32,
1.));
#127280=DIRECTION('ref_axis',(-0.339889301582586,-0.940465450013823,-3.87611902374441E-32));
#127281=DIRECTION('center_axis',(3.87611902374449E-32,2.72063969588177E-32,
-1.));
#127282=DIRECTION('ref_axis',(0.339889301582614,0.940465450013812,3.87611902374449E-32));
#127283=DIRECTION('center_axis',(0.613109346662684,0.789998056348784,4.84115764592981E-32));
#127284=DIRECTION('ref_axis',(-0.789998056348784,0.613109346662684,-1.27752829161939E-32));
#127285=DIRECTION('',(-3.97740386869698E-32,-3.04124059454475E-32,1.));
#127286=DIRECTION('',(-0.578126701407848,0.44867817248392,-0.681511125848853));
#127287=DIRECTION('center_axis',(-0.613113144562907,-0.789995108820064,
2.13514017973777E-6));
#127288=DIRECTION('ref_axis',(0.783309583130661,-0.607924174624544,0.129824092073606));
#127289=DIRECTION('',(9.67881184176422E-33,5.37690012186172E-32,-1.));
#127290=DIRECTION('center_axis',(0.129229316621269,-0.991614735532707,-2.50174180397231E-32));
#127291=DIRECTION('ref_axis',(0.991614735532707,0.129229316621269,4.3370697290786E-32));
#127292=DIRECTION('center_axis',(-0.129229316621292,0.991614735532704,1.20022317556764E-14));
#127293=DIRECTION('ref_axis',(0.984175994800074,0.12825988429344,-0.122257978636643));
#127294=DIRECTION('',(0.725671350092337,0.0945710156411612,0.681511125848848));
#127295=DIRECTION('',(-3.97740386869698E-32,-3.04124059454475E-32,1.));
#127296=DIRECTION('',(-1.99816041856844E-33,-2.54893740879476E-32,1.));
#127297=DIRECTION('center_axis',(-3.97740386869698E-32,-3.04124059454475E-32,
1.));
#127298=DIRECTION('ref_axis',(0.262101682939102,0.96504026226914,3.97740386869699E-32));
#127299=DIRECTION('center_axis',(0.327798383466009,-0.0890289362322958,
-0.940543496235244));
#127300=DIRECTION('ref_axis',(0.907631092727719,-0.24663306644432,0.339673269554962));
#127301=DIRECTION('center_axis',(0.327798383466009,-0.0890289362322958,
-0.940543496235244));
#127302=DIRECTION('ref_axis',(0.907631092727719,-0.24663306644432,0.339673269554962));
#127303=DIRECTION('center_axis',(-0.728052403601425,-0.0948813195392077,
-0.678923583927297));
#127304=DIRECTION('ref_axis',(-0.682985944474809,0.185496680780628,0.706485089063615));
#127305=DIRECTION('center_axis',(0.580023635344843,-0.450150363355031,0.678923583927297));
#127306=DIRECTION('ref_axis',(0.682985944474808,-0.185496680780635,-0.706485089063613));
#127307=DIRECTION('center_axis',(-0.593372847443218,-0.804560976221234,
-0.0242960790882418));
#127308=DIRECTION('ref_axis',(-0.54392253522018,0.423033500529492,-0.724700581695238));
#127309=DIRECTION('center_axis',(3.97740386869698E-32,3.04124059454475E-32,
-1.));
#127310=DIRECTION('ref_axis',(-0.262101682939102,-0.96504026226914,-3.97740386869699E-32));
#127311=DIRECTION('center_axis',(5.3102855389809E-35,-4.12293233664482E-32,
1.));
#127312=DIRECTION('ref_axis',(-0.667701070818532,0.744429499702817,3.0727781400178E-32));
#127313=DIRECTION('center_axis',(-3.97740386869698E-32,-3.04124059454475E-32,
1.));
#127314=DIRECTION('ref_axis',(0.262101682939102,0.96504026226914,3.97740386869699E-32));
#127315=DIRECTION('center_axis',(0.725354239968486,0.0945296891832773,0.681854357192688));
#127316=DIRECTION('ref_axis',(0.685714489681731,-0.186237744463339,-0.703641344136153));
#127317=DIRECTION('center_axis',(0.725992527899325,0.0946128722080492,0.681163162426516));
#127318=DIRECTION('ref_axis',(0.685071224877309,-0.186063035910322,-0.704313824593084));
#127319=DIRECTION('center_axis',(-0.578382576834238,0.448876754764262,-0.681163162426516));
#127320=DIRECTION('ref_axis',(-0.68507122487731,0.186063035910324,0.704313824593083));
#127321=DIRECTION('center_axis',(-0.577874066616828,0.448482105227263,-0.681854357192686));
#127322=DIRECTION('ref_axis',(-0.685714489681731,0.186237744463328,0.703641344136155));
#127323=DIRECTION('center_axis',(-3.97740386869698E-32,-3.04124059454475E-32,
1.));
#127324=DIRECTION('ref_axis',(0.262101682939102,0.96504026226914,3.97740386869699E-32));
#127325=DIRECTION('center_axis',(5.3102855389809E-35,-4.12293233664482E-32,
1.));
#127326=DIRECTION('ref_axis',(-0.952552585008684,-0.304374067215448,-1.24985535794138E-32));
#127327=DIRECTION('center_axis',(-3.97740386869698E-32,-3.04124059454475E-32,
1.));
#127328=DIRECTION('ref_axis',(-0.262101682939063,-0.965040262269151,-3.97740386869687E-32));
#127329=DIRECTION('center_axis',(3.97740386869698E-32,3.04124059454475E-32,
-1.));
#127330=DIRECTION('ref_axis',(0.262101682939099,0.965040262269141,3.97740386869698E-32));
#127331=DIRECTION('center_axis',(0.546677100313063,0.837343506569019,5.03629144939245E-32));
#127332=DIRECTION('ref_axis',(-0.837343506569019,0.546677100313063,-1.55132813600715E-32));
#127333=DIRECTION('',(-4.05221974712874E-32,-3.36903037531139E-32,1.));
#127334=DIRECTION('',(-0.612774468883391,0.400062539647137,-0.681511125848845));
#127335=DIRECTION('center_axis',(-0.546681125827074,-0.837340878412062,
2.13514019490064E-6));
#127336=DIRECTION('ref_axis',(0.830254649042338,-0.542054354171433,0.129824092014448));
#127337=DIRECTION('',(8.62333066391302E-33,5.45161415039565E-32,-1.));
#127338=DIRECTION('center_axis',(0.209625123378862,-0.977781830291603,-2.44472962222985E-32));
#127339=DIRECTION('ref_axis',(0.977781830291603,0.209625123378862,4.6684202491831E-32));
#127340=DIRECTION('center_axis',(-0.209625123378866,0.977781830291602,-1.86998205414277E-15));
#127341=DIRECTION('ref_axis',(0.970446859081431,0.208052590327751,-0.122257978704452));
#127342=DIRECTION('',(0.715548322809351,0.153405290224829,0.681511125848846));
#127343=DIRECTION('',(-4.05221974712874E-32,-3.36903037531139E-32,1.));
#127344=DIRECTION('',(-3.27328812111774E-33,-2.57045681049799E-32,1.));
#127345=DIRECTION('center_axis',(-4.05221974712874E-32,-3.36903037531139E-32,
1.));
#127346=DIRECTION('ref_axis',(0.182569820839361,0.983192890799503,4.05221974712875E-32));
#127347=DIRECTION('center_axis',(0.333964346193912,-0.0620140884071856,
-0.940543496235182));
#127348=DIRECTION('ref_axis',(0.924713909685948,-0.171832055167397,0.339673269555136));
#127349=DIRECTION('center_axis',(0.333964346193912,-0.0620140884071856,
-0.940543496235182));
#127350=DIRECTION('ref_axis',(0.924713909685948,-0.171832055167397,0.339673269555136));
#127351=DIRECTION('center_axis',(-0.717896160910897,-0.153908639577868,
-0.678923583927297));
#127352=DIRECTION('ref_axis',(-0.695833066637731,0.129209760870875,0.706485089063614));
#127353=DIRECTION('center_axis',(0.614785088152334,-0.401375214198437,0.678923583927297));
#127354=DIRECTION('ref_axis',(0.695833066637729,-0.129209760870883,-0.706485089063614));
#127355=DIRECTION('center_axis',(-0.525819259512051,-0.850249261609663,
-0.0242960790750349));
#127356=DIRECTION('ref_axis',(-0.576593278623329,0.377290828495695,-0.724701194824069));
#127357=DIRECTION('center_axis',(4.05221974712874E-32,3.36903037531139E-32,
-1.));
#127358=DIRECTION('ref_axis',(-0.182569820839353,-0.983192890799505,-4.05221974712873E-32));
#127359=DIRECTION('center_axis',(5.41017322714156E-35,-4.12249470008839E-32,
1.));
#127360=DIRECTION('ref_axis',(-0.726157265758901,0.687528636047661,2.83826179486338E-32));
#127361=DIRECTION('center_axis',(-4.05221974712875E-32,-3.36903037531139E-32,
1.));
#127362=DIRECTION('ref_axis',(0.182569820839353,0.983192890799505,4.05221974712873E-32));
#127363=DIRECTION('center_axis',(0.715235636333248,0.153338253858326,0.681854357192688));
#127364=DIRECTION('ref_axis',(0.698612936405406,-0.129725956960371,-0.703641344136153));
#127365=DIRECTION('center_axis',(0.7158650202249,0.153473186490385,0.681163162426516));
#127366=DIRECTION('ref_axis',(0.69795757164257,-0.129604261788992,-0.704313824593084));
#127367=DIRECTION('center_axis',(-0.613045679204792,0.400239604938646,-0.681163162426516));
#127368=DIRECTION('ref_axis',(-0.697957571642569,0.129604261788998,0.704313824593084));
#127369=DIRECTION('center_axis',(-0.612506693412169,0.399887716868923,-0.681854357192686));
#127370=DIRECTION('ref_axis',(-0.698612936405406,0.129725956960361,0.703641344136155));
#127371=DIRECTION('center_axis',(-4.05221974712874E-32,-3.36903037531139E-32,
1.));
#127372=DIRECTION('ref_axis',(0.182569820839353,0.983192890799505,4.05221974712873E-32));
#127373=DIRECTION('center_axis',(5.41017322714156E-35,-4.12249470008839E-32,
1.));
#127374=DIRECTION('ref_axis',(-0.924573732713088,-0.381003166360843,-1.56568142998423E-32));
#127375=DIRECTION('center_axis',(-4.05221974712875E-32,-3.36903037531139E-32,
1.));
#127376=DIRECTION('ref_axis',(-0.182569820839333,-0.983192890799508,-4.05221974712866E-32));
#127377=DIRECTION('center_axis',(4.05221974712874E-32,3.36903037531139E-32,
-1.));
#127378=DIRECTION('ref_axis',(0.182569820839359,0.983192890799503,4.05221974712874E-32));
#127379=DIRECTION('center_axis',(0.476606808056231,0.879116573904992,5.20845873207013E-32));
#127380=DIRECTION('ref_axis',(-0.879116573904992,0.476606808056231,-1.84012215051566E-32));
#127381=DIRECTION('',(-4.10006877171256E-32,-3.7018276512722E-32,1.));
#127382=DIRECTION('',(-0.643344323369166,0.348784556614685,-0.68151112584885));
#127383=DIRECTION('center_axis',(-0.476611034394921,-0.879114282609744,
2.13514022319101E-6));
#127384=DIRECTION('ref_axis',(0.871674507249432,-0.472577251423886,0.129824091940232));
#127385=DIRECTION('',(7.51046264324289E-33,5.51747642270271E-32,-1.));
#127386=DIRECTION('center_axis',(0.288625909526079,-0.957441948292555,-2.36089900032229E-32));
#127387=DIRECTION('ref_axis',(0.957441948292555,0.288625909526079,4.99402120567917E-32));
#127388=DIRECTION('center_axis',(-0.288625909526091,0.957441948292551,1.95902881862569E-15));
#127389=DIRECTION('ref_axis',(0.950259559641614,0.28646074070239,-0.12225797865973));
#127390=DIRECTION('',(0.700663439495228,0.211218677912143,0.681511125848847));
#127391=DIRECTION('',(-4.10006877171256E-32,-3.7018276512722E-32,1.));
#127392=DIRECTION('',(-4.52663263127555E-33,-2.60229808271385E-32,1.));
#127393=DIRECTION('center_axis',(-4.10006877171256E-32,-3.7018276512722E-32,
1.));
#127394=DIRECTION('ref_axis',(0.101822986703838,0.994802532857004,4.10006877171259E-32));
#127395=DIRECTION('center_axis',(0.337907831297878,-0.0345865470552739,
-0.940543496235213));
#127396=DIRECTION('ref_axis',(0.935642908142144,-0.0958875299144513,0.339673269555049));
#127397=DIRECTION('center_axis',(0.337907831297878,-0.0345865470552739,
-0.940543496235213));
#127398=DIRECTION('ref_axis',(0.935642908142144,-0.0958875299144513,0.339673269555049));
#127399=DIRECTION('center_axis',(-0.702962437714035,-0.211911723013277,
-0.678923583927297));
#127400=DIRECTION('ref_axis',(-0.704049534546554,0.0720629713206354,0.706485089063614));
#127401=DIRECTION('center_axis',(0.645455247630571,-0.349928979213601,0.678923583927297));
#127402=DIRECTION('ref_axis',(0.704049534546552,-0.072062971320644,-0.706485089063614));
#127403=DIRECTION('center_axis',(-0.454766431155998,-0.890279278448852,
-0.0242960790710806));
#127404=DIRECTION('ref_axis',(-0.60542764494557,0.329037829144449,-0.724700954689291));
#127405=DIRECTION('center_axis',(4.10006877171256E-32,3.7018276512722E-32,
-1.));
#127406=DIRECTION('ref_axis',(-0.101822986703825,-0.994802532857005,-4.10006877171253E-32));
#127407=DIRECTION('center_axis',(5.47405710508952E-35,-4.1220503779576E-32,
1.));
#127408=DIRECTION('ref_axis',(-0.779781003903195,0.626052382753812,2.58488802669644E-32));
#127409=DIRECTION('center_axis',(-4.10006877171256E-32,-3.7018276512722E-32,
1.));
#127410=DIRECTION('ref_axis',(0.101822986703825,0.994802532857005,4.10006877171253E-32));
#127411=DIRECTION('center_axis',(0.700357257543786,0.211126377752979,0.681854357192688));
#127412=DIRECTION('ref_axis',(0.706862229300325,-0.0723508646171092,-0.703641344136153));
#127413=DIRECTION('center_axis',(0.700973548950293,0.21131216203792,0.681163162426516));
#127414=DIRECTION('ref_axis',(0.706199125923443,-0.0722829926886559,-0.704313824593084));
#127415=DIRECTION('center_axis',(-0.643629063725655,0.348938926577051,-0.681163162426516));
#127416=DIRECTION('ref_axis',(-0.706199125923443,0.0722829926886583,0.704313824593083));
#127417=DIRECTION('center_axis',(-0.643063189219342,0.34863214173165,-0.681854357192686));
#127418=DIRECTION('ref_axis',(-0.706862229300325,0.0723508646170959,0.703641344136154));
#127419=DIRECTION('center_axis',(-4.10006877171256E-32,-3.7018276512722E-32,
1.));
#127420=DIRECTION('ref_axis',(0.101822986703825,0.994802532857005,4.10006877171253E-32));
#127421=DIRECTION('center_axis',(5.47405710508952E-35,-4.1220503779576E-32,
1.));
#127422=DIRECTION('ref_axis',(-0.89044199477021,-0.455096752295211,-1.87105740947761E-32));
#127423=DIRECTION('center_axis',(-4.10006877171256E-32,-3.7018276512722E-32,
1.));
#127424=DIRECTION('ref_axis',(-0.101822986703824,-0.994802532857005,-4.10006877171254E-32));
#127425=DIRECTION('center_axis',(4.10006877171256E-32,3.7018276512722E-32,
-1.));
#127426=DIRECTION('ref_axis',(0.101822986703832,0.994802532857004,4.10006877171256E-32));
#127427=DIRECTION('center_axis',(0.403364776126373,0.915039265485652,5.35651374910224E-32));
#127428=DIRECTION('ref_axis',(-0.915039265485652,0.403364776126373,-2.14198845862603E-32));
#127429=DIRECTION('',(-4.12063251508437E-32,-4.03741771146334E-32,1.));
#127430=DIRECTION('',(-0.669632827527267,0.295185469903361,-0.681511125848852));
#127431=DIRECTION('center_axis',(-0.403369175164062,-0.915037326300357,
2.13514020751955E-6));
#127432=DIRECTION('ref_axis',(0.907293515386185,-0.399955225018066,0.129824092212985));
#127433=DIRECTION('',(6.34761373282109E-33,5.5740486362272E-32,-1.));
#127434=DIRECTION('center_axis',(0.365705937865323,-0.930730448094423,-2.25080781720736E-32));
#127435=DIRECTION('ref_axis',(0.930730448094423,0.365705937865323,5.31170577792169E-32));
#127436=DIRECTION('center_axis',(-0.365705937865339,0.930730448094416,6.81843796612823E-15));
#127437=DIRECTION('ref_axis',(0.923748439609161,0.362962542109338,-0.122257978656478));
#127438=DIRECTION('',(0.681115756592596,0.267626440146581,0.681511125848847));
#127439=DIRECTION('',(-4.12063251508437E-32,-4.03741771146334E-32,1.));
#127440=DIRECTION('',(-5.74985314811402E-33,-2.64424932702919E-32,1.));
#127441=DIRECTION('center_axis',(-4.12063251508437E-32,-4.03741771146334E-32,
1.));
#127442=DIRECTION('ref_axis',(0.0203985373914037,0.999791928189207,4.12063251508437E-32));
#127443=DIRECTION('center_axis',(0.339602595535507,-0.0069288379391035,
-0.940543496235214));
#127444=DIRECTION('ref_axis',(0.940345357414828,-0.0193048889705321,0.339673269555046));
#127445=DIRECTION('center_axis',(0.339602595535507,-0.0069288379391035,
-0.940543496235214));
#127446=DIRECTION('ref_axis',(0.940345357414828,-0.0193048889705321,0.339673269555046));
#127447=DIRECTION('center_axis',(-0.683350615474825,-0.268504568895005,
-0.678923583927297));
#127448=DIRECTION('ref_axis',(-0.707580668962966,0.0144366145858088,0.706485089063614));
#127449=DIRECTION('center_axis',(0.671830008928446,-0.296154024606316,0.678923583927297));
#127450=DIRECTION('ref_axis',(0.707580668962966,-0.014436614585817,-0.706485089063614));
#127451=DIRECTION('center_axis',(-0.380687207232623,-0.924384633575987,
-0.0242960790666857));
#127452=DIRECTION('ref_axis',(-0.630232780927451,0.278595012725823,-0.724700945720889));
#127453=DIRECTION('center_axis',(4.12063251508437E-32,4.03741771146334E-32,
-1.));
#127454=DIRECTION('ref_axis',(-0.0203985373913968,-0.999791928189207,-4.12063251508434E-32));
#127455=DIRECTION('center_axis',(5.50151203616034E-35,-4.12160232714292E-32,
1.));
#127456=DIRECTION('ref_axis',(-0.828215428121308,0.560409854144125,2.31434299614059E-32));
#127457=DIRECTION('center_axis',(-4.12063251508437E-32,-4.03741771146334E-32,
1.));
#127458=DIRECTION('ref_axis',(0.0203985373913968,0.999791928189207,4.12063251508434E-32));
#127459=DIRECTION('center_axis',(0.680818116756184,0.267509490437086,0.681854357192688));
#127460=DIRECTION('ref_axis',(0.710407470683308,-0.0144942892068718,-0.703641344136153));
#127461=DIRECTION('center_axis',(0.681417214359916,0.267744890011146,0.681163162426516));
#127462=DIRECTION('ref_axis',(0.70974104153595,-0.0144806921978297,-0.704313824593084));
#127463=DIRECTION('center_axis',(-0.669929203018745,0.295316117229956,-0.681163162426516));
#127464=DIRECTION('ref_axis',(-0.70974104153595,0.0144806921978318,0.704313824593083));
#127465=DIRECTION('center_axis',(-0.669340205600219,0.295056477211407,-0.681854357192686));
#127466=DIRECTION('ref_axis',(-0.710407470683307,0.0144942892068606,0.703641344136155));
#127467=DIRECTION('center_axis',(-4.12063251508437E-32,-4.03741771146334E-32,
1.));
#127468=DIRECTION('ref_axis',(0.0203985373913968,0.999791928189207,4.12063251508434E-32));
#127469=DIRECTION('center_axis',(5.50151203616034E-35,-4.12160232714292E-32,
1.));
#127470=DIRECTION('ref_axis',(-0.850384512264726,-0.52616174442873,-2.16395106966144E-32));
#127471=DIRECTION('center_axis',(-4.12063251508437E-32,-4.03741771146334E-32,
1.));
#127472=DIRECTION('ref_axis',(-0.0203985373913968,-0.999791928189207,-4.12063251508434E-32));
#127473=DIRECTION('center_axis',(4.12063251508437E-32,4.03741771146334E-32,
-1.));
#127474=DIRECTION('ref_axis',(0.0203985373914021,0.999791928189207,4.12063251508437E-32));
#127475=DIRECTION('center_axis',(0.327438418161898,0.944872521725357,5.47947121877778E-32));
#127476=DIRECTION('ref_axis',(-0.944872521725356,0.327438418161898,-2.45491818986221E-32));
#127477=DIRECTION('',(-4.11377412892479E-32,-4.37356725940272E-32,1.));
#127478=DIRECTION('',(-0.691465035699823,0.239621972591999,-0.681511125848846));
#127479=DIRECTION('center_axis',(-0.327442960623831,-0.944870947554925,
2.13514022945096E-6));
#127480=DIRECTION('ref_axis',(0.936874634876281,-0.324671562585836,0.129824092423197));
#127481=DIRECTION('',(5.14252250028993E-33,5.62095431222186E-32,-1.));
#127482=DIRECTION('center_axis',(0.440352253525306,-0.897825090323936,-2.11518871154492E-32));
#127483=DIRECTION('ref_axis',(0.897825090323936,0.440352253525306,5.61935982749666E-32));
#127484=DIRECTION('center_axis',(-0.440352253525287,0.897825090323946,-7.17462502405725E-15));
#127485=DIRECTION('ref_axis',(0.891089926119414,0.43704888768344,-0.12225797864829));
#127486=DIRECTION('',(0.657035360706024,0.322253192577101,0.681511125848853));
#127487=DIRECTION('',(-4.11377412892479E-32,-4.37356725940272E-32,1.));
#127488=DIRECTION('',(-6.9348093409108E-33,-2.69603136483457E-32,1.));
#127489=DIRECTION('center_axis',(-4.11377412892479E-32,-4.37356725940272E-32,
1.));
#127490=DIRECTION('ref_axis',(-0.0611616608218504,0.998127873193366,4.11377412892477E-32));
#127491=DIRECTION('center_axis',(0.339037360530247,0.0207749814503661,-0.940543496235246));
#127492=DIRECTION('ref_axis',(0.938789963480034,0.0574062228247189,0.339673269554958));
#127493=DIRECTION('center_axis',(0.339037360530247,0.0207749814503661,-0.940543496235246));
#127494=DIRECTION('ref_axis',(0.938789963480034,0.0574062228247189,0.339673269554958));
#127495=DIRECTION('center_axis',(-0.659191207634545,-0.323310561170872,
-0.678923583927297));
#127496=DIRECTION('ref_axis',(-0.706402970770023,-0.0432858154372093,0.706485089063614));
#127497=DIRECTION('center_axis',(0.693733852361051,-0.240408213827251,0.678923583927297));
#127498=DIRECTION('ref_axis',(0.706402970770023,0.0432858154372054,-0.706485089063614));
#127499=DIRECTION('center_axis',(-0.304074572747413,-0.952338361482043,
-0.0242960790700016));
#127500=DIRECTION('ref_axis',(-0.650843724041517,0.226298162138698,-0.724701034005345));
#127501=DIRECTION('center_axis',(4.11377412892479E-32,4.37356725940272E-32,
-1.));
#127502=DIRECTION('ref_axis',(0.0611616608218468,-0.998127873193367,-4.11377412892479E-32));
#127503=DIRECTION('center_axis',(5.49235531231428E-35,-4.12115352934861E-32,
1.));
#127504=DIRECTION('ref_axis',(-0.871138215311196,0.491037890416234,2.02842713573738E-32));
#127505=DIRECTION('center_axis',(-4.11377412892479E-32,-4.37356725940272E-32,
1.));
#127506=DIRECTION('ref_axis',(-0.0611616608218468,0.998127873193367,4.11377412892479E-32));
#127507=DIRECTION('center_axis',(0.656748243728652,0.322112371598294,0.681854357192688));
#127508=DIRECTION('ref_axis',(0.709225067557877,0.0434587433066445,-0.703641344136153));
#127509=DIRECTION('center_axis',(0.657326160633901,0.322395819916145,0.681163162426516));
#127510=DIRECTION('ref_axis',(0.708559747616064,0.0434179749104281,-0.704313824593084));
#127511=DIRECTION('center_axis',(-0.691771073996284,0.239728027846425,-0.681163162426516));
#127512=DIRECTION('ref_axis',(-0.708559747616064,-0.0434179749104245,0.704313824593084));
#127513=DIRECTION('center_axis',(-0.691162873346186,0.239517260516214,-0.681854357192686));
#127514=DIRECTION('ref_axis',(-0.709225067557875,-0.043458743306661,0.703641344136154));
#127515=DIRECTION('center_axis',(-4.11377412892479E-32,-4.37356725940272E-32,
1.));
#127516=DIRECTION('ref_axis',(-0.0611616608218468,0.998127873193367,4.11377412892479E-32));
#127517=DIRECTION('center_axis',(5.49235531231428E-35,-4.12115352934861E-32,
1.));
#127518=DIRECTION('ref_axis',(-0.804667861133695,-0.593725216963643,-2.44241325155124E-32));
#127519=DIRECTION('center_axis',(-4.11377412892479E-32,-4.37356725940272E-32,
1.));
#127520=DIRECTION('ref_axis',(0.0611616608218468,-0.998127873193367,-4.11377412892479E-32));
#127521=DIRECTION('center_axis',(4.11377412892479E-32,4.37356725940272E-32,
-1.));
#127522=DIRECTION('ref_axis',(-0.0611616608218463,0.998127873193367,4.11377412892479E-32));
#127523=DIRECTION('center_axis',(0.249333011548091,0.968417807225972,5.57651287942261E-32));
#127524=DIRECTION('ref_axis',(-0.968417807225972,0.249333011548091,-2.7768288484926E-32));
#127525=DIRECTION('',(-4.07953925466218E-32,-4.70803927530955E-32,1.));
#127526=DIRECTION('',(-0.708695658143486,0.182463830587886,-0.681511125848849));
#127527=DIRECTION('center_axis',(-0.249337667204796,-0.968416608546297,
2.13514020965652E-6));
#127528=DIRECTION('ref_axis',(0.960221008293694,-0.247227264488722,0.129824092235863));
#127529=DIRECTION('',(3.90320862897581E-33,5.65788130115185E-32,-1.));
#127530=DIRECTION('center_axis',(0.512068097591086,-0.858944854708058,-1.95494420610757E-32));
#127531=DIRECTION('ref_axis',(0.858944854708058,0.512068097591086,5.9149359674635E-32));
#127532=DIRECTION('center_axis',(-0.512068097591103,0.858944854708047,4.5541059549879E-15));
#127533=DIRECTION('ref_axis',(0.852501356187244,0.508226745016147,-0.122257978672975));
#127534=DIRECTION('',(0.628582502897165,0.374735403179052,0.681511125848852));
#127535=DIRECTION('',(-4.07953925466218E-32,-4.70803927530955E-32,1.));
#127536=DIRECTION('',(-8.0736155217068E-33,-2.75729959521182E-32,1.));
#127537=DIRECTION('center_axis',(-4.07953925466218E-32,-4.70803927530955E-32,
1.));
#127538=DIRECTION('ref_axis',(-0.142314838273288,0.989821441880932,4.07953925466219E-32));
#127539=DIRECTION('center_axis',(0.336215887827956,0.048340546765909,-0.940543496235252));
#127540=DIRECTION('ref_axis',(0.930987077227732,0.133735305678126,0.33967326955494));
#127541=DIRECTION('center_axis',(0.336215887827956,0.048340546765909,-0.940543496235252));
#127542=DIRECTION('ref_axis',(0.930987077227732,0.133735305678126,0.33967326955494));
#127543=DIRECTION('center_axis',(-0.630644991066351,-0.375964975004635,
-0.678923583927297));
#127544=DIRECTION('ref_axis',(-0.700524277354892,-0.100720185500151,0.706485089063614));
#127545=DIRECTION('center_axis',(0.711021011464223,-0.183062526049729,0.678923583927297));
#127546=DIRECTION('ref_axis',(0.700524277354892,0.100720185500147,-0.706485089063614));
#127547=DIRECTION('center_axis',(-0.225438372144987,-0.97395443471759,-0.0242960790778839));
#127548=DIRECTION('ref_axis',(-0.66712375661312,0.172495421980205,-0.724700781535572));
#127549=DIRECTION('center_axis',(4.07953925466218E-32,4.70803927530955E-32,
-1.));
#127550=DIRECTION('ref_axis',(0.142314838273279,-0.989821441880933,-4.07953925466223E-32));
#127551=DIRECTION('center_axis',(5.44664787004251E-35,-4.12070697124994E-32,
1.));
#127552=DIRECTION('ref_axis',(-0.908263721405877,0.418398150543173,1.72904316836497E-32));
#127553=DIRECTION('center_axis',(-4.07953925466218E-32,-4.70803927530955E-32,
1.));
#127554=DIRECTION('ref_axis',(-0.142314838273279,0.989821441880933,4.07953925466223E-32));
#127555=DIRECTION('center_axis',(0.628307819494939,0.374571648071316,0.681854357192688));
#127556=DIRECTION('ref_axis',(0.703322888621748,0.101122565053646,-0.703641344136153));
#127557=DIRECTION('center_axis',(0.62886070976005,0.374901258831168,0.681163162426516));
#127558=DIRECTION('ref_axis',(0.702663105479923,0.101027702559117,-0.704313824593084));
#127559=DIRECTION('center_axis',(-0.70900932261057,0.182544587989916,-0.681163162426516));
#127560=DIRECTION('ref_axis',(-0.702663105479923,-0.101027702559114,0.704313824593084));
#127561=DIRECTION('center_axis',(-0.708385966203883,0.182384095969852,-0.681854357192686));
#127562=DIRECTION('ref_axis',(-0.703322888621744,-0.101122565053659,0.703641344136155));
#127563=DIRECTION('center_axis',(-4.07953925466218E-32,-4.70803927530955E-32,
1.));
#127564=DIRECTION('ref_axis',(-0.142314838273279,0.989821441880933,4.07953925466223E-32));
#127565=DIRECTION('center_axis',(5.44664787004251E-35,-4.12070697124994E-32,
1.));
#127566=DIRECTION('ref_axis',(-0.753596278147675,-0.657337546137426,-2.70459083526957E-32));
#127567=DIRECTION('center_axis',(-4.07953925466218E-32,-4.70803927530955E-32,
1.));
#127568=DIRECTION('ref_axis',(0.142314838273299,-0.989821441880931,-4.07953925466213E-32));
#127569=DIRECTION('center_axis',(4.07953925466218E-32,4.70803927530955E-32,
-1.));
#127570=DIRECTION('ref_axis',(-0.142314838273289,0.989821441880932,4.07953925466218E-32));
#127571=DIRECTION('center_axis',(0.169568334879484,0.98551843199719,5.64699293479589E-32));
#127572=DIRECTION('ref_axis',(-0.98551843199719,0.169568334879484,-3.10557817219554E-32));
#127573=DIRECTION('',(-4.01815571973639E-32,-5.03860790310199E-32,1.));
#127574=DIRECTION('',(-0.721210027908761,0.124091421895619,-0.68151112584885));
#127575=DIRECTION('center_axis',(-0.169573072748393,-0.985517616785266,
2.13514019657982E-6));
#127576=DIRECTION('ref_axis',(0.977177269309663,-0.168137709729232,0.129824092184458));
#127577=DIRECTION('',(2.63791954821996E-33,5.68458385999837E-32,-1.));
#127578=DIRECTION('center_axis',(0.580376212952687,-0.814348482800022,-1.77114070164052E-32));
#127579=DIRECTION('ref_axis',(0.814348482800022,0.580376212952687,6.19646718737737E-32));
#127580=DIRECTION('center_axis',(-0.580376212952658,0.814348482800042,-1.36623178649604E-14));
#127581=DIRECTION('ref_axis',(0.808239530379992,0.576022437209787,-0.12225797872543));
#127582=DIRECTION('',(0.595946532240335,0.424723811499838,0.681511125848852));
#127583=DIRECTION('',(-4.01815571973639E-32,-5.03860790310199E-32,1.));
#127584=DIRECTION('',(-9.15869312325864E-33,-2.82764628819632E-32,1.));
#127585=DIRECTION('center_axis',(-4.01815571973639E-32,-5.03860790310199E-32,
1.));
#127586=DIRECTION('ref_axis',(-0.222520933956323,0.974927912181822,4.01815571973636E-32));
#127587=DIRECTION('center_axis',(0.331156953864098,0.0755844137184014,-0.940543496235181));
#127588=DIRECTION('ref_axis',(0.916988625578409,0.209174402137411,0.339673269555138));
#127589=DIRECTION('center_axis',(0.331156953864098,0.0755844137184014,-0.940543496235181));
#127590=DIRECTION('ref_axis',(0.916988625578409,0.209174402137411,0.339673269555138));
#127591=DIRECTION('center_axis',(-0.59790193613171,-0.426117403959597,-0.678923583927297));
#127592=DIRECTION('ref_axis',(-0.68998371045233,-0.157484279346259,0.706485089063615));
#127593=DIRECTION('center_axis',(0.723576443046309,-0.124498587364537,0.678923583927297));
#127594=DIRECTION('ref_axis',(0.689983710452334,0.157484279346249,-0.706485089063614));
#127595=DIRECTION('center_axis',(-0.145301916380709,-0.989089001878846,
-0.0242960790746493));
#127596=DIRECTION('ref_axis',(-0.678963644165877,0.117544642290695,-0.724701060417153));
#127597=DIRECTION('center_axis',(4.01815571973639E-32,5.03860790310199E-32,
-1.));
#127598=DIRECTION('ref_axis',(0.222520933956312,-0.974927912181824,-4.01815571973642E-32));
#127599=DIRECTION('center_axis',(5.36469388482745E-35,-4.12026562461737E-32,
1.));
#127600=DIRECTION('ref_axis',(-0.939344882287572,0.342974040009076,1.41818344493129E-32));
#127601=DIRECTION('center_axis',(-4.01815571973639E-32,-5.03860790310199E-32,
1.));
#127602=DIRECTION('ref_axis',(-0.222520933956312,0.974927912181824,4.01815571973642E-32));
#127603=DIRECTION('center_axis',(0.595686110385981,0.424538212026394,0.681854357192688));
#127604=DIRECTION('ref_axis',(0.692740211901949,0.158113432814265,-0.703641344136153));
#127605=DIRECTION('center_axis',(0.596210294617459,0.424911791723024,0.681163162426516));
#127606=DIRECTION('ref_axis',(0.692090356308065,0.157965107515673,-0.704313824593084));
#127607=DIRECTION('center_axis',(-0.721529231161188,0.124146344018072,-0.681163162426516));
#127608=DIRECTION('ref_axis',(-0.692090356308066,-0.157965107515671,0.704313824593084));
#127609=DIRECTION('center_axis',(-0.720894867331949,0.124037195356069,-0.681854357192686));
#127610=DIRECTION('ref_axis',(-0.692740211901944,-0.158113432814279,0.703641344136154));
#127611=DIRECTION('center_axis',(-4.01815571973639E-32,-5.03860790310199E-32,
1.));
#127612=DIRECTION('ref_axis',(-0.222520933956312,0.974927912181824,4.01815571973642E-32));
#127613=DIRECTION('center_axis',(5.36469388482745E-35,-4.12026562461737E-32,
1.));
#127614=DIRECTION('ref_axis',(-0.697509636265204,-0.71657540239474,-2.94873907225313E-32));
#127615=DIRECTION('center_axis',(-4.01815571973639E-32,-5.03860790310199E-32,
1.));
#127616=DIRECTION('ref_axis',(0.222520933956312,-0.974927912181824,-4.01815571973642E-32));
#127617=DIRECTION('center_axis',(4.01815571973639E-32,5.03860790310199E-32,
-1.));
#127618=DIRECTION('ref_axis',(-0.222520933956318,0.974927912181823,4.01815571973639E-32));
#127619=DIRECTION('center_axis',(0.088675208919059,0.996060594202562,5.69044235175751E-32));
#127620=DIRECTION('ref_axis',(-0.996060594202562,0.088675208919059,-3.4389783884616E-32));
#127621=DIRECTION('',(-3.93003202144478E-32,-5.36307326310205E-32,1.));
#127622=DIRECTION('',(-0.728924863929587,0.0648932052642835,-0.681511125848845));
#127623=DIRECTION('center_axis',(-0.0886799974704105,-0.996060167883491,
2.13514018734458E-6));
#127624=DIRECTION('ref_axis',(0.987630576850999,-0.0879292262537851,0.129824091906604));
#127625=DIRECTION('',(1.35507554809678E-33,5.70088428763789E-32,-1.));
#127626=DIRECTION('center_axis',(0.644822020372422,-0.764332756096995,-1.56500138014056E-32));
#127627=DIRECTION('ref_axis',(0.764332756096995,0.644822020372422,6.46207994341911E-32));
#127628=DIRECTION('center_axis',(-0.644822020372427,0.76433275609699,-1.04311924108636E-15));
#127629=DIRECTION('ref_axis',(0.758599003860373,0.639984795129837,-0.122257978654446));
#127630=DIRECTION('',(0.559344635735712,0.471885752929584,0.681511125848847));
#127631=DIRECTION('',(-3.93003202144478E-32,-5.36307326310205E-32,1.));
#127632=DIRECTION('',(-1.01828211331532E-32,-2.90660329815266E-32,1.));
#127633=DIRECTION('center_axis',(-3.93003202144478E-32,-5.36307326310205E-32,
1.));
#127634=DIRECTION('ref_axis',(-0.301246189537239,0.953546398078926,3.93003202144478E-32));
#127635=DIRECTION('center_axis',(0.323894225008962,0.102325278868066,-0.940543496235244));
#127636=DIRECTION('ref_axis',(0.896887765918468,0.283221477461758,0.339673269554964));
#127637=DIRECTION('center_axis',(0.323894225008962,0.102325278868066,-0.940543496235244));
#127638=DIRECTION('ref_axis',(0.896887765918468,0.283221477461758,0.339673269554964));
#127639=DIRECTION('center_axis',(-0.561179942458989,-0.473434091895631,
-0.678923583927297));
#127640=DIRECTION('ref_axis',(-0.674851415796016,-0.213200341296378,0.706485089063613));
#127641=DIRECTION('center_axis',(0.731316592781633,-0.0651061311212549,
0.678923583927297));
#127642=DIRECTION('ref_axis',(0.674851415796015,0.213200341296374,-0.706485089063615));
#127643=DIRECTION('center_axis',(-0.0641985003308254,-0.997641344921486,
-0.0242960790771001));
#127644=DIRECTION('ref_axis',(-0.686286248571427,0.0618117157998334,-0.724700280675838));
#127645=DIRECTION('center_axis',(3.93003202144478E-32,5.36307326310205E-32,
-1.));
#127646=DIRECTION('ref_axis',(0.301246189537229,-0.953546398078929,-3.93003202144483E-32));
#127647=DIRECTION('center_axis',(5.24703874692283E-35,-4.11983242653993E-32,
1.));
#127648=DIRECTION('ref_axis',(-0.964174857958642,0.265267493825445,1.09791668560757E-32));
#127649=DIRECTION('center_axis',(-3.93003202144478E-32,-5.36307326310205E-32,
1.));
#127650=DIRECTION('ref_axis',(-0.301246189537229,0.953546398078929,3.93003202144483E-32));
#127651=DIRECTION('center_axis',(0.559100208493694,0.471679544224312,0.681854357192688));
#127652=DIRECTION('ref_axis',(0.677547463366034,0.214052081766382,-0.703641344136152));
#127653=DIRECTION('center_axis',(0.559592198331965,0.472094606746474,0.681163162426516));
#127654=DIRECTION('ref_axis',(0.676911860001846,0.213851280744125,-0.704313824593085));
#127655=DIRECTION('center_axis',(-0.729247481722371,0.0649219266094926,
-0.681163162426516));
#127656=DIRECTION('ref_axis',(-0.676911860001849,-0.21385128074412,0.704313824593084));
#127657=DIRECTION('center_axis',(-0.728606332057203,0.0648648476718873,
-0.681854357192686));
#127658=DIRECTION('ref_axis',(-0.677547463366027,-0.214052081766397,0.703641344136154));
#127659=DIRECTION('center_axis',(-3.93003202144478E-32,-5.36307326310205E-32,
1.));
#127660=DIRECTION('ref_axis',(-0.301246189537229,0.953546398078929,3.93003202144483E-32));
#127661=DIRECTION('center_axis',(5.24703874692283E-35,-4.11983242653993E-32,
1.));
#127662=DIRECTION('ref_axis',(-0.63678118283439,-0.771044567575724,-3.17323319626628E-32));
#127663=DIRECTION('center_axis',(-3.93003202144478E-32,-5.36307326310205E-32,
1.));
#127664=DIRECTION('ref_axis',(0.301246189537247,-0.953546398078924,-3.93003202144473E-32));
#127665=DIRECTION('center_axis',(3.93003202144478E-32,5.36307326310205E-32,
-1.));
#127666=DIRECTION('ref_axis',(-0.301246189537238,0.953546398078926,3.93003202144478E-32));
#127667=DIRECTION('center_axis',(0.00719196407365769,0.999974137491947,
5.70657198160623E-32));
#127668=DIRECTION('ref_axis',(-0.999974137491947,0.00719196407365769,-3.77481077385869E-32));
#127669=DIRECTION('',(-3.8157546084601E-32,-5.67927609187195E-32,1.));
#127670=DIRECTION('',(-0.731788825245097,0.00526313505853439,-0.681511125848842));
#127671=DIRECTION('center_axis',(-0.00719677144045609,-0.999974102902808,
2.13514018812815E-6));
#127672=DIRECTION('ref_axis',(0.991511365803085,-0.00713558827868622,0.129824091998437));
#127673=DIRECTION('',(6.32137437727758E-35,5.70667410741387E-32,-1.));
#127674=DIRECTION('center_axis',(0.704976643634723,-0.70923052100817,-1.33789806478166E-32));
#127675=DIRECTION('ref_axis',(0.70923052100817,0.704976643634723,6.7100066265203E-32));
#127676=DIRECTION('center_axis',(-0.704976643634742,0.709230521008152,5.59722519607366E-15));
#127677=DIRECTION('ref_axis',(0.703910126118507,0.699688159818815,-0.122257978705639));
#127678=DIRECTION('',(0.519020392965623,0.515907372529259,0.68151112584885));
#127679=DIRECTION('',(-3.8157546084601E-32,-5.67927609187195E-32,1.));
#127680=DIRECTION('',(-1.11391841484539E-32,-2.99364517920656E-32,1.));
#127681=DIRECTION('center_axis',(-3.8157546084601E-32,-5.67927609187195E-32,
1.));
#127682=DIRECTION('ref_axis',(-0.377966701428907,0.925819190020898,3.81575460846012E-32));
#127683=DIRECTION('center_axis',(0.314476033525515,0.12838518616945,-0.940543496235179));
#127684=DIRECTION('ref_axis',(0.870818266152426,0.355383760581436,0.339673269555142));
#127685=DIRECTION('center_axis',(0.314476033525515,0.12838518616945,-0.940543496235179));
#127686=DIRECTION('ref_axis',(0.870818266152426,0.355383760581436,0.339673269555142));
#127687=DIRECTION('center_axis',(-0.520723388857375,-0.517600154061226,
-0.678923583927297));
#127688=DIRECTION('ref_axis',(-0.655228096310218,-0.267497590150762,0.706485089063614));
#127689=DIRECTION('center_axis',(0.734189951250739,-0.00528040431711646,
0.678923583927297));
#127690=DIRECTION('ref_axis',(0.655228096310221,0.267497590150755,-0.706485089063614));
#127691=DIRECTION('center_axis',(0.0173321461446417,-0.999554549412633,
-0.0242960790772608));
#127692=DIRECTION('ref_axis',(-0.689040598198203,0.00566735485295386,-0.724700583084927));
#127693=DIRECTION('center_axis',(3.8157546084601E-32,5.67927609187195E-32,
-1.));
#127694=DIRECTION('ref_axis',(0.377966701428909,-0.925819190020897,-3.81575460846011E-32));
#127695=DIRECTION('center_axis',(5.09446543185543E-35,-4.11941025987936E-32,
1.));
#127696=DIRECTION('ref_axis',(-0.982588409027649,0.185795636236468,7.70374212836853E-33));
#127697=DIRECTION('center_axis',(-3.8157546084601E-32,-5.67927609187195E-32,
1.));
#127698=DIRECTION('ref_axis',(-0.377966701428909,0.925819190020897,3.81575460846011E-32));
#127699=DIRECTION('center_axis',(0.518793586958923,0.515681926877064,0.681854357192688));
#127700=DIRECTION('ref_axis',(0.657845748248879,0.268566249430454,-0.703641344136152));
#127701=DIRECTION('center_axis',(0.519250108292784,0.516135710052153,0.681163162426516));
#127702=DIRECTION('ref_axis',(0.657228626949917,0.268314308982192,-0.704313824593083));
#127703=DIRECTION('center_axis',(-0.732112710610057,0.00526546449069082,
-0.681163162426516));
#127704=DIRECTION('ref_axis',(-0.657228626949916,-0.268314308982189,0.704313824593084));
#127705=DIRECTION('center_axis',(-0.731469041854199,0.00526083512839615,
-0.681854357192686));
#127706=DIRECTION('ref_axis',(-0.657845748248872,-0.268566249430465,0.703641344136155));
#127707=DIRECTION('center_axis',(-3.8157546084601E-32,-5.67927609187195E-32,
1.));
#127708=DIRECTION('ref_axis',(-0.377966701428909,0.925819190020897,3.81575460846011E-32));
#127709=DIRECTION('center_axis',(5.09446543185543E-35,-4.11941025987936E-32,
1.));
#127710=DIRECTION('ref_axis',(-0.571815055693287,-0.820382558372911,-3.37657923595281E-32));
#127711=DIRECTION('center_axis',(-3.8157546084601E-32,-5.67927609187195E-32,
1.));
#127712=DIRECTION('ref_axis',(0.377966701428889,-0.925819190020905,-3.81575460846024E-32));
#127713=DIRECTION('center_axis',(3.8157546084601E-32,5.67927609187195E-32,
-1.));
#127714=DIRECTION('ref_axis',(-0.37796670142891,0.925819190020897,3.8157546084601E-32));
#127715=DIRECTION('center_axis',(-0.0743391421060632,0.997233017880442,
5.69527448431661E-32));
#127716=DIRECTION('ref_axis',(-0.997233017880442,-0.0743391421060632,-4.11084041927044E-32));
#127717=DIRECTION('',(-3.67608397811132E-32,-5.98511211175602E-32,1.));
#127718=DIRECTION('',(-0.729782852665248,-0.0544019604426628,-0.68151112584885));
#127719=DIRECTION('center_axis',(0.0743343479160154,-0.997233375251421,
2.13514020042163E-6));
#127720=DIRECTION('ref_axis',(0.988793810213182,0.0737055358578386,0.129824092016876));
#127721=DIRECTION('',(-1.22906873758652E-33,5.70191478903094E-32,-1.));
#127722=DIRECTION('center_axis',(0.760439763646594,-0.649408473816836,-1.09134209065814E-32));
#127723=DIRECTION('ref_axis',(0.649408473816836,0.760439763646594,6.93859732550991E-32));
#127724=DIRECTION('center_axis',(-0.760439763646603,0.649408473816825,4.04526730079985E-15));
#127725=DIRECTION('ref_axis',(0.644536842633876,0.754735215254185,-0.122257978646687));
#127726=DIRECTION('',(0.475242155112692,0.556495713683474,0.681511125848848));
#127727=DIRECTION('',(-3.67608397811132E-32,-5.98511211175602E-32,1.));
#127728=DIRECTION('',(-1.20214177310826E-32,-3.08819268200052E-32,1.));
#127729=DIRECTION('center_axis',(-3.67608397811132E-32,-5.98511211175602E-32,
1.));
#127730=DIRECTION('ref_axis',(-0.452171907282689,0.891930808002692,3.67608397811132E-32));
#127731=DIRECTION('center_axis',(0.302965055923512,0.153590711238812,-0.940543496235245));
#127732=DIRECTION('ref_axis',(0.838953614500091,0.425181023408944,0.339673269554959));
#127733=DIRECTION('center_axis',(0.302965055923512,0.153590711238812,-0.940543496235245));
#127734=DIRECTION('ref_axis',(0.838953614500091,0.425181023408944,0.339673269554959));
#127735=DIRECTION('center_axis',(-0.476801507016228,-0.558321672599558,
-0.678923583927297));
#127736=DIRECTION('ref_axis',(-0.631244341948508,-0.320014686676681,0.706485089063613));
#127737=DIRECTION('center_axis',(0.732177396727087,0.054580462706547,0.678923583927297));
#127738=DIRECTION('ref_axis',(0.631244341948508,0.320014686676676,-0.706485089063615));
#127739=DIRECTION('center_axis',(0.0987474500471282,-0.994815883292307,
-0.0242960790774368));
#127740=DIRECTION('ref_axis',(-0.687209671238742,-0.0505146907306731,-0.724700720143374));
#127741=DIRECTION('center_axis',(3.67608397811132E-32,5.98511211175602E-32,
-1.));
#127742=DIRECTION('ref_axis',(0.452171907282684,-0.891930808002695,-3.67608397811135E-32));
#127743=DIRECTION('center_axis',(4.90798928986703E-35,-4.11900193408512E-32,
1.));
#127744=DIRECTION('ref_axis',(-0.994462996350253,0.105087339342457,4.37735767734696E-33));
#127745=DIRECTION('center_axis',(-3.67608397811132E-32,-5.98511211175602E-32,
1.));
#127746=DIRECTION('ref_axis',(-0.452171907282684,0.891930808002695,3.67608397811135E-32));
#127747=DIRECTION('center_axis',(0.475034479697857,0.556252531387978,0.681854357192688));
#127748=DIRECTION('ref_axis',(0.633766178214038,0.321293153014877,-0.703641344136152));
#127749=DIRECTION('center_axis',(0.475452494453153,0.556742015363834,0.681163162426516));
#127750=DIRECTION('ref_axis',(0.633171645820719,0.320991749762738,-0.704313824593084));
#127751=DIRECTION('center_axis',(-0.730105850198729,-0.0544260384255558,
-0.681163162426516));
#127752=DIRECTION('ref_axis',(-0.633171645820721,-0.320991749762735,0.704313824593083));
#127753=DIRECTION('center_axis',(-0.729463945861553,-0.0543781874048979,
-0.681854357192686));
#127754=DIRECTION('ref_axis',(-0.633766178214029,-0.321293153014888,0.703641344136155));
#127755=DIRECTION('center_axis',(-3.67608397811132E-32,-5.98511211175602E-32,
1.));
#127756=DIRECTION('ref_axis',(-0.452171907282684,0.891930808002695,3.67608397811135E-32));
#127757=DIRECTION('center_axis',(4.90798928986703E-35,-4.11900193408512E-32,
1.));
#127758=DIRECTION('ref_axis',(-0.503043593699408,-0.864261038597706,-3.55742395696816E-32));
#127759=DIRECTION('center_axis',(-3.67608397811132E-32,-5.98511211175602E-32,
1.));
#127760=DIRECTION('ref_axis',(0.4521719072827,-0.891930808002687,-3.67608397811125E-32));
#127761=DIRECTION('center_axis',(3.67608397811132E-32,5.98511211175602E-32,
-1.));
#127762=DIRECTION('ref_axis',(-0.452171907282689,0.891930808002692,3.67608397811132E-32));
#127763=DIRECTION('center_axis',(-0.155375533560164,0.98785547706681,5.65662504286916E-32));
#127764=DIRECTION('ref_axis',(-0.98785547706681,-0.155375533560164,-4.44483110284763E-32));
#127765=DIRECTION('',(-3.51194961539937E-32,-6.27854603450134E-32,1.));
#127766=DIRECTION('',(-0.722920295606614,-0.113705019872821,-0.68151112584885));
#127767=DIRECTION('center_axis',(0.15537078445142,-0.987856224019666,2.13514022059604E-6));
#127768=DIRECTION('ref_axis',(0.979495994957281,0.154056161813633,0.129824092024161));
#127769=DIRECTION('',(-2.51317196927925E-33,5.68663800496771E-32,-1.));
#127770=DIRECTION('center_axis',(0.810842282495128,-0.585264720377106,-8.26974247098904E-33));
#127771=DIRECTION('ref_axis',(0.585264720377106,0.810842282495128,7.14633080700099E-32));
#127772=DIRECTION('center_axis',(-0.810842282495157,0.585264720377065,3.42448414268799E-14));
#127773=DIRECTION('ref_axis',(0.580874272795154,0.804759632346359,-0.122257978678096));
#127774=DIRECTION('',(0.428301259126908,0.593380667678461,0.681511125848852));
#127775=DIRECTION('',(-3.51194961539937E-32,-6.27854603450134E-32,1.));
#127776=DIRECTION('',(-1.28236507621053E-32,-3.18961660850267E-32,1.));
#127777=DIRECTION('center_axis',(-3.51194961539936E-32,-6.27854603450134E-32,
1.));
#127778=DIRECTION('ref_axis',(-0.523367983696617,0.852106773615454,3.51194961539936E-32));
#127779=DIRECTION('center_axis',(0.289437895860302,0.177774115465673,-0.940543496235213));
#127780=DIRECTION('ref_axis',(0.801505864960677,0.492148776675732,0.339673269555049));
#127781=DIRECTION('center_axis',(0.289437895860302,0.177774115465673,-0.940543496235213));
#127782=DIRECTION('ref_axis',(0.801505864960677,0.492148776675732,0.339673269555049));
#127783=DIRECTION('center_axis',(-0.429706589812599,-0.595327652523332,
-0.678923583927297));
#127784=DIRECTION('ref_axis',(-0.603059760639106,-0.370402138261486,0.706485089063615));
#127785=DIRECTION('center_axis',(0.725292322428983,0.114078105756041,0.678923583927297));
#127786=DIRECTION('ref_axis',(0.603059760639111,0.37040213826148,-0.706485089063613));
#127787=DIRECTION('center_axis',(0.179505605959122,-0.983456881602261,-0.0242960790746993));
#127788=DIRECTION('ref_axis',(-0.680805576941664,-0.106360566013795,-0.724700763351573));
#127789=DIRECTION('center_axis',(3.51194961539936E-32,6.27854603450134E-32,
-1.));
#127790=DIRECTION('ref_axis',(0.523367983696608,-0.852106773615459,-3.51194961539942E-32));
#127791=DIRECTION('center_axis',(4.6888512889172E-35,-4.11861016649801E-32,
1.));
#127792=DIRECTION('ref_axis',(-0.999719596506991,0.023679703543321,1.02215004271818E-33));
#127793=DIRECTION('center_axis',(-3.51194961539936E-32,-6.27854603450134E-32,
1.));
#127794=DIRECTION('ref_axis',(-0.523367983696608,0.852106773615459,3.51194961539942E-32));
#127795=DIRECTION('center_axis',(0.428114096349574,0.593121367077712,0.681854357192688));
#127796=DIRECTION('ref_axis',(0.605468998827241,0.371881903675627,-0.703641344136152));
#127797=DIRECTION('center_axis',(0.428490822707076,0.593643294419234,0.681163162426516));
#127798=DIRECTION('ref_axis',(0.604901011854561,0.371533043408514,-0.704313824593082));
#127799=DIRECTION('center_axis',(-0.723240255813313,-0.113755345035745,
-0.681163162426516));
#127800=DIRECTION('ref_axis',(-0.60490101185456,-0.37153304340851,0.704313824593085));
#127801=DIRECTION('center_axis',(-0.722604387662277,-0.113655332072782,
-0.681854357192686));
#127802=DIRECTION('ref_axis',(-0.60546899882723,-0.371881903675639,0.703641344136154));
#127803=DIRECTION('center_axis',(-3.51194961539936E-32,-6.27854603450134E-32,
1.));
#127804=DIRECTION('ref_axis',(-0.523367983696608,0.852106773615459,3.51194961539942E-32));
#127805=DIRECTION('center_axis',(4.6888512889172E-35,-4.11861016649801E-32,
1.));
#127806=DIRECTION('ref_axis',(-0.430924459585822,-0.902388004203661,-3.7145638675313E-32));
#127807=DIRECTION('center_axis',(-3.51194961539936E-32,-6.27854603450134E-32,
1.));
#127808=DIRECTION('ref_axis',(0.52336798369665,-0.852106773615433,-3.51194961539911E-32));
#127809=DIRECTION('center_axis',(3.51194961539936E-32,6.27854603450134E-32,
-1.));
#127810=DIRECTION('ref_axis',(-0.523367983696616,0.852106773615454,3.51194961539936E-32));
#127811=DIRECTION('center_axis',(-0.23537792647358,0.971903921037979,5.59088086291999E-32));
#127812=DIRECTION('ref_axis',(-0.971903921037979,-0.23537792647358,-4.77456017169564E-32));
#127813=DIRECTION('',(-3.32444380742783E-32,-6.5576251057652E-32,1.));
#127814=DIRECTION('',(-0.711246823254172,-0.172251391155723,-0.68151112584885));
#127815=DIRECTION('center_axis',(0.235373254050727,-0.971905052601854,2.13514020080356E-6));
#127816=DIRECTION('ref_axis',(0.963679795426648,0.233381569421748,0.129824092296828));
#127817=DIRECTION('',(-3.78055045616061E-33,5.66094541970164E-32,-1.));
#127818=DIRECTION('center_axis',(0.855848779733215,-0.517226126785149,-5.46553858485233E-33));
#127819=DIRECTION('ref_axis',(0.517226126785149,0.855848779733215,7.33182463894781E-32));
#127820=DIRECTION('center_axis',(-0.855848779733223,0.517226126785135,3.05303192513103E-16));
#127821=DIRECTION('ref_axis',(0.513346080509126,0.849428506860947,-0.122257978708549));
#127822=DIRECTION('',(0.378510088926399,0.626316771230954,0.681511125848847));
#127823=DIRECTION('',(-3.32444380742783E-32,-6.5576251057652E-32,1.));
#127824=DIRECTION('',(-1.35405445130596E-32,-3.29724199921591E-32,1.));
#127825=DIRECTION('center_axis',(-3.32444380742783E-32,-6.5576251057652E-32,
1.));
#127826=DIRECTION('ref_axis',(-0.591081132528682,0.806612109237526,3.32444380742781E-32));
#127827=DIRECTION('center_axis',(0.273984574353956,0.200774462284739,-0.940543496235212));
#127828=DIRECTION('ref_axis',(0.75872422612919,0.555841361032482,0.339673269555053));
#127829=DIRECTION('center_axis',(0.273984574353956,0.200774462284739,-0.940543496235212));
#127830=DIRECTION('ref_axis',(0.75872422612919,0.555841361032482,0.339673269555053));
#127831=DIRECTION('center_axis',(-0.379752046150365,-0.628371825141711,
-0.678923583927297));
#127832=DIRECTION('ref_axis',(-0.570861916120514,-0.418324624728203,0.706485089063615));
#127833=DIRECTION('center_axis',(0.713580547389924,0.172816577833291,0.678923583927297));
#127834=DIRECTION('ref_axis',(0.57086191612052,0.418324624728196,-0.706485089063614));
#127835=DIRECTION('center_axis',(0.2590691816723,-0.965553136626766,-0.0242960790634893));
#127836=DIRECTION('ref_axis',(-0.669870625097031,-0.161498560364775,-0.72470101464826));
#127837=DIRECTION('center_axis',(3.32444380742783E-32,6.5576251057652E-32,
-1.));
#127838=DIRECTION('ref_axis',(0.59108113252868,-0.806612109237527,-3.32444380742783E-32));
#127839=DIRECTION('center_axis',(4.43850975624469E-35,-4.11823756426669E-32,
1.));
#127840=DIRECTION('ref_axis',(-0.998323227691098,-0.0578855167760327,-2.33955242228056E-33));
#127841=DIRECTION('center_axis',(-3.32444380742783E-32,-6.5576251057652E-32,
1.));
#127842=DIRECTION('ref_axis',(-0.59108113252868,0.806612109237527,3.32444380742783E-32));
#127843=DIRECTION('center_axis',(0.378344684323938,0.626043077927682,0.681854357192688));
#127844=DIRECTION('ref_axis',(0.573142523148597,0.419995841623614,-0.703641344136153));
#127845=DIRECTION('center_axis',(0.378677615231892,0.626593975294525,0.681163162426516));
#127846=DIRECTION('ref_axis',(0.572604861456137,0.41960184594906,-0.704313824593086));
#127847=DIRECTION('center_axis',(-0.711561616851703,-0.172327628593032,
-0.681163162426516));
#127848=DIRECTION('ref_axis',(-0.572604861456143,-0.419601845949057,0.704313824593082));
#127849=DIRECTION('center_axis',(-0.710936016484441,-0.172176119257531,
-0.681854357192686));
#127850=DIRECTION('ref_axis',(-0.573142523148589,-0.419995841623623,0.703641344136154));
#127851=DIRECTION('center_axis',(-3.32444380742783E-32,-6.5576251057652E-32,
1.));
#127852=DIRECTION('ref_axis',(-0.59108113252868,0.806612109237527,3.32444380742783E-32));
#127853=DIRECTION('center_axis',(4.43850975624469E-35,-4.11823756426669E-32,
1.));
#127854=DIRECTION('ref_axis',(-0.355937594291196,-0.934509726525196,-3.84695322746377E-32));
#127855=DIRECTION('center_axis',(-3.32444380742783E-32,-6.5576251057652E-32,
1.));
#127856=DIRECTION('ref_axis',(0.591081132528663,-0.80661210923754,-3.32444380742797E-32));
#127857=DIRECTION('center_axis',(3.32444380742783E-32,6.5576251057652E-32,
-1.));
#127858=DIRECTION('ref_axis',(-0.59108113252868,0.806612109237527,3.32444380742783E-32));
#127859=DIRECTION('center_axis',(-0.313813918120938,0.9494845047675,5.49847946113966E-32));
#127860=DIRECTION('ref_axis',(-0.9494845047675,-0.313813918120938,-5.09783333326273E-32));
#127861=DIRECTION('',(-3.11481437441248E-32,-6.82049210037316E-32,1.));
#127862=DIRECTION('',(-0.694840120640444,-0.229651457849954,-0.681511125848848));
#127863=DIRECTION('center_axis',(0.31380935347816,-0.949486013412025,2.13514018838833E-6));
#127864=DIRECTION('ref_axis',(0.941450465909118,0.311153861202889,0.129824092132539));
#127865=DIRECTION('',(-5.02277000350315E-33,5.62500801314868E-32,-1.));
#127866=DIRECTION('center_axis',(0.895159744547287,-0.44574547865574,-2.51947076237234E-33));
#127867=DIRECTION('ref_axis',(0.44574547865574,0.895159744547288,7.4938443905031E-32));
#127868=DIRECTION('center_axis',(-0.895159744547308,0.445745478655699,2.32539264964185E-14));
#127869=DIRECTION('ref_axis',(0.442401654758204,0.888444574816553,-0.122257978660848));
#127870=DIRECTION('',(0.326199996533836,0.655084840005904,0.681511125848848));
#127871=DIRECTION('',(-3.11481437441248E-32,-6.82049210037316E-32,1.));
#127872=DIRECTION('',(-1.41673281743121E-32,-3.41035262492199E-32,1.));
#127873=DIRECTION('center_axis',(-3.11481437441248E-32,-6.82049210037316E-32,
1.));
#127874=DIRECTION('ref_axis',(-0.654860733945287,0.755749574354256,3.1148143744125E-32));
#127875=DIRECTION('center_axis',(0.256707930709546,0.222438688182747,-0.940543496235215));
#127876=DIRECTION('ref_axis',(0.710893402753043,0.615834912839461,0.339673269555044));
#127877=DIRECTION('center_axis',(0.256707930709546,0.222438688182747,-0.940543496235215));
#127878=DIRECTION('ref_axis',(0.710893402753043,0.615834912839461,0.339673269555044));
#127879=DIRECTION('center_axis',(-0.327270315275677,-0.657234286937827,
-0.678923583927297));
#127880=DIRECTION('ref_axis',(-0.534865079735733,-0.463463229836053,0.706485089063613));
#127881=DIRECTION('center_axis',(0.697120011540489,0.230404984097789,0.678923583927297));
#127882=DIRECTION('ref_axis',(0.534865079735735,0.463463229836049,-0.706485089063615));
#127883=DIRECTION('center_axis',(0.336908694744834,-0.941223794826141,-0.0242960790748523));
#127884=DIRECTION('ref_axis',(-0.654478525247296,-0.215562043042521,-0.724700535110509));
#127885=DIRECTION('center_axis',(3.11481437441248E-32,6.82049210037316E-32,
-1.));
#127886=DIRECTION('ref_axis',(0.654860733945285,-0.755749574354258,-3.11481437441251E-32));
#127887=DIRECTION('center_axis',(4.1586306734472E-35,-4.11788660699752E-32,
1.));
#127888=DIRECTION('ref_axis',(-0.990283182506659,-0.139065518531672,-5.68537814238565E-33));
#127889=DIRECTION('center_axis',(-3.11481437441248E-32,-6.82049210037316E-32,
1.));
#127890=DIRECTION('ref_axis',(-0.654860733945285,0.755749574354258,3.11481437441251E-32));
#127891=DIRECTION('center_axis',(0.326057450846606,0.65479857538388,0.681854357192688));
#127892=DIRECTION('ref_axis',(0.537001878540266,0.465314776540025,-0.703641344136153));
#127893=DIRECTION('center_axis',(0.32634437070475,0.655374776644959,0.681163162426516));
#127894=DIRECTION('ref_axis',(0.536498120177896,0.464878267434227,-0.704313824593083));
#127895=DIRECTION('center_axis',(-0.695147652729348,-0.22975310021409,-0.681163162426516));
#127896=DIRECTION('ref_axis',(-0.536498120177896,-0.464878267434224,0.704313824593084));
#127897=DIRECTION('center_axis',(-0.694536483413087,-0.229551102775682,
-0.681854357192686));
#127898=DIRECTION('ref_axis',(-0.537001878540256,-0.465314776540035,0.703641344136155));
#127899=DIRECTION('center_axis',(-3.11481437441248E-32,-6.82049210037316E-32,
1.));
#127900=DIRECTION('ref_axis',(-0.654860733945285,0.755749574354258,3.11481437441251E-32));
#127901=DIRECTION('center_axis',(4.1586306734472E-35,-4.11788660699752E-32,
1.));
#127902=DIRECTION('ref_axis',(-0.278582023032155,-0.960412440799947,-3.95371100741784E-32));
#127903=DIRECTION('center_axis',(-3.11481437441248E-32,-6.82049210037316E-32,
1.));
#127904=DIRECTION('ref_axis',(0.654860733945243,-0.755749574354294,-3.11481437441289E-32));
#127905=DIRECTION('center_axis',(3.11481437441248E-32,6.82049210037316E-32,
-1.));
#127906=DIRECTION('ref_axis',(-0.654860733945289,0.755749574354255,3.11481437441248E-32));
#127907=DIRECTION('center_axis',(-0.390161529918854,0.92074642577171,5.38003575361184E-32));
#127908=DIRECTION('ref_axis',(-0.92074642577171,-0.390161529918854,-5.41249925799502E-32));
#127909=DIRECTION('',(-2.88445636564362E-32,-7.06539768184611E-32,1.));
#127910=DIRECTION('',(-0.673809371664394,-0.285523231982033,-0.681511125848851));
#127911=DIRECTION('center_axis',(0.390157103433078,-0.920748301457109,2.13514019164445E-6));
#127912=DIRECTION('ref_axis',(0.912955938858505,0.386855475373679,0.129824092049167));
#127913=DIRECTION('',(-6.23156384517107E-33,5.57906494282019E-32,-1.));
#127914=DIRECTION('center_axis',(0.928513568952359,-0.371298467908706,5.48855401159282E-34));
#127915=DIRECTION('ref_axis',(0.371298467908706,0.928513568952359,7.63131184695165E-32));
#127916=DIRECTION('center_axis',(-0.928513568952349,0.371298467908731,-1.56722305490052E-14));
#127917=DIRECTION('ref_axis',(0.368513118979584,0.921548190696015,-0.122257978736933));
#127918=DIRECTION('',(0.271719096983559,0.679493427252001,0.681511125848851));
#127919=DIRECTION('',(-2.88445636564362E-32,-7.06539768184611E-32,1.));
#127920=DIRECTION('',(-1.46998306040091E-32,-3.52819575306877E-32,1.));
#127921=DIRECTION('center_axis',(-2.88445636564362E-32,-7.06539768184611E-32,
1.));
#127922=DIRECTION('ref_axis',(-0.714282345221906,0.69985765074356,2.88445636564363E-32));
#127923=DIRECTION('center_axis',(0.237722938140168,0.242622621310774,-0.94054349623518));
#127924=DIRECTION('ref_axis',(0.658331701071381,0.671730184906247,0.339673269555142));
#127925=DIRECTION('center_axis',(0.237722938140168,0.242622621310774,-0.94054349623518));
#127926=DIRECTION('ref_axis',(0.658331701071381,0.671730184906247,0.339673269555142));
#127927=DIRECTION('center_axis',(-0.27261065444863,-0.681722962990395,-0.678923583927297));
#127928=DIRECTION('ref_axis',(-0.495308804491826,-0.505517563615405,0.706485089063614));
#127929=DIRECTION('center_axis',(0.676020257030958,0.286460083207263,0.678923583927297));
#127930=DIRECTION('ref_axis',(0.495308804491831,0.505517563615401,-0.706485089063614));
#127931=DIRECTION('center_axis',(0.412506136031845,-0.910630763963938,-0.0242960790773052));
#127932=DIRECTION('ref_axis',(-0.63473071784112,-0.268190961384672,-0.724700299475902));
#127933=DIRECTION('center_axis',(2.88445636564362E-32,7.06539768184611E-32,
-1.));
#127934=DIRECTION('ref_axis',(0.714282345221904,-0.699857650743561,-2.88445636564365E-32));
#127935=DIRECTION('center_axis',(3.85107658964331E-35,-4.11755963025323E-32,
1.));
#127936=DIRECTION('ref_axis',(-0.975652966127864,-0.219320062205675,-8.99306119945245E-33));
#127937=DIRECTION('center_axis',(-2.88445636564362E-32,-7.06539768184611E-32,
1.));
#127938=DIRECTION('ref_axis',(-0.714282345221904,0.699857650743561,2.88445636564365E-32));
#127939=DIRECTION('center_axis',(0.271600358829583,0.679196496355059,0.681854357192688));
#127940=DIRECTION('ref_axis',(0.497287575029324,0.507537118390098,-0.703641344136152));
#127941=DIRECTION('center_axis',(0.271839358233598,0.679794166986047,0.681163162426516));
#127942=DIRECTION('ref_axis',(0.496821072425813,0.507061000749148,-0.704313824593084));
#127943=DIRECTION('center_axis',(-0.674107595669369,-0.285649602859816,
-0.681163162426516));
#127944=DIRECTION('ref_axis',(-0.496821072425817,-0.507061000749145,0.704313824593083));
#127945=DIRECTION('center_axis',(-0.673514924635072,-0.285398461578126,
-0.681854357192686));
#127946=DIRECTION('ref_axis',(-0.497287575029312,-0.507537118390104,0.703641344136156));
#127947=DIRECTION('center_axis',(-2.88445636564362E-32,-7.06539768184611E-32,
1.));
#127948=DIRECTION('ref_axis',(-0.714282345221904,0.699857650743561,2.88445636564365E-32));
#127949=DIRECTION('center_axis',(3.85107658964331E-35,-4.11755963025323E-32,
1.));
#127950=DIRECTION('ref_axis',(-0.199372534372617,-0.979923768738079,-4.03412675198177E-32));
#127951=DIRECTION('center_axis',(-2.88445636564362E-32,-7.06539768184611E-32,
1.));
#127952=DIRECTION('ref_axis',(0.714282345221909,-0.699857650743556,-2.8844563656436E-32));
#127953=DIRECTION('center_axis',(2.88445636564362E-32,7.06539768184611E-32,
-1.));
#127954=DIRECTION('ref_axis',(-0.714282345221907,0.699857650743558,2.88445636564362E-32));
#127955=DIRECTION('center_axis',(-0.463912681107281,0.885880931224876,5.2363379636683E-32));
#127956=DIRECTION('ref_axis',(-0.885880931224876,-0.463912681107281,-5.71646389607962E-32));
#127957=DIRECTION('',(-2.6349027756632E-32,-7.29071204394592E-32,1.));
#127958=DIRECTION('',(-0.648294532490652,-0.339494896113273,-0.681511125848848));
#127959=DIRECTION('center_axis',(0.463908422236103,-0.885883161468741,2.13514017017263E-6));
#127960=DIRECTION('ref_axis',(0.878385840636379,0.459982630171223,0.129824092179707));
#127961=DIRECTION('',(-7.39888765758507E-33,5.52342195226914E-32,-1.));
#127962=DIRECTION('center_axis',(0.955688288750009,-0.294380527117673,3.71902070136243E-33));
#127963=DIRECTION('ref_axis',(0.294380527117673,0.955688288750009,7.74331218505131E-32));
#127964=DIRECTION('center_axis',(-0.955688288750012,0.294380527117663,1.47563209714676E-15));
#127965=DIRECTION('ref_axis',(0.292172189203034,0.948519055433948,-0.122257978614886));
#127966=DIRECTION('',(0.215429951673331,0.699380097848275,0.681511125848847));
#127967=DIRECTION('',(-2.6349027756632E-32,-7.29071204394592E-32,1.));
#127968=DIRECTION('',(-1.51345080863378E-32,-3.64998715708118E-32,1.));
#127969=DIRECTION('center_axis',(-2.6349027756632E-32,-7.29071204394592E-32,
1.));
#127970=DIRECTION('ref_axis',(-0.768950525339364,0.639308289935549,2.63490277566321E-32));
#127971=DIRECTION('center_axis',(0.217155938638854,0.26119194092375,-0.940543496235215));
#127972=DIRECTION('ref_axis',(0.601388910536204,0.723155203420306,0.339673269555043));
#127973=DIRECTION('center_axis',(0.217155938638854,0.26119194092375,-0.940543496235215));
#127974=DIRECTION('ref_axis',(0.601388910536204,0.723155203420306,0.339673269555043));
#127975=DIRECTION('center_axis',(-0.21613681469382,-0.701674885200634,-0.678923583927297));
#127976=DIRECTION('ref_axis',(-0.452456330874236,-0.544207761413417,0.706485089063613));
#127977=DIRECTION('center_axis',(0.650421699246377,0.340608837725579,0.678923583927297));
#127978=DIRECTION('ref_axis',(0.45245633087424,0.544207761413411,-0.706485089063615));
#127979=DIRECTION('center_axis',(0.485358417045744,-0.87397763560859,-0.0242960790842656));
#127980=DIRECTION('ref_axis',(-0.610758275705588,-0.319034804460315,-0.724700712156478));
#127981=DIRECTION('center_axis',(2.6349027756632E-32,7.29071204394592E-32,
-1.));
#127982=DIRECTION('ref_axis',(0.768950525339369,-0.639308289935542,-2.63490277566315E-32));
#127983=DIRECTION('center_axis',(3.51789422651897E-35,-4.1172588100101E-32,
1.));
#127984=DIRECTION('ref_axis',(-0.954529940230895,-0.298115067050969,-1.22405895084658E-32));
#127985=DIRECTION('center_axis',(-2.6349027756632E-32,-7.29071204394592E-32,
1.));
#127986=DIRECTION('ref_axis',(-0.768950525339369,0.639308289935542,2.63490277566315E-32));
#127987=DIRECTION('center_axis',(0.215335811235453,0.69907447670253,0.681854357192688));
#127988=DIRECTION('ref_axis',(0.454263904753227,0.54638188445502,-0.703641344136153));
#127989=DIRECTION('center_axis',(0.215525299683739,0.699689639303987,0.681163162426516));
#127990=DIRECTION('ref_axis',(0.453837762406455,0.545869326763252,-0.704313824593083));
#127991=DIRECTION('center_axis',(-0.648581463780135,-0.339645154527377,
-0.681163162426516));
#127992=DIRECTION('ref_axis',(-0.453837762406457,-0.545869326763248,0.704313824593085));
#127993=DIRECTION('center_axis',(-0.648011235155752,-0.3393465407062,-0.681854357192686));
#127994=DIRECTION('ref_axis',(-0.454263904753214,-0.54638188445503,0.703641344136153));
#127995=DIRECTION('center_axis',(-2.6349027756632E-32,-7.29071204394592E-32,
1.));
#127996=DIRECTION('ref_axis',(-0.768950525339369,0.639308289935542,2.63490277566315E-32));
#127997=DIRECTION('center_axis',(3.51789422651897E-35,-4.1172588100101E-32,
1.));
#127998=DIRECTION('ref_axis',(-0.118836254390997,-0.992913865671297,-4.08766530764311E-32));
#127999=DIRECTION('center_axis',(-2.6349027756632E-32,-7.29071204394592E-32,
1.));
#128000=DIRECTION('ref_axis',(0.768950525339356,-0.639308289935559,-2.63490277566331E-32));
#128001=DIRECTION('center_axis',(2.6349027756632E-32,7.29071204394592E-32,
-1.));
#128002=DIRECTION('ref_axis',(-0.768950525339365,0.639308289935547,2.6349027756632E-32));
#128003=DIRECTION('center_axis',(-0.534576569943144,0.845120045240807,5.06834237639265E-32));
#128004=DIRECTION('ref_axis',(-0.845120045240807,-0.534576569943144,-6.00770441300072E-32));
#128005=DIRECTION('',(-2.3678143424391E-32,-7.49493575676706E-32,1.));
#128006=DIRECTION('',(-0.618465400164238,-0.391207277723611,-0.681511125848852));
#128007=DIRECTION('center_axis',(0.534572507028513,-0.845122615201304,2.13514020294021E-6));
#128008=DIRECTION('ref_axis',(0.837970229577547,0.530048676459173,0.129824092238814));
#128009=DIRECTION('',(-8.51697309336836E-33,5.4584493364172E-32,-1.));
#128010=DIRECTION('center_axis',(0.976503060663496,-0.215503532488041,6.96992821120469E-33));
#128011=DIRECTION('ref_axis',(0.215503532488041,0.976503060663496,7.82910006103078E-32));
#128012=DIRECTION('center_axis',(-0.97650306066349,0.215503532488069,-1.70588158816704E-14));
#128013=DIRECTION('ref_axis',(0.213886901704482,0.969177682327868,-0.122257978704212));
#128014=DIRECTION('',(0.157707155578177,0.714612509282951,0.681511125848848));
#128015=DIRECTION('',(-2.3678143424391E-32,-7.49493575676706E-32,1.));
#128016=DIRECTION('',(-1.54684679143701E-32,-3.7749163352597E-32,1.));
#128017=DIRECTION('center_axis',(-2.36781434243909E-32,-7.49493575676706E-32,
1.));
#128018=DIRECTION('ref_axis',(-0.818501466578596,0.574504437936459,2.3678143424391E-32));
#128019=DIRECTION('center_axis',(0.195143802194235,0.278023071263677,-0.940543496235177));
#128020=DIRECTION('ref_axis',(0.540443976022996,0.769767743368199,0.33967326955515));
#128021=DIRECTION('center_axis',(0.195143802194235,0.278023071263677,-0.940543496235177));
#128022=DIRECTION('ref_axis',(0.540443976022996,0.769767743368199,0.33967326955515));
#128023=DIRECTION('center_axis',(-0.158224620097287,-0.716957276818071,
-0.678923583927297));
#128024=DIRECTION('ref_axis',(-0.406592835024712,-0.579276346347187,0.706485089063613));
#128025=DIRECTION('center_axis',(0.620494692365338,0.392490896625334,0.678923583927297));
#128026=DIRECTION('ref_axis',(0.406592835024718,0.57927634634718,-0.706485089063615));
#128027=DIRECTION('center_axis',(0.5549807178787,-0.83150833027891,-0.0242960790997562));
#128028=DIRECTION('ref_axis',(-0.582721524349687,-0.367755567997614,-0.724700950231424));
#128029=DIRECTION('center_axis',(2.36781434243909E-32,7.49493575676706E-32,
-1.));
#128030=DIRECTION('ref_axis',(0.818501466578592,-0.574504437936465,-2.36781434243915E-32));
#128031=DIRECTION('center_axis',(3.1613008577281E-35,-4.11698614817723E-32,
1.));
#128032=DIRECTION('ref_axis',(-0.927054675068042,-0.374926165310569,-1.54063513043337E-32));
#128033=DIRECTION('center_axis',(-2.3678143424391E-32,-7.49493575676706E-32,
1.));
#128034=DIRECTION('ref_axis',(-0.818501466578592,0.574504437936465,2.36781434243915E-32));
#128035=DIRECTION('center_axis',(0.15763823934546,0.714300231746714,0.681854357192688));
#128036=DIRECTION('ref_axis',(0.408217183139275,0.581590569225554,-0.703641344136152));
#128037=DIRECTION('center_axis',(0.157776955823656,0.714928792513023,0.681163162426516));
#128038=DIRECTION('ref_axis',(0.407834236956233,0.581044982469851,-0.704313824593084));
#128039=DIRECTION('center_axis',(-0.618739129257853,-0.391380423729065,
-0.681163162426516));
#128040=DIRECTION('ref_axis',(-0.407834236956234,-0.581044982469851,0.704313824593083));
#128041=DIRECTION('center_axis',(-0.618195137820799,-0.391036324594112,
-0.681854357192686));
#128042=DIRECTION('ref_axis',(-0.408217183139263,-0.58159056922556,0.703641344136155));
#128043=DIRECTION('center_axis',(-2.36781434243909E-32,-7.49493575676706E-32,
1.));
#128044=DIRECTION('ref_axis',(-0.818501466578592,0.574504437936465,2.36781434243915E-32));
#128045=DIRECTION('center_axis',(3.1613008577281E-35,-4.11698614817723E-32,
1.));
#128046=DIRECTION('ref_axis',(-0.0375091387429898,-0.999296284647731,-4.1139703841472E-32));
#128047=DIRECTION('center_axis',(-2.3678143424391E-32,-7.49493575676706E-32,
1.));
#128048=DIRECTION('ref_axis',(0.818501466578589,-0.57450443793647,-2.3678143424392E-32));
#128049=DIRECTION('center_axis',(2.36781434243909E-32,7.49493575676706E-32,
-1.));
#128050=DIRECTION('ref_axis',(-0.818501466578597,0.574504437936459,2.36781434243909E-32));
#128051=DIRECTION('center_axis',(-0.601682939904961,0.798735024790652,4.87716697470088E-32));
#128052=DIRECTION('ref_axis',(-0.798735024790652,-0.601682939904961,-6.2842826511695E-32));
#128053=DIRECTION('',(-2.08496849542793E-32,-7.67670974519526E-32,1.));
#128054=DIRECTION('',(-0.584520482639347,-0.440316239445355,-0.681511125848849));
#128055=DIRECTION('center_axis',(0.601679099984979,-0.798737917365081,2.13514018879469E-6));
#128056=DIRECTION('ref_axis',(0.791978064924971,0.596587336277332,0.129824092029237));
#128057=DIRECTION('',(-9.57837947841694E-33,5.38457947730313E-32,-1.));
#128058=DIRECTION('center_axis',(0.990819365819932,-0.135192397405281,1.02799436775701E-32));
#128059=DIRECTION('ref_axis',(0.135192397405281,0.990819365819932,7.88810457072945E-32));
#128060=DIRECTION('center_axis',(-0.990819365819942,0.135192397405208,3.91233320239215E-14));
#128061=DIRECTION('ref_axis',(0.134178232167426,0.983386591662394,-0.12225797868051));
#128062=DIRECTION('',(0.0989348443824835,0.725089292371126,0.681511125848841));
#128063=DIRECTION('',(-2.08496849542793E-32,-7.67670974519526E-32,1.));
#128064=DIRECTION('',(-1.56994876405497E-32,-3.90215190453539E-32,1.));
#128065=DIRECTION('center_axis',(-2.08496849542793E-32,-7.67670974519526E-32,
1.));
#128066=DIRECTION('ref_axis',(-0.862605415600981,0.505877353689468,2.08496849542797E-32));
#128067=DIRECTION('center_axis',(0.171833015942407,0.293004003934834,-0.940543496235178));
#128068=DIRECTION('ref_axis',(0.475902476016994,0.811257605986293,0.339673269555146));
#128069=DIRECTION('center_axis',(0.171833015942407,0.293004003934834,-0.940543496235178));
#128070=DIRECTION('ref_axis',(0.475902476016994,0.811257605986293,0.339673269555146));
#128071=DIRECTION('center_axis',(-0.099259466759231,-0.727468436047907,
-0.678923583927297));
#128072=DIRECTION('ref_axis',(-0.358023530941186,-0.610489942769888,0.706485089063615));
#128073=DIRECTION('center_axis',(0.586438395681026,0.441760993364488,0.678923583927297));
#128074=DIRECTION('ref_axis',(0.358023530941192,0.610489942769888,-0.706485089063612));
#128075=DIRECTION('center_axis',(0.620909713570593,-0.783505474221586,-0.0242960790765126));
#128076=DIRECTION('ref_axis',(-0.550807437478925,-0.414029407872834,-0.724700501058451));
#128077=DIRECTION('center_axis',(2.08496849542793E-32,7.67670974519526E-32,
-1.));
#128078=DIRECTION('ref_axis',(0.862605415600986,-0.505877353689459,-2.08496849542789E-32));
#128079=DIRECTION('center_axis',(2.78366955330785E-35,-4.11674345927412E-32,
1.));
#128080=DIRECTION('ref_axis',(-0.89341001399587,-0.449242191798477,-1.84692789646177E-32));
#128081=DIRECTION('center_axis',(-2.08496849542793E-32,-7.67670974519526E-32,
1.));
#128082=DIRECTION('ref_axis',(-0.862605415600986,0.505877353689459,2.08496849542789E-32));
#128083=DIRECTION('center_axis',(0.0988916109811012,0.724772436599867,0.681854357192688));
#128084=DIRECTION('ref_axis',(0.359453843522623,0.612928864713583,-0.703641344136152));
#128085=DIRECTION('center_axis',(0.0989786323539316,0.725410212562833,0.681163162426516));
#128086=DIRECTION('ref_axis',(0.359116641946984,0.612353879683786,-0.704313824593084));
#128087=DIRECTION('center_axis',(-0.584779187915131,-0.44051112078406,-0.681163162426516));
#128088=DIRECTION('ref_axis',(-0.359116641946989,-0.612353879683783,0.704313824593084));
#128089=DIRECTION('center_axis',(-0.584265053838666,-0.440123826258303,
-0.681854357192686));
#128090=DIRECTION('ref_axis',(-0.359453843522612,-0.612928864713587,0.703641344136155));
#128091=DIRECTION('center_axis',(-2.08496849542793E-32,-7.67670974519526E-32,
1.));
#128092=DIRECTION('ref_axis',(-0.862605415600986,0.505877353689459,2.08496849542789E-32));
#128093=DIRECTION('center_axis',(2.78366955330785E-35,-4.11674345927412E-32,
1.));
#128094=DIRECTION('ref_axis',(0.0440675940347559,-0.999028551722116,-4.11286692554992E-32));
#128095=DIRECTION('center_axis',(-2.08496849542793E-32,-7.67670974519526E-32,
1.));
#128096=DIRECTION('ref_axis',(0.862605415600975,-0.505877353689478,-2.08496849542806E-32));
#128097=DIRECTION('center_axis',(2.08496849542793E-32,7.67670974519526E-32,
-1.));
#128098=DIRECTION('ref_axis',(-0.862605415600984,0.505877353689463,2.08496849542793E-32));
#128099=DIRECTION('center_axis',(-0.664785209172408,0.747034554532518,4.66408399934953E-32));
#128100=DIRECTION('ref_axis',(-0.747034554532518,-0.664785209172408,-6.54435802804316E-32));
#128101=DIRECTION('',(-1.78824752707528E-32,-7.83482433332812E-32,1.));
#128102=DIRECTION('',(-0.546685677741588,-0.486494969240645,-0.681511125848848));
#128103=DIRECTION('center_axis',(0.664781617801125,-0.747037750471259,2.1351401964272E-6));
#128104=DIRECTION('ref_axis',(0.740715416865343,0.659155805762135,0.129824092325236));
#128105=DIRECTION('',(-1.0576043328358E-32,5.30230396665167E-32,-1.));
#128106=DIRECTION('center_axis',(0.998541931570525,-0.0539815792229644,
1.3627039493644E-32));
#128107=DIRECTION('ref_axis',(0.0539815792229644,0.998541931570525,7.9199330488703E-32));
#128108=DIRECTION('center_axis',(-0.998541931570525,0.0539815792229708,
-4.59862933722826E-15));
#128109=DIRECTION('ref_axis',(0.0535766286324845,0.991051225469743,-0.122257978714264));
#128110=DIRECTION('',(0.0395041381205371,0.730740725849866,0.681511125848848));
#128111=DIRECTION('',(-1.78824752707528E-32,-7.83482433332812E-32,1.));
#128112=DIRECTION('',(-1.58260298667146E-32,-4.03084713318713E-32,1.));
#128113=DIRECTION('center_axis',(-1.78824752707528E-32,-7.83482433332812E-32,
1.));
#128114=DIRECTION('ref_axis',(-0.900968867902422,0.433883739117552,1.78824752707527E-32));
#128115=DIRECTION('center_axis',(0.147378709319891,0.306035043301973,-0.940543496235215));
#128116=DIRECTION('ref_axis',(0.408193923551509,0.847348683084722,0.339673269555042));
#128117=DIRECTION('center_axis',(0.147378709319891,0.306035043301973,-0.940543496235215));
#128118=DIRECTION('ref_axis',(0.408193923551509,0.847348683084722,0.339673269555042));
#128119=DIRECTION('center_axis',(-0.0396337580465518,-0.733138412859687,
-0.678923583927297));
#128120=DIRECTION('ref_axis',(-0.307071639328989,-0.6376408293472,0.706485089063613));
#128121=DIRECTION('center_axis',(0.548479448228981,0.488091243578234,0.678923583927297));
#128122=DIRECTION('ref_axis',(0.307071639328996,0.637640829347195,-0.706485089063615));
#128123=DIRECTION('center_axis',(0.682706657579583,-0.73028851848977,-0.024296079077326));
#128124=DIRECTION('ref_axis',(-0.515227392569887,-0.457547641377844,-0.724700551824826));
#128125=DIRECTION('center_axis',(1.78824752707528E-32,7.83482433332812E-32,
-1.));
#128126=DIRECTION('ref_axis',(0.900968867902418,-0.433883739117559,-1.78824752707533E-32));
#128127=DIRECTION('center_axis',(2.3875133872833E-35,-4.11653235835539E-32,
1.));
#128128=DIRECTION('ref_axis',(-0.853819856682831,-0.520568585619714,-2.14089892110869E-32));
#128129=DIRECTION('center_axis',(-1.78824752707528E-32,-7.83482433332812E-32,
1.));
#128130=DIRECTION('ref_axis',(-0.900968867902418,0.433883739117559,1.78824752707533E-32));
#128131=DIRECTION('center_axis',(0.0394868752616308,0.730421400466483,0.681854357192688));
#128132=DIRECTION('ref_axis',(0.308298397883036,0.640188219733089,-0.703641344136153));
#128133=DIRECTION('center_axis',(0.039521622416217,0.731064147332297,0.681163162426516));
#128134=DIRECTION('ref_axis',(0.30800918493565,0.639587662859704,-0.704313824593085));
#128135=DIRECTION('center_axis',(-0.546927637558608,-0.486710289009456,
-0.681163162426516));
#128136=DIRECTION('ref_axis',(-0.308009184935655,-0.639587662859703,0.704313824593083));
#128137=DIRECTION('center_axis',(-0.546446782320186,-0.486282376474064,
-0.681854357192686));
#128138=DIRECTION('ref_axis',(-0.308298397883024,-0.640188219733093,0.703641344136155));
#128139=DIRECTION('center_axis',(-1.78824752707528E-32,-7.83482433332812E-32,
1.));
#128140=DIRECTION('ref_axis',(-0.900968867902418,0.433883739117559,1.78824752707533E-32));
#128141=DIRECTION('center_axis',(2.3875133872833E-35,-4.11653235835539E-32,
1.));
#128142=DIRECTION('ref_axis',(0.125351064244853,-0.992112448612899,-4.08436227518619E-32));
#128143=DIRECTION('center_axis',(-1.78824752707528E-32,-7.83482433332812E-32,
1.));
#128144=DIRECTION('ref_axis',(0.900968867902418,-0.433883739117559,-1.78824752707533E-32));
#128145=DIRECTION('center_axis',(1.78824752707528E-32,7.83482433332812E-32,
-1.));
#128146=DIRECTION('ref_axis',(-0.900968867902422,0.433883739117553,1.78824752707528E-32));
#128147=DIRECTION('center_axis',(-0.723463442554651,0.690362692565997,4.43051148238335E-32));
#128148=DIRECTION('ref_axis',(-0.690362692565997,-0.723463442554651,-6.78619978489802E-32));
#128149=DIRECTION('',(-1.47962606647001E-32,-7.96822729466869E-32,1.));
#128150=DIRECTION('',(-0.505212769855237,-0.529436155281667,-0.68151112584885));
#128151=DIRECTION('center_axis',(0.723460123632049,-0.690366170600603,2.13514018696377E-6));
#128152=DIRECTION('ref_axis',(0.68452342996416,0.717337702154071,0.129824092134003));
#128153=DIRECTION('',(-1.15033253548732E-32,5.2121703344117E-32,-1.));
#128154=DIRECTION('center_axis',(0.999619365514338,0.0275884774627474,1.69889412890025E-32));
#128155=DIRECTION('ref_axis',(-0.0275884774627475,0.999619365514338,7.92437368218264E-32));
#128156=DIRECTION('center_axis',(-0.999619365514337,-0.0275884774627805,
1.09002780451937E-14));
#128157=DIRECTION('ref_axis',(0.0273815185261964,-0.992120576893031,0.122257978670674));
#128158=DIRECTION('',(-0.0201894616628749,0.731529200361817,0.681511125848847));
#128159=DIRECTION('',(-1.47962606647001E-32,-7.96822729466869E-32,1.));
#128160=DIRECTION('',(-1.58472524752277E-32,-4.16014557570146E-32,1.));
#128161=DIRECTION('center_axis',(-1.47962606647001E-32,-7.96822729466869E-32,
1.));
#128162=DIRECTION('ref_axis',(-0.933336521037368,0.359002699847595,1.47962606647003E-32));
#128163=DIRECTION('center_axis',(0.121943621702684,0.317029469948265,-0.940543496235211));
#128164=DIRECTION('ref_axis',(0.337768907871411,0.877800794500173,0.339673269555054));
#128165=DIRECTION('center_axis',(0.121943621702684,0.317029469948265,-0.940543496235211));
#128166=DIRECTION('ref_axis',(0.337768907871411,0.877800794500173,0.339673269555054));
#128167=DIRECTION('center_axis',(0.0202557067868174,-0.733929474493211,
-0.678923583927297));
#128168=DIRECTION('ref_axis',(-0.254076236620299,-0.660548321408542,0.706485089063614));
#128169=DIRECTION('center_axis',(0.506870460541712,0.531173327095353,0.678923583927297));
#128170=DIRECTION('ref_axis',(0.254076236620306,0.66054832140854,-0.706485089063614));
#128171=DIRECTION('center_axis',(0.739960301410276,-0.672211613168882,-0.0242960790602786));
#128172=DIRECTION('ref_axis',(0.476218817981084,0.498021215428875,0.724700287279815));
#128173=DIRECTION('center_axis',(1.47962606647001E-32,7.96822729466869E-32,
-1.));
#128174=DIRECTION('ref_axis',(0.93333652103737,-0.35900269984759,-1.47962606646999E-32));
#128175=DIRECTION('center_axis',(1.97546871357812E-35,-4.11635425026281E-32,
1.));
#128176=DIRECTION('ref_axis',(-0.808547669093927,-0.588430681391426,-2.42059187570691E-32));
#128177=DIRECTION('center_axis',(-1.47962606647001E-32,-7.96822729466869E-32,
1.));
#128178=DIRECTION('ref_axis',(-0.933336521037369,0.359002699847592,1.47962606647E-32));
#128179=DIRECTION('center_axis',(-0.02018063909783,0.731209530424043,0.681854357192688));
#128180=DIRECTION('ref_axis',(0.255091277271195,0.663187227773891,-0.703641344136153));
#128181=DIRECTION('center_axis',(-0.0201983973980688,0.731852970818359,
0.681163162426516));
#128182=DIRECTION('ref_axis',(0.254851977616513,0.662565095663826,-0.704313824593084));
#128183=DIRECTION('center_axis',(-0.505436374010841,-0.52967048056304,-0.681163162426516));
#128184=DIRECTION('ref_axis',(-0.254851977616511,-0.662565095663829,0.704313824593082));
#128185=DIRECTION('center_axis',(-0.504991997622738,-0.529204797705336,
-0.681854357192686));
#128186=DIRECTION('ref_axis',(-0.255091277271183,-0.663187227773893,0.703641344136155));
#128187=DIRECTION('center_axis',(-1.47962606647001E-32,-7.96822729466869E-32,
1.));
#128188=DIRECTION('ref_axis',(-0.933336521037369,0.359002699847592,1.47962606647E-32));
#128189=DIRECTION('center_axis',(1.97546871357812E-35,-4.11635425026281E-32,
1.));
#128190=DIRECTION('ref_axis',(0.205800343803877,-0.978594000845195,-4.02864612680124E-32));
#128191=DIRECTION('center_axis',(-1.47962606647001E-32,-7.96822729466869E-32,
1.));
#128192=DIRECTION('ref_axis',(0.933336521037371,-0.359002699847589,-1.47962606646997E-32));
#128193=DIRECTION('center_axis',(1.47962606647001E-32,7.96822729466869E-32,
-1.));
#128194=DIRECTION('ref_axis',(-0.933336521037369,0.359002699847593,1.47962606647001E-32));
#128195=DIRECTION('center_axis',(-0.77732714608976,0.629096580782275,4.178003810366E-32));
#128196=DIRECTION('ref_axis',(-0.629096580782275,-0.77732714608976,-7.00819850474328E-32));
#128197=DIRECTION('',(-1.16115793851351E-32,-8.07603085451918E-32,1.));
#128198=DIRECTION('',(-0.460377754339743,-0.568854031060101,-0.681511125848851));
#128199=DIRECTION('center_axis',(0.777324121702722,-0.629100317766994,2.13514018757423E-6));
#128200=DIRECTION('ref_axis',(0.623776052559492,0.7707458344779,0.129824092094895));
#128201=DIRECTION('',(-1.23540546490668E-32,5.11477840503477E-32,-1.));
#128202=DIRECTION('center_axis',(0.994044497506239,0.108974937382723,2.03432761618721E-32));
#128203=DIRECTION('ref_axis',(-0.108974937382723,0.994044497506239,7.90139691898444E-32));
#128204=DIRECTION('center_axis',(-0.99404449750624,-0.108974937382713,-6.7166702352874E-15));
#128205=DIRECTION('ref_axis',(0.108157446196492,-0.986587529556189,0.122257978702698));
#128206=DIRECTION('',(-0.0797487039099568,0.727449468739176,0.681511125848855));
#128207=DIRECTION('',(-1.16115793851351E-32,-8.07603085451918E-32,1.));
#128208=DIRECTION('',(-1.57630142331307E-32,-4.28918677227618E-32,1.));
#128209=DIRECTION('center_axis',(-1.16115793851351E-32,-8.07603085451918E-32,
1.));
#128210=DIRECTION('ref_axis',(-0.959492973614498,0.281732556841428,1.16115793851355E-32));
#128211=DIRECTION('center_axis',(0.0956970194023197,0.325914117778219,-0.940543496235212));
#128212=DIRECTION('ref_axis',(0.265096095837727,0.902411286455005,0.33967326955505));
#128213=DIRECTION('center_axis',(0.0956970194023197,0.325914117778219,-0.940543496235212));
#128214=DIRECTION('ref_axis',(0.265096095837727,0.902411286455005,0.33967326955505));
#128215=DIRECTION('center_axis',(0.080010373233477,-0.729836356563822,-0.678923583927297));
#128216=DIRECTION('ref_axis',(-0.199389998476538,-0.67905997337371,0.706485089063613));
#128217=DIRECTION('center_axis',(0.461888333567277,0.570720539758084,0.678923583927297));
#128218=DIRECTION('ref_axis',(0.199389998476547,0.679059973373706,-0.706485089063615));
#128219=DIRECTION('center_axis',(0.792289631536735,-0.609661250450763,-0.0242960790704409));
#128220=DIRECTION('ref_axis',(0.434040406814599,0.535179691247669,0.724701057904752));
#128221=DIRECTION('center_axis',(1.16115793851351E-32,8.07603085451918E-32,
-1.));
#128222=DIRECTION('ref_axis',(0.959492973614501,-0.281732556841418,-1.16115793851346E-32));
#128223=DIRECTION('center_axis',(1.5502776215132E-35,-4.11621032027636E-32,
1.));
#128224=DIRECTION('ref_axis',(-0.757894730168191,-0.65237686806269,-2.68414544978957E-32));
#128225=DIRECTION('center_axis',(-1.16115793851351E-32,-8.07603085451918E-32,
1.));
#128226=DIRECTION('ref_axis',(-0.959492973614501,0.281732556841418,1.16115793851346E-32));
#128227=DIRECTION('center_axis',(-0.0797138546336661,0.727131581597711,
0.681854357192688));
#128228=DIRECTION('ref_axis',(0.200186566296209,0.681772834232049,-0.703641344136153));
#128229=DIRECTION('center_axis',(-0.0797840002101718,0.727771433530866,
0.681163162426516));
#128230=DIRECTION('ref_axis',(0.199998772433955,0.681133267071852,-0.704313824593083));
#128231=DIRECTION('center_axis',(-0.460581514785163,-0.569105802457955,
-0.681163162426516));
#128232=DIRECTION('ref_axis',(-0.19999877243396,-0.681133267071849,0.704313824593084));
#128233=DIRECTION('center_axis',(-0.460176574498925,-0.568605448320524,
-0.681854357192686));
#128234=DIRECTION('ref_axis',(-0.200186566296196,-0.681772834232052,0.703641344136154));
#128235=DIRECTION('center_axis',(-1.16115793851351E-32,-8.07603085451918E-32,
1.));
#128236=DIRECTION('ref_axis',(-0.959492973614501,0.281732556841418,1.16115793851346E-32));
#128237=DIRECTION('center_axis',(1.5502776215132E-35,-4.11621032027636E-32,
1.));
#128238=DIRECTION('ref_axis',(0.284880056029549,-0.958563171458512,-3.94608926217004E-32));
#128239=DIRECTION('center_axis',(-1.16115793851351E-32,-8.07603085451918E-32,
1.));
#128240=DIRECTION('ref_axis',(0.959492973614495,-0.281732556841437,-1.16115793851362E-32));
#128241=DIRECTION('center_axis',(1.16115793851351E-32,8.07603085451918E-32,
-1.));
#128242=DIRECTION('ref_axis',(-0.959492973614499,0.281732556841424,1.16115793851351E-32));
#128243=DIRECTION('center_axis',(-0.826017865717592,0.563643935047077,3.90824138019391E-32));
#128244=DIRECTION('ref_axis',(-0.563643935047077,-0.826017865717592,-7.2088768227256E-32));
#128245=DIRECTION('',(-8.34962496053772E-33,-8.15751759797513E-32,1.));
#128246=DIRECTION('',(-0.412479000826099,-0.60448627711615,-0.681511125848844));
#128247=DIRECTION('center_axis',(0.826015155992845,-0.563647906112989,2.13514022960205E-6));
#128248=DIRECTION('ref_axis',(0.558877548446757,0.819024780447331,0.129824091968115));
#128249=DIRECTION('',(-1.31225697478464E-32,5.01077630574236E-32,-1.));
#128250=DIRECTION('center_axis',(0.981854427373034,0.189636187074016,2.36677215671002E-32));
#128251=DIRECTION('ref_axis',(-0.189636187074016,0.981854427373034,7.85115566584388E-32));
#128252=DIRECTION('center_axis',(-0.981854427373031,-0.189636187074032,
7.88699913992152E-15));
#128253=DIRECTION('ref_axis',(0.188213603907529,-0.974488904990992,0.122257978690955));
#128254=DIRECTION('',(-0.138777231690123,0.718528680922799,0.681511125848851));
#128255=DIRECTION('',(-8.34962496053772E-33,-8.15751759797513E-32,1.));
#128256=DIRECTION('',(-1.55738757320265E-32,-4.41711197503839E-32,1.));
#128257=DIRECTION('center_axis',(-8.34962496053772E-33,-8.15751759797513E-32,
1.));
#128258=DIRECTION('ref_axis',(-0.979264158757423,0.202587530152072,8.34962496053749E-33));
#128259=DIRECTION('center_axis',(0.0688135692266905,0.332629860926233,-0.940543496235277));
#128260=DIRECTION('ref_axis',(0.190659113023962,0.921016380185944,0.339673269554872));
#128261=DIRECTION('center_axis',(0.0688135692266905,0.332629860926233,-0.940543496235277));
#128262=DIRECTION('ref_axis',(0.190659113023962,0.921016380185944,0.339673269554872));
#128263=DIRECTION('center_axis',(0.13923258384705,-0.720886298096023,-0.678923583927297));
#128264=DIRECTION('ref_axis',(-0.143376852789944,-0.693052593253087,0.706485089063614));
#128265=DIRECTION('center_axis',(0.413832415939163,0.606469701390985,0.678923583927297));
#128266=DIRECTION('ref_axis',(0.143376852789952,0.693052593253084,-0.706485089063615));
#128267=DIRECTION('center_axis',(0.839346404882638,-0.543053692697053,-0.0242960790804773));
#128268=DIRECTION('ref_axis',(0.388973769514727,0.568776775077145,0.724701584628009));
#128269=DIRECTION('center_axis',(8.34962496053772E-33,8.15751759797513E-32,
-1.));
#128270=DIRECTION('ref_axis',(0.979264158757421,-0.202587530152081,-8.34962496053827E-33));
#128271=DIRECTION('center_axis',(1.11476968765511E-35,-4.11610152622635E-32,
1.));
#128272=DIRECTION('ref_axis',(-0.702198126856995,-0.711981594311628,-2.92980573780462E-32));
#128273=DIRECTION('center_axis',(-8.34962496053772E-33,-8.15751759797513E-32,
1.));
#128274=DIRECTION('ref_axis',(-0.979264158757421,0.202587530152081,8.34962496053823E-33));
#128275=DIRECTION('center_axis',(-0.138716587618775,0.718214692064113,0.681854357192688));
#128276=DIRECTION('ref_axis',(0.143949646750982,0.695821354962993,-0.703641344136153));
#128277=DIRECTION('center_axis',(-0.138838653664309,0.71884669742706,0.681163162426516));
#128278=DIRECTION('ref_axis',(0.14381460841832,0.695168608966593,-0.704313824593084));
#128279=DIRECTION('center_axis',(-0.412661561569192,-0.60475381913336,-0.681163162426516));
#128280=DIRECTION('ref_axis',(-0.143814608418327,-0.695168608966591,0.704313824593084));
#128281=DIRECTION('center_axis',(-0.412298752195612,-0.604222123490434,
-0.681854357192686));
#128282=DIRECTION('ref_axis',(-0.143949646750973,-0.695821354962993,0.703641344136155));
#128283=DIRECTION('center_axis',(-8.34962496053772E-33,-8.15751759797513E-32,
1.));
#128284=DIRECTION('ref_axis',(-0.979264158757421,0.202587530152081,8.34962496053827E-33));
#128285=DIRECTION('center_axis',(1.11476968765511E-35,-4.11610152622635E-32,
1.));
#128286=DIRECTION('ref_axis',(0.362063938484242,-0.932153262317565,-3.83724108360582E-32));
#128287=DIRECTION('center_axis',(-8.34962496053772E-33,-8.15751759797513E-32,
1.));
#128288=DIRECTION('ref_axis',(0.979264158757421,-0.202587530152081,-8.34962496053827E-33));
#128289=DIRECTION('center_axis',(8.34962496053772E-33,8.15751759797513E-32,
-1.));
#128290=DIRECTION('ref_axis',(-0.979264158757422,0.202587530152075,8.34962496053772E-33));
#128291=DIRECTION('center_axis',(-0.869211572732429,0.494440331918844,3.62301941633223E-32));
#128292=DIRECTION('ref_axis',(-0.494440331918845,-0.869211572732429,-7.38689925774838E-32));
#128293=DIRECTION('',(-5.03210515941913E-33,-8.2121452442032E-32,1.));
#128294=DIRECTION('',(-0.361835267616208,-0.636095766731185,-0.681511125848854));
#128295=DIRECTION('center_axis',(0.869209195702802,-0.494444510639091,2.13514022868713E-6));
#128296=DIRECTION('ref_axis',(0.490259806413637,0.861853251561129,0.129824092481988));
#128297=DIRECTION('',(-1.38037563100257E-32,4.90085615334611E-32,-1.));
#128298=DIRECTION('center_axis',(0.963130278020239,0.269035439228099,2.694015386901E-32));
#128299=DIRECTION('ref_axis',(-0.269035439228099,0.963130278020239,7.77398427001138E-32));
#128300=DIRECTION('center_axis',(-0.963130278020243,-0.269035439228087,
-8.44672165952822E-15));
#128301=DIRECTION('ref_axis',(0.267017231139236,-0.955905217547563,0.122257978635677));
#128302=DIRECTION('',(-0.196882219890024,0.704826203283764,0.681511125848853));
#128303=DIRECTION('',(-5.03210515941913E-33,-8.2121452442032E-32,1.));
#128304=DIRECTION('',(-1.52810956574343E-32,-4.54306986286987E-32,1.));
#128305=DIRECTION('center_axis',(-5.03210515941913E-33,-8.2121452442032E-32,
1.));
#128306=DIRECTION('ref_axis',(-0.992518502491028,0.122094316874159,5.03210515941961E-33));
#128307=DIRECTION('center_axis',(0.0414721761013757,0.337132007230186,-0.940543496235215));
#128308=DIRECTION('ref_axis',(0.114953325269262,0.933492261863657,0.339673269555043));
#128309=DIRECTION('center_axis',(0.0414721761013757,0.337132007230186,-0.940543496235215));
#128310=DIRECTION('ref_axis',(0.114953325269262,0.933492261863657,0.339673269555043));
#128311=DIRECTION('center_axis',(0.19752822458688,-0.707138860252263,-0.678923583927297));
#128312=DIRECTION('ref_axis',(-0.0864095578035487,-0.702433062469993,0.706485089063614));
#128313=DIRECTION('center_axis',(0.363022511860516,0.638182907221586,0.678923583927297));
#128314=DIRECTION('ref_axis',(0.0864095578035559,0.702433062469992,-0.706485089063614));
#128315=DIRECTION('center_axis',(0.880817466376868,-0.472832202231631,-0.0242960790709246));
#128316=DIRECTION('ref_axis',(0.341319657785829,0.598590676133594,0.724700002521658));
#128317=DIRECTION('center_axis',(5.03210515941913E-33,8.2121452442032E-32,
-1.));
#128318=DIRECTION('ref_axis',(0.992518502491028,-0.122094316874158,-5.03210515941954E-33));
#128319=DIRECTION('center_axis',(6.71843145449713E-36,-4.11602859211924E-32,
1.));
#128320=DIRECTION('ref_axis',(-0.641828510866114,-0.766848200519103,-3.15593791106624E-32));
#128321=DIRECTION('center_axis',(-5.03210515941913E-33,-8.2121452442032E-32,
1.));
#128322=DIRECTION('ref_axis',(-0.992518502491028,0.122094316874158,5.03210515941954E-33));
#128323=DIRECTION('center_axis',(-0.196796184599907,0.704518202251912,0.681854357192688));
#128324=DIRECTION('ref_axis',(0.0867547660566476,0.7052392993791,-0.703641344136153));
#128325=DIRECTION('center_axis',(-0.196969358785076,0.705138155153233,0.681163162426516));
#128326=DIRECTION('ref_axis',(0.0866733819114015,0.704577718463409,-0.704313824593084));
#128327=DIRECTION('center_axis',(-0.361995413745342,-0.636377298919789,
-0.681163162426516));
#128328=DIRECTION('ref_axis',(-0.086673381911405,-0.704577718463409,0.704313824593084));
#128329=DIRECTION('center_axis',(-0.361677149720944,-0.635817800118149,
-0.681854357192686));
#128330=DIRECTION('ref_axis',(-0.0867547660566364,-0.7052392993791,0.703641344136155));
#128331=DIRECTION('center_axis',(-5.03210515941913E-33,-8.2121452442032E-32,
1.));
#128332=DIRECTION('ref_axis',(-0.992518502491028,0.122094316874158,5.03210515941954E-33));
#128333=DIRECTION('center_axis',(6.71843145449713E-36,-4.11602859211924E-32,
1.));
#128334=DIRECTION('ref_axis',(0.436838345164685,-0.899540027010349,-3.70282595777818E-32));
#128335=DIRECTION('center_axis',(-5.03210515941913E-33,-8.2121452442032E-32,
1.));
#128336=DIRECTION('ref_axis',(0.992518502491028,-0.122094316874158,-5.03210515941954E-33));
#128337=DIRECTION('center_axis',(5.03210515941913E-33,8.2121452442032E-32,
-1.));
#128338=DIRECTION('ref_axis',(-0.992518502491028,0.122094316874153,5.03210515941913E-33));
#128339=DIRECTION('center_axis',(-0.906620820140547,0.421946309958604,3.32423602389212E-32));
#128340=DIRECTION('ref_axis',(-0.421946309958604,-0.906620820140547,-7.54108109987818E-32));
#128341=DIRECTION('',(-1.68109752870352E-33,-8.23955025523068E-32,1.));
#128342=DIRECTION('',(-0.308783580398942,-0.663472143967058,-0.681511125848849));
#128343=DIRECTION('center_axis',(0.906618791624814,-0.421950668524419,2.13514018813373E-6));
#128344=DIRECTION('ref_axis',(0.418379466321284,0.898946231596081,0.12982409198574));
#128345=DIRECTION('',(-1.43930811514213E-32,4.78574944832467E-32,-1.));
#128346=DIRECTION('center_axis',(0.937996655572531,0.346644304921843,3.01387955705455E-32));
#128347=DIRECTION('ref_axis',(-0.346644304921843,0.937996655572531,7.67039629439384E-32));
#128348=DIRECTION('center_axis',(-0.937996655572521,-0.346644304921869,
1.02276569491927E-14));
#128349=DIRECTION('ref_axis',(0.3440439027509,-0.930960138587007,0.122257978643482));
#128350=DIRECTION('',(-0.253676989399839,0.686433223550012,0.681511125848854));
#128351=DIRECTION('',(-1.68109752870352E-33,-8.23955025523068E-32,1.));
#128352=DIRECTION('',(-1.48866224124453E-32,-4.66622220680871E-32,1.));
#128353=DIRECTION('center_axis',(-1.68109752870351E-33,-8.23955025523068E-32,
1.));
#128354=DIRECTION('ref_axis',(-0.999167799344583,0.040788586061579,1.68109752870351E-33));
#128355=DIRECTION('center_axis',(0.0138547924865009,0.339390595648716,-0.940543496235217));
#128356=DIRECTION('ref_axis',(0.038482542101349,0.939755906554042,0.339673269555038));
#128357=DIRECTION('center_axis',(0.0138547924865009,0.339390595648716,-0.940543496235217));
#128358=DIRECTION('ref_axis',(0.038482542101349,0.939755906554042,0.339673269555038));
#128359=DIRECTION('center_axis',(0.254509347581947,-0.688685529963223,-0.678923583927297));
#128360=DIRECTION('ref_axis',(-0.0288672214665463,-0.707138955549458,0.706485089063614));
#128361=DIRECTION('center_axis',(0.309796752859936,0.665649111097397,0.678923583927297));
#128362=DIRECTION('ref_axis',(0.028867221466551,0.707138955549458,-0.706485089063614));
#128363=DIRECTION('center_axis',(0.916426832965552,-0.399464091455001,-0.0242960790819855));
#128364=DIRECTION('ref_axis',(0.291392765240331,0.624418455476463,0.724701213484552));
#128365=DIRECTION('center_axis',(1.68109752870351E-33,8.23955025523068E-32,
-1.));
#128366=DIRECTION('ref_axis',(0.999167799344583,-0.0407885860615856,-1.68109752870405E-33));
#128367=DIRECTION('center_axis',(2.24445597957705E-36,-4.11599200331947E-32,
1.));
#128368=DIRECTION('ref_axis',(-0.577187632029668,-0.816611558473173,-3.36103709727063E-32));
#128369=DIRECTION('center_axis',(-1.68109752870351E-33,-8.23955025523068E-32,
1.));
#128370=DIRECTION('ref_axis',(-0.999167799344583,0.0407885860615856,1.68109752870405E-33));
#128371=DIRECTION('center_axis',(-0.253566135441612,0.686133260041045,0.681854357192688));
#128372=DIRECTION('ref_axis',(0.0289825467077354,0.709963992614134,-0.703641344136153));
#128373=DIRECTION('center_axis',(-0.253789265320785,0.686737034796468,0.681163162426516));
#128374=DIRECTION('ref_axis',(0.0289553583479641,0.709297979490992,-0.704313824593084));
#128375=DIRECTION('center_axis',(-0.308920246168057,-0.663765792776771,
-0.681163162426516));
#128376=DIRECTION('ref_axis',(-0.0289553583479713,-0.709297979490991,0.704313824593084));
#128377=DIRECTION('center_axis',(-0.308648645487412,-0.66318221418863,-0.681854357192686));
#128378=DIRECTION('ref_axis',(-0.0289825467077237,-0.709963992614133,0.703641344136154));
#128379=DIRECTION('center_axis',(-1.68109752870351E-33,-8.23955025523068E-32,
1.));
#128380=DIRECTION('ref_axis',(-0.999167799344583,0.0407885860615856,1.68109752870405E-33));
#128381=DIRECTION('center_axis',(2.24445597957705E-36,-4.11599200331947E-32,
1.));
#128382=DIRECTION('ref_axis',(0.508705664731289,-0.860940501237047,-3.54373839517265E-32));
#128383=DIRECTION('center_axis',(-1.68109752870351E-33,-8.23955025523068E-32,
1.));
#128384=DIRECTION('ref_axis',(0.999167799344584,-0.0407885860615658,-1.68109752870242E-33));
#128385=DIRECTION('center_axis',(1.68109752870351E-33,8.23955025523068E-32,
-1.));
#128386=DIRECTION('ref_axis',(-0.999167799344583,0.0407885860615791,1.68109752870351E-33));
#128387=DIRECTION('center_axis',(-0.937996655572535,0.34664430492183,3.01387955705449E-32));
#128388=DIRECTION('ref_axis',(-0.34664430492183,-0.937996655572535,-7.67039629439386E-32));
#128389=DIRECTION('',(1.68109752870407E-33,-8.23955025523068E-32,1.));
#128390=DIRECTION('',(-0.25367698939983,-0.686433223550014,-0.681511125848856));
#128391=DIRECTION('center_axis',(0.937994989070099,-0.346648814327739,2.13514018660772E-6));
#128392=DIRECTION('ref_axis',(0.343714879873078,0.930056872710369,0.129824092055537));
#128393=DIRECTION('',(-1.48866224124453E-32,4.66622220680869E-32,-1.));
#128394=DIRECTION('center_axis',(0.906620820140541,0.421946309958617,3.32423602389217E-32));
#128395=DIRECTION('ref_axis',(-0.421946309958617,0.906620820140541,7.54108109987816E-32));
#128396=DIRECTION('center_axis',(-0.906620820140535,-0.42194630995863,4.98661881104643E-15));
#128397=DIRECTION('ref_axis',(0.418781018951358,-0.89981967349873,0.12225797867911));
#128398=DIRECTION('',(-0.30878358039895,0.663472143967056,0.681511125848847));
#128399=DIRECTION('',(1.68109752870407E-33,-8.23955025523068E-32,1.));
#128400=DIRECTION('',(-1.43930811514212E-32,-4.78574944832469E-32,1.));
#128401=DIRECTION('center_axis',(1.68109752870407E-33,-8.23955025523068E-32,
1.));
#128402=DIRECTION('ref_axis',(-0.999167799344583,-0.0407885860615916,-1.68109752870399E-33));
#128403=DIRECTION('center_axis',(-0.0138547924865081,0.33939059564882,-0.940543496235179));
#128404=DIRECTION('ref_axis',(-0.0382443360354119,0.939765630735095,0.339673269555142));
#128405=DIRECTION('center_axis',(-0.0138547924865081,0.33939059564882,-0.940543496235179));
#128406=DIRECTION('ref_axis',(-0.0382443360354119,0.939765630735095,0.339673269555142));
#128407=DIRECTION('center_axis',(0.309796752859944,-0.665649111097393,-0.678923583927297));
#128408=DIRECTION('ref_axis',(0.0288672214665601,-0.707138955549458,0.706485089063614));
#128409=DIRECTION('center_axis',(0.254509347581939,0.688685529963227,0.678923583927297));
#128410=DIRECTION('ref_axis',(-0.0288672214665556,0.707138955549458,-0.706485089063614));
#128411=DIRECTION('center_axis',(0.945937530174914,-0.323437613069393,-0.0242960790778483));
#128412=DIRECTION('ref_axis',(0.23952750141689,0.646092673476846,0.724700512863433));
#128413=DIRECTION('center_axis',(-1.68109752870407E-33,8.23955025523068E-32,
-1.));
#128414=DIRECTION('ref_axis',(0.999167799344583,0.0407885860615856,1.68109752870349E-33));
#128415=DIRECTION('center_axis',(-2.24445597957774E-36,-4.11599200331947E-32,
1.));
#128416=DIRECTION('ref_axis',(-0.508705664731306,-0.860940501237037,-3.5437383951726E-32));
#128417=DIRECTION('center_axis',(1.68109752870407E-33,-8.23955025523068E-32,
1.));
#128418=DIRECTION('ref_axis',(-0.999167799344583,-0.0407885860615856,-1.68109752870349E-33));
#128419=DIRECTION('center_axis',(-0.30864864548742,0.663182214188625,0.681854357192688));
#128420=DIRECTION('ref_axis',(-0.028982546707734,0.709963992614134,-0.703641344136153));
#128421=DIRECTION('center_axis',(-0.308920246168066,0.663765792776767,0.681163162426516));
#128422=DIRECTION('ref_axis',(-0.028955358347981,0.709297979490991,-0.704313824593084));
#128423=DIRECTION('center_axis',(-0.253789265320776,-0.686737034796471,
-0.681163162426516));
#128424=DIRECTION('ref_axis',(0.0289553583479736,-0.709297979490991,0.704313824593084));
#128425=DIRECTION('center_axis',(-0.253566135441603,-0.68613326004105,-0.681854357192686));
#128426=DIRECTION('ref_axis',(0.0289825467077455,-0.709963992614132,0.703641344136154));
#128427=DIRECTION('center_axis',(1.68109752870407E-33,-8.23955025523068E-32,
1.));
#128428=DIRECTION('ref_axis',(-0.999167799344583,-0.0407885860615856,-1.68109752870349E-33));
#128429=DIRECTION('center_axis',(-2.24445597957774E-36,-4.11599200331947E-32,
1.));
#128430=DIRECTION('ref_axis',(0.577187632029642,-0.816611558473192,-3.3610370972707E-32));
#128431=DIRECTION('center_axis',(1.68109752870407E-33,-8.23955025523068E-32,
1.));
#128432=DIRECTION('ref_axis',(0.999167799344582,0.0407885860616053,1.68109752870512E-33));
#128433=DIRECTION('center_axis',(-1.68109752870407E-33,8.23955025523068E-32,
-1.));
#128434=DIRECTION('ref_axis',(-0.999167799344583,-0.0407885860615926,-1.68109752870407E-33));
#128435=DIRECTION('center_axis',(-0.963130278020243,0.269035439228086,2.69401538690095E-32));
#128436=DIRECTION('ref_axis',(-0.269035439228086,-0.963130278020243,-7.7739842700114E-32));
#128437=DIRECTION('',(5.03210515941968E-33,-8.2121452442032E-32,1.));
#128438=DIRECTION('',(-0.196882219890014,-0.704826203283771,-0.681511125848848));
#128439=DIRECTION('center_axis',(0.963128984621398,-0.269040069464747,2.13514019551156E-6));
#128440=DIRECTION('ref_axis',(0.266762927617273,0.95497813881199,0.129824091909976));
#128441=DIRECTION('',(-1.52810956574344E-32,4.54306986286985E-32,-1.));
#128442=DIRECTION('center_axis',(0.869211572732422,0.494440331918856,3.62301941633227E-32));
#128443=DIRECTION('ref_axis',(-0.494440331918856,0.869211572732422,7.38689925774835E-32));
#128444=DIRECTION('center_axis',(-0.869211572732398,-0.4944403319189,1.68425594536402E-14));
#128445=DIRECTION('ref_axis',(0.490731216567359,-0.86269105694913,0.122257978661159));
#128446=DIRECTION('',(-0.361835267616211,0.636095766731196,0.681511125848842));
#128447=DIRECTION('',(5.03210515941968E-33,-8.2121452442032E-32,1.));
#128448=DIRECTION('',(-1.38037563100256E-32,-4.90085615334613E-32,1.));
#128449=DIRECTION('center_axis',(5.03210515941968E-33,-8.2121452442032E-32,
1.));
#128450=DIRECTION('ref_axis',(-0.992518502491026,-0.122094316874172,-5.0321051594201E-33));
#128451=DIRECTION('center_axis',(-0.0414721761013823,0.337132007230191,
-0.940543496235213));
#128452=DIRECTION('ref_axis',(-0.114716704425453,0.933521369694099,0.339673269555049));
#128453=DIRECTION('center_axis',(-0.0414721761013823,0.337132007230191,
-0.940543496235213));
#128454=DIRECTION('ref_axis',(-0.114716704425453,0.933521369694099,0.339673269555049));
#128455=DIRECTION('center_axis',(0.363022511860524,-0.638182907221582,-0.678923583927297));
#128456=DIRECTION('ref_axis',(0.0864095578035654,-0.70243306246999,0.706485089063614));
#128457=DIRECTION('center_axis',(0.197528224586871,0.707138860252265,0.678923583927297));
#128458=DIRECTION('ref_axis',(-0.0864095578035587,0.702433062469992,-0.706485089063614));
#128459=DIRECTION('center_axis',(0.969153169190729,-0.245258710730287,-0.0242960790763212));
#128460=DIRECTION('ref_axis',(0.186067957636303,0.663466634656043,0.724700448350379));
#128461=DIRECTION('center_axis',(-5.03210515941968E-33,8.2121452442032E-32,
-1.));
#128462=DIRECTION('ref_axis',(0.992518502491028,0.122094316874159,5.03210515941902E-33));
#128463=DIRECTION('center_axis',(-6.7184314544985E-36,-4.11602859211924E-32,
1.));
#128464=DIRECTION('ref_axis',(-0.436838345164698,-0.899540027010343,-3.70282595777815E-32));
#128465=DIRECTION('center_axis',(5.03210515941968E-33,-8.2121452442032E-32,
1.));
#128466=DIRECTION('ref_axis',(-0.992518502491028,-0.122094316874159,-5.03210515941902E-33));
#128467=DIRECTION('center_axis',(-0.361677149720952,0.635817800118143,0.681854357192688));
#128468=DIRECTION('ref_axis',(-0.0867547660566466,0.7052392993791,-0.703641344136153));
#128469=DIRECTION('center_axis',(-0.361995413745351,0.636377298919785,0.681163162426516));
#128470=DIRECTION('ref_axis',(-0.0866733819114143,0.704577718463408,-0.704313824593084));
#128471=DIRECTION('center_axis',(-0.196969358785067,-0.705138155153235,
-0.681163162426516));
#128472=DIRECTION('ref_axis',(0.0866733819114115,-0.704577718463408,0.704313824593084));
#128473=DIRECTION('center_axis',(-0.196796184599898,-0.704518202251916,
-0.681854357192686));
#128474=DIRECTION('ref_axis',(0.0867547660566579,-0.705239299379098,0.703641344136154));
#128475=DIRECTION('center_axis',(5.03210515941968E-33,-8.2121452442032E-32,
1.));
#128476=DIRECTION('ref_axis',(-0.992518502491028,-0.122094316874159,-5.032105159419E-33));
#128477=DIRECTION('center_axis',(-6.7184314544985E-36,-4.11602859211924E-32,
1.));
#128478=DIRECTION('ref_axis',(0.641828510866092,-0.766848200519122,-3.15593791106632E-32));
#128479=DIRECTION('center_axis',(5.03210515941968E-33,-8.2121452442032E-32,
1.));
#128480=DIRECTION('ref_axis',(0.992518502491028,0.122094316874158,5.03210515941899E-33));
#128481=DIRECTION('center_axis',(-5.03210515941968E-33,8.2121452442032E-32,
-1.));
#128482=DIRECTION('ref_axis',(-0.992518502491027,-0.122094316874167,-5.03210515941968E-33));
#128483=DIRECTION('center_axis',(-0.981854427373037,0.189636187074003,2.36677215670997E-32));
#128484=DIRECTION('ref_axis',(-0.189636187074003,-0.981854427373037,-7.85115566584389E-32));
#128485=DIRECTION('',(8.34962496053827E-33,-8.15751759797512E-32,1.));
#128486=DIRECTION('',(-0.13877723169011,-0.718528680922806,-0.681511125848846));
#128487=DIRECTION('center_axis',(0.981853515685139,-0.189640907327967,2.13514020548389E-6));
#128488=DIRECTION('ref_axis',(0.18803571207698,0.973544182904009,0.129824092207375));
#128489=DIRECTION('',(-1.55738757320266E-32,4.41711197503837E-32,-1.));
#128490=DIRECTION('center_axis',(0.826017865717585,0.563643935047088,3.90824138019396E-32));
#128491=DIRECTION('ref_axis',(-0.563643935047088,0.826017865717585,7.20887682272556E-32));
#128492=DIRECTION('center_axis',(-0.82601786571759,-0.56364393504708,2.03535461675383E-16));
#128493=DIRECTION('ref_axis',(0.559415678899174,-0.819821373744855,0.122257978687999));
#128494=DIRECTION('',(-0.412479000826111,0.604486277116134,0.681511125848852));
#128495=DIRECTION('',(8.34962496053827E-33,-8.15751759797512E-32,1.));
#128496=DIRECTION('',(-1.31225697478463E-32,-5.01077630574238E-32,1.));
#128497=DIRECTION('center_axis',(8.34962496053827E-33,-8.15751759797512E-32,
1.));
#128498=DIRECTION('ref_axis',(-0.97926415875742,-0.202587530152084,-8.34962496053794E-33));
#128499=DIRECTION('center_axis',(-0.0688135692267322,0.332629860926406,
-0.940543496235213));
#128500=DIRECTION('ref_axis',(-0.190425652074282,0.921064677957996,0.339673269555049));
#128501=DIRECTION('center_axis',(-0.0688135692267322,0.332629860926406,
-0.940543496235213));
#128502=DIRECTION('ref_axis',(-0.190425652074282,0.921064677957996,0.339673269555049));
#128503=DIRECTION('center_axis',(0.41383241593917,-0.606469701390979,-0.678923583927297));
#128504=DIRECTION('ref_axis',(0.143376852789961,-0.693052593253083,0.706485089063614));
#128505=DIRECTION('center_axis',(0.139232583847041,0.720886298096025,0.678923583927297));
#128506=DIRECTION('ref_axis',(-0.143376852789953,0.693052593253085,-0.706485089063614));
#128507=DIRECTION('center_axis',(0.985919253765162,-0.165447652133925,-0.024296079077036));
#128508=DIRECTION('ref_axis',(0.131370100254809,0.676424981841651,0.724700724919993));
#128509=DIRECTION('center_axis',(-8.34962496053827E-33,8.15751759797512E-32,
-1.));
#128510=DIRECTION('ref_axis',(0.979264158757421,0.202587530152081,8.34962496053771E-33));
#128511=DIRECTION('center_axis',(-1.11476968765511E-35,-4.11610152622635E-32,
1.));
#128512=DIRECTION('ref_axis',(-0.362063938484265,-0.932153262317556,-3.83724108360578E-32));
#128513=DIRECTION('center_axis',(8.34962496053827E-33,-8.15751759797512E-32,
1.));
#128514=DIRECTION('ref_axis',(-0.979264158757421,-0.202587530152081,-8.34962496053772E-33));
#128515=DIRECTION('center_axis',(-0.41229875219562,0.604222123490427,0.681854357192688));
#128516=DIRECTION('ref_axis',(-0.143949646750983,0.695821354962992,-0.703641344136154));
#128517=DIRECTION('center_axis',(-0.4126615615692,0.604753819133354,0.681163162426516));
#128518=DIRECTION('ref_axis',(-0.143814608418336,0.695168608966589,-0.704313824593084));
#128519=DIRECTION('center_axis',(-0.1388386536643,-0.718846697427061,-0.681163162426516));
#128520=DIRECTION('ref_axis',(0.14381460841833,-0.695168608966591,0.704313824593083));
#128521=DIRECTION('center_axis',(-0.138716587618766,-0.718214692064117,
-0.681854357192686));
#128522=DIRECTION('ref_axis',(0.143949646750992,-0.695821354962989,0.703641344136154));
#128523=DIRECTION('center_axis',(8.34962496053827E-33,-8.15751759797512E-32,
1.));
#128524=DIRECTION('ref_axis',(-0.979264158757421,-0.202587530152082,-8.34962496053776E-33));
#128525=DIRECTION('center_axis',(-1.11476968765511E-35,-4.11610152622635E-32,
1.));
#128526=DIRECTION('ref_axis',(0.702198126856968,-0.711981594311654,-2.92980573780472E-32));
#128527=DIRECTION('center_axis',(8.34962496053827E-33,-8.15751759797512E-32,
1.));
#128528=DIRECTION('ref_axis',(0.979264158757421,0.202587530152081,8.34962496053772E-33));
#128529=DIRECTION('center_axis',(-8.34962496053827E-33,8.15751759797512E-32,
-1.));
#128530=DIRECTION('ref_axis',(-0.97926415875742,-0.202587530152088,-8.34962496053827E-33));
#128531=DIRECTION('center_axis',(-0.994044497506241,0.10897493738271,2.03432761618715E-32));
#128532=DIRECTION('ref_axis',(-0.10897493738271,-0.994044497506241,-7.90139691898445E-32));
#128533=DIRECTION('',(1.16115793851356E-32,-8.07603085451917E-32,1.));
#128534=DIRECTION('',(-0.0797487039099476,-0.727449468739181,-0.681511125848849));
#128535=DIRECTION('center_axis',(0.994043973596433,-0.108979716241397,2.13514018988893E-6));
#128536=DIRECTION('ref_axis',(0.108057149906186,0.985631451112966,0.129824092259876));
#128537=DIRECTION('',(-1.57630142331307E-32,4.28918677227616E-32,-1.));
#128538=DIRECTION('center_axis',(0.777327146089751,0.629096580782285,4.17800381036604E-32));
#128539=DIRECTION('ref_axis',(-0.629096580782285,0.777327146089751,7.00819850474325E-32));
#128540=DIRECTION('center_axis',(-0.777327146089761,-0.629096580782273,
-4.29968662789252E-15));
#128541=DIRECTION('ref_axis',(0.624377322184423,-0.771495914559359,0.122257978717246));
#128542=DIRECTION('',(-0.46037775433975,0.568854031060099,0.681511125848848));
#128543=DIRECTION('',(1.16115793851356E-32,-8.07603085451917E-32,1.));
#128544=DIRECTION('',(-1.23540546490667E-32,-5.11477840503479E-32,1.));
#128545=DIRECTION('center_axis',(1.16115793851356E-32,-8.07603085451917E-32,
1.));
#128546=DIRECTION('ref_axis',(-0.959492973614494,-0.281732556841442,-1.1611579385136E-32));
#128547=DIRECTION('center_axis',(-0.0956970194023252,0.325914117778227,
-0.940543496235209));
#128548=DIRECTION('ref_axis',(-0.264867348426973,0.90247845275499,0.339673269555059));
#128549=DIRECTION('center_axis',(-0.0956970194023252,0.325914117778227,
-0.940543496235209));
#128550=DIRECTION('ref_axis',(-0.264867348426973,0.90247845275499,0.339673269555059));
#128551=DIRECTION('center_axis',(0.461888333567284,-0.570720539758078,-0.678923583927297));
#128552=DIRECTION('ref_axis',(0.199389998476552,-0.679059973373706,0.706485089063614));
#128553=DIRECTION('center_axis',(0.0800103732334678,0.729836356563823,0.678923583927297));
#128554=DIRECTION('ref_axis',(-0.199389998476543,0.679059973373708,-0.706485089063614));
#128555=DIRECTION('center_axis',(0.996124208370885,-0.0845355667096835,
-0.0242960790776955));
#128556=DIRECTION('ref_axis',(0.0757980692347224,0.684882242683267,0.724700604634374));
#128557=DIRECTION('center_axis',(-1.16115793851356E-32,8.07603085451917E-32,
-1.));
#128558=DIRECTION('ref_axis',(0.959492973614495,0.281732556841437,1.16115793851356E-32));
#128559=DIRECTION('center_axis',(-1.55027762151293E-35,-4.11621032027636E-32,
1.));
#128560=DIRECTION('ref_axis',(-0.284880056029572,-0.958563171458506,-3.94608926217002E-32));
#128561=DIRECTION('center_axis',(1.16115793851356E-32,-8.07603085451917E-32,
1.));
#128562=DIRECTION('ref_axis',(-0.959492973614495,-0.281732556841437,-1.16115793851356E-32));
#128563=DIRECTION('center_axis',(-0.460176574498932,0.568605448320517,0.681854357192688));
#128564=DIRECTION('ref_axis',(-0.200186566296206,0.68177283423205,-0.703641344136153));
#128565=DIRECTION('center_axis',(-0.460581514785171,0.569105802457949,0.681163162426516));
#128566=DIRECTION('ref_axis',(-0.199998772433969,0.681133267071847,-0.704313824593085));
#128567=DIRECTION('center_axis',(-0.0797840002101624,-0.727771433530867,
-0.681163162426516));
#128568=DIRECTION('ref_axis',(0.199998772433964,-0.681133267071849,0.704313824593083));
#128569=DIRECTION('center_axis',(-0.0797138546336566,-0.727131581597714,
-0.681854357192686));
#128570=DIRECTION('ref_axis',(0.200186566296219,-0.681772834232045,0.703641344136154));
#128571=DIRECTION('center_axis',(1.16115793851356E-32,-8.07603085451917E-32,
1.));
#128572=DIRECTION('ref_axis',(-0.959492973614495,-0.281732556841437,-1.16115793851356E-32));
#128573=DIRECTION('center_axis',(-1.55027762151293E-35,-4.11621032027636E-32,
1.));
#128574=DIRECTION('ref_axis',(0.757894730168159,-0.652376868062727,-2.68414544978973E-32));
#128575=DIRECTION('center_axis',(1.16115793851356E-32,-8.07603085451917E-32,
1.));
#128576=DIRECTION('ref_axis',(0.959492973614495,0.281732556841437,1.16115793851356E-32));
#128577=DIRECTION('center_axis',(-1.16115793851356E-32,8.07603085451917E-32,
-1.));
#128578=DIRECTION('ref_axis',(-0.959492973614495,-0.281732556841437,-1.16115793851356E-32));
#128579=DIRECTION('center_axis',(-0.999619365514338,0.0275884774627343,
1.69889412890019E-32));
#128580=DIRECTION('ref_axis',(-0.0275884774627343,-0.999619365514338,-7.92437368218264E-32));
#128581=DIRECTION('',(1.47962606647006E-32,-7.96822729466867E-32,1.));
#128582=DIRECTION('',(-0.020189461662872,-0.731529200361817,-0.681511125848847));
#128583=DIRECTION('center_axis',(0.999619232869144,-0.027593283123731,2.13514020813021E-6));
#128584=DIRECTION('ref_axis',(0.0273594852325617,0.9911595046472,0.129824092199122));
#128585=DIRECTION('',(-1.58472524752277E-32,4.16014557570144E-32,-1.));
#128586=DIRECTION('center_axis',(0.723463442554642,0.690362692566006,4.43051148238339E-32));
#128587=DIRECTION('ref_axis',(-0.690362692566006,0.723463442554642,6.78619978489798E-32));
#128588=DIRECTION('center_axis',(-0.723463442554664,-0.690362692565983,
-7.07285729322285E-15));
#128589=DIRECTION('ref_axis',(0.685183837413238,-0.718036277359265,0.122257978650548));
#128590=DIRECTION('',(-0.505212769855248,0.529436155281655,0.68151112584885));
#128591=DIRECTION('',(1.47962606647006E-32,-7.96822729466867E-32,1.));
#128592=DIRECTION('',(-1.15033253548731E-32,-5.21217033441171E-32,1.));
#128593=DIRECTION('center_axis',(1.47962606647006E-32,-7.96822729466867E-32,
1.));
#128594=DIRECTION('ref_axis',(-0.933336521037364,-0.359002699847607,-1.47962606647007E-32));
#128595=DIRECTION('center_axis',(-0.121943621702652,0.317029469948172,-0.940543496235247));
#128596=DIRECTION('ref_axis',(-0.337546396275881,0.877886382347404,0.339673269554955));
#128597=DIRECTION('center_axis',(-0.121943621702652,0.317029469948172,-0.940543496235247));
#128598=DIRECTION('ref_axis',(-0.337546396275881,0.877886382347404,0.339673269554955));
#128599=DIRECTION('center_axis',(0.506870460541718,-0.531173327095347,-0.678923583927297));
#128600=DIRECTION('ref_axis',(0.254076236620314,-0.660548321408537,0.706485089063614));
#128601=DIRECTION('center_axis',(0.0202557067868084,0.733929474493211,0.678923583927297));
#128602=DIRECTION('ref_axis',(-0.254076236620308,0.660548321408539,-0.706485089063614));
#128603=DIRECTION('center_axis',(0.999700120718703,-0.00306091103506829,
-0.0242960790796926));
#128604=DIRECTION('ref_axis',(0.0197215887137683,0.688781988546106,0.72470023540294));
#128605=DIRECTION('center_axis',(-1.47962606647006E-32,7.96822729466867E-32,
-1.));
#128606=DIRECTION('ref_axis',(0.933336521037363,0.359002699847609,1.4796260664701E-32));
#128607=DIRECTION('center_axis',(-1.9754687135784E-35,-4.11635425026281E-32,
1.));
#128608=DIRECTION('ref_axis',(-0.205800343803899,-0.978594000845191,-4.02864612680122E-32));
#128609=DIRECTION('center_axis',(1.47962606647006E-32,-7.96822729466867E-32,
1.));
#128610=DIRECTION('ref_axis',(-0.933336521037363,-0.359002699847609,-1.4796260664701E-32));
#128611=DIRECTION('center_axis',(-0.504991997622744,0.529204797705328,0.681854357192688));
#128612=DIRECTION('ref_axis',(-0.255091277271192,0.663187227773891,-0.703641344136153));
#128613=DIRECTION('center_axis',(-0.505436374010848,0.529670480563034,0.681163162426516));
#128614=DIRECTION('ref_axis',(-0.254851977616527,0.66256509566382,-0.704313824593084));
#128615=DIRECTION('center_axis',(-0.0201983973980596,-0.731852970818359,
-0.681163162426516));
#128616=DIRECTION('ref_axis',(0.254851977616525,-0.662565095663822,0.704313824593083));
#128617=DIRECTION('center_axis',(-0.0201806390978207,-0.731209530424045,
-0.681854357192686));
#128618=DIRECTION('ref_axis',(0.255091277271204,-0.663187227773886,0.703641344136154));
#128619=DIRECTION('center_axis',(1.47962606647006E-32,-7.96822729466867E-32,
1.));
#128620=DIRECTION('ref_axis',(-0.933336521037363,-0.359002699847609,-1.4796260664701E-32));
#128621=DIRECTION('center_axis',(-1.9754687135784E-35,-4.11635425026281E-32,
1.));
#128622=DIRECTION('ref_axis',(0.808547669093915,-0.588430681391443,-2.42059187570697E-32));
#128623=DIRECTION('center_axis',(1.47962606647006E-32,-7.96822729466867E-32,
1.));
#128624=DIRECTION('ref_axis',(0.933336521037362,0.359002699847611,1.47962606647011E-32));
#128625=DIRECTION('center_axis',(-1.47962606647006E-32,7.96822729466867E-32,
-1.));
#128626=DIRECTION('ref_axis',(-0.933336521037364,-0.359002699847605,-1.47962606647006E-32));
#128627=DIRECTION('center_axis',(-0.998541931570524,-0.0539815792229779,
1.36270394936435E-32));
#128628=DIRECTION('ref_axis',(0.0539815792229779,-0.998541931570524,-7.91993304887029E-32));
#128629=DIRECTION('',(1.78824752707533E-32,-7.8348243333281E-32,1.));
#128630=DIRECTION('',(0.0395041381205485,-0.730740725849866,-0.681511125848848));
#128631=DIRECTION('center_axis',(0.998542191072677,0.0539767787406583,2.13514018280428E-6));
#128632=DIRECTION('ref_axis',(0.053520252301274,-0.990091555181766,-0.1298240923379));
#128633=DIRECTION('',(-1.58260298667146E-32,4.03084713318711E-32,-1.));
#128634=DIRECTION('center_axis',(0.664785209172398,0.747034554532527,4.66408399934957E-32));
#128635=DIRECTION('ref_axis',(-0.747034554532527,0.664785209172398,6.54435802804312E-32));
#128636=DIRECTION('center_axis',(-0.664785209172376,-0.747034554532547,
9.84602795854721E-15));
#128637=DIRECTION('ref_axis',(0.74143056723946,-0.659798227188434,0.122257978725204));
#128638=DIRECTION('',(-0.546685677741585,0.486494969240643,0.681511125848852));
#128639=DIRECTION('',(1.78824752707533E-32,-7.8348243333281E-32,1.));
#128640=DIRECTION('',(-1.05760433283579E-32,-5.30230396665168E-32,1.));
#128641=DIRECTION('center_axis',(1.78824752707533E-32,-7.8348243333281E-32,
1.));
#128642=DIRECTION('ref_axis',(-0.900968867902416,-0.433883739117564,-1.78824752707532E-32));
#128643=DIRECTION('center_axis',(-0.147378709319897,0.306035043301976,-0.940543496235213));
#128644=DIRECTION('ref_axis',(-0.407979128548356,0.847452122906485,0.339673269555048));
#128645=DIRECTION('center_axis',(-0.147378709319897,0.306035043301976,-0.940543496235213));
#128646=DIRECTION('ref_axis',(-0.407979128548356,0.847452122906485,0.339673269555048));
#128647=DIRECTION('center_axis',(0.548479448228987,-0.488091243578226,-0.678923583927297));
#128648=DIRECTION('ref_axis',(0.307071639329003,-0.637640829347192,0.706485089063615));
#128649=DIRECTION('center_axis',(-0.0396337580465611,0.733138412859687,
0.678923583927297));
#128650=DIRECTION('ref_axis',(-0.307071639328998,0.637640829347196,-0.706485089063613));
#128651=DIRECTION('center_axis',(0.996623193701797,0.0784341144969083,-0.0242960790811355));
#128652=DIRECTION('ref_axis',(-0.0364860723690897,0.688096759915976,0.724701052514906));
#128653=DIRECTION('center_axis',(-1.78824752707533E-32,7.8348243333281E-32,
-1.));
#128654=DIRECTION('ref_axis',(0.900968867902417,0.433883739117563,1.78824752707531E-32));
#128655=DIRECTION('center_axis',(-2.38751338728303E-35,-4.11653235835539E-32,
1.));
#128656=DIRECTION('ref_axis',(-0.125351064244871,-0.992112448612897,-4.08436227518618E-32));
#128657=DIRECTION('center_axis',(1.78824752707533E-32,-7.8348243333281E-32,
1.));
#128658=DIRECTION('ref_axis',(-0.900968867902417,-0.433883739117563,-1.78824752707531E-32));
#128659=DIRECTION('center_axis',(-0.546446782320192,0.486282376474056,0.681854357192688));
#128660=DIRECTION('ref_axis',(-0.308298397883032,0.64018821973309,-0.703641344136153));
#128661=DIRECTION('center_axis',(-0.546927637558614,0.486710289009449,0.681163162426516));
#128662=DIRECTION('ref_axis',(-0.308009184935663,0.639587662859699,-0.704313824593083));
#128663=DIRECTION('center_axis',(0.0395216224162265,-0.731064147332296,
-0.681163162426516));
#128664=DIRECTION('ref_axis',(0.308009184935658,-0.6395876628597,0.704313824593084));
#128665=DIRECTION('center_axis',(0.0394868752616406,-0.730421400466484,
-0.681854357192686));
#128666=DIRECTION('ref_axis',(0.308298397883045,-0.640188219733083,0.703641344136154));
#128667=DIRECTION('center_axis',(1.78824752707533E-32,-7.8348243333281E-32,
1.));
#128668=DIRECTION('ref_axis',(-0.900968867902417,-0.433883739117563,-1.78824752707531E-32));
#128669=DIRECTION('center_axis',(-2.38751338728303E-35,-4.11653235835539E-32,
1.));
#128670=DIRECTION('ref_axis',(0.85381985668282,-0.520568585619733,-2.14089892110877E-32));
#128671=DIRECTION('center_axis',(1.78824752707533E-32,-7.8348243333281E-32,
1.));
#128672=DIRECTION('ref_axis',(0.900968867902428,0.43388373911754,1.7882475270751E-32));
#128673=DIRECTION('center_axis',(-1.78824752707533E-32,7.8348243333281E-32,
-1.));
#128674=DIRECTION('ref_axis',(-0.900968867902416,-0.433883739117565,-1.78824752707533E-32));
#128675=DIRECTION('center_axis',(-0.99081936581993,-0.135192397405294,1.02799436775695E-32));
#128676=DIRECTION('ref_axis',(0.135192397405294,-0.99081936581993,-7.88810457072944E-32));
#128677=DIRECTION('',(2.08496849542798E-32,-7.67670974519523E-32,1.));
#128678=DIRECTION('',(0.0989348443825012,-0.725089292371119,-0.681511125848845));
#128679=DIRECTION('center_axis',(0.990820015742491,0.135187634047982,2.13514019614746E-6));
#128680=DIRECTION('ref_axis',(0.134043821391896,-0.98243470983393,-0.129824091986731));
#128681=DIRECTION('',(-1.56994876405497E-32,3.90215190453537E-32,-1.));
#128682=DIRECTION('center_axis',(0.60168293990495,0.79873502479066,4.87716697470091E-32));
#128683=DIRECTION('ref_axis',(-0.79873502479066,0.60168293990495,6.28428265116946E-32));
#128684=DIRECTION('center_axis',(-0.601682939904999,-0.798735024790623,
-3.64582895726031E-14));
#128685=DIRECTION('ref_axis',(0.792743198971836,-0.597169328679565,0.122257978751077));
#128686=DIRECTION('',(-0.584520482639353,0.440316239445344,0.68151112584885));
#128687=DIRECTION('',(2.08496849542798E-32,-7.67670974519523E-32,1.));
#128688=DIRECTION('',(-9.57837947841676E-33,-5.38457947730315E-32,1.));
#128689=DIRECTION('center_axis',(2.08496849542798E-32,-7.67670974519523E-32,
1.));
#128690=DIRECTION('ref_axis',(-0.862605415600979,-0.505877353689471,-2.08496849542794E-32));
#128691=DIRECTION('center_axis',(-0.171833015942314,0.293004003934667,-0.940543496235247));
#128692=DIRECTION('ref_axis',(-0.475696827032618,0.81137820940727,0.339673269554954));
#128693=DIRECTION('center_axis',(-0.171833015942314,0.293004003934667,-0.940543496235247));
#128694=DIRECTION('ref_axis',(-0.475696827032618,0.81137820940727,0.339673269554954));
#128695=DIRECTION('center_axis',(0.586438395681031,-0.44176099336448,-0.678923583927297));
#128696=DIRECTION('ref_axis',(0.358023530941208,-0.610489942769876,0.706485089063615));
#128697=DIRECTION('center_axis',(-0.0992594667592402,0.727468436047905,
0.678923583927297));
#128698=DIRECTION('ref_axis',(-0.3580235309412,0.610489942769881,-0.706485089063614));
#128699=DIRECTION('center_axis',(0.986913903762582,0.159407173933681,-0.0242960790782657));
#128700=DIRECTION('ref_axis',(-0.0924509953873511,0.682833509827438,0.724700773636009));
#128701=DIRECTION('center_axis',(-2.08496849542798E-32,7.67670974519523E-32,
-1.));
#128702=DIRECTION('ref_axis',(0.862605415600975,0.505877353689478,2.084968495428E-32));
#128703=DIRECTION('center_axis',(-2.7836695533073E-35,-4.11674345927413E-32,
1.));
#128704=DIRECTION('ref_axis',(-0.0440675940347879,-0.999028551722114,-4.11286692554992E-32));
#128705=DIRECTION('center_axis',(2.08496849542798E-32,-7.67670974519523E-32,
1.));
#128706=DIRECTION('ref_axis',(-0.862605415600975,-0.505877353689478,-2.084968495428E-32));
#128707=DIRECTION('center_axis',(-0.584265053838671,0.440123826258294,0.681854357192688));
#128708=DIRECTION('ref_axis',(-0.35945384352262,0.612928864713584,-0.703641344136153));
#128709=DIRECTION('center_axis',(-0.584779187915136,0.440511120784053,0.681163162426516));
#128710=DIRECTION('ref_axis',(-0.359116641946996,0.612353879683779,-0.704313824593084));
#128711=DIRECTION('center_axis',(0.0989786323539411,-0.725410212562831,
-0.681163162426516));
#128712=DIRECTION('ref_axis',(0.359116641946992,-0.612353879683781,0.704313824593084));
#128713=DIRECTION('center_axis',(0.098891610981111,-0.724772436599868,-0.681854357192686));
#128714=DIRECTION('ref_axis',(0.359453843522631,-0.612928864713577,0.703641344136154));
#128715=DIRECTION('center_axis',(2.08496849542798E-32,-7.67670974519523E-32,
1.));
#128716=DIRECTION('ref_axis',(-0.862605415600975,-0.505877353689478,-2.084968495428E-32));
#128717=DIRECTION('center_axis',(-2.7836695533073E-35,-4.11674345927413E-32,
1.));
#128718=DIRECTION('ref_axis',(0.893410013995863,-0.44924219179849,-1.84692789646182E-32));
#128719=DIRECTION('center_axis',(2.08496849542798E-32,-7.67670974519523E-32,
1.));
#128720=DIRECTION('ref_axis',(0.862605415600984,0.505877353689463,2.08496849542787E-32));
#128721=DIRECTION('center_axis',(-2.08496849542798E-32,7.67670974519523E-32,
-1.));
#128722=DIRECTION('ref_axis',(-0.862605415600977,-0.505877353689475,-2.08496849542798E-32));
#128723=DIRECTION('center_axis',(-0.976503060663493,-0.215503532488054,
6.96992821120416E-33));
#128724=DIRECTION('ref_axis',(0.215503532488054,-0.976503060663493,-7.82910006103078E-32));
#128725=DIRECTION('',(2.36781434243914E-32,-7.49493575676703E-32,1.));
#128726=DIRECTION('',(0.157707155578178,-0.714612509282946,-0.681511125848854));
#128727=DIRECTION('center_axis',(0.976504096681335,0.215498837955129,2.1351402057377E-6));
#128728=DIRECTION('ref_axis',(0.213675350959354,-0.968239923513829,-0.129824092164478));
#128729=DIRECTION('',(-1.546846791437E-32,3.77491633525967E-32,-1.));
#128730=DIRECTION('center_axis',(0.534576569943133,0.845120045240814,5.06834237639268E-32));
#128731=DIRECTION('ref_axis',(-0.845120045240814,0.534576569943133,6.00770441300067E-32));
#128732=DIRECTION('center_axis',(-0.53457656994313,-0.845120045240815,-5.3936897343997E-15));
#128733=DIRECTION('ref_axis',(0.838780255517472,-0.530566366820449,0.122257978688485));
#128734=DIRECTION('',(-0.618465400164244,0.3912072777236,0.681511125848853));
#128735=DIRECTION('',(2.36781434243914E-32,-7.49493575676703E-32,1.));
#128736=DIRECTION('',(-8.51697309336819E-33,-5.45844933641721E-32,1.));
#128737=DIRECTION('center_axis',(2.36781434243914E-32,-7.49493575676703E-32,
1.));
#128738=DIRECTION('ref_axis',(-0.818501466578588,-0.574504437936471,-2.36781434243915E-32));
#128739=DIRECTION('center_axis',(-0.195143802194123,0.278023071263506,-0.94054349623525));
#128740=DIRECTION('ref_axis',(-0.540248841617448,0.769904707792372,0.339673269554946));
#128741=DIRECTION('center_axis',(-0.195143802194123,0.278023071263506,-0.94054349623525));
#128742=DIRECTION('ref_axis',(-0.540248841617448,0.769904707792372,0.339673269554946));
#128743=DIRECTION('center_axis',(0.620494692365343,-0.392490896625326,-0.678923583927297));
#128744=DIRECTION('ref_axis',(0.406592835024724,-0.579276346347177,0.706485089063615));
#128745=DIRECTION('center_axis',(-0.158224620097296,0.716957276818069,0.678923583927297));
#128746=DIRECTION('ref_axis',(-0.406592835024719,0.579276346347181,-0.706485089063613));
#128747=DIRECTION('center_axis',(0.970636864621209,0.239319404937,-0.0242960790850888));
#128748=DIRECTION('ref_axis',(-0.147800561463386,0.673025524458571,0.724701067653673));
#128749=DIRECTION('center_axis',(-2.36781434243914E-32,7.49493575676703E-32,
-1.));
#128750=DIRECTION('ref_axis',(0.818501466578589,0.57450443793647,2.36781434243914E-32));
#128751=DIRECTION('center_axis',(-3.16130085772864E-35,-4.11698614817723E-32,
1.));
#128752=DIRECTION('ref_axis',(0.0375091387429715,-0.999296284647732,-4.11397038414721E-32));
#128753=DIRECTION('center_axis',(2.36781434243914E-32,-7.49493575676703E-32,
1.));
#128754=DIRECTION('ref_axis',(-0.818501466578589,-0.57450443793647,-2.36781434243914E-32));
#128755=DIRECTION('center_axis',(-0.618195137820803,0.391036324594103,0.681854357192688));
#128756=DIRECTION('ref_axis',(-0.40821718313927,0.581590569225557,-0.703641344136153));
#128757=DIRECTION('center_axis',(-0.618739129257858,0.391380423729057,0.681163162426516));
#128758=DIRECTION('ref_axis',(-0.407834236956245,0.581044982469842,-0.704313824593084));
#128759=DIRECTION('center_axis',(0.157776955823665,-0.714928792513021,-0.681163162426516));
#128760=DIRECTION('ref_axis',(0.40783423695624,-0.581044982469846,0.704313824593084));
#128761=DIRECTION('center_axis',(0.15763823934547,-0.714300231746714,-0.681854357192686));
#128762=DIRECTION('ref_axis',(0.408217183139275,-0.581590569225551,0.703641344136156));
#128763=DIRECTION('center_axis',(2.36781434243914E-32,-7.49493575676703E-32,
1.));
#128764=DIRECTION('ref_axis',(-0.818501466578589,-0.57450443793647,-2.36781434243914E-32));
#128765=DIRECTION('center_axis',(-3.16130085772864E-35,-4.11698614817723E-32,
1.));
#128766=DIRECTION('ref_axis',(0.927054675068037,-0.374926165310579,-1.54063513043341E-32));
#128767=DIRECTION('center_axis',(2.36781434243914E-32,-7.49493575676703E-32,
1.));
#128768=DIRECTION('ref_axis',(0.818501466578589,0.57450443793647,2.36781434243914E-32));
#128769=DIRECTION('center_axis',(-2.36781434243914E-32,7.49493575676703E-32,
-1.));
#128770=DIRECTION('ref_axis',(-0.818501466578589,-0.57450443793647,-2.36781434243914E-32));
#128771=DIRECTION('center_axis',(-0.955688288750005,-0.294380527117686,
3.7190207013619E-33));
#128772=DIRECTION('ref_axis',(0.294380527117686,-0.955688288750005,-7.74331218505129E-32));
#128773=DIRECTION('',(2.63490277566324E-32,-7.29071204394588E-32,1.));
#128774=DIRECTION('',(0.215429951673336,-0.699380097848277,-0.681511125848844));
#128775=DIRECTION('center_axis',(0.955689703968581,0.29437593265056,2.13514017770259E-6));
#128776=DIRECTION('ref_axis',(0.291884906313846,-0.947601660243299,-0.129824092410852));
#128777=DIRECTION('',(-1.51345080863378E-32,3.64998715708116E-32,-1.));
#128778=DIRECTION('center_axis',(0.463912681107269,0.885880931224883,5.23633796366833E-32));
#128779=DIRECTION('ref_axis',(-0.885880931224883,0.463912681107269,5.71646389607957E-32));
#128780=DIRECTION('center_axis',(-0.463912681107264,-0.885880931224885,
5.80076065774857E-15));
#128781=DIRECTION('ref_axis',(0.879235367844626,-0.460432573322416,0.122257978695964));
#128782=DIRECTION('',(-0.648294532490651,0.339494896113278,0.681511125848847));
#128783=DIRECTION('',(2.63490277566324E-32,-7.29071204394588E-32,1.));
#128784=DIRECTION('',(-7.39888765758488E-33,-5.52342195226915E-32,1.));
#128785=DIRECTION('center_axis',(2.63490277566324E-32,-7.29071204394588E-32,
1.));
#128786=DIRECTION('ref_axis',(-0.768950525339359,-0.639308289935555,-2.63490277566321E-32));
#128787=DIRECTION('center_axis',(-0.217155938638808,0.261191940923687,-0.940543496235244));
#128788=DIRECTION('ref_axis',(-0.601205589296476,0.723307617372109,0.339673269554964));
#128789=DIRECTION('center_axis',(-0.217155938638808,0.261191940923687,-0.940543496235244));
#128790=DIRECTION('ref_axis',(-0.601205589296476,0.723307617372109,0.339673269554964));
#128791=DIRECTION('center_axis',(0.650421699246381,-0.340608837725571,-0.678923583927297));
#128792=DIRECTION('ref_axis',(0.452456330874242,-0.544207761413412,0.706485089063613));
#128793=DIRECTION('center_axis',(-0.216136814693829,0.701674885200632,0.678923583927297));
#128794=DIRECTION('ref_axis',(-0.452456330874235,0.544207761413415,-0.706485089063615));
#128795=DIRECTION('center_axis',(0.947900397295688,0.317639004765663,-0.0242960790695897));
#128796=DIRECTION('ref_axis',(-0.202166797592671,0.658739529255004,0.724700502654731));
#128797=DIRECTION('center_axis',(-2.63490277566324E-32,7.29071204394588E-32,
-1.));
#128798=DIRECTION('ref_axis',(0.768950525339356,0.639308289935559,2.63490277566325E-32));
#128799=DIRECTION('center_axis',(-3.51789422651897E-35,-4.1172588100101E-32,
1.));
#128800=DIRECTION('ref_axis',(0.118836254390979,-0.992913865671299,-4.08766530764312E-32));
#128801=DIRECTION('center_axis',(2.63490277566324E-32,-7.29071204394588E-32,
1.));
#128802=DIRECTION('ref_axis',(-0.768950525339356,-0.639308289935559,-2.63490277566325E-32));
#128803=DIRECTION('center_axis',(-0.648011235155756,0.339346540706191,0.681854357192688));
#128804=DIRECTION('ref_axis',(-0.454263904753227,0.54638188445502,-0.703641344136153));
#128805=DIRECTION('center_axis',(-0.648581463780139,0.339645154527369,0.681163162426516));
#128806=DIRECTION('ref_axis',(-0.453837762406458,0.545869326763249,-0.704313824593083));
#128807=DIRECTION('center_axis',(0.215525299683748,-0.699689639303984,-0.681163162426516));
#128808=DIRECTION('ref_axis',(0.453837762406454,-0.54586932676325,0.704313824593085));
#128809=DIRECTION('center_axis',(0.215335811235463,-0.699074476702528,-0.681854357192686));
#128810=DIRECTION('ref_axis',(0.454263904753234,-0.546381884455012,0.703641344136155));
#128811=DIRECTION('center_axis',(2.63490277566324E-32,-7.29071204394588E-32,
1.));
#128812=DIRECTION('ref_axis',(-0.768950525339356,-0.639308289935559,-2.63490277566325E-32));
#128813=DIRECTION('center_axis',(-3.51789422651897E-35,-4.1172588100101E-32,
1.));
#128814=DIRECTION('ref_axis',(0.954529940230887,-0.298115067050994,-1.22405895084668E-32));
#128815=DIRECTION('center_axis',(2.63490277566324E-32,-7.29071204394588E-32,
1.));
#128816=DIRECTION('ref_axis',(0.768950525339356,0.639308289935559,2.63490277566325E-32));
#128817=DIRECTION('center_axis',(-2.63490277566324E-32,7.29071204394588E-32,
-1.));
#128818=DIRECTION('ref_axis',(-0.768950525339357,-0.639308289935558,-2.63490277566324E-32));
#128819=DIRECTION('center_axis',(-0.928513568952355,-0.371298467908718,
5.48855401158773E-34));
#128820=DIRECTION('ref_axis',(0.371298467908718,-0.928513568952355,-7.63131184695163E-32));
#128821=DIRECTION('',(2.88445636564366E-32,-7.06539768184607E-32,1.));
#128822=DIRECTION('',(0.271719096983558,-0.679493427252004,-0.681511125848849));
#128823=DIRECTION('center_axis',(0.928515353953652,0.371294004082703,2.13514021011526E-6));
#128824=DIRECTION('ref_axis',(0.368152015798042,-0.92065726434055,-0.129824092066201));
#128825=DIRECTION('',(-1.4699830604009E-32,3.52819575306875E-32,-1.));
#128826=DIRECTION('center_axis',(0.390161529918842,0.920746425771715,5.38003575361186E-32));
#128827=DIRECTION('ref_axis',(-0.920746425771715,0.390161529918842,5.41249925799497E-32));
#128828=DIRECTION('center_axis',(-0.39016152991884,-0.920746425771716,-4.1979188970568E-15));
#128829=DIRECTION('ref_axis',(0.913839313871822,-0.387234677019114,0.122257978619719));
#128830=DIRECTION('',(-0.673809371664399,0.285523231982022,0.68151112584885));
#128831=DIRECTION('',(2.88445636564366E-32,-7.06539768184607E-32,1.));
#128832=DIRECTION('',(-6.23156384517089E-33,-5.5790649428202E-32,1.));
#128833=DIRECTION('center_axis',(2.88445636564366E-32,-7.06539768184607E-32,
1.));
#128834=DIRECTION('ref_axis',(-0.7142823452219,-0.699857650743566,-2.88445636564364E-32));
#128835=DIRECTION('center_axis',(-0.237722938140167,0.242622621310766,-0.940543496235182));
#128836=DIRECTION('ref_axis',(-0.658161412970005,0.671897034096037,0.339673269555136));
#128837=DIRECTION('center_axis',(-0.237722938140167,0.242622621310766,-0.940543496235182));
#128838=DIRECTION('ref_axis',(-0.658161412970005,0.671897034096037,0.339673269555136));
#128839=DIRECTION('center_axis',(0.676020257030961,-0.286460083207254,-0.678923583927297));
#128840=DIRECTION('ref_axis',(0.49530880449184,-0.50551756361539,0.706485089063615));
#128841=DIRECTION('center_axis',(-0.272610654448639,0.681722962990392,0.678923583927297));
#128842=DIRECTION('ref_axis',(-0.495308804491836,0.505517563615396,-0.706485089063613));
#128843=DIRECTION('center_axis',(0.918855809212912,0.393844769442579,-0.0242960790747627));
#128844=DIRECTION('ref_axis',(-0.255187276864415,0.640068686911497,0.724700993349614));
#128845=DIRECTION('center_axis',(-2.88445636564366E-32,7.06539768184607E-32,
-1.));
#128846=DIRECTION('ref_axis',(0.714282345221899,0.699857650743566,2.88445636564364E-32));
#128847=DIRECTION('center_axis',(-3.85107658964385E-35,-4.11755963025323E-32,
1.));
#128848=DIRECTION('ref_axis',(0.199372534372595,-0.979923768738083,-4.03412675198179E-32));
#128849=DIRECTION('center_axis',(2.88445636564366E-32,-7.06539768184607E-32,
1.));
#128850=DIRECTION('ref_axis',(-0.714282345221899,-0.699857650743566,-2.88445636564364E-32));
#128851=DIRECTION('center_axis',(-0.673514924635075,0.285398461578117,0.681854357192688));
#128852=DIRECTION('ref_axis',(-0.497287575029315,0.507537118390106,-0.703641344136152));
#128853=DIRECTION('center_axis',(-0.674107595669373,0.285649602859807,0.681163162426516));
#128854=DIRECTION('ref_axis',(-0.496821072425826,0.507061000749135,-0.704313824593084));
#128855=DIRECTION('center_axis',(0.271839358233607,-0.679794166986044,-0.681163162426516));
#128856=DIRECTION('ref_axis',(0.496821072425819,-0.507061000749142,0.704313824593084));
#128857=DIRECTION('center_axis',(0.271600358829592,-0.679196496355057,-0.681854357192686));
#128858=DIRECTION('ref_axis',(0.497287575029323,-0.507537118390095,0.703641344136155));
#128859=DIRECTION('center_axis',(2.88445636564366E-32,-7.06539768184607E-32,
1.));
#128860=DIRECTION('ref_axis',(-0.714282345221899,-0.699857650743566,-2.88445636564364E-32));
#128861=DIRECTION('center_axis',(-3.85107658964385E-35,-4.11755963025323E-32,
1.));
#128862=DIRECTION('ref_axis',(0.975652966127861,-0.219320062205688,-8.99306119945298E-33));
#128863=DIRECTION('center_axis',(2.88445636564366E-32,-7.06539768184607E-32,
1.));
#128864=DIRECTION('ref_axis',(0.714282345221914,0.699857650743551,2.88445636564349E-32));
#128865=DIRECTION('center_axis',(-2.88445636564366E-32,7.06539768184607E-32,
-1.));
#128866=DIRECTION('ref_axis',(-0.714282345221898,-0.699857650743568,-2.88445636564366E-32));
#128867=DIRECTION('center_axis',(-0.895159744547281,-0.445745478655752,
-2.51947076237285E-33));
#128868=DIRECTION('ref_axis',(0.445745478655752,-0.895159744547281,-7.49384439050308E-32));
#128869=DIRECTION('',(3.11481437441252E-32,-6.82049210037312E-32,1.));
#128870=DIRECTION('',(0.326199996533838,-0.655084840005901,-0.68151112584885));
#128871=DIRECTION('center_axis',(0.895161887452382,0.445741175176952,2.13514017251284E-6));
#128872=DIRECTION('ref_axis',(0.441969134348745,-0.887586046206353,-0.129824091996805));
#128873=DIRECTION('',(-1.4167328174312E-32,3.41035262492197E-32,-1.));
#128874=DIRECTION('center_axis',(0.313813918120925,0.949484504767504,5.49847946113968E-32));
#128875=DIRECTION('ref_axis',(-0.949484504767504,0.313813918120925,5.09783333326269E-32));
#128876=DIRECTION('center_axis',(-0.313813918120886,-0.949484504767517,
1.07873794688004E-14));
#128877=DIRECTION('ref_axis',(0.942361810024425,-0.311459797823307,0.122257978665416));
#128878=DIRECTION('',(-0.694840120640441,0.229651457849955,0.68151112584885));
#128879=DIRECTION('',(3.11481437441252E-32,-6.82049210037312E-32,1.));
#128880=DIRECTION('',(-5.02277000350294E-33,-5.62500801314869E-32,1.));
#128881=DIRECTION('center_axis',(3.11481437441252E-32,-6.82049210037312E-32,
1.));
#128882=DIRECTION('ref_axis',(-0.654860733945281,-0.755749574354262,-3.1148143744125E-32));
#128883=DIRECTION('center_axis',(-0.256707930709543,0.222438688182738,-0.940543496235218));
#128884=DIRECTION('ref_axis',(0.710737281029233,-0.616015086913434,-0.339673269555036));
#128885=DIRECTION('center_axis',(-0.256707930709543,0.222438688182738,-0.940543496235218));
#128886=DIRECTION('ref_axis',(0.710737281029233,-0.616015086913434,-0.339673269555036));
#128887=DIRECTION('center_axis',(0.697120011540492,-0.23040498409778,-0.678923583927297));
#128888=DIRECTION('ref_axis',(0.534865079735741,-0.463463229836042,0.706485089063615));
#128889=DIRECTION('center_axis',(-0.327270315275685,0.657234286937823,0.678923583927297));
#128890=DIRECTION('ref_axis',(-0.534865079735737,0.463463229836048,-0.706485089063613));
#128891=DIRECTION('center_axis',(0.883696387322955,0.467429562152471,-0.0242960790726872));
#128892=DIRECTION('ref_axis',(-0.306509859595482,0.617139060430464,0.724700687223189));
#128893=DIRECTION('center_axis',(-3.11481437441252E-32,6.82049210037312E-32,
-1.));
#128894=DIRECTION('ref_axis',(0.65486073394528,0.755749574354262,3.1148143744125E-32));
#128895=DIRECTION('center_axis',(-4.15863067344775E-35,-4.11788660699752E-32,
1.));
#128896=DIRECTION('ref_axis',(0.278582023032134,-0.960412440799953,-3.95371100741787E-32));
#128897=DIRECTION('center_axis',(3.11481437441252E-32,-6.82049210037312E-32,
1.));
#128898=DIRECTION('ref_axis',(-0.65486073394528,-0.755749574354262,-3.1148143744125E-32));
#128899=DIRECTION('center_axis',(-0.694536483413088,0.229551102775672,0.681854357192688));
#128900=DIRECTION('ref_axis',(-0.537001878540263,0.465314776540028,-0.703641344136153));
#128901=DIRECTION('center_axis',(-0.695147652729352,0.229753100214081,0.681163162426516));
#128902=DIRECTION('ref_axis',(-0.536498120177901,0.464878267434217,-0.704313824593085));
#128903=DIRECTION('center_axis',(0.326344370704758,-0.655374776644954,-0.681163162426516));
#128904=DIRECTION('ref_axis',(0.5364981201779,-0.464878267434222,0.704313824593083));
#128905=DIRECTION('center_axis',(0.326057450846616,-0.654798575383877,-0.681854357192686));
#128906=DIRECTION('ref_axis',(0.537001878540269,-0.465314776540019,0.703641344136155));
#128907=DIRECTION('center_axis',(3.11481437441252E-32,-6.82049210037312E-32,
1.));
#128908=DIRECTION('ref_axis',(-0.65486073394528,-0.755749574354262,-3.1148143744125E-32));
#128909=DIRECTION('center_axis',(-4.15863067344775E-35,-4.11788660699752E-32,
1.));
#128910=DIRECTION('ref_axis',(0.990283182506655,-0.139065518531698,-5.68537814238674E-33));
#128911=DIRECTION('center_axis',(3.11481437441252E-32,-6.82049210037312E-32,
1.));
#128912=DIRECTION('ref_axis',(0.65486073394528,0.755749574354262,3.1148143744125E-32));
#128913=DIRECTION('center_axis',(-3.11481437441252E-32,6.82049210037312E-32,
-1.));
#128914=DIRECTION('ref_axis',(-0.654860733945278,-0.755749574354264,-3.11481437441252E-32));
#128915=DIRECTION('center_axis',(-0.855848779733208,-0.51722612678516,-5.46553858485279E-33));
#128916=DIRECTION('ref_axis',(0.51722612678516,-0.855848779733208,-7.33182463894778E-32));
#128917=DIRECTION('',(3.32444380742786E-32,-6.55762510576516E-32,1.));
#128918=DIRECTION('',(0.378510088926395,-0.626316771230952,-0.681511125848851));
#128919=DIRECTION('center_axis',(0.855851266281428,0.517222012292514,2.13514017393721E-6));
#128920=DIRECTION('ref_axis',(0.512845021223353,-0.848608089361961,-0.129824092047128));
#128921=DIRECTION('',(-1.35405445130595E-32,3.29724199921589E-32,-1.));
#128922=DIRECTION('center_axis',(0.235377926473567,0.971903921037982,5.59088086292001E-32));
#128923=DIRECTION('ref_axis',(-0.971903921037982,0.235377926473567,4.77456017169558E-32));
#128924=DIRECTION('center_axis',(-0.235377926473611,-0.971903921037972,
-2.4983977920653E-14));
#128925=DIRECTION('ref_axis',(0.964613043805694,-0.233612205060252,0.122257978744951));
#128926=DIRECTION('',(-0.711246823254173,0.172251391155712,0.681511125848851));
#128927=DIRECTION('',(3.32444380742786E-32,-6.55762510576516E-32,1.));
#128928=DIRECTION('',(-3.78055045616041E-33,-5.66094541970164E-32,1.));
#128929=DIRECTION('center_axis',(3.32444380742786E-32,-6.55762510576516E-32,
1.));
#128930=DIRECTION('ref_axis',(-0.591081132528671,-0.806612109237534,-3.32444380742785E-32));
#128931=DIRECTION('center_axis',(-0.273984574353886,0.200774462284682,-0.940543496235244));
#128932=DIRECTION('ref_axis',(0.758583309747373,-0.556033660961783,-0.339673269554962));
#128933=DIRECTION('center_axis',(-0.273984574353886,0.200774462284682,-0.940543496235244));
#128934=DIRECTION('ref_axis',(0.758583309747373,-0.556033660961783,-0.339673269554962));
#128935=DIRECTION('center_axis',(0.713580547389926,-0.172816577833282,-0.678923583927297));
#128936=DIRECTION('ref_axis',(0.570861916120529,-0.418324624728181,0.706485089063615));
#128937=DIRECTION('center_axis',(-0.379752046150372,0.628371825141707,0.678923583927297));
#128938=DIRECTION('ref_axis',(-0.570861916120528,0.418324624728188,-0.706485089063612));
#128939=DIRECTION('center_axis',(0.842656111769909,0.537903688254794,-0.0242960790809713));
#128940=DIRECTION('ref_axis',(-0.355792274931549,0.590101793195228,0.724701132030859));
#128941=DIRECTION('center_axis',(-3.32444380742786E-32,6.55762510576516E-32,
-1.));
#128942=DIRECTION('ref_axis',(0.591081132528676,0.806612109237531,3.32444380742781E-32));
#128943=DIRECTION('center_axis',(-4.43850975624469E-35,-4.11823756426669E-32,
1.));
#128944=DIRECTION('ref_axis',(0.355937594291176,-0.934509726525203,-3.8469532274638E-32));
#128945=DIRECTION('center_axis',(3.32444380742786E-32,-6.55762510576516E-32,
1.));
#128946=DIRECTION('ref_axis',(-0.591081132528676,-0.806612109237531,-3.32444380742781E-32));
#128947=DIRECTION('center_axis',(-0.710936016484441,0.172176119257522,0.681854357192688));
#128948=DIRECTION('ref_axis',(-0.573142523148596,0.419995841623616,-0.703641344136153));
#128949=DIRECTION('center_axis',(-0.711561616851706,0.172327628593023,0.681163162426516));
#128950=DIRECTION('ref_axis',(-0.572604861456151,0.419601845949043,-0.704313824593084));
#128951=DIRECTION('center_axis',(0.3786776152319,-0.62659397529452,-0.681163162426516));
#128952=DIRECTION('ref_axis',(0.572604861456151,-0.419601845949045,0.704313824593083));
#128953=DIRECTION('center_axis',(0.378344684323947,-0.626043077927678,-0.681854357192686));
#128954=DIRECTION('ref_axis',(0.5731425231486,-0.419995841623607,0.703641344136155));
#128955=DIRECTION('center_axis',(3.32444380742786E-32,-6.55762510576516E-32,
1.));
#128956=DIRECTION('ref_axis',(-0.591081132528676,-0.806612109237531,-3.32444380742781E-32));
#128957=DIRECTION('center_axis',(-4.43850975624469E-35,-4.11823756426669E-32,
1.));
#128958=DIRECTION('ref_axis',(0.998323227691097,-0.0578855167760517,-2.33955242228133E-33));
#128959=DIRECTION('center_axis',(3.32444380742786E-32,-6.55762510576516E-32,
1.));
#128960=DIRECTION('ref_axis',(0.59108113252868,0.806612109237527,3.32444380742778E-32));
#128961=DIRECTION('center_axis',(-3.32444380742786E-32,6.55762510576516E-32,
-1.));
#128962=DIRECTION('ref_axis',(-0.59108113252867,-0.806612109237535,-3.32444380742786E-32));
#128963=DIRECTION('center_axis',(-0.810842282495119,-0.585264720377117,
-8.26974247098951E-33));
#128964=DIRECTION('ref_axis',(0.585264720377117,-0.810842282495119,-7.14633080700095E-32));
#128965=DIRECTION('',(3.51194961539939E-32,-6.27854603450129E-32,1.));
#128966=DIRECTION('',(0.428301259126928,-0.593380667678451,-0.681511125848847));
#128967=DIRECTION('center_axis',(0.810845096138937,0.585260822251823,2.13514021087779E-6));
#128968=DIRECTION('ref_axis',(0.580308009067981,-0.803982785657608,-0.129824092439688));
#128969=DIRECTION('',(-1.28236507621051E-32,3.18961660850265E-32,-1.));
#128970=DIRECTION('center_axis',(0.15537553356015,0.987855477066812,5.65662504286917E-32));
#128971=DIRECTION('ref_axis',(-0.987855477066812,0.15537553356015,4.44483110284758E-32));
#128972=DIRECTION('center_axis',(-0.155375533560178,-0.987855477066808,
-1.41457145864412E-14));
#128973=DIRECTION('ref_axis',(0.980444936943974,-0.154209961619461,0.122257978709985));
#128974=DIRECTION('',(-0.722920295606621,0.113705019872803,0.681511125848845));
#128975=DIRECTION('',(3.51194961539939E-32,-6.27854603450129E-32,1.));
#128976=DIRECTION('',(-2.51317196927904E-33,-5.68663800496772E-32,1.));
#128977=DIRECTION('center_axis',(3.51194961539939E-32,-6.27854603450129E-32,
1.));
#128978=DIRECTION('ref_axis',(-0.523367983696605,-0.852106773615461,-3.51194961539939E-32));
#128979=DIRECTION('center_axis',(-0.289437895860387,0.177774115465721,-0.940543496235178));
#128980=DIRECTION('ref_axis',(0.801381091695437,-0.492351922736925,-0.339673269555146));
#128981=DIRECTION('center_axis',(-0.289437895860387,0.177774115465721,-0.940543496235178));
#128982=DIRECTION('ref_axis',(0.801381091695437,-0.492351922736925,-0.339673269555146));
#128983=DIRECTION('center_axis',(0.725292322428984,-0.114078105756032,-0.678923583927297));
#128984=DIRECTION('ref_axis',(0.603059760639116,-0.370402138261472,0.706485089063613));
#128985=DIRECTION('center_axis',(-0.429706589812607,0.595327652523326,0.678923583927297));
#128986=DIRECTION('ref_axis',(-0.603059760639109,0.370402138261479,-0.706485089063615));
#128987=DIRECTION('center_axis',(0.796008098829182,0.604798154048084,-0.0242960790742329));
#128988=DIRECTION('ref_axis',(-0.402707478164874,0.559138279076155,0.724700677453694));
#128989=DIRECTION('center_axis',(-3.51194961539939E-32,6.27854603450129E-32,
-1.));
#128990=DIRECTION('ref_axis',(0.523367983696608,0.852106773615459,3.51194961539936E-32));
#128991=DIRECTION('center_axis',(-4.6888512889172E-35,-4.11861016649801E-32,
1.));
#128992=DIRECTION('ref_axis',(0.4309244595858,-0.902388004203672,-3.71456386753134E-32));
#128993=DIRECTION('center_axis',(3.51194961539939E-32,-6.27854603450129E-32,
1.));
#128994=DIRECTION('ref_axis',(-0.523367983696608,-0.852106773615459,-3.51194961539936E-32));
#128995=DIRECTION('center_axis',(-0.722604387662277,0.113655332072772,0.681854357192688));
#128996=DIRECTION('ref_axis',(-0.605468998827237,0.371881903675631,-0.703641344136153));
#128997=DIRECTION('center_axis',(-0.723240255813315,0.113755345035735,0.681163162426516));
#128998=DIRECTION('ref_axis',(-0.604901011854562,0.371533043408511,-0.704313824593083));
#128999=DIRECTION('center_axis',(0.428490822707084,-0.593643294419229,-0.681163162426516));
#129000=DIRECTION('ref_axis',(0.60490101185456,-0.371533043408513,0.704313824593084));
#129001=DIRECTION('center_axis',(0.428114096349583,-0.593121367077708,-0.681854357192686));
#129002=DIRECTION('ref_axis',(0.605468998827243,-0.371881903675619,0.703641344136154));
#129003=DIRECTION('center_axis',(3.51194961539939E-32,-6.27854603450129E-32,
1.));
#129004=DIRECTION('ref_axis',(-0.523367983696608,-0.852106773615459,-3.51194961539936E-32));
#129005=DIRECTION('center_axis',(-4.6888512889172E-35,-4.11861016649801E-32,
1.));
#129006=DIRECTION('ref_axis',(0.999719596506991,0.023679703543303,1.02215004271744E-33));
#129007=DIRECTION('center_axis',(3.51194961539939E-32,-6.27854603450129E-32,
1.));
#129008=DIRECTION('ref_axis',(0.52336798369659,0.85210677361547,3.5119496153995E-32));
#129009=DIRECTION('center_axis',(-3.51194961539939E-32,6.27854603450129E-32,
-1.));
#129010=DIRECTION('ref_axis',(-0.523367983696604,-0.852106773615461,-3.51194961539939E-32));
#129011=DIRECTION('center_axis',(-0.760439763646586,-0.649408473816846,
-1.09134209065818E-32));
#129012=DIRECTION('ref_axis',(0.649408473816846,-0.760439763646586,-6.93859732550988E-32));
#129013=DIRECTION('',(3.67608397811134E-32,-5.98511211175597E-32,1.));
#129014=DIRECTION('',(0.475242155112699,-0.556495713683465,-0.681511125848851));
#129015=DIRECTION('center_axis',(0.760442885661614,0.649404818000358,2.13514019846297E-6));
#129016=DIRECTION('ref_axis',(0.643909142906818,-0.754007109234366,-0.129824092159517));
#129017=DIRECTION('',(-1.20214177310824E-32,3.0881926820005E-32,-1.));
#129018=DIRECTION('center_axis',(0.0743391421060497,0.997233017880443,5.69527448431661E-32));
#129019=DIRECTION('ref_axis',(-0.997233017880443,0.0743391421060497,4.11084041927039E-32));
#129020=DIRECTION('center_axis',(-0.0743391421060833,-0.997233017880441,
-1.97365792993271E-14));
#129021=DIRECTION('ref_axis',(0.989752130775784,-0.0737814763252889,0.122257978782798));
#129022=DIRECTION('',(-0.729782852665251,0.054401960442657,0.681511125848848));
#129023=DIRECTION('',(3.67608397811134E-32,-5.98511211175597E-32,1.));
#129024=DIRECTION('',(-1.22906873758631E-33,-5.70191478903094E-32,1.));
#129025=DIRECTION('center_axis',(3.67608397811134E-32,-5.98511211175597E-32,
1.));
#129026=DIRECTION('ref_axis',(-0.452171907282676,-0.891930808002699,-3.67608397811135E-32));
#129027=DIRECTION('center_axis',(-0.302965055923595,0.153590711238846,-0.940543496235213));
#129028=DIRECTION('ref_axis',(0.838845814697296,-0.425393663698242,-0.339673269555049));
#129029=DIRECTION('center_axis',(-0.302965055923595,0.153590711238846,-0.940543496235213));
#129030=DIRECTION('ref_axis',(0.838845814697296,-0.425393663698242,-0.339673269555049));
#129031=DIRECTION('center_axis',(0.732177396727087,-0.0545804627065377,
-0.678923583927297));
#129032=DIRECTION('ref_axis',(0.631244341948513,-0.320014686676667,0.706485089063615));
#129033=DIRECTION('center_axis',(-0.476801507016236,0.558321672599552,0.678923583927297));
#129034=DIRECTION('ref_axis',(-0.631244341948511,0.320014686676674,-0.706485089063613));
#129035=DIRECTION('center_axis',(0.744062783317934,0.667667787917529,-0.0242960790763298));
#129036=DIRECTION('ref_axis',(-0.446942527076936,0.52445346295967,0.724700588298155));
#129037=DIRECTION('center_axis',(-3.67608397811134E-32,5.98511211175597E-32,
-1.));
#129038=DIRECTION('ref_axis',(0.45217190728268,0.891930808002697,3.67608397811132E-32));
#129039=DIRECTION('center_axis',(-4.90798928986758E-35,-4.11900193408512E-32,
1.));
#129040=DIRECTION('ref_axis',(0.503043593699387,-0.864261038597718,-3.55742395696821E-32));
#129041=DIRECTION('center_axis',(3.67608397811134E-32,-5.98511211175597E-32,
1.));
#129042=DIRECTION('ref_axis',(-0.45217190728268,-0.891930808002697,-3.67608397811132E-32));
#129043=DIRECTION('center_axis',(-0.729463945861552,0.054378187404888,0.681854357192688));
#129044=DIRECTION('ref_axis',(-0.633766178214033,0.321293153014888,-0.703641344136152));
#129045=DIRECTION('center_axis',(-0.730105850198729,0.0544260384255464,
0.681163162426516));
#129046=DIRECTION('ref_axis',(-0.633171645820725,0.320991749762727,-0.704313824593084));
#129047=DIRECTION('center_axis',(0.47545249445316,-0.556742015363827,-0.681163162426516));
#129048=DIRECTION('ref_axis',(0.633171645820723,-0.32099174976273,0.704313824593084));
#129049=DIRECTION('center_axis',(0.475034479697865,-0.556252531387972,-0.681854357192686));
#129050=DIRECTION('ref_axis',(0.633766178214041,-0.321293153014869,0.703641344136154));
#129051=DIRECTION('center_axis',(3.67608397811134E-32,-5.98511211175597E-32,
1.));
#129052=DIRECTION('ref_axis',(-0.45217190728268,-0.891930808002697,-3.67608397811132E-32));
#129053=DIRECTION('center_axis',(-4.90798928986758E-35,-4.11900193408512E-32,
1.));
#129054=DIRECTION('ref_axis',(0.994462996350255,0.105087339342442,4.37735767734634E-33));
#129055=DIRECTION('center_axis',(3.67608397811134E-32,-5.98511211175597E-32,
1.));
#129056=DIRECTION('ref_axis',(0.45217190728268,0.891930808002697,3.67608397811132E-32));
#129057=DIRECTION('center_axis',(-3.67608397811134E-32,5.98511211175597E-32,
-1.));
#129058=DIRECTION('ref_axis',(-0.452171907282677,-0.891930808002698,-3.67608397811134E-32));
#129059=DIRECTION('center_axis',(-0.704976643634714,-0.70923052100818,-1.3378980647817E-32));
#129060=DIRECTION('ref_axis',(0.70923052100818,-0.704976643634714,-6.71000662652026E-32));
#129061=DIRECTION('',(3.81575460846013E-32,-5.6792760918719E-32,1.));
#129062=DIRECTION('',(0.519020392965634,-0.515907372529247,-0.68151112584885));
#129063=DIRECTION('center_axis',(0.704980053244474,0.709227131829331,2.13514018106101E-6));
#129064=DIRECTION('ref_axis',(0.703225167629535,-0.699013639885662,-0.129824092009961));
#129065=DIRECTION('',(-1.11391841484537E-32,2.99364517920655E-32,-1.));
#129066=DIRECTION('center_axis',(-0.00719196407367123,0.999974137491947,
5.70657198160623E-32));
#129067=DIRECTION('ref_axis',(-0.999974137491947,-0.00719196407367123,3.77481077385863E-32));
#129068=DIRECTION('center_axis',(0.00719196407364449,-0.999974137491947,
-1.32083383781831E-14));
#129069=DIRECTION('ref_axis',(0.992472687497606,0.00713801251946082,0.122257978670317));
#129070=DIRECTION('',(-0.731788825245092,-0.00526313505855431,0.681511125848847));
#129071=DIRECTION('',(3.81575460846013E-32,-5.6792760918719E-32,1.));
#129072=DIRECTION('',(6.32137437729893E-35,-5.70667410741387E-32,1.));
#129073=DIRECTION('center_axis',(3.81575460846012E-32,-5.6792760918719E-32,
1.));
#129074=DIRECTION('ref_axis',(-0.377966701428894,-0.925819190020903,-3.81575460846015E-32));
#129075=DIRECTION('center_axis',(-0.314476033525425,0.128385186169416,-0.940543496235214));
#129076=DIRECTION('ref_axis',(0.870728157202492,-0.355604480011906,-0.339673269555046));
#129077=DIRECTION('center_axis',(-0.314476033525425,0.128385186169416,-0.940543496235214));
#129078=DIRECTION('ref_axis',(0.870728157202492,-0.355604480011906,-0.339673269555046));
#129079=DIRECTION('center_axis',(0.734189951250738,0.00528040431712579,
-0.678923583927297));
#129080=DIRECTION('ref_axis',(0.655228096310224,-0.267497590150746,0.706485089063614));
#129081=DIRECTION('center_axis',(-0.520723388857382,0.517600154061219,0.678923583927297));
#129082=DIRECTION('ref_axis',(-0.655228096310221,0.267497590150754,-0.706485089063614));
#129083=DIRECTION('center_axis',(0.687165852736339,0.726094202823528,-0.0242960790911833));
#129084=DIRECTION('ref_axis',(-0.488202805279804,0.486278075709505,0.724701079067218));
#129085=DIRECTION('center_axis',(-3.81575460846012E-32,5.6792760918719E-32,
-1.));
#129086=DIRECTION('ref_axis',(0.377966701428891,0.925819190020905,3.81575460846017E-32));
#129087=DIRECTION('center_axis',(-5.09446543185489E-35,-4.11941025987936E-32,
1.));
#129088=DIRECTION('ref_axis',(0.57181505569327,-0.820382558372923,-3.37657923595285E-32));
#129089=DIRECTION('center_axis',(3.81575460846013E-32,-5.6792760918719E-32,
1.));
#129090=DIRECTION('ref_axis',(-0.377966701428889,-0.925819190020905,-3.81575460846018E-32));
#129091=DIRECTION('center_axis',(-0.731469041854198,-0.00526083512840586,
0.681854357192688));
#129092=DIRECTION('ref_axis',(-0.657845748248876,0.26856624943046,-0.703641344136153));
#129093=DIRECTION('center_axis',(-0.732112710610057,-0.00526546449070042,
0.681163162426516));
#129094=DIRECTION('ref_axis',(-0.657228626949919,0.268314308982185,-0.704313824593084));
#129095=DIRECTION('center_axis',(0.519250108292791,-0.516135710052146,-0.681163162426516));
#129096=DIRECTION('ref_axis',(0.65722862694992,-0.268314308982184,0.704313824593083));
#129097=DIRECTION('center_axis',(0.518793586958931,-0.515681926877058,-0.681854357192686));
#129098=DIRECTION('ref_axis',(0.657845748248881,-0.268566249430445,0.703641344136154));
#129099=DIRECTION('center_axis',(3.81575460846012E-32,-5.6792760918719E-32,
1.));
#129100=DIRECTION('ref_axis',(-0.377966701428889,-0.925819190020905,-3.81575460846018E-32));
#129101=DIRECTION('center_axis',(-5.09446543185489E-35,-4.11941025987936E-32,
1.));
#129102=DIRECTION('ref_axis',(0.982588409027654,0.18579563623644,7.70374212836736E-33));
#129103=DIRECTION('center_axis',(3.81575460846013E-32,-5.6792760918719E-32,
1.));
#129104=DIRECTION('ref_axis',(0.377966701428909,0.925819190020897,3.81575460846005E-32));
#129105=DIRECTION('center_axis',(-3.81575460846012E-32,5.6792760918719E-32,
-1.));
#129106=DIRECTION('ref_axis',(-0.377966701428898,-0.925819190020902,-3.81575460846012E-32));
#129107=DIRECTION('center_axis',(-0.644822020372411,-0.764332756097003,
-1.56500138014059E-32));
#129108=DIRECTION('ref_axis',(0.764332756097004,-0.644822020372411,-6.46207994341907E-32));
#129109=DIRECTION('',(3.9300320214448E-32,-5.363073263102E-32,1.));
#129110=DIRECTION('',(0.559344635735722,-0.471885752929575,-0.681511125848846));
#129111=DIRECTION('center_axis',(0.644825694886489,0.76432965611024,2.13514017444585E-6));
#129112=DIRECTION('ref_axis',(0.757861344882821,-0.639368350086046,-0.129824091911515));
#129113=DIRECTION('',(-1.0182821133153E-32,2.90660329815265E-32,-1.));
#129114=DIRECTION('center_axis',(-0.0886752089190725,0.996060594202561,
5.6904423517575E-32));
#129115=DIRECTION('ref_axis',(-0.996060594202561,-0.0886752089190725,3.43897838846154E-32));
#129116=DIRECTION('center_axis',(0.0886752089190568,-0.996060594202562,
-1.22948139818278E-14));
#129117=DIRECTION('ref_axis',(0.988588502211445,0.0880099990691413,0.122257978713791));
#129118=DIRECTION('',(-0.728924863929587,-0.0648932052642919,0.681511125848845));
#129119=DIRECTION('',(3.9300320214448E-32,-5.363073263102E-32,1.));
#129120=DIRECTION('',(1.355075548097E-33,-5.70088428763789E-32,1.));
#129121=DIRECTION('center_axis',(3.9300320214448E-32,-5.363073263102E-32,
1.));
#129122=DIRECTION('ref_axis',(-0.301246189537227,-0.95354639807893,-3.93003202144479E-32));
#129123=DIRECTION('center_axis',(-0.323894225009133,0.102325278868117,-0.94054349623518));
#129124=DIRECTION('ref_axis',(0.896815947481311,-0.283448807182034,-0.339673269555142));
#129125=DIRECTION('center_axis',(-0.323894225009133,0.102325278868117,-0.94054349623518));
#129126=DIRECTION('ref_axis',(0.896815947481311,-0.283448807182034,-0.339673269555142));
#129127=DIRECTION('center_axis',(0.731316592781632,0.0651061311212643,-0.678923583927297));
#129128=DIRECTION('ref_axis',(0.674851415796019,-0.213200341296364,0.706485089063614));
#129129=DIRECTION('center_axis',(-0.561179942458995,0.473434091895624,0.678923583927297));
#129130=DIRECTION('ref_axis',(-0.674851415796018,0.213200341296369,-0.706485089063613));
#129131=DIRECTION('center_axis',(0.625695946790193,0.779688580595619,-0.0242960790892782));
#129132=DIRECTION('ref_axis',(-0.526214352956803,0.444866830484855,0.724701288722887));
#129133=DIRECTION('center_axis',(-3.9300320214448E-32,5.363073263102E-32,
-1.));
#129134=DIRECTION('ref_axis',(0.301246189537228,0.95354639807893,3.93003202144479E-32));
#129135=DIRECTION('center_axis',(-5.24703874692173E-35,-4.11983242653994E-32,
1.));
#129136=DIRECTION('ref_axis',(0.636781182834359,-0.771044567575749,-3.17323319626639E-32));
#129137=DIRECTION('center_axis',(3.9300320214448E-32,-5.363073263102E-32,
1.));
#129138=DIRECTION('ref_axis',(-0.301246189537228,-0.95354639807893,-3.93003202144479E-32));
#129139=DIRECTION('center_axis',(-0.728606332057201,-0.064864847671897,
0.681854357192688));
#129140=DIRECTION('ref_axis',(-0.677547463366032,0.214052081766387,-0.703641344136153));
#129141=DIRECTION('center_axis',(-0.72924748172237,-0.0649219266095021,
0.681163162426516));
#129142=DIRECTION('ref_axis',(-0.676911860001852,0.21385128074411,-0.704313824593084));
#129143=DIRECTION('center_axis',(0.559592198331971,-0.472094606746467,-0.681163162426516));
#129144=DIRECTION('ref_axis',(0.676911860001849,-0.213851280744116,0.704313824593085));
#129145=DIRECTION('center_axis',(0.559100208493701,-0.471679544224305,-0.681854357192686));
#129146=DIRECTION('ref_axis',(0.677547463366035,-0.214052081766373,0.703641344136154));
#129147=DIRECTION('center_axis',(3.9300320214448E-32,-5.363073263102E-32,
1.));
#129148=DIRECTION('ref_axis',(-0.301246189537228,-0.95354639807893,-3.93003202144479E-32));
#129149=DIRECTION('center_axis',(-5.24703874692173E-35,-4.11983242653994E-32,
1.));
#129150=DIRECTION('ref_axis',(0.96417485795865,0.265267493825414,1.09791668560744E-32));
#129151=DIRECTION('center_axis',(3.9300320214448E-32,-5.363073263102E-32,
1.));
#129152=DIRECTION('ref_axis',(0.301246189537229,0.953546398078929,3.93003202144478E-32));
#129153=DIRECTION('center_axis',(-3.9300320214448E-32,5.363073263102E-32,
-1.));
#129154=DIRECTION('ref_axis',(-0.301246189537225,-0.95354639807893,-3.9300320214448E-32));
#129155=DIRECTION('center_axis',(-0.580376212952675,-0.81434848280003,-1.77114070164055E-32));
#129156=DIRECTION('ref_axis',(0.81434848280003,-0.580376212952675,-6.19646718737732E-32));
#129157=DIRECTION('',(4.0181557197364E-32,-5.03860790310193E-32,1.));
#129158=DIRECTION('',(0.595946532240344,-0.42472381149983,-0.681511125848849));
#129159=DIRECTION('center_axis',(0.580380127917873,0.814345692635182,2.13514021281083E-6));
#129160=DIRECTION('ref_axis',(0.807454079866993,-0.575468169361725,-0.129824092361983));
#129161=DIRECTION('',(-9.15869312325847E-33,2.82764628819631E-32,-1.));
#129162=DIRECTION('center_axis',(-0.169568334879497,0.985518431997187,5.64699293479588E-32));
#129163=DIRECTION('ref_axis',(-0.985518431997187,-0.169568334879497,3.10557817219548E-32));
#129164=DIRECTION('center_axis',(0.169568334879536,-0.985518431997181,1.77457480648256E-14));
#129165=DIRECTION('ref_axis',(0.978125423555369,0.168296293595959,0.122257978702795));
#129166=DIRECTION('',(-0.72121002790876,-0.124091421895629,0.68151112584885));
#129167=DIRECTION('',(4.0181557197364E-32,-5.03860790310193E-32,1.));
#129168=DIRECTION('',(2.63791954822017E-33,-5.68458385999836E-32,1.));
#129169=DIRECTION('center_axis',(4.0181557197364E-32,-5.03860790310193E-32,
1.));
#129170=DIRECTION('ref_axis',(-0.222520933956311,-0.974927912181825,-4.01815571973637E-32));
#129171=DIRECTION('center_axis',(-0.331156953863924,0.0755844137183558,
-0.940543496235245));
#129172=DIRECTION('ref_axis',(0.916935575593894,-0.209406829306347,-0.339673269554959));
#129173=DIRECTION('center_axis',(-0.331156953863924,0.0755844137183558,
-0.940543496235245));
#129174=DIRECTION('ref_axis',(0.916935575593894,-0.209406829306347,-0.339673269554959));
#129175=DIRECTION('center_axis',(0.723576443046308,0.124498587364546,-0.678923583927297));
#129176=DIRECTION('ref_axis',(0.689983710452336,-0.157484279346239,0.706485089063614));
#129177=DIRECTION('center_axis',(-0.597901936131716,0.42611740395959,0.678923583927297));
#129178=DIRECTION('ref_axis',(-0.689983710452336,0.157484279346243,-0.706485089063614));
#129179=DIRECTION('center_axis',(0.560062137560471,0.828094259497534,-0.0242960790751506));
#129180=DIRECTION('ref_axis',(-0.560724628992771,0.40049549721625,0.724700798364696));
#129181=DIRECTION('center_axis',(-4.0181557197364E-32,5.03860790310193E-32,
-1.));
#129182=DIRECTION('ref_axis',(0.222520933956312,0.974927912181824,4.01815571973637E-32));
#129183=DIRECTION('center_axis',(-5.36469388482745E-35,-4.12026562461737E-32,
1.));
#129184=DIRECTION('ref_axis',(0.697509636265186,-0.716575402394757,-2.9487390722532E-32));
#129185=DIRECTION('center_axis',(4.0181557197364E-32,-5.03860790310193E-32,
1.));
#129186=DIRECTION('ref_axis',(-0.222520933956312,-0.974927912181824,-4.01815571973637E-32));
#129187=DIRECTION('center_axis',(-0.720894867331946,-0.124037195356078,
0.681854357192688));
#129188=DIRECTION('ref_axis',(-0.692740211901948,0.158113432814269,-0.703641344136153));
#129189=DIRECTION('center_axis',(-0.721529231161186,-0.124146344018081,
0.681163162426516));
#129190=DIRECTION('ref_axis',(-0.692090356308068,0.157965107515661,-0.704313824593084));
#129191=DIRECTION('center_axis',(0.596210294617465,-0.424911791723016,-0.681163162426516));
#129192=DIRECTION('ref_axis',(0.692090356308068,-0.157965107515664,0.704313824593083));
#129193=DIRECTION('center_axis',(0.595686110385987,-0.424538212026387,-0.681854357192686));
#129194=DIRECTION('ref_axis',(0.692740211901949,-0.158113432814256,0.703641344136154));
#129195=DIRECTION('center_axis',(4.0181557197364E-32,-5.03860790310193E-32,
1.));
#129196=DIRECTION('ref_axis',(-0.222520933956312,-0.974927912181824,-4.01815571973637E-32));
#129197=DIRECTION('center_axis',(-5.36469388482745E-35,-4.12026562461737E-32,
1.));
#129198=DIRECTION('ref_axis',(0.939344882287581,0.342974040009052,1.41818344493119E-32));
#129199=DIRECTION('center_axis',(4.0181557197364E-32,-5.03860790310193E-32,
1.));
#129200=DIRECTION('ref_axis',(0.222520933956292,0.974927912181829,4.01815571973647E-32));
#129201=DIRECTION('center_axis',(-4.0181557197364E-32,5.03860790310193E-32,
-1.));
#129202=DIRECTION('ref_axis',(-0.222520933956305,-0.974927912181826,-4.0181557197364E-32));
#129203=DIRECTION('center_axis',(-0.512068097591075,-0.858944854708064,
-1.9549442061076E-32));
#129204=DIRECTION('ref_axis',(0.858944854708064,-0.512068097591075,-5.91493596746345E-32));
#129205=DIRECTION('',(4.07953925466219E-32,-4.7080392753095E-32,1.));
#129206=DIRECTION('',(0.628582502897166,-0.374735403179047,-0.681511125848853));
#129207=DIRECTION('center_axis',(0.512072226953903,0.858942392933258,2.13514021047182E-6));
#129208=DIRECTION('ref_axis',(0.851673341205892,-0.507738342948244,-0.12982409244575));
#129209=DIRECTION('',(-8.07361552170662E-33,2.75729959521181E-32,-1.));
#129210=DIRECTION('center_axis',(-0.249333011548104,0.968417807225968,5.57651287942259E-32));
#129211=DIRECTION('ref_axis',(-0.968417807225968,-0.249333011548104,2.77682884849255E-32));
#129212=DIRECTION('center_axis',(0.24933301154813,-0.968417807225962,1.37386436630902E-14));
#129213=DIRECTION('ref_axis',(0.961153081584414,0.247462604055867,0.122257978695353));
#129214=DIRECTION('',(-0.708695658143485,-0.182463830587896,0.681511125848848));
#129215=DIRECTION('',(4.07953925466219E-32,-4.7080392753095E-32,1.));
#129216=DIRECTION('',(3.90320862897602E-33,-5.65788130115185E-32,1.));
#129217=DIRECTION('center_axis',(4.07953925466219E-32,-4.7080392753095E-32,
1.));
#129218=DIRECTION('ref_axis',(-0.142314838273275,-0.989821441880934,-4.07953925466219E-32));
#129219=DIRECTION('center_axis',(-0.336215887828166,0.0483405467659331,
-0.940543496235176));
#129220=DIRECTION('ref_axis',(0.930953148734462,-0.133971283531599,-0.339673269555151));
#129221=DIRECTION('center_axis',(-0.336215887828166,0.0483405467659331,
-0.940543496235176));
#129222=DIRECTION('ref_axis',(0.930953148734462,-0.133971283531599,-0.339673269555151));
#129223=DIRECTION('center_axis',(0.71102101146422,0.183062526049738,-0.678923583927297));
#129224=DIRECTION('ref_axis',(0.700524277354893,-0.100720185500137,0.706485089063614));
#129225=DIRECTION('center_axis',(-0.630644991066356,0.375964975004627,0.678923583927297));
#129226=DIRECTION('ref_axis',(-0.700524277354893,0.100720185500142,-0.706485089063613));
#129227=DIRECTION('center_axis',(0.490701207201861,0.870989107734654,-0.0242960790710487));
#129228=DIRECTION('ref_axis',(-0.591503219222111,0.353458754255722,0.724700524830686));
#129229=DIRECTION('center_axis',(-4.07953925466219E-32,4.7080392753095E-32,
-1.));
#129230=DIRECTION('ref_axis',(0.142314838273279,0.989821441880934,4.07953925466217E-32));
#129231=DIRECTION('center_axis',(-5.44664787004196E-35,-4.12070697124994E-32,
1.));
#129232=DIRECTION('ref_axis',(0.753596278147652,-0.657337546137452,-2.70459083526968E-32));
#129233=DIRECTION('center_axis',(4.07953925466219E-32,-4.7080392753095E-32,
1.));
#129234=DIRECTION('ref_axis',(-0.142314838273279,-0.989821441880934,-4.07953925466217E-32));
#129235=DIRECTION('center_axis',(-0.708385966203879,-0.182384095969861,
0.681854357192688));
#129236=DIRECTION('ref_axis',(-0.703322888621747,0.101122565053652,-0.703641344136153));
#129237=DIRECTION('center_axis',(-0.709009322610568,-0.182544587989925,
0.681163162426516));
#129238=DIRECTION('ref_axis',(-0.702663105479925,0.101027702559104,-0.704313824593084));
#129239=DIRECTION('center_axis',(0.628860709760055,-0.37490125883116,-0.681163162426516));
#129240=DIRECTION('ref_axis',(0.702663105479925,-0.101027702559108,0.704313824593083));
#129241=DIRECTION('center_axis',(0.628307819494945,-0.374571648071308,-0.681854357192686));
#129242=DIRECTION('ref_axis',(0.703322888621748,-0.101122565053635,0.703641344136154));
#129243=DIRECTION('center_axis',(4.07953925466219E-32,-4.7080392753095E-32,
1.));
#129244=DIRECTION('ref_axis',(-0.142314838273279,-0.989821441880934,-4.07953925466217E-32));
#129245=DIRECTION('center_axis',(-5.44664787004196E-35,-4.12070697124994E-32,
1.));
#129246=DIRECTION('ref_axis',(0.908263721405892,0.41839815054314,1.72904316836483E-32));
#129247=DIRECTION('center_axis',(4.07953925466219E-32,-4.7080392753095E-32,
1.));
#129248=DIRECTION('ref_axis',(0.142314838273279,0.989821441880934,4.07953925466217E-32));
#129249=DIRECTION('center_axis',(-4.07953925466219E-32,4.7080392753095E-32,
-1.));
#129250=DIRECTION('ref_axis',(-0.142314838273276,-0.989821441880934,-4.07953925466219E-32));
#129251=DIRECTION('center_axis',(-0.440352253525294,-0.897825090323942,
-2.11518871154494E-32));
#129252=DIRECTION('ref_axis',(0.897825090323942,-0.440352253525294,-5.61935982749661E-32));
#129253=DIRECTION('',(4.1137741289248E-32,-4.37356725940266E-32,1.));
#129254=DIRECTION('',(0.657035360706032,-0.322253192577091,-0.68151112584885));
#129255=DIRECTION('center_axis',(0.440356569805478,0.89782297332191,2.13514019612196E-6));
#129256=DIRECTION('ref_axis',(0.890224857059004,-0.436629601676368,-0.129824091809693));
#129257=DIRECTION('',(-6.93480934091059E-33,2.69603136483456E-32,-1.));
#129258=DIRECTION('center_axis',(-0.32743841816191,0.944872521725352,5.47947121877776E-32));
#129259=DIRECTION('ref_axis',(-0.944872521725352,-0.32743841816191,2.45491818986216E-32));
#129260=DIRECTION('center_axis',(0.327438418161922,-0.944872521725348,7.70890561095581E-15));
#129261=DIRECTION('ref_axis',(0.937784424431734,0.324982091713398,0.122257978712338));
#129262=DIRECTION('',(-0.691465035699815,-0.239621972592011,0.68151112584885));
#129263=DIRECTION('',(4.1137741289248E-32,-4.37356725940266E-32,1.));
#129264=DIRECTION('',(5.14252250029012E-33,-5.62095431222185E-32,1.));
#129265=DIRECTION('center_axis',(4.1137741289248E-32,-4.37356725940266E-32,
1.));
#129266=DIRECTION('ref_axis',(-0.0611616608218378,-0.998127873193367,-4.11377412892478E-32));
#129267=DIRECTION('center_axis',(-0.339037360530528,0.0207749814503773,
-0.940543496235145));
#129268=DIRECTION('ref_axis',(0.938775382266798,-0.0576441809680795,-0.339673269555239));
#129269=DIRECTION('center_axis',(-0.339037360530528,0.0207749814503773,
-0.940543496235145));
#129270=DIRECTION('ref_axis',(0.938775382266798,-0.0576441809680795,-0.339673269555239));
#129271=DIRECTION('center_axis',(0.693733852361048,0.24040821382726,-0.678923583927297));
#129272=DIRECTION('ref_axis',(0.706402970770023,-0.0432858154371954,0.706485089063614));
#129273=DIRECTION('center_axis',(-0.659191207634549,0.323310561170864,0.678923583927297));
#129274=DIRECTION('ref_axis',(-0.706402970770023,0.0432858154371997,-0.706485089063614));
#129275=DIRECTION('center_axis',(0.418074741256616,0.908087667169007,-0.0242960790821249));
#129276=DIRECTION('ref_axis',(-0.618344947077174,0.304069531647683,0.724700797810852));
#129277=DIRECTION('center_axis',(-4.1137741289248E-32,4.37356725940266E-32,
-1.));
#129278=DIRECTION('ref_axis',(0.0611616608218271,0.998127873193368,4.11377412892482E-32));
#129279=DIRECTION('center_axis',(-5.49235531231592E-35,-4.12115352934861E-32,
1.));
#129280=DIRECTION('ref_axis',(0.804667861133691,-0.593725216963649,-2.44241325155126E-32));
#129281=DIRECTION('center_axis',(4.1137741289248E-32,-4.37356725940266E-32,
1.));
#129282=DIRECTION('ref_axis',(-0.0611616608218271,-0.998127873193368,-4.11377412892482E-32));
#129283=DIRECTION('center_axis',(-0.691162873346182,-0.239517260516223,
0.681854357192688));
#129284=DIRECTION('ref_axis',(-0.709225067557877,0.0434587433066506,-0.703641344136153));
#129285=DIRECTION('center_axis',(-0.691771073996281,-0.239728027846433,
0.681163162426516));
#129286=DIRECTION('ref_axis',(-0.708559747616065,0.0434179749104152,-0.704313824593084));
#129287=DIRECTION('center_axis',(0.657326160633905,-0.322395819916137,-0.681163162426516));
#129288=DIRECTION('ref_axis',(0.708559747616065,-0.0434179749104186,0.704313824593084));
#129289=DIRECTION('center_axis',(0.656748243728657,-0.322112371598286,-0.681854357192686));
#129290=DIRECTION('ref_axis',(0.709225067557877,-0.0434587433066342,0.703641344136154));
#129291=DIRECTION('center_axis',(4.1137741289248E-32,-4.37356725940266E-32,
1.));
#129292=DIRECTION('ref_axis',(-0.0611616608218271,-0.998127873193368,-4.11377412892482E-32));
#129293=DIRECTION('center_axis',(-5.49235531231592E-35,-4.12115352934861E-32,
1.));
#129294=DIRECTION('ref_axis',(0.87113821531121,0.491037890416208,2.02842713573728E-32));
#129295=DIRECTION('center_axis',(4.1137741289248E-32,-4.37356725940266E-32,
1.));
#129296=DIRECTION('ref_axis',(0.0611616608218468,0.998127873193367,4.11377412892474E-32));
#129297=DIRECTION('center_axis',(-4.1137741289248E-32,4.37356725940266E-32,
-1.));
#129298=DIRECTION('ref_axis',(-0.061161660821833,-0.998127873193367,-4.1137741289248E-32));
#129299=DIRECTION('center_axis',(-0.365705937865311,-0.930730448094427,
-2.25080781720738E-32));
#129300=DIRECTION('ref_axis',(0.930730448094427,-0.365705937865311,-5.31170577792164E-32));
#129301=DIRECTION('',(4.12063251508437E-32,-4.03741771146329E-32,1.));
#129302=DIRECTION('',(0.681115756592598,-0.267626440146573,-0.681511125848849));
#129303=DIRECTION('center_axis',(0.365710412338692,0.930728689953471,2.13514017632895E-6));
#129304=DIRECTION('ref_axis',(0.922852073287589,-0.362615162399107,-0.129824091859205));
#129305=DIRECTION('',(-5.74985314811383E-33,2.64424932702918E-32,-1.));
#129306=DIRECTION('center_axis',(-0.403364776126385,0.915039265485646,5.35651374910222E-32));
#129307=DIRECTION('ref_axis',(-0.915039265485647,-0.403364776126385,2.14198845862598E-32));
#129308=DIRECTION('center_axis',(0.403364776126428,-0.915039265485627,1.55704628181689E-14));
#129309=DIRECTION('ref_axis',(0.908174966659921,0.400338877169377,0.122257978713101));
#129310=DIRECTION('',(-0.669632827527271,-0.295185469903366,0.681511125848845));
#129311=DIRECTION('',(4.12063251508437E-32,-4.03741771146329E-32,1.));
#129312=DIRECTION('',(6.34761373282129E-33,-5.57404863622719E-32,1.));
#129313=DIRECTION('center_axis',(4.12063251508437E-32,-4.03741771146329E-32,
1.));
#129314=DIRECTION('ref_axis',(0.0203985373914164,-0.999791928189206,-4.12063251508437E-32));
#129315=DIRECTION('center_axis',(-0.339602595535508,-0.00692883793910648,
-0.940543496235214));
#129316=DIRECTION('ref_axis',(0.940350220517251,0.0190665341093361,-0.339673269555047));
#129317=DIRECTION('center_axis',(-0.339602595535508,-0.00692883793910648,
-0.940543496235214));
#129318=DIRECTION('ref_axis',(0.940350220517251,0.0190665341093361,-0.339673269555047));
#129319=DIRECTION('center_axis',(0.671830008928442,0.296154024606325,-0.678923583927297));
#129320=DIRECTION('ref_axis',(0.707580668962965,0.0144366145858262,0.706485089063614));
#129321=DIRECTION('center_axis',(-0.683350615474828,0.268504568894996,0.678923583927297));
#129322=DIRECTION('ref_axis',(-0.707580668962965,-0.0144366145858181,-0.706485089063614));
#129323=DIRECTION('center_axis',(0.342666056897038,0.939143052996711,-0.0242960790798164));
#129324=DIRECTION('ref_axis',(-0.641072217977139,0.252657004280955,0.72470052402744));
#129325=DIRECTION('center_axis',(-4.12063251508437E-32,4.03741771146329E-32,
-1.));
#129326=DIRECTION('ref_axis',(-0.0203985373914165,0.999791928189206,4.12063251508437E-32));
#129327=DIRECTION('center_axis',(-5.50151203615979E-35,-4.12160232714292E-32,
1.));
#129328=DIRECTION('ref_axis',(0.850384512264717,-0.526161744428744,-2.16395106966151E-32));
#129329=DIRECTION('center_axis',(4.12063251508437E-32,-4.03741771146329E-32,
1.));
#129330=DIRECTION('ref_axis',(0.0203985373914165,-0.999791928189206,-4.12063251508437E-32));
#129331=DIRECTION('center_axis',(-0.669340205600213,-0.295056477211415,
0.681854357192688));
#129332=DIRECTION('ref_axis',(-0.710407470683308,-0.0144942892068705,-0.703641344136153));
#129333=DIRECTION('center_axis',(-0.669929203018742,-0.295316117229964,
0.681163162426516));
#129334=DIRECTION('ref_axis',(-0.70974104153595,-0.0144806921978409,-0.704313824593084));
#129335=DIRECTION('center_axis',(0.681417214359919,-0.267744890011138,-0.681163162426516));
#129336=DIRECTION('ref_axis',(0.70974104153595,0.014480692197839,0.704313824593084));
#129337=DIRECTION('center_axis',(0.680818116756189,-0.267509490437078,-0.681854357192686));
#129338=DIRECTION('ref_axis',(0.710407470683307,0.0144942892068817,0.703641344136154));
#129339=DIRECTION('center_axis',(4.12063251508437E-32,-4.03741771146329E-32,
1.));
#129340=DIRECTION('ref_axis',(0.0203985373914165,-0.999791928189206,-4.12063251508437E-32));
#129341=DIRECTION('center_axis',(-5.50151203615979E-35,-4.12160232714292E-32,
1.));
#129342=DIRECTION('ref_axis',(0.828215428121325,0.560409854144099,2.31434299614049E-32));
#129343=DIRECTION('center_axis',(4.12063251508437E-32,-4.03741771146329E-32,
1.));
#129344=DIRECTION('ref_axis',(-0.0203985373914165,0.999791928189206,4.12063251508437E-32));
#129345=DIRECTION('center_axis',(-4.12063251508437E-32,4.03741771146329E-32,
-1.));
#129346=DIRECTION('ref_axis',(0.0203985373914152,-0.999791928189206,-4.12063251508436E-32));
#129347=DIRECTION('center_axis',(-0.288625909526066,-0.957441948292559,
-2.36089900032231E-32));
#129348=DIRECTION('ref_axis',(0.957441948292559,-0.288625909526066,-4.99402120567912E-32));
#129349=DIRECTION('',(4.10006877171256E-32,-3.70182765127214E-32,1.));
#129350=DIRECTION('',(0.700663439495224,-0.211218677912134,-0.681511125848854));
#129351=DIRECTION('center_axis',(0.288630512415857,0.957440560712779,2.13514019988738E-6));
#129352=DIRECTION('ref_axis',(0.949337861193843,-0.286187579034176,-0.129824092180372));
#129353=DIRECTION('',(-4.52663263127535E-33,2.60229808271384E-32,-1.));
#129354=DIRECTION('center_axis',(-0.476606808056242,0.879116573904986,5.20845873207011E-32));
#129355=DIRECTION('ref_axis',(-0.879116573904986,-0.476606808056242,1.84012215051561E-32));
#129356=DIRECTION('center_axis',(0.476606808056274,-0.879116573904968,1.26700824892938E-14));
#129357=DIRECTION('ref_axis',(0.872521754329768,0.473031473452491,0.122257978654438));
#129358=DIRECTION('',(-0.643344323369171,-0.348784556614691,0.681511125848843));
#129359=DIRECTION('',(4.10006877171256E-32,-3.70182765127214E-32,1.));
#129360=DIRECTION('',(7.51046264324308E-33,-5.5174764227027E-32,1.));
#129361=DIRECTION('center_axis',(4.10006877171256E-32,-3.70182765127214E-32,
1.));
#129362=DIRECTION('ref_axis',(0.101822986703851,-0.994802532857002,-4.10006877171258E-32));
#129363=DIRECTION('center_axis',(-0.337907831297874,-0.0345865470552825,
-0.940543496235214));
#129364=DIRECTION('ref_axis',(0.935667183196969,0.0956503645473177,-0.339673269555046));
#129365=DIRECTION('center_axis',(-0.337907831297874,-0.0345865470552825,
-0.940543496235214));
#129366=DIRECTION('ref_axis',(0.935667183196969,0.0956503645473177,-0.339673269555046));
#129367=DIRECTION('center_axis',(0.645455247630566,0.349928979213609,-0.678923583927297));
#129368=DIRECTION('ref_axis',(0.704049534546552,0.0720629713206514,0.706485089063614));
#129369=DIRECTION('center_axis',(-0.702962437714038,0.211911723013268,0.678923583927297));
#129370=DIRECTION('ref_axis',(-0.704049534546553,-0.072062971320643,-0.706485089063614));
#129371=DIRECTION('center_axis',(0.264976986461482,0.96394859675559,-0.0242960790812061));
#129372=DIRECTION('ref_axis',(-0.65953300266963,0.199562973807333,0.724700515989023));
#129373=DIRECTION('center_axis',(-4.10006877171256E-32,3.70182765127214E-32,
-1.));
#129374=DIRECTION('ref_axis',(-0.101822986703844,0.994802532857003,4.10006877171255E-32));
#129375=DIRECTION('center_axis',(-5.47405710508952E-35,-4.1220503779576E-32,
1.));
#129376=DIRECTION('ref_axis',(0.890441994770205,-0.455096752295222,-1.87105740947765E-32));
#129377=DIRECTION('center_axis',(4.10006877171256E-32,-3.70182765127214E-32,
1.));
#129378=DIRECTION('ref_axis',(0.101822986703844,-0.994802532857003,-4.10006877171255E-32));
#129379=DIRECTION('center_axis',(-0.643063189219336,-0.348632141731658,
0.681854357192688));
#129380=DIRECTION('ref_axis',(-0.706862229300326,-0.072350864617104,-0.703641344136153));
#129381=DIRECTION('center_axis',(-0.643629063725651,-0.348938926577059,
0.681163162426516));
#129382=DIRECTION('ref_axis',(-0.706199125923442,-0.0722829926886655,-0.704313824593083));
#129383=DIRECTION('center_axis',(0.700973548950295,-0.211312162037912,-0.681163162426516));
#129384=DIRECTION('ref_axis',(0.706199125923442,0.0722829926886657,0.704313824593083));
#129385=DIRECTION('center_axis',(0.70035725754379,-0.211126377752971,-0.681854357192686));
#129386=DIRECTION('ref_axis',(0.706862229300322,0.0723508646171196,0.703641344136154));
#129387=DIRECTION('center_axis',(4.10006877171256E-32,-3.70182765127214E-32,
1.));
#129388=DIRECTION('ref_axis',(0.101822986703844,-0.994802532857003,-4.10006877171255E-32));
#129389=DIRECTION('center_axis',(-5.47405710508952E-35,-4.1220503779576E-32,
1.));
#129390=DIRECTION('ref_axis',(0.779781003903207,0.626052382753797,2.58488802669637E-32));
#129391=DIRECTION('center_axis',(4.10006877171256E-32,-3.70182765127214E-32,
1.));
#129392=DIRECTION('ref_axis',(-0.101822986703844,0.994802532857003,4.10006877171255E-32));
#129393=DIRECTION('center_axis',(-4.10006877171256E-32,3.70182765127214E-32,
-1.));
#129394=DIRECTION('ref_axis',(0.101822986703845,-0.994802532857003,-4.10006877171256E-32));
#129395=DIRECTION('center_axis',(-0.209625123378848,-0.977781830291606,
-2.44472962222986E-32));
#129396=DIRECTION('ref_axis',(0.977781830291606,-0.209625123378848,-4.66842024918305E-32));
#129397=DIRECTION('',(4.05221974712874E-32,-3.36903037531133E-32,1.));
#129398=DIRECTION('',(0.715548322809352,-0.153405290224818,-0.681511125848847));
#129399=DIRECTION('center_axis',(0.209629824053555,0.977780822507128,2.13514020421289E-6));
#129400=DIRECTION('ref_axis',(0.969505962273401,-0.207855464557473,-0.129824092409397));
#129401=DIRECTION('',(-3.27328812111754E-33,2.57045681049798E-32,-1.));
#129402=DIRECTION('center_axis',(-0.546677100313074,0.837343506569012,5.03629144939242E-32));
#129403=DIRECTION('ref_axis',(-0.837343506569012,-0.546677100313074,1.5513281360071E-32));
#129404=DIRECTION('center_axis',(0.54667710031302,-0.837343506569048,-3.81120151987269E-14));
#129405=DIRECTION('ref_axis',(0.831062053671047,0.542576123319591,0.122257978682561));
#129406=DIRECTION('',(-0.612774468883382,-0.400062539647147,0.681511125848848));
#129407=DIRECTION('',(4.05221974712874E-32,-3.36903037531133E-32,1.));
#129408=DIRECTION('',(8.62333066391321E-33,-5.45161415039564E-32,1.));
#129409=DIRECTION('center_axis',(4.05221974712873E-32,-3.36903037531133E-32,
1.));
#129410=DIRECTION('ref_axis',(0.182569820839374,-0.983192890799501,-4.05221974712874E-32));
#129411=DIRECTION('center_axis',(-0.333964346193833,-0.0620140884071742,
-0.94054349623521));
#129412=DIRECTION('ref_axis',(0.924757435146628,0.171597657591262,-0.339673269555057));
#129413=DIRECTION('center_axis',(-0.333964346193833,-0.0620140884071742,
-0.94054349623521));
#129414=DIRECTION('ref_axis',(0.924757435146628,0.171597657591262,-0.339673269555057));
#129415=DIRECTION('center_axis',(0.614785088152329,0.401375214198445,-0.678923583927297));
#129416=DIRECTION('ref_axis',(0.695833066637727,0.129209760870893,0.706485089063614));
#129417=DIRECTION('center_axis',(-0.717896160910899,0.153908639577859,0.678923583927297));
#129418=DIRECTION('ref_axis',(-0.695833066637729,-0.129209760870885,-0.706485089063614));
#129419=DIRECTION('center_axis',(0.185524537903959,0.982339221642399,-0.0242960790772642));
#129420=DIRECTION('ref_axis',(-0.673604703596412,0.145140883200304,0.724700508704544));
#129421=DIRECTION('center_axis',(-4.05221974712873E-32,3.36903037531133E-32,
-1.));
#129422=DIRECTION('ref_axis',(-0.182569820839372,0.983192890799501,4.05221974712873E-32));
#129423=DIRECTION('center_axis',(-5.41017322714046E-35,-4.12249470008839E-32,
1.));
#129424=DIRECTION('ref_axis',(0.924573732713069,-0.381003166360887,-1.56568142998441E-32));
#129425=DIRECTION('center_axis',(4.05221974712874E-32,-3.36903037531133E-32,
1.));
#129426=DIRECTION('ref_axis',(0.182569820839372,-0.983192890799501,-4.05221974712873E-32));
#129427=DIRECTION('center_axis',(-0.612506693412162,-0.399887716868931,
0.681854357192688));
#129428=DIRECTION('ref_axis',(-0.698612936405406,-0.129725956960371,-0.703641344136153));
#129429=DIRECTION('center_axis',(-0.613045679204787,-0.400239604938655,
0.681163162426516));
#129430=DIRECTION('ref_axis',(-0.697957571642567,-0.129604261789008,-0.704313824593084));
#129431=DIRECTION('center_axis',(0.715865020224902,-0.153473186490375,-0.681163162426516));
#129432=DIRECTION('ref_axis',(0.697957571642568,0.129604261789002,0.704313824593084));
#129433=DIRECTION('center_axis',(0.715235636333251,-0.153338253858317,-0.681854357192686));
#129434=DIRECTION('ref_axis',(0.698612936405403,0.129725956960381,0.703641344136154));
#129435=DIRECTION('center_axis',(4.05221974712873E-32,-3.36903037531133E-32,
1.));
#129436=DIRECTION('ref_axis',(0.182569820839373,-0.983192890799501,-4.05221974712874E-32));
#129437=DIRECTION('center_axis',(-5.41017322714046E-35,-4.12249470008839E-32,
1.));
#129438=DIRECTION('ref_axis',(0.726157265758936,0.687528636047624,2.83826179486323E-32));
#129439=DIRECTION('center_axis',(4.05221974712874E-32,-3.36903037531133E-32,
1.));
#129440=DIRECTION('ref_axis',(-0.182569820839373,0.983192890799501,4.05221974712874E-32));
#129441=DIRECTION('center_axis',(-4.05221974712873E-32,3.36903037531133E-32,
-1.));
#129442=DIRECTION('ref_axis',(0.182569820839372,-0.983192890799501,-4.05221974712874E-32));
#129443=DIRECTION('center_axis',(-0.129229316621256,-0.991614735532708,
-2.50174180397232E-32));
#129444=DIRECTION('ref_axis',(0.991614735532709,-0.129229316621256,-4.33706972907855E-32));
#129445=DIRECTION('',(3.97740386869697E-32,-3.04124059454469E-32,1.));
#129446=DIRECTION('',(0.725671350092338,-0.0945710156411471,-0.681511125848849));
#129447=DIRECTION('center_axis',(0.129234083798628,0.991614114250181,2.1351401914929E-6));
#129448=DIRECTION('ref_axis',(0.983222161215371,-0.12814010627372,-0.129824091982705));
#129449=DIRECTION('',(-1.99816041856823E-33,2.54893740879476E-32,-1.));
#129450=DIRECTION('center_axis',(-0.613109346662695,0.789998056348776,4.84115764592977E-32));
#129451=DIRECTION('ref_axis',(-0.789998056348776,-0.613109346662695,1.27752829161934E-32));
#129452=DIRECTION('center_axis',(0.613109346662686,-0.789998056348782,-1.11181245940181E-14));
#129453=DIRECTION('ref_axis',(0.784071772166395,0.608510018608646,0.122257978654787));
#129454=DIRECTION('',(-0.578126701407853,-0.448678172483924,0.681511125848846));
#129455=DIRECTION('',(3.97740386869697E-32,-3.04124059454469E-32,1.));
#129456=DIRECTION('',(9.67881184176439E-33,-5.3769001218617E-32,1.));
#129457=DIRECTION('center_axis',(3.97740386869697E-32,-3.04124059454469E-32,
1.));
#129458=DIRECTION('ref_axis',(0.262101682939114,-0.965040262269137,-3.97740386869697E-32));
#129459=DIRECTION('center_axis',(-0.327798383466007,-0.0890289362323012,
-0.940543496235245));
#129460=DIRECTION('ref_axis',(0.907693578939827,0.246402996534641,-0.339673269554961));
#129461=DIRECTION('center_axis',(-0.327798383466007,-0.0890289362323012,
-0.940543496235245));
#129462=DIRECTION('ref_axis',(0.907693578939827,0.246402996534641,-0.339673269554961));
#129463=DIRECTION('center_axis',(0.580023635344838,0.450150363355038,-0.678923583927297));
#129464=DIRECTION('ref_axis',(0.682985944474806,0.185496680780643,0.706485089063614));
#129465=DIRECTION('center_axis',(-0.728052403601427,0.0948813195391983,
0.678923583927297));
#129466=DIRECTION('ref_axis',(-0.682985944474806,-0.185496680780638,-0.706485089063615));
#129467=DIRECTION('center_axis',(0.104837454158456,0.994192541084149,-0.0242960790708589));
#129468=DIRECTION('ref_axis',(-0.683193733447373,0.0897529074021294,0.724700447213264));
#129469=DIRECTION('center_axis',(-3.97740386869697E-32,3.04124059454469E-32,
-1.));
#129470=DIRECTION('ref_axis',(-0.262101682939122,0.965040262269135,3.977403868697E-32));
#129471=DIRECTION('center_axis',(-5.31028553898035E-35,-4.12293233664482E-32,
1.));
#129472=DIRECTION('ref_axis',(0.952552585008677,-0.304374067215469,-1.24985535794147E-32));
#129473=DIRECTION('center_axis',(3.97740386869697E-32,-3.04124059454469E-32,
1.));
#129474=DIRECTION('ref_axis',(0.262101682939122,-0.965040262269135,-3.977403868697E-32));
#129475=DIRECTION('center_axis',(-0.577874066616821,-0.44848210522727,0.681854357192688));
#129476=DIRECTION('ref_axis',(-0.68571448968173,-0.186237744463338,-0.703641344136153));
#129477=DIRECTION('center_axis',(-0.578382576834232,-0.448876754764269,
0.681163162426516));
#129478=DIRECTION('ref_axis',(-0.685071224877307,-0.186063035910333,-0.704313824593083));
#129479=DIRECTION('center_axis',(0.725992527899326,-0.0946128722080396,
-0.681163162426516));
#129480=DIRECTION('ref_axis',(0.685071224877307,0.186063035910332,0.704313824593084));
#129481=DIRECTION('center_axis',(0.725354239968488,-0.0945296891832677,
-0.681854357192686));
#129482=DIRECTION('ref_axis',(0.685714489681727,0.186237744463349,0.703641344136154));
#129483=DIRECTION('center_axis',(3.97740386869697E-32,-3.04124059454469E-32,
1.));
#129484=DIRECTION('ref_axis',(0.262101682939122,-0.965040262269135,-3.977403868697E-32));
#129485=DIRECTION('center_axis',(-5.31028553898035E-35,-4.12293233664482E-32,
1.));
#129486=DIRECTION('ref_axis',(0.667701070818543,0.744429499702807,3.07277814001776E-32));
#129487=DIRECTION('center_axis',(3.97740386869697E-32,-3.04124059454469E-32,
1.));
#129488=DIRECTION('ref_axis',(-0.262101682939102,0.96504026226914,3.97740386869693E-32));
#129489=DIRECTION('center_axis',(-3.97740386869697E-32,3.04124059454469E-32,
-1.));
#129490=DIRECTION('ref_axis',(0.262101682939113,-0.965040262269137,-3.97740386869697E-32));
#129491=DIRECTION('center_axis',(-0.0479735100828851,-0.998848608313756,
-2.53155613888654E-32));
#129492=DIRECTION('ref_axis',(0.998848608313756,-0.0479735100828851,-4.00217472840792E-32));
#129493=DIRECTION('',(3.87611902374447E-32,-2.72063969588172E-32,1.));
#129494=DIRECTION('',(0.730965154267801,-0.0351073865515025,-0.681511125848855));
#129495=DIRECTION('center_axis',(0.0479783120381316,0.998848377667708,2.13514018274057E-6));
#129496=DIRECTION('ref_axis',(0.990395178825938,-0.0475719967119414,-0.12982409209071));
#129497=DIRECTION('',(-7.09735288106608E-34,2.53788308567206E-32,-1.));
#129498=DIRECTION('center_axis',(-0.675461451466197,0.737395299404043,4.6243559049494E-32));
#129499=DIRECTION('ref_axis',(-0.737395299404043,-0.675461451466197,1.02054471014294E-32));
#129500=DIRECTION('center_axis',(0.675461451466204,-0.737395299404037,2.77317066532683E-15));
#129501=DIRECTION('ref_axis',(0.731863622371199,0.670394380112939,0.122257978728159));
#129502=DIRECTION('',(-0.539631596118641,-0.494307926109512,0.681511125848846));
#129503=DIRECTION('',(3.87611902374447E-32,-2.72063969588172E-32,1.));
#129504=DIRECTION('',(1.06698821237002E-32,-5.29383154663383E-32,1.));
#129505=DIRECTION('center_axis',(3.87611902374447E-32,-2.72063969588172E-32,
1.));
#129506=DIRECTION('ref_axis',(0.339889301582633,-0.940465450013806,-3.87611902374448E-32));
#129507=DIRECTION('center_axis',(-0.319450976579395,-0.115451311175618,
-0.940543496235183));
#129508=DIRECTION('ref_axis',(0.88458917172373,0.319568564190617,-0.339673269555132));
#129509=DIRECTION('center_axis',(-0.319450976579395,-0.115451311175618,
-0.940543496235183));
#129510=DIRECTION('ref_axis',(0.88458917172373,0.319568564190617,-0.339673269555132));
#129511=DIRECTION('center_axis',(0.54140222094129,0.495929836113086,-0.678923583927297));
#129512=DIRECTION('ref_axis',(0.66559366353615,0.240549150884602,0.706485089063614));
#129513=DIRECTION('center_axis',(-0.733363577666179,0.0352225799733199,
0.678923583927297));
#129514=DIRECTION('ref_axis',(-0.665593663536153,-0.240549150884596,-0.706485089063614));
#129515=DIRECTION('center_axis',(0.0234526944418836,0.999429673196143,-0.0242960790759765));
#129516=DIRECTION('ref_axis',(-0.68823614950775,0.0337676302669961,0.724700455123975));
#129517=DIRECTION('center_axis',(-3.87611902374447E-32,2.72063969588172E-32,
-1.));
#129518=DIRECTION('ref_axis',(-0.339889301582625,0.940465450013808,3.87611902374446E-32));
#129519=DIRECTION('center_axis',(-5.17505877669431E-35,-4.12336037522781E-32,
1.));
#129520=DIRECTION('ref_axis',(0.974192357011155,-0.225719408870948,-9.25680963750974E-33));
#129521=DIRECTION('center_axis',(3.87611902374447E-32,-2.72063969588172E-32,
1.));
#129522=DIRECTION('ref_axis',(0.339889301582624,-0.940465450013809,-3.87611902374446E-32));
#129523=DIRECTION('center_axis',(-0.539395783250655,-0.494091919169661,
0.681854357192688));
#129524=DIRECTION('ref_axis',(-0.668252726164151,-0.241510150503965,-0.703641344136153));
#129525=DIRECTION('center_axis',(-0.539870433841254,-0.49452670384638,0.681163162426516));
#129526=DIRECTION('ref_axis',(-0.667625842139282,-0.241283591225921,-0.704313824593083));
#129527=DIRECTION('center_axis',(0.731288675080916,-0.0351229248711846,
-0.681163162426516));
#129528=DIRECTION('ref_axis',(0.667625842139283,0.241283591225917,0.704313824593084));
#129529=DIRECTION('center_axis',(0.730645730811761,-0.0350920450230047,
-0.681854357192686));
#129530=DIRECTION('ref_axis',(0.668252726164146,0.241510150503977,0.703641344136154));
#129531=DIRECTION('center_axis',(3.87611902374447E-32,-2.72063969588172E-32,
1.));
#129532=DIRECTION('ref_axis',(0.339889301582624,-0.940465450013809,-3.87611902374446E-32));
#129533=DIRECTION('center_axis',(-5.17505877669431E-35,-4.12336037522781E-32,
1.));
#129534=DIRECTION('ref_axis',(0.604801435414776,0.796376307859687,3.28687639457536E-32));
#129535=DIRECTION('center_axis',(3.87611902374447E-32,-2.72063969588172E-32,
1.));
#129536=DIRECTION('ref_axis',(-0.339889301582644,0.940465450013802,3.87611902374452E-32));
#129537=DIRECTION('center_axis',(-3.87611902374447E-32,2.72063969588172E-32,
-1.));
#129538=DIRECTION('ref_axis',(0.339889301582627,-0.940465450013808,-3.87611902374447E-32));
#129539=DIRECTION('center_axis',(0.0336015522500152,-0.999435308404896,
-2.53397421749269E-32));
#129540=DIRECTION('ref_axis',(0.999435308404896,0.0336015522500152,-3.66596391814683E-32));
#129541=DIRECTION('',(3.74903924620357E-32,-2.40936122540758E-32,1.));
#129542=DIRECTION('',(0.731394505942384,0.0245898764033321,-0.681511125848849));
#129543=DIRECTION('center_axis',(-0.0335967474730231,0.999435469930238,
2.13514021539847E-6));
#129544=DIRECTION('ref_axis',(0.990977279923771,0.0333126966366988,-0.129824092208173));
#129545=DIRECTION('',(5.8341301359928E-34,2.53736740582643E-32,-1.));
#129546=DIRECTION('center_axis',(-0.733318471753486,0.679885298403438,4.38732900626775E-32));
#129547=DIRECTION('ref_axis',(-0.679885298403438,-0.733318471753486,7.82087574913321E-33));
#129548=DIRECTION('center_axis',(0.73331847175353,-0.67988529840339,3.17515320213748E-14));
#129549=DIRECTION('ref_axis',(0.674785040937491,0.727817377643653,0.122257978581793));
#129550=DIRECTION('',(-0.497545331590206,-0.536648142041902,0.68151112584885));
#129551=DIRECTION('',(3.74903924620357E-32,-2.40936122540758E-32,1.));
#129552=DIRECTION('',(1.15899461005094E-32,-5.20296123237482E-32,1.));
#129553=DIRECTION('center_axis',(3.74903924620357E-32,-2.40936122540758E-32,
1.));
#129554=DIRECTION('ref_axis',(0.415415013001901,-0.909631995354512,-3.74903924620359E-32));
#129555=DIRECTION('center_axis',(-0.308977676149106,-0.141105376691099,
-0.940543496235214));
#129556=DIRECTION('ref_axis',(0.855597969517219,0.390607455775997,-0.339673269555045));
#129557=DIRECTION('center_axis',(-0.308977676149106,-0.141105376691099,
-0.940543496235214));
#129558=DIRECTION('ref_axis',(0.855597969517219,0.390607455775997,-0.339673269555045));
#129559=DIRECTION('center_axis',(0.499177864082457,0.538408977634465,-0.678923583927297));
#129560=DIRECTION('ref_axis',(0.643771966581886,0.294000806077242,0.706485089063615));
#129561=DIRECTION('center_axis',(-0.733794338118036,-0.0246705600509643,
0.678923583927297));
#129562=DIRECTION('ref_axis',(-0.64377196658189,-0.294000806077234,-0.706485089063614));
#129563=DIRECTION('center_axis',(-0.0580881390785779,0.998015765727227,
-0.0242960790722294));
#129564=DIRECTION('ref_axis',(-0.688697894046278,-0.0224423168364948,0.724701009486831));
#129565=DIRECTION('center_axis',(-3.74903924620357E-32,2.40936122540758E-32,
-1.));
#129566=DIRECTION('ref_axis',(-0.415415013001888,0.909631995354518,3.74903924620355E-32));
#129567=DIRECTION('center_axis',(-5.00539285207335E-35,-4.12377596731122E-32,
1.));
#129568=DIRECTION('ref_axis',(0.989349039608153,-0.145562625101453,-5.95315574521045E-33));
#129569=DIRECTION('center_axis',(3.74903924620357E-32,-2.40936122540758E-32,
1.));
#129570=DIRECTION('ref_axis',(0.415415013001888,-0.909631995354518,-3.74903924620355E-32));
#129571=DIRECTION('center_axis',(-0.497327909940996,-0.536413632909406,
0.681854357192688));
#129572=DIRECTION('ref_axis',(-0.646343851007884,-0.295175346339365,-0.703641344136154));
#129573=DIRECTION('center_axis',(-0.497765542183414,-0.536885659305555,
0.681163162426516));
#129574=DIRECTION('ref_axis',(-0.64573751957233,-0.294898444050892,-0.704313824593084));
#129575=DIRECTION('center_axis',(0.731718216783981,0.0246007597358135,-0.681163162426516));
#129576=DIRECTION('ref_axis',(0.645737519572332,0.294898444050891,0.704313824593083));
#129577=DIRECTION('center_axis',(0.731074894864541,0.0245791309071065,-0.681854357192686));
#129578=DIRECTION('ref_axis',(0.64634385100788,0.295175346339376,0.703641344136153));
#129579=DIRECTION('center_axis',(3.74903924620357E-32,-2.40936122540758E-32,
1.));
#129580=DIRECTION('ref_axis',(0.415415013001888,-0.909631995354518,-3.74903924620355E-32));
#129581=DIRECTION('center_axis',(-5.00539285207335E-35,-4.12377596731122E-32,
1.));
#129582=DIRECTION('ref_axis',(0.537876946243533,0.843023363080604,3.4791317699757E-32));
#129583=DIRECTION('center_axis',(3.74903924620357E-32,-2.40936122540758E-32,
1.));
#129584=DIRECTION('ref_axis',(-0.415415013001928,0.9096319953545,3.74903924620366E-32));
#129585=DIRECTION('center_axis',(-3.74903924620357E-32,2.40936122540758E-32,
-1.));
#129586=DIRECTION('ref_axis',(0.415415013001897,-0.909631995354514,-3.74903924620357E-32));
#129587=DIRECTION('center_axis',(0.114953001796558,-0.99337093141382,-2.5089799478766E-32));
#129588=DIRECTION('ref_axis',(0.99337093141382,0.114953001796558,-3.33067472576671E-32));
#129589=DIRECTION('',(3.59701023102713E-32,-2.10947668998596E-32,1.));
#129590=DIRECTION('',(0.726956547851512,0.0841234977877359,-0.681511125848852));
#129591=DIRECTION('center_axis',(-0.114948226172968,0.99337148403562,2.13514017304701E-6));
#129592=DIRECTION('ref_axis',(0.984964590732422,0.113975699484092,-0.129824092257272));
#129593=DIRECTION('',(1.87267879795604E-33,2.54739380102217E-32,-1.));
#129594=DIRECTION('center_axis',(-0.786295378600288,0.617850772915135,4.13165432478888E-32));
#129595=DIRECTION('ref_axis',(-0.617850772915135,-0.786295378600288,5.63743778822766E-33));
#129596=DIRECTION('center_axis',(0.786295378600298,-0.617850772915122,1.21103599696864E-14));
#129597=DIRECTION('ref_axis',(0.613215876366603,0.780396870584852,0.122257978689773));
#129598=DIRECTION('',(-0.452147984969242,-0.575417053129717,0.68151112584885));
#129599=DIRECTION('',(3.59701023102713E-32,-2.10947668998596E-32,1.));
#129600=DIRECTION('',(1.24328808982262E-32,-5.10489390603351E-32,1.));
#129601=DIRECTION('center_axis',(3.59701023102713E-32,-2.10947668998596E-32,
1.));
#129602=DIRECTION('ref_axis',(0.48817620604829,-0.872745089844851,-3.59701023102713E-32));
#129603=DIRECTION('center_axis',(-0.29644818026194,-0.165820409205535,-0.940543496235179));
#129604=DIRECTION('ref_axis',(0.820912903986917,0.459046919189624,-0.339673269555144));
#129605=DIRECTION('center_axis',(-0.29644818026194,-0.165820409205535,-0.940543496235179));
#129606=DIRECTION('ref_axis',(0.820912903986917,0.459046919189624,-0.339673269555144));
#129607=DIRECTION('center_axis',(0.453631560896706,0.577305096240915,-0.678923583927297));
#129608=DIRECTION('ref_axis',(0.617666073404923,0.345495934412147,0.706485089063613));
#129609=DIRECTION('center_axis',(-0.729341818317261,-0.0843995215684652,
0.678923583927297));
#129610=DIRECTION('ref_axis',(-0.617666073404925,-0.345495934412141,-0.706485089063615));
#129611=DIRECTION('center_axis',(-0.139242405632141,0.989960227996504,-0.024296079084576));
#129612=DIRECTION('ref_axis',(-0.684577178647174,-0.0785029346967517,0.724700887069605));
#129613=DIRECTION('center_axis',(-3.59701023102713E-32,2.10947668998596E-32,
-1.));
#129614=DIRECTION('ref_axis',(-0.48817620604829,0.872745089844851,3.59701023102713E-32));
#129615=DIRECTION('center_axis',(-4.80241686385389E-35,-4.1241763471983E-32,
1.));
#129616=DIRECTION('ref_axis',(0.997921767577655,-0.0644371460780812,-2.60957717410763E-33));
#129617=DIRECTION('center_axis',(3.59701023102713E-32,-2.10947668998597E-32,
1.));
#129618=DIRECTION('ref_axis',(0.48817620604829,-0.872745089844851,-3.59701023102713E-32));
#129619=DIRECTION('center_axis',(-0.451950401444009,-0.575165602424159,
0.681854357192688));
#129620=DIRECTION('ref_axis',(-0.620133664162392,-0.346876198945375,-0.703641344136154));
#129621=DIRECTION('center_axis',(-0.452348102967877,-0.575671729281951,
0.681163162426516));
#129622=DIRECTION('ref_axis',(-0.619551920351823,-0.346550796385513,-0.704313824593082));
#129623=DIRECTION('center_axis',(0.727278294479357,0.0841607303456094,-0.681163162426516));
#129624=DIRECTION('ref_axis',(0.619551920351821,0.346550796385511,0.704313824593085));
#129625=DIRECTION('center_axis',(0.726638876110865,0.0840867367763019,-0.681854357192686));
#129626=DIRECTION('ref_axis',(0.620133664162387,0.346876198945386,0.703641344136153));
#129627=DIRECTION('center_axis',(3.59701023102713E-32,-2.10947668998596E-32,
1.));
#129628=DIRECTION('ref_axis',(0.48817620604829,-0.872745089844851,-3.59701023102713E-32));
#129629=DIRECTION('center_axis',(-4.80241686385389E-35,-4.1241763471983E-32,
1.));
#129630=DIRECTION('ref_axis',(0.467372974738516,0.884060236909268,3.64826483841532E-32));
#129631=DIRECTION('center_axis',(3.59701023102713E-32,-2.10947668998597E-32,
1.));
#129632=DIRECTION('ref_axis',(-0.488176206048286,0.872745089844853,3.59701023102712E-32));
#129633=DIRECTION('center_axis',(-3.59701023102713E-32,2.10947668998596E-32,
-1.));
#129634=DIRECTION('ref_axis',(0.488176206048291,-0.872745089844851,-3.59701023102713E-32));
#129635=DIRECTION('center_axis',(0.195539458082054,-0.980695834768853,-2.45673966277879E-32));
#129636=DIRECTION('ref_axis',(0.980695834768853,0.195539458082054,-2.99853844552401E-32));
#129637=DIRECTION('',(3.42104370622812E-32,-1.82298177172263E-32,1.));
#129638=DIRECTION('',(0.717680813874082,0.143097291173771,-0.681511125848848));
#129639=DIRECTION('center_axis',(-0.195534743392682,0.980696774809523,2.13514020054857E-6));
#129640=DIRECTION('ref_axis',(0.97239712468431,0.193880212852231,-0.129824092409923));
#129641=DIRECTION('',(3.14948221388265E-33,2.56789554725347E-32,-1.));
#129642=DIRECTION('center_axis',(-0.83403961943211,0.551704552471285,3.85903333333466E-32));
#129643=DIRECTION('ref_axis',(-0.551704552471285,-0.83403961943211,3.66966363810075E-33));
#129644=DIRECTION('center_axis',(0.834039619432123,-0.551704552471265,-1.65372562611265E-15));
#129645=DIRECTION('ref_axis',(0.54756586131972,0.827782951116591,0.122257978708552));
#129646=DIRECTION('',(-0.403741668107477,-0.610356658666085,0.681511125848848));
#129647=DIRECTION('',(3.42104370622812E-32,-1.82298177172263E-32,1.));
#129648=DIRECTION('',(1.31930769248463E-32,-5.00028218948674E-32,1.));
#129649=DIRECTION('center_axis',(3.42104370622812E-32,-1.82298177172263E-32,
1.));
#129650=DIRECTION('ref_axis',(0.557688666986836,-0.830050209755076,-3.42104370622811E-32));
#129651=DIRECTION('center_axis',(-0.281945870645394,-0.189431934254999,
-0.940543496235246));
#129652=DIRECTION('ref_axis',(0.780764798521982,0.524431501093111,-0.339673269554957));
#129653=DIRECTION('center_axis',(-0.281945870645394,-0.189431934254999,
-0.940543496235246));
#129654=DIRECTION('ref_axis',(0.780764798521982,0.524431501093111,-0.339673269554957));
#129655=DIRECTION('center_axis',(0.405066414517127,0.612359344680518,-0.678923583927297));
#129656=DIRECTION('ref_axis',(0.587449714417171,0.394691844306367,0.706485089063614));
#129657=DIRECTION('center_axis',(-0.720035649048515,-0.143566818194869,
0.678923583927297));
#129658=DIRECTION('ref_axis',(-0.587449714417177,-0.394691844306358,-0.706485089063614));
#129659=DIRECTION('center_axis',(-0.219470036920007,0.97531666828596,-0.0242960790644273));
#129660=DIRECTION('ref_axis',(-0.675901111825593,-0.134041249019664,0.724700372977809));
#129661=DIRECTION('center_axis',(-3.42104370622812E-32,1.82298177172263E-32,
-1.));
#129662=DIRECTION('ref_axis',(-0.557688666986844,0.830050209755071,3.42104370622813E-32));
#129663=DIRECTION('center_axis',(-4.56748158374851E-35,-4.12455885042696E-32,
1.));
#129664=DIRECTION('ref_axis',(0.999853490829434,0.0171171515210855,7.51675112062014E-34));
#129665=DIRECTION('center_axis',(3.42104370622812E-32,-1.82298177172263E-32,
1.));
#129666=DIRECTION('ref_axis',(0.557688666986844,-0.830050209755071,-3.42104370622813E-32));
#129667=DIRECTION('center_axis',(-0.40356523759198,-0.610089939750423,0.681854357192688));
#129668=DIRECTION('ref_axis',(-0.589796590096757,-0.396268647677944,-0.703641344136153));
#129669=DIRECTION('center_axis',(-0.403920361759272,-0.610626798879125,
0.681163162426516));
#129670=DIRECTION('ref_axis',(-0.589243305320234,-0.39589691034706,-0.704313824593084));
#129671=DIRECTION('center_axis',(0.717998455117445,0.143160625180498,-0.681163162426516));
#129672=DIRECTION('ref_axis',(0.589243305320236,0.395896910347057,0.704313824593083));
#129673=DIRECTION('center_axis',(0.717367195523647,0.143034759285586,-0.681854357192686));
#129674=DIRECTION('ref_axis',(0.589796590096751,0.396268647677949,0.703641344136156));
#129675=DIRECTION('center_axis',(3.42104370622812E-32,-1.82298177172263E-32,
1.));
#129676=DIRECTION('ref_axis',(0.557688666986844,-0.830050209755071,-3.42104370622813E-32));
#129677=DIRECTION('center_axis',(-4.56748158374851E-35,-4.12455885042696E-32,
1.));
#129678=DIRECTION('ref_axis',(0.393758713197697,0.919213835720989,3.79315004722889E-32));
#129679=DIRECTION('center_axis',(3.42104370622812E-32,-1.82298177172263E-32,
1.));
#129680=DIRECTION('ref_axis',(-0.557688666986862,0.830050209755059,3.42104370622817E-32));
#129681=DIRECTION('center_axis',(-3.42104370622812E-32,1.82298177172263E-32,
-1.));
#129682=DIRECTION('ref_axis',(0.557688666986839,-0.830050209755074,-3.42104370622812E-32));
#409622=CARTESIAN_POINT('',(0.,0.,0.));
#409623=CARTESIAN_POINT('Origin',(0.,-1.11022302462516E-14,-14.21875));
#409624=CARTESIAN_POINT('',(-8.32001735975286E-31,-1.17524047358087,-13.9375));
#409625=CARTESIAN_POINT('',(-1.43925448419923E-16,-1.17524047358087,-14.));
#409626=CARTESIAN_POINT('',(1.43925448419925E-16,-1.1752404735809,-14.21875));
#409627=CARTESIAN_POINT('',(-0.823407874165272,-0.838564036615699,-14.));
#409628=CARTESIAN_POINT('Ctrl Pts',(-0.823407874165272,-0.838564036615699,
-14.));
#409629=CARTESIAN_POINT('Ctrl Pts',(-0.480534359260996,-1.17524047358087,
-13.9670084971875));
#409630=CARTESIAN_POINT('Ctrl Pts',(-1.43925448419923E-16,-1.17524047358087,
-13.9375));
#409631=CARTESIAN_POINT('Origin',(0.,2.54061283442571E-15,-14.));
#409632=CARTESIAN_POINT('Origin',(0.,-1.11022302462516E-14,-14.21875));
#409633=CARTESIAN_POINT('',(-8.32001735975286E-31,-1.17524047358087,-13.4375));
#409634=CARTESIAN_POINT('',(-8.32001735975286E-31,-1.17524047358087,-13.5));
#409635=CARTESIAN_POINT('',(1.43925448419925E-16,-1.1752404735809,-14.21875));
#409636=CARTESIAN_POINT('Ctrl Pts',(-1.43925448419923E-16,-1.17524047358087,
-13.9375));
#409637=CARTESIAN_POINT('Ctrl Pts',(0.678525403784459,-1.17524047358087,
-13.8958333333333));
#409638=CARTESIAN_POINT('Ctrl Pts',(1.01778810567669,-0.587620236790434,
-13.8541666666667));
#409639=CARTESIAN_POINT('Ctrl Pts',(1.35705080756892,2.29132664526027E-15,
-13.8125));
#409640=CARTESIAN_POINT('Ctrl Pts',(1.01778810567669,0.587620236790438,
-13.7708333333333));
#409641=CARTESIAN_POINT('Ctrl Pts',(0.67852540378446,1.17524047358087,-13.7291666666667));
#409642=CARTESIAN_POINT('Ctrl Pts',(0.,1.17524047358087,-13.6875));
#409643=CARTESIAN_POINT('Ctrl Pts',(-0.678525403784459,1.17524047358087,
-13.6458333333333));
#409644=CARTESIAN_POINT('Ctrl Pts',(-1.01778810567669,0.587620236790438,
-13.6041666666667));
#409645=CARTESIAN_POINT('Ctrl Pts',(-1.35705080756892,2.62370823081419E-15,
-13.5625));
#409646=CARTESIAN_POINT('Ctrl Pts',(-1.01778810567669,-0.587620236790433,
-13.5208333333333));
#409647=CARTESIAN_POINT('Ctrl Pts',(-0.67852540378446,-1.17524047358087,
-13.4791666666667));
#409648=CARTESIAN_POINT('Ctrl Pts',(-1.43925448419923E-16,-1.17524047358087,
-13.4375));
#409649=CARTESIAN_POINT('Ctrl Pts',(-1.43925448419923E-16,-1.17524047358087,
-14.));
#409650=CARTESIAN_POINT('Ctrl Pts',(0.67852540378446,-1.17524047358087,
-13.9583333333333));
#409651=CARTESIAN_POINT('Ctrl Pts',(1.01778810567669,-0.587620236790434,
-13.9166666666667));
#409652=CARTESIAN_POINT('Ctrl Pts',(1.35705080756892,2.29132664526027E-15,
-13.875));
#409653=CARTESIAN_POINT('Ctrl Pts',(1.01778810567669,0.587620236790438,
-13.8333333333333));
#409654=CARTESIAN_POINT('Ctrl Pts',(0.67852540378446,1.17524047358087,-13.7916666666667));
#409655=CARTESIAN_POINT('Ctrl Pts',(0.,1.17524047358087,-13.75));
#409656=CARTESIAN_POINT('Ctrl Pts',(-0.678525403784459,1.17524047358087,
-13.7083333333333));
#409657=CARTESIAN_POINT('Ctrl Pts',(-1.01778810567669,0.587620236790438,
-13.6666666666667));
#409658=CARTESIAN_POINT('Ctrl Pts',(-1.35705080756892,2.62370823081419E-15,
-13.625));
#409659=CARTESIAN_POINT('Ctrl Pts',(-1.01778810567669,-0.587620236790433,
-13.5833333333333));
#409660=CARTESIAN_POINT('Ctrl Pts',(-0.67852540378446,-1.17524047358087,
-13.5416666666667));
#409661=CARTESIAN_POINT('Ctrl Pts',(-1.43925448419923E-16,-1.17524047358087,
-13.5));
#409662=CARTESIAN_POINT('Origin',(0.,-1.11022302462516E-14,-14.21875));
#409663=CARTESIAN_POINT('',(-8.32001735975286E-31,-1.17524047358087,-12.9375));
#409664=CARTESIAN_POINT('',(-8.32001735975286E-31,-1.17524047358087,-13.));
#409665=CARTESIAN_POINT('',(1.43925448419925E-16,-1.1752404735809,-14.21875));
#409666=CARTESIAN_POINT('Ctrl Pts',(-1.43925448419923E-16,-1.17524047358087,
-13.4375));
#409667=CARTESIAN_POINT('Ctrl Pts',(0.678525403784459,-1.17524047358087,
-13.3958333333333));
#409668=CARTESIAN_POINT('Ctrl Pts',(1.01778810567669,-0.587620236790434,
-13.3541666666667));
#409669=CARTESIAN_POINT('Ctrl Pts',(1.35705080756892,2.29132664526027E-15,
-13.3125));
#409670=CARTESIAN_POINT('Ctrl Pts',(1.01778810567669,0.587620236790438,
-13.2708333333333));
#409671=CARTESIAN_POINT('Ctrl Pts',(0.67852540378446,1.17524047358087,-13.2291666666667));
#409672=CARTESIAN_POINT('Ctrl Pts',(0.,1.17524047358087,-13.1875));
#409673=CARTESIAN_POINT('Ctrl Pts',(-0.678525403784459,1.17524047358087,
-13.1458333333333));
#409674=CARTESIAN_POINT('Ctrl Pts',(-1.01778810567669,0.587620236790438,
-13.1041666666667));
#409675=CARTESIAN_POINT('Ctrl Pts',(-1.35705080756892,2.62370823081419E-15,
-13.0625));
#409676=CARTESIAN_POINT('Ctrl Pts',(-1.01778810567669,-0.587620236790433,
-13.0208333333333));
#409677=CARTESIAN_POINT('Ctrl Pts',(-0.67852540378446,-1.17524047358087,
-12.9791666666667));
#409678=CARTESIAN_POINT('Ctrl Pts',(-1.43925448419923E-16,-1.17524047358087,
-12.9375));
#409679=CARTESIAN_POINT('Ctrl Pts',(-1.43925448419923E-16,-1.17524047358087,
-13.5));
#409680=CARTESIAN_POINT('Ctrl Pts',(0.678525403784459,-1.17524047358087,
-13.4583333333333));
#409681=CARTESIAN_POINT('Ctrl Pts',(1.01778810567669,-0.587620236790434,
-13.4166666666667));
#409682=CARTESIAN_POINT('Ctrl Pts',(1.35705080756892,2.29132664526027E-15,
-13.375));
#409683=CARTESIAN_POINT('Ctrl Pts',(1.01778810567669,0.587620236790438,
-13.3333333333333));
#409684=CARTESIAN_POINT('Ctrl Pts',(0.67852540378446,1.17524047358087,-13.2916666666667));
#409685=CARTESIAN_POINT('Ctrl Pts',(0.,1.17524047358087,-13.25));
#409686=CARTESIAN_POINT('Ctrl Pts',(-0.678525403784459,1.17524047358087,
-13.2083333333333));
#409687=CARTESIAN_POINT('Ctrl Pts',(-1.01778810567669,0.587620236790438,
-13.1666666666667));
#409688=CARTESIAN_POINT('Ctrl Pts',(-1.35705080756892,2.62370823081419E-15,
-13.125));
#409689=CARTESIAN_POINT('Ctrl Pts',(-1.01778810567669,-0.587620236790433,
-13.0833333333333));
#409690=CARTESIAN_POINT('Ctrl Pts',(-0.67852540378446,-1.17524047358087,
-13.0416666666667));
#409691=CARTESIAN_POINT('Ctrl Pts',(-1.43925448419923E-16,-1.17524047358087,
-13.));
#409692=CARTESIAN_POINT('Origin',(0.,-1.11022302462516E-14,-14.21875));
#409693=CARTESIAN_POINT('',(-8.32001735975286E-31,-1.17524047358087,-12.4375));
#409694=CARTESIAN_POINT('',(-8.32001735975286E-31,-1.17524047358087,-12.5));
#409695=CARTESIAN_POINT('',(1.43925448419925E-16,-1.1752404735809,-14.21875));
#409696=CARTESIAN_POINT('Ctrl Pts',(-1.43925448419923E-16,-1.17524047358087,
-12.9375));
#409697=CARTESIAN_POINT('Ctrl Pts',(0.678525403784459,-1.17524047358087,
-12.8958333333333));
#409698=CARTESIAN_POINT('Ctrl Pts',(1.01778810567669,-0.587620236790434,
-12.8541666666667));
#409699=CARTESIAN_POINT('Ctrl Pts',(1.35705080756892,2.29132664526027E-15,
-12.8125));
#409700=CARTESIAN_POINT('Ctrl Pts',(1.01778810567669,0.587620236790438,
-12.7708333333333));
#409701=CARTESIAN_POINT('Ctrl Pts',(0.67852540378446,1.17524047358087,-12.7291666666667));
#409702=CARTESIAN_POINT('Ctrl Pts',(0.,1.17524047358087,-12.6875));
#409703=CARTESIAN_POINT('Ctrl Pts',(-0.678525403784459,1.17524047358087,
-12.6458333333333));
#409704=CARTESIAN_POINT('Ctrl Pts',(-1.01778810567669,0.587620236790438,
-12.6041666666667));
#409705=CARTESIAN_POINT('Ctrl Pts',(-1.35705080756892,2.62370823081419E-15,
-12.5625));
#409706=CARTESIAN_POINT('Ctrl Pts',(-1.01778810567669,-0.587620236790433,
-12.5208333333333));
#409707=CARTESIAN_POINT('Ctrl Pts',(-0.67852540378446,-1.17524047358087,
-12.4791666666667));
#409708=CARTESIAN_POINT('Ctrl Pts',(-1.43925448419923E-16,-1.17524047358087,
-12.4375));
#409709=CARTESIAN_POINT('Ctrl Pts',(-1.43925448419923E-16,-1.17524047358087,
-13.));
#409710=CARTESIAN_POINT('Ctrl Pts',(0.678525403784459,-1.17524047358087,
-12.9583333333333));
#409711=CARTESIAN_POINT('Ctrl Pts',(1.01778810567669,-0.587620236790434,
-12.9166666666667));
#409712=CARTESIAN_POINT('Ctrl Pts',(1.35705080756892,2.29132664526027E-15,
-12.875));
#409713=CARTESIAN_POINT('Ctrl Pts',(1.01778810567669,0.587620236790438,
-12.8333333333333));
#409714=CARTESIAN_POINT('Ctrl Pts',(0.67852540378446,1.17524047358087,-12.7916666666667));
#409715=CARTESIAN_POINT('Ctrl Pts',(0.,1.17524047358087,-12.75));
#409716=CARTESIAN_POINT('Ctrl Pts',(-0.678525403784459,1.17524047358087,
-12.7083333333333));
#409717=CARTESIAN_POINT('Ctrl Pts',(-1.01778810567669,0.587620236790438,
-12.6666666666667));
#409718=CARTESIAN_POINT('Ctrl Pts',(-1.35705080756892,2.62370823081419E-15,
-12.625));
#409719=CARTESIAN_POINT('Ctrl Pts',(-1.01778810567669,-0.587620236790433,
-12.5833333333333));
#409720=CARTESIAN_POINT('Ctrl Pts',(-0.67852540378446,-1.17524047358087,
-12.5416666666667));
#409721=CARTESIAN_POINT('Ctrl Pts',(-1.43925448419923E-16,-1.17524047358087,
-12.5));
#409722=CARTESIAN_POINT('Origin',(0.,-1.11022302462516E-14,-14.21875));
#409723=CARTESIAN_POINT('',(-8.32001735975286E-31,-1.17524047358087,-11.9375));
#409724=CARTESIAN_POINT('',(-8.32001735975286E-31,-1.17524047358087,-12.));
#409725=CARTESIAN_POINT('',(1.43925448419925E-16,-1.1752404735809,-14.21875));
#409726=CARTESIAN_POINT('Ctrl Pts',(-1.43925448419923E-16,-1.17524047358087,
-12.4375));
#409727=CARTESIAN_POINT('Ctrl Pts',(0.678525403784459,-1.17524047358087,
-12.3958333333333));
#409728=CARTESIAN_POINT('Ctrl Pts',(1.01778810567669,-0.587620236790434,
-12.3541666666667));
#409729=CARTESIAN_POINT('Ctrl Pts',(1.35705080756892,2.29132664526027E-15,
-12.3125));
#409730=CARTESIAN_POINT('Ctrl Pts',(1.01778810567669,0.587620236790438,
-12.2708333333333));
#409731=CARTESIAN_POINT('Ctrl Pts',(0.67852540378446,1.17524047358087,-12.2291666666667));
#409732=CARTESIAN_POINT('Ctrl Pts',(0.,1.17524047358087,-12.1875));
#409733=CARTESIAN_POINT('Ctrl Pts',(-0.678525403784459,1.17524047358087,
-12.1458333333333));
#409734=CARTESIAN_POINT('Ctrl Pts',(-1.01778810567669,0.587620236790438,
-12.1041666666667));
#409735=CARTESIAN_POINT('Ctrl Pts',(-1.35705080756892,2.62370823081419E-15,
-12.0625));
#409736=CARTESIAN_POINT('Ctrl Pts',(-1.01778810567669,-0.587620236790433,
-12.0208333333333));
#409737=CARTESIAN_POINT('Ctrl Pts',(-0.67852540378446,-1.17524047358087,
-11.9791666666667));
#409738=CARTESIAN_POINT('Ctrl Pts',(-1.43925448419923E-16,-1.17524047358087,
-11.9375));
#409739=CARTESIAN_POINT('Ctrl Pts',(-1.43925448419923E-16,-1.17524047358087,
-12.5));
#409740=CARTESIAN_POINT('Ctrl Pts',(0.678525403784459,-1.17524047358087,
-12.4583333333333));
#409741=CARTESIAN_POINT('Ctrl Pts',(1.01778810567669,-0.587620236790434,
-12.4166666666667));
#409742=CARTESIAN_POINT('Ctrl Pts',(1.35705080756892,2.29132664526027E-15,
-12.375));
#409743=CARTESIAN_POINT('Ctrl Pts',(1.01778810567669,0.587620236790438,
-12.3333333333333));
#409744=CARTESIAN_POINT('Ctrl Pts',(0.67852540378446,1.17524047358087,-12.2916666666667));
#409745=CARTESIAN_POINT('Ctrl Pts',(0.,1.17524047358087,-12.25));
#409746=CARTESIAN_POINT('Ctrl Pts',(-0.678525403784459,1.17524047358087,
-12.2083333333333));
#409747=CARTESIAN_POINT('Ctrl Pts',(-1.01778810567669,0.587620236790438,
-12.1666666666667));
#409748=CARTESIAN_POINT('Ctrl Pts',(-1.35705080756892,2.62370823081419E-15,
-12.125));
#409749=CARTESIAN_POINT('Ctrl Pts',(-1.01778810567669,-0.587620236790433,
-12.0833333333333));
#409750=CARTESIAN_POINT('Ctrl Pts',(-0.67852540378446,-1.17524047358087,
-12.0416666666667));
#409751=CARTESIAN_POINT('Ctrl Pts',(-1.43925448419923E-16,-1.17524047358087,
-12.));
#409752=CARTESIAN_POINT('Origin',(0.,-1.11022302462516E-14,-14.21875));
#409753=CARTESIAN_POINT('',(-8.32001735975286E-31,-1.17524047358087,-11.4375));
#409754=CARTESIAN_POINT('',(-8.32001735975286E-31,-1.17524047358087,-11.5));
#409755=CARTESIAN_POINT('',(1.43925448419925E-16,-1.1752404735809,-14.21875));
#409756=CARTESIAN_POINT('Ctrl Pts',(-1.43925448419923E-16,-1.17524047358087,
-11.9375));
#409757=CARTESIAN_POINT('Ctrl Pts',(0.678525403784459,-1.17524047358087,
-11.8958333333333));
#409758=CARTESIAN_POINT('Ctrl Pts',(1.01778810567669,-0.587620236790434,
-11.8541666666667));
#409759=CARTESIAN_POINT('Ctrl Pts',(1.35705080756892,2.29132664526027E-15,
-11.8125));
#409760=CARTESIAN_POINT('Ctrl Pts',(1.01778810567669,0.587620236790438,
-11.7708333333333));
#409761=CARTESIAN_POINT('Ctrl Pts',(0.67852540378446,1.17524047358087,-11.7291666666667));
#409762=CARTESIAN_POINT('Ctrl Pts',(0.,1.17524047358087,-11.6875));
#409763=CARTESIAN_POINT('Ctrl Pts',(-0.678525403784459,1.17524047358087,
-11.6458333333333));
#409764=CARTESIAN_POINT('Ctrl Pts',(-1.01778810567669,0.587620236790438,
-11.6041666666667));
#409765=CARTESIAN_POINT('Ctrl Pts',(-1.35705080756892,2.62370823081419E-15,
-11.5625));
#409766=CARTESIAN_POINT('Ctrl Pts',(-1.01778810567669,-0.587620236790433,
-11.5208333333333));
#409767=CARTESIAN_POINT('Ctrl Pts',(-0.67852540378446,-1.17524047358087,
-11.4791666666667));
#409768=CARTESIAN_POINT('Ctrl Pts',(-1.43925448419923E-16,-1.17524047358087,
-11.4375));
#409769=CARTESIAN_POINT('Ctrl Pts',(-1.43925448419923E-16,-1.17524047358087,
-12.));
#409770=CARTESIAN_POINT('Ctrl Pts',(0.678525403784459,-1.17524047358087,
-11.9583333333333));
#409771=CARTESIAN_POINT('Ctrl Pts',(1.01778810567669,-0.587620236790434,
-11.9166666666667));
#409772=CARTESIAN_POINT('Ctrl Pts',(1.35705080756892,2.29132664526027E-15,
-11.875));
#409773=CARTESIAN_POINT('Ctrl Pts',(1.01778810567669,0.587620236790438,
-11.8333333333333));
#409774=CARTESIAN_POINT('Ctrl Pts',(0.67852540378446,1.17524047358087,-11.7916666666667));
#409775=CARTESIAN_POINT('Ctrl Pts',(0.,1.17524047358087,-11.75));
#409776=CARTESIAN_POINT('Ctrl Pts',(-0.678525403784459,1.17524047358087,
-11.7083333333333));
#409777=CARTESIAN_POINT('Ctrl Pts',(-1.01778810567669,0.587620236790438,
-11.6666666666667));
#409778=CARTESIAN_POINT('Ctrl Pts',(-1.35705080756892,2.62370823081419E-15,
-11.625));
#409779=CARTESIAN_POINT('Ctrl Pts',(-1.01778810567669,-0.587620236790433,
-11.5833333333333));
#409780=CARTESIAN_POINT('Ctrl Pts',(-0.67852540378446,-1.17524047358087,
-11.5416666666667));
#409781=CARTESIAN_POINT('Ctrl Pts',(-1.43925448419923E-16,-1.17524047358087,
-11.5));
#409782=CARTESIAN_POINT('Origin',(0.,-1.11022302462516E-14,-14.21875));
#409783=CARTESIAN_POINT('',(-8.32001735975286E-31,-1.17524047358087,-10.9375));
#409784=CARTESIAN_POINT('',(-8.32001735975286E-31,-1.17524047358087,-11.));
#409785=CARTESIAN_POINT('',(1.43925448419925E-16,-1.1752404735809,-14.21875));
#409786=CARTESIAN_POINT('Ctrl Pts',(-1.43925448419923E-16,-1.17524047358087,
-11.4375));
#409787=CARTESIAN_POINT('Ctrl Pts',(0.678525403784459,-1.17524047358087,
-11.3958333333333));
#409788=CARTESIAN_POINT('Ctrl Pts',(1.01778810567669,-0.587620236790434,
-11.3541666666667));
#409789=CARTESIAN_POINT('Ctrl Pts',(1.35705080756892,2.29132664526027E-15,
-11.3125));
#409790=CARTESIAN_POINT('Ctrl Pts',(1.01778810567669,0.587620236790438,
-11.2708333333333));
#409791=CARTESIAN_POINT('Ctrl Pts',(0.67852540378446,1.17524047358087,-11.2291666666667));
#409792=CARTESIAN_POINT('Ctrl Pts',(0.,1.17524047358087,-11.1875));
#409793=CARTESIAN_POINT('Ctrl Pts',(-0.678525403784459,1.17524047358087,
-11.1458333333333));
#409794=CARTESIAN_POINT('Ctrl Pts',(-1.01778810567669,0.587620236790438,
-11.1041666666667));
#409795=CARTESIAN_POINT('Ctrl Pts',(-1.35705080756892,2.62370823081419E-15,
-11.0625));
#409796=CARTESIAN_POINT('Ctrl Pts',(-1.01778810567669,-0.587620236790433,
-11.0208333333333));
#409797=CARTESIAN_POINT('Ctrl Pts',(-0.67852540378446,-1.17524047358087,
-10.9791666666667));
#409798=CARTESIAN_POINT('Ctrl Pts',(-1.43925448419923E-16,-1.17524047358087,
-10.9375));
#409799=CARTESIAN_POINT('Ctrl Pts',(-1.43925448419923E-16,-1.17524047358087,
-11.5));
#409800=CARTESIAN_POINT('Ctrl Pts',(0.678525403784459,-1.17524047358087,
-11.4583333333333));
#409801=CARTESIAN_POINT('Ctrl Pts',(1.01778810567669,-0.587620236790434,
-11.4166666666667));
#409802=CARTESIAN_POINT('Ctrl Pts',(1.35705080756892,2.29132664526027E-15,
-11.375));
#409803=CARTESIAN_POINT('Ctrl Pts',(1.01778810567669,0.587620236790438,
-11.3333333333333));
#409804=CARTESIAN_POINT('Ctrl Pts',(0.67852540378446,1.17524047358087,-11.2916666666667));
#409805=CARTESIAN_POINT('Ctrl Pts',(0.,1.17524047358087,-11.25));
#409806=CARTESIAN_POINT('Ctrl Pts',(-0.678525403784459,1.17524047358087,
-11.2083333333333));
#409807=CARTESIAN_POINT('Ctrl Pts',(-1.01778810567669,0.587620236790438,
-11.1666666666667));
#409808=CARTESIAN_POINT('Ctrl Pts',(-1.35705080756892,2.62370823081419E-15,
-11.125));
#409809=CARTESIAN_POINT('Ctrl Pts',(-1.01778810567669,-0.587620236790433,
-11.0833333333333));
#409810=CARTESIAN_POINT('Ctrl Pts',(-0.67852540378446,-1.17524047358087,
-11.0416666666667));
#409811=CARTESIAN_POINT('Ctrl Pts',(-1.43925448419923E-16,-1.17524047358087,
-11.));
#409812=CARTESIAN_POINT('Origin',(0.,-1.11022302462516E-14,-14.21875));
#409813=CARTESIAN_POINT('',(-8.32001735975286E-31,-1.17524047358087,-10.4375));
#409814=CARTESIAN_POINT('',(-8.32001735975286E-31,-1.17524047358087,-10.5));
#409815=CARTESIAN_POINT('',(1.43925448419925E-16,-1.1752404735809,-14.21875));
#409816=CARTESIAN_POINT('Ctrl Pts',(-1.43925448419923E-16,-1.17524047358087,
-10.9375));
#409817=CARTESIAN_POINT('Ctrl Pts',(0.678525403784459,-1.17524047358087,
-10.8958333333333));
#409818=CARTESIAN_POINT('Ctrl Pts',(1.01778810567669,-0.587620236790434,
-10.8541666666667));
#409819=CARTESIAN_POINT('Ctrl Pts',(1.35705080756892,2.29132664526027E-15,
-10.8125));
#409820=CARTESIAN_POINT('Ctrl Pts',(1.01778810567669,0.587620236790438,
-10.7708333333333));
#409821=CARTESIAN_POINT('Ctrl Pts',(0.67852540378446,1.17524047358087,-10.7291666666667));
#409822=CARTESIAN_POINT('Ctrl Pts',(0.,1.17524047358087,-10.6875));
#409823=CARTESIAN_POINT('Ctrl Pts',(-0.678525403784459,1.17524047358087,
-10.6458333333333));
#409824=CARTESIAN_POINT('Ctrl Pts',(-1.01778810567669,0.587620236790438,
-10.6041666666667));
#409825=CARTESIAN_POINT('Ctrl Pts',(-1.35705080756892,2.62370823081419E-15,
-10.5625));
#409826=CARTESIAN_POINT('Ctrl Pts',(-1.01778810567669,-0.587620236790433,
-10.5208333333333));
#409827=CARTESIAN_POINT('Ctrl Pts',(-0.67852540378446,-1.17524047358087,
-10.4791666666667));
#409828=CARTESIAN_POINT('Ctrl Pts',(-1.43925448419923E-16,-1.17524047358087,
-10.4375));
#409829=CARTESIAN_POINT('Ctrl Pts',(-1.43925448419923E-16,-1.17524047358087,
-11.));
#409830=CARTESIAN_POINT('Ctrl Pts',(0.678525403784459,-1.17524047358087,
-10.9583333333333));
#409831=CARTESIAN_POINT('Ctrl Pts',(1.01778810567669,-0.587620236790434,
-10.9166666666667));
#409832=CARTESIAN_POINT('Ctrl Pts',(1.35705080756892,2.29132664526027E-15,
-10.875));
#409833=CARTESIAN_POINT('Ctrl Pts',(1.01778810567669,0.587620236790438,
-10.8333333333333));
#409834=CARTESIAN_POINT('Ctrl Pts',(0.67852540378446,1.17524047358087,-10.7916666666667));
#409835=CARTESIAN_POINT('Ctrl Pts',(0.,1.17524047358087,-10.75));
#409836=CARTESIAN_POINT('Ctrl Pts',(-0.678525403784459,1.17524047358087,
-10.7083333333333));
#409837=CARTESIAN_POINT('Ctrl Pts',(-1.01778810567669,0.587620236790438,
-10.6666666666667));
#409838=CARTESIAN_POINT('Ctrl Pts',(-1.35705080756892,2.62370823081419E-15,
-10.625));
#409839=CARTESIAN_POINT('Ctrl Pts',(-1.01778810567669,-0.587620236790433,
-10.5833333333333));
#409840=CARTESIAN_POINT('Ctrl Pts',(-0.67852540378446,-1.17524047358087,
-10.5416666666667));
#409841=CARTESIAN_POINT('Ctrl Pts',(-1.43925448419923E-16,-1.17524047358087,
-10.5));
#409842=CARTESIAN_POINT('Origin',(0.,-1.11022302462516E-14,-14.21875));
#409843=CARTESIAN_POINT('',(-8.32001735975286E-31,-1.17524047358087,-9.93749999999999));
#409844=CARTESIAN_POINT('',(-8.32001735975286E-31,-1.17524047358087,-9.99999999999999));
#409845=CARTESIAN_POINT('',(1.43925448419925E-16,-1.1752404735809,-14.21875));
#409846=CARTESIAN_POINT('Ctrl Pts',(-1.43925448419923E-16,-1.17524047358087,
-10.4375));
#409847=CARTESIAN_POINT('Ctrl Pts',(0.678525403784459,-1.17524047358087,
-10.3958333333333));
#409848=CARTESIAN_POINT('Ctrl Pts',(1.01778810567669,-0.587620236790434,
-10.3541666666667));
#409849=CARTESIAN_POINT('Ctrl Pts',(1.35705080756892,2.29132664526027E-15,
-10.3125));
#409850=CARTESIAN_POINT('Ctrl Pts',(1.01778810567669,0.587620236790438,
-10.2708333333333));
#409851=CARTESIAN_POINT('Ctrl Pts',(0.67852540378446,1.17524047358087,-10.2291666666667));
#409852=CARTESIAN_POINT('Ctrl Pts',(0.,1.17524047358087,-10.1875));
#409853=CARTESIAN_POINT('Ctrl Pts',(-0.678525403784459,1.17524047358087,
-10.1458333333333));
#409854=CARTESIAN_POINT('Ctrl Pts',(-1.01778810567669,0.587620236790438,
-10.1041666666667));
#409855=CARTESIAN_POINT('Ctrl Pts',(-1.35705080756892,2.62370823081419E-15,
-10.0625));
#409856=CARTESIAN_POINT('Ctrl Pts',(-1.01778810567669,-0.587620236790433,
-10.0208333333333));
#409857=CARTESIAN_POINT('Ctrl Pts',(-0.67852540378446,-1.17524047358087,
-9.97916666666666));
#409858=CARTESIAN_POINT('Ctrl Pts',(-1.43925448419923E-16,-1.17524047358087,
-9.93749999999999));
#409859=CARTESIAN_POINT('Ctrl Pts',(-1.43925448419923E-16,-1.17524047358087,
-10.5));
#409860=CARTESIAN_POINT('Ctrl Pts',(0.678525403784459,-1.17524047358087,
-10.4583333333333));
#409861=CARTESIAN_POINT('Ctrl Pts',(1.01778810567669,-0.587620236790434,
-10.4166666666667));
#409862=CARTESIAN_POINT('Ctrl Pts',(1.35705080756892,2.29132664526027E-15,
-10.375));
#409863=CARTESIAN_POINT('Ctrl Pts',(1.01778810567669,0.587620236790438,
-10.3333333333333));
#409864=CARTESIAN_POINT('Ctrl Pts',(0.67852540378446,1.17524047358087,-10.2916666666667));
#409865=CARTESIAN_POINT('Ctrl Pts',(0.,1.17524047358087,-10.25));
#409866=CARTESIAN_POINT('Ctrl Pts',(-0.678525403784459,1.17524047358087,
-10.2083333333333));
#409867=CARTESIAN_POINT('Ctrl Pts',(-1.01778810567669,0.587620236790438,
-10.1666666666667));
#409868=CARTESIAN_POINT('Ctrl Pts',(-1.35705080756892,2.62370823081419E-15,
-10.125));
#409869=CARTESIAN_POINT('Ctrl Pts',(-1.01778810567669,-0.587620236790433,
-10.0833333333333));
#409870=CARTESIAN_POINT('Ctrl Pts',(-0.67852540378446,-1.17524047358087,
-10.0416666666667));
#409871=CARTESIAN_POINT('Ctrl Pts',(-1.43925448419923E-16,-1.17524047358087,
-9.99999999999999));
#409872=CARTESIAN_POINT('Origin',(0.,-1.11022302462516E-14,-14.21875));
#409873=CARTESIAN_POINT('',(-8.32001735975286E-31,-1.17524047358087,-9.43749999999999));
#409874=CARTESIAN_POINT('',(-8.32001735975286E-31,-1.17524047358087,-9.49999999999999));
#409875=CARTESIAN_POINT('',(1.43925448419925E-16,-1.1752404735809,-14.21875));
#409876=CARTESIAN_POINT('Ctrl Pts',(-1.43925448419923E-16,-1.17524047358087,
-9.93749999999999));
#409877=CARTESIAN_POINT('Ctrl Pts',(0.678525403784459,-1.17524047358087,
-9.89583333333332));
#409878=CARTESIAN_POINT('Ctrl Pts',(1.01778810567669,-0.587620236790434,
-9.85416666666666));
#409879=CARTESIAN_POINT('Ctrl Pts',(1.35705080756892,2.29132664526027E-15,
-9.81249999999999));
#409880=CARTESIAN_POINT('Ctrl Pts',(1.01778810567669,0.587620236790438,
-9.77083333333332));
#409881=CARTESIAN_POINT('Ctrl Pts',(0.67852540378446,1.17524047358087,-9.72916666666666));
#409882=CARTESIAN_POINT('Ctrl Pts',(0.,1.17524047358087,-9.68749999999999));
#409883=CARTESIAN_POINT('Ctrl Pts',(-0.678525403784459,1.17524047358087,
-9.64583333333332));
#409884=CARTESIAN_POINT('Ctrl Pts',(-1.01778810567669,0.587620236790438,
-9.60416666666666));
#409885=CARTESIAN_POINT('Ctrl Pts',(-1.35705080756892,2.62370823081419E-15,
-9.56249999999999));
#409886=CARTESIAN_POINT('Ctrl Pts',(-1.01778810567669,-0.587620236790433,
-9.52083333333332));
#409887=CARTESIAN_POINT('Ctrl Pts',(-0.67852540378446,-1.17524047358087,
-9.47916666666666));
#409888=CARTESIAN_POINT('Ctrl Pts',(-1.43925448419923E-16,-1.17524047358087,
-9.43749999999999));
#409889=CARTESIAN_POINT('Ctrl Pts',(-1.43925448419923E-16,-1.17524047358087,
-9.99999999999999));
#409890=CARTESIAN_POINT('Ctrl Pts',(0.678525403784459,-1.17524047358087,
-9.95833333333332));
#409891=CARTESIAN_POINT('Ctrl Pts',(1.01778810567669,-0.587620236790434,
-9.91666666666666));
#409892=CARTESIAN_POINT('Ctrl Pts',(1.35705080756892,2.29132664526027E-15,
-9.87499999999999));
#409893=CARTESIAN_POINT('Ctrl Pts',(1.01778810567669,0.587620236790438,
-9.83333333333332));
#409894=CARTESIAN_POINT('Ctrl Pts',(0.67852540378446,1.17524047358087,-9.79166666666666));
#409895=CARTESIAN_POINT('Ctrl Pts',(0.,1.17524047358087,-9.74999999999999));
#409896=CARTESIAN_POINT('Ctrl Pts',(-0.678525403784459,1.17524047358087,
-9.70833333333332));
#409897=CARTESIAN_POINT('Ctrl Pts',(-1.01778810567669,0.587620236790438,
-9.66666666666666));
#409898=CARTESIAN_POINT('Ctrl Pts',(-1.35705080756892,2.62370823081419E-15,
-9.62499999999999));
#409899=CARTESIAN_POINT('Ctrl Pts',(-1.01778810567669,-0.587620236790433,
-9.58333333333332));
#409900=CARTESIAN_POINT('Ctrl Pts',(-0.67852540378446,-1.17524047358087,
-9.54166666666666));
#409901=CARTESIAN_POINT('Ctrl Pts',(-1.43925448419923E-16,-1.17524047358087,
-9.49999999999999));
#409902=CARTESIAN_POINT('Origin',(0.,-1.11022302462516E-14,-14.21875));
#409903=CARTESIAN_POINT('',(-8.32001735975286E-31,-1.17524047358087,-8.93749999999999));
#409904=CARTESIAN_POINT('',(-8.32001735975286E-31,-1.17524047358087,-8.99999999999999));
#409905=CARTESIAN_POINT('',(1.43925448419925E-16,-1.1752404735809,-14.21875));
#409906=CARTESIAN_POINT('Ctrl Pts',(-1.43925448419923E-16,-1.17524047358087,
-9.43749999999999));
#409907=CARTESIAN_POINT('Ctrl Pts',(0.678525403784459,-1.17524047358087,
-9.39583333333332));
#409908=CARTESIAN_POINT('Ctrl Pts',(1.01778810567669,-0.587620236790434,
-9.35416666666666));
#409909=CARTESIAN_POINT('Ctrl Pts',(1.35705080756892,2.29132664526027E-15,
-9.31249999999999));
#409910=CARTESIAN_POINT('Ctrl Pts',(1.01778810567669,0.587620236790438,
-9.27083333333332));
#409911=CARTESIAN_POINT('Ctrl Pts',(0.67852540378446,1.17524047358087,-9.22916666666666));
#409912=CARTESIAN_POINT('Ctrl Pts',(0.,1.17524047358087,-9.18749999999999));
#409913=CARTESIAN_POINT('Ctrl Pts',(-0.678525403784459,1.17524047358087,
-9.14583333333333));
#409914=CARTESIAN_POINT('Ctrl Pts',(-1.01778810567669,0.587620236790438,
-9.10416666666666));
#409915=CARTESIAN_POINT('Ctrl Pts',(-1.35705080756892,2.62370823081419E-15,
-9.06249999999999));
#409916=CARTESIAN_POINT('Ctrl Pts',(-1.01778810567669,-0.587620236790433,
-9.02083333333332));
#409917=CARTESIAN_POINT('Ctrl Pts',(-0.67852540378446,-1.17524047358087,
-8.97916666666666));
#409918=CARTESIAN_POINT('Ctrl Pts',(-1.43925448419923E-16,-1.17524047358087,
-8.93749999999999));
#409919=CARTESIAN_POINT('Ctrl Pts',(-1.43925448419923E-16,-1.17524047358087,
-9.49999999999999));
#409920=CARTESIAN_POINT('Ctrl Pts',(0.678525403784459,-1.17524047358087,
-9.45833333333333));
#409921=CARTESIAN_POINT('Ctrl Pts',(1.01778810567669,-0.587620236790434,
-9.41666666666666));
#409922=CARTESIAN_POINT('Ctrl Pts',(1.35705080756892,2.29132664526027E-15,
-9.37499999999999));
#409923=CARTESIAN_POINT('Ctrl Pts',(1.01778810567669,0.587620236790438,
-9.33333333333332));
#409924=CARTESIAN_POINT('Ctrl Pts',(0.67852540378446,1.17524047358087,-9.29166666666666));
#409925=CARTESIAN_POINT('Ctrl Pts',(0.,1.17524047358087,-9.24999999999999));
#409926=CARTESIAN_POINT('Ctrl Pts',(-0.678525403784459,1.17524047358087,
-9.20833333333332));
#409927=CARTESIAN_POINT('Ctrl Pts',(-1.01778810567669,0.587620236790438,
-9.16666666666666));
#409928=CARTESIAN_POINT('Ctrl Pts',(-1.35705080756892,2.62370823081419E-15,
-9.12499999999999));
#409929=CARTESIAN_POINT('Ctrl Pts',(-1.01778810567669,-0.587620236790433,
-9.08333333333332));
#409930=CARTESIAN_POINT('Ctrl Pts',(-0.67852540378446,-1.17524047358087,
-9.04166666666666));
#409931=CARTESIAN_POINT('Ctrl Pts',(-1.43925448419923E-16,-1.17524047358087,
-8.99999999999999));
#409932=CARTESIAN_POINT('Origin',(0.,-1.11022302462516E-14,-14.21875));
#409933=CARTESIAN_POINT('',(-8.32001735975286E-31,-1.17524047358087,-8.43749999999999));
#409934=CARTESIAN_POINT('',(-8.32001735975286E-31,-1.17524047358087,-8.49999999999999));
#409935=CARTESIAN_POINT('',(1.43925448419925E-16,-1.1752404735809,-14.21875));
#409936=CARTESIAN_POINT('Ctrl Pts',(-1.43925448419923E-16,-1.17524047358087,
-8.93749999999999));
#409937=CARTESIAN_POINT('Ctrl Pts',(0.678525403784459,-1.17524047358087,
-8.89583333333332));
#409938=CARTESIAN_POINT('Ctrl Pts',(1.01778810567669,-0.587620236790434,
-8.85416666666666));
#409939=CARTESIAN_POINT('Ctrl Pts',(1.35705080756892,2.29132664526027E-15,
-8.81249999999999));
#409940=CARTESIAN_POINT('Ctrl Pts',(1.01778810567669,0.587620236790438,
-8.77083333333332));
#409941=CARTESIAN_POINT('Ctrl Pts',(0.67852540378446,1.17524047358087,-8.72916666666666));
#409942=CARTESIAN_POINT('Ctrl Pts',(0.,1.17524047358087,-8.68749999999999));
#409943=CARTESIAN_POINT('Ctrl Pts',(-0.678525403784459,1.17524047358087,
-8.64583333333333));
#409944=CARTESIAN_POINT('Ctrl Pts',(-1.01778810567669,0.587620236790438,
-8.60416666666666));
#409945=CARTESIAN_POINT('Ctrl Pts',(-1.35705080756892,2.62370823081419E-15,
-8.56249999999999));
#409946=CARTESIAN_POINT('Ctrl Pts',(-1.01778810567669,-0.587620236790433,
-8.52083333333333));
#409947=CARTESIAN_POINT('Ctrl Pts',(-0.67852540378446,-1.17524047358087,
-8.47916666666666));
#409948=CARTESIAN_POINT('Ctrl Pts',(-1.43925448419923E-16,-1.17524047358087,
-8.43749999999999));
#409949=CARTESIAN_POINT('Ctrl Pts',(-1.43925448419923E-16,-1.17524047358087,
-8.99999999999999));
#409950=CARTESIAN_POINT('Ctrl Pts',(0.678525403784459,-1.17524047358087,
-8.95833333333332));
#409951=CARTESIAN_POINT('Ctrl Pts',(1.01778810567669,-0.587620236790434,
-8.91666666666666));
#409952=CARTESIAN_POINT('Ctrl Pts',(1.35705080756892,2.29132664526027E-15,
-8.87499999999999));
#409953=CARTESIAN_POINT('Ctrl Pts',(1.01778810567669,0.587620236790438,
-8.83333333333333));
#409954=CARTESIAN_POINT('Ctrl Pts',(0.67852540378446,1.17524047358087,-8.79166666666666));
#409955=CARTESIAN_POINT('Ctrl Pts',(0.,1.17524047358087,-8.74999999999999));
#409956=CARTESIAN_POINT('Ctrl Pts',(-0.678525403784459,1.17524047358087,
-8.70833333333333));
#409957=CARTESIAN_POINT('Ctrl Pts',(-1.01778810567669,0.587620236790438,
-8.66666666666666));
#409958=CARTESIAN_POINT('Ctrl Pts',(-1.35705080756892,2.62370823081419E-15,
-8.62499999999999));
#409959=CARTESIAN_POINT('Ctrl Pts',(-1.01778810567669,-0.587620236790433,
-8.58333333333333));
#409960=CARTESIAN_POINT('Ctrl Pts',(-0.67852540378446,-1.17524047358087,
-8.54166666666666));
#409961=CARTESIAN_POINT('Ctrl Pts',(-1.43925448419923E-16,-1.17524047358087,
-8.49999999999999));
#409962=CARTESIAN_POINT('Origin',(0.,-1.11022302462516E-14,-14.21875));
#409963=CARTESIAN_POINT('',(-8.32001735975286E-31,-1.17524047358087,-7.93749999999999));
#409964=CARTESIAN_POINT('',(-8.32001735975286E-31,-1.17524047358087,-7.99999999999999));
#409965=CARTESIAN_POINT('',(1.43925448419925E-16,-1.1752404735809,-14.21875));
#409966=CARTESIAN_POINT('Ctrl Pts',(-1.43925448419923E-16,-1.17524047358087,
-8.43749999999999));
#409967=CARTESIAN_POINT('Ctrl Pts',(0.678525403784459,-1.17524047358087,
-8.39583333333333));
#409968=CARTESIAN_POINT('Ctrl Pts',(1.01778810567669,-0.587620236790434,
-8.35416666666666));
#409969=CARTESIAN_POINT('Ctrl Pts',(1.35705080756892,2.29132664526027E-15,
-8.31249999999999));
#409970=CARTESIAN_POINT('Ctrl Pts',(1.01778810567669,0.587620236790438,
-8.27083333333333));
#409971=CARTESIAN_POINT('Ctrl Pts',(0.67852540378446,1.17524047358087,-8.22916666666666));
#409972=CARTESIAN_POINT('Ctrl Pts',(0.,1.17524047358087,-8.18749999999999));
#409973=CARTESIAN_POINT('Ctrl Pts',(-0.678525403784459,1.17524047358087,
-8.14583333333333));
#409974=CARTESIAN_POINT('Ctrl Pts',(-1.01778810567669,0.587620236790438,
-8.10416666666666));
#409975=CARTESIAN_POINT('Ctrl Pts',(-1.35705080756892,2.62370823081419E-15,
-8.06249999999999));
#409976=CARTESIAN_POINT('Ctrl Pts',(-1.01778810567669,-0.587620236790433,
-8.02083333333333));
#409977=CARTESIAN_POINT('Ctrl Pts',(-0.67852540378446,-1.17524047358087,
-7.97916666666666));
#409978=CARTESIAN_POINT('Ctrl Pts',(-1.43925448419923E-16,-1.17524047358087,
-7.93749999999999));
#409979=CARTESIAN_POINT('Ctrl Pts',(-1.43925448419923E-16,-1.17524047358087,
-8.49999999999999));
#409980=CARTESIAN_POINT('Ctrl Pts',(0.678525403784459,-1.17524047358087,
-8.45833333333333));
#409981=CARTESIAN_POINT('Ctrl Pts',(1.01778810567669,-0.587620236790434,
-8.41666666666666));
#409982=CARTESIAN_POINT('Ctrl Pts',(1.35705080756892,2.29132664526027E-15,
-8.37499999999999));
#409983=CARTESIAN_POINT('Ctrl Pts',(1.01778810567669,0.587620236790438,
-8.33333333333333));
#409984=CARTESIAN_POINT('Ctrl Pts',(0.67852540378446,1.17524047358087,-8.29166666666666));
#409985=CARTESIAN_POINT('Ctrl Pts',(0.,1.17524047358087,-8.24999999999999));
#409986=CARTESIAN_POINT('Ctrl Pts',(-0.678525403784459,1.17524047358087,
-8.20833333333333));
#409987=CARTESIAN_POINT('Ctrl Pts',(-1.01778810567669,0.587620236790438,
-8.16666666666666));
#409988=CARTESIAN_POINT('Ctrl Pts',(-1.35705080756892,2.62370823081419E-15,
-8.12499999999999));
#409989=CARTESIAN_POINT('Ctrl Pts',(-1.01778810567669,-0.587620236790433,
-8.08333333333333));
#409990=CARTESIAN_POINT('Ctrl Pts',(-0.67852540378446,-1.17524047358087,
-8.04166666666666));
#409991=CARTESIAN_POINT('Ctrl Pts',(-1.43925448419923E-16,-1.17524047358087,
-7.99999999999999));
#409992=CARTESIAN_POINT('Origin',(0.,-1.11022302462516E-14,-14.21875));
#409993=CARTESIAN_POINT('',(-8.32001735975286E-31,-1.17524047358087,-7.43749999999999));
#409994=CARTESIAN_POINT('',(-8.32001735975286E-31,-1.17524047358087,-7.49999999999999));
#409995=CARTESIAN_POINT('',(1.43925448419925E-16,-1.1752404735809,-14.21875));
#409996=CARTESIAN_POINT('Ctrl Pts',(-1.43925448419923E-16,-1.17524047358087,
-7.93749999999999));
#409997=CARTESIAN_POINT('Ctrl Pts',(0.678525403784459,-1.17524047358087,
-7.89583333333332));
#409998=CARTESIAN_POINT('Ctrl Pts',(1.01778810567669,-0.587620236790434,
-7.85416666666666));
#409999=CARTESIAN_POINT('Ctrl Pts',(1.35705080756892,2.29132664526027E-15,
-7.81249999999999));
#410000=CARTESIAN_POINT('Ctrl Pts',(1.01778810567669,0.587620236790438,
-7.77083333333332));
#410001=CARTESIAN_POINT('Ctrl Pts',(0.67852540378446,1.17524047358087,-7.72916666666666));
#410002=CARTESIAN_POINT('Ctrl Pts',(0.,1.17524047358087,-7.68749999999999));
#410003=CARTESIAN_POINT('Ctrl Pts',(-0.678525403784459,1.17524047358087,
-7.64583333333333));
#410004=CARTESIAN_POINT('Ctrl Pts',(-1.01778810567669,0.587620236790438,
-7.60416666666666));
#410005=CARTESIAN_POINT('Ctrl Pts',(-1.35705080756892,2.62370823081419E-15,
-7.56249999999999));
#410006=CARTESIAN_POINT('Ctrl Pts',(-1.01778810567669,-0.587620236790433,
-7.52083333333332));
#410007=CARTESIAN_POINT('Ctrl Pts',(-0.67852540378446,-1.17524047358087,
-7.47916666666666));
#410008=CARTESIAN_POINT('Ctrl Pts',(-1.43925448419923E-16,-1.17524047358087,
-7.43749999999999));
#410009=CARTESIAN_POINT('Ctrl Pts',(-1.43925448419923E-16,-1.17524047358087,
-7.99999999999999));
#410010=CARTESIAN_POINT('Ctrl Pts',(0.678525403784459,-1.17524047358087,
-7.95833333333333));
#410011=CARTESIAN_POINT('Ctrl Pts',(1.01778810567669,-0.587620236790434,
-7.91666666666666));
#410012=CARTESIAN_POINT('Ctrl Pts',(1.35705080756892,2.29132664526027E-15,
-7.87499999999999));
#410013=CARTESIAN_POINT('Ctrl Pts',(1.01778810567669,0.587620236790438,
-7.83333333333332));
#410014=CARTESIAN_POINT('Ctrl Pts',(0.67852540378446,1.17524047358087,-7.79166666666666));
#410015=CARTESIAN_POINT('Ctrl Pts',(0.,1.17524047358087,-7.74999999999999));
#410016=CARTESIAN_POINT('Ctrl Pts',(-0.678525403784459,1.17524047358087,
-7.70833333333332));
#410017=CARTESIAN_POINT('Ctrl Pts',(-1.01778810567669,0.587620236790438,
-7.66666666666666));
#410018=CARTESIAN_POINT('Ctrl Pts',(-1.35705080756892,2.62370823081419E-15,
-7.62499999999999));
#410019=CARTESIAN_POINT('Ctrl Pts',(-1.01778810567669,-0.587620236790433,
-7.58333333333332));
#410020=CARTESIAN_POINT('Ctrl Pts',(-0.67852540378446,-1.17524047358087,
-7.54166666666666));
#410021=CARTESIAN_POINT('Ctrl Pts',(-1.43925448419923E-16,-1.17524047358087,
-7.49999999999999));
#410022=CARTESIAN_POINT('Origin',(0.,-1.11022302462516E-14,-14.21875));
#410023=CARTESIAN_POINT('',(-8.32001735975286E-31,-1.17524047358087,-6.93749999999999));
#410024=CARTESIAN_POINT('',(-8.32001735975286E-31,-1.17524047358087,-6.99999999999999));
#410025=CARTESIAN_POINT('',(1.43925448419925E-16,-1.1752404735809,-14.21875));
#410026=CARTESIAN_POINT('Ctrl Pts',(-1.43925448419923E-16,-1.17524047358087,
-7.43749999999999));
#410027=CARTESIAN_POINT('Ctrl Pts',(0.678525403784459,-1.17524047358087,
-7.39583333333332));
#410028=CARTESIAN_POINT('Ctrl Pts',(1.01778810567669,-0.587620236790434,
-7.35416666666666));
#410029=CARTESIAN_POINT('Ctrl Pts',(1.35705080756892,2.29132664526027E-15,
-7.31249999999999));
#410030=CARTESIAN_POINT('Ctrl Pts',(1.01778810567669,0.587620236790438,
-7.27083333333332));
#410031=CARTESIAN_POINT('Ctrl Pts',(0.67852540378446,1.17524047358087,-7.22916666666666));
#410032=CARTESIAN_POINT('Ctrl Pts',(0.,1.17524047358087,-7.18749999999999));
#410033=CARTESIAN_POINT('Ctrl Pts',(-0.678525403784459,1.17524047358087,
-7.14583333333332));
#410034=CARTESIAN_POINT('Ctrl Pts',(-1.01778810567669,0.587620236790438,
-7.10416666666666));
#410035=CARTESIAN_POINT('Ctrl Pts',(-1.35705080756892,2.62370823081419E-15,
-7.06249999999999));
#410036=CARTESIAN_POINT('Ctrl Pts',(-1.01778810567669,-0.587620236790433,
-7.02083333333332));
#410037=CARTESIAN_POINT('Ctrl Pts',(-0.67852540378446,-1.17524047358087,
-6.97916666666666));
#410038=CARTESIAN_POINT('Ctrl Pts',(-1.43925448419923E-16,-1.17524047358087,
-6.93749999999999));
#410039=CARTESIAN_POINT('Ctrl Pts',(-1.43925448419923E-16,-1.17524047358087,
-7.49999999999999));
#410040=CARTESIAN_POINT('Ctrl Pts',(0.678525403784459,-1.17524047358087,
-7.45833333333332));
#410041=CARTESIAN_POINT('Ctrl Pts',(1.01778810567669,-0.587620236790434,
-7.41666666666666));
#410042=CARTESIAN_POINT('Ctrl Pts',(1.35705080756892,2.29132664526027E-15,
-7.37499999999999));
#410043=CARTESIAN_POINT('Ctrl Pts',(1.01778810567669,0.587620236790438,
-7.33333333333332));
#410044=CARTESIAN_POINT('Ctrl Pts',(0.67852540378446,1.17524047358087,-7.29166666666666));
#410045=CARTESIAN_POINT('Ctrl Pts',(0.,1.17524047358087,-7.24999999999999));
#410046=CARTESIAN_POINT('Ctrl Pts',(-0.678525403784459,1.17524047358087,
-7.20833333333332));
#410047=CARTESIAN_POINT('Ctrl Pts',(-1.01778810567669,0.587620236790438,
-7.16666666666666));
#410048=CARTESIAN_POINT('Ctrl Pts',(-1.35705080756892,2.62370823081419E-15,
-7.12499999999999));
#410049=CARTESIAN_POINT('Ctrl Pts',(-1.01778810567669,-0.587620236790433,
-7.08333333333332));
#410050=CARTESIAN_POINT('Ctrl Pts',(-0.67852540378446,-1.17524047358087,
-7.04166666666666));
#410051=CARTESIAN_POINT('Ctrl Pts',(-1.43925448419923E-16,-1.17524047358087,
-6.99999999999999));
#410052=CARTESIAN_POINT('Origin',(0.,-1.11022302462516E-14,-14.21875));
#410053=CARTESIAN_POINT('',(-8.32001735975286E-31,-1.17524047358087,-6.43749999999999));
#410054=CARTESIAN_POINT('',(-8.32001735975286E-31,-1.17524047358087,-6.49999999999999));
#410055=CARTESIAN_POINT('',(1.43925448419925E-16,-1.1752404735809,-14.21875));
#410056=CARTESIAN_POINT('Ctrl Pts',(-1.43925448419923E-16,-1.17524047358087,
-6.93749999999999));
#410057=CARTESIAN_POINT('Ctrl Pts',(0.678525403784459,-1.17524047358087,
-6.89583333333332));
#410058=CARTESIAN_POINT('Ctrl Pts',(1.01778810567669,-0.587620236790434,
-6.85416666666666));
#410059=CARTESIAN_POINT('Ctrl Pts',(1.35705080756892,2.29132664526027E-15,
-6.81249999999999));
#410060=CARTESIAN_POINT('Ctrl Pts',(1.01778810567669,0.587620236790438,
-6.77083333333333));
#410061=CARTESIAN_POINT('Ctrl Pts',(0.67852540378446,1.17524047358087,-6.72916666666666));
#410062=CARTESIAN_POINT('Ctrl Pts',(0.,1.17524047358087,-6.68749999999999));
#410063=CARTESIAN_POINT('Ctrl Pts',(-0.678525403784459,1.17524047358087,
-6.64583333333332));
#410064=CARTESIAN_POINT('Ctrl Pts',(-1.01778810567669,0.587620236790438,
-6.60416666666666));
#410065=CARTESIAN_POINT('Ctrl Pts',(-1.35705080756892,2.62370823081419E-15,
-6.56249999999999));
#410066=CARTESIAN_POINT('Ctrl Pts',(-1.01778810567669,-0.587620236790433,
-6.52083333333333));
#410067=CARTESIAN_POINT('Ctrl Pts',(-0.67852540378446,-1.17524047358087,
-6.47916666666666));
#410068=CARTESIAN_POINT('Ctrl Pts',(-1.43925448419923E-16,-1.17524047358087,
-6.43749999999999));
#410069=CARTESIAN_POINT('Ctrl Pts',(-1.43925448419923E-16,-1.17524047358087,
-6.99999999999999));
#410070=CARTESIAN_POINT('Ctrl Pts',(0.678525403784459,-1.17524047358087,
-6.95833333333332));
#410071=CARTESIAN_POINT('Ctrl Pts',(1.01778810567669,-0.587620236790434,
-6.91666666666666));
#410072=CARTESIAN_POINT('Ctrl Pts',(1.35705080756892,2.29132664526027E-15,
-6.87499999999999));
#410073=CARTESIAN_POINT('Ctrl Pts',(1.01778810567669,0.587620236790438,
-6.83333333333333));
#410074=CARTESIAN_POINT('Ctrl Pts',(0.67852540378446,1.17524047358087,-6.79166666666666));
#410075=CARTESIAN_POINT('Ctrl Pts',(0.,1.17524047358087,-6.74999999999999));
#410076=CARTESIAN_POINT('Ctrl Pts',(-0.678525403784459,1.17524047358087,
-6.70833333333333));
#410077=CARTESIAN_POINT('Ctrl Pts',(-1.01778810567669,0.587620236790438,
-6.66666666666666));
#410078=CARTESIAN_POINT('Ctrl Pts',(-1.35705080756892,2.62370823081419E-15,
-6.62499999999999));
#410079=CARTESIAN_POINT('Ctrl Pts',(-1.01778810567669,-0.587620236790433,
-6.58333333333332));
#410080=CARTESIAN_POINT('Ctrl Pts',(-0.67852540378446,-1.17524047358087,
-6.54166666666666));
#410081=CARTESIAN_POINT('Ctrl Pts',(-1.43925448419923E-16,-1.17524047358087,
-6.49999999999999));
#410082=CARTESIAN_POINT('Origin',(0.,-1.11022302462516E-14,-14.21875));
#410083=CARTESIAN_POINT('',(-8.32001735975286E-31,-1.17524047358087,-5.93749999999999));
#410084=CARTESIAN_POINT('',(-8.32001735975286E-31,-1.17524047358087,-5.99999999999999));
#410085=CARTESIAN_POINT('',(1.43925448419925E-16,-1.1752404735809,-14.21875));
#410086=CARTESIAN_POINT('Ctrl Pts',(-1.43925448419923E-16,-1.17524047358087,
-6.43749999999999));
#410087=CARTESIAN_POINT('Ctrl Pts',(0.678525403784459,-1.17524047358087,
-6.39583333333333));
#410088=CARTESIAN_POINT('Ctrl Pts',(1.01778810567669,-0.587620236790434,
-6.35416666666666));
#410089=CARTESIAN_POINT('Ctrl Pts',(1.35705080756892,2.29132664526027E-15,
-6.31249999999999));
#410090=CARTESIAN_POINT('Ctrl Pts',(1.01778810567669,0.587620236790438,
-6.27083333333332));
#410091=CARTESIAN_POINT('Ctrl Pts',(0.67852540378446,1.17524047358087,-6.22916666666666));
#410092=CARTESIAN_POINT('Ctrl Pts',(0.,1.17524047358087,-6.18749999999999));
#410093=CARTESIAN_POINT('Ctrl Pts',(-0.678525403784459,1.17524047358087,
-6.14583333333333));
#410094=CARTESIAN_POINT('Ctrl Pts',(-1.01778810567669,0.587620236790438,
-6.10416666666666));
#410095=CARTESIAN_POINT('Ctrl Pts',(-1.35705080756892,2.62370823081419E-15,
-6.06249999999999));
#410096=CARTESIAN_POINT('Ctrl Pts',(-1.01778810567669,-0.587620236790433,
-6.02083333333332));
#410097=CARTESIAN_POINT('Ctrl Pts',(-0.67852540378446,-1.17524047358087,
-5.97916666666666));
#410098=CARTESIAN_POINT('Ctrl Pts',(-1.43925448419923E-16,-1.17524047358087,
-5.93749999999999));
#410099=CARTESIAN_POINT('Ctrl Pts',(-1.43925448419923E-16,-1.17524047358087,
-6.49999999999999));
#410100=CARTESIAN_POINT('Ctrl Pts',(0.678525403784459,-1.17524047358087,
-6.45833333333333));
#410101=CARTESIAN_POINT('Ctrl Pts',(1.01778810567669,-0.587620236790434,
-6.41666666666666));
#410102=CARTESIAN_POINT('Ctrl Pts',(1.35705080756892,2.29132664526027E-15,
-6.37499999999999));
#410103=CARTESIAN_POINT('Ctrl Pts',(1.01778810567669,0.587620236790438,
-6.33333333333332));
#410104=CARTESIAN_POINT('Ctrl Pts',(0.67852540378446,1.17524047358087,-6.29166666666666));
#410105=CARTESIAN_POINT('Ctrl Pts',(0.,1.17524047358087,-6.24999999999999));
#410106=CARTESIAN_POINT('Ctrl Pts',(-0.678525403784459,1.17524047358087,
-6.20833333333333));
#410107=CARTESIAN_POINT('Ctrl Pts',(-1.01778810567669,0.587620236790438,
-6.16666666666666));
#410108=CARTESIAN_POINT('Ctrl Pts',(-1.35705080756892,2.62370823081419E-15,
-6.12499999999999));
#410109=CARTESIAN_POINT('Ctrl Pts',(-1.01778810567669,-0.587620236790433,
-6.08333333333333));
#410110=CARTESIAN_POINT('Ctrl Pts',(-0.67852540378446,-1.17524047358087,
-6.04166666666666));
#410111=CARTESIAN_POINT('Ctrl Pts',(-1.43925448419923E-16,-1.17524047358087,
-5.99999999999999));
#410112=CARTESIAN_POINT('Origin',(0.,-1.11022302462516E-14,-14.21875));
#410113=CARTESIAN_POINT('',(-8.32001735975286E-31,-1.17524047358087,-5.43749999999999));
#410114=CARTESIAN_POINT('',(-8.32001735975286E-31,-1.17524047358087,-5.49999999999999));
#410115=CARTESIAN_POINT('',(1.43925448419925E-16,-1.1752404735809,-14.21875));
#410116=CARTESIAN_POINT('Ctrl Pts',(-1.43925448419923E-16,-1.17524047358087,
-5.93749999999999));
#410117=CARTESIAN_POINT('Ctrl Pts',(0.678525403784459,-1.17524047358087,
-5.89583333333333));
#410118=CARTESIAN_POINT('Ctrl Pts',(1.01778810567669,-0.587620236790434,
-5.85416666666666));
#410119=CARTESIAN_POINT('Ctrl Pts',(1.35705080756892,2.29132664526027E-15,
-5.81249999999999));
#410120=CARTESIAN_POINT('Ctrl Pts',(1.01778810567669,0.587620236790438,
-5.77083333333332));
#410121=CARTESIAN_POINT('Ctrl Pts',(0.67852540378446,1.17524047358087,-5.72916666666666));
#410122=CARTESIAN_POINT('Ctrl Pts',(0.,1.17524047358087,-5.68749999999999));
#410123=CARTESIAN_POINT('Ctrl Pts',(-0.678525403784459,1.17524047358087,
-5.64583333333332));
#410124=CARTESIAN_POINT('Ctrl Pts',(-1.01778810567669,0.587620236790438,
-5.60416666666666));
#410125=CARTESIAN_POINT('Ctrl Pts',(-1.35705080756892,2.62370823081419E-15,
-5.56249999999999));
#410126=CARTESIAN_POINT('Ctrl Pts',(-1.01778810567669,-0.587620236790433,
-5.52083333333333));
#410127=CARTESIAN_POINT('Ctrl Pts',(-0.67852540378446,-1.17524047358087,
-5.47916666666666));
#410128=CARTESIAN_POINT('Ctrl Pts',(-1.43925448419923E-16,-1.17524047358087,
-5.43749999999999));
#410129=CARTESIAN_POINT('Ctrl Pts',(-1.43925448419923E-16,-1.17524047358087,
-5.99999999999999));
#410130=CARTESIAN_POINT('Ctrl Pts',(0.678525403784459,-1.17524047358087,
-5.95833333333332));
#410131=CARTESIAN_POINT('Ctrl Pts',(1.01778810567669,-0.587620236790434,
-5.91666666666666));
#410132=CARTESIAN_POINT('Ctrl Pts',(1.35705080756892,2.29132664526027E-15,
-5.87499999999999));
#410133=CARTESIAN_POINT('Ctrl Pts',(1.01778810567669,0.587620236790438,
-5.83333333333333));
#410134=CARTESIAN_POINT('Ctrl Pts',(0.67852540378446,1.17524047358087,-5.79166666666666));
#410135=CARTESIAN_POINT('Ctrl Pts',(0.,1.17524047358087,-5.74999999999999));
#410136=CARTESIAN_POINT('Ctrl Pts',(-0.678525403784459,1.17524047358087,
-5.70833333333332));
#410137=CARTESIAN_POINT('Ctrl Pts',(-1.01778810567669,0.587620236790438,
-5.66666666666666));
#410138=CARTESIAN_POINT('Ctrl Pts',(-1.35705080756892,2.62370823081419E-15,
-5.62499999999999));
#410139=CARTESIAN_POINT('Ctrl Pts',(-1.01778810567669,-0.587620236790433,
-5.58333333333333));
#410140=CARTESIAN_POINT('Ctrl Pts',(-0.67852540378446,-1.17524047358087,
-5.54166666666666));
#410141=CARTESIAN_POINT('Ctrl Pts',(-1.43925448419923E-16,-1.17524047358087,
-5.49999999999999));
#410142=CARTESIAN_POINT('Origin',(0.,-1.11022302462516E-14,-14.21875));
#410143=CARTESIAN_POINT('',(-8.32001735975286E-31,-1.17524047358087,-4.93749999999999));
#410144=CARTESIAN_POINT('',(-8.32001735975286E-31,-1.17524047358087,-4.99999999999999));
#410145=CARTESIAN_POINT('',(1.43925448419925E-16,-1.1752404735809,-14.21875));
#410146=CARTESIAN_POINT('Ctrl Pts',(-1.43925448419923E-16,-1.17524047358087,
-5.43749999999999));
#410147=CARTESIAN_POINT('Ctrl Pts',(0.678525403784459,-1.17524047358087,
-5.39583333333332));
#410148=CARTESIAN_POINT('Ctrl Pts',(1.01778810567669,-0.587620236790434,
-5.35416666666666));
#410149=CARTESIAN_POINT('Ctrl Pts',(1.35705080756892,2.29132664526027E-15,
-5.31249999999999));
#410150=CARTESIAN_POINT('Ctrl Pts',(1.01778810567669,0.587620236790438,
-5.27083333333332));
#410151=CARTESIAN_POINT('Ctrl Pts',(0.67852540378446,1.17524047358087,-5.22916666666666));
#410152=CARTESIAN_POINT('Ctrl Pts',(0.,1.17524047358087,-5.18749999999999));
#410153=CARTESIAN_POINT('Ctrl Pts',(-0.678525403784459,1.17524047358087,
-5.14583333333332));
#410154=CARTESIAN_POINT('Ctrl Pts',(-1.01778810567669,0.587620236790438,
-5.10416666666666));
#410155=CARTESIAN_POINT('Ctrl Pts',(-1.35705080756892,2.62370823081419E-15,
-5.06249999999999));
#410156=CARTESIAN_POINT('Ctrl Pts',(-1.01778810567669,-0.587620236790433,
-5.02083333333332));
#410157=CARTESIAN_POINT('Ctrl Pts',(-0.67852540378446,-1.17524047358087,
-4.97916666666666));
#410158=CARTESIAN_POINT('Ctrl Pts',(-1.43925448419923E-16,-1.17524047358087,
-4.93749999999999));
#410159=CARTESIAN_POINT('Ctrl Pts',(-1.43925448419923E-16,-1.17524047358087,
-5.49999999999999));
#410160=CARTESIAN_POINT('Ctrl Pts',(0.678525403784459,-1.17524047358087,
-5.45833333333332));
#410161=CARTESIAN_POINT('Ctrl Pts',(1.01778810567669,-0.587620236790434,
-5.41666666666666));
#410162=CARTESIAN_POINT('Ctrl Pts',(1.35705080756892,2.29132664526027E-15,
-5.37499999999999));
#410163=CARTESIAN_POINT('Ctrl Pts',(1.01778810567669,0.587620236790438,
-5.33333333333332));
#410164=CARTESIAN_POINT('Ctrl Pts',(0.67852540378446,1.17524047358087,-5.29166666666666));
#410165=CARTESIAN_POINT('Ctrl Pts',(0.,1.17524047358087,-5.24999999999999));
#410166=CARTESIAN_POINT('Ctrl Pts',(-0.678525403784459,1.17524047358087,
-5.20833333333332));
#410167=CARTESIAN_POINT('Ctrl Pts',(-1.01778810567669,0.587620236790438,
-5.16666666666666));
#410168=CARTESIAN_POINT('Ctrl Pts',(-1.35705080756892,2.62370823081419E-15,
-5.12499999999999));
#410169=CARTESIAN_POINT('Ctrl Pts',(-1.01778810567669,-0.587620236790433,
-5.08333333333332));
#410170=CARTESIAN_POINT('Ctrl Pts',(-0.67852540378446,-1.17524047358087,
-5.04166666666666));
#410171=CARTESIAN_POINT('Ctrl Pts',(-1.43925448419923E-16,-1.17524047358087,
-4.99999999999999));
#410172=CARTESIAN_POINT('Origin',(0.,-1.11022302462516E-14,-14.21875));
#410173=CARTESIAN_POINT('',(-8.32001735975286E-31,-1.17524047358087,-4.43749999999999));
#410174=CARTESIAN_POINT('',(-8.32001735975286E-31,-1.17524047358087,-4.49999999999999));
#410175=CARTESIAN_POINT('',(1.43925448419925E-16,-1.1752404735809,-14.21875));
#410176=CARTESIAN_POINT('Ctrl Pts',(-1.43925448419923E-16,-1.17524047358087,
-4.93749999999999));
#410177=CARTESIAN_POINT('Ctrl Pts',(0.678525403784459,-1.17524047358087,
-4.89583333333332));
#410178=CARTESIAN_POINT('Ctrl Pts',(1.01778810567669,-0.587620236790434,
-4.85416666666666));
#410179=CARTESIAN_POINT('Ctrl Pts',(1.35705080756892,2.29132664526027E-15,
-4.81249999999999));
#410180=CARTESIAN_POINT('Ctrl Pts',(1.01778810567669,0.587620236790438,
-4.77083333333332));
#410181=CARTESIAN_POINT('Ctrl Pts',(0.67852540378446,1.17524047358087,-4.72916666666666));
#410182=CARTESIAN_POINT('Ctrl Pts',(0.,1.17524047358087,-4.68749999999999));
#410183=CARTESIAN_POINT('Ctrl Pts',(-0.678525403784459,1.17524047358087,
-4.64583333333332));
#410184=CARTESIAN_POINT('Ctrl Pts',(-1.01778810567669,0.587620236790438,
-4.60416666666666));
#410185=CARTESIAN_POINT('Ctrl Pts',(-1.35705080756892,2.62370823081419E-15,
-4.56249999999999));
#410186=CARTESIAN_POINT('Ctrl Pts',(-1.01778810567669,-0.587620236790433,
-4.52083333333332));
#410187=CARTESIAN_POINT('Ctrl Pts',(-0.67852540378446,-1.17524047358087,
-4.47916666666666));
#410188=CARTESIAN_POINT('Ctrl Pts',(-1.43925448419923E-16,-1.17524047358087,
-4.43749999999999));
#410189=CARTESIAN_POINT('Ctrl Pts',(-1.43925448419923E-16,-1.17524047358087,
-4.99999999999999));
#410190=CARTESIAN_POINT('Ctrl Pts',(0.678525403784459,-1.17524047358087,
-4.95833333333332));
#410191=CARTESIAN_POINT('Ctrl Pts',(1.01778810567669,-0.587620236790434,
-4.91666666666666));
#410192=CARTESIAN_POINT('Ctrl Pts',(1.35705080756892,2.29132664526027E-15,
-4.87499999999999));
#410193=CARTESIAN_POINT('Ctrl Pts',(1.01778810567669,0.587620236790438,
-4.83333333333332));
#410194=CARTESIAN_POINT('Ctrl Pts',(0.67852540378446,1.17524047358087,-4.79166666666666));
#410195=CARTESIAN_POINT('Ctrl Pts',(0.,1.17524047358087,-4.74999999999999));
#410196=CARTESIAN_POINT('Ctrl Pts',(-0.678525403784459,1.17524047358087,
-4.70833333333332));
#410197=CARTESIAN_POINT('Ctrl Pts',(-1.01778810567669,0.587620236790438,
-4.66666666666666));
#410198=CARTESIAN_POINT('Ctrl Pts',(-1.35705080756892,2.62370823081419E-15,
-4.62499999999999));
#410199=CARTESIAN_POINT('Ctrl Pts',(-1.01778810567669,-0.587620236790433,
-4.58333333333332));
#410200=CARTESIAN_POINT('Ctrl Pts',(-0.67852540378446,-1.17524047358087,
-4.54166666666666));
#410201=CARTESIAN_POINT('Ctrl Pts',(-1.43925448419923E-16,-1.17524047358087,
-4.49999999999999));
#410202=CARTESIAN_POINT('Origin',(0.,-1.11022302462516E-14,-14.21875));
#410203=CARTESIAN_POINT('',(-8.32001735975286E-31,-1.17524047358087,-3.93749999999999));
#410204=CARTESIAN_POINT('',(-8.32001735975286E-31,-1.17524047358087,-3.99999999999999));
#410205=CARTESIAN_POINT('',(1.43925448419925E-16,-1.1752404735809,-14.21875));
#410206=CARTESIAN_POINT('Ctrl Pts',(-1.43925448419923E-16,-1.17524047358087,
-4.43749999999999));
#410207=CARTESIAN_POINT('Ctrl Pts',(0.678525403784459,-1.17524047358087,
-4.39583333333332));
#410208=CARTESIAN_POINT('Ctrl Pts',(1.01778810567669,-0.587620236790434,
-4.35416666666666));
#410209=CARTESIAN_POINT('Ctrl Pts',(1.35705080756892,2.29132664526027E-15,
-4.31249999999999));
#410210=CARTESIAN_POINT('Ctrl Pts',(1.01778810567669,0.587620236790438,
-4.27083333333332));
#410211=CARTESIAN_POINT('Ctrl Pts',(0.67852540378446,1.17524047358087,-4.22916666666666));
#410212=CARTESIAN_POINT('Ctrl Pts',(0.,1.17524047358087,-4.18749999999999));
#410213=CARTESIAN_POINT('Ctrl Pts',(-0.678525403784459,1.17524047358087,
-4.14583333333332));
#410214=CARTESIAN_POINT('Ctrl Pts',(-1.01778810567669,0.587620236790438,
-4.10416666666666));
#410215=CARTESIAN_POINT('Ctrl Pts',(-1.35705080756892,2.62370823081419E-15,
-4.06249999999999));
#410216=CARTESIAN_POINT('Ctrl Pts',(-1.01778810567669,-0.587620236790433,
-4.02083333333333));
#410217=CARTESIAN_POINT('Ctrl Pts',(-0.67852540378446,-1.17524047358087,
-3.97916666666666));
#410218=CARTESIAN_POINT('Ctrl Pts',(-1.43925448419923E-16,-1.17524047358087,
-3.93749999999999));
#410219=CARTESIAN_POINT('Ctrl Pts',(-1.43925448419923E-16,-1.17524047358087,
-4.49999999999999));
#410220=CARTESIAN_POINT('Ctrl Pts',(0.678525403784459,-1.17524047358087,
-4.45833333333332));
#410221=CARTESIAN_POINT('Ctrl Pts',(1.01778810567669,-0.587620236790434,
-4.41666666666666));
#410222=CARTESIAN_POINT('Ctrl Pts',(1.35705080756892,2.29132664526027E-15,
-4.37499999999999));
#410223=CARTESIAN_POINT('Ctrl Pts',(1.01778810567669,0.587620236790438,
-4.33333333333333));
#410224=CARTESIAN_POINT('Ctrl Pts',(0.67852540378446,1.17524047358087,-4.29166666666666));
#410225=CARTESIAN_POINT('Ctrl Pts',(0.,1.17524047358087,-4.24999999999999));
#410226=CARTESIAN_POINT('Ctrl Pts',(-0.678525403784459,1.17524047358087,
-4.20833333333332));
#410227=CARTESIAN_POINT('Ctrl Pts',(-1.01778810567669,0.587620236790438,
-4.16666666666666));
#410228=CARTESIAN_POINT('Ctrl Pts',(-1.35705080756892,2.62370823081419E-15,
-4.12499999999999));
#410229=CARTESIAN_POINT('Ctrl Pts',(-1.01778810567669,-0.587620236790433,
-4.08333333333332));
#410230=CARTESIAN_POINT('Ctrl Pts',(-0.67852540378446,-1.17524047358087,
-4.04166666666666));
#410231=CARTESIAN_POINT('Ctrl Pts',(-1.43925448419923E-16,-1.17524047358087,
-3.99999999999999));
#410232=CARTESIAN_POINT('Origin',(0.,-1.11022302462516E-14,-14.21875));
#410233=CARTESIAN_POINT('',(-8.32001735975286E-31,-1.17524047358087,-3.43749999999999));
#410234=CARTESIAN_POINT('',(-8.32001735975286E-31,-1.17524047358087,-3.49999999999999));
#410235=CARTESIAN_POINT('',(1.43925448419925E-16,-1.1752404735809,-14.21875));
#410236=CARTESIAN_POINT('Ctrl Pts',(-1.43925448419923E-16,-1.17524047358087,
-3.93749999999999));
#410237=CARTESIAN_POINT('Ctrl Pts',(0.678525403784459,-1.17524047358087,
-3.89583333333332));
#410238=CARTESIAN_POINT('Ctrl Pts',(1.01778810567669,-0.587620236790434,
-3.85416666666666));
#410239=CARTESIAN_POINT('Ctrl Pts',(1.35705080756892,2.29132664526027E-15,
-3.81249999999999));
#410240=CARTESIAN_POINT('Ctrl Pts',(1.01778810567669,0.587620236790438,
-3.77083333333332));
#410241=CARTESIAN_POINT('Ctrl Pts',(0.67852540378446,1.17524047358087,-3.72916666666666));
#410242=CARTESIAN_POINT('Ctrl Pts',(0.,1.17524047358087,-3.68749999999999));
#410243=CARTESIAN_POINT('Ctrl Pts',(-0.678525403784459,1.17524047358087,
-3.64583333333332));
#410244=CARTESIAN_POINT('Ctrl Pts',(-1.01778810567669,0.587620236790438,
-3.60416666666666));
#410245=CARTESIAN_POINT('Ctrl Pts',(-1.35705080756892,2.62370823081419E-15,
-3.56249999999999));
#410246=CARTESIAN_POINT('Ctrl Pts',(-1.01778810567669,-0.587620236790433,
-3.52083333333332));
#410247=CARTESIAN_POINT('Ctrl Pts',(-0.67852540378446,-1.17524047358087,
-3.47916666666666));
#410248=CARTESIAN_POINT('Ctrl Pts',(-1.43925448419923E-16,-1.17524047358087,
-3.43749999999999));
#410249=CARTESIAN_POINT('Ctrl Pts',(-1.43925448419923E-16,-1.17524047358087,
-3.99999999999999));
#410250=CARTESIAN_POINT('Ctrl Pts',(0.678525403784459,-1.17524047358087,
-3.95833333333332));
#410251=CARTESIAN_POINT('Ctrl Pts',(1.01778810567669,-0.587620236790434,
-3.91666666666666));
#410252=CARTESIAN_POINT('Ctrl Pts',(1.35705080756892,2.29132664526027E-15,
-3.87499999999999));
#410253=CARTESIAN_POINT('Ctrl Pts',(1.01778810567669,0.587620236790438,
-3.83333333333332));
#410254=CARTESIAN_POINT('Ctrl Pts',(0.67852540378446,1.17524047358087,-3.79166666666666));
#410255=CARTESIAN_POINT('Ctrl Pts',(0.,1.17524047358087,-3.74999999999999));
#410256=CARTESIAN_POINT('Ctrl Pts',(-0.678525403784459,1.17524047358087,
-3.70833333333332));
#410257=CARTESIAN_POINT('Ctrl Pts',(-1.01778810567669,0.587620236790438,
-3.66666666666666));
#410258=CARTESIAN_POINT('Ctrl Pts',(-1.35705080756892,2.62370823081419E-15,
-3.62499999999999));
#410259=CARTESIAN_POINT('Ctrl Pts',(-1.01778810567669,-0.587620236790433,
-3.58333333333332));
#410260=CARTESIAN_POINT('Ctrl Pts',(-0.67852540378446,-1.17524047358087,
-3.54166666666666));
#410261=CARTESIAN_POINT('Ctrl Pts',(-1.43925448419923E-16,-1.17524047358087,
-3.49999999999999));
#410262=CARTESIAN_POINT('Origin',(0.,-1.11022302462516E-14,-14.21875));
#410263=CARTESIAN_POINT('',(-8.32001735975286E-31,-1.17524047358087,-2.93749999999999));
#410264=CARTESIAN_POINT('',(-8.32001735975286E-31,-1.17524047358087,-2.99999999999999));
#410265=CARTESIAN_POINT('',(1.43925448419925E-16,-1.1752404735809,-14.21875));
#410266=CARTESIAN_POINT('Ctrl Pts',(-1.43925448419923E-16,-1.17524047358087,
-3.43749999999999));
#410267=CARTESIAN_POINT('Ctrl Pts',(0.678525403784459,-1.17524047358087,
-3.39583333333332));
#410268=CARTESIAN_POINT('Ctrl Pts',(1.01778810567669,-0.587620236790434,
-3.35416666666666));
#410269=CARTESIAN_POINT('Ctrl Pts',(1.35705080756892,2.29132664526027E-15,
-3.31249999999999));
#410270=CARTESIAN_POINT('Ctrl Pts',(1.01778810567669,0.587620236790438,
-3.27083333333332));
#410271=CARTESIAN_POINT('Ctrl Pts',(0.67852540378446,1.17524047358087,-3.22916666666666));
#410272=CARTESIAN_POINT('Ctrl Pts',(0.,1.17524047358087,-3.18749999999999));
#410273=CARTESIAN_POINT('Ctrl Pts',(-0.678525403784459,1.17524047358087,
-3.14583333333332));
#410274=CARTESIAN_POINT('Ctrl Pts',(-1.01778810567669,0.587620236790438,
-3.10416666666666));
#410275=CARTESIAN_POINT('Ctrl Pts',(-1.35705080756892,2.62370823081419E-15,
-3.06249999999999));
#410276=CARTESIAN_POINT('Ctrl Pts',(-1.01778810567669,-0.587620236790433,
-3.02083333333332));
#410277=CARTESIAN_POINT('Ctrl Pts',(-0.67852540378446,-1.17524047358087,
-2.97916666666666));
#410278=CARTESIAN_POINT('Ctrl Pts',(-1.43925448419923E-16,-1.17524047358087,
-2.93749999999999));
#410279=CARTESIAN_POINT('Ctrl Pts',(-1.43925448419923E-16,-1.17524047358087,
-3.49999999999999));
#410280=CARTESIAN_POINT('Ctrl Pts',(0.678525403784459,-1.17524047358087,
-3.45833333333333));
#410281=CARTESIAN_POINT('Ctrl Pts',(1.01778810567669,-0.587620236790434,
-3.41666666666666));
#410282=CARTESIAN_POINT('Ctrl Pts',(1.35705080756892,2.29132664526027E-15,
-3.37499999999999));
#410283=CARTESIAN_POINT('Ctrl Pts',(1.01778810567669,0.587620236790438,
-3.33333333333332));
#410284=CARTESIAN_POINT('Ctrl Pts',(0.67852540378446,1.17524047358087,-3.29166666666666));
#410285=CARTESIAN_POINT('Ctrl Pts',(0.,1.17524047358087,-3.24999999999999));
#410286=CARTESIAN_POINT('Ctrl Pts',(-0.678525403784459,1.17524047358087,
-3.20833333333332));
#410287=CARTESIAN_POINT('Ctrl Pts',(-1.01778810567669,0.587620236790438,
-3.16666666666666));
#410288=CARTESIAN_POINT('Ctrl Pts',(-1.35705080756892,2.62370823081419E-15,
-3.12499999999999));
#410289=CARTESIAN_POINT('Ctrl Pts',(-1.01778810567669,-0.587620236790433,
-3.08333333333332));
#410290=CARTESIAN_POINT('Ctrl Pts',(-0.67852540378446,-1.17524047358087,
-3.04166666666666));
#410291=CARTESIAN_POINT('Ctrl Pts',(-1.43925448419923E-16,-1.17524047358087,
-2.99999999999999));
#410292=CARTESIAN_POINT('Origin',(0.,-1.11022302462516E-14,-14.21875));
#410293=CARTESIAN_POINT('',(-8.32001735975286E-31,-1.17524047358087,-2.43749999999999));
#410294=CARTESIAN_POINT('',(-8.32001735975286E-31,-1.17524047358087,-2.49999999999999));
#410295=CARTESIAN_POINT('',(1.43925448419925E-16,-1.1752404735809,-14.21875));
#410296=CARTESIAN_POINT('Ctrl Pts',(-1.43925448419923E-16,-1.17524047358087,
-2.93749999999999));
#410297=CARTESIAN_POINT('Ctrl Pts',(0.678525403784459,-1.17524047358087,
-2.89583333333332));
#410298=CARTESIAN_POINT('Ctrl Pts',(1.01778810567669,-0.587620236790434,
-2.85416666666666));
#410299=CARTESIAN_POINT('Ctrl Pts',(1.35705080756892,2.29132664526027E-15,
-2.81249999999999));
#410300=CARTESIAN_POINT('Ctrl Pts',(1.01778810567669,0.587620236790438,
-2.77083333333332));
#410301=CARTESIAN_POINT('Ctrl Pts',(0.67852540378446,1.17524047358087,-2.72916666666666));
#410302=CARTESIAN_POINT('Ctrl Pts',(0.,1.17524047358087,-2.68749999999999));
#410303=CARTESIAN_POINT('Ctrl Pts',(-0.678525403784459,1.17524047358087,
-2.64583333333332));
#410304=CARTESIAN_POINT('Ctrl Pts',(-1.01778810567669,0.587620236790438,
-2.60416666666666));
#410305=CARTESIAN_POINT('Ctrl Pts',(-1.35705080756892,2.62370823081419E-15,
-2.56249999999999));
#410306=CARTESIAN_POINT('Ctrl Pts',(-1.01778810567669,-0.587620236790433,
-2.52083333333333));
#410307=CARTESIAN_POINT('Ctrl Pts',(-0.67852540378446,-1.17524047358087,
-2.47916666666666));
#410308=CARTESIAN_POINT('Ctrl Pts',(-1.43925448419923E-16,-1.17524047358087,
-2.43749999999999));
#410309=CARTESIAN_POINT('Ctrl Pts',(-1.43925448419923E-16,-1.17524047358087,
-2.99999999999999));
#410310=CARTESIAN_POINT('Ctrl Pts',(0.678525403784459,-1.17524047358087,
-2.95833333333332));
#410311=CARTESIAN_POINT('Ctrl Pts',(1.01778810567669,-0.587620236790434,
-2.91666666666666));
#410312=CARTESIAN_POINT('Ctrl Pts',(1.35705080756892,2.29132664526027E-15,
-2.87499999999999));
#410313=CARTESIAN_POINT('Ctrl Pts',(1.01778810567669,0.587620236790438,
-2.83333333333332));
#410314=CARTESIAN_POINT('Ctrl Pts',(0.67852540378446,1.17524047358087,-2.79166666666666));
#410315=CARTESIAN_POINT('Ctrl Pts',(0.,1.17524047358087,-2.74999999999999));
#410316=CARTESIAN_POINT('Ctrl Pts',(-0.678525403784459,1.17524047358087,
-2.70833333333332));
#410317=CARTESIAN_POINT('Ctrl Pts',(-1.01778810567669,0.587620236790438,
-2.66666666666666));
#410318=CARTESIAN_POINT('Ctrl Pts',(-1.35705080756892,2.62370823081419E-15,
-2.62499999999999));
#410319=CARTESIAN_POINT('Ctrl Pts',(-1.01778810567669,-0.587620236790433,
-2.58333333333332));
#410320=CARTESIAN_POINT('Ctrl Pts',(-0.67852540378446,-1.17524047358087,
-2.54166666666666));
#410321=CARTESIAN_POINT('Ctrl Pts',(-1.43925448419923E-16,-1.17524047358087,
-2.49999999999999));
#410322=CARTESIAN_POINT('Origin',(0.,-1.11022302462516E-14,-14.21875));
#410323=CARTESIAN_POINT('',(-8.32001735975286E-31,-1.17524047358087,-1.93749999999999));
#410324=CARTESIAN_POINT('',(-8.32001735975286E-31,-1.17524047358087,-1.99999999999999));
#410325=CARTESIAN_POINT('',(1.43925448419925E-16,-1.1752404735809,-14.21875));
#410326=CARTESIAN_POINT('Ctrl Pts',(-1.43925448419923E-16,-1.17524047358087,
-2.43749999999999));
#410327=CARTESIAN_POINT('Ctrl Pts',(0.678525403784459,-1.17524047358087,
-2.39583333333333));
#410328=CARTESIAN_POINT('Ctrl Pts',(1.01778810567669,-0.587620236790434,
-2.35416666666666));
#410329=CARTESIAN_POINT('Ctrl Pts',(1.35705080756892,2.29132664526027E-15,
-2.31249999999999));
#410330=CARTESIAN_POINT('Ctrl Pts',(1.01778810567669,0.587620236790438,
-2.27083333333332));
#410331=CARTESIAN_POINT('Ctrl Pts',(0.67852540378446,1.17524047358087,-2.22916666666666));
#410332=CARTESIAN_POINT('Ctrl Pts',(0.,1.17524047358087,-2.18749999999999));
#410333=CARTESIAN_POINT('Ctrl Pts',(-0.678525403784459,1.17524047358087,
-2.14583333333332));
#410334=CARTESIAN_POINT('Ctrl Pts',(-1.01778810567669,0.587620236790438,
-2.10416666666666));
#410335=CARTESIAN_POINT('Ctrl Pts',(-1.35705080756892,2.62370823081419E-15,
-2.06249999999999));
#410336=CARTESIAN_POINT('Ctrl Pts',(-1.01778810567669,-0.587620236790433,
-2.02083333333332));
#410337=CARTESIAN_POINT('Ctrl Pts',(-0.67852540378446,-1.17524047358087,
-1.97916666666666));
#410338=CARTESIAN_POINT('Ctrl Pts',(-1.43925448419923E-16,-1.17524047358087,
-1.93749999999999));
#410339=CARTESIAN_POINT('Ctrl Pts',(-1.43925448419923E-16,-1.17524047358087,
-2.49999999999999));
#410340=CARTESIAN_POINT('Ctrl Pts',(0.678525403784459,-1.17524047358087,
-2.45833333333332));
#410341=CARTESIAN_POINT('Ctrl Pts',(1.01778810567669,-0.587620236790434,
-2.41666666666666));
#410342=CARTESIAN_POINT('Ctrl Pts',(1.35705080756892,2.29132664526027E-15,
-2.37499999999999));
#410343=CARTESIAN_POINT('Ctrl Pts',(1.01778810567669,0.587620236790438,
-2.33333333333332));
#410344=CARTESIAN_POINT('Ctrl Pts',(0.67852540378446,1.17524047358087,-2.29166666666666));
#410345=CARTESIAN_POINT('Ctrl Pts',(0.,1.17524047358087,-2.24999999999999));
#410346=CARTESIAN_POINT('Ctrl Pts',(-0.678525403784459,1.17524047358087,
-2.20833333333332));
#410347=CARTESIAN_POINT('Ctrl Pts',(-1.01778810567669,0.587620236790438,
-2.16666666666666));
#410348=CARTESIAN_POINT('Ctrl Pts',(-1.35705080756892,2.62370823081419E-15,
-2.12499999999999));
#410349=CARTESIAN_POINT('Ctrl Pts',(-1.01778810567669,-0.587620236790433,
-2.08333333333332));
#410350=CARTESIAN_POINT('Ctrl Pts',(-0.67852540378446,-1.17524047358087,
-2.04166666666666));
#410351=CARTESIAN_POINT('Ctrl Pts',(-1.43925448419923E-16,-1.17524047358087,
-1.99999999999999));
#410352=CARTESIAN_POINT('Origin',(0.,-1.11022302462516E-14,-14.21875));
#410353=CARTESIAN_POINT('',(-8.32001735975286E-31,-1.17524047358087,-1.43749999999999));
#410354=CARTESIAN_POINT('',(-8.32001735975286E-31,-1.17524047358087,-1.49999999999999));
#410355=CARTESIAN_POINT('',(1.43925448419925E-16,-1.1752404735809,-14.21875));
#410356=CARTESIAN_POINT('Ctrl Pts',(-1.43925448419923E-16,-1.17524047358087,
-1.93749999999999));
#410357=CARTESIAN_POINT('Ctrl Pts',(0.678525403784459,-1.17524047358087,
-1.89583333333332));
#410358=CARTESIAN_POINT('Ctrl Pts',(1.01778810567669,-0.587620236790434,
-1.85416666666666));
#410359=CARTESIAN_POINT('Ctrl Pts',(1.35705080756892,2.29132664526027E-15,
-1.81249999999999));
#410360=CARTESIAN_POINT('Ctrl Pts',(1.01778810567669,0.587620236790438,
-1.77083333333332));
#410361=CARTESIAN_POINT('Ctrl Pts',(0.67852540378446,1.17524047358087,-1.72916666666666));
#410362=CARTESIAN_POINT('Ctrl Pts',(0.,1.17524047358087,-1.68749999999999));
#410363=CARTESIAN_POINT('Ctrl Pts',(-0.678525403784459,1.17524047358087,
-1.64583333333332));
#410364=CARTESIAN_POINT('Ctrl Pts',(-1.01778810567669,0.587620236790438,
-1.60416666666666));
#410365=CARTESIAN_POINT('Ctrl Pts',(-1.35705080756892,2.62370823081419E-15,
-1.56249999999999));
#410366=CARTESIAN_POINT('Ctrl Pts',(-1.01778810567669,-0.587620236790433,
-1.52083333333332));
#410367=CARTESIAN_POINT('Ctrl Pts',(-0.67852540378446,-1.17524047358087,
-1.47916666666666));
#410368=CARTESIAN_POINT('Ctrl Pts',(-1.43925448419923E-16,-1.17524047358087,
-1.43749999999999));
#410369=CARTESIAN_POINT('Ctrl Pts',(-1.43925448419923E-16,-1.17524047358087,
-1.99999999999999));
#410370=CARTESIAN_POINT('Ctrl Pts',(0.678525403784459,-1.17524047358087,
-1.95833333333332));
#410371=CARTESIAN_POINT('Ctrl Pts',(1.01778810567669,-0.587620236790434,
-1.91666666666666));
#410372=CARTESIAN_POINT('Ctrl Pts',(1.35705080756892,2.29132664526027E-15,
-1.87499999999999));
#410373=CARTESIAN_POINT('Ctrl Pts',(1.01778810567669,0.587620236790438,
-1.83333333333332));
#410374=CARTESIAN_POINT('Ctrl Pts',(0.67852540378446,1.17524047358087,-1.79166666666666));
#410375=CARTESIAN_POINT('Ctrl Pts',(0.,1.17524047358087,-1.74999999999999));
#410376=CARTESIAN_POINT('Ctrl Pts',(-0.678525403784459,1.17524047358087,
-1.70833333333332));
#410377=CARTESIAN_POINT('Ctrl Pts',(-1.01778810567669,0.587620236790438,
-1.66666666666666));
#410378=CARTESIAN_POINT('Ctrl Pts',(-1.35705080756892,2.62370823081419E-15,
-1.62499999999999));
#410379=CARTESIAN_POINT('Ctrl Pts',(-1.01778810567669,-0.587620236790433,
-1.58333333333332));
#410380=CARTESIAN_POINT('Ctrl Pts',(-0.67852540378446,-1.17524047358087,
-1.54166666666666));
#410381=CARTESIAN_POINT('Ctrl Pts',(-1.43925448419923E-16,-1.17524047358087,
-1.49999999999999));
#410382=CARTESIAN_POINT('Origin',(0.,-1.11022302462516E-14,-14.21875));
#410383=CARTESIAN_POINT('',(-8.32001735975286E-31,-1.17524047358087,-0.937499999999991));
#410384=CARTESIAN_POINT('',(-8.32001735975286E-31,-1.17524047358087,-0.99999999999999));
#410385=CARTESIAN_POINT('',(1.43925448419925E-16,-1.1752404735809,-14.21875));
#410386=CARTESIAN_POINT('Ctrl Pts',(-1.43925448419923E-16,-1.17524047358087,
-1.43749999999999));
#410387=CARTESIAN_POINT('Ctrl Pts',(0.678525403784459,-1.17524047358087,
-1.39583333333332));
#410388=CARTESIAN_POINT('Ctrl Pts',(1.01778810567669,-0.587620236790434,
-1.35416666666666));
#410389=CARTESIAN_POINT('Ctrl Pts',(1.35705080756892,2.29132664526027E-15,
-1.31249999999999));
#410390=CARTESIAN_POINT('Ctrl Pts',(1.01778810567669,0.587620236790438,
-1.27083333333332));
#410391=CARTESIAN_POINT('Ctrl Pts',(0.67852540378446,1.17524047358087,-1.22916666666666));
#410392=CARTESIAN_POINT('Ctrl Pts',(0.,1.17524047358087,-1.18749999999999));
#410393=CARTESIAN_POINT('Ctrl Pts',(-0.678525403784459,1.17524047358087,
-1.14583333333332));
#410394=CARTESIAN_POINT('Ctrl Pts',(-1.01778810567669,0.587620236790438,
-1.10416666666666));
#410395=CARTESIAN_POINT('Ctrl Pts',(-1.35705080756892,2.62370823081419E-15,
-1.06249999999999));
#410396=CARTESIAN_POINT('Ctrl Pts',(-1.01778810567669,-0.587620236790433,
-1.02083333333332));
#410397=CARTESIAN_POINT('Ctrl Pts',(-0.67852540378446,-1.17524047358087,
-0.979166666666658));
#410398=CARTESIAN_POINT('Ctrl Pts',(-1.43925448419923E-16,-1.17524047358087,
-0.937499999999991));
#410399=CARTESIAN_POINT('Ctrl Pts',(-1.43925448419923E-16,-1.17524047358087,
-1.49999999999999));
#410400=CARTESIAN_POINT('Ctrl Pts',(0.678525403784459,-1.17524047358087,
-1.45833333333332));
#410401=CARTESIAN_POINT('Ctrl Pts',(1.01778810567669,-0.587620236790434,
-1.41666666666666));
#410402=CARTESIAN_POINT('Ctrl Pts',(1.35705080756892,2.29132664526027E-15,
-1.37499999999999));
#410403=CARTESIAN_POINT('Ctrl Pts',(1.01778810567669,0.587620236790438,
-1.33333333333332));
#410404=CARTESIAN_POINT('Ctrl Pts',(0.67852540378446,1.17524047358087,-1.29166666666666));
#410405=CARTESIAN_POINT('Ctrl Pts',(0.,1.17524047358087,-1.24999999999999));
#410406=CARTESIAN_POINT('Ctrl Pts',(-0.678525403784459,1.17524047358087,
-1.20833333333332));
#410407=CARTESIAN_POINT('Ctrl Pts',(-1.01778810567669,0.587620236790438,
-1.16666666666666));
#410408=CARTESIAN_POINT('Ctrl Pts',(-1.35705080756892,2.62370823081419E-15,
-1.12499999999999));
#410409=CARTESIAN_POINT('Ctrl Pts',(-1.01778810567669,-0.587620236790433,
-1.08333333333332));
#410410=CARTESIAN_POINT('Ctrl Pts',(-0.67852540378446,-1.17524047358087,
-1.04166666666666));
#410411=CARTESIAN_POINT('Ctrl Pts',(-1.43925448419923E-16,-1.17524047358087,
-0.99999999999999));
#410412=CARTESIAN_POINT('Origin',(0.,-1.11022302462516E-14,-14.21875));
#410413=CARTESIAN_POINT('',(-8.32001735975286E-31,-1.17524047358087,-0.43749999999999));
#410414=CARTESIAN_POINT('',(-8.32001735975286E-31,-1.17524047358087,-0.49999999999999));
#410415=CARTESIAN_POINT('',(1.43925448419925E-16,-1.1752404735809,-14.21875));
#410416=CARTESIAN_POINT('Ctrl Pts',(-1.43925448419923E-16,-1.17524047358087,
-0.937499999999991));
#410417=CARTESIAN_POINT('Ctrl Pts',(0.678525403784459,-1.17524047358087,
-0.895833333333323));
#410418=CARTESIAN_POINT('Ctrl Pts',(1.01778810567669,-0.587620236790434,
-0.854166666666658));
#410419=CARTESIAN_POINT('Ctrl Pts',(1.35705080756892,2.29132664526027E-15,
-0.81249999999999));
#410420=CARTESIAN_POINT('Ctrl Pts',(1.01778810567669,0.587620236790438,
-0.770833333333323));
#410421=CARTESIAN_POINT('Ctrl Pts',(0.67852540378446,1.17524047358087,-0.729166666666658));
#410422=CARTESIAN_POINT('Ctrl Pts',(0.,1.17524047358087,-0.68749999999999));
#410423=CARTESIAN_POINT('Ctrl Pts',(-0.678525403784459,1.17524047358087,
-0.645833333333325));
#410424=CARTESIAN_POINT('Ctrl Pts',(-1.01778810567669,0.587620236790438,
-0.604166666666657));
#410425=CARTESIAN_POINT('Ctrl Pts',(-1.35705080756892,2.62370823081419E-15,
-0.56249999999999));
#410426=CARTESIAN_POINT('Ctrl Pts',(-1.01778810567669,-0.587620236790433,
-0.520833333333325));
#410427=CARTESIAN_POINT('Ctrl Pts',(-0.67852540378446,-1.17524047358087,
-0.479166666666657));
#410428=CARTESIAN_POINT('Ctrl Pts',(-1.43925448419923E-16,-1.17524047358087,
-0.43749999999999));
#410429=CARTESIAN_POINT('Ctrl Pts',(-1.43925448419923E-16,-1.17524047358087,
-0.99999999999999));
#410430=CARTESIAN_POINT('Ctrl Pts',(0.678525403784459,-1.17524047358087,
-0.958333333333323));
#410431=CARTESIAN_POINT('Ctrl Pts',(1.01778810567669,-0.587620236790434,
-0.916666666666658));
#410432=CARTESIAN_POINT('Ctrl Pts',(1.35705080756892,2.29132664526027E-15,
-0.87499999999999));
#410433=CARTESIAN_POINT('Ctrl Pts',(1.01778810567669,0.587620236790438,
-0.833333333333323));
#410434=CARTESIAN_POINT('Ctrl Pts',(0.67852540378446,1.17524047358087,-0.791666666666657));
#410435=CARTESIAN_POINT('Ctrl Pts',(0.,1.17524047358087,-0.74999999999999));
#410436=CARTESIAN_POINT('Ctrl Pts',(-0.678525403784459,1.17524047358087,
-0.708333333333325));
#410437=CARTESIAN_POINT('Ctrl Pts',(-1.01778810567669,0.587620236790438,
-0.666666666666658));
#410438=CARTESIAN_POINT('Ctrl Pts',(-1.35705080756892,2.62370823081419E-15,
-0.62499999999999));
#410439=CARTESIAN_POINT('Ctrl Pts',(-1.01778810567669,-0.587620236790433,
-0.583333333333325));
#410440=CARTESIAN_POINT('Ctrl Pts',(-0.67852540378446,-1.17524047358087,
-0.541666666666657));
#410441=CARTESIAN_POINT('Ctrl Pts',(-1.43925448419923E-16,-1.17524047358087,
-0.49999999999999));
#410442=CARTESIAN_POINT('Origin',(0.,-1.11022302462516E-14,-14.21875));
#410443=CARTESIAN_POINT('',(-8.32001735975286E-31,-1.17524047358087,0.0625000000000087));
#410444=CARTESIAN_POINT('',(-8.32001735975286E-31,-1.17524047358087,8.67361737988404E-15));
#410445=CARTESIAN_POINT('',(1.43925448419925E-16,-1.1752404735809,-14.21875));
#410446=CARTESIAN_POINT('Ctrl Pts',(-1.43925448419923E-16,-1.17524047358087,
-0.43749999999999));
#410447=CARTESIAN_POINT('Ctrl Pts',(0.678525403784459,-1.17524047358087,
-0.395833333333324));
#410448=CARTESIAN_POINT('Ctrl Pts',(1.01778810567669,-0.587620236790434,
-0.354166666666657));
#410449=CARTESIAN_POINT('Ctrl Pts',(1.35705080756892,2.29132664526027E-15,
-0.31249999999999));
#410450=CARTESIAN_POINT('Ctrl Pts',(1.01778810567669,0.587620236790438,
-0.270833333333324));
#410451=CARTESIAN_POINT('Ctrl Pts',(0.67852540378446,1.17524047358087,-0.229166666666657));
#410452=CARTESIAN_POINT('Ctrl Pts',(0.,1.17524047358087,-0.18749999999999));
#410453=CARTESIAN_POINT('Ctrl Pts',(-0.678525403784459,1.17524047358087,
-0.145833333333324));
#410454=CARTESIAN_POINT('Ctrl Pts',(-1.01778810567669,0.587620236790438,
-0.104166666666657));
#410455=CARTESIAN_POINT('Ctrl Pts',(-1.35705080756892,2.62370823081419E-15,
-0.0624999999999914));
#410456=CARTESIAN_POINT('Ctrl Pts',(-1.01778810567669,-0.587620236790433,
-0.0208333333333241));
#410457=CARTESIAN_POINT('Ctrl Pts',(-0.67852540378446,-1.17524047358087,
0.0208333333333432));
#410458=CARTESIAN_POINT('Ctrl Pts',(-1.43925448419923E-16,-1.17524047358087,
0.0625000000000087));
#410459=CARTESIAN_POINT('Ctrl Pts',(-1.43925448419923E-16,-1.17524047358087,
-0.49999999999999));
#410460=CARTESIAN_POINT('Ctrl Pts',(0.678525403784459,-1.17524047358087,
-0.458333333333324));
#410461=CARTESIAN_POINT('Ctrl Pts',(1.01778810567669,-0.587620236790434,
-0.416666666666657));
#410462=CARTESIAN_POINT('Ctrl Pts',(1.35705080756892,2.29132664526027E-15,
-0.37499999999999));
#410463=CARTESIAN_POINT('Ctrl Pts',(1.01778810567669,0.587620236790438,
-0.333333333333324));
#410464=CARTESIAN_POINT('Ctrl Pts',(0.67852540378446,1.17524047358087,-0.291666666666657));
#410465=CARTESIAN_POINT('Ctrl Pts',(0.,1.17524047358087,-0.24999999999999));
#410466=CARTESIAN_POINT('Ctrl Pts',(-0.678525403784459,1.17524047358087,
-0.208333333333324));
#410467=CARTESIAN_POINT('Ctrl Pts',(-1.01778810567669,0.587620236790438,
-0.166666666666657));
#410468=CARTESIAN_POINT('Ctrl Pts',(-1.35705080756892,2.62370823081419E-15,
-0.124999999999991));
#410469=CARTESIAN_POINT('Ctrl Pts',(-1.01778810567669,-0.587620236790433,
-0.0833333333333242));
#410470=CARTESIAN_POINT('Ctrl Pts',(-0.67852540378446,-1.17524047358087,
-0.0416666666666569));
#410471=CARTESIAN_POINT('Ctrl Pts',(-1.43925448419923E-16,-1.17524047358087,
8.67361737988404E-15));
#410472=CARTESIAN_POINT('Origin',(0.,-1.11022302462516E-14,-14.21875));
#410473=CARTESIAN_POINT('',(-8.32001735975286E-31,-1.17524047358087,0.562500000000009));
#410474=CARTESIAN_POINT('',(-8.32001735975286E-31,-1.17524047358087,0.500000000000009));
#410475=CARTESIAN_POINT('',(1.43925448419925E-16,-1.1752404735809,-14.21875));
#410476=CARTESIAN_POINT('Ctrl Pts',(-1.43925448419923E-16,-1.17524047358087,
0.0625000000000087));
#410477=CARTESIAN_POINT('Ctrl Pts',(0.678525403784459,-1.17524047358087,
0.104166666666676));
#410478=CARTESIAN_POINT('Ctrl Pts',(1.01778810567669,-0.587620236790434,
0.145833333333343));
#410479=CARTESIAN_POINT('Ctrl Pts',(1.35705080756892,2.29132664526027E-15,
0.187500000000009));
#410480=CARTESIAN_POINT('Ctrl Pts',(1.01778810567669,0.587620236790438,
0.229166666666676));
#410481=CARTESIAN_POINT('Ctrl Pts',(0.67852540378446,1.17524047358087,0.270833333333343));
#410482=CARTESIAN_POINT('Ctrl Pts',(0.,1.17524047358087,0.312500000000009));
#410483=CARTESIAN_POINT('Ctrl Pts',(-0.678525403784459,1.17524047358087,
0.354166666666676));
#410484=CARTESIAN_POINT('Ctrl Pts',(-1.01778810567669,0.587620236790438,
0.395833333333344));
#410485=CARTESIAN_POINT('Ctrl Pts',(-1.35705080756892,2.62370823081419E-15,
0.437500000000009));
#410486=CARTESIAN_POINT('Ctrl Pts',(-1.01778810567669,-0.587620236790433,
0.479166666666676));
#410487=CARTESIAN_POINT('Ctrl Pts',(-0.67852540378446,-1.17524047358087,
0.520833333333344));
#410488=CARTESIAN_POINT('Ctrl Pts',(-1.43925448419923E-16,-1.17524047358087,
0.562500000000009));
#410489=CARTESIAN_POINT('Ctrl Pts',(-1.43925448419923E-16,-1.17524047358087,
8.67361737988404E-15));
#410490=CARTESIAN_POINT('Ctrl Pts',(0.678525403784459,-1.17524047358087,
0.041666666666676));
#410491=CARTESIAN_POINT('Ctrl Pts',(1.01778810567669,-0.587620236790434,
0.0833333333333432));
#410492=CARTESIAN_POINT('Ctrl Pts',(1.35705080756892,2.29132664526027E-15,
0.125000000000009));
#410493=CARTESIAN_POINT('Ctrl Pts',(1.01778810567669,0.587620236790438,
0.166666666666676));
#410494=CARTESIAN_POINT('Ctrl Pts',(0.67852540378446,1.17524047358087,0.208333333333343));
#410495=CARTESIAN_POINT('Ctrl Pts',(0.,1.17524047358087,0.250000000000009));
#410496=CARTESIAN_POINT('Ctrl Pts',(-0.678525403784459,1.17524047358087,
0.291666666666676));
#410497=CARTESIAN_POINT('Ctrl Pts',(-1.01778810567669,0.587620236790438,
0.333333333333343));
#410498=CARTESIAN_POINT('Ctrl Pts',(-1.35705080756892,2.62370823081419E-15,
0.375000000000009));
#410499=CARTESIAN_POINT('Ctrl Pts',(-1.01778810567669,-0.587620236790433,
0.416666666666676));
#410500=CARTESIAN_POINT('Ctrl Pts',(-0.67852540378446,-1.17524047358087,
0.458333333333344));
#410501=CARTESIAN_POINT('Ctrl Pts',(-1.43925448419923E-16,-1.17524047358087,
0.500000000000009));
#410502=CARTESIAN_POINT('Origin',(0.,-1.11022302462516E-14,-14.21875));
#410503=CARTESIAN_POINT('',(-8.32001735975286E-31,-1.17524047358087,1.06250000000001));
#410504=CARTESIAN_POINT('',(-8.32001735975286E-31,-1.17524047358087,1.00000000000001));
#410505=CARTESIAN_POINT('',(1.43925448419925E-16,-1.1752404735809,-14.21875));
#410506=CARTESIAN_POINT('Ctrl Pts',(-1.43925448419923E-16,-1.17524047358087,
0.562500000000009));
#410507=CARTESIAN_POINT('Ctrl Pts',(0.678525403784459,-1.17524047358087,
0.604166666666677));
#410508=CARTESIAN_POINT('Ctrl Pts',(1.01778810567669,-0.587620236790434,
0.645833333333342));
#410509=CARTESIAN_POINT('Ctrl Pts',(1.35705080756892,2.29132664526027E-15,
0.687500000000009));
#410510=CARTESIAN_POINT('Ctrl Pts',(1.01778810567669,0.587620236790438,
0.729166666666677));
#410511=CARTESIAN_POINT('Ctrl Pts',(0.67852540378446,1.17524047358087,0.770833333333342));
#410512=CARTESIAN_POINT('Ctrl Pts',(0.,1.17524047358087,0.812500000000009));
#410513=CARTESIAN_POINT('Ctrl Pts',(-0.678525403784459,1.17524047358087,
0.854166666666677));
#410514=CARTESIAN_POINT('Ctrl Pts',(-1.01778810567669,0.587620236790438,
0.895833333333342));
#410515=CARTESIAN_POINT('Ctrl Pts',(-1.35705080756892,2.62370823081419E-15,
0.93750000000001));
#410516=CARTESIAN_POINT('Ctrl Pts',(-1.01778810567669,-0.587620236790433,
0.979166666666677));
#410517=CARTESIAN_POINT('Ctrl Pts',(-0.67852540378446,-1.17524047358087,
1.02083333333334));
#410518=CARTESIAN_POINT('Ctrl Pts',(-1.43925448419923E-16,-1.17524047358087,
1.06250000000001));
#410519=CARTESIAN_POINT('Ctrl Pts',(-1.43925448419923E-16,-1.17524047358087,
0.500000000000009));
#410520=CARTESIAN_POINT('Ctrl Pts',(0.678525403784459,-1.17524047358087,
0.541666666666676));
#410521=CARTESIAN_POINT('Ctrl Pts',(1.01778810567669,-0.587620236790434,
0.583333333333342));
#410522=CARTESIAN_POINT('Ctrl Pts',(1.35705080756892,2.29132664526027E-15,
0.625000000000009));
#410523=CARTESIAN_POINT('Ctrl Pts',(1.01778810567669,0.587620236790438,
0.666666666666677));
#410524=CARTESIAN_POINT('Ctrl Pts',(0.67852540378446,1.17524047358087,0.708333333333342));
#410525=CARTESIAN_POINT('Ctrl Pts',(0.,1.17524047358087,0.750000000000009));
#410526=CARTESIAN_POINT('Ctrl Pts',(-0.678525403784459,1.17524047358087,
0.791666666666677));
#410527=CARTESIAN_POINT('Ctrl Pts',(-1.01778810567669,0.587620236790438,
0.833333333333342));
#410528=CARTESIAN_POINT('Ctrl Pts',(-1.35705080756892,2.62370823081419E-15,
0.87500000000001));
#410529=CARTESIAN_POINT('Ctrl Pts',(-1.01778810567669,-0.587620236790433,
0.916666666666677));
#410530=CARTESIAN_POINT('Ctrl Pts',(-0.67852540378446,-1.17524047358087,
0.958333333333342));
#410531=CARTESIAN_POINT('Ctrl Pts',(-1.43925448419923E-16,-1.17524047358087,
1.00000000000001));
#410532=CARTESIAN_POINT('Origin',(0.,-1.11022302462516E-14,-14.21875));
#410533=CARTESIAN_POINT('',(-8.32001735975286E-31,-1.17524047358087,1.56250000000001));
#410534=CARTESIAN_POINT('',(-8.32001735975286E-31,-1.17524047358087,1.50000000000001));
#410535=CARTESIAN_POINT('',(1.43925448419925E-16,-1.1752404735809,-14.21875));
#410536=CARTESIAN_POINT('Ctrl Pts',(-1.43925448419923E-16,-1.17524047358087,
1.06250000000001));
#410537=CARTESIAN_POINT('Ctrl Pts',(0.678525403784459,-1.17524047358087,
1.10416666666668));
#410538=CARTESIAN_POINT('Ctrl Pts',(1.01778810567669,-0.587620236790434,
1.14583333333334));
#410539=CARTESIAN_POINT('Ctrl Pts',(1.35705080756892,2.29132664526027E-15,
1.18750000000001));
#410540=CARTESIAN_POINT('Ctrl Pts',(1.01778810567669,0.587620236790438,
1.22916666666668));
#410541=CARTESIAN_POINT('Ctrl Pts',(0.67852540378446,1.17524047358087,1.27083333333334));
#410542=CARTESIAN_POINT('Ctrl Pts',(0.,1.17524047358087,1.31250000000001));
#410543=CARTESIAN_POINT('Ctrl Pts',(-0.678525403784459,1.17524047358087,
1.35416666666668));
#410544=CARTESIAN_POINT('Ctrl Pts',(-1.01778810567669,0.587620236790438,
1.39583333333334));
#410545=CARTESIAN_POINT('Ctrl Pts',(-1.35705080756892,2.62370823081419E-15,
1.43750000000001));
#410546=CARTESIAN_POINT('Ctrl Pts',(-1.01778810567669,-0.587620236790433,
1.47916666666668));
#410547=CARTESIAN_POINT('Ctrl Pts',(-0.67852540378446,-1.17524047358087,
1.52083333333334));
#410548=CARTESIAN_POINT('Ctrl Pts',(-1.43925448419923E-16,-1.17524047358087,
1.56250000000001));
#410549=CARTESIAN_POINT('Ctrl Pts',(-1.43925448419923E-16,-1.17524047358087,
1.00000000000001));
#410550=CARTESIAN_POINT('Ctrl Pts',(0.678525403784459,-1.17524047358087,
1.04166666666668));
#410551=CARTESIAN_POINT('Ctrl Pts',(1.01778810567669,-0.587620236790434,
1.08333333333334));
#410552=CARTESIAN_POINT('Ctrl Pts',(1.35705080756892,2.29132664526027E-15,
1.12500000000001));
#410553=CARTESIAN_POINT('Ctrl Pts',(1.01778810567669,0.587620236790438,
1.16666666666668));
#410554=CARTESIAN_POINT('Ctrl Pts',(0.67852540378446,1.17524047358087,1.20833333333334));
#410555=CARTESIAN_POINT('Ctrl Pts',(0.,1.17524047358087,1.25000000000001));
#410556=CARTESIAN_POINT('Ctrl Pts',(-0.678525403784459,1.17524047358087,
1.29166666666668));
#410557=CARTESIAN_POINT('Ctrl Pts',(-1.01778810567669,0.587620236790438,
1.33333333333334));
#410558=CARTESIAN_POINT('Ctrl Pts',(-1.35705080756892,2.62370823081419E-15,
1.37500000000001));
#410559=CARTESIAN_POINT('Ctrl Pts',(-1.01778810567669,-0.587620236790433,
1.41666666666668));
#410560=CARTESIAN_POINT('Ctrl Pts',(-0.67852540378446,-1.17524047358087,
1.45833333333334));
#410561=CARTESIAN_POINT('Ctrl Pts',(-1.43925448419923E-16,-1.17524047358087,
1.50000000000001));
#410562=CARTESIAN_POINT('Origin',(0.,-1.11022302462516E-14,-14.21875));
#410563=CARTESIAN_POINT('',(-8.32001735975286E-31,-1.17524047358087,2.06250000000001));
#410564=CARTESIAN_POINT('',(-8.32001735975286E-31,-1.17524047358087,2.00000000000001));
#410565=CARTESIAN_POINT('',(1.43925448419925E-16,-1.1752404735809,-14.21875));
#410566=CARTESIAN_POINT('Ctrl Pts',(-1.43925448419923E-16,-1.17524047358087,
1.56250000000001));
#410567=CARTESIAN_POINT('Ctrl Pts',(0.678525403784459,-1.17524047358087,
1.60416666666668));
#410568=CARTESIAN_POINT('Ctrl Pts',(1.01778810567669,-0.587620236790434,
1.64583333333334));
#410569=CARTESIAN_POINT('Ctrl Pts',(1.35705080756892,2.29132664526027E-15,
1.68750000000001));
#410570=CARTESIAN_POINT('Ctrl Pts',(1.01778810567669,0.587620236790438,
1.72916666666668));
#410571=CARTESIAN_POINT('Ctrl Pts',(0.67852540378446,1.17524047358087,1.77083333333334));
#410572=CARTESIAN_POINT('Ctrl Pts',(0.,1.17524047358087,1.81250000000001));
#410573=CARTESIAN_POINT('Ctrl Pts',(-0.678525403784459,1.17524047358087,
1.85416666666668));
#410574=CARTESIAN_POINT('Ctrl Pts',(-1.01778810567669,0.587620236790438,
1.89583333333334));
#410575=CARTESIAN_POINT('Ctrl Pts',(-1.35705080756892,2.62370823081419E-15,
1.93750000000001));
#410576=CARTESIAN_POINT('Ctrl Pts',(-1.01778810567669,-0.587620236790433,
1.97916666666668));
#410577=CARTESIAN_POINT('Ctrl Pts',(-0.67852540378446,-1.17524047358087,
2.02083333333334));
#410578=CARTESIAN_POINT('Ctrl Pts',(-1.43925448419923E-16,-1.17524047358087,
2.06250000000001));
#410579=CARTESIAN_POINT('Ctrl Pts',(-1.43925448419923E-16,-1.17524047358087,
1.50000000000001));
#410580=CARTESIAN_POINT('Ctrl Pts',(0.678525403784459,-1.17524047358087,
1.54166666666668));
#410581=CARTESIAN_POINT('Ctrl Pts',(1.01778810567669,-0.587620236790434,
1.58333333333334));
#410582=CARTESIAN_POINT('Ctrl Pts',(1.35705080756892,2.29132664526027E-15,
1.62500000000001));
#410583=CARTESIAN_POINT('Ctrl Pts',(1.01778810567669,0.587620236790438,
1.66666666666668));
#410584=CARTESIAN_POINT('Ctrl Pts',(0.67852540378446,1.17524047358087,1.70833333333334));
#410585=CARTESIAN_POINT('Ctrl Pts',(0.,1.17524047358087,1.75000000000001));
#410586=CARTESIAN_POINT('Ctrl Pts',(-0.678525403784459,1.17524047358087,
1.79166666666668));
#410587=CARTESIAN_POINT('Ctrl Pts',(-1.01778810567669,0.587620236790438,
1.83333333333334));
#410588=CARTESIAN_POINT('Ctrl Pts',(-1.35705080756892,2.62370823081419E-15,
1.87500000000001));
#410589=CARTESIAN_POINT('Ctrl Pts',(-1.01778810567669,-0.587620236790433,
1.91666666666668));
#410590=CARTESIAN_POINT('Ctrl Pts',(-0.67852540378446,-1.17524047358087,
1.95833333333334));
#410591=CARTESIAN_POINT('Ctrl Pts',(-1.43925448419923E-16,-1.17524047358087,
2.00000000000001));
#410592=CARTESIAN_POINT('Origin',(0.,-1.11022302462516E-14,-14.21875));
#410593=CARTESIAN_POINT('',(-8.32001735975286E-31,-1.17524047358087,2.56250000000001));
#410594=CARTESIAN_POINT('',(-8.32001735975286E-31,-1.17524047358087,2.50000000000001));
#410595=CARTESIAN_POINT('',(1.43925448419925E-16,-1.1752404735809,-14.21875));
#410596=CARTESIAN_POINT('Ctrl Pts',(-1.43925448419923E-16,-1.17524047358087,
2.06250000000001));
#410597=CARTESIAN_POINT('Ctrl Pts',(0.678525403784459,-1.17524047358087,
2.10416666666668));
#410598=CARTESIAN_POINT('Ctrl Pts',(1.01778810567669,-0.587620236790434,
2.14583333333334));
#410599=CARTESIAN_POINT('Ctrl Pts',(1.35705080756892,2.29132664526027E-15,
2.18750000000001));
#410600=CARTESIAN_POINT('Ctrl Pts',(1.01778810567669,0.587620236790438,
2.22916666666668));
#410601=CARTESIAN_POINT('Ctrl Pts',(0.67852540378446,1.17524047358087,2.27083333333334));
#410602=CARTESIAN_POINT('Ctrl Pts',(0.,1.17524047358087,2.31250000000001));
#410603=CARTESIAN_POINT('Ctrl Pts',(-0.678525403784459,1.17524047358087,
2.35416666666668));
#410604=CARTESIAN_POINT('Ctrl Pts',(-1.01778810567669,0.587620236790438,
2.39583333333334));
#410605=CARTESIAN_POINT('Ctrl Pts',(-1.35705080756892,2.62370823081419E-15,
2.43750000000001));
#410606=CARTESIAN_POINT('Ctrl Pts',(-1.01778810567669,-0.587620236790433,
2.47916666666668));
#410607=CARTESIAN_POINT('Ctrl Pts',(-0.67852540378446,-1.17524047358087,
2.52083333333334));
#410608=CARTESIAN_POINT('Ctrl Pts',(-1.43925448419923E-16,-1.17524047358087,
2.56250000000001));
#410609=CARTESIAN_POINT('Ctrl Pts',(-1.43925448419923E-16,-1.17524047358087,
2.00000000000001));
#410610=CARTESIAN_POINT('Ctrl Pts',(0.678525403784459,-1.17524047358087,
2.04166666666668));
#410611=CARTESIAN_POINT('Ctrl Pts',(1.01778810567669,-0.587620236790434,
2.08333333333334));
#410612=CARTESIAN_POINT('Ctrl Pts',(1.35705080756892,2.29132664526027E-15,
2.12500000000001));
#410613=CARTESIAN_POINT('Ctrl Pts',(1.01778810567669,0.587620236790438,
2.16666666666668));
#410614=CARTESIAN_POINT('Ctrl Pts',(0.67852540378446,1.17524047358087,2.20833333333334));
#410615=CARTESIAN_POINT('Ctrl Pts',(0.,1.17524047358087,2.25000000000001));
#410616=CARTESIAN_POINT('Ctrl Pts',(-0.678525403784459,1.17524047358087,
2.29166666666668));
#410617=CARTESIAN_POINT('Ctrl Pts',(-1.01778810567669,0.587620236790438,
2.33333333333334));
#410618=CARTESIAN_POINT('Ctrl Pts',(-1.35705080756892,2.62370823081419E-15,
2.37500000000001));
#410619=CARTESIAN_POINT('Ctrl Pts',(-1.01778810567669,-0.587620236790433,
2.41666666666668));
#410620=CARTESIAN_POINT('Ctrl Pts',(-0.67852540378446,-1.17524047358087,
2.45833333333334));
#410621=CARTESIAN_POINT('Ctrl Pts',(-1.43925448419923E-16,-1.17524047358087,
2.50000000000001));
#410622=CARTESIAN_POINT('Origin',(0.,-1.11022302462516E-14,-14.21875));
#410623=CARTESIAN_POINT('',(-8.32001735975286E-31,-1.17524047358087,3.06250000000001));
#410624=CARTESIAN_POINT('',(-8.32001735975286E-31,-1.17524047358087,3.00000000000001));
#410625=CARTESIAN_POINT('',(1.43925448419925E-16,-1.1752404735809,-14.21875));
#410626=CARTESIAN_POINT('Ctrl Pts',(-1.43925448419923E-16,-1.17524047358087,
2.56250000000001));
#410627=CARTESIAN_POINT('Ctrl Pts',(0.678525403784459,-1.17524047358087,
2.60416666666668));
#410628=CARTESIAN_POINT('Ctrl Pts',(1.01778810567669,-0.587620236790434,
2.64583333333334));
#410629=CARTESIAN_POINT('Ctrl Pts',(1.35705080756892,2.29132664526027E-15,
2.68750000000001));
#410630=CARTESIAN_POINT('Ctrl Pts',(1.01778810567669,0.587620236790438,
2.72916666666668));
#410631=CARTESIAN_POINT('Ctrl Pts',(0.67852540378446,1.17524047358087,2.77083333333334));
#410632=CARTESIAN_POINT('Ctrl Pts',(0.,1.17524047358087,2.81250000000001));
#410633=CARTESIAN_POINT('Ctrl Pts',(-0.678525403784459,1.17524047358087,
2.85416666666668));
#410634=CARTESIAN_POINT('Ctrl Pts',(-1.01778810567669,0.587620236790438,
2.89583333333334));
#410635=CARTESIAN_POINT('Ctrl Pts',(-1.35705080756892,2.62370823081419E-15,
2.93750000000001));
#410636=CARTESIAN_POINT('Ctrl Pts',(-1.01778810567669,-0.587620236790433,
2.97916666666668));
#410637=CARTESIAN_POINT('Ctrl Pts',(-0.67852540378446,-1.17524047358087,
3.02083333333334));
#410638=CARTESIAN_POINT('Ctrl Pts',(-1.43925448419923E-16,-1.17524047358087,
3.06250000000001));
#410639=CARTESIAN_POINT('Ctrl Pts',(-1.43925448419923E-16,-1.17524047358087,
2.50000000000001));
#410640=CARTESIAN_POINT('Ctrl Pts',(0.678525403784459,-1.17524047358087,
2.54166666666668));
#410641=CARTESIAN_POINT('Ctrl Pts',(1.01778810567669,-0.587620236790434,
2.58333333333334));
#410642=CARTESIAN_POINT('Ctrl Pts',(1.35705080756892,2.29132664526027E-15,
2.62500000000001));
#410643=CARTESIAN_POINT('Ctrl Pts',(1.01778810567669,0.587620236790438,
2.66666666666668));
#410644=CARTESIAN_POINT('Ctrl Pts',(0.67852540378446,1.17524047358087,2.70833333333334));
#410645=CARTESIAN_POINT('Ctrl Pts',(0.,1.17524047358087,2.75000000000001));
#410646=CARTESIAN_POINT('Ctrl Pts',(-0.678525403784459,1.17524047358087,
2.79166666666668));
#410647=CARTESIAN_POINT('Ctrl Pts',(-1.01778810567669,0.587620236790438,
2.83333333333334));
#410648=CARTESIAN_POINT('Ctrl Pts',(-1.35705080756892,2.62370823081419E-15,
2.87500000000001));
#410649=CARTESIAN_POINT('Ctrl Pts',(-1.01778810567669,-0.587620236790433,
2.91666666666668));
#410650=CARTESIAN_POINT('Ctrl Pts',(-0.67852540378446,-1.17524047358087,
2.95833333333334));
#410651=CARTESIAN_POINT('Ctrl Pts',(-1.43925448419923E-16,-1.17524047358087,
3.00000000000001));
#410652=CARTESIAN_POINT('Origin',(0.,-1.11022302462516E-14,-14.21875));
#410653=CARTESIAN_POINT('',(-8.32001735975286E-31,-1.17524047358087,3.56250000000001));
#410654=CARTESIAN_POINT('',(-8.32001735975286E-31,-1.17524047358087,3.50000000000001));
#410655=CARTESIAN_POINT('',(1.43925448419925E-16,-1.1752404735809,-14.21875));
#410656=CARTESIAN_POINT('Ctrl Pts',(-1.43925448419923E-16,-1.17524047358087,
3.06250000000001));
#410657=CARTESIAN_POINT('Ctrl Pts',(0.678525403784459,-1.17524047358087,
3.10416666666668));
#410658=CARTESIAN_POINT('Ctrl Pts',(1.01778810567669,-0.587620236790434,
3.14583333333334));
#410659=CARTESIAN_POINT('Ctrl Pts',(1.35705080756892,2.29132664526027E-15,
3.18750000000001));
#410660=CARTESIAN_POINT('Ctrl Pts',(1.01778810567669,0.587620236790438,
3.22916666666668));
#410661=CARTESIAN_POINT('Ctrl Pts',(0.67852540378446,1.17524047358087,3.27083333333334));
#410662=CARTESIAN_POINT('Ctrl Pts',(0.,1.17524047358087,3.31250000000001));
#410663=CARTESIAN_POINT('Ctrl Pts',(-0.678525403784459,1.17524047358087,
3.35416666666668));
#410664=CARTESIAN_POINT('Ctrl Pts',(-1.01778810567669,0.587620236790438,
3.39583333333334));
#410665=CARTESIAN_POINT('Ctrl Pts',(-1.35705080756892,2.62370823081419E-15,
3.43750000000001));
#410666=CARTESIAN_POINT('Ctrl Pts',(-1.01778810567669,-0.587620236790433,
3.47916666666668));
#410667=CARTESIAN_POINT('Ctrl Pts',(-0.67852540378446,-1.17524047358087,
3.52083333333334));
#410668=CARTESIAN_POINT('Ctrl Pts',(-1.43925448419923E-16,-1.17524047358087,
3.56250000000001));
#410669=CARTESIAN_POINT('Ctrl Pts',(-1.43925448419923E-16,-1.17524047358087,
3.00000000000001));
#410670=CARTESIAN_POINT('Ctrl Pts',(0.678525403784459,-1.17524047358087,
3.04166666666668));
#410671=CARTESIAN_POINT('Ctrl Pts',(1.01778810567669,-0.587620236790434,
3.08333333333334));
#410672=CARTESIAN_POINT('Ctrl Pts',(1.35705080756892,2.29132664526027E-15,
3.12500000000001));
#410673=CARTESIAN_POINT('Ctrl Pts',(1.01778810567669,0.587620236790438,
3.16666666666668));
#410674=CARTESIAN_POINT('Ctrl Pts',(0.67852540378446,1.17524047358087,3.20833333333334));
#410675=CARTESIAN_POINT('Ctrl Pts',(0.,1.17524047358087,3.25000000000001));
#410676=CARTESIAN_POINT('Ctrl Pts',(-0.678525403784459,1.17524047358087,
3.29166666666668));
#410677=CARTESIAN_POINT('Ctrl Pts',(-1.01778810567669,0.587620236790438,
3.33333333333334));
#410678=CARTESIAN_POINT('Ctrl Pts',(-1.35705080756892,2.62370823081419E-15,
3.37500000000001));
#410679=CARTESIAN_POINT('Ctrl Pts',(-1.01778810567669,-0.587620236790433,
3.41666666666668));
#410680=CARTESIAN_POINT('Ctrl Pts',(-0.67852540378446,-1.17524047358087,
3.45833333333334));
#410681=CARTESIAN_POINT('Ctrl Pts',(-1.43925448419923E-16,-1.17524047358087,
3.50000000000001));
#410682=CARTESIAN_POINT('Origin',(0.,-1.19311743680736E-13,1002.5));
#410683=CARTESIAN_POINT('',(0.,1.50000000000006,4.00000000000002));
#410684=CARTESIAN_POINT('',(2.65829355574649E-12,1.22263611415551,3.72263611415551));
#410685=CARTESIAN_POINT('',(-1.22464679914734E-13,999.999999999989,1002.5));
#410686=CARTESIAN_POINT('',(1.16245326511943,-0.172894699617312,3.67524047358081));
#410687=CARTESIAN_POINT('Ctrl Pts',(5.09848710616739E-14,1.5000000000003,
4.00000000000016));
#410688=CARTESIAN_POINT('Ctrl Pts',(0.0614459419740359,1.49300527352564,
3.9930052735255));
#410689=CARTESIAN_POINT('Ctrl Pts',(0.176619180984774,1.47627277954793,
3.97963189845153));
#410690=CARTESIAN_POINT('Ctrl Pts',(0.407741104272866,1.39313746098645,
3.94828274522662));
#410691=CARTESIAN_POINT('Ctrl Pts',(0.496650592209766,1.35004412327267,
3.93518797642063));
#410692=CARTESIAN_POINT('Ctrl Pts',(0.73463717654934,1.20168003430334,3.89686512472376));
#410693=CARTESIAN_POINT('Ctrl Pts',(0.868548220680461,1.07608400562327,
3.87108844075398));
#410694=CARTESIAN_POINT('Ctrl Pts',(1.05190674105084,0.820029611618427,
3.82725385858292));
#410695=CARTESIAN_POINT('Ctrl Pts',(1.14450211555196,0.659211935335112,
3.80455972666058));
#410696=CARTESIAN_POINT('Ctrl Pts',(1.21470849431358,0.34856178753037,3.75902940895801));
#410697=CARTESIAN_POINT('Ctrl Pts',(1.22403973629944,0.238553492192828,
3.74234909593137));
#410698=CARTESIAN_POINT('Ctrl Pts',(1.21272207332383,0.0262843883317015,
3.70875263493674));
#410699=CARTESIAN_POINT('Ctrl Pts',(1.19398876028483,-0.0751524073185166,
3.69205355609417));
#410700=CARTESIAN_POINT('Ctrl Pts',(1.16245326511929,-0.172894699617247,
3.67524047358073));
#410701=CARTESIAN_POINT('',(0.943477955796025,0.700742119234707,3.67524047358081));
#410702=CARTESIAN_POINT('Origin',(-5.55111512312578E-16,5.58580959264532E-15,
3.67524047358089));
#410703=CARTESIAN_POINT('Ctrl Pts',(0.943477955795997,0.700742119234686,
3.67524047358083));
#410704=CARTESIAN_POINT('Ctrl Pts',(0.894463001055356,0.772758356925599,
3.67883146777442));
#410705=CARTESIAN_POINT('Ctrl Pts',(0.837726504812894,0.839196987658124,
3.68256694202216));
#410706=CARTESIAN_POINT('Ctrl Pts',(0.712851122357575,0.956652840655983,
3.69006027251154));
#410707=CARTESIAN_POINT('Ctrl Pts',(0.645482378604126,1.00776531764839,
3.69379267345778));
#410708=CARTESIAN_POINT('Ctrl Pts',(0.447490290696521,1.12733650300416,
3.70398399106719));
#410709=CARTESIAN_POINT('Ctrl Pts',(0.308736215403076,1.17946143006525,
3.71032040612255));
#410710=CARTESIAN_POINT('Ctrl Pts',(0.108169821062047,1.21501394733954,
3.71850309831));
#410711=CARTESIAN_POINT('Ctrl Pts',(0.0533501263262607,1.22063965939443,
3.72063965939443));
#410712=CARTESIAN_POINT('Ctrl Pts',(5.31673684123335E-12,1.22263611415551,
3.72263611415551));
#410713=CARTESIAN_POINT('Origin',(0.,2.54061283442571E-15,-14.));
#410714=CARTESIAN_POINT('',(1.4102143475861E-12,1.33373412263468,-13.8415063509462));
#410715=CARTESIAN_POINT('',(-1.43925448419923E-16,1.17524047358087,-14.));
#410716=CARTESIAN_POINT('',(-1.43925448419923E-16,1.17524047358087,-14.));
#410717=CARTESIAN_POINT('Ctrl Pts',(2.82059203049461E-12,1.33373412263468,
-13.8415063509462));
#410718=CARTESIAN_POINT('Ctrl Pts',(0.0503707035999144,1.33200617731085,
-13.84323429627));
#410719=CARTESIAN_POINT('Ctrl Pts',(0.101566648626412,1.32733503529964,
-13.8450537305792));
#410720=CARTESIAN_POINT('Ctrl Pts',(0.311597220248351,1.29512418775187,
-13.8528065966954));
#410721=CARTESIAN_POINT('Ctrl Pts',(0.464060849169011,1.2419652779919,-13.8590957478521));
#410722=CARTESIAN_POINT('Ctrl Pts',(0.752305458718201,1.07737853149812,
-13.8724606339434));
#410723=CARTESIAN_POINT('Ctrl Pts',(0.883244570548725,0.963577263216904,
-13.8794314317899));
#410724=CARTESIAN_POINT('Ctrl Pts',(1.05897345549616,0.736523802329364,
-13.8904755074827));
#410725=CARTESIAN_POINT('Ctrl Pts',(1.15669334597624,0.586782768129815,
-13.8964531882757));
#410726=CARTESIAN_POINT('Ctrl Pts',(1.25343072844487,0.22591559097259,-13.9112797109474));
#410727=CARTESIAN_POINT('Ctrl Pts',(1.26526290710797,0.0682549586007996,
-13.9178507152948));
#410728=CARTESIAN_POINT('Ctrl Pts',(1.22916289389683,-0.252389992813634,
-13.9314343166522));
#410729=CARTESIAN_POINT('Ctrl Pts',(1.1780317000175,-0.411978763297157,
-13.9383169357496));
#410730=CARTESIAN_POINT('Ctrl Pts',(0.998487821188208,-0.73449306440248,
-13.9524375659778));
#410731=CARTESIAN_POINT('Ctrl Pts',(0.881213268978223,-0.845390401721151,
-13.9587809847204));
#410732=CARTESIAN_POINT('Ctrl Pts',(0.688202236191876,-1.00009299759695,
-13.9693507574149));
#410733=CARTESIAN_POINT('Ctrl Pts',(0.564231790739783,-1.06795850550759,
-13.9755497402544));
#410734=CARTESIAN_POINT('Ctrl Pts',(0.292597606675929,-1.15980721556296,
-13.9880801320964));
#410735=CARTESIAN_POINT('Ctrl Pts',(0.146401631267334,-1.18094002160998,
-13.9943004519709));
#410736=CARTESIAN_POINT('Ctrl Pts',(-2.42861286636753E-16,-1.17524047358088,
-14.));
#410737=CARTESIAN_POINT('Origin',(0.,2.54061283442571E-15,-14.));
#410738=CARTESIAN_POINT('Origin',(0.,2.5406128344257E-15,14.));
#410739=CARTESIAN_POINT('',(-1.2271251213284E-13,1.50000000000006,-13.4375));
#410740=CARTESIAN_POINT('',(-1.76090861703506E-14,1.50000000000006,-13.5));
#410741=CARTESIAN_POINT('',(-1.8369701987211E-16,1.50000000000006,14.));
#410742=CARTESIAN_POINT('',(0.2433378840056,-1.48013062741362,-13.6752404735808));
#410743=CARTESIAN_POINT('Ctrl Pts',(-2.45289899503121E-13,1.50000000000006,
-13.4375));
#410744=CARTESIAN_POINT('Ctrl Pts',(0.154099018422491,1.50000000000008,
-13.4449140924807));
#410745=CARTESIAN_POINT('Ctrl Pts',(0.3075139555236,1.47625956742878,-13.4529547285437));
#410746=CARTESIAN_POINT('Ctrl Pts',(0.642809422800748,1.36956233159267,
-13.4720504513412));
#410747=CARTESIAN_POINT('Ctrl Pts',(0.817133592085943,1.27326193964589,
-13.4831126377338));
#410748=CARTESIAN_POINT('Ctrl Pts',(1.11308167833158,1.02332674485026,-13.5042940909721));
#410749=CARTESIAN_POINT('Ctrl Pts',(1.23365593605882,0.874188091054278,
-13.5139339949414));
#410750=CARTESIAN_POINT('Ctrl Pts',(1.41682962140902,0.531160231905482,
-13.5329910982275));
#410751=CARTESIAN_POINT('Ctrl Pts',(1.47467131896198,0.338905698544985,
-13.5436719056364));
#410752=CARTESIAN_POINT('Ctrl Pts',(1.51168174079155,-0.053055686762387,
-13.5654475381535));
#410753=CARTESIAN_POINT('Ctrl Pts',(1.49200417916322,-0.248854522257683,
-13.5763252512365));
#410754=CARTESIAN_POINT('Ctrl Pts',(1.38003397123258,-0.617986951620019,
-13.5968326084233));
#410755=CARTESIAN_POINT('Ctrl Pts',(1.29034581469085,-0.788293050011382,
-13.6056485705454));
#410756=CARTESIAN_POINT('Ctrl Pts',(1.05637903511238,-1.08064599775905,
-13.6250262176915));
#410757=CARTESIAN_POINT('Ctrl Pts',(0.916265143532659,-1.20173932499309,
-13.6351311539775));
#410758=CARTESIAN_POINT('Ctrl Pts',(0.599147008227846,-1.38737752273559,
-13.6555451239801));
#410759=CARTESIAN_POINT('Ctrl Pts',(0.424766445511276,-1.45030323148159,
-13.6656829490696));
#410760=CARTESIAN_POINT('Ctrl Pts',(0.243337884005714,-1.4801306274136,
-13.6752404735808));
#410761=CARTESIAN_POINT('',(1.20419349529495,-0.894381364905089,-13.6752404735808));
#410762=CARTESIAN_POINT('Origin',(0.,2.54061283442571E-15,-13.6752404735808));
#410763=CARTESIAN_POINT('Ctrl Pts',(1.20419349529495,-0.894381364905085,
-13.6752404735808));
#410764=CARTESIAN_POINT('Ctrl Pts',(1.26487937350023,-0.812674005317148,
-13.6700510740269));
#410765=CARTESIAN_POINT('Ctrl Pts',(1.3170709609443,-0.725038800233257,
-13.6652799333463));
#410766=CARTESIAN_POINT('Ctrl Pts',(1.40415555674086,-0.537868414461984,
-13.6548815785812));
#410767=CARTESIAN_POINT('Ctrl Pts',(1.43825077374835,-0.438617967969369,
-13.6493676648871));
#410768=CARTESIAN_POINT('Ctrl Pts',(1.50578641792733,-0.145369370312591,
-13.6330760761284));
#410769=CARTESIAN_POINT('Ctrl Pts',(1.51186815437617,0.052697405544391,
-13.6220723663586));
#410770=CARTESIAN_POINT('Ctrl Pts',(1.44677677093112,0.443724946936882,
-13.600348614059));
#410771=CARTESIAN_POINT('Ctrl Pts',(1.37474540067206,0.632529457136806,
-13.5902388728971));
#410772=CARTESIAN_POINT('Ctrl Pts',(1.16558432059299,0.963340423632484,
-13.570986412226));
#410773=CARTESIAN_POINT('Ctrl Pts',(1.03334003549703,1.10399171713937,-13.5607168257176));
#410774=CARTESIAN_POINT('Ctrl Pts',(0.717145150131488,1.33236982232222,
-13.5391600559473));
#410775=CARTESIAN_POINT('Ctrl Pts',(0.534471089831185,1.41557611950021,
-13.5280598600906));
#410776=CARTESIAN_POINT('Ctrl Pts',(0.228875537835284,1.48689143938017,
-13.5113759061321));
#410777=CARTESIAN_POINT('Ctrl Pts',(0.114507097818563,1.50000000000006,
-13.5055092253125));
#410778=CARTESIAN_POINT('Ctrl Pts',(-3.33413852082742E-14,1.50000000000006,
-13.5));
#410779=CARTESIAN_POINT('Origin',(0.,2.5406128344257E-15,14.));
#410780=CARTESIAN_POINT('',(-1.4424133868457E-14,1.50000000000006,-12.9375));
#410781=CARTESIAN_POINT('',(-1.17935083679999E-13,1.50000000000006,-13.));
#410782=CARTESIAN_POINT('',(-1.8369701987211E-16,1.50000000000006,14.));
#410783=CARTESIAN_POINT('Ctrl Pts',(-2.86576318231369E-14,1.50000000000006,
-12.9375));
#410784=CARTESIAN_POINT('Ctrl Pts',(0.184852825957988,1.50000000000006,
-12.9463937357356));
#410785=CARTESIAN_POINT('Ctrl Pts',(0.368282906907539,1.4658328779758,-12.956168106343));
#410786=CARTESIAN_POINT('Ctrl Pts',(0.72389141137937,1.32831699878958,-12.9770972140245));
#410787=CARTESIAN_POINT('Ctrl Pts',(0.891143524743268,1.22242037256957,
-12.9880857080312));
#410788=CARTESIAN_POINT('Ctrl Pts',(1.17101075554248,0.956468513672169,
-13.0089383780871));
#410789=CARTESIAN_POINT('Ctrl Pts',(1.28259586684403,0.800644978114965,
-13.0180197234381));
#410790=CARTESIAN_POINT('Ctrl Pts',(1.44543345949742,0.447528023135354,
-13.037637332048));
#410791=CARTESIAN_POINT('Ctrl Pts',(1.49196279374196,0.252162578720567,
-13.0484909678489));
#410792=CARTESIAN_POINT('Ctrl Pts',(1.50595370549604,-0.140261693065969,
-13.0702923162814));
#410793=CARTESIAN_POINT('Ctrl Pts',(1.47524935824808,-0.333499915715787,
-13.0810277730953));
#410794=CARTESIAN_POINT('Ctrl Pts',(1.34246640649021,-0.69629608957844,
-13.1011831160877));
#410795=CARTESIAN_POINT('Ctrl Pts',(1.24216320762647,-0.862598601288366,
-13.1100308003996));
#410796=CARTESIAN_POINT('Ctrl Pts',(0.979665680373286,-1.15321907962225,
-13.1307330096329));
#410797=CARTESIAN_POINT('Ctrl Pts',(0.818085798325511,-1.2729432454608,
-13.1418326966058));
#410798=CARTESIAN_POINT('Ctrl Pts',(0.4644476501586,-1.43909739126499,-13.1634625128815));
#410799=CARTESIAN_POINT('Ctrl Pts',(0.276987275447283,-1.48661095844317,
-13.1738015256755));
#410800=CARTESIAN_POINT('Ctrl Pts',(-0.112827305776877,-1.50890274072842,
-13.1931757046337));
#410801=CARTESIAN_POINT('Ctrl Pts',(-0.311602660346058,-1.48069201022844,
-13.2030283230351));
#410802=CARTESIAN_POINT('Ctrl Pts',(-0.684567164515238,-1.34908723753913,
-13.2246282742387));
#410803=CARTESIAN_POINT('Ctrl Pts',(-0.855341639053257,-1.24782221144681,
-13.2356575823673));
#410804=CARTESIAN_POINT('Ctrl Pts',(-1.14309366854786,-0.989654320961702,
-13.2566733886326));
#410805=CARTESIAN_POINT('Ctrl Pts',(-1.25906862022969,-0.837139245306665,
-13.2659922641496));
#410806=CARTESIAN_POINT('Ctrl Pts',(-1.43195153850576,-0.488941921447512,
-13.2853365599196));
#410807=CARTESIAN_POINT('Ctrl Pts',(-1.48407800628601,-0.29502430488665,
-13.2961097608396));
#410808=CARTESIAN_POINT('Ctrl Pts',(-1.50940514181516,0.0973417379654638,
-13.3179078743314));
#410809=CARTESIAN_POINT('Ctrl Pts',(-1.48410708479636,0.291918192051283,
-13.3287176773362));
#410810=CARTESIAN_POINT('Ctrl Pts',(-1.36157410946492,0.657874819395,-13.3490486010775));
#410811=CARTESIAN_POINT('Ctrl Pts',(-1.26655798730886,0.826143729909582,
-13.3578444706988));
#410812=CARTESIAN_POINT('Ctrl Pts',(-1.01301440814474,1.12414268541646,
-13.3783208406031));
#410813=CARTESIAN_POINT('Ctrl Pts',(-0.854503038877091,1.24888216839119,
-13.3894122080509));
#410814=CARTESIAN_POINT('Ctrl Pts',(-0.504746456989134,1.42553331513728,
-13.4111468557414));
#410815=CARTESIAN_POINT('Ctrl Pts',(-0.318170363476253,1.4784117155096,
-13.4215923466807));
#410816=CARTESIAN_POINT('Ctrl Pts',(-0.0844779885570294,1.49821791269636,
-13.4333860484554));
#410817=CARTESIAN_POINT('Ctrl Pts',(-0.0422157010777418,1.50000000000005,
-13.4354688961349));
#410818=CARTESIAN_POINT('Ctrl Pts',(-2.45241327245807E-13,1.50000000000006,
-13.4375));
#410819=CARTESIAN_POINT('Ctrl Pts',(-3.5034475320829E-14,1.50000000000006,
-13.5));
#410820=CARTESIAN_POINT('Ctrl Pts',(-0.0777857544300243,1.50000000000006,
-13.496257531145));
#410821=CARTESIAN_POINT('Ctrl Pts',(-0.155619149278412,1.4939502636561,
-13.4923447219576));
#410822=CARTESIAN_POINT('Ctrl Pts',(-0.423998845455286,1.45178591133617,
-13.4782610657959));
#410823=CARTESIAN_POINT('Ctrl Pts',(-0.60756485963818,1.38502997963198,
-13.4675749103845));
#410824=CARTESIAN_POINT('Ctrl Pts',(-0.94375800148565,1.18273677189161,
-13.4457805545352));
#410825=CARTESIAN_POINT('Ctrl Pts',(-1.09209305825346,1.04732852804349,
-13.434882440682));
#410826=CARTESIAN_POINT('Ctrl Pts',(-1.3221095209703,0.733599132438725,
-13.4151010630262));
#410827=CARTESIAN_POINT('Ctrl Pts',(-1.40434608742343,0.560323983928858,
-13.4061291102182));
#410828=CARTESIAN_POINT('Ctrl Pts',(-1.50114237669675,0.186782615875113,
-13.385376811993));
#410829=CARTESIAN_POINT('Ctrl Pts',(-1.51268012037893,-0.0104892337438368,
-13.3744172647919));
#410830=CARTESIAN_POINT('Ctrl Pts',(-1.45891178653008,-0.401398254268275,
-13.352700096985));
#410831=CARTESIAN_POINT('Ctrl Pts',(-1.39291869469351,-0.590987184595628,
-13.3422671879284));
#410832=CARTESIAN_POINT('Ctrl Pts',(-1.19502793232843,-0.926443398889491,
-13.3234279360101));
#410833=CARTESIAN_POINT('Ctrl Pts',(-1.06766380281429,-1.07072827672343,
-13.3132922131986));
#410834=CARTESIAN_POINT('Ctrl Pts',(-0.759913809545176,-1.30835035009972,
-13.2918849715945));
#410835=CARTESIAN_POINT('Ctrl Pts',(-0.580652095742315,-1.3971751572685,
-13.2807928826132));
#410836=CARTESIAN_POINT('Ctrl Pts',(-0.201378097004742,-1.49910542573291,
-13.2597136574947));
#410837=CARTESIAN_POINT('Ctrl Pts',(-0.00544640710581742,-1.51255858965364,
-13.2506108900966));
#410838=CARTESIAN_POINT('Ctrl Pts',(0.379052846273133,-1.46408732054578,
-13.2307652370012));
#410839=CARTESIAN_POINT('Ctrl Pts',(0.564029572780868,-1.4032415620624,
-13.2201753801398));
#410840=CARTESIAN_POINT('Ctrl Pts',(0.907438980410449,-1.21111096966877,
-13.1983161264118));
#410841=CARTESIAN_POINT('Ctrl Pts',(1.06109936088841,-1.07903671034705,
-13.1872544084835));
#410842=CARTESIAN_POINT('Ctrl Pts',(1.30116498830284,-0.770235999508398,
-13.167126448076));
#410843=CARTESIAN_POINT('Ctrl Pts',(1.38836336564338,-0.598954100754246,
-13.1582752278196));
#410844=CARTESIAN_POINT('Ctrl Pts',(1.4953150158834,-0.228343295009018,
-13.1376857386115));
#410845=CARTESIAN_POINT('Ctrl Pts',(1.51230785211533,-0.0320201587424078,
-13.1267788977078));
#410846=CARTESIAN_POINT('Ctrl Pts',(1.46975295761758,0.359626694949958,
-13.1050207391693));
#410847=CARTESIAN_POINT('Ctrl Pts',(1.40921800047594,0.551031376972371,
-13.0943871457237));
#410848=CARTESIAN_POINT('Ctrl Pts',(1.2211769228825,0.891569478800854,-13.0754683622887));
#410849=CARTESIAN_POINT('Ctrl Pts',(1.09838808096619,1.03911396724531,-13.0656486109837));
#410850=CARTESIAN_POINT('Ctrl Pts',(0.798522165802527,1.28505980419314,
-13.0443894766095));
#410851=CARTESIAN_POINT('Ctrl Pts',(0.622543558908819,1.37893394517422,
-13.0333150869105));
#410852=CARTESIAN_POINT('Ctrl Pts',(0.292600113075803,1.47852197007691,
-13.0146743414463));
#410853=CARTESIAN_POINT('Ctrl Pts',(0.146573787712378,1.50000000000008,
-13.0070520346493));
#410854=CARTESIAN_POINT('Ctrl Pts',(-2.35471364629092E-13,1.50000000000006,
-13.));
#410855=CARTESIAN_POINT('Origin',(0.,2.5406128344257E-15,14.));
#410856=CARTESIAN_POINT('',(9.46300839574452E-15,1.50000000000006,-12.4375));
#410857=CARTESIAN_POINT('',(-3.99037522836055E-14,1.50000000000006,-12.5));
#410858=CARTESIAN_POINT('',(-1.8369701987211E-16,1.50000000000006,14.));
#410859=CARTESIAN_POINT('Ctrl Pts',(1.91097138113612E-14,1.50000000000006,
-12.4375));
#410860=CARTESIAN_POINT('Ctrl Pts',(0.0144712148980006,1.50000000000006,
-12.4381962466514));
#410861=CARTESIAN_POINT('Ctrl Pts',(0.0289506003252937,1.49979058477179,
-12.4388987034969));
#410862=CARTESIAN_POINT('Ctrl Pts',(0.242185688672286,1.49361360589839,
-12.4493295642149));
#410863=CARTESIAN_POINT('Ctrl Pts',(0.437789212302859,1.44839601290101,
-12.4599965873837));
#410864=CARTESIAN_POINT('Ctrl Pts',(0.796491878951723,1.28593468629028,
-12.4817674921075));
#410865=CARTESIAN_POINT('Ctrl Pts',(0.95675559810253,1.17160325035686,-12.4926540571106));
#410866=CARTESIAN_POINT('Ctrl Pts',(1.2215744375202,0.891136897701778,-12.5131858914808));
#410867=CARTESIAN_POINT('Ctrl Pts',(1.32484055345982,0.728809131594151,
-12.5220106038003));
#410868=CARTESIAN_POINT('Ctrl Pts',(1.46863560718626,0.36507643645482,-12.5422179757525));
#410869=CARTESIAN_POINT('Ctrl Pts',(1.50421453234514,0.165813395109599,
-12.5532881447161));
#410870=CARTESIAN_POINT('Ctrl Pts',(1.49516690833387,-0.227209539152673,
-12.5751227521751));
#410871=CARTESIAN_POINT('Ctrl Pts',(1.45363347765981,-0.417271052511157,
-12.5856817251395));
#410872=CARTESIAN_POINT('Ctrl Pts',(1.29997176929002,-0.773385643877929,
-12.6054658691043));
#410873=CARTESIAN_POINT('Ctrl Pts',(1.18850487773847,-0.93569056662924,
-12.6146427703706));
#410874=CARTESIAN_POINT('Ctrl Pts',(0.907589738804474,-1.21056091538983,
-12.6357935937598));
#410875=CARTESIAN_POINT('Ctrl Pts',(0.740111695936488,-1.31962373145034,
-12.6468809075226));
#410876=CARTESIAN_POINT('Ctrl Pts',(0.379276311980173,-1.46372383810901,
-12.6682443887681));
#410877=CARTESIAN_POINT('Ctrl Pts',(0.190452331770557,-1.50000248438981,
-12.6783367889045));
#410878=CARTESIAN_POINT('Ctrl Pts',(-0.198819746662407,-1.49999740672085,
-12.6970657915568));
#410879=CARTESIAN_POINT('Ctrl Pts',(-0.39561299924559,-1.46047412053578,
-12.707631880397));
#410880=CARTESIAN_POINT('Ctrl Pts',(-0.759347989869126,-1.30829369300126,
-12.729359322391));
#410881=CARTESIAN_POINT('Ctrl Pts',(-0.923268236624447,-1.19825844329666,
-12.7403024736542));
#410882=CARTESIAN_POINT('Ctrl Pts',(-1.1958717752218,-0.925246685340456,
-12.7610017774634));
#410883=CARTESIAN_POINT('Ctrl Pts',(-1.30343461885677,-0.76631653272979,
-12.7699268592928));
#410884=CARTESIAN_POINT('Ctrl Pts',(-1.45688562510155,-0.408718687921794,
-12.7897934062266));
#410885=CARTESIAN_POINT('Ctrl Pts',(-1.4981782275804,-0.212156984428337,
-12.8007135008651));
#410886=CARTESIAN_POINT('Ctrl Pts',(-1.50165481736864,0.18002650253877,
-12.8225014723633));
#410887=CARTESIAN_POINT('Ctrl Pts',(-1.46597742543479,0.371889550365959,
-12.8331605305759));
#410888=CARTESIAN_POINT('Ctrl Pts',(-1.32367068114965,0.731678966310704,
-12.8531488314617));
#410889=CARTESIAN_POINT('Ctrl Pts',(-1.21834364925858,0.896159005203687,
-12.862109052878));
#410890=CARTESIAN_POINT('Ctrl Pts',(-0.947471792132494,1.17971885604868,
-12.8830180437038));
#410891=CARTESIAN_POINT('Ctrl Pts',(-0.783139322974793,1.29465224984847,
-12.8941170875847));
#410892=CARTESIAN_POINT('Ctrl Pts',(-0.426123079502387,1.45084226121507,
-12.9156326510344));
#410893=CARTESIAN_POINT('Ctrl Pts',(-0.237968535444941,1.49329096691863,
-12.9258643714701));
#410894=CARTESIAN_POINT('Ctrl Pts',(-0.0312538598267095,1.49975594898516,
-12.9359895187731));
#410895=CARTESIAN_POINT('Ctrl Pts',(-0.0156221697085717,1.50000000000006,
-12.9367483780095));
#410896=CARTESIAN_POINT('Ctrl Pts',(-2.86645707170419E-14,1.50000000000006,
-12.9375));
#410897=CARTESIAN_POINT('Ctrl Pts',(-2.35686470340126E-13,1.50000000000006,
-13.));
#410898=CARTESIAN_POINT('Ctrl Pts',(-0.0488561908367927,1.50000000000005,
-12.9976494054224));
#410899=CARTESIAN_POINT('Ctrl Pts',(-0.0977668133780745,1.49761321556351,
-12.9952298924304));
#410900=CARTESIAN_POINT('Ctrl Pts',(-0.338072805258772,1.47402088263108,
-12.9830128224239));
#410901=CARTESIAN_POINT('Ctrl Pts',(-0.52416483036909,1.41854276041394,
-12.9725184067408));
#410902=CARTESIAN_POINT('Ctrl Pts',(-0.871927326752233,1.2368262397146,
-12.9507389947019));
#410903=CARTESIAN_POINT('Ctrl Pts',(-1.0288946842114,1.10967845678737,-12.9396550163359));
#410904=CARTESIAN_POINT('Ctrl Pts',(-1.27806597055699,0.808135776262727,
-12.9192905716619));
#410905=CARTESIAN_POINT('Ctrl Pts',(-1.37052783126929,0.638898595859914,
-12.9104943664366));
#410906=CARTESIAN_POINT('Ctrl Pts',(-1.48802713407293,0.271417741405987,
-12.8900787634113));
#410907=CARTESIAN_POINT('Ctrl Pts',(-1.51065228263555,0.0762387495105381,
-12.8792354860838));
#410908=CARTESIAN_POINT('Ctrl Pts',(-1.47975611674998,-0.315978046570199,
-12.8574456640793));
#410909=CARTESIAN_POINT('Ctrl Pts',(-1.4248986350945,-0.50912454103883,
-12.8467153032755));
#410910=CARTESIAN_POINT('Ctrl Pts',(-1.24710381956909,-0.854870564928091,
-12.8275071908372));
#410911=CARTESIAN_POINT('Ctrl Pts',(-1.12894714535878,-1.0057727497918,
-12.8180450295841));
#410912=CARTESIAN_POINT('Ctrl Pts',(-0.837297925413553,-1.26004460532475,
-12.7969499428489));
#410913=CARTESIAN_POINT('Ctrl Pts',(-0.664820905826346,-1.35896785705792,
-12.7859037702712));
#410914=CARTESIAN_POINT('Ctrl Pts',(-0.290553549488137,-1.48484308526585,
-12.7644002895768));
#410915=CARTESIAN_POINT('Ctrl Pts',(-0.0923424899387176,-1.51017590176458,
-12.7547254940565));
#410916=CARTESIAN_POINT('Ctrl Pts',(0.296492136046974,-1.48287582776257,
-12.7352593440023));
#410917=CARTESIAN_POINT('Ctrl Pts',(0.483553291929648,-1.43282385304763,
-12.7248690273126));
#410918=CARTESIAN_POINT('Ctrl Pts',(0.835393916110487,-1.26169561153856,
-12.7031875251249));
#410919=CARTESIAN_POINT('Ctrl Pts',(0.995541605556879,-1.13959079644599,
-12.6920906154047));
#410920=CARTESIAN_POINT('Ctrl Pts',(1.25381344303546,-0.8454676424949,-12.6714944182206));
#410921=CARTESIAN_POINT('Ctrl Pts',(1.35161198790032,-0.678239112822272,
-12.6626799507123));
#410922=CARTESIAN_POINT('Ctrl Pts',(1.47956707389454,-0.313945143036675,
-12.6424413968353));
#410923=CARTESIAN_POINT('Ctrl Pts',(1.50773153685902,-0.120058126980392,
-12.6316698959433));
#410924=CARTESIAN_POINT('Ctrl Pts',(1.48840274776665,0.272379766589699,
-12.6098677907449));
#410925=CARTESIAN_POINT('Ctrl Pts',(1.43923156534188,0.467083856763257,
-12.5990508968464));
#410926=CARTESIAN_POINT('Ctrl Pts',(1.2716553361612,0.817895896734298,-12.5795613390702));
#410927=CARTESIAN_POINT('Ctrl Pts',(1.15801103262477,0.972156887553523,
-12.5703771404632));
#410928=CARTESIAN_POINT('Ctrl Pts',(0.874438668330924,1.23446705149296,
-12.5494473652821));
#410929=CARTESIAN_POINT('Ctrl Pts',(0.705518706497666,1.33820509943847,
-12.5384385873862));
#410930=CARTESIAN_POINT('Ctrl Pts',(0.354347959586764,1.46839643927147,
-12.5179264508413));
#410931=CARTESIAN_POINT('Ctrl Pts',(0.177787084102027,1.50000000000007,
-12.508553785072));
#410932=CARTESIAN_POINT('Ctrl Pts',(-7.95891130778159E-14,1.50000000000006,
-12.5));
#410933=CARTESIAN_POINT('Origin',(0.,2.5406128344257E-15,14.));
#410934=CARTESIAN_POINT('',(1.24121291263909E-13,1.50000000000006,-11.9375));
#410935=CARTESIAN_POINT('',(7.83583777527795E-15,1.50000000000006,-12.));
#410936=CARTESIAN_POINT('',(-1.8369701987211E-16,1.50000000000006,14.));
#410937=CARTESIAN_POINT('Ctrl Pts',(2.4842627954769E-13,1.50000000000006,
-11.9375));
#410938=CARTESIAN_POINT('Ctrl Pts',(0.0429770385529035,1.50000000000006,
-11.9395677337315));
#410939=CARTESIAN_POINT('Ctrl Pts',(0.0860016566600157,1.49815305830009,
-11.9416890605714));
#410940=CARTESIAN_POINT('Ctrl Pts',(0.320455096552336,1.47792193396156,
-11.9535311826337));
#410941=CARTESIAN_POINT('Ctrl Pts',(0.506977512895046,1.42474532959968,
-11.963982374473));
#410942=CARTESIAN_POINT('Ctrl Pts',(0.856509125031369,1.24751244453871,
-11.9857223576989));
#410943=CARTESIAN_POINT('Ctrl Pts',(1.01484528553922,1.12249598149265,-11.9968129893023));
#410944=CARTESIAN_POINT('Ctrl Pts',(1.26788852442334,0.824089509044983,
-12.0172766064886));
#410945=CARTESIAN_POINT('Ctrl Pts',(1.3626114035016,0.65571019094691,-12.0260716560585));
#410946=CARTESIAN_POINT('Ctrl Pts',(1.48456931942257,0.289578440662951,
-12.0464123088521));
#410947=CARTESIAN_POINT('Ctrl Pts',(1.50956256359297,0.0949313160154064,
-12.0572260379991));
#410948=CARTESIAN_POINT('Ctrl Pts',(1.48359916209213,-0.29742169655306,
-12.0790234275863));
#410949=CARTESIAN_POINT('Ctrl Pts',(1.4311600520702,-0.491253205265574,
-12.089791844737));
#410950=CARTESIAN_POINT('Ctrl Pts',(1.25771526043269,-0.839171630783029,
-12.1091206461546));
#410951=CARTESIAN_POINT('Ctrl Pts',(1.1414919566941,-0.991502066499563,
-12.1184550000298));
#410952=CARTESIAN_POINT('Ctrl Pts',(0.853295509986717,-1.24922733560828,
-12.13947989329));
#410953=CARTESIAN_POINT('Ctrl Pts',(0.682325569135146,-1.35022705898739,
-12.1505112362762));
#410954=CARTESIAN_POINT('Ctrl Pts',(0.309210501082249,-1.48117904653476,
-12.1721002985674));
#410955=CARTESIAN_POINT('Ctrl Pts',(0.110499711440047,-1.50906111074809,
-12.1819318826338));
#410956=CARTESIAN_POINT('Ctrl Pts',(-0.279204309035193,-1.48619976188739,
-12.2013165635293));
#410957=CARTESIAN_POINT('Ctrl Pts',(-0.466621070585969,-1.43839788599238,
-12.2116614865596));
#410958=CARTESIAN_POINT('Ctrl Pts',(-0.820058580331773,-1.27167812486944,
-12.2332973611513));
#410959=CARTESIAN_POINT('Ctrl Pts',(-0.98147757103943,-1.15168288128523,
-12.2443968371735));
#410960=CARTESIAN_POINT('Ctrl Pts',(-1.24349615035991,-0.860663422680281,
-12.2650870857989));
#410961=CARTESIAN_POINT('Ctrl Pts',(-1.34351447886236,-0.694256212190225,
-12.2739302104339));
#410962=CARTESIAN_POINT('Ctrl Pts',(-1.47575101472088,-0.331289623800945,
-12.2940950208999));
#410963=CARTESIAN_POINT('Ctrl Pts',(-1.50616850407291,-0.137976327667566,
-12.3048346484629));
#410964=CARTESIAN_POINT('Ctrl Pts',(-1.49157364495768,0.254453151885936,
-12.3266362862159));
#410965=CARTESIAN_POINT('Ctrl Pts',(-1.44474483714684,0.449745590823751,
-12.3374858661569));
#410966=CARTESIAN_POINT('Ctrl Pts',(-1.28137026340723,0.802602783636924,
-12.3570890435354));
#410967=CARTESIAN_POINT('Ctrl Pts',(-1.16955280914026,0.958249070463121,
-12.3661812273027));
#410968=CARTESIAN_POINT('Ctrl Pts',(-0.8892670011538,1.22379091712043,-12.3870426469341));
#410969=CARTESIAN_POINT('Ctrl Pts',(-0.721825367529755,1.32944528069627,
-12.3980335297206));
#410970=CARTESIAN_POINT('Ctrl Pts',(-0.366722866655218,1.46612261404421,
-12.4189149993528));
#410971=CARTESIAN_POINT('Ctrl Pts',(-0.184066879677061,1.50000000000006,
-12.4286440781225));
#410972=CARTESIAN_POINT('Ctrl Pts',(1.85962356624714E-14,1.50000000000006,
-12.4375));
#410973=CARTESIAN_POINT('Ctrl Pts',(-7.96238075473389E-14,1.50000000000006,
-12.5));
#410974=CARTESIAN_POINT('Ctrl Pts',(-0.021657246306187,1.50000000000006,
-12.4989580152512));
#410975=CARTESIAN_POINT('Ctrl Pts',(-0.0433314544011003,1.49953096835747,
-12.4979021857713));
#410976=CARTESIAN_POINT('Ctrl Pts',(-0.256228705129635,1.49029566327074,
-12.4874026257674));
#410977=CARTESIAN_POINT('Ctrl Pts',(-0.444075622041309,1.44547885186977,
-12.4771199253358));
#410978=CARTESIAN_POINT('Ctrl Pts',(-0.799546902645559,1.28462353593294,
-12.4555491021532));
#410979=CARTESIAN_POINT('Ctrl Pts',(-0.962609755641049,1.16744345672824,
-12.4444487347804));
#410980=CARTESIAN_POINT('Ctrl Pts',(-1.22957527214838,0.880569908863771,
-12.4236356407158));
#410981=CARTESIAN_POINT('Ctrl Pts',(-1.33254855999195,0.715241436593647,
-12.4147356353662));
#410982=CARTESIAN_POINT('Ctrl Pts',(-1.47041968409356,0.354043071868654,
-12.3946690595482));
#410983=CARTESIAN_POINT('Ctrl Pts',(-1.50378740274652,0.161523925225723,
-12.3839735514014));
#410984=CARTESIAN_POINT('Ctrl Pts',(-1.4954171406393,-0.230806974685007,
-12.3621773902952));
#410985=CARTESIAN_POINT('Ctrl Pts',(-1.45168177601164,-0.42682950454516,
-12.3512872497474));
#410986=CARTESIAN_POINT('Ctrl Pts',(-1.293852642627,-0.782351512525683,
-12.3315360270818));
#410987=CARTESIAN_POINT('Ctrl Pts',(-1.18442272180316,-0.93983065716822,
-12.3225458242953));
#410988=CARTESIAN_POINT('Ctrl Pts',(-0.908443732773366,-1.20957450506437,
-12.301774894331));
#410989=CARTESIAN_POINT('Ctrl Pts',(-0.742965177194812,-1.31770197949868,
-12.2908097626571));
#410990=CARTESIAN_POINT('Ctrl Pts',(-0.376990871830196,-1.46540920331455,
-12.2690988372412));
#410991=CARTESIAN_POINT('Ctrl Pts',(-0.179674896831448,-1.50240134587015,
-12.2587113165562));
#410992=CARTESIAN_POINT('Ctrl Pts',(0.209843827240239,-1.49745737468072,
-12.2398332556734));
#410993=CARTESIAN_POINT('Ctrl Pts',(0.398413433063471,-1.45864864120757,
-12.2296826759089));
#410994=CARTESIAN_POINT('Ctrl Pts',(0.757686743020997,-1.3096518332869,
-12.2082583305042));
#410995=CARTESIAN_POINT('Ctrl Pts',(0.923911465244628,-1.19819476089986,
-12.1971648100389));
#410996=CARTESIAN_POINT('Ctrl Pts',(1.20075829432931,-0.919774214948045,
-12.17611110671));
#410997=CARTESIAN_POINT('Ctrl Pts',(1.30972221446346,-0.756588576841831,
-12.1670326987134));
#410998=CARTESIAN_POINT('Ctrl Pts',(1.45879219593834,-0.398976183610319,
-12.1471653435339));
#410999=CARTESIAN_POINT('Ctrl Pts',(1.49796783200108,-0.208165256817152,
-12.1365647364898));
#411000=CARTESIAN_POINT('Ctrl Pts',(1.50195600485459,0.185450445196111,
-12.1146971974891));
#411001=CARTESIAN_POINT('Ctrl Pts',(1.46370705882602,0.38450287225785,-12.103638729319));
#411002=CARTESIAN_POINT('Ctrl Pts',(1.31503358379335,0.746295760438966,
-12.08353912442));
#411003=CARTESIAN_POINT('Ctrl Pts',(1.20977572079829,0.907038528106464,
-12.0746765135022));
#411004=CARTESIAN_POINT('Ctrl Pts',(0.941346093386267,1.18406121176143,
-12.0540666124858));
#411005=CARTESIAN_POINT('Ctrl Pts',(0.779375800537106,1.29641804195596,
-12.0431527900767));
#411006=CARTESIAN_POINT('Ctrl Pts',(0.418306890734359,1.45413978895109,
-12.0213996944154));
#411007=CARTESIAN_POINT('Ctrl Pts',(0.222131420495649,1.49672539385334,
-12.0107782642334));
#411008=CARTESIAN_POINT('Ctrl Pts',(0.0155552563317659,1.49993952719833,
-12.0007500824192));
#411009=CARTESIAN_POINT('Ctrl Pts',(0.00777642948193762,1.50000000000006,
-12.0003741436379));
#411010=CARTESIAN_POINT('Ctrl Pts',(1.91097138113612E-14,1.50000000000006,
-12.));
#411011=CARTESIAN_POINT('Origin',(0.,2.5406128344257E-15,14.));
#411012=CARTESIAN_POINT('',(0.,1.50000000000006,-11.4375));
#411013=CARTESIAN_POINT('',(9.54567205468683E-14,1.50000000000006,-11.5));
#411014=CARTESIAN_POINT('',(-1.8369701987211E-16,1.50000000000006,14.));
#411015=CARTESIAN_POINT('Ctrl Pts',(-9.19750386962903E-13,1.50000000000006,
-11.4375));
#411016=CARTESIAN_POINT('Ctrl Pts',(0.130329120553406,1.50000000000014,
-11.4437704627362));
#411017=CARTESIAN_POINT('Ctrl Pts',(0.26015361750193,1.48301567758715,-11.4504884334916));
#411018=CARTESIAN_POINT('Ctrl Pts',(0.516680461991447,1.41466440933564,
-11.464729233392));
#411019=CARTESIAN_POINT('Ctrl Pts',(0.641864718321054,1.36243900991012,
-11.4722028692724));
#411020=CARTESIAN_POINT('Ctrl Pts',(0.929939979719385,1.19363353633602,
-11.4907519376813));
#411021=CARTESIAN_POINT('Ctrl Pts',(1.07984591957781,1.0599528663692,-11.501677642519));
#411022=CARTESIAN_POINT('Ctrl Pts',(1.31358155055579,0.748798092663026,
-11.5215664414662));
#411023=CARTESIAN_POINT('Ctrl Pts',(1.39786282863566,0.576352382580591,
-11.53048042319));
#411024=CARTESIAN_POINT('Ctrl Pts',(1.49886862959217,0.204015777895458,
-11.5511657901169));
#411025=CARTESIAN_POINT('Ctrl Pts',(1.51267080067798,0.00711890021125362,
-11.5621045055438));
#411026=CARTESIAN_POINT('Ctrl Pts',(1.46355675398347,-0.384053847316768,
-11.5838363248509));
#411027=CARTESIAN_POINT('Ctrl Pts',(1.39985149987318,-0.574402771986881,
-11.5944112651104));
#411028=CARTESIAN_POINT('Ctrl Pts',(1.20606174238502,-0.911964039249115,
-11.6131646688472));
#411029=CARTESIAN_POINT('Ctrl Pts',(1.08062285433907,-1.05762666739877,
-11.6232203605518));
#411030=CARTESIAN_POINT('Ctrl Pts',(0.77609634100543,-1.29877885517542,
-11.6445705711385));
#411031=CARTESIAN_POINT('Ctrl Pts',(0.598186717455987,-1.3897227112928,
-11.6556564701179));
#411032=CARTESIAN_POINT('Ctrl Pts',(0.219887652524674,-1.49658312679679,
-11.6768257372407));
#411033=CARTESIAN_POINT('Ctrl Pts',(0.0234993071507874,-1.51246494816405,
-11.6860231404975));
#411034=CARTESIAN_POINT('Ctrl Pts',(-0.361925055423086,-1.46838628355445,
-11.7057912861381));
#411035=CARTESIAN_POINT('Ctrl Pts',(-0.547387505842392,-1.4097863714055,
-11.7163421277817));
#411036=CARTESIAN_POINT('Ctrl Pts',(-0.892657118595693,-1.22200577535338,
-11.7381700474387));
#411037=CARTESIAN_POINT('Ctrl Pts',(-1.04772076955362,-1.09198521825952,
-11.7492422329653));
#411038=CARTESIAN_POINT('Ctrl Pts',(-1.29160959565064,-0.786212353699829,
-11.7694700302642));
#411039=CARTESIAN_POINT('Ctrl Pts',(-1.38100924390979,-0.6157939870204,
-11.7782892229433));
#411040=CARTESIAN_POINT('Ctrl Pts',(-1.49240059316123,-0.24649002818514,
-11.7988061095453));
#411041=CARTESIAN_POINT('Ctrl Pts',(-1.5117689175907,-0.0506288538669847,
-11.8096872858963));
#411042=CARTESIAN_POINT('Ctrl Pts',(-1.47411867367302,0.341300262638134,
-11.8314611257021));
#411043=CARTESIAN_POINT('Ctrl Pts',(-1.41596555384023,0.533458715529244,
-11.8421365953072));
#411044=CARTESIAN_POINT('Ctrl Pts',(-1.23222972897185,0.876200481622434,
-11.8611778045346));
#411045=CARTESIAN_POINT('Ctrl Pts',(-1.11140103543713,1.02515495807662,
-11.8708375526976));
#411046=CARTESIAN_POINT('Ctrl Pts',(-0.815001814868391,1.27463261018898,
-11.8920280016271));
#411047=CARTESIAN_POINT('Ctrl Pts',(-0.640485714472906,1.37065535694332,
-11.9030917099432));
#411048=CARTESIAN_POINT('Ctrl Pts',(-0.305798716040215,1.47652567288713,
-11.9221351877727));
#411049=CARTESIAN_POINT('Ctrl Pts',(-0.153233117418503,1.50000000000006,
-11.9301275682008));
#411050=CARTESIAN_POINT('Ctrl Pts',(2.49522624784504E-13,1.50000000000006,
-11.9375));
#411051=CARTESIAN_POINT('Ctrl Pts',(1.96370697480575E-14,1.50000000000006,
-12.));
#411052=CARTESIAN_POINT('Ctrl Pts',(-0.182328550940932,1.50000000000006,
-11.9912277135028));
#411053=CARTESIAN_POINT('Ctrl Pts',(-0.363251579039296,1.46675784955459,
-11.9815996571869));
#411054=CARTESIAN_POINT('Ctrl Pts',(-0.718522420562673,1.33145425339341,
-11.9607482476278));
#411055=CARTESIAN_POINT('Ctrl Pts',(-0.887482234234511,1.22532586195463,
-11.949671153929));
#411056=CARTESIAN_POINT('Ctrl Pts',(-1.17333378627438,0.954820941023825,
-11.9284040891377));
#411057=CARTESIAN_POINT('Ctrl Pts',(-1.28786816289331,0.793586004890666,
-11.9190881113828));
#411058=CARTESIAN_POINT('Ctrl Pts',(-1.44708864380716,0.439306103519968,
-11.89940589464));
#411059=CARTESIAN_POINT('Ctrl Pts',(-1.49145651876931,0.250189188814036,
-11.8888993993785));
#411060=CARTESIAN_POINT('Ctrl Pts',(-1.50660286706077,-0.142032459715299,
-11.8671093077936));
#411061=CARTESIAN_POINT('Ctrl Pts',(-1.47425057730889,-0.341504197234316,
-11.8560275445981));
#411062=CARTESIAN_POINT('Ctrl Pts',(-1.3363660810813,-0.707550522178523,
-11.8356916376567));
#411063=CARTESIAN_POINT('Ctrl Pts',(-1.23549743422695,-0.871808664519378,
-11.8268926573384));
#411064=CARTESIAN_POINT('Ctrl Pts',(-0.975027265118679,-1.15639102726546,
-11.8064557148523));
#411065=CARTESIAN_POINT('Ctrl Pts',(-0.816841961747075,-1.27305859663344,
-11.7956042550796));
#411066=CARTESIAN_POINT('Ctrl Pts',(-0.461060686783883,-1.44115980884466,
-11.7738172423899));
#411067=CARTESIAN_POINT('Ctrl Pts',(-0.266191369136677,-1.48952496009485,
-11.7630981115496));
#411068=CARTESIAN_POINT('Ctrl Pts',(0.122211266267834,-1.50703124582293,
-11.7439247953262));
#411069=CARTESIAN_POINT('Ctrl Pts',(0.311899438227977,-1.4794688418196,
-11.7344234213321));
#411070=CARTESIAN_POINT('Ctrl Pts',(0.677562252474723,-1.35267066814931,
-11.7133082894881));
#411071=CARTESIAN_POINT('Ctrl Pts',(0.849164217990212,-1.25208995182803,
-11.7022581772861));
#411072=CARTESIAN_POINT('Ctrl Pts',(1.14420642225097,-0.989889976456594,
-11.6807796199659));
#411073=CARTESIAN_POINT('Ctrl Pts',(1.26454579811548,-0.830658622661461,
-11.671147701259));
#411074=CARTESIAN_POINT('Ctrl Pts',(1.43408482697798,-0.479847056524478,
-11.6516581698069));
#411075=CARTESIAN_POINT('Ctrl Pts',(1.48365214893905,-0.292589613456167,
-11.6412549785253));
#411076=CARTESIAN_POINT('Ctrl Pts',(1.51003368203839,0.0979048979622877,
-11.6195608390021));
#411077=CARTESIAN_POINT('Ctrl Pts',(1.48364921311269,0.297630447443781,
-11.608464975142));
#411078=CARTESIAN_POINT('Ctrl Pts',(1.35675031906872,0.667868610533521,
-11.5878961883037));
#411079=CARTESIAN_POINT('Ctrl Pts',(1.26029844307481,0.835743730818598,
-11.5790877001469));
#411080=CARTESIAN_POINT('Ctrl Pts',(1.00783525764039,1.12781802743597,-11.5588278845682));
#411081=CARTESIAN_POINT('Ctrl Pts',(0.853538474200204,1.24866561166777,
-11.5480473997739));
#411082=CARTESIAN_POINT('Ctrl Pts',(0.503332749649789,1.42695064705156,
-11.5262457569015));
#411083=CARTESIAN_POINT('Ctrl Pts',(0.309941789457643,1.48104345618317,
-11.5154386519596));
#411084=CARTESIAN_POINT('Ctrl Pts',(0.074421646781362,1.49861678005269,
-11.5036190359265));
#411085=CARTESIAN_POINT('Ctrl Pts',(0.0371922855396213,1.50000000000006,
-11.5017894146723));
#411086=CARTESIAN_POINT('Ctrl Pts',(1.91097138113609E-13,1.50000000000006,
-11.5));
#411087=CARTESIAN_POINT('Origin',(0.,2.5406128344257E-15,14.));
#411088=CARTESIAN_POINT('',(-1.27489940585681E-13,1.50000000000006,-10.9375));
#411089=CARTESIAN_POINT('',(5.40523406222535E-14,1.50000000000006,-11.));
#411090=CARTESIAN_POINT('',(-1.8369701987211E-16,1.50000000000006,14.));
#411091=CARTESIAN_POINT('Ctrl Pts',(-2.56114573993216E-13,1.50000000000006,
-10.9375));
#411092=CARTESIAN_POINT('Ctrl Pts',(0.15246223475462,1.50000000000008,-10.9448353426897));
#411093=CARTESIAN_POINT('Ctrl Pts',(0.304271509779819,1.47676131292171,
-10.9527847889253));
#411094=CARTESIAN_POINT('Ctrl Pts',(0.638415184845918,1.37162524087191,
-10.9717817304334));
#411095=CARTESIAN_POINT('Ctrl Pts',(0.813101815135945,1.27585000938268,
-10.9828467679488));
#411096=CARTESIAN_POINT('Ctrl Pts',(1.1099025941224,1.02678001623993,-11.0040452130064));
#411097=CARTESIAN_POINT('Ctrl Pts',(1.23095788496071,0.877989340494405,
-11.013722814417));
#411098=CARTESIAN_POINT('Ctrl Pts',(1.41519370737247,0.535502360679354,
-11.0327498688511));
#411099=CARTESIAN_POINT('Ctrl Pts',(1.47362374455104,0.343429821589083,
-11.0434205654673));
#411100=CARTESIAN_POINT('Ctrl Pts',(1.51184320099172,-0.0484697043042123,
-11.0651927613502));
#411101=CARTESIAN_POINT('Ctrl Pts',(1.49275011288303,-0.244385935541777,
-11.076076996419));
#411102=CARTESIAN_POINT('Ctrl Pts',(1.38187379427068,-0.613842289581186,
-11.0966023494212));
#411103=CARTESIAN_POINT('Ctrl Pts',(1.29273054755267,-0.784360605764299,
-11.1054246004696));
#411104=CARTESIAN_POINT('Ctrl Pts',(1.04928595722263,-1.09048672473935,
-11.1256408370878));
#411105=CARTESIAN_POINT('Ctrl Pts',(0.894384273913469,-1.22074701582039,
-11.1367118892198));
#411106=CARTESIAN_POINT('Ctrl Pts',(0.549328415459523,-1.40903475174676,
-11.1585436118369));
#411107=CARTESIAN_POINT('Ctrl Pts',(0.363921115990155,-1.46789621378336,
-11.1690990653039));
#411108=CARTESIAN_POINT('Ctrl Pts',(-0.0213961478304139,-1.51248668470138,
-11.1888762749953));
#411109=CARTESIAN_POINT('Ctrl Pts',(-0.217730804231609,-1.49688877070679,
-11.1980620012388));
#411110=CARTESIAN_POINT('Ctrl Pts',(-0.596145126370211,-1.39060384306678,
-11.2192208279025));
#411111=CARTESIAN_POINT('Ctrl Pts',(-0.774213802494401,-1.29990630406645,
-11.2303075371604));
#411112=CARTESIAN_POINT('Ctrl Pts',(-1.07912867173849,-1.05915598008962,
-11.2516652696463));
#411113=CARTESIAN_POINT('Ctrl Pts',(-1.20478920020793,-0.913649509470577,
-11.2617416939183));
#411114=CARTESIAN_POINT('Ctrl Pts',(-1.39905600226516,-0.576337019190607,
-11.2804812767116));
#411115=CARTESIAN_POINT('Ctrl Pts',(-1.46302376087178,-0.386078227174812,
-11.2910512096014));
#411116=CARTESIAN_POINT('Ctrl Pts',(-1.51268251626141,0.00505016793965425,
-11.3127805648855));
#411117=CARTESIAN_POINT('Ctrl Pts',(-1.49914603176655,0.201992420713084,
-11.3237218011507));
#411118=CARTESIAN_POINT('Ctrl Pts',(-1.39863454333612,0.574471234174373,
-11.3444150685652));
#411119=CARTESIAN_POINT('Ctrl Pts',(-1.31459423506811,0.747014100127693,
-11.3533352803792));
#411120=CARTESIAN_POINT('Ctrl Pts',(-1.08129627686726,1.05847310449937,
-11.3732114726369));
#411121=CARTESIAN_POINT('Ctrl Pts',(-0.931574318326271,1.19235826159576,
-11.3841340058674));
#411122=CARTESIAN_POINT('Ctrl Pts',(-0.643429812963329,1.36173533849175,
-11.4027022836482));
#411123=CARTESIAN_POINT('Ctrl Pts',(-0.517971561185671,1.41422566649052,
-11.4101964612678));
#411124=CARTESIAN_POINT('Ctrl Pts',(-0.260825662036353,1.48292743037495,
-11.4244767814392));
#411125=CARTESIAN_POINT('Ctrl Pts',(-0.130667240233891,1.50000000000014,
-11.4312132694731));
#411126=CARTESIAN_POINT('Ctrl Pts',(9.27764809421916E-13,1.50000000000006,
-11.4375));
#411127=CARTESIAN_POINT('Ctrl Pts',(1.91097138113609E-13,1.50000000000006,
-11.5));
#411128=CARTESIAN_POINT('Ctrl Pts',(-0.152179298203859,1.50000000000006,
-11.4926782701014));
#411129=CARTESIAN_POINT('Ctrl Pts',(-0.303676254544889,1.47684734021558,
-11.4847462399525));
#411130=CARTESIAN_POINT('Ctrl Pts',(-0.636699084008757,1.37229479658189,
-11.4658194342763));
#411131=CARTESIAN_POINT('Ctrl Pts',(-0.810725317540163,1.27722399917584,
-11.4548057377282));
#411132=CARTESIAN_POINT('Ctrl Pts',(-1.11472321897743,1.023353851667,-11.4331276833339));
#411133=CARTESIAN_POINT('Ctrl Pts',(-1.24084474511904,0.866101820708982,
-11.4231167678172));
#411134=CARTESIAN_POINT('Ctrl Pts',(-1.42041058582733,0.518739623571149,
-11.4038188679762));
#411135=CARTESIAN_POINT('Ctrl Pts',(-1.47494686773213,0.333417035429076,
-11.3935231686349));
#411136=CARTESIAN_POINT('Ctrl Pts',(-1.51212516926065,-0.0551064641573005,
-11.371938529769));
#411137=CARTESIAN_POINT('Ctrl Pts',(-1.49150504579564,-0.254913980230995,
-11.3608381122094));
#411138=CARTESIAN_POINT('Ctrl Pts',(-1.37529802672603,-0.629097571714455,
-11.3400501349048));
#411139=CARTESIAN_POINT('Ctrl Pts',(-1.28310967384223,-0.800522046839755,
-11.3311635861094));
#411140=CARTESIAN_POINT('Ctrl Pts',(-1.03834424508844,-1.09970222827409,
-11.3110767433324));
#411141=CARTESIAN_POINT('Ctrl Pts',(-0.887855420222202,-1.22441934816545,
-11.3003719819287));
#411142=CARTESIAN_POINT('Ctrl Pts',(-0.543238920911026,-1.41224451967927,
-11.2785742469997));
#411143=CARTESIAN_POINT('Ctrl Pts',(-0.351419082558947,-1.47175647476156,
-11.2676922008605));
#411144=CARTESIAN_POINT('Ctrl Pts',(0.0354848897897921,-1.51157456061957,
-11.2479712168712));
#411145=CARTESIAN_POINT('Ctrl Pts',(0.226498491371865,-1.49493353218255,
-11.2389618510358));
#411146=CARTESIAN_POINT('Ctrl Pts',(0.597791346128348,-1.38960800183643,
-11.218172306056));
#411147=CARTESIAN_POINT('Ctrl Pts',(0.773938384141673,-1.29976144194085,
-11.2072016899633));
#411148=CARTESIAN_POINT('Ctrl Pts',(1.08409107868713,-1.0556017091574,-11.18549724669));
#411149=CARTESIAN_POINT('Ctrl Pts',(1.2142845463122,-0.902779300458576,
-11.175154405581));
#411150=CARTESIAN_POINT('Ctrl Pts',(1.40366694131897,-0.562277595161398,
-11.1562376441756));
#411151=CARTESIAN_POINT('Ctrl Pts',(1.46374313140388,-0.379301091450682,
-11.1460722828584));
#411152=CARTESIAN_POINT('Ctrl Pts',(1.51303027236692,0.00664128631009762,
-11.1246310396494));
#411153=CARTESIAN_POINT('Ctrl Pts',(1.49891009334133,0.206348046807697,
-11.1135362196218));
#411154=CARTESIAN_POINT('Ctrl Pts',(1.39487942862602,0.584852432951371,
-11.0925081981694));
#411155=CARTESIAN_POINT('Ctrl Pts',(1.30751165546829,0.760360591944268,
-11.0834532229671));
#411156=CARTESIAN_POINT('Ctrl Pts',(1.07140318405049,1.06741553266847,-11.0635641449305));
#411157=CARTESIAN_POINT('Ctrl Pts',(0.925266340380091,1.19630551001658,
-11.0529528556127));
#411158=CARTESIAN_POINT('Ctrl Pts',(0.585586951813232,1.39548565578919,
-11.0310772415834));
#411159=CARTESIAN_POINT('Ctrl Pts',(0.393779769791798,1.46124850900595,
-11.020022168313));
#411160=CARTESIAN_POINT('Ctrl Pts',(0.130016188590412,1.49577813346715,
-11.0063726808605));
#411161=CARTESIAN_POINT('Ctrl Pts',(0.0649794055432486,1.50000000000006,
-11.0031263231068));
#411162=CARTESIAN_POINT('Ctrl Pts',(1.08288378264379E-13,1.50000000000006,
-11.));
#411163=CARTESIAN_POINT('Origin',(0.,2.5406128344257E-15,14.));
#411164=CARTESIAN_POINT('',(-1.92015623212974E-14,1.50000000000006,-10.4375));
#411165=CARTESIAN_POINT('',(6.27805609385103E-15,1.50000000000006,-10.5));
#411166=CARTESIAN_POINT('',(-1.8369701987211E-16,1.50000000000006,14.));
#411167=CARTESIAN_POINT('Ctrl Pts',(-3.67067487516692E-14,1.50000000000006,
-10.4375));
#411168=CARTESIAN_POINT('Ctrl Pts',(0.183341851414791,1.50000000000006,
-10.446321038939));
#411169=CARTESIAN_POINT('Ctrl Pts',(0.365304389821094,1.46638951329501,
-10.4560093402806));
#411170=CARTESIAN_POINT('Ctrl Pts',(0.719975731075,1.33045184597326,-10.4768495194574));
#411171=CARTESIAN_POINT('Ctrl Pts',(0.887586608293778,1.22501447146067,
-10.4878425175062));
#411172=CARTESIAN_POINT('Ctrl Pts',(1.16824672940074,0.959839578059451,
-10.50871175314));
#411173=CARTESIAN_POINT('Ctrl Pts',(1.28027201600136,0.804351637745947,
-10.517813797903));
#411174=CARTESIAN_POINT('Ctrl Pts',(1.44412642835151,0.451726875043387,
-10.5374040624976));
#411175=CARTESIAN_POINT('Ctrl Pts',(1.49122282301231,0.256500091922007,
-10.5482499948932));
#411176=CARTESIAN_POINT('Ctrl Pts',(1.50635756973098,-0.135933250839795,
-10.5700518472689));
#411177=CARTESIAN_POINT('Ctrl Pts',(1.47619662265256,-0.32931329751153,
-10.5807951831951));
#411178=CARTESIAN_POINT('Ctrl Pts',(1.34444850226405,-0.69243201844072,
-10.6009684454689));
#411179=CARTESIAN_POINT('Ctrl Pts',(1.24468450252906,-0.85893283475972,
-10.6098076676941));
#411180=CARTESIAN_POINT('Ctrl Pts',(0.983093886227757,-1.15030836951905,
-10.6304872169434));
#411181=CARTESIAN_POINT('Ctrl Pts',(0.821818972027301,-1.27054556457984,
-10.6415864819557));
#411182=CARTESIAN_POINT('Ctrl Pts',(0.468561415029391,-1.4377703342,-10.6632277265806));
#411183=CARTESIAN_POINT('Ctrl Pts',(0.281183978764755,-1.48582969927626,
-10.6735779100495));
#411184=CARTESIAN_POINT('Ctrl Pts',(-0.108421139476547,-1.50919956519595,
-10.6929719579829));
#411185=CARTESIAN_POINT('Ctrl Pts',(-0.307074366045606,-1.48161063819315,
-10.7027849379306));
#411186=CARTESIAN_POINT('Ctrl Pts',(-0.680323335747035,-1.35124120973445,
-10.7243642603709));
#411187=CARTESIAN_POINT('Ctrl Pts',(-0.851467393385639,-1.25047857568158,
-10.7353973947403));
#411188=CARTESIAN_POINT('Ctrl Pts',(-1.14006036034653,-0.993148583284006,
-10.7564303856814));
#411189=CARTESIAN_POINT('Ctrl Pts',(-1.25650534277258,-0.840982730153672,
-10.7657787372137));
#411190=CARTESIAN_POINT('Ctrl Pts',(-1.43045107049838,-0.493313284731216,
-10.7850937064038));
#411191=CARTESIAN_POINT('Ctrl Pts',(-1.48316886680921,-0.299559002937378,
-10.7958578331701));
#411192=CARTESIAN_POINT('Ctrl Pts',(-1.50969970494823,0.0927815138316741,
-10.8176545285462));
#411193=CARTESIAN_POINT('Ctrl Pts',(-1.48497842356764,0.287491265907305,
-10.8284717369948));
#411194=CARTESIAN_POINT('Ctrl Pts',(-1.36353336161468,0.653778980238932,
-10.8488210544577));
#411195=CARTESIAN_POINT('Ctrl Pts',(-1.26907168900137,0.822256806340053,
-10.8576155600706));
#411196=CARTESIAN_POINT('Ctrl Pts',(-1.01647448726449,1.12102612866584,
-10.8780677964479));
#411197=CARTESIAN_POINT('Ctrl Pts',(-0.858294843992598,1.24628920901697,
-10.889157748093));
#411198=CARTESIAN_POINT('Ctrl Pts',(-0.508964490595935,1.42404024301286,
-10.9109024412792));
#411199=CARTESIAN_POINT('Ctrl Pts',(-0.322490301199188,1.47748253414703,
-10.9213586929867));
#411200=CARTESIAN_POINT('Ctrl Pts',(-0.0873593104501269,1.49809429307222,
-10.9332439869127));
#411201=CARTESIAN_POINT('Ctrl Pts',(-0.0436554318174992,1.50000000000005,
-10.9353996270574));
#411202=CARTESIAN_POINT('Ctrl Pts',(-2.54796184151489E-13,1.50000000000006,
-10.9375));
#411203=CARTESIAN_POINT('Ctrl Pts',(1.08628384065668E-13,1.50000000000006,
-11.));
#411204=CARTESIAN_POINT('Ctrl Pts',(-0.124646908673343,1.50000000000006,
-10.9940029228103));
#411205=CARTESIAN_POINT('Ctrl Pts',(-0.249040797105659,1.48446746031111,
-10.9875865596269));
#411206=CARTESIAN_POINT('Ctrl Pts',(-0.559623546914417,1.40534011798786,
-10.9704456583784));
#411207=CARTESIAN_POINT('Ctrl Pts',(-0.737680680456972,1.32059828077476,
-10.9595249406239));
#411208=CARTESIAN_POINT('Ctrl Pts',(-1.05402417833964,1.08560316763031,
-10.9377772149539));
#411209=CARTESIAN_POINT('Ctrl Pts',(-1.18846144249417,0.936529206524611,
-10.9271681557025));
#411210=CARTESIAN_POINT('Ctrl Pts',(-1.38704353413505,0.601926838882839,
-10.9083193601514));
#411211=CARTESIAN_POINT('Ctrl Pts',(-1.45217349406124,0.421245189850194,
-10.8984025105472));
#411212=CARTESIAN_POINT('Ctrl Pts',(-1.51249416857681,0.0378826690716671,
-10.8771045927262));
#411213=CARTESIAN_POINT('Ctrl Pts',(-1.50431993816539,-0.161551377855926,
-10.8660249234525));
#411214=CARTESIAN_POINT('Ctrl Pts',(-1.41156072865313,-0.543887259640766,
-10.8447840411311));
#411215=CARTESIAN_POINT('Ctrl Pts',(-1.32863515419284,-0.723211201647225,
-10.8355014552816));
#411216=CARTESIAN_POINT('Ctrl Pts',(-1.10043927435011,-1.03735898530839,
-10.8157960485697));
#411217=CARTESIAN_POINT('Ctrl Pts',(-0.95833502546804,-1.16989583252076,
-10.8052774756184));
#411218=CARTESIAN_POINT('Ctrl Pts',(-0.625381252791918,-1.37802505171501,
-10.7834768625617));
#411219=CARTESIAN_POINT('Ctrl Pts',(-0.436129666690129,-1.44908952748857,
-10.7723974781641));
#411220=CARTESIAN_POINT('Ctrl Pts',(-0.0499634214048842,-1.51128177490525,
-10.7520904835969));
#411221=CARTESIAN_POINT('Ctrl Pts',(0.14261394883706,-1.50536798104238,
-10.7432875937719));
#411222=CARTESIAN_POINT('Ctrl Pts',(0.518993104954484,-1.42077123144426,
-10.7228291334691));
#411223=CARTESIAN_POINT('Ctrl Pts',(0.698905132383966,-1.3414422246146,
-10.7119695284904));
#411224=CARTESIAN_POINT('Ctrl Pts',(1.02161140091051,-1.11616616552023,
-10.6901856475987));
#411225=CARTESIAN_POINT('Ctrl Pts',(1.16040271940615,-0.971085200685996,
-10.6794780203732));
#411226=CARTESIAN_POINT('Ctrl Pts',(1.36858524807366,-0.642698786671831,
-10.6603399889589));
#411227=CARTESIAN_POINT('Ctrl Pts',(1.43891951287201,-0.464360061117776,
-10.6507977811732));
#411228=CARTESIAN_POINT('Ctrl Pts',(1.51056087056471,-0.0839233962982022,
-10.6296624109055));
#411229=CARTESIAN_POINT('Ctrl Pts',(1.50850992412876,0.115047782240133,
-10.6186084565422));
#411230=CARTESIAN_POINT('Ctrl Pts',(1.42751338067791,0.501204863537782,
-10.597155285359));
#411231=CARTESIAN_POINT('Ctrl Pts',(1.34921578399448,0.684542255947699,
-10.5875657786751));
#411232=CARTESIAN_POINT('Ctrl Pts',(1.12917766884718,1.00590001882789,-10.5680525853997));
#411233=CARTESIAN_POINT('Ctrl Pts',(0.991275930217928,1.14202854718277,
-10.5576364368965));
#411234=CARTESIAN_POINT('Ctrl Pts',(0.665412928738204,1.35905904241428,
-10.5359297210604));
#411235=CARTESIAN_POINT('Ctrl Pts',(0.478910239367815,1.43543475483331,
-10.5248350586672));
#411236=CARTESIAN_POINT('Ctrl Pts',(0.189462195571091,1.49102689087079,
-10.5093647571659));
#411237=CARTESIAN_POINT('Ctrl Pts',(0.0947355526073646,1.50000000000006,
-10.5045579664));
#411238=CARTESIAN_POINT('Ctrl Pts',(1.27398092075742E-14,1.50000000000006,
-10.5));
#411239=CARTESIAN_POINT('Origin',(0.,2.5406128344257E-15,14.));
#411240=CARTESIAN_POINT('',(6.27805609385103E-15,1.50000000000006,-9.93750000000001));
#411241=CARTESIAN_POINT('',(-5.74209899440205E-14,1.50000000000006,-9.99999999999997));
#411242=CARTESIAN_POINT('',(-1.8369701987211E-16,1.50000000000006,14.));
#411243=CARTESIAN_POINT('Ctrl Pts',(1.27398092075742E-14,1.50000000000006,
-9.93750000000001));
#411244=CARTESIAN_POINT('Ctrl Pts',(0.0130597123856812,1.50000000000006,
-9.93812833570512));
#411245=CARTESIAN_POINT('Ctrl Pts',(0.0261258122046185,1.49982944441199,
-9.93876171638113));
#411246=CARTESIAN_POINT('Ctrl Pts',(0.237959275893557,1.49429234528671,
-9.94910736696385));
#411247=CARTESIAN_POINT('Ctrl Pts',(0.433686462421857,1.4496292512905,-9.95976493711623));
#411248=CARTESIAN_POINT('Ctrl Pts',(0.792893421544092,1.28816466813327,
-9.98153241730482));
#411249=CARTESIAN_POINT('Ctrl Pts',(0.953519043999357,1.17424763864805,
-9.99242488309857));
#411250=CARTESIAN_POINT('Ctrl Pts',(1.21910047056181,0.894506588847375,
-10.0129732601584));
#411251=CARTESIAN_POINT('Ctrl Pts',(1.32278711632104,0.73251490178467,-10.0218047276788));
#411252=CARTESIAN_POINT('Ctrl Pts',(1.46761467127421,0.36919049735013,-10.041989416814));
#411253=CARTESIAN_POINT('Ctrl Pts',(1.50375821813677,0.169969130532061,
-10.0530572705261));
#411254=CARTESIAN_POINT('Ctrl Pts',(1.49577953643009,-0.22318446197286,
-10.0748991367764));
#411255=CARTESIAN_POINT('Ctrl Pts',(1.454743772956,-0.413406885805721,-10.0854670492116));
#411256=CARTESIAN_POINT('Ctrl Pts',(1.30205361502608,-0.769839727586497,
-10.1052688737549));
#411257=CARTESIAN_POINT('Ctrl Pts',(1.19111863148761,-0.932331192165051,
-10.1144237001276));
#411258=CARTESIAN_POINT('Ctrl Pts',(0.911065034014979,-1.20795688997008,
-10.1355540545017));
#411259=CARTESIAN_POINT('Ctrl Pts',(0.743850001404811,-1.31752856339574,
-10.1466428491044));
#411260=CARTESIAN_POINT('Ctrl Pts',(0.383419024228178,-1.4626367917708,
-10.1680148767007));
#411261=CARTESIAN_POINT('Ctrl Pts',(0.194654648445902,-1.49948343696352,
-10.178120324887));
#411262=CARTESIAN_POINT('Ctrl Pts',(-0.194671049551621,-1.50052739221325,
-10.1968807650223));
#411263=CARTESIAN_POINT('Ctrl Pts',(-0.391587058361149,-1.46157443191237,
-10.2074076180211));
#411264=CARTESIAN_POINT('Ctrl Pts',(-0.755882702683686,-1.31030645551807,
-10.2291366886138));
#411265=CARTESIAN_POINT('Ctrl Pts',(-0.92013529308169,-1.20067408870343,
-10.2400846385766));
#411266=CARTESIAN_POINT('Ctrl Pts',(-1.19345565040318,-0.92835447691962,
-10.2607992040601));
#411267=CARTESIAN_POINT('Ctrl Pts',(-1.30141473190726,-0.769733557604032,
-10.2697370245777));
#411268=CARTESIAN_POINT('Ctrl Pts',(-1.45579786117595,-0.412575577740146,
-10.2895791345702));
#411269=CARTESIAN_POINT('Ctrl Pts',(-1.4976105257064,-0.216125919194418,
-10.3004930044894));
#411270=CARTESIAN_POINT('Ctrl Pts',(-1.50212738741465,0.176094060945907,
-10.322283003386));
#411271=CARTESIAN_POINT('Ctrl Pts',(-1.46694025700791,0.368098920177736,
-10.33294994001));
#411272=CARTESIAN_POINT('Ctrl Pts',(-1.32557692878723,0.728189256860354,
-10.3529549587146));
#411273=CARTESIAN_POINT('Ctrl Pts',(-1.22075258050671,0.89284974055885,
-10.3619012291016));
#411274=CARTESIAN_POINT('Ctrl Pts',(-0.950712416699731,1.1771181175009,
-10.3827898863443));
#411275=CARTESIAN_POINT('Ctrl Pts',(-0.786648129094687,1.29253158841395,
-10.3938893628095));
#411276=CARTESIAN_POINT('Ctrl Pts',(-0.429956265913086,1.44971739568654,
-10.4154169805026));
#411277=CARTESIAN_POINT('Ctrl Pts',(-0.241864830797446,1.49267108033264,
-10.4256596918008));
#411278=CARTESIAN_POINT('Ctrl Pts',(-0.0338291921616082,1.49971408378776,
-10.4358644501162));
#411279=CARTESIAN_POINT('Ctrl Pts',(-0.0169091055322462,1.50000000000006,
-10.4366864602808));
#411280=CARTESIAN_POINT('Ctrl Pts',(-3.82194276227227E-14,1.50000000000006,
-10.4375));
#411281=CARTESIAN_POINT('Ctrl Pts',(1.27398092075742E-14,1.50000000000006,
-10.5));
#411282=CARTESIAN_POINT('Ctrl Pts',(-0.0961640021789709,1.50000000000006,
-10.4953733072879));
#411283=CARTESIAN_POINT('Ctrl Pts',(-0.192312189894884,1.49075428983337,
-10.4904905501673));
#411284=CARTESIAN_POINT('Ctrl Pts',(-0.477782555963758,1.43508007583453,
-10.4752093448316));
#411285=CARTESIAN_POINT('Ctrl Pts',(-0.659394616266541,1.36121942857362,
-10.4644198458601));
#411286=CARTESIAN_POINT('Ctrl Pts',(-0.988185935655053,1.14587042885574,
-10.4426189494716));
#411287=CARTESIAN_POINT('Ctrl Pts',(-1.13122500556002,1.00492903946411,
-10.4318219404179));
#411288=CARTESIAN_POINT('Ctrl Pts',(-1.34897707229762,0.682873836252697,
-10.4123993613552));
#411289=CARTESIAN_POINT('Ctrl Pts',(-1.42451113759172,0.506797536541834,
-10.4031554186968));
#411290=CARTESIAN_POINT('Ctrl Pts',(-1.5072744310769,0.129344161205523,
-10.3821857867337));
#411291=CARTESIAN_POINT('Ctrl Pts',(-1.51123947488267,-0.0689901135617249,
-10.3711672159133));
#411292=CARTESIAN_POINT('Ctrl Pts',(-1.44197477365096,-0.458773265628078,
-10.349512596354));
#411293=CARTESIAN_POINT('Ctrl Pts',(-1.36829696590876,-0.646139569010169,
-10.3395505637719));
#411294=CARTESIAN_POINT('Ctrl Pts',(-1.15629839165518,-0.974502057759996,
-10.3202295973694));
#411295=CARTESIAN_POINT('Ctrl Pts',(-1.02257339529214,-1.11400279948846,
-10.3099207298785));
#411296=CARTESIAN_POINT('Ctrl Pts',(-0.703835080463324,-1.33947840127368,
-10.2883222143955));
#411297=CARTESIAN_POINT('Ctrl Pts',(-0.520145363547979,-1.42093085883445,
-10.2772218705043));
#411298=CARTESIAN_POINT('Ctrl Pts',(-0.137752926488043,-1.50604856638516,
-10.2564596250329));
#411299=CARTESIAN_POINT('Ctrl Pts',(0.0566843765573322,-1.51127194686497,
-10.2475858812965));
#411300=CARTESIAN_POINT('Ctrl Pts',(0.437895743281651,-1.44767912219312,
-10.2274783735115));
#411301=CARTESIAN_POINT('Ctrl Pts',(0.62098502059929,-1.37909085880787,
-10.2167642570109));
#411302=CARTESIAN_POINT('Ctrl Pts',(0.955323109226357,-1.17341366981076,
-10.1949651529719));
#411303=CARTESIAN_POINT('Ctrl Pts',(1.10231620339654,-1.03656187644939,
-10.1840915057267));
#411304=CARTESIAN_POINT('Ctrl Pts',(1.32918637441208,-0.720672929449274,
-10.1644015165622));
#411305=CARTESIAN_POINT('Ctrl Pts',(1.40969808132489,-0.546689096092594,
-10.1553716164496));
#411306=CARTESIAN_POINT('Ctrl Pts',(1.50291696629879,-0.172135111132355,
-10.1345630617296));
#411307=CARTESIAN_POINT('Ctrl Pts',(1.5125272829466,0.0254350087036306,
-10.1235869439609));
#411308=CARTESIAN_POINT('Ctrl Pts',(1.45482028604201,0.415991217406076,
-10.1018893768108));
#411309=CARTESIAN_POINT('Ctrl Pts',(1.38692473639455,0.604931293171288,
-10.0915914671261));
#411310=CARTESIAN_POINT('Ctrl Pts',(1.18555560683619,0.938573083172626,
-10.072635262863));
#411311=CARTESIAN_POINT('Ctrl Pts',(1.05658959252395,1.08169148113985,-10.0624548715517));
#411312=CARTESIAN_POINT('Ctrl Pts',(0.746057306961948,1.31633259720232,
-10.0409965712171));
#411313=CARTESIAN_POINT('Ctrl Pts',(0.565664761564748,1.40333993984853,
-10.0299005602009));
#411314=CARTESIAN_POINT('Ctrl Pts',(0.251256457537897,1.4841902328274,-10.0125277421489));
#411315=CARTESIAN_POINT('Ctrl Pts',(0.12575413515895,1.50000000000007,-10.0060503486488));
#411316=CARTESIAN_POINT('Ctrl Pts',(-1.14248888127833E-13,1.50000000000006,
-9.99999999999997));
#411317=CARTESIAN_POINT('Origin',(0.,2.5406128344257E-15,14.));
#411318=CARTESIAN_POINT('',(1.01826625150655E-13,1.50000000000006,-9.43750000000001));
#411319=CARTESIAN_POINT('',(-1.21120035981893E-13,1.50000000000006,-9.49999999999997));
#411320=CARTESIAN_POINT('',(-1.8369701987211E-16,1.50000000000006,14.));
#411321=CARTESIAN_POINT('Ctrl Pts',(2.03836947321181E-13,1.50000000000006,
-9.43750000000001));
#411322=CARTESIAN_POINT('Ctrl Pts',(0.0423644631912906,1.50000000000006,
-9.43953826118564));
#411323=CARTESIAN_POINT('Ctrl Pts',(0.0847727287843001,1.49820533233011,
-9.44162848169512));
#411324=CARTESIAN_POINT('Ctrl Pts',(0.32528689345542,1.4777501628067,-9.45376842399161));
#411325=CARTESIAN_POINT('Ctrl Pts',(0.518115985397973,1.42165119715189,
-9.46460422260485));
#411326=CARTESIAN_POINT('Ctrl Pts',(0.866288558520853,1.23982356349243,
-9.48640645094125));
#411327=CARTESIAN_POINT('Ctrl Pts',(1.0191904154483,1.11753375322258,-9.49715988413679));
#411328=CARTESIAN_POINT('Ctrl Pts',(1.26881896757184,0.822831198353581,
-9.51735632553032));
#411329=CARTESIAN_POINT('Ctrl Pts',(1.36370261923566,0.653658070164938,
-9.52618566276873));
#411330=CARTESIAN_POINT('Ctrl Pts',(1.48667902345296,0.281956269164541,
-9.5468357628243));
#411331=CARTESIAN_POINT('Ctrl Pts',(1.5109431375262,0.0821818978378209,
-9.55793433900912));
#411332=CARTESIAN_POINT('Ctrl Pts',(1.48058378314258,-0.307622245431263,
-9.57959012474629));
#411333=CARTESIAN_POINT('Ctrl Pts',(1.42918258544925,-0.494183852189728,
-9.58995465845509));
#411334=CARTESIAN_POINT('Ctrl Pts',(1.2559630345297,-0.843738403721386,
-9.6093743557624));
#411335=CARTESIAN_POINT('Ctrl Pts',(1.13351755852915,-1.00224760565162,
-9.61913715563922));
#411336=CARTESIAN_POINT('Ctrl Pts',(0.835190258339646,-1.26142024596133,
-9.6406896745704));
#411337=CARTESIAN_POINT('Ctrl Pts',(0.662681532840596,-1.35999168419044,
-9.65172760000214));
#411338=CARTESIAN_POINT('Ctrl Pts',(0.295926946589629,-1.48273874308817,
-9.67278272878528));
#411339=CARTESIAN_POINT('Ctrl Pts',(0.106010913449538,-1.50825160362181,
-9.68217033633698));
#411340=CARTESIAN_POINT('Ctrl Pts',(-0.282146492696278,-1.48658672961012,
-9.70144737030338));
#411341=CARTESIAN_POINT('Ctrl Pts',(-0.476497757838591,-1.43613145389777,
-9.71219963534377));
#411342=CARTESIAN_POINT('Ctrl Pts',(-0.830283464242,-1.26430209867626,-9.73399419572443));
#411343=CARTESIAN_POINT('Ctrl Pts',(-0.987065796433557,-1.14609850085419,
-9.74482082247184));
#411344=CARTESIAN_POINT('Ctrl Pts',(-1.24462862356872,-0.858783093545962,
-9.76519380330649));
#411345=CARTESIAN_POINT('Ctrl Pts',(-1.34389439900638,-0.693221006526352,
-9.77398772185978));
#411346=CARTESIAN_POINT('Ctrl Pts',(-1.47780558639996,-0.325642226491207,
-9.79440876519507));
#411347=CARTESIAN_POINT('Ctrl Pts',(-1.50799467343637,-0.126058655085577,
-9.80549674138427));
#411348=CARTESIAN_POINT('Ctrl Pts',(-1.48876910511602,0.265573728760382,
-9.82725409604237));
#411349=CARTESIAN_POINT('Ctrl Pts',(-1.44251008882995,0.454033490561692,
-9.83772408280911));
#411350=CARTESIAN_POINT('Ctrl Pts',(-1.27955557689145,0.807067726692858,
-9.85733709592751));
#411351=CARTESIAN_POINT('Ctrl Pts',(-1.16293731341604,0.967580676555588,
-9.86675872676962));
#411352=CARTESIAN_POINT('Ctrl Pts',(-0.873763612333058,1.23511086436131,
-9.88810299705557));
#411353=CARTESIAN_POINT('Ctrl Pts',(-0.703831043145741,1.33924652554451,
-9.89917153885769));
#411354=CARTESIAN_POINT('Ctrl Pts',(-0.352421064611548,1.46873171212293,
-9.9196755700712));
#411355=CARTESIAN_POINT('Ctrl Pts',(-0.176837209122336,1.50000000000006,
-9.92899191580921));
#411356=CARTESIAN_POINT('Ctrl Pts',(1.196959198424E-14,1.50000000000006,
-9.9375));
#411357=CARTESIAN_POINT('Ctrl Pts',(-1.14658282868169E-13,1.50000000000006,
-9.99999999999997));
#411358=CARTESIAN_POINT('Ctrl Pts',(-0.0675188942384693,1.50000000000005,
-9.99675149568631));
#411359=CARTESIAN_POINT('Ctrl Pts',(-0.135098082697613,1.49544172065095,
-9.99337347159485));
#411360=CARTESIAN_POINT('Ctrl Pts',(-0.393664768377399,1.46025115578112,
-9.97995566043897));
#411361=CARTESIAN_POINT('Ctrl Pts',(-0.578204640568276,1.39748667206119,
-9.96933352381739));
#411362=CARTESIAN_POINT('Ctrl Pts',(-0.919980234621133,1.20164805513356,
-9.94744987630033));
#411363=CARTESIAN_POINT('Ctrl Pts',(-1.07241923289505,1.06782789335319,
-9.93639842486017));
#411364=CARTESIAN_POINT('Ctrl Pts',(-1.30920251764387,0.756449592440474,
-9.91635678651348));
#411365=CARTESIAN_POINT('Ctrl Pts',(-1.39452034595421,0.584420019403402,
-9.90746777885578));
#411366=CARTESIAN_POINT('Ctrl Pts',(-1.49764701025264,0.212695779101129,
-9.88681643217232));
#411367=CARTESIAN_POINT('Ctrl Pts',(-1.51258840311147,0.0159976360466687,
-9.87588875755818));
#411368=CARTESIAN_POINT('Ctrl Pts',(-1.46581254175606,-0.375356815859686,
-9.85414684356338));
#411369=CARTESIAN_POINT('Ctrl Pts',(-1.40323545031248,-0.56608835829669,
-9.84355064676133));
#411370=CARTESIAN_POINT('Ctrl Pts',(-1.21149399001615,-0.904714767481383,
-9.82473806847329));
#411371=CARTESIAN_POINT('Ctrl Pts',(-1.08700372010449,-1.05104787787605,
-9.81476938314896));
#411372=CARTESIAN_POINT('Ctrl Pts',(-0.78414191969591,-1.29391841961372,
-9.79345153404571));
#411373=CARTESIAN_POINT('Ctrl Pts',(-0.606917337671277,-1.38591440254458,
-9.78236936839716));
#411374=CARTESIAN_POINT('Ctrl Pts',(-0.229116448644826,-1.49524029577133,
-9.76115558428146));
#411375=CARTESIAN_POINT('Ctrl Pts',(-0.0324969925423966,-1.51233971487207,
-9.75190628214028));
#411376=CARTESIAN_POINT('Ctrl Pts',(0.353383565241518,-1.47045095097361,
-9.73217701837269));
#411377=CARTESIAN_POINT('Ctrl Pts',(0.539077702549313,-1.41296972338044,
-9.72164610425942));
#411378=CARTESIAN_POINT('Ctrl Pts',(0.885253015832435,-1.22735984233263,
-9.69983490670441));
#411379=CARTESIAN_POINT('Ctrl Pts',(1.04100510498355,-1.09836632522092,
-9.68875812756812));
#411380=CARTESIAN_POINT('Ctrl Pts',(1.28679104961533,-0.794106348618159,
-9.66848107977669));
#411381=CARTESIAN_POINT('Ctrl Pts',(1.37728758213822,-0.62411371477506,
-9.65967298415421));
#411382=CARTESIAN_POINT('Ctrl Pts',(1.49087595034938,-0.255462173952587,
-9.63919234299741));
#411383=CARTESIAN_POINT('Ctrl Pts',(1.51141733568497,-0.0598401750380719,
-9.62832445416882));
#411384=CARTESIAN_POINT('Ctrl Pts',(1.4761958376045,0.332205859839538,-9.60654411889785));
#411385=CARTESIAN_POINT('Ctrl Pts',(1.41922573178766,0.524726274931734,
-9.59584854028161));
#411386=CARTESIAN_POINT('Ctrl Pts',(1.23762446457936,0.868552370279251,
-9.57674709054008));
#411387=CARTESIAN_POINT('Ctrl Pts',(1.11776010832914,1.0182063201762,-9.56716141605903));
#411388=CARTESIAN_POINT('Ctrl Pts',(0.823072067791609,1.26941697957466,
-9.54600515722591));
#411389=CARTESIAN_POINT('Ctrl Pts',(0.649285913538544,1.36649044792844,
-9.53494738174891));
#411390=CARTESIAN_POINT('Ctrl Pts',(0.312301830568179,1.4755086268206,-9.51570594475061));
#411391=CARTESIAN_POINT('Ctrl Pts',(0.156516666443393,1.50000000000008,
-9.50753041162529));
#411392=CARTESIAN_POINT('Ctrl Pts',(-2.41993924898765E-13,1.50000000000006,
-9.49999999999997));
#411393=CARTESIAN_POINT('Origin',(0.,2.5406128344257E-15,14.));
#411394=CARTESIAN_POINT('',(3.81275791127862E-14,1.50000000000006,-8.93750000000001));
#411395=CARTESIAN_POINT('',(-9.18485099360549E-17,1.50000000000006,-8.99999999999998));
#411396=CARTESIAN_POINT('',(-1.8369701987211E-16,1.50000000000006,14.));
#411397=CARTESIAN_POINT('Ctrl Pts',(7.64388552454446E-14,1.50000000000006,
-8.93750000000001));
#411398=CARTESIAN_POINT('Ctrl Pts',(0.0701697277412552,1.50000000000006,
-8.94087604260004));
#411399=CARTESIAN_POINT('Ctrl Pts',(0.140393881454839,1.49507682204823,
-8.94439145871407));
#411400=CARTESIAN_POINT('Ctrl Pts',(0.408745304662783,1.457103970486,-8.95835732401523));
#411401=CARTESIAN_POINT('Ctrl Pts',(0.599667970056199,1.3894626792969,-8.96942201979208));
#411402=CARTESIAN_POINT('Ctrl Pts',(0.937003600546002,1.18710465492744,
-8.99127314411378));
#411403=CARTESIAN_POINT('Ctrl Pts',(1.08172971331996,1.05691568366112,-9.00185264277413));
#411404=CARTESIAN_POINT('Ctrl Pts',(1.31505937341547,0.747358543121225,
-9.02167753073908));
#411405=CARTESIAN_POINT('Ctrl Pts',(1.4008716427756,0.570519225809976,-9.03080448745509));
#411406=CARTESIAN_POINT('Ctrl Pts',(1.50095938264119,0.190655899122854,
-9.05190800560437));
#411407=CARTESIAN_POINT('Ctrl Pts',(1.5129913597143,-0.00897481519057823,
-9.062998600844));
#411408=CARTESIAN_POINT('Ctrl Pts',(1.45982897099295,-0.394006866340737,
-9.08438927035234));
#411409=CARTESIAN_POINT('Ctrl Pts',(1.39798730795961,-0.576192500279294,
-9.09451069446004));
#411410=CARTESIAN_POINT('Ctrl Pts',(1.20537929923835,-0.91462821674284,
-9.11331267870802));
#411411=CARTESIAN_POINT('Ctrl Pts',(1.0737122353804,-1.06615396931563,-9.12378971735921));
#411412=CARTESIAN_POINT('Ctrl Pts',(0.761347951035123,-1.30714841853425,
-9.14551264125295));
#411413=CARTESIAN_POINT('Ctrl Pts',(0.584517842961423,-1.39521749262844,
-9.15646674696366));
#411414=CARTESIAN_POINT('Ctrl Pts',(0.212337725831777,-1.49702241144052,
-9.17720118560942));
#411415=CARTESIAN_POINT('Ctrl Pts',(0.0210784953152501,-1.51185650475691,
-9.18615651306704));
#411416=CARTESIAN_POINT('Ctrl Pts',(-0.365530383982027,-1.46831626746077,
-9.20596669248082));
#411417=CARTESIAN_POINT('Ctrl Pts',(-0.55677754231025,-1.40696314389929,
-9.21687232910829));
#411418=CARTESIAN_POINT('Ctrl Pts',(-0.899424319695077,-1.21591800100396,
-9.2386647393965));
#411419=CARTESIAN_POINT('Ctrl Pts',(-1.04859030674976,-1.08990528801022,
-9.24934184443354));
#411420=CARTESIAN_POINT('Ctrl Pts',(-1.29070978850643,-0.788305324551741,
-9.26936860019363));
#411421=CARTESIAN_POINT('Ctrl Pts',(-1.38142829751791,-0.615642971931764,
-9.27829761267055));
#411422=CARTESIAN_POINT('Ctrl Pts',(-1.49393087063595,-0.240125194098544,
-9.29915971143906));
#411423=CARTESIAN_POINT('Ctrl Pts',(-1.51256570660118,-0.0403266795942435,
-9.31025962891152));
#411424=CARTESIAN_POINT('Ctrl Pts',(-1.4716815678648,0.347448886442948,
-9.33180271591359));
#411425=CARTESIAN_POINT('Ctrl Pts',(-1.4154460993233,0.532073427304002,
-9.34205963485031));
#411426=CARTESIAN_POINT('Ctrl Pts',(-1.23241032036788,0.878223448450719,
-9.36129019158068));
#411427=CARTESIAN_POINT('Ctrl Pts',(-1.10425483612739,1.03478069252725,
-9.37144875588485));
#411428=CARTESIAN_POINT('Ctrl Pts',(-0.797154057907381,1.28570667084145,
-9.39319431503027));
#411429=CARTESIAN_POINT('Ctrl Pts',(-0.622323356335188,1.37884474301256,
-9.40419302975296));
#411430=CARTESIAN_POINT('Ctrl Pts',(-0.293385231348153,1.4784011982189,
-9.42278452975936));
#411431=CARTESIAN_POINT('Ctrl Pts',(-0.146985099260076,1.50000000000006,
-9.4304281761146));
#411432=CARTESIAN_POINT('Ctrl Pts',(2.02581007524572E-13,1.50000000000006,
-9.43750000000001));
#411433=CARTESIAN_POINT('Ctrl Pts',(-2.42056374943915E-13,1.50000000000006,
-9.49999999999997));
#411434=CARTESIAN_POINT('Ctrl Pts',(-0.0400937591764138,1.50000000000005,
-9.4980709881122));
#411435=CARTESIAN_POINT('Ctrl Pts',(-0.0802312376367462,1.4983925534736,
-9.49609522148706));
#411436=CARTESIAN_POINT('Ctrl Pts',(-0.311798731012663,1.47975813117801,
-9.48443630242584));
#411437=CARTESIAN_POINT('Ctrl Pts',(-0.49852193792271,1.4277110365756,-9.47400682531687));
#411438=CARTESIAN_POINT('Ctrl Pts',(-0.848900532454104,1.25268257467032,
-9.45228732560803));
#411439=CARTESIAN_POINT('Ctrl Pts',(-1.00789774150321,1.12871623256175,
-9.44119405931794));
#411440=CARTESIAN_POINT('Ctrl Pts',(-1.26283453615189,0.831854778879047,
-9.42068225557535));
#411441=CARTESIAN_POINT('Ctrl Pts',(-1.35866853382425,0.663892795229351,
-9.41188293306834));
#411442=CARTESIAN_POINT('Ctrl Pts',(-1.48280150205461,0.298424756848632,
-9.3915791531583));
#411443=CARTESIAN_POINT('Ctrl Pts',(-1.50894686669985,0.104047412402745,
-9.3807804118002));
#411444=CARTESIAN_POINT('Ctrl Pts',(-1.48539000906149,-0.288349426218138,
-9.35898058743237));
#411445=CARTESIAN_POINT('Ctrl Pts',(-1.43413424677483,-0.482503912567459,
-9.34819422707963));
#411446=CARTESIAN_POINT('Ctrl Pts',(-1.26281562140763,-0.831475645725152,
-9.32880690857087));
#411447=CARTESIAN_POINT('Ctrl Pts',(-1.14753048075311,-0.984504981270521,
-9.31952989207304));
#411448=CARTESIAN_POINT('Ctrl Pts',(-0.861013851284105,-1.24390106010667,
-9.2985394076761));
#411449=CARTESIAN_POINT('Ctrl Pts',(-0.690784490420879,-1.34590121332312,
-9.28751590614356));
#411450=CARTESIAN_POINT('Ctrl Pts',(-0.318241244180354,-1.47931981507511,
-9.26588583858086));
#411451=CARTESIAN_POINT('Ctrl Pts',(-0.119286155130846,-1.50844485536951,
-9.25597373713049));
#411452=CARTESIAN_POINT('Ctrl Pts',(0.270834169652757,-1.48773429007375,
-9.23662877077254));
#411453=CARTESIAN_POINT('Ctrl Pts',(0.458413226153797,-1.44102059205357,
-9.22630626648598));
#411454=CARTESIAN_POINT('Ctrl Pts',(0.812603298748567,-1.27643655127287,
-9.20469350976234));
#411455=CARTESIAN_POINT('Ctrl Pts',(0.974627172716593,-1.15746537014635,
-9.19359337746016));
#411456=CARTESIAN_POINT('Ctrl Pts',(1.23845215928419,-0.867953395363224,
-9.17285809257615));
#411457=CARTESIAN_POINT('Ctrl Pts',(1.33954625945943,-0.701940758562861,
-9.1639967088091));
#411458=CARTESIAN_POINT('Ctrl Pts',(1.47384264903161,-0.339617780380702,
-9.14386765446565));
#411459=CARTESIAN_POINT('Ctrl Pts',(1.50534068747472,-0.146589673115085,
-9.13314387072867));
#411460=CARTESIAN_POINT('Ctrl Pts',(1.49302224351914,0.245815292223104,
-9.11134359487654));
#411461=CARTESIAN_POINT('Ctrl Pts',(1.44732297201183,0.441380475807474,
-9.10047886245519));
#411462=CARTESIAN_POINT('Ctrl Pts',(1.28597357042616,0.795215414898501,
-9.08082136583902));
#411463=CARTESIAN_POINT('Ctrl Pts',(1.17503106654397,0.95153043233265,-9.07176897431654));
#411464=CARTESIAN_POINT('Ctrl Pts',(0.896322161173119,1.21861508181268,
-9.05094056781364));
#411465=CARTESIAN_POINT('Ctrl Pts',(0.729595943825354,1.32517998985375,
-9.03995881260694));
#411466=CARTESIAN_POINT('Ctrl Pts',(0.372645820190216,1.4650059210476,-9.01890098813199));
#411467=CARTESIAN_POINT('Ctrl Pts',(0.187073537795138,1.50000000000006,
-9.00900057978367));
#411468=CARTESIAN_POINT('Ctrl Pts',(-2.77555756156289E-16,1.50000000000006,
-8.99999999999998));
#411469=CARTESIAN_POINT('Origin',(0.,2.5406128344257E-15,14.));
#411470=CARTESIAN_POINT('',(-3.69404266092344E-16,1.50000000000006,-8.4375));
#411471=CARTESIAN_POINT('',(1.90178653014251E-14,1.50000000000006,-8.49999999999998));
#411472=CARTESIAN_POINT('',(-1.8369701987211E-16,1.50000000000006,14.));
#411473=CARTESIAN_POINT('Ctrl Pts',(6.93889390390723E-16,1.50000000000006,
-8.4375));
#411474=CARTESIAN_POINT('Ctrl Pts',(0.100048703118938,1.50000000000006,
-8.44231359547315));
#411475=CARTESIAN_POINT('Ctrl Pts',(0.200061577253575,1.48999234904905,
-8.44740345742775));
#411476=CARTESIAN_POINT('Ctrl Pts',(0.49392690742635,1.43030749600499,-8.46319997230237));
#411477=CARTESIAN_POINT('Ctrl Pts',(0.679423997631909,1.35207810285786,
-8.47429774391457));
#411478=CARTESIAN_POINT('Ctrl Pts',(1.00272579266332,1.13195669206866,-8.49596709241351));
#411479=CARTESIAN_POINT('Ctrl Pts',(1.1391209973992,0.994589792123244,-8.50634515698175));
#411480=CARTESIAN_POINT('Ctrl Pts',(1.35625249336917,0.670688029442479,
-8.52578917213798));
#411481=CARTESIAN_POINT('Ctrl Pts',(1.43288715691681,0.48590213439737,-8.535505436978));
#411482=CARTESIAN_POINT('Ctrl Pts',(1.50965805252362,0.0984174505511938,
-8.55703236385833));
#411483=CARTESIAN_POINT('Ctrl Pts',(1.50953122939287,-0.1003441745013,-8.56807467636125));
#411484=CARTESIAN_POINT('Ctrl Pts',(1.43386485159747,-0.479713406126239,
-8.58915074478486));
#411485=CARTESIAN_POINT('Ctrl Pts',(1.36165936049534,-0.657228892664954,
-8.59857682493578));
#411486=CARTESIAN_POINT('Ctrl Pts',(1.15002925545568,-0.983350391502387,
-8.61781781363514));
#411487=CARTESIAN_POINT('Ctrl Pts',(1.00969655551726,-1.12695819727209,
-8.62855867952476));
#411488=CARTESIAN_POINT('Ctrl Pts',(0.684767734231053,-1.34868488435149,
-8.65035089936894));
#411489=CARTESIAN_POINT('Ctrl Pts',(0.504225856506111,-1.42605189050979,
-8.66118630801538));
#411490=CARTESIAN_POINT('Ctrl Pts',(0.126938974991646,-1.50680375704638,
-8.68158163896951));
#411491=CARTESIAN_POINT('Ctrl Pts',(-0.0659595355830271,-1.51070142737475,
-8.69037621776393));
#411492=CARTESIAN_POINT('Ctrl Pts',(-0.451479814049411,-1.44435062852565,
-8.71076764855562));
#411493=CARTESIAN_POINT('Ctrl Pts',(-0.639764629794639,-1.37137527640744,
-8.72185359909125));
#411494=CARTESIAN_POINT('Ctrl Pts',(-0.970208871646639,-1.16003599972617,
-8.7436226405534));
#411495=CARTESIAN_POINT('Ctrl Pts',(-1.11082029581379,-1.02619964802706,
-8.75410548728899));
#411496=CARTESIAN_POINT('Ctrl Pts',(-1.3361091699828,-0.709470730845153,
-8.7737427287785));
#411497=CARTESIAN_POINT('Ctrl Pts',(-1.41739177297902,-0.528725606616922,
-8.78312635518803));
#411498=CARTESIAN_POINT('Ctrl Pts',(-1.50597586053692,-0.145012426518024,
-8.80444375408241));
#411499=CARTESIAN_POINT('Ctrl Pts',(-1.51196665413278,0.0542778614058951,
-8.81551543674485));
#411500=CARTESIAN_POINT('Ctrl Pts',(-1.44760783648443,0.436609821339279,
-8.83675610118559));
#411501=CARTESIAN_POINT('Ctrl Pts',(-1.38063092643955,0.616451079174067,
-8.8465313380023));
#411502=CARTESIAN_POINT('Ctrl Pts',(-1.17864065284233,0.948861810065223,
-8.86548323098553));
#411503=CARTESIAN_POINT('Ctrl Pts',(-1.04264761307,1.09653677036197,-8.8761282813927));
#411504=CARTESIAN_POINT('Ctrl Pts',(-0.724016606612002,1.32810974829059,
-8.89789100555883));
#411505=CARTESIAN_POINT('Ctrl Pts',(-0.545284169269985,1.41093880861734,
-8.90879108119116));
#411506=CARTESIAN_POINT('Ctrl Pts',(-0.239013467161963,1.48569846285508,
-8.9256031942789));
#411507=CARTESIAN_POINT('Ctrl Pts',(-0.119605100351261,1.50000000000006,
-8.93174549692631));
#411508=CARTESIAN_POINT('Ctrl Pts',(7.60502771868232E-14,1.50000000000006,
-8.93750000000001));
#411509=CARTESIAN_POINT('Ctrl Pts',(0.,1.50000000000006,-8.99999999999998));
#411510=CARTESIAN_POINT('Ctrl Pts',(-0.0114925749065063,1.50000000000006,
-8.99944706323198));
#411511=CARTESIAN_POINT('Ctrl Pts',(-0.0229904684161551,1.49986792103453,
-8.99889020171249));
#411512=CARTESIAN_POINT('Ctrl Pts',(-0.225457336202678,1.49521110800026,
-8.98901965407667));
#411513=CARTESIAN_POINT('Ctrl Pts',(-0.413805280348288,1.45438274491613,
-8.97882363819207));
#411514=CARTESIAN_POINT('Ctrl Pts',(-0.77184384434294,1.30139148024828,
-8.9573477423983));
#411515=CARTESIAN_POINT('Ctrl Pts',(-0.937027506192782,1.18800214473311,
-8.94625063599776));
#411516=CARTESIAN_POINT('Ctrl Pts',(-1.21056341325082,0.90672298017732,
-8.9252768234068));
#411517=CARTESIAN_POINT('Ctrl Pts',(-1.31750640773443,0.742820403229874,
-8.91626780017949));
#411518=CARTESIAN_POINT('Ctrl Pts',(-1.46283170239402,0.383998346248297,
-8.89633324145829));
#411519=CARTESIAN_POINT('Ctrl Pts',(-1.50007403509498,0.192597208439964,
-8.88569984491338));
#411520=CARTESIAN_POINT('Ctrl Pts',(-1.49992278590957,-0.201455252188196,
-8.86380804154515));
#411521=CARTESIAN_POINT('Ctrl Pts',(-1.45949387408537,-0.400310244540207,
-8.85276054197004));
#411522=CARTESIAN_POINT('Ctrl Pts',(-1.30684443782229,-0.760502260741033,
-8.83274987440333));
#411523=CARTESIAN_POINT('Ctrl Pts',(-1.19995386392689,-0.919958659763558,
-8.82384506664718));
#411524=CARTESIAN_POINT('Ctrl Pts',(-0.928567014099058,-1.19414298736089,
-8.80317172942481));
#411525=CARTESIAN_POINT('Ctrl Pts',(-0.765212590437898,-1.3048592710734,
-8.79223688372662));
#411526=CARTESIAN_POINT('Ctrl Pts',(-0.402246980449423,-1.45866182365666,
-8.77050139954652));
#411527=CARTESIAN_POINT('Ctrl Pts',(-0.205628964604913,-1.49907990593575,
-8.75991888634082));
#411528=CARTESIAN_POINT('Ctrl Pts',(0.183567016707029,-1.50085076540667,
-8.74114449541847));
#411529=CARTESIAN_POINT('Ctrl Pts',(0.372471377496952,-1.46545895758719,
-8.73111998909442));
#411530=CARTESIAN_POINT('Ctrl Pts',(0.733811676972188,-1.32312328078896,
-8.70978122703021));
#411531=CARTESIAN_POINT('Ctrl Pts',(0.901728634164142,-1.21491752126138,
-8.69869660311809));
#411532=CARTESIAN_POINT('Ctrl Pts',(1.18409112004873,-0.941320453907733,
-8.67751151314428));
#411533=CARTESIAN_POINT('Ctrl Pts',(1.29645387603392,-0.779329009794782,
-8.66829605609977));
#411534=CARTESIAN_POINT('Ctrl Pts',(1.45174678002209,-0.423750361571602,
-8.64854168675403));
#411535=CARTESIAN_POINT('Ctrl Pts',(1.49411427757351,-0.233961822461871,
-8.63799787902571));
#411536=CARTESIAN_POINT('Ctrl Pts',(1.50495464048548,0.158835443777422,
-8.61617580867909));
#411537=CARTESIAN_POINT('Ctrl Pts',(1.4703232657174,0.358164972608317,-8.60510194596626));
#411538=CARTESIAN_POINT('Ctrl Pts',(1.32826209597344,0.722580561232961,
-8.58485663548711));
#411539=CARTESIAN_POINT('Ctrl Pts',(1.22570099624627,0.88547346159937,-8.5760417482997));
#411540=CARTESIAN_POINT('Ctrl Pts',(0.962160812325709,1.16715358642565,
-8.55553771737712));
#411541=CARTESIAN_POINT('Ctrl Pts',(0.802505651928995,1.282176705519,-8.54466121824959));
#411542=CARTESIAN_POINT('Ctrl Pts',(0.444653951517676,1.44630416088315,
-8.52288497430371));
#411543=CARTESIAN_POINT('Ctrl Pts',(0.249261200892981,1.49244982176182,
-8.51220231229284));
#411544=CARTESIAN_POINT('Ctrl Pts',(0.0336834707125518,1.49971652858077,
-8.5016284709464));
#411545=CARTESIAN_POINT('Ctrl Pts',(0.0168366541021336,1.50000000000006,
-8.50081005389816));
#411546=CARTESIAN_POINT('Ctrl Pts',(3.82194276227224E-14,1.50000000000006,
-8.49999999999998));
#411547=CARTESIAN_POINT('Origin',(0.,2.5406128344257E-15,14.));
#411548=CARTESIAN_POINT('',(-7.65307037553809E-14,1.50000000000006,-7.93749999999999));
#411549=CARTESIAN_POINT('',(1.08196529754441E-13,1.50000000000006,-7.99999999999999));
#411550=CARTESIAN_POINT('',(-1.8369701987211E-16,1.50000000000006,14.));
#411551=CARTESIAN_POINT('Ctrl Pts',(-1.52933221642115E-13,1.50000000000006,
-7.93749999999999));
#411552=CARTESIAN_POINT('Ctrl Pts',(0.131087257000726,1.50000000000007,
-7.94380693859306));
#411553=CARTESIAN_POINT('Ctrl Pts',(0.261858013506839,1.48282092882581,
-7.95057584597053));
#411554=CARTESIAN_POINT('Ctrl Pts',(0.580344486051787,1.39730357656786,
-7.96827451553245));
#411555=CARTESIAN_POINT('Ctrl Pts',(0.759629638709708,1.30851601444969,
-7.97936669763146));
#411556=CARTESIAN_POINT('Ctrl Pts',(1.06743714486741,1.07095493849033,-8.00077501195301));
#411557=CARTESIAN_POINT('Ctrl Pts',(1.19483432966657,0.926693877796609,
-8.01091166355043));
#411558=CARTESIAN_POINT('Ctrl Pts',(1.39279680522045,0.591274626156194,
-8.02975333903075));
#411559=CARTESIAN_POINT('Ctrl Pts',(1.45882908968199,0.401698859921977,
-8.04018339667106));
#411560=CARTESIAN_POINT('Ctrl Pts',(1.51267846314344,0.0107967219430277,
-8.06190018211433));
#411561=CARTESIAN_POINT('Ctrl Pts',(1.50118032369557,-0.186481449343415,
-8.07286008051913));
#411562=CARTESIAN_POINT('Ctrl Pts',(1.40445759093839,-0.560043742577229,
-8.09361354125434));
#411563=CARTESIAN_POINT('Ctrl Pts',(1.32225660699352,-0.733333426955382,
-8.10258660563892));
#411564=CARTESIAN_POINT('Ctrl Pts',(1.09230497047696,-1.04710748744377,
-8.12236610503389));
#411565=CARTESIAN_POINT('Ctrl Pts',(0.94399744391964,-1.18254564038123,
-8.13326372514721));
#411566=CARTESIAN_POINT('Ctrl Pts',(0.607842213005839,-1.38490880839251,
-8.15505820034676));
#411567=CARTESIAN_POINT('Ctrl Pts',(0.424285848828745,-1.45170255815611,
-8.16574494197373));
#411568=CARTESIAN_POINT('Ctrl Pts',(0.0422983906788046,-1.51179188388456,
-8.18579247005979));
#411569=CARTESIAN_POINT('Ctrl Pts',(-0.152473772750104,-1.50467891416419,
-8.19470592797397));
#411570=CARTESIAN_POINT('Ctrl Pts',(-0.534175449206377,-1.41568829505058,
-8.21554252008703));
#411571=CARTESIAN_POINT('Ctrl Pts',(-0.716870672388642,-1.33251813997508,
-8.22664273019612));
#411572=CARTESIAN_POINT('Ctrl Pts',(-1.03311840696601,-1.10419976822846,
-8.24820038341315));
#411573=CARTESIAN_POINT('Ctrl Pts',(-1.16539340622638,-0.963572107969621,
-8.2584707911784));
#411574=CARTESIAN_POINT('Ctrl Pts',(-1.37461328749515,-0.632811755228003,
-8.27772467498541));
#411575=CARTESIAN_POINT('Ctrl Pts',(-1.446678866683,-0.444037130716313,
-8.28783127051582));
#411576=CARTESIAN_POINT('Ctrl Pts',(-1.51185690464234,-0.0530351822067093,
-8.30955360098858));
#411577=CARTESIAN_POINT('Ctrl Pts',(-1.50581899066547,0.145037362305904,
-8.32055763123928));
#411578=CARTESIAN_POINT('Ctrl Pts',(-1.41921969677474,0.521437507459838,
-8.34146875041449));
#411579=CARTESIAN_POINT('Ctrl Pts',(-1.34187002821176,0.696742341984953,
-8.35062653544363));
#411580=CARTESIAN_POINT('Ctrl Pts',(-1.12078621757607,1.01655997572849,
-8.37014725840183));
#411581=CARTESIAN_POINT('Ctrl Pts',(-0.97629141006827,1.15602332206968,
-8.38097324991224));
#411582=CARTESIAN_POINT('Ctrl Pts',(-0.645444276829998,1.36786188068275,
-8.4027755444378));
#411583=CARTESIAN_POINT('Ctrl Pts',(-0.463276097361062,1.43980272374935,
-8.41353847181083));
#411584=CARTESIAN_POINT('Ctrl Pts',(-0.182373624965341,1.49168715610955,
-8.42849463254753));
#411585=CARTESIAN_POINT('Ctrl Pts',(-0.0911831684366718,1.50000000000006,
-8.43311294776313));
#411586=CARTESIAN_POINT('Ctrl Pts',(0.,1.50000000000006,-8.4375));
#411587=CARTESIAN_POINT('Ctrl Pts',(3.84067777581265E-14,1.50000000000006,
-8.49999999999998));
#411588=CARTESIAN_POINT('Ctrl Pts',(-0.172932034887872,1.50000000000006,
-8.49167980359215));
#411589=CARTESIAN_POINT('Ctrl Pts',(-0.344713320132888,1.47009849013323,
-8.48258437515609));
#411590=CARTESIAN_POINT('Ctrl Pts',(-0.693324755588895,1.34469310157241,
-8.46232831663192));
#411591=CARTESIAN_POINT('Ctrl Pts',(-0.863935655426715,1.2419804931837,
-8.45126666787545));
#411592=CARTESIAN_POINT('Ctrl Pts',(-1.1554673236908,0.976580224102157,
-8.42986811424961));
#411593=CARTESIAN_POINT('Ctrl Pts',(-1.27357449666595,0.816581108131254,
-8.42036561711846));
#411594=CARTESIAN_POINT('Ctrl Pts',(-1.43917631272028,0.46443648140315,
-8.40080202674468));
#411595=CARTESIAN_POINT('Ctrl Pts',(-1.48676957695217,0.27645348818368,
-8.39035852712137));
#411596=CARTESIAN_POINT('Ctrl Pts',(-1.50887809365703,-0.114736495199806,
-8.36862575026674));
#411597=CARTESIAN_POINT('Ctrl Pts',(-1.48022027472746,-0.314385601088563,
-8.35753413327291));
#411598=CARTESIAN_POINT('Ctrl Pts',(-1.34912750600613,-0.683040129192743,
-8.33705332615602));
#411599=CARTESIAN_POINT('Ctrl Pts',(-1.25099477475441,-0.849530229743552,
-8.32825711889268));
#411600=CARTESIAN_POINT('Ctrl Pts',(-0.995486464685214,-1.1387680659669,
-8.30792958525325));
#411601=CARTESIAN_POINT('Ctrl Pts',(-0.839701779031076,-1.25804455982313,
-8.29712115512963));
#411602=CARTESIAN_POINT('Ctrl Pts',(-0.487346278273407,-1.43248760100607,
-8.27532280316236));
#411603=CARTESIAN_POINT('Ctrl Pts',(-0.293374043358508,-1.48441277650396,
-8.26454794367269));
#411604=CARTESIAN_POINT('Ctrl Pts',(0.0946013444325994,-1.50900837485635,
-8.245198258059));
#411605=CARTESIAN_POINT('Ctrl Pts',(0.284683234072073,-1.48493563279221,
-8.23588471686996));
#411606=CARTESIAN_POINT('Ctrl Pts',(0.652195181345535,-1.36502991310751,
-8.21487207562688));
#411607=CARTESIAN_POINT('Ctrl Pts',(0.825326317838232,-1.26787247932391,
-8.20384348233351));
#411608=CARTESIAN_POINT('Ctrl Pts',(1.12595209051725,-1.0108371779097,-8.18223974861799));
#411609=CARTESIAN_POINT('Ctrl Pts',(1.24988129516094,-0.852835770679252,
-8.1723797650378));
#411610=CARTESIAN_POINT('Ctrl Pts',(1.42567411081573,-0.50416634860906,
-8.15300924158945));
#411611=CARTESIAN_POINT('Ctrl Pts',(1.47835070174964,-0.3181012037514,-8.14267228909736));
#411612=CARTESIAN_POINT('Ctrl Pts',(1.51148122317105,0.0711973638489506,
-8.12104459089734));
#411613=CARTESIAN_POINT('Ctrl Pts',(1.48869659189733,0.270992937052696,
-8.10994483683046));
#411614=CARTESIAN_POINT('Ctrl Pts',(1.36846410711534,0.643707485225511,
-8.08923847304309));
#411615=CARTESIAN_POINT('Ctrl Pts',(1.27467455985319,0.813791482789087,
-8.0803891560554));
#411616=CARTESIAN_POINT('Ctrl Pts',(1.02702162401374,1.11031780191357,-8.06023710642645));
#411617=CARTESIAN_POINT('Ctrl Pts',(0.875097098422878,1.23360087097202,
-8.04950310458486));
#411618=CARTESIAN_POINT('Ctrl Pts',(0.528358954668116,1.41787727470082,
-8.02770186887279));
#411619=CARTESIAN_POINT('Ctrl Pts',(0.335933026065815,1.47536720299694,
-8.01684682961366));
#411620=CARTESIAN_POINT('Ctrl Pts',(0.0919672531652487,1.49788782491748,
-8.00448344806109));
#411621=CARTESIAN_POINT('Ctrl Pts',(0.0459596310377224,1.50000000000006,
-8.00221123377927));
#411622=CARTESIAN_POINT('Ctrl Pts',(2.16576756528755E-13,1.50000000000006,
-7.99999999999999));
#411623=CARTESIAN_POINT('Origin',(0.,2.5406128344257E-15,14.));
#411624=CARTESIAN_POINT('',(-1.02010322170531E-13,1.50000000000006,-7.43749999999999));
#411625=CARTESIAN_POINT('',(2.53877699052118E-14,1.50000000000006,-7.49999999999998));
#411626=CARTESIAN_POINT('',(-1.8369701987211E-16,1.50000000000006,14.));
#411627=CARTESIAN_POINT('Ctrl Pts',(-2.05148398269017E-13,1.50000000000006,
-7.43749999999999));
#411628=CARTESIAN_POINT('Ctrl Pts',(0.162224039161413,1.50000000000008,
-7.44530500772324));
#411629=CARTESIAN_POINT('Ctrl Pts',(0.323597657554839,1.47368937335663,
-7.45379995029834));
#411630=CARTESIAN_POINT('Ctrl Pts',(0.664507480107818,1.3591217960283,-7.47338441448693));
#411631=CARTESIAN_POINT('Ctrl Pts',(0.837011173684796,1.26023580039065,
-7.48443083552599));
#411632=CARTESIAN_POINT('Ctrl Pts',(1.12872193618759,1.00602573548763,-7.50552716682245));
#411633=CARTESIAN_POINT('Ctrl Pts',(1.24691313573543,0.855148909639087,
-7.51499172724232));
#411634=CARTESIAN_POINT('Ctrl Pts',(1.42478524268694,0.509441695054457,
-7.53419768360813));
#411635=CARTESIAN_POINT('Ctrl Pts',(1.47968565726979,0.316307665969748,
-7.54492735189061));
#411636=CARTESIAN_POINT('Ctrl Pts',(1.51066957180406,-0.0759061424649054,
-7.56671700791476));
#411637=CARTESIAN_POINT('Ctrl Pts',(1.48808662914522,-0.271094338745857,
-7.57756079659703));
#411638=CARTESIAN_POINT('Ctrl Pts',(1.37066665142521,-0.638599056246443,
-7.59797772534707));
#411639=CARTESIAN_POINT('Ctrl Pts',(1.27824481809212,-0.807851530565787,
-7.60677407114223));
#411640=CARTESIAN_POINT('Ctrl Pts',(1.02914229971986,-1.10944963628426,
-7.62713674680424));
#411641=CARTESIAN_POINT('Ctrl Pts',(0.872199458171957,-1.23663507764676,
-7.63822059171557));
#411642=CARTESIAN_POINT('Ctrl Pts',(0.52446883006992,-1.41843093624381,
-7.66000067432161));
#411643=CARTESIAN_POINT('Ctrl Pts',(0.338384687929842,-1.47394983452341,
-7.67049584340353));
#411644=CARTESIAN_POINT('Ctrl Pts',(-0.0482888071570643,-1.51199353587383,
-7.6901564500919));
#411645=CARTESIAN_POINT('Ctrl Pts',(-0.24531930706965,-1.49274497385977,
-7.69950445916845));
#411646=CARTESIAN_POINT('Ctrl Pts',(-0.622225557029383,-1.37907811866395,
-7.7207957822189));
#411647=CARTESIAN_POINT('Ctrl Pts',(-0.79822977627011,-1.28524213549069,
-7.73187034425347));
#411648=CARTESIAN_POINT('Ctrl Pts',(-1.09815687256819,-1.03935888441861,
-7.75313068370978));
#411649=CARTESIAN_POINT('Ctrl Pts',(-1.22098038921394,-0.891839198321561,
-7.76295337787107));
#411650=CARTESIAN_POINT('Ctrl Pts',(-1.40909722008401,-0.551340069333862,
-7.78186999614817));
#411651=CARTESIAN_POINT('Ctrl Pts',(-1.46967403244992,-0.35994893374625,
-7.79250283701415));
#411652=CARTESIAN_POINT('Ctrl Pts',(-1.51231529169579,0.0316923961372904,
-7.81426068867434));
#411653=CARTESIAN_POINT('Ctrl Pts',(-1.49536436400893,0.228023414670104,
-7.82516796748172));
#411654=CARTESIAN_POINT('Ctrl Pts',(-1.38849093405516,0.598657105883578,
-7.84575872810469));
#411655=CARTESIAN_POINT('Ctrl Pts',(-1.30133115946933,0.769954259128152,
-7.85461062704046));
#411656=CARTESIAN_POINT('Ctrl Pts',(-1.06133276307849,1.07880796692926,
-7.87473682493171));
#411657=CARTESIAN_POINT('Ctrl Pts',(-0.907697246875946,1.21091814756384,
-7.88579834439128));
#411658=CARTESIAN_POINT('Ctrl Pts',(-0.564320965471289,1.40312493807049,
-7.90765812094721));
#411659=CARTESIAN_POINT('Ctrl Pts',(-0.379353003860085,1.46401008524602,
-7.91824865023773));
#411660=CARTESIAN_POINT('Ctrl Pts',(-0.125455029964037,1.49606952593216,
-7.93135486222142));
#411661=CARTESIAN_POINT('Ctrl Pts',(-0.0626966099648303,1.50000000000005,
-7.93448350794663));
#411662=CARTESIAN_POINT('Ctrl Pts',(-1.5287771049089E-13,1.50000000000006,
-7.93749999999999));
#411663=CARTESIAN_POINT('Ctrl Pts',(2.16576756528755E-13,1.50000000000006,
-7.99999999999999));
#411664=CARTESIAN_POINT('Ctrl Pts',(-0.143393401176053,1.50000000000006,
-7.99310098176924));
#411665=CARTESIAN_POINT('Ctrl Pts',(-0.28626462010078,1.47944402194318,
-7.98565608765337));
#411666=CARTESIAN_POINT('Ctrl Pts',(-0.612336793066801,1.38328881735224,
-7.96729695501164));
#411667=CARTESIAN_POINT('Ctrl Pts',(-0.787711874190217,1.29149167000941,
-7.95630929672747));
#411668=CARTESIAN_POINT('Ctrl Pts',(-1.09695406145413,1.0426157800093,-7.934517655889));
#411669=CARTESIAN_POINT('Ctrl Pts',(-1.22652279206843,0.886541324990798,
-7.92425229583289));
#411670=CARTESIAN_POINT('Ctrl Pts',(-1.41195258880116,0.541233233830744,
-7.90506851299066));
#411671=CARTESIAN_POINT('Ctrl Pts',(-1.46935403187863,0.357098637279686,
-7.89483881318227));
#411672=CARTESIAN_POINT('Ctrl Pts',(-1.51278524446635,-0.0301414675088971,
-7.87332547402735));
#411673=CARTESIAN_POINT('Ctrl Pts',(-1.49551695163616,-0.229922671981429,
-7.86222651822332));
#411674=CARTESIAN_POINT('Ctrl Pts',(-1.38557150881023,-0.606351438922552,
-7.84131380894881));
#411675=CARTESIAN_POINT('Ctrl Pts',(-1.29586581063539,-0.779870624372747,
-7.83235096665115));
#411676=CARTESIAN_POINT('Ctrl Pts',(-1.05556652732417,-1.08312857069952,
-7.81236573014992));
#411677=CARTESIAN_POINT('Ctrl Pts',(-0.907314389496485,-1.21002224796578,
-7.80170812147452));
#411678=CARTESIAN_POINT('Ctrl Pts',(-0.566036474274492,-1.40326457176951,
-7.77992053779481));
#411679=CARTESIAN_POINT('Ctrl Pts',(-0.375192730029538,-1.46587763026472,
-7.76899931224386));
#411680=CARTESIAN_POINT('Ctrl Pts',(0.0112058963216531,-1.51197211392253,
-7.74912829734184));
#411681=CARTESIAN_POINT('Ctrl Pts',(0.202637680581194,-1.49837613065379,
-7.7402054825656));
#411682=CARTESIAN_POINT('Ctrl Pts',(0.575418572063417,-1.39897726956634,
-7.71950897408711));
#411683=CARTESIAN_POINT('Ctrl Pts',(0.752705296176225,-1.31212531947842,
-7.70856670842715));
#411684=CARTESIAN_POINT('Ctrl Pts',(1.06647525919953,-1.07337091032947,
-7.68683837712175));
#411685=CARTESIAN_POINT('Ctrl Pts',(1.19917431145225,-0.922769058598675,
-7.67627050622317));
#411686=CARTESIAN_POINT('Ctrl Pts',(1.39397565077775,-0.585754321668215,
-7.65753660194471));
#411687=CARTESIAN_POINT('Ctrl Pts',(1.45705662752588,-0.404129060630502,
-7.64745161447954));
#411688=CARTESIAN_POINT('Ctrl Pts',(1.51287229333397,-0.0196343197293993,
-7.62609079554058));
#411689=CARTESIAN_POINT('Ctrl Pts',(1.50226400674775,0.179932317560216,
-7.61500376013561));
#411690=CARTESIAN_POINT('Ctrl Pts',(1.40487393979614,0.560713900206558,
-7.59384922776636));
#411691=CARTESIAN_POINT('Ctrl Pts',(1.32012483986009,0.738466283954311,
-7.5846682503061));
#411692=CARTESIAN_POINT('Ctrl Pts',(1.08868961728264,1.04972226780596,-7.56488731841674));
#411693=CARTESIAN_POINT('Ctrl Pts',(0.944928743537071,1.18078550033665,
-7.55432997480567));
#411694=CARTESIAN_POINT('Ctrl Pts',(0.609202422940334,1.38528831244161,
-7.5324967010052));
#411695=CARTESIAN_POINT('Ctrl Pts',(0.418890910224135,1.45419997592632,
-7.52142612120591));
#411696=CARTESIAN_POINT('Ctrl Pts',(0.147445685704055,1.49456941122877,
-7.50724483354916));
#411697=CARTESIAN_POINT('Ctrl Pts',(0.0736975207194608,1.50000000000006,
-7.50354577361881));
#411698=CARTESIAN_POINT('Ctrl Pts',(5.09592368302956E-14,1.50000000000006,
-7.49999999999998));
#411699=CARTESIAN_POINT('Origin',(0.,2.5406128344257E-15,14.));
#411700=CARTESIAN_POINT('',(-4.77560189507343E-15,1.50000000000006,-6.9375));
#411701=CARTESIAN_POINT('',(-9.18485099360549E-17,1.50000000000006,-6.99999999999998));
#411702=CARTESIAN_POINT('',(-1.8369701987211E-16,1.50000000000006,14.));
#411703=CARTESIAN_POINT('Ctrl Pts',(-2.70616862252382E-15,1.50000000000006,
-6.9375));
#411704=CARTESIAN_POINT('Ctrl Pts',(0.192169407202027,1.50000000000006,
-6.94674575491484));
#411705=CARTESIAN_POINT('Ctrl Pts',(0.382677420613757,1.46307171491065,
-6.95693736168064));
#411706=CARTESIAN_POINT('Ctrl Pts',(0.742699722204964,1.31785219373169,
-6.97829281833044));
#411707=CARTESIAN_POINT('Ctrl Pts',(0.908203259366283,1.20975569530316,
-6.98925829148667));
#411708=CARTESIAN_POINT('Ctrl Pts',(1.18423666452601,0.940064710726509,
-7.01003037112276));
#411709=CARTESIAN_POINT('Ctrl Pts',(1.29369671188414,0.782608851879287,
-7.01902173045118));
#411710=CARTESIAN_POINT('Ctrl Pts',(1.45159619429717,0.42712040202094,-7.03877108877665));
#411711=CARTESIAN_POINT('Ctrl Pts',(1.49537080935378,0.231106803664808,
-7.04966073312977));
#411712=CARTESIAN_POINT('Ctrl Pts',(1.50381985831375,-0.161225965822973,
-7.07145699810131));
#411713=CARTESIAN_POINT('Ctrl Pts',(1.47048939491555,-0.353755446754854,
-7.0821530803753));
#411714=CARTESIAN_POINT('Ctrl Pts',(1.33268963618317,-0.714976358151295,
-7.10222090878621));
#411715=CARTESIAN_POINT('Ctrl Pts',(1.22975401776601,-0.88031848372283,
-7.11112005678171));
#411716=CARTESIAN_POINT('Ctrl Pts',(0.962851266472294,-1.16724498350365,
-7.13193160194008));
#411717=CARTESIAN_POINT('Ctrl Pts',(0.79980901962617,-1.28446099149317,
-7.14303197592083));
#411718=CARTESIAN_POINT('Ctrl Pts',(0.444363004845952,-1.44539102120805,
-7.16460365888367));
#411719=CARTESIAN_POINT('Ctrl Pts',(0.256521262648118,-1.49024580454317,
-7.17488716512267));
#411720=CARTESIAN_POINT('Ctrl Pts',(-0.134304007193784,-1.50727538523723,
-7.19416379859328));
#411721=CARTESIAN_POINT('Ctrl Pts',(-0.333680125512914,-1.47601109531253,
-7.20422055098758));
#411722=CARTESIAN_POINT('Ctrl Pts',(-0.705223902700816,-1.33836110897974,
-7.22592007003365));
#411723=CARTESIAN_POINT('Ctrl Pts',(-0.874170307055552,-1.23465777401047,
-7.23692915589664));
#411724=CARTESIAN_POINT('Ctrl Pts',(-1.15780181295661,-0.972405967335528,
-7.2578601554945));
#411725=CARTESIAN_POINT('Ctrl Pts',(-1.27147903464108,-0.818169802504755,
-7.26704612208311));
#411726=CARTESIAN_POINT('Ctrl Pts',(-1.43913063758303,-0.467394654101727,
-7.28653363032772));
#411727=CARTESIAN_POINT('Ctrl Pts',(-1.48834382299317,-0.27270139551403,
-7.29734992247148));
#411728=CARTESIAN_POINT('Ctrl Pts',(-1.50775766368768,0.119736123770694,
-7.31915200687619));
#411729=CARTESIAN_POINT('Ctrl Pts',(-1.47963375324009,0.313633208613137,
-7.32992406714521));
#411730=CARTESIAN_POINT('Ctrl Pts',(-1.35175556934947,0.677950891998563,
-7.3501639384444));
#411731=CARTESIAN_POINT('Ctrl Pts',(-1.25399669761929,0.845194191670035,
-7.3589780055242));
#411732=CARTESIAN_POINT('Ctrl Pts',(-0.995792057819326,1.13937273054366,
-7.37957250812857));
#411733=CARTESIAN_POINT('Ctrl Pts',(-0.835667372739517,1.2615152013883,
-7.39066935704381));
#411734=CARTESIAN_POINT('Ctrl Pts',(-0.483855828346957,1.43272224383282,
-7.41235164904442));
#411735=CARTESIAN_POINT('Ctrl Pts',(-0.296801282743105,1.48281448701481,
-7.42274276626538));
#411736=CARTESIAN_POINT('Ctrl Pts',(-0.0702489658411354,1.49876759045962,
-7.4340859114568));
#411737=CARTESIAN_POINT('Ctrl Pts',(-0.0351062050691992,1.50000000000005,
-7.43581095192109));
#411738=CARTESIAN_POINT('Ctrl Pts',(-2.03836947321191E-13,1.50000000000006,
-7.43749999999999));
#411739=CARTESIAN_POINT('Ctrl Pts',(5.14172038279526E-14,1.50000000000006,
-7.49999999999998));
#411740=CARTESIAN_POINT('Ctrl Pts',(-0.116196176765652,1.50000000000006,
-7.49440950883878));
#411741=CARTESIAN_POINT('Ctrl Pts',(-0.2322300038428,1.48650197062597,-7.4884518834703));
#411742=CARTESIAN_POINT('Ctrl Pts',(-0.535551554263825,1.41464350471122,
-7.47186225007378));
#411743=CARTESIAN_POINT('Ctrl Pts',(-0.714729433285352,1.33311116898231,
-7.46097676324637));
#411744=CARTESIAN_POINT('Ctrl Pts',(-1.03488686131942,1.10386586919407,
-7.43920525681404));
#411745=CARTESIAN_POINT('Ctrl Pts',(-1.17192391894225,0.957146838268963,
-7.42853652966828));
#411746=CARTESIAN_POINT('Ctrl Pts',(-1.37621483367608,0.626224824630856,
-7.40951530029378));
#411747=CARTESIAN_POINT('Ctrl Pts',(-1.4444387423633,0.446945444846318,
-7.39983030249153));
#411748=CARTESIAN_POINT('Ctrl Pts',(-1.51151136657269,0.0653142775771098,
-7.37862857097657));
#411749=CARTESIAN_POINT('Ctrl Pts',(-1.50698852864842,-0.133866114778471,
-7.36756299362348));
#411750=CARTESIAN_POINT('Ctrl Pts',(-1.42122317854349,-0.518496140675042,
-7.34619465885145));
#411751=CARTESIAN_POINT('Ctrl Pts',(-1.34104949567623,-0.700202904909598,
-7.33673785991857));
#411752=CARTESIAN_POINT('Ctrl Pts',(-1.11771606063643,-1.01866065302193,
-7.31714667645662));
#411753=CARTESIAN_POINT('Ctrl Pts',(-0.978111849779189,-1.15335892026023,
-7.30668834719569));
#411754=CARTESIAN_POINT('Ctrl Pts',(-0.649366617591477,-1.36683379620112,
-7.28494172717246));
#411755=CARTESIAN_POINT('Ctrl Pts',(-0.46174017790655,-1.44108321246924,
-7.27385206209897));
#411756=CARTESIAN_POINT('Ctrl Pts',(-0.0766622937430506,-1.51022042322309,
-7.25340451568241));
#411757=CARTESIAN_POINT('Ctrl Pts',(0.116456016918941,-1.50767431930412,
-7.24461018280988));
#411758=CARTESIAN_POINT('Ctrl Pts',(0.494342973444443,-1.42948992987289,
-7.2242572995418));
#411759=CARTESIAN_POINT('Ctrl Pts',(0.675293422908971,-1.35343442244846,
-7.21343866399876));
#411760=CARTESIAN_POINT('Ctrl Pts',(1.00168332648149,-1.13408805910721,
-7.19164226790414));
#411761=CARTESIAN_POINT('Ctrl Pts',(1.14303552835425,-0.99147254996331,
-7.18087991499999));
#411762=CARTESIAN_POINT('Ctrl Pts',(1.35696120970833,-0.666869061643454,
-7.16157064729252));
#411763=CARTESIAN_POINT('Ctrl Pts',(1.43041383923171,-0.48989658305268,
-7.15221647683633));
#411764=CARTESIAN_POINT('Ctrl Pts',(1.50874884321075,-0.111242738002618,
-7.13118015211132));
#411765=CARTESIAN_POINT('Ctrl Pts',(1.51031929183533,0.0873668471844137,
-7.1201462862676));
#411766=CARTESIAN_POINT('Ctrl Pts',(1.43636261111108,0.475722293543195,
-7.09857098369211));
#411767=CARTESIAN_POINT('Ctrl Pts',(1.36083598674517,0.661474591233649,
-7.08876562440499));
#411768=CARTESIAN_POINT('Ctrl Pts',(1.14563340563647,0.987057425931803,
-7.06936771776336));
#411769=CARTESIAN_POINT('Ctrl Pts',(1.0102402743431,1.1252341506302,-7.05901537034408));
#411770=CARTESIAN_POINT('Ctrl Pts',(0.688647512609778,1.34738325925165,
-7.03737192280824));
#411771=CARTESIAN_POINT('Ctrl Pts',(0.503824987368593,1.42683143991068,
-7.02627275100935));
#411772=CARTESIAN_POINT('Ctrl Pts',(0.207068836892841,1.48927712163816,
-7.01026046179241));
#411773=CARTESIAN_POINT('Ctrl Pts',(0.103562773678466,1.50000000000006,
-7.00498266627175));
#411774=CARTESIAN_POINT('Ctrl Pts',(2.16840434497101E-15,1.50000000000006,
-6.99999999999998));
#411775=CARTESIAN_POINT('Origin',(0.,2.5406128344257E-15,14.));
#411776=CARTESIAN_POINT('',(3.81275791127862E-14,1.50000000000006,-6.43750000000001));
#411777=CARTESIAN_POINT('',(-8.92705129629568E-14,1.50000000000006,-6.49999999999997));
#411778=CARTESIAN_POINT('',(-1.8369701987211E-16,1.50000000000006,14.));
#411779=CARTESIAN_POINT('Ctrl Pts',(7.64388552454446E-14,1.50000000000006,
-6.43750000000001));
#411780=CARTESIAN_POINT('Ctrl Pts',(0.0223909192234641,1.50000000000006,
-6.43857728360342));
#411781=CARTESIAN_POINT('Ctrl Pts',(0.0447986082402546,1.49949865191963,
-6.43966930037949));
#411782=CARTESIAN_POINT('Ctrl Pts',(0.265859390180722,1.48958421860951,
-6.45058049313482));
#411783=CARTESIAN_POINT('Ctrl Pts',(0.460739231284261,1.44126257265004,
-6.46129892180487));
#411784=CARTESIAN_POINT('Ctrl Pts',(0.816561570005715,1.27323910504439,
-6.48308575060318));
#411785=CARTESIAN_POINT('Ctrl Pts',(0.974775881668512,1.1566036373632,-6.49393771432445));
#411786=CARTESIAN_POINT('Ctrl Pts',(1.2353063956038,0.872078159699014,-6.51437598001117));
#411787=CARTESIAN_POINT('Ctrl Pts',(1.3362083087437,0.707846967653049,-6.52317516846374));
#411788=CARTESIAN_POINT('Ctrl Pts',(1.47417508943286,0.341832574128559,
-6.54350930143733));
#411789=CARTESIAN_POINT('Ctrl Pts',(1.50657223000472,0.142363393853101,
-6.55459092256374));
#411790=CARTESIAN_POINT('Ctrl Pts',(1.49151053899438,-0.249870029880412,
-6.57638166832671));
#411791=CARTESIAN_POINT('Ctrl Pts',(1.44718195164507,-0.439000366867817,
-6.58688890927046));
#411792=CARTESIAN_POINT('Ctrl Pts',(1.28803882385816,-0.793305960409002,
-6.60657255335608));
#411793=CARTESIAN_POINT('Ctrl Pts',(1.17354741695466,-0.954555822388696,
-6.61588644642036));
#411794=CARTESIAN_POINT('Ctrl Pts',(0.887764635743559,-1.22512200487875,
-6.63715190418358));
#411795=CARTESIAN_POINT('Ctrl Pts',(0.718825168003851,-1.33129149568386,
-6.6482291606373));
#411796=CARTESIAN_POINT('Ctrl Pts',(0.356301293923391,-1.46945047798051,
-6.66950884816954));
#411797=CARTESIAN_POINT('Ctrl Pts',(0.167199836508386,-1.5027415271631,
-6.679379440583));
#411798=CARTESIAN_POINT('Ctrl Pts',(-0.22180495506119,-1.49677377368313,
-6.69826121327373));
#411799=CARTESIAN_POINT('Ctrl Pts',(-0.417989425653454,-1.45423103388989,
-6.70888188578804));
#411800=CARTESIAN_POINT('Ctrl Pts',(-0.779096298556415,-1.29658665327939,
-6.73063465888362));
#411801=CARTESIAN_POINT('Ctrl Pts',(-0.941094149902954,-1.18426214075912,
-6.74154890948832));
#411802=CARTESIAN_POINT('Ctrl Pts',(-1.20958239972972,-0.907295564462036,
-6.76216007243922));
#411803=CARTESIAN_POINT('Ctrl Pts',(-1.31487261361647,-0.746578398793373,
-6.77102342228929));
#411804=CARTESIAN_POINT('Ctrl Pts',(-1.46362507518425,-0.384817140320505,
-6.79112126998222));
#411805=CARTESIAN_POINT('Ctrl Pts',(-1.50191729668966,-0.185768409758887,
-6.8021795327912));
#411806=CARTESIAN_POINT('Ctrl Pts',(-1.49801122233021,0.207856375514794,
-6.82404757641751));
#411807=CARTESIAN_POINT('Ctrl Pts',(-1.45887389293651,0.398679208278765,
-6.8346488449044));
#411808=CARTESIAN_POINT('Ctrl Pts',(-1.30987828284513,0.756315729510975,
-6.85451754052841));
#411809=CARTESIAN_POINT('Ctrl Pts',(-1.20095467590628,0.919515615594141,
-6.86359447498162));
#411810=CARTESIAN_POINT('Ctrl Pts',(-0.924173665643548,1.19799325378724,
-6.88464659749657));
#411811=CARTESIAN_POINT('Ctrl Pts',(-0.757969455871104,1.30948888087906,
-6.89574020202017));
#411812=CARTESIAN_POINT('Ctrl Pts',(-0.39872030251172,1.45856529901397,
-6.91716559658487));
#411813=CARTESIAN_POINT('Ctrl Pts',(-0.21015490020429,1.49741424319437,
-6.92731709107172));
#411814=CARTESIAN_POINT('Ctrl Pts',(-0.0128951306502747,1.49995844027621,
-6.93687842830057));
#411815=CARTESIAN_POINT('Ctrl Pts',(-0.00644668529117233,1.50000000000006,
-6.93718983370931));
#411816=CARTESIAN_POINT('Ctrl Pts',(0.,1.50000000000006,-6.9375));
#411817=CARTESIAN_POINT('Ctrl Pts',(0.,1.50000000000006,-6.99999999999998));
#411818=CARTESIAN_POINT('Ctrl Pts',(-0.0879059832725243,1.50000000000006,
-6.99577062140783));
#411819=CARTESIAN_POINT('Ctrl Pts',(-0.175831940964182,1.49227389480438,
-6.99132566776287));
#411820=CARTESIAN_POINT('Ctrl Pts',(-0.453702387718148,1.44283121748057,
-6.97658321195666));
#411821=CARTESIAN_POINT('Ctrl Pts',(-0.636225722901142,1.37215593521782,
-6.96583835161314));
#411822=CARTESIAN_POINT('Ctrl Pts',(-0.968405417509316,1.16263860615119,
-6.94403642279729));
#411823=CARTESIAN_POINT('Ctrl Pts',(-1.1138498412067,1.02415656188315,-6.93319200124758));
#411824=CARTESIAN_POINT('Ctrl Pts',(-1.33712258522154,0.70581867676277,
-6.91360706731149));
#411825=CARTESIAN_POINT('Ctrl Pts',(-1.41566700697667,0.531016324411727,
-6.90450090691183));
#411826=CARTESIAN_POINT('Ctrl Pts',(-1.5047766983895,0.155312068231135,
-6.88362844823513));
#411827=CARTESIAN_POINT('Ctrl Pts',(-1.51217018903453,-0.0425775048008003,
-6.87263458306669));
#411828=CARTESIAN_POINT('Ctrl Pts',(-1.44967773118986,-0.434367760739349,
-6.85086845773677));
#411829=CARTESIAN_POINT('Ctrl Pts',(-1.37867283939756,-0.624069013339944,
-6.84066284420873));
#411830=CARTESIAN_POINT('Ctrl Pts',(-1.17127304608703,-0.956393555802605,
-6.82145307970996));
#411831=CARTESIAN_POINT('Ctrl Pts',(-1.03994928531237,-1.09774863442188,
-6.81120823236212));
#411832=CARTESIAN_POINT('Ctrl Pts',(-0.72534010093098,-1.32790780096646,
-6.78967828073932));
#411833=CARTESIAN_POINT('Ctrl Pts',(-0.543302158706279,-1.41219268449493,
-6.77857872939579));
#411834=CARTESIAN_POINT('Ctrl Pts',(-0.162060018073507,-1.50371055676201,
-6.75769404523386));
#411835=CARTESIAN_POINT('Ctrl Pts',(0.0329338251145361,-1.51205838946905,
-6.74875042586349));
#411836=CARTESIAN_POINT('Ctrl Pts',(0.415421593607736,-1.45424864437687,
-6.72874214826915));
#411837=CARTESIAN_POINT('Ctrl Pts',(0.599272213566833,-1.38862246315805,
-6.71807368171384));
#411838=CARTESIAN_POINT('Ctrl Pts',(0.936590590215381,-1.1884214702369,
-6.6962833050582));
#411839=CARTESIAN_POINT('Ctrl Pts',(1.08574482652843,-1.05390894243789,
-6.68537065941216));
#411840=CARTESIAN_POINT('Ctrl Pts',(1.31769575376748,-0.741515702901603,
-6.66553332523502));
#411841=CARTESIAN_POINT('Ctrl Pts',(1.40099501903001,-0.568673068221014,
-6.65659294823457));
#411842=CARTESIAN_POINT('Ctrl Pts',(1.4999833846104,-0.195757297541112,
-6.63587540541902));
#411843=CARTESIAN_POINT('Ctrl Pts',(1.51270083303394,0.00132252290894246,
-6.62492652650512));
#411844=CARTESIAN_POINT('Ctrl Pts',(1.4613485562752,0.392429527145843,-6.60319835960307));
#411845=CARTESIAN_POINT('Ctrl Pts',(1.39652484251627,0.582407371418841,
-6.59267901694039));
#411846=CARTESIAN_POINT('Ctrl Pts',(1.20077481135644,0.91895845751198,-6.57391234789469));
#411847=CARTESIAN_POINT('Ctrl Pts',(1.07439799867235,1.06394985203442,-6.56380450192274));
#411848=CARTESIAN_POINT('Ctrl Pts',(0.768367751834957,1.30338393543321,
-6.54242966804569));
#411849=CARTESIAN_POINT('Ctrl Pts',(0.58980812046137,1.39331623132376,-6.5313405944454));
#411850=CARTESIAN_POINT('Ctrl Pts',(0.268717188983998,1.48190412985531,
-6.51343132484262));
#411851=CARTESIAN_POINT('Ctrl Pts',(0.134539763376071,1.50000000000007,
-6.50647304738347));
#411852=CARTESIAN_POINT('Ctrl Pts',(-1.76178516220205E-13,1.50000000000006,
-6.49999999999997));
#411853=CARTESIAN_POINT('Origin',(0.,2.5406128344257E-15,14.));
#411854=CARTESIAN_POINT('',(1.01826625150654E-13,1.50000000000006,-5.93750000000001));
#411855=CARTESIAN_POINT('',(-7.65307037553822E-14,1.50000000000006,-5.99999999999997));
#411856=CARTESIAN_POINT('',(-1.8369701987211E-16,1.50000000000006,14.));
#411857=CARTESIAN_POINT('Ctrl Pts',(2.0383694732118E-13,1.50000000000006,
-5.93750000000001));
#411858=CARTESIAN_POINT('Ctrl Pts',(0.0510987733573682,1.50000000000006,
-5.93995849087943));
#411859=CARTESIAN_POINT('Ctrl Pts',(0.102250512115221,1.49738908990297,
-5.94249205533837));
#411860=CARTESIAN_POINT('Ctrl Pts',(0.351120582172001,1.47182769766712,
-5.95517586083996));
#411861=CARTESIAN_POINT('Ctrl Pts',(0.542952324057759,1.41235470339066,
-5.96605739744349));
#411862=CARTESIAN_POINT('Ctrl Pts',(0.8876101135387,1.22459778685675,-5.98785522297513));
#411863=CARTESIAN_POINT('Ctrl Pts',(1.03812677018933,1.09990818804658,-5.99856055896165));
#411864=CARTESIAN_POINT('Ctrl Pts',(1.28294801490704,0.800779175428834,
-6.01864866582945));
#411865=CARTESIAN_POINT('Ctrl Pts',(1.37516734553438,0.629380715071977,
-6.02753440471824));
#411866=CARTESIAN_POINT('Ctrl Pts',(1.4914523471381,0.255225392585798,-6.04832081152303));
#411867=CARTESIAN_POINT('Ctrl Pts',(1.51211433236649,0.0554178923829198,
-6.05942122820097));
#411868=CARTESIAN_POINT('Ctrl Pts',(1.47501424209642,-0.333120996333186,
-6.08100672201853));
#411869=CARTESIAN_POINT('Ctrl Pts',(1.42051385648069,-0.518458128546809,
-6.09130322936373));
#411870=CARTESIAN_POINT('Ctrl Pts',(1.2410210843566,-0.865845748277928,
-6.11060254157101));
#411871=CARTESIAN_POINT('Ctrl Pts',(1.11494220537351,-1.02311234989756,
-6.12061043896357));
#411872=CARTESIAN_POINT('Ctrl Pts',(0.811009628192773,-1.27704415020625,
-6.14228706302082));
#411873=CARTESIAN_POINT('Ctrl Pts',(0.637000529064983,-1.37215550622816,
-6.15330106181778));
#411874=CARTESIAN_POINT('Ctrl Pts',(0.268408148724571,-1.48796287055158,
-6.17425184221655));
#411875=CARTESIAN_POINT('Ctrl Pts',(0.078078111214819,-1.5099541291653,
-6.18346696153479));
#411876=CARTESIAN_POINT('Ctrl Pts',(-0.309619763643558,-1.48111078536281,
-6.20292128823044));
#411877=CARTESIAN_POINT('Ctrl Pts',(-0.503022272435722,-1.42706009226701,
-6.21372777891475));
#411878=CARTESIAN_POINT('Ctrl Pts',(-0.853270230066218,-1.24884956416789,
-6.23552938408037));
#411879=CARTESIAN_POINT('Ctrl Pts',(-1.00759611314103,-1.12803237920182,
-6.24631042450745));
#411880=CARTESIAN_POINT('Ctrl Pts',(-1.26011862523612,-0.836013236021564,
-6.26657156240144));
#411881=CARTESIAN_POINT('Ctrl Pts',(-1.35660330600879,-0.668165169819857,
-6.27537971278781));
#411882=CARTESIAN_POINT('Ctrl Pts',(-1.48358411268202,-0.29795776991751,
-6.29594679056016));
#411883=CARTESIAN_POINT('Ctrl Pts',(-1.51001292576806,-0.0982334731576826,
-6.3070425848246));
#411884=CARTESIAN_POINT('Ctrl Pts',(-1.48371466166908,0.292275046451878,
-6.32873750258068));
#411885=CARTESIAN_POINT('Ctrl Pts',(-1.43418576814065,0.479546844896079,
-6.33914149138313));
#411886=CARTESIAN_POINT('Ctrl Pts',(-1.26472362376772,0.830384557303938,
-6.35863247540579));
#411887=CARTESIAN_POINT('Ctrl Pts',(-1.14442804264367,0.989630948410885,
-6.36826176202628));
#411888=CARTESIAN_POINT('Ctrl Pts',(-0.849454429133955,1.25189379400266,
-6.38973876566747));
#411889=CARTESIAN_POINT('Ctrl Pts',(-0.677871610264382,1.35251631573508,
-6.40078911793748));
#411890=CARTESIAN_POINT('Ctrl Pts',(-0.333431466914826,1.47204231443247,
-6.42068116869151));
#411891=CARTESIAN_POINT('Ctrl Pts',(-0.167220233864083,1.50000000000006,
-6.42945461274705));
#411892=CARTESIAN_POINT('Ctrl Pts',(7.42461647718073E-14,1.50000000000006,
-6.43750000000001));
#411893=CARTESIAN_POINT('Ctrl Pts',(-1.78357328906041E-13,1.50000000000006,
-6.49999999999997));
#411894=CARTESIAN_POINT('Ctrl Pts',(-0.0595903002411327,1.50000000000005,
-6.49713296034287));
#411895=CARTESIAN_POINT('Ctrl Pts',(-0.119242125513032,1.49644931569961,
-6.49416433044197));
#411896=CARTESIAN_POINT('Ctrl Pts',(-0.370113691097197,1.46635750255132,
-6.48125838291657));
#411897=CARTESIAN_POINT('Ctrl Pts',(-0.555347452026265,1.40668430766311,
-6.47068873069172));
#411898=CARTESIAN_POINT('Ctrl Pts',(-0.899735077112571,1.21682354738176,
-6.44884546334648));
#411899=CARTESIAN_POINT('Ctrl Pts',(-1.05413164380482,1.08582017118329,
-6.43777807239582));
#411900=CARTESIAN_POINT('Ctrl Pts',(-1.29619584274994,0.778598789967767,
-6.41759782593799));
#411901=CARTESIAN_POINT('Ctrl Pts',(-1.38454342506231,0.607769253882239,
-6.40876495854908));
#411902=CARTESIAN_POINT('Ctrl Pts',(-1.4938179707455,0.237840271712374,
-6.38821334842853));
#411903=CARTESIAN_POINT('Ctrl Pts',(-1.51205448725794,0.0417552688562912,
-6.37731973715875));
#411904=CARTESIAN_POINT('Ctrl Pts',(-1.47206513533382,-0.350046935975517,
-6.35555294800142));
#411905=CARTESIAN_POINT('Ctrl Pts',(-1.41277488246974,-0.541849710410891,
-6.34489723831057));
#411906=CARTESIAN_POINT('Ctrl Pts',(-1.22698498723903,-0.883542857306007,
-6.32591428570529));
#411907=CARTESIAN_POINT('Ctrl Pts',(-1.10522364937168,-1.03182450512569,
-6.31617997248098));
#411908=CARTESIAN_POINT('Ctrl Pts',(-0.807172993588271,-1.27962322772243,
-6.29495670576867));
#411909=CARTESIAN_POINT('Ctrl Pts',(-0.63195745332706,-1.37462575956,-6.28388768493963));
#411910=CARTESIAN_POINT('Ctrl Pts',(-0.255634334161712,-1.49106465969635,
-6.26254741653425));
#411911=CARTESIAN_POINT('Ctrl Pts',(-0.0583387744756356,-1.51168935334255,
-6.25313152985522));
#411912=CARTESIAN_POINT('Ctrl Pts',(0.328834283097292,-1.47609403814029,
-6.23351489868188));
#411913=CARTESIAN_POINT('Ctrl Pts',(0.515155646496236,-1.42182325827318,
-6.22304298624273));
#411914=CARTESIAN_POINT('Ctrl Pts',(0.863853447184978,-1.24245742104462,
-6.20128387111747));
#411915=CARTESIAN_POINT('Ctrl Pts',(1.02154251735958,-1.1164262843335,-6.1901961872827));
#411916=CARTESIAN_POINT('Ctrl Pts',(1.2727472828134,-0.816526860684084,
-6.16977955282384));
#411917=CARTESIAN_POINT('Ctrl Pts',(1.36639478227305,-0.647740995638743,
-6.16098561086889));
#411918=CARTESIAN_POINT('Ctrl Pts',(1.48623755001811,-0.280967317389404,
-6.14060929541059));
#411919=CARTESIAN_POINT('Ctrl Pts',(1.51010841709342,-0.0860643245424332,
-6.12978135136354));
#411920=CARTESIAN_POINT('Ctrl Pts',(1.48180480103135,0.306231837685586,
-6.10798712012865));
#411921=CARTESIAN_POINT('Ctrl Pts',(1.42821715856248,0.499742212899848,
-6.09723654373264));
#411922=CARTESIAN_POINT('Ctrl Pts',(1.24863114595614,0.854688722499666,
-6.07751729319949));
#411923=CARTESIAN_POINT('Ctrl Pts',(1.12439779350244,1.01258611140633,-6.06763688874604));
#411924=CARTESIAN_POINT('Ctrl Pts',(0.823302480797979,1.26918280696206,
-6.04602274777158));
#411925=CARTESIAN_POINT('Ctrl Pts',(0.650045418940008,1.36605055780344,
-6.03499614263965));
#411926=CARTESIAN_POINT('Ctrl Pts',(0.313274881536552,1.4753481073596,-6.015757219561));
#411927=CARTESIAN_POINT('Ctrl Pts',(0.157027605796477,1.50000000000007,
-6.00755499420638));
#411928=CARTESIAN_POINT('Ctrl Pts',(-1.55535306856081E-13,1.50000000000006,
-5.99999999999997));
#411929=CARTESIAN_POINT('Origin',(0.,2.5406128344257E-15,14.));
#411930=CARTESIAN_POINT('',(1.26479606976381E-14,1.50000000000006,-5.4375));
#411931=CARTESIAN_POINT('',(3.43726226250065E-8,1.50000000000006,-5.50000000330749));
#411932=CARTESIAN_POINT('',(-1.8369701987211E-16,1.50000000000006,14.));
#411933=CARTESIAN_POINT('Ctrl Pts',(2.54796184151483E-14,1.50000000000006,
-5.4375));
#411934=CARTESIAN_POINT('Ctrl Pts',(0.0795944837401856,1.50000000000006,
-5.44132949138445));
#411935=CARTESIAN_POINT('Ctrl Pts',(0.15922969186804,1.49366568974591,-5.44533689518454));
#411936=CARTESIAN_POINT('Ctrl Pts',(0.435800272974986,1.44918926665121,
-5.45987885966928));
#411937=CARTESIAN_POINT('Ctrl Pts',(0.625072366798754,1.37816585861796,
-5.47095808997459));
#411938=CARTESIAN_POINT('Ctrl Pts',(0.958079568685715,1.17010572017913,
-5.49275935473552));
#411939=CARTESIAN_POINT('Ctrl Pts',(1.10021566829197,1.03759688973605,-5.50327868186193));
#411940=CARTESIAN_POINT('Ctrl Pts',(1.32847369204001,0.723504427834313,
-5.52298554175827));
#411941=CARTESIAN_POINT('Ctrl Pts',(1.41143431922926,0.544210755578284,
-5.53226606913455));
#411942=CARTESIAN_POINT('Ctrl Pts',(1.5042825817161,0.161904499934741,-5.55350530555919));
#411943=CARTESIAN_POINT('Ctrl Pts',(1.51250349955024,-0.0375323642426384,
-5.56458513134683));
#411944=CARTESIAN_POINT('Ctrl Pts',(1.45226919806415,-0.420916767003066,
-5.58588426483352));
#411945=CARTESIAN_POINT('Ctrl Pts',(1.38717863442111,-0.601616447661832,
-5.59580423815753));
#411946=CARTESIAN_POINT('Ctrl Pts',(1.18866924285327,-0.936265388385543,
-5.61465082962138));
#411947=CARTESIAN_POINT('Ctrl Pts',(1.05426528172485,-1.08536896823951,
-5.62525910932324));
#411948=CARTESIAN_POINT('Ctrl Pts',(0.73797091627172,-1.32043673692573,
-5.64700648931765));
#411949=CARTESIAN_POINT('Ctrl Pts',(0.559928386797814,-1.40521926727854,
-5.65792763479848));
#411950=CARTESIAN_POINT('Ctrl Pts',(0.186138296614603,-1.5005351890038,
-5.67855928338982));
#411951=CARTESIAN_POINT('Ctrl Pts',(-0.00559503723360701,-1.51202380497154,
-5.68743519677188));
#411952=CARTESIAN_POINT('Ctrl Pts',(-0.393461389634301,-1.46133488882452,
-5.70750445080109));
#411953=CARTESIAN_POINT('Ctrl Pts',(-0.585287170187141,-1.39561205665681,
-5.71855930719795));
#411954=CARTESIAN_POINT('Ctrl Pts',(-0.925016032529776,-1.19649970050167,
-5.74043541849045));
#411955=CARTESIAN_POINT('Ctrl Pts',(-1.07118271998264,-1.06763747941812,
-5.75104737266061));
#411956=CARTESIAN_POINT('Ctrl Pts',(-1.30735011096432,-0.760635726307789,
-5.77093780803232));
#411957=CARTESIAN_POINT('Ctrl Pts',(-1.39475081741657,-0.585155686287264,
-5.77999135076184));
#411958=CARTESIAN_POINT('Ctrl Pts',(-1.49886490316819,-0.2066802660096,
-5.80101776299948));
#411959=CARTESIAN_POINT('Ctrl Pts',(-1.51302935444535,-0.00697212379655653,
-5.81211265978909));
#411960=CARTESIAN_POINT('Ctrl Pts',(-1.46382445182473,0.378989125746192,
-5.83355495143036));
#411961=CARTESIAN_POINT('Ctrl Pts',(-1.40378576732709,0.561982200655421,
-5.84372123336976));
#411962=CARTESIAN_POINT('Ctrl Pts',(-1.21447194321652,0.902527345162545,
-5.8626404080646));
#411963=CARTESIAN_POINT('Ctrl Pts',(-1.08430982587707,1.05537707770781,
-5.87298048244842));
#411964=CARTESIAN_POINT('Ctrl Pts',(-0.774204305694343,1.29960365670428,
-5.89468451288344));
#411965=CARTESIAN_POINT('Ctrl Pts',(-0.598071925790781,1.38948781563103,
-5.90565546815504));
#411966=CARTESIAN_POINT('Ctrl Pts',(-0.276132584520466,1.48088242042997,
-5.92368352095599));
#411967=CARTESIAN_POINT('Ctrl Pts',(-0.138285900790439,1.50000000000006,
-5.93084671649612));
#411968=CARTESIAN_POINT('Ctrl Pts',(2.02650396463611E-13,1.50000000000006,
-5.93750000000001));
#411969=CARTESIAN_POINT('Ctrl Pts',(-1.52877710490892E-13,1.50000000000006,
-5.99999999999997));
#411970=CARTESIAN_POINT('Ctrl Pts',(-0.0323929666453449,1.50000000000005,
-5.9984414926656));
#411971=CARTESIAN_POINT('Ctrl Pts',(-0.0648163575003628,1.49895072128399,
-5.99685237491475));
#411972=CARTESIAN_POINT('Ctrl Pts',(-0.295674150388503,1.48395653246627,
-5.98532871893077));
#411973=CARTESIAN_POINT('Ctrl Pts',(-0.489567254683016,1.43173032325572,
-5.97454930456728));
#411974=CARTESIAN_POINT('Ctrl Pts',(-0.841627107281658,1.25675283670217,
-5.95275033127395));
#411975=CARTESIAN_POINT('Ctrl Pts',(-0.997206350427106,1.13725736378339,
-5.94194570275591));
#411976=CARTESIAN_POINT('Ctrl Pts',(-1.25229285749514,0.847625748925076,
-5.92162752482742));
#411977=CARTESIAN_POINT('Ctrl Pts',(-1.35019291269777,0.680944445183578,
-5.91283024695462));
#411978=CARTESIAN_POINT('Ctrl Pts',(-1.48070595156035,0.312069812220314,
-5.89233721178999));
#411979=CARTESIAN_POINT('Ctrl Pts',(-1.5090491438535,0.112408640779034,
-5.8812449244877));
#411980=CARTESIAN_POINT('Ctrl Pts',(-1.48634874747747,-0.278687847272671,
-5.85951734181816));
#411981=CARTESIAN_POINT('Ctrl Pts',(-1.43848179378996,-0.466571689567029,
-5.84907935057959));
#411982=CARTESIAN_POINT('Ctrl Pts',(-1.27233558890935,-0.818532709912457,
-5.8295259605604));
#411983=CARTESIAN_POINT('Ctrl Pts',(-1.1539210474878,-0.978425934983905,
-5.8200062207552));
#411984=CARTESIAN_POINT('Ctrl Pts',(-0.861904234968412,-1.24338603709022,
-5.79859655247592));
#411985=CARTESIAN_POINT('Ctrl Pts',(-0.691155026874305,-1.34580496779026,
-5.78753640707394));
#411986=CARTESIAN_POINT('Ctrl Pts',(-0.32650762138883,-1.47632419313749,
-5.76636676656016));
#411987=CARTESIAN_POINT('Ctrl Pts',(-0.137019981631298,-1.50576570776158,
-5.75675253548884));
#411988=CARTESIAN_POINT('Ctrl Pts',(0.251593498909031,-1.49205864866609,
-5.73767460904724));
#411989=CARTESIAN_POINT('Ctrl Pts',(0.44691574301208,-1.44560713225594,
-5.72698684329599));
#411990=CARTESIAN_POINT('Ctrl Pts',(0.804485093324531,-1.28093116860153,
-5.70520894758419));
#411991=CARTESIAN_POINT('Ctrl Pts',(0.963938915732993,-1.16568062196933,
-5.69433581790351));
#411992=CARTESIAN_POINT('Ctrl Pts',(1.22705706108838,-0.883600522245535,
-5.67384098190704));
#411993=CARTESIAN_POINT('Ctrl Pts',(1.32938548142279,-0.720520643564737,
-5.66502892464246));
#411994=CARTESIAN_POINT('Ctrl Pts',(1.47087362554104,-0.355880128331265,
-5.6447711182406));
#411995=CARTESIAN_POINT('Ctrl Pts',(1.50519202463025,-0.156529588792126,
-5.63369608826621));
#411996=CARTESIAN_POINT('Ctrl Pts',(1.4937598411501,0.236191378066057,-5.61187825677409));
#411997=CARTESIAN_POINT('Ctrl Pts',(1.45111716001254,0.425888946128527,
-5.60133950299284));
#411998=CARTESIAN_POINT('Ctrl Pts',(1.2952852599377,0.781290057897524,-5.58159499678345));
#411999=CARTESIAN_POINT('Ctrl Pts',(1.18262570593498,0.943177834697634,
-5.5723663881755));
#412000=CARTESIAN_POINT('Ctrl Pts',(0.8997847440267,1.21635276615106,-5.55117000351049));
#412001=CARTESIAN_POINT('Ctrl Pts',(0.731723497799739,1.32427458714632,
-5.54008632467039));
#412002=CARTESIAN_POINT('Ctrl Pts',(0.373037218568292,1.46492065660309,
-5.51892218775196));
#412003=CARTESIAN_POINT('Ctrl Pts',(0.187294198304379,1.49999999569822,
-5.50901119643687));
#412004=CARTESIAN_POINT('Ctrl Pts',(3.44525195872247E-8,1.50000000000006,
-5.50000000165758));
#412005=CARTESIAN_POINT('Origin',(0.,2.5406128344257E-15,14.));
#412006=CARTESIAN_POINT('',(-1.28316577175103E-14,1.50000000000006,-4.9375));
#412007=CARTESIAN_POINT('',(5.08673883203602E-14,1.50000000000006,-4.99999999999998));
#412008=CARTESIAN_POINT('',(-1.8369701987211E-16,1.50000000000006,14.));
#412009=CARTESIAN_POINT('Ctrl Pts',(-2.76167977375508E-14,1.50000000000006,
-4.9375));
#412010=CARTESIAN_POINT('Ctrl Pts',(0.109269337069246,1.50000000000006,
-4.94275722343093));
#412011=CARTESIAN_POINT('Ctrl Pts',(0.218442531916599,1.48806306207715,
-4.94834140282602));
#412012=CARTESIAN_POINT('Ctrl Pts',(0.519839210729197,1.4210434978429,-4.96470401185852));
#412013=CARTESIAN_POINT('Ctrl Pts',(0.703550414914408,1.33962857731798,
-4.97580434686111));
#412014=CARTESIAN_POINT('Ctrl Pts',(1.02234269722919,1.11421518287066,-4.99740373087437));
#412015=CARTESIAN_POINT('Ctrl Pts',(1.15609916907398,0.974739148629399,
-5.00771342641097));
#412016=CARTESIAN_POINT('Ctrl Pts',(1.36815812327421,0.64642889660756,-5.02703584682477));
#412017=CARTESIAN_POINT('Ctrl Pts',(1.44187087134556,0.459093108451167,
-5.03699482730827));
#412018=CARTESIAN_POINT('Ctrl Pts',(1.51122419412768,0.0693366424525717,
-5.0586479643082));
#412019=CARTESIAN_POINT('Ctrl Pts',(1.5073042347895,-0.129003083014963,
-5.06966683794528));
#412020=CARTESIAN_POINT('Ctrl Pts',(1.42462434211619,-0.506479220501661,
-5.09063773447232));
#412021=CARTESIAN_POINT('Ctrl Pts',(1.3491296193332,-0.682572342742748,
-5.09988364711283));
#412022=CARTESIAN_POINT('Ctrl Pts',(1.13144981391291,-1.00467588146163,
-5.11930409215418));
#412023=CARTESIAN_POINT('Ctrl Pts',(0.988442453312266,-1.14564911851928,
-5.13010046025069));
#412024=CARTESIAN_POINT('Ctrl Pts',(0.659696086921869,-1.36107394947,-5.1519013002602));
#412025=CARTESIAN_POINT('Ctrl Pts',(0.478096294840362,-1.4349761464713,
-5.16269136313604));
#412026=CARTESIAN_POINT('Ctrl Pts',(0.0992354215259686,-1.50894882765366,
-5.18297411210168));
#412027=CARTESIAN_POINT('Ctrl Pts',(-0.0942526461744661,-1.50926821554021,
-5.19177728212173));
#412028=CARTESIAN_POINT('Ctrl Pts',(-0.478585218942584,-1.43554379017561,
-5.21231639235513));
#412029=CARTESIAN_POINT('Ctrl Pts',(-0.665109437551782,-1.35920826021576,
-5.22341097439494));
#412030=CARTESIAN_POINT('Ctrl Pts',(-0.991027454802751,-1.14224485890758,
-5.24511847345852));
#412031=CARTESIAN_POINT('Ctrl Pts',(-1.12896161876897,-1.00614326332682,
-5.25553543389379));
#412032=CARTESIAN_POINT('Ctrl Pts',(-1.34906238708656,-0.684840480971374,
-5.27505011433453));
#412033=CARTESIAN_POINT('Ctrl Pts',(-1.42739574278363,-0.501534207257007,
-5.28463698848573));
#412034=CARTESIAN_POINT('Ctrl Pts',(-1.50848317223173,-0.115405944629524,
-5.3060885586317));
#412035=CARTESIAN_POINT('Ctrl Pts',(-1.5105810897978,0.0835694927427195,
-5.31714274959683));
#412036=CARTESIAN_POINT('Ctrl Pts',(-1.43902654246891,0.464029024789088,
-5.33827939026607));
#412037=CARTESIAN_POINT('Ctrl Pts',(-1.36873250934293,0.642385562050137,
-5.34782420316381));
#412038=CARTESIAN_POINT('Ctrl Pts',(-1.16062414028608,0.970820501985276,
-5.36696001451442));
#412039=CARTESIAN_POINT('Ctrl Pts',(-1.02186611078168,1.11593292892111,
-5.37766691406986));
#412040=CARTESIAN_POINT('Ctrl Pts',(-0.69920801948096,1.34128499831296,
-5.39945058843091));
#412041=CARTESIAN_POINT('Ctrl Pts',(-0.519309753398982,1.42065610626999,
-5.41031070079215));
#412042=CARTESIAN_POINT('Ctrl Pts',(-0.220948667218012,1.48778609346505,
-5.42653032711053));
#412043=CARTESIAN_POINT('Ctrl Pts',(-0.110530101937365,1.50000000000006,
-5.43218211799108));
#412044=CARTESIAN_POINT('Ctrl Pts',(2.47371567674293E-14,1.50000000000006,
-5.4375));
#412045=CARTESIAN_POINT('Ctrl Pts',(3.445252073021E-8,1.50000000000006,
-5.50000000165758));
#412046=CARTESIAN_POINT('Ctrl Pts',(-0.0030264165990009,1.50000000006957,
-5.4998543914654));
#412047=CARTESIAN_POINT('Ctrl Pts',(-0.00605324838429755,1.49999084073414,
-5.49970850852725));
#412048=CARTESIAN_POINT('Ctrl Pts',(-0.20788471157704,1.49876900874675,
-5.48996394794938));
#412049=CARTESIAN_POINT('Ctrl Pts',(-0.404443727576196,1.45805455571796,
-5.47937604085424));
#412050=CARTESIAN_POINT('Ctrl Pts',(-0.767152755435887,1.30371527062883,
-5.45763799225129));
#412051=CARTESIAN_POINT('Ctrl Pts',(-0.930319052752223,1.19277390477609,
-5.44670594550442));
#412052=CARTESIAN_POINT('Ctrl Pts',(-1.20130239453414,0.918201320588246,
-5.42604123716667));
#412053=CARTESIAN_POINT('Ctrl Pts',(-1.30797008719554,0.758570011130649,
-5.41714277839612));
#412054=CARTESIAN_POINT('Ctrl Pts',(-1.46007803199233,0.398158926653063,
-5.39711994036959));
#412055=CARTESIAN_POINT('Ctrl Pts',(-1.50020986801038,0.199275680323789,
-5.38607087112908));
#412056=CARTESIAN_POINT('Ctrl Pts',(-1.49979656184853,-0.194719759397786,
-5.36418223558899));
#412057=CARTESIAN_POINT('Ctrl Pts',(-1.46229033066513,-0.386041612060154,
-5.35355324377441));
#412058=CARTESIAN_POINT('Ctrl Pts',(-1.31645491820166,-0.744699508638727,
-5.33362780507561));
#412059=CARTESIAN_POINT('Ctrl Pts',(-1.20923768704089,-0.908504467636363,
-5.32460990679846));
#412060=CARTESIAN_POINT('Ctrl Pts',(-0.935251135154752,-1.18939613626271,
-5.30362517632391));
#412061=CARTESIAN_POINT('Ctrl Pts',(-0.769924675502597,-1.30252333730794,
-5.29252848107396));
#412062=CARTESIAN_POINT('Ctrl Pts',(-0.411715710282321,-1.45497215413585,
-5.27105945484296));
#412063=CARTESIAN_POINT('Ctrl Pts',(-0.223336374296281,-1.49552600518349,
-5.26086955395209));
#412064=CARTESIAN_POINT('Ctrl Pts',(0.16632152960155,-1.50394222476273,
-5.24188834543261));
#412065=CARTESIAN_POINT('Ctrl Pts',(0.363977751682049,-1.46869754317824,
-5.23161859956776));
#412066=CARTESIAN_POINT('Ctrl Pts',(0.731417505948437,-1.32417154059065,
-5.20992553496505));
#412067=CARTESIAN_POINT('Ctrl Pts',(0.897974983620369,-1.21739343234583,
-5.19894597602191));
#412068=CARTESIAN_POINT('Ctrl Pts',(1.17631320393585,-0.949946835432454,
-5.17812535001668));
#412069=CARTESIAN_POINT('Ctrl Pts',(1.28705016781589,-0.793474227452975,
-5.16908190152514));
#412070=CARTESIAN_POINT('Ctrl Pts',(1.44792263388295,-0.439409787751528,
-5.14941165487506));
#412071=CARTESIAN_POINT('Ctrl Pts',(1.49335585960036,-0.243781396431966,
-5.13854341091286));
#412072=CARTESIAN_POINT('Ctrl Pts',(1.50513872685418,0.148615868687943,
-5.11674356285065));
#412073=CARTESIAN_POINT('Ctrl Pts',(1.47338673581346,0.34157600081826,-5.10602355551008));
#412074=CARTESIAN_POINT('Ctrl Pts',(1.33860559942787,0.703747047495497,
-5.08590294180578));
#412075=CARTESIAN_POINT('Ctrl Pts',(1.23725759045547,0.869666870875445,
-5.0770368371623));
#412076=CARTESIAN_POINT('Ctrl Pts',(0.973007151132674,1.15882272906179,
-5.05629097480075));
#412077=CARTESIAN_POINT('Ctrl Pts',(0.810841581687545,1.27755206180981,
-5.04519074318227));
#412078=CARTESIAN_POINT('Ctrl Pts',(0.456475916524015,1.4416321264999,-5.02358353759307));
#412079=CARTESIAN_POINT('Ctrl Pts',(0.268859507157415,1.48808922179552,
-5.0132663640194));
#412080=CARTESIAN_POINT('Ctrl Pts',(0.0516984644742341,1.49933241652207,
-5.00250588751722));
#412081=CARTESIAN_POINT('Ctrl Pts',(0.0258378280804302,1.50000000000006,
-5.0012431230831));
#412082=CARTESIAN_POINT('Ctrl Pts',(1.01918473660593E-13,1.50000000000006,
-4.99999999999998));
#412083=CARTESIAN_POINT('Origin',(0.,2.5406128344257E-15,14.));
#412084=CARTESIAN_POINT('',(-1.14750131378106E-13,1.50000000000006,-4.43749999999999));
#412085=CARTESIAN_POINT('',(1.14566434358229E-13,1.50000000000006,-4.49999999999999));
#412086=CARTESIAN_POINT('',(-1.8369701987211E-16,1.50000000000006,14.));
#412087=CARTESIAN_POINT('Ctrl Pts',(-2.29122276707017E-13,1.50000000000006,
-4.43749999999999));
#412088=CARTESIAN_POINT('Ctrl Pts',(0.140686638566558,1.50000000000008,
-4.44426878905398));
#412089=CARTESIAN_POINT('Ctrl Pts',(0.28092139039079,1.48021278852266,-4.4515654814602));
#412090=CARTESIAN_POINT('Ctrl Pts',(0.606578491376407,1.38606342884529,
-4.4698489260277));
#412091=CARTESIAN_POINT('Ctrl Pts',(0.783829808490253,1.29410824334802,
-4.48093124470678));
#412092=CARTESIAN_POINT('Ctrl Pts',(1.0867563390801,1.05130438926325,-4.50225035570753));
#412093=CARTESIAN_POINT('Ctrl Pts',(1.21128345120294,0.904997383834726,
-4.51222236756474));
#412094=CARTESIAN_POINT('Ctrl Pts',(1.40310466101198,0.566412353089952,
-4.53103264705056));
#412095=CARTESIAN_POINT('Ctrl Pts',(1.46572570783402,0.375695574426209,
-4.54162802364299));
#412096=CARTESIAN_POINT('Ctrl Pts',(1.51259258447563,-0.0156520677943056,
-4.56336955932191));
#412097=CARTESIAN_POINT('Ctrl Pts',(1.49769549865608,-0.21235806681055,
-4.57429767037837));
#412098=CARTESIAN_POINT('Ctrl Pts',(1.39465136130354,-0.584106202407536,
-4.5949503445782));
#412099=CARTESIAN_POINT('Ctrl Pts',(1.30937394853824,-0.75615194678466,
-4.60384027060582));
#412100=CARTESIAN_POINT('Ctrl Pts',(1.07266136335201,-1.06758554856354,
-4.62388004355339));
#412101=CARTESIAN_POINT('Ctrl Pts',(0.920248839321891,-1.20144313925951,
-4.634931260943));
#412102=CARTESIAN_POINT('Ctrl Pts',(0.578508805863792,-1.39736135123195,
-4.65681540852361));
#412103=CARTESIAN_POINT('Ctrl Pts',(0.393978543135256,-1.4601670655122,
-4.66743822810306));
#412104=CARTESIAN_POINT('Ctrl Pts',(0.0102969179095393,-1.51246850181074,
-4.68735093657861));
#412105=CARTESIAN_POINT('Ctrl Pts',(-0.185244500910995,-1.50111857634093,
-4.69638150864055));
#412106=CARTESIAN_POINT('Ctrl Pts',(-0.565342644764746,-1.40347038284783,
-4.71738143893251));
#412107=CARTESIAN_POINT('Ctrl Pts',(-0.745759245698529,-1.31650216516527,
-4.72847752051664));
#412108=CARTESIAN_POINT('Ctrl Pts',(-1.05635088702636,-1.08192531971329,
-4.74993689131214));
#412109=CARTESIAN_POINT('Ctrl Pts',(-1.18535113736414,-0.938832127839702,
-4.76011822963568));
#412110=CARTESIAN_POINT('Ctrl Pts',(-1.38679467642429,-0.605229638034621,
-4.77907692225551));
#412111=CARTESIAN_POINT('Ctrl Pts',(-1.45473095668339,-0.416303676317022,
-4.78937201798239));
#412112=CARTESIAN_POINT('Ctrl Pts',(-1.512522389727,-0.0257554426009429,
-4.81106914207773));
#412113=CARTESIAN_POINT('Ctrl Pts',(-1.5029534509004,0.171820870721142,
-4.82204560392896));
#412114=CARTESIAN_POINT('Ctrl Pts',(-1.40981131471766,0.546396466236992,
-4.84285535923539));
#412115=CARTESIAN_POINT('Ctrl Pts',(-1.32933648675551,0.72039554288347,
-4.85188658909633));
#412116=CARTESIAN_POINT('Ctrl Pts',(-1.10253366911848,1.03633053760265,
-4.87157461682318));
#412117=CARTESIAN_POINT('Ctrl Pts',(-0.955569431244047,1.17321305285376,
-4.88244772910499));
#412118=CARTESIAN_POINT('Ctrl Pts',(-0.621271389160603,1.3789624257096,
-4.90424691151096));
#412119=CARTESIAN_POINT('Ctrl Pts',(-0.438192504050617,1.4475898433492,
-4.91496161563439));
#412120=CARTESIAN_POINT('Ctrl Pts',(-0.165262371926965,1.49317620308316,
-4.92935926050907));
#412121=CARTESIAN_POINT('Ctrl Pts',(-0.0826129292005308,1.50000000000006,
-4.93352528359063));
#412122=CARTESIAN_POINT('Ctrl Pts',(-2.54796184151484E-14,1.50000000000006,
-4.9375));
#412123=CARTESIAN_POINT('Ctrl Pts',(1.00544572667616E-13,1.50000000000006,
-4.99999999999998));
#412124=CARTESIAN_POINT('Ctrl Pts',(-0.17292231118257,1.50000000000006,
-4.99168027142414));
#412125=CARTESIAN_POINT('Ctrl Pts',(-0.344744171988474,1.47010316998468,
-4.98258302079129));
#412126=CARTESIAN_POINT('Ctrl Pts',(-0.692778521710343,1.34487169787487,
-4.96235955832998));
#412127=CARTESIAN_POINT('Ctrl Pts',(-0.862832126126676,1.242635998465,-4.95133796993361));
#412128=CARTESIAN_POINT('Ctrl Pts',(-1.14895166932908,0.982845840631448,
-4.93035564371977));
#412129=CARTESIAN_POINT('Ctrl Pts',(-1.2640152602166,0.829650895874937,
-4.92109171643747));
#412130=CARTESIAN_POINT('Ctrl Pts',(-1.43483033665852,0.480430526065497,
-4.90169058478139));
#412131=CARTESIAN_POINT('Ctrl Pts',(-1.48580573172146,0.286200686399114,
-4.89090003813326));
#412132=CARTESIAN_POINT('Ctrl Pts',(-1.50879309595032,-0.106204351893178,
-4.86909975822813));
#412133=CARTESIAN_POINT('Ctrl Pts',(-1.48237539572975,-0.300516866633261,
-4.85830461852035));
#412134=CARTESIAN_POINT('Ctrl Pts',(-1.35772770294869,-0.665827304141286,
-4.83800959421435));
#412135=CARTESIAN_POINT('Ctrl Pts',(-1.26162996716907,-0.833690626640661,
-4.8292087938013));
#412136=CARTESIAN_POINT('Ctrl Pts',(-1.00624462373624,-1.13018499056488,
-4.80868560618301));
#412137=CARTESIAN_POINT('Ctrl Pts',(-0.847091637501807,-1.25390183086628,
-4.79759177566535));
#412138=CARTESIAN_POINT('Ctrl Pts',(-0.496514174446316,-1.42840698812214,
-4.77587724413045));
#412139=CARTESIAN_POINT('Ctrl Pts',(-0.309744342612185,-1.48018614779825,
-4.76545296641562));
#412140=CARTESIAN_POINT('Ctrl Pts',(0.0784150369271338,-1.5108862399228,
-4.74592485922336));
#412141=CARTESIAN_POINT('Ctrl Pts',(0.276247764099956,-1.48749184875031,
-4.73636157460697));
#412142=CARTESIAN_POINT('Ctrl Pts',(0.651372897503971,-1.36549254627417,
-4.71492448869786));
#412143=CARTESIAN_POINT('Ctrl Pts',(0.824984713488039,-1.2681702002274,
-4.70386818780549));
#412144=CARTESIAN_POINT('Ctrl Pts',(1.11926587085391,-1.01654845378523,
-4.68272008606354));
#412145=CARTESIAN_POINT('Ctrl Pts',(1.23890122426214,-0.866727828361343,
-4.67315154602005));
#412146=CARTESIAN_POINT('Ctrl Pts',(1.41999400300323,-0.522644239024955,
-4.65403579105691));
#412147=CARTESIAN_POINT('Ctrl Pts',(1.47668210722216,-0.330038749918022,
-4.64333548610653));
#412148=CARTESIAN_POINT('Ctrl Pts',(1.51132536145765,0.0620328913360232,
-4.62155372825908));
#412149=CARTESIAN_POINT('Ctrl Pts',(1.49050500756459,0.257596930718835,
-4.61068905940448));
#412150=CARTESIAN_POINT('Ctrl Pts',(1.37639368179086,0.626092620808326,
-4.59021707662173));
#412151=CARTESIAN_POINT('Ctrl Pts',(1.28563530462021,0.795984064244105,
-4.58141115564893));
#412152=CARTESIAN_POINT('Ctrl Pts',(1.03939729146344,1.09988249420353,-4.56112240066277));
#412153=CARTESIAN_POINT('Ctrl Pts',(0.883481933791372,1.22863050053394,
-4.55004458601002));
#412154=CARTESIAN_POINT('Ctrl Pts',(0.537092514099401,1.41372193594228,
-4.52823748852338));
#412155=CARTESIAN_POINT('Ctrl Pts',(0.351344087889412,1.470936179403,-4.51771137865998));
#412156=CARTESIAN_POINT('Ctrl Pts',(0.106649080622681,1.49715980908738,
-4.50521005047585));
#412157=CARTESIAN_POINT('Ctrl Pts',(0.0532953547121679,1.50000000000006,
-4.50256417394911));
#412158=CARTESIAN_POINT('Ctrl Pts',(2.29316565736331E-13,1.50000000000006,
-4.49999999999999));
#412159=CARTESIAN_POINT('Origin',(0.,2.5406128344257E-15,14.));
#412160=CARTESIAN_POINT('',(-6.37908945478066E-14,1.50000000000006,-3.9375));
#412161=CARTESIAN_POINT('',(1.26479606976381E-14,1.50000000000006,-3.99999999999998));
#412162=CARTESIAN_POINT('',(-1.8369701987211E-16,1.50000000000006,14.));
#412163=CARTESIAN_POINT('Ctrl Pts',(-1.28994037673635E-13,1.50000000000006,
-3.9375));
#412164=CARTESIAN_POINT('Ctrl Pts',(0.172039702205682,1.50000000000007,
-3.94577726403165));
#412165=CARTESIAN_POINT('Ctrl Pts',(0.343000950453755,1.47040772692418,
-3.95482464850851));
#412166=CARTESIAN_POINT('Ctrl Pts',(0.690459276951828,1.34606876560196,
-3.97499560507322));
#412167=CARTESIAN_POINT('Ctrl Pts',(0.860717259763783,1.24410703881113,
-3.9860194162792));
#412168=CARTESIAN_POINT('Ctrl Pts',(1.14729861126686,0.984775223523742,
-4.00701122951788));
#412169=CARTESIAN_POINT('Ctrl Pts',(1.26261987063918,0.831772866439156,
-4.01629039630894));
#412170=CARTESIAN_POINT('Ctrl Pts',(1.43402053602185,0.482841671967244,
-4.03567546266849));
#412171=CARTESIAN_POINT('Ctrl Pts',(1.48532197293877,0.288699503772824,
-4.04646113867929));
#412172=CARTESIAN_POINT('Ctrl Pts',(1.50897163146507,-0.103695919934746,
-4.06826088444082));
#412173=CARTESIAN_POINT('Ctrl Pts',(1.482870655935,-0.298083792777715,-4.07906021070988));
#412174=CARTESIAN_POINT('Ctrl Pts',(1.35882156308033,-0.663577493177654,
-4.09936541628765));
#412175=CARTESIAN_POINT('Ctrl Pts',(1.26303051316353,-0.831555557395231,
-4.10816451491907));
#412176=CARTESIAN_POINT('Ctrl Pts',(1.00816679456882,-1.12847677588431,
-4.12867446292187));
#412177=CARTESIAN_POINT('Ctrl Pts',(0.84919499381207,-1.25248373891458,
-4.13976763511386));
#412178=CARTESIAN_POINT('Ctrl Pts',(0.498848862514922,-1.42759741543611,
-4.16148794000729));
#412179=CARTESIAN_POINT('Ctrl Pts',(0.31213328570595,-1.47968814757021,
-4.1719182621665));
#412180=CARTESIAN_POINT('Ctrl Pts',(-0.0759035487285916,-1.51100097165255,
-4.19145749373681));
#412181=CARTESIAN_POINT('Ctrl Pts',(-0.273668536656642,-1.48795461836484,
-4.20100147754327));
#412182=CARTESIAN_POINT('Ctrl Pts',(-0.648945994403652,-1.36665261103511,
-4.22242652285112));
#412183=CARTESIAN_POINT('Ctrl Pts',(-0.822760499348426,-1.26961968984822,
-4.23348453604122));
#412184=CARTESIAN_POINT('Ctrl Pts',(-1.11751477203434,-1.01847598257923,
-4.2546421216887));
#412185=CARTESIAN_POINT('Ctrl Pts',(-1.2374164158246,-0.868849150927716,
-4.26423060272624));
#412186=CARTESIAN_POINT('Ctrl Pts',(-1.41910042027154,-0.525064982580511,
-4.28332972318997));
#412187=CARTESIAN_POINT('Ctrl Pts',(-1.47611640453722,-0.332558451995796,
-4.29402453044468));
#412188=CARTESIAN_POINT('Ctrl Pts',(-1.51143200208983,0.0594833347478576,
-4.31580462970822));
#412189=CARTESIAN_POINT('Ctrl Pts',(-1.4909360257503,0.255114728648251,
-4.32667304048046));
#412190=CARTESIAN_POINT('Ctrl Pts',(-1.37743276400524,0.623791612541792,
-4.34715508958566));
#412191=CARTESIAN_POINT('Ctrl Pts',(-1.28697881671843,0.793800719434514,
-4.35596355612815));
#412192=CARTESIAN_POINT('Ctrl Pts',(-1.04126642406067,1.09811948207782,
-4.37623869809415));
#412193=CARTESIAN_POINT('Ctrl Pts',(-0.885540927381995,1.22715291585369,
-4.38731530659574));
#412194=CARTESIAN_POINT('Ctrl Pts',(-0.539400512018695,1.41284710562235,
-4.40912716703271));
#412195=CARTESIAN_POINT('Ctrl Pts',(-0.353715241139075,1.47037175692501,
-4.41965886077391));
#412196=CARTESIAN_POINT('Ctrl Pts',(-0.108237918196274,1.49707454363554,
-4.43221113805595));
#412197=CARTESIAN_POINT('Ctrl Pts',(-0.054089489701269,1.50000000000005,
-4.43489761821339));
#412198=CARTESIAN_POINT('Ctrl Pts',(-2.2931656573634E-13,1.50000000000006,
-4.43749999999999));
#412199=CARTESIAN_POINT('Ctrl Pts',(2.29781471627888E-13,1.50000000000006,
-4.49999999999999));
#412200=CARTESIAN_POINT('Ctrl Pts',(-0.141577531670121,1.50000000000006,
-4.49318834783158));
#412201=CARTESIAN_POINT('Ctrl Pts',(-0.282689337369424,1.47996137754507,
-4.48584247451284));
#412202=CARTESIAN_POINT('Ctrl Pts',(-0.609000595035613,1.38499600125823,
-4.46750488968933));
#412203=CARTESIAN_POINT('Ctrl Pts',(-0.786060544261131,1.29274925770904,
-4.45642367936729));
#412204=CARTESIAN_POINT('Ctrl Pts',(-1.08852416186224,1.04946871871112,
-4.43511359903051));
#412205=CARTESIAN_POINT('Ctrl Pts',(-1.21278787608726,0.902974963502137,
-4.42516527575009));
#412206=CARTESIAN_POINT('Ctrl Pts',(-1.40403857665283,0.564094086222278,
-4.40633856034565));
#412207=CARTESIAN_POINT('Ctrl Pts',(-1.46634512329181,0.373271928921311,
-4.39573732938449));
#412208=CARTESIAN_POINT('Ctrl Pts',(-1.51256093779731,-0.0181239560558907,
-4.37399311355242));
#412209=CARTESIAN_POINT('Ctrl Pts',(-1.49734697663919,-0.214773544814063,
-4.36306813639919));
#412210=CARTESIAN_POINT('Ctrl Pts',(-1.39371254638348,-0.586350644688788,
-4.34242496418393));
#412211=CARTESIAN_POINT('Ctrl Pts',(-1.30814590608173,-0.758280757418019,
-4.33354151154521));
#412212=CARTESIAN_POINT('Ctrl Pts',(-1.07092751429217,-1.06931851797489,
-4.3134883985556));
#412213=CARTESIAN_POINT('Ctrl Pts',(-0.918325738887209,-1.2029081661107,
-4.30243551865386));
#412214=CARTESIAN_POINT('Ctrl Pts',(-0.576331635108706,-1.39825667542624,
-4.28055497218306));
#412215=CARTESIAN_POINT('Ctrl Pts',(-0.391732808216006,-1.46076732220635,
-4.26993705012818));
#412216=CARTESIAN_POINT('Ctrl Pts',(-0.00792746944280439,-1.51249229130345,
-4.25003440245961));
#412217=CARTESIAN_POINT('Ctrl Pts',(0.18767220073635,-1.50082665512782,
-4.24099357967453));
#412218=CARTESIAN_POINT('Ctrl Pts',(0.567647827130084,-1.40253498937952,
-4.2199816697773));
#412219=CARTESIAN_POINT('Ctrl Pts',(0.747892048125426,-1.31528683774872,
-4.20888610588382));
#412220=CARTESIAN_POINT('Ctrl Pts',(1.05805850941218,-1.08025023573789,
-4.18743442055706));
#412221=CARTESIAN_POINT('Ctrl Pts',(1.18681357666561,-0.936976785220399,
-4.17725987142561));
#412222=CARTESIAN_POINT('Ctrl Pts',(1.38772429140754,-0.603093330689266,
-4.15831900975202));
#412223=CARTESIAN_POINT('Ctrl Pts',(1.45536894277558,-0.414066520732329,
-4.14800369559621));
#412224=CARTESIAN_POINT('Ctrl Pts',(1.51255592246496,-0.023461578934196,
-4.12630342105187));
#412225=CARTESIAN_POINT('Ctrl Pts',(1.50269082588817,0.174070211172446,
-4.11532943271261));
#412226=CARTESIAN_POINT('Ctrl Pts',(1.40899932305871,0.548491012942113,
-4.09452827705874));
#412227=CARTESIAN_POINT('Ctrl Pts',(1.32826040088197,0.722381015149212,
-4.08550648569052));
#412228=CARTESIAN_POINT('Ctrl Pts',(1.10097533275185,1.03798614056905,-4.06580441871211));
#412229=CARTESIAN_POINT('Ctrl Pts',(0.953804601754212,1.17464851975854,
-4.05492748641587));
#412230=CARTESIAN_POINT('Ctrl Pts',(0.619220134669781,1.379880816514,-4.03312888660562));
#412231=CARTESIAN_POINT('Ctrl Pts',(0.436067013375301,1.44822782335987,
-4.02241839998083));
#412232=CARTESIAN_POINT('Ctrl Pts',(0.163816553264131,1.49329524616321,
-4.00806787075583));
#412233=CARTESIAN_POINT('Ctrl Pts',(0.0818890695196856,1.50000000000006,
-4.00393988969422));
#412234=CARTESIAN_POINT('Ctrl Pts',(2.54796184151483E-14,1.50000000000006,
-3.99999999999998));
#412235=CARTESIAN_POINT('Origin',(0.,2.5406128344257E-15,14.));
#412236=CARTESIAN_POINT('',(-9.18485099360549E-17,1.50000000000006,-3.4375));
#412237=CARTESIAN_POINT('',(-1.28316577175101E-14,1.50000000000006,-3.49999999999998));
#412238=CARTESIAN_POINT('',(-1.8369701987211E-16,1.50000000000006,14.));
#412239=CARTESIAN_POINT('Ctrl Pts',(0.,1.50000000000006,-3.4375));
#412240=CARTESIAN_POINT('Ctrl Pts',(0.00383837813561547,1.50000000000006,
-3.43768467405416));
#412241=CARTESIAN_POINT('Ctrl Pts',(0.00767739578047216,1.49998526685652,
-3.4378697881307));
#412242=CARTESIAN_POINT('Ctrl Pts',(0.202238742844605,1.49849138480775,
-3.44727212202939));
#412243=CARTESIAN_POINT('Ctrl Pts',(0.390908433348299,1.46066537786935,
-3.45740021916103));
#412244=CARTESIAN_POINT('Ctrl Pts',(0.750766726921418,1.31361521777901,
-3.47879863605226));
#412245=CARTESIAN_POINT('Ctrl Pts',(0.917490048972587,1.20310145349813,
-3.48988994241004));
#412246=CARTESIAN_POINT('Ctrl Pts',(1.19594419717257,0.926078500633437,
-3.51098215588574));
#412247=CARTESIAN_POINT('Ctrl Pts',(1.30589435374069,0.763240789073974,
-3.52009773394034));
#412248=CARTESIAN_POINT('Ctrl Pts',(1.45677965863356,0.406218634455983,
-3.53993229808578));
#412249=CARTESIAN_POINT('Ctrl Pts',(1.49688916537199,0.215700620374207,
-3.55051663220144));
#412250=CARTESIAN_POINT('Ctrl Pts',(1.50287980214477,-0.177688244323054,
-3.57237156912906));
#412251=CARTESIAN_POINT('Ctrl Pts',(1.46568688458079,-0.376828077812292,
-3.58343489316959));
#412252=CARTESIAN_POINT('Ctrl Pts',(1.31767783831337,-0.742513459048994,
-3.60375074768186));
#412253=CARTESIAN_POINT('Ctrl Pts',(1.21077959263397,-0.906431974948015,
-3.61275833899274));
#412254=CARTESIAN_POINT('Ctrl Pts',(0.937317259507124,-1.18777435698962,
-3.63373036779756));
#412255=CARTESIAN_POINT('Ctrl Pts',(0.772156944208706,-1.30120646379647,
-3.64482753902805));
#412256=CARTESIAN_POINT('Ctrl Pts',(0.414146270442482,-1.45428625375279,
-3.66630455198837));
#412257=CARTESIAN_POINT('Ctrl Pts',(0.225803487910649,-1.49515942344655,
-3.67650156416275));
#412258=CARTESIAN_POINT('Ctrl Pts',(-0.163876543756407,-1.5042113469918,
-3.69550149574852));
#412259=CARTESIAN_POINT('Ctrl Pts',(-0.36159342079996,-1.46928677785985,
-3.70575031662912));
#412260=CARTESIAN_POINT('Ctrl Pts',(-0.729298491551781,-1.3253443539406,
-3.72743993575863));
#412261=CARTESIAN_POINT('Ctrl Pts',(-0.896052225884826,-1.21881426941551,
-3.73842204755701));
#412262=CARTESIAN_POINT('Ctrl Pts',(-1.17482162487293,-0.951788713600149,
-3.75925172306973));
#412263=CARTESIAN_POINT('Ctrl Pts',(-1.28579767645339,-0.795499399800528,
-3.76830558889997));
#412264=CARTESIAN_POINT('Ctrl Pts',(-1.44722487940157,-0.441701926218901,
-3.78796100409895));
#412265=CARTESIAN_POINT('Ctrl Pts',(-1.4929675491793,-0.246147090610459,
-3.79882516163276));
#412266=CARTESIAN_POINT('Ctrl Pts',(-1.5053733798314,0.146259061249358,
-3.82062550340274));
#412267=CARTESIAN_POINT('Ctrl Pts',(-1.47391678701098,0.339298227844982,
-3.83134990154694));
#412268=CARTESIAN_POINT('Ctrl Pts',(-1.3396994859131,0.701645977298669,
-3.85148033207215));
#412269=CARTESIAN_POINT('Ctrl Pts',(-1.23864678493202,0.867673758381413,
-3.86034096095132));
#412270=CARTESIAN_POINT('Ctrl Pts',(-0.974891200229205,1.15724378580217,
-3.88107451930982));
#412271=CARTESIAN_POINT('Ctrl Pts',(-0.812890468197538,1.27625439466436,
-3.89217463340994));
#412272=CARTESIAN_POINT('Ctrl Pts',(-0.458729099058795,1.44092061171477,
-3.91378829181207));
#412273=CARTESIAN_POINT('Ctrl Pts',(-0.271156167309856,1.48767615682011,
-3.92411166384038));
#412274=CARTESIAN_POINT('Ctrl Pts',(-0.053221028040331,1.4992925278947,
-3.93491975009161));
#412275=CARTESIAN_POINT('Ctrl Pts',(-0.0265985578625327,1.50000000000006,
-3.93622027628817));
#412276=CARTESIAN_POINT('Ctrl Pts',(-1.27398092075741E-13,1.50000000000006,
-3.9375));
#412277=CARTESIAN_POINT('Ctrl Pts',(2.36963226818432E-14,1.50000000000006,
-3.99999999999998));
#412278=CARTESIAN_POINT('Ctrl Pts',(-0.110052726427567,1.50000000000006,
-3.99470508573098));
#412279=CARTESIAN_POINT('Ctrl Pts',(-0.220003344823943,1.48789131581819,
-3.98907873179852));
#412280=CARTESIAN_POINT('Ctrl Pts',(-0.522031754807368,1.42023516921341,
-3.97266804574226));
#412281=CARTESIAN_POINT('Ctrl Pts',(-0.705588874943954,1.33855147507351,
-3.96156765817816));
#412282=CARTESIAN_POINT('Ctrl Pts',(-1.02399430683489,1.11269274086527,
-3.93997451596569));
#412283=CARTESIAN_POINT('Ctrl Pts',(-1.15752520872903,0.973039871272125,
-3.92967076107529));
#412284=CARTESIAN_POINT('Ctrl Pts',(-1.36915150890351,0.644355439731411,
-3.91035876286249));
#412285=CARTESIAN_POINT('Ctrl Pts',(-1.44261380520885,0.456800911229985,
-3.90037782840163));
#412286=CARTESIAN_POINT('Ctrl Pts',(-1.5113319384233,0.0668534138670467,
-3.87871407854813));
#412287=CARTESIAN_POINT('Ctrl Pts',(-1.50708896300539,-0.131447031997297,
-3.86769738711122));
#412288=CARTESIAN_POINT('Ctrl Pts',(-1.42381150292164,-0.508759949520183,
-3.84673555835995));
#412289=CARTESIAN_POINT('Ctrl Pts',(-1.34803476855501,-0.684732585148491,
-3.83750367012102));
#412290=CARTESIAN_POINT('Ctrl Pts',(-1.12983704425607,-1.00648950719521,
-3.8180679349369));
#412291=CARTESIAN_POINT('Ctrl Pts',(-0.986602540188378,-1.14723428560259,
-3.80726698446885));
#412292=CARTESIAN_POINT('Ctrl Pts',(-0.657534322830927,-1.3621153227703,
-3.78546576478033));
#412293=CARTESIAN_POINT('Ctrl Pts',(-0.47584679406526,-1.43571963639234,
-3.77467975520961));
#412294=CARTESIAN_POINT('Ctrl Pts',(-0.0968522807454996,-1.50910999280203,
-3.75440675217435));
#412295=CARTESIAN_POINT('Ctrl Pts',(0.096687802629267,-1.50912053837361,
-3.74560145421517));
#412296=CARTESIAN_POINT('Ctrl Pts',(0.480915377804278,-1.43476027526918,
-3.72504973352138));
#412297=CARTESIAN_POINT('Ctrl Pts',(0.667285027080797,-1.35813672393646,
-3.71395458760836));
#412298=CARTESIAN_POINT('Ctrl Pts',(0.992808230103471,-1.14069248982998,
-3.69225272758658));
#412299=CARTESIAN_POINT('Ctrl Pts',(1.13050975804057,-1.00439792698175,
-3.6818415996556));
#412300=CARTESIAN_POINT('Ctrl Pts',(1.35016111046359,-0.682700899589308,
-3.66233759049615));
#412301=CARTESIAN_POINT('Ctrl Pts',(1.4282378851341,-0.499171310846436,
-3.65273173949143));
#412302=CARTESIAN_POINT('Ctrl Pts',(1.50867319600023,-0.112836516586951,
-3.6312686953659));
#412303=CARTESIAN_POINT('Ctrl Pts',(1.51043421116519,0.0861081306614081,
-3.62021621496322));
#412304=CARTESIAN_POINT('Ctrl Pts',(1.43825701295304,0.466403501236634,
-3.5990886943757));
#412305=CARTESIAN_POINT('Ctrl Pts',(1.36767430010884,0.644632336067039,
-3.58956247333128));
#412306=CARTESIAN_POINT('Ctrl Pts',(1.15903383410136,0.972718921660573,
-3.57041073796369));
#412307=CARTESIAN_POINT('Ctrl Pts',(1.02003707809547,1.11760539553946,-3.5596986291479));
#412308=CARTESIAN_POINT('Ctrl Pts',(0.697033656120665,1.34241177158974,
-3.53791349820543));
#412309=CARTESIAN_POINT('Ctrl Pts',(0.517036849960877,1.42148070619577,
-3.52705703853668));
#412310=CARTESIAN_POINT('Ctrl Pts',(0.21937372040268,1.48796019164546,-3.51088906216489));
#412311=CARTESIAN_POINT('Ctrl Pts',(0.109739389385378,1.50000000000006,
-3.50527983883351));
#412312=CARTESIAN_POINT('Ctrl Pts',(-2.51534904016637E-14,1.50000000000006,
-3.49999999999998));
#412313=CARTESIAN_POINT('Origin',(0.,2.5406128344257E-15,14.));
#412314=CARTESIAN_POINT('',(1.01826625150656E-13,1.50000000000006,-2.93750000000001));
#412315=CARTESIAN_POINT('',(-1.02010322170531E-13,1.50000000000006,-2.99999999999997));
#412316=CARTESIAN_POINT('',(-1.8369701987211E-16,1.50000000000006,14.));
#412317=CARTESIAN_POINT('Ctrl Pts',(2.03836947321183E-13,1.50000000000006,
-2.93750000000001));
#412318=CARTESIAN_POINT('Ctrl Pts',(0.0324756869089283,1.50000000000006,
-2.93906248721492));
#412319=CARTESIAN_POINT('Ctrl Pts',(0.0649840153771657,1.49894535575732,
-2.940655840571));
#412320=CARTESIAN_POINT('Ctrl Pts',(0.288880046979268,1.48436511741472,
-2.95183305003462));
#412321=CARTESIAN_POINT('Ctrl Pts',(0.476101178240112,1.43530432034879,
-2.96220353083074));
#412322=CARTESIAN_POINT('Ctrl Pts',(0.828652016994215,1.26611675306727,
-2.98386529561559));
#412323=CARTESIAN_POINT('Ctrl Pts',(0.989363137339907,1.14493989035571,
-2.99496353696258));
#412324=CARTESIAN_POINT('Ctrl Pts',(1.24928737459687,0.852181743983836,
-3.0156013183909));
#412325=CARTESIAN_POINT('Ctrl Pts',(1.34806301023252,0.685315955484659,
-3.02442689136197));
#412326=CARTESIAN_POINT('Ctrl Pts',(1.47790784661234,0.321606136235137,
-3.04463299243138));
#412327=CARTESIAN_POINT('Ctrl Pts',(1.50706790262235,0.127969168176114,
-3.055390601768));
#412328=CARTESIAN_POINT('Ctrl Pts',(1.48982890756442,-0.26447209595403,
-3.07719289421967));
#412329=CARTESIAN_POINT('Ctrl Pts',(1.44169067460576,-0.459439433716649,
-3.08802441298426));
#412330=CARTESIAN_POINT('Ctrl Pts',(1.27596769337458,-0.811156292291829,
-3.10756423846066));
#412331=CARTESIAN_POINT('Ctrl Pts',(1.16313112751449,-0.966027961343561,
-3.11670627090622));
#412332=CARTESIAN_POINT('Ctrl Pts',(0.881010866199492,-1.22976870676216,
-3.13760592012457));
#412333=CARTESIAN_POINT('Ctrl Pts',(0.712741931599012,-1.33435652805513,
-3.14860698027336));
#412334=CARTESIAN_POINT('Ctrl Pts',(0.341730513984731,-1.47422035071018,
-3.17034238161089));
#412335=CARTESIAN_POINT('Ctrl Pts',(0.142133268152913,-1.50660749914951,
-3.18047806830456));
#412336=CARTESIAN_POINT('Ctrl Pts',(-0.249056218867613,-1.49149956395815,
-3.1997188461406));
#412337=CARTESIAN_POINT('Ctrl Pts',(-0.437027570806907,-1.44761338497599,
-3.20998168255473));
#412338=CARTESIAN_POINT('Ctrl Pts',(-0.793113212309265,-1.28859010546988,
-3.231531174289));
#412339=CARTESIAN_POINT('Ctrl Pts',(-0.956678639165735,-1.17229153401868,
-3.24263123543145));
#412340=CARTESIAN_POINT('Ctrl Pts',(-1.22518115568791,-0.886717531374876,
-3.26348217996535));
#412341=CARTESIAN_POINT('Ctrl Pts',(-1.32907835748031,-0.721723178031133,
-3.27240426788716));
#412342=CARTESIAN_POINT('Ctrl Pts',(-1.46869612189956,-0.361077840727507,
-3.29244011995959));
#412343=CARTESIAN_POINT('Ctrl Pts',(-1.50297472700881,-0.168813816207088,
-3.30312145465516));
#412344=CARTESIAN_POINT('Ctrl Pts',(-1.49653225858235,0.22346636602509,
-3.32491479811251));
#412345=CARTESIAN_POINT('Ctrl Pts',(-1.45375805612543,0.419704959757398,
-3.33581694220875));
#412346=CARTESIAN_POINT('Ctrl Pts',(-1.29765159028516,0.77604672184972,
-3.35561370676943));
#412347=CARTESIAN_POINT('Ctrl Pts',(-1.18895813516421,0.934096362618708,
-3.36457667956784));
#412348=CARTESIAN_POINT('Ctrl Pts',(-0.914309896105459,1.20513119150952,
-3.38531944437755));
#412349=CARTESIAN_POINT('Ctrl Pts',(-0.749443660648884,1.31401401265434,
-3.39627609763889));
#412350=CARTESIAN_POINT('Ctrl Pts',(-0.387862014064975,1.46205087779341,
-3.41778483786408));
#412351=CARTESIAN_POINT('Ctrl Pts',(-0.194804848327324,1.50000000000006,
-3.4281274473649));
#412352=CARTESIAN_POINT('Ctrl Pts',(-2.08166817117217E-16,1.50000000000006,
-3.4375));
#412353=CARTESIAN_POINT('Ctrl Pts',(-2.5479618415148E-14,1.50000000000006,
-3.49999999999998));
#412354=CARTESIAN_POINT('Ctrl Pts',(-0.0804207493428627,1.50000000000006,
-3.49613075489319));
#412355=CARTESIAN_POINT('Ctrl Pts',(-0.160880446843173,1.49353351058198,
-3.49208001118622));
#412356=CARTESIAN_POINT('Ctrl Pts',(-0.438164433049878,1.44847159565109,
-3.47748745932049));
#412357=CARTESIAN_POINT('Ctrl Pts',(-0.627289115656694,1.37715349031037,
-3.46640713530435));
#412358=CARTESIAN_POINT('Ctrl Pts',(-0.959912447691088,1.1685977213517,
-3.44461057197587));
#412359=CARTESIAN_POINT('Ctrl Pts',(-1.10181977458662,1.03588792780666,
-3.43409666937325));
#412360=CARTESIAN_POINT('Ctrl Pts',(-1.32963155482614,0.721398345008406,
-3.4144002482417));
#412361=CARTESIAN_POINT('Ctrl Pts',(-1.4123404120215,0.541887207449783,
-3.40510484485828));
#412362=CARTESIAN_POINT('Ctrl Pts',(-1.50454901637742,0.159368380791001,
-3.38385379893279));
#412363=CARTESIAN_POINT('Ctrl Pts',(-1.5124346897935,-0.0400480155845899,
-3.37277511024526));
#412364=CARTESIAN_POINT('Ctrl Pts',(-1.45158020500728,-0.423275149142189,
-3.3514847139365));
#412365=CARTESIAN_POINT('Ctrl Pts',(-1.38620666532733,-0.603845409694176,
-3.3415870823456));
#412366=CARTESIAN_POINT('Ctrl Pts',(-1.18717508162013,-0.938159660953878,
-3.32272466383028));
#412367=CARTESIAN_POINT('Ctrl Pts',(-1.05253201765593,-1.08705028686621,
-3.31211079567514));
#412368=CARTESIAN_POINT('Ctrl Pts',(-0.73588505348936,-1.32159586462227,
-3.29036095657084));
#412369=CARTESIAN_POINT('Ctrl Pts',(-0.557737809492486,-1.40608600177566,
-3.2794428950435));
#412370=CARTESIAN_POINT('Ctrl Pts',(-0.183806347653259,-1.50082579247428,
-3.25882044834481));
#412371=CARTESIAN_POINT('Ctrl Pts',(0.00797042321779684,-1.51201637084181,
-3.24995031091303));
#412372=CARTESIAN_POINT('Ctrl Pts',(0.395749055373477,-1.46071256652466,
-3.22986819709913));
#412373=CARTESIAN_POINT('Ctrl Pts',(0.587440997207792,-1.39470222434833,
-3.2188117936315));
#412374=CARTESIAN_POINT('Ctrl Pts',(0.926814016028979,-1.19510294647768,
-3.19693927726519));
#412375=CARTESIAN_POINT('Ctrl Pts',(1.07276611057427,-1.06604139951997,
-3.18633211087127));
#412376=CARTESIAN_POINT('Ctrl Pts',(1.30850996460848,-0.758657436181772,
-3.16645143597967));
#412377=CARTESIAN_POINT('Ctrl Pts',(1.39567389041817,-0.582975167886414,
-3.15738750932697));
#412378=CARTESIAN_POINT('Ctrl Pts',(1.49918814551487,-0.204291668769085,
-3.13634953715379));
#412379=CARTESIAN_POINT('Ctrl Pts',(1.51303434523764,-0.00459367178653105,
-3.12525520398809));
#412380=CARTESIAN_POINT('Ctrl Pts',(1.46323834401043,0.381231522641316,
-3.10382047096433));
#412381=CARTESIAN_POINT('Ctrl Pts',(1.40293011990794,0.564105294316241,
-3.09366081698239));
#412382=CARTESIAN_POINT('Ctrl Pts',(1.21312354373214,0.904337840515582,
-3.0747590088602));
#412383=CARTESIAN_POINT('Ctrl Pts',(1.08273616549221,1.05699100076919,-3.06439897358483));
#412384=CARTESIAN_POINT('Ctrl Pts',(0.772291797635089,1.30073681401173,
-3.04269199493775));
#412385=CARTESIAN_POINT('Ctrl Pts',(0.596054210534769,1.39035061333762,
-3.03172348787145));
#412386=CARTESIAN_POINT('Ctrl Pts',(0.274703075377376,1.48108107196493,
-3.01374218365507));
#412387=CARTESIAN_POINT('Ctrl Pts',(0.137565591228464,1.50000000000008,
-3.00661862759389));
#412388=CARTESIAN_POINT('Ctrl Pts',(-2.01123839804751E-13,1.50000000000006,
-2.99999999999997));
#412389=CARTESIAN_POINT('Origin',(0.,2.5406128344257E-15,14.));
#412390=CARTESIAN_POINT('',(8.90868159430818E-14,1.50000000000006,-2.43750000000001));
#412391=CARTESIAN_POINT('',(-3.83112761326589E-14,1.50000000000006,-2.49999999999998));
#412392=CARTESIAN_POINT('',(-1.8369701987211E-16,1.50000000000006,14.));
#412393=CARTESIAN_POINT('Ctrl Pts',(1.78357328906036E-13,1.50000000000006,
-2.43750000000001));
#412394=CARTESIAN_POINT('Ctrl Pts',(0.0600879399513488,1.50000000000006,
-2.44039098235884));
#412395=CARTESIAN_POINT('Ctrl Pts',(0.120237511888765,1.49638976980839,
-2.44338521415997));
#412396=CARTESIAN_POINT('Ctrl Pts',(0.371594894559314,1.46598534480668,
-2.45632321923343));
#412397=CARTESIAN_POINT('Ctrl Pts',(0.556786599151176,1.40611792381491,
-2.46689624319135));
#412398=CARTESIAN_POINT('Ctrl Pts',(0.90101324791975,1.21588098464547,-2.48874221497345));
#412399=CARTESIAN_POINT('Ctrl Pts',(1.05528840530818,1.0847000191656,-2.49980869765185));
#412400=CARTESIAN_POINT('Ctrl Pts',(1.29702193219735,0.777216808900992,
-2.51998030767211));
#412401=CARTESIAN_POINT('Ctrl Pts',(1.38517914898652,0.606312573661868,
-2.5288159681299));
#412402=CARTESIAN_POINT('Ctrl Pts',(1.49406967424139,0.23627057962875,-2.5493738566873));
#412403=CARTESIAN_POINT('Ctrl Pts',(1.51210070438813,0.040145667640204,
-2.5602696851311));
#412404=CARTESIAN_POINT('Ctrl Pts',(1.47168711793412,-0.351632015056332,
-2.58203511194758));
#412405=CARTESIAN_POINT('Ctrl Pts',(1.41219086138491,-0.543369537820228,
-2.59268719654557));
#412406=CARTESIAN_POINT('Ctrl Pts',(1.22602859424387,-0.884872044443282,
-2.61165955802463));
#412407=CARTESIAN_POINT('Ctrl Pts',(1.10409768497012,-1.03303174243462,
-2.62140773487632));
#412408=CARTESIAN_POINT('Ctrl Pts',(0.805747149264772,-1.28052490725735,
-2.64263694185214));
#412409=CARTESIAN_POINT('Ctrl Pts',(0.63040513309612,-1.37534153192259,
-2.653706883668));
#412410=CARTESIAN_POINT('Ctrl Pts',(0.253988236008872,-1.49133760693743,
-2.67503936326793));
#412411=CARTESIAN_POINT('Ctrl Pts',(0.056735146934851,-1.51174226604393,
-2.68444415491362));
#412412=CARTESIAN_POINT('Ctrl Pts',(-0.330358459802904,-1.47575618930825,
-2.70406781799391));
#412413=CARTESIAN_POINT('Ctrl Pts',(-0.516642541644576,-1.42128629030263,
-2.71454346781048));
#412414=CARTESIAN_POINT('Ctrl Pts',(-0.86518719180043,-1.24153256240151,
-2.73630598921819));
#412415=CARTESIAN_POINT('Ctrl Pts',(-1.02275779116148,-1.11531704960142,
-2.74739309468131));
#412416=CARTESIAN_POINT('Ctrl Pts',(-1.27362754231302,-0.815146322030976,
-2.76780114697707));
#412417=CARTESIAN_POINT('Ctrl Pts',(-1.36707943671908,-0.646286224586017,
-2.77659520974523));
#412418=CARTESIAN_POINT('Ctrl Pts',(-1.48653640943523,-0.279395834257768,
-2.79697800920791));
#412419=CARTESIAN_POINT('Ctrl Pts',(-1.51020235437782,-0.0844468628666044,
-2.80780850761853));
#412420=CARTESIAN_POINT('Ctrl Pts',(-1.48147191155196,0.307837417286106,
-2.82960207873812));
#412421=CARTESIAN_POINT('Ctrl Pts',(-1.42767502471587,0.501288471586699,
-2.8403493595326));
#412422=CARTESIAN_POINT('Ctrl Pts',(-1.25178881578139,0.847990517851818,
-2.8596105843251));
#412423=CARTESIAN_POINT('Ctrl Pts',(-1.1344827645406,0.999519102451551,
-2.86901492538767));
#412424=CARTESIAN_POINT('Ctrl Pts',(-0.844351111619898,1.25531200884321,
-2.89007924955807));
#412425=CARTESIAN_POINT('Ctrl Pts',(-0.672533943798328,1.35515124245936,
-2.90111911894406));
#412426=CARTESIAN_POINT('Ctrl Pts',(-0.329578927356474,1.47269892284544,
-2.92088476321));
#412427=CARTESIAN_POINT('Ctrl Pts',(-0.165248197152967,1.50000000000006,
-2.92954949240754));
#412428=CARTESIAN_POINT('Ctrl Pts',(2.06536177049799E-13,1.50000000000006,
-2.93750000000001));
#412429=CARTESIAN_POINT('Ctrl Pts',(-2.03836947321191E-13,1.50000000000006,
-2.99999999999997));
#412430=CARTESIAN_POINT('Ctrl Pts',(-0.0518260929528506,1.50000000000005,
-2.9975065159402));
#412431=CARTESIAN_POINT('Ctrl Pts',(-0.103705738237255,1.49731424103594,
-2.99493585092696));
#412432=CARTESIAN_POINT('Ctrl Pts',(-0.353266974646312,1.47131413802241,
-2.98220660525825));
#412433=CARTESIAN_POINT('Ctrl Pts',(-0.54501292939842,1.41156100563729,
-2.97132141447598));
#412434=CARTESIAN_POINT('Ctrl Pts',(-0.889373472362353,1.22331342656655,
-2.94952426070914));
#412435=CARTESIAN_POINT('Ctrl Pts',(-1.03968986359049,1.09842604100824,
-2.93882306592093));
#412436=CARTESIAN_POINT('Ctrl Pts',(-1.2841096181562,0.798929079940786,
-2.91874405496679));
#412437=CARTESIAN_POINT('Ctrl Pts',(-1.37610609764512,0.627343402167794,
-2.90985241123149));
#412438=CARTESIAN_POINT('Ctrl Pts',(-1.49183001336424,0.25298485137627,
-2.88905471396529));
#412439=CARTESIAN_POINT('Ctrl Pts',(-1.51219086513934,0.0531774261397621,
-2.87795430145215));
#412440=CARTESIAN_POINT('Ctrl Pts',(-1.47452822492152,-0.335250409489197,
-2.85637497725055));
#412441=CARTESIAN_POINT('Ctrl Pts',(-1.41976968043836,-0.520482757750941,
-2.84608429123601));
#412442=CARTESIAN_POINT('Ctrl Pts',(-1.23975119921595,-0.867687374307577,
-2.82679514587175));
#412443=CARTESIAN_POINT('Ctrl Pts',(-1.11336531714322,-1.02484909043133,
-2.81676545017344));
#412444=CARTESIAN_POINT('Ctrl Pts',(-0.808962734118458,-1.27833699989068,
-2.79507854325084));
#412445=CARTESIAN_POINT('Ctrl Pts',(-0.634830535031274,-1.37315641783766,
-2.7840667311953));
#412446=CARTESIAN_POINT('Ctrl Pts',(-0.266085452798857,-1.48838022607664,
-2.76312481381456));
#412447=CARTESIAN_POINT('Ctrl Pts',(-0.0757192170299246,-1.51007466876446,
-2.75392289443798));
#412448=CARTESIAN_POINT('Ctrl Pts',(0.311937677340601,-1.48062452446617,
-2.73445368384764));
#412449=CARTESIAN_POINT('Ctrl Pts',(0.505256838331555,-1.42627069813305,
-2.72364278286858));
#412450=CARTESIAN_POINT('Ctrl Pts',(0.855200408835475,-1.24752402307782,
-2.70184092956442));
#412451=CARTESIAN_POINT('Ctrl Pts',(1.00931667627001,-1.1264881489645,-2.69106389957601));
#412452=CARTESIAN_POINT('Ctrl Pts',(1.26141201577951,-0.834072016097783,
-2.67081228654133));
#412453=CARTESIAN_POINT('Ctrl Pts',(1.357660476778,-0.666029048452036,-2.66200161380283));
#412454=CARTESIAN_POINT('Ctrl Pts',(1.4840513178019,-0.295600261189045,
-2.64142223673266));
#412455=CARTESIAN_POINT('Ctrl Pts',(1.51016080587006,-0.0958671553656366,
-2.63032595307581));
#412456=CARTESIAN_POINT('Ctrl Pts',(1.48326298845563,0.294540097335906,
-2.60863666125906));
#412457=CARTESIAN_POINT('Ctrl Pts',(1.43345743851258,0.481708341663057,
-2.5982384254631));
#412458=CARTESIAN_POINT('Ctrl Pts',(1.26344156569277,0.832357644120056,
-2.57875790865994));
#412459=CARTESIAN_POINT('Ctrl Pts',(1.14283038815684,0.991495693057255,
-2.56910957232394));
#412460=CARTESIAN_POINT('Ctrl Pts',(0.847362746460884,1.2533054056592,-2.54762138676805));
#412461=CARTESIAN_POINT('Ctrl Pts',(0.675642217353411,1.35362668747019,
-2.53657277668673));
#412462=CARTESIAN_POINT('Ctrl Pts',(0.331809149845769,1.47231630234661,
-2.51673316676667));
#412463=CARTESIAN_POINT('Ctrl Pts',(0.166399292541067,1.50000000000007,
-2.50800588969511));
#412464=CARTESIAN_POINT('Ctrl Pts',(-7.5842110369706E-14,1.50000000000006,
-2.49999999999998));
#412465=CARTESIAN_POINT('Origin',(0.,2.5406128344257E-15,14.));
#412466=CARTESIAN_POINT('',(-9.18485099360549E-17,1.50000000000006,-1.9375));
#412467=CARTESIAN_POINT('',(-9.18485099360549E-17,1.50000000000006,-1.99999999999998));
#412468=CARTESIAN_POINT('',(-1.8369701987211E-16,1.50000000000006,14.));
#412469=CARTESIAN_POINT('Ctrl Pts',(0.,1.50000000000006,-1.9375));
#412470=CARTESIAN_POINT('Ctrl Pts',(0.0884346922698931,1.50000000000006,
-1.94175481611565));
#412471=CARTESIAN_POINT('Ctrl Pts',(0.176887442546984,1.49218068882933,
-1.94622770413565));
#412472=CARTESIAN_POINT('Ctrl Pts',(0.455248451650143,1.4423468729858,-1.96100462709277));
#412473=CARTESIAN_POINT('Ctrl Pts',(0.637715067491748,1.37146729159052,
-1.9717524335016));
#412474=CARTESIAN_POINT('Ctrl Pts',(0.9696808619442,1.16157486684138,-1.99355449036593));
#412475=CARTESIAN_POINT('Ctrl Pts',(1.11497252727397,1.02293403844781,-2.0043959729954));
#412476=CARTESIAN_POINT('Ctrl Pts',(1.33789230088642,0.70435701525361,-2.02397056735937));
#412477=CARTESIAN_POINT('Ctrl Pts',(1.41624395528717,0.529473866680497,
-2.03308478518443));
#412478=CARTESIAN_POINT('Ctrl Pts',(1.50494935985186,0.153657189248088,
-2.05396348948623));
#412479=CARTESIAN_POINT('Ctrl Pts',(1.51212460110494,-0.0442624750681964,
-2.06495902639269));
#412480=CARTESIAN_POINT('Ctrl Pts',(1.44919905003476,-0.435926284301219,
-2.08671812690563));
#412481=CARTESIAN_POINT('Ctrl Pts',(1.37802303447125,-0.625478046433682,
-2.0969075593536));
#412482=CARTESIAN_POINT('Ctrl Pts',(1.17033003825317,-0.957550954397508,
-2.11612444073665));
#412483=CARTESIAN_POINT('Ctrl Pts',(1.03885296706329,-1.09878942465052,
-2.12637342511399));
#412484=CARTESIAN_POINT('Ctrl Pts',(0.723979451729282,-1.32865319096229,
-2.14790788880366));
#412485=CARTESIAN_POINT('Ctrl Pts',(0.541835318178859,-1.41275905719967,
-2.15900757657719));
#412486=CARTESIAN_POINT('Ctrl Pts',(0.160518770808986,-1.5038703194419,
-2.17988454591201));
#412487=CARTESIAN_POINT('Ctrl Pts',(-0.0344392415867986,-1.5120193721805,
-2.18882308733395));
#412488=CARTESIAN_POINT('Ctrl Pts',(-0.416846838764254,-1.45384321412457,
-2.20883768582194));
#412489=CARTESIAN_POINT('Ctrl Pts',(-0.600650674242951,-1.38802936907984,
-2.21950911434194));
#412490=CARTESIAN_POINT('Ctrl Pts',(-0.937783113429846,-1.18748053264542,
-2.24130020739709));
#412491=CARTESIAN_POINT('Ctrl Pts',(-1.08680170895694,-1.05281891773745,
-2.25221046833136));
#412492=CARTESIAN_POINT('Ctrl Pts',(-1.31843158101191,-0.740203475262216,
-2.27203852803761));
#412493=CARTESIAN_POINT('Ctrl Pts',(-1.40155435336872,-0.567289223907575,
-2.28098393200514));
#412494=CARTESIAN_POINT('Ctrl Pts',(-1.50017929656928,-0.194269468680472,
-2.30170725173998));
#412495=CARTESIAN_POINT('Ctrl Pts',(-1.51270123839612,0.00284267445957186,
-2.31265792635887));
#412496=CARTESIAN_POINT('Ctrl Pts',(-1.46094827900459,0.393917806733193,
-2.33438432259629));
#412497=CARTESIAN_POINT('Ctrl Pts',(-1.39593051208723,0.583831626159538,
-2.34488914042747));
#412498=CARTESIAN_POINT('Ctrl Pts',(-1.19982509667869,0.920202086774228,
-2.36366789053141));
#412499=CARTESIAN_POINT('Ctrl Pts',(-1.07328430176859,1.06507678699389,
-2.37378038459347));
#412500=CARTESIAN_POINT('Ctrl Pts',(-0.766968168801068,1.30421123790918,
-2.39516065004883));
#412501=CARTESIAN_POINT('Ctrl Pts',(-0.588291662986361,1.39396025608546,
-2.40625025572567));
#412502=CARTESIAN_POINT('Ctrl Pts',(-0.267616746180307,1.48205285089828,
-2.42412575137661));
#412503=CARTESIAN_POINT('Ctrl Pts',(-0.133985757708595,1.50000000000006,
-2.43105360722661));
#412504=CARTESIAN_POINT('Ctrl Pts',(1.80827575135822E-13,1.50000000000006,
-2.43750000000001));
#412505=CARTESIAN_POINT('Ctrl Pts',(-7.64388552454456E-14,1.50000000000006,
-2.49999999999998));
#412506=CARTESIAN_POINT('Ctrl Pts',(-0.0231921828888836,1.50000000000006,
-2.49888416558048));
#412507=CARTESIAN_POINT('Ctrl Pts',(-0.0464021685713373,1.49946212869069,
-2.49775253375393));
#412508=CARTESIAN_POINT('Ctrl Pts',(-0.268251541006387,1.48915550948133,
-2.48679250586798));
#412509=CARTESIAN_POINT('Ctrl Pts',(-0.463055320247125,1.44052039061579,
-2.47606902914529));
#412510=CARTESIAN_POINT('Ctrl Pts',(-0.818581347624592,1.27193687377749,
-2.45428089971003));
#412511=CARTESIAN_POINT('Ctrl Pts',(-0.976586466450202,1.15507021883168,
-2.44343257891537));
#412512=CARTESIAN_POINT('Ctrl Pts',(-1.23668201868617,0.87013486144992,
-2.42300385478546));
#412513=CARTESIAN_POINT('Ctrl Pts',(-1.33734414935178,0.705709309724037,
-2.41420607276238));
#412514=CARTESIAN_POINT('Ctrl Pts',(-1.47471766045293,0.339464868050829,
-2.39385915933609));
#412515=CARTESIAN_POINT('Ctrl Pts',(-1.50679147360988,0.13997746957944,
-2.38277652608768));
#412516=CARTESIAN_POINT('Ctrl Pts',(-1.49111956561788,-0.252170665171258,
-2.36099051860153));
#412517=CARTESIAN_POINT('Ctrl Pts',(-1.44650782625784,-0.441204057198859,
-2.35048866348889));
#412518=CARTESIAN_POINT('Ctrl Pts',(-1.28680700536982,-0.795324315558441,
-2.33081531580225));
#412519=CARTESIAN_POINT('Ctrl Pts',(-1.17200561889551,-0.956466540493105,
-2.32148629828299));
#412520=CARTESIAN_POINT('Ctrl Pts',(-0.885726973651313,-1.22659071766639,
-2.30020926117582));
#412521=CARTESIAN_POINT('Ctrl Pts',(-0.716640993231907,-1.3324637283606,
-2.28913319118615));
#412522=CARTESIAN_POINT('Ctrl Pts',(-0.353946633413566,-1.47001633807981,
-2.26786214483773));
#412523=CARTESIAN_POINT('Ctrl Pts',(-0.164815750605185,-1.50300220280088,
-2.25801309602039));
#412524=CARTESIAN_POINT('Ctrl Pts',(0.224159970903297,-1.49642314518495,
-2.23911574129319));
#412525=CARTESIAN_POINT('Ctrl Pts',(0.42027929336073,-1.45357120372873,
-2.2284896142849));
#412526=CARTESIAN_POINT('Ctrl Pts',(0.781111913268854,-1.29536887785472,
-2.20673453771315));
#412527=CARTESIAN_POINT('Ctrl Pts',(0.942910806682508,-1.18281136012676,
-2.19582338710957));
#412528=CARTESIAN_POINT('Ctrl Pts',(1.21097606234339,-0.905440080178825,
-2.17522133370689));
#412529=CARTESIAN_POINT('Ctrl Pts',(1.31603285800529,-0.744538088387238,
-2.16636322713255));
#412530=CARTESIAN_POINT('Ctrl Pts',(1.46421523239754,-0.382548700011401,
-2.14625270555612));
#412531=CARTESIAN_POINT('Ctrl Pts',(1.5021951427484,-0.183473494950709,
-2.13519297194164));
#412532=CARTESIAN_POINT('Ctrl Pts',(1.49769664685549,0.21008536290726,-2.11332859094953));
#412533=CARTESIAN_POINT('Ctrl Pts',(1.45828293090147,0.400822100376607,
-2.10273210553457));
#412534=CARTESIAN_POINT('Ctrl Pts',(1.30875056254787,0.758284389247239,
-2.0828730894862));
#412535=CARTESIAN_POINT('Ctrl Pts',(1.1995358429708,0.921381433655664,-2.07378543310742));
#412536=CARTESIAN_POINT('Ctrl Pts',(0.922279745513901,1.19944673044089,
-2.05272190687718));
#412537=CARTESIAN_POINT('Ctrl Pts',(0.755927642276091,1.31066393616686,
-2.04162892075274));
#412538=CARTESIAN_POINT('Ctrl Pts',(0.396504479944567,1.45916553552777,
-2.02021112136562));
#412539=CARTESIAN_POINT('Ctrl Pts',(0.207908921595368,1.49772417893426,
-2.01006623990592));
#412540=CARTESIAN_POINT('Ctrl Pts',(0.0114144356045565,1.4999674356079,
-2.00055008185546));
#412541=CARTESIAN_POINT('Ctrl Pts',(0.00570652334405782,1.50000000000006,
-2.00027455523238));
#412542=CARTESIAN_POINT('Ctrl Pts',(0.,1.50000000000006,-1.99999999999998));
#412543=CARTESIAN_POINT('Origin',(0.,2.5406128344257E-15,14.));
#412544=CARTESIAN_POINT('',(-2.5584277190752E-14,1.50000000000006,-1.4375));
#412545=CARTESIAN_POINT('',(1.01826625150654E-13,1.50000000000006,-1.49999999999999));
#412546=CARTESIAN_POINT('',(-1.8369701987211E-16,1.50000000000006,14.));
#412547=CARTESIAN_POINT('Ctrl Pts',(-4.93702301262999E-14,1.50000000000006,
-1.4375));
#412548=CARTESIAN_POINT('Ctrl Pts',(0.116751179473137,1.50000000000006,
-1.44311719374142));
#412549=CARTESIAN_POINT('Ctrl Pts',(0.233334609588104,1.48637273636851,
-1.44910485173897));
#412550=CARTESIAN_POINT('Ctrl Pts',(0.537138132706308,1.4140448040146,-1.46573071479211));
#412551=CARTESIAN_POINT('Ctrl Pts',(0.716244104631243,1.33230116510943,
-1.47661861152039));
#412552=CARTESIAN_POINT('Ctrl Pts',(1.03615413605409,1.10267614366661,-1.49838876290145));
#412553=CARTESIAN_POINT('Ctrl Pts',(1.17302165631554,0.955800930784408,
-1.50905367156481));
#412554=CARTESIAN_POINT('Ctrl Pts',(1.37693820904,0.624636156461619,-1.52806363279108));
#412555=CARTESIAN_POINT('Ctrl Pts',(1.44495918238456,0.445265642356491,
-1.5377630198691));
#412556=CARTESIAN_POINT('Ctrl Pts',(1.51159087068747,0.0635201654975268,
-1.55897110191681));
#412557=CARTESIAN_POINT('Ctrl Pts',(1.50682949726965,-0.135678810543036,
-1.57003771169684));
#412558=CARTESIAN_POINT('Ctrl Pts',(1.42060545718522,-0.52016035689412,
-1.59139779760524));
#412559=CARTESIAN_POINT('Ctrl Pts',(1.34025132827086,-0.701710520174848,
-1.60084242013051));
#412560=CARTESIAN_POINT('Ctrl Pts',(1.11660007662252,-1.01988768661049,
-1.6204411006157));
#412561=CARTESIAN_POINT('Ctrl Pts',(0.976832004464489,-1.1544465360711,
-1.6309034409411));
#412562=CARTESIAN_POINT('Ctrl Pts',(0.647810048663878,-1.36757561427195,
-1.65265376934258));
#412563=CARTESIAN_POINT('Ctrl Pts',(0.460076169110209,-1.44161857982056,
-1.66374286887695));
#412564=CARTESIAN_POINT('Ctrl Pts',(0.074925950513314,-1.51030351218679,
-1.68418133219702));
#412565=CARTESIAN_POINT('Ctrl Pts',(-0.118156433969195,-1.5075379825504,
-1.69297541567572));
#412566=CARTESIAN_POINT('Ctrl Pts',(-0.495946428459652,-1.42893732519622,
-1.71333519685357));
#412567=CARTESIAN_POINT('Ctrl Pts',(-0.676831290210769,-1.3526691172112,
-1.72415658515518));
#412568=CARTESIAN_POINT('Ctrl Pts',(-1.00298556684726,-1.13293629016934,
-1.74595237974635));
#412569=CARTESIAN_POINT('Ctrl Pts',(-1.14417301262309,-0.990159439007331,
-1.75671128754181));
#412570=CARTESIAN_POINT('Ctrl Pts',(-1.35772687033861,-0.665309528353912,
-1.77600951094095));
#412571=CARTESIAN_POINT('Ctrl Pts',(-1.43097742256505,-0.488249372379978,
-1.78537503486779));
#412572=CARTESIAN_POINT('Ctrl Pts',(-1.50888079237126,-0.10947940505863,
-1.80641781083008));
#412573=CARTESIAN_POINT('Ctrl Pts',(-1.5102177655482,0.0891554783909032,
-1.81745308213284));
#412574=CARTESIAN_POINT('Ctrl Pts',(-1.43580522297629,0.477370605819653,
-1.83902058921221));
#412575=CARTESIAN_POINT('Ctrl Pts',(-1.36009907443075,0.662966271740376,
-1.84881126587498));
#412576=CARTESIAN_POINT('Ctrl Pts',(-1.14458440528513,0.988277507115257,
-1.86821664343363));
#412577=CARTESIAN_POINT('Ctrl Pts',(-1.00902902661727,1.12632385521272,
-1.87857317541112));
#412578=CARTESIAN_POINT('Ctrl Pts',(-0.687159260872402,1.34814616795105,
-1.90022087264525));
#412579=CARTESIAN_POINT('Ctrl Pts',(-0.502227210977496,1.42739777272394,
-1.91131985351021));
#412580=CARTESIAN_POINT('Ctrl Pts',(-0.205936556405633,1.48939438257698,
-1.9272972723263));
#412581=CARTESIAN_POINT('Ctrl Pts',(-0.102994860314799,1.50000000000006,
-1.93254465747268));
#412582=CARTESIAN_POINT('Ctrl Pts',(-6.41847686111419E-16,1.50000000000006,
-1.9375));
#412583=CARTESIAN_POINT('Ctrl Pts',(-7.63278329429795E-16,1.50000000000006,
-1.99999999999998));
#412584=CARTESIAN_POINT('Ctrl Pts',(-0.192917176739438,1.50000000000006,
-1.99071826800649));
#412585=CARTESIAN_POINT('Ctrl Pts',(-0.384148717671948,1.46278348849279,
-1.98048384421722));
#412586=CARTESIAN_POINT('Ctrl Pts',(-0.744615514215288,1.31676651004499,
-1.95908485020326));
#412587=CARTESIAN_POINT('Ctrl Pts',(-0.909938568354587,1.20844650284776,
-1.94812185196357));
#412588=CARTESIAN_POINT('Ctrl Pts',(-1.18557905621631,0.938373943019263,
-1.92735807725724));
#412589=CARTESIAN_POINT('Ctrl Pts',(-1.29482159251507,0.780749871870283,
-1.91837499288161));
#412590=CARTESIAN_POINT('Ctrl Pts',(-1.4522129484349,0.425019177606191,
-1.8986121765336));
#412591=CARTESIAN_POINT('Ctrl Pts',(-1.49570405827205,0.228941258167677,
-1.88771895878702));
#412592=CARTESIAN_POINT('Ctrl Pts',(-1.50358414165862,-0.163377651610241,
-1.86592346379936));
#412593=CARTESIAN_POINT('Ctrl Pts',(-1.46998468639679,-0.355832339875636,
-1.8552315366735));
#412594=CARTESIAN_POINT('Ctrl Pts',(-1.33166952614332,-0.716890331994617,
-1.83517275933356));
#412595=CARTESIAN_POINT('Ctrl Pts',(-1.22846171708624,-0.882133856646464,
-1.82626734034715));
#412596=CARTESIAN_POINT('Ctrl Pts',(-0.961105613395692,-1.16867768044156,
-1.80544461314991));
#412597=CARTESIAN_POINT('Ctrl Pts',(-0.797914674599878,-1.28563405408433,
-1.79434429728958));
#412598=CARTESIAN_POINT('Ctrl Pts',(-0.442286477948419,-1.44602425107628,
-1.77277884445079));
#412599=CARTESIAN_POINT('Ctrl Pts',(-0.25440752314352,-1.49060470774768,
-1.7625011680045));
#412600=CARTESIAN_POINT('Ctrl Pts',(0.136521115123568,-1.50709030388568,
-1.74323467190033));
#412601=CARTESIAN_POINT('Ctrl Pts',(0.335959743335738,-1.47550857771446,
-1.73315581202657));
#412602=CARTESIAN_POINT('Ctrl Pts',(0.707353561594332,-1.33723222712268,
-1.71144610887566));
#412603=CARTESIAN_POINT('Ctrl Pts',(0.876108720190405,-1.23327818046135,
-1.70043926011485));
#412604=CARTESIAN_POINT('Ctrl Pts',(1.15931277117352,-0.970604750688442,
-1.6795171146986));
#412605=CARTESIAN_POINT('Ctrl Pts',(1.27275210847479,-0.816189071901462,
-1.67034383732778));
#412606=CARTESIAN_POINT('Ctrl Pts',(1.43985875024554,-0.465147354053559,
-1.65084151966956));
#412607=CARTESIAN_POINT('Ctrl Pts',(1.48876823392591,-0.270376001889668,
-1.64002088899379));
#412608=CARTESIAN_POINT('Ctrl Pts',(1.50756724114496,0.122063805581502,
-1.61821867746762));
#412609=CARTESIAN_POINT('Ctrl Pts',(1.4791502374132,0.315887913870442,-1.60745067145156));
#412610=CARTESIAN_POINT('Ctrl Pts',(1.35071611931521,0.680034066690072,
-1.58722032962825));
#412611=CARTESIAN_POINT('Ctrl Pts',(1.25267028978167,0.84717060780074,-1.57840327720084));
#412612=CARTESIAN_POINT('Ctrl Pts',(0.993979789467423,1.14094847596908,
-1.55779652836339));
#412613=CARTESIAN_POINT('Ctrl Pts',(0.833688936219203,1.26281854097953,
-1.54669925150715));
#412614=CARTESIAN_POINT('Ctrl Pts',(0.481667483160786,1.43345561613014,
-1.52502269269598));
#412615=CARTESIAN_POINT('Ctrl Pts',(0.294565327051418,1.48325663576675,
-1.51463737435643));
#412616=CARTESIAN_POINT('Ctrl Pts',(0.0687623041536401,1.49881918806375,
-1.50334112823258));
#412617=CARTESIAN_POINT('Ctrl Pts',(0.0343634242159142,1.50000000000006,
-1.50165331101842));
#412618=CARTESIAN_POINT('Ctrl Pts',(2.0383694732118E-13,1.50000000000006,
-1.49999999999999));
#412619=CARTESIAN_POINT('Origin',(0.,2.5406128344257E-15,14.));
#412620=CARTESIAN_POINT('',(-1.02008187126244E-13,1.50000000000006,-0.937499999999992));
#412621=CARTESIAN_POINT('',(7.63841236998029E-14,1.50000000000006,-0.999999999999987));
#412622=CARTESIAN_POINT('',(-1.8369701987211E-16,1.50000000000006,14.));
#412623=CARTESIAN_POINT('Ctrl Pts',(-2.07854566891541E-13,1.50000000000006,
-0.937499999999992));
#412624=CARTESIAN_POINT('Ctrl Pts',(0.143984182832987,1.50000000000008,
-0.944427442226474));
#412625=CARTESIAN_POINT('Ctrl Pts',(0.287436109780675,1.47927426985385,
-0.951904991006021));
#412626=CARTESIAN_POINT('Ctrl Pts',(0.613981995335455,1.38256263179278,
-0.970302371640589));
#412627=CARTESIAN_POINT('Ctrl Pts',(0.789268204116796,1.29054467388821,
-0.981291887678922));
#412628=CARTESIAN_POINT('Ctrl Pts',(1.09815839824932,1.04133076500178,-1.00307598265347));
#412629=CARTESIAN_POINT('Ctrl Pts',(1.22749428546384,0.885176755556808,
-1.01332351358019));
#412630=CARTESIAN_POINT('Ctrl Pts',(1.41253059674625,0.539729966787636,
-1.03251500184514));
#412631=CARTESIAN_POINT('Ctrl Pts',(1.46974075814148,0.355514378153379,
-1.04274920121371));
#412632=CARTESIAN_POINT('Ctrl Pts',(1.51275388252878,-0.0318148201579883,
-1.06426749000879));
#412633=CARTESIAN_POINT('Ctrl Pts',(1.49526116535058,-0.231599490017907,
-1.07536663833434));
#412634=CARTESIAN_POINT('Ctrl Pts',(1.38489535340168,-0.607879061196219,
-1.09627105895536));
#412635=CARTESIAN_POINT('Ctrl Pts',(1.29502325176767,-0.781257261786077,
-1.10522808868728));
#412636=CARTESIAN_POINT('Ctrl Pts',(1.05442509401626,-1.08424333824674,
-1.12522015285099));
#412637=CARTESIAN_POINT('Ctrl Pts',(0.906022693938836,-1.21099293928177,
-1.13588098890472));
#412638=CARTESIAN_POINT('Ctrl Pts',(0.564519249383978,-1.40387549529209,
-1.15766942981969));
#412639=CARTESIAN_POINT('Ctrl Pts',(0.373608740790731,-1.46628204988311,
-1.16858813135228));
#412640=CARTESIAN_POINT('Ctrl Pts',(-0.0128248159912985,-1.51195748147707,
-1.18844918651034));
#412641=CARTESIAN_POINT('Ctrl Pts',(-0.204228069040268,-1.49815846947414,
-1.19737708117877));
#412642=CARTESIAN_POINT('Ctrl Pts',(-0.576910843083501,-1.39836541638178,
-1.21807981875769));
#412643=CARTESIAN_POINT('Ctrl Pts',(-0.754123327422173,-1.31131393576137,
-1.22902405506964));
#412644=CARTESIAN_POINT('Ctrl Pts',(-1.06773753463044,-1.07213603112307,
-1.25075665633349));
#412645=CARTESIAN_POINT('Ctrl Pts',(-1.20024082815659,-0.921356835669098,
-1.26131350912951));
#412646=CARTESIAN_POINT('Ctrl Pts',(-1.39468136007972,-0.584114630158508,
-1.28004918721343));
#412647=CARTESIAN_POINT('Ctrl Pts',(-1.45752703712634,-0.40238829166349,
-1.2901450949076));
#412648=CARTESIAN_POINT('Ctrl Pts',(-1.51289686949854,-0.0178933003594045,
-1.31150592775782));
#412649=CARTESIAN_POINT('Ctrl Pts',(-1.5020561457567,0.1816844768087,-1.32259358204494));
#412650=CARTESIAN_POINT('Ctrl Pts',(-1.40422510707694,0.562316600134008,
-1.34373981111857));
#412651=CARTESIAN_POINT('Ctrl Pts',(-1.3193022688901,0.739919605343474,
-1.35291169569682));
#412652=CARTESIAN_POINT('Ctrl Pts',(-1.08755774812862,1.0508986120432,-1.37269981489221));
#412653=CARTESIAN_POINT('Ctrl Pts',(-0.943639096864894,1.18181973459741,
-1.38326080207832));
#412654=CARTESIAN_POINT('Ctrl Pts',(-0.607649407629921,1.3859735809312,
-1.40509705371465));
#412655=CARTESIAN_POINT('Ctrl Pts',(-0.417237669683396,1.4546784054474,
-1.41616671007568));
#412656=CARTESIAN_POINT('Ctrl Pts',(-0.146295653475665,1.49465386686708,
-1.43031284339225));
#412657=CARTESIAN_POINT('Ctrl Pts',(-0.0731221438195881,1.50000000000006,
-1.43398190921517));
#412658=CARTESIAN_POINT('Ctrl Pts',(-5.09848573616319E-14,1.50000000000006,
-1.4375));
#412659=CARTESIAN_POINT('Ctrl Pts',(2.01557520673745E-13,1.50000000000006,
-1.49999999999999));
#412660=CARTESIAN_POINT('Ctrl Pts',(-0.163076993215546,1.50000000000006,
-1.49215395450569));
#412661=CARTESIAN_POINT('Ctrl Pts',(-0.325284941199979,1.47341187781026,
-1.48361116201977));
#412662=CARTESIAN_POINT('Ctrl Pts',(-0.666774070055783,1.35800653720901,
-1.46397555474166));
#412663=CARTESIAN_POINT('Ctrl Pts',(-0.839084622063507,1.25885117771763,
-1.45293094390141));
#412664=CARTESIAN_POINT('Ctrl Pts',(-1.13035010986776,1.00419423254928,
-1.43184362255317));
#412665=CARTESIAN_POINT('Ctrl Pts',(-1.24829156360079,0.853133852358968,
-1.42239632513096));
#412666=CARTESIAN_POINT('Ctrl Pts',(-1.425604258413,0.507145912590032,-1.40317477292158));
#412667=CARTESIAN_POINT('Ctrl Pts',(-1.4801939064406,0.313921894434058,
-1.39244010524625));
#412668=CARTESIAN_POINT('Ctrl Pts',(-1.51054280030923,-0.0783130896786427,
-1.37064927279555));
#412669=CARTESIAN_POINT('Ctrl Pts',(-1.48765448455202,-0.273434472762779,
-1.35980919595754));
#412670=CARTESIAN_POINT('Ctrl Pts',(-1.36966045789988,-0.640766391251696,
-1.3394018671526));
#412671=CARTESIAN_POINT('Ctrl Pts',(-1.27694880415301,-0.80990821445398,
-1.33060644425));
#412672=CARTESIAN_POINT('Ctrl Pts',(-1.02734853964785,-1.11110493461528,
-1.31023097036481));
#412673=CARTESIAN_POINT('Ctrl Pts',(-0.870228411340921,-1.23801764817459,
-1.29914617151263));
#412674=CARTESIAN_POINT('Ctrl Pts',(-0.522267470058889,-1.41923902210377,
-1.27737096586599));
#412675=CARTESIAN_POINT('Ctrl Pts',(-0.336126458157626,-1.47446270144526,
-1.26688126116247));
#412676=CARTESIAN_POINT('Ctrl Pts',(0.0506655324405109,-1.5119274905271,
-1.24723103425251));
#412677=CARTESIAN_POINT('Ctrl Pts',(0.247758477655687,-1.49235408951537,
-1.23786732828351));
#412678=CARTESIAN_POINT('Ctrl Pts',(0.624527801942727,-1.37803234427684,
-1.21656440168249));
#412679=CARTESIAN_POINT('Ctrl Pts',(0.80034635329346,-1.28392016920687,
-1.2054911006013));
#412680=CARTESIAN_POINT('Ctrl Pts',(1.09983031217248,-1.03758380842166,
-1.1842394952231));
#412681=CARTESIAN_POINT('Ctrl Pts',(1.22240274388499,-0.889884415739311,
-1.17443802309653));
#412682=CARTESIAN_POINT('Ctrl Pts',(1.40997071439767,-0.549103068721887,
-1.15550572604001));
#412683=CARTESIAN_POINT('Ctrl Pts',(1.47024422577187,-0.357614005740911,
-1.14486744476329));
#412684=CARTESIAN_POINT('Ctrl Pts',(1.51225978779453,0.0340669096270831,
-1.12310739390951));
#412685=CARTESIAN_POINT('Ctrl Pts',(1.49500530224573,0.230340624900049,
-1.11220329861657));
#412686=CARTESIAN_POINT('Ctrl Pts',(1.38756521684153,0.600808416508208,
-1.09162175463834));
#412687=CARTESIAN_POINT('Ctrl Pts',(1.30012565076874,0.771995093330025,
-1.08277468305615));
#412688=CARTESIAN_POINT('Ctrl Pts',(1.05964010826565,1.08046460082033,-1.0626357195675));
#412689=CARTESIAN_POINT('Ctrl Pts',(0.905824574968569,1.21231434941454,
-1.05157277325478));
#412690=CARTESIAN_POINT('Ctrl Pts',(0.562208588186646,1.4039687863011,-1.02971680702462));
#412691=CARTESIAN_POINT('Ctrl Pts',(0.377177291438441,1.46456844624561,
-1.01913116072177));
#412692=CARTESIAN_POINT('Ctrl Pts',(0.123991130493491,1.49616075506402,
-1.00607217173987));
#412693=CARTESIAN_POINT('Ctrl Pts',(0.0619646518964964,1.50000000000006,
-1.00298127570437));
#412694=CARTESIAN_POINT('Ctrl Pts',(1.52951944419478E-13,1.50000000000006,
-0.999999999999987));
#412695=CARTESIAN_POINT('Origin',(0.,2.5406128344257E-15,14.));
#412696=CARTESIAN_POINT('',(-2.5584277190752E-14,1.50000000000006,-0.437499999999999));
#412697=CARTESIAN_POINT('',(-9.18485099360549E-17,1.50000000000006,-0.499999999999979));
#412698=CARTESIAN_POINT('',(-1.8369701987211E-16,1.50000000000006,14.));
#412699=CARTESIAN_POINT('Ctrl Pts',(-6.21377949094892E-14,1.50000000000006,
-0.437499999999998));
#412700=CARTESIAN_POINT('Ctrl Pts',(0.173580596425634,1.50000000000006,
-0.44585140033937));
#412701=CARTESIAN_POINT('Ctrl Pts',(0.345993724196958,1.46987362435102,
-0.454983474584967));
#412702=CARTESIAN_POINT('Ctrl Pts',(0.695072954621779,1.34379403305005,
-0.47528076775896));
#412703=CARTESIAN_POINT('Ctrl Pts',(0.865571975060887,1.24084475054896,
-0.486343607996248));
#412704=CARTESIAN_POINT('Ctrl Pts',(1.15671230200722,0.975089906948394,
-0.507733182496353));
#412705=CARTESIAN_POINT('Ctrl Pts',(1.27457179400174,0.815005418983616,
-0.517221921167599));
#412706=CARTESIAN_POINT('Ctrl Pts',(1.43973441003759,0.462712829251458,
-0.536793731708271));
#412707=CARTESIAN_POINT('Ctrl Pts',(1.48710669693086,0.274650118336476,
-0.547241660092437));
#412708=CARTESIAN_POINT('Ctrl Pts',(1.50873745620068,-0.116614669232582,
-0.56897859273516));
#412709=CARTESIAN_POINT('Ctrl Pts',(1.47982573747034,-0.316253690432183,
-0.58006964946847));
#412710=CARTESIAN_POINT('Ctrl Pts',(1.34826529463441,-0.684730366235242,
-0.600540575901972));
#412711=CARTESIAN_POINT('Ctrl Pts',(1.24994476750033,-0.851066300014426,
-0.609336068223602));
#412712=CARTESIAN_POINT('Ctrl Pts',(0.994095986485352,-1.13998606148232,
-0.629671147369168));
#412713=CARTESIAN_POINT('Ctrl Pts',(0.838145624621811,-1.25908547839775,
-0.640482629789217));
#412714=CARTESIAN_POINT('Ctrl Pts',(0.485551981950049,-1.4330965882011,
-0.662280441270788));
#412715=CARTESIAN_POINT('Ctrl Pts',(0.29151619983436,-1.48477858918177,
-0.673051603328882));
#412716=CARTESIAN_POINT('Ctrl Pts',(-0.0964898530872458,-1.50888896974836,
-0.692389286047522));
#412717=CARTESIAN_POINT('Ctrl Pts',(-0.286543981390868,-1.48457803169005,
-0.701714741741183));
#412718=CARTESIAN_POINT('Ctrl Pts',(-0.653931217369355,-1.36420266800585,
-0.722734428475939));
#412719=CARTESIAN_POINT('Ctrl Pts',(-0.826960249159726,-1.2668112528236,
-0.733764608737817));
#412720=CARTESIAN_POINT('Ctrl Pts',(-1.1272064357018,-1.00942186759203,
-0.755359915268406));
#412721=CARTESIAN_POINT('Ctrl Pts',(-1.25089002162263,-0.851336442437078,
-0.765203530975736));
#412722=CARTESIAN_POINT('Ctrl Pts',(-1.42625796427823,-0.502520518591022,
-0.784582193411627));
#412723=CARTESIAN_POINT('Ctrl Pts',(-1.47872436454764,-0.31637284196314,
-0.794923731002064));
#412724=CARTESIAN_POINT('Ctrl Pts',(-1.51139791543748,0.0730104938014621,
-0.816556138544541));
#412725=CARTESIAN_POINT('Ctrl Pts',(-1.4883691825351,0.27280329776716,-0.827655738764857));
#412726=CARTESIAN_POINT('Ctrl Pts',(-1.36768356350131,0.64535123374593,
-0.848352846319232));
#412727=CARTESIAN_POINT('Ctrl Pts',(-1.27371349050755,0.815284648275066,
-0.857198560234187));
#412728=CARTESIAN_POINT('Ctrl Pts',(-1.02573471227558,1.11151062047477,
-0.877357943992418));
#412729=CARTESIAN_POINT('Ctrl Pts',(-0.873648710432303,1.23463054467116,
-0.88809518306211));
#412730=CARTESIAN_POINT('Ctrl Pts',(-0.52667301189673,1.41850422189462,
-0.909896661286518));
#412731=CARTESIAN_POINT('Ctrl Pts',(-0.334179940101096,1.47576515148728,
-0.920748569898953));
#412732=CARTESIAN_POINT('Ctrl Pts',(-0.0907817741771738,1.49794192209733,
-0.933075091022824));
#412733=CARTESIAN_POINT('Ctrl Pts',(-0.0453672191895883,1.50000000000005,
-0.935317268649044));
#412734=CARTESIAN_POINT('Ctrl Pts',(-2.03832677232616E-13,1.50000000000006,
-0.937499999999992));
#412735=CARTESIAN_POINT('Ctrl Pts',(1.46913731180476E-13,1.50000000000006,
-0.999999999999986));
#412736=CARTESIAN_POINT('Ctrl Pts',(-0.131899581151311,1.50000000000006,
-0.993653978443012));
#412737=CARTESIAN_POINT('Ctrl Pts',(-0.263472160605492,1.48260736580286,
-0.986840561034739));
#412738=CARTESIAN_POINT('Ctrl Pts',(-0.582573966398612,1.39637102289311,
-0.969092314275562));
#412739=CARTESIAN_POINT('Ctrl Pts',(-0.761689021652897,1.30731357265555,
-0.958000819099493));
#412740=CARTESIAN_POINT('Ctrl Pts',(-1.06907929995926,1.06931057908566,
-0.936600303173127));
#412741=CARTESIAN_POINT('Ctrl Pts',(-1.19623673913263,0.924877016116167,
-0.926470394612626));
#412742=CARTESIAN_POINT('Ctrl Pts',(-1.39367914953313,0.589190131513344,
-0.907646306529701));
#412743=CARTESIAN_POINT('Ctrl Pts',(-1.45942723684233,0.399519099757115,
-0.897195505541958));
#412744=CARTESIAN_POINT('Ctrl Pts',(-1.51268906272795,0.00856741889772205,
-0.875475967716439));
#412745=CARTESIAN_POINT('Ctrl Pts',(-1.50090383822517,-0.188664743856311,
-0.864518625341217));
#412746=CARTESIAN_POINT('Ctrl Pts',(-1.40364785614872,-0.562075240715819,
-0.843773597737913));
#412747=CARTESIAN_POINT('Ctrl Pts',(-1.32118880347593,-0.735259580504762,
-0.834808515375079));
#412748=CARTESIAN_POINT('Ctrl Pts',(-1.0907670814543,-1.04870959175978,
-0.815015400348303));
#412749=CARTESIAN_POINT('Ctrl Pts',(-0.942260035311356,-1.18393070164062,
-0.804114209818238));
#412750=CARTESIAN_POINT('Ctrl Pts',(-0.605830191961757,-1.38578633010734,
-0.782320620642388));
#412751=CARTESIAN_POINT('Ctrl Pts',(-0.422204016207854,-1.45230578227655,
-0.771638139581986));
#412752=CARTESIAN_POINT('Ctrl Pts',(-0.0400986940400851,-1.51185958119907,
-0.751599816505332));
#412753=CARTESIAN_POINT('Ctrl Pts',(0.154725281291594,-1.50445690023413,
-0.74267957921716));
#412754=CARTESIAN_POINT('Ctrl Pts',(0.536319722570401,-1.41487308640885,
-0.721831668828105));
#412755=CARTESIAN_POINT('Ctrl Pts',(0.718861257413663,-1.33144084341973,
-0.710731572832847));
#412756=CARTESIAN_POINT('Ctrl Pts',(1.0347253322851,-1.10268938550674,-0.689180348280738));
#412757=CARTESIAN_POINT('Ctrl Pts',(1.16677741219797,-0.961890420146206,
-0.678915907252553));
#412758=CARTESIAN_POINT('Ctrl Pts',(1.37557057361387,-0.630762884694104,
-0.659672354494296));
#412759=CARTESIAN_POINT('Ctrl Pts',(1.4473878108606,-0.441771302548477,
-0.649542850141474));
#412760=CARTESIAN_POINT('Ctrl Pts',(1.51193683368003,-0.0505838155729788,
-0.62781021197617));
#412761=CARTESIAN_POINT('Ctrl Pts',(1.50558094216201,0.147446649609004,
-0.61680851946606));
#412762=CARTESIAN_POINT('Ctrl Pts',(1.41839292597098,0.523684067536241,
-0.595906440692327));
#412763=CARTESIAN_POINT('Ctrl Pts',(1.34076354521001,0.698870895164634,
-0.586761102390866));
#412764=CARTESIAN_POINT('Ctrl Pts',(1.11916700372969,1.01834261045172,-0.567225319504408));
#412765=CARTESIAN_POINT('Ctrl Pts',(0.9744492721012,1.15757682489316,-0.55639496732724));
#412766=CARTESIAN_POINT('Ctrl Pts',(0.643288707878562,1.36887271675508,
-0.534592666922834));
#412767=CARTESIAN_POINT('Ctrl Pts',(0.461036608622036,1.44051741693377,
-0.523833928148471));
#412768=CARTESIAN_POINT('Ctrl Pts',(0.180842166400501,1.49182645708902,
-0.508927815646213));
#412769=CARTESIAN_POINT('Ctrl Pts',(0.0904158668629034,1.50000000000006,
-0.504350135422671));
#412770=CARTESIAN_POINT('Ctrl Pts',(0.,1.50000000000006,-0.499999999999979));
#412771=CARTESIAN_POINT('Origin',(0.,2.5406128344257E-15,14.));
#412772=CARTESIAN_POINT('',(-9.18485099360549E-17,1.50000000000006,0.0624999999999975));
#412773=CARTESIAN_POINT('',(-2.55842840407684E-14,1.50000000000006,2.41061511030425E-14));
#412774=CARTESIAN_POINT('',(-1.8369701987211E-16,1.50000000000006,14.));
#412775=CARTESIAN_POINT('Ctrl Pts',(0.,1.50000000000006,0.0624999999999976));
#412776=CARTESIAN_POINT('Ctrl Pts',(0.012054289146646,1.50000000000006,
0.0619200377430222));
#412777=CARTESIAN_POINT('Ctrl Pts',(0.0241143953777522,1.49985469449604,
0.0613357593474155));
#412778=CARTESIAN_POINT('Ctrl Pts',(0.227159790220428,1.49495612231971,
0.0514306617838963));
#412779=CARTESIAN_POINT('Ctrl Pts',(0.415482244731523,1.45390737684839,
0.0412297505369348));
#412780=CARTESIAN_POINT('Ctrl Pts',(0.773383422037556,1.30048073774713,
0.0197483710290463));
#412781=CARTESIAN_POINT('Ctrl Pts',(0.93845214862749,1.18688107122445,0.00865095192579394));
#412782=CARTESIAN_POINT('Ctrl Pts',(1.2116261284016,0.905291054690885,-0.0123140822077631));
#412783=CARTESIAN_POINT('Ctrl Pts',(1.31834906133297,0.741310066150857,
-0.021316107436091));
#412784=CARTESIAN_POINT('Ctrl Pts',(1.4632645623403,0.382356276828995,-0.0412579846206378));
#412785=CARTESIAN_POINT('Ctrl Pts',(1.50029477690078,0.19089170271958,-0.0518949054044928));
#412786=CARTESIAN_POINT('Ctrl Pts',(1.4996898553524,-0.203205997702154,
-0.0737892220945868));
#412787=CARTESIAN_POINT('Ctrl Pts',(1.45902227025322,-0.402037982209106,
-0.084835443456084));
#412788=CARTESIAN_POINT('Ctrl Pts',(1.30593786665162,-0.762053788740558,
-0.104836321596719));
#412789=CARTESIAN_POINT('Ctrl Pts',(1.19886813597746,-0.921369750070448,
-0.113746367416195));
#412790=CARTESIAN_POINT('Ctrl Pts',(0.927156984189888,-1.19524181015156,
-0.134426633526201));
#412791=CARTESIAN_POINT('Ctrl Pts',(0.763651532865142,-1.30577691246609,
-0.14536371272963));
#412792=CARTESIAN_POINT('Ctrl Pts',(0.400480218338332,-1.45914764262538,
-0.16709709880661));
#412793=CARTESIAN_POINT('Ctrl Pts',(0.203815102558579,-1.4993273908806,
-0.177675257719447));
#412794=CARTESIAN_POINT('Ctrl Pts',(-0.185401401652342,-1.50062783086148,
-0.196437568842183));
#412795=CARTESIAN_POINT('Ctrl Pts',(-0.374284202094425,-1.46499993765963,
-0.20647998102331));
#412796=CARTESIAN_POINT('Ctrl Pts',(-0.735490393930043,-1.3221946159591,
-0.227825336522426));
#412797=CARTESIAN_POINT('Ctrl Pts',(-0.903290925767023,-1.21376054447359,
-0.238910700915876));
#412798=CARTESIAN_POINT('Ctrl Pts',(-1.1852683061334,-0.939824153228578,
-0.26008668815545));
#412799=CARTESIAN_POINT('Ctrl Pts',(-1.2973924118842,-0.77774928530609,
-0.269291706371907));
#412800=CARTESIAN_POINT('Ctrl Pts',(-1.4522514080294,-0.422027875514621,
-0.289054006915876));
#412801=CARTESIAN_POINT('Ctrl Pts',(-1.49439722341846,-0.232166380326087,
-0.299601867759683));
#412802=CARTESIAN_POINT('Ctrl Pts',(-1.50476095174324,0.160691684605172,
-0.321427315811418));
#412803=CARTESIAN_POINT('Ctrl Pts',(-1.46987757693276,0.360003953280259,
-0.3325002196267));
#412804=CARTESIAN_POINT('Ctrl Pts',(-1.32735514008263,0.724238208405123,
-0.352735456022524));
#412805=CARTESIAN_POINT('Ctrl Pts',(-1.22460662669361,0.886980672789432,
-0.361552771557538));
#412806=CARTESIAN_POINT('Ctrl Pts',(-0.960726520483816,1.16833841263676,
-0.382064201860574));
#412807=CARTESIAN_POINT('Ctrl Pts',(-0.800909367067889,1.28317803984535,
-0.392943397884075));
#412808=CARTESIAN_POINT('Ctrl Pts',(-0.442830785125446,1.44686319665528,
-0.414718271601753));
#412809=CARTESIAN_POINT('Ctrl Pts',(-0.247381584421267,1.49276234346049,
-0.425396801955183));
#412810=CARTESIAN_POINT('Ctrl Pts',(-0.0324259740880306,1.49973729413911,
-0.435932607209287));
#412811=CARTESIAN_POINT('Ctrl Pts',(-0.0162082427937986,1.50000000000006,
-0.436720180554994));
#412812=CARTESIAN_POINT('Ctrl Pts',(-5.09848573616319E-14,1.50000000000006,
-0.437499999999999));
#412813=CARTESIAN_POINT('Ctrl Pts',(7.45931094670027E-16,1.50000000000006,
-0.499999999999979));
#412814=CARTESIAN_POINT('Ctrl Pts',(-0.100870160085812,1.50000000000006,
-0.495146882160084));
#412815=CARTESIAN_POINT('Ctrl Pts',(-0.20169983483153,1.48982736637166,
-0.490013139015587));
#412816=CARTESIAN_POINT('Ctrl Pts',(-0.496243158183144,1.42950096301812,
-0.474166183337012));
#412817=CARTESIAN_POINT('Ctrl Pts',(-0.681583232330906,1.3509861438843,
-0.463068037663782));
#412818=CARTESIAN_POINT('Ctrl Pts',(-1.00448658647526,1.13038954226337,
-0.441404659415633));
#412819=CARTESIAN_POINT('Ctrl Pts',(-1.14064794355933,0.992832675357211,
-0.431032568987764));
#412820=CARTESIAN_POINT('Ctrl Pts',(-1.3573289981967,0.668537834146947,
-0.411599306852214));
#412821=CARTESIAN_POINT('Ctrl Pts',(-1.43370523838309,0.48352662619307,
-0.401862590343936));
#412822=CARTESIAN_POINT('Ctrl Pts',(-1.50981966629285,0.095837857719107,
-0.380324325428716));
#412823=CARTESIAN_POINT('Ctrl Pts',(-1.50935560392058,-0.102889185679314,
-0.369283934128803));
#412824=CARTESIAN_POINT('Ctrl Pts',(-1.43306586861821,-0.482091858059621,
-0.348217118996566));
#412825=CARTESIAN_POINT('Ctrl Pts',(-1.36056953424563,-0.659480305237118,
-0.338808201536163));
#412826=CARTESIAN_POINT('Ctrl Pts',(-1.14840390936391,-0.985248392224554,
-0.319551264622214));
#412827=CARTESIAN_POINT('Ctrl Pts',(-1.00783288225427,-1.12862552383915,
-0.308805339826642));
#412828=CARTESIAN_POINT('Ctrl Pts',(-0.682561860333359,-1.34979812671681,
-0.287012047074571));
#412829=CARTESIAN_POINT('Ctrl Pts',(-0.501923892968732,-1.42685954182922,
-0.276180503953351));
#412830=CARTESIAN_POINT('Ctrl Pts',(-0.124496714670119,-1.50701298862099,
-0.255795045737731));
#412831=CARTESIAN_POINT('Ctrl Pts',(0.0684526444356624,-1.51059602506114,
-0.247000904638357));
#412832=CARTESIAN_POINT('Ctrl Pts',(0.453870608993343,-1.44359645502584,
-0.226596375005052));
#412833=CARTESIAN_POINT('Ctrl Pts',(0.642002889011626,-1.37032399989127,
-0.21550951048644));
#412834=CARTESIAN_POINT('Ctrl Pts',(0.972052791411423,-1.15848637848887,
-0.193745598781109));
#412835=CARTESIAN_POINT('Ctrl Pts',(1.11243019608887,-1.02444870831659,
-0.183268419133659));
#412836=CARTESIAN_POINT('Ctrl Pts',(1.33726432612642,-0.707317214958666,
-0.163641873859811));
#412837=CARTESIAN_POINT('Ctrl Pts',(1.41828932336204,-0.526348860670041,
-0.154241603370399));
#412838=CARTESIAN_POINT('Ctrl Pts',(1.50621864088017,-0.142421766452506,
-0.132912320358315));
#412839=CARTESIAN_POINT('Ctrl Pts',(1.51186799289991,0.0568439120604016,
-0.121842004885376));
#412840=CARTESIAN_POINT('Ctrl Pts',(1.44687788961899,0.439013439406849,
-0.100610364477241));
#412841=CARTESIAN_POINT('Ctrl Pts',(1.37961132542521,0.6187237847525,-0.0908564757104214));
#412842=CARTESIAN_POINT('Ctrl Pts',(1.1770866073687,0.950789355903772,-0.0718884570267085));
#412843=CARTESIAN_POINT('Ctrl Pts',(1.040850589036,1.09824308004335,-0.0612378617569129));
#412844=CARTESIAN_POINT('Ctrl Pts',(0.721863706966089,1.32927659203654,
-0.039473000682295));
#412845=CARTESIAN_POINT('Ctrl Pts',(0.543027040436241,1.41180481335541,
-0.0285762669599376));
#412846=CARTESIAN_POINT('Ctrl Pts',(0.237438697047166,1.48588709847123,
-0.0118157996803148));
#412847=CARTESIAN_POINT('Ctrl Pts',(0.118813593213069,1.50000000000006,
-0.00571642166872418));
#412848=CARTESIAN_POINT('Ctrl Pts',(-4.74273398332059E-14,1.50000000000006,
2.38090797077817E-14));
#412849=CARTESIAN_POINT('Origin',(0.,2.5406128344257E-15,14.));
#412850=CARTESIAN_POINT('',(1.27348944451369E-13,1.50000000000006,0.562499999999986));
#412851=CARTESIAN_POINT('',(-1.01921478372424E-13,1.50000000000006,0.50000000000003));
#412852=CARTESIAN_POINT('',(-1.8369701987211E-16,1.50000000000006,14.));
#412853=CARTESIAN_POINT('Ctrl Pts',(2.54881585922611E-13,1.50000000000006,
0.562499999999986));
#412854=CARTESIAN_POINT('Ctrl Pts',(0.0406408989401091,1.50000000000006,
0.560544663838062));
#412855=CARTESIAN_POINT('Ctrl Pts',(0.0813262693164112,1.4983483840002,
0.558541309820913));
#412856=CARTESIAN_POINT('Ctrl Pts',(0.313442176157069,1.47941358982352,
0.546847661541202));
#412857=CARTESIAN_POINT('Ctrl Pts',(0.500127801022325,1.4271521204739,0.536414037745119));
#412858=CARTESIAN_POINT('Ctrl Pts',(0.850346715884616,1.25170506897473,
0.514690593139223));
#412859=CARTESIAN_POINT('Ctrl Pts',(1.00921900268806,1.12753921057511,0.503597795054284));
#412860=CARTESIAN_POINT('Ctrl Pts',(1.26379674107868,0.830384213019557,
0.483095112417506));
#412861=CARTESIAN_POINT('Ctrl Pts',(1.35941976917598,0.662343199038309,
0.474296844390982));
#412862=CARTESIAN_POINT('Ctrl Pts',(1.48314056992831,0.296749108474254,
0.45398606158187));
#412863=CARTESIAN_POINT('Ctrl Pts',(1.5090677735988,0.102320123342678,0.443184451296783));
#412864=CARTESIAN_POINT('Ctrl Pts',(1.4850548862901,-0.290069550070151,
0.421385024996072));
#412865=CARTESIAN_POINT('Ctrl Pts',(1.43357470864608,-0.484163398894276,
0.410602033394734));
#412866=CARTESIAN_POINT('Ctrl Pts',(1.26185297329218,-0.832935861582507,
0.391225785467612));
#412867=CARTESIAN_POINT('Ctrl Pts',(1.14639029827533,-0.985832644872433,
0.381938155473427));
#412868=CARTESIAN_POINT('Ctrl Pts',(0.859555578540014,-1.24491280118131,
0.360941142577173));
#412869=CARTESIAN_POINT('Ctrl Pts',(0.689185616573045,-1.34672400738396,
0.349916124899035));
#412870=CARTESIAN_POINT('Ctrl Pts',(0.316533522162275,-1.47967569734543,
0.328293790148262));
#412871=CARTESIAN_POINT('Ctrl Pts',(0.117624745672662,-1.50856522554025,
0.318397146146432));
#412872=CARTESIAN_POINT('Ctrl Pts',(-0.27241708027596,-1.48744781999047,
0.299044655447275));
#412873=CARTESIAN_POINT('Ctrl Pts',(-0.459965936736015,-1.44052839410447,
0.288717889497935));
#412874=CARTESIAN_POINT('Ctrl Pts',(-0.814014715386158,-1.27554039433401,
0.267100709699319));
#412875=CARTESIAN_POINT('Ctrl Pts',(-0.975924727411788,-1.156375414924,
0.256000672296751));
#412876=CARTESIAN_POINT('Ctrl Pts',(-1.23940847168001,-0.866578105453092,
0.235273879476976));
#412877=CARTESIAN_POINT('Ctrl Pts',(-1.34029906880132,-0.700490994357527,
0.226416166353165));
#412878=CARTESIAN_POINT('Ctrl Pts',(-1.47420654920234,-0.338046251999789,
0.206280347333291));
#412879=CARTESIAN_POINT('Ctrl Pts',(-1.50550075040419,-0.144963845736001,
0.195553546985305));
#412880=CARTESIAN_POINT('Ctrl Pts',(-1.49275257816999,0.247446765567662,
0.173752957468437));
#412881=CARTESIAN_POINT('Ctrl Pts',(-1.44683992264741,0.442960968548592,
0.162891057302831));
#412882=CARTESIAN_POINT('Ctrl Pts',(-1.28510797535013,0.796611616917752,
0.143243799060103));
#412883=CARTESIAN_POINT('Ctrl Pts',(-1.17400046898735,0.952800260806589,
0.134184116655229));
#412884=CARTESIAN_POINT('Ctrl Pts',(-0.894994052729665,1.21959421410027,
0.113349471047183));
#412885=CARTESIAN_POINT('Ctrl Pts',(-0.728132560453016,1.32598777580278,
0.102365967042949));
#412886=CARTESIAN_POINT('Ctrl Pts',(-0.371528935965003,1.46521793089753,
0.0813413628520834));
#412887=CARTESIAN_POINT('Ctrl Pts',(-0.186506457465428,1.50000000000006,
0.0714732961186032));
#412888=CARTESIAN_POINT('Ctrl Pts',(-3.15719672627779E-15,1.50000000000006,
0.0624999999999978));
#412889=CARTESIAN_POINT('Ctrl Pts',(-5.09848710616648E-14,1.50000000000006,
2.38546161990259E-14));
#412890=CARTESIAN_POINT('Ctrl Pts',(-0.0709875012889099,1.50000000000006,
0.00341538774820884));
#412891=CARTESIAN_POINT('Ctrl Pts',(-0.142028686340236,1.49496141470086,
0.00697331906053692));
#412892=CARTESIAN_POINT('Ctrl Pts',(-0.411099076206722,1.45643705631314,
0.0209890952952234));
#412893=CARTESIAN_POINT('Ctrl Pts',(-0.601880785957816,1.38850081793605,
0.0320552023180216));
#412894=CARTESIAN_POINT('Ctrl Pts',(-0.938844531503994,1.18564451242515,
0.0539022754598391));
#412895=CARTESIAN_POINT('Ctrl Pts',(-1.08334734961584,1.05525225377623,
0.0644766777224905));
#412896=CARTESIAN_POINT('Ctrl Pts',(-1.31623827713633,0.74530117362232,
0.0842913999236317));
#412897=CARTESIAN_POINT('Ctrl Pts',(-1.40180453069513,0.568250798011601,
0.0934305112217602));
#412898=CARTESIAN_POINT('Ctrl Pts',(-1.50126820996767,0.188174214398025,
0.114545876978065));
#412899=CARTESIAN_POINT('Ctrl Pts',(-1.51297047242782,-0.0114425435933111,
0.12563569686647));
#412900=CARTESIAN_POINT('Ctrl Pts',(-1.4591968707338,-0.396327239575063,
0.147018179976564));
#412901=CARTESIAN_POINT('Ctrl Pts',(-1.39707708900367,-0.578386341706428,
0.157132574539417));
#412902=CARTESIAN_POINT('Ctrl Pts',(-1.20396132549991,-0.916492801378582,
0.175916266743421));
#412903=CARTESIAN_POINT('Ctrl Pts',(-1.07206249365286,-1.06781241836371,
0.186415158624291));
#412904=CARTESIAN_POINT('Ctrl Pts',(-0.759351410534148,-1.30830487595872,
0.208140823670025));
#412905=CARTESIAN_POINT('Ctrl Pts',(-0.582414938121718,-1.39609256486489,
0.219092230581993));
#412906=CARTESIAN_POINT('Ctrl Pts',(-0.210095445423381,-1.49734090530431,
0.23981791442758));
#412907=CARTESIAN_POINT('Ctrl Pts',(-0.0187966379690382,-1.51188883256379,
0.248765400985086));
#412908=CARTESIAN_POINT('Ctrl Pts',(0.36776423073231,-1.46775849240247,
0.268589662234254));
#412909=CARTESIAN_POINT('Ctrl Pts',(0.558918940856327,-1.40611402825547,
0.279498943739474));
#412910=CARTESIAN_POINT('Ctrl Pts',(0.901250708619873,-1.21456036593823,
0.301290323659713));
#412911=CARTESIAN_POINT('Ctrl Pts',(1.0502060064706,-1.08834353623334,0.31196296181635));
#412912=CARTESIAN_POINT('Ctrl Pts',(1.29190529576069,-0.786360349714089,
0.331980146141988));
#412913=CARTESIAN_POINT('Ctrl Pts',(1.38239012590076,-0.613500578045895,
0.340916634553032));
#412914=CARTESIAN_POINT('Ctrl Pts',(1.49430302141388,-0.237771999146122,
0.361790444491908));
#412915=CARTESIAN_POINT('Ctrl Pts',(1.5126224446182,-0.0379766749085486,
0.372890184727328));
#412916=CARTESIAN_POINT('Ctrl Pts',(1.47115013980118,0.349676795606788,
0.394426488644846));
#412917=CARTESIAN_POINT('Ctrl Pts',(1.41464528846236,0.534188936917993,
0.404677163162135));
#412918=CARTESIAN_POINT('Ctrl Pts',(1.23105735621897,0.880145184501605,
0.423896954694558));
#412919=CARTESIAN_POINT('Ctrl Pts',(1.1025766449906,1.03659133669472,0.434079793564812));
#412920=CARTESIAN_POINT('Ctrl Pts',(0.794982012712315,1.28704585517344,
0.455836017168149));
#412921=CARTESIAN_POINT('Ctrl Pts',(0.620024979142385,1.37987519435246,
0.466832234125473));
#412922=CARTESIAN_POINT('Ctrl Pts',(0.291744411200726,1.47864384033826,
0.485370213814313));
#412923=CARTESIAN_POINT('Ctrl Pts',(0.146157289931562,1.50000000000008,
0.49296800410952));
#412924=CARTESIAN_POINT('Ctrl Pts',(-2.06189232354603E-13,1.50000000000006,
0.50000000000003));
#412925=CARTESIAN_POINT('Origin',(0.,2.5406128344257E-15,14.));
#412926=CARTESIAN_POINT('',(5.08396327447441E-14,1.50000000000006,1.06249999999999));
#412927=CARTESIAN_POINT('',(-9.18485099360549E-17,1.50000000000006,1.00000000000002));
#412928=CARTESIAN_POINT('',(-1.8369701987211E-16,1.50000000000006,14.));
#412929=CARTESIAN_POINT('Ctrl Pts',(1.0186296250936E-13,1.50000000000006,
1.06249999999999));
#412930=CARTESIAN_POINT('Ctrl Pts',(0.0680382842757857,1.50000000000006,
1.05922650652151));
#412931=CARTESIAN_POINT('Ctrl Pts',(0.136136544871693,1.49537132922985,
1.05582155324288));
#412932=CARTESIAN_POINT('Ctrl Pts',(0.395203876533196,1.45983798970958,
1.0423701332279));
#412933=CARTESIAN_POINT('Ctrl Pts',(0.579696520662932,1.39687125311336,
1.03174465073202));
#412934=CARTESIAN_POINT('Ctrl Pts',(0.921297492681591,1.20064222399006,
1.00985855993829));
#412935=CARTESIAN_POINT('Ctrl Pts',(1.07360653158139,1.06663849347069,0.998808262039792));
#412936=CARTESIAN_POINT('Ctrl Pts',(1.31004293758201,0.754988953245441,
0.978775778479312));
#412937=CARTESIAN_POINT('Ctrl Pts',(1.3951625075513,0.582880009906409,0.969882222772534));
#412938=CARTESIAN_POINT('Ctrl Pts',(1.49788420655235,0.211038565719377,
0.949224364762146));
#412939=CARTESIAN_POINT('Ctrl Pts',(1.51260816412702,0.0143019682214694,
0.93829455379004));
#412940=CARTESIAN_POINT('Ctrl Pts',(1.46538570869696,-0.377018865546308,
0.91655450746961));
#412941=CARTESIAN_POINT('Ctrl Pts',(1.40259296866089,-0.567677864245,0.905962340875239));
#412942=CARTESIAN_POINT('Ctrl Pts',(1.21046020806795,-0.906101173453465,
0.887161045919216));
#412943=CARTESIAN_POINT('Ctrl Pts',(1.08578909657305,-1.05230619708041,
0.877175991235747));
#412944=CARTESIAN_POINT('Ctrl Pts',(0.782609624085623,-1.29484936108939,
0.855851951953274));
#412945=CARTESIAN_POINT('Ctrl Pts',(0.605253911944434,-1.38664503724576,
0.844769041381123));
#412946=CARTESIAN_POINT('Ctrl Pts',(0.227357440291247,-1.49550062377031,
0.823563722619211));
#412947=CARTESIAN_POINT('Ctrl Pts',(0.0307822054468046,-1.51236761327203,
0.81432455436315));
#412948=CARTESIAN_POINT('Ctrl Pts',(-0.355011658420151,-1.47006145389006,
0.794587867339601));
#412949=CARTESIAN_POINT('Ctrl Pts',(-0.540662172389121,-1.41236706042891,
0.784053130781083));
#412950=CARTESIAN_POINT('Ctrl Pts',(-0.886665972559036,-1.22634334768617,
0.762238689829726));
#412951=CARTESIAN_POINT('Ctrl Pts',(-1.04228741892642,-1.09715391965502,
0.751162754277315));
#412952=CARTESIAN_POINT('Ctrl Pts',(-1.28771223104499,-0.792605411430979,
0.730895066714778));
#412953=CARTESIAN_POINT('Ctrl Pts',(-1.37799972031613,-0.622531871559214,
0.722085103975474));
#412954=CARTESIAN_POINT('Ctrl Pts',(-1.49117016866574,-0.253755936497839,
0.701597552027621));
#412955=CARTESIAN_POINT('Ctrl Pts',(-1.5114885454466,-0.0580879035252565,
0.690727105751367));
#412956=CARTESIAN_POINT('Ctrl Pts',(-1.47580497889151,0.333937053169343,
0.668947941490558));
#412957=CARTESIAN_POINT('Ctrl Pts',(-1.41860962415413,0.526389181544339,
0.658256156580836));
#412958=CARTESIAN_POINT('Ctrl Pts',(-1.23660211030209,0.87000933239387,
0.639166148200308));
#412959=CARTESIAN_POINT('Ctrl Pts',(-1.11655459910737,1.0195301344132,0.629566643351781));
#412960=CARTESIAN_POINT('Ctrl Pts',(-0.821541279919785,1.270411883044,0.608403870952528));
#412961=CARTESIAN_POINT('Ctrl Pts',(-0.647615965374159,1.36728612241562,
0.597344934261222));
#412962=CARTESIAN_POINT('Ctrl Pts',(-0.311066258152681,1.47570356486116,
0.578141083299403));
#412963=CARTESIAN_POINT('Ctrl Pts',(-0.155892677277793,1.50000000000006,
0.570000389932598));
#412964=CARTESIAN_POINT('Ctrl Pts',(2.56461518688411E-13,1.50000000000006,
0.562499999999986));
#412965=CARTESIAN_POINT('Ctrl Pts',(-2.03659259724975E-13,1.50000000000006,
0.50000000000003));
#412966=CARTESIAN_POINT('Ctrl Pts',(-0.043191708028036,1.50000000000005,
0.502078062021416));
#412967=CARTESIAN_POINT('Ctrl Pts',(-0.0864282246675912,1.49813456320497,
0.504210097586897));
#412968=CARTESIAN_POINT('Ctrl Pts',(-0.327738068046906,1.47720865117899,
0.516401398173714));
#412969=CARTESIAN_POINT('Ctrl Pts',(-0.520475306897241,1.42078936554684,
0.527241675280143));
#412970=CARTESIAN_POINT('Ctrl Pts',(-0.868319352452527,1.23839726903149,
0.549043776850346));
#412971=CARTESIAN_POINT('Ctrl Pts',(-1.02099688329402,1.11587823707962,
0.559792784420996));
#412972=CARTESIAN_POINT('Ctrl Pts',(-1.27017123344605,0.820755811782216,
0.579979036079432));
#412973=CARTESIAN_POINT('Ctrl Pts',(-1.36480343662259,0.651373723038201,
0.588812570942347));
#412974=CARTESIAN_POINT('Ctrl Pts',(-1.48714974026619,0.279438547031942,
0.609475636276026));
#412975=CARTESIAN_POINT('Ctrl Pts',(-1.51107383067189,0.0796583666816162,
0.620574535184376));
#412976=CARTESIAN_POINT('Ctrl Pts',(-1.48007727192697,-0.310031319599864,
0.642223962200013));
#412977=CARTESIAN_POINT('Ctrl Pts',(-1.42838264999849,-0.49647962280372,
0.652582201266895));
#412978=CARTESIAN_POINT('Ctrl Pts',(-1.25457208539778,-0.845831340986355,
0.671990630054817));
#412979=CARTESIAN_POINT('Ctrl Pts',(-1.13178665459598,-1.00422413691273,
0.68177533743958));
#412980=CARTESIAN_POINT('Ctrl Pts',(-0.832931565108941,-1.26290740472686,
0.70333965596475));
#412981=CARTESIAN_POINT('Ctrl Pts',(-0.660279040728227,-1.36115474455317,
0.71437549718999));
#412982=CARTESIAN_POINT('Ctrl Pts',(-0.293350074741007,-1.48324987324057,
0.7354209066496));
#412983=CARTESIAN_POINT('Ctrl Pts',(-0.103396430208456,-1.50843250688356,
0.744791100629857));
#412984=CARTESIAN_POINT('Ctrl Pts',(0.2847199519682,-1.48609621704444,0.764084811269269));
#412985=CARTESIAN_POINT('Ctrl Pts',(0.478985398772131,-1.43530395959292,
0.774842307976797));
#412986=CARTESIAN_POINT('Ctrl Pts',(0.832445184826515,-1.26287480719448,
0.796637848540046));
#412987=CARTESIAN_POINT('Ctrl Pts',(0.988999606252736,-1.14442470702295,
0.807460357213135));
#412988=CARTESIAN_POINT('Ctrl Pts',(1.24609216178188,-0.856668614388136,
0.827822953353661));
#412989=CARTESIAN_POINT('Ctrl Pts',(1.34509862215902,-0.690894590198938,
0.836616967211182));
#412990=CARTESIAN_POINT('Ctrl Pts',(1.47836546238066,-0.323069043266823,
0.857051719818521));
#412991=CARTESIAN_POINT('Ctrl Pts',(1.50820423027976,-0.123469482155708,
0.868140584324693));
#412992=CARTESIAN_POINT('Ctrl Pts',(1.48831877173615,0.268063539597317,
0.889892418866527));
#412993=CARTESIAN_POINT('Ctrl Pts',(1.44175418543378,0.45641507535595,0.90035639307534));
#412994=CARTESIAN_POINT('Ctrl Pts',(1.27819434454985,0.809246369246787,
0.919958131624831));
#412995=CARTESIAN_POINT('Ctrl Pts',(1.16123647414513,0.969641981338816,
0.929397816903269));
#412996=CARTESIAN_POINT('Ctrl Pts',(0.871523790004527,1.23668668522225,
0.950754533359159));
#412997=CARTESIAN_POINT('Ctrl Pts',(0.701435278023972,1.34049769856449,
0.961821559966836));
#412998=CARTESIAN_POINT('Ctrl Pts',(0.350660738991283,1.46904663991433,
0.982269011771168));
#412999=CARTESIAN_POINT('Ctrl Pts',(0.175945122352012,1.50000000000006,
0.991534836353976));
#413000=CARTESIAN_POINT('Ctrl Pts',(3.41740524767431E-15,1.50000000000006,
1.00000000000002));
#413001=CARTESIAN_POINT('Origin',(0.,2.5406128344257E-15,14.));
#413002=CARTESIAN_POINT('',(-9.18485099360549E-17,1.50000000000006,1.5625));
#413003=CARTESIAN_POINT('',(-9.18485099360549E-17,1.50000000000006,1.50000000000002));
#413004=CARTESIAN_POINT('',(-1.8369701987211E-16,1.50000000000006,14.));
#413005=CARTESIAN_POINT('Ctrl Pts',(0.,1.50000000000006,1.5625));
#413006=CARTESIAN_POINT('Ctrl Pts',(0.0966928609426964,1.50000000000006,
1.55784786255883));
#413007=CARTESIAN_POINT('Ctrl Pts',(0.193367170400976,1.49065233465526,
1.55293696030564));
#413008=CARTESIAN_POINT('Ctrl Pts',(0.479319745183868,1.43457013871789,
1.53762122186073));
#413009=CARTESIAN_POINT('Ctrl Pts',(0.660871598557134,1.3605059032998,1.52682896436994));
#413010=CARTESIAN_POINT('Ctrl Pts',(0.989442467783122,1.14478539925305,
1.50502835483013));
#413011=CARTESIAN_POINT('Ctrl Pts',(1.13232608393568,1.00368801786495,1.49423449193753));
#413012=CARTESIAN_POINT('Ctrl Pts',(1.34972401676549,0.681396013205005,
1.47482237333249));
#413013=CARTESIAN_POINT('Ctrl Pts',(1.4250652882199,0.505237233551949,1.46556873519728));
#413014=CARTESIAN_POINT('Ctrl Pts',(1.50741977300721,0.127672340085819,
1.44459290778249));
#413015=CARTESIAN_POINT('Ctrl Pts',(1.51116381860928,-0.0706885550306063,
1.4335728580538));
#413016=CARTESIAN_POINT('Ctrl Pts',(1.44146481134182,-0.460340823710175,
1.41192550979383));
#413017=CARTESIAN_POINT('Ctrl Pts',(1.3676157802519,-0.647557592297102,
1.40197840067584));
#413018=CARTESIAN_POINT('Ctrl Pts',(1.15532125302563,-0.975663988445489,
1.3826503089127));
#413019=CARTESIAN_POINT('Ctrl Pts',(1.02144199305684,-1.11504353664287,
1.37233738589762));
#413020=CARTESIAN_POINT('Ctrl Pts',(0.702439219068069,-1.34021405169521,
1.35073462124883));
#413021=CARTESIAN_POINT('Ctrl Pts',(0.518644232623378,-1.4214824349833,
1.3396343257492));
#413022=CARTESIAN_POINT('Ctrl Pts',(0.136178992505056,-1.50618660754137,
1.31888006462221));
#413023=CARTESIAN_POINT('Ctrl Pts',(-0.058222912169048,-1.51120841051425,
1.31001009356864));
#413024=CARTESIAN_POINT('Ctrl Pts',(-0.439350732684371,-1.44724076227978,
1.28989619363684));
#413025=CARTESIAN_POINT('Ctrl Pts',(-0.622388972984679,-1.37846051901595,
1.27917919988151));
#413026=CARTESIAN_POINT('Ctrl Pts',(-0.956530543513232,-1.17242945138438,
1.25737972086184));
#413027=CARTESIAN_POINT('Ctrl Pts',(-1.10338207804408,-1.0354270734641,
1.24650870150359));
#413028=CARTESIAN_POINT('Ctrl Pts',(-1.32992195461779,-0.719312385456412,
1.22682833305432));
#413029=CARTESIAN_POINT('Ctrl Pts',(-1.41025282826834,-0.54525377106231,
1.21779187617008));
#413030=CARTESIAN_POINT('Ctrl Pts',(-1.50309527717499,-0.170593837017244,
1.1969774353898));
#413031=CARTESIAN_POINT('Ctrl Pts',(-1.51250263433437,0.027006577808505,
1.18599963456615));
#413032=CARTESIAN_POINT('Ctrl Pts',(-1.45438152330554,0.417523507132094,
1.16430424960373));
#413033=CARTESIAN_POINT('Ctrl Pts',(-1.38628623378875,0.60639427834552,
1.15402010867801));
#413034=CARTESIAN_POINT('Ctrl Pts',(-1.18455223017824,0.939843159453667,
1.13505170798423));
#413035=CARTESIAN_POINT('Ctrl Pts',(-1.05541834887102,1.08283785496255,
1.1248666763478));
#413036=CARTESIAN_POINT('Ctrl Pts',(-0.744595072247187,1.31716361140241,
1.10340313568871));
#413037=CARTESIAN_POINT('Ctrl Pts',(-0.564084622698752,1.40397900186252,
1.09230678401163));
#413038=CARTESIAN_POINT('Ctrl Pts',(-0.250118003558327,1.48433383807843,
1.07496897922141));
#413039=CARTESIAN_POINT('Ctrl Pts',(-0.125181652506405,1.50000000000006,
1.06852280506435));
#413040=CARTESIAN_POINT('Ctrl Pts',(1.04569131131882E-13,1.50000000000006,
1.06249999999999));
#413041=CARTESIAN_POINT('Ctrl Pts',(0.,1.50000000000006,1.00000000000002));
#413042=CARTESIAN_POINT('Ctrl Pts',(-0.0139210510018308,1.50000000000006,
1.00066977687863));
#413043=CARTESIAN_POINT('Ctrl Pts',(-0.0278492894904031,1.49980620499738,
1.00134528275986));
#413044=CARTESIAN_POINT('Ctrl Pts',(-0.240537711569285,1.49387972184136,
1.01174288377037));
#413045=CARTESIAN_POINT('Ctrl Pts',(-0.436189653169356,1.44887832885034,
1.02240623089375));
#413046=CARTESIAN_POINT('Ctrl Pts',(-0.795089312113688,1.28680552109984,
1.04417582122323));
#413047=CARTESIAN_POINT('Ctrl Pts',(-0.955494288648501,1.17263556134334,
1.05506469702606));
#413048=CARTESIAN_POINT('Ctrl Pts',(-1.22061058356622,0.892451995158634,
1.07560298755096));
#413049=CARTESIAN_POINT('Ctrl Pts',(-1.32404072569848,0.730255405911734,
1.08443025522714));
#413050=CARTESIAN_POINT('Ctrl Pts',(-1.46823865828982,0.366681879396492,
1.10462878447799));
#413051=CARTESIAN_POINT('Ctrl Pts',(-1.50403786499845,0.167434914266591,
1.11569806031854));
#413052=CARTESIAN_POINT('Ctrl Pts',(-1.49540721658617,-0.225639333643708,
1.13753551853577));
#413053=CARTESIAN_POINT('Ctrl Pts',(-1.45406788653697,-0.415763779928748,
1.14809798777383));
#413054=CARTESIAN_POINT('Ctrl Pts',(-1.30078525664892,-0.772002631184901,
1.16788903506584));
#413055=CARTESIAN_POINT('Ctrl Pts',(-1.18952605275022,-0.934380352713317,
1.17705724423399));
#413056=CARTESIAN_POINT('Ctrl Pts',(-0.90894711489216,-1.20954569071685,
1.19820008628697));
#413057=CARTESIAN_POINT('Ctrl Pts',(-0.741571552574805,-1.31880719574008,
1.20928798858982));
#413058=CARTESIAN_POINT('Ctrl Pts',(-0.380954539113411,-1.46327655339019,
1.23065122045201));
#413059=CARTESIAN_POINT('Ctrl Pts',(-0.192160135790726,-1.49980121533441,
1.24074916935989));
#413060=CARTESIAN_POINT('Ctrl Pts',(0.19713022252603,-1.50020556531808,
1.25949014240114));
#413061=CARTESIAN_POINT('Ctrl Pts',(0.393978862733631,-1.46093121186798,
1.27004056098599));
#413062=CARTESIAN_POINT('Ctrl Pts',(0.757995919010254,-1.30908048418716,
1.29177241554081));
#413063=CARTESIAN_POINT('Ctrl Pts',(0.922046013593202,-1.19920238796898,
1.30271744873588));
#413064=CARTESIAN_POINT('Ctrl Pts',(1.19492942175059,-0.92646074969302,
1.32342271445107));
#413065=CARTESIAN_POINT('Ctrl Pts',(1.30264695433063,-0.767651402828271,
1.3323526998429));
#413066=CARTESIAN_POINT('Ctrl Pts',(1.45646204507119,-0.410225232893653,
1.35220970928371));
#413067=CARTESIAN_POINT('Ctrl Pts',(1.49795778001533,-0.213707117097209,
1.36312738238351));
#413068=CARTESIAN_POINT('Ctrl Pts',(1.50184059064658,0.17849095181665,1.38491616398984));
#413069=CARTESIAN_POINT('Ctrl Pts',(1.46635459727517,0.370409526770628,
1.39557830704284));
#413070=CARTESIAN_POINT('Ctrl Pts',(1.3244162876751,0.730316542399309,1.41557314124443));
#413071=CARTESIAN_POINT('Ctrl Pts',(1.2192857036431,0.894867051655917,1.4245278406668));
#413072=CARTESIAN_POINT('Ctrl Pts',(0.948738703363631,1.17870384636733,
1.44542889469543));
#413073=CARTESIAN_POINT('Ctrl Pts',(0.784510847160999,1.29382486837113,
1.45652811727779));
#413074=CARTESIAN_POINT('Ctrl Pts',(0.427621011032748,1.45040399534779,
1.47804840771823));
#413075=CARTESIAN_POINT('Ctrl Pts',(0.239490962892949,1.49304999447822,
1.48828442996654));
#413076=CARTESIAN_POINT('Ctrl Pts',(0.0322600286735331,1.49973998657262,
1.4984406660516));
#413077=CARTESIAN_POINT('Ctrl Pts',(0.0161249733935312,1.50000000000006,
1.4992241868559));
#413078=CARTESIAN_POINT('Ctrl Pts',(0.,1.50000000000006,1.50000000000002));
#413079=CARTESIAN_POINT('Origin',(0.,2.5406128344257E-15,14.));
#413080=CARTESIAN_POINT('',(-5.10233297646144E-14,1.50000000000006,2.0625));
#413081=CARTESIAN_POINT('',(-1.01921478372424E-13,1.50000000000006,2.00000000000003));
#413082=CARTESIAN_POINT('',(-1.8369701987211E-16,1.50000000000006,14.));
#413083=CARTESIAN_POINT('Ctrl Pts',(-1.04048714089089E-13,1.50000000000006,
2.0625));
#413084=CARTESIAN_POINT('Ctrl Pts',(0.12517267806619,1.50000000000007,2.05647762671861));
#413085=CARTESIAN_POINT('Ctrl Pts',(0.250086085653614,1.4843361608151,2.05003262094985));
#413086=CARTESIAN_POINT('Ctrl Pts',(0.561115034207491,1.40474810468895,
2.03285745434856));
#413087=CARTESIAN_POINT('Ctrl Pts',(0.739100615817919,1.31980715676613,
2.02193464828504));
#413088=CARTESIAN_POINT('Ctrl Pts',(1.05520352380897,1.08445660057722,2.00018862458367));
#413089=CARTESIAN_POINT('Ctrl Pts',(1.18947775543681,0.935237772913789,
1.98958338516728));
#413090=CARTESIAN_POINT('Ctrl Pts',(1.38770404920368,0.600407544068855,
1.97074537847158));
#413091=CARTESIAN_POINT('Ctrl Pts',(1.45264120120664,0.419637605253057,
1.96081320029176));
#413092=CARTESIAN_POINT('Ctrl Pts',(1.51253906744299,0.0361680336928372,
1.93950933520509));
#413093=CARTESIAN_POINT('Ctrl Pts',(1.5041363021745,-0.163279701360834,
1.92842890547989));
#413094=CARTESIAN_POINT('Ctrl Pts',(1.41094126534843,-0.545470493318642,
1.90719608370446));
#413095=CARTESIAN_POINT('Ctrl Pts',(1.32784413751172,-0.724646312094739,
1.8979235332946));
#413096=CARTESIAN_POINT('Ctrl Pts',(1.09934406827611,-1.03852324259145,
1.87821101496277));
#413097=CARTESIAN_POINT('Ctrl Pts',(0.957083938063734,-1.17092285550576,
1.86768875423129));
#413098=CARTESIAN_POINT('Ctrl Pts',(0.623868722042991,-1.37871374742355,
1.84588496045572));
#413099=CARTESIAN_POINT('Ctrl Pts',(0.434516816534613,-1.44957711310134,
1.83480633582993));
#413100=CARTESIAN_POINT('Ctrl Pts',(0.0482837836795281,-1.51133308800197,
1.8145082466253));
#413101=CARTESIAN_POINT('Ctrl Pts',(-0.144260380713892,-1.50520783480527,
1.80570393127465));
#413102=CARTESIAN_POINT('Ctrl Pts',(-0.520543454270307,-1.4202068029843,
1.7852388636844));
#413103=CARTESIAN_POINT('Ctrl Pts',(-0.700388001592572,-1.34067165157295,
1.77437677910558));
#413104=CARTESIAN_POINT('Ctrl Pts',(-1.02285817948285,-1.11502347609753,
1.75259392056372));
#413105=CARTESIAN_POINT('Ctrl Pts',(-1.16148641546404,-0.969788519798059,
1.74188986210865));
#413106=CARTESIAN_POINT('Ctrl Pts',(-1.369305754301,-0.641164531862946,
1.72276270539765));
#413107=CARTESIAN_POINT('Ctrl Pts',(-1.43944299511357,-0.4627385332705,
1.71320769629275));
#413108=CARTESIAN_POINT('Ctrl Pts',(-1.51065911408002,-0.0821899165916949,
1.69206610647726));
#413109=CARTESIAN_POINT('Ctrl Pts',(-1.50837808077227,0.116802018761552,
1.68101099895764));
#413110=CARTESIAN_POINT('Ctrl Pts',(-1.42693643557648,0.502817858674299,
1.65956567451804));
#413111=CARTESIAN_POINT('Ctrl Pts',(-1.34846371621931,0.686002866464551,
1.649989022283));
#413112=CARTESIAN_POINT('Ctrl Pts',(-1.12811871027367,1.00709126310415,
1.63046854611269));
#413113=CARTESIAN_POINT('Ctrl Pts',(-0.990058164560742,1.14308777164135,
1.62004842421734));
#413114=CARTESIAN_POINT('Ctrl Pts',(-0.663925760947525,1.35978943579843,
1.59833788096152));
#413115=CARTESIAN_POINT('Ctrl Pts',(-0.477317675891636,1.43596823386572,
1.58724361755909));
#413116=CARTESIAN_POINT('Ctrl Pts',(-0.188340196669765,1.49113307834988,
1.57180782531633));
#413117=CARTESIAN_POINT('Ctrl Pts',(-0.0941732849861451,1.50000000000006,
1.56703091428643));
#413118=CARTESIAN_POINT('Ctrl Pts',(0.,1.50000000000006,1.5625));
#413119=CARTESIAN_POINT('',(-1.8369701987211E-16,-1.50000000000005,1.75000000000002));
#413120=CARTESIAN_POINT('Ctrl Pts',(-4.1286418728248E-15,1.50000000000006,
1.50000000000002));
#413121=CARTESIAN_POINT('Ctrl Pts',(-0.184262216122471,1.50000000000006,
1.50886532000667));
#413122=CARTESIAN_POINT('Ctrl Pts',(-0.367118755739811,1.46605100166279,
1.51860603710253));
#413123=CARTESIAN_POINT('Ctrl Pts',(-0.722361712575998,1.32915277951315,
1.53950040022534));
#413124=CARTESIAN_POINT('Ctrl Pts',(-0.8897541949698,1.22343551296505,1.55049066552698));
#413125=CARTESIAN_POINT('Ctrl Pts',(-1.16993138802411,0.957787239945069,
1.57134981570788));
#413126=CARTESIAN_POINT('Ctrl Pts',(-1.28168854585672,0.802094977551391,
1.58043916791386));
#413127=CARTESIAN_POINT('Ctrl Pts',(-1.44492382107869,0.449170364453763,
1.60004609086372));
#413128=CARTESIAN_POINT('Ctrl Pts',(-1.49167494434391,0.253858939542195,
1.61089672558103));
#413129=CARTESIAN_POINT('Ctrl Pts',(-1.50611310936441,-0.138569278761815,
1.63269829326459));
#413130=CARTESIAN_POINT('Ctrl Pts',(-1.47562118216477,-0.331863137943603,
1.64343684099692));
#413131=CARTESIAN_POINT('Ctrl Pts',(-1.34324288372284,-0.694785535748963,
1.66359919643055));
#413132=CARTESIAN_POINT('Ctrl Pts',(-1.24315068270372,-0.861165580826581,
1.67244348435894));
#413133=CARTESIAN_POINT('Ctrl Pts',(-0.98100786127297,-1.15208159054694,
1.69313683700554));
#413134=CARTESIAN_POINT('Ctrl Pts',(-0.81954709883969,-1.27200654544351,
1.70423637030721));
#413135=CARTESIAN_POINT('Ctrl Pts',(-0.53802415872237,-1.40466713678027,
1.72146616550488));
#413136=CARTESIAN_POINT('Ctrl Pts',(-0.431603932160252,-1.44093061146929,
1.72759362978394));
#413137=CARTESIAN_POINT('Ctrl Pts',(-0.216284089425334,-1.48827659240416,
1.73926837668476));
#413138=CARTESIAN_POINT('Ctrl Pts',(-0.10828047712643,-1.50000000000005,
1.74479035311528));
#413139=CARTESIAN_POINT('Ctrl Pts',(-6.34908792207511E-15,-1.50000000000005,
1.75000000000002));
#413140=CARTESIAN_POINT('Ctrl Pts',(-4.71844785465692E-15,-1.50000000000005,
1.75000000000002));
#413141=CARTESIAN_POINT('Ctrl Pts',(0.128403685255941,-1.50000000000005,
1.75617782518731));
#413142=CARTESIAN_POINT('Ctrl Pts',(0.256326208420938,-1.48351384584679,
1.76279044917918));
#413143=CARTESIAN_POINT('Ctrl Pts',(0.509319919036628,-1.41714236576765,
1.77680626698088));
#413144=CARTESIAN_POINT('Ctrl Pts',(0.632935497437535,-1.36641436013271,
1.78416283553733));
#413145=CARTESIAN_POINT('Ctrl Pts',(0.922300322214955,-1.19987495267307,
1.80271100181225));
#413146=CARTESIAN_POINT('Ctrl Pts',(1.07451020764395,-1.06573144674092,
1.81376041183752));
#413147=CARTESIAN_POINT('Ctrl Pts',(1.31068226001403,-0.753875344699292,
1.83378591450625));
#413148=CARTESIAN_POINT('Ctrl Pts',(1.39565079861265,-0.581705867170076,
1.84268300737946));
#413149=CARTESIAN_POINT('Ctrl Pts',(1.49806378045915,-0.20977516263816,
1.8633458242979));
#413150=CARTESIAN_POINT('Ctrl Pts',(1.51262195103989,-0.013009410980133,
1.87427725494557));
#413151=CARTESIAN_POINT('Ctrl Pts',(1.46505908465797,0.378285452977615,
1.89601585849878));
#413152=CARTESIAN_POINT('Ctrl Pts',(1.40210202271853,0.568888986002621,
1.90660494366683));
#413153=CARTESIAN_POINT('Ctrl Pts',(1.20967102284127,0.907157376390545,
1.92539763202172));
#413154=CARTESIAN_POINT('Ctrl Pts',(1.08486195850373,1.05326477583204,1.93539524290294));
#413155=CARTESIAN_POINT('Ctrl Pts',(0.781440253264683,1.2955581387605,1.9567239976952));
#413156=CARTESIAN_POINT('Ctrl Pts',(0.603984679494169,1.3872009278219,1.96780746599849));
#413157=CARTESIAN_POINT('Ctrl Pts',(0.279029618057427,1.48048001337916,
1.98603295939133));
#413158=CARTESIAN_POINT('Ctrl Pts',(0.139733470854763,1.50000000000008,
1.99327707024896));
#413159=CARTESIAN_POINT('Ctrl Pts',(-2.07299455379228E-13,1.50000000000006,
2.00000000000003));
#413160=CARTESIAN_POINT('Origin',(0.,2.5406128344257E-15,14.));
#413161=CARTESIAN_POINT('',(-1.02008187126244E-13,1.50000000000006,2.56250000000001));
#413162=CARTESIAN_POINT('',(-5.10753851888394E-14,1.50000000000006,2.50000000000003));
#413163=CARTESIAN_POINT('',(-1.8369701987211E-16,1.50000000000006,14.));
#413164=CARTESIAN_POINT('Ctrl Pts',(-2.03205507975923E-13,1.50000000000006,
2.56250000000001));
#413165=CARTESIAN_POINT('Ctrl Pts',(0.152713236942429,1.50000000000008,
2.55515258096187));
#413166=CARTESIAN_POINT('Ctrl Pts',(0.30473367800193,1.47668454310575,2.54719084250068));
#413167=CARTESIAN_POINT('Ctrl Pts',(0.638172333335415,1.37161328158764,
2.52822962156282));
#413168=CARTESIAN_POINT('Ctrl Pts',(0.812114721878652,1.27634425022348,
2.51721445250974));
#413169=CARTESIAN_POINT('Ctrl Pts',(1.11579326242716,1.02217281916496,2.49554339438594));
#413170=CARTESIAN_POINT('Ctrl Pts',(1.24170636010353,0.864849575481081,
2.48554719863771));
#413171=CARTESIAN_POINT('Ctrl Pts',(1.42091497161675,0.517363128589665,
2.46624239603264));
#413172=CARTESIAN_POINT('Ctrl Pts',(1.47527571320793,0.331969496264806,
2.45594274979237));
#413173=CARTESIAN_POINT('Ctrl Pts',(1.51207157545589,-0.0566290982231031,
2.43435393898749));
#413174=CARTESIAN_POINT('Ctrl Pts',(1.49124677003707,-0.256436455976549,
2.42325353022342));
#413175=CARTESIAN_POINT('Ctrl Pts',(1.37465850715388,-0.630481773494482,
2.40247323480576));
#413176=CARTESIAN_POINT('Ctrl Pts',(1.28231869436786,-0.801779084055222,
2.39359061239114));
#413177=CARTESIAN_POINT('Ctrl Pts',(1.03728034493493,-1.10070901891445,
2.3734975900056));
#413178=CARTESIAN_POINT('Ctrl Pts',(0.886655461639068,-1.22529149545185,
2.36279002258088));
#413179=CARTESIAN_POINT('Ctrl Pts',(0.541837171242186,-1.4127827946624,
2.3409918532043));
#413180=CARTESIAN_POINT('Ctrl Pts',(0.349959198744996,-1.47210419758972,
2.33011230320026));
#413181=CARTESIAN_POINT('Ctrl Pts',(-0.0369745037304581,-1.5115377391189,
2.31040057060645));
#413182=CARTESIAN_POINT('Ctrl Pts',(-0.227963124566986,-1.49470983444342,
2.30138517001216));
#413183=CARTESIAN_POINT('Ctrl Pts',(-0.599163506202012,-1.38901960020766,
2.28058994348392));
#413184=CARTESIAN_POINT('Ctrl Pts',(-0.775238772760863,-1.29898915396473,
2.26961767254284));
#413185=CARTESIAN_POINT('Ctrl Pts',(-1.08516059471296,-1.05450253849513,
2.24791525705771));
#413186=CARTESIAN_POINT('Ctrl Pts',(-1.21520066557894,-0.901546538308134,
2.2375859187948));
#413187=CARTESIAN_POINT('Ctrl Pts',(-1.40424756528659,-0.560832488679741,
2.21865736048212));
#413188=CARTESIAN_POINT('Ctrl Pts',(-1.46414026274044,-0.377775002516861,
2.20848750013974));
#413189=CARTESIAN_POINT('Ctrl Pts',(-1.51302509452222,0.0082595196597254,
2.1870411377966));
#413190=CARTESIAN_POINT('Ctrl Pts',(-1.49868835278631,0.207972947953393,
2.17594594733584));
#413191=CARTESIAN_POINT('Ctrl Pts',(-1.39424969182913,0.586335583316973,
2.15492580092676));
#413192=CARTESIAN_POINT('Ctrl Pts',(-1.30672083828862,0.761706235670994,
2.1458777957653));
#413193=CARTESIAN_POINT('Ctrl Pts',(-1.07032415199273,1.06850094754418,
2.12598207956313));
#413194=CARTESIAN_POINT('Ctrl Pts',(-0.924041350037075,1.19725506618534,
2.11536754167697));
#413195=CARTESIAN_POINT('Ctrl Pts',(-0.584120040911811,1.39610344662897,
2.09348950394298));
#413196=CARTESIAN_POINT('Ctrl Pts',(-0.392221943321926,1.4616704545275,
2.08243549664298));
#413197=CARTESIAN_POINT('Ctrl Pts',(-0.12893753989064,1.49584792717374,
2.0688188456366));
#413198=CARTESIAN_POINT('Ctrl Pts',(-0.064440010018234,1.50000000000005,
2.06560037142755));
#413199=CARTESIAN_POINT('Ctrl Pts',(-1.01862962509357E-13,1.50000000000006,
2.0625));
#413200=CARTESIAN_POINT('Ctrl Pts',(-2.03659259724975E-13,1.50000000000006,
2.00000000000003));
#413201=CARTESIAN_POINT('Ctrl Pts',(-0.0549400060433684,1.50000000000005,
2.00264330227322));
#413202=CARTESIAN_POINT('Ctrl Pts',(-0.10993950796974,1.4969818263819,2.00537330519949));
#413203=CARTESIAN_POINT('Ctrl Pts',(-0.356253708025767,1.46976303075573,
2.0179801803314));
#413204=CARTESIAN_POINT('Ctrl Pts',(-0.5418707719965,1.41190599495831,2.02851782536881));
#413205=CARTESIAN_POINT('Ctrl Pts',(-0.887743372098913,1.2255665984787,
2.05033472294666));
#413206=CARTESIAN_POINT('Ctrl Pts',(-1.04326496929328,1.09622775919434,
2.06141000481609));
#413207=CARTESIAN_POINT('Ctrl Pts',(-1.28841412800607,0.791459185658804,
2.08167054292328));
#413208=CARTESIAN_POINT('Ctrl Pts',(-1.37854213118331,0.621323847434963,
2.09048200847586));
#413209=CARTESIAN_POINT('Ctrl Pts',(-1.49139348533716,0.25245302547749,
2.11097483191794));
#413210=CARTESIAN_POINT('Ctrl Pts',(-1.51154154601725,0.0567500141491085,
2.12184722143618));
#413211=CARTESIAN_POINT('Ctrl Pts',(-1.47550519730677,-0.335258481026087,
2.14362547116814));
#413212=CARTESIAN_POINT('Ctrl Pts',(-1.41813792564057,-0.527658291165775,
2.15431434950923));
#413213=CARTESIAN_POINT('Ctrl Pts',(-1.23582029636045,-0.871121096433655,
2.17339561646856));
#413214=CARTESIAN_POINT('Ctrl Pts',(-1.11563285200374,-1.02054026590828,
2.1830057634346));
#413215=CARTESIAN_POINT('Ctrl Pts',(-0.820371101776589,-1.2711706465811,
2.20417350603454));
#413216=CARTESIAN_POINT('Ctrl Pts',(-0.646339631367295,-1.36789256596225,
2.21523331904138));
#413217=CARTESIAN_POINT('Ctrl Pts',(-0.270899415401483,-1.48844644321116,
2.23664541366655));
#413218=CARTESIAN_POINT('Ctrl Pts',(-0.0732069894380748,-1.51111961532319,
2.24616894887505));
#413219=CARTESIAN_POINT('Ctrl Pts',(0.314698002855619,-1.47914902699323,
2.2657201084165));
#413220=CARTESIAN_POINT('Ctrl Pts',(0.501354739620307,-1.4267237235383,
2.27615689328056));
#413221=CARTESIAN_POINT('Ctrl Pts',(0.851451281918399,-1.25095683228224,
2.29788333467141));
#413222=CARTESIAN_POINT('Ctrl Pts',(1.01022792711823,-1.1266385612444,2.30897576488195));
#413223=CARTESIAN_POINT('Ctrl Pts',(1.26453115601539,-0.82925932324522,
2.32947146907578));
#413224=CARTESIAN_POINT('Ctrl Pts',(1.35999298008976,-0.661157855585676,
2.33826900802304));
#413225=CARTESIAN_POINT('Ctrl Pts',(1.48339858266622,-0.295467457128719,
2.35858514127065));
#413226=CARTESIAN_POINT('Ctrl Pts',(1.50915889939786,-0.100999143947135,
2.3693889364474));
#413227=CARTESIAN_POINT('Ctrl Pts',(1.48479726843207,0.291384690358864,
2.39118803835329));
#413228=CARTESIAN_POINT('Ctrl Pts',(1.43314552716761,0.485431988898048,
2.40196844382769));
#413229=CARTESIAN_POINT('Ctrl Pts',(1.26111558532972,0.834051958767407,
2.42133621993154));
#413230=CARTESIAN_POINT('Ctrl Pts',(1.14551706690535,0.986847410654543,
2.43063204582883));
#413231=CARTESIAN_POINT('Ctrl Pts',(0.858439019841868,1.24568575260506,
2.45163404875111));
#413232=CARTESIAN_POINT('Ctrl Pts',(0.687961617920957,1.3473522652111,2.46266021636987));
#413233=CARTESIAN_POINT('Ctrl Pts',(0.341125347611844,1.47073361724696,
2.48277464398429));
#413234=CARTESIAN_POINT('Ctrl Pts',(0.171090208316003,1.50000000000007,
2.49176841851444));
#413235=CARTESIAN_POINT('Ctrl Pts',(-1.0325074129014E-13,1.50000000000006,
2.50000000000003));
#413236=CARTESIAN_POINT('Origin',(0.,2.5406128344257E-15,14.));
#413237=CARTESIAN_POINT('',(6.67357304637349E-15,1.50000000000006,3.0625));
#413238=CARTESIAN_POINT('',(-9.18485099360549E-17,1.50000000000006,3.00000000000002));
#413239=CARTESIAN_POINT('',(-1.8369701987211E-16,1.50000000000006,14.));
#413240=CARTESIAN_POINT('Ctrl Pts',(3.64291929955129E-15,1.50000000000006,
3.0625));
#413241=CARTESIAN_POINT('Ctrl Pts',(0.182882853306852,1.50000000000006,
3.05370104461776));
#413242=CARTESIAN_POINT('Ctrl Pts',(0.364344307785531,1.46655523112887,
3.04404145496085));
#413243=CARTESIAN_POINT('Ctrl Pts',(0.719999996592976,1.33065906568766,
3.02315506917039));
#413244=CARTESIAN_POINT('Ctrl Pts',(0.888860395184684,1.224330073046,3.01207718632626));
#413245=CARTESIAN_POINT('Ctrl Pts',(1.17437618710092,0.953526175329834,
2.99081797089076));
#413246=CARTESIAN_POINT('Ctrl Pts',(1.28870083644925,0.792218373209365,
2.98151213184482));
#413247=CARTESIAN_POINT('Ctrl Pts',(1.44754363339846,0.437813070668275,
2.96182294837032));
#413248=CARTESIAN_POINT('Ctrl Pts',(1.49171964063901,0.248630694274393,
2.95131281634844));
#413249=CARTESIAN_POINT('Ctrl Pts',(1.50645258404152,-0.143648281191507,
2.92951953993367));
#413250=CARTESIAN_POINT('Ctrl Pts',(1.47388129179558,-0.343107440067577,
2.91843847555167));
#413251=CARTESIAN_POINT('Ctrl Pts',(1.33559504363155,-0.708997785802925,
2.89811123412193));
#413252=CARTESIAN_POINT('Ctrl Pts',(1.23456394643513,-0.873124364491001,
2.88931119766451));
#413253=CARTESIAN_POINT('Ctrl Pts',(0.973799092840822,-1.15742887662232,
2.86886779523715));
#413254=CARTESIAN_POINT('Ctrl Pts',(0.815472175779737,-1.27393959786869,
2.85801387896488));
#413255=CARTESIAN_POINT('Ctrl Pts',(0.459490510962695,-1.44166101725917,
2.83622777481443));
#413256=CARTESIAN_POINT('Ctrl Pts',(0.26456989253311,-1.48981367055675,
2.82551207848497));
#413257=CARTESIAN_POINT('Ctrl Pts',(-0.123856795158379,-1.50689770288092,
2.8063493343066));
#413258=CARTESIAN_POINT('Ctrl Pts',(-0.313522320195767,-1.47912677479024,
2.79683583852498));
#413259=CARTESIAN_POINT('Ctrl Pts',(-0.679073137343345,-1.35191598287377,
2.77571463352598));
#413260=CARTESIAN_POINT('Ctrl Pts',(-0.850581476939661,-1.25113107802357,
2.76466335399951));
#413261=CARTESIAN_POINT('Ctrl Pts',(-1.14528857231865,-0.98862407240659,
2.74319239099495));
#413262=CARTESIAN_POINT('Ctrl Pts',(-1.26541405236657,-0.829319266629043,
2.73357329259036));
#413263=CARTESIAN_POINT('Ctrl Pts',(-1.43457743682025,-0.478379997782074,
2.71407666654331));
#413264=CARTESIAN_POINT('Ctrl Pts',(-1.48395695812464,-0.291052487239219,
2.70366958262427));
#413265=CARTESIAN_POINT('Ctrl Pts',(-1.50993158675046,0.0995103046966565,
2.68197164973895));
#413266=CARTESIAN_POINT('Ctrl Pts',(-1.48333044076327,0.299229642968109,
2.67087613094609));
#413267=CARTESIAN_POINT('Ctrl Pts',(-1.35603134593058,0.669317429512583,
2.65031569836029));
#413268=CARTESIAN_POINT('Ctrl Pts',(-1.25941917298638,0.83706039188798,
2.64150882232628));
#413269=CARTESIAN_POINT('Ctrl Pts',(-1.00666608391223,1.12886512042551,
2.6212425467545));
#413270=CARTESIAN_POINT('Ctrl Pts',(-0.852227140816204,1.24956407323514,
2.61045935095119));
#413271=CARTESIAN_POINT('Ctrl Pts',(-0.501815166956722,1.4274848830235,
2.58865790228193));
#413272=CARTESIAN_POINT('Ctrl Pts',(-0.308367856338849,1.48137183976405,
2.57785380430087));
#413273=CARTESIAN_POINT('Ctrl Pts',(-0.0733611638817185,1.49865591149239,
2.56606692643469));
#413274=CARTESIAN_POINT('Ctrl Pts',(-0.0366624048499707,1.50000000000005,
2.56426392077577));
#413275=CARTESIAN_POINT('Ctrl Pts',(-2.03832677232616E-13,1.50000000000006,
2.56250000000001));
#413276=CARTESIAN_POINT('Ctrl Pts',(-1.01967073357807E-13,1.50000000000006,
2.50000000000003));
#413277=CARTESIAN_POINT('Ctrl Pts',(-0.0274177145351737,1.50000000000006,
2.50131913540564));
#413278=CARTESIAN_POINT('Ctrl Pts',(-0.0548605401926219,1.49924828163703,
2.50266036003634));
#413279=CARTESIAN_POINT('Ctrl Pts',(-0.273628599396303,1.48722738833696,
2.51351975689506));
#413280=CARTESIAN_POINT('Ctrl Pts',(-0.461154186550479,1.4401504841588,
2.5238497776964));
#413281=CARTESIAN_POINT('Ctrl Pts',(-0.815094499336094,1.27485332480795,
2.5454703266948));
#413282=CARTESIAN_POINT('Ctrl Pts',(-0.976917197504026,1.15554005927025,
2.55657028226653));
#413283=CARTESIAN_POINT('Ctrl Pts',(-1.24013964613848,0.865524440878566,
2.57729056763096));
#413284=CARTESIAN_POINT('Ctrl Pts',(-1.34087450658538,0.699380283990824,
2.58614553977831));
#413285=CARTESIAN_POINT('Ctrl Pts',(-1.47448412598132,0.336842361844777,
2.60628653545309));
#413286=CARTESIAN_POINT('Ctrl Pts',(-1.50562215511498,0.143718511421741,
2.61701563825437));
#413287=CARTESIAN_POINT('Ctrl Pts',(-1.49254483650425,-0.248696103796777,
2.63881645021095));
#413288=CARTESIAN_POINT('Ctrl Pts',(-1.44646879082916,-0.444171099187499,
2.6496761721771));
#413289=CARTESIAN_POINT('Ctrl Pts',(-1.28444391432844,-0.797680502985018,
2.66931558349919));
#413290=CARTESIAN_POINT('Ctrl Pts',(-1.17320997448533,-0.953772395014446,
2.67838091975722));
#413291=CARTESIAN_POINT('Ctrl Pts',(-0.893975630318868,-1.2203435216428,
2.6992203419223));
#413292=CARTESIAN_POINT('Ctrl Pts',(-0.727010595442072,-1.32660567225268,
2.71020517731408));
#413293=CARTESIAN_POINT('Ctrl Pts',(-0.359020312185557,-1.46991806658127,
2.73189101791465));
#413294=CARTESIAN_POINT('Ctrl Pts',(-0.161238567423123,-1.50449720087997,
2.74211748356123));
#413295=CARTESIAN_POINT('Ctrl Pts',(0.228464169802661,-1.49475941767255,
2.76113755922599));
#413296=CARTESIAN_POINT('Ctrl Pts',(0.416766918687362,-1.45354179816621,
2.77134221333097));
#413297=CARTESIAN_POINT('Ctrl Pts',(0.774562466398808,-1.29978160830849,
2.79282777603141));
#413298=CARTESIAN_POINT('Ctrl Pts',(0.93954294283116,-1.1860208389091,2.80392542427689));
#413299=CARTESIAN_POINT('Ctrl Pts',(1.21243949942647,-0.904192764779027,
2.82488372359255));
#413300=CARTESIAN_POINT('Ctrl Pts',(1.3189938637598,-0.740151664975824,
2.83388046305692));
#413301=CARTESIAN_POINT('Ctrl Pts',(1.46359518940313,-0.38109696698799,
2.85382794627847));
#413302=CARTESIAN_POINT('Ctrl Pts',(1.50046270778976,-0.189583912945483,
2.86446756039169));
#413303=CARTESIAN_POINT('Ctrl Pts',(1.49952874275399,0.196746644945994,
2.88593036916345));
#413304=CARTESIAN_POINT('Ctrl Pts',(1.46177059901948,0.387992437134483,
2.89655513539638));
#413305=CARTESIAN_POINT('Ctrl Pts',(1.31544793633266,0.746493348129332,
2.91647185267387));
#413306=CARTESIAN_POINT('Ctrl Pts',(1.20796845018551,0.910205053758987,
2.92549839789162));
#413307=CARTESIAN_POINT('Ctrl Pts',(0.933551340114328,1.19072603442544,
2.94649354671873));
#413308=CARTESIAN_POINT('Ctrl Pts',(0.768088770422058,1.30360253054627,
2.95758982654036));
#413309=CARTESIAN_POINT('Ctrl Pts',(0.409717686637218,1.45553271405181,
2.97905224622326));
#413310=CARTESIAN_POINT('Ctrl Pts',(0.221308716892194,1.49582417711568,
2.98923628431392));
#413311=CARTESIAN_POINT('Ctrl Pts',(0.0202523014979187,1.49989750363487,
2.99902276356864));
#413312=CARTESIAN_POINT('Ctrl Pts',(0.010124057874074,1.50000000000006,
2.99951290603844));
#413313=CARTESIAN_POINT('Ctrl Pts',(0.,1.50000000000006,3.00000000000002));
#413314=CARTESIAN_POINT('Origin',(0.,2.5406128344257E-15,14.));
#413315=CARTESIAN_POINT('',(-1.8369701987211E-16,1.50000000000006,10.875));
#413316=CARTESIAN_POINT('Origin',(0.,2.12729453971344E-15,10.875));
#413317=CARTESIAN_POINT('',(-1.8369701987211E-16,1.50000000000006,14.));
#413318=CARTESIAN_POINT('',(1.05094390383309,1.07028823734368,4.));
#413319=CARTESIAN_POINT('Origin',(0.,2.96923921412725E-15,4.));
#413320=CARTESIAN_POINT('',(2.54005801708804E-14,1.50000000000006,3.56249999999999));
#413321=CARTESIAN_POINT('Ctrl Pts',(1.05094390383236,1.0702882373444,4.00000000000005));
#413322=CARTESIAN_POINT('Ctrl Pts',(1.13819986706457,0.98460933381889,3.9934219259693));
#413323=CARTESIAN_POINT('Ctrl Pts',(1.21465675291404,0.888578028464408,
3.98707585607391));
#413324=CARTESIAN_POINT('Ctrl Pts',(1.34189007761835,0.681157619080558,
3.97519266184647));
#413325=CARTESIAN_POINT('Ctrl Pts',(1.3924635746937,0.570707296225168,3.96920596090126));
#413326=CARTESIAN_POINT('Ctrl Pts',(1.48831628150228,0.269842273341566,
3.95249123740774));
#413327=CARTESIAN_POINT('Ctrl Pts',(1.5107358108084,0.0746185298859356,
3.94164547388242));
#413328=CARTESIAN_POINT('Ctrl Pts',(1.47941220484531,-0.317583526733779,
3.91985647073689));
#413329=CARTESIAN_POINT('Ctrl Pts',(1.42434561767773,-0.510669207825729,
3.90912948845401));
#413330=CARTESIAN_POINT('Ctrl Pts',(1.24617432945898,-0.856226129726136,
3.88993188168177));
#413331=CARTESIAN_POINT('Ctrl Pts',(1.12784943062945,-1.00700480087526,
3.88045799211828));
#413332=CARTESIAN_POINT('Ctrl Pts',(0.835900384523997,-1.26097554236673,
3.85935684426919));
#413333=CARTESIAN_POINT('Ctrl Pts',(0.663293475671837,-1.3597172074586,
3.84830946646471));
#413334=CARTESIAN_POINT('Ctrl Pts',(0.288927509018431,-1.48515116315491,
3.82681349894903));
#413335=CARTESIAN_POINT('Ctrl Pts',(0.0907596703675172,-1.51026295578127,
3.81715175878143));
#413336=CARTESIAN_POINT('Ctrl Pts',(-0.297998583554222,-1.4825762872731,
3.79767854444359));
#413337=CARTESIAN_POINT('Ctrl Pts',(-0.485027444519739,-1.43232807704285,
3.78728433055736));
#413338=CARTESIAN_POINT('Ctrl Pts',(-0.836726191001619,-1.26081585576662,
3.765598988359));
#413339=CARTESIAN_POINT('Ctrl Pts',(-0.996761692002802,-1.13852756988451,
3.75450237989703));
#413340=CARTESIAN_POINT('Ctrl Pts',(-1.25470601413975,-0.844134566990372,
3.73391444449817));
#413341=CARTESIAN_POINT('Ctrl Pts',(-1.35231124109025,-0.676834035612717,
3.72510189086725));
#413342=CARTESIAN_POINT('Ctrl Pts',(-1.47989147440158,-0.312424518808318,
3.70485691771146));
#413343=CARTESIAN_POINT('Ctrl Pts',(-1.5078582402593,-0.118488502263773,
3.6940826945701));
#413344=CARTESIAN_POINT('Ctrl Pts',(-1.4881148687202,0.273947391756074,
3.67228070045789));
#413345=CARTESIAN_POINT('Ctrl Pts',(-1.43873897053923,0.46859859659788,
3.66146674463334));
#413346=CARTESIAN_POINT('Ctrl Pts',(-1.27079537012017,0.819230759889241,
3.64198718000605));
#413347=CARTESIAN_POINT('Ctrl Pts',(-1.15699057424196,0.973370756955023,
3.63279432504184));
#413348=CARTESIAN_POINT('Ctrl Pts',(-0.873129892992125,1.23539635915665,
3.61185858269747));
#413349=CARTESIAN_POINT('Ctrl Pts',(-0.704081077148935,1.33896510422339,
3.60084830816784));
#413350=CARTESIAN_POINT('Ctrl Pts',(-0.353261863578898,1.46859190696227,
3.58036876636469));
#413351=CARTESIAN_POINT('Ctrl Pts',(-0.177236729236581,1.50000000000006,
3.57102730611125));
#413352=CARTESIAN_POINT('Ctrl Pts',(4.85722573273506E-14,1.50000000000006,
3.5625));
#413353=CARTESIAN_POINT('',(1.27227548117872E-13,1.50000000000006,3.50000000000001));
#413354=CARTESIAN_POINT('',(-1.8369701987211E-16,1.50000000000006,14.));
#413355=CARTESIAN_POINT('Ctrl Pts',(2.56704379975048E-13,1.50000000000006,
3.50000000000001));
#413356=CARTESIAN_POINT('Ctrl Pts',(-0.158046323335796,1.50000000000006,
3.50760400727687));
#413357=CARTESIAN_POINT('Ctrl Pts',(-0.315330238810465,1.4750274495662,
3.51586501514492));
#413358=CARTESIAN_POINT('Ctrl Pts',(-0.653374864141001,1.36453160991631,
3.53519852364348));
#413359=CARTESIAN_POINT('Ctrl Pts',(-0.826818998759573,1.26697063414261,
3.54625338556592));
#413360=CARTESIAN_POINT('Ctrl Pts',(-1.12070945700276,1.01495450578277,
3.56739364484083));
#413361=CARTESIAN_POINT('Ctrl Pts',(-1.24012502110656,0.864973703597631,
3.57694590535571));
#413362=CARTESIAN_POINT('Ctrl Pts',(-1.42072919648182,0.52064298505673,
3.59607538971909));
#413363=CARTESIAN_POINT('Ctrl Pts',(-1.4771462620762,0.327956166591618,
3.60678021296716));
#413364=CARTESIAN_POINT('Ctrl Pts',(-1.51123400863953,-0.0641392666801464,
3.62856329259336));
#413365=CARTESIAN_POINT('Ctrl Pts',(-1.49014576997854,-0.259647257636294,
3.63942484764648));
#413366=CARTESIAN_POINT('Ctrl Pts',(-1.37553208625951,-0.627993035281357,
3.6598885019601));
#413367=CARTESIAN_POINT('Ctrl Pts',(-1.28452190376951,-0.797787326061387,
3.66869250348051));
#413368=CARTESIAN_POINT('Ctrl Pts',(-1.03784945108146,-1.10133792947263,
3.6889924985998));
#413369=CARTESIAN_POINT('Ctrl Pts',(-0.881777476509032,-1.22984971864792,
3.70007128689903));
#413370=CARTESIAN_POINT('Ctrl Pts',(-0.535182924356041,-1.41444249945224,
3.72187440230903));
#413371=CARTESIAN_POINT('Ctrl Pts',(-0.349382661133372,-1.47140002254497,
3.73239587506053));
#413372=CARTESIAN_POINT('Ctrl Pts',(0.0367104195384525,-1.51226310178053,
3.75210687259969));
#413373=CARTESIAN_POINT('Ctrl Pts',(0.233438879771808,-1.49459180630664,
3.76138156094225));
#413374=CARTESIAN_POINT('Ctrl Pts',(0.611003620457198,-1.3841094382759,
3.7826161076657));
#413375=CARTESIAN_POINT('Ctrl Pts',(0.787904850030921,-1.29162169817824,
3.7936963759335));
#413376=CARTESIAN_POINT('Ctrl Pts',(1.08998526853455,-1.0479469575977,3.81499896963907));
#413377=CARTESIAN_POINT('Ctrl Pts',(1.21403107573361,-0.901298500932676,
3.82492786105932));
#413378=CARTESIAN_POINT('Ctrl Pts',(1.40480917993946,-0.562172842280676,
3.84376817542888));
#413379=CARTESIAN_POINT('Ctrl Pts',(1.46685510831189,-0.371263810872641,
3.85437423272932));
#413380=CARTESIAN_POINT('Ctrl Pts',(1.51253167011941,0.0201712061737881,
3.87612062256523));
#413381=CARTESIAN_POINT('Ctrl Pts',(1.49705537048712,0.216773695591539,
3.88704298308844));
#413382=CARTESIAN_POINT('Ctrl Pts',(1.39293210601042,0.58820894756761,3.90767827486489));
#413383=CARTESIAN_POINT('Ctrl Pts',(1.307125692317,0.760043369025171,3.91655653494596));
#413384=CARTESIAN_POINT('Ctrl Pts',(1.06948823490166,1.07075281541671,3.93662069040197));
#413385=CARTESIAN_POINT('Ctrl Pts',(0.916729933887096,1.2041201811228,3.94767492663366));
#413386=CARTESIAN_POINT('Ctrl Pts',(0.627705282594136,1.36871201538997,
3.96615262704884));
#413387=CARTESIAN_POINT('Ctrl Pts',(0.505012804915808,1.4185740311113,3.9734407276257));
#413388=CARTESIAN_POINT('Ctrl Pts',(0.25408959443158,1.4838014838608,3.98732514990643));
#413389=CARTESIAN_POINT('Ctrl Pts',(0.127278690505086,1.50000000000006,
3.99387630114792));
#413390=CARTESIAN_POINT('Ctrl Pts',(2.56739074444567E-14,1.50000000000006,
4.00000000000002));
#413391=CARTESIAN_POINT('Origin',(1.05441810806075E-15,7.08435492480263E-16,
12.4908873016278));
#413392=CARTESIAN_POINT('',(2.29888601477292,1.49740593435477,12.5064436508139));
#413393=CARTESIAN_POINT('',(2.25522951324155,1.56238320643934,12.5064436508139));
#413394=CARTESIAN_POINT('Origin',(4.27850903389135E-31,-2.27990188045099E-31,
12.5064436508139));
#413395=CARTESIAN_POINT('',(2.30428529106063,1.50092281527121,12.4908873016278));
#413396=CARTESIAN_POINT('Origin',(2.28585100873214,1.48891543274904,12.4908873016278));
#413397=CARTESIAN_POINT('',(2.26052625573157,1.56605269615942,12.4908873016278));
#413398=CARTESIAN_POINT('Origin',(2.10883621612149E-15,1.41687098496053E-15,
12.4908873016278));
#413399=CARTESIAN_POINT('Origin',(2.24244204568572,1.55352427459015,12.4908873016278));
#413400=CARTESIAN_POINT('Origin',(1.10865368822092E-15,6.20133367273767E-16,
12.4908873016278));
#413401=CARTESIAN_POINT('',(2.41328914609189,1.30504288761499,12.5064436508139));
#413402=CARTESIAN_POINT('',(2.37507415886241,1.37336236334895,12.5064436508139));
#413403=CARTESIAN_POINT('Origin',(4.49858057657419E-31,-2.63820513560149E-31,
12.5064436508139));
#413404=CARTESIAN_POINT('',(2.41895711517698,1.30810797525842,12.4908873016278));
#413405=CARTESIAN_POINT('Origin',(2.39960545825556,1.29764311145636,12.4908873016278));
#413406=CARTESIAN_POINT('',(2.38065237435682,1.3765879094592,12.4908873016278));
#413407=CARTESIAN_POINT('Origin',(2.21730737644184E-15,1.24026673454754E-15,
12.4908873016278));
#413408=CARTESIAN_POINT('Origin',(2.36160715536196,1.36557520618352,12.4908873016278));
#413409=CARTESIAN_POINT('Origin',(1.15551136100097E-15,5.27704356822869E-16,
12.4908873016278));
#413410=CARTESIAN_POINT('',(2.5116322363083,1.10399499577506,12.5064436508139));
#413411=CARTESIAN_POINT('',(2.47911307781569,1.17520202031931,12.5064436508139));
#413412=CARTESIAN_POINT('Origin',(4.68871480773348E-31,-3.01325404000159E-31,
12.5064436508139));
#413413=CARTESIAN_POINT('',(2.51753117879165,1.10658789249292,12.4908873016278));
#413414=CARTESIAN_POINT('Origin',(2.49739092936132,1.09773518935297,12.4908873016278));
#413415=CARTESIAN_POINT('',(2.48493564421071,1.17796215734254,12.4908873016278));
#413416=CARTESIAN_POINT('Origin',(2.31102272200194E-15,1.05540871364574E-15,
12.4908873016278));
#413417=CARTESIAN_POINT('Origin',(2.46505615905703,1.1685384600838,12.4908873016278));
#413418=CARTESIAN_POINT('Origin',(1.19467929631951E-15,4.31763560942405E-16,
12.4908873016278));
#413419=CARTESIAN_POINT('',(2.59326082838222,0.895600199384597,12.5064436508139));
#413420=CARTESIAN_POINT('',(2.56665390826098,0.969220901739124,12.5064436508139));
#413421=CARTESIAN_POINT('Origin',(4.8476464154308E-31,-3.40255270507121E-31,
12.5064436508139));
#413422=CARTESIAN_POINT('',(2.59935148777488,0.897703649877022,12.4908873016278));
#413423=CARTESIAN_POINT('Origin',(2.57855667587268,0.890522020678006,12.4908873016278));
#413424=CARTESIAN_POINT('',(2.57268207733791,0.971497261418848,12.4908873016278));
#413425=CARTESIAN_POINT('Origin',(2.38935859263903E-15,8.63527121884811E-16,
12.4908873016278));
#413426=CARTESIAN_POINT('Origin',(2.5521006207192,0.963725283327497,12.4908873016278));
#413427=CARTESIAN_POINT('Origin',(1.22589683802926E-15,3.32949449799843E-16,
12.4908873016278));
#413428=CARTESIAN_POINT('',(2.65763169750119,0.681245331430862,12.5064436508139));
#413429=CARTESIAN_POINT('',(2.63711408041488,0.756789777968061,12.5064436508139));
#413430=CARTESIAN_POINT('Origin',(4.97431773603878E-31,-3.80351041242409E-31,
12.5064436508139));
#413431=CARTESIAN_POINT('',(2.66387354146977,0.682845337581871,12.4908873016278));
#413432=CARTESIAN_POINT('Origin',(2.64256255313801,0.677382574881216,12.4908873016278));
#413433=CARTESIAN_POINT('',(2.64330773570308,0.758567211506177,12.4908873016278));
#413434=CARTESIAN_POINT('Origin',(2.45179367605852E-15,6.65898899599686E-16,
12.4908873016278));
#413435=CARTESIAN_POINT('Origin',(2.62216127381746,0.752498673814127,12.4908873016278));
#413436=CARTESIAN_POINT('Origin',(1.24895623854066E-15,2.31919615001655E-16,
12.4908873016278));
#413437=CARTESIAN_POINT('',(2.70431646615165,0.462356888194023,12.5064436508139));
#413438=CARTESIAN_POINT('',(2.69002469345682,0.539322343086144,12.5064436508139));
#413439=CARTESIAN_POINT('Origin',(5.06788579281809E-31,-4.21345885467116E-31,
12.5064436508139));
#413440=CARTESIAN_POINT('',(2.71066795625438,0.463442802226664,12.4908873016278));
#413441=CARTESIAN_POINT('Origin',(2.68898261260435,0.45973525980885,12.4908873016278));
#413442=CARTESIAN_POINT('',(2.69634261720223,0.540589021955712,12.4908873016278));
#413443=CARTESIAN_POINT('Origin',(2.49791247708132E-15,4.63839230003311E-16,
12.4908873016278));
#413444=CARTESIAN_POINT('Origin',(2.67477187626461,0.536264309780066,12.4908873016278));
#413445=CARTESIAN_POINT('Origin',(1.26370404134785E-15,1.29346393429673E-16,
12.4908873016278));
#413446=CARTESIAN_POINT('',(2.73300445490068,0.240391536149767,12.5064436508139));
#413447=CARTESIAN_POINT('',(2.72503363598663,0.318265806992911,12.5064436508139));
#413448=CARTESIAN_POINT('Origin',(5.12772790578849E-31,-4.62966989256598E-31,
12.5064436508139));
#413449=CARTESIAN_POINT('',(2.73942332301885,0.240956131485315,12.4908873016278));
#413450=CARTESIAN_POINT('Origin',(2.7175079364347,0.239028482433433,12.4908873016278));
#413451=CARTESIAN_POINT('',(2.73143378344912,0.31901330165504,12.4908873016278));
#413452=CARTESIAN_POINT('Origin',(2.5274080826957E-15,2.58692786859347E-16,
12.4908873016278));
#413453=CARTESIAN_POINT('Origin',(2.70958231318152,0.316461195241799,12.4908873016278));
#413454=CARTESIAN_POINT('Origin',(1.27004210225636E-15,2.59123929500705E-17,
12.4908873016278));
#413455=CARTESIAN_POINT('',(2.74350474991634,0.0168264180942478,12.5064436508139));
#413456=CARTESIAN_POINT('',(2.74190792926786,0.0950912644643034,12.5064436508139));
#413457=CARTESIAN_POINT('Origin',(5.15344583556142E-31,-5.04937371032137E-31,
12.5064436508139));
#413458=CARTESIAN_POINT('',(2.74994827954166,0.0168659374438978,12.4908873016278));
#413459=CARTESIAN_POINT('Origin',(2.72794869330533,0.0167310099443466,12.4908873016278));
#413460=CARTESIAN_POINT('',(2.748347708522,0.0953146004653459,12.4908873016278));
#413461=CARTESIAN_POINT('Origin',(2.54008420451272E-15,5.18247859001415E-17,
12.4908873016278));
#413462=CARTESIAN_POINT('Origin',(2.72636092685383,0.0945520836616232,12.4908873016278));
#413463=CARTESIAN_POINT('Origin',(1.26792824251655E-15,-7.76940502293709E-17,
12.4908873016278));
#413464=CARTESIAN_POINT('',(2.73574747346773,-0.206850676997525,12.5064436508139));
#413465=CARTESIAN_POINT('',(2.74053527766277,-0.128716094740359,12.5064436508139));
#413466=CARTESIAN_POINT('Origin',(5.1448684335574E-31,-5.4697772482764E-31,
12.5064436508139));
#413467=CARTESIAN_POINT('',(2.74217278397365,-0.207336496628525,12.4908873016278));
#413468=CARTESIAN_POINT('Origin',(2.72023540170186,-0.205677804655497,12.4908873016278));
#413469=CARTESIAN_POINT('',(2.74697183304013,-0.129018403664643,12.4908873016278));
#413470=CARTESIAN_POINT('Origin',(2.5358564850331E-15,-1.55388100458741E-16,
12.4908873016278));
#413471=CARTESIAN_POINT('Origin',(2.72499605837581,-0.127986256435326,12.4908873016278));
#413472=CARTESIAN_POINT('Origin',(1.25737652951623E-15,-1.80783452323152E-16,
12.4908873016278));
#413473=CARTESIAN_POINT('',(2.70978424894975,-0.429151214961838,12.5064436508139));
#413474=CARTESIAN_POINT('',(2.72092481594134,-0.351666869571186,12.5064436508139));
#413475=CARTESIAN_POINT('Origin',(5.1020527809716E-31,-5.8880827902477E-31,
12.5064436508139));
#413476=CARTESIAN_POINT('',(2.71614858095496,-0.430159140523999,12.4908873016278));
#413477=CARTESIAN_POINT('Origin',(2.69441939230732,-0.426717867399807,12.4908873016278));
#413478=CARTESIAN_POINT('',(2.72731531322782,-0.352492811604782,12.4908873016278));
#413479=CARTESIAN_POINT('Origin',(2.51475305903246E-15,-3.61566904646303E-16,
12.4908873016278));
#413480=CARTESIAN_POINT('Origin',(2.705496790722,-0.349672869111943,12.4908873016278));
#413481=CARTESIAN_POINT('Origin',(1.2384571831645E-15,-2.82669770368892E-16,
12.4908873016278));
#413482=CARTESIAN_POINT('',(2.66578785733794,-0.648595822395547,12.5064436508139));
#413483=CARTESIAN_POINT('',(2.6832070484908,-0.572277359405966,12.5064436508139));
#413484=CARTESIAN_POINT('Origin',(5.02528380890789E-31,-6.30150658186899E-31,
12.5064436508139));
#413485=CARTESIAN_POINT('',(2.67204885726299,-0.650119146310548,12.4908873016278));
#413486=CARTESIAN_POINT('Origin',(2.65067246640489,-0.644918193140064,12.4908873016278));
#413487=CARTESIAN_POINT('',(2.68950895998134,-0.573621438040911,12.4908873016278));
#413488=CARTESIAN_POINT('Origin',(2.476914366329E-15,-5.65339540737784E-16,
12.4908873016278));
#413489=CARTESIAN_POINT('Origin',(2.66799288830148,-0.569032466536583,12.4908873016278));
#413490=CARTESIAN_POINT('Origin',(1.21129610858987E-15,-3.82674967730057E-16,
12.4908873016278));
#413491=CARTESIAN_POINT('',(2.60405108735959,-0.863724131641991,12.5064436508139));
#413492=CARTESIAN_POINT('',(2.62763298083056,-0.789079437833017,12.5064436508139));
#413493=CARTESIAN_POINT('Origin',(4.91507240220936E-31,-6.70729735601718E-31,
12.5064436508139));
#413494=CARTESIAN_POINT('',(2.61016708928296,-0.86575271644051,12.4908873016278));
#413495=CARTESIAN_POINT('Origin',(2.5892857525687,-0.858826694708985,12.4908873016278));
#413496=CARTESIAN_POINT('',(2.63380436834392,-0.790932708447753,12.4908873016278));
#413497=CARTESIAN_POINT('Origin',(2.42259221717973E-15,-7.65349935460113E-16,
12.4908873016278));
#413498=CARTESIAN_POINT('Origin',(2.61273393339717,-0.784605246780171,12.4908873016278));
#413499=CARTESIAN_POINT('Origin',(1.17607405826236E-15,-4.80133526317904E-16,
12.4908873016278));
#413500=CARTESIAN_POINT('',(2.52498478703305,-1.07310449929681,12.5064436508139));
#413501=CARTESIAN_POINT('',(2.55457244921182,-1.00063032279023,12.5064436508139));
#413502=CARTESIAN_POINT('Origin',(4.772151999604E-31,-7.10275464204105E-31,
12.5064436508139));
#413503=CARTESIAN_POINT('',(2.53091508997101,-1.0756248450817,12.4908873016278));
#413504=CARTESIAN_POINT('Origin',(2.51066776925124,-1.06701984632105,12.4908873016278));
#413505=CARTESIAN_POINT('',(2.56057224318231,-1.00298045217459,12.4908873016278));
#413506=CARTESIAN_POINT('Origin',(2.35214811652471E-15,-9.60267052635807E-16,
12.4908873016278));
#413507=CARTESIAN_POINT('Origin',(2.54008766523685,-0.99495660855719,12.4908873016278));
#413508=CARTESIAN_POINT('Origin',(1.13302542911567E-15,-5.74396875504561E-16,
12.4908873016278));
#413509=CARTESIAN_POINT('',(2.42911512954197,-1.27534353355859,12.5064436508139));
#413510=CARTESIAN_POINT('',(2.46451165941837,-1.20552217804166,12.5064436508139));
#413511=CARTESIAN_POINT('Origin',(4.59747371279093E-31,-7.48524673694799E-31,
12.5064436508139));
#413512=CARTESIAN_POINT('',(2.4348202683069,-1.27833886784449,12.4908873016278));
#413513=CARTESIAN_POINT('Origin',(2.41534170616044,-1.26811215690173,12.4908873016278));
#413514=CARTESIAN_POINT('',(2.470299932207,-1.20835352647233,12.4908873016278));
#413515=CARTESIAN_POINT('Origin',(2.26605085823134E-15,-1.14879375100912E-15,
12.4908873016278));
#413516=CARTESIAN_POINT('Origin',(2.45053753274934,-1.19868669826055,12.4908873016278));
#413517=CARTESIAN_POINT('Origin',(1.08243670267426E-15,-6.64837708253549E-16,
12.4908873016278));
#413518=CARTESIAN_POINT('',(2.31708011163957,-1.4690953670214,12.5064436508139));
#413519=CARTESIAN_POINT('',(2.35804995114728,-1.40239148209538,12.5064436508139));
#413520=CARTESIAN_POINT('Origin',(4.39219999694901E-31,-7.85222821895314E-31,
12.5064436508139));
#413521=CARTESIAN_POINT('',(2.32252211947427,-1.47254575635283,12.4908873016278));
#413522=CARTESIAN_POINT('Origin',(2.30394194251848,-1.46076539030201,12.4908873016278));
#413523=CARTESIAN_POINT('',(2.36358818275365,-1.40568520741569,12.4908873016278));
#413524=CARTESIAN_POINT('Origin',(2.16487340534852E-15,-1.3296754165071E-15,
12.4908873016278));
#413525=CARTESIAN_POINT('Origin',(2.34467947729162,-1.39443972575636,12.4908873016278));
#413526=CARTESIAN_POINT('Origin',(1.02464453856604E-15,-7.50854155744611E-16,
12.4908873016278));
#413527=CARTESIAN_POINT('',(2.18962530788552,-1.65307061320037,12.5064436508139));
#413528=CARTESIAN_POINT('',(2.23589580950217,-1.58992810221407,12.5064436508139));
#413529=CARTESIAN_POINT('Origin',(4.15769691478938E-31,-8.20125688684145E-31,
12.5064436508139));
#413530=CARTESIAN_POINT('',(2.19476796912572,-1.6569530958056,12.4908873016278));
#413531=CARTESIAN_POINT('Origin',(2.17720982537272,-1.64369747103915,12.4908873016278));
#413532=CARTESIAN_POINT('',(2.24114714390868,-1.59366228522544,12.4908873016278));
#413533=CARTESIAN_POINT('Origin',(2.04928907713207E-15,-1.50170831148922E-15,
12.4908873016278));
#413534=CARTESIAN_POINT('Origin',(2.22321796675741,-1.58091298694363,12.4908873016278));
#413535=CARTESIAN_POINT('Origin',(9.60033534108104E-16,-8.31873792711407E-16,
12.4908873016278));
#413536=CARTESIAN_POINT('',(2.04759890897023,-1.82604494718594,12.5064436508139));
#413537=CARTESIAN_POINT('',(2.09886215014166,-1.76688401313219,12.5064436508139));
#413538=CARTESIAN_POINT('Origin',(3.89552504563353E-31,-8.53001001241378E-31,
12.5064436508139));
#413539=CARTESIAN_POINT('',(2.05240800005387,-1.83033368578379,12.4908873016278));
#413540=CARTESIAN_POINT('Origin',(2.03598873605344,-1.81569101629752,12.4908873016278));
#413541=CARTESIAN_POINT('',(2.10379164058425,-1.77103380346278,12.4908873016278));
#413542=CARTESIAN_POINT('Origin',(1.92006706821621E-15,-1.66374758542281E-15,
12.4908873016278));
#413543=CARTESIAN_POINT('Origin',(2.08696130745958,-1.75686553303508,12.4908873016278));
#413544=CARTESIAN_POINT('Origin',(8.89033664875066E-16,-9.07357446837224E-16,
12.4908873016278));
#413545=CARTESIAN_POINT('',(1.89194607714579,-1.98686725332419,12.5064436508139));
#413546=CARTESIAN_POINT('',(1.94786090945984,-1.93208160245826,12.5064436508139));
#413547=CARTESIAN_POINT('Origin',(3.60742910001539E-31,-8.83629979785991E-31,
12.5064436508139));
#413548=CARTESIAN_POINT('',(1.89638959436514,-1.9915337070669,12.4908873016278));
#413549=CARTESIAN_POINT('Origin',(1.88121847761022,-1.97560143741037,12.4908873016278));
#413550=CARTESIAN_POINT('',(1.95243575099292,-1.93661938393808,12.4908873016278));
#413551=CARTESIAN_POINT('Origin',(1.77806732975013E-15,-1.81471489367445E-15,
12.4908873016278));
#413552=CARTESIAN_POINT('Origin',(1.93681626498497,-1.92112642886658,12.4908873016278));
#413553=CARTESIAN_POINT('Origin',(8.12117423282514E-16,-9.7680278685778E-16,
12.4908873016278));
#413554=CARTESIAN_POINT('',(1.72370265632708,-2.1344672857016,12.5064436508139));
#413555=CARTESIAN_POINT('',(1.78389697579999,-2.084421507491,12.5064436508139));
#413556=CARTESIAN_POINT('Origin',(3.29532630892054E-31,-9.11808793519194E-31,
12.5064436508139));
#413557=CARTESIAN_POINT('',(1.72775102880817,-2.13948040010941,12.4908873016278));
#413558=CARTESIAN_POINT('Origin',(1.7139290205777,-2.12236455690854,12.4908873016278));
#413559=CARTESIAN_POINT('',(1.78808672360795,-2.08931708193299,12.4908873016278));
#413560=CARTESIAN_POINT('Origin',(1.62423484656503E-15,-1.95360557371556E-15,
12.4908873016278));
#413561=CARTESIAN_POINT('Origin',(1.77378202981909,-2.07260254527753,12.4908873016278));
#413562=CARTESIAN_POINT('Origin',(7.29796674227961E-16,-1.03974766549291E-15,
12.4908873016278));
#413563=CARTESIAN_POINT('',(1.54398827872143,-2.26786279045497,12.5064436508139));
#413564=CARTESIAN_POINT('',(1.60806150208848,-2.22288993129672,12.5064436508139));
#413565=CARTESIAN_POINT('Origin',(2.96129366493041E-31,-9.37349917084771E-31,
12.5064436508139));
#413566=CARTESIAN_POINT('',(1.54761456521333,-2.27318920407861,12.4908873016278));
#413567=CARTESIAN_POINT('Origin',(1.53523364869163,-2.25500369044598,12.4908873016278));
#413568=CARTESIAN_POINT('',(1.61183827409092,-2.22811071946068,12.4908873016278));
#413569=CARTESIAN_POINT('Origin',(1.45959334845592E-15,-2.07949533098583E-15,
12.4908873016278));
#413570=CARTESIAN_POINT('Origin',(1.59894356789819,-2.210285833705,12.4908873016278));
#413571=CARTESIAN_POINT('Origin',(6.42619248714396E-16,-1.09577319496048E-15,
12.4908873016278));
#413572=CARTESIAN_POINT('',(1.35399891386102,-2.38616604250889,12.5064436508139));
#413573=CARTESIAN_POINT('',(1.42152464439204,-2.34656538936069,12.5064436508139));
#413574=CARTESIAN_POINT('Origin',(2.60755410017922E-31,-9.60083378519382E-31,
12.5064436508139));
#413575=CARTESIAN_POINT('',(1.35717898202543,-2.39177030894449,12.4908873016278));
#413576=CARTESIAN_POINT('Origin',(1.34632155016923,-2.37263614647293,12.4908873016278));
#413577=CARTESIAN_POINT('',(1.42486330679441,-2.35207664776276,12.4908873016278));
#413578=CARTESIAN_POINT('Origin',(1.28523849742879E-15,-2.19154638992096E-15,
12.4908873016278));
#413579=CARTESIAN_POINT('Origin',(1.41346440034005,-2.33326003458066,12.4908873016278));
#413580=CARTESIAN_POINT('Origin',(5.5116529812535E-16,-1.14450653460544E-15,
12.4908873016278));
#413581=CARTESIAN_POINT('',(1.15499890962297,-2.4885897532396,12.5064436508139));
#413582=CARTESIAN_POINT('',(1.22552777472223,-2.4546248419145,12.5064436508139));
#413583=CARTESIAN_POINT('Origin',(2.23646169310749E-31,-9.79857890387934E-31,
12.5064436508139));
#413584=CARTESIAN_POINT('',(1.15771159663093,-2.49443457701866,12.4908873016278));
#413585=CARTESIAN_POINT('Origin',(1.14844990385788,-2.47447910040251,12.4908873016278));
#413586=CARTESIAN_POINT('',(1.22840610927708,-2.46038989403931,12.4908873016278));
#413587=CARTESIAN_POINT('Origin',(1.1023305962507E-15,-2.28901306921088E-15,
12.4908873016278));
#413588=CARTESIAN_POINT('Origin',(1.21857886040286,-2.44070677488699,12.4908873016278));
#413589=CARTESIAN_POINT('Origin',(4.56043433413153E-16,-1.18562337209288E-15,
12.4908873016278));
#413590=CARTESIAN_POINT('',(0.948312578202777,-2.57445230975091,12.5064436508139));
#413591=CARTESIAN_POINT('',(1.02137521990949,-2.54634917112996,12.5064436508139));
#413592=CARTESIAN_POINT('Origin',(1.85048600245833E-31,-9.9654185657651E-31,
12.5064436508139));
#413593=CARTESIAN_POINT('',(0.950539831569808,-2.58049879453552,12.4908873016278));
#413594=CARTESIAN_POINT('Origin',(0.942935512917249,-2.55985480417923,12.4908873016278));
#413595=CARTESIAN_POINT('',(1.02377407177525,-2.55232965150678,12.4908873016278));
#413596=CARTESIAN_POINT('Origin',(9.12086866826306E-16,-2.37124674418577E-15,
12.4908873016278));
#413597=CARTESIAN_POINT('Origin',(1.01558387920105,-2.53191101429473,12.4908873016278));
#413598=CARTESIAN_POINT('Origin',(3.57886674893462E-16,-1.21885008165314E-15,
12.4908873016278));
#413599=CARTESIAN_POINT('',(0.735315383035209,-2.64318231089556,12.5064436508139));
#413600=CARTESIAN_POINT('',(0.810425581523304,-2.62112796672959,12.5064436508139));
#413601=CARTESIAN_POINT('Origin',(1.45219563277151E-31,-1.01002424804278E-30,
12.5064436508139));
#413602=CARTESIAN_POINT('',(0.737042380757625,-2.64939021832707,12.4908873016278));
#413603=CARTESIAN_POINT('Origin',(0.731146041711564,-2.62819509658045,12.4908873016278));
#413604=CARTESIAN_POINT('',(0.812328986736591,-2.62728407624823,12.4908873016278));
#413605=CARTESIAN_POINT('Origin',(7.15773349786924E-16,-2.43770016330627E-15,
12.4908873016278));
#413606=CARTESIAN_POINT('Origin',(0.805830354842698,-2.60626580363824,12.4908873016278));
#413607=CARTESIAN_POINT('Origin',(2.573482395995E-16,-1.2439655450161E-15,
12.4908873016278));
#413608=CARTESIAN_POINT('',(0.517424785312041,-2.69432236985558,12.5064436508139));
#413609=CARTESIAN_POINT('',(0.59408269460289,-2.67846358816631,12.5064436508139));
#413610=CARTESIAN_POINT('Origin',(1.04424114074401E-31,-1.02021534169599E-30,
12.5064436508139));
#413611=CARTESIAN_POINT('',(0.518640034504934,-2.70065038733427,12.4908873016278));
#413612=CARTESIAN_POINT('Origin',(0.514490914228895,-2.67904518423559,12.4908873016278));
#413613=CARTESIAN_POINT('',(0.595477986316048,-2.6847543589336,12.4908873016278));
#413614=CARTESIAN_POINT('Origin',(5.14696479198999E-16,-2.48793109003219E-15,
12.4908873016278));
#413615=CARTESIAN_POINT('Origin',(0.59071416242552,-2.66327632406214,12.4908873016278));
#413616=CARTESIAN_POINT('Origin',(1.55097194230474E-16,-1.26080262291684E-15,
12.4908873016278));
#413617=CARTESIAN_POINT('',(0.296090811011702,-2.72753215797611,12.5064436508139));
#413618=CARTESIAN_POINT('',(0.373786285366639,-2.71797447633917,12.5064436508139));
#413619=CARTESIAN_POINT('Origin',(6.29337396212522E-32,-1.02704731748927E-30,
12.5064436508139));
#413620=CARTESIAN_POINT('',(0.296786224392195,-2.73393817358971,12.4908873016278));
#413621=CARTESIAN_POINT('Origin',(0.294411934597058,-2.71206666820099,12.4908873016278));
#413622=CARTESIAN_POINT('',(0.374664178143524,-2.72435804431357,12.4908873016278));
#413623=CARTESIAN_POINT('Origin',(3.10194388460947E-16,-2.52160524583369E-15,
12.4908873016278));
#413624=CARTESIAN_POINT('Origin',(0.371666864718376,-2.70256317995906,12.4908873016278));
#413625=CARTESIAN_POINT('Origin',(5.18140026230798E-17,-1.26924926737987E-15,
12.4908873016278));
#413626=CARTESIAN_POINT('',(0.0727864012156247,-2.74259066959644,12.5064436508139));
#413627=CARTESIAN_POINT('',(0.151002390071669,-2.73939769280622,12.5064436508139));
#413628=CARTESIAN_POINT('Origin',(2.102455151426E-32,-1.03047470975092E-30,
12.5064436508139));
#413629=CARTESIAN_POINT('',(0.0729573509224068,-2.74903205236796,12.4908873016278));
#413630=CARTESIAN_POINT('Origin',(0.0723736921150276,-2.72703979594902,
12.4908873016278));
#413631=CARTESIAN_POINT('',(0.151357041680694,-2.74583157639606,12.4908873016278));
#413632=CARTESIAN_POINT('Origin',(1.0362800524616E-16,-2.53849853475974E-15,
12.4908873016278));
#413633=CARTESIAN_POINT('Origin',(0.150146185347248,-2.72386492378489,12.4908873016278));
#413634=CARTESIAN_POINT('Origin',(-5.18140026230626E-17,-1.26924926737987E-15,
12.4908873016278));
#413635=CARTESIAN_POINT('',(-0.151002390071633,-2.73939769280622,12.5064436508139));
#413636=CARTESIAN_POINT('',(-0.0727864012155879,-2.74259066959644,12.5064436508139));
#413637=CARTESIAN_POINT('Origin',(-2.1024551514253E-32,-1.03047470975092E-30,
12.5064436508139));
#413638=CARTESIAN_POINT('',(-0.151357041680656,-2.74583157639606,12.4908873016278));
#413639=CARTESIAN_POINT('Origin',(-0.150146185347211,-2.72386492378489,
12.4908873016278));
#413640=CARTESIAN_POINT('',(-0.0729573509223692,-2.74903205236796,12.4908873016278));
#413641=CARTESIAN_POINT('Origin',(-1.03628005246125E-16,-2.53849853475974E-15,
12.4908873016278));
#413642=CARTESIAN_POINT('Origin',(-0.0723736921149902,-2.72703979594902,
12.4908873016278));
#413643=CARTESIAN_POINT('Origin',(-1.55097194230457E-16,-1.26080262291685E-15,
12.4908873016278));
#413644=CARTESIAN_POINT('',(-0.373786285366603,-2.71797447633918,12.5064436508139));
#413645=CARTESIAN_POINT('',(-0.296090811011665,-2.72753215797611,12.5064436508139));
#413646=CARTESIAN_POINT('Origin',(-6.29337396212453E-32,-1.02704731748927E-30,
12.5064436508139));
#413647=CARTESIAN_POINT('',(-0.374664178143487,-2.72435804431357,12.4908873016278));
#413648=CARTESIAN_POINT('Origin',(-0.371666864718339,-2.70256317995906,
12.4908873016278));
#413649=CARTESIAN_POINT('',(-0.296786224392158,-2.73393817358971,12.4908873016278));
#413650=CARTESIAN_POINT('Origin',(-3.10194388460913E-16,-2.52160524583369E-15,
12.4908873016278));
#413651=CARTESIAN_POINT('Origin',(-0.294411934597021,-2.71206666820099,
12.4908873016278));
#413652=CARTESIAN_POINT('Origin',(-2.57348239599483E-16,-1.2439655450161E-15,
12.4908873016278));
#413653=CARTESIAN_POINT('',(-0.594082694602854,-2.67846358816632,12.5064436508139));
#413654=CARTESIAN_POINT('',(-0.517424785312005,-2.69432236985558,12.5064436508139));
#413655=CARTESIAN_POINT('Origin',(-1.04424114074394E-31,-1.02021534169599E-30,
12.5064436508139));
#413656=CARTESIAN_POINT('',(-0.595477986316011,-2.68475435893361,12.4908873016278));
#413657=CARTESIAN_POINT('Origin',(-0.590714162425483,-2.66327632406214,
12.4908873016278));
#413658=CARTESIAN_POINT('',(-0.518640034504897,-2.70065038733427,12.4908873016278));
#413659=CARTESIAN_POINT('Origin',(-5.14696479198966E-16,-2.4879310900322E-15,
12.4908873016278));
#413660=CARTESIAN_POINT('Origin',(-0.514490914228858,-2.6790451842356,12.4908873016278));
#413661=CARTESIAN_POINT('Origin',(-3.57886674893445E-16,-1.21885008165314E-15,
12.4908873016278));
#413662=CARTESIAN_POINT('',(-0.810425581523269,-2.6211279667296,12.5064436508139));
#413663=CARTESIAN_POINT('',(-0.735315383035173,-2.64318231089557,12.5064436508139));
#413664=CARTESIAN_POINT('Origin',(-1.45219563277144E-31,-1.01002424804279E-30,
12.5064436508139));
#413665=CARTESIAN_POINT('',(-0.812328986736555,-2.62728407624824,12.4908873016278));
#413666=CARTESIAN_POINT('Origin',(-0.805830354842662,-2.60626580363825,
12.4908873016278));
#413667=CARTESIAN_POINT('',(-0.737042380757589,-2.64939021832708,12.4908873016278));
#413668=CARTESIAN_POINT('Origin',(-7.15773349786891E-16,-2.43770016330628E-15,
12.4908873016278));
#413669=CARTESIAN_POINT('Origin',(-0.731146041711528,-2.62819509658046,
12.4908873016278));
#413670=CARTESIAN_POINT('Origin',(-4.56043433413137E-16,-1.18562337209289E-15,
12.4908873016278));
#413671=CARTESIAN_POINT('',(-1.02137521990946,-2.54634917112997,12.5064436508139));
#413672=CARTESIAN_POINT('',(-0.948312578202743,-2.57445230975092,12.5064436508139));
#413673=CARTESIAN_POINT('Origin',(-1.85048600245827E-31,-9.96541856576512E-31,
12.5064436508139));
#413674=CARTESIAN_POINT('',(-1.02377407177522,-2.5523296515068,12.4908873016278));
#413675=CARTESIAN_POINT('Origin',(-1.01558387920101,-2.53191101429474,12.4908873016278));
#413676=CARTESIAN_POINT('',(-0.950539831569773,-2.58049879453553,12.4908873016278));
#413677=CARTESIAN_POINT('Origin',(-9.12086866826275E-16,-2.37124674418578E-15,
12.4908873016278));
#413678=CARTESIAN_POINT('Origin',(-0.942935512917215,-2.55985480417924,
12.4908873016278));
#413679=CARTESIAN_POINT('Origin',(-5.51165298125335E-16,-1.14450653460545E-15,
12.4908873016278));
#413680=CARTESIAN_POINT('',(-1.22552777472219,-2.45462484191451,12.5064436508139));
#413681=CARTESIAN_POINT('',(-1.15499890962293,-2.48858975323962,12.5064436508139));
#413682=CARTESIAN_POINT('Origin',(-2.23646169310743E-31,-9.79857890387937E-31,
12.5064436508139));
#413683=CARTESIAN_POINT('',(-1.22840610927704,-2.46038989403932,12.4908873016278));
#413684=CARTESIAN_POINT('Origin',(-1.21857886040283,-2.44070677488701,12.4908873016278));
#413685=CARTESIAN_POINT('',(-1.15771159663089,-2.49443457701868,12.4908873016278));
#413686=CARTESIAN_POINT('Origin',(-1.10233059625067E-15,-2.28901306921089E-15,
12.4908873016278));
#413687=CARTESIAN_POINT('Origin',(-1.14844990385785,-2.47447910040253,12.4908873016278));
#413688=CARTESIAN_POINT('Origin',(-6.42619248714382E-16,-1.09577319496049E-15,
12.4908873016278));
#413689=CARTESIAN_POINT('',(-1.42152464439201,-2.34656538936071,12.5064436508139));
#413690=CARTESIAN_POINT('',(-1.35399891386099,-2.38616604250891,12.5064436508139));
#413691=CARTESIAN_POINT('Origin',(-2.60755410017916E-31,-9.60083378519385E-31,
12.5064436508139));
#413692=CARTESIAN_POINT('',(-1.42486330679438,-2.35207664776278,12.4908873016278));
#413693=CARTESIAN_POINT('Origin',(-1.41346440034002,-2.33326003458068,12.4908873016278));
#413694=CARTESIAN_POINT('',(-1.3571789820254,-2.39177030894451,12.4908873016278));
#413695=CARTESIAN_POINT('Origin',(-1.28523849742876E-15,-2.19154638992098E-15,
12.4908873016278));
#413696=CARTESIAN_POINT('Origin',(-1.3463215501692,-2.37263614647295,12.4908873016278));
#413697=CARTESIAN_POINT('Origin',(-7.29796674227947E-16,-1.03974766549292E-15,
12.4908873016278));
#413698=CARTESIAN_POINT('',(-1.60806150208845,-2.22288993129674,12.5064436508139));
#413699=CARTESIAN_POINT('',(-1.5439882787214,-2.26786279045499,12.5064436508139));
#413700=CARTESIAN_POINT('Origin',(-2.96129366493035E-31,-9.37349917084775E-31,
12.5064436508139));
#413701=CARTESIAN_POINT('',(-1.61183827409089,-2.22811071946071,12.4908873016278));
#413702=CARTESIAN_POINT('Origin',(-1.59894356789816,-2.21028583370502,12.4908873016278));
#413703=CARTESIAN_POINT('',(-1.5476145652133,-2.27318920407863,12.4908873016278));
#413704=CARTESIAN_POINT('Origin',(-1.45959334845589E-15,-2.07949533098585E-15,
12.4908873016278));
#413705=CARTESIAN_POINT('Origin',(-1.5352336486916,-2.255003690446,12.4908873016278));
#413706=CARTESIAN_POINT('Origin',(-8.12117423282501E-16,-9.76802786857791E-16,
12.4908873016278));
#413707=CARTESIAN_POINT('',(-1.78389697579996,-2.08442150749102,12.5064436508139));
#413708=CARTESIAN_POINT('',(-1.72370265632705,-2.13446728570162,12.5064436508139));
#413709=CARTESIAN_POINT('Origin',(-3.29532630892049E-31,-9.11808793519199E-31,
12.5064436508139));
#413710=CARTESIAN_POINT('',(-1.78808672360792,-2.08931708193301,12.4908873016278));
#413711=CARTESIAN_POINT('Origin',(-1.77378202981906,-2.07260254527755,12.4908873016278));
#413712=CARTESIAN_POINT('',(-1.72775102880814,-2.13948040010943,12.4908873016278));
#413713=CARTESIAN_POINT('Origin',(-1.624234846565E-15,-1.95360557371558E-15,
12.4908873016278));
#413714=CARTESIAN_POINT('Origin',(-1.71392902057767,-2.12236455690856,12.4908873016278));
#413715=CARTESIAN_POINT('Origin',(-8.89033664875054E-16,-9.07357446837236E-16,
12.4908873016278));
#413716=CARTESIAN_POINT('',(-1.94786090945981,-1.93208160245828,12.5064436508139));
#413717=CARTESIAN_POINT('',(-1.89194607714577,-1.98686725332422,12.5064436508139));
#413718=CARTESIAN_POINT('Origin',(-3.60742910001534E-31,-8.83629979785995E-31,
12.5064436508139));
#413719=CARTESIAN_POINT('',(-1.95243575099289,-1.93661938393811,12.4908873016278));
#413720=CARTESIAN_POINT('Origin',(-1.93681626498495,-1.92112642886661,12.4908873016278));
#413721=CARTESIAN_POINT('',(-1.89638959436511,-1.99153370706693,12.4908873016278));
#413722=CARTESIAN_POINT('Origin',(-1.77806732975011E-15,-1.81471489367447E-15,
12.4908873016278));
#413723=CARTESIAN_POINT('Origin',(-1.88121847761019,-1.97560143741039,12.4908873016278));
#413724=CARTESIAN_POINT('Origin',(-9.60033534108093E-16,-8.3187379271142E-16,
12.4908873016278));
#413725=CARTESIAN_POINT('',(-2.09886215014164,-1.76688401313222,12.5064436508139));
#413726=CARTESIAN_POINT('',(-2.04759890897021,-1.82604494718596,12.5064436508139));
#413727=CARTESIAN_POINT('Origin',(-3.89552504563349E-31,-8.53001001241383E-31,
12.5064436508139));
#413728=CARTESIAN_POINT('',(-2.10379164058423,-1.77103380346281,12.4908873016278));
#413729=CARTESIAN_POINT('Origin',(-2.08696130745955,-1.7568655330351,12.4908873016278));
#413730=CARTESIAN_POINT('',(-2.05240800005384,-1.83033368578382,12.4908873016278));
#413731=CARTESIAN_POINT('Origin',(-1.92006706821618E-15,-1.66374758542284E-15,
12.4908873016278));
#413732=CARTESIAN_POINT('Origin',(-2.03598873605341,-1.81569101629755,12.4908873016278));
#413733=CARTESIAN_POINT('Origin',(-1.02464453856603E-15,-7.50854155744624E-16,
12.4908873016278));
#413734=CARTESIAN_POINT('',(-2.23589580950215,-1.5899281022141,12.5064436508139));
#413735=CARTESIAN_POINT('',(-2.18962530788549,-1.6530706132004,12.5064436508139));
#413736=CARTESIAN_POINT('Origin',(-4.15769691478934E-31,-8.2012568868415E-31,
12.5064436508139));
#413737=CARTESIAN_POINT('',(-2.24114714390866,-1.59366228522547,12.4908873016278));
#413738=CARTESIAN_POINT('Origin',(-2.22321796675739,-1.58091298694366,12.4908873016278));
#413739=CARTESIAN_POINT('',(-2.1947679691257,-1.65695309580563,12.4908873016278));
#413740=CARTESIAN_POINT('Origin',(-2.04928907713205E-15,-1.50170831148925E-15,
12.4908873016278));
#413741=CARTESIAN_POINT('Origin',(-2.1772098253727,-1.64369747103918,12.4908873016278));
#413742=CARTESIAN_POINT('Origin',(-1.08243670267425E-15,-6.64837708253564E-16,
12.4908873016278));
#413743=CARTESIAN_POINT('',(-2.35804995114726,-1.40239148209542,12.5064436508139));
#413744=CARTESIAN_POINT('',(-2.31708011163955,-1.46909536702144,12.5064436508139));
#413745=CARTESIAN_POINT('Origin',(-4.39219999694897E-31,-7.8522282189532E-31,
12.5064436508139));
#413746=CARTESIAN_POINT('',(-2.36358818275363,-1.40568520741572,12.4908873016278));
#413747=CARTESIAN_POINT('Origin',(-2.3446794772916,-1.3944397257564,12.4908873016278));
#413748=CARTESIAN_POINT('',(-2.32252211947425,-1.47254575635286,12.4908873016278));
#413749=CARTESIAN_POINT('Origin',(-2.1648734053485E-15,-1.32967541650713E-15,
12.4908873016278));
#413750=CARTESIAN_POINT('Origin',(-2.30394194251846,-1.46076539030204,12.4908873016278));
#413751=CARTESIAN_POINT('Origin',(-1.13302542911566E-15,-5.74396875504576E-16,
12.4908873016278));
#413752=CARTESIAN_POINT('',(-2.46451165941835,-1.20552217804169,12.5064436508139));
#413753=CARTESIAN_POINT('',(-2.42911512954195,-1.27534353355862,12.5064436508139));
#413754=CARTESIAN_POINT('Origin',(-4.5974737127909E-31,-7.48524673694805E-31,
12.5064436508139));
#413755=CARTESIAN_POINT('',(-2.47029993220698,-1.20835352647236,12.4908873016278));
#413756=CARTESIAN_POINT('Origin',(-2.45053753274933,-1.19868669826058,12.4908873016278));
#413757=CARTESIAN_POINT('',(-2.43482026830688,-1.27833886784452,12.4908873016278));
#413758=CARTESIAN_POINT('Origin',(-2.26605085823133E-15,-1.14879375100915E-15,
12.4908873016278));
#413759=CARTESIAN_POINT('Origin',(-2.41534170616043,-1.26811215690176,12.4908873016278));
#413760=CARTESIAN_POINT('Origin',(-1.17607405826235E-15,-4.8013352631792E-16,
12.4908873016278));
#413761=CARTESIAN_POINT('',(-2.55457244921181,-1.00063032279027,12.5064436508139));
#413762=CARTESIAN_POINT('',(-2.52498478703303,-1.07310449929684,12.5064436508139));
#413763=CARTESIAN_POINT('Origin',(-4.77215199960397E-31,-7.10275464204111E-31,
12.5064436508139));
#413764=CARTESIAN_POINT('',(-2.56057224318229,-1.00298045217462,12.4908873016278));
#413765=CARTESIAN_POINT('Origin',(-2.54008766523683,-0.994956608557225,
12.4908873016278));
#413766=CARTESIAN_POINT('',(-2.530915089971,-1.07562484508174,12.4908873016278));
#413767=CARTESIAN_POINT('Origin',(-2.3521481165247E-15,-9.60267052635839E-16,
12.4908873016278));
#413768=CARTESIAN_POINT('Origin',(-2.51066776925123,-1.06701984632108,12.4908873016278));
#413769=CARTESIAN_POINT('Origin',(-1.21129610858986E-15,-3.82674967730074E-16,
12.4908873016278));
#413770=CARTESIAN_POINT('',(-2.62763298083055,-0.789079437833052,12.5064436508139));
#413771=CARTESIAN_POINT('',(-2.60405108735958,-0.863724131642026,12.5064436508139));
#413772=CARTESIAN_POINT('Origin',(-4.91507240220934E-31,-6.70729735601724E-31,
12.5064436508139));
#413773=CARTESIAN_POINT('',(-2.63380436834391,-0.79093270844779,12.4908873016278));
#413774=CARTESIAN_POINT('Origin',(-2.61273393339716,-0.784605246780207,
12.4908873016278));
#413775=CARTESIAN_POINT('',(-2.61016708928295,-0.865752716440546,12.4908873016278));
#413776=CARTESIAN_POINT('Origin',(-2.42259221717972E-15,-7.65349935460146E-16,
12.4908873016278));
#413777=CARTESIAN_POINT('Origin',(-2.58928575256869,-0.858826694709021,
12.4908873016278));
#413778=CARTESIAN_POINT('Origin',(-1.2384571831645E-15,-2.82669770368909E-16,
12.4908873016278));
#413779=CARTESIAN_POINT('',(-2.68320704849079,-0.572277359406002,12.5064436508139));
#413780=CARTESIAN_POINT('',(-2.66578785733794,-0.648595822395582,12.5064436508139));
#413781=CARTESIAN_POINT('Origin',(-5.02528380890787E-31,-6.30150658186906E-31,
12.5064436508139));
#413782=CARTESIAN_POINT('',(-2.68950895998133,-0.573621438040948,12.4908873016278));
#413783=CARTESIAN_POINT('Origin',(-2.66799288830148,-0.56903246653662,12.4908873016278));
#413784=CARTESIAN_POINT('',(-2.67204885726298,-0.650119146310585,12.4908873016278));
#413785=CARTESIAN_POINT('Origin',(-2.476914366329E-15,-5.65339540737817E-16,
12.4908873016278));
#413786=CARTESIAN_POINT('Origin',(-2.65067246640488,-0.6449181931401,12.4908873016278));
#413787=CARTESIAN_POINT('Origin',(-1.25737652951623E-15,-1.80783452323169E-16,
12.4908873016278));
#413788=CARTESIAN_POINT('',(-2.72092481594133,-0.351666869571222,12.5064436508139));
#413789=CARTESIAN_POINT('',(-2.70978424894974,-0.429151214961874,12.5064436508139));
#413790=CARTESIAN_POINT('Origin',(-5.10205278097159E-31,-5.88808279024776E-31,
12.5064436508139));
#413791=CARTESIAN_POINT('',(-2.72731531322782,-0.352492811604818,12.4908873016278));
#413792=CARTESIAN_POINT('Origin',(-2.70549679072199,-0.34967286911198,12.4908873016278));
#413793=CARTESIAN_POINT('',(-2.71614858095496,-0.430159140524035,12.4908873016278));
#413794=CARTESIAN_POINT('Origin',(-2.51475305903245E-15,-3.61566904646336E-16,
12.4908873016278));
#413795=CARTESIAN_POINT('Origin',(-2.69441939230732,-0.426717867399843,
12.4908873016278));
#413796=CARTESIAN_POINT('Origin',(-1.26792824251655E-15,-7.76940502293878E-17,
12.4908873016278));
#413797=CARTESIAN_POINT('',(-2.74053527766277,-0.128716094740396,12.5064436508139));
#413798=CARTESIAN_POINT('',(-2.73574747346772,-0.206850676997561,12.5064436508139));
#413799=CARTESIAN_POINT('Origin',(-5.1448684335574E-31,-5.46977724827647E-31,
12.5064436508139));
#413800=CARTESIAN_POINT('',(-2.74697183304013,-0.12901840366468,12.4908873016278));
#413801=CARTESIAN_POINT('Origin',(-2.7249960583758,-0.127986256435362,12.4908873016278));
#413802=CARTESIAN_POINT('',(-2.74217278397365,-0.207336496628562,12.4908873016278));
#413803=CARTESIAN_POINT('Origin',(-2.5358564850331E-15,-1.55388100458775E-16,
12.4908873016278));
#413804=CARTESIAN_POINT('Origin',(-2.72023540170186,-0.205677804655533,
12.4908873016278));
#413805=CARTESIAN_POINT('Origin',(-1.27004210225636E-15,2.59123929500539E-17,
12.4908873016278));
#413806=CARTESIAN_POINT('',(-2.74190792926786,0.0950912644642679,12.5064436508139));
#413807=CARTESIAN_POINT('',(-2.74350474991634,0.0168264180942123,12.5064436508139));
#413808=CARTESIAN_POINT('Origin',(-5.15344583556142E-31,-5.04937371032143E-31,
12.5064436508139));
#413809=CARTESIAN_POINT('',(-2.748347708522,0.0953146004653095,12.4908873016278));
#413810=CARTESIAN_POINT('Origin',(-2.72636092685383,0.0945520836615871,
12.4908873016278));
#413811=CARTESIAN_POINT('',(-2.74994827954166,0.0168659374438614,12.4908873016278));
#413812=CARTESIAN_POINT('Origin',(-2.54008420451272E-15,5.18247859001083E-17,
12.4908873016278));
#413813=CARTESIAN_POINT('Origin',(-2.72794869330533,0.0167310099443105,
12.4908873016278));
#413814=CARTESIAN_POINT('Origin',(-1.26370404134785E-15,1.29346393429657E-16,
12.4908873016278));
#413815=CARTESIAN_POINT('',(-2.72503363598664,0.318265806992875,12.5064436508139));
#413816=CARTESIAN_POINT('',(-2.73300445490068,0.240391536149731,12.5064436508139));
#413817=CARTESIAN_POINT('Origin',(-5.12772790578849E-31,-4.62966989256605E-31,
12.5064436508139));
#413818=CARTESIAN_POINT('',(-2.73143378344912,0.319013301655004,12.4908873016278));
#413819=CARTESIAN_POINT('Origin',(-2.70958231318153,0.316461195241764,12.4908873016278));
#413820=CARTESIAN_POINT('',(-2.73942332301885,0.240956131485279,12.4908873016278));
#413821=CARTESIAN_POINT('Origin',(-2.52740808269571E-15,2.58692786859314E-16,
12.4908873016278));
#413822=CARTESIAN_POINT('Origin',(-2.7175079364347,0.239028482433397,12.4908873016278));
#413823=CARTESIAN_POINT('Origin',(-1.24895623854067E-15,2.31919615001638E-16,
12.4908873016278));
#413824=CARTESIAN_POINT('',(-2.69002469345683,0.539322343086108,12.5064436508139));
#413825=CARTESIAN_POINT('',(-2.70431646615165,0.462356888193986,12.5064436508139));
#413826=CARTESIAN_POINT('Origin',(-5.0678857928181E-31,-4.21345885467123E-31,
12.5064436508139));
#413827=CARTESIAN_POINT('',(-2.69634261720224,0.540589021955675,12.4908873016278));
#413828=CARTESIAN_POINT('Origin',(-2.67477187626462,0.536264309780029,12.4908873016278));
#413829=CARTESIAN_POINT('',(-2.71066795625439,0.463442802226626,12.4908873016278));
#413830=CARTESIAN_POINT('Origin',(-2.49791247708133E-15,4.63839230003276E-16,
12.4908873016278));
#413831=CARTESIAN_POINT('Origin',(-2.68898261260435,0.459735259808813,12.4908873016278));
#413832=CARTESIAN_POINT('Origin',(-1.22589683802926E-15,3.32949449799826E-16,
12.4908873016278));
#413833=CARTESIAN_POINT('',(-2.63711408041489,0.756789777968025,12.5064436508139));
#413834=CARTESIAN_POINT('',(-2.6576316975012,0.681245331430826,12.5064436508139));
#413835=CARTESIAN_POINT('Origin',(-4.9743177360388E-31,-3.80351041242416E-31,
12.5064436508139));
#413836=CARTESIAN_POINT('',(-2.64330773570309,0.75856721150614,12.4908873016278));
#413837=CARTESIAN_POINT('Origin',(-2.62216127381747,0.752498673814091,12.4908873016278));
#413838=CARTESIAN_POINT('',(-2.66387354146978,0.682845337581834,12.4908873016278));
#413839=CARTESIAN_POINT('Origin',(-2.45179367605853E-15,6.65898899599653E-16,
12.4908873016278));
#413840=CARTESIAN_POINT('Origin',(-2.64256255313802,0.677382574881179,12.4908873016278));
#413841=CARTESIAN_POINT('Origin',(-1.19467929631952E-15,4.31763560942389E-16,
12.4908873016278));
#413842=CARTESIAN_POINT('',(-2.566653908261,0.969220901739089,12.5064436508139));
#413843=CARTESIAN_POINT('',(-2.59326082838224,0.895600199384562,12.5064436508139));
#413844=CARTESIAN_POINT('Origin',(-4.84764641543082E-31,-3.40255270507128E-31,
12.5064436508139));
#413845=CARTESIAN_POINT('',(-2.57268207733792,0.971497261418813,12.4908873016278));
#413846=CARTESIAN_POINT('Origin',(-2.55210062071922,0.963725283327462,12.4908873016278));
#413847=CARTESIAN_POINT('',(-2.59935148777489,0.897703649876986,12.4908873016278));
#413848=CARTESIAN_POINT('Origin',(-2.38935859263904E-15,8.63527121884779E-16,
12.4908873016278));
#413849=CARTESIAN_POINT('Origin',(-2.57855667587269,0.89052202067797,12.4908873016278));
#413850=CARTESIAN_POINT('Origin',(-1.15551136100098E-15,5.27704356822854E-16,
12.4908873016278));
#413851=CARTESIAN_POINT('',(-2.47911307781571,1.17520202031927,12.5064436508139));
#413852=CARTESIAN_POINT('',(-2.51163223630831,1.10399499577503,12.5064436508139));
#413853=CARTESIAN_POINT('Origin',(-4.68871480773351E-31,-3.01325404000165E-31,
12.5064436508139));
#413854=CARTESIAN_POINT('',(-2.48493564421073,1.17796215734251,12.4908873016278));
#413855=CARTESIAN_POINT('Origin',(-2.46505615905704,1.16853846008377,12.4908873016278));
#413856=CARTESIAN_POINT('',(-2.51753117879167,1.10658789249288,12.4908873016278));
#413857=CARTESIAN_POINT('Origin',(-2.31102272200196E-15,1.05540871364571E-15,
12.4908873016278));
#413858=CARTESIAN_POINT('Origin',(-2.49739092936133,1.09773518935294,12.4908873016278));
#413859=CARTESIAN_POINT('Origin',(-1.10865368822093E-15,6.20133367273753E-16,
12.4908873016278));
#413860=CARTESIAN_POINT('',(-2.37507415886243,1.37336236334892,12.5064436508139));
#413861=CARTESIAN_POINT('',(-2.4132891460919,1.30504288761496,12.5064436508139));
#413862=CARTESIAN_POINT('Origin',(-4.49858057657423E-31,-2.63820513560155E-31,
12.5064436508139));
#413863=CARTESIAN_POINT('',(-2.38065237435684,1.37658790945917,12.4908873016278));
#413864=CARTESIAN_POINT('Origin',(-2.36160715536198,1.36557520618349,12.4908873016278));
#413865=CARTESIAN_POINT('',(-2.41895711517699,1.30810797525839,12.4908873016278));
#413866=CARTESIAN_POINT('Origin',(-2.21730737644186E-15,1.24026673454751E-15,
12.4908873016278));
#413867=CARTESIAN_POINT('Origin',(-2.39960545825558,1.29764311145632,12.4908873016278));
#413868=CARTESIAN_POINT('Origin',(-1.05441810806075E-15,7.08435492480249E-16,
12.4908873016278));
#413869=CARTESIAN_POINT('',(-2.25522951324157,1.56238320643931,12.5064436508139));
#413870=CARTESIAN_POINT('',(-2.29888601477294,1.49740593435474,12.5064436508139));
#413871=CARTESIAN_POINT('Origin',(-4.27850903389139E-31,-2.27990188045105E-31,
12.5064436508139));
#413872=CARTESIAN_POINT('',(-2.2605262557316,1.56605269615939,12.4908873016278));
#413873=CARTESIAN_POINT('Origin',(-2.24244204568574,1.55352427459012,12.4908873016278));
#413874=CARTESIAN_POINT('',(-2.30428529106065,1.50092281527118,12.4908873016278));
#413875=CARTESIAN_POINT('Origin',(-2.10883621612151E-15,1.4168709849605E-15,
12.4908873016278));
#413876=CARTESIAN_POINT('Origin',(-2.28585100873216,1.48891543274901,12.4908873016278));
#413877=CARTESIAN_POINT('Origin',(-9.93165549358178E-16,7.92023096367917E-16,
12.4908873016278));
#413878=CARTESIAN_POINT('',(-2.12037668729676,1.74100664706594,12.5064436508139));
#413879=CARTESIAN_POINT('',(-2.16918417631515,1.67980399165597,12.5064436508139));
#413880=CARTESIAN_POINT('Origin',(-4.0299647194923E-31,-1.9407287235973E-31,
12.5064436508139));
#413881=CARTESIAN_POINT('',(-2.12535670783504,1.74509566054718,12.4908873016278));
#413882=CARTESIAN_POINT('Origin',(-2.10835385417236,1.7311348952628,12.4908873016278));
#413883=CARTESIAN_POINT('',(-2.1742788285126,1.68374926158317,12.4908873016278));
#413884=CARTESIAN_POINT('Origin',(-1.98633109871636E-15,1.58404619273583E-15,
12.4908873016278));
#413885=CARTESIAN_POINT('Origin',(-2.1568845978845,1.6702792674905,12.4908873016278));
#413886=CARTESIAN_POINT('Origin',(-9.25303637785404E-16,8.7033991722387E-16,
12.4908873016278));
#413887=CARTESIAN_POINT('',(-1.97141310433553,1.90804397570222,12.5064436508139));
#413888=CARTESIAN_POINT('',(-2.02504677505419,1.85102323054089,12.5064436508139));
#413889=CARTESIAN_POINT('Origin',(-3.75460165478238E-31,-1.62294280643953E-31,
12.5064436508139));
#413890=CARTESIAN_POINT('',(-1.97604326170702,1.91252530123455,12.4908873016278));
#413891=CARTESIAN_POINT('Origin',(-1.96023491561336,1.89722509882467,12.4908873016278));
#413892=CARTESIAN_POINT('',(-2.02980289909156,1.8553706343584,12.4908873016278));
#413893=CARTESIAN_POINT('Origin',(-1.85060727557081E-15,1.74067983444774E-15,
12.4908873016278));
#413894=CARTESIAN_POINT('Origin',(-2.01356447589883,1.84052766928353,12.4908873016278));
#413895=CARTESIAN_POINT('Origin',(-8.51283983167522E-16,9.42864769526676E-16,
12.4908873016278));
#413896=CARTESIAN_POINT('',(-1.80933009242521,2.0623835864853,12.5064436508139));
#413897=CARTESIAN_POINT('',(-1.86743302161444,2.00992421522389,12.5064436508139));
#413898=CARTESIAN_POINT('Origin',(-3.45425233552554E-31,-1.32865894182544E-31,
12.5064436508139));
#413899=CARTESIAN_POINT('',(-1.81357957369652,2.06722740158666,12.4908873016278));
#413900=CARTESIAN_POINT('Origin',(-1.79907093710695,2.05068958237397,12.4908873016278));
#413901=CARTESIAN_POINT('',(-1.87181896627098,2.01464482167658,12.4908873016278));
#413902=CARTESIAN_POINT('Origin',(-1.70256796633504E-15,1.88572953905335E-15,
12.4908873016278));
#413903=CARTESIAN_POINT('Origin',(-1.85684441454081,1.99852766310317,12.4908873016278));
#413904=CARTESIAN_POINT('Origin',(-7.71599174093631E-16,1.00911501235002E-15,
12.4908873016278));
#413905=CARTESIAN_POINT('',(-1.63520628726825,2.20299837476966,12.5064436508139));
#413906=CARTESIAN_POINT('',(-1.6973918095206,2.15544948586873,12.5064436508139));
#413907=CARTESIAN_POINT('Origin',(-3.1309155368873E-31,-1.05983554032062E-31,
12.5064436508139));
#413908=CARTESIAN_POINT('',(-1.63904681284264,2.20817244464973,12.4908873016278));
#413909=CARTESIAN_POINT('Origin',(-1.6259344383399,2.19050706509254,12.4908873016278));
#413910=CARTESIAN_POINT('',(-1.70137838705825,2.1605118800995,12.4908873016278));
#413911=CARTESIAN_POINT('Origin',(-1.54319834818726E-15,2.01823002470004E-15,
12.4908873016278));
#413912=CARTESIAN_POINT('Origin',(-1.68776735996178,2.14322778505871,12.4908873016278));
#413913=CARTESIAN_POINT('Origin',(-6.86779499821049E-16,1.06864976125843E-15,
12.4908873016278));
#413914=CARTESIAN_POINT('',(-1.45020045405957,2.32895257233908,12.5064436508139));
#413915=CARTESIAN_POINT('',(-1.51605473498434,2.28663059580924,12.5064436508139));
#413916=CARTESIAN_POINT('Origin',(-2.78674301191578E-31,-8.18261577309334E-32,
12.5064436508139));
#413917=CARTESIAN_POINT('',(-1.45360646587299,2.33442246441647,12.4908873016278));
#413918=CARTESIAN_POINT('Origin',(-1.441977614146,2.31574708470114,12.4908873016278));
#413919=CARTESIAN_POINT('',(-1.51961541538732,2.29200108841973,12.4908873016278));
#413920=CARTESIAN_POINT('Origin',(-1.3735589996421E-15,2.13729952251686E-15,
12.4908873016278));
#413921=CARTESIAN_POINT('Origin',(-1.50745849206422,2.27366507971237,12.4908873016278));
#413922=CARTESIAN_POINT('Origin',(-5.97389421287801E-16,1.12107282232047E-15,
12.4908873016278));
#413923=CARTESIAN_POINT('',(-1.25554377609535,2.43940797478971,12.5064436508139));
#413924=CARTESIAN_POINT('',(-1.32462856631819,2.40259455640214,12.5064436508139));
#413925=CARTESIAN_POINT('Origin',(-2.42402517198019E-31,-6.05544687658534E-32,
12.5064436508139));
#413926=CARTESIAN_POINT('',(-1.25849260770113,2.44513728783511,12.4908873016278));
#413927=CARTESIAN_POINT('Origin',(-1.24842466683952,2.42557618953242,12.4908873016278));
#413928=CARTESIAN_POINT('',(-1.32773965384588,2.40823740765009,12.4908873016278));
#413929=CARTESIAN_POINT('Origin',(-1.1947788425756E-15,2.24214564464094E-15,
12.4908873016278));
#413930=CARTESIAN_POINT('Origin',(-1.31711773661511,2.38897150838889,12.4908873016278));
#413931=CARTESIAN_POINT('Origin',(-5.04023814718198E-16,1.16603532871396E-15,
12.4908873016278));
#413932=CARTESIAN_POINT('',(-1.05253166145136,2.53362951964209,12.5064436508139));
#413933=CARTESIAN_POINT('',(-1.12438721309152,2.50256964662238,12.5064436508139));
#413934=CARTESIAN_POINT('Origin',(-2.04517584446108E-31,-4.23100467173029E-32,
12.5064436508139));
#413935=CARTESIAN_POINT('',(-1.05500368886169,2.53958012602246,12.4908873016278));
#413936=CARTESIAN_POINT('Origin',(-1.0465636593508,2.51926348501428,12.4908873016278));
#413937=CARTESIAN_POINT('',(-1.12702800396973,2.50844730426374,12.4908873016278));
#413938=CARTESIAN_POINT('Origin',(-1.0080476294364E-15,2.33207065742792E-15,
12.4908873016278));
#413939=CARTESIAN_POINT('Origin',(-1.11801177993797,2.48837972582963,12.4908873016278));
#413940=CARTESIAN_POINT('Origin',(-4.07304012819722E-16,1.20323806237714E-15,
12.4908873016278));
#413941=CARTESIAN_POINT('',(-0.842515122255916,2.61099017806071,12.5064436508139));
#413942=CARTESIAN_POINT('',(-0.916663248472555,2.58589054873928,12.5064436508139));
#413943=CARTESIAN_POINT('Origin',(-1.65271620912734E-31,-2.72143052038969E-32,
12.5064436508139));
#413944=CARTESIAN_POINT('',(-0.844493894536228,2.61712247747236,12.4908873016278));
#413945=CARTESIAN_POINT('Origin',(-0.837737943379938,2.59618549765258,12.4908873016278));
#413946=CARTESIAN_POINT('',(-0.918816168673682,2.59196389793219,12.4908873016278));
#413947=CARTESIAN_POINT('Origin',(-8.14608025639444E-16,2.40647612475429E-15,
12.4908873016278));
#413948=CARTESIAN_POINT('Origin',(-0.911465639324292,2.57122818674873,12.4908873016278));
#413949=CARTESIAN_POINT('Origin',(-3.07873669916363E-16,1.23243344525552E-15,
12.4908873016278));
#413950=CARTESIAN_POINT('',(-0.626891783927067,2.67097512762739,12.5064436508139));
#413951=CARTESIAN_POINT('',(-0.702839041173797,2.65200277589623,12.5064436508139));
#413952=CARTESIAN_POINT('Origin',(-1.24925802010084E-31,-1.53677038947852E-32,
12.5064436508139));
#413953=CARTESIAN_POINT('',(-0.628364132674314,2.67724831062949,12.4908873016278));
#413954=CARTESIAN_POINT('Origin',(-0.62333721961292,2.65583032414446,12.4908873016278));
#413955=CARTESIAN_POINT('',(-0.704489763369112,2.65823139950384,12.4908873016278));
#413956=CARTESIAN_POINT('Origin',(-6.15747339832725E-16,2.46486689051103E-15,
12.4908873016278));
#413957=CARTESIAN_POINT('Origin',(-0.698853845262159,2.63696554830781,12.4908873016278));
#413958=CARTESIAN_POINT('Origin',(-2.0639447853529E-16,1.25342718689292E-15,
12.4908873016278));
#413959=CARTESIAN_POINT('',(-0.407096584206047,2.71318517839958,12.5064436508139));
#413960=CARTESIAN_POINT('',(-0.484337556016306,2.70046636212924,12.5064436508139));
#413961=CARTESIAN_POINT('Origin',(-8.37486225063633E-32,-6.84907996712842E-33,
12.5064436508139));
#413962=CARTESIAN_POINT('',(-0.408052711182237,2.71955749799427,12.4908873016278));
#413963=CARTESIAN_POINT('Origin',(-0.404788289492779,2.69780103801031,12.4908873016278));
#413964=CARTESIAN_POINT('',(-0.485475094921951,2.7068088096891,12.4908873016278));
#413965=CARTESIAN_POINT('Origin',(-4.1278895707058E-16,2.50685437378584E-15,
12.4908873016278));
#413966=CARTESIAN_POINT('Origin',(-0.481591294162575,2.68515433921159,12.4908873016278));
#413967=CARTESIAN_POINT('Origin',(9.93165549358168E-16,7.9202309636793E-16,
12.4908873016278));
#413968=CARTESIAN_POINT('',(2.16918417631513,1.679803991656,12.5064436508139));
#413969=CARTESIAN_POINT('',(2.12037668729674,1.74100664706597,12.5064436508139));
#413970=CARTESIAN_POINT('Origin',(4.02996471949226E-31,-1.94072872359725E-31,
12.5064436508139));
#413971=CARTESIAN_POINT('',(2.17427882851258,1.6837492615832,12.4908873016278));
#413972=CARTESIAN_POINT('Origin',(2.15688459788448,1.67027926749053,12.4908873016278));
#413973=CARTESIAN_POINT('',(2.12535670783502,1.74509566054721,12.4908873016278));
#413974=CARTESIAN_POINT('Origin',(1.98633109871634E-15,1.58404619273586E-15,
12.4908873016278));
#413975=CARTESIAN_POINT('Origin',(2.10835385417234,1.73113489526283,12.4908873016278));
#413976=CARTESIAN_POINT('Origin',(9.25303637785393E-16,8.70339917223882E-16,
12.4908873016278));
#413977=CARTESIAN_POINT('',(2.02504677505416,1.85102323054091,12.5064436508139));
#413978=CARTESIAN_POINT('',(1.9714131043355,1.90804397570225,12.5064436508139));
#413979=CARTESIAN_POINT('Origin',(3.75460165478233E-31,-1.62294280643948E-31,
12.5064436508139));
#413980=CARTESIAN_POINT('',(2.02980289909154,1.85537063435843,12.4908873016278));
#413981=CARTESIAN_POINT('Origin',(2.01356447589881,1.84052766928356,12.4908873016278));
#413982=CARTESIAN_POINT('',(1.97604326170699,1.91252530123458,12.4908873016278));
#413983=CARTESIAN_POINT('Origin',(1.85060727557078E-15,1.74067983444776E-15,
12.4908873016278));
#413984=CARTESIAN_POINT('Origin',(1.96023491561333,1.8972250988247,12.4908873016278));
#413985=CARTESIAN_POINT('Origin',(8.5128398316751E-16,9.42864769526687E-16,
12.4908873016278));
#413986=CARTESIAN_POINT('',(1.86743302161441,2.00992421522391,12.5064436508139));
#413987=CARTESIAN_POINT('',(1.80933009242518,2.06238358648533,12.5064436508139));
#413988=CARTESIAN_POINT('Origin',(3.45425233552549E-31,-1.3286589418254E-31,
12.5064436508139));
#413989=CARTESIAN_POINT('',(1.87181896627095,2.01464482167661,12.4908873016278));
#413990=CARTESIAN_POINT('Origin',(1.85684441454078,1.99852766310319,12.4908873016278));
#413991=CARTESIAN_POINT('',(1.81357957369649,2.06722740158669,12.4908873016278));
#413992=CARTESIAN_POINT('Origin',(1.70256796633502E-15,1.88572953905338E-15,
12.4908873016278));
#413993=CARTESIAN_POINT('Origin',(1.79907093710692,2.05068958237399,12.4908873016278));
#413994=CARTESIAN_POINT('Origin',(7.71599174093617E-16,1.00911501235003E-15,
12.4908873016278));
#413995=CARTESIAN_POINT('',(1.69739180952057,2.15544948586875,12.5064436508139));
#413996=CARTESIAN_POINT('',(1.63520628726822,2.20299837476969,12.5064436508139));
#413997=CARTESIAN_POINT('Origin',(3.13091553688725E-31,-1.05983554032057E-31,
12.5064436508139));
#413998=CARTESIAN_POINT('',(1.70137838705821,2.16051188009953,12.4908873016278));
#413999=CARTESIAN_POINT('Origin',(1.68776735996175,2.14322778505873,12.4908873016278));
#414000=CARTESIAN_POINT('',(1.63904681284261,2.20817244464976,12.4908873016278));
#414001=CARTESIAN_POINT('Origin',(1.54319834818723E-15,2.01823002470006E-15,
12.4908873016278));
#414002=CARTESIAN_POINT('Origin',(1.62593443833987,2.19050706509256,12.4908873016278));
#414003=CARTESIAN_POINT('Origin',(6.86779499821035E-16,1.06864976125844E-15,
12.4908873016278));
#414004=CARTESIAN_POINT('',(1.51605473498431,2.28663059580926,12.5064436508139));
#414005=CARTESIAN_POINT('',(1.45020045405953,2.3289525723391,12.5064436508139));
#414006=CARTESIAN_POINT('Origin',(2.78674301191572E-31,-8.18261577309295E-32,
12.5064436508139));
#414007=CARTESIAN_POINT('',(1.51961541538728,2.29200108841975,12.4908873016278));
#414008=CARTESIAN_POINT('Origin',(1.50745849206419,2.2736650797124,12.4908873016278));
#414009=CARTESIAN_POINT('',(1.45360646587295,2.33442246441649,12.4908873016278));
#414010=CARTESIAN_POINT('Origin',(1.37355899964207E-15,2.13729952251688E-15,
12.4908873016278));
#414011=CARTESIAN_POINT('Origin',(1.44197761414597,2.31574708470116,12.4908873016278));
#414012=CARTESIAN_POINT('Origin',(5.97389421287786E-16,1.12107282232048E-15,
12.4908873016278));
#414013=CARTESIAN_POINT('',(1.32462856631816,2.40259455640216,12.5064436508139));
#414014=CARTESIAN_POINT('',(1.25554377609532,2.43940797478972,12.5064436508139));
#414015=CARTESIAN_POINT('Origin',(2.42402517198013E-31,-6.05544687658502E-32,
12.5064436508139));
#414016=CARTESIAN_POINT('',(1.32773965384585,2.40823740765011,12.4908873016278));
#414017=CARTESIAN_POINT('Origin',(1.31711773661508,2.38897150838891,12.4908873016278));
#414018=CARTESIAN_POINT('',(1.2584926077011,2.44513728783512,12.4908873016278));
#414019=CARTESIAN_POINT('Origin',(1.19477884257557E-15,2.24214564464095E-15,
12.4908873016278));
#414020=CARTESIAN_POINT('Origin',(1.24842466683949,2.42557618953244,12.4908873016278));
#414021=CARTESIAN_POINT('Origin',(5.04023814718182E-16,1.16603532871397E-15,
12.4908873016278));
#414022=CARTESIAN_POINT('',(1.12438721309149,2.5025696466224,12.5064436508139));
#414023=CARTESIAN_POINT('',(1.05253166145133,2.53362951964211,12.5064436508139));
#414024=CARTESIAN_POINT('Origin',(2.04517584446102E-31,-4.23100467173001E-32,
12.5064436508139));
#414025=CARTESIAN_POINT('',(1.12702800396969,2.50844730426376,12.4908873016278));
#414026=CARTESIAN_POINT('Origin',(1.11801177993793,2.48837972582965,12.4908873016278));
#414027=CARTESIAN_POINT('',(1.05500368886165,2.53958012602247,12.4908873016278));
#414028=CARTESIAN_POINT('Origin',(1.00804762943636E-15,2.33207065742793E-15,
12.4908873016278));
#414029=CARTESIAN_POINT('Origin',(1.04656365935076,2.51926348501429,12.4908873016278));
#414030=CARTESIAN_POINT('Origin',(4.07304012819706E-16,1.20323806237715E-15,
12.4908873016278));
#414031=CARTESIAN_POINT('',(0.916663248472521,2.58589054873929,12.5064436508139));
#414032=CARTESIAN_POINT('',(0.842515122255881,2.61099017806072,12.5064436508139));
#414033=CARTESIAN_POINT('Origin',(1.65271620912728E-31,-2.72143052038947E-32,
12.5064436508139));
#414034=CARTESIAN_POINT('',(0.918816168673646,2.5919638979322,12.4908873016278));
#414035=CARTESIAN_POINT('Origin',(0.911465639324257,2.57122818674874,12.4908873016278));
#414036=CARTESIAN_POINT('',(0.844493894536193,2.61712247747237,12.4908873016278));
#414037=CARTESIAN_POINT('Origin',(8.14608025639412E-16,2.4064761247543E-15,
12.4908873016278));
#414038=CARTESIAN_POINT('Origin',(0.837737943379903,2.59618549765259,12.4908873016278));
#414039=CARTESIAN_POINT('Origin',(3.07873669916346E-16,1.23243344525552E-15,
12.4908873016278));
#414040=CARTESIAN_POINT('',(0.702839041173762,2.65200277589623,12.5064436508139));
#414041=CARTESIAN_POINT('',(0.626891783927031,2.67097512762739,12.5064436508139));
#414042=CARTESIAN_POINT('Origin',(1.24925802010077E-31,-1.53677038947836E-32,
12.5064436508139));
#414043=CARTESIAN_POINT('',(0.704489763369076,2.65823139950385,12.4908873016278));
#414044=CARTESIAN_POINT('Origin',(0.698853845262123,2.63696554830782,12.4908873016278));
#414045=CARTESIAN_POINT('',(0.628364132674278,2.6772483106295,12.4908873016278));
#414046=CARTESIAN_POINT('Origin',(6.15747339832692E-16,2.46486689051104E-15,
12.4908873016278));
#414047=CARTESIAN_POINT('Origin',(0.623337219612883,2.65583032414446,12.4908873016278));
#414048=CARTESIAN_POINT('Origin',(2.06394478535273E-16,1.25342718689292E-15,
12.4908873016278));
#414049=CARTESIAN_POINT('',(0.484337556016271,2.70046636212925,12.5064436508139));
#414050=CARTESIAN_POINT('',(0.407096584206011,2.71318517839958,12.5064436508139));
#414051=CARTESIAN_POINT('Origin',(8.37486225063565E-32,-6.84907996712733E-33,
12.5064436508139));
#414052=CARTESIAN_POINT('',(0.485475094921914,2.70680880968911,12.4908873016278));
#414053=CARTESIAN_POINT('Origin',(0.481591294162539,2.6851543392116,12.4908873016278));
#414054=CARTESIAN_POINT('',(0.408052711182201,2.71955749799427,12.4908873016278));
#414055=CARTESIAN_POINT('Origin',(4.12788957070546E-16,2.50685437378585E-15,
12.4908873016278));
#414056=CARTESIAN_POINT('Origin',(0.404788289492743,2.69780103801032,12.4908873016278));
#414057=CARTESIAN_POINT('Origin',(1.0354176595224E-16,1.26607957740248E-15,
12.4908873016278));
#414058=CARTESIAN_POINT('',(0.262612884333563,2.73095879026788,12.5064436508139));
#414059=CARTESIAN_POINT('',(0.184592223883309,2.73733942945357,12.5064436508139));
#414060=CARTESIAN_POINT('Origin',(4.2014109737406E-32,-1.71512345769042E-33,
12.5064436508139));
#414061=CARTESIAN_POINT('',(0.2632296698158,2.7373728538379,12.4908873016278));
#414062=CARTESIAN_POINT('Origin',(0.261123832457273,2.7154738710072,12.4908873016278));
#414063=CARTESIAN_POINT('',(0.185025766221164,2.7437684789053,12.4908873016278));
#414064=CARTESIAN_POINT('Origin',(2.0708353190448E-16,2.53215915480496E-15,
12.4908873016278));
#414065=CARTESIAN_POINT('Origin',(0.183545560091395,2.72181833107405,12.4908873016278));
#414066=CARTESIAN_POINT('Origin',(-1.03541765952257E-16,1.26607957740248E-15,
12.4908873016278));
#414067=CARTESIAN_POINT('',(-0.184592223883345,2.73733942945357,12.5064436508139));
#414068=CARTESIAN_POINT('',(-0.262612884333599,2.73095879026787,12.5064436508139));
#414069=CARTESIAN_POINT('Origin',(-4.20141097374128E-32,-1.71512345769099E-33,
12.5064436508139));
#414070=CARTESIAN_POINT('',(-0.185025766221201,2.74376847890529,12.4908873016278));
#414071=CARTESIAN_POINT('Origin',(-0.183545560091431,2.72181833107405,12.4908873016278));
#414072=CARTESIAN_POINT('',(-0.263229669815836,2.7373728538379,12.4908873016278));
#414073=CARTESIAN_POINT('Origin',(-2.07083531904513E-16,2.53215915480496E-15,
12.4908873016278));
#414074=CARTESIAN_POINT('Origin',(-0.261123832457309,2.7154738710072,12.4908873016278));
#414075=CARTESIAN_POINT('Origin',(0.,1.27030641721285E-15,12.4908873016278));
#414076=CARTESIAN_POINT('',(0.0391405672337278,2.74327713823376,12.5064436508139));
#414077=CARTESIAN_POINT('',(-0.0391405672337274,2.74327713823376,12.5064436508139));
#414078=CARTESIAN_POINT('Origin',(0.,0.,12.5064436508139));
#414079=CARTESIAN_POINT('',(0.0392324946869353,2.74972013327914,12.4908873016278));
#414080=CARTESIAN_POINT('Origin',(0.0389186347294398,2.72772237221291,12.4908873016278));
#414081=CARTESIAN_POINT('',(-3.36777869765522E-16,2.75,12.4908873016278));
#414082=CARTESIAN_POINT('Origin',(0.,2.5406128344257E-15,12.4908873016278));
#414083=CARTESIAN_POINT('',(-0.0392324946869358,2.74972013327914,12.4908873016278));
#414084=CARTESIAN_POINT('Origin',(0.,2.5406128344257E-15,12.4908873016278));
#414085=CARTESIAN_POINT('Origin',(-0.0389186347294403,2.72772237221291,
12.4908873016278));
#414086=CARTESIAN_POINT('Origin',(0.,2.5406128344257E-15,14.));
#414087=CARTESIAN_POINT('Ctrl Pts',(5.09848573616328E-14,1.50000000000006,
3.56249999999999));
#414088=CARTESIAN_POINT('Ctrl Pts',(0.0221291496324529,1.50000000000006,
3.56143531079189));
#414089=CARTESIAN_POINT('Ctrl Pts',(0.0442758983615595,1.49951030585925,
3.56035617223172));
#414090=CARTESIAN_POINT('Ctrl Pts',(0.257655251405688,1.49005198771531,
3.54982722226221));
#414091=CARTESIAN_POINT('Ctrl Pts',(0.4454768622445,1.44505001124848,3.53954059589557));
#414092=CARTESIAN_POINT('Ctrl Pts',(0.800824790268939,1.28383039135365,
3.51796558796231));
#414093=CARTESIAN_POINT('Ctrl Pts',(0.963787085995833,1.16647513895563,
3.50686519273134));
#414094=CARTESIAN_POINT('Ctrl Pts',(1.23044649741185,0.879343431360836,
3.48605965505124));
#414095=CARTESIAN_POINT('Ctrl Pts',(1.33323611595351,0.713948364951426,
3.47716379805274));
#414096=CARTESIAN_POINT('Ctrl Pts',(1.47075916267875,0.352640067717556,
3.45709111487308));
#414097=CARTESIAN_POINT('Ctrl Pts',(1.50394514491438,0.160070583293647,
3.44639281018286));
#414098=CARTESIAN_POINT('Ctrl Pts',(1.49519059383191,-0.232269284766078,
3.42459615084621));
#414099=CARTESIAN_POINT('Ctrl Pts',(1.45126380539184,-0.428248175400973,
3.41370843469983));
#414100=CARTESIAN_POINT('Ctrl Pts',(1.29309157908641,-0.783606459655687,
3.39396630779679));
#414101=CARTESIAN_POINT('Ctrl Pts',(1.18351469246117,-0.940972047829285,
3.38497043141703));
#414102=CARTESIAN_POINT('Ctrl Pts',(0.907270262029569,-1.21045797416603,
3.36419389488503));
#414103=CARTESIAN_POINT('Ctrl Pts',(0.741669889100236,-1.31843428196421,
3.35322710134436));
#414104=CARTESIAN_POINT('Ctrl Pts',(0.375529554756225,-1.46578458593757,
3.33151810229555));
#414105=CARTESIAN_POINT('Ctrl Pts',(0.178174599457163,-1.50258046483778,
3.32114410899197));
#414106=CARTESIAN_POINT('Ctrl Pts',(-0.211361302901406,-1.49724634791122,
3.30225438423687));
#414107=CARTESIAN_POINT('Ctrl Pts',(-0.399910321477038,-1.45824144824317,
3.29209934591581));
#414108=CARTESIAN_POINT('Ctrl Pts',(-0.75906562043593,-1.30885629638807,
3.27066989098638));
#414109=CARTESIAN_POINT('Ctrl Pts',(-0.925190190968117,-1.19721116860686,
3.25957596531059));
#414110=CARTESIAN_POINT('Ctrl Pts',(-1.20171588727651,-0.918512169742024,
3.23852997768644));
#414111=CARTESIAN_POINT('Ctrl Pts',(-1.31048317138742,-0.755257014255049,
3.22945872301403));
#414112=CARTESIAN_POINT('Ctrl Pts',(-1.45919026539019,-0.397526930631808,
3.20958482947941));
#414113=CARTESIAN_POINT('Ctrl Pts',(-1.49817895313977,-0.206657980265481,
3.1989809989035));
#414114=CARTESIAN_POINT('Ctrl Pts',(-1.50176649068865,0.187001885967594,
3.177111006335));
#414115=CARTESIAN_POINT('Ctrl Pts',(-1.46330637831753,0.386036190213434,
3.16605354498801));
#414116=CARTESIAN_POINT('Ctrl Pts',(-1.31424750513171,0.74767468120116,
3.14596251771092));
#414117=CARTESIAN_POINT('Ctrl Pts',(-1.20883176095049,0.908292547458259,
3.13709626334183));
#414118=CARTESIAN_POINT('Ctrl Pts',(-0.940116049528959,1.18504136043139,
3.11648020562108));
#414119=CARTESIAN_POINT('Ctrl Pts',(-0.778011313664844,1.29724039855353,
3.10556429793257));
#414120=CARTESIAN_POINT('Ctrl Pts',(-0.416757278153209,1.45458446347175,
3.08381278657525));
#414121=CARTESIAN_POINT('Ctrl Pts',(-0.220537971993564,1.49696084199159,
3.07319505918041));
#414122=CARTESIAN_POINT('Ctrl Pts',(-0.0144919151713928,1.4999475112981,
3.06319870061314));
#414123=CARTESIAN_POINT('Ctrl Pts',(-0.00724491145173278,1.50000000000006,
3.06284857096474));
#414124=CARTESIAN_POINT('Ctrl Pts',(0.,1.50000000000006,3.0625));
#414125=CARTESIAN_POINT('Ctrl Pts',(-2.98372437868011E-15,1.50000000000006,
3.00000000000002));
#414126=CARTESIAN_POINT('Ctrl Pts',(-0.188455291586078,1.50000000000006,
3.00906705944397));
#414127=CARTESIAN_POINT('Ctrl Pts',(-0.375366776561344,1.46448662492846,
3.01904632509861));
#414128=CARTESIAN_POINT('Ctrl Pts',(-0.733157320802567,1.32320528790295,
3.04018501226858));
#414129=CARTESIAN_POINT('Ctrl Pts',(-0.899553263327317,1.21622363549137,
3.05116245335296));
#414130=CARTESIAN_POINT('Ctrl Pts',(-1.1775370644247,0.948431228996448,
3.07197563317732));
#414131=CARTESIAN_POINT('Ctrl Pts',(-1.28807755391854,0.791807805127463,
3.08101067749294));
#414132=CARTESIAN_POINT('Ctrl Pts',(-1.44849369979861,0.437524057649878,
3.10069310790836));
#414133=CARTESIAN_POINT('Ctrl Pts',(-1.49367236884049,0.241835556225419,
3.11156469132083));
#414134=CARTESIAN_POINT('Ctrl Pts',(-1.50494300158585,-0.15055365529281,
3.13336409196073));
#414135=CARTESIAN_POINT('Ctrl Pts',(-1.47294822231951,-0.343448461845158,
3.14408047010253));
#414136=CARTESIAN_POINT('Ctrl Pts',(-1.33770341904721,-0.705474016485607,
3.16419300091589));
#414137=CARTESIAN_POINT('Ctrl Pts',(-1.23611227524098,-0.871305075546333,
3.17306377252695));
#414138=CARTESIAN_POINT('Ctrl Pts',(-0.971454761532004,-1.16011981675612,
3.19381974479247));
#414139=CARTESIAN_POINT('Ctrl Pts',(-0.809153893177124,-1.27861751448815,
3.20492005167678));
#414140=CARTESIAN_POINT('Ctrl Pts',(-0.454620812975482,-1.44221503163789,
3.22652190792741));
#414141=CARTESIAN_POINT('Ctrl Pts',(-0.266968976146824,-1.48842649888177,
3.23683396300421));
#414142=CARTESIAN_POINT('Ctrl Pts',(0.123342579191924,-1.50814342958972,
3.25616052898576));
#414143=CARTESIAN_POINT('Ctrl Pts',(0.322410969801838,-1.47844242014425,
3.26611082667975));
#414144=CARTESIAN_POINT('Ctrl Pts',(0.694687026706395,-1.34388282867076,
3.28775973324846));
#414145=CARTESIAN_POINT('Ctrl Pts',(0.86457198998191,-1.24142178853681,
3.29877946735871));
#414146=CARTESIAN_POINT('Ctrl Pts',(1.15031108047358,-0.981254372061885,
3.31975396843968));
#414147=CARTESIAN_POINT('Ctrl Pts',(1.26516247843284,-0.827900610361255,
3.32900552164662));
#414148=CARTESIAN_POINT('Ctrl Pts',(1.43549475582945,-0.478442146227225,
3.34841988076518));
#414149=CARTESIAN_POINT('Ctrl Pts',(1.48620129994845,-0.284140467929323,
3.35921441844839));
#414150=CARTESIAN_POINT('Ctrl Pts',(1.50864280780171,0.10827164962177,3.38101509164567));
#414151=CARTESIAN_POINT('Ctrl Pts',(1.48196418538353,0.302521670583031,
3.39180675947686));
#414152=CARTESIAN_POINT('Ctrl Pts',(1.35682312299937,0.667680854124861,
3.41209338078474));
#414153=CARTESIAN_POINT('Ctrl Pts',(1.26047230423381,0.835449643206916,
3.42089576585393));
#414154=CARTESIAN_POINT('Ctrl Pts',(1.00465686502723,1.13159161946978,3.44142985791863));
#414155=CARTESIAN_POINT('Ctrl Pts',(0.845354804113819,1.25506895416932,
3.45252420786174));
#414156=CARTESIAN_POINT('Ctrl Pts',(0.494587291621475,1.42907193518553,
3.47423393381445));
#414157=CARTESIAN_POINT('Ctrl Pts',(0.307773091644003,1.48059404892646,
3.4846532060277));
#414158=CARTESIAN_POINT('Ctrl Pts',(0.07754992579976,1.49849817898652,3.49622716020497));
#414159=CARTESIAN_POINT('Ctrl Pts',(0.0387540406423458,1.50000000000006,
3.49813544535027));
#414160=CARTESIAN_POINT('Ctrl Pts',(2.54638793255616E-13,1.50000000000006,
3.50000000000001));
#414161=CARTESIAN_POINT('Origin',(0.,2.54061283442571E-15,-14.));
#414162=CARTESIAN_POINT('Origin',(0.,2.54061283442571E-15,-14.));
#414163=CARTESIAN_POINT('Ctrl Pts',(-0.823407874165269,-0.838564036615697,
-14.));
#414164=CARTESIAN_POINT('Ctrl Pts',(-0.756416185228378,-0.929775963188785,
-13.9818543033194));
#414165=CARTESIAN_POINT('Ctrl Pts',(-0.676968561320634,-1.01110546462205,
-13.9635779264192));
#414166=CARTESIAN_POINT('Ctrl Pts',(-0.493123550224768,-1.15288970360126,
-13.9268301874654));
#414167=CARTESIAN_POINT('Ctrl Pts',(-0.388650102107146,-1.21130894798347,
-13.9085879752964));
#414168=CARTESIAN_POINT('Ctrl Pts',(-0.0867303172682547,-1.32599918452642,
-13.8617929132792));
#414169=CARTESIAN_POINT('Ctrl Pts',(0.0922000261171598,-1.33900590687874,
-13.8403605160919));
#414170=CARTESIAN_POINT('Ctrl Pts',(0.415180403822383,-1.32700291925115,
-13.7965652989098));
#414171=CARTESIAN_POINT('Ctrl Pts',(0.594058047496376,-1.2850341936251,
-13.7710785130787));
#414172=CARTESIAN_POINT('Ctrl Pts',(0.927045689042117,-1.1348132370896,
-13.7211832277058));
#414173=CARTESIAN_POINT('Ctrl Pts',(1.07787156833995,-1.02758606827755,
-13.6972272991397));
#414174=CARTESIAN_POINT('Ctrl Pts',(1.20419349529485,-0.894381364905194,
-13.6752404735808));
#414175=CARTESIAN_POINT('Ctrl Pts',(0.2433378840056,-1.48013062741362,-13.6752404735808));
#414176=CARTESIAN_POINT('Ctrl Pts',(0.0878351636314239,-1.50046100868921,
-13.6804058622075));
#414177=CARTESIAN_POINT('Ctrl Pts',(-0.113668939415186,-1.50249934332334,
-13.6862245455364));
#414178=CARTESIAN_POINT('Ctrl Pts',(-0.508346872926709,-1.39607161064129,
-13.7001701627267));
#414179=CARTESIAN_POINT('Ctrl Pts',(-0.670210107973824,-1.31887778576118,
-13.7065578661612));
#414180=CARTESIAN_POINT('Ctrl Pts',(-0.960585995374814,-1.10865683103123,
-13.7194722663245));
#414181=CARTESIAN_POINT('Ctrl Pts',(-1.08605380403871,-0.976577419570047,
-13.7258892843333));
#414182=CARTESIAN_POINT('Ctrl Pts',(-1.28730702605004,-0.666237733335184,
-13.738138899672));
#414183=CARTESIAN_POINT('Ctrl Pts',(-1.35775902821766,-0.490214386563022,
-13.7441298583672));
#414184=CARTESIAN_POINT('Ctrl Pts',(-1.42412756405518,-0.123231367734631,
-13.7576357071516));
#414185=CARTESIAN_POINT('Ctrl Pts',(-1.42122151653519,0.062238330299575,
-13.764557557877));
#414186=CARTESIAN_POINT('Ctrl Pts',(-1.34076312397572,0.439251787203608,
-13.7788380930996));
#414187=CARTESIAN_POINT('Ctrl Pts',(-1.26392881942988,0.592902262433157,
-13.7847532065818));
#414188=CARTESIAN_POINT('Ctrl Pts',(-1.10178307552258,0.850803513425684,
-13.7948280321824));
#414189=CARTESIAN_POINT('Ctrl Pts',(-0.97694301654997,0.982455774393795,
-13.8014111507482));
#414190=CARTESIAN_POINT('Ctrl Pts',(-0.687878136749956,1.18635983250677,
-13.814959411892));
#414191=CARTESIAN_POINT('Ctrl Pts',(-0.527665126931193,1.25844424723993,
-13.8217821937768));
#414192=CARTESIAN_POINT('Ctrl Pts',(-0.246854066918538,1.32456649908357,
-13.8327263387908));
#414193=CARTESIAN_POINT('Ctrl Pts',(-0.126033019444995,1.33805763116345,
-13.8371828424174));
#414194=CARTESIAN_POINT('Ctrl Pts',(2.82071241364257E-12,1.33373412263468,
-13.8415063509462));
#414195=CARTESIAN_POINT('Origin',(0.,2.12729453971344E-15,10.875));
#414196=CARTESIAN_POINT('',(-1.99005104861452E-16,1.62500000000006,11.));
#414197=CARTESIAN_POINT('Origin',(0.,2.1119864547241E-15,11.));
#414198=CARTESIAN_POINT('',(-1.8369701987211E-16,1.50000000000006,10.875));
#414199=CARTESIAN_POINT('Origin',(0.,-1.19311743680736E-13,1002.5));
#414200=CARTESIAN_POINT('Ctrl Pts',(5.31356209032552E-12,1.22263611415557,
3.72263611415548));
#414201=CARTESIAN_POINT('Ctrl Pts',(-0.115140231501621,1.22694486240484,
3.72694486240474));
#414202=CARTESIAN_POINT('Ctrl Pts',(-0.223387617715824,1.21491489606931,
3.73130199756615));
#414203=CARTESIAN_POINT('Ctrl Pts',(-0.477646668670485,1.15783281542956,
3.7420580001785));
#414204=CARTESIAN_POINT('Ctrl Pts',(-0.626800140389253,1.09224861512651,
3.74894844269113));
#414205=CARTESIAN_POINT('Ctrl Pts',(-0.883097504433533,0.913997938980513,
3.76196824108044));
#414206=CARTESIAN_POINT('Ctrl Pts',(-0.990260824443083,0.806192221606663,
3.76801225902082));
#414207=CARTESIAN_POINT('Ctrl Pts',(-1.1594027114994,0.559881561084235,
3.77898658930956));
#414208=CARTESIAN_POINT('Ctrl Pts',(-1.23589039363347,0.402018119962777,
3.78540611680621));
#414209=CARTESIAN_POINT('Ctrl Pts',(-1.30922461006992,0.052236834727649,
3.79979386655726));
#414210=CARTESIAN_POINT('Ctrl Pts',(-1.31196909528878,-0.114702199266043,
3.80655334440203));
#414211=CARTESIAN_POINT('Ctrl Pts',(-1.25359061453279,-0.447247862144007,
3.81982054016495));
#414212=CARTESIAN_POINT('Ctrl Pts',(-1.19080632970482,-0.607717569079429,
3.82575565648249));
#414213=CARTESIAN_POINT('Ctrl Pts',(-1.0090355403278,-0.894191254356796,
3.83788884476785));
#414214=CARTESIAN_POINT('Ctrl Pts',(-0.894427795580347,-1.01729807198153,
3.84429372566382));
#414215=CARTESIAN_POINT('Ctrl Pts',(-0.615801045481274,-1.22339207350308,
3.85780068559773));
#414216=CARTESIAN_POINT('Ctrl Pts',(-0.451389920483652,-1.30044995450671,
3.86478375140228));
#414217=CARTESIAN_POINT('Ctrl Pts',(-0.0544533398554264,-1.39747377486497,
3.87971469241723));
#414218=CARTESIAN_POINT('Ctrl Pts',(0.137352170431063,-1.3850270031156,
3.88569345776851));
#414219=CARTESIAN_POINT('Ctrl Pts',(0.441490712532983,-1.33694519343306,
3.89675172792063));
#414220=CARTESIAN_POINT('Ctrl Pts',(0.609869556531502,-1.27636341835511,
3.90343513599766));
#414221=CARTESIAN_POINT('Ctrl Pts',(0.922667308153377,-1.09142050062308,
3.91702496349085));
#414222=CARTESIAN_POINT('Ctrl Pts',(1.06243642188326,-0.965913476410583,
3.92379303130526));
#414223=CARTESIAN_POINT('Ctrl Pts',(1.28233086394066,-0.671442131958786,
3.93607517114796));
#414224=CARTESIAN_POINT('Ctrl Pts',(1.36257154856445,-0.505299200941526,
3.94189107383887));
#414225=CARTESIAN_POINT('Ctrl Pts',(1.4594463320603,-0.149070381108668,
3.95499431856923));
#414226=CARTESIAN_POINT('Ctrl Pts',(1.4732980264083,0.0398859931747112,
3.96184849000785));
#414227=CARTESIAN_POINT('Ctrl Pts',(1.43253582146537,0.380306004358064,
3.97402788695104));
#414228=CARTESIAN_POINT('Ctrl Pts',(1.38965366882792,0.53041702884642,3.97933564957226));
#414229=CARTESIAN_POINT('Ctrl Pts',(1.25552926384395,0.817304591643929,
3.98938551561423));
#414230=CARTESIAN_POINT('Ctrl Pts',(1.16283360252483,0.952666431224754,
3.99446704079842));
#414231=CARTESIAN_POINT('Ctrl Pts',(1.05094390383308,1.07028823734367,4.));
#414232=CARTESIAN_POINT('Origin',(0.,2.35813972515597E-15,12.5));
#414233=CARTESIAN_POINT('',(0.,2.35813972515597E-15,11.778312163513));
#414234=CARTESIAN_POINT('',(-1.25,2.35813972515597E-15,12.5));
#414235=CARTESIAN_POINT('',(-1.25,2.20505887526255E-15,12.5));
#414236=CARTESIAN_POINT('',(-0.624999999999998,-1.08253175473054,12.5));
#414237=CARTESIAN_POINT('Origin',(0.,2.35813972515597E-15,12.5));
#414238=CARTESIAN_POINT('',(0.624999999999998,-1.08253175473054,12.5));
#414239=CARTESIAN_POINT('Origin',(0.,2.35813972515597E-15,12.5));
#414240=CARTESIAN_POINT('',(1.25,1.79477175062954E-15,12.5));
#414241=CARTESIAN_POINT('Origin',(0.,2.35813972515597E-15,12.5));
#414242=CARTESIAN_POINT('',(0.624999999999999,1.08253175473055,12.5));
#414243=CARTESIAN_POINT('Origin',(0.,2.35813972515597E-15,12.5));
#414244=CARTESIAN_POINT('',(-0.624999999999998,1.08253175473055,12.5));
#414245=CARTESIAN_POINT('Origin',(0.,2.35813972515597E-15,12.5));
#414246=CARTESIAN_POINT('Origin',(0.,2.35813972515597E-15,12.5));
#414247=CARTESIAN_POINT('Origin',(0.,-1.34815096107107E-30,14.));
#414248=CARTESIAN_POINT('',(1.25,0.721687836487035,14.));
#414249=CARTESIAN_POINT('',(1.25,-0.721687836487022,14.));
#414250=CARTESIAN_POINT('Ctrl Pts',(1.25,0.721687836487029,14.));
#414251=CARTESIAN_POINT('Ctrl Pts',(1.25,3.60822483003176E-15,13.6391560817565));
#414252=CARTESIAN_POINT('Ctrl Pts',(1.25,-0.721687836487019,14.));
#414253=CARTESIAN_POINT('Origin',(0.,-1.34815096107107E-30,14.));
#414254=CARTESIAN_POINT('Origin',(0.,2.60208521396521E-15,11.088));
#414255=CARTESIAN_POINT('',(-3.12992118721911E-16,2.55577460325564,11.0257746032556));
#414256=CARTESIAN_POINT('Origin',(0.,2.5406128344257E-15,11.0257746032556));
#414257=CARTESIAN_POINT('',(-3.05371705427039E-16,2.49354920651122,11.));
#414258=CARTESIAN_POINT('Origin',(-3.05371705427039E-16,2.49354920651122,
11.088));
#414259=CARTESIAN_POINT('Origin',(0.,2.5406128344257E-15,11.));
#414260=CARTESIAN_POINT('Origin',(0.,2.5406128344257E-15,11.0257746032556));
#414261=CARTESIAN_POINT('',(-3.33621391227899E-16,2.72422539674443,11.1942253967444));
#414262=CARTESIAN_POINT('Origin',(0.,2.5406128344257E-15,11.1942253967444));
#414263=CARTESIAN_POINT('',(-3.12992118721911E-16,2.55577460325564,11.0257746032556));
#414264=CARTESIAN_POINT('Origin',(0.,2.60208521396521E-15,11.2564507934888));
#414265=CARTESIAN_POINT('',(-3.36777869765522E-16,2.75,11.2564507934888));
#414266=CARTESIAN_POINT('Origin',(0.,2.5406128344257E-15,11.2564507934888));
#414267=CARTESIAN_POINT('Origin',(-3.26000977933025E-16,2.662,11.2564507934888));
#414268=CARTESIAN_POINT('Origin',(0.,2.5406128344257E-15,13.8057746032556));
#414269=CARTESIAN_POINT('',(3.7272661817839E-12,2.65571825406948,13.8742817459305));
#414270=CARTESIAN_POINT('',(-0.0523410482444132,2.69040761867485,13.8390832900376));
#414271=CARTESIAN_POINT('Ctrl Pts',(3.72682759446776E-12,2.65571825406948,
13.8742817459305));
#414272=CARTESIAN_POINT('Ctrl Pts',(-0.000866695601887436,2.65571825406942,
13.8742817459306));
#414273=CARTESIAN_POINT('Ctrl Pts',(-0.00173384839344961,2.65573803419417,
13.8742615387396));
#414274=CARTESIAN_POINT('Ctrl Pts',(-0.00259288537059199,2.65577720866165,
13.8742215255972));
#414275=CARTESIAN_POINT('Ctrl Pts',(-0.00713269347825356,2.65598423649613,
13.8740100655633));
#414276=CARTESIAN_POINT('Ctrl Pts',(-0.0116665345428952,2.65675308215573,
13.8732246156103));
#414277=CARTESIAN_POINT('Ctrl Pts',(-0.0158696469572718,2.65797057625734,
13.8719820486038));
#414278=CARTESIAN_POINT('Ctrl Pts',(-0.0201451887618009,2.6592090506104,
13.8707180692815));
#414279=CARTESIAN_POINT('Ctrl Pts',(-0.0241780317224058,2.66093171307035,
13.868960862563));
#414280=CARTESIAN_POINT('Ctrl Pts',(-0.0277864605543921,2.66294927630088,
13.8669057591701));
#414281=CARTESIAN_POINT('Ctrl Pts',(-0.033342610859648,2.66605585954836,
13.8637413727084));
#414282=CARTESIAN_POINT('Ctrl Pts',(-0.038077514536549,2.66993490073839,
13.8597962563956));
#414283=CARTESIAN_POINT('Ctrl Pts',(-0.041917102398969,2.6741245431149,
13.855546950204));
#414284=CARTESIAN_POINT('Ctrl Pts',(-0.0464962509255301,2.6791211717643,
13.850479165618));
#414285=CARTESIAN_POINT('Ctrl Pts',(-0.0499450320083385,2.68468912462994,
13.8448473071436));
#414286=CARTESIAN_POINT('Ctrl Pts',(-0.0523410482444142,2.69040761867485,
13.8390832900376));
#414287=CARTESIAN_POINT('',(-0.0661728417005766,2.72342159191127,13.8057746032556));
#414288=CARTESIAN_POINT('',(-0.0523410482444132,2.69040761867485,13.8390832900376));
#414289=CARTESIAN_POINT('',(-0.156031485724598,2.71975333214794,13.8057746032556));
#414290=CARTESIAN_POINT('Origin',(0.,2.5406128344257E-15,13.8057746032556));
#414291=CARTESIAN_POINT('',(-0.167126309723535,2.68572179060922,13.8390832900376));
#414292=CARTESIAN_POINT('',(-0.156031485724598,2.71975333214794,13.8057746032556));
#414293=CARTESIAN_POINT('',(-0.27146008517196,2.67718922792421,13.8390832900376));
#414294=CARTESIAN_POINT('Ctrl Pts',(-0.167126309723536,2.68572179060922,
13.8390832900376));
#414295=CARTESIAN_POINT('Ctrl Pts',(-0.169287253635042,2.67909395725023,
13.8455641171218));
#414296=CARTESIAN_POINT('Ctrl Pts',(-0.172798832469115,2.67252844642108,
13.851896480191));
#414297=CARTESIAN_POINT('Ctrl Pts',(-0.17782767861645,2.66662913816789,
13.8574481026913));
#414298=CARTESIAN_POINT('Ctrl Pts',(-0.181226763520718,2.6626416927298,
13.8612005412592));
#414299=CARTESIAN_POINT('Ctrl Pts',(-0.185412613168551,2.6588765980049,
13.8646714234115));
#414300=CARTESIAN_POINT('Ctrl Pts',(-0.190316524340427,2.65572590449234,
13.8674635290331));
#414301=CARTESIAN_POINT('Ctrl Pts',(-0.194268697023493,2.65318668948689,
13.8697137499649));
#414302=CARTESIAN_POINT('Ctrl Pts',(-0.198787314993229,2.65099882204377,
13.8715630732995));
#414303=CARTESIAN_POINT('Ctrl Pts',(-0.203607653128417,2.64944501921187,
13.8727429581918));
#414304=CARTESIAN_POINT('Ctrl Pts',(-0.208483548820085,2.64787330778389,
13.873936442031));
#414305=CARTESIAN_POINT('Ctrl Pts',(-0.213819966241819,2.64691770663781,
13.8744652622107));
#414306=CARTESIAN_POINT('Ctrl Pts',(-0.219073920661324,2.64672829398743,
13.8742206332401));
#414307=CARTESIAN_POINT('Ctrl Pts',(-0.223596332596698,2.64656525450091,
13.8740100655633));
#414308=CARTESIAN_POINT('Ctrl Pts',(-0.228177755399591,2.64696202456949,
13.8732246156103));
#414309=CARTESIAN_POINT('Ctrl Pts',(-0.232466119376086,2.64783287487835,
13.8719820486038));
#414310=CARTESIAN_POINT('Ctrl Pts',(-0.236828381825177,2.6487187319609,
13.8707180692815));
#414311=CARTESIAN_POINT('Ctrl Pts',(-0.24098821881642,2.65010694826325,
13.868960862563));
#414312=CARTESIAN_POINT('Ctrl Pts',(-0.244749091032574,2.65182367776974,
13.8669057591701));
#414313=CARTESIAN_POINT('Ctrl Pts',(-0.25053996908082,2.65446704628708,
13.8637413727084));
#414314=CARTESIAN_POINT('Ctrl Pts',(-0.255575295624587,2.65794724168118,
13.8597962563956));
#414315=CARTESIAN_POINT('Ctrl Pts',(-0.259743602323567,2.66180998131253,
13.855546950204));
#414316=CARTESIAN_POINT('Ctrl Pts',(-0.264714785732522,2.66641674097663,
13.850479165618));
#414317=CARTESIAN_POINT('Ctrl Pts',(-0.268605931129685,2.67168505926326,
13.8448473071436));
#414318=CARTESIAN_POINT('Ctrl Pts',(-0.27146008517196,2.67718922792421,
13.8390832900376));
#414319=CARTESIAN_POINT('',(-0.287936799781984,2.70896593031337,13.8057746032556));
#414320=CARTESIAN_POINT('',(-0.27146008517196,2.67718922792421,13.8390832900376));
#414321=CARTESIAN_POINT('',(-0.377197449355658,2.69798556268688,13.8057746032556));
#414322=CARTESIAN_POINT('Origin',(0.,2.5406128344257E-15,13.8057746032556));
#414323=CARTESIAN_POINT('',(-0.385481469674173,2.66316292713999,13.8390832900376));
#414324=CARTESIAN_POINT('',(-0.377197449355658,2.69798556268688,13.8057746032556));
#414325=CARTESIAN_POINT('',(-0.488772600020449,2.64615458456686,13.8390832900376));
#414326=CARTESIAN_POINT('Ctrl Pts',(-0.385481469674174,2.66316292713999,
13.8390832900376));
#414327=CARTESIAN_POINT('Ctrl Pts',(-0.387094993274519,2.65638101035973,
13.8455641171218));
#414328=CARTESIAN_POINT('Ctrl Pts',(-0.390059737535903,2.64955111945136,
13.851896480191));
#414329=CARTESIAN_POINT('Ctrl Pts',(-0.394591002223392,2.64326154301319,
13.8574481026913));
#414330=CARTESIAN_POINT('Ctrl Pts',(-0.397653763132204,2.6390103084956,
13.8612005412592));
#414331=CARTESIAN_POINT('Ctrl Pts',(-0.401518794537129,2.63491655620696,
13.8646714234115));
#414332=CARTESIAN_POINT('Ctrl Pts',(-0.406149577578239,2.63137663208095,
13.8674635290331));
#414333=CARTESIAN_POINT('Ctrl Pts',(-0.409881630136867,2.62852372734011,
13.8697137499649));
#414334=CARTESIAN_POINT('Ctrl Pts',(-0.414206881270284,2.62597483053209,
13.8715630732995));
#414335=CARTESIAN_POINT('Ctrl Pts',(-0.418884530772376,2.62403329554307,
13.8727429581918));
#414336=CARTESIAN_POINT('Ctrl Pts',(-0.423616093250925,2.62206938309073,
13.873936442031));
#414337=CARTESIAN_POINT('Ctrl Pts',(-0.42885686381914,2.62068199406788,
13.8744652622107));
#414338=CARTESIAN_POINT('Ctrl Pts',(-0.434077897249308,2.62006496561196,
13.8742206332401));
#414339=CARTESIAN_POINT('Ctrl Pts',(-0.438571972000304,2.61953385006912,
13.8740100655633));
#414340=CARTESIAN_POINT('Ctrl Pts',(-0.443170490940781,2.61955587142774,
13.8732246156103));
#414341=CARTESIAN_POINT('Ctrl Pts',(-0.447515568124662,2.62007428257872,
13.8719820486038));
#414342=CARTESIAN_POINT('Ctrl Pts',(-0.451935521081438,2.62060162715804,
13.8707180692815));
#414343=CARTESIAN_POINT('Ctrl Pts',(-0.456194669074472,2.62164615895233,
13.868960862563));
#414344=CARTESIAN_POINT('Ctrl Pts',(-0.460082956690694,2.62305063018316,
13.8669057591701));
#414345=CARTESIAN_POINT('Ctrl Pts',(-0.466070025143948,2.62521319278899,
13.8637413727084));
#414346=CARTESIAN_POINT('Ctrl Pts',(-0.4713722652872,2.62827138226101,13.8597962563956));
#414347=CARTESIAN_POINT('Ctrl Pts',(-0.47584155142938,2.63178151325225,
13.855546950204));
#414348=CARTESIAN_POINT('Ctrl Pts',(-0.48117168731533,2.63596774670555,
13.850479165618));
#414349=CARTESIAN_POINT('Ctrl Pts',(-0.485479302096222,2.6409013706242,
13.8448473071436));
#414350=CARTESIAN_POINT('Ctrl Pts',(-0.488772600020449,2.64615458456686,
13.8390832900376));
#414351=CARTESIAN_POINT('',(-0.50778458596707,2.67648254739715,13.8057746032556));
#414352=CARTESIAN_POINT('',(-0.488772600020449,2.64615458456686,13.8390832900376));
#414353=CARTESIAN_POINT('',(-0.595853226194454,2.65826314444243,13.8057746032556));
#414354=CARTESIAN_POINT('Origin',(0.,2.5406128344257E-15,13.8057746032556));
#414355=CARTESIAN_POINT('',(-0.601271314044095,2.62288115378159,13.8390832900376));
#414356=CARTESIAN_POINT('',(-0.595853226194454,2.65826314444243,13.8057746032556));
#414357=CARTESIAN_POINT('',(-0.702832413857604,2.597510219034,13.8390832900376));
#414358=CARTESIAN_POINT('Ctrl Pts',(-0.601271314044095,2.62288115378159,
13.8390832900376));
#414359=CARTESIAN_POINT('Ctrl Pts',(-0.602326679599933,2.61599028611731,
13.8455641171218));
#414360=CARTESIAN_POINT('Ctrl Pts',(-0.604724859404717,2.60894146692686,
13.851896480191));
#414361=CARTESIAN_POINT('Ctrl Pts',(-0.608728387813473,2.6023034783972,
13.8574481026913));
#414362=CARTESIAN_POINT('Ctrl Pts',(-0.611434442558301,2.5978167460644,
13.8612005412592));
#414363=CARTESIAN_POINT('Ctrl Pts',(-0.614952934574,2.5934215794581,13.8646714234115));
#414364=CARTESIAN_POINT('Ctrl Pts',(-0.619279772387232,2.58951598232965,
13.8674635290331));
#414365=CARTESIAN_POINT('Ctrl Pts',(-0.62276686862739,2.58636837346377,
13.8697137499649));
#414366=CARTESIAN_POINT('Ctrl Pts',(-0.626869969091811,2.58347540977857,
13.8715630732995));
#414367=CARTESIAN_POINT('Ctrl Pts',(-0.631373800975127,2.58115906322746,
13.8727429581918));
#414368=CARTESIAN_POINT('Ctrl Pts',(-0.635929542472916,2.57881601926411,
13.873936442031));
#414369=CARTESIAN_POINT('Ctrl Pts',(-0.641039789724145,2.57700607520953,
13.8744652622107));
#414370=CARTESIAN_POINT('Ctrl Pts',(-0.646193157048908,2.57596553717062,
13.8742206332401));
#414371=CARTESIAN_POINT('Ctrl Pts',(-0.650628987289528,2.57506988005778,
13.8740100655633));
#414372=CARTESIAN_POINT('Ctrl Pts',(-0.655213999982748,2.57471700615793,
13.8732246156103));
#414373=CARTESIAN_POINT('Ctrl Pts',(-0.659586874602242,2.57487952821036,
13.8719820486038));
#414374=CARTESIAN_POINT('Ctrl Pts',(-0.664035104009018,2.57504485089527,
13.8707180692815));
#414375=CARTESIAN_POINT('Ctrl Pts',(-0.668365219076652,2.57573874699475,
13.868960862563));
#414376=CARTESIAN_POINT('Ctrl Pts',(-0.67235504618038,2.5768216134256,13.8669057591701));
#414377=CARTESIAN_POINT('Ctrl Pts',(-0.678498462085881,2.57848897862259,
13.8637413727084));
#414378=CARTESIAN_POINT('Ctrl Pts',(-0.684032330295278,2.58110481042614,
13.8597962563956));
#414379=CARTESIAN_POINT('Ctrl Pts',(-0.688772853518762,2.58423897343466,
13.855546950204));
#414380=CARTESIAN_POINT('Ctrl Pts',(-0.694426470706797,2.58797682198422,
13.850479165618));
#414381=CARTESIAN_POINT('Ctrl Pts',(-0.699121888405755,2.59254291908168,
13.8448473071436));
#414382=CARTESIAN_POINT('Ctrl Pts',(-0.702832413857603,2.597510219034,13.8390832900376));
#414383=CARTESIAN_POINT('',(-0.724253149511105,2.62618761471653,13.8057746032556));
#414384=CARTESIAN_POINT('',(-0.702832413857604,2.597510219034,13.8390832900376));
#414385=CARTESIAN_POINT('',(-0.810543698121789,2.60085042355425,13.8057746032556));
#414386=CARTESIAN_POINT('Origin',(0.,2.5406128344257E-15,13.8057746032556));
#414387=CARTESIAN_POINT('',(-0.813059797021838,2.56514453908971,13.8390832900376));
#414388=CARTESIAN_POINT('',(-0.810543698121789,2.60085042355425,13.8057746032556));
#414389=CARTESIAN_POINT('',(-0.912214993939723,2.53157985155249,13.8390832900376));
#414390=CARTESIAN_POINT('Ctrl Pts',(-0.813059797021838,2.56514453908971,
13.8390832900376));
#414391=CARTESIAN_POINT('Ctrl Pts',(-0.813549981249516,2.55819057812879,
13.8455641171218));
#414392=CARTESIAN_POINT('Ctrl Pts',(-0.81536563710677,2.55096973938501,
13.851896480191));
#414393=CARTESIAN_POINT('Ctrl Pts',(-0.818814786415766,2.54402751348232,
13.8574481026913));
#414394=CARTESIAN_POINT('Ctrl Pts',(-0.821146126648752,2.53933514179775,
13.8612005412592));
#414395=CARTESIAN_POINT('Ctrl Pts',(-0.824294664291374,2.53466780998238,
13.8646714234115));
#414396=CARTESIAN_POINT('Ctrl Pts',(-0.828288762484958,2.53042253095601,
13.8674635290331));
#414397=CARTESIAN_POINT('Ctrl Pts',(-0.831507696356497,2.52700116478278,
13.8697137499649));
#414398=CARTESIAN_POINT('Ctrl Pts',(-0.835361340695299,2.5237833864164,
13.8715630732995));
#414399=CARTESIAN_POINT('Ctrl Pts',(-0.839661382701735,2.52110764320733,
13.8727429581918));
#414400=CARTESIAN_POINT('Ctrl Pts',(-0.844010985510741,2.51840106030397,
13.873936442031));
#414401=CARTESIAN_POINT('Ctrl Pts',(-0.848956701592656,2.51618060609673,
13.8744652622107));
#414402=CARTESIAN_POINT('Ctrl Pts',(-0.854008108002714,2.51472348308381,
13.8742206332401));
#414403=CARTESIAN_POINT('Ctrl Pts',(-0.858356174014567,2.51346924485128,
13.8740100655633));
#414404=CARTESIAN_POINT('Ctrl Pts',(-0.862897167957527,2.51274382401054,
13.8732246156103));
#414405=CARTESIAN_POINT('Ctrl Pts',(-0.867268739253517,2.51254937540697,
13.8719820486038));
#414406=CARTESIAN_POINT('Ctrl Pts',(-0.871715642877495,2.51235157600229,
13.8707180692815));
#414407=CARTESIAN_POINT('Ctrl Pts',(-0.876087908818377,2.5126902186429,
13.868960862563));
#414408=CARTESIAN_POINT('Ctrl Pts',(-0.880152723768509,2.51344427397633,
13.8669057591701));
#414409=CARTESIAN_POINT('Ctrl Pts',(-0.886411603706999,2.51460534572418,
13.8637413727084));
#414410=CARTESIAN_POINT('Ctrl Pts',(-0.892140273002629,2.51676141193022,
13.8597962563956));
#414411=CARTESIAN_POINT('Ctrl Pts',(-0.897120485907497,2.51949874961829,
13.855546950204));
#414412=CARTESIAN_POINT('Ctrl Pts',(-0.903059960508011,2.5227633384987,
13.850479165618));
#414413=CARTESIAN_POINT('Ctrl Pts',(-0.908111933894941,2.52693152215215,
13.8448473071436));
#414414=CARTESIAN_POINT('Ctrl Pts',(-0.912214993939722,2.53157985155249,
13.8390832900376));
#414415=CARTESIAN_POINT('',(-0.935901927838502,2.55841583675044,13.8057746032556));
#414416=CARTESIAN_POINT('',(-0.912214993939723,2.53157985155249,13.8390832900376));
#414417=CARTESIAN_POINT('',(-1.01984013546842,2.52612947220744,13.8057746032556));
#414418=CARTESIAN_POINT('Origin',(0.,2.5406128344257E-15,13.8057746032556));
#414419=CARTESIAN_POINT('',(-1.01943750119583,2.49033731070925,13.8390832900376));
#414420=CARTESIAN_POINT('',(-1.01984013546842,2.52612947220744,13.8057746032556));
#414421=CARTESIAN_POINT('',(-1.11552693374205,2.44880223784017,13.8390832900376));
#414422=CARTESIAN_POINT('Ctrl Pts',(-1.01943750119582,2.49033731070925,
13.8390832900376));
#414423=CARTESIAN_POINT('Ctrl Pts',(-1.01935924200018,2.48336653391456,
13.8455641171218));
#414424=CARTESIAN_POINT('Ctrl Pts',(-1.02058029101974,2.47602172910793,
13.851896480191));
#414425=CARTESIAN_POINT('Ctrl Pts',(-1.02345210770939,2.46882146520022,
13.8574481026913));
#414426=CARTESIAN_POINT('Ctrl Pts',(-1.02539321874593,2.46395468112323,
13.8612005412592));
#414427=CARTESIAN_POINT('Ctrl Pts',(-1.02815084901694,2.45904624442198,
13.8646714234115));
#414428=CARTESIAN_POINT('Ctrl Pts',(-1.03178562752637,2.45448953512919,
13.8674635290331));
#414429=CARTESIAN_POINT('Ctrl Pts',(-1.03471497755547,2.450817180276,13.8697137499649));
#414430=CARTESIAN_POINT('Ctrl Pts',(-1.03829352040138,2.44729600101259,
13.8715630732995));
#414431=CARTESIAN_POINT('Ctrl Pts',(-1.04236115646084,2.44427866777515,
13.8727429581918));
#414432=CARTESIAN_POINT('Ctrl Pts',(-1.046475674692,2.44122655779444,13.873936442031));
#414433=CARTESIAN_POINT('Ctrl Pts',(-1.05122394668006,2.43861037019094,
13.8744652622107));
#414434=CARTESIAN_POINT('Ctrl Pts',(-1.05613977589918,2.43674635911725,
13.8742206332401));
#414435=CARTESIAN_POINT('Ctrl Pts',(-1.06037114202034,2.43514188651353,
13.8740100655633));
#414436=CARTESIAN_POINT('Ctrl Pts',(-1.06483789764756,2.43404874628791,
13.8732246156103));
#414437=CARTESIAN_POINT('Ctrl Pts',(-1.06917907353433,2.43349862105172,
13.8719820486038));
#414438=CARTESIAN_POINT('Ctrl Pts',(-1.07359505796558,2.43293901587984,
13.8707180692815));
#414439=CARTESIAN_POINT('Ctrl Pts',(-1.07798037807125,2.43292015145069,
13.868960862563));
#414440=CARTESIAN_POINT('Ctrl Pts',(-1.08209313019494,2.43334037757286,
13.8669057591701));
#414441=CARTESIAN_POINT('Ctrl Pts',(-1.08842582235307,2.43398742913067,
13.8637413727084));
#414442=CARTESIAN_POINT('Ctrl Pts',(-1.09431116938593,2.43566938147429,
13.8597962563956));
#414443=CARTESIAN_POINT('Ctrl Pts',(-1.09949792947698,2.43799167731123,
13.855546950204));
#414444=CARTESIAN_POINT('Ctrl Pts',(-1.10568373526645,2.44076128122212,
13.850479165618));
#414445=CARTESIAN_POINT('Ctrl Pts',(-1.11105864429198,2.44450381285705,
13.8448473071436));
#414446=CARTESIAN_POINT('Ctrl Pts',(-1.11552693374205,2.44880223784017,
13.8390832900376));
#414447=CARTESIAN_POINT('',(-1.14132243324908,2.47361822349967,13.8057746032556));
#414448=CARTESIAN_POINT('',(-1.11552693374205,2.44880223784017,13.8390832900376));
#414449=CARTESIAN_POINT('',(-1.22234970497529,2.43459754600511,13.8057746032556));
#414450=CARTESIAN_POINT('Origin',(0.,2.5406128344257E-15,13.8057746032556));
#414451=CARTESIAN_POINT('',(-1.2190310169947,2.39895729840275,13.8390832900376));
#414452=CARTESIAN_POINT('',(-1.22234970497529,2.43459754600511,13.8057746032556));
#414453=CARTESIAN_POINT('',(-1.31141522584932,2.34972824925896,13.8390832900376));
#414454=CARTESIAN_POINT('Ctrl Pts',(-1.2190310169947,2.39895729840275,13.8390832900376));
#414455=CARTESIAN_POINT('Ctrl Pts',(-1.21838483517778,2.39201609514376,
13.8455641171218));
#414456=CARTESIAN_POINT('Ctrl Pts',(-1.21900315147987,2.38459620273847,
13.851896480191));
#414457=CARTESIAN_POINT('Ctrl Pts',(-1.22127852408393,2.37718581739407,
13.8574481026913));
#414458=CARTESIAN_POINT('Ctrl Pts',(-1.22281648815033,2.37217700856975,
13.8612005412592));
#414459=CARTESIAN_POINT('Ctrl Pts',(-1.22516485947524,2.36706013181903,
13.8646714234115));
#414460=CARTESIAN_POINT('Ctrl Pts',(-1.22841612944925,2.36222231640835,
13.8674635290331));
#414461=CARTESIAN_POINT('Ctrl Pts',(-1.23103640129476,2.35832341179085,
13.8697137499649));
#414462=CARTESIAN_POINT('Ctrl Pts',(-1.23431602803556,2.35452226449745,
13.8715630732995));
#414463=CARTESIAN_POINT('Ctrl Pts',(-1.23812418870118,2.35118342108651,
13.8727429581918));
#414464=CARTESIAN_POINT('Ctrl Pts',(-1.24197624091452,2.34780609531682,
13.873936442031));
#414465=CARTESIAN_POINT('Ctrl Pts',(-1.24649546984206,2.34481158461392,
13.8744652622107));
#414466=CARTESIAN_POINT('Ctrl Pts',(-1.25124300783784,2.34255309016562,
13.8742206332401));
#414467=CARTESIAN_POINT('Ctrl Pts',(-1.25532951502489,2.34060906069116,
13.8740100655633));
#414468=CARTESIAN_POINT('Ctrl Pts',(-1.25969230681464,2.33915547574851,
13.8732246156103));
#414469=CARTESIAN_POINT('Ctrl Pts',(-1.2639741974829,2.33825333487238,13.8719820486038));
#414470=CARTESIAN_POINT('Ctrl Pts',(-1.26832987507362,2.3373356480134,13.8707180692815));
#414471=CARTESIAN_POINT('Ctrl Pts',(-1.27269906576229,2.33695940205415,
13.868960862563));
#414472=CARTESIAN_POINT('Ctrl Pts',(-1.27683238537272,2.33704300242955,
13.8669057591701));
#414473=CARTESIAN_POINT('Ctrl Pts',(-1.283196746729,2.33717172777594,13.8637413727084));
#414474=CARTESIAN_POINT('Ctrl Pts',(-1.28919960548561,2.33836837314182,
13.8597962563956));
#414475=CARTESIAN_POINT('Ctrl Pts',(-1.29455839573018,2.34026017263199,
13.855546950204));
#414476=CARTESIAN_POINT('Ctrl Pts',(-1.30094936719167,2.34251636031628,
13.850479165618));
#414477=CARTESIAN_POINT('Ctrl Pts',(-1.30661144272303,2.34580833400213,
13.8448473071436));
#414478=CARTESIAN_POINT('Ctrl Pts',(-1.31141522584932,2.34972824925896,
13.8390832900376));
#414479=CARTESIAN_POINT('',(-1.33914762617134,2.37235908908979,13.8057746032556));
#414480=CARTESIAN_POINT('',(-1.31141522584932,2.34972824925896,13.8390832900376));
#414481=CARTESIAN_POINT('',(-1.41672473886905,2.32686377481444,13.8057746032556));
#414482=CARTESIAN_POINT('Origin',(0.,2.5406128344257E-15,13.8057746032556));
#414483=CARTESIAN_POINT('',(-1.41051208250144,2.29161262107548,13.8390832900376));
#414484=CARTESIAN_POINT('',(-1.41672473886905,2.32686377481444,13.8057746032556));
#414485=CARTESIAN_POINT('',(-1.49857626599684,2.2350172068568,13.8390832900376));
#414486=CARTESIAN_POINT('Ctrl Pts',(-1.41051208250144,2.29161262107548,
13.8390832900376));
#414487=CARTESIAN_POINT('Ctrl Pts',(-1.40930227829661,2.28474718391466,
13.8455641171218));
#414488=CARTESIAN_POINT('Ctrl Pts',(-1.40931374708826,2.27730158207046,
13.851896480191));
#414489=CARTESIAN_POINT('Ctrl Pts',(-1.41097753337746,2.26973039018123,
13.8574481026913));
#414490=CARTESIAN_POINT('Ctrl Pts',(-1.4121021155766,2.2646128894059,13.8612005412592));
#414491=CARTESIAN_POINT('Ctrl Pts',(-1.41402559993171,2.25932162457625,
13.8646714234115));
#414492=CARTESIAN_POINT('Ctrl Pts',(-1.41687172470503,2.25423489791106,
13.8674635290331));
#414493=CARTESIAN_POINT('Ctrl Pts',(-1.41916548089014,2.25013539009621,
13.8697137499649));
#414494=CARTESIAN_POINT('Ctrl Pts',(-1.42212436615097,2.24607957078092,
13.8715630732995));
#414495=CARTESIAN_POINT('Ctrl Pts',(-1.42564770874183,2.2424414366485,13.8727429581918));
#414496=CARTESIAN_POINT('Ctrl Pts',(-1.4292116601654,2.23876137063561,13.873936442031));
#414497=CARTESIAN_POINT('Ctrl Pts',(-1.43347177130953,2.23540846480797,
13.8744652622107));
#414498=CARTESIAN_POINT('Ctrl Pts',(-1.4380194239999,2.23277051689298,13.8742206332401));
#414499=CARTESIAN_POINT('Ctrl Pts',(-1.44193387722174,2.2304998677432,13.8740100655633));
#414500=CARTESIAN_POINT('Ctrl Pts',(-1.44616367151446,2.22869551145149,
13.8732246156103));
#414501=CARTESIAN_POINT('Ctrl Pts',(-1.45035778168829,2.22744735853411,
13.8719820486038));
#414502=CARTESIAN_POINT('Ctrl Pts',(-1.45462416612275,2.22617769704267,
13.8707180692815));
#414503=CARTESIAN_POINT('Ctrl Pts',(-1.45894815115126,2.22544657340809,
13.868960862563));
#414504=CARTESIAN_POINT('Ctrl Pts',(-1.46307453168836,2.22519299169003,
13.8669057591701));
#414505=CARTESIAN_POINT('Ctrl Pts',(-1.46942820846801,2.22480253417906,
13.8637413727084));
#414506=CARTESIAN_POINT('Ctrl Pts',(-1.47550863091374,2.22550590908972,
13.8597962563956));
#414507=CARTESIAN_POINT('Ctrl Pts',(-1.4810037894469,2.22695462261963,13.855546950204));
#414508=CARTESIAN_POINT('Ctrl Pts',(-1.48755739571976,2.22868237952053,
13.850479165618));
#414509=CARTESIAN_POINT('Ctrl Pts',(-1.49346895757847,2.23150188771555,
13.8448473071436));
#414510=CARTESIAN_POINT('Ctrl Pts',(-1.49857626599684,2.23501720685679,
13.8390832900376));
#414511=CARTESIAN_POINT('',(-1.52806101258523,2.25531229635372,13.8057746032556));
#414512=CARTESIAN_POINT('',(-1.49857626599684,2.2350172068568,13.8390832900376));
#414513=CARTESIAN_POINT('',(-1.60167170336877,2.20364510910788,13.8057746032556));
#414514=CARTESIAN_POINT('Origin',(0.,2.5406128344257E-15,13.8057746032556));
#414515=CARTESIAN_POINT('',(-1.59260642281724,2.16901763984442,13.8390832900376));
#414516=CARTESIAN_POINT('',(-1.60167170336877,2.20364510910788,13.8057746032556));
#414517=CARTESIAN_POINT('',(-1.67576452834183,2.10543249369488,13.8390832900376));
#414518=CARTESIAN_POINT('Ctrl Pts',(-1.59260642281724,2.16901763984442,
13.8390832900376));
#414519=CARTESIAN_POINT('Ctrl Pts',(-1.59084104727189,2.16227365713336,
13.8455641171218));
#414520=CARTESIAN_POINT('Ctrl Pts',(-1.59024559223018,2.15485189510208,
13.851896480191));
#414521=CARTESIAN_POINT('Ctrl Pts',(-1.59128671998126,2.14717028170087,
13.8574481026913));
#414522=CARTESIAN_POINT('Ctrl Pts',(-1.59199043640417,2.14197814509787,
13.8612005412592));
#414523=CARTESIAN_POINT('Ctrl Pts',(-1.59347623331844,2.13654770468375,
13.8646714234115));
#414524=CARTESIAN_POINT('Ctrl Pts',(-1.59589827240028,2.13124591809075,
13.8674635290331));
#414525=CARTESIAN_POINT('Ctrl Pts',(-1.59785024835603,2.12697308862669,
13.8697137499649));
#414526=CARTESIAN_POINT('Ctrl Pts',(-1.60046870124365,2.12268958809788,
13.8715630732995));
#414527=CARTESIAN_POINT('Ctrl Pts',(-1.60368377849611,2.11877637442639,
13.8727429581918));
#414528=CARTESIAN_POINT('Ctrl Pts',(-1.60693591162122,2.11481805840244,
13.873936442031));
#414529=CARTESIAN_POINT('Ctrl Pts',(-1.61090855464514,2.11112907048516,
13.8744652622107));
#414530=CARTESIAN_POINT('Ctrl Pts',(-1.61522605815175,2.10812922421163,
13.8742206332401));
#414531=CARTESIAN_POINT('Ctrl Pts',(-1.61894240736803,2.10554706618199,
13.8740100655633));
#414532=CARTESIAN_POINT('Ctrl Pts',(-1.62301105558057,2.10340394623464,
13.8732246156103));
#414533=CARTESIAN_POINT('Ctrl Pts',(-1.62708947414873,2.10181808752774,
13.8719820486038));
#414534=CARTESIAN_POINT('Ctrl Pts',(-1.63123817334242,2.10020490079158,
13.8707180692815));
#414535=CARTESIAN_POINT('Ctrl Pts',(-1.63548817730382,2.09912376498884,
13.868960862563));
#414536=CARTESIAN_POINT('Ctrl Pts',(-1.63958015838592,2.0985346887218,13.8669057591701));
#414537=CARTESIAN_POINT('Ctrl Pts',(-1.64588086791825,2.0976276467838,13.8637413727084));
#414538=CARTESIAN_POINT('Ctrl Pts',(-1.65199838984492,2.09783307039525,
13.8597962563956));
#414539=CARTESIAN_POINT('Ctrl Pts',(-1.65759334729327,2.09882905701538,
13.855546950204));
#414540=CARTESIAN_POINT('Ctrl Pts',(-1.66426597520903,2.10001688519578,
13.850479165618));
#414541=CARTESIAN_POINT('Ctrl Pts',(-1.67038768292626,2.10234516453813,
13.8448473071436));
#414542=CARTESIAN_POINT('Ctrl Pts',(-1.67576452834183,2.10543249369488,
13.8390832900376));
#414543=CARTESIAN_POINT('',(-1.70680540507268,2.12325677238575,13.8057746032556));
#414544=CARTESIAN_POINT('',(-1.67576452834183,2.10543249369488,13.8390832900376));
#414545=CARTESIAN_POINT('',(-1.7759598069398,2.06576154877605,13.8057746032556));
#414546=CARTESIAN_POINT('Origin',(0.,2.5406128344257E-15,13.8057746032556));
#414547=CARTESIAN_POINT('',(-1.76410223015076,2.03198820408291,13.8390832900376));
#414548=CARTESIAN_POINT('',(-1.7759598069398,2.06576154877605,13.8057746032556));
#414549=CARTESIAN_POINT('',(-1.84180085423239,1.96183647465934,13.8390832900376));
#414550=CARTESIAN_POINT('Ctrl Pts',(-1.76410223015076,2.03198820408291,
13.8390832900376));
#414551=CARTESIAN_POINT('Ctrl Pts',(-1.76179303154787,2.02541055591388,
13.8455641171218));
#414552=CARTESIAN_POINT('Ctrl Pts',(-1.76059461532786,2.01806202429734,
13.851896480191));
#414553=CARTESIAN_POINT('Ctrl Pts',(-1.76100615600743,2.01032110925397,
13.8574481026913));
#414554=CARTESIAN_POINT('Ctrl Pts',(-1.76128432353739,2.00508888963573,
13.8612005412592));
#414555=CARTESIAN_POINT('Ctrl Pts',(-1.7623225452775,1.99955541232213,13.8646714234115));
#414556=CARTESIAN_POINT('Ctrl Pts',(-1.76430438039739,1.99407384831637,
13.8674635290331));
#414557=CARTESIAN_POINT('Ctrl Pts',(-1.76590158604583,1.98965613217822,
13.8697137499649));
#414558=CARTESIAN_POINT('Ctrl Pts',(-1.76816218118831,1.98517345642518,
13.8715630732995));
#414559=CARTESIAN_POINT('Ctrl Pts',(-1.77104759729371,1.98101120500597,
13.8727429581918));
#414560=CARTESIAN_POINT('Ctrl Pts',(-1.77396626971095,1.97680098091103,
13.873936442031));
#414561=CARTESIAN_POINT('Ctrl Pts',(-1.77762500733078,1.97280046051005,
13.8744652622107));
#414562=CARTESIAN_POINT('Ctrl Pts',(-1.78168362938013,1.96945867935999,
13.8742206332401));
#414563=CARTESIAN_POINT('Ctrl Pts',(-1.78517714289997,1.96658219628615,
13.8740100655633));
#414564=CARTESIAN_POINT('Ctrl Pts',(-1.78905756884977,1.96411457479282,
13.8732246156103));
#414565=CARTESIAN_POINT('Ctrl Pts',(-1.79299315460958,1.96220156392444,
13.8719820486038));
#414566=CARTESIAN_POINT('Ctrl Pts',(-1.79699655965385,1.96025558743515,
13.8707180692815));
#414567=CARTESIAN_POINT('Ctrl Pts',(-1.80114429947297,1.95883163424464,
13.868960862563));
#414568=CARTESIAN_POINT('Ctrl Pts',(-1.80517464964111,1.95791098363399,
13.8669057591701));
#414569=CARTESIAN_POINT('Ctrl Pts',(-1.81138046174373,1.95649339348339,
13.8637413727084));
#414570=CARTESIAN_POINT('Ctrl Pts',(-1.81749437205224,1.95619949873539,
13.8597962563956));
#414571=CARTESIAN_POINT('Ctrl Pts',(-1.82315189489706,1.95673613031912,
13.855546950204));
#414572=CARTESIAN_POINT('Ctrl Pts',(-1.82989913921785,1.95737612497844,
13.850479165618));
#414573=CARTESIAN_POINT('Ctrl Pts',(-1.83619025383874,1.95919768115324,
13.8448473071436));
#414574=CARTESIAN_POINT('Ctrl Pts',(-1.84180085423239,1.96183647465934,
13.8390832900376));
#414575=CARTESIAN_POINT('',(-1.87419128919245,1.97707132491026,13.8057746032556));
#414576=CARTESIAN_POINT('',(-1.84180085423239,1.96183647465934,13.8390832900376));
#414577=CARTESIAN_POINT('',(-1.93842919100838,1.91413068616379,13.8057746032556));
#414578=CARTESIAN_POINT('Origin',(0.,2.5406128344257E-15,13.8057746032556));
#414579=CARTESIAN_POINT('',(-1.92385822819901,1.88143622207769,13.8390832900376));
#414580=CARTESIAN_POINT('',(-1.93842919100838,1.91413068616379,13.8057746032556));
#414581=CARTESIAN_POINT('',(-1.99558029931379,1.80518475756518,13.8390832900376));
#414582=CARTESIAN_POINT('Ctrl Pts',(-1.923858228199,1.88143622207769,13.8390832900376));
#414583=CARTESIAN_POINT('Ctrl Pts',(-1.92102057387428,1.87506868161401,
13.8455641171218));
#414584=CARTESIAN_POINT('Ctrl Pts',(-1.91922717173821,1.8678422836777,13.851896480191));
#414585=CARTESIAN_POINT('Ctrl Pts',(-1.91900638661092,1.86009358150461,
13.8574481026913));
#414586=CARTESIAN_POINT('Ctrl Pts',(-1.91885715408894,1.85485609842945,
13.8612005412592));
#414587=CARTESIAN_POINT('Ctrl Pts',(-1.91944089146049,1.84925640859494,
13.8646714234115));
#414588=CARTESIAN_POINT('Ctrl Pts',(-1.92096933383269,1.84363154608048,
13.8674635290331));
#414589=CARTESIAN_POINT('Ctrl Pts',(-1.92220114003376,1.83909834244026,
13.8697137499649));
#414590=CARTESIAN_POINT('Ctrl Pts',(-1.92408883354338,1.83444632293054,
13.8715630732995));
#414591=CARTESIAN_POINT('Ctrl Pts',(-1.9266253865336,1.83006273286008,13.8727429581918));
#414592=CARTESIAN_POINT('Ctrl Pts',(-1.9291911749596,1.82562861904085,13.873936442031));
#414593=CARTESIAN_POINT('Ctrl Pts',(-1.93251165888012,1.82134318895941,
13.8744652622107));
#414594=CARTESIAN_POINT('Ctrl Pts',(-1.9362843900121,1.81768171193502,13.8742206332401));
#414595=CARTESIAN_POINT('Ctrl Pts',(-1.93953181907942,1.81453004633725,
13.8740100655633));
#414596=CARTESIAN_POINT('Ctrl Pts',(-1.94319819917199,1.81175434491185,
13.8732246156103));
#414597=CARTESIAN_POINT('Ctrl Pts',(-1.94696476144955,1.80952691265371,
13.8719820486038));
#414598=CARTESIAN_POINT('Ctrl Pts',(-1.95079623034435,1.80726109656374,
13.8707180692815));
#414599=CARTESIAN_POINT('Ctrl Pts',(-1.95481410349702,1.805503802159,13.868960862563));
#414600=CARTESIAN_POINT('Ctrl Pts',(-1.95875600143578,1.80425770398267,
13.8669057591701));
#414601=CARTESIAN_POINT('Ctrl Pts',(-1.96482561745304,1.80233899944804,
13.8637413727084));
#414602=CARTESIAN_POINT('Ctrl Pts',(-1.97089522907902,1.80154774216165,
13.8597962563956));
#414603=CARTESIAN_POINT('Ctrl Pts',(-1.9765776674392,1.80162144751432,13.855546950204));
#414604=CARTESIAN_POINT('Ctrl Pts',(-1.98335462636727,1.80170934959371,
13.850479165618));
#414605=CARTESIAN_POINT('Ctrl Pts',(-1.98977328156199,1.80301206044513,
13.8448473071436));
#414606=CARTESIAN_POINT('Ctrl Pts',(-1.99558029931379,1.80518475756518,
13.8390832900376));
#414607=CARTESIAN_POINT('',(-2.02910473950244,1.8177287939613,13.8057746032556));
#414608=CARTESIAN_POINT('',(-1.99558029931379,1.80518475756518,13.8390832900376));
#414609=CARTESIAN_POINT('',(-2.08799864862912,1.74976159964444,13.8057746032556));
#414610=CARTESIAN_POINT('Origin',(0.,2.5406128344257E-15,13.8057746032556));
#414611=CARTESIAN_POINT('',(-2.07081126715285,1.71836359242966,13.8390832900376));
#414612=CARTESIAN_POINT('',(-2.08799864862912,1.74976159964444,13.8057746032556));
#414613=CARTESIAN_POINT('',(-2.13607948675083,1.63651983374394,13.8390832900376));
#414614=CARTESIAN_POINT('Ctrl Pts',(-2.07081126715285,1.71836359242966,
13.8390832900376));
#414615=CARTESIAN_POINT('Ctrl Pts',(-2.06746404122766,1.71224853460256,
13.8455641171218));
#414616=CARTESIAN_POINT('Ctrl Pts',(-2.06508758797082,1.70519236083247,
13.851896480191));
#414617=CARTESIAN_POINT('Ctrl Pts',(-2.06423594632529,1.69748743786418,
13.8574481026913));
#414618=CARTESIAN_POINT('Ctrl Pts',(-2.06366030686916,1.69227954591784,
13.8612005412592));
#414619=CARTESIAN_POINT('Ctrl Pts',(-2.06378567519628,1.68665090857437,
13.8646714234115));
#414620=CARTESIAN_POINT('Ctrl Pts',(-2.06485055328896,1.68092018008321,
13.8674635290331));
#414621=CARTESIAN_POINT('Ctrl Pts',(-2.06570876257563,1.67630165666322,
13.8697137499649));
#414622=CARTESIAN_POINT('Ctrl Pts',(-2.06721099216353,1.67151125181913,
13.8715630732995));
#414623=CARTESIAN_POINT('Ctrl Pts',(-2.06938180169692,1.6669354951661,13.8727429581918));
#414624=CARTESIAN_POINT('Ctrl Pts',(-2.07157763123302,1.66230699991848,
13.873936442031));
#414625=CARTESIAN_POINT('Ctrl Pts',(-2.07453776418159,1.65776517898672,
13.8744652622107));
#414626=CARTESIAN_POINT('Ctrl Pts',(-2.07799949749298,1.65380837261349,
13.8742206332401));
#414627=CARTESIAN_POINT('Ctrl Pts',(-2.08097923100311,1.65040249830636,
13.8740100655633));
#414628=CARTESIAN_POINT('Ctrl Pts',(-2.08440716608385,1.64733718878392,
13.8732246156103));
#414629=CARTESIAN_POINT('Ctrl Pts',(-2.08797963902864,1.64481015833018,
13.8719820486038));
#414630=CARTESIAN_POINT('Ctrl Pts',(-2.09161367398063,1.64223958127179,
13.8707180692815));
#414631=CARTESIAN_POINT('Ctrl Pts',(-2.09547494218393,1.64016064015716,
13.868960862563));
#414632=CARTESIAN_POINT('Ctrl Pts',(-2.0993021552129,1.63859738699291,13.8669057591701));
#414633=CARTESIAN_POINT('Ctrl Pts',(-2.10519518285161,1.63619033673636,
13.8637413727084));
#414634=CARTESIAN_POINT('Ctrl Pts',(-2.11118010353109,1.63490698259828,
13.8597962563956));
#414635=CARTESIAN_POINT('Ctrl Pts',(-2.11684964171689,1.63451727122293,
13.855546950204));
#414636=CARTESIAN_POINT('Ctrl Pts',(-2.1236112157087,1.63405249574854,13.850479165618));
#414637=CARTESIAN_POINT('Ctrl Pts',(-2.13011469638593,1.63482769195082,
13.8448473071436));
#414638=CARTESIAN_POINT('Ctrl Pts',(-2.13607948675083,1.63651983374394,
13.8390832900376));
#414639=CARTESIAN_POINT('',(-2.17051483254976,1.64628957779267,13.8057746032556));
#414640=CARTESIAN_POINT('',(-2.13607948675083,1.63651983374394,13.8390832900376));
#414641=CARTESIAN_POINT('',(-2.22367281973875,1.5737481383698,13.8057746032556));
#414642=CARTESIAN_POINT('Origin',(0.,2.5406128344257E-15,13.8057746032556));
#414643=CARTESIAN_POINT('',(-2.20398339878361,1.54385553658406,13.8390832900376));
#414644=CARTESIAN_POINT('',(-2.22367281973875,1.5737481383698,13.8057746032556));
#414645=CARTESIAN_POINT('',(-2.26236341763185,1.4569641404359,13.8390832900376));
#414646=CARTESIAN_POINT('Ctrl Pts',(-2.2039833987836,1.54385553658406,13.8390832900376));
#414647=CARTESIAN_POINT('Ctrl Pts',(-2.20014887649421,1.53803365609445,
13.8455641171218));
#414648=CARTESIAN_POINT('Ctrl Pts',(-2.19720518702096,1.53119466416283,
13.851896480191));
#414649=CARTESIAN_POINT('Ctrl Pts',(-2.19572835639182,1.52358479539047,
13.8574481026913));
#414650=CARTESIAN_POINT('Ctrl Pts',(-2.19473014078716,1.51844115223462,
13.8612005412592));
#414651=CARTESIAN_POINT('Ctrl Pts',(-2.1943963057643,1.51282102503506,13.8646714234115));
#414652=CARTESIAN_POINT('Ctrl Pts',(-2.19499053298945,1.5070225676198,13.8674635290331));
#414653=CARTESIAN_POINT('Ctrl Pts',(-2.19546943412051,1.5023494599314,13.8697137499649));
#414654=CARTESIAN_POINT('Ctrl Pts',(-2.19657620269664,1.49745254910681,
13.8715630732995));
#414655=CARTESIAN_POINT('Ctrl Pts',(-2.19836682239391,1.49271507677678,
13.8727429581918));
#414656=CARTESIAN_POINT('Ctrl Pts',(-2.20017808015684,1.487923001973,13.873936442031));
#414657=CARTESIAN_POINT('Ctrl Pts',(-2.20275816293707,1.48315501525987,
13.8744652622107));
#414658=CARTESIAN_POINT('Ctrl Pts',(-2.20588586116382,1.4789292114314,13.8742206332401));
#414659=CARTESIAN_POINT('Ctrl Pts',(-2.20857806948188,1.47529179394649,
13.8740100655633));
#414660=CARTESIAN_POINT('Ctrl Pts',(-2.21174474720841,1.47195727545613,
13.8732246156103));
#414661=CARTESIAN_POINT('Ctrl Pts',(-2.2150993566024,1.46914746377755,13.8719820486038));
#414662=CARTESIAN_POINT('Ctrl Pts',(-2.21851177370854,1.46628923251693,
13.8707180692815));
#414663=CARTESIAN_POINT('Ctrl Pts',(-2.22219074085963,1.46390247970253,
13.868960862563));
#414664=CARTESIAN_POINT('Ctrl Pts',(-2.22587779950755,1.46203247474225,
13.8669057591701));
#414665=CARTESIAN_POINT('Ctrl Pts',(-2.23155502164105,1.45915309728611,
13.8637413727084));
#414666=CARTESIAN_POINT('Ctrl Pts',(-2.23741542271437,1.45738618680638,
13.8597962563956));
#414667=CARTESIAN_POINT('Ctrl Pts',(-2.24303433088457,1.45653565216792,
13.855546950204));
#414668=CARTESIAN_POINT('Ctrl Pts',(-2.24973552278078,1.45552129214386,
13.850479165618));
#414669=CARTESIAN_POINT('Ctrl Pts',(-2.25628054934961,1.45576381489416,
13.8448473071436));
#414670=CARTESIAN_POINT('Ctrl Pts',(-2.26236341763184,1.4569641404359,13.8390832900376));
#414671=CARTESIAN_POINT('',(-2.2974805074962,1.46389457610249,13.8057746032556));
#414672=CARTESIAN_POINT('',(-2.26236341763185,1.4569641404359,13.8390832900376));
#414673=CARTESIAN_POINT('',(-2.34454881511321,1.38726164288447,13.8057746032556));
#414674=CARTESIAN_POINT('Origin',(0.,2.5406128344257E-15,13.8057746032556));
#414675=CARTESIAN_POINT('',(-2.32248838452712,1.35907337686072,13.8390832900376));
#414676=CARTESIAN_POINT('',(-2.34454881511321,1.38726164288447,13.8057746032556));
#414677=CARTESIAN_POINT('',(-2.37359169323221,1.26771259115543,13.8390832900376));
#414678=CARTESIAN_POINT('Ctrl Pts',(-2.32248838452712,1.35907337686072,
13.8390832900376));
#414679=CARTESIAN_POINT('Ctrl Pts',(-2.31819208398671,1.35358341736272,
13.8455641171218));
#414680=CARTESIAN_POINT('Ctrl Pts',(-2.31470074806482,1.34700711963253,
13.851896480191));
#414681=CARTESIAN_POINT('Ctrl Pts',(-2.31260855651624,1.33954294747724,
13.8574481026913));
#414682=CARTESIAN_POINT('Ctrl Pts',(-2.31119440772321,1.33449778320843,
13.8612005412592));
#414683=CARTESIAN_POINT('Ctrl Pts',(-2.31040359096736,1.32892356717203,
13.8646714234115));
#414684=CARTESIAN_POINT('Ctrl Pts',(-2.31052321284085,1.32309596861009,
13.8674635290331));
#414685=CARTESIAN_POINT('Ctrl Pts',(-2.31061961880828,1.31839937541394,
13.8697137499649));
#414686=CARTESIAN_POINT('Ctrl Pts',(-2.31132356101037,1.31342854674246,
13.8715630732995));
#414687=CARTESIAN_POINT('Ctrl Pts',(-2.31272207459287,1.30856088583217,
13.8727429581918));
#414688=CARTESIAN_POINT('Ctrl Pts',(-2.31413670696105,1.3036371219394,13.873936442031));
#414689=CARTESIAN_POINT('Ctrl Pts',(-2.31631956954772,1.29867469960982,
13.8744652622107));
#414690=CARTESIAN_POINT('Ctrl Pts',(-2.31909241837417,1.29420802035337,
13.8742206332401));
#414691=CARTESIAN_POINT('Ctrl Pts',(-2.32147918529799,1.29036326610391,
13.8740100655633));
#414692=CARTESIAN_POINT('Ctrl Pts',(-2.32436353195249,1.28678172931604,
13.8732246156103));
#414693=CARTESIAN_POINT('Ctrl Pts',(-2.32747795342363,1.28370783524574,
13.8719820486038));
#414694=CARTESIAN_POINT('Ctrl Pts',(-2.33064604361109,1.28058097084037,
13.8707180692815));
#414695=CARTESIAN_POINT('Ctrl Pts',(-2.33411822679057,1.27790228977239,
13.868960862563));
#414696=CARTESIAN_POINT('Ctrl Pts',(-2.33764059429046,1.27573797759056,
13.8669057591701));
#414697=CARTESIAN_POINT('Ctrl Pts',(-2.34306422994214,1.27240543471673,
13.8637413727084));
#414698=CARTESIAN_POINT('Ctrl Pts',(-2.34876111140704,1.27016672639309,
13.8597962563956));
#414699=CARTESIAN_POINT('Ctrl Pts',(-2.35429199665482,1.2688610286592,13.855546950204));
#414700=CARTESIAN_POINT('Ctrl Pts',(-2.36088821112899,1.26730383448407,
13.850479165618));
#414701=CARTESIAN_POINT('Ctrl Pts',(-2.36743122751746,1.2670120698335,13.8448473071436));
#414702=CARTESIAN_POINT('Ctrl Pts',(-2.37359169323221,1.26771259115543,
13.8390832900376));
#414703=CARTESIAN_POINT('',(-2.40915682872285,1.27175759753395,13.8057746032556));
#414704=CARTESIAN_POINT('',(-2.37359169323221,1.26771259115543,13.8390832900376));
#414705=CARTESIAN_POINT('',(-2.44982222494642,1.19154315004781,13.8057746032556));
#414706=CARTESIAN_POINT('Origin',(0.,2.5406128344257E-15,13.8057746032556));
#414707=CARTESIAN_POINT('',(-2.42553759325522,1.16524680804569,13.8390832900376));
#414708=CARTESIAN_POINT('',(-2.44982222494642,1.19154315004781,13.8057746032556));
#414709=CARTESIAN_POINT('',(-2.46902410772919,1.07002462373867,13.8390832900376));
#414710=CARTESIAN_POINT('Ctrl Pts',(-2.42553759325522,1.16524680804569,
13.8390832900376));
#414711=CARTESIAN_POINT('Ctrl Pts',(-2.42080810563505,1.16012530431399,
13.8455641171218));
#414712=CARTESIAN_POINT('Ctrl Pts',(-2.41679235752905,1.1538554649616,13.851896480191));
#414713=CARTESIAN_POINT('Ctrl Pts',(-2.4140987282506,1.14658666225758,13.8574481026913));
#414714=CARTESIAN_POINT('Ctrl Pts',(-2.41227805719609,1.14167355161162,
13.8612005412592));
#414715=CARTESIAN_POINT('Ctrl Pts',(-2.4110355214623,1.13618234222643,13.8646714234115));
#414716=CARTESIAN_POINT('Ctrl Pts',(-2.41067974192029,1.13036438422476,
13.8674635290331));
#414717=CARTESIAN_POINT('Ctrl Pts',(-2.41039301115828,1.12567556057369,
13.8697137499649));
#414718=CARTESIAN_POINT('Ctrl Pts',(-2.41068944236712,1.1206638941,13.8715630732995));
#414719=CARTESIAN_POINT('Ctrl Pts',(-2.41168654295769,1.1156984380897,13.8727429581918));
#414720=CARTESIAN_POINT('Ctrl Pts',(-2.41269513578612,1.11067575194429,
13.873936442031));
#414721=CARTESIAN_POINT('Ctrl Pts',(-2.41446625158886,1.10555191810012,
13.8744652622107));
#414722=CARTESIAN_POINT('Ctrl Pts',(-2.41686579816356,1.10087408842919,
13.8742206332401));
#414723=CARTESIAN_POINT('Ctrl Pts',(-2.41893124015304,1.09684758362037,
13.8740100655633));
#414724=CARTESIAN_POINT('Ctrl Pts',(-2.42151406088441,1.09304286307139,
13.8732246156103));
#414725=CARTESIAN_POINT('Ctrl Pts',(-2.42436756847166,1.08972534286726,
13.8719820486038));
#414726=CARTESIAN_POINT('Ctrl Pts',(-2.42727024862294,1.08635065408386,
13.8707180692815));
#414727=CARTESIAN_POINT('Ctrl Pts',(-2.43051254102462,1.08339787094285,
13.868960862563));
#414728=CARTESIAN_POINT('Ctrl Pts',(-2.43384677660192,1.08095365467996,
13.8669057591701));
#414729=CARTESIAN_POINT('Ctrl Pts',(-2.43898073237136,1.07719012391144,
13.8637413727084));
#414730=CARTESIAN_POINT('Ctrl Pts',(-2.44447618242161,1.0744945159784,13.8597962563956));
#414731=CARTESIAN_POINT('Ctrl Pts',(-2.44988223761817,1.07274234435208,
13.855546950204));
#414732=CARTESIAN_POINT('Ctrl Pts',(-2.45632957795126,1.0706526788962,13.850479165618));
#414733=CARTESIAN_POINT('Ctrl Pts',(-2.46282704146483,1.06982856849037,
13.8448473071436));
#414734=CARTESIAN_POINT('Ctrl Pts',(-2.46902410772918,1.07002462373867,
13.8390832900376));
#414735=CARTESIAN_POINT('',(-2.50480060873725,1.07115728197906,13.8057746032556));
#414736=CARTESIAN_POINT('',(-2.46902410772919,1.07002462373867,13.8390832900376));
#414737=CARTESIAN_POINT('',(-2.53879247206483,0.98789513413836,13.8057746032556));
#414738=CARTESIAN_POINT('Origin',(0.,2.5406128344257E-15,13.8057746032556));
#414739=CARTESIAN_POINT('',(-2.51244524948573,0.963665713975314,13.8390832900376));
#414740=CARTESIAN_POINT('',(-2.53879247206483,0.98789513413836,13.8057746032556));
#414741=CARTESIAN_POINT('',(-2.54802557414952,0.865215818992561,13.8390832900376));
#414742=CARTESIAN_POINT('Ctrl Pts',(-2.51244524948573,0.963665713975314,
13.8390832900376));
#414743=CARTESIAN_POINT('Ctrl Pts',(-2.50731404874562,0.958946748772246,
13.8455641171218));
#414744=CARTESIAN_POINT('Ctrl Pts',(-2.50280061259659,0.953025092544104,
13.851896480191));
#414745=CARTESIAN_POINT('Ctrl Pts',(-2.49952347124671,0.946000031974073,
13.8574481026913));
#414746=CARTESIAN_POINT('Ctrl Pts',(-2.4973083941962,0.941251670891716,
13.8612005412592));
#414747=CARTESIAN_POINT('Ctrl Pts',(-2.49562240835476,0.935880011250207,
13.8646714234115));
#414748=CARTESIAN_POINT('Ctrl Pts',(-2.49479359505141,0.930110411359408,
13.8674635290331));
#414749=CARTESIAN_POINT('Ctrl Pts',(-2.49412563570588,0.925460560601219,
13.8697137499649));
#414750=CARTESIAN_POINT('Ctrl Pts',(-2.49401258322068,0.920441408138835,
13.8715630732995));
#414751=CARTESIAN_POINT('Ctrl Pts',(-2.49460163527941,0.91541120131902,
13.8727429581918));
#414752=CARTESIAN_POINT('Ctrl Pts',(-2.4951974765492,0.910323018068578,
13.873936442031));
#414753=CARTESIAN_POINT('Ctrl Pts',(-2.49654505908457,0.905071870978679,
13.8744652622107));
#414754=CARTESIAN_POINT('Ctrl Pts',(-2.49855533482095,0.900214021077945,
13.8742206332401));
#414755=CARTESIAN_POINT('Ctrl Pts',(-2.50028570670044,0.896032561434943,
13.8740100655633));
#414756=CARTESIAN_POINT('Ctrl Pts',(-2.50254981326285,0.892029976912383,
13.8732246156103));
#414757=CARTESIAN_POINT('Ctrl Pts',(-2.505123417344,0.888490908124015,13.8719820486038));
#414758=CARTESIAN_POINT('Ctrl Pts',(-2.50774137060161,0.884890852959653,
13.8707180692815));
#414759=CARTESIAN_POINT('Ctrl Pts',(-2.5107321953045,0.881683618030249,
13.868960862563));
#414760=CARTESIAN_POINT('Ctrl Pts',(-2.51385611017155,0.878975763542255,
13.8669057591701));
#414761=CARTESIAN_POINT('Ctrl Pts',(-2.51866622043013,0.874806290555372,
13.8637413727084));
#414762=CARTESIAN_POINT('Ctrl Pts',(-2.52392366775234,0.871671721838992,
13.8597962563956));
#414763=CARTESIAN_POINT('Ctrl Pts',(-2.52916891649229,0.869484736733329,
13.855546950204));
#414764=CARTESIAN_POINT('Ctrl Pts',(-2.53542447669813,0.866876506375528,
13.850479165618));
#414765=CARTESIAN_POINT('Ctrl Pts',(-2.54183314778912,0.865525534533235,
13.8448473071436));
#414766=CARTESIAN_POINT('Ctrl Pts',(-2.54802557414952,0.865215818992561,
13.8390832900376));
#414767=CARTESIAN_POINT('',(-2.58377535396352,0.863428591441109,13.8057746032556));
#414768=CARTESIAN_POINT('',(-2.54802557414952,0.865215818992561,13.8390832900376));
#414769=CARTESIAN_POINT('',(-2.61086747415291,0.777672839102445,13.8057746032556));
#414770=CARTESIAN_POINT('Origin',(0.,2.5406128344257E-15,13.8057746032556));
#414771=CARTESIAN_POINT('',(-2.58263299710521,0.755671583572082,13.8390832900376));
#414772=CARTESIAN_POINT('',(-2.61086747415291,0.777672839102445,13.8057746032556));
#414773=CARTESIAN_POINT('',(-2.61007035076852,0.654649145721622,13.8390832900376));
#414774=CARTESIAN_POINT('Ctrl Pts',(-2.58263299710521,0.755671583572082,
13.8390832900376));
#414775=CARTESIAN_POINT('Ctrl Pts',(-2.57713423053948,0.751386560832503,
13.8455641171218));
#414776=CARTESIAN_POINT('Ctrl Pts',(-2.57215314252033,0.7458524953738,13.851896480191));
#414777=CARTESIAN_POINT('Ctrl Pts',(-2.56831429793401,0.739117927556801,
13.8574481026913));
#414778=CARTESIAN_POINT('Ctrl Pts',(-2.56571955585981,0.734565915597623,
13.8612005412592));
#414779=CARTESIAN_POINT('Ctrl Pts',(-2.56360133986834,0.729349553208446,
13.8646714234115));
#414780=CARTESIAN_POINT('Ctrl Pts',(-2.56230500841943,0.723666707163876,
13.8674635290331));
#414781=CARTESIAN_POINT('Ctrl Pts',(-2.56126026564962,0.719086773288191,
13.8697137499649));
#414782=CARTESIAN_POINT('Ctrl Pts',(-2.56073848181602,0.714093536468648,
13.8715630732995));
#414783=CARTESIAN_POINT('Ctrl Pts',(-2.56091556529863,0.709032054035785,
13.8727429581918));
#414784=CARTESIAN_POINT('Ctrl Pts',(-2.56109468978446,0.703912234700355,
13.873936442031));
#414785=CARTESIAN_POINT('Ctrl Pts',(-2.562009771113,0.698568719882228,13.8744652622107));
#414786=CARTESIAN_POINT('Ctrl Pts',(-2.56361739795772,0.693563177941289,
13.8742206332401));
#414787=CARTESIAN_POINT('Ctrl Pts',(-2.56500118438785,0.689254590388136,
13.8740100655633));
#414788=CARTESIAN_POINT('Ctrl Pts',(-2.56693150952567,0.685080778431609,
13.8732246156103));
#414789=CARTESIAN_POINT('Ctrl Pts',(-2.5692080831902,0.681343712977893,
13.8719820486038));
#414790=CARTESIAN_POINT('Ctrl Pts',(-2.57152388750712,0.677542249205719,
13.8707180692815));
#414791=CARTESIAN_POINT('Ctrl Pts',(-2.57424334106628,0.674101906107217,
13.868960862563));
#414792=CARTESIAN_POINT('Ctrl Pts',(-2.57713614608504,0.671148433718975,
13.8669057591701));
#414793=CARTESIAN_POINT('Ctrl Pts',(-2.58159040034262,0.666600765668538,
13.8637413727084));
#414794=CARTESIAN_POINT('Ctrl Pts',(-2.58657485749227,0.66304809620646,
13.8597962563956));
#414795=CARTESIAN_POINT('Ctrl Pts',(-2.59162439351065,0.660440851646503,
13.855546950204));
#414796=CARTESIAN_POINT('Ctrl Pts',(-2.59764654386817,0.657331413729489,
13.850479165618));
#414797=CARTESIAN_POINT('Ctrl Pts',(-2.60392377388782,0.655462570945439,
13.8448473071436));
#414798=CARTESIAN_POINT('Ctrl Pts',(-2.61007035076852,0.654649145721622,
13.8390832900376));
#414799=CARTESIAN_POINT('',(-2.64555550050208,0.649953926082808,13.8057746032556));
#414800=CARTESIAN_POINT('',(-2.61007035076852,0.654649145721622,13.8390832900376));
#414801=CARTESIAN_POINT('',(-2.66556758396333,0.562275259629291,13.8057746032556));
#414802=CARTESIAN_POINT('Origin',(0.,2.5406128344257E-15,13.8057746032556));
#414803=CARTESIAN_POINT('',(-2.6356337482334,0.542648583457214,13.8390832900376));
#414804=CARTESIAN_POINT('',(-2.66556758396333,0.562275259629291,13.8057746032556));
#414805=CARTESIAN_POINT('',(-2.65474553983446,0.439725890395412,13.8390832900376));
#414806=CARTESIAN_POINT('Ctrl Pts',(-2.6356337482334,0.542648583457214,
13.8390832900376));
#414807=CARTESIAN_POINT('Ctrl Pts',(-2.62980400922631,0.538826019300476,
13.8455641171218));
#414808=CARTESIAN_POINT('Ctrl Pts',(-2.624388417656,0.533716372903784,13.851896480191));
#414809=CARTESIAN_POINT('Ctrl Pts',(-2.6200134167106,0.527317115277512,
13.8574481026913));
#414810=CARTESIAN_POINT('Ctrl Pts',(-2.6170562771931,0.522991745330072,
13.8612005412592));
#414811=CARTESIAN_POINT('Ctrl Pts',(-2.61451992742954,0.517965394224288,
13.8646714234115));
#414812=CARTESIAN_POINT('Ctrl Pts',(-2.61276470470699,0.512407120428769,
13.8674635290331));
#414813=CARTESIAN_POINT('Ctrl Pts',(-2.61135013110366,0.507927582139896,
13.8697137499649));
#414814=CARTESIAN_POINT('Ctrl Pts',(-2.61042308830698,0.502993490130399,
13.8715630732995));
#414815=CARTESIAN_POINT('Ctrl Pts',(-2.61018702475212,0.497934415414992,
13.8727429581918));
#414816=CARTESIAN_POINT('Ctrl Pts',(-2.60994824041008,0.49281703154754,
13.873936442031));
#414817=CARTESIAN_POINT('Ctrl Pts',(-2.61042473081654,0.487416709210687,
13.8744652622107));
#414818=CARTESIAN_POINT('Ctrl Pts',(-2.61161901027819,0.482296786285305,
13.8742206332401));
#414819=CARTESIAN_POINT('Ctrl Pts',(-2.61264700238856,0.477889743761299,
13.8740100655633));
#414820=CARTESIAN_POINT('Ctrl Pts',(-2.6142307001065,0.473572480400745,
13.8732246156103));
#414821=CARTESIAN_POINT('Ctrl Pts',(-2.61619509313225,0.469662287835703,
13.8719820486038));
#414822=CARTESIAN_POINT('Ctrl Pts',(-2.61819333721286,0.465684713569924,
13.8707180692815));
#414823=CARTESIAN_POINT('Ctrl Pts',(-2.62062332211352,0.462034157218028,
13.868960862563));
#414824=CARTESIAN_POINT('Ctrl Pts',(-2.62326576614388,0.458854721800992,
13.8669057591701));
#414825=CARTESIAN_POINT('Ctrl Pts',(-2.62733452207326,0.453959122667565,
13.8637413727084));
#414826=CARTESIAN_POINT('Ctrl Pts',(-2.6320128183104,0.450011994888908,
13.8597962563956));
#414827=CARTESIAN_POINT('Ctrl Pts',(-2.63683303777813,0.447001841657038,
13.855546950204));
#414828=CARTESIAN_POINT('Ctrl Pts',(-2.64258170187027,0.443411888977129,
13.850479165618));
#414829=CARTESIAN_POINT('Ctrl Pts',(-2.64868571688848,0.44103761209171,
13.8448473071436));
#414830=CARTESIAN_POINT('Ctrl Pts',(-2.65474553983446,0.43972589039541,
13.8390832900376));
#414831=CARTESIAN_POINT('',(-2.68972991167074,0.432153924581275,13.8057746032556));
#414832=CARTESIAN_POINT('',(-2.65474553983446,0.439725890395412,13.8390832900376));
#414833=CARTESIAN_POINT('',(-2.70252878129016,0.34313583107219,13.8057746032556));
#414834=CARTESIAN_POINT('Origin',(0.,2.5406128344257E-15,13.8057746032556));
#414835=CARTESIAN_POINT('',(-2.67109479161606,0.326014346550151,13.8390832900376));
#414836=CARTESIAN_POINT('',(-2.70252878129016,0.34313583107219,13.8057746032556));
#414837=CARTESIAN_POINT('',(-2.68175383533497,0.221876331818285,13.8390832900376));
#414838=CARTESIAN_POINT('Ctrl Pts',(-2.67109479161606,0.326014346550149,
13.8390832900376));
#414839=CARTESIAN_POINT('Ctrl Pts',(-2.66497287611887,0.322679679510038,
13.8455641171218));
#414840=CARTESIAN_POINT('Ctrl Pts',(-2.65915882086578,0.318028456029097,
13.851896480191));
#414841=CARTESIAN_POINT('Ctrl Pts',(-2.65427677847076,0.312007094597252,
13.8574481026913));
#414842=CARTESIAN_POINT('Ctrl Pts',(-2.65097692078557,0.307937151284914,
13.8612005412592));
#414843=CARTESIAN_POINT('Ctrl Pts',(-2.64803931623913,0.30313426099984,
13.8646714234115));
#414844=CARTESIAN_POINT('Ctrl Pts',(-2.64583688296055,0.297737548848432,
13.8674635290331));
#414845=CARTESIAN_POINT('Ctrl Pts',(-2.64406189227765,0.29338821673461,
13.8697137499649));
#414846=CARTESIAN_POINT('Ctrl Pts',(-2.64273575983475,0.288546105103419,
13.8715630732995));
#414847=CARTESIAN_POINT('Ctrl Pts',(-2.64208812020644,0.28352310541301,
13.8727429581918));
#414848=CARTESIAN_POINT('Ctrl Pts',(-2.64143301610692,0.278442212358865,
13.873936442031));
#414849=CARTESIAN_POINT('Ctrl Pts',(-2.64146774462626,0.273021020757444,
13.8744652622107));
#414850=CARTESIAN_POINT('Ctrl Pts',(-2.64224072897206,0.267820789089958,
13.8742206332401));
#414851=CARTESIAN_POINT('Ctrl Pts',(-2.64290608564479,0.263344619735988,
13.8740100655633));
#414852=CARTESIAN_POINT('Ctrl Pts',(-2.64413261669582,0.258912635646773,
13.8732246156103));
#414853=CARTESIAN_POINT('Ctrl Pts',(-2.64577175637132,0.254855337656788,
13.8719820486038));
#414854=CARTESIAN_POINT('Ctrl Pts',(-2.64743914223093,0.250728122997891,
13.8707180692815));
#414855=CARTESIAN_POINT('Ctrl Pts',(-2.64956348732451,0.246891647242822,
13.868960862563));
#414856=CARTESIAN_POINT('Ctrl Pts',(-2.65193798533742,0.243507407415124,
13.8669057591701));
#414857=CARTESIAN_POINT('Ctrl Pts',(-2.65559416603919,0.238296456603223,
13.8637413727084));
#414858=CARTESIAN_POINT('Ctrl Pts',(-2.65993516807423,0.233981137992124,
13.8597962563956));
#414859=CARTESIAN_POINT('Ctrl Pts',(-2.66449399322602,0.230588108161459,
13.855546950204));
#414860=CARTESIAN_POINT('Ctrl Pts',(-2.66993091464172,0.226541531261439,
13.850479165618));
#414861=CARTESIAN_POINT('Ctrl Pts',(-2.67582109344563,0.223677620695598,
13.8448473071436));
#414862=CARTESIAN_POINT('Ctrl Pts',(-2.68175383533497,0.221876331818284,
13.8390832900376));
#414863=CARTESIAN_POINT('',(-2.71600461405142,0.211478010012032,13.8057746032556));
#414864=CARTESIAN_POINT('',(-2.68175383533497,0.221876331818285,13.8390832900376));
#414865=CARTESIAN_POINT('',(-2.72150509546337,0.121712890172733,13.8057746032556));
#414866=CARTESIAN_POINT('Origin',(0.,2.5406128344257E-15,13.8057746032556));
#414867=CARTESIAN_POINT('',(-2.68878013986014,0.107210537955378,13.8390832900376));
#414868=CARTESIAN_POINT('',(-2.72150509546337,0.121712890172733,13.8057746032556));
#414869=CARTESIAN_POINT('',(-2.69091550151957,0.00255022285992577,13.8390832900376));
#414870=CARTESIAN_POINT('Ctrl Pts',(-2.68878013986013,0.107210537955379,
13.8390832900376));
#414871=CARTESIAN_POINT('Ctrl Pts',(-2.68240678821043,0.104385959690864,
13.8455641171218));
#414872=CARTESIAN_POINT('Ctrl Pts',(-2.67623296085302,0.100224112250538,
13.851896480191));
#414873=CARTESIAN_POINT('Ctrl Pts',(-2.67087636619504,0.0946207181799948,
13.8574481026913));
#414874=CARTESIAN_POINT('Ctrl Pts',(-2.66725575035062,0.0908332863040082,
13.8612005412592));
#414875=CARTESIAN_POINT('Ctrl Pts',(-2.66393644029487,0.0862858192820752,
13.8646714234115));
#414876=CARTESIAN_POINT('Ctrl Pts',(-2.66130145329037,0.0810865830037507,
13.8674635290331));
#414877=CARTESIAN_POINT('Ctrl Pts',(-2.65917785779804,0.0768964011526091,
13.8697137499649));
#414878=CARTESIAN_POINT('Ctrl Pts',(-2.65746146090153,0.0721784933537311,
13.8715630732994));
#414879=CARTESIAN_POINT('Ctrl Pts',(-2.65640655513463,0.0672249959225243,
13.8727429581918));
#414880=CARTESIAN_POINT('Ctrl Pts',(-2.65533949088734,0.0622144061866732,
13.873936442031));
#414881=CARTESIAN_POINT('Ctrl Pts',(-2.654932226407,0.0568084224563586,
13.8744652622107));
#414882=CARTESIAN_POINT('Ctrl Pts',(-2.65527877155365,0.0515624887305395,
13.8742206332401));
#414883=CARTESIAN_POINT('Ctrl Pts',(-2.65557706494987,0.0470469807151382,
13.8740100655633));
#414884=CARTESIAN_POINT('Ctrl Pts',(-2.6564382669722,0.0425297700201496,
13.8732246156103));
#414885=CARTESIAN_POINT('Ctrl Pts',(-2.65774124509335,0.0383523672539394,
13.8719820486038));
#414886=CARTESIAN_POINT('Ctrl Pts',(-2.65906667655417,0.0341029781345346,
13.8707180692815));
#414887=CARTESIAN_POINT('Ctrl Pts',(-2.66087124467455,0.0301061140894697,
13.868960862563));
#414888=CARTESIAN_POINT('Ctrl Pts',(-2.6629619947775,0.0265395914088023,
13.8669057591701));
#414889=CARTESIAN_POINT('Ctrl Pts',(-2.66618126897233,0.0210479669363342,
13.8637413727084));
#414890=CARTESIAN_POINT('Ctrl Pts',(-2.67015608815293,0.0163931752261725,
13.8597962563956));
#414891=CARTESIAN_POINT('Ctrl Pts',(-2.67442318075955,0.0126398488504258,
13.855546950204));
#414892=CARTESIAN_POINT('Ctrl Pts',(-2.67951217768382,0.0081635770319262,
13.850479165618));
#414893=CARTESIAN_POINT('Ctrl Pts',(-2.6851493221053,0.00482909163796583,
13.8448473071436));
#414894=CARTESIAN_POINT('Ctrl Pts',(-2.69091550151957,0.0025502228599249,
13.8390832900376));
#414895=CARTESIAN_POINT('',(-2.72420475383482,-0.0106052558224246,13.8057746032556));
#414896=CARTESIAN_POINT('',(-2.69091550151957,0.00255022285992577,13.8390832900376));
#414897=CARTESIAN_POINT('',(-2.722370242243,-0.100520029929612,13.8057746032556));
#414898=CARTESIAN_POINT('Origin',(0.,2.5406128344257E-15,13.8057746032556));
#414899=CARTESIAN_POINT('',(-2.68857209989094,-0.112306739080994,13.8390832900376));
#414900=CARTESIAN_POINT('',(-2.722370242243,-0.100520029929612,13.8057746032556));
#414901=CARTESIAN_POINT('',(-2.68216956901137,-0.21679285741081,13.8390832900376));
#414902=CARTESIAN_POINT('Ctrl Pts',(-2.68857209989094,-0.112306739080995,
13.8390832900376));
#414903=CARTESIAN_POINT('Ctrl Pts',(-2.68198972569242,-0.114602431467585,
13.8455641171218));
#414904=CARTESIAN_POINT('Ctrl Pts',(-2.67549721203314,-0.118247206459234,
13.851896480191));
#414905=CARTESIAN_POINT('Ctrl Pts',(-2.66970171236588,-0.123395343505431,
13.8574481026913));
#414906=CARTESIAN_POINT('Ctrl Pts',(-2.6657844329633,-0.126875059210813,
13.8612005412592));
#414907=CARTESIAN_POINT('Ctrl Pts',(-2.66210550685903,-0.131136840326858,
13.8646714234115));
#414908=CARTESIAN_POINT('Ctrl Pts',(-2.65905550153238,-0.136104000672482,
13.8674635290331));
#414909=CARTESIAN_POINT('Ctrl Pts',(-2.65659743340824,-0.140107147292054,
13.8697137499649));
#414910=CARTESIAN_POINT('Ctrl Pts',(-2.65450219439629,-0.144669454360612,
13.8715630732994));
#414911=CARTESIAN_POINT('Ctrl Pts',(-2.65304704271464,-0.149520484824482,
13.8727429581918));
#414912=CARTESIAN_POINT('Ctrl Pts',(-2.65157511945608,-0.154427426594036,
13.873936442031));
#414913=CARTESIAN_POINT('Ctrl Pts',(-2.65072857225398,-0.159782226523443,
13.8744652622107));
#414914=CARTESIAN_POINT('Ctrl Pts',(-2.65064637200072,-0.165038951484169,
13.8742206332401));
#414915=CARTESIAN_POINT('Ctrl Pts',(-2.65057561702708,-0.169563748200165,
13.8740100655633));
#414916=CARTESIAN_POINT('Ctrl Pts',(-2.65106575886334,-0.174136124209039,
13.8732246156103));
#414917=CARTESIAN_POINT('Ctrl Pts',(-2.65202390432573,-0.178405831825289,
13.8719820486038));
#414918=CARTESIAN_POINT('Ctrl Pts',(-2.65299856086007,-0.182749116421712,
13.8707180692815));
#414919=CARTESIAN_POINT('Ctrl Pts',(-2.65447134290414,-0.186879770285992,
13.868960862563));
#414920=CARTESIAN_POINT('Ctrl Pts',(-2.65626443150014,-0.190604841199624,
13.8669057591701));
#414921=CARTESIAN_POINT('Ctrl Pts',(-2.6590253754494,-0.196340593477848,
13.8637413727084));
#414922=CARTESIAN_POINT('Ctrl Pts',(-2.66260756000972,-0.201303881416225,
13.8597962563956));
#414923=CARTESIAN_POINT('Ctrl Pts',(-2.6665545232739,-0.205392526569279,
13.855546950204));
#414924=CARTESIAN_POINT('Ctrl Pts',(-2.67126172927182,-0.210268704455839,
13.850479165618));
#414925=CARTESIAN_POINT('Ctrl Pts',(-2.67660832504481,-0.214051574227772,
13.8448473071436));
#414926=CARTESIAN_POINT('Ctrl Pts',(-2.68216956901137,-0.21679285741081,
13.8390832900376));
#414927=CARTESIAN_POINT('',(-2.71427576044359,-0.232617945429128,13.8057746032556));
#414928=CARTESIAN_POINT('',(-2.68216956901137,-0.21679285741081,13.8390832900376));
#414929=CARTESIAN_POINT('',(-2.70511846421998,-0.322084005817412,13.8057746032556));
#414930=CARTESIAN_POINT('Origin',(0.,2.5406128344257E-15,13.8057746032556));
#414931=CARTESIAN_POINT('',(-2.67047205618014,-0.33107663329809,13.8390832900376));
#414932=CARTESIAN_POINT('',(-2.70511846421998,-0.322084005817412,13.8057746032556));
#414933=CARTESIAN_POINT('',(-2.65557424054822,-0.434693216983779,13.8390832900376));
#414934=CARTESIAN_POINT('Ctrl Pts',(-2.67047205618014,-0.33107663329809,
13.8390832900376));
#414935=CARTESIAN_POINT('Ctrl Pts',(-2.66372446404708,-0.332828162352686,
13.8455641171218));
#414936=CARTESIAN_POINT('Ctrl Pts',(-2.65695647069315,-0.335931609519436,
13.851896480191));
#414937=CARTESIAN_POINT('Ctrl Pts',(-2.6507606341107,-0.340590229538627,
13.8574481026913));
#414938=CARTESIAN_POINT('Ctrl Pts',(-2.64657275999809,-0.343739072139498,
13.8612005412592));
#414939=CARTESIAN_POINT('Ctrl Pts',(-2.64255870049154,-0.34768680589947,
13.8646714234115));
#414940=CARTESIAN_POINT('Ctrl Pts',(-2.63911397412497,-0.352388834679815,
13.8674635290331));
#414941=CARTESIAN_POINT('Ctrl Pts',(-2.63633779140684,-0.356178305787539,
13.8697137499649));
#414942=CARTESIAN_POINT('Ctrl Pts',(-2.63387765374937,-0.360554650724966,
13.8715630732994));
#414943=CARTESIAN_POINT('Ctrl Pts',(-2.63203193994732,-0.365270931414125,
13.8727429581918));
#414944=CARTESIAN_POINT('Ctrl Pts',(-2.63016495308394,-0.370041570329494,
13.873936442031));
#414945=CARTESIAN_POINT('Ctrl Pts',(-2.62888475679204,-0.375309551147947,
13.8744652622107));
#414946=CARTESIAN_POINT('Ctrl Pts',(-2.62837435816798,-0.380542084706265,
13.8742206332401));
#414947=CARTESIAN_POINT('Ctrl Pts',(-2.62793502568717,-0.385046058347249,
13.8740100655633));
#414948=CARTESIAN_POINT('Ctrl Pts',(-2.62805084552431,-0.389643171262055,
13.8732246156103));
#414949=CARTESIAN_POINT('Ctrl Pts',(-2.62865778202796,-0.393976769528611,
13.8719820486038));
#414950=CARTESIAN_POINT('Ctrl Pts',(-2.62927517745739,-0.398385045759653,
13.8707180692815));
#414951=CARTESIAN_POINT('Ctrl Pts',(-2.63040637230365,-0.402622000623186,
13.868960862563));
#414952=CARTESIAN_POINT('Ctrl Pts',(-2.63188986668393,-0.406480830037446,
13.8669057591701));
#414953=CARTESIAN_POINT('Ctrl Pts',(-2.63417410676116,-0.412422539636349,
13.8637413727084));
#414954=CARTESIAN_POINT('Ctrl Pts',(-2.63733981785397,-0.417661293940601,
13.8597962563956));
#414955=CARTESIAN_POINT('Ctrl Pts',(-2.64094038538639,-0.422058048612047,
13.855546950204));
#414956=CARTESIAN_POINT('Ctrl Pts',(-2.64523447477869,-0.427301682407345,
13.850479165618));
#414957=CARTESIAN_POINT('Ctrl Pts',(-2.65025494119044,-0.431507762183049,
13.8448473071436));
#414958=CARTESIAN_POINT('Ctrl Pts',(-2.65557424054822,-0.434693216983779,
13.8390832900376));
#414959=CARTESIAN_POINT('',(-2.68628370969058,-0.453082600988259,13.8057746032556));
#414960=CARTESIAN_POINT('',(-2.65557424054822,-0.434693216983779,13.8390832900376));
#414961=CARTESIAN_POINT('',(-2.66986456913071,-0.541504565786618,13.8057746032556));
#414962=CARTESIAN_POINT('Origin',(0.,2.5406128344257E-15,13.8057746032556));
#414963=CARTESIAN_POINT('',(-2.63460046153234,-0.547643267144387,13.8390832900376));
#414964=CARTESIAN_POINT('',(-2.66986456913071,-0.541504565786618,13.8057746032556));
#414965=CARTESIAN_POINT('',(-2.61130650365314,-0.649700764917055,13.8390832900376));
#414966=CARTESIAN_POINT('Ctrl Pts',(-2.63460046153233,-0.547643267144386,
13.8390832900376));
#414967=CARTESIAN_POINT('Ctrl Pts',(-2.62773255557711,-0.548838976730111,
13.8455641171218));
#414968=CARTESIAN_POINT('Ctrl Pts',(-2.62073412240766,-0.5513804431431,
13.851896480191));
#414969=CARTESIAN_POINT('Ctrl Pts',(-2.61417918118023,-0.555518543787676,
13.8574481026913));
#414970=CARTESIAN_POINT('Ctrl Pts',(-2.60974858196886,-0.558315558256049,
13.8612005412592));
#414971=CARTESIAN_POINT('Ctrl Pts',(-2.60542610196377,-0.561922973143106,
13.8646714234115));
#414972=CARTESIAN_POINT('Ctrl Pts',(-2.60160957864291,-0.566328579132419,
13.8674635290331));
#414973=CARTESIAN_POINT('Ctrl Pts',(-2.59853375636875,-0.569879156423292,
13.8697137499649));
#414974=CARTESIAN_POINT('Ctrl Pts',(-2.59572509187598,-0.574040415376077,
13.8715630732994));
#414975=CARTESIAN_POINT('Ctrl Pts',(-2.59350109887437,-0.578590560220671,
13.8727429581918));
#414976=CARTESIAN_POINT('Ctrl Pts',(-2.5912514728957,-0.583193148466973,
13.873936442031));
#414977=CARTESIAN_POINT('Ctrl Pts',(-2.5895461470091,-0.588339252631275,
13.8744652622107));
#414978=CARTESIAN_POINT('Ctrl Pts',(-2.58861094663289,-0.593512773139661,
13.8742206332401));
#414979=CARTESIAN_POINT('Ctrl Pts',(-2.58780596033007,-0.597965950504156,
13.8740100655633));
#414980=CARTESIAN_POINT('Ctrl Pts',(-2.58754668740619,-0.602557207296923,
13.8732246156103));
#414981=CARTESIAN_POINT('Ctrl Pts',(-2.5877983758888,-0.606925856832314,
13.8719820486038));
#414982=CARTESIAN_POINT('Ctrl Pts',(-2.5880544015486,-0.611369788346972,
13.8707180692815));
#414983=CARTESIAN_POINT('Ctrl Pts',(-2.58883648128198,-0.615684847974192,
13.868960862563));
#414984=CARTESIAN_POINT('Ctrl Pts',(-2.59000050903621,-0.61965175601599,
13.8669057591701));
#414985=CARTESIAN_POINT('Ctrl Pts',(-2.59179284400056,-0.625759881838503,
13.8637413727084));
#414986=CARTESIAN_POINT('Ctrl Pts',(-2.59452101434085,-0.631239239463067,
13.8597962563956));
#414987=CARTESIAN_POINT('Ctrl Pts',(-2.59775122495862,-0.63591484397598,
13.855546950204));
#414988=CARTESIAN_POINT('Ctrl Pts',(-2.60160362128887,-0.641491038162247,
13.850479165618));
#414989=CARTESIAN_POINT('Ctrl Pts',(-2.60626454796374,-0.646092337174765,
13.8448473071436));
#414990=CARTESIAN_POINT('Ctrl Pts',(-2.61130650365314,-0.649700764917052,
13.8390832900376));
#414991=CARTESIAN_POINT('',(-2.6404148840552,-0.670532066591181,13.8057746032556));
#414992=CARTESIAN_POINT('',(-2.61130650365314,-0.649700764917055,13.8390832900376));
#414993=CARTESIAN_POINT('',(-2.61684316583052,-0.757321502212479,13.8057746032556));
#414994=CARTESIAN_POINT('Origin',(0.,2.5406128344257E-15,13.8057746032556));
#414995=CARTESIAN_POINT('',(-2.58119603549152,-0.760565425402617,13.8390832900376));
#414996=CARTESIAN_POINT('',(-2.61684316583052,-0.757321502212479,13.8057746032556));
#414997=CARTESIAN_POINT('',(-2.54966095281149,-0.860384661452888,13.8390832900376));
#414998=CARTESIAN_POINT('Ctrl Pts',(-2.58119603549151,-0.760565425402616,
13.8390832900376));
#414999=CARTESIAN_POINT('Ctrl Pts',(-2.57425352049513,-0.761197358269454,
13.8455641171218));
#415000=CARTESIAN_POINT('Ctrl Pts',(-2.56707122092824,-0.763159930889019,
13.851896480191));
#415001=CARTESIAN_POINT('Ctrl Pts',(-2.56020079710822,-0.766749973781928,
13.8574481026913));
#415002=CARTESIAN_POINT('Ctrl Pts',(-2.55555695770483,-0.769176546447992,
13.8612005412592));
#415003=CARTESIAN_POINT('Ctrl Pts',(-2.55095482259248,-0.772419635711239,
13.8646714234115));
#415004=CARTESIAN_POINT('Ctrl Pts',(-2.54679190065035,-0.776499500328535,
13.8674635290331));
#415005=CARTESIAN_POINT('Ctrl Pts',(-2.54343690790991,-0.779787555296489,
13.8697137499649));
#415006=CARTESIAN_POINT('Ctrl Pts',(-2.54029840778065,-0.783706035772858,
13.8715630732994));
#415007=CARTESIAN_POINT('Ctrl Pts',(-2.53771093588596,-0.788059764309667,
13.8727429581918));
#415008=CARTESIAN_POINT('Ctrl Pts',(-2.53509364168175,-0.792463672421497,
13.873936442031));
#415009=CARTESIAN_POINT('Ctrl Pts',(-2.53297453486286,-0.797453653457486,
13.8744652622107));
#415010=CARTESIAN_POINT('Ctrl Pts',(-2.53162075633869,-0.802533731990528,
13.8742206332401));
#415011=CARTESIAN_POINT('Ctrl Pts',(-2.5304554732649,-0.806906477917896,
13.8740100655633));
#415012=CARTESIAN_POINT('Ctrl Pts',(-2.52982283299853,-0.811461324532166,
13.8732246156103));
#415013=CARTESIAN_POINT('Ctrl Pts',(-2.52971759851478,-0.81583595269451,
13.8719820486038));
#415014=CARTESIAN_POINT('Ctrl Pts',(-2.52961055059642,-0.820285965861752,
13.8707180692815));
#415015=CARTESIAN_POINT('Ctrl Pts',(-2.53003831060533,-0.824650414242775,
13.868960862563));
#415016=CARTESIAN_POINT('Ctrl Pts',(-2.53087512532085,-0.828699001793586,
13.8669057591701));
#415017=CARTESIAN_POINT('Ctrl Pts',(-2.53216362747886,-0.834932895270131,
13.8637413727084));
#415018=CARTESIAN_POINT('Ctrl Pts',(-2.53443610154312,-0.840616391994046,
13.8597962563956));
#415019=CARTESIAN_POINT('Ctrl Pts',(-2.53727445872754,-0.845539730971813,
13.855546950204));
#415020=CARTESIAN_POINT('Ctrl Pts',(-2.54065952493376,-0.851411376896747,
13.850479165618));
#415021=CARTESIAN_POINT('Ctrl Pts',(-2.54492989417372,-0.856377274260319,
13.8448473071436));
#415022=CARTESIAN_POINT('Ctrl Pts',(-2.54966095281148,-0.860384661452887,
13.8390832900376));
#415023=CARTESIAN_POINT('',(-2.57697453300422,-0.883519251920942,13.8057746032556));
#415024=CARTESIAN_POINT('',(-2.54966095281149,-0.860384661452888,13.8390832900376));
#415025=CARTESIAN_POINT('',(-2.54640710301046,-0.968098588990368,13.8057746032556));
#415026=CARTESIAN_POINT('Origin',(0.,2.5406128344257E-15,13.8057746032556));
#415027=CARTESIAN_POINT('',(-2.51061417570187,-0.968426146239254,13.8390832900376));
#415028=CARTESIAN_POINT('',(-2.54640710301046,-0.968098588990368,13.8057746032556));
#415029=CARTESIAN_POINT('',(-2.47104782899332,-1.06534284002023,13.8390832900376));
#415030=CARTESIAN_POINT('Ctrl Pts',(-2.51061417570186,-0.968426146239253,
13.8390832900376));
#415031=CARTESIAN_POINT('Ctrl Pts',(-2.50364325295619,-0.968490096978238,
13.8455641171218));
#415032=CARTESIAN_POINT('Ctrl Pts',(-2.49632488401048,-0.969860715207392,
13.851896480191));
#415033=CARTESIAN_POINT('Ctrl Pts',(-2.48918469913484,-0.972878809205498,
13.8574481026913));
#415034=CARTESIAN_POINT('Ctrl Pts',(-2.4843585235245,-0.974918791628515,
13.8612005412592));
#415035=CARTESIAN_POINT('Ctrl Pts',(-2.47950735975475,-0.977775973043983,
13.8646714234115));
#415036=CARTESIAN_POINT('Ctrl Pts',(-2.47502574275005,-0.981502945463366,
13.8674635290331));
#415037=CARTESIAN_POINT('Ctrl Pts',(-2.47141390646648,-0.984506596645081,
13.8697137499649));
#415038=CARTESIAN_POINT('Ctrl Pts',(-2.46796645690127,-0.988156221803966,
13.8715630732994));
#415039=CARTESIAN_POINT('Ctrl Pts',(-2.46503272531207,-0.992284560687893,
13.8727429581918));
#415040=CARTESIAN_POINT('Ctrl Pts',(-2.4620651805434,-0.99646048138336,
13.873936442031));
#415041=CARTESIAN_POINT('Ctrl Pts',(-2.45954639509848,-1.00126113179053,
13.8744652622107));
#415042=CARTESIAN_POINT('Ctrl Pts',(-2.45778304759909,-1.00621396126374,
13.8742206332401));
#415043=CARTESIAN_POINT('Ctrl Pts',(-2.45626522252092,-1.01047717585129,
13.8740100655633));
#415044=CARTESIAN_POINT('Ctrl Pts',(-2.45526342502865,-1.01496530053435,
13.8732246156103));
#415045=CARTESIAN_POINT('Ctrl Pts',(-2.45480196789667,-1.01931679489499,
13.8719820486038));
#415046=CARTESIAN_POINT('Ctrl Pts',(-2.45433255878639,-1.02374327561139,
13.8707180692815));
#415047=CARTESIAN_POINT('Ctrl Pts',(-2.45440315239855,-1.02812806806232,
13.868960862563));
#415048=CARTESIAN_POINT('Ctrl Pts',(-2.45490718521148,-1.03223139243996,
13.8669057591701));
#415049=CARTESIAN_POINT('Ctrl Pts',(-2.45568327979387,-1.03854956803797,
13.8637413727084));
#415050=CARTESIAN_POINT('Ctrl Pts',(-2.45748493464214,-1.04439938112825,
13.8597962563956));
#415051=CARTESIAN_POINT('Ctrl Pts',(-2.45991254959444,-1.04953769056227,
13.855546950204));
#415052=CARTESIAN_POINT('Ctrl Pts',(-2.46280775861952,-1.05566571339099,
13.850479165618));
#415053=CARTESIAN_POINT('Ctrl Pts',(-2.46665915182185,-1.06096316187798,
13.8448473071436));
#415054=CARTESIAN_POINT('Ctrl Pts',(-2.47104782899332,-1.06534284002023,
13.8390832900376));
#415055=CARTESIAN_POINT('',(-2.49638484160697,-1.09062676239959,13.8057746032556));
#415056=CARTESIAN_POINT('',(-2.47104782899332,-1.06534284002023,13.8390832900376));
#415057=CARTESIAN_POINT('',(-2.45902512104747,-1.17243313938355,13.8057746032556));
#415058=CARTESIAN_POINT('Origin',(0.,2.5406128344257E-15,13.8057746032556));
#415059=CARTESIAN_POINT('',(-2.42332459279511,-1.16984215085174,13.8390832900376));
#415060=CARTESIAN_POINT('',(-2.45902512104747,-1.17243313938355,13.8057746032556));
#415061=CARTESIAN_POINT('',(-2.3759902895674,-1.26321133775643,13.8390832900376));
#415062=CARTESIAN_POINT('Ctrl Pts',(-2.4233245927951,-1.16984215085174,
13.8390832900376));
#415063=CARTESIAN_POINT('Ctrl Pts',(-2.41637165264089,-1.16933769388125,
13.8455641171218));
#415064=CARTESIAN_POINT('Ctrl Pts',(-2.40896591685425,-1.17010723648182,
13.851896480191));
#415065=CARTESIAN_POINT('Ctrl Pts',(-2.4016034876753,-1.17253329666751,
13.8574481026913));
#415066=CARTESIAN_POINT('Ctrl Pts',(-2.39662709326041,-1.17417311310103,
13.8612005412592));
#415067=CARTESIAN_POINT('Ctrl Pts',(-2.39155918452778,-1.1766253725978,
13.8646714234115));
#415068=CARTESIAN_POINT('Ctrl Pts',(-2.38678869688225,-1.17997465043272,
13.8674635290331));
#415069=CARTESIAN_POINT('Ctrl Pts',(-2.38294405323011,-1.18267390902515,
13.8697137499649));
#415070=CARTESIAN_POINT('Ctrl Pts',(-2.37921059643702,-1.18603039121327,
13.8715630732994));
#415071=CARTESIAN_POINT('Ctrl Pts',(-2.375950128653,-1.18990586703017,13.8727429581918));
#415072=CARTESIAN_POINT('Ctrl Pts',(-2.37265208184071,-1.19382601024602,
13.873936442031));
#415073=CARTESIAN_POINT('Ctrl Pts',(-2.36975037987132,-1.19840538248796,
13.8744652622107));
#415074=CARTESIAN_POINT('Ctrl Pts',(-2.36758919818337,-1.20319800263837,
13.8742206332401));
#415075=CARTESIAN_POINT('Ctrl Pts',(-2.3657289319763,-1.20732331489639,
13.8740100655633));
#415076=CARTESIAN_POINT('Ctrl Pts',(-2.36436464405516,-1.21171484991895,
13.8732246156103));
#415077=CARTESIAN_POINT('Ctrl Pts',(-2.36355003519602,-1.21601425200087,
13.8719820486038));
#415078=CARTESIAN_POINT('Ctrl Pts',(-2.36272138873401,-1.22038774276757,
13.8707180692815));
#415079=CARTESIAN_POINT('Ctrl Pts',(-2.36243434616056,-1.22476369921809,
13.868960862563));
#415080=CARTESIAN_POINT('Ctrl Pts',(-2.36260224281571,-1.22889445347584,
13.8669057591701));
#415081=CARTESIAN_POINT('Ctrl Pts',(-2.36286076504108,-1.23525486477913,
13.8637413727084));
#415082=CARTESIAN_POINT('Ctrl Pts',(-2.3641796109576,-1.24123206469481,
13.8597962563956));
#415083=CARTESIAN_POINT('Ctrl Pts',(-2.3661803283008,-1.24655114998356,
13.855546950204));
#415084=CARTESIAN_POINT('Ctrl Pts',(-2.36856641300636,-1.2528947687352,
13.850479165618));
#415085=CARTESIAN_POINT('Ctrl Pts',(-2.37197319978472,-1.25848851469993,
13.8448473071436));
#415086=CARTESIAN_POINT('Ctrl Pts',(-2.3759902895674,-1.26321133775643,
13.8390832900376));
#415087=CARTESIAN_POINT('',(-2.39918212096334,-1.29047633171521,13.8057746032556));
#415088=CARTESIAN_POINT('',(-2.3759902895674,-1.26321133775643,13.8390832900376));
#415089=CARTESIAN_POINT('',(-2.35527873261449,-1.36896534067199,13.8057746032556));
#415090=CARTESIAN_POINT('Origin',(0.,2.5406128344257E-15,13.8057746032556));
#415091=CARTESIAN_POINT('',(-2.31990818454371,-1.36347304896067,13.8390832900376));
#415092=CARTESIAN_POINT('',(-2.35527873261449,-1.36896534067199,13.8057746032556));
#415093=CARTESIAN_POINT('',(-2.26512092677521,-1.45267337245507,13.8390832900376));
#415094=CARTESIAN_POINT('Ctrl Pts',(-2.3199081845437,-1.36347304896067,
13.8390832900376));
#415095=CARTESIAN_POINT('Ctrl Pts',(-2.31301949765052,-1.36240354135862,
13.8455641171218));
#415096=CARTESIAN_POINT('Ctrl Pts',(-2.30557567897275,-1.36256688715156,
13.851896480191));
#415097=CARTESIAN_POINT('Ctrl Pts',(-2.29804000124195,-1.36438476849458,
13.8574481026913));
#415098=CARTESIAN_POINT('Ctrl Pts',(-2.29294650510632,-1.36561350623079,
13.8612005412592));
#415099=CARTESIAN_POINT('Ctrl Pts',(-2.28769557750727,-1.3676445244265,
13.8646714234115));
#415100=CARTESIAN_POINT('Ctrl Pts',(-2.28266796602911,-1.37059381878557,
13.8674635290331));
#415101=CARTESIAN_POINT('Ctrl Pts',(-2.27861610047759,-1.37297072166812,
13.8697137499649));
#415102=CARTESIAN_POINT('Ctrl Pts',(-2.27462148199559,-1.37601172405029,
13.8715630732994));
#415103=CARTESIAN_POINT('Ctrl Pts',(-2.27105597589192,-1.37960854614801,
13.8727429581918));
#415104=CARTESIAN_POINT('Ctrl Pts',(-2.2674493749934,-1.38324682397793,
13.873936442031));
#415105=CARTESIAN_POINT('Ctrl Pts',(-2.26418406684741,-1.38757444308791,
13.8744652622107));
#415106=CARTESIAN_POINT('Ctrl Pts',(-2.26163943327847,-1.39217495981913,
13.8742206332401));
#415107=CARTESIAN_POINT('Ctrl Pts',(-2.25944910570718,-1.39613491647519,
13.8740100655633));
#415108=CARTESIAN_POINT('Ctrl Pts',(-2.25773140646819,-1.40040063689623,
13.8732246156103));
#415109=CARTESIAN_POINT('Ctrl Pts',(-2.25656906696945,-1.40461933488791,
13.8719820486038));
#415110=CARTESIAN_POINT('Ctrl Pts',(-2.25538669766119,-1.40891073084545,
13.8707180692815));
#415111=CARTESIAN_POINT('Ctrl Pts',(-2.25474392912311,-1.41324873002736,
13.868960862563));
#415112=CARTESIAN_POINT('Ctrl Pts',(-2.25457457229593,-1.41737942467715,
13.8669057591701));
#415113=CARTESIAN_POINT('Ctrl Pts',(-2.25431380174153,-1.4237397441979,
13.8637413727084));
#415114=CARTESIAN_POINT('Ctrl Pts',(-2.25514106202431,-1.42980455365971,
13.8597962563956));
#415115=CARTESIAN_POINT('Ctrl Pts',(-2.25670156731458,-1.43526901716817,
13.855546950204));
#415116=CARTESIAN_POINT('Ctrl Pts',(-2.25856264870058,-1.44178601610656,
13.850479165618));
#415117=CARTESIAN_POINT('Ctrl Pts',(-2.26150215745105,-1.44763883409255,
13.8448473071436));
#415118=CARTESIAN_POINT('Ctrl Pts',(-2.26512092677521,-1.45267337245507,
13.8390832900376));
#415119=CARTESIAN_POINT('',(-2.28601323914187,-1.48173799395688,13.8057746032556));
#415120=CARTESIAN_POINT('',(-2.26512092677521,-1.45267337245507,13.8390832900376));
#415121=CARTESIAN_POINT('',(-2.2358583528096,-1.55638730348163,13.8057746032556));
#415122=CARTESIAN_POINT('Origin',(0.,2.5406128344257E-15,13.8057746032556));
#415123=CARTESIAN_POINT('',(-2.20105317008208,-1.54803025888599,13.8390832900376));
#415124=CARTESIAN_POINT('',(-2.2358583528096,-1.55638730348163,13.8057746032556));
#415125=CARTESIAN_POINT('',(-2.13917755793398,-1.63246810553425,13.8390832900376));
#415126=CARTESIAN_POINT('Ctrl Pts',(-2.20105317008207,-1.54803025888599,
13.8390832900376));
#415127=CARTESIAN_POINT('Ctrl Pts',(-2.19427457952464,-1.54640281804902,
13.8455641171218));
#415128=CARTESIAN_POINT('Ctrl Pts',(-2.18684221534089,-1.54595887999502,
13.851896480191));
#415129=CARTESIAN_POINT('Ctrl Pts',(-2.17918343775026,-1.54715648479496,
13.8574481026913));
#415130=CARTESIAN_POINT('Ctrl Pts',(-2.17400673627028,-1.54796596678695,
13.8612005412592));
#415131=CARTESIAN_POINT('Ctrl Pts',(-2.16860773386164,-1.54956222759061,
13.8646714234115));
#415132=CARTESIAN_POINT('Ctrl Pts',(-2.16335645647575,-1.55209191140646,
13.8674635290331));
#415133=CARTESIAN_POINT('Ctrl Pts',(-2.15912433352158,-1.55413064068262,
13.8697137499649));
#415134=CARTESIAN_POINT('Ctrl Pts',(-2.15489513687762,-1.55683592588971,
13.8715630732994));
#415135=CARTESIAN_POINT('Ctrl Pts',(-2.15104832030914,-1.56013015801062,
13.8727429581918));
#415136=CARTESIAN_POINT('Ctrl Pts',(-2.14715716665832,-1.56346235831592,
13.873936442031));
#415137=CARTESIAN_POINT('Ctrl Pts',(-2.1435499824227,-1.56750942470278,
13.8744652622107));
#415138=CARTESIAN_POINT('Ctrl Pts',(-2.14063883108934,-1.571887222335,13.8742206332401));
#415139=CARTESIAN_POINT('Ctrl Pts',(-2.13813301842244,-1.57565547053088,
13.8740100655633));
#415140=CARTESIAN_POINT('Ctrl Pts',(-2.13607333887064,-1.57976698868481,
13.8732246156103));
#415141=CARTESIAN_POINT('Ctrl Pts',(-2.13457100390989,-1.58387690784716,
13.8719820486038));
#415142=CARTESIAN_POINT('Ctrl Pts',(-2.13304278022804,-1.58805765046345,
13.8707180692815));
#415143=CARTESIAN_POINT('Ctrl Pts',(-2.13204856324391,-1.59232882370792,
13.868960862563));
#415144=CARTESIAN_POINT('Ctrl Pts',(-2.13154307997614,-1.59643196965837,
13.8669057591701));
#415145=CARTESIAN_POINT('Ctrl Pts',(-2.13076475202698,-1.60274987051955,
13.8637413727084));
#415146=CARTESIAN_POINT('Ctrl Pts',(-2.13109492139534,-1.60886192922114,
13.8597962563956));
#415147=CARTESIAN_POINT('Ctrl Pts',(-2.13220482972745,-1.61443540584625,
13.855546950204));
#415148=CARTESIAN_POINT('Ctrl Pts',(-2.13352852260432,-1.62108241541868,
13.850479165618));
#415149=CARTESIAN_POINT('Ctrl Pts',(-2.13598119138114,-1.62715535588788,
13.8448473071436));
#415150=CARTESIAN_POINT('Ctrl Pts',(-2.13917755793398,-1.63246810553424,
13.8390832900376));
#415151=CARTESIAN_POINT('',(-2.15763131637956,-1.66313893431832,13.8057746032556));
#415152=CARTESIAN_POINT('',(-2.13917755793398,-1.63246810553425,13.8390832900376));
#415153=CARTESIAN_POINT('',(-2.10155870455742,-1.73345176557244,13.8057746032556));
#415154=CARTESIAN_POINT('Origin',(0.,2.5406128344257E-15,13.8057746032556));
#415155=CARTESIAN_POINT('',(-2.06755050992176,-1.72228558284544,13.8390832900376));
#415156=CARTESIAN_POINT('',(-2.10155870455742,-1.73345176557244,13.8057746032556));
#415157=CARTESIAN_POINT('',(-1.99899831538416,-1.80139903270938,13.8390832900376));
#415158=CARTESIAN_POINT('Ctrl Pts',(-2.06755050992176,-1.72228558284543,
13.8390832900376));
#415159=CARTESIAN_POINT('Ctrl Pts',(-2.06092712610185,-1.7201110391238,
13.8455641171218));
#415160=CARTESIAN_POINT('Ctrl Pts',(-2.05355567756952,-1.71906277155738,
13.851896480191));
#415161=CARTESIAN_POINT('Ctrl Pts',(-2.04582476802029,-1.71963212995188,
13.8574481026913));
#415162=CARTESIAN_POINT('Ctrl Pts',(-2.04059931129023,-1.72001696923055,
13.8612005412592));
#415163=CARTESIAN_POINT('Ctrl Pts',(-2.03508816354226,-1.72116784978987,
13.8646714234115));
#415164=CARTESIAN_POINT('Ctrl Pts',(-2.02964816663325,-1.72326108843407,
13.8674635290331));
#415165=CARTESIAN_POINT('Ctrl Pts',(-2.02526395035643,-1.72494807669687,
13.8697137499649));
#415166=CARTESIAN_POINT('Ctrl Pts',(-2.02082832015639,-1.72729964150218,
13.8715630732994));
#415167=CARTESIAN_POINT('Ctrl Pts',(-2.01672579305269,-1.73026936107504,
13.8727429581918));
#415168=CARTESIAN_POINT('Ctrl Pts',(-2.01257598163513,-1.73327330861246,
13.873936442031));
#415169=CARTESIAN_POINT('Ctrl Pts',(-2.00865092652582,-1.7370128897171,
13.8744652622107));
#415170=CARTESIAN_POINT('Ctrl Pts',(-2.00539263065985,-1.74113883472936,
13.8742206332401));
#415171=CARTESIAN_POINT('Ctrl Pts',(-2.00258800866722,-1.74469029739505,
13.8740100655633));
#415172=CARTESIAN_POINT('Ctrl Pts',(-2.00020005563019,-1.74862025180689,
13.8732246156103));
#415173=CARTESIAN_POINT('Ctrl Pts',(-1.99836772299873,-1.75259404130597,
13.8719820486038));
#415174=CARTESIAN_POINT('Ctrl Pts',(-1.99650381501977,-1.7566363084287,
13.8707180692815));
#415175=CARTESIAN_POINT('Ctrl Pts',(-1.99516476593957,-1.76081223178248,
13.868960862563));
#415176=CARTESIAN_POINT('Ctrl Pts',(-1.99432652013897,-1.76486052327426,
13.8669057591701));
#415177=CARTESIAN_POINT('Ctrl Pts',(-1.99303581443913,-1.77109396088801,
13.8637413727084));
#415178=CARTESIAN_POINT('Ctrl Pts',(-1.99286669567039,-1.77721259408715,
13.8597962563956));
#415179=CARTESIAN_POINT('Ctrl Pts',(-1.9935186207875,-1.78285799326152,
13.855546950204));
#415180=CARTESIAN_POINT('Ctrl Pts',(-1.99429611619754,-1.78959077871597,
13.850479165618));
#415181=CARTESIAN_POINT('Ctrl Pts',(-1.99624562289467,-1.79584342725151,
13.8448473071436));
#415182=CARTESIAN_POINT('Ctrl Pts',(-1.99899831538415,-1.80139903270938,
13.8390832900376));
#415183=CARTESIAN_POINT('',(-2.01489071319085,-1.83347195947049,13.8057746032556));
#415184=CARTESIAN_POINT('',(-1.99899831538416,-1.80139903270938,13.8390832900376));
#415185=CARTESIAN_POINT('',(-1.95327352985919,-1.89898039216277,13.8057746032556));
#415186=CARTESIAN_POINT('Origin',(0.,2.5406128344257E-15,13.8057746032556));
#415187=CARTESIAN_POINT('',(-1.92028864223974,-1.88507938040817,13.8390832900376));
#415188=CARTESIAN_POINT('',(-1.95327352985919,-1.89898039216277,13.8057746032556));
#415189=CARTESIAN_POINT('',(-1.84551606885696,-1.95834194653175,13.8390832900376));
#415190=CARTESIAN_POINT('Ctrl Pts',(-1.92028864223974,-1.88507938040816,
13.8390832900376));
#415191=CARTESIAN_POINT('Ctrl Pts',(-1.91386454268389,-1.88237220503155,
13.8455641171218));
#415192=CARTESIAN_POINT('Ctrl Pts',(-1.90660306557675,-1.88072658400041,
13.851896480191));
#415193=CARTESIAN_POINT('Ctrl Pts',(-1.89885147199648,-1.8806639070033,
13.8574481026913));
#415194=CARTESIAN_POINT('Ctrl Pts',(-1.89361203456873,-1.88062154252675,
13.8612005412592));
#415195=CARTESIAN_POINT('Ctrl Pts',(-1.88802541726042,-1.88131938392148,
13.8646714234115));
#415196=CARTESIAN_POINT('Ctrl Pts',(-1.88243290311017,-1.88296224723623,
13.8674635290331));
#415197=CARTESIAN_POINT('Ctrl Pts',(-1.87792576974669,-1.88428626785711,
13.8697137499649));
#415198=CARTESIAN_POINT('Ctrl Pts',(-1.87331322437773,-1.88626846298484,
13.8715630732994));
#415199=CARTESIAN_POINT('Ctrl Pts',(-1.86898228837981,-1.88889390701584,
13.8727429581918));
#415200=CARTESIAN_POINT('Ctrl Pts',(-1.86460143550582,-1.89154961101014,
13.873936442031));
#415201=CARTESIAN_POINT('Ctrl Pts',(-1.86038463011699,-1.89495682053731,
13.8744652622107));
#415202=CARTESIAN_POINT('Ctrl Pts',(-1.85680087313982,-1.89880345544629,
13.8742206332401));
#415203=CARTESIAN_POINT('Ctrl Pts',(-1.85371610611807,-1.90211449818369,
13.8740100655633));
#415204=CARTESIAN_POINT('Ctrl Pts',(-1.85101577102931,-1.90583673565523,
13.8732246156103));
#415205=CARTESIAN_POINT('Ctrl Pts',(-1.84886563459848,-1.90964795057756,
13.8719820486038));
#415206=CARTESIAN_POINT('Ctrl Pts',(-1.84667844632248,-1.91352484158593,
13.8707180692815));
#415207=CARTESIAN_POINT('Ctrl Pts',(-1.84500347629691,-1.91757772496808,
13.868960862563));
#415208=CARTESIAN_POINT('Ctrl Pts',(-1.84383804635098,-1.92154422128925,
13.8669057591701));
#415209=CARTESIAN_POINT('Ctrl Pts',(-1.84204355233396,-1.9276517131567,
13.8637413727084));
#415210=CARTESIAN_POINT('Ctrl Pts',(-1.84137627088561,-1.93373620235893,
13.8597962563956));
#415211=CARTESIAN_POINT('Ctrl Pts',(-1.84156587433364,-1.93941595488249,
13.855546950204));
#415212=CARTESIAN_POINT('Ctrl Pts',(-1.84179199817318,-1.94618971064259,
13.850479165618));
#415213=CARTESIAN_POINT('Ctrl Pts',(-1.84322536914519,-1.95258045690009,
13.8448473071436));
#415214=CARTESIAN_POINT('Ctrl Pts',(-1.84551606885695,-1.95834194653174,
13.8390832900376));
#415215=CARTESIAN_POINT('',(-1.85874134473942,-1.99160353123396,13.8057746032556));
#415216=CARTESIAN_POINT('',(-1.84551606885696,-1.95834194653175,13.8390832900376));
#415217=CARTESIAN_POINT('',(-1.7919896420872,-2.05187161755297,13.8057746032556));
#415218=CARTESIAN_POINT('Origin',(0.,2.5406128344257E-15,13.8057746032556));
#415219=CARTESIAN_POINT('',(-1.76024757046894,-2.03532828571048,13.8390832900376));
#415220=CARTESIAN_POINT('',(-1.7919896420872,-2.05187161755297,13.8057746032556));
#415221=CARTESIAN_POINT('',(-1.67975221738023,-2.10225241780362,13.8390832900376));
#415222=CARTESIAN_POINT('Ctrl Pts',(-1.76024757046894,-2.03532828571048,
13.8390832900376));
#415223=CARTESIAN_POINT('Ctrl Pts',(-1.7540655064998,-2.03210649448438,
13.8455641171218));
#415224=CARTESIAN_POINT('Ctrl Pts',(-1.74696232474994,-2.02987447132497,
13.851896480191));
#415225=CARTESIAN_POINT('Ctrl Pts',(-1.73924163271497,-2.02918017604132,
13.8574481026913));
#415226=CARTESIAN_POINT('Ctrl Pts',(-1.73402308218118,-2.02871088973814,
13.8612005412592));
#415227=CARTESIAN_POINT('Ctrl Pts',(-1.72839817332898,-2.02895104794895,
13.8646714234115));
#415228=CARTESIAN_POINT('Ctrl Pts',(-1.72269035919646,-2.03013260294993,
13.8674635290331));
#415229=CARTESIAN_POINT('Ctrl Pts',(-1.71809030297523,-2.03108484479011,
13.8697137499649));
#415230=CARTESIAN_POINT('Ctrl Pts',(-1.71333153816577,-2.03268447905872,
13.8715630732994));
#415231=CARTESIAN_POINT('Ctrl Pts',(-1.70880101493814,-2.03494817565101,
13.8727429581918));
#415232=CARTESIAN_POINT('Ctrl Pts',(-1.70421827446081,-2.03723796283027,
13.873936442031));
#415233=CARTESIAN_POINT('Ctrl Pts',(-1.69973778093659,-2.04029012636271,
13.8744652622107));
#415234=CARTESIAN_POINT('Ctrl Pts',(-1.69585241215962,-2.04383185244774,
13.8742206332401));
#415235=CARTESIAN_POINT('Ctrl Pts',(-1.69250802872435,-2.04688044081372,
13.8740100655633));
#415236=CARTESIAN_POINT('Ctrl Pts',(-1.68951328186832,-2.05037019046872,
13.8732246156103));
#415237=CARTESIAN_POINT('Ctrl Pts',(-1.68705965044134,-2.05399346780779,
13.8719820486038));
#415238=CARTESIAN_POINT('Ctrl Pts',(-1.68456373724541,-2.05767918263179,
13.8707180692815));
#415239=CARTESIAN_POINT('Ctrl Pts',(-1.68256399292365,-2.06158205477208,
13.868960862563));
#415240=CARTESIAN_POINT('Ctrl Pts',(-1.68107913457639,-2.06544035954403,
13.8669057591701));
#415241=CARTESIAN_POINT('Ctrl Pts',(-1.67879279430379,-2.07138126131447,
13.8637413727084));
#415242=CARTESIAN_POINT('Ctrl Pts',(-1.67763179082379,-2.07739111524804,
13.8597962563956));
#415243=CARTESIAN_POINT('Ctrl Pts',(-1.67735781082307,-2.08306742330483,
13.855546950204));
#415244=CARTESIAN_POINT('Ctrl Pts',(-1.67703105827525,-2.08983707114359,
13.850479165618));
#415245=CARTESIAN_POINT('Ctrl Pts',(-1.67793875467482,-2.0963233857611,
13.8448473071436));
#415246=CARTESIAN_POINT('Ctrl Pts',(-1.67975221738023,-2.10225241780362,
13.8390832900376));
#415247=CARTESIAN_POINT('',(-1.69022235930949,-2.13648131008852,13.8057746032556));
#415248=CARTESIAN_POINT('',(-1.67975221738023,-2.10225241780362,13.8390832900376));
#415249=CARTESIAN_POINT('',(-1.6187803589046,-2.19110797586335,13.8057746032556));
#415250=CARTESIAN_POINT('Origin',(0.,2.5406128344257E-15,13.8057746032556));
#415251=CARTESIAN_POINT('',(-1.58849234153707,-2.17203241707693,13.8390832900376));
#415252=CARTESIAN_POINT('',(-1.6187803589046,-2.19110797586335,13.8057746032556));
#415253=CARTESIAN_POINT('',(-1.50280989203645,-2.23217274608225,13.8390832900376));
#415254=CARTESIAN_POINT('Ctrl Pts',(-1.58849234153707,-2.17203241707693,
13.8390832900376));
#415255=CARTESIAN_POINT('Ctrl Pts',(-1.58259345377038,-2.16831745049039,
13.8455641171218));
#415256=CARTESIAN_POINT('Ctrl Pts',(-1.57569583788041,-2.16551387894857,
13.851896480191));
#415257=CARTESIAN_POINT('Ctrl Pts',(-1.56805742732242,-2.16419258579895,
13.8574481026913));
#415258=CARTESIAN_POINT('Ctrl Pts',(-1.56289449227537,-2.16329950069206,
13.8612005412592));
#415259=CARTESIAN_POINT('Ctrl Pts',(-1.55726872471966,-2.16308037750568,
13.8646714234115));
#415260=CARTESIAN_POINT('Ctrl Pts',(-1.5514835951662,-2.1637927611393,13.8674635290331));
#415261=CARTESIAN_POINT('Ctrl Pts',(-1.54682122870241,-2.16436688718645,
13.8697137499649));
#415262=CARTESIAN_POINT('Ctrl Pts',(-1.54194791324711,-2.1655733152938,
13.8715630732994));
#415263=CARTESIAN_POINT('Ctrl Pts',(-1.53724795267438,-2.16746019992005,
13.8727429581918));
#415264=CARTESIAN_POINT('Ctrl Pts',(-1.53249382197548,-2.16936883212836,
13.873936442031));
#415265=CARTESIAN_POINT('Ctrl Pts',(-1.52777945726104,-2.17204563802134,
13.8744652622107));
#415266=CARTESIAN_POINT('Ctrl Pts',(-1.52361833317245,-2.17525888567967,
13.8742206332401));
#415267=CARTESIAN_POINT('Ctrl Pts',(-1.52003658964363,-2.17802473182164,
13.8740100655633));
#415268=CARTESIAN_POINT('Ctrl Pts',(-1.51676736056658,-2.1812587699519,
13.8732246156103));
#415269=CARTESIAN_POINT('Ctrl Pts',(-1.51402656265576,-2.18466999739483,
13.8719820486038));
#415270=CARTESIAN_POINT('Ctrl Pts',(-1.51123853443043,-2.18814000821041,
13.8707180692815));
#415271=CARTESIAN_POINT('Ctrl Pts',(-1.508927323781,-2.19186689613867,13.868960862563));
#415272=CARTESIAN_POINT('Ctrl Pts',(-1.50713291851973,-2.19559133297972,
13.8669057591701));
#415273=CARTESIAN_POINT('Ctrl Pts',(-1.50436994720885,-2.20132610893205,
13.8637413727084));
#415274=CARTESIAN_POINT('Ctrl Pts',(-1.50272294798381,-2.20722133301058,
13.8597962563956));
#415275=CARTESIAN_POINT('Ctrl Pts',(-1.50198720782604,-2.21285642170701,
13.855546950204));
#415276=CARTESIAN_POINT('Ctrl Pts',(-1.50110975337516,-2.21957691073497,
13.850479165618));
#415277=CARTESIAN_POINT('Ctrl Pts',(-1.50148573463251,-2.22611562835888,
13.8448473071436));
#415278=CARTESIAN_POINT('Ctrl Pts',(-1.50280989203645,-2.23217274608225,
13.8390832900376));
#415279=CARTESIAN_POINT('',(-1.51045522294541,-2.26714115831904,13.8057746032556));
#415280=CARTESIAN_POINT('',(-1.50280989203645,-2.23217274608225,13.8390832900376));
#415281=CARTESIAN_POINT('',(-1.43479835951345,-2.31576287210172,13.8057746032556));
#415282=CARTESIAN_POINT('Origin',(0.,2.5406128344257E-15,13.8057746032556));
#415283=CARTESIAN_POINT('',(-1.40616595815507,-2.29428203106785,13.8390832900376));
#415284=CARTESIAN_POINT('',(-1.43479835951345,-2.31576287210172,13.8057746032556));
#415285=CARTESIAN_POINT('',(-1.31586661480734,-2.34723833301828,13.8390832900376));
#415286=CARTESIAN_POINT('Ctrl Pts',(-1.40616595815506,-2.29428203106785,
13.8390832900376));
#415287=CARTESIAN_POINT('Ctrl Pts',(-1.40058950271566,-2.29009861161057,
13.8455641171218));
#415288=CARTESIAN_POINT('Ctrl Pts',(-1.3939433551813,-2.28674214899241,
13.851896480191));
#415289=CARTESIAN_POINT('Ctrl Pts',(-1.38643805846229,-2.28480265096473,
13.8574481026913));
#415290=CARTESIAN_POINT('Ctrl Pts',(-1.38136509738292,-2.28349171038817,
13.8612005412592));
#415291=CARTESIAN_POINT('Ctrl Pts',(-1.37577590967858,-2.28281476403325,
13.8646714234115));
#415292=CARTESIAN_POINT('Ctrl Pts',(-1.36995196378689,-2.28305323550397,
13.8674635290331));
#415293=CARTESIAN_POINT('Ctrl Pts',(-1.36525831436012,-2.28324542504396,
13.8697137499649));
#415294=CARTESIAN_POINT('Ctrl Pts',(-1.36030287936929,-2.28405061841004,
13.8715630732994));
#415295=CARTESIAN_POINT('Ctrl Pts',(-1.35546475891363,-2.28554813416437,
13.8727429581918));
#415296=CARTESIAN_POINT('Ctrl Pts',(-1.35057087594858,-2.28706290976931,
13.873936442031));
#415297=CARTESIAN_POINT('Ctrl Pts',(-1.3456540133633,-2.28934654432125,
13.8744652622107));
#415298=CARTESIAN_POINT('Ctrl Pts',(-1.34124482555735,-2.29220992991985,
13.8742206332401));
#415299=CARTESIAN_POINT('Ctrl Pts',(-1.33744955784721,-2.29467462758807,
13.8740100655632));
#415300=CARTESIAN_POINT('Ctrl Pts',(-1.33392760272927,-2.29763143220342,
13.8732246156103));
#415301=CARTESIAN_POINT('Ctrl Pts',(-1.3309178778925,-2.30080790859438,
13.8719820486038));
#415302=CARTESIAN_POINT('Ctrl Pts',(-1.32785628850562,-2.30403912305207,
13.8707180692815));
#415303=CARTESIAN_POINT('Ctrl Pts',(-1.32524899225408,-2.30756522494404,
13.868960862563));
#415304=CARTESIAN_POINT('Ctrl Pts',(-1.32315698154976,-2.31113100834151,
13.8669057591701));
#415305=CARTESIAN_POINT('Ctrl Pts',(-1.3199357663188,-2.31662149448792,
13.8637413727084));
#415306=CARTESIAN_POINT('Ctrl Pts',(-1.31781373185682,-2.32236285696783,
13.8597962563956));
#415307=CARTESIAN_POINT('Ctrl Pts',(-1.31662112777136,-2.32791922571834,
13.855546950204));
#415308=CARTESIAN_POINT('Ctrl Pts',(-1.31519881073203,-2.33454583218982,
13.850479165618));
#415309=CARTESIAN_POINT('Ctrl Pts',(-1.31504057475392,-2.34109343873316,
13.8448473071436));
#415310=CARTESIAN_POINT('Ctrl Pts',(-1.31586661480734,-2.34723833301828,
13.8390832900376));
#415311=CARTESIAN_POINT('',(-1.3206362562802,-2.38271355619292,13.8057746032556));
#415312=CARTESIAN_POINT('',(-1.31586661480734,-2.34723833301828,13.8390832900376));
#415313=CARTESIAN_POINT('',(-1.2412680137648,-2.42500674850023,13.8057746032556));
#415314=CARTESIAN_POINT('Origin',(0.,2.5406128344257E-15,13.8057746032556));
#415315=CARTESIAN_POINT('',(-1.21448177232259,-2.40126357667191,13.8390832900376));
#415316=CARTESIAN_POINT('',(-1.2412680137648,-2.42500674850023,13.8057746032556));
#415317=CARTESIAN_POINT('',(-1.1201664623594,-2.44668343611514,13.8390832900376));
#415318=CARTESIAN_POINT('Ctrl Pts',(-1.21448177232259,-2.40126357667191,
13.8390832900376));
#415319=CARTESIAN_POINT('Ctrl Pts',(-1.20926485960137,-2.39663954431017,
13.8455641171218));
#415320=CARTESIAN_POINT('Ctrl Pts',(-1.20291440943792,-2.39275252732061,
13.851896480191));
#415321=CARTESIAN_POINT('Ctrl Pts',(-1.19559217306928,-2.39020773145424,
13.8574481026913));
#415322=CARTESIAN_POINT('Ctrl Pts',(-1.19064294567658,-2.38848765950126,
13.8612005412592));
#415323=CARTESIAN_POINT('Ctrl Pts',(-1.18512753294564,-2.3873573949441,
13.8646714234115));
#415324=CARTESIAN_POINT('Ctrl Pts',(-1.17930352811473,-2.38712036726362,
13.8674635290331));
#415325=CARTESIAN_POINT('Ctrl Pts',(-1.17460983118752,-2.38692934130678,
13.8697137499649));
#415326=CARTESIAN_POINT('Ctrl Pts',(-1.16960525426345,-2.38732794150259,
13.8715630732994));
#415327=CARTESIAN_POINT('Ctrl Pts',(-1.16466117081825,-2.38842612266473,
13.8727429581918));
#415328=CARTESIAN_POINT('Ctrl Pts',(-1.15966010357076,-2.38953696108456,
13.873936442031));
#415329=CARTESIAN_POINT('Ctrl Pts',(-1.1545734640239,-2.39141222708429,
13.8744652622107));
#415330=CARTESIAN_POINT('Ctrl Pts',(-1.14994555491799,-2.39390669526444,
13.8742206332401));
#415331=CARTESIAN_POINT('Ctrl Pts',(-1.14596201990697,-2.39605384230257,
13.8740100655633));
#415332=CARTESIAN_POINT('Ctrl Pts',(-1.14221077677835,-2.39871373635613,
13.8732246156103));
#415333=CARTESIAN_POINT('Ctrl Pts',(-1.13895215423787,-2.40163432276882,
13.8719820486038));
#415334=CARTESIAN_POINT('Ctrl Pts',(-1.13563737806167,-2.40460523766952,
13.8707180692815));
#415335=CARTESIAN_POINT('Ctrl Pts',(-1.13275134733439,-2.40790708789886,
13.868960862563));
#415336=CARTESIAN_POINT('Ctrl Pts',(-1.1303756531731,-2.41129048815256,
13.8669057591701));
#415337=CARTESIAN_POINT('Ctrl Pts',(-1.12671763067797,-2.41650014621362,
13.8637413727084));
#415338=CARTESIAN_POINT('Ctrl Pts',(-1.12413468276829,-2.42204943927485,
13.8597962563956));
#415339=CARTESIAN_POINT('Ctrl Pts',(-1.12249315133856,-2.42749011136215,
13.855546950204));
#415340=CARTESIAN_POINT('Ctrl Pts',(-1.12053543699601,-2.43397873630441,
13.850479165618));
#415341=CARTESIAN_POINT('Ctrl Pts',(-1.11984403681677,-2.4404916585259,
13.8448473071436));
#415342=CARTESIAN_POINT('Ctrl Pts',(-1.1201664623594,-2.44668343611514,
13.8390832900376));
#415343=CARTESIAN_POINT('',(-1.12202867321909,-2.48242938847039,13.8057746032556));
#415344=CARTESIAN_POINT('',(-1.1201664623594,-2.44668343611514,13.8390832900376));
#415345=CARTESIAN_POINT('',(-1.03947723417935,-2.51811260508543,13.8057746032556));
#415346=CARTESIAN_POINT('Origin',(0.,2.5406128344257E-15,13.8057746032556));
#415347=CARTESIAN_POINT('',(-1.01471541067069,-2.49226510935382,13.8390832900376));
#415348=CARTESIAN_POINT('',(-1.03947723417935,-2.51811260508543,13.8057746032556));
#415349=CARTESIAN_POINT('',(-0.917011786918914,-2.52984626461901,13.8390832900376));
#415350=CARTESIAN_POINT('Ctrl Pts',(-1.01471541067069,-2.49226510935381,
13.8390832900376));
#415351=CARTESIAN_POINT('Ctrl Pts',(-1.0098927583611,-2.48723123626007,
13.8455641171218));
#415352=CARTESIAN_POINT('Ctrl Pts',(-1.00388026676664,-2.48283953235586,
13.851896480191));
#415353=CARTESIAN_POINT('Ctrl Pts',(-0.996789819023321,-2.47970637384743,
13.8574481026913));
#415354=CARTESIAN_POINT('Ctrl Pts',(-0.991997261609015,-2.4775886173131,
13.8612005412592));
#415355=CARTESIAN_POINT('Ctrl Pts',(-0.986592328013226,-2.47601255627784,
13.8646714234115));
#415356=CARTESIAN_POINT('Ctrl Pts',(-0.980807022034365,-2.47530160682628,
13.8674635290331));
#415357=CARTESIAN_POINT('Ctrl Pts',(-0.976144513385357,-2.47472863661882,
13.8697137499649));
#415358=CARTESIAN_POINT('Ctrl Pts',(-0.971124099161771,-2.47471799102583,
13.8715630732994));
#415359=CARTESIAN_POINT('Ctrl Pts',(-0.966106954786642,-2.47540952938133,
13.8727429581918));
#415360=CARTESIAN_POINT('Ctrl Pts',(-0.961031984534124,-2.47610903816964,
13.873936442031));
#415361=CARTESIAN_POINT('Ctrl Pts',(-0.955809418772643,-2.47756345603133,
13.8744652622107));
#415362=CARTESIAN_POINT('Ctrl Pts',(-0.95099358633831,-2.47967240651884,
13.8742206332401));
#415363=CARTESIAN_POINT('Ctrl Pts',(-0.946848293794672,-2.4814877140176,
13.8740100655632));
#415364=CARTESIAN_POINT('Ctrl Pts',(-0.942892726559494,-2.4838329963533,
13.8732246156103));
#415365=CARTESIAN_POINT('Ctrl Pts',(-0.939406891910658,-2.48647825676701,
13.8719820486038));
#415366=CARTESIAN_POINT('Ctrl Pts',(-0.935860988233707,-2.48916910116222,
13.8707180692815));
#415367=CARTESIAN_POINT('Ctrl Pts',(-0.932715429089015,-2.49222472646043,
13.868960862563));
#415368=CARTESIAN_POINT('Ctrl Pts',(-0.930071861323431,-2.49540322759987,
13.8669057591701));
#415369=CARTESIAN_POINT('Ctrl Pts',(-0.926001375100309,-2.50029738816073,
13.8637413727084));
#415370=CARTESIAN_POINT('Ctrl Pts',(-0.922974702835103,-2.50561768217352,
13.8597962563956));
#415371=CARTESIAN_POINT('Ctrl Pts',(-0.920895168181939,-2.51090645082252,
13.855546950204));
#415372=CARTESIAN_POINT('Ctrl Pts',(-0.918415084802115,-2.5172139135071,
13.850479165618));
#415373=CARTESIAN_POINT('Ctrl Pts',(-0.917195121575857,-2.52364880898393,
13.8448473071436));
#415374=CARTESIAN_POINT('Ctrl Pts',(-0.917011786918912,-2.52984626461901,
13.8390832900376));
#415375=CARTESIAN_POINT('',(-0.915954174459406,-2.56562506273962,13.8057746032556));
#415376=CARTESIAN_POINT('',(-0.917011786918914,-2.52984626461901,13.8390832900376));
#415377=CARTESIAN_POINT('',(-0.830768905102112,-2.59446083774312,13.8057746032556));
#415378=CARTESIAN_POINT('Origin',(0.,2.5406128344257E-15,13.8057746032556));
#415379=CARTESIAN_POINT('',(-0.808196285377042,-2.56668102892777,13.8390832900376));
#415380=CARTESIAN_POINT('',(-0.830768905102112,-2.59446083774312,13.8057746032556));
#415381=CARTESIAN_POINT('',(-0.707754549332778,-2.59617338362709,13.8390832900376));
#415382=CARTESIAN_POINT('Ctrl Pts',(-0.808196285377041,-2.56668102892777,
13.8390832900376));
#415383=CARTESIAN_POINT('Ctrl Pts',(-0.803799987434504,-2.56127081469693,
13.8455641171218));
#415384=CARTESIAN_POINT('Ctrl Pts',(-0.798165466548616,-2.55640364994298,
13.851896480191));
#415385=CARTESIAN_POINT('Ctrl Pts',(-0.791353993190503,-2.55270297944543,
13.8574481026913));
#415386=CARTESIAN_POINT('Ctrl Pts',(-0.786749999433474,-2.55020163165006,
13.8612005412592));
#415387=CARTESIAN_POINT('Ctrl Pts',(-0.781491513914159,-2.54819026256287,
13.8646714234115));
#415388=CARTESIAN_POINT('Ctrl Pts',(-0.775783407044123,-2.54701012259152,
13.8674635290331));
#415389=CARTESIAN_POINT('Ctrl Pts',(-0.77118311489912,-2.54605902115565,
13.8697137499649));
#415390=CARTESIAN_POINT('Ctrl Pts',(-0.766180273404364,-2.54563920061852,
13.8715630732994));
#415391=CARTESIAN_POINT('Ctrl Pts',(-0.761123456367358,-2.54591949409372,
13.8727429581918));
#415392=CARTESIAN_POINT('Ctrl Pts',(-0.756008356199529,-2.54620301813494,
13.873936442031));
#415393=CARTESIAN_POINT('Ctrl Pts',(-0.750684619536904,-2.54722690894767,
13.8744652622107));
#415394=CARTESIAN_POINT('Ctrl Pts',(-0.745712912344444,-2.54893630702501,
13.8742206332401));
#415395=CARTESIAN_POINT('Ctrl Pts',(-0.741433448506141,-2.55040769441249,
13.8740100655632));
#415396=CARTESIAN_POINT('Ctrl Pts',(-0.737299880811726,-2.55242275756334,
13.8732246156103));
#415397=CARTESIAN_POINT('Ctrl Pts',(-0.733610031709007,-2.55477508820644,
13.8719820486038));
#415398=CARTESIAN_POINT('Ctrl Pts',(-0.729856597935234,-2.55716795497067,
13.8707180692815));
#415399=CARTESIAN_POINT('Ctrl Pts',(-0.726472443550261,-2.55995702065554,
13.868960862563));
#415400=CARTESIAN_POINT('Ctrl Pts',(-0.723578594687708,-2.56290947028007,
13.8669057591701));
#415401=CARTESIAN_POINT('Ctrl Pts',(-0.71912273315082,-2.56745556350967,
13.8637413727084));
#415402=CARTESIAN_POINT('Ctrl Pts',(-0.715672478534653,-2.57251145279515,
13.8597962563956));
#415403=CARTESIAN_POINT('Ctrl Pts',(-0.713168779618072,-2.57761312212307,
13.855546950204));
#415404=CARTESIAN_POINT('Ctrl Pts',(-0.710182831746682,-2.58369744742648,
13.850479165618));
#415405=CARTESIAN_POINT('Ctrl Pts',(-0.708442424127407,-2.59001149299092,
13.8448473071436));
#415406=CARTESIAN_POINT('Ctrl Pts',(-0.707754549332779,-2.59617338362709,
13.8390832900376));
#415407=CARTESIAN_POINT('',(-0.703784151790496,-2.63174692551465,13.8057746032556));
#415408=CARTESIAN_POINT('',(-0.707754549332778,-2.59617338362709,13.8390832900376));
#415409=CARTESIAN_POINT('',(-0.61653194602864,-2.65354336158153,13.8057746032556));
#415410=CARTESIAN_POINT('Origin',(0.,2.5406128344257E-15,13.8057746032556));
#415411=CARTESIAN_POINT('',(-0.596298747147209,-2.62401610972678,13.8390832900376));
#415412=CARTESIAN_POINT('',(-0.61653194602864,-2.65354336158153,13.8057746032556));
#415413=CARTESIAN_POINT('',(-0.493787321992115,-2.64522339710559,13.8390832900376));
#415414=CARTESIAN_POINT('Ctrl Pts',(-0.596298747147209,-2.62401610972677,
13.8390832900376));
#415415=CARTESIAN_POINT('Ctrl Pts',(-0.592358060209198,-2.61826555844192,
13.8455641171218));
#415416=CARTESIAN_POINT('Ctrl Pts',(-0.587139006838742,-2.61295532301663,
13.851896480191));
#415417=CARTESIAN_POINT('Ctrl Pts',(-0.58065183709722,-2.60871176788156,
13.8574481026913));
#415418=CARTESIAN_POINT('Ctrl Pts',(-0.576267045816317,-2.60584347488205,
13.8612005412592));
#415419=CARTESIAN_POINT('Ctrl Pts',(-0.571190002727019,-2.60341018307235,
13.8646714234115));
#415420=CARTESIAN_POINT('Ctrl Pts',(-0.565597081475258,-2.60176870621801,
13.8674635290331));
#415421=CARTESIAN_POINT('Ctrl Pts',(-0.561089620019488,-2.60044580297686,
13.8697137499649));
#415422=CARTESIAN_POINT('Ctrl Pts',(-0.5561376443383,-2.599619601332,13.8715630732994));
#415423=CARTESIAN_POINT('Ctrl Pts',(-0.55107480692248,-2.59948678462006,
13.8727429581918));
#415424=CARTESIAN_POINT('Ctrl Pts',(-0.545953616987025,-2.59935243710847,
13.873936442031));
#415425=CARTESIAN_POINT('Ctrl Pts',(-0.540564138012391,-2.59993898704783,
13.8744652622107));
#415426=CARTESIAN_POINT('Ctrl Pts',(-0.535469641952897,-2.60123745695282,
13.8742206332401));
#415427=CARTESIAN_POINT('Ctrl Pts',(-0.531084485945711,-2.60235513238873,
13.8740100655632));
#415428=CARTESIAN_POINT('Ctrl Pts',(-0.526800426003079,-2.6040265664419,
13.8732246156103));
#415429=CARTESIAN_POINT('Ctrl Pts',(-0.522931117783473,-2.60607031294209,
13.8719820486038));
#415430=CARTESIAN_POINT('Ctrl Pts',(-0.518995132395369,-2.60814927794181,
13.8707180692815));
#415431=CARTESIAN_POINT('Ctrl Pts',(-0.5153949037592,-2.61065322324136,
13.868960862563));
#415432=CARTESIAN_POINT('Ctrl Pts',(-0.512270031886407,-2.61335997328585,
13.8669057591701));
#415433=CARTESIAN_POINT('Ctrl Pts',(-0.50745844805912,-2.61752774568379,
13.8637413727084));
#415434=CARTESIAN_POINT('Ctrl Pts',(-0.503607571967207,-2.62228558413294,
13.8597962563956));
#415435=CARTESIAN_POINT('Ctrl Pts',(-0.500696370490418,-2.62716620337213,
13.855546950204));
#415436=CARTESIAN_POINT('Ctrl Pts',(-0.497224429117898,-2.6329869011133,
13.850479165618));
#415437=CARTESIAN_POINT('Ctrl Pts',(-0.494975159231157,-2.63913807783387,
13.8448473071436));
#415438=CARTESIAN_POINT('Ctrl Pts',(-0.493787321992114,-2.64522339710559,
13.8390832900376));
#415439=CARTESIAN_POINT('',(-0.486930561707634,-2.68035494670806,13.8057746032556));
#415440=CARTESIAN_POINT('',(-0.493787321992115,-2.64522339710559,13.8390832900376));
#415441=CARTESIAN_POINT('',(-0.398192068574959,-2.69496699215246,13.8057746032556));
#415442=CARTESIAN_POINT('Origin',(0.,2.5406128344257E-15,13.8057746032556));
#415443=CARTESIAN_POINT('',(-0.380432939137479,-2.66388879624773,13.8390832900376));
#415444=CARTESIAN_POINT('',(-0.398192068574959,-2.69496699215246,13.8057746032556));
#415445=CARTESIAN_POINT('',(-0.276534021492768,-2.67666988530749,13.8390832900376));
#415446=CARTESIAN_POINT('Ctrl Pts',(-0.380432939137479,-2.66388879624773,
13.8390832900376));
#415447=CARTESIAN_POINT('Ctrl Pts',(-0.376974087825399,-2.65783617687889,
13.8455641171218));
#415448=CARTESIAN_POINT('Ctrl Pts',(-0.372205233909475,-2.6521182095229,
13.851896480191));
#415449=CARTESIAN_POINT('Ctrl Pts',(-0.366085538828865,-2.64736000990959,
13.8574481026913));
#415450=CARTESIAN_POINT('Ctrl Pts',(-0.361949130086624,-2.6441438597226,
13.8612005412592));
#415451=CARTESIAN_POINT('Ctrl Pts',(-0.357087316311448,-2.64130483834592,
13.8646714234115));
#415452=CARTESIAN_POINT('Ctrl Pts',(-0.351646800646126,-2.63921294836624,
13.8674635290331));
#415453=CARTESIAN_POINT('Ctrl Pts',(-0.347262166291898,-2.63752704702261,
13.8697137499649));
#415454=CARTESIAN_POINT('Ctrl Pts',(-0.342394011005417,-2.63629996250565,
13.8715630732994));
#415455=CARTESIAN_POINT('Ctrl Pts',(-0.337358845558476,-2.63575491947989,
13.8727429581918));
#415456=CARTESIAN_POINT('Ctrl Pts',(-0.332265646529479,-2.63520359447602,
13.873936442031));
#415457=CARTESIAN_POINT('Ctrl Pts',(-0.326846291336212,-2.63534890014893,
13.8744652622107));
#415458=CARTESIAN_POINT('Ctrl Pts',(-0.321662909440426,-2.63622780077858,
13.8742206332401));
#415459=CARTESIAN_POINT('Ctrl Pts',(-0.317201243754086,-2.63698432631728,
13.8740100655632));
#415460=CARTESIAN_POINT('Ctrl Pts',(-0.312795201275329,-2.63830100815493,
13.8732246156103));
#415461=CARTESIAN_POINT('Ctrl Pts',(-0.308772183546646,-2.64002256971644,
13.8719820486038));
#415462=CARTESIAN_POINT('Ctrl Pts',(-0.304679839877579,-2.64177379778259,
13.8707180692815));
#415463=CARTESIAN_POINT('Ctrl Pts',(-0.300887495917791,-2.64397595935398,
13.868960862563));
#415464=CARTESIAN_POINT('Ctrl Pts',(-0.297552396541504,-2.64641899684345,
13.8669057591701));
#415465=CARTESIAN_POINT('Ctrl Pts',(-0.292417110720329,-2.65018071257207,
13.8637413727084));
#415466=CARTESIAN_POINT('Ctrl Pts',(-0.288191240097716,-2.654608837555,
13.8597962563956));
#415467=CARTESIAN_POINT('Ctrl Pts',(-0.284891909626231,-2.65923592698965,
13.855546950204));
#415468=CARTESIAN_POINT('Ctrl Pts',(-0.280957079949588,-2.66475426138547,
13.850479165618));
#415469=CARTESIAN_POINT('Ctrl Pts',(-0.278213916315381,-2.67070163419597,
13.8448473071436));
#415470=CARTESIAN_POINT('Ctrl Pts',(-0.276534021492769,-2.67666988530749,
13.8390832900376));
#415471=CARTESIAN_POINT('',(-0.266836529074495,-2.71112564795857,13.8057746032556));
#415472=CARTESIAN_POINT('',(-0.276534021492768,-2.67666988530749,13.8390832900376));
#415473=CARTESIAN_POINT('',(-0.177202288601978,-2.71845606202887,13.8057746032556));
#415474=CARTESIAN_POINT('Origin',(0.,2.5406128344257E-15,13.8057746032556));
#415475=CARTESIAN_POINT('',(-0.162035412684806,-2.68603374234038,13.8390832900376));
#415476=CARTESIAN_POINT('',(-0.177202288601978,-2.71845606202887,13.8057746032556));
#415477=CARTESIAN_POINT('',(-0.057440432705288,-2.69030357704212,13.8390832900376));
#415478=CARTESIAN_POINT('Ctrl Pts',(-0.162035412684806,-2.68603374234037,
13.8390832900376));
#415479=CARTESIAN_POINT('Ctrl Pts',(-0.15908141508347,-2.67971933407083,
13.8455641171218));
#415480=CARTESIAN_POINT('Ctrl Pts',(-0.15479449655808,-2.67363168691349,
13.851896480191));
#415481=CARTESIAN_POINT('Ctrl Pts',(-0.149083001699466,-2.66839050785533,
13.8574481026913));
#415482=CARTESIAN_POINT('Ctrl Pts',(-0.145222502613606,-2.66484790342974,
13.8612005412592));
#415483=CARTESIAN_POINT('Ctrl Pts',(-0.140608272721084,-2.66162204570493,
13.8646714234115));
#415484=CARTESIAN_POINT('Ctrl Pts',(-0.13535636837633,-2.65909366378258,
13.8674635290331));
#415485=CARTESIAN_POINT('Ctrl Pts',(-0.131123740141859,-2.65705598373177,
13.8697137499649));
#415486=CARTESIAN_POINT('Ctrl Pts',(-0.126371802020328,-2.65543618238771,
13.8715630732994));
#415487=CARTESIAN_POINT('Ctrl Pts',(-0.121397816737571,-2.65448254021954,
13.8727429581918));
#415488=CARTESIAN_POINT('Ctrl Pts',(-0.116366503014253,-2.65351790670031,
13.873936442031));
#415489=CARTESIAN_POINT('Ctrl Pts',(-0.110953336517032,-2.65322100112149,
13.8744652622107));
#415490=CARTESIAN_POINT('Ctrl Pts',(-0.105715563336274,-2.65367448353713,
13.8742206332401));
#415491=CARTESIAN_POINT('Ctrl Pts',(-0.101207079619797,-2.65406482462599,
13.8740100655632));
#415492=CARTESIAN_POINT('Ctrl Pts',(-0.0967083760906725,-2.65501799194772,
13.8732246156103));
#415493=CARTESIAN_POINT('Ctrl Pts',(-0.0925584213721455,-2.65640591186238,
13.8719820486038));
#415494=CARTESIAN_POINT('Ctrl Pts',(-0.0883369532940422,-2.65781774886112,
13.8707180692815));
#415495=CARTESIAN_POINT('Ctrl Pts',(-0.0843777314339956,-2.65970347168242,
13.868960862563));
#415496=CARTESIAN_POINT('Ctrl Pts',(-0.0808545990903116,-2.66186653860547,
13.8669057591701));
#415497=CARTESIAN_POINT('Ctrl Pts',(-0.0754297857551275,-2.66519716406723,
13.8637413727084));
#415498=CARTESIAN_POINT('Ctrl Pts',(-0.070857043073586,-2.66926610714275,
13.8597962563956));
#415499=CARTESIAN_POINT('Ctrl Pts',(-0.0671915401073441,-2.67360887425611,
13.855546950204));
#415500=CARTESIAN_POINT('Ctrl Pts',(-0.0628200077688717,-2.67878812170163,
13.850479165618));
#415501=CARTESIAN_POINT('Ctrl Pts',(-0.059601205688587,-2.68449211181725,
13.8448473071436));
#415502=CARTESIAN_POINT('Ctrl Pts',(-0.0574404327052869,-2.69030357704211,
13.8390832900376));
#415503=CARTESIAN_POINT('',(-0.0449667433652931,-2.72385425532615,13.8057746032556));
#415504=CARTESIAN_POINT('',(-0.057440432705288,-2.69030357704212,13.8390832900376));
#415505=CARTESIAN_POINT('',(-3.33621391227898E-16,-2.72422539674441,13.8057746032556));
#415506=CARTESIAN_POINT('Origin',(0.,2.5406128344257E-15,13.8057746032556));
#415507=CARTESIAN_POINT('',(-3.12992118721904E-16,-2.55577460325558,13.9742253967444));
#415508=CARTESIAN_POINT('',(-3.33621391227897E-16,-2.72422539674441,13.8057746032556));
#415509=CARTESIAN_POINT('',(3.12992118721905E-16,2.55577460325559,13.9742253967444));
#415510=CARTESIAN_POINT('Origin',(0.,2.5406128344257E-15,13.9742253967444));
#415511=CARTESIAN_POINT('Origin',(0.,2.5406128344257E-15,13.9742253967444));
#415512=CARTESIAN_POINT('',(0.04496674336533,-2.72385425532615,13.8057746032556));
#415513=CARTESIAN_POINT('Origin',(0.,2.5406128344257E-15,13.8057746032556));
#415514=CARTESIAN_POINT('',(0.0574404327053243,-2.69030357704212,13.8390832900376));
#415515=CARTESIAN_POINT('',(0.04496674336533,-2.72385425532615,13.8057746032556));
#415516=CARTESIAN_POINT('',(0.162035412684842,-2.68603374234037,13.8390832900376));
#415517=CARTESIAN_POINT('Ctrl Pts',(0.057440432705324,-2.69030357704211,
13.8390832900376));
#415518=CARTESIAN_POINT('Ctrl Pts',(0.0598699182292554,-2.6837694012171,
13.8455641171218));
#415519=CARTESIAN_POINT('Ctrl Pts',(0.0636463726286157,-2.67735258654585,
13.851896480191));
#415520=CARTESIAN_POINT('Ctrl Pts',(0.0689116582092796,-2.67166330722473,
13.8574481026913));
#415521=CARTESIAN_POINT('Ctrl Pts',(0.0724705566542799,-2.6678178240085,
13.8612005412592));
#415522=CARTESIAN_POINT('Ctrl Pts',(0.0768064957255092,-2.66422659748649,
13.8646714234115));
#415523=CARTESIAN_POINT('Ctrl Pts',(0.0818348381927834,-2.66127854958601,
13.8674635290331));
#415524=CARTESIAN_POINT('Ctrl Pts',(0.0858872928649317,-2.65890265125256,
13.8697137499649));
#415525=CARTESIAN_POINT('Ctrl Pts',(0.0904913904573281,-2.65690091259211,
13.8715630732994));
#415526=CARTESIAN_POINT('Ctrl Pts',(0.0953710945244929,-2.65554501761281,
13.8727429581918));
#415527=CARTESIAN_POINT('Ctrl Pts',(0.100307040379415,-2.65417349505516,
13.873936442031));
#415528=CARTESIAN_POINT('Ctrl Pts',(0.105677994450658,-2.65343635408224,
13.8744652622107));
#415529=CARTESIAN_POINT('Ctrl Pts',(0.110935302400043,-2.65346140043321,
13.8742206332401));
#415530=CARTESIAN_POINT('Ctrl Pts',(0.115460600931368,-2.65348295941668,
13.8740100655632));
#415531=CARTESIAN_POINT('Ctrl Pts',(0.120022027381112,-2.65406626905123,
13.8732246156103));
#415532=CARTESIAN_POINT('Ctrl Pts',(0.124271301825525,-2.65511131094102,
13.8719820486038));
#415533=CARTESIAN_POINT('Ctrl Pts',(0.128593801139098,-2.65617436133005,
13.8707180692815));
#415534=CARTESIAN_POINT('Ctrl Pts',(0.132693552931151,-2.657731096227,13.868960862563));
#415535=CARTESIAN_POINT('Ctrl Pts',(0.136381272377762,-2.65959979773012,
13.8669057591701));
#415536=CARTESIAN_POINT('Ctrl Pts',(0.14205951198924,-2.66247716816209,
13.8637413727084));
#415537=CARTESIAN_POINT('Ctrl Pts',(0.146948695881612,-2.66615985118538,
13.8597962563956));
#415538=CARTESIAN_POINT('Ctrl Pts',(0.150955978025139,-2.6701893955788,
13.855546950204));
#415539=CARTESIAN_POINT('Ctrl Pts',(0.155735121198977,-2.67499508903679,
13.850479165618));
#415540=CARTESIAN_POINT('Ctrl Pts',(0.159408141128555,-2.68041773734441,
13.8448473071436));
#415541=CARTESIAN_POINT('Ctrl Pts',(0.162035412684842,-2.68603374234037,
13.8390832900376));
#415542=CARTESIAN_POINT('',(0.177202288602015,-2.71845606202886,13.8057746032556));
#415543=CARTESIAN_POINT('',(0.162035412684842,-2.68603374234037,13.8390832900376));
#415544=CARTESIAN_POINT('',(0.266836529074531,-2.71112564795856,13.8057746032556));
#415545=CARTESIAN_POINT('Origin',(0.,2.5406128344257E-15,13.8057746032556));
#415546=CARTESIAN_POINT('',(0.276534021492804,-2.67666988530749,13.8390832900376));
#415547=CARTESIAN_POINT('',(0.266836529074531,-2.71112564795856,13.8057746032556));
#415548=CARTESIAN_POINT('',(0.380432939137515,-2.66388879624773,13.8390832900376));
#415549=CARTESIAN_POINT('Ctrl Pts',(0.276534021492803,-2.67666988530748,
13.8390832900376));
#415550=CARTESIAN_POINT('Ctrl Pts',(0.278422827114005,-2.66995942578906,
13.8455641171218));
#415551=CARTESIAN_POINT('Ctrl Pts',(0.281663685706382,-2.66325614644683,
13.851896480191));
#415552=CARTESIAN_POINT('Ctrl Pts',(0.286447722402268,-2.65715662807797,
13.8574481026913));
#415553=CARTESIAN_POINT('Ctrl Pts',(0.289681336324433,-2.65303385712744,
13.8612005412592));
#415554=CARTESIAN_POINT('Ctrl Pts',(0.293710129615224,-2.64910116082823,
13.8646714234115));
#415555=CARTESIAN_POINT('Ctrl Pts',(0.298481447415517,-2.64575306572201,
13.8674635290331));
#415556=CARTESIAN_POINT('Ctrl Pts',(0.302326760108108,-2.64305476031733,
13.8697137499649));
#415557=CARTESIAN_POINT('Ctrl Pts',(0.306752377661515,-2.640684405581,13.8715630732994));
#415558=CARTESIAN_POINT('Ctrl Pts',(0.311505326887615,-2.63893528104795,
13.8727429581918));
#415559=CARTESIAN_POINT('Ctrl Pts',(0.316313056968849,-2.63716599670821,
13.873936442031));
#415560=CARTESIAN_POINT('Ctrl Pts',(0.321606055800918,-2.63599352589276,
13.8744652622107));
#415561=CARTESIAN_POINT('Ctrl Pts',(0.326847912001921,-2.63558996949972,
13.8742206332401));
#415562=CARTESIAN_POINT('Ctrl Pts',(0.331359910232991,-2.63524260290633,
13.8740100655632));
#415563=CARTESIAN_POINT('Ctrl Pts',(0.335953704062915,-2.63545217302432,
13.8732246156103));
#415564=CARTESIAN_POINT('Ctrl Pts',(0.340274020012868,-2.63614738230787,
13.8719820486038));
#415565=CARTESIAN_POINT('Ctrl Pts',(0.34466878504214,-2.63685457166224,
13.8707180692815));
#415566=CARTESIAN_POINT('Ctrl Pts',(0.348881783594433,-2.63807195882096,
13.868960862563));
#415567=CARTESIAN_POINT('Ctrl Pts',(0.352709548979483,-2.63963385900397,
13.8669057591701));
#415568=CARTESIAN_POINT('Ctrl Pts',(0.358603427119485,-2.64203882598065,
13.8637413727084));
#415569=CARTESIAN_POINT('Ctrl Pts',(0.363776515510545,-2.64531074130378,
13.8597962563956));
#415570=CARTESIAN_POINT('Ctrl Pts',(0.368098909029846,-2.64900024702416,
13.855546950204));
#415571=CARTESIAN_POINT('Ctrl Pts',(0.373253858629733,-2.65340040539754,
13.850479165618));
#415572=CARTESIAN_POINT('Ctrl Pts',(0.377356653066979,-2.65850562506734,
13.8448473071436));
#415573=CARTESIAN_POINT('Ctrl Pts',(0.380432939137514,-2.66388879624772,
13.8390832900376));
#415574=CARTESIAN_POINT('',(0.398192068574995,-2.69496699215245,13.8057746032556));
#415575=CARTESIAN_POINT('',(0.380432939137515,-2.66388879624773,13.8390832900376));
#415576=CARTESIAN_POINT('',(0.48693056170767,-2.68035494670805,13.8057746032556));
#415577=CARTESIAN_POINT('Origin',(0.,2.5406128344257E-15,13.8057746032556));
#415578=CARTESIAN_POINT('',(0.493787321992151,-2.64522339710558,13.8390832900376));
#415579=CARTESIAN_POINT('',(0.48693056170767,-2.68035494670805,13.8057746032556));
#415580=CARTESIAN_POINT('',(0.596298747147245,-2.62401610972677,13.8390832900376));
#415581=CARTESIAN_POINT('Ctrl Pts',(0.49378732199215,-2.64522339710558,
13.8390832900376));
#415582=CARTESIAN_POINT('Ctrl Pts',(0.495122878020844,-2.63838131089468,
13.8455641171218));
#415583=CARTESIAN_POINT('Ctrl Pts',(0.497806573427004,-2.63143617609955,
13.851896480191));
#415584=CARTESIAN_POINT('Ctrl Pts',(0.502077524263211,-2.62496700997134,
13.8574481026913));
#415585=CARTESIAN_POINT('Ctrl Pts',(0.504964334495399,-2.62059438764698,
13.8612005412592));
#415586=CARTESIAN_POINT('Ctrl Pts',(0.508659171051115,-2.61634639301559,
13.8646714234115));
#415587=CARTESIAN_POINT('Ctrl Pts',(0.513141711851679,-2.61262053172415,
13.8674635290331));
#415588=CARTESIAN_POINT('Ctrl Pts',(0.516754292643173,-2.60961777602553,
13.8697137499649));
#415589=CARTESIAN_POINT('Ctrl Pts',(0.520971978402944,-2.60689457953301,
13.8715630732994));
#415590=CARTESIAN_POINT('Ctrl Pts',(0.525566542695062,-2.6047638655814,
13.8727429581918));
#415591=CARTESIAN_POINT('Ctrl Pts',(0.530214062352137,-2.60260859375493,
13.873936442031));
#415592=CARTESIAN_POINT('Ctrl Pts',(0.535393881911091,-2.60100859569678,
13.8744652622107));
#415593=CARTESIAN_POINT('Ctrl Pts',(0.540585402675539,-2.60017912216095,
13.8742206332401));
#415594=CARTESIAN_POINT('Ctrl Pts',(0.545054074002554,-2.59946514165806,
13.8740100655632));
#415595=CARTESIAN_POINT('Ctrl Pts',(0.549649664272639,-2.59929957760493,
13.8732246156103));
#415596=CARTESIAN_POINT('Ctrl Pts',(0.554012270738286,-2.59964032777916,
13.8719820486038));
#415597=CARTESIAN_POINT('Ctrl Pts',(0.558450055047073,-2.5999869498704,
13.8707180692815));
#415598=CARTESIAN_POINT('Ctrl Pts',(0.562748263549338,-2.60085688778019,
13.868960862563));
#415599=CARTESIAN_POINT('Ctrl Pts',(0.566690601725727,-2.60210159245507,
13.8669057591701));
#415600=CARTESIAN_POINT('Ctrl Pts',(0.572760895607653,-2.60401815131803,
13.8637413727084));
#415601=CARTESIAN_POINT('Ctrl Pts',(0.578183462447657,-2.60685752488436,
13.8597962563956));
#415602=CARTESIAN_POINT('Ctrl Pts',(0.582792202527004,-2.61018243887984,
13.855546950204));
#415603=CARTESIAN_POINT('Ctrl Pts',(0.588288653213859,-2.61414777984062,
13.850479165618));
#415604=CARTESIAN_POINT('Ctrl Pts',(0.592793918738707,-2.61890159647799,
13.8448473071436));
#415605=CARTESIAN_POINT('Ctrl Pts',(0.596298747147244,-2.62401610972677,
13.8390832900376));
#415606=CARTESIAN_POINT('',(0.616531946028676,-2.65354336158152,13.8057746032556));
#415607=CARTESIAN_POINT('',(0.596298747147245,-2.62401610972677,13.8390832900376));
#415608=CARTESIAN_POINT('',(0.703784151790532,-2.63174692551464,13.8057746032556));
#415609=CARTESIAN_POINT('Origin',(0.,2.5406128344257E-15,13.8057746032556));
#415610=CARTESIAN_POINT('',(0.707754549332813,-2.59617338362708,13.8390832900376));
#415611=CARTESIAN_POINT('',(0.703784151790532,-2.63174692551464,13.8057746032556));
#415612=CARTESIAN_POINT('',(0.808196285377077,-2.56668102892776,13.8390832900376));
#415613=CARTESIAN_POINT('Ctrl Pts',(0.707754549332813,-2.59617338362708,
13.8390832900376));
#415614=CARTESIAN_POINT('Ctrl Pts',(0.70852796786398,-2.58924520367858,
13.8455641171218));
#415615=CARTESIAN_POINT('Ctrl Pts',(0.710636640533773,-2.58210443215673,
13.851896480191));
#415616=CARTESIAN_POINT('Ctrl Pts',(0.714366083037144,-2.57530866950241,
13.8574481026913));
#415617=CARTESIAN_POINT('Ctrl Pts',(0.716886878333549,-2.57071529488436,
13.8612005412592));
#415618=CARTESIAN_POINT('Ctrl Pts',(0.720223169626513,-2.5661802716242,
13.8646714234115));
#415619=CARTESIAN_POINT('Ctrl Pts',(0.724387102857885,-2.56210143913972,
13.8674635290331));
#415620=CARTESIAN_POINT('Ctrl Pts',(0.727742910619151,-2.5588142159909,
13.8697137499649));
#415621=CARTESIAN_POINT('Ctrl Pts',(0.731724596582433,-2.55575630016556,
13.8715630732994));
#415622=CARTESIAN_POINT('Ctrl Pts',(0.736130199873256,-2.55325817634519,
13.8727429581918));
#415623=CARTESIAN_POINT('Ctrl Pts',(0.740586580629639,-2.55073126001041,
13.873936442031));
#415624=CARTESIAN_POINT('Ctrl Pts',(0.745618750070919,-2.54871438243265,
13.8744652622107));
#415625=CARTESIAN_POINT('Ctrl Pts',(0.750725386684666,-2.54746451176355,
13.8742206332401));
#415626=CARTESIAN_POINT('Ctrl Pts',(0.755120992837223,-2.54638866877362,
13.8740100655633));
#415627=CARTESIAN_POINT('Ctrl Pts',(0.75968779665244,-2.54584907235083,
13.8732246156103));
#415628=CARTESIAN_POINT('Ctrl Pts',(0.764063661207532,-2.54583309577955,
13.8719820486038));
#415629=CARTESIAN_POINT('Ctrl Pts',(0.768514932073442,-2.54581684389483,
13.8707180692815));
#415630=CARTESIAN_POINT('Ctrl Pts',(0.77286974665725,-2.54633354326244,
13.868960862563));
#415631=CARTESIAN_POINT('Ctrl Pts',(0.776900422014854,-2.54725276912493,
13.8669057591701));
#415632=CARTESIAN_POINT('Ctrl Pts',(0.783106734834446,-2.54866816549114,
13.8637413727084));
#415633=CARTESIAN_POINT('Ctrl Pts',(0.788742693835735,-2.55105610173805,
13.8597962563956));
#415634=CARTESIAN_POINT('Ctrl Pts',(0.79360711007029,-2.55399429725457,
13.855546950204));
#415635=CARTESIAN_POINT('Ctrl Pts',(0.799408483871643,-2.55749843211288,
13.850479165618));
#415636=CARTESIAN_POINT('Ctrl Pts',(0.804286238685342,-2.56186920985244,
13.8448473071436));
#415637=CARTESIAN_POINT('Ctrl Pts',(0.808196285377076,-2.56668102892776,
13.8390832900376));
#415638=CARTESIAN_POINT('',(0.830768905102147,-2.5944608377431,13.8057746032556));
#415639=CARTESIAN_POINT('',(0.808196285377077,-2.56668102892776,13.8390832900376));
#415640=CARTESIAN_POINT('',(0.915954174459439,-2.5656250627396,13.8057746032556));
#415641=CARTESIAN_POINT('Origin',(0.,2.5406128344257E-15,13.8057746032556));
#415642=CARTESIAN_POINT('',(0.917011786918948,-2.529846264619,13.8390832900376));
#415643=CARTESIAN_POINT('',(0.915954174459439,-2.5656250627396,13.8057746032556));
#415644=CARTESIAN_POINT('',(1.01471541067073,-2.4922651093538,13.8390832900376));
#415645=CARTESIAN_POINT('Ctrl Pts',(0.917011786918946,-2.529846264619,13.8390832900376));
#415646=CARTESIAN_POINT('Ctrl Pts',(0.917217920979866,-2.52287809682738,
13.8455641171218));
#415647=CARTESIAN_POINT('Ctrl Pts',(0.918737538044587,-2.51558920923515,
13.851896480191));
#415648=CARTESIAN_POINT('Ctrl Pts',(0.921900653390576,-2.50851207473398,
13.8574481026913));
#415649=CARTESIAN_POINT('Ctrl Pts',(0.924038658274404,-2.50372851597246,
13.8612005412592));
#415650=CARTESIAN_POINT('Ctrl Pts',(0.926994201836504,-2.49893664391509,
13.8646714234115));
#415651=CARTESIAN_POINT('Ctrl Pts',(0.930811817210032,-2.4945319841948,
13.8674635290331));
#415652=CARTESIAN_POINT('Ctrl Pts',(0.933888519594087,-2.49098216952349,
13.8697137499649));
#415653=CARTESIAN_POINT('Ctrl Pts',(0.937607708297721,-2.48760988429062,
13.8715630732994));
#415654=CARTESIAN_POINT('Ctrl Pts',(0.941795032024219,-2.48476097520335,
13.8727429581918));
#415655=CARTESIAN_POINT('Ctrl Pts',(0.94603061740123,-2.48187923057155,
13.873936442031));
#415656=CARTESIAN_POINT('Ctrl Pts',(0.950881648467455,-2.47945889546171,
13.8744652622107));
#415657=CARTESIAN_POINT('Ctrl Pts',(0.955869417106374,-2.47779694534243,
13.8742206332401));
#415658=CARTESIAN_POINT('Ctrl Pts',(0.960162706050751,-2.47636639942305,
13.8740100655632));
#415659=CARTESIAN_POINT('Ctrl Pts',(0.964670332085183,-2.47545636155576,
13.8732246156103));
#415660=CARTESIAN_POINT('Ctrl Pts',(0.969030334073073,-2.47508376456042,
13.8719820486038));
#415661=CARTESIAN_POINT('Ctrl Pts',(0.973465469022901,-2.47470474685335,
13.8707180692815));
#415662=CARTESIAN_POINT('Ctrl Pts',(0.977847909115691,-2.47486476912973,
13.868960862563));
#415663=CARTESIAN_POINT('Ctrl Pts',(0.98194009817502,-2.47545239888339,
13.8669057591701));
#415664=CARTESIAN_POINT('Ctrl Pts',(0.988241127944434,-2.47635721352356,
13.8637413727084));
#415665=CARTESIAN_POINT('Ctrl Pts',(0.994052972729721,-2.4782778211293,
13.8597962563956));
#415666=CARTESIAN_POINT('Ctrl Pts',(0.999140693232015,-2.48080974496047,
13.855546950204));
#415667=CARTESIAN_POINT('Ctrl Pts',(1.00520838296238,-2.48382935427698,
13.850479165618));
#415668=CARTESIAN_POINT('Ctrl Pts',(1.01042616641141,-2.48778800631399,
13.8448473071436));
#415669=CARTESIAN_POINT('Ctrl Pts',(1.01471541067073,-2.4922651093538,13.8390832900376));
#415670=CARTESIAN_POINT('',(1.03947723417938,-2.51811260508541,13.8057746032556));
#415671=CARTESIAN_POINT('',(1.01471541067073,-2.4922651093538,13.8390832900376));
#415672=CARTESIAN_POINT('',(1.12202867321912,-2.48242938847038,13.8057746032556));
#415673=CARTESIAN_POINT('Origin',(0.,2.5406128344257E-15,13.8057746032556));
#415674=CARTESIAN_POINT('',(1.12016646235943,-2.44668343611513,13.8390832900376));
#415675=CARTESIAN_POINT('',(1.12202867321912,-2.48242938847038,13.8057746032556));
#415676=CARTESIAN_POINT('',(1.21448177232262,-2.40126357667189,13.8390832900376));
#415677=CARTESIAN_POINT('Ctrl Pts',(1.12016646235943,-2.44668343611513,
13.8390832900376));
#415678=CARTESIAN_POINT('Ctrl Pts',(1.11980394016194,-2.43972165248739,
13.8455641171218));
#415679=CARTESIAN_POINT('Ctrl Pts',(1.12072438882074,-2.43233315516911,
13.851896480191));
#415680=CARTESIAN_POINT('Ctrl Pts',(1.1233001269986,-2.42502174598354,13.8574481026913));
#415681=CARTESIAN_POINT('Ctrl Pts',(1.12504111340009,-2.42007983687289,
13.8612005412592));
#415682=CARTESIAN_POINT('Ctrl Pts',(1.12759624057656,-2.41506300513624,
13.8646714234115));
#415683=CARTESIAN_POINT('Ctrl Pts',(1.13104213249179,-2.41036183046386,
13.8674635290331));
#415684=CARTESIAN_POINT('Ctrl Pts',(1.13381925455189,-2.40657304770102,
13.8697137499649));
#415685=CARTESIAN_POINT('Ctrl Pts',(1.13725119540868,-2.40290883506246,
13.8715630732994));
#415686=CARTESIAN_POINT('Ctrl Pts',(1.14119237362231,-2.39972809972824,
13.8727429581918));
#415687=CARTESIAN_POINT('Ctrl Pts',(1.14517897649809,-2.39651070433449,
13.873936442031));
#415688=CARTESIAN_POINT('Ctrl Pts',(1.14981658637787,-2.39370301862339,
13.8744652622107));
#415689=CARTESIAN_POINT('Ctrl Pts',(1.15465229426459,-2.39164004905777,
13.8742206332401));
#415690=CARTESIAN_POINT('Ctrl Pts',(1.15881469487121,-2.38986432025601,
13.8740100655633));
#415691=CARTESIAN_POINT('Ctrl Pts',(1.1632331456173,-2.38858989709609,13.8732246156103));
#415692=CARTESIAN_POINT('Ctrl Pts',(1.16754826994411,-2.38786315924821,
13.8719820486038));
#415693=CARTESIAN_POINT('Ctrl Pts',(1.17193775388651,-2.38712389801911,
13.8707180692815));
#415694=CARTESIAN_POINT('Ctrl Pts',(1.17631865507252,-2.38692617828241,
13.868960862563));
#415695=CARTESIAN_POINT('Ctrl Pts',(1.18044512499054,-2.38717830134817,
13.8669057591701));
#415696=CARTESIAN_POINT('Ctrl Pts',(1.18679893939626,-2.38756651287016,
13.8637413727084));
#415697=CARTESIAN_POINT('Ctrl Pts',(1.19274799309739,-2.38900701050799,
13.8597962563956));
#415698=CARTESIAN_POINT('Ctrl Pts',(1.19802515992689,-2.39111581311846,
13.855546950204));
#415699=CARTESIAN_POINT('Ctrl Pts',(1.20431878611221,-2.39363080189135,
13.850479165618));
#415700=CARTESIAN_POINT('Ctrl Pts',(1.2098418747086,-2.39715098404964,13.8448473071436));
#415701=CARTESIAN_POINT('Ctrl Pts',(1.21448177232262,-2.40126357667189,
13.8390832900376));
#415702=CARTESIAN_POINT('',(1.24126801376483,-2.42500674850021,13.8057746032556));
#415703=CARTESIAN_POINT('',(1.21448177232262,-2.40126357667189,13.8390832900376));
#415704=CARTESIAN_POINT('',(1.32063625628023,-2.3827135561929,13.8057746032556));
#415705=CARTESIAN_POINT('Origin',(0.,2.5406128344257E-15,13.8057746032556));
#415706=CARTESIAN_POINT('',(1.31586661480737,-2.34723833301827,13.8390832900376));
#415707=CARTESIAN_POINT('',(1.32063625628023,-2.3827135561929,13.8057746032556));
#415708=CARTESIAN_POINT('',(1.4061659581551,-2.29428203106783,13.8390832900376));
#415709=CARTESIAN_POINT('Ctrl Pts',(1.31586661480737,-2.34723833301826,
13.8390832900376));
#415710=CARTESIAN_POINT('Ctrl Pts',(1.31493784887688,-2.34032926307583,
13.8455641171218));
#415711=CARTESIAN_POINT('Ctrl Pts',(1.31525300369579,-2.33289032526215,
13.851896480191));
#415712=CARTESIAN_POINT('Ctrl Pts',(1.31722422359291,-2.32539329761401,
13.8574481026913));
#415713=CARTESIAN_POINT('Ctrl Pts',(1.31855660553481,-2.320325925744,13.8612005412592));
#415714=CARTESIAN_POINT('Ctrl Pts',(1.32069431237585,-2.31511752051557,
13.8646714234115));
#415715=CARTESIAN_POINT('Ctrl Pts',(1.32374554899063,-2.3101511164329,13.8674635290331));
#415716=CARTESIAN_POINT('Ctrl Pts',(1.32620460943766,-2.30614857930271,
13.8697137499649));
#415717=CARTESIAN_POINT('Ctrl Pts',(1.32932646344742,-2.30221682398901,
13.8715630732994));
#415718=CARTESIAN_POINT('Ctrl Pts',(1.33299526825743,-2.2987254296767,13.8727429581918));
#415719=CARTESIAN_POINT('Ctrl Pts',(1.33670635844757,-2.29519379475651,
13.873936442031));
#415720=CARTESIAN_POINT('Ctrl Pts',(1.34109968461233,-2.29201744312933,
13.8744652622107));
#415721=CARTESIAN_POINT('Ctrl Pts',(1.3457511509087,-2.28956718283947,13.8742206332401));
#415722=CARTESIAN_POINT('Ctrl Pts',(1.34975496308826,-2.28745808833752,
13.8740100655633));
#415723=CARTESIAN_POINT('Ctrl Pts',(1.35405483448529,-2.28582776096083,
13.8732246156103));
#415724=CARTESIAN_POINT('Ctrl Pts',(1.35829636471057,-2.2847517185809,13.8719820486038));
#415725=CARTESIAN_POINT('Ctrl Pts',(1.36261098635412,-2.28365713349126,
13.8707180692815));
#415726=CARTESIAN_POINT('Ctrl Pts',(1.36696119445875,-2.28310298753372,
13.868960862563));
#415727=CARTESIAN_POINT('Ctrl Pts',(1.37109448425899,-2.28301792607418,
13.8669057591701));
#415728=CARTESIAN_POINT('Ctrl Pts',(1.37745879971445,-2.28288695099435,
13.8637413727084));
#415729=CARTESIAN_POINT('Ctrl Pts',(1.38350547236056,-2.28383775239016,
13.8597962563956));
#415730=CARTESIAN_POINT('Ctrl Pts',(1.38893696684269,-2.28550940004648,
13.855546950204));
#415731=CARTESIAN_POINT('Ctrl Pts',(1.39541464643907,-2.28750303144043,
13.850479165618));
#415732=CARTESIAN_POINT('Ctrl Pts',(1.40120628493946,-2.29056131748852,
13.8448473071436));
#415733=CARTESIAN_POINT('Ctrl Pts',(1.40616595815509,-2.29428203106783,
13.8390832900376));
#415734=CARTESIAN_POINT('',(1.43479835951348,-2.3157628721017,13.8057746032556));
#415735=CARTESIAN_POINT('',(1.4061659581551,-2.29428203106783,13.8390832900376));
#415736=CARTESIAN_POINT('',(1.51045522294544,-2.26714115831902,13.8057746032556));
#415737=CARTESIAN_POINT('Origin',(0.,2.5406128344257E-15,13.8057746032556));
#415738=CARTESIAN_POINT('',(1.50280989203648,-2.23217274608223,13.8390832900376));
#415739=CARTESIAN_POINT('',(1.51045522294544,-2.26714115831902,13.8057746032556));
#415740=CARTESIAN_POINT('',(1.5884923415371,-2.17203241707691,13.8390832900376));
#415741=CARTESIAN_POINT('Ctrl Pts',(1.50280989203647,-2.23217274608223,
13.8390832900376));
#415742=CARTESIAN_POINT('Ctrl Pts',(1.50132106315701,-2.22536236854565,
13.8455641171218));
#415743=CARTESIAN_POINT('Ctrl Pts',(1.50102882683272,-2.21792249514038,
13.851896480191));
#415744=CARTESIAN_POINT('Ctrl Pts',(1.50238241030592,-2.21028974051175,
13.8574481026913));
#415745=CARTESIAN_POINT('Ctrl Pts',(1.50329732100622,-2.20513062840611,
13.8612005412592));
#415746=CARTESIAN_POINT('Ctrl Pts',(1.50500338142551,-2.19976531076337,
13.8646714234115));
#415747=CARTESIAN_POINT('Ctrl Pts',(1.50763965726358,-2.19456672787018,
13.8674635290331));
#415748=CARTESIAN_POINT('Ctrl Pts',(1.50976429145597,-2.19037707259687,
13.8697137499649));
#415749=CARTESIAN_POINT('Ctrl Pts',(1.51255528319535,-2.18620393979096,
13.8715630732994));
#415750=CARTESIAN_POINT('Ctrl Pts',(1.51592729931104,-2.18242512115366,
13.8727429581918));
#415751=CARTESIAN_POINT('Ctrl Pts',(1.51933818012262,-2.17860274915475,
13.873936442031));
#415752=CARTESIAN_POINT('Ctrl Pts',(1.52345798571156,-2.1750788697075,13.8744652622107));
#415753=CARTESIAN_POINT('Ctrl Pts',(1.52789425567682,-2.17225762477136,
13.8742206332401));
#415754=CARTESIAN_POINT('Ctrl Pts',(1.53171283471986,-2.16982920024517,
13.8740100655633));
#415755=CARTESIAN_POINT('Ctrl Pts',(1.53586551183311,-2.16785381821142,
13.8732246156103));
#415756=CARTESIAN_POINT('Ctrl Pts',(1.54000522127301,-2.16643563218393,
13.8719820486038));
#415757=CARTESIAN_POINT('Ctrl Pts',(1.54421626752253,-2.16499300751694,
13.8707180692815));
#415758=CARTESIAN_POINT('Ctrl Pts',(1.54850683262858,-2.16408612308847,
13.868960862563));
#415759=CARTESIAN_POINT('Ctrl Pts',(1.55261943594936,-2.16366444317361,
13.8669057591701));
#415760=CARTESIAN_POINT('Ctrl Pts',(1.55895189898524,-2.16301515310951,
13.8637413727084));
#415761=CARTESIAN_POINT('Ctrl Pts',(1.5650559509675,-2.16346993083689,13.8597962563956));
#415762=CARTESIAN_POINT('Ctrl Pts',(1.57060562740263,-2.1646932989997,13.855546950204));
#415763=CARTESIAN_POINT('Ctrl Pts',(1.5772242525211,-2.1661523057267,13.850479165618));
#415764=CARTESIAN_POINT('Ctrl Pts',(1.58324589852681,-2.16872834327552,
13.8448473071436));
#415765=CARTESIAN_POINT('Ctrl Pts',(1.5884923415371,-2.17203241707691,13.8390832900376));
#415766=CARTESIAN_POINT('',(1.61878035890463,-2.19110797586332,13.8057746032556));
#415767=CARTESIAN_POINT('',(1.5884923415371,-2.17203241707691,13.8390832900376));
#415768=CARTESIAN_POINT('',(1.69022235930951,-2.13648131008849,13.8057746032556));
#415769=CARTESIAN_POINT('Origin',(0.,2.5406128344257E-15,13.8057746032556));
#415770=CARTESIAN_POINT('',(1.67975221738026,-2.1022524178036,13.8390832900376));
#415771=CARTESIAN_POINT('',(1.69022235930951,-2.13648131008849,13.8057746032556));
#415772=CARTESIAN_POINT('',(1.76024757046897,-2.03532828571046,13.8390832900376));
#415773=CARTESIAN_POINT('Ctrl Pts',(1.67975221738026,-2.1022524178036,13.8390832900376));
#415774=CARTESIAN_POINT('Ctrl Pts',(1.67771323346238,-2.09558605461174,
13.8455641171218));
#415775=CARTESIAN_POINT('Ctrl Pts',(1.67681555077941,-2.0881947567449,13.851896480191));
#415776=CARTESIAN_POINT('Ctrl Pts',(1.67754248995399,-2.08047706985852,
13.8574481026913));
#415777=CARTESIAN_POINT('Ctrl Pts',(1.67803384083294,-2.07526055055712,
13.8612005412592));
#415778=CARTESIAN_POINT('Ctrl Pts',(1.67929690127987,-2.06977402580377,
13.8646714234115));
#415779=CARTESIAN_POINT('Ctrl Pts',(1.68150067236047,-2.06437785981151,
13.8674635290331));
#415780=CARTESIAN_POINT('Ctrl Pts',(1.68327674120823,-2.06002896785967,
13.8697137499649));
#415781=CARTESIAN_POINT('Ctrl Pts',(1.68571829708768,-2.05564222907186,
13.8715630732994));
#415782=CARTESIAN_POINT('Ctrl Pts',(1.68877108429812,-2.05160113352414,
13.8727429581918));
#415783=CARTESIAN_POINT('Ctrl Pts',(1.69185905688211,-2.04751346170152,
13.873936442031));
#415784=CARTESIAN_POINT('Ctrl Pts',(1.69567792526876,-2.04366550527053,
13.8744652622107));
#415785=CARTESIAN_POINT('Ctrl Pts',(1.69986947625822,-2.04049205060769,
13.8742206332401));
#415786=CARTESIAN_POINT('Ctrl Pts',(1.70347741015123,-2.03776045682181,
13.8740100655632));
#415787=CARTESIAN_POINT('Ctrl Pts',(1.70745525759965,-2.03545316597251,
13.8732246156103));
#415788=CARTESIAN_POINT('Ctrl Pts',(1.71146559717085,-2.0337022740915,13.8719820486038));
#415789=CARTESIAN_POINT('Ctrl Pts',(1.71554504420834,-2.0319212102763,13.8707180692815));
#415790=CARTESIAN_POINT('Ctrl Pts',(1.71974741331291,-2.03066762254314,
13.868960862563));
#415791=CARTESIAN_POINT('Ctrl Pts',(1.72381196145766,-2.02991213038323,
13.8669057591701));
#415792=CARTESIAN_POINT('Ctrl Pts',(1.73007043057724,-2.02874884625311,
13.8637413727084));
#415793=CARTESIAN_POINT('Ctrl Pts',(1.73619124043682,-2.02870457384131,
13.8597962563956));
#415794=CARTESIAN_POINT('Ctrl Pts',(1.74182216664388,-2.02947152119733,
13.855546950204));
#415795=CARTESIAN_POINT('Ctrl Pts',(1.74853769142628,-2.03038619380833,
13.850479165618));
#415796=CARTESIAN_POINT('Ctrl Pts',(1.75474927187666,-2.03246283975302,
13.8448473071436));
#415797=CARTESIAN_POINT('Ctrl Pts',(1.76024757046896,-2.03532828571046,
13.8390832900376));
#415798=CARTESIAN_POINT('',(1.79198964208723,-2.05187161755295,13.8057746032556));
#415799=CARTESIAN_POINT('',(1.76024757046897,-2.03532828571046,13.8390832900376));
#415800=CARTESIAN_POINT('',(1.85874134473945,-1.99160353123393,13.8057746032556));
#415801=CARTESIAN_POINT('Origin',(0.,2.5406128344257E-15,13.8057746032556));
#415802=CARTESIAN_POINT('',(1.84551606885698,-1.95834194653172,13.8390832900376));
#415803=CARTESIAN_POINT('',(1.85874134473945,-1.99160353123393,13.8057746032556));
#415804=CARTESIAN_POINT('',(1.92028864223977,-1.88507938040814,13.8390832900376));
#415805=CARTESIAN_POINT('Ctrl Pts',(1.84551606885698,-1.95834194653172,
13.8390832900376));
#415806=CARTESIAN_POINT('Ctrl Pts',(1.84294049900225,-1.95186396123175,
13.8455641171218));
#415807=CARTESIAN_POINT('Ctrl Pts',(1.84144334389075,-1.94457042677117,
13.851896480191));
#415808=CARTESIAN_POINT('Ctrl Pts',(1.84153880110644,-1.93681916755994,
13.8574481026913));
#415809=CARTESIAN_POINT('Ctrl Pts',(1.84160332230502,-1.93157995613807,
13.8612005412592));
#415810=CARTESIAN_POINT('Ctrl Pts',(1.84241497732068,-1.92600873619112,
13.8646714234115));
#415811=CARTESIAN_POINT('Ctrl Pts',(1.84417157791089,-1.92045089769417,
13.8674635290331));
#415812=CARTESIAN_POINT('Ctrl Pts',(1.84558726196885,-1.91597171022223,
13.8697137499649));
#415813=CARTESIAN_POINT('Ctrl Pts',(1.84766313383683,-1.91140055847537,
13.8715630732994));
#415814=CARTESIAN_POINT('Ctrl Pts',(1.85037637634683,-1.90712407884138,
13.8727429581918));
#415815=CARTESIAN_POINT('Ctrl Pts',(1.85312089075514,-1.90279830997661,
13.873936442031));
#415816=CARTESIAN_POINT('Ctrl Pts',(1.85661340800045,-1.89865188407705,
13.8744652622107));
#415817=CARTESIAN_POINT('Ctrl Pts',(1.86053234593384,-1.89514733850471,
13.8742206332401));
#415818=CARTESIAN_POINT('Ctrl Pts',(1.86390562447202,-1.89213075376511,
13.8740100655633));
#415819=CARTESIAN_POINT('Ctrl Pts',(1.86768217033715,-1.88950690874019,
13.8732246156103));
#415820=CARTESIAN_POINT('Ctrl Pts',(1.87153645189147,-1.88743496290225,
13.8719820486038));
#415821=CARTESIAN_POINT('Ctrl Pts',(1.87545715166994,-1.88532731262467,
13.8707180692815));
#415822=CARTESIAN_POINT('Ctrl Pts',(1.8795433587,-1.88373536400636,13.868960862563));
#415823=CARTESIAN_POINT('Ctrl Pts',(1.88353280277142,-1.88265108727707,
13.8669057591701));
#415824=CARTESIAN_POINT('Ctrl Pts',(1.88967562889528,-1.88098155054489,
13.8637413727084));
#415825=CARTESIAN_POINT('Ctrl Pts',(1.89577246365241,-1.8804385226195,13.8597962563956));
#415826=CARTESIAN_POINT('Ctrl Pts',(1.90144716674655,-1.88074394526063,
13.855546950204));
#415827=CARTESIAN_POINT('Ctrl Pts',(1.90821490048343,-1.88110819676032,
13.850479165618));
#415828=CARTESIAN_POINT('Ctrl Pts',(1.91457507833541,-1.88267163136473,
13.8448473071436));
#415829=CARTESIAN_POINT('Ctrl Pts',(1.92028864223976,-1.88507938040814,
13.8390832900376));
#415830=CARTESIAN_POINT('',(1.95327352985922,-1.89898039216275,13.8057746032556));
#415831=CARTESIAN_POINT('',(1.92028864223977,-1.88507938040814,13.8390832900376));
#415832=CARTESIAN_POINT('',(2.01489071319087,-1.83347195947046,13.8057746032556));
#415833=CARTESIAN_POINT('Origin',(0.,2.5406128344257E-15,13.8057746032556));
#415834=CARTESIAN_POINT('',(1.99899831538418,-1.80139903270935,13.8390832900376));
#415835=CARTESIAN_POINT('',(2.01489071319087,-1.83347195947046,13.8057746032556));
#415836=CARTESIAN_POINT('',(2.06755050992179,-1.72228558284541,13.8390832900376));
#415837=CARTESIAN_POINT('Ctrl Pts',(1.99899831538418,-1.80139903270935,
13.8390832900376));
#415838=CARTESIAN_POINT('Ctrl Pts',(1.99590329958504,-1.79515253522466,
13.8455641171218));
#415839=CARTESIAN_POINT('Ctrl Pts',(1.99381663536526,-1.78800530143882,
13.851896480191));
#415840=CARTESIAN_POINT('Ctrl Pts',(1.99327997537005,-1.78027205325392,
13.8574481026913));
#415841=CARTESIAN_POINT('Ctrl Pts',(1.99291723751031,-1.77504501579918,
13.8612005412592));
#415842=CARTESIAN_POINT('Ctrl Pts',(1.99327208566451,-1.76942617620819,
13.8646714234115));
#415843=CARTESIAN_POINT('Ctrl Pts',(1.99456982587721,-1.76374365170476,
13.8674635290331));
#415844=CARTESIAN_POINT('Ctrl Pts',(1.99561570400154,-1.75916397696634,
13.8697137499649));
#415845=CARTESIAN_POINT('Ctrl Pts',(1.99731207727325,-1.75443883252113,
13.8715630732994));
#415846=CARTESIAN_POINT('Ctrl Pts',(1.99966771890155,-1.74995542806726,
13.8727429581918));
#415847=CARTESIAN_POINT('Ctrl Pts',(2.00205051084362,-1.74542034943843,
13.873936442031));
#415848=CARTESIAN_POINT('Ctrl Pts',(2.00519343482156,-1.74100304785055,
13.8744652622107));
#415849=CARTESIAN_POINT('Ctrl Pts',(2.0088136798135,-1.73719073354128,13.8742206332401));
#415850=CARTESIAN_POINT('Ctrl Pts',(2.01192985438474,-1.7339092327217,13.8740100655633));
#415851=CARTESIAN_POINT('Ctrl Pts',(2.01547996637693,-1.7309862947769,13.8732246156103));
#415852=CARTESIAN_POINT('Ctrl Pts',(2.01915254030653,-1.72860708343973,
13.8719820486038));
#415853=CARTESIAN_POINT('Ctrl Pts',(2.02288840121583,-1.72618687276463,
13.8707180692815));
#415854=CARTESIAN_POINT('Ctrl Pts',(2.02683125313777,-1.72426715741658,
13.868960862563));
#415855=CARTESIAN_POINT('Ctrl Pts',(2.03071904404377,-1.72286131180065,
13.8669057591701));
#415856=CARTESIAN_POINT('Ctrl Pts',(2.03670534767756,-1.7206966329579,13.8637413727084));
#415857=CARTESIAN_POINT('Ctrl Pts',(2.04273763390285,-1.71965846328019,
13.8597962563956));
#415858=CARTESIAN_POINT('Ctrl Pts',(2.04841834967123,-1.71950032866912,
13.855546950204));
#415859=CARTESIAN_POINT('Ctrl Pts',(2.05519325421116,-1.71931173502386,
13.850479165618));
#415860=CARTESIAN_POINT('Ctrl Pts',(2.0616597035305,-1.72035155388866,13.8448473071436));
#415861=CARTESIAN_POINT('Ctrl Pts',(2.06755050992178,-1.72228558284541,
13.8390832900376));
#415862=CARTESIAN_POINT('',(2.10155870455744,-1.73345176557241,13.8057746032556));
#415863=CARTESIAN_POINT('',(2.06755050992179,-1.72228558284541,13.8390832900376));
#415864=CARTESIAN_POINT('',(2.15763131637958,-1.66313893431829,13.8057746032556));
#415865=CARTESIAN_POINT('Origin',(0.,2.5406128344257E-15,13.8057746032556));
#415866=CARTESIAN_POINT('',(2.13917755793401,-1.63246810553422,13.8390832900376));
#415867=CARTESIAN_POINT('',(2.15763131637958,-1.66313893431829,13.8057746032556));
#415868=CARTESIAN_POINT('',(2.2010531700821,-1.54803025888596,13.8390832900376));
#415869=CARTESIAN_POINT('Ctrl Pts',(2.139177557934,-1.63246810553422,13.8390832900376));
#415870=CARTESIAN_POINT('Ctrl Pts',(2.13558369300996,-1.62649466527496,
13.8455641171218));
#415871=CARTESIAN_POINT('Ctrl Pts',(2.132921406088,-1.6195412958255,13.851896480191));
#415872=CARTESIAN_POINT('Ctrl Pts',(2.13175620026561,-1.6118775221577,13.8574481026913));
#415873=CARTESIAN_POINT('Ctrl Pts',(2.13096861730817,-1.60669744374196,
13.8612005412592));
#415874=CARTESIAN_POINT('Ctrl Pts',(2.13086429714498,-1.60106837695737,
13.8646714234115));
#415875=CARTESIAN_POINT('Ctrl Pts',(2.13169454073316,-1.59529898271048,
13.8674635290331));
#415876=CARTESIAN_POINT('Ctrl Pts',(2.13236365277751,-1.59064929768537,
13.8697137499649));
#415877=CARTESIAN_POINT('Ctrl Pts',(2.13366923836871,-1.58580160559849,
13.8715630732994));
#415878=CARTESIAN_POINT('Ctrl Pts',(2.13565160270894,-1.58114111264167,
13.8727429581918));
#415879=CARTESIAN_POINT('Ctrl Pts',(2.13765681509752,-1.57642690444882,
13.873936442031));
#415880=CARTESIAN_POINT('Ctrl Pts',(2.14042923016756,-1.57176812358589,
13.8744652622107));
#415881=CARTESIAN_POINT('Ctrl Pts',(2.14372669008493,-1.56767341086243,
13.8742206332401));
#415882=CARTESIAN_POINT('Ctrl Pts',(2.1465650230616,-1.56414883180941,13.8740100655633));
#415883=CARTESIAN_POINT('Ctrl Pts',(2.14986507577125,-1.56094625261451,
13.8732246156103));
#415884=CARTESIAN_POINT('Ctrl Pts',(2.15333150170257,-1.55827560903701,
13.8719820486038));
#415885=CARTESIAN_POINT('Ctrl Pts',(2.15685766220472,-1.55555894406714,
13.8707180692815));
#415886=CARTESIAN_POINT('Ctrl Pts',(2.16063091998952,-1.55332423737825,
13.868960862563));
#415887=CARTESIAN_POINT('Ctrl Pts',(2.16439118512307,-1.5516061785463,13.8669057591701));
#415888=CARTESIAN_POINT('Ctrl Pts',(2.17018112840377,-1.54896076317355,
13.8637413727084));
#415889=CARTESIAN_POINT('Ctrl Pts',(2.17610872222764,-1.54743436059142,
13.8597962563956));
#415890=CARTESIAN_POINT('Ctrl Pts',(2.18175764644407,-1.54681372108791,
13.855546950204));
#415891=CARTESIAN_POINT('Ctrl Pts',(2.18849463591514,-1.5460735373573,13.850479165618));
#415892=CARTESIAN_POINT('Ctrl Pts',(2.1950243235485,-1.54658282065948,13.8448473071436));
#415893=CARTESIAN_POINT('Ctrl Pts',(2.2010531700821,-1.54803025888596,13.8390832900376));
#415894=CARTESIAN_POINT('',(2.23585835280962,-1.55638730348161,13.8057746032556));
#415895=CARTESIAN_POINT('',(2.2010531700821,-1.54803025888596,13.8390832900376));
#415896=CARTESIAN_POINT('',(2.28601323914189,-1.48173799395684,13.8057746032556));
#415897=CARTESIAN_POINT('Origin',(0.,2.5406128344257E-15,13.8057746032556));
#415898=CARTESIAN_POINT('',(2.26512092677523,-1.45267337245503,13.8390832900376));
#415899=CARTESIAN_POINT('',(2.28601323914189,-1.48173799395684,13.8057746032556));
#415900=CARTESIAN_POINT('',(2.31990818454372,-1.36347304896064,13.8390832900376));
#415901=CARTESIAN_POINT('Ctrl Pts',(2.26512092677523,-1.45267337245503,
13.8390832900376));
#415902=CARTESIAN_POINT('Ctrl Pts',(2.26105212930441,-1.44701274168059,
13.8455641171218));
#415903=CARTESIAN_POINT('Ctrl Pts',(2.25783193676049,-1.44029951009396,
13.851896480191));
#415904=CARTESIAN_POINT('Ctrl Pts',(2.25604593936343,-1.4327562120926,13.8574481026913));
#415905=CARTESIAN_POINT('Ctrl Pts',(2.25483875254292,-1.42765756528305,
13.8612005412592));
#415906=CARTESIAN_POINT('Ctrl Pts',(2.25427595829582,-1.42205573181558,
13.8646714234115));
#415907=CARTESIAN_POINT('Ctrl Pts',(2.25463318012539,-1.41623786219207,
13.8674635290331));
#415908=CARTESIAN_POINT('Ctrl Pts',(2.25492107325948,-1.41154910976695,
13.8697137499649));
#415909=CARTESIAN_POINT('Ctrl Pts',(2.25582718271348,-1.40661113062945,
13.8715630732994));
#415910=CARTESIAN_POINT('Ctrl Pts',(2.25742307745801,-1.40180456398137,
13.8727429581918));
#415911=CARTESIAN_POINT('Ctrl Pts',(2.2590373659355,-1.39694259850223,13.873936442031));
#415912=CARTESIAN_POINT('Ctrl Pts',(2.26142082213276,-1.39207334178225,
13.8744652622107));
#415913=CARTESIAN_POINT('Ctrl Pts',(2.26437355292386,-1.38772348028219,
13.8742206332401));
#415914=CARTESIAN_POINT('Ctrl Pts',(2.26691515566827,-1.38397927848782,
13.8740100655633));
#415915=CARTESIAN_POINT('Ctrl Pts',(2.26994318778909,-1.38051837067896,
13.8732246156103));
#415916=CARTESIAN_POINT('Ctrl Pts',(2.27318039722948,-1.37757406755353,
13.8719820486038));
#415917=CARTESIAN_POINT('Ctrl Pts',(2.27647339130811,-1.37457902724603,
13.8707180692815));
#415918=CARTESIAN_POINT('Ctrl Pts',(2.28005194454775,-1.37204420082063,
13.868960862563));
#415919=CARTESIAN_POINT('Ctrl Pts',(2.28365965996478,-1.37002536217072,
13.8669057591701));
#415920=CARTESIAN_POINT('Ctrl Pts',(2.28921471177514,-1.36691681507081,
13.8637413727084));
#415921=CARTESIAN_POINT('Ctrl Pts',(2.29499816603867,-1.36491233754161,
13.8597962563956));
#415922=CARTESIAN_POINT('Ctrl Pts',(2.30057770604451,-1.36383332339915,
13.855546950204));
#415923=CARTESIAN_POINT('Ctrl Pts',(2.3072319468933,-1.36254647538379,13.850479165618));
#415924=CARTESIAN_POINT('Ctrl Pts',(2.3137814188468,-1.36252183392703,13.8448473071436));
#415925=CARTESIAN_POINT('Ctrl Pts',(2.31990818454372,-1.36347304896064,
13.8390832900376));
#415926=CARTESIAN_POINT('',(2.35527873261451,-1.36896534067195,13.8057746032556));
#415927=CARTESIAN_POINT('',(2.31990818454372,-1.36347304896064,13.8390832900376));
#415928=CARTESIAN_POINT('',(2.39918212096335,-1.29047633171518,13.8057746032556));
#415929=CARTESIAN_POINT('Origin',(0.,2.5406128344257E-15,13.8057746032556));
#415930=CARTESIAN_POINT('',(2.37599028956742,-1.2632113377564,13.8390832900376));
#415931=CARTESIAN_POINT('',(2.39918212096335,-1.29047633171518,13.8057746032556));
#415932=CARTESIAN_POINT('',(2.42332459279512,-1.1698421508517,13.8390832900376));
#415933=CARTESIAN_POINT('Ctrl Pts',(2.37599028956742,-1.2632113377564,13.8390832900376));
#415934=CARTESIAN_POINT('Ctrl Pts',(2.37147363672568,-1.25790118703063,
13.8455641171218));
#415935=CARTESIAN_POINT('Ctrl Pts',(2.36771696840989,-1.25147276875544,
13.851896480191));
#415936=CARTESIAN_POINT('Ctrl Pts',(2.36532206495616,-1.24410014582415,
13.8574481026913));
#415937=CARTESIAN_POINT('Ctrl Pts',(2.3637033079017,-1.2391168612741,13.8612005412592));
#415938=CARTESIAN_POINT('Ctrl Pts',(2.36268578487355,-1.23357954040124,
13.8646714234115));
#415939=CARTESIAN_POINT('Ctrl Pts',(2.36256760769217,-1.22775191236357,
13.8674635290331));
#415940=CARTESIAN_POINT('Ctrl Pts',(2.36247236603471,-1.22305529541225,
13.8697137499649));
#415941=CARTESIAN_POINT('Ctrl Pts',(2.36297296934257,-1.21805989066056,
13.8715630732994));
#415942=CARTESIAN_POINT('Ctrl Pts',(2.36417177407519,-1.21313923722925,
13.8727429581918));
#415943=CARTESIAN_POINT('Ctrl Pts',(2.3653843958181,-1.20816187004193,13.873936442031));
#415944=CARTESIAN_POINT('Ctrl Pts',(2.36736303163483,-1.20311454156498,
13.8744652622107));
#415945=CARTESIAN_POINT('Ctrl Pts',(2.36995138336341,-1.19853847889894,
13.8742206332401));
#415946=CARTESIAN_POINT('Ctrl Pts',(2.37217934192864,-1.19459957140841,
13.8740100655633));
#415947=CARTESIAN_POINT('Ctrl Pts',(2.37491520240646,-1.19090336675605,
13.8732246156103));
#415948=CARTESIAN_POINT('Ctrl Pts',(2.37790165226118,-1.1877049979342,13.8719820486038));
#415949=CARTESIAN_POINT('Ctrl Pts',(2.38093956558401,-1.18445151378818,
13.8707180692815));
#415950=CARTESIAN_POINT('Ctrl Pts',(2.3842995995971,-1.1816334364779,13.868960862563));
#415951=CARTESIAN_POINT('Ctrl Pts',(2.38773075654675,-1.17932725304818,
13.8669057591701));
#415952=CARTESIAN_POINT('Ctrl Pts',(2.39301394893348,-1.17577626108917,
13.8637413727084));
#415953=CARTESIAN_POINT('Ctrl Pts',(2.39861477570277,-1.17330704808014,
13.8597962563956));
#415954=CARTESIAN_POINT('Ctrl Pts',(2.40408780057982,-1.17177683995984,
13.855546950204));
#415955=CARTESIAN_POINT('Ctrl Pts',(2.41061500993135,-1.16995189142096,
13.850479165618));
#415956=CARTESIAN_POINT('Ctrl Pts',(2.41714068054974,-1.16939348919007,
13.8448473071436));
#415957=CARTESIAN_POINT('Ctrl Pts',(2.42332459279512,-1.1698421508517,13.8390832900376));
#415958=CARTESIAN_POINT('',(2.45902512104748,-1.17243313938352,13.8057746032556));
#415959=CARTESIAN_POINT('',(2.42332459279512,-1.1698421508517,13.8390832900376));
#415960=CARTESIAN_POINT('',(2.49638484160699,-1.09062676239955,13.8057746032556));
#415961=CARTESIAN_POINT('Origin',(0.,2.5406128344257E-15,13.8057746032556));
#415962=CARTESIAN_POINT('',(2.47104782899334,-1.06534284002019,13.8390832900376));
#415963=CARTESIAN_POINT('',(2.49638484160699,-1.09062676239955,13.8057746032556));
#415964=CARTESIAN_POINT('',(2.51061417570188,-0.96842614623922,13.8390832900376));
#415965=CARTESIAN_POINT('Ctrl Pts',(2.47104782899333,-1.06534284002019,
13.8390832900376));
#415966=CARTESIAN_POINT('Ctrl Pts',(2.46611337836014,-1.06041850752007,
13.8455641171218));
#415967=CARTESIAN_POINT('Ctrl Pts',(2.46184523428033,-1.05431768261933,
13.851896480191));
#415968=CARTESIAN_POINT('Ctrl Pts',(2.45885736245727,-1.04716479834732,
13.8574481026913));
#415969=CARTESIAN_POINT('Ctrl Pts',(2.45683780772999,-1.04233003899326,
13.8612005412592));
#415970=CARTESIAN_POINT('Ctrl Pts',(2.45537232736866,-1.03689408067184,
13.8646714234115));
#415971=CARTESIAN_POINT('Ctrl Pts',(2.45477953762597,-1.03109547612309,
13.8674635290331));
#415972=CARTESIAN_POINT('Ctrl Pts',(2.45430179499447,-1.0264222498565,13.8697137499649));
#415973=CARTESIAN_POINT('Ctrl Pts',(2.45439356072379,-1.02140266308507,
13.8715630732994));
#415974=CARTESIAN_POINT('Ctrl Pts',(2.45518729759679,-1.01640066900726,
13.8727429581918));
#415975=CARTESIAN_POINT('Ctrl Pts',(2.4559901828075,-1.01134102366916,13.873936442031));
#415976=CARTESIAN_POINT('Ctrl Pts',(2.45755083074879,-1.00614921257353,
13.8744652622107));
#415977=CARTESIAN_POINT('Ctrl Pts',(2.45975757836114,-1.00137740168355,
13.8742206332401));
#415978=CARTESIAN_POINT('Ctrl Pts',(2.46165706605052,-0.99727000127633,
13.8740100655633));
#415979=CARTESIAN_POINT('Ctrl Pts',(2.46408254818524,-0.993363097412604,
13.8732246156103));
#415980=CARTESIAN_POINT('Ctrl Pts',(2.46679836412324,-0.989931947511155,
13.8719820486038));
#415981=CARTESIAN_POINT('Ctrl Pts',(2.46956097987833,-0.986441670926813,
13.8707180692815));
#415982=CARTESIAN_POINT('Ctrl Pts',(2.47268013419288,-0.983359096571208,
13.868960862563));
#415983=CARTESIAN_POINT('Ctrl Pts',(2.47591189889175,-0.980780915631897,
13.8669057591701));
#415984=CARTESIAN_POINT('Ctrl Pts',(2.48088807308118,-0.976811110079414,
13.8637413727084));
#415985=CARTESIAN_POINT('Ctrl Pts',(2.48626899977814,-0.973893593795741,
13.8597962563956));
#415986=CARTESIAN_POINT('Ctrl Pts',(2.49159908744885,-0.97192237498016,
13.855546950204));
#415987=CARTESIAN_POINT('Ctrl Pts',(2.4979558278018,-0.969571470649191,
13.850479165618));
#415988=CARTESIAN_POINT('Ctrl Pts',(2.50441426982377,-0.968483023718886,
13.8448473071436));
#415989=CARTESIAN_POINT('Ctrl Pts',(2.51061417570188,-0.96842614623922,
13.8390832900376));
#415990=CARTESIAN_POINT('',(2.54640710301047,-0.968098588990333,13.8057746032556));
#415991=CARTESIAN_POINT('',(2.51061417570188,-0.96842614623922,13.8390832900376));
#415992=CARTESIAN_POINT('',(2.57697453300423,-0.883519251920907,13.8057746032556));
#415993=CARTESIAN_POINT('Origin',(0.,2.5406128344257E-15,13.8057746032556));
#415994=CARTESIAN_POINT('',(2.5496609528115,-0.860384661452853,13.8390832900376));
#415995=CARTESIAN_POINT('',(2.57697453300423,-0.883519251920907,13.8057746032556));
#415996=CARTESIAN_POINT('',(2.58119603549153,-0.760565425402582,13.8390832900376));
#415997=CARTESIAN_POINT('Ctrl Pts',(2.5496609528115,-0.860384661452853,
13.8390832900376));
#415998=CARTESIAN_POINT('Ctrl Pts',(2.54434154234169,-0.855878917798706,
13.8455641171218));
#415999=CARTESIAN_POINT('Ctrl Pts',(2.5395903262925,-0.850146286255557,
13.851896480191));
#416000=CARTESIAN_POINT('Ctrl Pts',(2.53602936989415,-0.843260741907522,
13.8574481026913));
#416001=CARTESIAN_POINT('Ctrl Pts',(2.53362245729755,-0.838606682275279,
13.8612005412592));
#416002=CARTESIAN_POINT('Ctrl Pts',(2.53171877213306,-0.833308261911033,
13.8646714234115));
#416003=CARTESIAN_POINT('Ctrl Pts',(2.53065531474699,-0.827577269607798,
13.8674635290331));
#416004=CARTESIAN_POINT('Ctrl Pts',(2.52979825043985,-0.822958533575708,
13.8697137499649));
#416005=CARTESIAN_POINT('Ctrl Pts',(2.52948056790483,-0.817948169306319,
13.8715630732994));
#416006=CARTESIAN_POINT('Ctrl Pts',(2.52986395473027,-0.812898122027324,
13.8727429581918));
#416007=CARTESIAN_POINT('Ctrl Pts',(2.53025176034016,-0.807789869643406,
13.873936442031));
#416008=CARTESIAN_POINT('Ctrl Pts',(2.53138403455146,-0.802488126575336,
13.8744652622107));
#416009=CARTESIAN_POINT('Ctrl Pts',(2.5331944925063,-0.797552323075592,
13.8742206332401));
#416010=CARTESIAN_POINT('Ctrl Pts',(2.53475286854267,-0.793303763823721,
13.8740100655633));
#416011=CARTESIAN_POINT('Ctrl Pts',(2.53685183115084,-0.789212160549251,
13.8732246156103));
#416012=CARTESIAN_POINT('Ctrl Pts',(2.53927893986515,-0.785571063304695,
13.8719820486038));
#416013=CARTESIAN_POINT('Ctrl Pts',(2.54174787330044,-0.781867221496848,
13.8707180692815));
#416014=CARTESIAN_POINT('Ctrl Pts',(2.54460539045911,-0.778540664119665,
13.868960862563));
#416015=CARTESIAN_POINT('Ctrl Pts',(2.54761625604633,-0.775707643039546,
13.8669057591701));
#416016=CARTESIAN_POINT('Ctrl Pts',(2.55225229642025,-0.771345442294568,
13.8637413727084));
#416017=CARTESIAN_POINT('Ctrl Pts',(2.5573775138655,-0.767999038325763,
13.8597962563956));
#416018=CARTESIAN_POINT('Ctrl Pts',(2.56252919347581,-0.765599926950894,
13.855546950204));
#416019=CARTESIAN_POINT('Ctrl Pts',(2.56867316177193,-0.762738711708286,
13.850479165618));
#416020=CARTESIAN_POINT('Ctrl Pts',(2.57502139533138,-0.761127463513312,
13.8448473071436));
#416021=CARTESIAN_POINT('Ctrl Pts',(2.58119603549152,-0.760565425402582,
13.8390832900376));
#416022=CARTESIAN_POINT('',(2.61684316583053,-0.757321502212443,13.8057746032556));
#416023=CARTESIAN_POINT('',(2.58119603549153,-0.760565425402582,13.8390832900376));
#416024=CARTESIAN_POINT('',(2.64041488405521,-0.670532066591146,13.8057746032556));
#416025=CARTESIAN_POINT('Origin',(0.,2.5406128344257E-15,13.8057746032556));
#416026=CARTESIAN_POINT('',(2.61130650365315,-0.649700764917019,13.8390832900376));
#416027=CARTESIAN_POINT('',(2.64041488405521,-0.670532066591146,13.8057746032556));
#416028=CARTESIAN_POINT('',(2.63460046153234,-0.547643267144351,13.8390832900376));
#416029=CARTESIAN_POINT('Ctrl Pts',(2.61130650365314,-0.649700764917019,
13.8390832900376));
#416030=CARTESIAN_POINT('Ctrl Pts',(2.60563753314576,-0.645643595089471,
13.8455641171218));
#416031=CARTESIAN_POINT('Ctrl Pts',(2.6004348636861,-0.640317306621022,
13.851896480191));
#416032=CARTESIAN_POINT('Ctrl Pts',(2.59632452028977,-0.633744924358559,
13.8574481026913));
#416033=CARTESIAN_POINT('Ctrl Pts',(2.59354626743007,-0.629302536447119,
13.8612005412592));
#416034=CARTESIAN_POINT('Ctrl Pts',(2.5912170461731,-0.624176914153404,
13.8646714234115));
#416035=CARTESIAN_POINT('Ctrl Pts',(2.5896899982771,-0.618551672903904,
13.8674635290331));
#416036=CARTESIAN_POINT('Ctrl Pts',(2.58845931591587,-0.614018164032572,
13.8697137499649));
#416037=CARTESIAN_POINT('Ctrl Pts',(2.58773429924137,-0.609050365412783,
13.8715630732994));
#416038=CARTESIAN_POINT('Ctrl Pts',(2.58770478464319,-0.603985872164047,
13.8727429581918));
#416039=CARTESIAN_POINT('Ctrl Pts',(2.58767492986991,-0.598863007311117,
13.873936442031));
#416040=CARTESIAN_POINT('Ctrl Pts',(2.58837129525315,-0.593486614496006,
13.8744652622107));
#416041=CARTESIAN_POINT('Ctrl Pts',(2.58977341525151,-0.588419665344441,
13.8742206332401));
#416042=CARTESIAN_POINT('Ctrl Pts',(2.59098030889944,-0.584058220708777,
13.8740100655633));
#416043=CARTESIAN_POINT('Ctrl Pts',(2.59273878373123,-0.579809146968282,
13.8732246156103));
#416044=CARTESIAN_POINT('Ctrl Pts',(2.59486103321378,-0.575982333282046,
13.8719820486038));
#416045=CARTESIAN_POINT('Ctrl Pts',(2.59701985398461,-0.572089574706832,
13.8707180692815));
#416046=CARTESIAN_POINT('Ctrl Pts',(2.59959671768218,-0.568541171998573,
13.868960862563));
#416047=CARTESIAN_POINT('Ctrl Pts',(2.60236664734402,-0.565472164065521,
13.8669057591701));
#416048=CARTESIAN_POINT('Ctrl Pts',(2.60663170181863,-0.560746597854291,
13.8637413727084));
#416049=CARTESIAN_POINT('Ctrl Pts',(2.61146710253567,-0.556993575966648,
13.8597962563956));
#416050=CARTESIAN_POINT('Ctrl Pts',(2.61640609050775,-0.554182537722866,
13.855546950204));
#416051=CARTESIAN_POINT('Ctrl Pts',(2.62229639965171,-0.550830052483992,
13.850479165618));
#416052=CARTESIAN_POINT('Ctrl Pts',(2.62849217830169,-0.548706725615247,
13.8448473071436));
#416053=CARTESIAN_POINT('Ctrl Pts',(2.63460046153234,-0.547643267144351,
13.8390832900376));
#416054=CARTESIAN_POINT('',(2.66986456913072,-0.541504565786582,13.8057746032556));
#416055=CARTESIAN_POINT('',(2.63460046153234,-0.547643267144351,13.8390832900376));
#416056=CARTESIAN_POINT('',(2.68628370969059,-0.453082600988223,13.8057746032556));
#416057=CARTESIAN_POINT('Origin',(0.,2.5406128344257E-15,13.8057746032556));
#416058=CARTESIAN_POINT('',(2.65557424054823,-0.434693216983744,13.8390832900376));
#416059=CARTESIAN_POINT('',(2.68628370969059,-0.453082600988223,13.8057746032556));
#416060=CARTESIAN_POINT('',(2.67047205618014,-0.331076633298054,13.8390832900376));
#416061=CARTESIAN_POINT('Ctrl Pts',(2.65557424054823,-0.434693216983744,
13.8390832900376));
#416062=CARTESIAN_POINT('Ctrl Pts',(2.64959343606668,-0.43111162077861,
13.8455641171218));
#416063=CARTESIAN_POINT('Ctrl Pts',(2.64397393610343,-0.426227120955838,
13.851896480191));
#416064=CARTESIAN_POINT('Ctrl Pts',(2.63934155936626,-0.420011638898538,
13.8574481026913));
#416065=CARTESIAN_POINT('Ctrl Pts',(2.63621045505786,-0.415810486066509,
13.8612005412592));
#416066=CARTESIAN_POINT('Ctrl Pts',(2.63347119829158,-0.41089177201402,
13.8646714234115));
#416067=CARTESIAN_POINT('Ctrl Pts',(2.63149072213746,-0.405409716870673,
13.8674635290331));
#416068=CARTESIAN_POINT('Ctrl Pts',(2.6298946117102,-0.40099160491366,13.8697137499649));
#416069=CARTESIAN_POINT('Ctrl Pts',(2.62876708576257,-0.396099431823667,
13.8715630732994));
#416070=CARTESIAN_POINT('Ctrl Pts',(2.62832486615555,-0.391054195972177,
13.8727429581918));
#416071=CARTESIAN_POINT('Ctrl Pts',(2.6278775496777,-0.385950810470619,
13.873936442031));
#416072=CARTESIAN_POINT('Ctrl Pts',(2.62813337203614,-0.3805355469156,13.8744652622107));
#416073=CARTESIAN_POINT('Ctrl Pts',(2.62911782320076,-0.375371171822829,
13.8742206332401));
#416074=CARTESIAN_POINT('Ctrl Pts',(2.62996520278216,-0.370925866497836,
13.8740100655633));
#416075=CARTESIAN_POINT('Ctrl Pts',(2.63137148747768,-0.366547599176018,
13.8732246156103));
#416076=CARTESIAN_POINT('Ctrl Pts',(2.63317475450832,-0.362560535861801,
13.8719820486038));
#416077=CARTESIAN_POINT('Ctrl Pts',(2.63500909601863,-0.358504766185281,
13.8707180692815));
#416078=CARTESIAN_POINT('Ctrl Pts',(2.63728815765234,-0.354758132180522,
13.868960862563));
#416079=CARTESIAN_POINT('Ctrl Pts',(2.63979871796391,-0.351473561135978,
13.8669057591701));
#416080=CARTESIAN_POINT('Ctrl Pts',(2.64366440330536,-0.34641607732197,
13.8637413727084));
#416081=CARTESIAN_POINT('Ctrl Pts',(2.64817780850021,-0.342281413256947,
13.8597962563956));
#416082=CARTESIAN_POINT('Ctrl Pts',(2.65287123668398,-0.339077155139974,
13.855546950204));
#416083=CARTESIAN_POINT('Ctrl Pts',(2.65846868764025,-0.335255710140978,
13.850479165618));
#416084=CARTESIAN_POINT('Ctrl Pts',(2.66447077949609,-0.33263443498845,
13.8448473071436));
#416085=CARTESIAN_POINT('Ctrl Pts',(2.67047205618014,-0.331076633298055,
13.8390832900376));
#416086=CARTESIAN_POINT('',(2.70511846421999,-0.322084005817376,13.8057746032556));
#416087=CARTESIAN_POINT('',(2.67047205618014,-0.331076633298054,13.8390832900376));
#416088=CARTESIAN_POINT('',(2.71427576044359,-0.232617945429092,13.8057746032556));
#416089=CARTESIAN_POINT('Origin',(0.,2.5406128344257E-15,13.8057746032556));
#416090=CARTESIAN_POINT('',(2.68216956901137,-0.216792857410774,13.8390832900376));
#416091=CARTESIAN_POINT('',(2.71427576044359,-0.232617945429092,13.8057746032556));
#416092=CARTESIAN_POINT('',(2.68857209989094,-0.112306739080959,13.8390832900376));
#416093=CARTESIAN_POINT('Ctrl Pts',(2.68216956901137,-0.216792857410774,
13.8390832900376));
#416094=CARTESIAN_POINT('Ctrl Pts',(2.67591673182272,-0.213710669759878,
13.8455641171218));
#416095=CARTESIAN_POINT('Ctrl Pts',(2.66991779820098,-0.209300464123221,
13.851896480191));
#416096=CARTESIAN_POINT('Ctrl Pts',(2.66479421582587,-0.203483245278693,
13.8574481026913));
#416097=CARTESIAN_POINT('Ctrl Pts',(2.66133109705134,-0.199551285505029,
13.8612005412592));
#416098=CARTESIAN_POINT('Ctrl Pts',(2.65820003407759,-0.194872212924259,
13.8646714234115));
#416099=CARTESIAN_POINT('Ctrl Pts',(2.6557793094074,-0.189569826059568,
13.8674635290331));
#416100=CARTESIAN_POINT('Ctrl Pts',(2.65382839276567,-0.18529651282301,
13.8697137499649));
#416101=CARTESIAN_POINT('Ctrl Pts',(2.65230586104407,-0.180512521867566,
13.8715630732994));
#416102=CARTESIAN_POINT('Ctrl Pts',(2.65145387932672,-0.175520118625508,
13.8727429581918));
#416103=CARTESIAN_POINT('Ctrl Pts',(2.65059207796165,-0.170470174663835,
13.873936442031));
#416104=CARTESIAN_POINT('Ctrl Pts',(2.65040565483971,-0.165052078054418,
13.8744652622107));
#416105=CARTESIAN_POINT('Ctrl Pts',(2.65096588581051,-0.159824645084622,
13.8742206332401));
#416106=CARTESIAN_POINT('Ctrl Pts',(2.65144811215407,-0.155325061843814,
13.8740100655633));
#416107=CARTESIAN_POINT('Ctrl Pts',(2.6524928481207,-0.150846737587331,
13.8732246156103));
#416108=CARTESIAN_POINT('Ctrl Pts',(2.65396513225485,-0.146725957893671,
13.8719820486038));
#416109=CARTESIAN_POINT('Ctrl Pts',(2.65546278726455,-0.142534167593885,
13.8707180692815));
#416110=CARTESIAN_POINT('Ctrl Pts',(2.65742888005524,-0.13861423552378,
13.868960862563));
#416111=CARTESIAN_POINT('Ctrl Pts',(2.65966336365188,-0.135135959646133,
13.8669057591701));
#416112=CARTESIAN_POINT('Ctrl Pts',(2.66310395436203,-0.129780214949702,
13.8637413727084));
#416113=CARTESIAN_POINT('Ctrl Pts',(2.66726532806777,-0.125291424214479,
13.8597962563956));
#416114=CARTESIAN_POINT('Ctrl Pts',(2.67168196247302,-0.12171527003342,
13.855546950204));
#416115=CARTESIAN_POINT('Ctrl Pts',(2.67694930512901,-0.117450296360274,
13.850479165618));
#416116=CARTESIAN_POINT('Ctrl Pts',(2.68271776725967,-0.114348517077624,
13.8448473071436));
#416117=CARTESIAN_POINT('Ctrl Pts',(2.68857209989094,-0.112306739080959,
13.8390832900376));
#416118=CARTESIAN_POINT('',(2.722370242243,-0.100520029929576,13.8057746032556));
#416119=CARTESIAN_POINT('',(2.68857209989094,-0.112306739080959,13.8390832900376));
#416120=CARTESIAN_POINT('',(2.72420475383482,-0.010605255822389,13.8057746032556));
#416121=CARTESIAN_POINT('Origin',(0.,2.5406128344257E-15,13.8057746032556));
#416122=CARTESIAN_POINT('',(2.69091550151957,0.00255022285996096,13.8390832900376));
#416123=CARTESIAN_POINT('',(2.72420475383482,-0.010605255822389,13.8057746032556));
#416124=CARTESIAN_POINT('',(2.68878013986014,0.107210537955413,13.8390832900376));
#416125=CARTESIAN_POINT('Ctrl Pts',(2.69091550151957,0.00255022285996075,
13.8390832900376));
#416126=CARTESIAN_POINT('Ctrl Pts',(2.68443224322366,0.00511249050632783,
13.8455641171218));
#416127=CARTESIAN_POINT('Ctrl Pts',(2.67809379785693,0.00901905276598984,
13.851896480191));
#416128=CARTESIAN_POINT('Ctrl Pts',(2.67251310643925,0.0143992957661106,
13.8574481026913));
#416129=CARTESIAN_POINT('Ctrl Pts',(2.66874101968268,0.0180358959378414,
13.8612005412592));
#416130=CARTESIAN_POINT('Ctrl Pts',(2.66523898720895,0.0224441885908644,
13.8646714234115));
#416131=CARTESIAN_POINT('Ctrl Pts',(2.66239412354597,0.0275316206671468,
13.8674635290331));
#416132=CARTESIAN_POINT('Ctrl Pts',(2.66010138371815,0.0316316969887058,
13.8697137499649));
#416133=CARTESIAN_POINT('Ctrl Pts',(2.65819397841997,0.0362756691390899,
13.8715630732994));
#416134=CARTESIAN_POINT('Ctrl Pts',(2.65693790439007,0.0411820161518279,
13.8727429581918));
#416135=CARTESIAN_POINT('Ctrl Pts',(2.65566735328368,0.0461449120297329,
13.873936442031));
#416136=CARTESIAN_POINT('Ctrl Pts',(2.65503992529648,0.0515297851545395,
13.8744652622107));
#416137=CARTESIAN_POINT('Ctrl Pts',(2.65517220782878,0.0567854882974133,
13.8742206332401));
#416138=CARTESIAN_POINT('Ctrl Pts',(2.65528607179774,0.0613094054699473,
13.8740100655633));
#416139=CARTESIAN_POINT('Ctrl Pts',(2.65596230648999,0.0658579841520367,
13.8732246156103));
#416140=CARTESIAN_POINT('Ctrl Pts',(2.65709380991966,0.070085057116158,
13.8719820486038));
#416141=CARTESIAN_POINT('Ctrl Pts',(2.65824481178174,0.0743849723663609,
13.8707180692815));
#416142=CARTESIAN_POINT('Ctrl Pts',(2.65988485170627,0.0784521160006324,
13.868960862563));
#416143=CARTESIAN_POINT('Ctrl Pts',(2.66182838846831,0.0821009493592947,
13.8669057591701));
#416144=CARTESIAN_POINT('Ctrl Pts',(2.66482098798363,0.0877193133408292,
13.8637413727084));
#416145=CARTESIAN_POINT('Ctrl Pts',(2.66860263694484,0.0925323585845062,
13.8597962563956));
#416146=CARTESIAN_POINT('Ctrl Pts',(2.6727130855983,0.0964566101136009,
13.855546950204));
#416147=CARTESIAN_POINT('Ctrl Pts',(2.67761526665769,0.101136729764772,
13.850479165618));
#416148=CARTESIAN_POINT('Ctrl Pts',(2.68311171089942,0.104698371348177,
13.8448473071436));
#416149=CARTESIAN_POINT('Ctrl Pts',(2.68878013986013,0.107210537955413,
13.8390832900376));
#416150=CARTESIAN_POINT('',(2.72150509546337,0.121712890172768,13.8057746032556));
#416151=CARTESIAN_POINT('',(2.68878013986014,0.107210537955413,13.8390832900376));
#416152=CARTESIAN_POINT('',(2.71600461405142,0.211478010012068,13.8057746032556));
#416153=CARTESIAN_POINT('Origin',(0.,2.5406128344257E-15,13.8057746032556));
#416154=CARTESIAN_POINT('',(2.68175383533497,0.22187633181832,13.8390832900376));
#416155=CARTESIAN_POINT('',(2.71600461405142,0.211478010012068,13.8057746032556));
#416156=CARTESIAN_POINT('',(2.67109479161606,0.326014346550186,13.8390832900376));
#416157=CARTESIAN_POINT('Ctrl Pts',(2.68175383533497,0.22187633181832,13.8390832900376));
#416158=CARTESIAN_POINT('Ctrl Pts',(2.67508330094609,0.223901627991715,
13.8455641171218));
#416159=CARTESIAN_POINT('Ctrl Pts',(2.66844752514252,0.227278549347082,
13.851896480191));
#416160=CARTESIAN_POINT('Ctrl Pts',(2.66244686326291,0.232186011873307,
13.8574481026913));
#416161=CARTESIAN_POINT('Ctrl Pts',(2.6583909111393,0.235503051468959,13.8612005412592));
#416162=CARTESIAN_POINT('Ctrl Pts',(2.65454121461392,0.239611227733946,
13.8646714234115));
#416163=CARTESIAN_POINT('Ctrl Pts',(2.65129114405646,0.244449849000719,
13.8674635290331));
#416164=CARTESIAN_POINT('Ctrl Pts',(2.64867183884781,0.248349403075825,
13.8697137499649));
#416165=CARTESIAN_POINT('Ctrl Pts',(2.64639225344063,0.252822451552694,
13.8715630732994));
#416166=CARTESIAN_POINT('Ctrl Pts',(2.6447404460636,0.257610091406232,13.8727429581918));
#416167=CARTESIAN_POINT('Ctrl Pts',(2.64306960052388,0.262452911947122,
13.873936442031));
#416168=CARTESIAN_POINT('Ctrl Pts',(2.64200534310115,0.267768726145111,
13.8744652622107));
#416169=CARTESIAN_POINT('Ctrl Pts',(2.64170879687653,0.273017723623774,
13.8742206332401));
#416170=CARTESIAN_POINT('Ctrl Pts',(2.64145354072497,0.277535868805646,
13.8740100655633));
#416171=CARTESIAN_POINT('Ctrl Pts',(2.64175677391253,0.282124431872679,
13.8732246156103));
#416172=CARTESIAN_POINT('Ctrl Pts',(2.64253996666907,0.286429667634104,
13.8719820486038));
#416173=CARTESIAN_POINT('Ctrl Pts',(2.64333665565605,0.29080909260817,13.8707180692815));
#416174=CARTESIAN_POINT('Ctrl Pts',(2.64463972851931,0.294996381636749,
13.868960862563));
#416175=CARTESIAN_POINT('Ctrl Pts',(2.64627938453026,0.298791490092439,
13.8669057591701));
#416176=CARTESIAN_POINT('Ctrl Pts',(2.64880407759472,0.304635084073745,
13.8637413727084));
#416177=CARTESIAN_POINT('Ctrl Pts',(2.65218083556149,0.309740353803876,
13.8597962563956));
#416178=CARTESIAN_POINT('Ctrl Pts',(2.65595774410555,0.313986587434537,
13.855546950204));
#416179=CARTESIAN_POINT('Ctrl Pts',(2.66046214036218,0.319050707639619,
13.850479165618));
#416180=CARTESIAN_POINT('Ctrl Pts',(2.66564998878541,0.32304850938667,13.8448473071436));
#416181=CARTESIAN_POINT('Ctrl Pts',(2.67109479161606,0.326014346550185,
13.8390832900376));
#416182=CARTESIAN_POINT('',(2.70252878129015,0.343135831072226,13.8057746032556));
#416183=CARTESIAN_POINT('',(2.67109479161606,0.326014346550186,13.8390832900376));
#416184=CARTESIAN_POINT('',(2.68972991167073,0.432153924581312,13.8057746032556));
#416185=CARTESIAN_POINT('Origin',(0.,2.5406128344257E-15,13.8057746032556));
#416186=CARTESIAN_POINT('',(2.65474553983445,0.439725890395448,13.8390832900376));
#416187=CARTESIAN_POINT('',(2.68972991167073,0.432153924581312,13.8057746032556));
#416188=CARTESIAN_POINT('',(2.6356337482334,0.54264858345725,13.8390832900376));
#416189=CARTESIAN_POINT('Ctrl Pts',(2.65474553983445,0.439725890395448,
13.8390832900376));
#416190=CARTESIAN_POINT('Ctrl Pts',(2.64793212065841,0.441200737083988,
13.8455641171218));
#416191=CARTESIAN_POINT('Ctrl Pts',(2.64104317441114,0.444025544680594,
13.851896480191));
#416192=CARTESIAN_POINT('Ctrl Pts',(2.63466247548437,0.448427568379484,
13.8574481026913));
#416193=CARTESIAN_POINT('Ctrl Pts',(2.63034964968591,0.451402973047822,
13.8612005412592));
#416194=CARTESIAN_POINT('Ctrl Pts',(2.6261779082041,0.45518369368953,13.8646714234115));
#416195=CARTESIAN_POINT('Ctrl Pts',(2.6225442594355,0.459741303920579,13.8674635290331));
#416196=CARTESIAN_POINT('Ctrl Pts',(2.61961581989004,0.463414384860244,
13.8697137499649));
#416197=CARTESIAN_POINT('Ctrl Pts',(2.61697922463863,0.467686742263982,
13.8715630732995));
#416198=CARTESIAN_POINT('Ctrl Pts',(2.61494267642004,0.472323814005002,
13.8727429581918));
#416199=CARTESIAN_POINT('Ctrl Pts',(2.61288265564838,0.477014331037186,
13.873936442031));
#416200=CARTESIAN_POINT('Ctrl Pts',(2.61138865124768,0.482225710441918,
13.8744652622107));
#416201=CARTESIAN_POINT('Ctrl Pts',(2.61066524973233,0.487433071044176,
13.8742206332401));
#416202=CARTESIAN_POINT('Ctrl Pts',(2.61004257214782,0.491915376724641,
13.8740100655633));
#416203=CARTESIAN_POINT('Ctrl Pts',(2.60997078586386,0.496513388046464,
13.8732246156103));
#416204=CARTESIAN_POINT('Ctrl Pts',(2.6104004559287,0.500868135971515,13.8719820486038));
#416205=CARTESIAN_POINT('Ctrl Pts',(2.61083753020681,0.505297926318795,
13.8707180692815));
#416206=CARTESIAN_POINT('Ctrl Pts',(2.6117949642739,0.509577495024053,13.868960862563));
#416207=CARTESIAN_POINT('Ctrl Pts',(2.61311982789352,0.513493622756147,
13.8669057591701));
#416208=CARTESIAN_POINT('Ctrl Pts',(2.61515981309133,0.519523558583403,
13.8637413727084));
#416209=CARTESIAN_POINT('Ctrl Pts',(2.6181092082965,0.524887078072245,13.8597962563956));
#416210=CARTESIAN_POINT('Ctrl Pts',(2.62152744202795,0.529427035820237,
13.855546950204));
#416211=CARTESIAN_POINT('Ctrl Pts',(2.62560407746791,0.534841455694789,
13.850479165618));
#416212=CARTESIAN_POINT('Ctrl Pts',(2.63044880579731,0.53924881289445,13.8448473071436));
#416213=CARTESIAN_POINT('Ctrl Pts',(2.63563374823339,0.542648583457249,
13.8390832900376));
#416214=CARTESIAN_POINT('',(2.66556758396332,0.562275259629327,13.8057746032556));
#416215=CARTESIAN_POINT('',(2.6356337482334,0.54264858345725,13.8390832900376));
#416216=CARTESIAN_POINT('',(2.64555550050207,0.649953926082844,13.8057746032556));
#416217=CARTESIAN_POINT('Origin',(0.,2.5406128344257E-15,13.8057746032556));
#416218=CARTESIAN_POINT('',(2.61007035076852,0.654649145721658,13.8390832900376));
#416219=CARTESIAN_POINT('',(2.64555550050207,0.649953926082844,13.8057746032556));
#416220=CARTESIAN_POINT('',(2.5826329971052,0.755671583572118,13.8390832900376));
#416221=CARTESIAN_POINT('Ctrl Pts',(2.61007035076851,0.654649145721657,
13.8390832900376));
#416222=CARTESIAN_POINT('Ctrl Pts',(2.60315938898579,0.655563728063963,
13.8455641171218));
#416223=CARTESIAN_POINT('Ctrl Pts',(2.5960631170955,0.657817623273311,13.851896480191));
#416224=CARTESIAN_POINT('Ctrl Pts',(2.58934484362018,0.661684913403435,
13.8574481026913));
#416225=CARTESIAN_POINT('Ctrl Pts',(2.58480384529101,0.664298882317296,
13.8612005412592));
#416226=CARTESIAN_POINT('Ctrl Pts',(2.58033782110404,0.667726987263631,
13.8646714234115));
#416227=CARTESIAN_POINT('Ctrl Pts',(2.57634477545734,0.671973256314823,
13.8674635290331));
#416228=CARTESIAN_POINT('Ctrl Pts',(2.57312668985709,0.675395420371407,
13.8697137499649));
#416229=CARTESIAN_POINT('Ctrl Pts',(2.57015063086784,0.679438654868381,
13.8715630732995));
#416230=CARTESIAN_POINT('Ctrl Pts',(2.56774289470007,0.683894299549507,
13.8727429581918));
#416231=CARTESIAN_POINT('Ctrl Pts',(2.56530740779484,0.688401298456017,
13.873936442031));
#416232=CARTESIAN_POINT('Ctrl Pts',(2.56339359876896,0.693473562197373,
13.8744652622107));
#416233=CARTESIAN_POINT('Ctrl Pts',(2.56224815608062,0.698604631797571,
13.8742206332401));
#416234=CARTESIAN_POINT('Ctrl Pts',(2.56126220087975,0.703021268971854,
13.8740100655633));
#416235=CARTESIAN_POINT('Ctrl Pts',(2.56081587285014,0.70759812954174,13.8732246156103));
#416236=CARTESIAN_POINT('Ctrl Pts',(2.56088916083988,0.711973409501458,
13.8719820486038));
#416237=CARTESIAN_POINT('Ctrl Pts',(2.56096371175193,0.716424085698055,
13.8707180692815));
#416238=CARTESIAN_POINT('Ctrl Pts',(2.56156913545708,0.720767454256337,
13.868960862563));
#416239=CARTESIAN_POINT('Ctrl Pts',(2.56257038993658,0.724778540080894,
13.8669057591701));
#416240=CARTESIAN_POINT('Ctrl Pts',(2.56411209150282,0.73095468952604,13.8637413727084));
#416241=CARTESIAN_POINT('Ctrl Pts',(2.56661449620793,0.736540765436313,
13.8597962563956));
#416242=CARTESIAN_POINT('Ctrl Pts',(2.56965130734524,0.741344234631866,
13.855546950204));
#416243=CARTESIAN_POINT('Ctrl Pts',(2.57327305263227,0.747072922104936,
13.850479165618));
#416244=CARTESIAN_POINT('Ctrl Pts',(2.57774242000014,0.751860504522207,
13.8448473071436));
#416245=CARTESIAN_POINT('Ctrl Pts',(2.5826329971052,0.755671583572117,13.8390832900376));
#416246=CARTESIAN_POINT('',(2.6108674741529,0.777672839102481,13.8057746032556));
#416247=CARTESIAN_POINT('',(2.5826329971052,0.755671583572118,13.8390832900376));
#416248=CARTESIAN_POINT('',(2.5837753539635,0.863428591441144,13.8057746032556));
#416249=CARTESIAN_POINT('Origin',(0.,2.5406128344257E-15,13.8057746032556));
#416250=CARTESIAN_POINT('',(2.54802557414951,0.865215818992596,13.8390832900376));
#416251=CARTESIAN_POINT('',(2.5837753539635,0.863428591441144,13.8057746032556));
#416252=CARTESIAN_POINT('',(2.51244524948572,0.963665713975349,13.8390832900376));
#416253=CARTESIAN_POINT('Ctrl Pts',(2.54802557414951,0.865215818992595,
13.8390832900376));
#416254=CARTESIAN_POINT('Ctrl Pts',(2.54106306107054,0.865564050594074,
13.8455641171218));
#416255=CARTESIAN_POINT('Ctrl Pts',(2.53380668805586,0.867232034115413,
13.851896480191));
#416256=CARTESIAN_POINT('Ctrl Pts',(2.52679554903354,0.870538854499011,
13.8574481026913));
#416257=CARTESIAN_POINT('Ctrl Pts',(2.52205659776832,0.872773992126551,
13.8612005412592));
#416258=CARTESIAN_POINT('Ctrl Pts',(2.5173260115303,0.87582666790469,13.8646714234115));
#416259=CARTESIAN_POINT('Ctrl Pts',(2.51300014206548,0.879733337556075,
13.8674635290331));
#416260=CARTESIAN_POINT('Ctrl Pts',(2.50951382623916,0.882881810792399,
13.8697137499649));
#416261=CARTESIAN_POINT('Ctrl Pts',(2.50621810869362,0.88666901532412,13.8715630732995));
#416262=CARTESIAN_POINT('Ctrl Pts',(2.50345520766364,0.890913581365129,
13.8727429581918));
#416263=CARTESIAN_POINT('Ctrl Pts',(2.50066046238834,0.895207068811845,
13.873936442031));
#416264=CARTESIAN_POINT('Ctrl Pts',(2.49833958482061,0.900106461811489,
13.8744652622107));
#416265=CARTESIAN_POINT('Ctrl Pts',(2.49677972369137,0.905127093988005,
13.8742206332401));
#416266=CARTESIAN_POINT('Ctrl Pts',(2.49543705224334,0.909448670664406,
13.8740100655633));
#416267=CARTESIAN_POINT('Ctrl Pts',(2.49461915270749,0.91397392223039,13.8732246156103));
#416268=CARTESIAN_POINT('Ctrl Pts',(2.49433557090265,0.918340617458513,
13.8719820486038));
#416269=CARTESIAN_POINT('Ctrl Pts',(2.4940471023246,0.92278256098865,13.8707180692815));
#416270=CARTESIAN_POINT('Ctrl Pts',(2.49429648667295,0.927160824998806,
13.868960862563));
#416271=CARTESIAN_POINT('Ctrl Pts',(2.49496746882896,0.931240175801445,
13.8669057591701));
#416272=CARTESIAN_POINT('Ctrl Pts',(2.49600062699407,0.937521437608915,
13.8637413727084));
#416273=CARTESIAN_POINT('Ctrl Pts',(2.49803938810867,0.943292895527074,
13.8597962563956));
#416274=CARTESIAN_POINT('Ctrl Pts',(2.50067456717477,0.948327909875208,
13.855546950204));
#416275=CARTESIAN_POINT('Ctrl Pts',(2.50381732019154,0.954332741476831,
13.850479165618));
#416276=CARTESIAN_POINT('Ctrl Pts',(2.50788158369544,0.959468688540621,
13.8448473071436));
#416277=CARTESIAN_POINT('Ctrl Pts',(2.51244524948572,0.96366571397535,13.8390832900376));
#416278=CARTESIAN_POINT('',(2.53879247206481,0.987895134138395,13.8057746032556));
#416279=CARTESIAN_POINT('',(2.51244524948572,0.963665713975349,13.8390832900376));
#416280=CARTESIAN_POINT('',(2.50480060873724,1.07115728197909,13.8057746032556));
#416281=CARTESIAN_POINT('Origin',(0.,2.5406128344257E-15,13.8057746032556));
#416282=CARTESIAN_POINT('',(2.46902410772917,1.0700246237387,13.8390832900376));
#416283=CARTESIAN_POINT('',(2.50480060873724,1.07115728197909,13.8057746032556));
#416284=CARTESIAN_POINT('',(2.4255375932552,1.16524680804573,13.8390832900376));
#416285=CARTESIAN_POINT('Ctrl Pts',(2.46902410772917,1.0700246237387,13.8390832900376));
#416286=CARTESIAN_POINT('Ctrl Pts',(2.46205637772976,1.0698041871755,13.8455641171218));
#416287=CARTESIAN_POINT('Ctrl Pts',(2.45468819355588,1.07087515885369,13.851896480191));
#416288=CARTESIAN_POINT('Ctrl Pts',(2.44743084695999,1.0735995031467,13.8574481026913));
#416289=CARTESIAN_POINT('Ctrl Pts',(2.44252547969752,1.07544093501578,13.8612005412592));
#416290=CARTESIAN_POINT('Ctrl Pts',(2.43756181267939,1.07809786657207,13.8646714234115));
#416291=CARTESIAN_POINT('Ctrl Pts',(2.43293190734402,1.08163893858167,13.8674635290331));
#416292=CARTESIAN_POINT('Ctrl Pts',(2.42920056214825,1.08449276842781,13.8697137499649));
#416293=CARTESIAN_POINT('Ctrl Pts',(2.42560711850294,1.08799873977297,13.8715630732995));
#416294=CARTESIAN_POINT('Ctrl Pts',(2.42250743926123,1.09200398028716,13.8727429581918));
#416295=CARTESIAN_POINT('Ctrl Pts',(2.4193720341846,1.0960553838235,13.873936442031));
#416296=CARTESIAN_POINT('Ctrl Pts',(2.41665953313229,1.10074930142936,13.8744652622107));
#416297=CARTESIAN_POINT('Ctrl Pts',(2.41469563418062,1.10562608470341,13.8742206332401));
#416298=CARTESIAN_POINT('Ctrl Pts',(2.41300518174238,1.10982384150215,13.8740100655633));
#416299=CARTESIAN_POINT('Ctrl Pts',(2.41182115368675,1.11426736926168,13.8732246156103));
#416300=CARTESIAN_POINT('Ctrl Pts',(2.41118258927746,1.11859642012192,13.8719820486038));
#416301=CARTESIAN_POINT('Ctrl Pts',(2.41053302092011,1.12300007058427,13.8707180692815));
#416302=CARTESIAN_POINT('Ctrl Pts',(2.41042470629996,1.12738409342168,13.868960862563));
#416303=CARTESIAN_POINT('Ctrl Pts',(2.41076095085695,1.13150456179585,13.8669057591701));
#416304=CARTESIAN_POINT('Ctrl Pts',(2.41127869012379,1.13784913520465,13.8637413727084));
#416305=CARTESIAN_POINT('Ctrl Pts',(2.41284024002903,1.14376756703048,13.8597962563956));
#416306=CARTESIAN_POINT('Ctrl Pts',(2.41505625034202,1.14900061934142,13.855546950204));
#416307=CARTESIAN_POINT('Ctrl Pts',(2.41769909658571,1.15524163390802,13.850479165618));
#416308=CARTESIAN_POINT('Ctrl Pts',(2.42133120922257,1.16069176673799,13.8448473071436));
#416309=CARTESIAN_POINT('Ctrl Pts',(2.4255375932552,1.16524680804572,13.8390832900376));
#416310=CARTESIAN_POINT('',(2.4498222249464,1.19154315004784,13.8057746032556));
#416311=CARTESIAN_POINT('',(2.4255375932552,1.16524680804573,13.8390832900376));
#416312=CARTESIAN_POINT('',(2.40915682872283,1.27175759753398,13.8057746032556));
#416313=CARTESIAN_POINT('Origin',(0.,2.5406128344257E-15,13.8057746032556));
#416314=CARTESIAN_POINT('',(2.3735916932322,1.26771259115546,13.8390832900376));
#416315=CARTESIAN_POINT('',(2.40915682872283,1.27175759753398,13.8057746032556));
#416316=CARTESIAN_POINT('',(2.3224883845271,1.35907337686075,13.8390832900376));
#416317=CARTESIAN_POINT('Ctrl Pts',(2.3735916932322,1.26771259115546,13.8390832900376));
#416318=CARTESIAN_POINT('Ctrl Pts',(2.36666511540589,1.26692495339653,13.8455641171218));
#416319=CARTESIAN_POINT('Ctrl Pts',(2.35923415412283,1.26739178609176,13.851896480191));
#416320=CARTESIAN_POINT('Ctrl Pts',(2.3517788963976,1.26951552423239,13.8574481026913));
#416321=CARTESIAN_POINT('Ctrl Pts',(2.34673975754768,1.27095099591773,13.8612005412592));
#416322=CARTESIAN_POINT('Ctrl Pts',(2.34157604213449,1.27319450181105,13.8646714234115));
#416323=CARTESIAN_POINT('Ctrl Pts',(2.33667291218469,1.27634641092888,13.8674635290331));
#416324=CARTESIAN_POINT('Ctrl Pts',(2.33272136910612,1.27888660561805,13.8697137499649));
#416325=CARTESIAN_POINT('Ctrl Pts',(2.32885411313562,1.28208801211578,13.8715630732995));
#416326=CARTESIAN_POINT('Ctrl Pts',(2.32543828353614,1.28582727288836,13.8727429581918));
#416327=CARTESIAN_POINT('Ctrl Pts',(2.32198308426163,1.28960963109222,13.873936442031));
#416328=CARTESIAN_POINT('Ctrl Pts',(2.31889701097173,1.29406683605708,13.8744652622107));
#416329=CARTESIAN_POINT('Ctrl Pts',(2.31654214362114,1.29876731624057,13.8742206332401));
#416330=CARTESIAN_POINT('Ctrl Pts',(2.31451515987476,1.30281331778275,13.8740100655633));
#416331=CARTESIAN_POINT('Ctrl Pts',(2.31297288281071,1.30714555079171,13.8732246156103));
#416332=CARTESIAN_POINT('Ctrl Pts',(2.31198358533776,1.31140814816483,13.8719820486038));
#416333=CARTESIAN_POINT('Ctrl Pts',(2.31097723997135,1.31574419999212,13.8707180692815));
#416334=CARTESIAN_POINT('Ctrl Pts',(2.31051194719864,1.32010480670811,13.868960862563));
#416335=CARTESIAN_POINT('Ctrl Pts',(2.31051121650454,1.32423897161662,13.8669057591701));
#416336=CARTESIAN_POINT('Ctrl Pts',(2.31051009140371,1.3306046345375,13.8637413727084));
#416337=CARTESIAN_POINT('Ctrl Pts',(2.31158403824262,1.33663065408365,13.8597962563956));
#416338=CARTESIAN_POINT('Ctrl Pts',(2.31336613261947,1.34202691925768,13.855546950204));
#416339=CARTESIAN_POINT('Ctrl Pts',(2.31549148438438,1.348462583867,13.850479165618));
#416340=CARTESIAN_POINT('Ctrl Pts',(2.31866727504386,1.35419063272837,13.8448473071436));
#416341=CARTESIAN_POINT('Ctrl Pts',(2.3224883845271,1.35907337686075,13.8390832900376));
#416342=CARTESIAN_POINT('',(2.34454881511319,1.3872616428845,13.8057746032556));
#416343=CARTESIAN_POINT('',(2.3224883845271,1.35907337686075,13.8390832900376));
#416344=CARTESIAN_POINT('',(2.29748050749618,1.46389457610252,13.8057746032556));
#416345=CARTESIAN_POINT('Origin',(0.,2.5406128344257E-15,13.8057746032556));
#416346=CARTESIAN_POINT('',(2.26236341763183,1.45696414043593,13.8390832900376));
#416347=CARTESIAN_POINT('',(2.29748050749618,1.46389457610252,13.8057746032556));
#416348=CARTESIAN_POINT('',(2.20398339878359,1.54385553658409,13.8390832900376));
#416349=CARTESIAN_POINT('Ctrl Pts',(2.26236341763183,1.45696414043593,13.8390832900376));
#416350=CARTESIAN_POINT('Ctrl Pts',(2.25552408721126,1.45561454308062,13.8455641171218));
#416351=CARTESIAN_POINT('Ctrl Pts',(2.24807980064034,1.45547413009832,13.851896480191));
#416352=CARTESIAN_POINT('Ctrl Pts',(2.24047624529588,1.45698312895964,13.8574481026913));
#416353=CARTESIAN_POINT('Ctrl Pts',(2.23533686949616,1.45800308763402,13.8612005412592));
#416354=CARTESIAN_POINT('Ctrl Pts',(2.23000746936204,1.45981823770277,13.8646714234115));
#416355=CARTESIAN_POINT('Ctrl Pts',(2.22486374431866,1.46256000849368,13.8674635290331));
#416356=CARTESIAN_POINT('Ctrl Pts',(2.22071830022452,1.46476966344934,13.8697137499649));
#416357=CARTESIAN_POINT('Ctrl Pts',(2.21660296787927,1.4676452002676,13.8715630732995));
#416358=CARTESIAN_POINT('Ctrl Pts',(2.21289371970442,1.47109359713505,13.8727429581918));
#416359=CARTESIAN_POINT('Ctrl Pts',(2.20914172001316,1.47458173903663,13.873936442031));
#416360=CARTESIAN_POINT('Ctrl Pts',(2.20570261179423,1.47877256939683,13.8744652622107));
#416361=CARTESIAN_POINT('Ctrl Pts',(2.2029724472984,1.48326546556968,13.8742206332401));
#416362=CARTESIAN_POINT('Ctrl Pts',(2.20062242148629,1.48713278638257,13.8740100655633));
#416363=CARTESIAN_POINT('Ctrl Pts',(2.19873215901322,1.49132489434505,13.8732246156103));
#416364=CARTESIAN_POINT('Ctrl Pts',(2.19739871208807,1.49549267134882,13.8719820486038));
#416365=CARTESIAN_POINT('Ctrl Pts',(2.19604228677498,1.49973226883154,13.8707180692815));
#416366=CARTESIAN_POINT('Ctrl Pts',(2.19522311229634,1.50404044030786,13.868960862563));
#416367=CARTESIAN_POINT('Ctrl Pts',(2.1948854112138,1.50816078956533,13.8669057591701));
#416368=CARTESIAN_POINT('Ctrl Pts',(2.19436542923268,1.51450517956181,13.8637413727084));
#416369=CARTESIAN_POINT('Ctrl Pts',(2.19494462606623,1.52059868466244,13.8597962563956));
#416370=CARTESIAN_POINT('Ctrl Pts',(2.19628094496288,1.52612225144513,13.855546950204));
#416371=CARTESIAN_POINT('Ctrl Pts',(2.19787465838367,1.53270973781101,13.850479165618));
#416372=CARTESIAN_POINT('Ctrl Pts',(2.2005729927029,1.53867758348368,13.8448473071436));
#416373=CARTESIAN_POINT('Ctrl Pts',(2.20398339878358,1.54385553658408,13.8390832900376));
#416374=CARTESIAN_POINT('',(2.22367281973873,1.57374813836983,13.8057746032556));
#416375=CARTESIAN_POINT('',(2.20398339878359,1.54385553658409,13.8390832900376));
#416376=CARTESIAN_POINT('',(2.17051483254974,1.6462895777927,13.8057746032556));
#416377=CARTESIAN_POINT('Origin',(0.,2.5406128344257E-15,13.8057746032556));
#416378=CARTESIAN_POINT('',(2.13607948675081,1.63651983374397,13.8390832900376));
#416379=CARTESIAN_POINT('',(2.17051483254974,1.6462895777927,13.8057746032556));
#416380=CARTESIAN_POINT('',(2.07081126715283,1.71836359242969,13.8390832900376));
#416381=CARTESIAN_POINT('Ctrl Pts',(2.13607948675081,1.63651983374397,13.8390832900376));
#416382=CARTESIAN_POINT('Ctrl Pts',(2.12937291835152,1.63461725814,13.8455641171218));
#416383=CARTESIAN_POINT('Ctrl Pts',(2.12196484699164,1.6338705339054,13.851896480191));
#416384=CARTESIAN_POINT('Ctrl Pts',(2.11426359443428,1.63475475134896,13.8574481026913));
#416385=CARTESIAN_POINT('Ctrl Pts',(2.10905818338277,1.63535240935567,13.8612005412592));
#416386=CARTESIAN_POINT('Ctrl Pts',(2.10359856480631,1.63672712407565,13.8646714234115));
#416387=CARTESIAN_POINT('Ctrl Pts',(2.09824847531087,1.63904051050738,13.8674635290331));
#416388=CARTESIAN_POINT('Ctrl Pts',(2.09393671744766,1.64090492084036,13.8697137499649));
#416389=CARTESIAN_POINT('Ctrl Pts',(2.08960069558542,1.64343545175605,13.8715630732995));
#416390=CARTESIAN_POINT('Ctrl Pts',(2.08562271326984,1.64657003620617,13.8727429581918));
#416391=CARTESIAN_POINT('Ctrl Pts',(2.08159888210072,1.64974074879662,13.873936442031));
#416392=CARTESIAN_POINT('Ctrl Pts',(2.07782962565056,1.65363731526754,13.8744652622107));
#416393=CARTESIAN_POINT('Ctrl Pts',(2.07474233280376,1.657892727947,13.8742206332401));
#416394=CARTESIAN_POINT('Ctrl Pts',(2.07208490395997,1.66155563164865,13.8740100655633));
#416395=CARTESIAN_POINT('Ctrl Pts',(2.06985923546278,1.66557971677782,13.8732246156103));
#416396=CARTESIAN_POINT('Ctrl Pts',(2.06819051295471,1.66962493754391,13.8719820486038));
#416397=CARTESIAN_POINT('Ctrl Pts',(2.06649303448161,1.67373986686029,13.8707180692815));
#416398=CARTESIAN_POINT('Ctrl Pts',(2.06532542976803,1.67796693292656,13.868960862563));
#416399=CARTESIAN_POINT('Ctrl Pts',(2.06465300564205,1.68204604628849,13.8669057591701));
#416400=CARTESIAN_POINT('Ctrl Pts',(2.06361762717491,1.6883269424919,13.8637413727084));
#416401=CARTESIAN_POINT('Ctrl Pts',(2.06369821954374,1.69444738187593,13.8597962563956));
#416402=CARTESIAN_POINT('Ctrl Pts',(2.06457986997842,1.70006149184166,13.855546950204));
#416403=CARTESIAN_POINT('Ctrl Pts',(2.06563133915521,1.7067569613292,13.850479165618));
#416404=CARTESIAN_POINT('Ctrl Pts',(2.0678342601645,1.71292488878483,13.8448473071436));
#416405=CARTESIAN_POINT('Ctrl Pts',(2.07081126715283,1.71836359242969,13.8390832900376));
#416406=CARTESIAN_POINT('',(2.08799864862909,1.74976159964447,13.8057746032556));
#416407=CARTESIAN_POINT('',(2.07081126715283,1.71836359242969,13.8390832900376));
#416408=CARTESIAN_POINT('',(2.02910473950242,1.81772879396133,13.8057746032556));
#416409=CARTESIAN_POINT('Origin',(0.,2.5406128344257E-15,13.8057746032556));
#416410=CARTESIAN_POINT('',(1.99558029931377,1.80518475756521,13.8390832900376));
#416411=CARTESIAN_POINT('',(2.02910473950242,1.81772879396133,13.8057746032556));
#416412=CARTESIAN_POINT('',(1.92385822819898,1.88143622207771,13.8390832900376));
#416413=CARTESIAN_POINT('Ctrl Pts',(1.99558029931377,1.80518475756521,13.8390832900376));
#416414=CARTESIAN_POINT('Ctrl Pts',(1.98905112404195,1.80274186503932,13.8455641171218));
#416415=CARTESIAN_POINT('Ctrl Pts',(1.98172856738576,1.801393798879,13.851896480191));
#416416=CARTESIAN_POINT('Ctrl Pts',(1.97398086818066,1.80164735058359,13.8574481026913));
#416417=CARTESIAN_POINT('Ctrl Pts',(1.96874406302907,1.80181873060722,13.8612005412592));
#416418=CARTESIAN_POINT('Ctrl Pts',(1.96319055887113,1.80274386147876,13.8646714234115));
#416419=CARTESIAN_POINT('Ctrl Pts',(1.95766970888652,1.8046134683463,13.8674635290331));
#416420=CARTESIAN_POINT('Ctrl Pts',(1.95322033129143,1.80612022671344,13.8697137499649));
#416421=CARTESIAN_POINT('Ctrl Pts',(1.94869247542231,1.80828891146083,13.8715630732995));
#416422=CARTESIAN_POINT('Ctrl Pts',(1.94447223178197,1.81108882335126,13.8727429581918));
#416423=CARTESIAN_POINT('Ctrl Pts',(1.94020334706754,1.81392100606143,13.873936442031));
#416424=CARTESIAN_POINT('Ctrl Pts',(1.93612902616594,1.81749737763611,13.8744652622107));
#416425=CARTESIAN_POINT('Ctrl Pts',(1.93270515039271,1.82148698775288,13.8742206332401));
#416426=CARTESIAN_POINT('Ctrl Pts',(1.92975800326775,1.8249210983235,13.8740100655633));
#416427=CARTESIAN_POINT('Ctrl Pts',(1.92721174020306,1.82875038099674,13.8732246156103));
#416428=CARTESIAN_POINT('Ctrl Pts',(1.92521884718504,1.83264612524836,13.8719820486038));
#416429=CARTESIAN_POINT('Ctrl Pts',(1.92319161199111,1.83660900222272,13.8707180692815));
#416430=CARTESIAN_POINT('Ctrl Pts',(1.92168334725933,1.8407268324517,13.868960862563));
#416431=CARTESIAN_POINT('Ctrl Pts',(1.92068067496151,1.84473756409168,13.8669057591701));
#416432=CARTESIAN_POINT('Ctrl Pts',(1.91913679028124,1.85091316817404,13.8637413727084));
#416433=CARTESIAN_POINT('Ctrl Pts',(1.91871824185642,1.85701981132716,13.8597962563956));
#416434=CARTESIAN_POINT('Ctrl Pts',(1.91913935659095,1.86268710350039,13.855546950204));
#416435=CARTESIAN_POINT('Ctrl Pts',(1.91964158416986,1.86944599886481,13.850479165618));
#416436=CARTESIAN_POINT('Ctrl Pts',(1.92133443179333,1.87577296156384,13.8448473071436));
#416437=CARTESIAN_POINT('Ctrl Pts',(1.92385822819898,1.88143622207771,13.8390832900376));
#416438=CARTESIAN_POINT('',(1.93842919100836,1.91413068616381,13.8057746032556));
#416439=CARTESIAN_POINT('',(1.92385822819898,1.88143622207771,13.8390832900376));
#416440=CARTESIAN_POINT('',(1.87419128919243,1.97707132491028,13.8057746032556));
#416441=CARTESIAN_POINT('Origin',(0.,2.5406128344257E-15,13.8057746032556));
#416442=CARTESIAN_POINT('',(1.84180085423237,1.96183647465937,13.8390832900376));
#416443=CARTESIAN_POINT('',(1.87419128919243,1.97707132491028,13.8057746032556));
#416444=CARTESIAN_POINT('',(1.76410223015073,2.03198820408293,13.8390832900376));
#416445=CARTESIAN_POINT('Ctrl Pts',(1.84180085423237,1.96183647465937,13.8390832900376));
#416446=CARTESIAN_POINT('Ctrl Pts',(1.83549252267221,1.95886952225828,13.8455641171218));
#416447=CARTESIAN_POINT('Ctrl Pts',(1.82830421112613,1.95692908533012,13.851896480191));
#416448=CARTESIAN_POINT('Ctrl Pts',(1.82056162493321,1.95655028395099,13.8574481026913));
#416449=CARTESIAN_POINT('Ctrl Pts',(1.81532827575582,1.95629424548574,13.8612005412592));
#416450=CARTESIAN_POINT('Ctrl Pts',(1.80971784367031,1.95676363591553,13.8646714234115));
#416451=CARTESIAN_POINT('Ctrl Pts',(1.8040629735423,1.95817702129363,13.8674635290331));
#416452=CARTESIAN_POINT('Ctrl Pts',(1.79950558608912,1.9593161004666,13.8697137499649));
#416453=CARTESIAN_POINT('Ctrl Pts',(1.79481602834688,1.9611085068065,13.8715630732995));
#416454=CARTESIAN_POINT('Ctrl Pts',(1.79038160840693,1.96355511318558,13.8727429581918));
#416455=CARTESIAN_POINT('Ctrl Pts',(1.78589607887065,1.9660299183068,13.873936442031));
#416456=CARTESIAN_POINT('Ctrl Pts',(1.78154380745099,1.96926229482246,13.8744652622107));
#416457=CARTESIAN_POINT('Ctrl Pts',(1.77780613407969,1.97295955217946,13.8742206332401));
#416458=CARTESIAN_POINT('Ctrl Pts',(1.77458888145144,1.97614201617978,13.8740100655633));
#416459=CARTESIAN_POINT('Ctrl Pts',(1.77173896877985,1.9797510131527,13.8732246156103));
#416460=CARTESIAN_POINT('Ctrl Pts',(1.76943516762612,1.98347135535462,13.8719820486038));
#416461=CARTESIAN_POINT('Ctrl Pts',(1.76709166662709,1.98725580769452,13.8707180692815));
#416462=CARTESIAN_POINT('Ctrl Pts',(1.76525277913004,1.99123699860542,13.868960862563));
#416463=CARTESIAN_POINT('Ctrl Pts',(1.76392653127912,1.9951526577661,13.8669057591701));
#416464=CARTESIAN_POINT('Ctrl Pts',(1.76188441468353,2.00118187210117,13.8637413727084));
#416465=CARTESIAN_POINT('Ctrl Pts',(1.76096951083578,2.00723408032072,13.8597962563956));
#416466=CARTESIAN_POINT('Ctrl Pts',(1.76092728742108,2.01291683980706,13.855546950204));
#416467=CARTESIAN_POINT('Ctrl Pts',(1.76087693116042,2.01969418171487,13.850479165618));
#416468=CARTESIAN_POINT('Ctrl Pts',(1.76204843977646,2.02613807476439,13.8448473071436));
#416469=CARTESIAN_POINT('Ctrl Pts',(1.76410223015073,2.03198820408293,13.8390832900376));
#416470=CARTESIAN_POINT('',(1.77595980693977,2.06576154877607,13.8057746032556));
#416471=CARTESIAN_POINT('',(1.76410223015073,2.03198820408293,13.8390832900376));
#416472=CARTESIAN_POINT('',(1.70680540507266,2.12325677238577,13.8057746032556));
#416473=CARTESIAN_POINT('Origin',(0.,2.5406128344257E-15,13.8057746032556));
#416474=CARTESIAN_POINT('',(1.6757645283418,2.10543249369491,13.8390832900376));
#416475=CARTESIAN_POINT('',(1.70680540507266,2.12325677238577,13.8057746032556));
#416476=CARTESIAN_POINT('',(1.59260642281721,2.16901763984444,13.8390832900376));
#416477=CARTESIAN_POINT('Ctrl Pts',(1.6757645283418,2.10543249369491,13.8390832900376));
#416478=CARTESIAN_POINT('Ctrl Pts',(1.66971902139905,2.10196122599733,13.8455641171218));
#416479=CARTESIAN_POINT('Ctrl Pts',(1.66271279199042,2.09944133158894,13.851896480191));
#416480=CARTESIAN_POINT('Ctrl Pts',(1.65502684444336,2.09843269798676,13.8574481026913));
#416481=CARTESIAN_POINT('Ctrl Pts',(1.6498317783155,2.09775094492638,13.8612005412592));
#416482=CARTESIAN_POINT('Ctrl Pts',(1.64420175480229,2.09776147119857,13.8646714234115));
#416483=CARTESIAN_POINT('Ctrl Pts',(1.63845049675859,2.09870922924073,13.8674635290331));
#416484=CARTESIAN_POINT('Ctrl Pts',(1.63381542810891,2.09947304883556,13.8697137499649));
#416485=CARTESIAN_POINT('Ctrl Pts',(1.62899537672661,2.10087724859951,13.8715630732995));
#416486=CARTESIAN_POINT('Ctrl Pts',(1.62437629082011,2.10295426770544,13.8727429581918));
#416487=CARTESIAN_POINT('Ctrl Pts',(1.61970396692098,2.10505522581794,13.873936442031));
#416488=CARTESIAN_POINT('Ctrl Pts',(1.61510270863149,2.10792209634218,13.8744652622107));
#416489=CARTESIAN_POINT('Ctrl Pts',(1.61107611126174,2.1113023963017,13.8742206332401));
#416490=CARTESIAN_POINT('Ctrl Pts',(1.60761016341562,2.11421203495888,13.8740100655633));
#416491=CARTESIAN_POINT('Ctrl Pts',(1.60447556683576,2.11757672895205,13.8732246156103));
#416492=CARTESIAN_POINT('Ctrl Pts',(1.60187618896289,2.12109691084073,13.8719820486038));
#416493=CARTESIAN_POINT('Ctrl Pts',(1.59923201777126,2.12467775364024,13.8707180692815));
#416494=CARTESIAN_POINT('Ctrl Pts',(1.59707474500186,2.12849581106441,13.868960862563));
#416495=CARTESIAN_POINT('Ctrl Pts',(1.59543374755844,2.13229033968011,13.8669057591701));
#416496=CARTESIAN_POINT('Ctrl Pts',(1.59290698899657,2.13813304084123,13.8637413727084));
#416497=CARTESIAN_POINT('Ctrl Pts',(1.59150181826004,2.14409053768006,13.8597962563956));
#416498=CARTESIAN_POINT('Ctrl Pts',(1.59099653768597,2.14975094665272,13.855546950204));
#416499=CARTESIAN_POINT('Ctrl Pts',(1.59039393269836,2.15650163301169,13.850479165618));
#416500=CARTESIAN_POINT('Ctrl Pts',(1.59103630611039,2.16301957336664,13.8448473071436));
#416501=CARTESIAN_POINT('Ctrl Pts',(1.59260642281721,2.16901763984444,13.8390832900376));
#416502=CARTESIAN_POINT('',(1.60167170336874,2.2036451091079,13.8057746032556));
#416503=CARTESIAN_POINT('',(1.59260642281721,2.16901763984444,13.8390832900376));
#416504=CARTESIAN_POINT('',(1.5280610125852,2.25531229635374,13.8057746032556));
#416505=CARTESIAN_POINT('Origin',(0.,2.5406128344257E-15,13.8057746032556));
#416506=CARTESIAN_POINT('',(1.49857626599681,2.23501720685682,13.8390832900376));
#416507=CARTESIAN_POINT('',(1.5280610125852,2.25531229635374,13.8057746032556));
#416508=CARTESIAN_POINT('',(1.41051208250141,2.2916126210755,13.8390832900376));
#416509=CARTESIAN_POINT('Ctrl Pts',(1.49857626599681,2.23501720685682,13.8390832900376));
#416510=CARTESIAN_POINT('Ctrl Pts',(1.49283381552271,2.23106472457656,13.8455641171218));
#416511=CARTESIAN_POINT('Ctrl Pts',(1.48605629355232,2.22798214216948,13.851896480191));
#416512=CARTESIAN_POINT('Ctrl Pts',(1.47847813336395,2.22635038863446,13.8574481026913));
#416513=CARTESIAN_POINT('Ctrl Pts',(1.47335592259357,2.22524745793309,13.8612005412592));
#416514=CARTESIAN_POINT('Ctrl Pts',(1.46774377453025,2.22479904999705,13.8646714234115));
#416515=CARTESIAN_POINT('Ctrl Pts',(1.46193440224425,2.22527487352988,13.8674635290331));
#416516=CARTESIAN_POINT('Ctrl Pts',(1.4572524980152,2.2256583504532,13.8697137499649));
#416517=CARTESIAN_POINT('Ctrl Pts',(1.45233402963954,2.22666499892343,13.8715630732995));
#416518=CARTESIAN_POINT('Ctrl Pts',(1.44756101702111,2.22835860853675,13.8727429581918));
#416519=CARTESIAN_POINT('Ctrl Pts',(1.4427329923038,2.23007173811093,13.873936442031));
#416520=CARTESIAN_POINT('Ctrl Pts',(1.43791336775924,2.23255402409341,13.8744652622107));
#416521=CARTESIAN_POINT('Ctrl Pts',(1.43362464273219,2.23559487131693,13.8742206332401));
#416522=CARTESIAN_POINT('Ctrl Pts',(1.42993306497928,2.23821232146575,13.8740100655633));
#416523=CARTESIAN_POINT('Ctrl Pts',(1.42653464471422,2.2413103209958,13.8732246156103));
#416524=CARTESIAN_POINT('Ctrl Pts',(1.42365698855308,2.24460691634155,13.8719820486038));
#416525=CARTESIAN_POINT('Ctrl Pts',(1.42072974369188,2.24796031968264,13.8707180692815));
#416526=CARTESIAN_POINT('Ctrl Pts',(1.41826844194447,2.25158983507785,13.868960862563));
#416527=CARTESIAN_POINT('Ctrl Pts',(1.41632361547581,2.25523798118669,13.8669057591701));
#416528=CARTESIAN_POINT('Ctrl Pts',(1.41332903010898,2.26085528696161,13.8637413727084));
#416529=CARTESIAN_POINT('Ctrl Pts',(1.4114429436631,2.26667842626117,13.8597962563956));
#416530=CARTESIAN_POINT('Ctrl Pts',(1.41047796848851,2.27227881563235,13.855546950204));
#416531=CARTESIAN_POINT('Ctrl Pts',(1.40932712501071,2.27895792173855,13.850479165618));
#416532=CARTESIAN_POINT('Ctrl Pts',(1.40943608832967,2.28550653358124,13.8448473071436));
#416533=CARTESIAN_POINT('Ctrl Pts',(1.41051208250141,2.2916126210755,13.8390832900376));
#416534=CARTESIAN_POINT('',(1.41672473886902,2.32686377481446,13.8057746032556));
#416535=CARTESIAN_POINT('',(1.41051208250141,2.2916126210755,13.8390832900376));
#416536=CARTESIAN_POINT('',(1.33914762617131,2.37235908908981,13.8057746032556));
#416537=CARTESIAN_POINT('Origin',(0.,2.5406128344257E-15,13.8057746032556));
#416538=CARTESIAN_POINT('',(1.31141522584929,2.34972824925897,13.8390832900376));
#416539=CARTESIAN_POINT('',(1.33914762617131,2.37235908908981,13.8057746032556));
#416540=CARTESIAN_POINT('',(1.21903101699467,2.39895729840277,13.8390832900376));
#416541=CARTESIAN_POINT('Ctrl Pts',(1.31141522584929,2.34972824925897,13.8390832900376));
#416542=CARTESIAN_POINT('Ctrl Pts',(1.30601404690432,2.3453208555135,13.8455641171218));
#416543=CARTESIAN_POINT('Ctrl Pts',(1.29951033566265,2.34169609918505,13.851896480191));
#416544=CARTESIAN_POINT('Ctrl Pts',(1.29209039423872,2.33945208476775,13.8574481026913));
#416545=CARTESIAN_POINT('Ctrl Pts',(1.2870751262934,2.33793531624723,13.8612005412592));
#416546=CARTESIAN_POINT('Ctrl Pts',(1.28151820159939,2.33703095818381,13.8646714234115));
#416547=CARTESIAN_POINT('Ctrl Pts',(1.27568937548518,2.3370316806802,13.8674635290331));
#416548=CARTESIAN_POINT('Ctrl Pts',(1.27099179297695,2.33703226295634,13.8697137499649));
#416549=CARTESIAN_POINT('Ctrl Pts',(1.26600763920347,2.33763466105338,13.8715630732995));
#416550=CARTESIAN_POINT('Ctrl Pts',(1.26111246348459,2.33893359048154,13.8727429581918));
#416551=CARTESIAN_POINT('Ctrl Pts',(1.25616086765703,2.34024749092273,13.873936442031));
#416552=CARTESIAN_POINT('Ctrl Pts',(1.25115495066356,2.34232867315978,13.8744652622107));
#416553=CARTESIAN_POINT('Ctrl Pts',(1.24663263873668,2.34500983131073,13.8742206332401));
#416554=CARTESIAN_POINT('Ctrl Pts',(1.24273999791786,2.34731767425231,13.8740100655633));
#416555=CARTESIAN_POINT('Ctrl Pts',(1.23910036989375,2.35012836264349,13.8732246156103));
#416556=CARTESIAN_POINT('Ctrl Pts',(1.23596358577132,2.35317943314819,13.8719820486038));
#416557=CARTESIAN_POINT('Ctrl Pts',(1.23277274757214,2.3562830806849,13.8707180692815));
#416558=CARTESIAN_POINT('Ctrl Pts',(1.23002379640377,2.35969990022501,13.868960862563));
#416559=CARTESIAN_POINT('Ctrl Pts',(1.22778808340914,2.36317738601655,13.8669057591701));
#416560=CARTESIAN_POINT('Ctrl Pts',(1.22434559970891,2.36853191416212,13.8637413727084));
#416561=CARTESIAN_POINT('Ctrl Pts',(1.22199114914778,2.37418194389113,13.8597962563956));
#416562=CARTESIAN_POINT('Ctrl Pts',(1.22057290112324,2.37968504399355,13.855546950204));
#416563=CARTESIAN_POINT('Ctrl Pts',(1.21888147782873,2.38624812149782,13.850479165618));
#416564=CARTESIAN_POINT('Ctrl Pts',(1.21845630592171,2.39278382489689,13.8448473071436));
#416565=CARTESIAN_POINT('Ctrl Pts',(1.21903101699467,2.39895729840277,13.8390832900376));
#416566=CARTESIAN_POINT('',(1.22234970497526,2.43459754600513,13.8057746032556));
#416567=CARTESIAN_POINT('',(1.21903101699467,2.39895729840277,13.8390832900376));
#416568=CARTESIAN_POINT('',(1.14132243324905,2.47361822349969,13.8057746032556));
#416569=CARTESIAN_POINT('Origin',(0.,2.5406128344257E-15,13.8057746032556));
#416570=CARTESIAN_POINT('',(1.11552693374202,2.44880223784019,13.8390832900376));
#416571=CARTESIAN_POINT('',(1.14132243324905,2.47361822349969,13.8057746032556));
#416572=CARTESIAN_POINT('',(1.01943750119579,2.49033731070927,13.8390832900376));
#416573=CARTESIAN_POINT('Ctrl Pts',(1.11552693374202,2.44880223784019,13.8390832900376));
#416574=CARTESIAN_POINT('Ctrl Pts',(1.11050297028093,2.44396926310771,13.8455641171218));
#416575=CARTESIAN_POINT('Ctrl Pts',(1.10431635089327,2.43982645501321,13.851896480191));
#416576=CARTESIAN_POINT('Ctrl Pts',(1.09710400671974,2.43698511325934,13.8574481026913));
#416577=CARTESIAN_POINT('Ctrl Pts',(1.0922290573802,2.43506460076393,13.8612005412592));
#416578=CARTESIAN_POINT('Ctrl Pts',(1.08676433647251,2.43371031092683,13.8646714234115));
#416579=CARTESIAN_POINT('Ctrl Pts',(1.08095484640619,2.43323592757868,13.8674635290331));
#416580=CARTESIAN_POINT('Ctrl Pts',(1.07627284725532,2.43285361133269,13.8697137499649));
#416581=CARTESIAN_POINT('Ctrl Pts',(1.07125617680505,2.4330477501966,13.8715630732995));
#416582=CARTESIAN_POINT('Ctrl Pts',(1.06627141457249,2.43394335527855,13.8727429581918));
#416583=CARTESIAN_POINT('Ctrl Pts',(1.06122919968795,2.43484928279609,13.873936442031));
#416584=CARTESIAN_POINT('Ctrl Pts',(1.05607030379724,2.43651551136331,13.8744652622107));
#416585=CARTESIAN_POINT('Ctrl Pts',(1.05134450021028,2.43881913777655,13.8742206332401));
#416586=CARTESIAN_POINT('Ctrl Pts',(1.04727670120795,2.44080201519688,13.8740100655633));
#416587=CARTESIAN_POINT('Ctrl Pts',(1.04342008654881,2.44330668778168,13.8732246156103));
#416588=CARTESIAN_POINT('Ctrl Pts',(1.04004504924589,2.44609192907451,13.8719820486038));
#416589=CARTESIAN_POINT('Ctrl Pts',(1.0366118522105,2.44892516654454,13.8707180692815));
#416590=CARTESIAN_POINT('Ctrl Pts',(1.03359354543764,2.45210655185927,13.868960862563));
#416591=CARTESIAN_POINT('Ctrl Pts',(1.03108182421815,2.45539023523929,13.8669057591701));
#416592=CARTESIAN_POINT('Ctrl Pts',(1.02721435134557,2.46044635225415,13.8637413727084));
#416593=CARTESIAN_POINT('Ctrl Pts',(1.02440720514922,2.46588567239695,13.8597962563956));
#416594=CARTESIAN_POINT('Ctrl Pts',(1.02254512248136,2.47125486100738,13.855546950204));
#416595=CARTESIAN_POINT('Ctrl Pts',(1.02032437551309,2.47765823371176,13.850479165618));
#416596=CARTESIAN_POINT('Ctrl Pts',(1.01936789782898,2.4841375346394,13.8448473071436));
#416597=CARTESIAN_POINT('Ctrl Pts',(1.01943750119579,2.49033731070927,13.8390832900376));
#416598=CARTESIAN_POINT('',(1.01984013546839,2.52612947220745,13.8057746032556));
#416599=CARTESIAN_POINT('',(1.01943750119579,2.49033731070927,13.8390832900376));
#416600=CARTESIAN_POINT('',(0.935901927838467,2.55841583675045,13.8057746032556));
#416601=CARTESIAN_POINT('Origin',(0.,2.5406128344257E-15,13.8057746032556));
#416602=CARTESIAN_POINT('',(0.912214993939689,2.5315798515525,13.8390832900376));
#416603=CARTESIAN_POINT('',(0.935901927838467,2.55841583675045,13.8057746032556));
#416604=CARTESIAN_POINT('',(0.813059797021804,2.56514453908973,13.8390832900376));
#416605=CARTESIAN_POINT('Ctrl Pts',(0.912214993939688,2.5315798515525,13.8390832900376));
#416606=CARTESIAN_POINT('Ctrl Pts',(0.907601679610414,2.52635345848247,
13.8455641171218));
#416607=CARTESIAN_POINT('Ctrl Pts',(0.901773323008058,2.52172016832629,
13.851896480191));
#416608=CARTESIAN_POINT('Ctrl Pts',(0.894816573045464,2.51830040789643,
13.8574481026913));
#416609=CARTESIAN_POINT('Ctrl Pts',(0.890114384295236,2.51598893211992,
13.8612005412592));
#416610=CARTESIAN_POINT('Ctrl Pts',(0.884778233989902,2.51419372308456,
13.8646714234115));
#416611=CARTESIAN_POINT('Ctrl Pts',(0.879026741169359,2.51324739083479,
13.8674635290331));
#416612=CARTESIAN_POINT('Ctrl Pts',(0.874391483307722,2.51248472031822,
13.8697137499649));
#416613=CARTESIAN_POINT('Ctrl Pts',(0.869375681294828,2.51226930798688,
13.8715630732995));
#416614=CARTESIAN_POINT('Ctrl Pts',(0.864334505318809,2.51275562861857,
13.8727429581918));
#416615=CARTESIAN_POINT('Ctrl Pts',(0.859235226485449,2.51324755441431,
13.873936442031));
#416616=CARTESIAN_POINT('Ctrl Pts',(0.853957683298495,2.51448774083547,
13.8744652622107));
#416617=CARTESIAN_POINT('Ctrl Pts',(0.849059837494611,2.5163985052573,13.8742206332401));
#416618=CARTESIAN_POINT('Ctrl Pts',(0.844843950840004,2.5180432214343,13.8740100655633));
#416619=CARTESIAN_POINT('Ctrl Pts',(0.840796014680084,2.52022521002991,
13.8732246156103));
#416620=CARTESIAN_POINT('Ctrl Pts',(0.837205184513088,2.5227260867896,13.8719820486038));
#416621=CARTESIAN_POINT('Ctrl Pts',(0.833552476001309,2.52527005946504,
13.8707180692815));
#416622=CARTESIAN_POINT('Ctrl Pts',(0.830284899957549,2.52819483896,13.868960862563));
#416623=CARTESIAN_POINT('Ctrl Pts',(0.827513885603518,2.53126286755739,
13.8669057591701));
#416624=CARTESIAN_POINT('Ctrl Pts',(0.823247160952463,2.535986925817,13.8637413727084));
#416625=CARTESIAN_POINT('Ctrl Pts',(0.820006000215689,2.54117933859546,
13.8597962563956));
#416626=CARTESIAN_POINT('Ctrl Pts',(0.817712474757428,2.54637888464955,
13.855546950204));
#416627=CARTESIAN_POINT('Ctrl Pts',(0.814977182820077,2.55257993916518,
13.850479165618));
#416628=CARTESIAN_POINT('Ctrl Pts',(0.813495764560061,2.55895971894273,
13.8448473071436));
#416629=CARTESIAN_POINT('Ctrl Pts',(0.813059797021804,2.56514453908973,
13.8390832900376));
#416630=CARTESIAN_POINT('',(0.810543698121754,2.60085042355426,13.8057746032556));
#416631=CARTESIAN_POINT('',(0.813059797021804,2.56514453908973,13.8390832900376));
#416632=CARTESIAN_POINT('',(0.72425314951107,2.62618761471654,13.8057746032556));
#416633=CARTESIAN_POINT('Origin',(0.,2.5406128344257E-15,13.8057746032556));
#416634=CARTESIAN_POINT('',(0.702832413857569,2.59751021903401,13.8390832900376));
#416635=CARTESIAN_POINT('',(0.72425314951107,2.62618761471654,13.8057746032556));
#416636=CARTESIAN_POINT('',(0.601271314044061,2.6228811537816,13.8390832900376));
#416637=CARTESIAN_POINT('Ctrl Pts',(0.702832413857569,2.59751021903401,
13.8390832900376));
#416638=CARTESIAN_POINT('Ctrl Pts',(0.698660449505827,2.59192518841002,
13.8455641171218));
#416639=CARTESIAN_POINT('Ctrl Pts',(0.693229142440357,2.58683224997369,
13.851896480191));
#416640=CARTESIAN_POINT('Ctrl Pts',(0.686574282711912,2.58285682880929,
13.8574481026913));
#416641=CARTESIAN_POINT('Ctrl Pts',(0.682076146841327,2.58016977224161,
13.8612005412592));
#416642=CARTESIAN_POINT('Ctrl Pts',(0.676904078338221,2.57794559082794,
13.8646714234115));
#416643=CARTESIAN_POINT('Ctrl Pts',(0.67124885799925,2.57653360736153,13.8674635290331));
#416644=CARTESIAN_POINT('Ctrl Pts',(0.666691188303154,2.57539565802083,
13.8697137499649));
#416645=CARTESIAN_POINT('Ctrl Pts',(0.661709634062478,2.57477212802776,
13.8715630732995));
#416646=CARTESIAN_POINT('Ctrl Pts',(0.656645592537388,2.57484592782563,
13.8727429581918));
#416647=CARTESIAN_POINT('Ctrl Pts',(0.651523184614516,2.57492057821455,
13.873936442031));
#416648=CARTESIAN_POINT('Ctrl Pts',(0.6461621153105,2.57572646925365,13.8744652622107));
#416649=CARTESIAN_POINT('Ctrl Pts',(0.641124821645433,2.57723165586209,
13.8742206332401));
#416650=CARTESIAN_POINT('Ctrl Pts',(0.636788903368657,2.57852726548096,
13.8740100655633));
#416651=CARTESIAN_POINT('Ctrl Pts',(0.632576584055241,2.58037204931328,
13.8732246156103));
#416652=CARTESIAN_POINT('Ctrl Pts',(0.628793857406481,2.58257191861761,
13.8719820486038));
#416653=CARTESIAN_POINT('Ctrl Pts',(0.624945945590808,2.58480969678004,
13.8707180692815));
#416654=CARTESIAN_POINT('Ctrl Pts',(0.621450845455611,2.58745840653024,
13.868960862563));
#416655=CARTESIAN_POINT('Ctrl Pts',(0.618438978610375,2.59029036312087,
13.8669057591701));
#416656=CARTESIAN_POINT('Ctrl Pts',(0.61380139652944,2.59465092479693,13.8637413727084));
#416657=CARTESIAN_POINT('Ctrl Pts',(0.610147790642189,2.59956187556069,
13.8597962563956));
#416658=CARTESIAN_POINT('Ctrl Pts',(0.607438085427048,2.60455717693733,
13.855546950204));
#416659=CARTESIAN_POINT('Ctrl Pts',(0.604206451437169,2.61051464626949,
13.850479165618));
#416660=CARTESIAN_POINT('Ctrl Pts',(0.602209951195348,2.61675244851512,
13.8448473071436));
#416661=CARTESIAN_POINT('Ctrl Pts',(0.601271314044061,2.6228811537816,13.8390832900376));
#416662=CARTESIAN_POINT('',(0.595853226194419,2.65826314444243,13.8057746032556));
#416663=CARTESIAN_POINT('',(0.601271314044061,2.6228811537816,13.8390832900376));
#416664=CARTESIAN_POINT('',(0.507784585967034,2.67648254739715,13.8057746032556));
#416665=CARTESIAN_POINT('Origin',(0.,2.5406128344257E-15,13.8057746032556));
#416666=CARTESIAN_POINT('',(0.488772600020414,2.64615458456687,13.8390832900376));
#416667=CARTESIAN_POINT('',(0.507784585967034,2.67648254739715,13.8057746032556));
#416668=CARTESIAN_POINT('',(0.385481469674138,2.66316292713999,13.8390832900376));
#416669=CARTESIAN_POINT('Ctrl Pts',(0.488772600020413,2.64615458456687,
13.8390832900376));
#416670=CARTESIAN_POINT('Ctrl Pts',(0.48506974938064,2.64024808384625,13.8455641171218));
#416671=CARTESIAN_POINT('Ctrl Pts',(0.48007163630447,2.6347293897948,13.851896480191));
#416672=CARTESIAN_POINT('Ctrl Pts',(0.473762953803692,2.6302247636678,13.8574481026913));
#416673=CARTESIAN_POINT('Ctrl Pts',(0.469498805164829,2.62718000822708,
13.8612005412592));
#416674=CARTESIAN_POINT('Ctrl Pts',(0.46452523772651,2.62454165599543,13.8646714234115));
#416675=CARTESIAN_POINT('Ctrl Pts',(0.459003924427422,2.62267341782939,
13.8674635290331));
#416676=CARTESIAN_POINT('Ctrl Pts',(0.454554173436733,2.62116776252968,
13.8697137499649));
#416677=CARTESIAN_POINT('Ctrl Pts',(0.449640018389848,2.62014026436412,
13.8715630732995));
#416678=CARTESIAN_POINT('Ctrl Pts',(0.444586811676528,2.61980105220269,
13.8727429581918));
#416679=CARTESIAN_POINT('Ctrl Pts',(0.439475363443734,2.61945793039877,
13.873936442031));
#416680=CARTESIAN_POINT('Ctrl Pts',(0.434066445054353,2.6198241629839,13.8744652622107));
#416681=CARTESIAN_POINT('Ctrl Pts',(0.428923225886351,2.62091375501042,
13.8742206332401));
#416682=CARTESIAN_POINT('Ctrl Pts',(0.424496130808162,2.6218516360029,13.8740100655633));
#416683=CARTESIAN_POINT('Ctrl Pts',(0.420147460631299,2.62334693833989,
13.8732246156103));
#416684=CARTESIAN_POINT('Ctrl Pts',(0.416198010922517,2.62523116042159,
13.8719820486038));
#416685=CARTESIAN_POINT('Ctrl Pts',(0.412180503021224,2.62714785202654,
13.8707180692815));
#416686=CARTESIAN_POINT('Ctrl Pts',(0.408481138109338,2.6295028653056,13.868960862563));
#416687=CARTESIAN_POINT('Ctrl Pts',(0.405248462249829,2.63207990368561,
13.8669057591701));
#416688=CARTESIAN_POINT('Ctrl Pts',(0.400270885082617,2.63604794995961,
13.8637413727084));
#416689=CARTESIAN_POINT('Ctrl Pts',(0.396229148189263,2.64064475714159,
13.8597962563956));
#416690=CARTESIAN_POINT('Ctrl Pts',(0.39312129585838,2.64540257093427,13.855546950204));
#416691=CARTESIAN_POINT('Ctrl Pts',(0.389414825806991,2.65107680910749,
13.850479165618));
#416692=CARTESIAN_POINT('Ctrl Pts',(0.386916529963079,2.65713112227642,
13.8448473071436));
#416693=CARTESIAN_POINT('Ctrl Pts',(0.385481469674138,2.66316292713999,
13.8390832900376));
#416694=CARTESIAN_POINT('',(0.377197449355622,2.69798556268689,13.8057746032556));
#416695=CARTESIAN_POINT('',(0.385481469674138,2.66316292713999,13.8390832900376));
#416696=CARTESIAN_POINT('',(0.287936799781948,2.70896593031337,13.8057746032556));
#416697=CARTESIAN_POINT('Origin',(0.,2.5406128344257E-15,13.8057746032556));
#416698=CARTESIAN_POINT('',(0.271460085171925,2.67718922792421,13.8390832900376));
#416699=CARTESIAN_POINT('',(0.287936799781948,2.70896593031337,13.8057746032556));
#416700=CARTESIAN_POINT('',(0.1671263097235,2.68572179060922,13.8390832900376));
#416701=CARTESIAN_POINT('Ctrl Pts',(0.271460085171925,2.67718922792421,
13.8390832900376));
#416702=CARTESIAN_POINT('Ctrl Pts',(0.268250990104199,2.67100056389476,
13.8455641171218));
#416703=CARTESIAN_POINT('Ctrl Pts',(0.263719332635224,2.66509284022658,
13.851896480191));
#416704=CARTESIAN_POINT('Ctrl Pts',(0.257798810603297,2.66008898668065,
13.8574481026913));
#416705=CARTESIAN_POINT('Ctrl Pts',(0.253797026401811,2.65670679471198,
13.8612005412592));
#416706=CARTESIAN_POINT('Ctrl Pts',(0.249055058299,2.65367182946117,13.8646714234115));
#416707=CARTESIAN_POINT('Ctrl Pts',(0.243704395468847,2.65135976941226,
13.8674635290331));
#416708=CARTESIAN_POINT('Ctrl Pts',(0.239392175542249,2.64949642804114,
13.8697137499649));
#416709=CARTESIAN_POINT('Ctrl Pts',(0.234578122580215,2.64807179953385,
13.8715630732995));
#416710=CARTESIAN_POINT('Ctrl Pts',(0.229569378935621,2.64732183281409,
13.8727429581918));
#416711=CARTESIAN_POINT('Ctrl Pts',(0.224502906237564,2.64656322223632,
13.873936442031));
#416712=CARTESIAN_POINT('Ctrl Pts',(0.219082134222294,2.64648735915005,
13.8744652622107));
#416713=CARTESIAN_POINT('Ctrl Pts',(0.213867216826347,2.64715410553948,
13.8742206332401));
#416714=CARTESIAN_POINT('Ctrl Pts',(0.209378406534072,2.64772801646231,
13.8740100655633));
#416715=CARTESIAN_POINT('Ctrl Pts',(0.204922325176305,2.64886388631363,
13.8732246156103));
#416716=CARTESIAN_POINT('Ctrl Pts',(0.2008324353437,2.65041992198562,13.8719820486038));
#416717=CARTESIAN_POINT('Ctrl Pts',(0.196672067209027,2.65200277176669,
13.8707180692815));
#416718=CARTESIAN_POINT('Ctrl Pts',(0.192793056183592,2.6540484163498,13.868960862563));
#416719=CARTESIAN_POINT('Ctrl Pts',(0.1893610842343,2.65635338675394,13.8669057591701));
#416720=CARTESIAN_POINT('Ctrl Pts',(0.184076636935616,2.6599025109326,13.8637413727084));
#416721=CARTESIAN_POINT('Ctrl Pts',(0.179673666128347,2.66415458353943,
13.8597962563956));
#416722=CARTESIAN_POINT('Ctrl Pts',(0.176188348926224,2.66864324728235,
13.855546950204));
#416723=CARTESIAN_POINT('Ctrl Pts',(0.172031708759995,2.67399649317776,
13.850479165618));
#416724=CARTESIAN_POINT('Ctrl Pts',(0.169048243060639,2.67982702681473,
13.8448473071436));
#416725=CARTESIAN_POINT('Ctrl Pts',(0.1671263097235,2.68572179060922,13.8390832900376));
#416726=CARTESIAN_POINT('',(0.156031485724562,2.71975333214795,13.8057746032556));
#416727=CARTESIAN_POINT('',(0.1671263097235,2.68572179060922,13.8390832900376));
#416728=CARTESIAN_POINT('',(0.0661728417005766,2.72342159191127,13.8057746032556));
#416729=CARTESIAN_POINT('Origin',(0.,2.5406128344257E-15,13.8057746032556));
#416730=CARTESIAN_POINT('',(0.0523410482444132,2.69040761867485,13.8390832900376));
#416731=CARTESIAN_POINT('',(0.0661728417005766,2.72342159191127,13.8057746032556));
#416732=CARTESIAN_POINT('Ctrl Pts',(0.0523410482444132,2.69040761867485,
13.8390832900376));
#416733=CARTESIAN_POINT('Ctrl Pts',(0.0496470647469476,2.68397797587462,
13.8455641171218));
#416734=CARTESIAN_POINT('Ctrl Pts',(0.0456120587089066,2.67772051809082,
13.851896480191));
#416735=CARTESIAN_POINT('Ctrl Pts',(0.0401285192509084,2.67226017679703,
13.8574385412955));
#416736=CARTESIAN_POINT('Ctrl Pts',(0.0364062442971185,2.66855364896174,
13.8612005412592));
#416737=CARTESIAN_POINT('Ctrl Pts',(0.031927461700894,2.66514225178075,
13.8646714234115));
#416738=CARTESIAN_POINT('Ctrl Pts',(0.0267845789591358,2.66240257155708,
13.8674627013498));
#416739=CARTESIAN_POINT('Ctrl Pts',(0.0226370596760621,2.66019313433526,
13.8697137499649));
#416740=CARTESIAN_POINT('Ctrl Pts',(0.0179551393667713,2.65838087216932,
13.8715630732995));
#416741=CARTESIAN_POINT('Ctrl Pts',(0.0130142993447968,2.657222802874,13.8727453272031));
#416742=CARTESIAN_POINT('Ctrl Pts',(0.0088450433803829,2.6562455829488,
13.8737429549582));
#416743=CARTESIAN_POINT('Ctrl Pts',(0.00439692111021513,2.65571825406977,
13.8742817459302));
#416744=CARTESIAN_POINT('Ctrl Pts',(3.72770476910004E-12,2.65571825406948,
13.8742817459305));
#416745=CARTESIAN_POINT('Origin',(0.,2.60208521396521E-15,13.912));
#416746=CARTESIAN_POINT('',(-3.05371705427032E-16,2.49354920651117,14.));
#416747=CARTESIAN_POINT('Origin',(0.,2.5406128344257E-15,14.));
#416748=CARTESIAN_POINT('Origin',(-3.05371705427032E-16,2.49354920651117,
13.912));
#416749=CARTESIAN_POINT('Origin',(0.,2.5406128344257E-15,14.));
#416750=CARTESIAN_POINT('',(-0.037827685004575,-2.74973981791863,13.7435492065112));
#416751=CARTESIAN_POINT('',(0.0378276850046121,-2.74973981791863,13.7435492065112));
#416752=CARTESIAN_POINT('Origin',(0.,2.5406128344257E-15,13.7435492065112));
#416753=CARTESIAN_POINT('',(-0.037827685004575,-2.74973981791863,12.5369868989719));
#416754=CARTESIAN_POINT('',(-0.037827685004575,-2.74973981791863,14.));
#416755=CARTESIAN_POINT('Ctrl Pts',(-0.0729573509223692,-2.74903205236796,
12.4908873016278));
#416756=CARTESIAN_POINT('Ctrl Pts',(-0.0707767921054796,-2.74908992284447,
12.4908873016278));
#416757=CARTESIAN_POINT('Ctrl Pts',(-0.0685838718709331,-2.74914546989179,
12.4911020829134));
#416758=CARTESIAN_POINT('Ctrl Pts',(-0.0664485864717655,-2.74919708012283,
12.4915448903141));
#416759=CARTESIAN_POINT('Ctrl Pts',(-0.0627953733565572,-2.749285378939,
12.4923024798169));
#416760=CARTESIAN_POINT('Ctrl Pts',(-0.0592269615777823,-2.7493639210411,
12.4937722312795));
#416761=CARTESIAN_POINT('Ctrl Pts',(-0.0560965908340369,-2.74942779001319,
12.4958030942394));
#416762=CARTESIAN_POINT('Ctrl Pts',(-0.0529883153033171,-2.74949120817652,
12.4978196226833));
#416763=CARTESIAN_POINT('Ctrl Pts',(-0.0502197797679206,-2.74954236051975,
12.5004326847668));
#416764=CARTESIAN_POINT('Ctrl Pts',(-0.0479357073569643,-2.74958218061585,
12.5033504258767));
#416765=CARTESIAN_POINT('Ctrl Pts',(-0.0452066442771379,-2.749629758597,
12.5068366111226));
#416766=CARTESIAN_POINT('Ctrl Pts',(-0.0430813958680921,-2.7496629604294,
12.5108395010833));
#416767=CARTESIAN_POINT('Ctrl Pts',(-0.0415315315886475,-2.7496863697309,
12.5149868989719));
#416768=CARTESIAN_POINT('Ctrl Pts',(-0.0389283867661261,-2.74972568788464,
12.5219528491417));
#416769=CARTESIAN_POINT('Ctrl Pts',(-0.0378276849660689,-2.74973981791945,
12.5295503425868));
#416770=CARTESIAN_POINT('Ctrl Pts',(-0.037827685004575,-2.74973981791863,
12.5369868989719));
#416771=CARTESIAN_POINT('',(-0.186427505996059,-2.74367359301505,12.5369868989719));
#416772=CARTESIAN_POINT('Ctrl Pts',(-0.186427505996059,-2.74367359301504,
12.5369868989719));
#416773=CARTESIAN_POINT('Ctrl Pts',(-0.186427505996057,-2.74367359301504,
12.5309445149785));
#416774=CARTESIAN_POINT('Ctrl Pts',(-0.185705362546179,-2.74372306599812,
12.5248274368704));
#416775=CARTESIAN_POINT('Ctrl Pts',(-0.184052403196883,-2.74383394411496,
12.5190199595513));
#416776=CARTESIAN_POINT('Ctrl Pts',(-0.182664021058617,-2.74392707477603,
12.5141420429941));
#416777=CARTESIAN_POINT('Ctrl Pts',(-0.180576035463166,-2.74406644051104,
12.5093757677094));
#416778=CARTESIAN_POINT('Ctrl Pts',(-0.177695111376414,-2.74425298531183,
12.5051960112707));
#416779=CARTESIAN_POINT('Ctrl Pts',(-0.175770455473429,-2.7443776100993,
12.5024036458141));
#416780=CARTESIAN_POINT('Ctrl Pts',(-0.173445221259834,-2.74452614690824,
12.4998248032393));
#416781=CARTESIAN_POINT('Ctrl Pts',(-0.170801591843253,-2.74469065947764,
12.4976950015772));
#416782=CARTESIAN_POINT('Ctrl Pts',(-0.168083475609416,-2.74485980734789,
12.495505190692));
#416783=CARTESIAN_POINT('Ctrl Pts',(-0.164958669846826,-2.74504999977299,
12.4937456938368));
#416784=CARTESIAN_POINT('Ctrl Pts',(-0.161668310532495,-2.74524377011761,
12.4925987732155));
#416785=CARTESIAN_POINT('Ctrl Pts',(-0.158378721149558,-2.74543749512071,
12.4914521209692));
#416786=CARTESIAN_POINT('Ctrl Pts',(-0.154841629042532,-2.74563949730457,
12.4908873016276));
#416787=CARTESIAN_POINT('Ctrl Pts',(-0.151357041680656,-2.74583157639606,
12.4908873016278));
#416788=CARTESIAN_POINT('',(-0.186427505996058,-2.74367359301505,13.7435492065112));
#416789=CARTESIAN_POINT('',(-0.186427505996058,-2.74367359301505,14.));
#416790=CARTESIAN_POINT('',(-0.261831139002666,-2.73750697800911,13.7435492065112));
#416791=CARTESIAN_POINT('Origin',(0.,2.5406128344257E-15,13.7435492065112));
#416792=CARTESIAN_POINT('',(-0.261831139002667,-2.73750697800911,12.5369868989719));
#416793=CARTESIAN_POINT('',(-0.261831139002667,-2.73750697800911,14.));
#416794=CARTESIAN_POINT('Ctrl Pts',(-0.296786224392158,-2.73393817358971,
12.4908873016278));
#416795=CARTESIAN_POINT('Ctrl Pts',(-0.294617638185927,-2.73417358729388,
12.4908873016278));
#416796=CARTESIAN_POINT('Ctrl Pts',(-0.292436542312588,-2.73440769287018,
12.4911020829134));
#416797=CARTESIAN_POINT('Ctrl Pts',(-0.290312568612394,-2.73463317695549,
12.4915448903141));
#416798=CARTESIAN_POINT('Ctrl Pts',(-0.286678708435701,-2.7350189527483,
12.4923024798169));
#416799=CARTESIAN_POINT('Ctrl Pts',(-0.283128572163218,-2.73538809219552,
12.4937722312795));
#416800=CARTESIAN_POINT('Ctrl Pts',(-0.28001382338404,-2.73570690292543,
12.4958030942394));
#416801=CARTESIAN_POINT('Ctrl Pts',(-0.276921059552791,-2.73602346338163,
12.4978196226833));
#416802=CARTESIAN_POINT('Ctrl Pts',(-0.274165905481849,-2.73630010686762,
12.5004326847668));
#416803=CARTESIAN_POINT('Ctrl Pts',(-0.271892678840921,-2.73652596757143,
12.5033504258767));
#416804=CARTESIAN_POINT('Ctrl Pts',(-0.269176574540517,-2.73679583121716,
12.5068366111226));
#416805=CARTESIAN_POINT('Ctrl Pts',(-0.267061103977803,-2.73700215004838,
12.5108395010833));
#416806=CARTESIAN_POINT('Ctrl Pts',(-0.265518304819288,-2.73715180978438,
12.5149868989719));
#416807=CARTESIAN_POINT('Ctrl Pts',(-0.262927026540961,-2.73740317757966,
12.5219528491417));
#416808=CARTESIAN_POINT('Ctrl Pts',(-0.261831138964355,-2.73750697801306,
12.5295503425868));
#416809=CARTESIAN_POINT('Ctrl Pts',(-0.261831139002667,-2.73750697800911,
12.5369868989719));
#416810=CARTESIAN_POINT('',(-0.409442052702697,-2.71934867302423,12.5369868989719));
#416811=CARTESIAN_POINT('Ctrl Pts',(-0.409442052702696,-2.71934867302422,
12.5369868989719));
#416812=CARTESIAN_POINT('Ctrl Pts',(-0.409442052702695,-2.71934867302422,
12.5309445149785));
#416813=CARTESIAN_POINT('Ctrl Pts',(-0.408726344632979,-2.71945684278525,
12.5248274368704));
#416814=CARTESIAN_POINT('Ctrl Pts',(-0.407087922965423,-2.71970208349659,
12.5190199595513));
#416815=CARTESIAN_POINT('Ctrl Pts',(-0.405711751567649,-2.71990807030645,
12.5141420429941));
#416816=CARTESIAN_POINT('Ctrl Pts',(-0.403642073173232,-2.72021716252342,
12.5093757677094));
#416817=CARTESIAN_POINT('Ctrl Pts',(-0.400785940256781,-2.72063790867004,
12.5051960112707));
#416818=CARTESIAN_POINT('Ctrl Pts',(-0.398877846564678,-2.72091899610253,
12.5024036458141));
#416819=CARTESIAN_POINT('Ctrl Pts',(-0.396572456504988,-2.72125656684232,
12.4998248032393));
#416820=CARTESIAN_POINT('Ctrl Pts',(-0.393951032848873,-2.72163601234943,
12.4976950015772));
#416821=CARTESIAN_POINT('Ctrl Pts',(-0.391255748044293,-2.72202614910091,
12.495505190692));
#416822=CARTESIAN_POINT('Ctrl Pts',(-0.388156842263406,-2.72247040935534,
12.4937456938368));
#416823=CARTESIAN_POINT('Ctrl Pts',(-0.38489322543022,-2.72293172977545,
12.4925987732155));
#416824=CARTESIAN_POINT('Ctrl Pts',(-0.381630372270791,-2.72339294224835,
12.4914521209692));
#416825=CARTESIAN_POINT('Ctrl Pts',(-0.378121514599243,-2.72388257813009,
12.4908873016276));
#416826=CARTESIAN_POINT('Ctrl Pts',(-0.374664178143486,-2.72435804431357,
12.4908873016278));
#416827=CARTESIAN_POINT('',(-0.409442052702696,-2.71934867302422,13.7435492065112));
#416828=CARTESIAN_POINT('',(-0.409442052702696,-2.71934867302423,14.));
#416829=CARTESIAN_POINT('',(-0.484092149969793,-2.7070564808178,13.7435492065112));
#416830=CARTESIAN_POINT('Origin',(0.,2.5406128344257E-15,13.7435492065112));
#416831=CARTESIAN_POINT('',(-0.484092149969793,-2.7070564808178,12.5369868989719));
#416832=CARTESIAN_POINT('',(-0.484092149969793,-2.7070564808178,14.));
#416833=CARTESIAN_POINT('Ctrl Pts',(-0.518640034504897,-2.70065038733427,
12.4908873016278));
#416834=CARTESIAN_POINT('Ctrl Pts',(-0.516497852492736,-2.70106177762674,
12.4908873016278));
#416835=CARTESIAN_POINT('Ctrl Pts',(-0.514343095813786,-2.70147288379803,
12.4911020829134));
#416836=CARTESIAN_POINT('Ctrl Pts',(-0.512244568507109,-2.70187074117823,
12.4915448903141));
#416837=CARTESIAN_POINT('Ctrl Pts',(-0.508654244008863,-2.70255142667342,
12.4923024798169));
#416838=CARTESIAN_POINT('Ctrl Pts',(-0.505146008813833,-2.70320870690365,
12.4937722312795));
#416839=CARTESIAN_POINT('Ctrl Pts',(-0.502067610138451,-2.70378033775857,
12.4958030942394));
#416840=CARTESIAN_POINT('Ctrl Pts',(-0.4990109398397,-2.70434793385003,
12.4978196226833));
#416841=CARTESIAN_POINT('Ctrl Pts',(-0.496287502328985,-2.70484822746203,
12.5004326847668));
#416842=CARTESIAN_POINT('Ctrl Pts',(-0.494040249406326,-2.70525862570782,
12.5033504258767));
#416843=CARTESIAN_POINT('Ctrl Pts',(-0.491355179111337,-2.7057489791201,
12.5068366111226));
#416844=CARTESIAN_POINT('Ctrl Pts',(-0.489263564502522,-2.70612704193236,
12.5108395010833));
#416845=CARTESIAN_POINT('Ctrl Pts',(-0.487738097538792,-2.706401956142,
12.5149868989719));
#416846=CARTESIAN_POINT('Ctrl Pts',(-0.485175930334071,-2.70686370076762,
12.5219528491417));
#416847=CARTESIAN_POINT('Ctrl Pts',(-0.484092149931931,-2.70705648082486,
12.5295503425868));
#416848=CARTESIAN_POINT('Ctrl Pts',(-0.484092149969793,-2.7070564808178,
12.5369868989719));
#416849=CARTESIAN_POINT('',(-0.629731830101783,-2.67692693627538,12.5369868989719));
#416850=CARTESIAN_POINT('Ctrl Pts',(-0.629731830101782,-2.67692693627537,
12.5369868989719));
#416851=CARTESIAN_POINT('Ctrl Pts',(-0.62973183010178,-2.67692693627537,
12.5309445149785));
#416852=CARTESIAN_POINT('Ctrl Pts',(-0.629027320331347,-2.67709308296243,
12.5248274368704));
#416853=CARTESIAN_POINT('Ctrl Pts',(-0.627414339771407,-2.67747105423181,
12.5190199595513));
#416854=CARTESIAN_POINT('Ctrl Pts',(-0.626059537307725,-2.67778852638223,
12.5141420429941));
#416855=CARTESIAN_POINT('Ctrl Pts',(-0.624021939482584,-2.67826528812344,
12.5093757677094));
#416856=CARTESIAN_POINT('Ctrl Pts',(-0.621209604829764,-2.6789174356197,
12.5051960112707));
#416857=CARTESIAN_POINT('Ctrl Pts',(-0.619330771397252,-2.67935311510673,
12.5024036458141));
#416858=CARTESIAN_POINT('Ctrl Pts',(-0.617060567481951,-2.6798774732998,
12.4998248032393));
#416859=CARTESIAN_POINT('Ctrl Pts',(-0.614478794728229,-2.68046932659736,
12.4976950015772));
#416860=CARTESIAN_POINT('Ctrl Pts',(-0.61182427802859,-2.68107785593437,
12.495505190692));
#416861=CARTESIAN_POINT('Ctrl Pts',(-0.608771894936094,-2.68177322753943,
12.4937456938368));
#416862=CARTESIAN_POINT('Ctrl Pts',(-0.60555673941562,-2.68249902802374,
12.4925987732155));
#416863=CARTESIAN_POINT('Ctrl Pts',(-0.602342336229141,-2.68322465867353,
12.4914521209692));
#416864=CARTESIAN_POINT('Ctrl Pts',(-0.598885063861954,-2.68399866980714,
12.4908873016276));
#416865=CARTESIAN_POINT('Ctrl Pts',(-0.59547798631601,-2.68475435893361,
12.4908873016278));
#416866=CARTESIAN_POINT('',(-0.629731830101781,-2.67692693627537,13.7435492065112));
#416867=CARTESIAN_POINT('',(-0.629731830101781,-2.67692693627538,14.));
#416868=CARTESIAN_POINT('',(-0.703131607548452,-2.65859096937952,13.7435492065112));
#416869=CARTESIAN_POINT('Origin',(0.,2.5406128344257E-15,13.7435492065112));
#416870=CARTESIAN_POINT('',(-0.703131607548453,-2.65859096937952,12.5369868989719));
#416871=CARTESIAN_POINT('',(-0.703131607548453,-2.65859096937952,14.));
#416872=CARTESIAN_POINT('Ctrl Pts',(-0.737042380757589,-2.64939021832708,
12.4908873016278));
#416873=CARTESIAN_POINT('Ctrl Pts',(-0.734940858807353,-2.64997484747332,
12.4908873016278));
#416874=CARTESIAN_POINT('Ctrl Pts',(-0.732826780872981,-2.65056021839586,
12.4911020829134));
#416875=CARTESIAN_POINT('Ctrl Pts',(-0.730767665312814,-2.65112780139571,
12.4915448903141));
#416876=CARTESIAN_POINT('Ctrl Pts',(-0.727244769510189,-2.65209886674363,
12.4923024798169));
#416877=CARTESIAN_POINT('Ctrl Pts',(-0.723801782119017,-2.65303991366538,
12.4937722312795));
#416878=CARTESIAN_POINT('Ctrl Pts',(-0.720780219782716,-2.65386056053629,
12.4958030942394));
#416879=CARTESIAN_POINT('Ctrl Pts',(-0.717779984652985,-2.65467541500467,
12.4978196226833));
#416880=CARTESIAN_POINT('Ctrl Pts',(-0.715106387729797,-2.65539602937123,
12.5004326847668));
#416881=CARTESIAN_POINT('Ctrl Pts',(-0.712900063622835,-2.65598823402638,
12.5033504258767));
#416882=CARTESIAN_POINT('Ctrl Pts',(-0.71026389603307,-2.65669581398415,
12.5068366111226));
#416883=CARTESIAN_POINT('Ctrl Pts',(-0.708210056728283,-2.65724310483181,
12.5108395010833));
#416884=CARTESIAN_POINT('Ctrl Pts',(-0.706712073690298,-2.65764144400639,
12.5149868989719));
#416885=CARTESIAN_POINT('Ctrl Pts',(-0.704196068359202,-2.65831049262804,
12.5219528491417));
#416886=CARTESIAN_POINT('Ctrl Pts',(-0.703131607511292,-2.65859096938964,
12.5295503425868));
#416887=CARTESIAN_POINT('Ctrl Pts',(-0.703131607548453,-2.65859096937952,
12.5369868989719));
#416888=CARTESIAN_POINT('',(-0.845830846069979,-2.61669069242747,12.5369868989719));
#416889=CARTESIAN_POINT('Ctrl Pts',(-0.845830846069978,-2.61669069242747,
12.5369868989719));
#416890=CARTESIAN_POINT('Ctrl Pts',(-0.845830846069976,-2.61669069242747,
12.5309445149785));
#416891=CARTESIAN_POINT('Ctrl Pts',(-0.845142222995113,-2.61691371036177,
12.5248274368704));
#416892=CARTESIAN_POINT('Ctrl Pts',(-0.843565417662293,-2.61742189685275,
12.5190199595513));
#416893=CARTESIAN_POINT('Ctrl Pts',(-0.842241000119572,-2.61784874161894,
12.5141420429941));
#416894=CARTESIAN_POINT('Ctrl Pts',(-0.840249042741053,-2.61849000011367,
12.5093757677094));
#416895=CARTESIAN_POINT('Ctrl Pts',(-0.837499221974976,-2.61936920902558,
12.5051960112707));
#416896=CARTESIAN_POINT('Ctrl Pts',(-0.835662152128562,-2.61995658119205,
12.5024036458141));
#416897=CARTESIAN_POINT('Ctrl Pts',(-0.833442242190149,-2.62066423732113,
12.4998248032393));
#416898=CARTESIAN_POINT('Ctrl Pts',(-0.830917301610533,-2.6214645597231,
12.4976950015772));
#416899=CARTESIAN_POINT('Ctrl Pts',(-0.828321218386507,-2.62228743198329,
12.495505190692));
#416900=CARTESIAN_POINT('Ctrl Pts',(-0.825335671088275,-2.62322928735568,
12.4937456938368));
#416901=CARTESIAN_POINT('Ctrl Pts',(-0.822190373210037,-2.62421473782172,
12.4925987732155));
#416902=CARTESIAN_POINT('Ctrl Pts',(-0.819045811319376,-2.62519995769615,
12.4914521209692));
#416903=CARTESIAN_POINT('Ctrl Pts',(-0.815663131833744,-2.62625319316524,
12.4908873016276));
#416904=CARTESIAN_POINT('Ctrl Pts',(-0.812328986736553,-2.62728407624824,
12.4908873016278));
#416905=CARTESIAN_POINT('',(-0.845830846069977,-2.61669069242747,13.7435492065112));
#416906=CARTESIAN_POINT('',(-0.845830846069978,-2.61669069242747,14.));
#416907=CARTESIAN_POINT('',(-0.917491840287427,-2.59243297367666,13.7435492065112));
#416908=CARTESIAN_POINT('Origin',(0.,2.5406128344257E-15,13.7435492065112));
#416909=CARTESIAN_POINT('',(-0.917491840287428,-2.59243297367666,12.5369868989719));
#416910=CARTESIAN_POINT('',(-0.917491840287428,-2.59243297367666,14.));
#416911=CARTESIAN_POINT('Ctrl Pts',(-0.950539831569773,-2.58049879453553,
12.4908873016278));
#416912=CARTESIAN_POINT('Ctrl Pts',(-0.948492954963315,-2.58125277192504,
12.4908873016278));
#416913=CARTESIAN_POINT('Ctrl Pts',(-0.946433624613375,-2.58200851205192,
12.4911020829134));
#416914=CARTESIAN_POINT('Ctrl Pts',(-0.944427623874041,-2.58274204350021,
12.4915448903141));
#416915=CARTESIAN_POINT('Ctrl Pts',(-0.940995601057367,-2.58399702642117,
12.4923024798169));
#416916=CARTESIAN_POINT('Ctrl Pts',(-0.937640773983089,-2.58521557752243,
12.4937722312795));
#416917=CARTESIAN_POINT('Ctrl Pts',(-0.934696155984694,-2.58627977913981,
12.4958030942394));
#416918=CARTESIAN_POINT('Ctrl Pts',(-0.931772322093767,-2.58733646926306,
12.4978196226833));
#416919=CARTESIAN_POINT('Ctrl Pts',(-0.929166358104517,-2.58827260881446,
12.5004326847668));
#416920=CARTESIAN_POINT('Ctrl Pts',(-0.927015645536167,-2.58904267885471,
12.5033504258767));
#416921=CARTESIAN_POINT('Ctrl Pts',(-0.924445923911998,-2.58996277653009,
12.5068366111226));
#416922=CARTESIAN_POINT('Ctrl Pts',(-0.922443527872953,-2.59067565328286,
12.5108395010833));
#416923=CARTESIAN_POINT('Ctrl Pts',(-0.92098299759068,-2.59119476654089,
12.5149868989719));
#416924=CARTESIAN_POINT('Ctrl Pts',(-0.918529897733577,-2.59206666675038,
12.5219528491417));
#416925=CARTESIAN_POINT('Ctrl Pts',(-0.917491840251216,-2.59243297368978,
12.5295503425868));
#416926=CARTESIAN_POINT('Ctrl Pts',(-0.917491840287428,-2.59243297367666,
12.5369868989719));
#416927=CARTESIAN_POINT('',(-1.05630099730985,-2.53904080374503,12.5369868989719));
#416928=CARTESIAN_POINT('Ctrl Pts',(-1.05630099730985,-2.53904080374503,
12.5369868989719));
#416929=CARTESIAN_POINT('Ctrl Pts',(-1.05630099730984,-2.53904080374503,
12.5309445149785));
#416930=CARTESIAN_POINT('Ctrl Pts',(-1.0556328436035,-2.53931920877903,
12.5248274368704));
#416931=CARTESIAN_POINT('Ctrl Pts',(-1.05410270687713,-2.53995422859434,
12.5190199595513));
#416932=CARTESIAN_POINT('Ctrl Pts',(-1.05281748803561,-2.54048760539481,
12.5141420429941));
#416933=CARTESIAN_POINT('Ctrl Pts',(-1.05088442725141,-2.54128909317358,
12.5093757677094));
#416934=CARTESIAN_POINT('Ctrl Pts',(-1.04821541997559,-2.54238951251089,
12.5051960112707));
#416935=CARTESIAN_POINT('Ctrl Pts',(-1.04643233911201,-2.54312466849194,
12.5024036458141));
#416936=CARTESIAN_POINT('Ctrl Pts',(-1.04427749628486,-2.54401091322224,
12.4998248032393));
#416937=CARTESIAN_POINT('Ctrl Pts',(-1.04182619094233,-2.5450143787151,
12.4976950015772));
#416938=CARTESIAN_POINT('Ctrl Pts',(-1.03930581769944,-2.54604611781934,
12.495505190692));
#416939=CARTESIAN_POINT('Ctrl Pts',(-1.03640697452017,-2.54722818906695,
12.4937456938368));
#416940=CARTESIAN_POINT('Ctrl Pts',(-1.03335246572261,-2.54846673150445,
12.4925987732155));
#416941=CARTESIAN_POINT('Ctrl Pts',(-1.03029867166833,-2.5497049841278,
12.4914521209692));
#416942=CARTESIAN_POINT('Ctrl Pts',(-1.02701309623813,-2.5510304348241,
12.4908873016276));
#416943=CARTESIAN_POINT('Ctrl Pts',(-1.02377407177521,-2.55232965150679,
12.4908873016278));
#416944=CARTESIAN_POINT('',(-1.05630099730985,-2.53904080374503,13.7435492065112));
#416945=CARTESIAN_POINT('',(-1.05630099730985,-2.53904080374504,14.));
#416946=CARTESIAN_POINT('',(-1.12574631620479,-2.50902276425531,13.7435492065112));
#416947=CARTESIAN_POINT('Origin',(0.,2.5406128344257E-15,13.7435492065112));
#416948=CARTESIAN_POINT('',(-1.12574631620479,-2.50902276425531,12.5369868989719));
#416949=CARTESIAN_POINT('',(-1.12574631620479,-2.50902276425531,14.));
#416950=CARTESIAN_POINT('Ctrl Pts',(-1.15771159663089,-2.49443457701868,
12.4908873016278));
#416951=CARTESIAN_POINT('Ctrl Pts',(-1.15573298699432,-2.49535288505633,
12.4908873016278));
#416952=CARTESIAN_POINT('Ctrl Pts',(-1.15374210873252,-2.49627396506169,
12.4911020829134));
#416953=CARTESIAN_POINT('Ctrl Pts',(-1.15180257241798,-2.49716856342766,
12.4915448903141));
#416954=CARTESIAN_POINT('Ctrl Pts',(-1.14848426213285,-2.49869911221738,
12.4923024798169));
#416955=CARTESIAN_POINT('Ctrl Pts',(-1.14523992119614,-2.50018705824162,
12.4937722312795));
#416956=CARTESIAN_POINT('Ctrl Pts',(-1.1423918434826,-2.50148773251928,
12.4958030942394));
#416957=CARTESIAN_POINT('Ctrl Pts',(-1.13956386846263,-2.50277922619898,
12.4978196226833));
#416958=CARTESIAN_POINT('Ctrl Pts',(-1.13704287966771,-2.50392466108096,
12.5004326847668));
#416959=CARTESIAN_POINT('Ctrl Pts',(-1.13496209127527,-2.50486747181724,
12.5033504258767));
#416960=CARTESIAN_POINT('Ctrl Pts',(-1.13247591669013,-2.50599396411201,
12.5068366111226));
#416961=CARTESIAN_POINT('Ctrl Pts',(-1.1305382895321,-2.50686768269271,
12.5108395010833));
#416962=CARTESIAN_POINT('Ctrl Pts',(-1.12912493159359,-2.5075041154211,
12.5149868989719));
#416963=CARTESIAN_POINT('Ctrl Pts',(-1.1267510621853,-2.5085730648664,12.5219528491417));
#416964=CARTESIAN_POINT('Ctrl Pts',(-1.12574631616977,-2.50902276427134,
12.5295503425868));
#416965=CARTESIAN_POINT('Ctrl Pts',(-1.12574631620479,-2.50902276425531,
12.5369868989719));
#416966=CARTESIAN_POINT('',(-1.25974163969002,-2.44449401742592,12.5369868989719));
#416967=CARTESIAN_POINT('Ctrl Pts',(-1.25974163969001,-2.44449401742592,
12.5369868989719));
#416968=CARTESIAN_POINT('Ctrl Pts',(-1.25974163969001,-2.44449401742592,
12.5309445149785));
#416969=CARTESIAN_POINT('Ctrl Pts',(-1.25909840180486,-2.44482595682003,
12.5248274368704));
#416970=CARTESIAN_POINT('Ctrl Pts',(-1.25762511649241,-2.4455835840076,
12.5190199595513));
#416971=CARTESIAN_POINT('Ctrl Pts',(-1.25638764927142,-2.44621994330773,
12.5141420429941));
#416972=CARTESIAN_POINT('Ctrl Pts',(-1.25452634928214,-2.44717632660161,
12.5093757677094));
#416973=CARTESIAN_POINT('Ctrl Pts',(-1.25195591729964,-2.44849063325519,
12.5051960112707));
#416974=CARTESIAN_POINT('Ctrl Pts',(-1.25023869152784,-2.44936868070905,
12.5024036458141));
#416975=CARTESIAN_POINT('Ctrl Pts',(-1.24816325593546,-2.45042761622812,
12.4998248032393));
#416976=CARTESIAN_POINT('Ctrl Pts',(-1.24580189886262,-2.45162754691455,
12.4976950015772));
#416977=CARTESIAN_POINT('Ctrl Pts',(-1.24337400826898,-2.45286128680934,
12.495505190692));
#416978=CARTESIAN_POINT('Ctrl Pts',(-1.24058116053174,-2.45427570744305,
12.4937456938368));
#416979=CARTESIAN_POINT('Ctrl Pts',(-1.23763776806695,-2.45575909955644,
12.4925987732155));
#416980=CARTESIAN_POINT('Ctrl Pts',(-1.23469506434464,-2.45724214456179,
12.4914521209692));
#416981=CARTESIAN_POINT('Ctrl Pts',(-1.23152845793228,-2.4588309898296,
12.4908873016276));
#416982=CARTESIAN_POINT('Ctrl Pts',(-1.22840610927704,-2.46038989403932,
12.4908873016278));
#416983=CARTESIAN_POINT('',(-1.25974163969001,-2.44449401742592,13.7435492065112));
#416984=CARTESIAN_POINT('',(-1.25974163969001,-2.44449401742592,14.));
#416985=CARTESIAN_POINT('',(-1.32650913612287,-2.40891542229746,13.7435492065112));
#416986=CARTESIAN_POINT('Origin',(0.,2.5406128344257E-15,13.7435492065112));
#416987=CARTESIAN_POINT('',(-1.32650913612287,-2.40891542229746,12.5369868989719));
#416988=CARTESIAN_POINT('',(-1.32650913612287,-2.40891542229746,14.));
#416989=CARTESIAN_POINT('Ctrl Pts',(-1.3571789820254,-2.39177030894451,
12.4908873016278));
#416990=CARTESIAN_POINT('Ctrl Pts',(-1.35528180667939,-2.39284683644181,
12.4908873016278));
#416991=CARTESIAN_POINT('Ctrl Pts',(-1.3533726294721,-2.39392712669018,
12.4911020829134));
#416992=CARTESIAN_POINT('Ctrl Pts',(-1.35151246487652,-2.3949768385693,
12.4915448903141));
#416993=CARTESIAN_POINT('Ctrl Pts',(-1.34832994993041,-2.39677276767812,
12.4923024798169));
#416994=CARTESIAN_POINT('Ctrl Pts',(-1.34521768568492,-2.39852020659005,
12.4937722312795));
#416995=CARTESIAN_POINT('Ctrl Pts',(-1.34248510174352,-2.40004869775525,
12.4958030942394));
#416996=CARTESIAN_POINT('Ctrl Pts',(-1.33977180530167,-2.40156640031404,
12.4978196226833));
#416997=CARTESIAN_POINT('Ctrl Pts',(-1.33735256846558,-2.40291350784645,
12.5004326847668));
#416998=CARTESIAN_POINT('Ctrl Pts',(-1.3353555515525,-2.40402278502886,
12.5033504258767));
#416999=CARTESIAN_POINT('Ctrl Pts',(-1.33296946908807,-2.40534817532266,
12.5068366111226));
#417000=CARTESIAN_POINT('Ctrl Pts',(-1.33110950540009,-2.4063769212783,
12.5108395010833));
#417001=CARTESIAN_POINT('Ctrl Pts',(-1.32975272546925,-2.40712643812225,
12.5149868989719));
#417002=CARTESIAN_POINT('Ctrl Pts',(-1.32747388421902,-2.40838532312115,
12.5219528491417));
#417003=CARTESIAN_POINT('Ctrl Pts',(-1.32650913608927,-2.40891542231629,
12.5295503425868));
#417004=CARTESIAN_POINT('Ctrl Pts',(-1.32650913612287,-2.40891542229746,
12.5369868989719));
#417005=CARTESIAN_POINT('',(-1.45479890930079,-2.33367952673396,12.5369868989719));
#417006=CARTESIAN_POINT('Ctrl Pts',(-1.45479890930078,-2.33367952673396,
12.5369868989719));
#417007=CARTESIAN_POINT('Ctrl Pts',(-1.45479890930078,-2.33367952673396,
12.5309445149785));
#417008=CARTESIAN_POINT('Ctrl Pts',(-1.45418486787883,-2.33406279148629,
12.5248274368704));
#417009=CARTESIAN_POINT('Ctrl Pts',(-1.45277823845097,-2.33493798416217,
12.5190199595513));
#417010=CARTESIAN_POINT('Ctrl Pts',(-1.45159675799071,-2.33567309109583,
12.5141420429941));
#417011=CARTESIAN_POINT('Ctrl Pts',(-1.44981960544068,-2.33677800533178,
12.5093757677094));
#417012=CARTESIAN_POINT('Ctrl Pts',(-1.44736485455224,-2.33829745280769,
12.5051960112707));
#417013=CARTESIAN_POINT('Ctrl Pts',(-1.44572491172643,-2.33931254847343,
12.5024036458141));
#417014=CARTESIAN_POINT('Ctrl Pts',(-1.44374269505025,-2.34053712774011,
12.4998248032393));
#417015=CARTESIAN_POINT('Ctrl Pts',(-1.44148700068882,-2.34192553827937,
12.4976950015772));
#417016=CARTESIAN_POINT('Ctrl Pts',(-1.43916774995576,-2.34335306862925,
12.495505190692));
#417017=CARTESIAN_POINT('Ctrl Pts',(-1.43649948360146,-2.3449904259131,
12.4937456938368));
#417018=CARTESIAN_POINT('Ctrl Pts',(-1.43368679526066,-2.34670879597261,
12.4925987732155));
#417019=CARTESIAN_POINT('Ctrl Pts',(-1.43087476507809,-2.34842676394015,
12.4914521209692));
#417020=CARTESIAN_POINT('Ctrl Pts',(-1.42784820092678,-2.35026843027634,
12.4908873016276));
#417021=CARTESIAN_POINT('Ctrl Pts',(-1.42486330679437,-2.35207664776278,
12.4908873016278));
#417022=CARTESIAN_POINT('',(-1.45479890930078,-2.33367952673396,13.7435492065112));
#417023=CARTESIAN_POINT('',(-1.45479890930078,-2.33367952673396,14.));
#417024=CARTESIAN_POINT('',(-1.51844425659866,-2.29277714564729,13.7435492065112));
#417025=CARTESIAN_POINT('Origin',(0.,2.5406128344257E-15,13.7435492065112));
#417026=CARTESIAN_POINT('',(-1.51844425659866,-2.29277714564729,12.5369868989719));
#417027=CARTESIAN_POINT('',(-1.51844425659866,-2.29277714564729,14.));
#417028=CARTESIAN_POINT('Ctrl Pts',(-1.5476145652133,-2.27318920407863,
12.4908873016278));
#417029=CARTESIAN_POINT('Ctrl Pts',(-1.54581144954677,-2.27441678692272,
12.4908873016278));
#417030=CARTESIAN_POINT('Ctrl Pts',(-1.54399667865332,-2.27564909826073,
12.4911020829134));
#417031=CARTESIAN_POINT('Ctrl Pts',(-1.54222826486516,-2.27684693799364,
12.4915448903141));
#417032=CARTESIAN_POINT('Ctrl Pts',(-1.53920272436996,-2.27889629580963,
12.4923024798169));
#417033=CARTESIAN_POINT('Ctrl Pts',(-1.53624324842076,-2.28089159869159,
12.4937722312795));
#417034=CARTESIAN_POINT('Ctrl Pts',(-1.53364434314679,-2.28263773488783,
12.4958030942394));
#417035=CARTESIAN_POINT('Ctrl Pts',(-1.53106378182322,-2.28437154626559,
12.4978196226833));
#417036=CARTESIAN_POINT('Ctrl Pts',(-1.52876239656796,-2.28591136167005,
12.5004326847668));
#417037=CARTESIAN_POINT('Ctrl Pts',(-1.52686244095231,-2.28717972324196,
12.5033504258767));
#417038=CARTESIAN_POINT('Ctrl Pts',(-1.5245923295937,-2.28869519128105,
12.5068366111226));
#417039=CARTESIAN_POINT('Ctrl Pts',(-1.52282240712726,-2.28987211847702,
12.5108395010833));
#417040=CARTESIAN_POINT('Ctrl Pts',(-1.52153123435067,-2.2907297315256,
12.5149868989719));
#417041=CARTESIAN_POINT('Ctrl Pts',(-1.51936258657103,-2.29217017440614,
12.5219528491417));
#417042=CARTESIAN_POINT('Ctrl Pts',(-1.51844425656671,-2.2927771456688,
12.5295503425868));
#417043=CARTESIAN_POINT('Ctrl Pts',(-1.51844425659866,-2.29277714564729,
12.5369868989719));
#417044=CARTESIAN_POINT('',(-1.64017473219509,-2.20733478382161,12.5369868989719));
#417045=CARTESIAN_POINT('Ctrl Pts',(-1.64017473219508,-2.20733478382161,
12.5369868989719));
#417046=CARTESIAN_POINT('Ctrl Pts',(-1.64017473219508,-2.20733478382161,
12.5309445149785));
#417047=CARTESIAN_POINT('Ctrl Pts',(-1.63959397358067,-2.20776682336847,
12.5248274368704));
#417048=CARTESIAN_POINT('Ctrl Pts',(-1.63826336092418,-2.20875375726979,
12.5190199595513));
#417049=CARTESIAN_POINT('Ctrl Pts',(-1.63714572978217,-2.20958271982161,
12.5141420429941));
#417050=CARTESIAN_POINT('Ctrl Pts',(-1.6354645513284,-2.2108288119777,12.5093757677094));
#417051=CARTESIAN_POINT('Ctrl Pts',(-1.63314181749619,-2.21254328860369,
12.5051960112707));
#417052=CARTESIAN_POINT('Ctrl Pts',(-1.63159007116529,-2.21368867718713,
12.5024036458141));
#417053=CARTESIAN_POINT('Ctrl Pts',(-1.62971426473026,-2.21507075082842,
12.4998248032393));
#417054=CARTESIAN_POINT('Ctrl Pts',(-1.62757924435406,-2.21663840157745,
12.4976950015772));
#417055=CARTESIAN_POINT('Ctrl Pts',(-1.62538406771255,-2.21825022240348,
12.495505190692));
#417056=CARTESIAN_POINT('Ctrl Pts',(-1.62285813961354,-2.22009961999489,
12.4937456938368));
#417057=CARTESIAN_POINT('Ctrl Pts',(-1.62019487337358,-2.22204153253128,
12.4925987732155));
#417058=CARTESIAN_POINT('Ctrl Pts',(-1.61753223032766,-2.22398299066762,
12.4914521209692));
#417059=CARTESIAN_POINT('Ctrl Pts',(-1.61466584972249,-2.22606522208659,
12.4908873016276));
#417060=CARTESIAN_POINT('Ctrl Pts',(-1.61183827409089,-2.2281107194607,
12.4908873016278));
#417061=CARTESIAN_POINT('',(-1.64017473219508,-2.20733478382161,13.7435492065112));
#417062=CARTESIAN_POINT('',(-1.64017473219508,-2.20733478382161,14.));
#417063=CARTESIAN_POINT('',(-1.70027438107246,-2.16138081537444,13.7435492065112));
#417064=CARTESIAN_POINT('Origin',(0.,2.5406128344257E-15,13.7435492065112));
#417065=CARTESIAN_POINT('',(-1.70027438107246,-2.16138081537444,12.5369868989719));
#417066=CARTESIAN_POINT('',(-1.70027438107246,-2.16138081537444,14.));
#417067=CARTESIAN_POINT('Ctrl Pts',(-1.72775102880814,-2.13948040010943,
12.4908873016278));
#417068=CARTESIAN_POINT('Ctrl Pts',(-1.72605397225836,-2.140850868939,12.4908873016278));
#417069=CARTESIAN_POINT('Ctrl Pts',(-1.72434568467961,-2.14222700053803,
12.4911020829134));
#417070=CARTESIAN_POINT('Ctrl Pts',(-1.72268079020089,-2.14356499669892,
12.4915448903141));
#417071=CARTESIAN_POINT('Ctrl Pts',(-1.71983235862941,-2.14585414508395,
12.4923024798169));
#417072=CARTESIAN_POINT('Ctrl Pts',(-1.71704536580065,-2.14808403352447,
12.4937722312795));
#417073=CARTESIAN_POINT('Ctrl Pts',(-1.71459743447992,-2.15003619450345,
12.4958030942394));
#417074=CARTESIAN_POINT('Ctrl Pts',(-1.71216678148448,-2.15197457647151,
12.4978196226833));
#417075=CARTESIAN_POINT('Ctrl Pts',(-1.70999856314922,-2.15369685253056,
12.5004326847668));
#417076=CARTESIAN_POINT('Ctrl Pts',(-1.70820831272215,-2.15511585775498,
12.5033504258767));
#417077=CARTESIAN_POINT('Ctrl Pts',(-1.70606927968592,-2.1568113183496,
12.5068366111226));
#417078=CARTESIAN_POINT('Ctrl Pts',(-1.70440117698301,-2.15812859452958,
12.5108395010833));
#417079=CARTESIAN_POINT('Ctrl Pts',(-1.70318420390247,-2.15908859650944,
12.5149868989719));
#417080=CARTESIAN_POINT('Ctrl Pts',(-1.7011401815866,-2.16070101136191,
12.5219528491417));
#417081=CARTESIAN_POINT('Ctrl Pts',(-1.70027438104236,-2.16138081539848,
12.5295503425868));
#417082=CARTESIAN_POINT('Ctrl Pts',(-1.70027438107246,-2.16138081537444,
12.5369868989719));
#417083=CARTESIAN_POINT('',(-1.81463546285641,-2.06630059210753,12.5369868989719));
#417084=CARTESIAN_POINT('Ctrl Pts',(-1.81463546285641,-2.06630059210752,
12.5369868989719));
#417085=CARTESIAN_POINT('Ctrl Pts',(-1.8146354628564,-2.06630059210752,
12.5309445149785));
#417086=CARTESIAN_POINT('Ctrl Pts',(-1.81409185190231,-2.06677853129701,
12.5248274368704));
#417087=CARTESIAN_POINT('Ctrl Pts',(-1.81284611102486,-2.0678706385415,
12.5190199595513));
#417088=CARTESIAN_POINT('Ctrl Pts',(-1.81179976685197,-2.06878794010247,
12.5141420429941));
#417089=CARTESIAN_POINT('Ctrl Pts',(-1.81022575045969,-2.07016691764099,
12.5093757677094));
#417090=CARTESIAN_POINT('Ctrl Pts',(-1.80805049109414,-2.07206501385797,
12.5051960112707));
#417091=CARTESIAN_POINT('Ctrl Pts',(-1.80659726787397,-2.07333307298707,
12.5024036458141));
#417092=CARTESIAN_POINT('Ctrl Pts',(-1.80484035486241,-2.07486344353092,
12.4998248032393));
#417093=CARTESIAN_POINT('Ctrl Pts',(-1.8028402166798,-2.07659990203263,
12.4976950015772));
#417094=CARTESIAN_POINT('Ctrl Pts',(-1.8007837226682,-2.07838528693313,
12.495505190692));
#417095=CARTESIAN_POINT('Ctrl Pts',(-1.79841694245924,-2.08043441739626,
12.4937456938368));
#417096=CARTESIAN_POINT('Ctrl Pts',(-1.79592082191755,-2.082586949302,12.4925987732155));
#417097=CARTESIAN_POINT('Ctrl Pts',(-1.79342528545844,-2.08473897752356,
12.4914521209692));
#417098=CARTESIAN_POINT('Ctrl Pts',(-1.7907381636894,-2.08704791711876,
12.4908873016276));
#417099=CARTESIAN_POINT('Ctrl Pts',(-1.78808672360792,-2.08931708193301,
12.4908873016278));
#417100=CARTESIAN_POINT('',(-1.81463546285641,-2.06630059210753,13.7435492065112));
#417101=CARTESIAN_POINT('',(-1.81463546285641,-2.06630059210753,14.));
#417102=CARTESIAN_POINT('',(-1.87078946006574,-2.01560085237801,13.7435492065112));
#417103=CARTESIAN_POINT('Origin',(0.,2.5406128344257E-15,13.7435492065112));
#417104=CARTESIAN_POINT('',(-1.87078946006574,-2.01560085237801,12.5369868989719));
#417105=CARTESIAN_POINT('',(-1.87078946006574,-2.01560085237801,14.));
#417106=CARTESIAN_POINT('Ctrl Pts',(-1.89638959436511,-1.99153370706693,
12.4908873016278));
#417107=CARTESIAN_POINT('Ctrl Pts',(-1.89480989056343,-1.99303794163803,
12.4908873016278));
#417108=CARTESIAN_POINT('Ctrl Pts',(-1.89321945467138,-1.99454873556932,
12.4911020829134));
#417109=CARTESIAN_POINT('Ctrl Pts',(-1.89166915910015,-1.99601798401451,
12.4915448903141));
#417110=CARTESIAN_POINT('Ctrl Pts',(-1.88901679229454,-1.99853168906375,
12.4923024798169));
#417111=CARTESIAN_POINT('Ctrl Pts',(-1.88642082956369,-2.00098132352316,
12.4937722312795));
#417112=CARTESIAN_POINT('Ctrl Pts',(-1.88414016277525,-2.00312651797565,
12.4958030942394));
#417113=CARTESIAN_POINT('Ctrl Pts',(-1.8818755937026,-2.00525657092182,
12.4978196226833));
#417114=CARTESIAN_POINT('Ctrl Pts',(-1.87985497142262,-2.00714984617245,
12.5004326847668));
#417115=CARTESIAN_POINT('Ctrl Pts',(-1.87818634000535,-2.00871005180372,
12.5033504258767));
#417116=CARTESIAN_POINT('Ctrl Pts',(-1.87619262020345,-2.01057422194334,
12.5068366111226));
#417117=CARTESIAN_POINT('Ctrl Pts',(-1.87463743821233,-2.01202308085171,
12.5108395010833));
#417118=CARTESIAN_POINT('Ctrl Pts',(-1.87350276358291,-2.01307908310806,
12.5149868989719));
#417119=CARTESIAN_POINT('Ctrl Pts',(-1.87159696936208,-2.01485273957765,
12.5219528491417));
#417120=CARTESIAN_POINT('Ctrl Pts',(-1.87078946003771,-2.01560085240442,
12.5295503425868));
#417121=CARTESIAN_POINT('Ctrl Pts',(-1.87078946006574,-2.01560085237801,
12.5369868989719));
#417122=CARTESIAN_POINT('',(-1.9770200939062,-1.91151551086857,12.5369868989719));
#417123=CARTESIAN_POINT('Ctrl Pts',(-1.9770200939062,-1.91151551086857,
12.5369868989719));
#417124=CARTESIAN_POINT('Ctrl Pts',(-1.9770200939062,-1.91151551086857,
12.5309445149785));
#417125=CARTESIAN_POINT('Ctrl Pts',(-1.97651724825362,-1.91203616909422,
12.5248274368704));
#417126=CARTESIAN_POINT('Ctrl Pts',(-1.97536466935523,-1.91322618188836,
12.5190199595513));
#417127=CARTESIAN_POINT('Ctrl Pts',(-1.97439657539929,-1.91422571796793,
12.5141420429941));
#417128=CARTESIAN_POINT('Ctrl Pts',(-1.9729401958879,-1.91572840402087,
12.5093757677094));
#417129=CARTESIAN_POINT('Ctrl Pts',(-1.97092688698119,-1.91779748831169,
12.5051960112707));
#417130=CARTESIAN_POINT('Ctrl Pts',(-1.96958185783251,-1.91917977926215,
12.5024036458141));
#417131=CARTESIAN_POINT('Ctrl Pts',(-1.96795553021065,-1.9208482623451,
12.4998248032393));
#417132=CARTESIAN_POINT('Ctrl Pts',(-1.96610358481123,-1.92274197275465,
12.4976950015772));
#417133=CARTESIAN_POINT('Ctrl Pts',(-1.9641994590579,-1.92468904028768,
12.495505190692));
#417134=CARTESIAN_POINT('Ctrl Pts',(-1.96200757727078,-1.92692426699738,
12.4937456938368));
#417135=CARTESIAN_POINT('Ctrl Pts',(-1.95969521369772,-1.92927309352777,
12.4925987732155));
#417136=CARTESIAN_POINT('Ctrl Pts',(-1.95738339120883,-1.93162137044181,
12.4914521209692));
#417137=CARTESIAN_POINT('Ctrl Pts',(-1.95489341062797,-1.93414165260117,
12.4908873016276));
#417138=CARTESIAN_POINT('Ctrl Pts',(-1.95243575099289,-1.93661938393811,
12.4908873016278));
#417139=CARTESIAN_POINT('',(-1.9770200939062,-1.91151551086857,13.7435492065112));
#417140=CARTESIAN_POINT('',(-1.9770200939062,-1.91151551086857,14.));
#417141=CARTESIAN_POINT('',(-2.02885474386082,-1.85640739825973,13.7435492065112));
#417142=CARTESIAN_POINT('Origin',(0.,2.5406128344257E-15,13.7435492065112));
#417143=CARTESIAN_POINT('',(-2.02885474386082,-1.85640739825973,12.5369868989719));
#417144=CARTESIAN_POINT('',(-2.02885474386082,-1.85640739825973,14.));
#417145=CARTESIAN_POINT('Ctrl Pts',(-2.05240800005384,-1.83033368578382,
12.4908873016278));
#417146=CARTESIAN_POINT('Ctrl Pts',(-2.05095616166842,-1.83196167566357,
12.4908873016278));
#417147=CARTESIAN_POINT('Ctrl Pts',(-2.04949416155152,-1.83359707784278,
12.4911020829134));
#417148=CARTESIAN_POINT('Ctrl Pts',(-2.04806878184904,-1.83518780096627,
12.4915448903141));
#417149=CARTESIAN_POINT('Ctrl Pts',(-2.04563013087279,-1.83790933438735,
12.4923024798169));
#417150=CARTESIAN_POINT('Ctrl Pts',(-2.04324247394351,-1.84056241295248,
12.4937722312795));
#417151=CARTESIAN_POINT('Ctrl Pts',(-2.04114424914856,-1.84288636496334,
12.4958030942394));
#417152=CARTESIAN_POINT('Ctrl Pts',(-2.03906083433224,-1.8451939137367,
12.4978196226833));
#417153=CARTESIAN_POINT('Ctrl Pts',(-2.03720125501545,-1.84724558874448,
12.5004326847668));
#417154=CARTESIAN_POINT('Ctrl Pts',(-2.03566534707476,-1.84893661187154,
12.5033504258767));
#417155=CARTESIAN_POINT('Ctrl Pts',(-2.03383020838352,-1.85095708581146,
12.5068366111226));
#417156=CARTESIAN_POINT('Ctrl Pts',(-2.03239829658376,-1.8525278855312,
12.5108395010833));
#417157=CARTESIAN_POINT('Ctrl Pts',(-2.0313534714779,-1.85367286054327,
12.5149868989719));
#417158=CARTESIAN_POINT('Ctrl Pts',(-2.02959858809823,-1.8555959552388,
12.5219528491417));
#417159=CARTESIAN_POINT('Ctrl Pts',(-2.02885474383503,-1.85640739828834,
12.5295503425868));
#417160=CARTESIAN_POINT('Ctrl Pts',(-2.02885474386082,-1.85640739825973,
12.5369868989719));
#417161=CARTESIAN_POINT('',(-2.1262479824164,-1.74400960928264,12.5369868989719));
#417162=CARTESIAN_POINT('Ctrl Pts',(-2.1262479824164,-1.74400960928264,
12.5369868989719));
#417163=CARTESIAN_POINT('Ctrl Pts',(-2.1262479824164,-1.74400960928264,
12.5309445149785));
#417164=CARTESIAN_POINT('Ctrl Pts',(-2.12578924842019,-1.74456952164988,
12.5248274368704));
#417165=CARTESIAN_POINT('Ctrl Pts',(-2.12473750172327,-1.74584952065485,
12.5190199595513));
#417166=CARTESIAN_POINT('Ctrl Pts',(-2.12385410048983,-1.74692463950532,
12.5141420429941));
#417167=CARTESIAN_POINT('Ctrl Pts',(-2.12252504982469,-1.74854103394493,
12.5093757677094));
#417168=CARTESIAN_POINT('Ctrl Pts',(-2.12068708961543,-1.750767336895,12.5051960112707));
#417169=CARTESIAN_POINT('Ctrl Pts',(-2.11945920548531,-1.75225466074862,
12.5024036458141));
#417170=CARTESIAN_POINT('Ctrl Pts',(-2.11797428619515,-1.75405015289102,
12.4998248032393));
#417171=CARTESIAN_POINT('Ctrl Pts',(-2.11628285796999,-1.75608851287808,
12.4976950015772));
#417172=CARTESIAN_POINT('Ctrl Pts',(-2.11454377211767,-1.75818430563045,
12.495505190692));
#417173=CARTESIAN_POINT('Ctrl Pts',(-2.11254137536405,-1.76059075352176,
12.4937456938368));
#417174=CARTESIAN_POINT('Ctrl Pts',(-2.1104281571577,-1.76312024362377,
12.4925987732155));
#417175=CARTESIAN_POINT('Ctrl Pts',(-2.10831543343625,-1.76564914183486,
12.4914521209692));
#417176=CARTESIAN_POINT('Ctrl Pts',(-2.10603916445351,-1.76836399449644,
12.4908873016276));
#417177=CARTESIAN_POINT('Ctrl Pts',(-2.10379164058422,-1.7710338034628,
12.4908873016278));
#417178=CARTESIAN_POINT('',(-2.1262479824164,-1.74400960928264,13.7435492065112));
#417179=CARTESIAN_POINT('',(-2.1262479824164,-1.74400960928264,14.));
#417180=CARTESIAN_POINT('',(-2.17341833407298,-1.68485985919169,13.7435492065112));
#417181=CARTESIAN_POINT('Origin',(0.,2.5406128344257E-15,13.7435492065112));
#417182=CARTESIAN_POINT('',(-2.17341833407298,-1.6848598591917,12.5369868989719));
#417183=CARTESIAN_POINT('',(-2.17341833407298,-1.6848598591917,14.));
#417184=CARTESIAN_POINT('Ctrl Pts',(-2.1947679691257,-1.65695309580563,
12.4908873016278));
#417185=CARTESIAN_POINT('Ctrl Pts',(-2.19345365790146,-1.65869400698998,
12.4908873016278));
#417186=CARTESIAN_POINT('Ctrl Pts',(-2.19212982292928,-1.66044313408541,
12.4911020829134));
#417187=CARTESIAN_POINT('Ctrl Pts',(-2.19083884476229,-1.66214474588727,
12.4915448903141));
#417188=CARTESIAN_POINT('Ctrl Pts',(-2.18863013843529,-1.6650559963243,
12.4923024798169));
#417189=CARTESIAN_POINT('Ctrl Pts',(-2.18646667677051,-1.66789486319503,
12.4937722312795));
#417190=CARTESIAN_POINT('Ctrl Pts',(-2.18456485730888,-1.67038210724704,
12.4958030942394));
#417191=CARTESIAN_POINT('Ctrl Pts',(-2.18267646153076,-1.67285179549123,
12.4978196226833));
#417192=CARTESIAN_POINT('Ctrl Pts',(-2.18099030037069,-1.67504821669748,
12.5004326847668));
#417193=CARTESIAN_POINT('Ctrl Pts',(-2.17959733712052,-1.67685880384043,
12.5033504258767));
#417194=CARTESIAN_POINT('Ctrl Pts',(-2.17793299208515,-1.67902213565991,
12.5068366111226));
#417195=CARTESIAN_POINT('Ctrl Pts',(-2.17663387961354,-1.68070442277808,
12.5108395010833));
#417196=CARTESIAN_POINT('Ctrl Pts',(-2.17568585716995,-1.68193075092606,
12.5149868989719));
#417197=CARTESIAN_POINT('Ctrl Pts',(-2.17409356309077,-1.68399048596961,
12.5219528491417));
#417198=CARTESIAN_POINT('Ctrl Pts',(-2.17341833404961,-1.68485985922231,
12.5295503425868));
#417199=CARTESIAN_POINT('Ctrl Pts',(-2.17341833407298,-1.6848598591917,
12.5369868989719));
#417200=CARTESIAN_POINT('',(-2.26132604140984,-1.56489761148827,12.5369868989719));
#417201=CARTESIAN_POINT('Ctrl Pts',(-2.26132604140984,-1.56489761148827,
12.5369868989719));
#417202=CARTESIAN_POINT('Ctrl Pts',(-2.26132604140984,-1.56489761148827,
12.5309445149785));
#417203=CARTESIAN_POINT('Ctrl Pts',(-2.26091447186907,-1.56549305187266,
12.5248274368704));
#417204=CARTESIAN_POINT('Ctrl Pts',(-2.25997055657435,-1.56685451890628,
12.5190199595513));
#417205=CARTESIAN_POINT('Ctrl Pts',(-2.25917772695287,-1.56799806578909,
12.5141420429941));
#417206=CARTESIAN_POINT('Ctrl Pts',(-2.25798484974689,-1.56971741177706,
12.5093757677094));
#417207=CARTESIAN_POINT('Ctrl Pts',(-2.25633446955702,-1.57208611770757,
12.5051960112707));
#417208=CARTESIAN_POINT('Ctrl Pts',(-2.25523190181175,-1.57366857656948,
12.5024036458141));
#417209=CARTESIAN_POINT('Ctrl Pts',(-2.25389827274618,-1.57557912906736,
12.4998248032393));
#417210=CARTESIAN_POINT('Ctrl Pts',(-2.25237861787107,-1.57774857368252,
12.4976950015772));
#417211=CARTESIAN_POINT('Ctrl Pts',(-2.25081614524916,-1.57997914449925,
12.495505190692));
#417212=CARTESIAN_POINT('Ctrl Pts',(-2.24901655914907,-1.58254079905848,
12.4937456938368));
#417213=CARTESIAN_POINT('Ctrl Pts',(-2.24711654942792,-1.58523411939283,
12.4925987732155));
#417214=CARTESIAN_POINT('Ctrl Pts',(-2.24521698430172,-1.5879268095006,
12.4914521209692));
#417215=CARTESIAN_POINT('Ctrl Pts',(-2.24316957511162,-1.59081816576785,
12.4908873016276));
#417216=CARTESIAN_POINT('Ctrl Pts',(-2.24114714390866,-1.59366228522547,
12.4908873016278));
#417217=CARTESIAN_POINT('',(-2.26132604140984,-1.56489761148827,13.7435492065112));
#417218=CARTESIAN_POINT('',(-2.26132604140984,-1.56489761148827,14.));
#417219=CARTESIAN_POINT('',(-2.30351818386066,-1.50209985574305,13.7435492065112));
#417220=CARTESIAN_POINT('Origin',(0.,2.5406128344257E-15,13.7435492065112));
#417221=CARTESIAN_POINT('',(-2.30351818386066,-1.50209985574305,12.5369868989719));
#417222=CARTESIAN_POINT('',(-2.30351818386066,-1.50209985574305,14.));
#417223=CARTESIAN_POINT('Ctrl Pts',(-2.32252211947425,-1.47254575635286,
12.4908873016278));
#417224=CARTESIAN_POINT('Ctrl Pts',(-2.32135408193554,-1.47438800336511,
12.4908873016278));
#417225=CARTESIAN_POINT('Ctrl Pts',(-2.32017722201141,-1.47623921522455,
12.4911020829134));
#417226=CARTESIAN_POINT('Ctrl Pts',(-2.31902923662661,-1.47804039175897,
12.4915448903141));
#417227=CARTESIAN_POINT('Ctrl Pts',(-2.31706517352506,-1.48112198532061,
12.4923024798169));
#417228=CARTESIAN_POINT('Ctrl Pts',(-2.31514030460521,-1.4841277483063,
12.4937722312795));
#417229=CARTESIAN_POINT('Ctrl Pts',(-2.31344754677164,-1.48676173220066,
12.4958030942394));
#417230=CARTESIAN_POINT('Ctrl Pts',(-2.31176673699406,-1.48937712454788,
12.4978196226833));
#417231=CARTESIAN_POINT('Ctrl Pts',(-2.31026521511504,-1.49170367513186,
12.5004326847668));
#417232=CARTESIAN_POINT('Ctrl Pts',(-2.30902446649599,-1.49362177713198,
12.5033504258767));
#417233=CARTESIAN_POINT('Ctrl Pts',(-2.30754199105811,-1.49591357021471,
12.5068366111226));
#417234=CARTESIAN_POINT('Ctrl Pts',(-2.30638432329381,-1.49769614938807,
12.5108395010833));
#417235=CARTESIAN_POINT('Ctrl Pts',(-2.30553941244542,-1.49899566966047,
12.5149868989719));
#417236=CARTESIAN_POINT('Ctrl Pts',(-2.30412030412113,-1.50117833785518,
12.5219528491417));
#417237=CARTESIAN_POINT('Ctrl Pts',(-2.30351818383986,-1.50209985577547,
12.5295503425868));
#417238=CARTESIAN_POINT('Ctrl Pts',(-2.30351818386066,-1.50209985574305,
12.5369868989719));
#417239=CARTESIAN_POINT('',(-2.38135534869024,-1.37537147827938,12.5369868989719));
#417240=CARTESIAN_POINT('Ctrl Pts',(-2.38135534869024,-1.37537147827937,
12.5369868989719));
#417241=CARTESIAN_POINT('Ctrl Pts',(-2.38135534869024,-1.37537147827938,
12.5309445149785));
#417242=CARTESIAN_POINT('Ctrl Pts',(-2.38099368253228,-1.37599848412341,
12.5248274368704));
#417243=CARTESIAN_POINT('Ctrl Pts',(-2.38016388024033,-1.37743235884718,
12.5190199595513));
#417244=CARTESIAN_POINT('Ctrl Pts',(-2.37946689838113,-1.3786367236465,
12.5141420429941));
#417245=CARTESIAN_POINT('Ctrl Pts',(-2.37841813303529,-1.38044757921895,
12.5093757677094));
#417246=CARTESIAN_POINT('Ctrl Pts',(-2.37696631587268,-1.38294292478273,
12.5051960112707));
#417247=CARTESIAN_POINT('Ctrl Pts',(-2.37599640191872,-1.38460998765031,
12.5024036458141));
#417248=CARTESIAN_POINT('Ctrl Pts',(-2.37482293815912,-1.38662288609201,
12.4998248032393));
#417249=CARTESIAN_POINT('Ctrl Pts',(-2.37348516968652,-1.38890897803929,
12.4976950015772));
#417250=CARTESIAN_POINT('Ctrl Pts',(-2.37210970829254,-1.39125948283961,
12.495505190692));
#417251=CARTESIAN_POINT('Ctrl Pts',(-2.37052490879456,-1.39395929667832,
12.4937456938368));
#417252=CARTESIAN_POINT('Ctrl Pts',(-2.36885075180983,-1.39679852364254,
12.4925987732155));
#417253=CARTESIAN_POINT('Ctrl Pts',(-2.36717698657139,-1.3996370862386,
12.4914521209692));
#417254=CARTESIAN_POINT('Ctrl Pts',(-2.36537206234429,-1.4026857046126,
12.4908873016276));
#417255=CARTESIAN_POINT('Ctrl Pts',(-2.36358818275363,-1.40568520741572,
12.4908873016278));
#417256=CARTESIAN_POINT('',(-2.38135534869024,-1.37537147827938,13.7435492065112));
#417257=CARTESIAN_POINT('',(-2.38135534869024,-1.37537147827938,14.));
#417258=CARTESIAN_POINT('',(-2.4182885001885,-1.30934362558346,13.7435492065112));
#417259=CARTESIAN_POINT('Origin',(0.,2.5406128344257E-15,13.7435492065112));
#417260=CARTESIAN_POINT('',(-2.4182885001885,-1.30934362558346,12.5369868989719));
#417261=CARTESIAN_POINT('',(-2.4182885001885,-1.30934362558346,14.));
#417262=CARTESIAN_POINT('Ctrl Pts',(-2.43482026830688,-1.27833886784452,
12.4908873016278));
#417263=CARTESIAN_POINT('Ctrl Pts',(-2.43380627755081,-1.28027019083474,
12.4908873016278));
#417264=CARTESIAN_POINT('Ctrl Pts',(-2.43278422448335,-1.28221116794868,
12.4911020829134));
#417265=CARTESIAN_POINT('Ctrl Pts',(-2.43178687153408,-1.28409992268301,
12.4915448903141));
#417266=CARTESIAN_POINT('Ctrl Pts',(-2.43008052217386,-1.28733135187254,
12.4923024798169));
#417267=CARTESIAN_POINT('Ctrl Pts',(-2.42840705568404,-1.29048400811643,
12.4937722312795));
#417268=CARTESIAN_POINT('Ctrl Pts',(-2.42693462450261,-1.2932472031249,
12.4958030942394));
#417269=CARTESIAN_POINT('Ctrl Pts',(-2.42547258623732,-1.29599089457059,
12.4978196226833));
#417270=CARTESIAN_POINT('Ctrl Pts',(-2.42416569601973,-1.29843209172202,
12.5004326847668));
#417271=CARTESIAN_POINT('Ctrl Pts',(-2.42308541900916,-1.30044494392697,
12.5033504258767));
#417272=CARTESIAN_POINT('Ctrl Pts',(-2.42179467879822,-1.30284994676809,
12.5068366111226));
#417273=CARTESIAN_POINT('Ctrl Pts',(-2.42078615982918,-1.30472095522636,
12.5108395010833));
#417274=CARTESIAN_POINT('Ctrl Pts',(-2.4200499833183,-1.30608501953017,
12.5149868989719));
#417275=CARTESIAN_POINT('Ctrl Pts',(-2.41881350468066,-1.3083760955793,
12.5219528491417));
#417276=CARTESIAN_POINT('Ctrl Pts',(-2.41828850017042,-1.30934362561747,
12.5295503425868));
#417277=CARTESIAN_POINT('Ctrl Pts',(-2.4182885001885,-1.30934362558346,
12.5369868989719));
#417278=CARTESIAN_POINT('',(-2.48553712902108,-1.17669247480285,12.5369868989719));
#417279=CARTESIAN_POINT('Ctrl Pts',(-2.48553712902108,-1.17669247480285,
12.5369868989719));
#417280=CARTESIAN_POINT('Ctrl Pts',(-2.48553712902107,-1.17669247480285,
12.5309445149785));
#417281=CARTESIAN_POINT('Ctrl Pts',(-2.48522777307455,-1.17734687348608,
12.5248274368704));
#417282=CARTESIAN_POINT('Ctrl Pts',(-2.4845176059827,-1.1788436137003,12.5190199595513));
#417283=CARTESIAN_POINT('Ctrl Pts',(-2.48392111018507,-1.18010078156709,
12.5141420429941));
#417284=CARTESIAN_POINT('Ctrl Pts',(-2.48302343605972,-1.18199109577896,
12.5093757677094));
#417285=CARTESIAN_POINT('Ctrl Pts',(-2.48177984352806,-1.18459647486299,
12.5051960112707));
#417286=CARTESIAN_POINT('Ctrl Pts',(-2.48094903798272,-1.18633704770789,
12.5024036458141));
#417287=CARTESIAN_POINT('Ctrl Pts',(-2.47994354873682,-1.18843889658639,
12.4998248032393));
#417288=CARTESIAN_POINT('Ctrl Pts',(-2.4787965692952,-1.19082642230106,
12.4976950015772));
#417289=CARTESIAN_POINT('Ctrl Pts',(-2.47761727259779,-1.19328121886333,
12.495505190692));
#417290=CARTESIAN_POINT('Ctrl Pts',(-2.4762578062811,-1.19610122516585,
12.4937456938368));
#417291=CARTESIAN_POINT('Ctrl Pts',(-2.47482064327132,-1.19906746417294,
12.4925987732155));
#417292=CARTESIAN_POINT('Ctrl Pts',(-2.47338381655214,-1.20203300909154,
12.4914521209692));
#417293=CARTESIAN_POINT('Ctrl Pts',(-2.47183338876099,-1.20521860152,12.4908873016276));
#417294=CARTESIAN_POINT('Ctrl Pts',(-2.47029993220698,-1.20835352647236,
12.4908873016278));
#417295=CARTESIAN_POINT('',(-2.48553712902108,-1.17669247480285,13.7435492065112));
#417296=CARTESIAN_POINT('',(-2.48553712902108,-1.17669247480285,14.));
#417297=CARTESIAN_POINT('',(-2.5169655055371,-1.10787392962211,13.7435492065112));
#417298=CARTESIAN_POINT('Origin',(0.,2.5406128344257E-15,13.7435492065112));
#417299=CARTESIAN_POINT('',(-2.51696550553711,-1.10787392962211,12.5369868989719));
#417300=CARTESIAN_POINT('',(-2.51696550553711,-1.10787392962211,14.));
#417301=CARTESIAN_POINT('Ctrl Pts',(-2.530915089971,-1.07562484508174,12.4908873016278));
#417302=CARTESIAN_POINT('Ctrl Pts',(-2.53006189393875,-1.07763239141408,
12.4908873016278));
#417303=CARTESIAN_POINT('Ctrl Pts',(-2.52920144932249,-1.07965021690007,
12.4911020829134));
#417304=CARTESIAN_POINT('Ctrl Pts',(-2.52836136602808,-1.08161398048317,
12.4915448903141));
#417305=CARTESIAN_POINT('Ctrl Pts',(-2.52692408588266,-1.08497374067248,
12.4923024798169));
#417306=CARTESIAN_POINT('Ctrl Pts',(-2.52551315846624,-1.08825230976742,
12.4937722312795));
#417307=CARTESIAN_POINT('Ctrl Pts',(-2.52427085272355,-1.09112632728312,
12.4958030942394));
#417308=CARTESIAN_POINT('Ctrl Pts',(-2.52303731559399,-1.09398005901338,
12.4978196226833));
#417309=CARTESIAN_POINT('Ctrl Pts',(-2.52193375417659,-1.09651965696798,
12.5004326847668));
#417310=CARTESIAN_POINT('Ctrl Pts',(-2.52102113783977,-1.09861386417844,
12.5033504258767));
#417311=CARTESIAN_POINT('Ctrl Pts',(-2.51993072251891,-1.10111607188084,
12.5068366111226));
#417312=CARTESIAN_POINT('Ctrl Pts',(-2.51907806387249,-1.10306305837143,
12.5108395010833));
#417313=CARTESIAN_POINT('Ctrl Pts',(-2.51845552083233,-1.10448258908376,
12.5149868989719));
#417314=CARTESIAN_POINT('Ctrl Pts',(-2.51740990044268,-1.10686682625421,
12.5219528491417));
#417315=CARTESIAN_POINT('Ctrl Pts',(-2.51696550552185,-1.10787392965748,
12.5295503425868));
#417316=CARTESIAN_POINT('Ctrl Pts',(-2.51696550553711,-1.10787392962211,
12.5369868989719));
#417317=CARTESIAN_POINT('',(-2.57317806984304,-0.97018277704711,12.5369868989719));
#417318=CARTESIAN_POINT('Ctrl Pts',(-2.57317806984304,-0.970182777047109,
12.5369868989719));
#417319=CARTESIAN_POINT('Ctrl Pts',(-2.57317806984304,-0.970182777047111,
12.5309445149785));
#417320=CARTESIAN_POINT('Ctrl Pts',(-2.57292308282073,-0.970860213654265,
12.5248274368704));
#417321=CARTESIAN_POINT('Ctrl Pts',(-2.57233727697381,-0.972409858799751,
12.5190199595513));
#417322=CARTESIAN_POINT('Ctrl Pts',(-2.57184523681886,-0.97371146348928,
12.5141420429941));
#417323=CARTESIAN_POINT('Ctrl Pts',(-2.57110462778719,-0.975668656611362,
12.5093757677094));
#417324=CARTESIAN_POINT('Ctrl Pts',(-2.5700775357896,-0.978366730847705,
12.5051960112707));
#417325=CARTESIAN_POINT('Ctrl Pts',(-2.56939136752673,-0.980169230444812,
12.5024036458141));
#417326=CARTESIAN_POINT('Ctrl Pts',(-2.56856054415956,-0.982346042302609,
12.4998248032393));
#417327=CARTESIAN_POINT('Ctrl Pts',(-2.56761198670786,-0.984819113194947,
12.4976950015772));
#417328=CARTESIAN_POINT('Ctrl Pts',(-2.56663670273197,-0.987361865253058,
12.495505190692));
#417329=CARTESIAN_POINT('Ctrl Pts',(-2.56551161662063,-0.990283297342725,
12.4937456938368));
#417330=CARTESIAN_POINT('Ctrl Pts',(-2.5643210116685,-0.993356808561481,
12.4925987732155));
#417331=CARTESIAN_POINT('Ctrl Pts',(-2.56313068531333,-0.996429600590463,
12.4914521209692));
#417332=CARTESIAN_POINT('Ctrl Pts',(-2.56184507179927,-0.999730967481363,
12.4908873016276));
#417333=CARTESIAN_POINT('Ctrl Pts',(-2.56057224318229,-1.00298045217462,
12.4908873016278));
#417334=CARTESIAN_POINT('',(-2.57317806984304,-0.970182777047111,13.7435492065112));
#417335=CARTESIAN_POINT('',(-2.57317806984304,-0.970182777047112,14.));
#417336=CARTESIAN_POINT('',(-2.59889252071644,-0.899031515445461,13.7435492065112));
#417337=CARTESIAN_POINT('Origin',(0.,2.5406128344257E-15,13.7435492065112));
#417338=CARTESIAN_POINT('',(-2.59889252071644,-0.899031515445462,12.5369868989719));
#417339=CARTESIAN_POINT('',(-2.59889252071644,-0.899031515445462,14.));
#417340=CARTESIAN_POINT('Ctrl Pts',(-2.61016708928295,-0.865752716440546,
12.4908873016278));
#417341=CARTESIAN_POINT('Ctrl Pts',(-2.60948036585335,-0.867823126225396,
12.4908873016278));
#417342=CARTESIAN_POINT('Ctrl Pts',(-2.60878725580526,-0.869904371787742,
12.4911020829134));
#417343=CARTESIAN_POINT('Ctrl Pts',(-2.60811003278142,-0.871930075696962,
12.4915448903141));
#417344=CARTESIAN_POINT('Ctrl Pts',(-2.60695138671304,-0.875395808236311,
12.4923024798169));
#417345=CARTESIAN_POINT('Ctrl Pts',(-2.60581238785919,-0.878778471845899,
12.4937722312795));
#417346=CARTESIAN_POINT('Ctrl Pts',(-2.60480847489498,-0.881744185756441,
12.4958030942394));
#417347=CARTESIAN_POINT('Ctrl Pts',(-2.60381164788723,-0.884688966657447,
12.4978196226833));
#417348=CARTESIAN_POINT('Ctrl Pts',(-2.60291875928919,-0.887310064809837,
12.5004326847668));
#417349=CARTESIAN_POINT('Ctrl Pts',(-2.60217987693727,-0.889471690422325,
12.5033504258767));
#417350=CARTESIAN_POINT('Ctrl Pts',(-2.60129704304054,-0.892054451206593,
12.5068366111226));
#417351=CARTESIAN_POINT('Ctrl Pts',(-2.60060591901935,-0.894064458855623,
12.5108395010833));
#417352=CARTESIAN_POINT('Ctrl Pts',(-2.60010115237114,-0.895530009233791,
12.5149868989719));
#417353=CARTESIAN_POINT('Ctrl Pts',(-2.59925334866065,-0.89799154082057,
12.5219528491417));
#417354=CARTESIAN_POINT('Ctrl Pts',(-2.59889252070412,-0.899031515481953,
12.5295503425868));
#417355=CARTESIAN_POINT('Ctrl Pts',(-2.59889252071644,-0.899031515445462,
12.5369868989719));
#417356=CARTESIAN_POINT('',(-2.6436949351547,-0.75721667297901,12.5369868989719));
#417357=CARTESIAN_POINT('Ctrl Pts',(-2.6436949351547,-0.757216672979009,
12.5369868989719));
#417358=CARTESIAN_POINT('Ctrl Pts',(-2.6436949351547,-0.757216672979011,
12.5309445149785));
#417359=CARTESIAN_POINT('Ctrl Pts',(-2.64349601395317,-0.757912639281242,
12.5248274368704));
#417360=CARTESIAN_POINT('Ctrl Pts',(-2.64303846779244,-0.759504876725223,
12.5190199595513));
#417361=CARTESIAN_POINT('Ctrl Pts',(-2.64265415772621,-0.760842256273028,
12.5141420429941));
#417362=CARTESIAN_POINT('Ctrl Pts',(-2.64207554241915,-0.762853303508013,
12.5093757677094));
#417363=CARTESIAN_POINT('Ctrl Pts',(-2.64127178608342,-0.76562611765777,
12.5051960112707));
#417364=CARTESIAN_POINT('Ctrl Pts',(-2.64073482143959,-0.767478548669664,
12.5024036458141));
#417365=CARTESIAN_POINT('Ctrl Pts',(-2.64008419294358,-0.769715837182991,
12.4998248032393));
#417366=CARTESIAN_POINT('Ctrl Pts',(-2.63934036997515,-0.77225799537424,
12.4976950015772));
#417367=CARTESIAN_POINT('Ctrl Pts',(-2.63857558907473,-0.774871781332769,
12.495505190692));
#417368=CARTESIAN_POINT('Ctrl Pts',(-2.63769237043116,-0.777875197561024,
12.4937456938368));
#417369=CARTESIAN_POINT('Ctrl Pts',(-2.63675624681621,-0.781035527281383,
12.4925987732155));
#417370=CARTESIAN_POINT('Ctrl Pts',(-2.63582034225057,-0.784195117496772,
12.4914521209692));
#417371=CARTESIAN_POINT('Ctrl Pts',(-2.63480809855942,-0.787590288798135,
12.4908873016276));
#417372=CARTESIAN_POINT('Ctrl Pts',(-2.63380436834391,-0.790932708447788,
12.4908873016278));
#417373=CARTESIAN_POINT('',(-2.6436949351547,-0.757216672979011,13.7435492065112));
#417374=CARTESIAN_POINT('',(-2.6436949351547,-0.757216672979012,14.));
#417375=CARTESIAN_POINT('',(-2.66352433495749,-0.684206194863278,13.7435492065112));
#417376=CARTESIAN_POINT('Origin',(0.,2.5406128344257E-15,13.7435492065112));
#417377=CARTESIAN_POINT('',(-2.66352433495749,-0.684206194863278,12.5369868989719));
#417378=CARTESIAN_POINT('',(-2.66352433495749,-0.684206194863278,14.));
#417379=CARTESIAN_POINT('Ctrl Pts',(-2.67204885726298,-0.650119146310585,
12.4908873016278));
#417380=CARTESIAN_POINT('Ctrl Pts',(-2.67153317646716,-0.652238641312415,
12.4908873016278));
#417381=CARTESIAN_POINT('Ctrl Pts',(-2.67101201352024,-0.654369456605282,
12.4911020829134));
#417382=CARTESIAN_POINT('Ctrl Pts',(-2.67050215757447,-0.656443620115327,
12.4915448903141));
#417383=CARTESIAN_POINT('Ctrl Pts',(-2.66962985618155,-0.659992261126472,
12.4923024798169));
#417384=CARTESIAN_POINT('Ctrl Pts',(-2.66877036573973,-0.663456508182488,
12.4937722312795));
#417385=CARTESIAN_POINT('Ctrl Pts',(-2.66801152642914,-0.666494182151103,
12.4958030942394));
#417386=CARTESIAN_POINT('Ctrl Pts',(-2.66725804326247,-0.669510415191811,
12.4978196226833));
#417387=CARTESIAN_POINT('Ctrl Pts',(-2.66658176951009,-0.672195570566237,
12.5004326847668));
#417388=CARTESIAN_POINT('Ctrl Pts',(-2.66602153828321,-0.674410229318952,
12.5033504258767));
#417389=CARTESIAN_POINT('Ctrl Pts',(-2.66535216092455,-0.677056355338186,
12.5068366111226));
#417390=CARTESIAN_POINT('Ctrl Pts',(-2.66482717084492,-0.679116007876387,
12.5108395010833));
#417391=CARTESIAN_POINT('Ctrl Pts',(-2.66444353972741,-0.680617824924426,
12.5149868989719));
#417392=CARTESIAN_POINT('Ctrl Pts',(-2.6637991946899,-0.683140269840942,
12.5219528491417));
#417393=CARTESIAN_POINT('Ctrl Pts',(-2.66352433494818,-0.684206194900652,
12.5295503425868));
#417394=CARTESIAN_POINT('Ctrl Pts',(-2.66352433495749,-0.684206194863278,
12.5369868989719));
#417395=CARTESIAN_POINT('',(-2.69661844685186,-0.539211416884192,12.5369868989719));
#417396=CARTESIAN_POINT('Ctrl Pts',(-2.69661844685186,-0.539211416884191,
12.5369868989719));
#417397=CARTESIAN_POINT('Ctrl Pts',(-2.69661844685186,-0.539211416884193,
12.5309445149785));
#417398=CARTESIAN_POINT('Ctrl Pts',(-2.69647691525889,-0.539921281340585,
12.5248274368704));
#417399=CARTESIAN_POINT('Ctrl Pts',(-2.69615067367856,-0.541545515005572,
12.5190199595513));
#417400=CARTESIAN_POINT('Ctrl Pts',(-2.69587665122115,-0.542909769371416,
12.5141420429941));
#417401=CARTESIAN_POINT('Ctrl Pts',(-2.69546388022809,-0.544961287531754,
12.5093757677094));
#417402=CARTESIAN_POINT('Ctrl Pts',(-2.69488880842001,-0.547790388974241,
12.5051960112707));
#417403=CARTESIAN_POINT('Ctrl Pts',(-2.69450462080634,-0.549680423778167,
12.5024036458141));
#417404=CARTESIAN_POINT('Ctrl Pts',(-2.69403851700679,-0.551963300161093,
12.4998248032393));
#417405=CARTESIAN_POINT('Ctrl Pts',(-2.69350437854076,-0.554557628007917,
12.4976950015772));
#417406=CARTESIAN_POINT('Ctrl Pts',(-2.69295519020651,-0.557225053552556,
12.495505190692));
#417407=CARTESIAN_POINT('Ctrl Pts',(-2.69231971670508,-0.560290466679928,
12.4937456938368));
#417408=CARTESIAN_POINT('Ctrl Pts',(-2.69164430417551,-0.563516583429017,
12.4925987732155));
#417409=CARTESIAN_POINT('Ctrl Pts',(-2.69096904968987,-0.566741945279226,
12.4914521209692));
#417410=CARTESIAN_POINT('Ctrl Pts',(-2.6902369121364,-0.570208326686206,
12.4908873016276));
#417411=CARTESIAN_POINT('Ctrl Pts',(-2.68950895998132,-0.573621438040947,
12.4908873016278));
#417412=CARTESIAN_POINT('',(-2.69661844685186,-0.539211416884193,13.7435492065112));
#417413=CARTESIAN_POINT('',(-2.69661844685186,-0.539211416884193,14.));
#417414=CARTESIAN_POINT('',(-2.71043083419997,-0.464827594940355,13.7435492065112));
#417415=CARTESIAN_POINT('Origin',(0.,2.5406128344257E-15,13.7435492065112));
#417416=CARTESIAN_POINT('',(-2.71043083419997,-0.464827594940355,12.5369868989719));
#417417=CARTESIAN_POINT('',(-2.71043083419998,-0.464827594940355,14.));
#417418=CARTESIAN_POINT('Ctrl Pts',(-2.71614858095496,-0.430159140524035,
12.4908873016278));
#417419=CARTESIAN_POINT('Ctrl Pts',(-2.71580737456352,-0.4323136158533,
12.4908873016278));
#417420=CARTESIAN_POINT('Ctrl Pts',(-2.71546162697122,-0.434479820652474,
12.4911020829134));
#417421=CARTESIAN_POINT('Ctrl Pts',(-2.7151225311107,-0.436588640547398,
12.4915448903141));
#417422=CARTESIAN_POINT('Ctrl Pts',(-2.71454237941509,-0.440196574409895,
12.4923024798169));
#417423=CARTESIAN_POINT('Ctrl Pts',(-2.71396811715238,-0.443719350919741,
12.4937722312795));
#417424=CARTESIAN_POINT('Ctrl Pts',(-2.71345940144583,-0.446808769727349,
12.4958030942394));
#417425=CARTESIAN_POINT('Ctrl Pts',(-2.7129542764264,-0.449876382374515,
12.4978196226833));
#417426=CARTESIAN_POINT('Ctrl Pts',(-2.71249911800992,-0.452607725704981,
12.5004326847668));
#417427=CARTESIAN_POINT('Ctrl Pts',(-2.71212126615447,-0.454860679409316,
12.5033504258767));
#417428=CARTESIAN_POINT('Ctrl Pts',(-2.71166979992975,-0.457552561131439,
12.5068366111226));
#417429=CARTESIAN_POINT('Ctrl Pts',(-2.71131443751405,-0.459648151910989,
12.5108395010833));
#417430=CARTESIAN_POINT('Ctrl Pts',(-2.71105449492904,-0.461176241284225,
12.5149868989719));
#417431=CARTESIAN_POINT('Ctrl Pts',(-2.71061789657441,-0.463742813075734,
12.5219528491417));
#417432=CARTESIAN_POINT('Ctrl Pts',(-2.71043083419375,-0.464827594978363,
12.5295503425868));
#417433=CARTESIAN_POINT('Ctrl Pts',(-2.71043083419997,-0.464827594940355,
12.5369868989719));
#417434=CARTESIAN_POINT('',(-2.73159640769595,-0.31761779777363,12.5369868989719));
#417435=CARTESIAN_POINT('Ctrl Pts',(-2.73159640769595,-0.317617797773629,
12.5369868989719));
#417436=CARTESIAN_POINT('Ctrl Pts',(-2.73159640769595,-0.317617797773631,
12.5309445149785));
#417437=CARTESIAN_POINT('Ctrl Pts',(-2.73151320758094,-0.318336836353346,
12.5248274368704));
#417438=CARTESIAN_POINT('Ctrl Pts',(-2.7313204416649,-0.319982257232279,
12.5190199595513));
#417439=CARTESIAN_POINT('Ctrl Pts',(-2.73115853039054,-0.321364307528444,
12.5141420429941));
#417440=CARTESIAN_POINT('Ctrl Pts',(-2.73091435063435,-0.323442644099255,
12.5093757677094));
#417441=CARTESIAN_POINT('Ctrl Pts',(-2.73057179036193,-0.326309205631141,
12.5051960112707));
#417442=CARTESIAN_POINT('Ctrl Pts',(-2.7303429364836,-0.328224266357311,
12.5024036458141));
#417443=CARTESIAN_POINT('Ctrl Pts',(-2.73006445922439,-0.330537538444158,
12.4998248032393));
#417444=CARTESIAN_POINT('Ctrl Pts',(-2.72974355986412,-0.333166771122769,
12.4976950015772));
#417445=CARTESIAN_POINT('Ctrl Pts',(-2.72941361885381,-0.335870084976612,
12.495505190692));
#417446=CARTESIAN_POINT('Ctrl Pts',(-2.72903011946582,-0.338977095184496,
12.4937456938368));
#417447=CARTESIAN_POINT('Ctrl Pts',(-2.72861991278058,-0.342247529687623,
12.4925987732155));
#417448=CARTESIAN_POINT('Ctrl Pts',(-2.72820980208213,-0.345517198921685,
12.4914521209692));
#417449=CARTESIAN_POINT('Ctrl Pts',(-2.72776264292095,-0.349031722237931,
12.4908873016276));
#417450=CARTESIAN_POINT('Ctrl Pts',(-2.72731531322781,-0.352492811604818,
12.4908873016278));
#417451=CARTESIAN_POINT('',(-2.73159640769595,-0.317617797773631,13.7435492065112));
#417452=CARTESIAN_POINT('',(-2.73159640769595,-0.317617797773632,14.));
#417453=CARTESIAN_POINT('',(-2.73929986343047,-0.242355644064259,13.7435492065112));
#417454=CARTESIAN_POINT('Origin',(0.,2.5406128344257E-15,13.7435492065112));
#417455=CARTESIAN_POINT('',(-2.73929986343047,-0.24235564406426,12.5369868989719));
#417456=CARTESIAN_POINT('',(-2.73929986343047,-0.24235564406426,14.));
#417457=CARTESIAN_POINT('Ctrl Pts',(-2.74217278397365,-0.207336496628562,
12.4908873016278));
#417458=CARTESIAN_POINT('Ctrl Pts',(-2.74200832265884,-0.209511614607407,
12.4908873016278));
#417459=CARTESIAN_POINT('Ctrl Pts',(-2.74184029131432,-0.211698793177349,
12.4911020829134));
#417460=CARTESIAN_POINT('Ctrl Pts',(-2.74167421216608,-0.213828235608682,
12.4915448903141));
#417461=CARTESIAN_POINT('Ctrl Pts',(-2.74139007098159,-0.217471452117943,
12.4923024798169));
#417462=CARTESIAN_POINT('Ctrl Pts',(-2.7411048585186,-0.221029314585163,
12.4937722312795));
#417463=CARTESIAN_POINT('Ctrl Pts',(-2.74084965183518,-0.224149918659317,
12.4958030942394));
#417464=CARTESIAN_POINT('Ctrl Pts',(-2.74059624648665,-0.227248496456896,
12.4978196226833));
#417465=CARTESIAN_POINT('Ctrl Pts',(-2.74036523241025,-0.230007851104178,
12.5004326847668));
#417466=CARTESIAN_POINT('Ctrl Pts',(-2.74017227446798,-0.232284106724942,
12.5033504258767));
#417467=CARTESIAN_POINT('Ctrl Pts',(-2.73994172381044,-0.235003830121222,
12.5068366111226));
#417468=CARTESIAN_POINT('Ctrl Pts',(-2.73975835393691,-0.23712141333123,
12.5108395010833));
#417469=CARTESIAN_POINT('Ctrl Pts',(-2.73962382975943,-0.238665605847002,
12.5149868989719));
#417470=CARTESIAN_POINT('Ctrl Pts',(-2.7393978835777,-0.241259224401685,
12.5219528491417));
#417471=CARTESIAN_POINT('Ctrl Pts',(-2.73929986342736,-0.242355644102649,
12.5295503425868));
#417472=CARTESIAN_POINT('Ctrl Pts',(-2.73929986343047,-0.24235564406426,
12.5369868989719));
#417473=CARTESIAN_POINT('',(-2.74839604512851,-0.0939104846221332,12.5369868989719));
#417474=CARTESIAN_POINT('Ctrl Pts',(-2.74839604512851,-0.093910484622133,
12.5369868989719));
#417475=CARTESIAN_POINT('Ctrl Pts',(-2.74839604512851,-0.0939104846221349,
12.5309445149785));
#417476=CARTESIAN_POINT('Ctrl Pts',(-2.74837173017449,-0.0946339122420582,
12.5248274368704));
#417477=CARTESIAN_POINT('Ctrl Pts',(-2.74831372274811,-0.0962895703304627,
12.5190199595513));
#417478=CARTESIAN_POINT('Ctrl Pts',(-2.74826500014963,-0.0976802192402491,
12.5141420429941));
#417479=CARTESIAN_POINT('Ctrl Pts',(-2.74819103660629,-0.0997715432345554,
12.5093757677094));
#417480=CARTESIAN_POINT('Ctrl Pts',(-2.74808326755163,-0.102656488361795,
12.5051960112707));
#417481=CARTESIAN_POINT('Ctrl Pts',(-2.74801127039343,-0.10458383059704,
12.5024036458141));
#417482=CARTESIAN_POINT('Ctrl Pts',(-2.74792227289478,-0.106912103943732,
12.4998248032393));
#417483=CARTESIAN_POINT('Ctrl Pts',(-2.74781674817257,-0.109558744344448,
12.4976950015772));
#417484=CARTESIAN_POINT('Ctrl Pts',(-2.74770825018919,-0.112279956399813,
12.495505190692));
#417485=CARTESIAN_POINT('Ctrl Pts',(-2.74757927703979,-0.115407887047896,
12.4937456938368));
#417486=CARTESIAN_POINT('Ctrl Pts',(-2.74743700605669,-0.118700875103026,
12.4925987732155));
#417487=CARTESIAN_POINT('Ctrl Pts',(-2.74729476836446,-0.121993092611647,
12.4914521209692));
#417488=CARTESIAN_POINT('Ctrl Pts',(-2.74713556336602,-0.125532369264345,
12.4908873016276));
#417489=CARTESIAN_POINT('Ctrl Pts',(-2.74697183304012,-0.129018403664679,
12.4908873016278));
#417490=CARTESIAN_POINT('',(-2.74839604512851,-0.0939104846221349,13.7435492065112));
#417491=CARTESIAN_POINT('',(-2.74839604512851,-0.093910484622135,14.));
#417492=CARTESIAN_POINT('',(-2.7499393040225,-0.0182708563627825,13.7435492065112));
#417493=CARTESIAN_POINT('Origin',(0.,2.5406128344257E-15,13.7435492065112));
#417494=CARTESIAN_POINT('',(-2.74993930402251,-0.0182708563627825,12.5369868989719));
#417495=CARTESIAN_POINT('',(-2.74993930402251,-0.0182708563627825,14.));
#417496=CARTESIAN_POINT('Ctrl Pts',(-2.74994827954166,0.0168659374438614,
12.4908873016278));
#417497=CARTESIAN_POINT('Ctrl Pts',(-2.7499616577664,0.0146846518667144,
12.4908873016278));
#417498=CARTESIAN_POINT('Ctrl Pts',(-2.74997246089054,0.0124910548385303,
12.4911020829134));
#417499=CARTESIAN_POINT('Ctrl Pts',(-2.74998050368389,0.0103551609588346,
12.4915448903141));
#417500=CARTESIAN_POINT('Ctrl Pts',(-2.74999426392324,0.00670090680759111,
12.4923024798169));
#417501=CARTESIAN_POINT('Ctrl Pts',(-2.74999999930185,0.00313163537071014,
12.4937722312795));
#417502=CARTESIAN_POINT('Ctrl Pts',(-2.74999999999993,6.13135258656274E-7,
12.4958030942394));
#417503=CARTESIAN_POINT('Ctrl Pts',(-2.75000000069309,-0.00310830928871901,
12.4978196226833));
#417504=CARTESIAN_POINT('Ctrl Pts',(-2.74999466831732,-0.00587731220289936,
12.5004326847668));
#417505=CARTESIAN_POINT('Ctrl Pts',(-2.74998788839151,-0.00816172163449239,
12.5033504258767));
#417506=CARTESIAN_POINT('Ctrl Pts',(-2.74997978757774,-0.0108911873944495,
12.5068366111226));
#417507=CARTESIAN_POINT('Ctrl Pts',(-2.74996963054264,-0.0130166708680302,
12.5108395010833));
#417508=CARTESIAN_POINT('Ctrl Pts',(-2.74996142000887,-0.0145666901799197,
12.5149868989719));
#417509=CARTESIAN_POINT('Ctrl Pts',(-2.74994762963462,-0.0171700953942134,
12.5219528491417));
#417510=CARTESIAN_POINT('Ctrl Pts',(-2.74993930402254,-0.0182708564012972,
12.5295503425868));
#417511=CARTESIAN_POINT('Ctrl Pts',(-2.74993930402251,-0.0182708563627825,
12.5369868989719));
#417512=CARTESIAN_POINT('',(-2.74690556033417,0.130421787310385,12.5369868989719));
#417513=CARTESIAN_POINT('Ctrl Pts',(-2.74690556033417,0.130421787310385,
12.5369868989719));
#417514=CARTESIAN_POINT('Ctrl Pts',(-2.74690556033417,0.130421787310383,
12.5309445149785));
#417515=CARTESIAN_POINT('Ctrl Pts',(-2.74694029235315,0.129698784941705,
12.5248274368704));
#417516=CARTESIAN_POINT('Ctrl Pts',(-2.74701742944628,0.128043907775242,
12.5190199595513));
#417517=CARTESIAN_POINT('Ctrl Pts',(-2.74708221976453,0.126653914790889,
12.5141420429941));
#417518=CARTESIAN_POINT('Ctrl Pts',(-2.74717896464922,0.124563520789225,
12.5093757677094));
#417519=CARTESIAN_POINT('Ctrl Pts',(-2.74730670399759,0.12167939090047,
12.5051960112707));
#417520=CARTESIAN_POINT('Ctrl Pts',(-2.74739204268874,0.119752593300737,
12.5024036458141));
#417521=CARTESIAN_POINT('Ctrl Pts',(-2.74749311721431,0.117424812969185,
12.4998248032393));
#417522=CARTESIAN_POINT('Ctrl Pts',(-2.74760366937978,0.114778377801565,
12.4976950015772));
#417523=CARTESIAN_POINT('Ctrl Pts',(-2.7477173364595,0.112057376761939,
12.495505190692));
#417524=CARTESIAN_POINT('Ctrl Pts',(-2.74784374784373,0.108929341536047,
12.4937456938368));
#417525=CARTESIAN_POINT('Ctrl Pts',(-2.7479703593527,0.105635714221117,
12.4925987732155));
#417526=CARTESIAN_POINT('Ctrl Pts',(-2.74809694123506,0.10234285760228,
12.4914521209692));
#417527=CARTESIAN_POINT('Ctrl Pts',(-2.74822674988235,0.0988023809153136,
12.4908873016276));
#417528=CARTESIAN_POINT('Ctrl Pts',(-2.748347708522,0.0953146004653097,
12.4908873016278));
#417529=CARTESIAN_POINT('',(-2.74690556033417,0.130421787310383,13.7435492065112));
#417530=CARTESIAN_POINT('',(-2.74690556033417,0.130421787310383,14.));
#417531=CARTESIAN_POINT('',(-2.74227835225431,0.205935520873309,13.7435492065112));
#417532=CARTESIAN_POINT('Origin',(0.,2.5406128344257E-15,13.7435492065112));
#417533=CARTESIAN_POINT('',(-2.74227835225432,0.205935520873309,12.5369868989719));
#417534=CARTESIAN_POINT('',(-2.74227835225432,0.205935520873309,14.));
#417535=CARTESIAN_POINT('Ctrl Pts',(-2.73942332301885,0.240956131485279,
12.4908873016278));
#417536=CARTESIAN_POINT('Ctrl Pts',(-2.73961445175325,0.23878319440546,
12.4908873016278));
#417537=CARTESIAN_POINT('Ctrl Pts',(-2.73980401745305,0.236597776945337,
12.4911020829134));
#417538=CARTESIAN_POINT('Ctrl Pts',(-2.73998612866454,0.234469645638651,
12.4915448903141));
#417539=CARTESIAN_POINT('Ctrl Pts',(-2.74029769875559,0.230828672303891,
12.4923024798169));
#417540=CARTESIAN_POINT('Ctrl Pts',(-2.7405943438078,0.227271744809874,
12.4937722312795));
#417541=CARTESIAN_POINT('Ctrl Pts',(-2.74084955188275,0.22415114084952,
12.4958030942394));
#417542=CARTESIAN_POINT('Ctrl Pts',(-2.74110295861298,0.221052563164939,
12.4978196226833));
#417543=CARTESIAN_POINT('Ctrl Pts',(-2.74132334342393,0.2182923392414,12.5004326847668));
#417544=CARTESIAN_POINT('Ctrl Pts',(-2.74150278663385,0.216014978366845,
12.5033504258767));
#417545=CARTESIAN_POINT('Ctrl Pts',(-2.74171718957344,0.213293934387513,
12.5068366111226));
#417546=CARTESIAN_POINT('Ctrl Pts',(-2.74188031297015,0.211174695392196,
12.5108395010833));
#417547=CARTESIAN_POINT('Ctrl Pts',(-2.74199847071986,0.209629164406974,
12.5149868989719));
#417548=CARTESIAN_POINT('Ctrl Pts',(-2.74219692792574,0.20703329776524,
12.5219528491417));
#417549=CARTESIAN_POINT('Ctrl Pts',(-2.74227835225749,0.205935520834925,
12.5295503425868));
#417550=CARTESIAN_POINT('Ctrl Pts',(-2.74227835225432,0.205935520873309,
12.5369868989719));
#417551=CARTESIAN_POINT('',(-2.72713487224332,0.353886123766432,12.5369868989719));
#417552=CARTESIAN_POINT('Ctrl Pts',(-2.72713487224332,0.353886123766432,
12.5369868989719));
#417553=CARTESIAN_POINT('Ctrl Pts',(-2.72713487224332,0.35388612376643,
12.5309445149785));
#417554=CARTESIAN_POINT('Ctrl Pts',(-2.72722842009945,0.353168358110474,
12.5248274368704));
#417555=CARTESIAN_POINT('Ctrl Pts',(-2.72744018837746,0.351525274800461,
12.5190199595513));
#417556=CARTESIAN_POINT('Ctrl Pts',(-2.72761806044356,0.350145187915518,
12.5141420429941));
#417557=CARTESIAN_POINT('Ctrl Pts',(-2.72788486993503,0.348069635133687,
12.5093757677094));
#417558=CARTESIAN_POINT('Ctrl Pts',(-2.72824726760215,0.345205513891979,
12.5051960112707));
#417559=CARTESIAN_POINT('Ctrl Pts',(-2.72848937422774,0.343292083447885,
12.5024036458141));
#417560=CARTESIAN_POINT('Ctrl Pts',(-2.72877984814325,0.340980287125521,
12.4998248032393));
#417561=CARTESIAN_POINT('Ctrl Pts',(-2.72910574148997,0.338351668780409,
12.4976950015772));
#417562=CARTESIAN_POINT('Ctrl Pts',(-2.72944081719713,0.335648986569506,
12.495505190692));
#417563=CARTESIAN_POINT('Ctrl Pts',(-2.72982177186808,0.332541663324144,
12.4937456938368));
#417564=CARTESIAN_POINT('Ctrl Pts',(-2.7302164232904,0.329269315295784,
12.4925987732155));
#417565=CARTESIAN_POINT('Ctrl Pts',(-2.73061098236582,0.325997732984245,
12.4914521209692));
#417566=CARTESIAN_POINT('Ctrl Pts',(-2.73102894080372,0.322479617551225,
12.4908873016276));
#417567=CARTESIAN_POINT('Ctrl Pts',(-2.73143378344912,0.319013301655004,
12.4908873016278));
#417568=CARTESIAN_POINT('',(-2.72713487224332,0.35388612376643,13.7435492065112));
#417569=CARTESIAN_POINT('',(-2.72713487224332,0.353886123766431,14.));
#417570=CARTESIAN_POINT('',(-2.71636799049595,0.428771431194959,13.7435492065112));
#417571=CARTESIAN_POINT('Origin',(0.,2.5406128344257E-15,13.7435492065112));
#417572=CARTESIAN_POINT('',(-2.71636799049596,0.428771431194959,12.5369868989719));
#417573=CARTESIAN_POINT('',(-2.71636799049596,0.428771431194959,14.));
#417574=CARTESIAN_POINT('Ctrl Pts',(-2.71066795625439,0.463442802226626,
12.4908873016278));
#417575=CARTESIAN_POINT('Ctrl Pts',(-2.71103556356826,0.461292674181891,
12.4908873016278));
#417576=CARTESIAN_POINT('Ctrl Pts',(-2.71140263031526,0.459129979882459,
12.4911020829134));
#417577=CARTESIAN_POINT('Ctrl Pts',(-2.71175759802481,0.457023773511512,
12.4915448903141));
#417578=CARTESIAN_POINT('Ctrl Pts',(-2.71236490452002,0.45342031107006,
12.4923024798169));
#417579=CARTESIAN_POINT('Ctrl Pts',(-2.71295048512196,0.449899398284527,
12.4937722312795));
#417580=CARTESIAN_POINT('Ctrl Pts',(-2.71345920220613,0.446809979703764,
12.4958030942394));
#417581=CARTESIAN_POINT('Ctrl Pts',(-2.71396432859346,0.443742367281841,
12.4978196226833));
#417582=CARTESIAN_POINT('Ctrl Pts',(-2.71440896396657,0.44100929118375,
12.5004326847668));
#417583=CARTESIAN_POINT('Ctrl Pts',(-2.71477343614727,0.438754134327114,
12.5033504258767));
#417584=CARTESIAN_POINT('Ctrl Pts',(-2.71520891602402,0.436059620227148,
12.5068366111226));
#417585=CARTESIAN_POINT('Ctrl Pts',(-2.71554423429326,0.43396072889596,
12.5108395010833));
#417586=CARTESIAN_POINT('Ctrl Pts',(-2.71578797400611,0.432429971491118,
12.5149868989719));
#417587=CARTESIAN_POINT('Ctrl Pts',(-2.71619735809216,0.429858918486156,
12.5219528491417));
#417588=CARTESIAN_POINT('Ctrl Pts',(-2.71636799050224,0.428771431156961,
12.5295503425868));
#417589=CARTESIAN_POINT('Ctrl Pts',(-2.71636799049596,0.428771431194959,
12.5369868989719));
#417590=CARTESIAN_POINT('',(-2.68921555152327,0.574995406455915,12.5369868989719));
#417591=CARTESIAN_POINT('Ctrl Pts',(-2.68921555152327,0.574995406455915,
12.5369868989719));
#417592=CARTESIAN_POINT('Ctrl Pts',(-2.68921555152327,0.574995406455913,
12.5309445149785));
#417593=CARTESIAN_POINT('Ctrl Pts',(-2.689367292671,0.574287654124696,12.5248274368704));
#417594=CARTESIAN_POINT('Ctrl Pts',(-2.68971228285094,0.57266729911947,
12.5190199595513));
#417595=CARTESIAN_POINT('Ctrl Pts',(-2.69000205295564,0.571306302584459,
12.5141420429941));
#417596=CARTESIAN_POINT('Ctrl Pts',(-2.69043715148075,0.569259403483782,
12.5093757677094));
#417597=CARTESIAN_POINT('Ctrl Pts',(-2.69103179576993,0.566434351143439,
12.5051960112707));
#417598=CARTESIAN_POINT('Ctrl Pts',(-2.69142905915031,0.564547021418895,
12.5024036458141));
#417599=CARTESIAN_POINT('Ctrl Pts',(-2.69190699939977,0.562266593728825,
12.4998248032393));
#417600=CARTESIAN_POINT('Ctrl Pts',(-2.69244606516129,0.559673285227614,
12.4976950015772));
#417601=CARTESIAN_POINT('Ctrl Pts',(-2.69300031962234,0.557006907749637,
12.495505190692));
#417602=CARTESIAN_POINT('Ctrl Pts',(-2.69363328238953,0.553940975208331,
12.4937456938368));
#417603=CARTESIAN_POINT('Ctrl Pts',(-2.69429334738511,0.55071168340277,
12.4925987732155));
#417604=CARTESIAN_POINT('Ctrl Pts',(-2.69495325792803,0.547483147239041,
12.4914521209692));
#417605=CARTESIAN_POINT('Ctrl Pts',(-2.69565658471209,0.544010805537726,
12.4908873016276));
#417606=CARTESIAN_POINT('Ctrl Pts',(-2.69634261720224,0.540589021955674,
12.4908873016278));
#417607=CARTESIAN_POINT('',(-2.68921555152327,0.574995406455913,13.7435492065112));
#417608=CARTESIAN_POINT('',(-2.68921555152327,0.574995406455914,14.));
#417609=CARTESIAN_POINT('',(-2.67238064793001,0.648753938384312,13.7435492065112));
#417610=CARTESIAN_POINT('Origin',(0.,2.5406128344257E-15,13.7435492065112));
#417611=CARTESIAN_POINT('',(-2.67238064793002,0.648753938384312,12.5369868989719));
#417612=CARTESIAN_POINT('',(-2.67238064793002,0.648753938384313,14.));
#417613=CARTESIAN_POINT('Ctrl Pts',(-2.66387354146978,0.682845337581834,
12.4908873016278));
#417614=CARTESIAN_POINT('Ctrl Pts',(-2.6644151809971,0.680732327319576,
12.4908873016278));
#417615=CARTESIAN_POINT('Ctrl Pts',(-2.66495730602266,0.678606748554576,
12.4911020829134));
#417616=CARTESIAN_POINT('Ctrl Pts',(-2.66548276797874,0.676536483575267,
12.4915448903141));
#417617=CARTESIAN_POINT('Ctrl Pts',(-2.66638176935357,0.672994512475143,
12.4923024798169));
#417618=CARTESIAN_POINT('Ctrl Pts',(-2.66725238856295,0.669533045491771,
12.4937722312795));
#417619=CARTESIAN_POINT('Ctrl Pts',(-2.66801122922809,0.666495371861536,
12.4958030942394));
#417620=CARTESIAN_POINT('Ctrl Pts',(-2.66876471373974,0.663479139156819,
12.4978196226833));
#417621=CARTESIAN_POINT('Ctrl Pts',(-2.66943064069996,0.660791399054683,
12.5004326847668));
#417622=CARTESIAN_POINT('Ctrl Pts',(-2.66997771634922,0.658573453912772,
12.5033504258767));
#417623=CARTESIAN_POINT('Ctrl Pts',(-2.6706313751164,0.655923401238945,
12.5068366111226));
#417624=CARTESIAN_POINT('Ctrl Pts',(-2.67113665677041,0.653858825347401,
12.5108395010833));
#417625=CARTESIAN_POINT('Ctrl Pts',(-2.67150435639882,0.652353028460911,
12.5149868989719));
#417626=CARTESIAN_POINT('Ctrl Pts',(-2.67212194298149,0.649823899026276,
12.5219528491417));
#417627=CARTESIAN_POINT('Ctrl Pts',(-2.67238064793938,0.648753938346953,
12.5295503425868));
#417628=CARTESIAN_POINT('Ctrl Pts',(-2.67238064793002,0.648753938384312,
12.5369868989719));
#417629=CARTESIAN_POINT('',(-2.63339994499717,0.792278189582998,12.5369868989719));
#417630=CARTESIAN_POINT('Ctrl Pts',(-2.63339994499717,0.792278189582997,
12.5369868989719));
#417631=CARTESIAN_POINT('Ctrl Pts',(-2.63339994499717,0.792278189582996,
12.5309445149785));
#417632=CARTESIAN_POINT('Ctrl Pts',(-2.63360886962419,0.79158516055151,
12.5248274368704));
#417633=CARTESIAN_POINT('Ctrl Pts',(-2.63408478585334,0.789998317046293,
12.5190199595513));
#417634=CARTESIAN_POINT('Ctrl Pts',(-2.6344845256244,0.788665468068605,
12.5141420429941));
#417635=CARTESIAN_POINT('Ctrl Pts',(-2.63508501767425,0.786660844424882,
12.5093757677094));
#417636=CARTESIAN_POINT('Ctrl Pts',(-2.63590795132585,0.783893661243128,
12.5051960112707));
#417637=CARTESIAN_POINT('Ctrl Pts',(-2.63645772773878,0.782044992106063,
12.5024036458141));
#417638=CARTESIAN_POINT('Ctrl Pts',(-2.63711995370868,0.779811108918321,
12.4998248032393));
#417639=CARTESIAN_POINT('Ctrl Pts',(-2.6378686044913,0.777270368301222,
12.4976950015772));
#417640=CARTESIAN_POINT('Ctrl Pts',(-2.63863834923425,0.774658039858365,
12.495505190692));
#417641=CARTESIAN_POINT('Ctrl Pts',(-2.63951910783489,0.771653901296335,
12.4937456938368));
#417642=CARTESIAN_POINT('Ctrl Pts',(-2.64044019378009,0.768489156117743,
12.4925987732155));
#417643=CARTESIAN_POINT('Ctrl Pts',(-2.64136106419473,0.765325151477321,
12.4914521209692));
#417644=CARTESIAN_POINT('Ctrl Pts',(-2.64234507880124,0.761921691368837,
12.4908873016276));
#417645=CARTESIAN_POINT('Ctrl Pts',(-2.64330773570309,0.75856721150614,
12.4908873016278));
#417646=CARTESIAN_POINT('',(-2.63339994499717,0.792278189582995,13.7435492065112));
#417647=CARTESIAN_POINT('',(-2.63339994499717,0.792278189582996,14.));
#417648=CARTESIAN_POINT('',(-2.61060905306387,0.864419095150583,13.7435492065112));
#417649=CARTESIAN_POINT('Origin',(0.,2.5406128344257E-15,13.7435492065112));
#417650=CARTESIAN_POINT('',(-2.61060905306387,0.864419095150584,12.5369868989719));
#417651=CARTESIAN_POINT('',(-2.61060905306387,0.864419095150584,14.));
#417652=CARTESIAN_POINT('Ctrl Pts',(-2.59935148777489,0.897703649876986,
12.4908873016278));
#417653=CARTESIAN_POINT('Ctrl Pts',(-2.60006355499397,0.895641819131877,
12.4908873016278));
#417654=CARTESIAN_POINT('Ctrl Pts',(-2.60077713054549,0.893567501277296,
12.4911020829134));
#417655=CARTESIAN_POINT('Ctrl Pts',(-2.60146958988548,0.891546954961492,
12.4915448903141));
#417656=CARTESIAN_POINT('Ctrl Pts',(-2.60265430343411,0.888090046435982,
12.4923024798169));
#417657=CARTESIAN_POINT('Ctrl Pts',(-2.60380416742372,0.884711060746445,
12.4937722312795));
#417658=CARTESIAN_POINT('Ctrl Pts',(-2.6048080817104,0.881745347283566,
12.4958030942394));
#417659=CARTESIAN_POINT('Ctrl Pts',(-2.60580491003127,0.878800566827061,
12.4978196226833));
#417660=CARTESIAN_POINT('Ctrl Pts',(-2.60668769694455,0.876176049187813,
12.5004326847668));
#417661=CARTESIAN_POINT('Ctrl Pts',(-2.60741373536419,0.874010075819612,
12.5033504258767));
#417662=CARTESIAN_POINT('Ctrl Pts',(-2.60828122303054,0.87142212023524,
12.5068366111226));
#417663=CARTESIAN_POINT('Ctrl Pts',(-2.60895310550328,0.869405599195268,
12.5108395010833));
#417664=CARTESIAN_POINT('Ctrl Pts',(-2.6094423180669,0.867934783656971,
12.5149868989719));
#417665=CARTESIAN_POINT('Ctrl Pts',(-2.61026399720937,0.865464408731773,
12.5219528491417));
#417666=CARTESIAN_POINT('Ctrl Pts',(-2.61060905307625,0.864419095114112,
12.5295503425868));
#417667=CARTESIAN_POINT('Ctrl Pts',(-2.61060905306387,0.864419095150584,
12.5369868989719));
#417668=CARTESIAN_POINT('',(-2.56005949631752,1.00428849207511,12.5369868989719));
#417669=CARTESIAN_POINT('Ctrl Pts',(-2.56005949631752,1.0042884920751,12.5369868989719));
#417670=CARTESIAN_POINT('Ctrl Pts',(-2.56005949631752,1.0042884920751,12.5309445149785));
#417671=CARTESIAN_POINT('Ctrl Pts',(-2.56032421406491,1.00361479833721,
12.5248274368704));
#417672=CARTESIAN_POINT('Ctrl Pts',(-2.56092788919928,1.00207202651372,
12.5190199595513));
#417673=CARTESIAN_POINT('Ctrl Pts',(-2.56143493843448,1.0007761949834,12.5141420429941));
#417674=CARTESIAN_POINT('Ctrl Pts',(-2.56219682783355,0.998827187236239,
12.5093757677094));
#417675=CARTESIAN_POINT('Ctrl Pts',(-2.5632425743599,0.996136288360594,
12.5051960112707));
#417676=CARTESIAN_POINT('Ctrl Pts',(-2.56394120513404,0.994338582399107,
12.5024036458141));
#417677=CARTESIAN_POINT('Ctrl Pts',(-2.56478330981982,0.992166109837743,
12.4998248032393));
#417678=CARTESIAN_POINT('Ctrl Pts',(-2.5657365634761,0.989694845314369,
12.4976950015772));
#417679=CARTESIAN_POINT('Ctrl Pts',(-2.56671667597669,0.987153950521416,
12.495505190692));
#417680=CARTESIAN_POINT('Ctrl Pts',(-2.56783936910761,0.984231597985143,
12.4937456938368));
#417681=CARTESIAN_POINT('Ctrl Pts',(-2.56901534632743,0.981152460290538,
12.4925987732155));
#417682=CARTESIAN_POINT('Ctrl Pts',(-2.5701910483731,0.978074043102282,
12.4914521209692));
#417683=CARTESIAN_POINT('Ctrl Pts',(-2.57144920234721,0.97476211405212,
12.4908873016276));
#417684=CARTESIAN_POINT('Ctrl Pts',(-2.57268207733792,0.971497261418812,
12.4908873016278));
#417685=CARTESIAN_POINT('',(-2.56005949631752,1.0042884920751,13.7435492065112));
#417686=CARTESIAN_POINT('',(-2.56005949631752,1.0042884920751,14.));
#417687=CARTESIAN_POINT('',(-2.53146428566977,1.07433168545774,13.7435492065112));
#417688=CARTESIAN_POINT('Origin',(0.,2.5406128344257E-15,13.7435492065112));
#417689=CARTESIAN_POINT('',(-2.53146428566977,1.07433168545774,12.5369868989719));
#417690=CARTESIAN_POINT('',(-2.53146428566977,1.07433168545774,14.));
#417691=CARTESIAN_POINT('Ctrl Pts',(-2.51753117879167,1.10658789249288,
12.4908873016278));
#417692=CARTESIAN_POINT('Ctrl Pts',(-2.51840893501265,1.10459096240835,
12.4908873016278));
#417693=CARTESIAN_POINT('Ctrl Pts',(-2.51928921236256,1.10258170970728,
12.4911020829134));
#417694=CARTESIAN_POINT('Ctrl Pts',(-2.52014406088379,1.10062432845734,
12.4915448903141));
#417695=CARTESIAN_POINT('Ctrl Pts',(-2.52160660253303,1.09727548766233,
12.4923024798169));
#417696=CARTESIAN_POINT('Ctrl Pts',(-2.52302805914774,1.0940014698589,12.4937722312795));
#417697=CARTESIAN_POINT('Ctrl Pts',(-2.52427036617201,1.09112745289717,
12.4958030942394));
#417698=CARTESIAN_POINT('Ctrl Pts',(-2.52550390457409,1.08827372171696,
12.4978196226833));
#417699=CARTESIAN_POINT('Ctrl Pts',(-2.52659767663917,1.08572989227247,
12.5004326847668));
#417700=CARTESIAN_POINT('Ctrl Pts',(-2.52749784616328,1.08363030487339,
12.5033504258767));
#417701=CARTESIAN_POINT('Ctrl Pts',(-2.52857338974152,1.0811216687959,12.5068366111226));
#417702=CARTESIAN_POINT('Ctrl Pts',(-2.52940740176599,1.07916662222232,
12.5108395010833));
#417703=CARTESIAN_POINT('Ctrl Pts',(-2.53001487163591,1.07774057606695,
12.5149868989719));
#417704=CARTESIAN_POINT('Ctrl Pts',(-2.53103517519907,1.07534539558874,
12.5219528491417));
#417705=CARTESIAN_POINT('Ctrl Pts',(-2.53146428568508,1.0743316854224,12.5295503425868));
#417706=CARTESIAN_POINT('Ctrl Pts',(-2.53146428566977,1.07433168545774,
12.5369868989719));
#417707=CARTESIAN_POINT('',(-2.46968227406997,1.20961542034839,12.5369868989719));
#417708=CARTESIAN_POINT('Ctrl Pts',(-2.46968227406996,1.20961542034839,
12.5369868989719));
#417709=CARTESIAN_POINT('Ctrl Pts',(-2.46968227406996,1.20961542034839,
12.5309445149785));
#417710=CARTESIAN_POINT('Ctrl Pts',(-2.4700010232848,1.20896554522477,12.5248274368704));
#417711=CARTESIAN_POINT('Ctrl Pts',(-2.47072843996596,1.20747711197495,
12.5190199595513));
#417712=CARTESIAN_POINT('Ctrl Pts',(-2.47133942433629,1.20622692143703,
12.5141420429941));
#417713=CARTESIAN_POINT('Ctrl Pts',(-2.47225764083634,1.20434649991142,
12.5093757677094));
#417714=CARTESIAN_POINT('Ctrl Pts',(-2.47351924096685,1.20174979282994,
12.5051960112707));
#417715=CARTESIAN_POINT('Ctrl Pts',(-2.47436207682967,1.2000150134806,12.5024036458141));
#417716=CARTESIAN_POINT('Ctrl Pts',(-2.47537845616357,1.19791840899208,
12.4998248032393));
#417717=CARTESIAN_POINT('Ctrl Pts',(-2.47652996894771,1.19553306642011,
12.4976950015772));
#417718=CARTESIAN_POINT('Ctrl Pts',(-2.47771392671894,1.19308051451269,
12.495505190692));
#417719=CARTESIAN_POINT('Ctrl Pts',(-2.47907108304259,1.19025939577614,
12.4937456938368));
#417720=CARTESIAN_POINT('Ctrl Pts',(-2.48049412560265,1.18728635671886,
12.4925987732155));
#417721=CARTESIAN_POINT('Ctrl Pts',(-2.48191683517623,1.18431401334126,
12.4914521209692));
#417722=CARTESIAN_POINT('Ctrl Pts',(-2.48344075571082,1.18111565569081,
12.4908873016276));
#417723=CARTESIAN_POINT('Ctrl Pts',(-2.48493564421073,1.17796215734251,
12.4908873016278));
#417724=CARTESIAN_POINT('',(-2.46968227406996,1.20961542034839,13.7435492065112));
#417725=CARTESIAN_POINT('',(-2.46968227406997,1.20961542034839,14.));
#417726=CARTESIAN_POINT('',(-2.43547304111673,1.27709477565043,13.7435492065112));
#417727=CARTESIAN_POINT('Origin',(0.,2.5406128344257E-15,13.7435492065112));
#417728=CARTESIAN_POINT('',(-2.43547304111673,1.27709477565043,12.5369868989719));
#417729=CARTESIAN_POINT('',(-2.43547304111674,1.27709477565043,14.));
#417730=CARTESIAN_POINT('Ctrl Pts',(-2.41895711517699,1.30810797525839,
12.4908873016278));
#417731=CARTESIAN_POINT('Ctrl Pts',(-2.41999471907704,1.30618923507468,
12.4908873016278));
#417732=CARTESIAN_POINT('Ctrl Pts',(-2.42103584012481,1.30425841877233,
12.4911020829134));
#417733=CARTESIAN_POINT('Ctrl Pts',(-2.42204738895142,1.30237722863754,
12.4915448903141));
#417734=CARTESIAN_POINT('Ctrl Pts',(-2.42377802572789,1.299158741556,12.4923024798169));
#417735=CARTESIAN_POINT('Ctrl Pts',(-2.42546161540846,1.29601147968699,
12.4937722312795));
#417736=CARTESIAN_POINT('Ctrl Pts',(-2.42693404782204,1.29324828533509,
12.4958030942394));
#417737=CARTESIAN_POINT('Ctrl Pts',(-2.42839608731078,1.29050459454135,
12.4978196226833));
#417738=CARTESIAN_POINT('Ctrl Pts',(-2.42969356565503,1.28805838205688,
12.5004326847668));
#417739=CARTESIAN_POINT('Ctrl Pts',(-2.43076187580395,1.28603915303464,
12.5033504258767));
#417740=CARTESIAN_POINT('Ctrl Pts',(-2.43203831772902,1.28362653102324,
12.5068366111226));
#417741=CARTESIAN_POINT('Ctrl Pts',(-2.43302890909279,1.28174596942844,
12.5108395010833));
#417742=CARTESIAN_POINT('Ctrl Pts',(-2.43375059365726,1.28037418275789,
12.5149868989719));
#417743=CARTESIAN_POINT('Ctrl Pts',(-2.43496273168923,1.27807013625756,
12.5219528491417));
#417744=CARTESIAN_POINT('Ctrl Pts',(-2.43547304113487,1.27709477561645,
12.5295503425868));
#417745=CARTESIAN_POINT('Ctrl Pts',(-2.43547304111673,1.27709477565043,
12.5369868989719));
#417746=CARTESIAN_POINT('',(-2.36286972375737,1.40689255757176,12.5369868989719));
#417747=CARTESIAN_POINT('Ctrl Pts',(-2.36286972375737,1.40689255757175,
12.5369868989719));
#417748=CARTESIAN_POINT('Ctrl Pts',(-2.36286972375737,1.40689255757175,
12.5309445149785));
#417749=CARTESIAN_POINT('Ctrl Pts',(-2.3632403832162,1.40627082587413,12.5248274368704));
#417750=CARTESIAN_POINT('Ctrl Pts',(-2.36408670060617,1.40484663647568,
12.5190199595513));
#417751=CARTESIAN_POINT('Ctrl Pts',(-2.36479755411145,1.40365040674193,
12.5141420429941));
#417752=CARTESIAN_POINT('Ctrl Pts',(-2.36586598713316,1.40185108533289,
12.5093757677094));
#417753=CARTESIAN_POINT('Ctrl Pts',(-2.3673350451271,1.39936585070276,12.5051960112707));
#417754=CARTESIAN_POINT('Ctrl Pts',(-2.368316477145,1.39770554263593,12.5024036458141));
#417755=CARTESIAN_POINT('Ctrl Pts',(-2.36950036729026,1.3956987587772,12.4998248032393));
#417756=CARTESIAN_POINT('Ctrl Pts',(-2.37084247607465,1.39341521221789,
12.4976950015772));
#417757=CARTESIAN_POINT('Ctrl Pts',(-2.37222240007291,1.3910673245243,12.495505190692));
#417758=CARTESIAN_POINT('Ctrl Pts',(-2.37380498793786,1.38836621366723,
12.4937456938368));
#417759=CARTESIAN_POINT('Ctrl Pts',(-2.37546562572471,1.38551905833168,
12.4925987732155));
#417760=CARTESIAN_POINT('Ctrl Pts',(-2.37712587492872,1.3826725692195,12.4914521209692));
#417761=CARTESIAN_POINT('Ctrl Pts',(-2.37890542058405,1.37960906751125,
12.4908873016276));
#417762=CARTESIAN_POINT('Ctrl Pts',(-2.38065237435684,1.37658790945917,
12.4908873016278));
#417763=CARTESIAN_POINT('',(-2.36286972375737,1.40689255757175,13.7435492065112));
#417764=CARTESIAN_POINT('',(-2.36286972375737,1.40689255757175,14.));
#417765=CARTESIAN_POINT('',(-2.32327412529984,1.47135901081696,13.7435492065112));
#417766=CARTESIAN_POINT('Origin',(0.,2.5406128344257E-15,13.7435492065112));
#417767=CARTESIAN_POINT('',(-2.32327412529984,1.47135901081697,12.5369868989719));
#417768=CARTESIAN_POINT('',(-2.32327412529984,1.47135901081697,14.));
#417769=CARTESIAN_POINT('Ctrl Pts',(-2.30428529106065,1.50092281527118,
12.4908873016278));
#417770=CARTESIAN_POINT('Ctrl Pts',(-2.305475837557,1.49909503388765,12.4908873016278));
#417771=CARTESIAN_POINT('Ctrl Pts',(-2.30667087381384,1.49725550324795,
12.4911020829134));
#417772=CARTESIAN_POINT('Ctrl Pts',(-2.30783239125528,1.49546302323827,
12.4915448903141));
#417773=CARTESIAN_POINT('Ctrl Pts',(-2.30981960605676,1.49239630837073,
12.4923024798169));
#417774=CARTESIAN_POINT('Ctrl Pts',(-2.31175412479163,1.48939674694459,
12.4937722312795));
#417775=CARTESIAN_POINT('Ctrl Pts',(-2.31344688379974,1.48676276380506,
12.4958030942394));
#417776=CARTESIAN_POINT('Ctrl Pts',(-2.31512769474357,1.48414737220734,
12.4978196226833));
#417777=CARTESIAN_POINT('Ctrl Pts',(-2.31662024486267,1.48181505582337,
12.5004326847668));
#417778=CARTESIAN_POINT('Ctrl Pts',(-2.31784958620863,1.47988962281398,
12.5033504258767));
#417779=CARTESIAN_POINT('Ctrl Pts',(-2.31931843197011,1.4775890704701,12.5068366111226));
#417780=CARTESIAN_POINT('Ctrl Pts',(-2.32045901045109,1.47579550868121,
12.5108395010833));
#417781=CARTESIAN_POINT('Ctrl Pts',(-2.32129010701841,1.47448711050944,
12.5149868989719));
#417782=CARTESIAN_POINT('Ctrl Pts',(-2.32268601294057,1.47228953103631,
12.5219528491417));
#417783=CARTESIAN_POINT('Ctrl Pts',(-2.32327412532069,1.47135901078458,
12.5295503425868));
#417784=CARTESIAN_POINT('Ctrl Pts',(-2.32327412529984,1.47135901081697,
12.5369868989719));
#417785=CARTESIAN_POINT('',(-2.24033266527923,1.59480705694541,12.5369868989719));
#417786=CARTESIAN_POINT('Ctrl Pts',(-2.24033266527923,1.59480705694541,
12.5369868989719));
#417787=CARTESIAN_POINT('Ctrl Pts',(-2.24033266527923,1.59480705694541,
12.5309445149785));
#417788=CARTESIAN_POINT('Ctrl Pts',(-2.24075276830452,1.59421760619565,
12.5248274368704));
#417789=CARTESIAN_POINT('Ctrl Pts',(-2.2417123543007,1.59286713839405,12.5190199595513));
#417790=CARTESIAN_POINT('Ctrl Pts',(-2.24251834632814,1.59173283017597,
12.5141420429941));
#417791=CARTESIAN_POINT('Ctrl Pts',(-2.24372988562603,1.5900265830706,12.5093757677094));
#417792=CARTESIAN_POINT('Ctrl Pts',(-2.24539662514483,1.58766935971827,
12.5051960112707));
#417793=CARTESIAN_POINT('Ctrl Pts',(-2.24651012204964,1.58609457201019,
12.5024036458141));
#417794=CARTESIAN_POINT('Ctrl Pts',(-2.24785364441266,1.58419096359675,
12.4998248032393));
#417795=CARTESIAN_POINT('Ctrl Pts',(-2.24937741768479,1.58202440967569,
12.4976950015772));
#417796=CARTESIAN_POINT('Ctrl Pts',(-2.25094412474353,1.57979681100116,
12.495505190692));
#417797=CARTESIAN_POINT('Ctrl Pts',(-2.25274161228866,1.57723368347067,
12.4937456938368));
#417798=CARTESIAN_POINT('Ctrl Pts',(-2.25462879403181,1.57453135920586,
12.4925987732155));
#417799=CARTESIAN_POINT('Ctrl Pts',(-2.25651553418172,1.57182966727451,
12.4914521209692));
#417800=CARTESIAN_POINT('Ctrl Pts',(-2.25853886237507,1.56892140860688,
12.4908873016276));
#417801=CARTESIAN_POINT('Ctrl Pts',(-2.2605262557316,1.56605269615939,12.4908873016278));
#417802=CARTESIAN_POINT('',(-2.24033266527923,1.59480705694541,13.7435492065112));
#417803=CARTESIAN_POINT('',(-2.24033266527923,1.59480705694541,14.));
#417804=CARTESIAN_POINT('',(-2.19561420349232,1.65583159452367,13.7435492065112));
#417805=CARTESIAN_POINT('Origin',(0.,2.5406128344257E-15,13.7435492065112));
#417806=CARTESIAN_POINT('',(-2.19561420349232,1.65583159452367,12.5369868989719));
#417807=CARTESIAN_POINT('',(-2.19561420349232,1.65583159452367,14.));
#417808=CARTESIAN_POINT('Ctrl Pts',(-2.1742788285126,1.68374926158317,12.4908873016278));
#417809=CARTESIAN_POINT('Ctrl Pts',(-2.17561439471476,1.68202460258336,
12.4908873016278));
#417810=CARTESIAN_POINT('Ctrl Pts',(-2.17695539341154,1.68028859937922,
12.4911020829134));
#417811=CARTESIAN_POINT('Ctrl Pts',(-2.17825914976087,1.67859675815339,
12.4915448903141));
#417812=CARTESIAN_POINT('Ctrl Pts',(-2.18048971800073,1.6757022239813,12.4923024798169));
#417813=CARTESIAN_POINT('Ctrl Pts',(-2.1826622918869,1.67287032458445,12.4937722312795));
#417814=CARTESIAN_POINT('Ctrl Pts',(-2.18456411245763,1.6703830813805,12.4958030942394));
#417815=CARTESIAN_POINT('Ctrl Pts',(-2.18645250933703,1.66791339397838,
12.4978196226833));
#417816=CARTESIAN_POINT('Ctrl Pts',(-2.1881301985562,1.66571049487564,12.5004326847668));
#417817=CARTESIAN_POINT('Ctrl Pts',(-2.18951239003535,1.66389167131809,
12.5033504258767));
#417818=CARTESIAN_POINT('Ctrl Pts',(-2.19116386470704,1.66171849843801,
12.5068366111226));
#417819=CARTESIAN_POINT('Ctrl Pts',(-2.19244683994363,1.66002387231283,
12.5108395010833));
#417820=CARTESIAN_POINT('Ctrl Pts',(-2.19338181770325,1.6587875698138,12.5149868989719));
#417821=CARTESIAN_POINT('Ctrl Pts',(-2.19495220199201,1.6567110818967,12.5219528491417));
#417822=CARTESIAN_POINT('Ctrl Pts',(-2.19561420351574,1.65583159449309,
12.5295503425868));
#417823=CARTESIAN_POINT('Ctrl Pts',(-2.19561420349232,1.65583159452367,
12.5369868989719));
#417824=CARTESIAN_POINT('',(-2.10288656254252,1.77210837847974,12.5369868989719));
#417825=CARTESIAN_POINT('Ctrl Pts',(-2.10288656254252,1.77210837847974,
12.5369868989719));
#417826=CARTESIAN_POINT('Ctrl Pts',(-2.10288656254253,1.77210837847974,
12.5309445149785));
#417827=CARTESIAN_POINT('Ctrl Pts',(-2.10335331341796,1.77155513137533,
12.5248274368704));
#417828=CARTESIAN_POINT('Ctrl Pts',(-2.10441978213385,1.77028737231098,
12.5190199595513));
#417829=CARTESIAN_POINT('Ctrl Pts',(-2.10531554893949,1.76922253424263,
12.5141420429941));
#417830=CARTESIAN_POINT('Ctrl Pts',(-2.10666213191942,1.76762071623391,
12.5093757677094));
#417831=CARTESIAN_POINT('Ctrl Pts',(-2.10851546108658,1.76540719109186,
12.5051960112707));
#417832=CARTESIAN_POINT('Ctrl Pts',(-2.10975361274012,1.76392840369491,
12.5024036458141));
#417833=CARTESIAN_POINT('Ctrl Pts',(-2.11124782640125,1.76214063892666,
12.4998248032393));
#417834=CARTESIAN_POINT('Ctrl Pts',(-2.11294312370139,1.76010549570275,
12.4976950015772));
#417835=CARTESIAN_POINT('Ctrl Pts',(-2.11468618764363,1.75801301034894,
12.495505190692));
#417836=CARTESIAN_POINT('Ctrl Pts',(-2.11668661288588,1.75560492333584,
12.4937456938368));
#417837=CARTESIAN_POINT('Ctrl Pts',(-2.1187877797022,1.75306541366391,12.4925987732155));
#417838=CARTESIAN_POINT('Ctrl Pts',(-2.12088845485359,1.75052649822744,
12.4914521209692));
#417839=CARTESIAN_POINT('Ctrl Pts',(-2.12314210066966,1.74779283658204,
12.4908873016276));
#417840=CARTESIAN_POINT('Ctrl Pts',(-2.12535670783504,1.74509566054718,
12.4908873016278));
#417841=CARTESIAN_POINT('',(-2.10288656254252,1.77210837847974,13.7435492065112));
#417842=CARTESIAN_POINT('',(-2.10288656254253,1.77210837847974,14.));
#417843=CARTESIAN_POINT('',(-2.05334283141141,1.82928489216179,13.7435492065112));
#417844=CARTESIAN_POINT('Origin',(0.,2.5406128344257E-15,13.7435492065112));
#417845=CARTESIAN_POINT('',(-2.05334283141141,1.8292848921618,12.5369868989719));
#417846=CARTESIAN_POINT('',(-2.05334283141141,1.8292848921618,14.));
#417847=CARTESIAN_POINT('Ctrl Pts',(-2.02980289909156,1.8553706343584,12.4908873016278));
#417848=CARTESIAN_POINT('Ctrl Pts',(-2.03127459702679,1.8537605750634,12.4908873016278));
#417849=CARTESIAN_POINT('Ctrl Pts',(-2.03275263403844,1.85213965210973,
12.4911020829134));
#417850=CARTESIAN_POINT('Ctrl Pts',(-2.03418995301227,1.85055970859196,
12.4915448903141));
#417851=CARTESIAN_POINT('Ctrl Pts',(-2.03664903062688,1.84785661776268,
12.4923024798169));
#417852=CARTESIAN_POINT('Ctrl Pts',(-2.03904520154358,1.84521122621838,
12.4937722312795));
#417853=CARTESIAN_POINT('Ctrl Pts',(-2.04114342737482,1.84288727514316,
12.4958030942394));
#417854=CARTESIAN_POINT('Ctrl Pts',(-2.04322684322012,1.84057972729882,
12.4978196226833));
#417855=CARTESIAN_POINT('Ctrl Pts',(-2.0450785067944,1.83852090540739,12.5004326847668));
#417856=CARTESIAN_POINT('Ctrl Pts',(-2.0466043501505,1.83682079527238,12.5033504258767));
#417857=CARTESIAN_POINT('Ctrl Pts',(-2.04842746344094,1.83478946396307,
12.5068366111226));
#417858=CARTESIAN_POINT('Ctrl Pts',(-2.04984429744461,1.83320505095887,
12.5108395010833));
#417859=CARTESIAN_POINT('Ctrl Pts',(-2.05087693427381,1.83204907152174,
12.5149868989719));
#417860=CARTESIAN_POINT('Ctrl Pts',(-2.05261134628081,1.83010749384515,
12.5219528491417));
#417861=CARTESIAN_POINT('Ctrl Pts',(-2.05334283143724,1.82928489213323,
12.5295503425868));
#417862=CARTESIAN_POINT('Ctrl Pts',(-2.05334283141141,1.8292848921618,12.5369868989719));
#417863=CARTESIAN_POINT('',(-1.95144609668396,1.93761661113259,12.5369868989719));
#417864=CARTESIAN_POINT('Ctrl Pts',(-1.95144609668396,1.93761661113259,
12.5369868989719));
#417865=CARTESIAN_POINT('Ctrl Pts',(-1.95144609668396,1.93761661113259,
12.5309445149785));
#417866=CARTESIAN_POINT('Ctrl Pts',(-1.95195638925947,1.93710324944173,
12.5248274368704));
#417867=CARTESIAN_POINT('Ctrl Pts',(-1.95312264352173,1.93592663584204,
12.5190199595513));
#417868=CARTESIAN_POINT('Ctrl Pts',(-1.95410222392526,1.93493835424507,
12.5141420429941));
#417869=CARTESIAN_POINT('Ctrl Pts',(-1.95557488929968,1.93345162516757,
12.5093757677094));
#417870=CARTESIAN_POINT('Ctrl Pts',(-1.95760247451537,1.93139652888042,
12.5051960112707));
#417871=CARTESIAN_POINT('Ctrl Pts',(-1.95895704122267,1.93002358288074,
12.5024036458141));
#417872=CARTESIAN_POINT('Ctrl Pts',(-1.96059200243651,1.92836355903727,
12.4998248032393));
#417873=CARTESIAN_POINT('Ctrl Pts',(-1.96244754184083,1.92647337005288,
12.4976950015772));
#417874=CARTESIAN_POINT('Ctrl Pts',(-1.96435536286362,1.92452992316457,
12.495505190692));
#417875=CARTESIAN_POINT('Ctrl Pts',(-1.96654541330306,1.92229290209064,
12.4937456938368));
#417876=CARTESIAN_POINT('Ctrl Pts',(-1.96884658227405,1.91993310702946,
12.4925987732155));
#417877=CARTESIAN_POINT('Ctrl Pts',(-1.97114721278038,1.91757386415122,
12.4914521209692));
#417878=CARTESIAN_POINT('Ctrl Pts',(-1.97361617857809,1.91503299159526,
12.4908873016276));
#417879=CARTESIAN_POINT('Ctrl Pts',(-1.97604326170702,1.91252530123455,
12.4908873016278));
#417880=CARTESIAN_POINT('',(-1.95144609668396,1.93761661113259,13.7435492065112));
#417881=CARTESIAN_POINT('',(-1.95144609668396,1.93761661113259,14.));
#417882=CARTESIAN_POINT('',(-1.89740680156517,1.99056460065335,13.7435492065112));
#417883=CARTESIAN_POINT('Origin',(0.,2.5406128344257E-15,13.7435492065112));
#417884=CARTESIAN_POINT('',(-1.89740680156517,1.99056460065335,12.5369868989719));
#417885=CARTESIAN_POINT('',(-1.89740680156517,1.99056460065335,14.));
#417886=CARTESIAN_POINT('Ctrl Pts',(-1.87181896627098,2.01464482167658,
12.4908873016278));
#417887=CARTESIAN_POINT('Ctrl Pts',(-1.87341700203234,2.01316007676537,
12.4908873016278));
#417888=CARTESIAN_POINT('Ctrl Pts',(-1.8750222412664,2.01166502103698,12.4911020829134));
#417889=CARTESIAN_POINT('Ctrl Pts',(-1.87658355774408,2.01020748949072,
12.4915448903141));
#417890=CARTESIAN_POINT('Ctrl Pts',(-1.87925477997766,2.00771383062773,
12.4923024798169));
#417891=CARTESIAN_POINT('Ctrl Pts',(-1.88185860180278,2.00527255158024,
12.4937722312795));
#417892=CARTESIAN_POINT('Ctrl Pts',(-1.88413926954779,2.00312735814474,
12.4958030942394));
#417893=CARTESIAN_POINT('Ctrl Pts',(-1.88640383957027,2.00099730620838,
12.4978196226833));
#417894=CARTESIAN_POINT('Ctrl Pts',(-1.88841715498409,1.99909626264826,
12.5004326847668));
#417895=CARTESIAN_POINT('Ctrl Pts',(-1.89007649598135,1.99752617988823,
12.5033504258767));
#417896=CARTESIAN_POINT('Ctrl Pts',(-1.89205911537238,1.99565020832441,
12.5068366111226));
#417897=CARTESIAN_POINT('Ctrl Pts',(-1.8936003793466,1.99418655244832,12.5108395010833));
#417898=CARTESIAN_POINT('Ctrl Pts',(-1.89472380321766,1.99311858892551,
12.5149868989719));
#417899=CARTESIAN_POINT('Ctrl Pts',(-1.89661070071715,1.99132484236854,
12.5219528491417));
#417900=CARTESIAN_POINT('Ctrl Pts',(-1.89740680159325,1.99056460062698,
12.5295503425868));
#417901=CARTESIAN_POINT('Ctrl Pts',(-1.89740680156517,1.99056460065335,
12.5369868989719));
#417902=CARTESIAN_POINT('',(-1.78701907901791,2.09023032492259,12.5369868989719));
#417903=CARTESIAN_POINT('Ctrl Pts',(-1.78701907901791,2.09023032492259,
12.5369868989719));
#417904=CARTESIAN_POINT('Ctrl Pts',(-1.78701907901791,2.09023032492258,
12.5309445149785));
#417905=CARTESIAN_POINT('Ctrl Pts',(-1.78756951738059,2.08976026498263,
12.5248274368704));
#417906=CARTESIAN_POINT('Ctrl Pts',(-1.78882779595953,2.08868262701698,
12.5190199595513));
#417907=CARTESIAN_POINT('Ctrl Pts',(-1.78988467101499,2.08777747874237,
12.5141420429941));
#417908=CARTESIAN_POINT('Ctrl Pts',(-1.79147361843879,2.0864157325328,12.5093757677094));
#417909=CARTESIAN_POINT('Ctrl Pts',(-1.79366196645792,2.08453274142727,
12.5051960112707));
#417910=CARTESIAN_POINT('Ctrl Pts',(-1.79512393380103,2.08327477355398,
12.5024036458141));
#417911=CARTESIAN_POINT('Ctrl Pts',(-1.79688876217047,2.08175353782007,
12.4998248032393));
#417912=CARTESIAN_POINT('Ctrl Pts',(-1.79889219537038,2.08002088197103,
12.4976950015772));
#417913=CARTESIAN_POINT('Ctrl Pts',(-1.80095207723957,2.07823940686663,
12.495505190692));
#417914=CARTESIAN_POINT('Ctrl Pts',(-1.80331717845186,2.07618833873803,
12.4937456938368));
#417915=CARTESIAN_POINT('Ctrl Pts',(-1.80580303567769,2.07402396233439,
12.4925987732155));
#417916=CARTESIAN_POINT('Ctrl Pts',(-1.80828831122251,2.07186009238648,
12.4914521209692));
#417917=CARTESIAN_POINT('Ctrl Pts',(-1.81095616644182,2.06952891800762,
12.4908873016276));
#417918=CARTESIAN_POINT('Ctrl Pts',(-1.81357957369652,2.06722740158666,
12.4908873016278));
#417919=CARTESIAN_POINT('',(-1.78701907901791,2.09023032492258,13.7435492065112));
#417920=CARTESIAN_POINT('',(-1.78701907901791,2.09023032492259,14.));
#417921=CARTESIAN_POINT('',(-1.72884384250461,2.1385974301476,13.7435492065112));
#417922=CARTESIAN_POINT('Origin',(0.,2.5406128344257E-15,13.7435492065112));
#417923=CARTESIAN_POINT('',(-1.72884384250461,2.1385974301476,12.5369868989719));
#417924=CARTESIAN_POINT('',(-1.72884384250461,2.1385974301476,14.));
#417925=CARTESIAN_POINT('Ctrl Pts',(-1.70137838705825,2.1605118800995,12.4908873016278));
#417926=CARTESIAN_POINT('Ctrl Pts',(-1.7030921259814,2.15916233030449,12.4908873016278));
#417927=CARTESIAN_POINT('Ctrl Pts',(-1.70481388483562,2.15780309115059,
12.4911020829134));
#417928=CARTESIAN_POINT('Ctrl Pts',(-1.70648880851361,2.1564776712078,12.4915448903141));
#417929=CARTESIAN_POINT('Ctrl Pts',(-1.70935439882289,2.15421003919943,
12.4923024798169));
#417930=CARTESIAN_POINT('Ctrl Pts',(-1.71214854355179,2.15198911895802,
12.4937722312795));
#417931=CARTESIAN_POINT('Ctrl Pts',(-1.71459647574302,2.15003695907061,
12.4958030942394));
#417932=CARTESIAN_POINT('Ctrl Pts',(-1.71702712960282,2.14809857818643,
12.4978196226833));
#417933=CARTESIAN_POINT('Ctrl Pts',(-1.71918869857426,2.14636796408887,
12.5004326847668));
#417934=CARTESIAN_POINT('Ctrl Pts',(-1.72097049457212,2.14493835734555,
12.5033504258767));
#417935=CARTESIAN_POINT('Ctrl Pts',(-1.7230994260588,2.14323022980845,12.5068366111226));
#417936=CARTESIAN_POINT('Ctrl Pts',(-1.72475486314611,2.14189707144884,
12.5108395010833));
#417937=CARTESIAN_POINT('Ctrl Pts',(-1.72596159785851,2.14092423096141,
12.5149868989719));
#417938=CARTESIAN_POINT('Ctrl Pts',(-1.72798842385895,2.13929025261145,
12.5219528491417));
#417939=CARTESIAN_POINT('Ctrl Pts',(-1.72884384253474,2.13859743012361,
12.5295503425868));
#417940=CARTESIAN_POINT('Ctrl Pts',(-1.72884384250461,2.1385974301476,12.5369868989719));
#417941=CARTESIAN_POINT('',(-1.61069974421839,2.22893390076396,12.5369868989719));
#417942=CARTESIAN_POINT('Ctrl Pts',(-1.61069974421839,2.22893390076395,
12.5369868989719));
#417943=CARTESIAN_POINT('Ctrl Pts',(-1.61069974421839,2.22893390076395,
12.5309445149785));
#417944=CARTESIAN_POINT('Ctrl Pts',(-1.61128666529176,2.22851027074625,
12.5248274368704));
#417945=CARTESIAN_POINT('Ctrl Pts',(-1.61262859455103,2.22753877991751,
12.5190199595513));
#417946=CARTESIAN_POINT('Ctrl Pts',(-1.61375573092929,2.22672278857768,
12.5141420429941));
#417947=CARTESIAN_POINT('Ctrl Pts',(-1.61545038621954,2.22549508743239,
12.5093757677094));
#417948=CARTESIAN_POINT('Ctrl Pts',(-1.6177849339471,2.22379673250362,12.5051960112707));
#417949=CARTESIAN_POINT('Ctrl Pts',(-1.61934457277456,2.22266211432536,
12.5024036458141));
#417950=CARTESIAN_POINT('Ctrl Pts',(-1.62122752365795,2.22128979027384,
12.4998248032393));
#417951=CARTESIAN_POINT('Ctrl Pts',(-1.62336551813605,2.21972619809896,
12.4976950015772));
#417952=CARTESIAN_POINT('Ctrl Pts',(-1.62556375267767,2.21811855020135,
12.495505190692));
#417953=CARTESIAN_POINT('Ctrl Pts',(-1.62808816530445,2.21626708453809,
12.4937456938368));
#417954=CARTESIAN_POINT('Ctrl Pts',(-1.63074216781542,2.21431253035986,
12.4925987732155));
#417955=CARTESIAN_POINT('Ctrl Pts',(-1.63339554930003,2.21235843353977,
12.4914521209692));
#417956=CARTESIAN_POINT('Ctrl Pts',(-1.63624453980463,2.21025247091888,
12.4908873016276));
#417957=CARTESIAN_POINT('Ctrl Pts',(-1.63904681284264,2.20817244464973,
12.4908873016278));
#417958=CARTESIAN_POINT('',(-1.61069974421839,2.22893390076395,13.7435492065112));
#417959=CARTESIAN_POINT('',(-1.61069974421839,2.22893390076395,14.));
#417960=CARTESIAN_POINT('',(-1.54877571291133,2.27239824658795,13.7435492065112));
#417961=CARTESIAN_POINT('Origin',(0.,2.5406128344257E-15,13.7435492065112));
#417962=CARTESIAN_POINT('',(-1.54877571291133,2.27239824658796,12.5369868989719));
#417963=CARTESIAN_POINT('',(-1.54877571291133,2.27239824658796,14.));
#417964=CARTESIAN_POINT('Ctrl Pts',(-1.51961541538732,2.29200108841973,
12.4908873016278));
#417965=CARTESIAN_POINT('Ctrl Pts',(-1.52143345282248,2.29079571477214,
12.4908873016278));
#417966=CARTESIAN_POINT('Ctrl Pts',(-1.52326027327575,2.28958133770505,
12.4911020829134));
#417967=CARTESIAN_POINT('Ctrl Pts',(-1.52503765781331,2.28839684981677,
12.4915448903141));
#417968=CARTESIAN_POINT('Ctrl Pts',(-1.52807854616758,2.28637033537988,
12.4923024798169));
#417969=CARTESIAN_POINT('Ctrl Pts',(-1.53104441922809,2.28438455380235,
12.4937722312795));
#417970=CARTESIAN_POINT('Ctrl Pts',(-1.53364332528069,2.282638418765,12.4958030942394));
#417971=CARTESIAN_POINT('Ctrl Pts',(-1.53622388737739,2.28090460853797,
12.4978196226833));
#417972=CARTESIAN_POINT('Ctrl Pts',(-1.53851932502158,2.27935594085425,
12.5004326847668));
#417973=CARTESIAN_POINT('Ctrl Pts',(-1.54041171846165,2.27807632392465,
12.5033504258767));
#417974=CARTESIAN_POINT('Ctrl Pts',(-1.54267279435619,2.27654740772122,
12.5068366111226));
#417975=CARTESIAN_POINT('Ctrl Pts',(-1.5444313878959,2.27535361882702,12.5108395010833));
#417976=CARTESIAN_POINT('Ctrl Pts',(-1.54571340282923,2.2744823754679,12.5149868989719));
#417977=CARTESIAN_POINT('Ctrl Pts',(-1.547866669138,2.27301903918127,12.5219528491417));
#417978=CARTESIAN_POINT('Ctrl Pts',(-1.54877571294331,2.2723982465665,12.5295503425868));
#417979=CARTESIAN_POINT('Ctrl Pts',(-1.54877571291133,2.27239824658796,
12.5369868989719));
#417980=CARTESIAN_POINT('',(-1.42366146836785,2.35280428924395,12.5369868989719));
#417981=CARTESIAN_POINT('Ctrl Pts',(-1.42366146836785,2.35280428924394,
12.5369868989719));
#417982=CARTESIAN_POINT('Ctrl Pts',(-1.42366146836785,2.35280428924394,
12.5309445149785));
#417983=CARTESIAN_POINT('Ctrl Pts',(-1.42428096628899,2.35242990833637,
12.5248274368704));
#417984=CARTESIAN_POINT('Ctrl Pts',(-1.42569761591078,2.35157102975571,
12.5190199595513));
#417985=CARTESIAN_POINT('Ctrl Pts',(-1.42688751270522,2.3508496256384,12.5141420429941));
#417986=CARTESIAN_POINT('Ctrl Pts',(-1.42867659821055,2.34976413970596,
12.5093757677094));
#417987=CARTESIAN_POINT('Ctrl Pts',(-1.43114180961658,2.34826172322579,
12.5051960112707));
#417988=CARTESIAN_POINT('Ctrl Pts',(-1.43278874078931,2.34725800543934,
12.5024036458141));
#417989=CARTESIAN_POINT('Ctrl Pts',(-1.43477728345921,2.34604372566035,
12.4998248032393));
#417990=CARTESIAN_POINT('Ctrl Pts',(-1.43703561121499,2.34465960260759,
12.4976950015772));
#417991=CARTESIAN_POINT('Ctrl Pts',(-1.43935756954084,2.34323648054829,
12.495505190692));
#417992=CARTESIAN_POINT('Ctrl Pts',(-1.44202449403258,2.34159693854887,
12.4937456938368));
#417993=CARTESIAN_POINT('Ctrl Pts',(-1.44482897987985,2.33986521383163,
12.4925987732155));
#417994=CARTESIAN_POINT('Ctrl Pts',(-1.44763280948825,2.3381338943313,12.4914521209692));
#417995=CARTESIAN_POINT('Ctrl Pts',(-1.45064397571638,2.33626715830216,
12.4908873016276));
#417996=CARTESIAN_POINT('Ctrl Pts',(-1.45360646587299,2.33442246441647,
12.4908873016278));
#417997=CARTESIAN_POINT('',(-1.42366146836785,2.35280428924394,13.7435492065112));
#417998=CARTESIAN_POINT('',(-1.42366146836785,2.35280428924395,14.));
#417999=CARTESIAN_POINT('',(-1.35840073647863,2.39107662761659,13.7435492065112));
#418000=CARTESIAN_POINT('Origin',(0.,2.5406128344257E-15,13.7435492065112));
#418001=CARTESIAN_POINT('',(-1.35840073647863,2.39107662761659,12.5369868989719));
#418002=CARTESIAN_POINT('',(-1.35840073647863,2.39107662761659,14.));
#418003=CARTESIAN_POINT('Ctrl Pts',(-1.32773965384588,2.40823740765009,
12.4908873016278));
#418004=CARTESIAN_POINT('Ctrl Pts',(-1.32964989105388,2.40718423171268,
12.4908873016278));
#418005=CARTESIAN_POINT('Ctrl Pts',(-1.33156961591748,2.40612279821141,
12.4911020829134));
#418006=CARTESIAN_POINT('Ctrl Pts',(-1.33343763311376,2.40508712494911,
12.4915448903141));
#418007=CARTESIAN_POINT('Ctrl Pts',(-1.33663358290274,2.40331521420294,
12.4923024798169));
#418008=CARTESIAN_POINT('Ctrl Pts',(-1.33975144689897,2.40157778633805,
12.4937722312795));
#418009=CARTESIAN_POINT('Ctrl Pts',(-1.34248403152195,2.40004929639134,
12.4958030942394));
#418010=CARTESIAN_POINT('Ctrl Pts',(-1.34519732864057,2.39853159504246,
12.4978196226833));
#418011=CARTESIAN_POINT('Ctrl Pts',(-1.34761135919871,2.39717517990051,
12.5004326847668));
#418012=CARTESIAN_POINT('Ctrl Pts',(-1.34960175651487,2.39605406842417,
12.5033504258767));
#418013=CARTESIAN_POINT('Ctrl Pts',(-1.35197992973024,2.39471453823949,
12.5068366111226));
#418014=CARTESIAN_POINT('Ctrl Pts',(-1.35382997657249,2.39366806327883,
12.5108395010833));
#418015=CARTESIAN_POINT('Ctrl Pts',(-1.35517874012889,2.39290421502882,
12.5149868989719));
#418016=CARTESIAN_POINT('Ctrl Pts',(-1.35744411711395,2.39162125906708,
12.5219528491417));
#418017=CARTESIAN_POINT('Ctrl Pts',(-1.35840073651226,2.39107662759781,
12.5295503425868));
#418018=CARTESIAN_POINT('Ctrl Pts',(-1.35840073647863,2.39107662761659,
12.5369868989719));
#418019=CARTESIAN_POINT('',(-1.22714896033293,2.4610171533644,12.5369868989719));
#418020=CARTESIAN_POINT('Ctrl Pts',(-1.22714896033293,2.4610171533644,12.5369868989719));
#418021=CARTESIAN_POINT('Ctrl Pts',(-1.22714896033293,2.4610171533644,12.5309445149785));
#418022=CARTESIAN_POINT('Ctrl Pts',(-1.2277969124454,2.46069451301012,12.5248274368704));
#418023=CARTESIAN_POINT('Ctrl Pts',(-1.22927885486019,2.4599539623728,12.5190199595513));
#418024=CARTESIAN_POINT('Ctrl Pts',(-1.23052359350396,2.45933194630339,
12.5141420429941));
#418025=CARTESIAN_POINT('Ctrl Pts',(-1.23239520315551,2.45839589931358,
12.5093757677094));
#418026=CARTESIAN_POINT('Ctrl Pts',(-1.23497467266485,2.45709941961581,
12.5051960112707));
#418027=CARTESIAN_POINT('Ctrl Pts',(-1.23669793612762,2.45623328179743,
12.5024036458141));
#418028=CARTESIAN_POINT('Ctrl Pts',(-1.23877883716064,2.45518512712256,
12.4998248032393));
#418029=CARTESIAN_POINT('Ctrl Pts',(-1.24114246939548,2.45398968430246,
12.4976950015772));
#418030=CARTESIAN_POINT('Ctrl Pts',(-1.243572699256,2.45276055872399,12.495505190692));
#418031=CARTESIAN_POINT('Ctrl Pts',(-1.24636438767022,2.45134385126991,
12.4937456938368));
#418032=CARTESIAN_POINT('Ctrl Pts',(-1.24930069346319,2.44984648035594,
12.4925987732155));
#418033=CARTESIAN_POINT('Ctrl Pts',(-1.25223631217193,2.44834945982099,
12.4914521209692));
#418034=CARTESIAN_POINT('Ctrl Pts',(-1.25538961530914,2.44673437320389,
12.4908873016276));
#418035=CARTESIAN_POINT('Ctrl Pts',(-1.25849260770113,2.44513728783511,
12.4908873016278));
#418036=CARTESIAN_POINT('',(-1.22714896033293,2.4610171533644,13.7435492065112));
#418037=CARTESIAN_POINT('',(-1.22714896033293,2.4610171533644,14.));
#418038=CARTESIAN_POINT('',(-1.15898582726502,2.49384278818831,13.7435492065112));
#418039=CARTESIAN_POINT('Origin',(0.,2.5406128344257E-15,13.7435492065112));
#418040=CARTESIAN_POINT('',(-1.15898582726502,2.49384278818831,12.5369868989719));
#418041=CARTESIAN_POINT('',(-1.15898582726502,2.49384278818831,14.));
#418042=CARTESIAN_POINT('Ctrl Pts',(-1.12702800396973,2.50844730426374,
12.4908873016278));
#418043=CARTESIAN_POINT('Ctrl Pts',(-1.12901772863711,2.50755333474861,
12.4908873016278));
#418044=CARTESIAN_POINT('Ctrl Pts',(-1.13101758245881,2.506651908478,12.4911020829134));
#418045=CARTESIAN_POINT('Ctrl Pts',(-1.13296380096757,2.50577194207636,
12.4915448903141));
#418046=CARTESIAN_POINT('Ctrl Pts',(-1.13629354367271,2.50426642679458,
12.4923024798169));
#418047=CARTESIAN_POINT('Ctrl Pts',(-1.13954264973418,2.50278891493811,
12.4937722312795));
#418048=CARTESIAN_POINT('Ctrl Pts',(-1.14239072802771,2.50148824193046,
12.4958030942394));
#418049=CARTESIAN_POINT('Ctrl Pts',(-1.14521870362358,2.5001967495118,12.4978196226833));
#418050=CARTESIAN_POINT('Ctrl Pts',(-1.1477352621206,2.49904161363059,12.5004326847668));
#418051=CARTESIAN_POINT('Ctrl Pts',(-1.14981041754709,2.49808646841942,
12.5033504258767));
#418052=CARTESIAN_POINT('Ctrl Pts',(-1.15228986173292,2.49694523860587,
12.5068366111226));
#418053=CARTESIAN_POINT('Ctrl Pts',(-1.15421905012122,2.49605304169695,
12.5108395010833));
#418054=CARTESIAN_POINT('Ctrl Pts',(-1.15562558650174,2.49540167184013,
12.5149868989719));
#418055=CARTESIAN_POINT('Ctrl Pts',(-1.15798799845303,2.49430763406354,
12.5219528491417));
#418056=CARTESIAN_POINT('Ctrl Pts',(-1.15898582730006,2.49384278817234,
12.5295503425868));
#418057=CARTESIAN_POINT('Ctrl Pts',(-1.15898582726502,2.49384278818831,
12.5369868989719));
#418058=CARTESIAN_POINT('',(-1.02246997843232,2.55285235436847,12.5369868989719));
#418059=CARTESIAN_POINT('Ctrl Pts',(-1.02246997843232,2.55285235436847,
12.5369868989719));
#418060=CARTESIAN_POINT('Ctrl Pts',(-1.02246997843232,2.55285235436847,
12.5309445149785));
#418061=CARTESIAN_POINT('Ctrl Pts',(-1.0231420727217,2.55258360168581,12.5248274368704));
#418062=CARTESIAN_POINT('Ctrl Pts',(-1.02467944584725,2.55196630723413,
12.5190199595513));
#418063=CARTESIAN_POINT('Ctrl Pts',(-1.02597074281003,2.55144781862693,
12.5141420429941));
#418064=CARTESIAN_POINT('Ctrl Pts',(-1.02791242135437,2.55066743981805,
12.5093757677094));
#418065=CARTESIAN_POINT('Ctrl Pts',(-1.030588983023,2.54958552476116,12.5051960112707));
#418066=CARTESIAN_POINT('Ctrl Pts',(-1.03237711074179,2.54886273091513,
12.5024036458141));
#418067=CARTESIAN_POINT('Ctrl Pts',(-1.03453652208488,2.5479876766408,12.4998248032393));
#418068=CARTESIAN_POINT('Ctrl Pts',(-1.03698972921624,2.5469888695281,12.4976950015772));
#418069=CARTESIAN_POINT('Ctrl Pts',(-1.03951205783267,2.54596192005838,
12.495505190692));
#418070=CARTESIAN_POINT('Ctrl Pts',(-1.04240993194356,2.54477747510402,
12.4937456938368));
#418071=CARTESIAN_POINT('Ctrl Pts',(-1.04545851705164,2.5435244227497,12.4925987732155));
#418072=CARTESIAN_POINT('Ctrl Pts',(-1.04850638880256,2.5422716636048,12.4914521209692));
#418073=CARTESIAN_POINT('Ctrl Pts',(-1.05178084413673,2.5409189745347,12.4908873016276));
#418074=CARTESIAN_POINT('Ctrl Pts',(-1.05500368886169,2.53958012602246,
12.4908873016278));
#418075=CARTESIAN_POINT('',(-1.02246997843232,2.55285235436846,13.7435492065112));
#418076=CARTESIAN_POINT('',(-1.02246997843232,2.55285235436847,14.));
#418077=CARTESIAN_POINT('',(-0.951858058590151,2.58001283645973,13.7435492065112));
#418078=CARTESIAN_POINT('Origin',(0.,2.5406128344257E-15,13.7435492065112));
#418079=CARTESIAN_POINT('',(-0.951858058590152,2.58001283645973,12.5369868989719));
#418080=CARTESIAN_POINT('',(-0.951858058590152,2.58001283645973,14.));
#418081=CARTESIAN_POINT('Ctrl Pts',(-0.918816168673682,2.59196389793219,
12.4908873016278));
#418082=CARTESIAN_POINT('Ctrl Pts',(-0.920872139511063,2.59123508405896,
12.4908873016278));
#418083=CARTESIAN_POINT('Ctrl Pts',(-0.922938813593644,2.59049966386211,
12.4911020829134));
#418084=CARTESIAN_POINT('Ctrl Pts',(-0.924950281651809,2.58978126035236,
12.4915448903141));
#418085=CARTESIAN_POINT('Ctrl Pts',(-0.928391658384763,2.58855215949077,
12.4923024798169));
#418086=CARTESIAN_POINT('Ctrl Pts',(-0.9317503842467,2.58734439624036,12.4937722312795));
#418087=CARTESIAN_POINT('Ctrl Pts',(-0.93469500271964,2.58628019593604,
12.4958030942394));
#418088=CARTESIAN_POINT('Ctrl Pts',(-0.937618837081762,2.58522350711657,
12.4978196226833));
#418089=CARTESIAN_POINT('Ctrl Pts',(-0.940221176236059,2.58427733773481,
12.5004326847668));
#418090=CARTESIAN_POINT('Ctrl Pts',(-0.942367279955908,2.58349451512259,
12.5033504258767));
#418091=CARTESIAN_POINT('Ctrl Pts',(-0.94493149482021,2.58255918037628,
12.5068366111226));
#418092=CARTESIAN_POINT('Ctrl Pts',(-0.94692698632412,2.58182719894233,
12.5108395010833));
#418093=CARTESIAN_POINT('Ctrl Pts',(-0.94838193526122,2.58129264223764,
12.5149868989719));
#418094=CARTESIAN_POINT('Ctrl Pts',(-0.950825660716975,2.58039480328709,
12.5219528491417));
#418095=CARTESIAN_POINT('Ctrl Pts',(-0.951858058626384,2.58001283644667,
12.5295503425868));
#418096=CARTESIAN_POINT('Ctrl Pts',(-0.951858058590152,2.58001283645973,
12.5369868989719));
#418097=CARTESIAN_POINT('',(-0.810986627520914,2.6276987441452,12.5369868989719));
#418098=CARTESIAN_POINT('Ctrl Pts',(-0.810986627520913,2.6276987441452,
12.5369868989719));
#418099=CARTESIAN_POINT('Ctrl Pts',(-0.810986627520915,2.6276987441452,
12.5309445149785));
#418100=CARTESIAN_POINT('Ctrl Pts',(-0.81167839131061,2.62748566763893,
12.5248274368704));
#418101=CARTESIAN_POINT('Ctrl Pts',(-0.813260964182396,2.62699573736562,
12.5190199595513));
#418102=CARTESIAN_POINT('Ctrl Pts',(-0.81459022609596,2.62658422667677,
12.5141420429941));
#418103=CARTESIAN_POINT('Ctrl Pts',(-0.816589051982728,2.62596470934103,
12.5093757677094));
#418104=CARTESIAN_POINT('Ctrl Pts',(-0.819344893734357,2.62510455889122,
12.5051960112707));
#418105=CARTESIAN_POINT('Ctrl Pts',(-0.82118598601421,2.62452991909133,
12.5024036458141));
#418106=CARTESIAN_POINT('Ctrl Pts',(-0.823409537141162,2.62383378855938,
12.4998248032393));
#418107=CARTESIAN_POINT('Ctrl Pts',(-0.825935993480318,2.62303826405062,
12.4976950015772));
#418108=CARTESIAN_POINT('Ctrl Pts',(-0.828533635171877,2.62222032486894,
12.495505190692));
#418109=CARTESIAN_POINT('Ctrl Pts',(-0.831518410105352,2.62127602470004,
12.4937456938368));
#418110=CARTESIAN_POINT('Ctrl Pts',(-0.834658986697622,2.62027562976205,
12.4925987732155));
#418111=CARTESIAN_POINT('Ctrl Pts',(-0.837798828407076,2.61927546891262,
12.4914521209692));
#418112=CARTESIAN_POINT('Ctrl Pts',(-0.841172644978215,2.61819417931211,
12.4908873016276));
#418113=CARTESIAN_POINT('Ctrl Pts',(-0.844493894536227,2.61712247747236,
12.4908873016278));
#418114=CARTESIAN_POINT('',(-0.810986627520915,2.6276987441452,13.7435492065112));
#418115=CARTESIAN_POINT('',(-0.810986627520915,2.6276987441452,14.));
#418116=CARTESIAN_POINT('',(-0.738395831580896,2.64901332497667,13.7435492065112));
#418117=CARTESIAN_POINT('Origin',(0.,2.5406128344257E-15,13.7435492065112));
#418118=CARTESIAN_POINT('',(-0.738395831580896,2.64901332497667,12.5369868989719));
#418119=CARTESIAN_POINT('',(-0.738395831580896,2.64901332497667,14.));
#418120=CARTESIAN_POINT('Ctrl Pts',(-0.704489763369112,2.65823139950384,
12.4908873016278));
#418121=CARTESIAN_POINT('Ctrl Pts',(-0.706598298229784,2.65767259140861,
12.4908873016278));
#418122=CARTESIAN_POINT('Ctrl Pts',(-0.708718039198195,2.65710807138559,
12.4911020829134));
#418123=CARTESIAN_POINT('Ctrl Pts',(-0.710781370817709,2.65655601162455,
12.4915448903141));
#418124=CARTESIAN_POINT('Ctrl Pts',(-0.714311479784112,2.6556115046466,
12.4923024798169));
#418125=CARTESIAN_POINT('Ctrl Pts',(-0.717757473680055,2.6546815274674,
12.4937722312795));
#418126=CARTESIAN_POINT('Ctrl Pts',(-0.720779036382295,2.65386088194386,
12.4958030942394));
#418127=CARTESIAN_POINT('Ctrl Pts',(-0.723779271875384,2.65304602881333,
12.4978196226833));
#418128=CARTESIAN_POINT('Ctrl Pts',(-0.726450073549245,2.65231512253215,
12.5004326847668));
#418129=CARTESIAN_POINT('Ctrl Pts',(-0.728652843596273,2.65170983207422,
12.5033504258767));
#418130=CARTESIAN_POINT('Ctrl Pts',(-0.731284764712195,2.65098661689357,
12.5068366111226));
#418131=CARTESIAN_POINT('Ctrl Pts',(-0.733333279664994,2.65041972215026,
12.5108395010833));
#418132=CARTESIAN_POINT('Ctrl Pts',(-0.734826958713545,2.65000553598437,
12.5149868989719));
#418133=CARTESIAN_POINT('Ctrl Pts',(-0.737335735084039,2.64930987082994,
12.5219528491417));
#418134=CARTESIAN_POINT('Ctrl Pts',(-0.738395831618072,2.64901332496661,
12.5295503425868));
#418135=CARTESIAN_POINT('Ctrl Pts',(-0.738395831580896,2.64901332497667,
12.5369868989719));
#418136=CARTESIAN_POINT('',(-0.594106294406732,2.68505823231943,12.5369868989719));
#418137=CARTESIAN_POINT('Ctrl Pts',(-0.594106294406732,2.68505823231942,
12.5369868989719));
#418138=CARTESIAN_POINT('Ctrl Pts',(-0.594106294406734,2.68505823231942,
12.5309445149785));
#418139=CARTESIAN_POINT('Ctrl Pts',(-0.594813124122851,2.68490224997853,
12.5248274368704));
#418140=CARTESIAN_POINT('Ctrl Pts',(-0.596430364979523,2.68454294428873,
12.5190199595513));
#418141=CARTESIAN_POINT('Ctrl Pts',(-0.597788745825149,2.68424115005398,
12.5141420429941));
#418142=CARTESIAN_POINT('Ctrl Pts',(-0.599831417197852,2.68378661697702,
12.5093757677094));
#418143=CARTESIAN_POINT('Ctrl Pts',(-0.6026481993603,2.68315395529362,12.5051960112707));
#418144=CARTESIAN_POINT('Ctrl Pts',(-0.604530004035857,2.68273129367294,
12.5024036458141));
#418145=CARTESIAN_POINT('Ctrl Pts',(-0.606802897580777,2.68221871951719,
12.4998248032393));
#418146=CARTESIAN_POINT('Ctrl Pts',(-0.609385789977635,2.68163177169673,
12.4976950015772));
#418147=CARTESIAN_POINT('Ctrl Pts',(-0.612041457867441,2.68102828605339,
12.495505190692));
#418148=CARTESIAN_POINT('Ctrl Pts',(-0.615093270438773,2.68033041483178,
12.4937456938368));
#418149=CARTESIAN_POINT('Ctrl Pts',(-0.61830493849617,2.67958933477338,
12.4925987732155));
#418150=CARTESIAN_POINT('Ctrl Pts',(-0.621515855035623,2.67884842812486,
12.4914521209692));
#418151=CARTESIAN_POINT('Ctrl Pts',(-0.624966580651088,2.67804573379783,
12.4908873016276));
#418152=CARTESIAN_POINT('Ctrl Pts',(-0.628364132674314,2.67724831062949,
12.4908873016278));
#418153=CARTESIAN_POINT('',(-0.594106294406733,2.68505823231942,13.7435492065112));
#418154=CARTESIAN_POINT('',(-0.594106294406734,2.68505823231942,14.));
#418155=CARTESIAN_POINT('',(-0.520019702139206,2.70038506687233,13.7435492065112));
#418156=CARTESIAN_POINT('Origin',(0.,2.5406128344257E-15,13.7435492065112));
#418157=CARTESIAN_POINT('',(-0.520019702139206,2.70038506687233,12.5369868989719));
#418158=CARTESIAN_POINT('',(-0.520019702139207,2.70038506687233,14.));
#418159=CARTESIAN_POINT('Ctrl Pts',(-0.485475094921951,2.7068088096891,
12.4908873016278));
#418160=CARTESIAN_POINT('Ctrl Pts',(-0.487622161854298,2.70642372614753,
12.4908873016278));
#418161=CARTESIAN_POINT('Ctrl Pts',(-0.489780863182127,2.70603386308596,
12.4911020829134));
#418162=CARTESIAN_POINT('Ctrl Pts',(-0.491882327231488,2.70565182094026,
12.4915448903141));
#418163=CARTESIAN_POINT('Ctrl Pts',(-0.495477676138597,2.70499819338406,
12.4923024798169));
#418164=CARTESIAN_POINT('Ctrl Pts',(-0.498988005547716,2.70435219112078,
12.4937722312795));
#418165=CARTESIAN_POINT('Ctrl Pts',(-0.502066404477997,2.70378056163856,
12.4958030942394));
#418166=CARTESIAN_POINT('Ctrl Pts',(-0.505123075029849,2.70321296691012,
12.4978196226833));
#418167=CARTESIAN_POINT('Ctrl Pts',(-0.507844565478785,2.70270218779023,
12.5004326847668));
#418168=CARTESIAN_POINT('Ctrl Pts',(-0.510089342781761,2.70227845759472,
12.5033504258767));
#418169=CARTESIAN_POINT('Ctrl Pts',(-0.512771455148514,2.70177217485743,
12.5068366111226));
#418170=CARTESIAN_POINT('Ctrl Pts',(-0.514859361021171,2.70137413939576,
12.5108395010833));
#418171=CARTESIAN_POINT('Ctrl Pts',(-0.516381829993545,2.70108308010926,
12.5149868989719));
#418172=CARTESIAN_POINT('Ctrl Pts',(-0.518938961785951,2.70059421828779,
12.5219528491417));
#418173=CARTESIAN_POINT('Ctrl Pts',(-0.520019702177079,2.70038506686532,
12.5295503425868));
#418174=CARTESIAN_POINT('Ctrl Pts',(-0.520019702139206,2.70038506687233,
12.5369868989719));
#418175=CARTESIAN_POINT('',(-0.373272281923912,2.72454910096099,12.5369868989719));
#418176=CARTESIAN_POINT('Ctrl Pts',(-0.373272281923913,2.72454910096099,
12.5369868989719));
#418177=CARTESIAN_POINT('Ctrl Pts',(-0.373272281923915,2.72454910096099,
12.5309445149785));
#418178=CARTESIAN_POINT('Ctrl Pts',(-0.373989473731312,2.72445125082222,
12.5248274368704));
#418179=CARTESIAN_POINT('Ctrl Pts',(-0.375630620101797,2.72422496083601,
12.5190199595513));
#418180=CARTESIAN_POINT('Ctrl Pts',(-0.37700908007907,2.72403489144618,
12.5141420429941));
#418181=CARTESIAN_POINT('Ctrl Pts',(-0.379082003296741,2.72374836747066,
12.5093757677094));
#418182=CARTESIAN_POINT('Ctrl Pts',(-0.381940980649454,2.72334740481279,
12.5051960112707));
#418183=CARTESIAN_POINT('Ctrl Pts',(-0.383850974621075,2.72307953411467,
12.5024036458141));
#418184=CARTESIAN_POINT('Ctrl Pts',(-0.386158084852425,2.72275392743156,
12.4998248032393));
#418185=CARTESIAN_POINT('Ctrl Pts',(-0.388780224584233,2.7223794623403,
12.4976950015772));
#418186=CARTESIAN_POINT('Ctrl Pts',(-0.391476245640631,2.72199444633269,
12.495505190692));
#418187=CARTESIAN_POINT('Ctrl Pts',(-0.39457478654067,2.72154764827621,
12.4937456938368));
#418188=CARTESIAN_POINT('Ctrl Pts',(-0.397836172942162,2.72107081486292,
12.4925987732155));
#418189=CARTESIAN_POINT('Ctrl Pts',(-0.401096796191809,2.72059409302681,
12.4914521209692));
#418190=CARTESIAN_POINT('Ctrl Pts',(-0.404601466841955,2.72007533577157,
12.4908873016276));
#418191=CARTESIAN_POINT('Ctrl Pts',(-0.408052711182237,2.71955749799427,
12.4908873016278));
#418192=CARTESIAN_POINT('',(-0.373272281923914,2.72454910096099,13.7435492065112));
#418193=CARTESIAN_POINT('',(-0.373272281923914,2.72454910096099,14.));
#418194=CARTESIAN_POINT('',(-0.298182927376992,2.73378619168012,13.7435492065112));
#418195=CARTESIAN_POINT('Origin',(0.,2.5406128344257E-15,13.7435492065112));
#418196=CARTESIAN_POINT('',(-0.298182927376992,2.73378619168012,12.5369868989719));
#418197=CARTESIAN_POINT('',(-0.298182927376992,2.73378619168012,14.));
#418198=CARTESIAN_POINT('Ctrl Pts',(-0.263229669815836,2.7373728538379,
12.4908873016278));
#418199=CARTESIAN_POINT('Ctrl Pts',(-0.265400980443666,2.73716405751743,
12.4908873016278));
#418200=CARTESIAN_POINT('Ctrl Pts',(-0.267584276329737,2.73695144589166,
12.4911020829134));
#418201=CARTESIAN_POINT('Ctrl Pts',(-0.269709887912413,2.73674196378875,
12.4915448903141));
#418202=CARTESIAN_POINT('Ctrl Pts',(-0.273346550306441,2.73638356543784,
12.4923024798169));
#418203=CARTESIAN_POINT('Ctrl Pts',(-0.276897854565684,2.73602583712895,
12.4937722312795));
#418204=CARTESIAN_POINT('Ctrl Pts',(-0.280012603487024,2.73570702778796,
12.4958030942394));
#418205=CARTESIAN_POINT('Ctrl Pts',(-0.283105367459432,2.73539046871088,
12.4978196226833));
#418206=CARTESIAN_POINT('Ctrl Pts',(-0.28585943561352,2.73510321590304,
12.5004326847668));
#418207=CARTESIAN_POINT('Ctrl Pts',(-0.288131281549855,2.73486386582449,
12.5033504258767));
#418208=CARTESIAN_POINT('Ctrl Pts',(-0.290845736152154,2.73457788475865,
12.5068366111226));
#418209=CARTESIAN_POINT('Ctrl Pts',(-0.292959138275568,2.73435135743893,
12.5108395010833));
#418210=CARTESIAN_POINT('Ctrl Pts',(-0.294500265391943,2.73418536198336,
12.5149868989719));
#418211=CARTESIAN_POINT('Ctrl Pts',(-0.297088735316081,2.7339065567896,
12.5219528491417));
#418212=CARTESIAN_POINT('Ctrl Pts',(-0.29818292741531,2.73378619167623,
12.5295503425868));
#418213=CARTESIAN_POINT('Ctrl Pts',(-0.298182927376992,2.73378619168012,
12.5369868989719));
#418214=CARTESIAN_POINT('',(-0.14995420399048,2.74590854485462,12.5369868989719));
#418215=CARTESIAN_POINT('Ctrl Pts',(-0.14995420399048,2.74590854485462,
12.5369868989719));
#418216=CARTESIAN_POINT('Ctrl Pts',(-0.149954203990483,2.74590854485462,
12.5309445149785));
#418217=CARTESIAN_POINT('Ctrl Pts',(-0.150676985096012,2.7458694780945,
12.5248274368704));
#418218=CARTESIAN_POINT('Ctrl Pts',(-0.152331115421984,2.7457777097344,
12.5190199595513));
#418219=CARTESIAN_POINT('Ctrl Pts',(-0.153720481107187,2.74570063006994,
12.5141420429941));
#418220=CARTESIAN_POINT('Ctrl Pts',(-0.155809861207817,2.74558402196563,
12.5093757677094));
#418221=CARTESIAN_POINT('Ctrl Pts',(-0.15869200772821,2.74541742667362,
12.5051960112707));
#418222=CARTESIAN_POINT('Ctrl Pts',(-0.160617480301142,2.74530612953335,
12.5024036458141));
#418223=CARTESIAN_POINT('Ctrl Pts',(-0.162943453780979,2.74516965718165,
12.4998248032393));
#418224=CARTESIAN_POINT('Ctrl Pts',(-0.165587390940443,2.74501016682298,
12.4976950015772));
#418225=CARTESIAN_POINT('Ctrl Pts',(-0.168305823588117,2.74484618266911,
12.495505190692));
#418226=CARTESIAN_POINT('Ctrl Pts',(-0.171430472538395,2.74465343114511,
12.4937456938368));
#418227=CARTESIAN_POINT('Ctrl Pts',(-0.174719873295569,2.74444401762462,
12.4925987732155));
#418228=CARTESIAN_POINT('Ctrl Pts',(-0.178008504345647,2.74423465310609,
12.4914521209692));
#418229=CARTESIAN_POINT('Ctrl Pts',(-0.181543797025532,2.74400328516659,
12.4908873016276));
#418230=CARTESIAN_POINT('Ctrl Pts',(-0.185025766221201,2.74376847890529,
12.4908873016278));
#418231=CARTESIAN_POINT('',(-0.149954203990482,2.74590854485461,13.7435492065112));
#418232=CARTESIAN_POINT('',(-0.149954203990482,2.74590854485462,14.));
#418233=CARTESIAN_POINT('',(-0.0743617944298036,2.74899442042525,13.7435492065112));
#418234=CARTESIAN_POINT('Origin',(0.,2.5406128344257E-15,13.7435492065112));
#418235=CARTESIAN_POINT('',(-0.0743617944298037,2.74899442042526,12.5369868989719));
#418236=CARTESIAN_POINT('',(-0.0743617944298037,2.74899442042526,14.));
#418237=CARTESIAN_POINT('Ctrl Pts',(-0.0392324946869358,2.74972013327914,
12.4908873016278));
#418238=CARTESIAN_POINT('Ctrl Pts',(-0.0414135992962603,2.74968901368484,
12.4908873016278));
#418239=CARTESIAN_POINT('Ctrl Pts',(-0.0436069602666705,2.74965506839015,
12.4911020829134));
#418240=CARTESIAN_POINT('Ctrl Pts',(-0.0457425737882799,2.74961954039886,
12.4915448903141));
#418241=CARTESIAN_POINT('Ctrl Pts',(-0.0493963482810018,2.74955875633514,
12.4923024798169));
#418242=CARTESIAN_POINT('Ctrl Pts',(-0.0529649940464467,2.74949168260351,
12.4937722312795));
#418243=CARTESIAN_POINT('Ctrl Pts',(-0.0560953648186719,2.74942781502731,
12.4958030942394));
#418244=CARTESIAN_POINT('Ctrl Pts',(-0.0592036403776707,2.74936439825002,
12.4978196226833));
#418245=CARTESIAN_POINT('Ctrl Pts',(-0.0619719583677341,2.74930258337428,
12.5004326847668));
#418246=CARTESIAN_POINT('Ctrl Pts',(-0.0642557541775498,2.74924920624797,
12.5033504258767));
#418247=CARTESIAN_POINT('Ctrl Pts',(-0.0669844867678712,2.74918543001039,
12.5068366111226));
#418248=CARTESIAN_POINT('Ctrl Pts',(-0.0691093207995963,2.74913191833457,
12.5108395010833));
#418249=CARTESIAN_POINT('Ctrl Pts',(-0.0706588501132809,2.74909209138229,
12.5149868989719));
#418250=CARTESIAN_POINT('Ctrl Pts',(-0.0732614323288725,2.74902519821882,
12.5219528491417));
#418251=CARTESIAN_POINT('Ctrl Pts',(-0.0743617944682905,2.7489944204245,
12.5295503425868));
#418252=CARTESIAN_POINT('Ctrl Pts',(-0.0743617944298037,2.74899442042526,
12.5369868989719));
#418253=CARTESIAN_POINT('',(-3.36777869765522E-16,2.75,14.));
#418254=CARTESIAN_POINT('',(0.0743617944298038,2.74899442042526,12.5369868989719));
#418255=CARTESIAN_POINT('Ctrl Pts',(0.0743617944298037,2.74899442042526,
12.5369868989719));
#418256=CARTESIAN_POINT('Ctrl Pts',(0.0743617944298037,2.74899442042526,
12.5309445149785));
#418257=CARTESIAN_POINT('Ctrl Pts',(0.0736382340151502,2.74901439702663,
12.5248274368704));
#418258=CARTESIAN_POINT('Ctrl Pts',(0.0719821276980976,2.74905776099595,
12.5190199595513));
#418259=CARTESIAN_POINT('Ctrl Pts',(0.070591102304372,2.7490941840093,12.5141420429941));
#418260=CARTESIAN_POINT('Ctrl Pts',(0.0684991698006262,2.7491482677839,
12.5093757677094));
#418261=CARTESIAN_POINT('Ctrl Pts',(0.0656130343221262,2.74921714852193,
12.5051960112707));
#418262=CARTESIAN_POINT('Ctrl Pts',(0.0636848968501762,2.74926316560363,
12.5024036458141));
#418263=CARTESIAN_POINT('Ctrl Pts',(0.061355539091602,2.7493167357843,12.4998248032393));
#418264=CARTESIAN_POINT('Ctrl Pts',(0.0587073994700591,2.74937328154026,
12.4976950015772));
#418265=CARTESIAN_POINT('Ctrl Pts',(0.0559846459518707,2.74943142052762,
12.495505190692));
#418266=CARTESIAN_POINT('Ctrl Pts',(0.0528546829745851,2.74949399826569,
12.4937456938368));
#418267=CARTESIAN_POINT('Ctrl Pts',(0.0495591582810547,2.74955339825043,
12.4925987732155));
#418268=CARTESIAN_POINT('Ctrl Pts',(0.0462644047275967,2.7496127843358,
12.4914521209692));
#418269=CARTESIAN_POINT('Ctrl Pts',(0.042722016807478,2.7496703454275,12.4908873016276));
#418270=CARTESIAN_POINT('Ctrl Pts',(0.0392324946869349,2.74972013327914,
12.4908873016278));
#418271=CARTESIAN_POINT('',(0.0743617944298037,2.74899442042525,13.7435492065112));
#418272=CARTESIAN_POINT('',(0.0743617944298038,2.74899442042526,14.));
#418273=CARTESIAN_POINT('',(0.149954203990446,2.74590854485462,13.7435492065112));
#418274=CARTESIAN_POINT('Origin',(0.,2.5406128344257E-15,13.7435492065112));
#418275=CARTESIAN_POINT('',(0.149954203990446,2.74590854485462,12.5369868989719));
#418276=CARTESIAN_POINT('',(0.149954203990446,2.74590854485462,14.));
#418277=CARTESIAN_POINT('Ctrl Pts',(0.185025766221164,2.7437684789053,12.4908873016278));
#418278=CARTESIAN_POINT('Ctrl Pts',(0.182849382521663,2.74391524313292,
12.4908873016278));
#418279=CARTESIAN_POINT('Ctrl Pts',(0.180660552922293,2.74406019006967,
12.4911020829134));
#418280=CARTESIAN_POINT('Ctrl Pts',(0.178529149617384,2.74419885262291,
12.4915448903141));
#418281=CARTESIAN_POINT('Ctrl Pts',(0.174882578292387,2.7444360873543,12.4923024798169));
#418282=CARTESIAN_POINT('Ctrl Pts',(0.171320339769525,2.74466011456455,
12.4937722312795));
#418283=CARTESIAN_POINT('Ctrl Pts',(0.168195179247428,2.74485161378132,
12.4958030942394));
#418284=CARTESIAN_POINT('Ctrl Pts',(0.165092077162855,2.745041761332,12.4978196226833));
#418285=CARTESIAN_POINT('Ctrl Pts',(0.1623279320363,2.74520579575617,12.5004326847668));
#418286=CARTESIAN_POINT('Ctrl Pts',(0.160047384637318,2.74533874679806,
12.5033504258767));
#418287=CARTESIAN_POINT('Ctrl Pts',(0.157322533324154,2.74549759980908,
12.5068366111226));
#418288=CARTESIAN_POINT('Ctrl Pts',(0.155200407804025,2.74561745988853,
12.5108395010833));
#418289=CARTESIAN_POINT('Ctrl Pts',(0.153652788154959,2.74570406648135,
12.5149868989719));
#418290=CARTESIAN_POINT('Ctrl Pts',(0.151053413403163,2.74584953051112,
12.5219528491417));
#418291=CARTESIAN_POINT('Ctrl Pts',(0.149954203952006,2.745908544857,12.5295503425868));
#418292=CARTESIAN_POINT('Ctrl Pts',(0.149954203990446,2.74590854485462,
12.5369868989719));
#418293=CARTESIAN_POINT('',(0.298182927376958,2.73378619168012,12.5369868989719));
#418294=CARTESIAN_POINT('Ctrl Pts',(0.298182927376958,2.73378619168012,
12.5369868989719));
#418295=CARTESIAN_POINT('Ctrl Pts',(0.298182927376955,2.73378619168012,
12.5309445149785));
#418296=CARTESIAN_POINT('Ctrl Pts',(0.297463402828359,2.73386507870201,
12.5248274368704));
#418297=CARTESIAN_POINT('Ctrl Pts',(0.295816341634529,2.73404328642068,
12.5190199595513));
#418298=CARTESIAN_POINT('Ctrl Pts',(0.294432913576771,2.73419296972269,
12.5141420429941));
#418299=CARTESIAN_POINT('Ctrl Pts',(0.292352350135577,2.7344173854576,12.5093757677094));
#418300=CARTESIAN_POINT('Ctrl Pts',(0.2894814324544,2.73472128383573,12.5051960112707));
#418301=CARTESIAN_POINT('Ctrl Pts',(0.287563461520187,2.73492430890331,
12.5024036458141));
#418302=CARTESIAN_POINT('Ctrl Pts',(0.285246220974444,2.73516756511565,
12.4998248032393));
#418303=CARTESIAN_POINT('Ctrl Pts',(0.282611501823092,2.73543977068356,
12.4976950015772));
#418304=CARTESIAN_POINT('Ctrl Pts',(0.279902546909829,2.73571964590677,
12.495505190692));
#418305=CARTESIAN_POINT('Ctrl Pts',(0.276788099292741,2.73603713646238,
12.4937456938368));
#418306=CARTESIAN_POINT('Ctrl Pts',(0.273508381835966,2.73636495465526,
12.4925987732155));
#418307=CARTESIAN_POINT('Ctrl Pts',(0.270229431820431,2.73669269613994,
12.4914521209692));
#418308=CARTESIAN_POINT('Ctrl Pts',(0.266703522667235,2.73703880320326,
12.4908873016276));
#418309=CARTESIAN_POINT('Ctrl Pts',(0.2632296698158,2.7373728538379,12.4908873016278));
#418310=CARTESIAN_POINT('',(0.298182927376956,2.73378619168012,13.7435492065112));
#418311=CARTESIAN_POINT('',(0.298182927376956,2.73378619168012,14.));
#418312=CARTESIAN_POINT('',(0.373272281923878,2.72454910096099,13.7435492065112));
#418313=CARTESIAN_POINT('Origin',(0.,2.5406128344257E-15,13.7435492065112));
#418314=CARTESIAN_POINT('',(0.373272281923878,2.72454910096099,12.5369868989719));
#418315=CARTESIAN_POINT('',(0.373272281923878,2.72454910096099,14.));
#418316=CARTESIAN_POINT('Ctrl Pts',(0.408052711182201,2.71955749799427,
12.4908873016278));
#418317=CARTESIAN_POINT('Ctrl Pts',(0.405895531866964,2.71988116935211,
12.4908873016278));
#418318=CARTESIAN_POINT('Ctrl Pts',(0.403725799938487,2.72020404392233,
12.4911020829134));
#418319=CARTESIAN_POINT('Ctrl Pts',(0.401612790987617,2.7205159742437,12.4915448903141));
#418320=CARTESIAN_POINT('Ctrl Pts',(0.397997690160871,2.72104964901219,
12.4923024798169));
#418321=CARTESIAN_POINT('Ctrl Pts',(0.394465564990232,2.72156328630021,
12.4937722312795));
#418322=CARTESIAN_POINT('Ctrl Pts',(0.391366412145924,2.72200887791426,
12.4958030942394));
#418323=CARTESIAN_POINT('Ctrl Pts',(0.388289134168174,2.72245132439233,
12.4978196226833));
#418324=CARTESIAN_POINT('Ctrl Pts',(0.385547556834892,2.72284011649437,
12.5004326847668));
#418325=CARTESIAN_POINT('Ctrl Pts',(0.38328543451342,2.72315851093723,12.5033504258767));
#418326=CARTESIAN_POINT('Ctrl Pts',(0.380582597913333,2.72353893605627,
12.5068366111226));
#418327=CARTESIAN_POINT('Ctrl Pts',(0.378477303300012,2.72383137024193,
12.5108395010833));
#418328=CARTESIAN_POINT('Ctrl Pts',(0.376941892468989,2.72404383402726,
12.5149868989719));
#418329=CARTESIAN_POINT('Ctrl Pts',(0.374363023591095,2.72440068721116,
12.5219528491417));
#418330=CARTESIAN_POINT('Ctrl Pts',(0.37327228188576,2.7245491009665,12.5295503425868));
#418331=CARTESIAN_POINT('Ctrl Pts',(0.373272281923878,2.72454910096099,
12.5369868989719));
#418332=CARTESIAN_POINT('',(0.520019702139173,2.70038506687233,12.5369868989719));
#418333=CARTESIAN_POINT('Ctrl Pts',(0.520019702139173,2.70038506687233,
12.5369868989719));
#418334=CARTESIAN_POINT('Ctrl Pts',(0.520019702139171,2.70038506687233,
12.5309445149785));
#418335=CARTESIAN_POINT('Ctrl Pts',(0.519309001773788,2.70052233933461,
12.5248274368704));
#418336=CARTESIAN_POINT('Ctrl Pts',(0.517681946623677,2.70083420485966,
12.5190199595513));
#418337=CARTESIAN_POINT('Ctrl Pts',(0.516315322387364,2.70109615233266,
12.5141420429941));
#418338=CARTESIAN_POINT('Ctrl Pts',(0.514259973815156,2.70148940657819,
12.5093757677094));
#418339=CARTESIAN_POINT('Ctrl Pts',(0.5114233794148,2.70202630020286,12.5051960112707));
#418340=CARTESIAN_POINT('Ctrl Pts',(0.509528338798451,2.70238498215798,
12.5024036458141));
#418341=CARTESIAN_POINT('Ctrl Pts',(0.507238636319051,2.70281630557204,
12.4998248032393));
#418342=CARTESIAN_POINT('Ctrl Pts',(0.504634871259143,2.70330235946874,
12.4976950015772));
#418343=CARTESIAN_POINT('Ctrl Pts',(0.501957742598808,2.70380210840438,
12.495505190692));
#418344=CARTESIAN_POINT('Ctrl Pts',(0.498879536476964,2.70437239893028,
12.4937456938368));
#418345=CARTESIAN_POINT('Ctrl Pts',(0.495637452235504,2.7049664537553,12.4925987732155));
#418346=CARTESIAN_POINT('Ctrl Pts',(0.492396126629256,2.70556036957378,
12.4914521209692));
#418347=CARTESIAN_POINT('Ctrl Pts',(0.488910160586661,2.70619271932333,
12.4908873016276));
#418348=CARTESIAN_POINT('Ctrl Pts',(0.485475094921914,2.70680880968911,
12.4908873016278));
#418349=CARTESIAN_POINT('',(0.52001970213917,2.70038506687233,13.7435492065112));
#418350=CARTESIAN_POINT('',(0.520019702139171,2.70038506687234,14.));
#418351=CARTESIAN_POINT('',(0.594106294406697,2.68505823231943,13.7435492065112));
#418352=CARTESIAN_POINT('Origin',(0.,2.5406128344257E-15,13.7435492065112));
#418353=CARTESIAN_POINT('',(0.594106294406698,2.68505823231943,12.5369868989719));
#418354=CARTESIAN_POINT('',(0.594106294406698,2.68505823231943,14.));
#418355=CARTESIAN_POINT('Ctrl Pts',(0.628364132674278,2.6772483106295,12.4908873016278));
#418356=CARTESIAN_POINT('Ctrl Pts',(0.62624051341574,2.67774673513806,12.4908873016278));
#418357=CARTESIAN_POINT('Ctrl Pts',(0.624104318366159,2.67824538866476,
12.4911020829134));
#418358=CARTESIAN_POINT('Ctrl Pts',(0.622023765495274,2.67872851090944,
12.4915448903141));
#418359=CARTESIAN_POINT('Ctrl Pts',(0.61846419306633,2.6795550741975,12.4923024798169));
#418360=CARTESIAN_POINT('Ctrl Pts',(0.614985686958166,2.68035490339187,
12.4937722312795));
#418361=CARTESIAN_POINT('Ctrl Pts',(0.611933166142502,2.68105162206453,
12.4958030942394));
#418362=CARTESIAN_POINT('Ctrl Pts',(0.608902191048801,2.68174342306169,
12.4978196226833));
#418363=CARTESIAN_POINT('Ctrl Pts',(0.606201426253617,2.6823543854943,12.5004326847668));
#418364=CARTESIAN_POINT('Ctrl Pts',(0.60397278306048,2.68285610447564,12.5033504258767));
#418365=CARTESIAN_POINT('Ctrl Pts',(0.601309948105109,2.68345557003629,
12.5068366111226));
#418366=CARTESIAN_POINT('Ctrl Pts',(0.599235494786896,2.68391863222692,
12.5108395010833));
#418367=CARTESIAN_POINT('Ctrl Pts',(0.597722510679673,2.68425553929331,
12.5149868989719));
#418368=CARTESIAN_POINT('Ctrl Pts',(0.595181309622579,2.68482140683228,
12.5219528491417));
#418369=CARTESIAN_POINT('Ctrl Pts',(0.594106294369155,2.68505823232803,
12.5295503425868));
#418370=CARTESIAN_POINT('Ctrl Pts',(0.594106294406698,2.68505823231943,
12.5369868989719));
#418371=CARTESIAN_POINT('',(0.738395831580863,2.64901332497668,12.5369868989719));
#418372=CARTESIAN_POINT('Ctrl Pts',(0.738395831580863,2.64901332497668,
12.5369868989719));
#418373=CARTESIAN_POINT('Ctrl Pts',(0.738395831580862,2.64901332497668,
12.5309445149785));
#418374=CARTESIAN_POINT('Ctrl Pts',(0.737698684992366,2.64920806935377,
12.5248274368704));
#418375=CARTESIAN_POINT('Ctrl Pts',(0.736102463669554,2.64965151727159,
12.5190199595513));
#418376=CARTESIAN_POINT('Ctrl Pts',(0.7347617379135,2.65002398569836,12.5141420429941));
#418377=CARTESIAN_POINT('Ctrl Pts',(0.732745282215917,2.65058346141239,
12.5093757677094));
#418378=CARTESIAN_POINT('Ctrl Pts',(0.729961888164113,2.6513497773451,12.5051960112707));
#418379=CARTESIAN_POINT('Ctrl Pts',(0.728102389048269,2.65186172921853,
12.5024036458141));
#418380=CARTESIAN_POINT('Ctrl Pts',(0.725855462227438,2.65247824944814,
12.4998248032393));
#418381=CARTESIAN_POINT('Ctrl Pts',(0.723299978885857,2.65317491706516,
12.4976950015772));
#418382=CARTESIAN_POINT('Ctrl Pts',(0.720672492327989,2.65389121396651,
12.495505190692));
#418383=CARTESIAN_POINT('Ctrl Pts',(0.717651012655261,2.65471050927333,
12.4937456938368));
#418384=CARTESIAN_POINT('Ctrl Pts',(0.714468137164836,2.65556684739364,
12.4925987732155));
#418385=CARTESIAN_POINT('Ctrl Pts',(0.711286006455004,2.65642298513414,
12.4914521209692));
#418386=CARTESIAN_POINT('Ctrl Pts',(0.707863182051883,2.65733736938667,
12.4908873016276));
#418387=CARTESIAN_POINT('Ctrl Pts',(0.704489763369076,2.65823139950385,
12.4908873016278));
#418388=CARTESIAN_POINT('',(0.73839583158086,2.64901332497668,13.7435492065112));
#418389=CARTESIAN_POINT('',(0.738395831580861,2.64901332497668,14.));
#418390=CARTESIAN_POINT('',(0.81098662752088,2.62769874414521,13.7435492065112));
#418391=CARTESIAN_POINT('Origin',(0.,2.5406128344257E-15,13.7435492065112));
#418392=CARTESIAN_POINT('',(0.81098662752088,2.62769874414521,12.5369868989719));
#418393=CARTESIAN_POINT('',(0.81098662752088,2.62769874414521,14.));
#418394=CARTESIAN_POINT('Ctrl Pts',(0.844493894536193,2.61712247747237,
12.4908873016278));
#418395=CARTESIAN_POINT('Ctrl Pts',(0.842417967670147,2.61779233819878,
12.4908873016278));
#418396=CARTESIAN_POINT('Ctrl Pts',(0.840329525525069,2.61846345222502,
12.4911020829134));
#418397=CARTESIAN_POINT('Ctrl Pts',(0.838295274470257,2.61911455129417,
12.4915448903141));
#418398=CARTESIAN_POINT('Ctrl Pts',(0.834814918806343,2.62022850245949,
12.4923024798169));
#418399=CARTESIAN_POINT('Ctrl Pts',(0.83141318064489,2.62130920082889,12.4937722312795));
#418400=CARTESIAN_POINT('Ctrl Pts',(0.828427605880267,2.62225241001234,
12.4958030942394));
#418401=CARTESIAN_POINT('Ctrl Pts',(0.825463104309788,2.62318896170709,
12.4978196226833));
#418402=CARTESIAN_POINT('Ctrl Pts',(0.822821125196819,2.62401802861609,
12.5004326847668));
#418403=CARTESIAN_POINT('Ctrl Pts',(0.820640792384768,2.62469973327886,
12.5033504258767));
#418404=CARTESIAN_POINT('Ctrl Pts',(0.818035679801402,2.62551424993673,
12.5068366111226));
#418405=CARTESIAN_POINT('Ctrl Pts',(0.816005872922871,2.62614485852983,
12.5108395010833));
#418406=CARTESIAN_POINT('Ctrl Pts',(0.814525384199056,2.62660396681635,
12.5149868989719));
#418407=CARTESIAN_POINT('Ctrl Pts',(0.812038762236529,2.62737508295528,
12.5219528491417));
#418408=CARTESIAN_POINT('Ctrl Pts',(0.810986627484164,2.62769874415684,
12.5295503425868));
#418409=CARTESIAN_POINT('Ctrl Pts',(0.81098662752088,2.62769874414521,12.5369868989719));
#418410=CARTESIAN_POINT('',(0.951858058590119,2.58001283645975,12.5369868989719));
#418411=CARTESIAN_POINT('Ctrl Pts',(0.951858058590119,2.58001283645974,
12.5369868989719));
#418412=CARTESIAN_POINT('Ctrl Pts',(0.951858058590117,2.58001283645975,
12.5309445149785));
#418413=CARTESIAN_POINT('Ctrl Pts',(0.951179105174035,2.58026375675994,
12.5248274368704));
#418414=CARTESIAN_POINT('Ctrl Pts',(0.94962434026807,2.5808358359978,12.5190199595513));
#418415=CARTESIAN_POINT('Ctrl Pts',(0.948318435300976,2.58131634666242,
12.5141420429941));
#418416=CARTESIAN_POINT('Ctrl Pts',(0.946354291657993,2.58203832062637,
12.5093757677094));
#418417=CARTESIAN_POINT('Ctrl Pts',(0.943642620982929,2.58302895916102,
12.5051960112707));
#418418=CARTESIAN_POINT('Ctrl Pts',(0.941831038027408,2.58369077399752,
12.5024036458141));
#418419=CARTESIAN_POINT('Ctrl Pts',(0.939641839792423,2.58448838820228,
12.4998248032393));
#418420=CARTESIAN_POINT('Ctrl Pts',(0.937151644489183,2.58539103333156,
12.4976950015772));
#418421=CARTESIAN_POINT('Ctrl Pts',(0.934591285523319,2.58631911136092,
12.495505190692));
#418422=CARTESIAN_POINT('Ctrl Pts',(0.93164663974842,2.58738195917357,12.4937456938368));
#418423=CARTESIAN_POINT('Ctrl Pts',(0.928544154520281,2.58849488180028,
12.4925987732155));
#418424=CARTESIAN_POINT('Ctrl Pts',(0.925442395261725,2.58960754400738,
12.4914521209692));
#418425=CARTESIAN_POINT('Ctrl Pts',(0.922105490829752,2.59079787768654,
12.4908873016276));
#418426=CARTESIAN_POINT('Ctrl Pts',(0.918816168673647,2.5919638979322,12.4908873016278));
#418427=CARTESIAN_POINT('',(0.951858058590117,2.58001283645974,13.7435492065112));
#418428=CARTESIAN_POINT('',(0.951858058590117,2.58001283645975,14.));
#418429=CARTESIAN_POINT('',(1.02246997843229,2.55285235436848,13.7435492065112));
#418430=CARTESIAN_POINT('Origin',(0.,2.5406128344257E-15,13.7435492065112));
#418431=CARTESIAN_POINT('',(1.02246997843229,2.55285235436848,12.5369868989719));
#418432=CARTESIAN_POINT('',(1.02246997843229,2.55285235436848,14.));
#418433=CARTESIAN_POINT('Ctrl Pts',(1.05500368886165,2.53958012602247,12.4908873016278));
#418434=CARTESIAN_POINT('Ctrl Pts',(1.05298926933889,2.54041696515413,12.4908873016278));
#418435=CARTESIAN_POINT('Ctrl Pts',(1.05096247833622,2.54125607352678,12.4911020829134));
#418436=CARTESIAN_POINT('Ctrl Pts',(1.04898806670263,2.54207081646352,12.4915448903141));
#418437=CARTESIAN_POINT('Ctrl Pts',(1.04561008899647,2.54346474234489,12.4923024798169));
#418438=CARTESIAN_POINT('Ctrl Pts',(1.04230775678794,2.54481911801997,12.4937722312795));
#418439=CARTESIAN_POINT('Ctrl Pts',(1.03940899658183,2.54600254081271,12.4958030942394));
#418440=CARTESIAN_POINT('Ctrl Pts',(1.03653069680342,2.54717761060804,12.4978196226833));
#418441=CARTESIAN_POINT('Ctrl Pts',(1.03396508530777,2.54821926468994,12.5004326847668));
#418442=CARTESIAN_POINT('Ctrl Pts',(1.03184757263194,2.54907641840208,12.5033504258767));
#418443=CARTESIAN_POINT('Ctrl Pts',(1.029317519015,2.5501005656832,12.5068366111226));
#418444=CARTESIAN_POINT('Ctrl Pts',(1.02734586660604,2.55089452408264,12.5108395010833));
#418445=CARTESIAN_POINT('Ctrl Pts',(1.02590772567382,2.55147277829938,12.5149868989719));
#418446=CARTESIAN_POINT('Ctrl Pts',(1.02349223086476,2.55244401138759,12.5219528491417));
#418447=CARTESIAN_POINT('Ctrl Pts',(1.02246997839664,2.55285235438306,12.5295503425868));
#418448=CARTESIAN_POINT('Ctrl Pts',(1.02246997843229,2.55285235436848,12.5369868989719));
#418449=CARTESIAN_POINT('',(1.15898582726498,2.49384278818832,12.5369868989719));
#418450=CARTESIAN_POINT('Ctrl Pts',(1.15898582726498,2.49384278818832,12.5369868989719));
#418451=CARTESIAN_POINT('Ctrl Pts',(1.15898582726498,2.49384278818832,12.5309445149785));
#418452=CARTESIAN_POINT('Ctrl Pts',(1.15832958534428,2.49414821457842,12.5248274368704));
#418453=CARTESIAN_POINT('Ctrl Pts',(1.15682662355909,2.49484511804338,12.5190199595513));
#418454=CARTESIAN_POINT('Ctrl Pts',(1.15556422996305,2.49543047322665,12.5141420429941));
#418455=CARTESIAN_POINT('Ctrl Pts',(1.15366546942655,2.49631014082293,12.5093757677094));
#418456=CARTESIAN_POINT('Ctrl Pts',(1.15104356784918,2.49751850942351,12.5051960112707));
#418457=CARTESIAN_POINT('Ctrl Pts',(1.14929195683966,2.49832578295453,12.5024036458141));
#418458=CARTESIAN_POINT('Ctrl Pts',(1.14717505594358,2.49929918314349,12.4998248032393));
#418459=CARTESIAN_POINT('Ctrl Pts',(1.14476672051757,2.50040179883063,12.4976950015772));
#418460=CARTESIAN_POINT('Ctrl Pts',(1.1422905279102,2.50153548178184,12.495505190692));
#418461=CARTESIAN_POINT('Ctrl Pts',(1.13944231216493,2.50283480902348,12.4937456938368));
#418462=CARTESIAN_POINT('Ctrl Pts',(1.1364408637264,2.50419690984012,12.4925987732155));
#418463=CARTESIAN_POINT('Ctrl Pts',(1.13344011761523,2.50555869193042,12.4914521209692));
#418464=CARTESIAN_POINT('Ctrl Pts',(1.13021133970285,2.50701705356197,12.4908873016276));
#418465=CARTESIAN_POINT('Ctrl Pts',(1.12702800396969,2.50844730426376,12.4908873016278));
#418466=CARTESIAN_POINT('',(1.15898582726498,2.49384278818832,13.7435492065112));
#418467=CARTESIAN_POINT('',(1.15898582726498,2.49384278818833,14.));
#418468=CARTESIAN_POINT('',(1.2271489603329,2.46101715336442,13.7435492065112));
#418469=CARTESIAN_POINT('Origin',(0.,2.5406128344257E-15,13.7435492065112));
#418470=CARTESIAN_POINT('',(1.2271489603329,2.46101715336442,12.5369868989719));
#418471=CARTESIAN_POINT('',(1.2271489603329,2.46101715336442,14.));
#418472=CARTESIAN_POINT('Ctrl Pts',(1.2584926077011,2.44513728783512,12.4908873016278));
#418473=CARTESIAN_POINT('Ctrl Pts',(1.25655310115118,2.44613553634567,12.4908873016278));
#418474=CARTESIAN_POINT('Ctrl Pts',(1.25460144925065,2.44713705493696,12.4911020829134));
#418475=CARTESIAN_POINT('Ctrl Pts',(1.25270001642194,2.44811001976147,12.4915448903141));
#418476=CARTESIAN_POINT('Ctrl Pts',(1.24944689655784,2.44977464401213,12.4923024798169));
#418477=CARTESIAN_POINT('Ctrl Pts',(1.24626594677824,2.45139368384623,12.4937722312795));
#418478=CARTESIAN_POINT('Ctrl Pts',(1.24347329190156,2.45280944476482,12.4958030942394));
#418479=CARTESIAN_POINT('Ctrl Pts',(1.24070034852535,2.45421521276512,12.4978196226833));
#418480=CARTESIAN_POINT('Ctrl Pts',(1.23822817836822,2.45546252198386,12.5004326847668));
#418481=CARTESIAN_POINT('Ctrl Pts',(1.2361875775261,2.45648942052885,12.5033504258767));
#418482=CARTESIAN_POINT('Ctrl Pts',(1.233749419965,2.45771638290202,12.5068366111226));
#418483=CARTESIAN_POINT('Ctrl Pts',(1.23184904304708,2.45866840744564,12.5108395010833));
#418484=CARTESIAN_POINT('Ctrl Pts',(1.23046282049709,2.45936195940621,12.5149868989719));
#418485=CARTESIAN_POINT('Ctrl Pts',(1.22813452756092,2.46052684604774,12.5219528491417));
#418486=CARTESIAN_POINT('Ctrl Pts',(1.22714896029856,2.46101715338186,12.5295503425868));
#418487=CARTESIAN_POINT('Ctrl Pts',(1.2271489603329,2.46101715336442,12.5369868989719));
#418488=CARTESIAN_POINT('',(1.3584007364786,2.39107662761661,12.5369868989719));
#418489=CARTESIAN_POINT('Ctrl Pts',(1.3584007364786,2.39107662761661,12.5369868989719));
#418490=CARTESIAN_POINT('Ctrl Pts',(1.3584007364786,2.39107662761661,12.5309445149785));
#418491=CARTESIAN_POINT('Ctrl Pts',(1.35777157323498,2.39143452753438,12.5248274368704));
#418492=CARTESIAN_POINT('Ctrl Pts',(1.35633041653328,2.39225161744886,12.5190199595513));
#418493=CARTESIAN_POINT('Ctrl Pts',(1.3551199353294,2.39293792170861,12.5141420429941));
#418494=CARTESIAN_POINT('Ctrl Pts',(1.35329919383748,2.39396942889448,12.5093757677094));
#418495=CARTESIAN_POINT('Ctrl Pts',(1.35078450968021,2.39538748606734,12.5051960112707));
#418496=CARTESIAN_POINT('Ctrl Pts',(1.34910452729897,2.39633484602071,12.5024036458141));
#418497=CARTESIAN_POINT('Ctrl Pts',(1.347074011368,2.39747755437623,12.4998248032393));
#418498=CARTESIAN_POINT('Ctrl Pts',(1.34476356289413,2.39877280289574,12.4976950015772));
#418499=CARTESIAN_POINT('Ctrl Pts',(1.34238801529851,2.40010454629581,12.495505190692));
#418500=CARTESIAN_POINT('Ctrl Pts',(1.33965518398873,2.40163170615802,12.4937456938368));
#418501=CARTESIAN_POINT('Ctrl Pts',(1.33677474648396,2.40323392060839,12.4925987732155));
#418502=CARTESIAN_POINT('Ctrl Pts',(1.33389498299045,2.40483576014675,12.4914521209692));
#418503=CARTESIAN_POINT('Ctrl Pts',(1.33079581858196,2.40655244457465,12.4908873016276));
#418504=CARTESIAN_POINT('Ctrl Pts',(1.32773965384585,2.40823740765011,12.4908873016278));
#418505=CARTESIAN_POINT('',(1.3584007364786,2.39107662761661,13.7435492065112));
#418506=CARTESIAN_POINT('',(1.3584007364786,2.39107662761661,14.));
#418507=CARTESIAN_POINT('',(1.42366146836782,2.35280428924396,13.7435492065112));
#418508=CARTESIAN_POINT('Origin',(0.,2.5406128344257E-15,13.7435492065112));
#418509=CARTESIAN_POINT('',(1.42366146836782,2.35280428924396,12.5369868989719));
#418510=CARTESIAN_POINT('',(1.42366146836782,2.35280428924396,14.));
#418511=CARTESIAN_POINT('Ctrl Pts',(1.45360646587295,2.33442246441649,12.4908873016278));
#418512=CARTESIAN_POINT('Ctrl Pts',(1.45175477939198,2.33557547912678,12.4908873016278));
#418513=CARTESIAN_POINT('Ctrl Pts',(1.44989125451499,2.33673274299572,12.4911020829134));
#418514=CARTESIAN_POINT('Ctrl Pts',(1.44807545421291,2.33785745478763,12.4915448903141));
#418515=CARTESIAN_POINT('Ctrl Pts',(1.44496884116685,2.33978169960783,12.4923024798169));
#418516=CARTESIAN_POINT('Ctrl Pts',(1.44193044251215,2.34165462915798,12.4937722312795));
#418517=CARTESIAN_POINT('Ctrl Pts',(1.43926247762233,2.3432933065471,12.4958030942394));
#418518=CARTESIAN_POINT('Ctrl Pts',(1.43661334412899,2.34492041759825,12.4978196226833));
#418519=CARTESIAN_POINT('Ctrl Pts',(1.43425106719491,2.34636508131678,12.5004326847668));
#418520=CARTESIAN_POINT('Ctrl Pts',(1.43230095804843,2.34755489085422,12.5033504258767));
#418521=CARTESIAN_POINT('Ctrl Pts',(1.42997092207945,2.34897650308729,12.5068366111226));
#418522=CARTESIAN_POINT('Ctrl Pts',(1.42815446734742,2.35008025820883,12.5108395010833));
#418523=CARTESIAN_POINT('Ctrl Pts',(1.42682938826203,2.35088449243935,12.5149868989719));
#418524=CARTESIAN_POINT('Ctrl Pts',(1.42460379160409,2.35223528050579,12.5219528491417));
#418525=CARTESIAN_POINT('Ctrl Pts',(1.42366146833502,2.35280428926415,12.5295503425868));
#418526=CARTESIAN_POINT('Ctrl Pts',(1.42366146836782,2.35280428924396,12.5369868989719));
#418527=CARTESIAN_POINT('',(1.5487757129113,2.27239824658798,12.5369868989719));
#418528=CARTESIAN_POINT('Ctrl Pts',(1.5487757129113,2.27239824658798,12.5369868989719));
#418529=CARTESIAN_POINT('Ctrl Pts',(1.5487757129113,2.27239824658798,12.5309445149785));
#418530=CARTESIAN_POINT('Ctrl Pts',(1.54817781532235,2.27280623826852,12.5248274368704));
#418531=CARTESIAN_POINT('Ctrl Pts',(1.5468080543642,2.27373807703395,12.5190199595513));
#418532=CARTESIAN_POINT('Ctrl Pts',(1.54565754110519,2.27452076312857,12.5141420429941));
#418533=CARTESIAN_POINT('Ctrl Pts',(1.54392693539208,2.2756972453939,12.5093757677094));
#418534=CARTESIAN_POINT('Ctrl Pts',(1.54153620346308,2.2773155542025,12.5051960112707));
#418535=CARTESIAN_POINT('Ctrl Pts',(1.53993902971568,2.27839669605405,12.5024036458141));
#418536=CARTESIAN_POINT('Ctrl Pts',(1.53800841149833,2.27970110804054,12.4998248032393));
#418537=CARTESIAN_POINT('Ctrl Pts',(1.53581122563,2.28118036972724,12.4976950015772));
#418538=CARTESIAN_POINT('Ctrl Pts',(1.53355213192344,2.28270131104355,12.495505190692));
#418539=CARTESIAN_POINT('Ctrl Pts',(1.53095287159063,2.28444614052942,12.4937456938368));
#418540=CARTESIAN_POINT('Ctrl Pts',(1.52821261385598,2.28627780614069,12.4925987732155));
#418541=CARTESIAN_POINT('Ctrl Pts',(1.52547299733106,2.28810904314927,12.4914521209692));
#418542=CARTESIAN_POINT('Ctrl Pts',(1.52252407085427,2.29007262612189,12.4908873016276));
#418543=CARTESIAN_POINT('Ctrl Pts',(1.51961541538728,2.29200108841975,12.4908873016278));
#418544=CARTESIAN_POINT('',(1.5487757129113,2.27239824658798,13.7435492065112));
#418545=CARTESIAN_POINT('',(1.5487757129113,2.27239824658798,14.));
#418546=CARTESIAN_POINT('',(1.61069974421836,2.22893390076397,13.7435492065112));
#418547=CARTESIAN_POINT('Origin',(0.,2.5406128344257E-15,13.7435492065112));
#418548=CARTESIAN_POINT('',(1.61069974421836,2.22893390076398,12.5369868989719));
#418549=CARTESIAN_POINT('',(1.61069974421836,2.22893390076398,14.));
#418550=CARTESIAN_POINT('Ctrl Pts',(1.63904681284261,2.20817244464976,12.4908873016278));
#418551=CARTESIAN_POINT('Ctrl Pts',(1.63729526909861,2.20947255243714,12.4908873016278));
#418552=CARTESIAN_POINT('Ctrl Pts',(1.63553227269574,2.21077786018362,12.4911020829134));
#418553=CARTESIAN_POINT('Ctrl Pts',(1.63381418877174,2.2120468341715,12.4915448903141));
#418554=CARTESIAN_POINT('Ctrl Pts',(1.63087475654097,2.21421789402945,12.4923024798169));
#418555=CARTESIAN_POINT('Ctrl Pts',(1.62799912905291,2.2163322492585,12.4937722312795));
#418556=CARTESIAN_POINT('Ctrl Pts',(1.62547360901613,2.21818293799049,12.4958030942394));
#418557=CARTESIAN_POINT('Ctrl Pts',(1.62296591495198,2.22002056393691,12.4978196226833));
#418558=CARTESIAN_POINT('Ctrl Pts',(1.62072925180418,2.22165296815653,12.5004326847668));
#418559=CARTESIAN_POINT('Ctrl Pts',(1.61888261200797,2.22299777070025,12.5033504258767));
#418560=CARTESIAN_POINT('Ctrl Pts',(1.61667620363606,2.22460457219836,12.5068366111226));
#418561=CARTESIAN_POINT('Ctrl Pts',(1.61495575929647,2.22585271258959,12.5108395010833));
#418562=CARTESIAN_POINT('Ctrl Pts',(1.61370064185836,2.22676227704395,12.5149868989719));
#418563=CARTESIAN_POINT('Ctrl Pts',(1.61159255245722,2.22828997726358,12.5219528491417));
#418564=CARTESIAN_POINT('Ctrl Pts',(1.61069974418731,2.22893390078676,12.5295503425868));
#418565=CARTESIAN_POINT('Ctrl Pts',(1.61069974421836,2.22893390076398,12.5369868989719));
#418566=CARTESIAN_POINT('',(1.72884384250458,2.13859743014762,12.5369868989719));
#418567=CARTESIAN_POINT('Ctrl Pts',(1.72884384250458,2.13859743014762,12.5369868989719));
#418568=CARTESIAN_POINT('Ctrl Pts',(1.72884384250458,2.13859743014762,12.5309445149785));
#418569=CARTESIAN_POINT('Ctrl Pts',(1.72828118948011,2.13905279847361,12.5248274368704));
#418570=CARTESIAN_POINT('Ctrl Pts',(1.72699193979871,2.14009318485675,12.5190199595513));
#418571=CARTESIAN_POINT('Ctrl Pts',(1.72590905096046,2.14096704413941,12.5141420429941));
#418572=CARTESIAN_POINT('Ctrl Pts',(1.72428009792165,2.14228067218884,12.5093757677094));
#418573=CARTESIAN_POINT('Ctrl Pts',(1.72202922814747,2.14408846305507,12.5051960112707));
#418574=CARTESIAN_POINT('Ctrl Pts',(1.72052549196169,2.14529619198414,12.5024036458141));
#418575=CARTESIAN_POINT('Ctrl Pts',(1.71870761940366,2.14675362695506,12.4998248032393));
#418576=CARTESIAN_POINT('Ctrl Pts',(1.71663831805031,2.14840705756647,12.4976950015772));
#418577=CARTESIAN_POINT('Ctrl Pts',(1.71451071212871,2.1501070751855,12.495505190692));
#418578=CARTESIAN_POINT('Ctrl Pts',(1.71206232042154,2.15205796274268,12.4937456938368));
#418579=CARTESIAN_POINT('Ctrl Pts',(1.70948047842012,2.15410689008242,12.4925987732155));
#418580=CARTESIAN_POINT('Ctrl Pts',(1.70689924055976,2.15615533798106,12.4914521209692));
#418581=CARTESIAN_POINT('Ctrl Pts',(1.70412017663384,2.15835275217767,12.4908873016276));
#418582=CARTESIAN_POINT('Ctrl Pts',(1.70137838705821,2.16051188009953,12.4908873016278));
#418583=CARTESIAN_POINT('',(1.72884384250458,2.13859743014762,13.7435492065112));
#418584=CARTESIAN_POINT('',(1.72884384250458,2.13859743014762,14.));
#418585=CARTESIAN_POINT('',(1.78701907901789,2.09023032492261,13.7435492065112));
#418586=CARTESIAN_POINT('Origin',(0.,2.5406128344257E-15,13.7435492065112));
#418587=CARTESIAN_POINT('',(1.78701907901789,2.09023032492261,12.5369868989719));
#418588=CARTESIAN_POINT('',(1.78701907901789,2.09023032492261,14.));
#418589=CARTESIAN_POINT('Ctrl Pts',(1.81357957369649,2.06722740158669,12.4908873016278));
#418590=CARTESIAN_POINT('Ctrl Pts',(1.81193982892409,2.06866595044833,12.4908873016278));
#418591=CARTESIAN_POINT('Ctrl Pts',(1.81028909344554,2.07011061546466,12.4911020829134));
#418592=CARTESIAN_POINT('Ctrl Pts',(1.80868015946465,2.071515406836,12.4915448903141));
#418593=CARTESIAN_POINT('Ctrl Pts',(1.8059274694857,2.07391883368654,12.4923024798169));
#418594=CARTESIAN_POINT('Ctrl Pts',(1.80323374999077,2.07626054390928,12.4937722312795));
#418595=CARTESIAN_POINT('Ctrl Pts',(1.80086748172618,2.07831092795597,12.4958030942394));
#418596=CARTESIAN_POINT('Ctrl Pts',(1.79851791538149,2.08034683970017,12.4978196226833));
#418597=CARTESIAN_POINT('Ctrl Pts',(1.7964217506442,2.08215612104013,12.5004326847668));
#418598=CARTESIAN_POINT('Ctrl Pts',(1.79469086928142,2.08364696715108,12.5033504258767));
#418599=CARTESIAN_POINT('Ctrl Pts',(1.79262277179027,2.08542826491537,12.5068366111226));
#418600=CARTESIAN_POINT('Ctrl Pts',(1.79100978711635,2.08681248440791,12.5108395010833));
#418601=CARTESIAN_POINT('Ctrl Pts',(1.78983298392499,2.08782132608473,12.5149868989719));
#418602=CARTESIAN_POINT('Ctrl Pts',(1.78785643076781,2.08951577186464,12.5219528491417));
#418603=CARTESIAN_POINT('Ctrl Pts',(1.7870190789888,2.09023032494785,12.5295503425868));
#418604=CARTESIAN_POINT('Ctrl Pts',(1.78701907901789,2.09023032492261,12.5369868989719));
#418605=CARTESIAN_POINT('',(1.89740680156515,1.99056460065338,12.5369868989719));
#418606=CARTESIAN_POINT('Ctrl Pts',(1.89740680156515,1.99056460065337,12.5369868989719));
#418607=CARTESIAN_POINT('Ctrl Pts',(1.89740680156515,1.99056460065338,12.5309445149785));
#418608=CARTESIAN_POINT('Ctrl Pts',(1.8968831374682,1.99106431522373,12.5248274368704));
#418609=CARTESIAN_POINT('Ctrl Pts',(1.89568297880746,1.99220632562485,12.5190199595513));
#418610=CARTESIAN_POINT('Ctrl Pts',(1.89467492083654,1.99316554270621,12.5141420429941));
#418611=CARTESIAN_POINT('Ctrl Pts',(1.89315846088574,1.99460757456179,12.5093757677094));
#418612=CARTESIAN_POINT('Ctrl Pts',(1.89106243243336,1.9965928169357,12.5051960112707));
#418613=CARTESIAN_POINT('Ctrl Pts',(1.88966214092542,1.99791909570554,12.5024036458141));
#418614=CARTESIAN_POINT('Ctrl Pts',(1.88796911166866,1.9995198546716,12.4998248032393));
#418615=CARTESIAN_POINT('Ctrl Pts',(1.88604146568939,2.0013364508998,12.4976950015772));
#418616=CARTESIAN_POINT('Ctrl Pts',(1.88405950641913,2.00320423148479,12.495505190692));
#418617=CARTESIAN_POINT('Ctrl Pts',(1.88177827698045,2.00534819427845,12.4937456938368));
#418618=CARTESIAN_POINT('Ctrl Pts',(1.8793720324448,2.00760074807326,12.4925987732155));
#418619=CARTESIAN_POINT('Ctrl Pts',(1.87696635096109,2.00985277477916,12.4914521209692));
#418620=CARTESIAN_POINT('Ctrl Pts',(1.87437564379794,2.01226939677085,12.4908873016276));
#418621=CARTESIAN_POINT('Ctrl Pts',(1.87181896627095,2.01464482167661,12.4908873016278));
#418622=CARTESIAN_POINT('',(1.89740680156514,1.99056460065337,13.7435492065112));
#418623=CARTESIAN_POINT('',(1.89740680156515,1.99056460065338,14.));
#418624=CARTESIAN_POINT('',(1.95144609668394,1.93761661113261,13.7435492065112));
#418625=CARTESIAN_POINT('Origin',(0.,2.5406128344257E-15,13.7435492065112));
#418626=CARTESIAN_POINT('',(1.95144609668394,1.93761661113261,12.5369868989719));
#418627=CARTESIAN_POINT('',(1.95144609668394,1.93761661113261,14.));
#418628=CARTESIAN_POINT('Ctrl Pts',(1.97604326170699,1.91252530123458,12.4908873016278));
#418629=CARTESIAN_POINT('Ctrl Pts',(1.97452622813711,1.91409271786515,12.4908873016278));
#418630=CARTESIAN_POINT('Ctrl Pts',(1.97299873895513,1.915667126144,12.4911020829134));
#418631=CARTESIAN_POINT('Ctrl Pts',(1.97150966210755,1.917198386244,12.4915448903141));
#418632=CARTESIAN_POINT('Ctrl Pts',(1.96896203307807,1.91981818567797,12.4923024798169));
#418633=CARTESIAN_POINT('Ctrl Pts',(1.96646814783507,1.92237166719923,12.4937722312795));
#418634=CARTESIAN_POINT('Ctrl Pts',(1.96427687846757,1.92460810159307,12.4958030942394));
#418635=CARTESIAN_POINT('Ctrl Pts',(1.9621010758187,1.9268287504783,12.4978196226833));
#418636=CARTESIAN_POINT('Ctrl Pts',(1.9601593591224,1.92880286846979,12.5004326847668));
#418637=CARTESIAN_POINT('Ctrl Pts',(1.95855575492296,1.93042983681308,12.5033504258767));
#418638=CARTESIAN_POINT('Ctrl Pts',(1.95663973116016,1.93237377660081,12.5068366111226));
#418639=CARTESIAN_POINT('Ctrl Pts',(1.95514494029879,1.93388486344232,12.5108395010833));
#418640=CARTESIAN_POINT('Ctrl Pts',(1.95405428278525,1.93498626866669,12.5149868989719));
#418641=CARTESIAN_POINT('Ctrl Pts',(1.95222241950718,1.93683618374979,12.5219528491417));
#418642=CARTESIAN_POINT('Ctrl Pts',(1.95144609665701,1.93761661116014,12.5295503425868));
#418643=CARTESIAN_POINT('Ctrl Pts',(1.95144609668394,1.93761661113261,12.5369868989719));
#418644=CARTESIAN_POINT('',(2.05334283141139,1.82928489216182,12.5369868989719));
#418645=CARTESIAN_POINT('Ctrl Pts',(2.05334283141138,1.82928489216182,12.5369868989719));
#418646=CARTESIAN_POINT('Ctrl Pts',(2.05334283141138,1.82928489216182,12.5309445149785));
#418647=CARTESIAN_POINT('Ctrl Pts',(2.05286164114013,1.82982562745853,12.5248274368704));
#418648=CARTESIAN_POINT('Ctrl Pts',(2.05175856035793,1.83106166198683,12.5190199595513));
#418649=CARTESIAN_POINT('Ctrl Pts',(2.05083204171381,1.83209985343546,12.5141420429941));
#418650=CARTESIAN_POINT('Ctrl Pts',(2.0494381666418,1.83366069261312,12.5093757677094));
#418651=CARTESIAN_POINT('Ctrl Pts',(2.04751092823475,1.83581017503425,12.5051960112707));
#418652=CARTESIAN_POINT('Ctrl Pts',(2.0462234001136,1.83724617747846,12.5024036458141));
#418653=CARTESIAN_POINT('Ctrl Pts',(2.04466648098848,1.83897960765286,12.4998248032393));
#418654=CARTESIAN_POINT('Ctrl Pts',(2.04289331854924,1.84094728034967,12.4976950015772));
#418655=CARTESIAN_POINT('Ctrl Pts',(2.04107019554226,1.84297039412899,12.495505190692));
#418656=CARTESIAN_POINT('Ctrl Pts',(2.03897130957761,1.84529316444047,12.4937456938368));
#418657=CARTESIAN_POINT('Ctrl Pts',(2.03675667566812,1.84773435431649,12.4925987732155));
#418658=CARTESIAN_POINT('Ctrl Pts',(2.03454255997442,1.85017497296348,12.4914521209692));
#418659=CARTESIAN_POINT('Ctrl Pts',(2.03215745030278,1.8527947205296,12.4908873016276));
#418660=CARTESIAN_POINT('Ctrl Pts',(2.02980289909154,1.85537063435843,12.4908873016278));
#418661=CARTESIAN_POINT('',(2.05334283141138,1.82928489216182,13.7435492065112));
#418662=CARTESIAN_POINT('',(2.05334283141138,1.82928489216182,14.));
#418663=CARTESIAN_POINT('',(2.1028865625425,1.77210837847977,13.7435492065112));
#418664=CARTESIAN_POINT('Origin',(0.,2.5406128344257E-15,13.7435492065112));
#418665=CARTESIAN_POINT('',(2.1028865625425,1.77210837847977,12.5369868989719));
#418666=CARTESIAN_POINT('',(2.1028865625425,1.77210837847977,14.));
#418667=CARTESIAN_POINT('Ctrl Pts',(2.12535670783502,1.74509566054721,12.4908873016278));
#418668=CARTESIAN_POINT('Ctrl Pts',(2.12397248107577,1.74678151404765,12.4908873016278));
#418669=CARTESIAN_POINT('Ctrl Pts',(2.12257840337886,1.74847518816168,12.4911020829134));
#418670=CARTESIAN_POINT('Ctrl Pts',(2.12121909322532,1.75012272670701,12.4915448903141));
#418671=CARTESIAN_POINT('Ctrl Pts',(2.11889347919617,1.75294146439141,12.4923024798169));
#418672=CARTESIAN_POINT('Ctrl Pts',(2.11661602459994,1.75568972421297,12.4937722312795));
#418673=CARTESIAN_POINT('Ctrl Pts',(2.11461433666563,1.75809732585206,12.4958030942394));
#418674=CARTESIAN_POINT('Ctrl Pts',(2.11262677732022,1.76048793382636,12.4978196226833));
#418675=CARTESIAN_POINT('Ctrl Pts',(2.11085243046918,1.76261375103985,12.5004326847668));
#418676=CARTESIAN_POINT('Ctrl Pts',(2.10938677515444,1.76436601440959,12.5033504258767));
#418677=CARTESIAN_POINT('Ctrl Pts',(2.107635575942,1.7664596596222,12.5068366111226));
#418678=CARTESIAN_POINT('Ctrl Pts',(2.10626892647974,1.76808755777907,12.5108395010833));
#418679=CARTESIAN_POINT('Ctrl Pts',(2.10527167278984,1.76927419688094,12.5149868989719));
#418680=CARTESIAN_POINT('Ctrl Pts',(2.10359669013875,1.77126727038755,12.5219528491417));
#418681=CARTESIAN_POINT('Ctrl Pts',(2.1028865625179,1.7721083785094,12.5295503425868));
#418682=CARTESIAN_POINT('Ctrl Pts',(2.1028865625425,1.77210837847977,12.5369868989719));
#418683=CARTESIAN_POINT('',(2.1956142034923,1.65583159452369,12.5369868989719));
#418684=CARTESIAN_POINT('Ctrl Pts',(2.1956142034923,1.65583159452369,12.5369868989719));
#418685=CARTESIAN_POINT('Ctrl Pts',(2.1956142034923,1.6558315945237,12.5309445149785));
#418686=CARTESIAN_POINT('Ctrl Pts',(2.1951786892886,1.65640975204257,12.5248274368704));
#418687=CARTESIAN_POINT('Ctrl Pts',(2.19418002720554,1.6577315850922,12.5190199595513));
#418688=CARTESIAN_POINT('Ctrl Pts',(2.19334121371695,1.6588418419153,12.5141420429941));
#418689=CARTESIAN_POINT('Ctrl Pts',(2.19207919953236,1.66051110128783,12.5093757677094));
#418690=CARTESIAN_POINT('Ctrl Pts',(2.19033357662426,1.6628105193053,12.5051960112707));
#418691=CARTESIAN_POINT('Ctrl Pts',(2.18916738017712,1.66434668906455,12.5024036458141));
#418692=CARTESIAN_POINT('Ctrl Pts',(2.18775693222355,1.66620125475547,12.4998248032393));
#418693=CARTESIAN_POINT('Ctrl Pts',(2.18615005342782,1.66830690938374,12.4976950015772));
#418694=CARTESIAN_POINT('Ctrl Pts',(2.18449789926693,1.67047189286897,12.495505190692));
#418695=CARTESIAN_POINT('Ctrl Pts',(2.18259532451612,1.67295801304508,12.4937456938368));
#418696=CARTESIAN_POINT('Ctrl Pts',(2.18058703925606,1.67557159328645,12.4925987732155));
#418697=CARTESIAN_POINT('Ctrl Pts',(2.17857922392701,1.67818456196012,12.4914521209692));
#418698=CARTESIAN_POINT('Ctrl Pts',(2.17641558425824,1.68099000111283,12.4908873016276));
#418699=CARTESIAN_POINT('Ctrl Pts',(2.17427882851258,1.6837492615832,12.4908873016278));
#418700=CARTESIAN_POINT('',(2.1956142034923,1.65583159452369,13.7435492065112));
#418701=CARTESIAN_POINT('',(2.1956142034923,1.6558315945237,14.));
#418702=CARTESIAN_POINT('',(2.2403326652792,1.59480705694544,13.7435492065112));
#418703=CARTESIAN_POINT('Origin',(0.,2.5406128344257E-15,13.7435492065112));
#418704=CARTESIAN_POINT('',(2.24033266527921,1.59480705694544,12.5369868989719));
#418705=CARTESIAN_POINT('',(2.24033266527921,1.59480705694544,14.));
#418706=CARTESIAN_POINT('Ctrl Pts',(2.26052625573157,1.56605269615942,12.4908873016278));
#418707=CARTESIAN_POINT('Ctrl Pts',(2.25928404758366,1.56784576745282,12.4908873016278));
#418708=CARTESIAN_POINT('Ctrl Pts',(2.25803265872888,1.56964743628024,12.4911020829134));
#418709=CARTESIAN_POINT('Ctrl Pts',(2.25681216125419,1.5714002891737,12.4915448903141));
#418710=CARTESIAN_POINT('Ctrl Pts',(2.25472403880304,1.57439920687432,12.4923024798169));
#418711=CARTESIAN_POINT('Ctrl Pts',(2.25267817093815,1.57732395578048,12.4937722312795));
#418712=CARTESIAN_POINT('Ctrl Pts',(2.25087938533999,1.57988670247315,12.4958030942394));
#418713=CARTESIAN_POINT('Ctrl Pts',(2.24909329617757,1.58243136043487,12.4978196226833));
#418714=CARTESIAN_POINT('Ctrl Pts',(2.24749812715732,1.58469472990755,12.5004326847668));
#418715=CARTESIAN_POINT('Ctrl Pts',(2.24618017442159,1.5865606272801,12.5033504258767));
#418716=CARTESIAN_POINT('Ctrl Pts',(2.24460545370135,1.58879004505414,12.5068366111226));
#418717=CARTESIAN_POINT('Ctrl Pts',(2.24337604046489,1.59052392113271,12.5108395010833));
#418718=CARTESIAN_POINT('Ctrl Pts',(2.24247882715739,1.59178789722463,12.5149868989719));
#418719=CARTESIAN_POINT('Ctrl Pts',(2.24097187186648,1.59391086557942,12.5219528491417));
#418720=CARTESIAN_POINT('Ctrl Pts',(2.2403326652571,1.59480705697698,12.5295503425868));
#418721=CARTESIAN_POINT('Ctrl Pts',(2.24033266527921,1.59480705694544,12.5369868989719));
#418722=CARTESIAN_POINT('',(2.32327412529982,1.47135901081699,12.5369868989719));
#418723=CARTESIAN_POINT('Ctrl Pts',(2.32327412529982,1.47135901081699,12.5369868989719));
#418724=CARTESIAN_POINT('Ctrl Pts',(2.32327412529982,1.471359010817,12.5309445149785));
#418725=CARTESIAN_POINT('Ctrl Pts',(2.32288718543885,1.47197074301514,12.5248274368704));
#418726=CARTESIAN_POINT('Ctrl Pts',(2.32199958798633,1.47336957800523,12.5190199595513));
#418727=CARTESIAN_POINT('Ctrl Pts',(2.32125406181863,1.47454451162683,12.5141420429941));
#418728=CARTESIAN_POINT('Ctrl Pts',(2.32013230701764,1.47631108254852,12.5093757677094));
#418729=CARTESIAN_POINT('Ctrl Pts',(2.31857991644094,1.4787451339148,12.5051960112707));
#418730=CARTESIAN_POINT('Ctrl Pts',(2.31754281251276,1.48037124803278,12.5024036458141));
#418731=CARTESIAN_POINT('Ctrl Pts',(2.31628822202915,1.48233460741154,12.4998248032393));
#418732=CARTESIAN_POINT('Ctrl Pts',(2.31485832039021,1.48456423118712,12.4976950015772));
#418733=CARTESIAN_POINT('Ctrl Pts',(2.31338812988877,1.48685667677036,12.495505190692));
#418734=CARTESIAN_POINT('Ctrl Pts',(2.31169452767286,1.48948960209151,12.4937456938368));
#418735=CARTESIAN_POINT('Ctrl Pts',(2.3099059558693,1.49225817975294,12.4925987732155));
#418736=CARTESIAN_POINT('Ctrl Pts',(2.30811780258464,1.49502610957787,12.4914521209692));
#418737=CARTESIAN_POINT('Ctrl Pts',(2.30619003158375,1.49799857058249,12.4908873016276));
#418738=CARTESIAN_POINT('Ctrl Pts',(2.30428529106062,1.50092281527121,12.4908873016278));
#418739=CARTESIAN_POINT('',(2.32327412529982,1.471359010817,13.7435492065112));
#418740=CARTESIAN_POINT('',(2.32327412529982,1.471359010817,14.));
#418741=CARTESIAN_POINT('',(2.36286972375735,1.40689255757178,13.7435492065112));
#418742=CARTESIAN_POINT('Origin',(0.,2.5406128344257E-15,13.7435492065112));
#418743=CARTESIAN_POINT('',(2.36286972375735,1.40689255757179,12.5369868989719));
#418744=CARTESIAN_POINT('',(2.36286972375735,1.40689255757179,14.));
#418745=CARTESIAN_POINT('Ctrl Pts',(2.38065237435682,1.3765879094592,12.4908873016278));
#418746=CARTESIAN_POINT('Ctrl Pts',(2.37956045151052,1.37847626595194,12.4908873016278));
#418747=CARTESIAN_POINT('Ctrl Pts',(2.37846007928423,1.38037393968396,12.4911020829134));
#418748=CARTESIAN_POINT('Ctrl Pts',(2.37738651669771,1.38222044197875,12.4915448903141));
#418749=CARTESIAN_POINT('Ctrl Pts',(2.37554978193495,1.38537958239306,12.4923024798169));
#418750=CARTESIAN_POINT('Ctrl Pts',(2.37374911571451,1.38846135666241,12.4937722312795));
#418751=CARTESIAN_POINT('Ctrl Pts',(2.37216520307387,1.39116219375223,12.4958030942394));
#418752=CARTESIAN_POINT('Ctrl Pts',(2.37059247022313,1.39384396742249,12.4978196226833));
#418753=CARTESIAN_POINT('Ctrl Pts',(2.36918709462032,1.39622982680393,12.5004326847668));
#418754=CARTESIAN_POINT('Ctrl Pts',(2.3680256152216,1.39819694094014,12.5033504258767));
#418755=CARTESIAN_POINT('Ctrl Pts',(2.36663785250014,1.40054729486815,12.5068366111226));
#418756=CARTESIAN_POINT('Ctrl Pts',(2.36555385703173,1.40237561020919,12.5108395010833));
#418757=CARTESIAN_POINT('Ctrl Pts',(2.36476265491317,1.40370851173882,12.5149868989719));
#418758=CARTESIAN_POINT('Ctrl Pts',(2.36343375552127,1.40594724693764,12.5219528491417));
#418759=CARTESIAN_POINT('Ctrl Pts',(2.36286972373789,1.40689255760502,12.5295503425868));
#418760=CARTESIAN_POINT('Ctrl Pts',(2.36286972375735,1.40689255757179,12.5369868989719));
#418761=CARTESIAN_POINT('',(2.43547304111672,1.27709477565046,12.5369868989719));
#418762=CARTESIAN_POINT('Ctrl Pts',(2.43547304111672,1.27709477565046,12.5369868989719));
#418763=CARTESIAN_POINT('Ctrl Pts',(2.43547304111672,1.27709477565046,12.5309445149785));
#418764=CARTESIAN_POINT('Ctrl Pts',(2.43513725061941,1.27773601155102,12.5248274368704));
#418765=CARTESIAN_POINT('Ctrl Pts',(2.43436662461203,1.27920253946551,12.5190199595513));
#418766=CARTESIAN_POINT('Ctrl Pts',(2.43371934711886,1.2804343308962,12.5141420429941));
#418767=CARTESIAN_POINT('Ctrl Pts',(2.4327453167946,1.28228645712903,12.5093757677094));
#418768=CARTESIAN_POINT('Ctrl Pts',(2.43139648945247,1.28483894363388,12.5051960112707));
#418769=CARTESIAN_POINT('Ctrl Pts',(2.43049537979877,1.28654418058943,12.5024036458141));
#418770=CARTESIAN_POINT('Ctrl Pts',(2.42940499587781,1.28860326782327,12.4998248032393));
#418771=CARTESIAN_POINT('Ctrl Pts',(2.42816158715514,1.29094202296781,12.4976950015772));
#418772=CARTESIAN_POINT('Ctrl Pts',(2.42688314418837,1.29334667480194,12.495505190692));
#418773=CARTESIAN_POINT('Ctrl Pts',(2.42540978515068,1.29610888358451,12.4937456938368));
#418774=CARTESIAN_POINT('Ctrl Pts',(2.42385282945388,1.29901403423845,12.4925987732155));
#418775=CARTESIAN_POINT('Ctrl Pts',(2.4222962380787,1.30191850509833,12.4914521209692));
#418776=CARTESIAN_POINT('Ctrl Pts',(2.42061716474365,1.30503820671729,12.4908873016276));
#418777=CARTESIAN_POINT('Ctrl Pts',(2.41895711517697,1.30810797525842,12.4908873016278));
#418778=CARTESIAN_POINT('',(2.43547304111672,1.27709477565046,13.7435492065112));
#418779=CARTESIAN_POINT('',(2.43547304111672,1.27709477565046,14.));
#418780=CARTESIAN_POINT('',(2.46968227406995,1.20961542034842,13.7435492065112));
#418781=CARTESIAN_POINT('Origin',(0.,2.5406128344257E-15,13.7435492065112));
#418782=CARTESIAN_POINT('',(2.46968227406995,1.20961542034842,12.5369868989719));
#418783=CARTESIAN_POINT('',(2.46968227406995,1.20961542034842,14.));
#418784=CARTESIAN_POINT('Ctrl Pts',(2.48493564421071,1.17796215734254,12.4908873016278));
#418785=CARTESIAN_POINT('Ctrl Pts',(2.48400127323241,1.17993323233373,12.4908873016278));
#418786=CARTESIAN_POINT('Ctrl Pts',(2.48305924043024,1.18191428226474,12.4911020829134));
#418787=CARTESIAN_POINT('Ctrl Pts',(2.48213975711378,1.18384214579275,12.4915448903141));
#418788=CARTESIAN_POINT('Ctrl Pts',(2.48056663320621,1.18714048536252,12.4923024798169));
#418789=CARTESIAN_POINT('Ctrl Pts',(2.47902315176683,1.19035877629576,12.4937722312795));
#418790=CARTESIAN_POINT('Ctrl Pts',(2.477664652761,1.1931797301575,12.4958030942394));
#418791=CARTESIAN_POINT('Ctrl Pts',(2.47631574249958,1.19598077277497,12.4978196226833));
#418792=CARTESIAN_POINT('Ctrl Pts',(2.47510951285698,1.19847324456464,12.5004326847668));
#418793=CARTESIAN_POINT('Ctrl Pts',(2.47411223624904,1.20052848464449,12.5033504258767));
#418794=CARTESIAN_POINT('Ctrl Pts',(2.47292066685831,1.20298413350885,12.5068366111226));
#418795=CARTESIAN_POINT('Ctrl Pts',(2.47198930296894,1.20489472097542,12.5108395010833));
#418796=CARTESIAN_POINT('Ctrl Pts',(2.47130937735888,1.20628767770299,12.5149868989719));
#418797=CARTESIAN_POINT('Ctrl Pts',(2.47016737747219,1.20862728133245,12.5219528491417));
#418798=CARTESIAN_POINT('Ctrl Pts',(2.46968227405327,1.20961542038314,12.5295503425868));
#418799=CARTESIAN_POINT('Ctrl Pts',(2.46968227406995,1.20961542034842,12.5369868989719));
#418800=CARTESIAN_POINT('',(2.53146428566975,1.07433168545777,12.5369868989719));
#418801=CARTESIAN_POINT('Ctrl Pts',(2.53146428566975,1.07433168545777,12.5369868989719));
#418802=CARTESIAN_POINT('Ctrl Pts',(2.53146428566975,1.07433168545777,12.5309445149785));
#418803=CARTESIAN_POINT('Ctrl Pts',(2.53118187916646,1.07499815774164,12.5248274368704));
#418804=CARTESIAN_POINT('Ctrl Pts',(2.53053335299317,1.07652261907921,12.5190199595513));
#418805=CARTESIAN_POINT('Ctrl Pts',(2.52998863169945,1.07780307095026,12.5141420429941));
#418806=CARTESIAN_POINT('Ctrl Pts',(2.52916880786301,1.07972842689972,12.5093757677094));
#418807=CARTESIAN_POINT('Ctrl Pts',(2.52803251997887,1.08238236216657,12.5051960112707));
#418808=CARTESIAN_POINT('Ctrl Pts',(2.52727340133573,1.08415537388909,12.5024036458141));
#418809=CARTESIAN_POINT('Ctrl Pts',(2.52635448030251,1.08629648609222,12.4998248032393));
#418810=CARTESIAN_POINT('Ctrl Pts',(2.52530583917602,1.08872880857609,12.4976950015772));
#418811=CARTESIAN_POINT('Ctrl Pts',(2.52422765157093,1.09122966409989,12.495505190692));
#418812=CARTESIAN_POINT('Ctrl Pts',(2.52298434067277,1.09410277430017,12.4937456938368));
#418813=CARTESIAN_POINT('Ctrl Pts',(2.52166936236601,1.09712516464832,12.4925987732155));
#418814=CARTESIAN_POINT('Ctrl Pts',(2.5203546917591,1.10014684776879,12.4914521209692));
#418815=CARTESIAN_POINT('Ctrl Pts',(2.51893549004589,1.10339302890254,12.4908873016276));
#418816=CARTESIAN_POINT('Ctrl Pts',(2.51753117879165,1.10658789249292,12.4908873016278));
#418817=CARTESIAN_POINT('',(2.53146428566975,1.07433168545777,13.7435492065112));
#418818=CARTESIAN_POINT('',(2.53146428566975,1.07433168545777,14.));
#418819=CARTESIAN_POINT('',(2.56005949631751,1.00428849207514,13.7435492065112));
#418820=CARTESIAN_POINT('Origin',(0.,2.5406128344257E-15,13.7435492065112));
#418821=CARTESIAN_POINT('',(2.56005949631751,1.00428849207514,12.5369868989719));
#418822=CARTESIAN_POINT('',(2.56005949631751,1.00428849207514,14.));
#418823=CARTESIAN_POINT('Ctrl Pts',(2.57268207733791,0.971497261418848,
12.4908873016278));
#418824=CARTESIAN_POINT('Ctrl Pts',(2.5719114763123,0.973537937729611,12.4908873016278));
#418825=CARTESIAN_POINT('Ctrl Pts',(2.57113405200711,0.975589180299189,
12.4911020829134));
#418826=CARTESIAN_POINT('Ctrl Pts',(2.57037476697048,0.977585575446697,
12.4915448903141));
#418827=CARTESIAN_POINT('Ctrl Pts',(2.56907572279817,0.98100116426628,12.4923024798169));
#418828=CARTESIAN_POINT('Ctrl Pts',(2.56779969775416,0.984334554668221,
12.4937722312795));
#418829=CARTESIAN_POINT('Ctrl Pts',(2.5666756529699,0.987256852319363,12.4958030942394));
#418830=CARTESIAN_POINT('Ctrl Pts',(2.56555954207303,0.99015852340758,12.4978196226833));
#418831=CARTESIAN_POINT('Ctrl Pts',(2.5645604856499,0.992741020616945,12.5004326847668));
#418832=CARTESIAN_POINT('Ctrl Pts',(2.56373404854403,0.99487070935678,12.5033504258767));
#418833=CARTESIAN_POINT('Ctrl Pts',(2.56274660218172,0.997415311219456,
12.5068366111226));
#418834=CARTESIAN_POINT('Ctrl Pts',(2.56197406794442,0.999395456167186,
12.5108395010833));
#418835=CARTESIAN_POINT('Ctrl Pts',(2.56140994363562,1.0008391981955,12.5149868989719));
#418836=CARTESIAN_POINT('Ctrl Pts',(2.56046244307496,1.00326410057947,12.5219528491417));
#418837=CARTESIAN_POINT('Ctrl Pts',(2.56005949630371,1.0042884921111,12.5295503425868));
#418838=CARTESIAN_POINT('Ctrl Pts',(2.56005949631751,1.00428849207514,12.5369868989719));
#418839=CARTESIAN_POINT('',(2.61060905306386,0.864419095150618,12.5369868989719));
#418840=CARTESIAN_POINT('Ctrl Pts',(2.61060905306386,0.864419095150617,
12.5369868989719));
#418841=CARTESIAN_POINT('Ctrl Pts',(2.61060905306386,0.864419095150619,
12.5309445149785));
#418842=CARTESIAN_POINT('Ctrl Pts',(2.61038190992327,0.865106368554689,
12.5248274368704));
#418843=CARTESIAN_POINT('Ctrl Pts',(2.60985979941874,0.866678618276671,
12.5190199595513));
#418844=CARTESIAN_POINT('Ctrl Pts',(2.60942125935482,0.86799920939213,12.5141420429941));
#418845=CARTESIAN_POINT('Ctrl Pts',(2.60876109779858,0.869984982132039,
12.5093757677094));
#418846=CARTESIAN_POINT('Ctrl Pts',(2.60784491118082,0.872722704659571,
12.5051960112707));
#418847=CARTESIAN_POINT('Ctrl Pts',(2.60723283535757,0.874551692048575,
12.5024036458141));
#418848=CARTESIAN_POINT('Ctrl Pts',(2.60649149247995,0.876760580472532,
12.4998248032393));
#418849=CARTESIAN_POINT('Ctrl Pts',(2.60564459748331,0.879270283590905,
12.4976950015772));
#418850=CARTESIAN_POINT('Ctrl Pts',(2.60477384040054,0.881850700023472,
12.495505190692));
#418851=CARTESIAN_POINT('Ctrl Pts',(2.6037688516708,0.884815591567119,12.4937456938368));
#418852=CARTESIAN_POINT('Ctrl Pts',(2.60270460171775,0.88793510810038,12.4925987732155));
#418853=CARTESIAN_POINT('Ctrl Pts',(2.60164060079509,0.891053894678799,
12.4914521209692));
#418854=CARTESIAN_POINT('Ctrl Pts',(2.60049071525699,0.894404952527469,
12.4908873016276));
#418855=CARTESIAN_POINT('Ctrl Pts',(2.59935148777488,0.897703649877021,
12.4908873016278));
#418856=CARTESIAN_POINT('',(2.61060905306386,0.864419095150619,13.7435492065112));
#418857=CARTESIAN_POINT('',(2.61060905306386,0.864419095150619,14.));
#418858=CARTESIAN_POINT('',(2.63339994499716,0.792278189583031,13.7435492065112));
#418859=CARTESIAN_POINT('Origin',(0.,2.5406128344257E-15,13.7435492065112));
#418860=CARTESIAN_POINT('',(2.63339994499716,0.792278189583032,12.5369868989719));
#418861=CARTESIAN_POINT('',(2.63339994499716,0.792278189583032,14.));
#418862=CARTESIAN_POINT('Ctrl Pts',(2.64330773570308,0.758567211506177,
12.4908873016278));
#418863=CARTESIAN_POINT('Ctrl Pts',(2.64270603285286,0.760663908772356,
12.4908873016278));
#418864=CARTESIAN_POINT('Ctrl Pts',(2.64209839067514,0.762771693299628,
12.4911020829134));
#418865=CARTESIAN_POINT('Ctrl Pts',(2.64150435683498,0.764823334386318,
12.4915448903141));
#418866=CARTESIAN_POINT('Ctrl Pts',(2.64048803732257,0.76833344227565,12.4923024798169));
#418867=CARTESIAN_POINT('Ctrl Pts',(2.63948796041007,0.77175974898314,12.4937722312795));
#418868=CARTESIAN_POINT('Ctrl Pts',(2.63860585017996,0.774763943014961,
12.4958030942394));
#418869=CARTESIAN_POINT('Ctrl Pts',(2.63772996618152,0.777746932431566,
12.4978196226833));
#418870=CARTESIAN_POINT('Ctrl Pts',(2.63694473153352,0.78040226896778,12.5004326847668));
#418871=CARTESIAN_POINT('Ctrl Pts',(2.6362946337323,0.782592233640416,12.5033504258767));
#418872=CARTESIAN_POINT('Ctrl Pts',(2.63551788169105,0.785208854595842,
12.5068366111226));
#418873=CARTESIAN_POINT('Ctrl Pts',(2.6349093181937,0.787245379486807,12.5108395010833));
#418874=CARTESIAN_POINT('Ctrl Pts',(2.63446474934035,0.788730298950861,
12.5149868989719));
#418875=CARTESIAN_POINT('Ctrl Pts',(2.63371805356563,0.791224362764048,
12.5219528491417));
#418876=CARTESIAN_POINT('Ctrl Pts',(2.63339994498634,0.792278189619995,
12.5295503425868));
#418877=CARTESIAN_POINT('Ctrl Pts',(2.63339994499716,0.792278189583032,
12.5369868989719));
#418878=CARTESIAN_POINT('',(2.67238064793001,0.648753938384347,12.5369868989719));
#418879=CARTESIAN_POINT('Ctrl Pts',(2.67238064793001,0.648753938384347,
12.5369868989719));
#418880=CARTESIAN_POINT('Ctrl Pts',(2.67238064793001,0.648753938384349,
12.5309445149785));
#418881=CARTESIAN_POINT('Ctrl Pts',(2.67221027975225,0.649457439217514,
12.5248274368704));
#418882=CARTESIAN_POINT('Ctrl Pts',(2.67181805947575,0.651067014261405,
12.5190199595513));
#418883=CARTESIAN_POINT('Ctrl Pts',(2.67148861905339,0.652418956305285,
12.5141420429941));
#418884=CARTESIAN_POINT('Ctrl Pts',(2.67099251304359,0.654451930845692,
12.5093757677094));
#418885=CARTESIAN_POINT('Ctrl Pts',(2.67030252476298,0.657255221542169,
12.5051960112707));
#418886=CARTESIAN_POINT('Ctrl Pts',(2.66984156502323,0.659128012988347,
12.5024036458141));
#418887=CARTESIAN_POINT('Ctrl Pts',(2.66928273381576,0.66138997784511,12.4998248032393));
#418888=CARTESIAN_POINT('Ctrl Pts',(2.66864322089545,0.663960359937809,
12.4976950015772));
#418889=CARTESIAN_POINT('Ctrl Pts',(2.66798568907971,0.666603165033526,
12.495505190692));
#418890=CARTESIAN_POINT('Ctrl Pts',(2.66722571055259,0.669640107056481,
12.4937456938368));
#418891=CARTESIAN_POINT('Ctrl Pts',(2.6664192713611,0.672835989907007,12.4925987732155));
#418892=CARTESIAN_POINT('Ctrl Pts',(2.66561302087327,0.676031124933269,
12.4914521209692));
#418893=CARTESIAN_POINT('Ctrl Pts',(2.66474010380881,0.679464758759762,
12.4908873016276));
#418894=CARTESIAN_POINT('Ctrl Pts',(2.66387354146977,0.682845337581871,
12.4908873016278));
#418895=CARTESIAN_POINT('',(2.67238064793001,0.648753938384349,13.7435492065112));
#418896=CARTESIAN_POINT('',(2.67238064793001,0.648753938384349,14.));
#418897=CARTESIAN_POINT('',(2.68921555152326,0.57499540645595,13.7435492065112));
#418898=CARTESIAN_POINT('Origin',(0.,2.5406128344257E-15,13.7435492065112));
#418899=CARTESIAN_POINT('',(2.68921555152326,0.57499540645595,12.5369868989719));
#418900=CARTESIAN_POINT('',(2.68921555152326,0.57499540645595,14.));
#418901=CARTESIAN_POINT('Ctrl Pts',(2.69634261720223,0.540589021955712,
12.4908873016278));
#418902=CARTESIAN_POINT('Ctrl Pts',(2.69591381676059,0.542727787002933,
12.4908873016278));
#418903=CARTESIAN_POINT('Ctrl Pts',(2.69548000046878,0.544878086529629,
12.4911020829134));
#418904=CARTESIAN_POINT('Ctrl Pts',(2.69505517102229,0.546971320222566,
12.4915448903141));
#418905=CARTESIAN_POINT('Ctrl Pts',(2.69432833960845,0.550552587992772,
12.4923024798169));
#418906=CARTESIAN_POINT('Ctrl Pts',(2.69361086617432,0.554049009499973,
12.4937722312795));
#418907=CARTESIAN_POINT('Ctrl Pts',(2.6929765607964,0.557115107496846,12.4958030942394));
#418908=CARTESIAN_POINT('Ctrl Pts',(2.69234673255987,0.560159563939431,
12.4978196226833));
#418909=CARTESIAN_POINT('Ctrl Pts',(2.69178054529403,0.562870068975945,
12.5004326847668));
#418910=CARTESIAN_POINT('Ctrl Pts',(2.69131111309108,0.565105735727806,
12.5033504258767));
#418911=CARTESIAN_POINT('Ctrl Pts',(2.69075022452756,0.567776962595234,
12.5068366111226));
#418912=CARTESIAN_POINT('Ctrl Pts',(2.69030968165983,0.569856314692288,
12.5108395010833));
#418913=CARTESIAN_POINT('Ctrl Pts',(2.68998762679431,0.571372529698046,
12.5149868989719));
#418914=CARTESIAN_POINT('Ctrl Pts',(2.68944670494271,0.573919157357266,
12.5219528491417));
#418915=CARTESIAN_POINT('Ctrl Pts',(2.68921555151549,0.574995406493672,
12.5295503425868));
#418916=CARTESIAN_POINT('Ctrl Pts',(2.68921555152326,0.57499540645595,12.5369868989719));
#418917=CARTESIAN_POINT('',(2.71636799049595,0.428771431194994,12.5369868989719));
#418918=CARTESIAN_POINT('Ctrl Pts',(2.71636799049595,0.428771431194994,
12.5369868989719));
#418919=CARTESIAN_POINT('Ctrl Pts',(2.71636799049595,0.428771431194996,
12.5309445149785));
#418920=CARTESIAN_POINT('Ctrl Pts',(2.71625553105313,0.429486477775282,
12.5248274368704));
#418921=CARTESIAN_POINT('Ctrl Pts',(2.71599581116589,0.431122666684725,
12.5190199595513));
#418922=CARTESIAN_POINT('Ctrl Pts',(2.71577766275676,0.432496962705779,
12.5141420429941));
#418923=CARTESIAN_POINT('Ctrl Pts',(2.71544891379703,0.434563609936534,
12.5093757677094));
#418924=CARTESIAN_POINT('Ctrl Pts',(2.71498971561175,0.437413813364882,
12.5051960112707));
#418925=CARTESIAN_POINT('Ctrl Pts',(2.71468293956652,0.439317945750148,
12.5024036458141));
#418926=CARTESIAN_POINT('Ctrl Pts',(2.71431033895867,0.441617934036794,
12.4998248032393));
#418927=CARTESIAN_POINT('Ctrl Pts',(2.71388246396767,0.444231889635074,
12.4976950015772));
#418928=CARTESIAN_POINT('Ctrl Pts',(2.71344253318471,0.446919495962061,
12.495505190692));
#418929=CARTESIAN_POINT('Ctrl Pts',(2.71293262239191,0.450008278116222,
12.4937456938368));
#418930=CARTESIAN_POINT('Ctrl Pts',(2.71238936068175,0.453259259210928,
12.4925987732155));
#418931=CARTESIAN_POINT('Ctrl Pts',(2.71184622609274,0.456509479588592,
12.4914521209692));
#418932=CARTESIAN_POINT('Ctrl Pts',(2.71125608662096,0.460002839126303,
12.4908873016276));
#418933=CARTESIAN_POINT('Ctrl Pts',(2.71066795625438,0.463442802226663,
12.4908873016278));
#418934=CARTESIAN_POINT('',(2.71636799049595,0.428771431194996,13.7435492065112));
#418935=CARTESIAN_POINT('',(2.71636799049595,0.428771431194996,14.));
#418936=CARTESIAN_POINT('',(2.72713487224331,0.353886123766466,13.7435492065112));
#418937=CARTESIAN_POINT('Origin',(0.,2.5406128344257E-15,13.7435492065112));
#418938=CARTESIAN_POINT('',(2.72713487224331,0.353886123766466,12.5369868989719));
#418939=CARTESIAN_POINT('',(2.72713487224331,0.353886123766466,14.));
#418940=CARTESIAN_POINT('Ctrl Pts',(2.73143378344912,0.31901330165504,12.4908873016278));
#418941=CARTESIAN_POINT('Ctrl Pts',(2.73118073901225,0.321179901354785,
12.4908873016278));
#418942=CARTESIAN_POINT('Ctrl Pts',(2.73092363558219,0.32335840599233,12.4911020829134));
#418943=CARTESIAN_POINT('Ctrl Pts',(2.73067083769925,0.325479302166645,
12.4915448903141));
#418944=CARTESIAN_POINT('Ctrl Pts',(2.73023833132712,0.329107897071582,
12.4923024798169));
#418945=CARTESIAN_POINT('Ctrl Pts',(2.72980823603868,0.332651165270232,
12.4937722312795));
#418946=CARTESIAN_POINT('Ctrl Pts',(2.72942595671059,0.335758762855861,
12.4958030942394));
#418947=CARTESIAN_POINT('Ctrl Pts',(2.72904637563899,0.338844425969099,
12.4978196226833));
#418948=CARTESIAN_POINT('Ctrl Pts',(2.72870300363815,0.341592061542097,
12.5004326847668));
#418949=CARTESIAN_POINT('Ctrl Pts',(2.72841736102732,0.343858552379808,
12.5033504258767));
#418950=CARTESIAN_POINT('Ctrl Pts',(2.72807606856238,0.346566608585158,
12.5068366111226));
#418951=CARTESIAN_POINT('Ctrl Pts',(2.72780647806437,0.348674950143163,
12.5108395010833));
#418952=CARTESIAN_POINT('Ctrl Pts',(2.72760908040867,0.350212370529921,
12.5149868989719));
#418953=CARTESIAN_POINT('Ctrl Pts',(2.72727753222588,0.352794614648265,
12.5219528491417));
#418954=CARTESIAN_POINT('Ctrl Pts',(2.72713487223864,0.353886123804696,
12.5295503425868));
#418955=CARTESIAN_POINT('Ctrl Pts',(2.72713487224331,0.353886123766466,
12.5369868989719));
#418956=CARTESIAN_POINT('',(2.74227835225431,0.205935520873343,12.5369868989719));
#418957=CARTESIAN_POINT('Ctrl Pts',(2.74227835225431,0.205935520873343,
12.5369868989719));
#418958=CARTESIAN_POINT('Ctrl Pts',(2.74227835225431,0.205935520873345,
12.5309445149785));
#418959=CARTESIAN_POINT('Ctrl Pts',(2.74222454994548,0.206657354683734,
12.5248274368704));
#418960=CARTESIAN_POINT('Ctrl Pts',(2.74209905884049,0.20830926889149,12.5190199595513));
#418961=CARTESIAN_POINT('Ctrl Pts',(2.74199365418625,0.20969677317644,12.5141420429941));
#418962=CARTESIAN_POINT('Ctrl Pts',(2.74183445004669,0.211783339901194,
12.5093757677094));
#418963=CARTESIAN_POINT('Ctrl Pts',(2.7416090978449,0.214661488427848,12.5051960112707));
#418964=CARTESIAN_POINT('Ctrl Pts',(2.74145854703816,0.216584290065338,
12.5024036458141));
#418965=CARTESIAN_POINT('Ctrl Pts',(2.7412746566255,0.218906995739292,12.4998248032393));
#418966=CARTESIAN_POINT('Ctrl Pts',(2.74106126700128,0.221547129399919,
12.4976950015772));
#418967=CARTESIAN_POINT('Ctrl Pts',(2.74084186491788,0.224261651381494,
12.495505190692));
#418968=CARTESIAN_POINT('Ctrl Pts',(2.74058541523159,0.227381718331238,
12.4937456938368));
#418969=CARTESIAN_POINT('Ctrl Pts',(2.74030894631981,0.230666162927312,
12.4925987732155));
#418970=CARTESIAN_POINT('Ctrl Pts',(2.74003254210069,0.233949838976013,
12.4914521209692));
#418971=CARTESIAN_POINT('Ctrl Pts',(2.73972910750241,0.237479676493582,
12.4908873016276));
#418972=CARTESIAN_POINT('Ctrl Pts',(2.73942332301885,0.240956131485315,
12.4908873016278));
#418973=CARTESIAN_POINT('',(2.74227835225431,0.205935520873345,13.7435492065112));
#418974=CARTESIAN_POINT('',(2.74227835225431,0.205935520873345,14.));
#418975=CARTESIAN_POINT('',(2.74690556033417,0.130421787310419,13.7435492065112));
#418976=CARTESIAN_POINT('Origin',(0.,2.5406128344257E-15,13.7435492065112));
#418977=CARTESIAN_POINT('',(2.74690556033417,0.130421787310419,12.5369868989719));
#418978=CARTESIAN_POINT('',(2.74690556033417,0.130421787310419,14.));
#418979=CARTESIAN_POINT('Ctrl Pts',(2.748347708522,0.0953146004653459,12.4908873016278));
#418980=CARTESIAN_POINT('Ctrl Pts',(2.74827210405888,0.0974946164540769,
12.4908873016278));
#418981=CARTESIAN_POINT('Ctrl Pts',(2.74819342447149,0.0996868286135354,
12.4911020829134));
#418982=CARTESIAN_POINT('Ctrl Pts',(2.74811434048029,0.101821273055113,
12.4915448903141));
#418983=CARTESIAN_POINT('Ctrl Pts',(2.74797903740842,0.105473047394364,
12.4923024798169));
#418984=CARTESIAN_POINT('Ctrl Pts',(2.74783918247886,0.1090395824192,12.4937722312795));
#418985=CARTESIAN_POINT('Ctrl Pts',(2.74771147320646,0.112167999044369,
12.4958030942394));
#418986=CARTESIAN_POINT('Ctrl Pts',(2.74758466534919,0.11527433424934,12.4978196226833));
#418987=CARTESIAN_POINT('Ctrl Pts',(2.74746639369736,0.118040815297413,
12.5004326847668));
#418988=CARTESIAN_POINT('Ctrl Pts',(2.7473664415831,0.120323047098392,12.5033504258767));
#418989=CARTESIAN_POINT('Ctrl Pts',(2.74724701646178,0.123049910974415,
12.5068366111226));
#418990=CARTESIAN_POINT('Ctrl Pts',(2.74715017241379,0.125173211328155,
12.5108395010833));
#418991=CARTESIAN_POINT('Ctrl Pts',(2.74707874561673,0.126721605816895,
12.5149868989719));
#418992=CARTESIAN_POINT('Ctrl Pts',(2.7469587775012,0.129322281985796,12.5219528491417));
#418993=CARTESIAN_POINT('Ctrl Pts',(2.74690556033263,0.130421787348903,
12.5295503425868));
#418994=CARTESIAN_POINT('Ctrl Pts',(2.74690556033417,0.130421787310419,
12.5369868989719));
#418995=CARTESIAN_POINT('',(2.74993930402251,-0.0182708563627483,12.5369868989719));
#418996=CARTESIAN_POINT('Ctrl Pts',(2.7499393040225,-0.0182708563627482,
12.5369868989719));
#418997=CARTESIAN_POINT('Ctrl Pts',(2.7499393040225,-0.0182708563627464,
12.5309445149785));
#418998=CARTESIAN_POINT('Ctrl Pts',(2.74994451689314,-0.0175470390071679,
12.5248274368704));
#418999=CARTESIAN_POINT('Ctrl Pts',(2.749954089693,-0.015890392717606,12.5190199595513));
#419000=CARTESIAN_POINT('Ctrl Pts',(2.74996213024424,-0.0144989137808532,
12.5141420429941));
#419001=CARTESIAN_POINT('Ctrl Pts',(2.74997353040213,-0.0124063133193932,
12.5093757677094));
#419002=CARTESIAN_POINT('Ctrl Pts',(2.74998352386555,-0.00951937329801796,
12.5051960112707));
#419003=CARTESIAN_POINT('Ctrl Pts',(2.74999020018808,-0.00759069833596158,
12.5024036458141));
#419004=CARTESIAN_POINT('Ctrl Pts',(2.74999624373097,-0.00526073249774117,
12.4998248032393));
#419005=CARTESIAN_POINT('Ctrl Pts',(2.74999875954626,-0.00261199042868737,
12.4976950015772));
#419006=CARTESIAN_POINT('Ctrl Pts',(2.75000134624709,0.000111382511553625,
12.495505190692));
#419007=CARTESIAN_POINT('Ctrl Pts',(2.75000006429767,0.00324197072610468,
12.4937456938368));
#419008=CARTESIAN_POINT('Ctrl Pts',(2.74999222803926,0.00653802138665501,
12.4925987732155));
#419009=CARTESIAN_POINT('Ctrl Pts',(2.74998439361451,0.00983330078405806,
12.4914521209692));
#419010=CARTESIAN_POINT('Ctrl Pts',(2.74996968319692,0.0133761257951871,
12.4908873016276));
#419011=CARTESIAN_POINT('Ctrl Pts',(2.74994827954166,0.0168659374438978,
12.4908873016278));
#419012=CARTESIAN_POINT('',(2.7499393040225,-0.0182708563627466,13.7435492065112));
#419013=CARTESIAN_POINT('',(2.74993930402251,-0.0182708563627466,14.));
#419014=CARTESIAN_POINT('',(2.74839604512851,-0.0939104846220984,13.7435492065112));
#419015=CARTESIAN_POINT('Origin',(0.,2.5406128344257E-15,13.7435492065112));
#419016=CARTESIAN_POINT('',(2.74839604512851,-0.0939104846220985,12.5369868989719));
#419017=CARTESIAN_POINT('',(2.74839604512851,-0.0939104846220985,14.));
#419018=CARTESIAN_POINT('Ctrl Pts',(2.74697183304013,-0.129018403664643,
12.4908873016278));
#419019=CARTESIAN_POINT('Ctrl Pts',(2.74707417168598,-0.126839479033654,
12.4908873016278));
#419020=CARTESIAN_POINT('Ctrl Pts',(2.74717443954093,-0.124648148162513,
12.4911020829134));
#419021=CARTESIAN_POINT('Ctrl Pts',(2.7472695957324,-0.122514359829273,
12.4915448903141));
#419022=CARTESIAN_POINT('Ctrl Pts',(2.7474323963804,-0.118863708011436,
12.4923024798169));
#419023=CARTESIAN_POINT('Ctrl Pts',(2.7475837125212,-0.115297640862568,
12.4937722312795));
#419024=CARTESIAN_POINT('Ctrl Pts',(2.74771142318862,-0.112169224294347,
12.4958030942394));
#419025=CARTESIAN_POINT('Ctrl Pts',(2.74783823243105,-0.109062889145921,
12.4978196226833));
#419026=CARTESIAN_POINT('Ctrl Pts',(2.74794584820655,-0.106295973097713,
12.5004326847668));
#419027=CARTESIAN_POINT('Ctrl Pts',(2.7480322517537,-0.104013188209558,
12.5033504258767));
#419028=CARTESIAN_POINT('Ctrl Pts',(2.74813548873049,-0.101285663492056,
12.5068366111226));
#419029=CARTESIAN_POINT('Ctrl Pts',(2.74821203561366,-0.0991615345561148,
12.5108395010833));
#419030=CARTESIAN_POINT('Ctrl Pts',(2.74826705500881,-0.0976124702752494,
12.5149868989719));
#419031=CARTESIAN_POINT('Ctrl Pts',(2.74835946532855,-0.0950106691266142,
12.5219528491417));
#419032=CARTESIAN_POINT('Ctrl Pts',(2.74839604513011,-0.093910484583617,
12.5295503425868));
#419033=CARTESIAN_POINT('Ctrl Pts',(2.74839604512851,-0.0939104846220985,
12.5369868989719));
#419034=CARTESIAN_POINT('',(2.73929986343048,-0.242355644064225,12.5369868989719));
#419035=CARTESIAN_POINT('Ctrl Pts',(2.73929986343047,-0.242355644064225,
12.5369868989719));
#419036=CARTESIAN_POINT('Ctrl Pts',(2.73929986343047,-0.242355644064223,
12.5309445149785));
#419037=CARTESIAN_POINT('Ctrl Pts',(2.73936405678979,-0.241634660048535,
12.5248274368704));
#419038=CARTESIAN_POINT('Ctrl Pts',(2.7395086297891,-0.239984306384896,
12.5190199595513));
#419039=CARTESIAN_POINT('Ctrl Pts',(2.73963006203727,-0.238598112859088,
12.5141420429941));
#419040=CARTESIAN_POINT('Ctrl Pts',(2.73981199062644,-0.236513404571738,
12.5093757677094));
#419041=CARTESIAN_POINT('Ctrl Pts',(2.74005726325022,-0.233636885165171,
12.5051960112707));
#419042=CARTESIAN_POINT('Ctrl Pts',(2.74022112227219,-0.231715171892212,
12.5024036458141));
#419043=CARTESIAN_POINT('Ctrl Pts',(2.74041705955186,-0.229393451427962,
12.4998248032393));
#419044=CARTESIAN_POINT('Ctrl Pts',(2.74063546406433,-0.226753727891939,
12.4976950015772));
#419045=CARTESIAN_POINT('Ctrl Pts',(2.74086002233531,-0.224039627590625,
12.495505190692));
#419046=CARTESIAN_POINT('Ctrl Pts',(2.74111391665392,-0.220919351659323,
12.4937456938368));
#419047=CARTESIAN_POINT('Ctrl Pts',(2.74137476519789,-0.217633629607633,
12.4925987732155));
#419048=CARTESIAN_POINT('Ctrl Pts',(2.74163555270431,-0.214348676402234,
12.4914521209692));
#419049=CARTESIAN_POINT('Ctrl Pts',(2.74190966436281,-0.210816440813469,
12.4908873016276));
#419050=CARTESIAN_POINT('Ctrl Pts',(2.74217278397365,-0.207336496628525,
12.4908873016278));
#419051=CARTESIAN_POINT('',(2.73929986343048,-0.242355644064223,13.7435492065112));
#419052=CARTESIAN_POINT('',(2.73929986343048,-0.242355644064223,14.));
#419053=CARTESIAN_POINT('',(2.73159640769596,-0.317617797773595,13.7435492065112));
#419054=CARTESIAN_POINT('Origin',(0.,2.5406128344257E-15,13.7435492065112));
#419055=CARTESIAN_POINT('',(2.73159640769596,-0.317617797773595,12.5369868989719));
#419056=CARTESIAN_POINT('',(2.73159640769596,-0.317617797773595,14.));
#419057=CARTESIAN_POINT('Ctrl Pts',(2.72731531322782,-0.352492811604782,
12.4908873016278));
#419058=CARTESIAN_POINT('Ctrl Pts',(2.72759491393585,-0.350329478715456,
12.4908873016278));
#419059=CARTESIAN_POINT('Ctrl Pts',(2.7278734619671,-0.348153612078037,
12.4911020829134));
#419060=CARTESIAN_POINT('Ctrl Pts',(2.72814222509247,-0.346034679862442,
12.4915448903141));
#419061=CARTESIAN_POINT('Ctrl Pts',(2.7286020460489,-0.342409445051551,
12.4923024798169));
#419062=CARTESIAN_POINT('Ctrl Pts',(2.72904352627611,-0.338867577367167,
12.4937722312795));
#419063=CARTESIAN_POINT('Ctrl Pts',(2.72942580698993,-0.335759979952003,
12.4958030942394));
#419064=CARTESIAN_POINT('Ctrl Pts',(2.72980538943748,-0.332674317008026,
12.4978196226833));
#419065=CARTESIAN_POINT('Ctrl Pts',(2.73013817647509,-0.329925379329474,
12.5004326847668));
#419066=CARTESIAN_POINT('Ctrl Pts',(2.73041036068228,-0.327657232910942,
12.5033504258767));
#419067=CARTESIAN_POINT('Ctrl Pts',(2.73073557273213,-0.324947198578946,
12.5068366111226));
#419068=CARTESIAN_POINT('Ctrl Pts',(2.73098500113959,-0.322836376788416,
12.5108395010833));
#419069=CARTESIAN_POINT('Ctrl Pts',(2.73116610058194,-0.321296951482636,
12.5149868989719));
#419070=CARTESIAN_POINT('Ctrl Pts',(2.73147027436152,-0.318711339911643,
12.5219528491417));
#419071=CARTESIAN_POINT('Ctrl Pts',(2.73159640770069,-0.317617797735372,
12.5295503425868));
#419072=CARTESIAN_POINT('Ctrl Pts',(2.73159640769596,-0.317617797773595,
12.5369868989719));
#419073=CARTESIAN_POINT('',(2.71043083419998,-0.464827594940321,12.5369868989719));
#419074=CARTESIAN_POINT('Ctrl Pts',(2.71043083419998,-0.46482759494032,
12.5369868989719));
#419075=CARTESIAN_POINT('Ctrl Pts',(2.71043083419998,-0.464827594940319,
12.5309445149785));
#419076=CARTESIAN_POINT('Ctrl Pts',(2.71055358085175,-0.464114242294192,
12.5248274368704));
#419077=CARTESIAN_POINT('Ctrl Pts',(2.71083219194106,-0.462481164087819,
12.5190199595513));
#419078=CARTESIAN_POINT('Ctrl Pts',(2.71106620777459,-0.461109480862163,
12.5141420429941));
#419079=CARTESIAN_POINT('Ctrl Pts',(2.71141745409029,-0.459046538138622,
12.5093757677094));
#419080=CARTESIAN_POINT('Ctrl Pts',(2.71189637362559,-0.456199582108923,
12.5051960112707));
#419081=CARTESIAN_POINT('Ctrl Pts',(2.71221632489224,-0.454297619209833,
12.5024036458141));
#419082=CARTESIAN_POINT('Ctrl Pts',(2.71260085197841,-0.451999594786184,
12.4998248032393));
#419083=CARTESIAN_POINT('Ctrl Pts',(2.71303369174207,-0.449386456707801,
12.4976950015772));
#419084=CARTESIAN_POINT('Ctrl Pts',(2.71347872718496,-0.446699690935124,
12.495505190692));
#419085=CARTESIAN_POINT('Ctrl Pts',(2.7139861081468,-0.443610492208585,
12.4937456938368));
#419086=CARTESIAN_POINT('Ctrl Pts',(2.71451390558913,-0.440356964703903,
12.4925987732155));
#419087=CARTESIAN_POINT('Ctrl Pts',(2.7150415795289,-0.437104198512112,
12.4914521209692));
#419088=CARTESIAN_POINT('Ctrl Pts',(2.71560268909562,-0.433606058790776,
12.4908873016276));
#419089=CARTESIAN_POINT('Ctrl Pts',(2.71614858095496,-0.430159140523998,
12.4908873016278));
#419090=CARTESIAN_POINT('',(2.71043083419998,-0.464827594940319,13.7435492065112));
#419091=CARTESIAN_POINT('',(2.71043083419998,-0.464827594940319,14.));
#419092=CARTESIAN_POINT('',(2.69661844685187,-0.539211416884157,13.7435492065112));
#419093=CARTESIAN_POINT('Origin',(0.,2.5406128344257E-15,13.7435492065112));
#419094=CARTESIAN_POINT('',(2.69661844685187,-0.539211416884157,12.5369868989719));
#419095=CARTESIAN_POINT('',(2.69661844685187,-0.539211416884157,14.));
#419096=CARTESIAN_POINT('Ctrl Pts',(2.68950895998134,-0.573621438040911,
12.4908873016278));
#419097=CARTESIAN_POINT('Ctrl Pts',(2.68996396205496,-0.571488093516703,
12.4908873016278));
#419098=CARTESIAN_POINT('Ctrl Pts',(2.69041893657132,-0.569342171146484,
12.4911020829134));
#419099=CARTESIAN_POINT('Ctrl Pts',(2.69085951805634,-0.56725219619283,
12.4915448903141));
#419100=CARTESIAN_POINT('Ctrl Pts',(2.6916132992886,-0.563676503728429,
12.4923024798169));
#419101=CARTESIAN_POINT('Ctrl Pts',(2.69234200562415,-0.560182406053602,
12.4937722312795));
#419102=CARTESIAN_POINT('Ctrl Pts',(2.69297631236929,-0.557116308339575,
12.4958030942394));
#419103=CARTESIAN_POINT('Ctrl Pts',(2.69360614196338,-0.554071852177842,
12.4978196226833));
#419104=CARTESIAN_POINT('Ctrl Pts',(2.69416188562028,-0.551359186595653,
12.5004326847668));
#419105=CARTESIAN_POINT('Ctrl Pts',(2.69461803914653,-0.549120772786941,
12.5033504258767));
#419106=CARTESIAN_POINT('Ctrl Pts',(2.6951630620369,-0.546446263671806,
12.5068366111226));
#419107=CARTESIAN_POINT('Ctrl Pts',(2.69558371206375,-0.544362796197442,
12.5108395010833));
#419108=CARTESIAN_POINT('Ctrl Pts',(2.6958896863664,-0.542843254488171,
12.5149868989719));
#419109=CARTESIAN_POINT('Ctrl Pts',(2.6964035993795,-0.54029103931323,12.5219528491417));
#419110=CARTESIAN_POINT('Ctrl Pts',(2.6966184468597,-0.539211416846447,
12.5295503425868));
#419111=CARTESIAN_POINT('Ctrl Pts',(2.69661844685187,-0.539211416884157,
12.5369868989719));
#419112=CARTESIAN_POINT('',(2.6635243349575,-0.684206194863244,12.5369868989719));
#419113=CARTESIAN_POINT('Ctrl Pts',(2.66352433495749,-0.684206194863243,
12.5369868989719));
#419114=CARTESIAN_POINT('Ctrl Pts',(2.66352433495749,-0.684206194863241,
12.5309445149785));
#419115=CARTESIAN_POINT('Ctrl Pts',(2.66370481804301,-0.683505220830841,
12.5248274368704));
#419116=CARTESIAN_POINT('Ctrl Pts',(2.66411561311148,-0.681900285947758,
12.5190199595513));
#419117=CARTESIAN_POINT('Ctrl Pts',(2.66446065519361,-0.680552241347809,
12.5141420429941));
#419118=CARTESIAN_POINT('Ctrl Pts',(2.66497888174957,-0.678524792731542,
12.5093757677094));
#419119=CARTESIAN_POINT('Ctrl Pts',(2.66568826106589,-0.675726346101373,
12.5051960112707));
#419120=CARTESIAN_POINT('Ctrl Pts',(2.66616217535433,-0.673856790825442,
12.5024036458141));
#419121=CARTESIAN_POINT('Ctrl Pts',(2.66673273328269,-0.671597755415789,
12.4998248032393));
#419122=CARTESIAN_POINT('Ctrl Pts',(2.66737712782032,-0.669028592797819,
12.4976950015772));
#419123=CARTESIAN_POINT('Ctrl Pts',(2.66803967879768,-0.666387041536711,
12.495505190692));
#419124=CARTESIAN_POINT('Ctrl Pts',(2.66879716986615,-0.663349478122779,
12.4937456938368));
#419125=CARTESIAN_POINT('Ctrl Pts',(2.66958840380194,-0.660149796853853,
12.4925987732155));
#419126=CARTESIAN_POINT('Ctrl Pts',(2.67037945259204,-0.656950864298008,
12.4914521209692));
#419127=CARTESIAN_POINT('Ctrl Pts',(2.67122382597541,-0.653510099986794,
12.4908873016276));
#419128=CARTESIAN_POINT('Ctrl Pts',(2.67204885726299,-0.650119146310548,
12.4908873016278));
#419129=CARTESIAN_POINT('',(2.66352433495749,-0.684206194863242,13.7435492065112));
#419130=CARTESIAN_POINT('',(2.6635243349575,-0.684206194863242,14.));
#419131=CARTESIAN_POINT('',(2.64369493515471,-0.757216672978976,13.7435492065112));
#419132=CARTESIAN_POINT('Origin',(0.,2.5406128344257E-15,13.7435492065112));
#419133=CARTESIAN_POINT('',(2.64369493515471,-0.757216672978976,12.5369868989719));
#419134=CARTESIAN_POINT('',(2.64369493515471,-0.757216672978976,14.));
#419135=CARTESIAN_POINT('Ctrl Pts',(2.63380436834392,-0.790932708447753,
12.4908873016278));
#419136=CARTESIAN_POINT('Ctrl Pts',(2.6344317438194,-0.788843549344495,
12.4908873016278));
#419137=CARTESIAN_POINT('Ctrl Pts',(2.63506011704054,-0.786741852000797,
12.4911020829134));
#419138=CARTESIAN_POINT('Ctrl Pts',(2.63566958488812,-0.784694742747579,
12.4915448903141));
#419139=CARTESIAN_POINT('Ctrl Pts',(2.63671231010647,-0.781192388273072,
12.4923024798169));
#419140=CARTESIAN_POINT('Ctrl Pts',(2.63772339312991,-0.777769313251341,
12.4937722312795));
#419141=CARTESIAN_POINT('Ctrl Pts',(2.63860550469964,-0.774765119612869,
12.4958030942394));
#419142=CARTESIAN_POINT('Ctrl Pts',(2.63948139002826,-0.771782130586836,
12.4978196226833));
#419143=CARTESIAN_POINT('Ctrl Pts',(2.64025639192208,-0.769123789442901,
12.5004326847668));
#419144=CARTESIAN_POINT('Ctrl Pts',(2.64089347914094,-0.766930004518594,
12.5033504258767));
#419145=CARTESIAN_POINT('Ctrl Pts',(2.64165468583441,-0.764308819037219,
12.5068366111226));
#419146=CARTESIAN_POINT('Ctrl Pts',(2.64224375812413,-0.762266571011315,
12.5108395010833));
#419147=CARTESIAN_POINT('Ctrl Pts',(2.64267257107857,-0.760777025197919,
12.5149868989719));
#419148=CARTESIAN_POINT('Ctrl Pts',(2.64339280331889,-0.758275190989934,
12.5219528491417));
#419149=CARTESIAN_POINT('Ctrl Pts',(2.64369493516559,-0.75721667294203,
12.5295503425868));
#419150=CARTESIAN_POINT('Ctrl Pts',(2.64369493515471,-0.757216672978976,
12.5369868989719));
#419151=CARTESIAN_POINT('',(2.59889252071645,-0.899031515445429,12.5369868989719));
#419152=CARTESIAN_POINT('Ctrl Pts',(2.59889252071645,-0.899031515445427,
12.5369868989719));
#419153=CARTESIAN_POINT('Ctrl Pts',(2.59889252071645,-0.899031515445425,
12.5309445149785));
#419154=CARTESIAN_POINT('Ctrl Pts',(2.59912953915055,-0.898347584893284,
12.5248274368704));
#419155=CARTESIAN_POINT('Ctrl Pts',(2.59966978442478,-0.896781473910343,
12.5190199595513));
#419156=CARTESIAN_POINT('Ctrl Pts',(2.60012355655737,-0.895466038950502,
12.5141420429941));
#419157=CARTESIAN_POINT('Ctrl Pts',(2.60080531464136,-0.893487576777544,
12.5093757677094));
#419158=CARTESIAN_POINT('Ctrl Pts',(2.6017404329364,-0.890756262747518,
12.5051960112707));
#419159=CARTESIAN_POINT('Ctrl Pts',(2.60236515642523,-0.888931556676653,
12.5024036458141));
#419160=CARTESIAN_POINT('Ctrl Pts',(2.6031179482269,-0.886726543788931,
12.4998248032393));
#419161=CARTESIAN_POINT('Ctrl Pts',(2.60396960919917,-0.884218453984716,
12.4976950015772));
#419162=CARTESIAN_POINT('Ctrl Pts',(2.60484526654355,-0.881639696322995,
12.495505190692));
#419163=CARTESIAN_POINT('Ctrl Pts',(2.60584782674059,-0.878673982705026,
12.4937456938368));
#419164=CARTESIAN_POINT('Ctrl Pts',(2.60689723163854,-0.875549441022792,
12.4925987732155));
#419165=CARTESIAN_POINT('Ctrl Pts',(2.60794639097979,-0.872425630471265,
12.4914521209692));
#419166=CARTESIAN_POINT('Ctrl Pts',(2.60906840901424,-0.869065139288977,
12.4908873016276));
#419167=CARTESIAN_POINT('Ctrl Pts',(2.61016708928296,-0.865752716440509,
12.4908873016278));
#419168=CARTESIAN_POINT('',(2.59889252071645,-0.899031515445426,13.7435492065112));
#419169=CARTESIAN_POINT('',(2.59889252071645,-0.899031515445427,14.));
#419170=CARTESIAN_POINT('',(2.57317806984305,-0.970182777047077,13.7435492065112));
#419171=CARTESIAN_POINT('Origin',(0.,2.5406128344257E-15,13.7435492065112));
#419172=CARTESIAN_POINT('',(2.57317806984306,-0.970182777047077,12.5369868989719));
#419173=CARTESIAN_POINT('',(2.57317806984306,-0.970182777047077,14.));
#419174=CARTESIAN_POINT('Ctrl Pts',(2.56057224318231,-1.00298045217459,
12.4908873016278));
#419175=CARTESIAN_POINT('Ctrl Pts',(2.56136781697937,-1.00094938150142,
12.4908873016278));
#419176=CARTESIAN_POINT('Ctrl Pts',(2.56216540718517,-0.998905895633315,
12.4911020829134));
#419177=CARTESIAN_POINT('Ctrl Pts',(2.56293970548734,-0.996915275254863,
12.4915448903141));
#419178=CARTESIAN_POINT('Ctrl Pts',(2.56426443552748,-0.99350956636143,
12.4923024798169));
#419179=CARTESIAN_POINT('Ctrl Pts',(2.56555116664813,-0.990180293992298,
12.4937722312795));
#419180=CARTESIAN_POINT('Ctrl Pts',(2.56667521273549,-0.987257996842386,
12.4958030942394));
#419181=CARTESIAN_POINT('Ctrl Pts',(2.56779132492627,-0.984356326251862,
12.4978196226833));
#419182=CARTESIAN_POINT('Ctrl Pts',(2.56878042754729,-0.9817700003679,12.5004326847668));
#419183=CARTESIAN_POINT('Ctrl Pts',(2.56959420874842,-0.979635443604719,
12.5033504258767));
#419184=CARTESIAN_POINT('Ctrl Pts',(2.57056653354004,-0.977085025314017,
12.5068366111226));
#419185=CARTESIAN_POINT('Ctrl Pts',(2.57132010791373,-0.975097587560238,
12.5108395010833));
#419186=CARTESIAN_POINT('Ctrl Pts',(2.5718689058405,-0.97364795032435,12.5149868989719));
#419187=CARTESIAN_POINT('Ctrl Pts',(2.5727906642813,-0.971213146377201,
12.5219528491417));
#419188=CARTESIAN_POINT('Ctrl Pts',(2.57317806985691,-0.970182777011141,
12.5295503425868));
#419189=CARTESIAN_POINT('Ctrl Pts',(2.57317806984306,-0.970182777047077,
12.5369868989719));
#419190=CARTESIAN_POINT('',(2.51696550553712,-1.10787392962208,12.5369868989719));
#419191=CARTESIAN_POINT('Ctrl Pts',(2.51696550553712,-1.10787392962208,
12.5369868989719));
#419192=CARTESIAN_POINT('Ctrl Pts',(2.51696550553712,-1.10787392962208,
12.5309445149785));
#419193=CARTESIAN_POINT('Ctrl Pts',(2.51725748200124,-1.10721159399518,
12.5248274368704));
#419194=CARTESIAN_POINT('Ctrl Pts',(2.51792358223806,-1.10569472912258,
12.5190199595513));
#419195=CARTESIAN_POINT('Ctrl Pts',(2.51848306464244,-1.10442065780548,
12.5141420429941));
#419196=CARTESIAN_POINT('Ctrl Pts',(2.51932381726689,-1.10250434841516,
12.5093757677094));
#419197=CARTESIAN_POINT('Ctrl Pts',(2.52047845148267,-1.09985834342952,
12.5051960112707));
#419198=CARTESIAN_POINT('Ctrl Pts',(2.52124982674015,-1.09809062968156,
12.5024036458141));
#419199=CARTESIAN_POINT('Ctrl Pts',(2.52217984270989,-1.09595431331274,
12.4998248032393));
#419200=CARTESIAN_POINT('Ctrl Pts',(2.52323310245354,-1.09352398724612,
12.4976950015772));
#419201=CARTESIAN_POINT('Ctrl Pts',(2.5243160388098,-1.09102518439056,12.495505190692));
#419202=CARTESIAN_POINT('Ctrl Pts',(2.52555699626269,-1.08815105690337,
12.4937456938368));
#419203=CARTESIAN_POINT('Ctrl Pts',(2.52685758850634,-1.08512244811721,
12.4925987732155));
#419204=CARTESIAN_POINT('Ctrl Pts',(2.52815787641643,-1.08209454801383,
12.4914521209692));
#419205=CARTESIAN_POINT('Ctrl Pts',(2.52955007225706,-1.07883669347485,
12.4908873016276));
#419206=CARTESIAN_POINT('Ctrl Pts',(2.53091508997101,-1.0756248450817,12.4908873016278));
#419207=CARTESIAN_POINT('',(2.51696550553712,-1.10787392962208,13.7435492065112));
#419208=CARTESIAN_POINT('',(2.51696550553712,-1.10787392962208,14.));
#419209=CARTESIAN_POINT('',(2.48553712902109,-1.17669247480282,13.7435492065112));
#419210=CARTESIAN_POINT('Origin',(0.,2.5406128344257E-15,13.7435492065112));
#419211=CARTESIAN_POINT('',(2.48553712902109,-1.17669247480282,12.5369868989719));
#419212=CARTESIAN_POINT('',(2.4855371290211,-1.17669247480282,14.));
#419213=CARTESIAN_POINT('Ctrl Pts',(2.470299932207,-1.20835352647233,12.4908873016278));
#419214=CARTESIAN_POINT('Ctrl Pts',(2.47125840991329,-1.20639406066948,
12.4908873016278));
#419215=CARTESIAN_POINT('Ctrl Pts',(2.47221990927252,-1.20442238533826,
12.4911020829134));
#419216=CARTESIAN_POINT('Ctrl Pts',(2.47315388520183,-1.20250150108477,
12.4915448903141));
#419217=CARTESIAN_POINT('Ctrl Pts',(2.47475180420392,-1.19921510220319,
12.4923024798169));
#419218=CARTESIAN_POINT('Ctrl Pts',(2.47630562043845,-1.19600178824498,
12.4937722312795));
#419219=CARTESIAN_POINT('Ctrl Pts',(2.47766412070218,-1.19318083498902,
12.4958030942394));
#419220=CARTESIAN_POINT('Ctrl Pts',(2.47901303221264,-1.19037979297304,
12.4978196226833));
#419221=CARTESIAN_POINT('Ctrl Pts',(2.48020965324611,-1.1878826939211,12.5004326847668));
#419222=CARTESIAN_POINT('Ctrl Pts',(2.48119471284988,-1.18582157044213,
12.5033504258767));
#419223=CARTESIAN_POINT('Ctrl Pts',(2.48237168507859,-1.18335889195503,
12.5068366111226));
#419224=CARTESIAN_POINT('Ctrl Pts',(2.48328474662312,-1.18143949054373,
12.5108395010833));
#419225=CARTESIAN_POINT('Ctrl Pts',(2.48394987736256,-1.18003940898198,
12.5149868989719));
#419226=CARTESIAN_POINT('Ctrl Pts',(2.4850670278535,-1.17768783851422,12.5219528491417));
#419227=CARTESIAN_POINT('Ctrl Pts',(2.48553712903783,-1.17669247476813,
12.5295503425868));
#419228=CARTESIAN_POINT('Ctrl Pts',(2.48553712902109,-1.17669247480282,
12.5369868989719));
#419229=CARTESIAN_POINT('',(2.41828850018852,-1.30934362558343,12.5369868989719));
#419230=CARTESIAN_POINT('Ctrl Pts',(2.41828850018852,-1.30934362558343,
12.5369868989719));
#419231=CARTESIAN_POINT('Ctrl Pts',(2.41828850018852,-1.30934362558343,
12.5309445149785));
#419232=CARTESIAN_POINT('Ctrl Pts',(2.41863349162745,-1.30870729261609,
12.5248274368704));
#419233=CARTESIAN_POINT('Ctrl Pts',(2.41942101403969,-1.3072497683393,12.5190199595513));
#419234=CARTESIAN_POINT('Ctrl Pts',(2.42008248345277,-1.30602553939934,
12.5141420429941));
#419235=CARTESIAN_POINT('Ctrl Pts',(2.42107663554767,-1.3041841355145,12.5093757677094));
#419236=CARTESIAN_POINT('Ctrl Pts',(2.422443101784,-1.30164104829985,12.5051960112707));
#419237=CARTESIAN_POINT('Ctrl Pts',(2.42335599543505,-1.29994209071815,
12.5024036458141));
#419238=CARTESIAN_POINT('Ctrl Pts',(2.42445704647003,-1.29788868770119,
12.4998248032393));
#419239=CARTESIAN_POINT('Ctrl Pts',(2.42570489571525,-1.29555229879116,
12.4976950015772));
#419240=CARTESIAN_POINT('Ctrl Pts',(2.4269879043206,-1.29315007986249,12.495505190692));
#419241=CARTESIAN_POINT('Ctrl Pts',(2.42845900066224,-1.29038666535032,
12.4937456938368));
#419242=CARTESIAN_POINT('Ctrl Pts',(2.4300021250248,-1.28747414435202,12.4925987732155));
#419243=CARTESIAN_POINT('Ctrl Pts',(2.4315448883022,-1.2845623048724,12.4914521209692));
#419244=CARTESIAN_POINT('Ctrl Pts',(2.4331979971154,-1.28142876746117,12.4908873016276));
#419245=CARTESIAN_POINT('Ctrl Pts',(2.4348202683069,-1.27833886784448,12.4908873016278));
#419246=CARTESIAN_POINT('',(2.41828850018852,-1.30934362558343,13.7435492065112));
#419247=CARTESIAN_POINT('',(2.41828850018852,-1.30934362558343,14.));
#419248=CARTESIAN_POINT('',(2.38135534869026,-1.37537147827934,13.7435492065112));
#419249=CARTESIAN_POINT('Origin',(0.,2.5406128344257E-15,13.7435492065112));
#419250=CARTESIAN_POINT('',(2.38135534869026,-1.37537147827934,12.5369868989719));
#419251=CARTESIAN_POINT('',(2.38135534869026,-1.37537147827935,14.));
#419252=CARTESIAN_POINT('Ctrl Pts',(2.36358818275365,-1.40568520741569,
12.4908873016278));
#419253=CARTESIAN_POINT('Ctrl Pts',(2.36470318585817,-1.4038103864048,12.4908873016278));
#419254=CARTESIAN_POINT('Ctrl Pts',(2.36582219575124,-1.40192364278449,
12.4911020829134));
#419255=CARTESIAN_POINT('Ctrl Pts',(2.36690963385196,-1.40008527782374,
12.4915448903141));
#419256=CARTESIAN_POINT('Ctrl Pts',(2.36877010792868,-1.39694005939636,
12.4923024798169));
#419257=CARTESIAN_POINT('Ctrl Pts',(2.37058066888642,-1.39386408792331,
12.4937722312795));
#419258=CARTESIAN_POINT('Ctrl Pts',(2.37216458273141,-1.39116325153978,
12.4958030942394));
#419259=CARTESIAN_POINT('Ctrl Pts',(2.373737316778,-1.38848147857083,12.4978196226833));
#419260=CARTESIAN_POINT('Ctrl Pts',(2.37513349290836,-1.3860902241331,12.5004326847668));
#419261=CARTESIAN_POINT('Ctrl Pts',(2.37628327550563,-1.38411625037503,
12.5033504258767));
#419262=CARTESIAN_POINT('Ctrl Pts',(2.37765706261544,-1.38175770041056,
12.5068366111226));
#419263=CARTESIAN_POINT('Ctrl Pts',(2.37872353505688,-1.37991910864144,
12.5108395010833));
#419264=CARTESIAN_POINT('Ctrl Pts',(2.37950057227366,-1.37857790006563,
12.5149868989719));
#419265=CARTESIAN_POINT('Ctrl Pts',(2.38080568036253,-1.37632521239074,
12.5219528491417));
#419266=CARTESIAN_POINT('Ctrl Pts',(2.38135534870977,-1.37537147824614,
12.5295503425868));
#419267=CARTESIAN_POINT('Ctrl Pts',(2.38135534869026,-1.37537147827934,
12.5369868989719));
#419268=CARTESIAN_POINT('',(2.30351818386068,-1.50209985574302,12.5369868989719));
#419269=CARTESIAN_POINT('Ctrl Pts',(2.30351818386068,-1.50209985574302,
12.5369868989719));
#419270=CARTESIAN_POINT('Ctrl Pts',(2.30351818386068,-1.50209985574302,
12.5309445149785));
#419271=CARTESIAN_POINT('Ctrl Pts',(2.30391389441333,-1.50149376012615,
12.5248274368704));
#419272=CARTESIAN_POINT('Ctrl Pts',(2.30481759816925,-1.50010527602875,
12.5190199595513));
#419273=CARTESIAN_POINT('Ctrl Pts',(2.30557665262123,-1.49893903650754,
12.5141420429941));
#419274=CARTESIAN_POINT('Ctrl Pts',(2.30671758826842,-1.49718479236722,
12.5093757677094));
#419275=CARTESIAN_POINT('Ctrl Pts',(2.30828679291793,-1.49476154674939,
12.5051960112707));
#419276=CARTESIAN_POINT('Ctrl Pts',(2.30933512980593,-1.49314265161635,
12.5024036458141));
#419277=CARTESIAN_POINT('Ctrl Pts',(2.31059988859316,-1.49118582700954,
12.4998248032393));
#419278=CARTESIAN_POINT('Ctrl Pts',(2.31203402310911,-1.48895892353883,
12.4976950015772));
#419279=CARTESIAN_POINT('Ctrl Pts',(2.31350856575296,-1.48666927490768,
12.495505190692));
#419280=CARTESIAN_POINT('Ctrl Pts',(2.31520001107991,-1.48403496343817,
12.4937456938368));
#419281=CARTESIAN_POINT('Ctrl Pts',(2.31697539832334,-1.48125791257444,
12.4925987732155));
#419282=CARTESIAN_POINT('Ctrl Pts',(2.318750370133,-1.4784815115299,12.4914521209692));
#419283=CARTESIAN_POINT('Ctrl Pts',(2.32065339075235,-1.4754931444209,12.4908873016276));
#419284=CARTESIAN_POINT('Ctrl Pts',(2.32252211947427,-1.47254575635283,
12.4908873016278));
#419285=CARTESIAN_POINT('',(2.30351818386068,-1.50209985574302,13.7435492065112));
#419286=CARTESIAN_POINT('',(2.30351818386068,-1.50209985574302,14.));
#419287=CARTESIAN_POINT('',(2.26132604140986,-1.56489761148824,13.7435492065112));
#419288=CARTESIAN_POINT('Origin',(0.,2.5406128344257E-15,13.7435492065112));
#419289=CARTESIAN_POINT('',(2.26132604140986,-1.56489761148824,12.5369868989719));
#419290=CARTESIAN_POINT('',(2.26132604140986,-1.56489761148824,14.));
#419291=CARTESIAN_POINT('Ctrl Pts',(2.24114714390868,-1.59366228522544,
12.4908873016278));
#419292=CARTESIAN_POINT('Ctrl Pts',(2.24241125224972,-1.591884585631,12.4908873016278));
#419293=CARTESIAN_POINT('Ctrl Pts',(2.24368032585042,-1.59009532968911,
12.4911020829134));
#419294=CARTESIAN_POINT('Ctrl Pts',(2.24491398940142,-1.5883517180366,12.4915448903141));
#419295=CARTESIAN_POINT('Ctrl Pts',(2.24702463740474,-1.58536861097313,
12.4923024798169));
#419296=CARTESIAN_POINT('Ctrl Pts',(2.24907989410123,-1.58245045206789,
12.4937722312795));
#419297=CARTESIAN_POINT('Ctrl Pts',(2.25087868084216,-1.57988770617733,
12.4958030942394));
#419298=CARTESIAN_POINT('Ctrl Pts',(2.25266477113929,-1.57734304901205,
12.4978196226833));
#419299=CARTESIAN_POINT('Ctrl Pts',(2.25425121104475,-1.57507355259229,
12.5004326847668));
#419300=CARTESIAN_POINT('Ctrl Pts',(2.25555806502204,-1.57319986502479,
12.5033504258767));
#419301=CARTESIAN_POINT('Ctrl Pts',(2.25711952468639,-1.57096113934383,
12.5068366111226));
#419302=CARTESIAN_POINT('Ctrl Pts',(2.25833231082659,-1.56921559274178,
12.5108395010833));
#419303=CARTESIAN_POINT('Ctrl Pts',(2.25921608346623,-1.56794218267368,
12.5149868989719));
#419304=CARTESIAN_POINT('Ctrl Pts',(2.26070046387404,-1.56580336905648,
12.5219528491417));
#419305=CARTESIAN_POINT('Ctrl Pts',(2.26132604143202,-1.56489761145674,
12.5295503425868));
#419306=CARTESIAN_POINT('Ctrl Pts',(2.26132604140986,-1.56489761148824,
12.5369868989719));
#419307=CARTESIAN_POINT('',(2.173418334073,-1.68485985919167,12.5369868989719));
#419308=CARTESIAN_POINT('Ctrl Pts',(2.17341833407299,-1.68485985919167,
12.5369868989719));
#419309=CARTESIAN_POINT('Ctrl Pts',(2.17341833407299,-1.68485985919166,
12.5309445149785));
#419310=CARTESIAN_POINT('Ctrl Pts',(2.17386213035091,-1.68428803439161,
12.5248274368704));
#419311=CARTESIAN_POINT('Ctrl Pts',(2.17487600145114,-1.68297783060618,
12.5190199595513));
#419312=CARTESIAN_POINT('Ctrl Pts',(2.17572758955986,-1.68187734163532,
12.5141420429941));
#419313=CARTESIAN_POINT('Ctrl Pts',(2.17700771602085,-1.68022193144484,
12.5093757677094));
#419314=CARTESIAN_POINT('Ctrl Pts',(2.17876921628551,-1.67793465372362,
12.5051960112707));
#419315=CARTESIAN_POINT('Ctrl Pts',(2.17994601990143,-1.67640659451924,
12.5024036458141));
#419316=CARTESIAN_POINT('Ctrl Pts',(2.18136606967986,-1.67455937066749,
12.4998248032393));
#419317=CARTESIAN_POINT('Ctrl Pts',(2.18297694553794,-1.67245677231128,
12.4976950015772));
#419318=CARTESIAN_POINT('Ctrl Pts',(2.18463320938228,-1.67029493121153,
12.495505190692));
#419319=CARTESIAN_POINT('Ctrl Pts',(2.18653374740496,-1.66780725369287,
12.4937456938368));
#419320=CARTESIAN_POINT('Ctrl Pts',(2.18852958262007,-1.66518415377903,
12.4925987732155));
#419321=CARTESIAN_POINT('Ctrl Pts',(2.19052495081744,-1.66256166766046,
12.4914521209692));
#419322=CARTESIAN_POINT('Ctrl Pts',(2.1926652189547,-1.65973835794374,12.4908873016276));
#419323=CARTESIAN_POINT('Ctrl Pts',(2.19476796912572,-1.6569530958056,12.4908873016278));
#419324=CARTESIAN_POINT('',(2.173418334073,-1.68485985919167,13.7435492065112));
#419325=CARTESIAN_POINT('',(2.173418334073,-1.68485985919167,14.));
#419326=CARTESIAN_POINT('',(2.12624798241642,-1.74400960928261,13.7435492065112));
#419327=CARTESIAN_POINT('Origin',(0.,2.5406128344257E-15,13.7435492065112));
#419328=CARTESIAN_POINT('',(2.12624798241642,-1.74400960928262,12.5369868989719));
#419329=CARTESIAN_POINT('',(2.12624798241642,-1.74400960928262,14.));
#419330=CARTESIAN_POINT('Ctrl Pts',(2.10379164058425,-1.77103380346278,
12.4908873016278));
#419331=CARTESIAN_POINT('Ctrl Pts',(2.10519644172938,-1.76936505558229,
12.4908873016278));
#419332=CARTESIAN_POINT('Ctrl Pts',(2.10660713356226,-1.76768519452191,
12.4911020829134));
#419333=CARTESIAN_POINT('Ctrl Pts',(2.10797881273614,-1.76604793962552,
12.4915448903141));
#419334=CARTESIAN_POINT('Ctrl Pts',(2.11032558865184,-1.76324679601128,
12.4923024798169));
#419335=CARTESIAN_POINT('Ctrl Pts',(2.11261186369286,-1.7605058695399,12.4937722312795));
#419336=CARTESIAN_POINT('Ctrl Pts',(2.11461355270075,-1.75809826879339,
12.4958030942394));
#419337=CARTESIAN_POINT('Ctrl Pts',(2.11660111311217,-1.75570766170538,
12.4978196226833));
#419338=CARTESIAN_POINT('Ctrl Pts',(2.11836725929691,-1.75357502642782,
12.5004326847668));
#419339=CARTESIAN_POINT('Ctrl Pts',(2.11982248775662,-1.75181409413252,
12.5033504258767));
#419340=CARTESIAN_POINT('Ctrl Pts',(2.12156122871905,-1.74971009108511,
12.5068366111226));
#419341=CARTESIAN_POINT('Ctrl Pts',(2.12291225766636,-1.74806920597476,
12.5108395010833));
#419342=CARTESIAN_POINT('Ctrl Pts',(2.12389688436776,-1.7468720687483,12.5149868989719));
#419343=CARTESIAN_POINT('Ctrl Pts',(2.12555065878779,-1.74486136264051,
12.5219528491417));
#419344=CARTESIAN_POINT('Ctrl Pts',(2.12624798244107,-1.74400960925302,
12.5295503425868));
#419345=CARTESIAN_POINT('Ctrl Pts',(2.12624798241642,-1.74400960928262,
12.5369868989719));
#419346=CARTESIAN_POINT('',(2.02885474386084,-1.8564073982597,12.5369868989719));
#419347=CARTESIAN_POINT('Ctrl Pts',(2.02885474386084,-1.8564073982597,12.5369868989719));
#419348=CARTESIAN_POINT('Ctrl Pts',(2.02885474386084,-1.8564073982597,12.5309445149785));
#419349=CARTESIAN_POINT('Ctrl Pts',(2.02934367247302,-1.85587364967614,
12.5248274368704));
#419350=CARTESIAN_POINT('Ctrl Pts',(2.03046096377265,-1.85465044539272,
12.5190199595513));
#419351=CARTESIAN_POINT('Ctrl Pts',(2.03139941835976,-1.85362303054475,
12.5141420429941));
#419352=CARTESIAN_POINT('Ctrl Pts',(2.03281021660416,-1.85207747078579,
12.5093757677094));
#419353=CARTESIAN_POINT('Ctrl Pts',(2.03475228999032,-1.84994138241705,
12.5051960112707));
#419354=CARTESIAN_POINT('Ctrl Pts',(2.03604972890026,-1.84851432812322,
12.5024036458141));
#419355=CARTESIAN_POINT('Ctrl Pts',(2.03761561947291,-1.8467889979965,12.4998248032393));
#419356=CARTESIAN_POINT('Ctrl Pts',(2.03939251656006,-1.84482469719994,
12.4976950015772));
#419357=CARTESIAN_POINT('Ctrl Pts',(2.04121947944228,-1.84280505032742,
12.495505190692));
#419358=CARTESIAN_POINT('Ctrl Pts',(2.04331646239371,-1.84048056184307,
12.4937456938368));
#419359=CARTESIAN_POINT('Ctrl Pts',(2.04551946362644,-1.83802886917627,
12.4925987732155));
#419360=CARTESIAN_POINT('Ctrl Pts',(2.04772194936537,-1.8355777501961,12.4914521209692));
#419361=CARTESIAN_POINT('Ctrl Pts',(2.0500852218892,-1.83293828653202,12.4908873016276));
#419362=CARTESIAN_POINT('Ctrl Pts',(2.05240800005387,-1.83033368578379,
12.4908873016278));
#419363=CARTESIAN_POINT('',(2.02885474386084,-1.8564073982597,13.7435492065112));
#419364=CARTESIAN_POINT('',(2.02885474386084,-1.8564073982597,14.));
#419365=CARTESIAN_POINT('',(1.97702009390622,-1.91151551086854,13.7435492065112));
#419366=CARTESIAN_POINT('Origin',(0.,2.5406128344257E-15,13.7435492065112));
#419367=CARTESIAN_POINT('',(1.97702009390622,-1.91151551086855,12.5369868989719));
#419368=CARTESIAN_POINT('',(1.97702009390622,-1.91151551086855,14.));
#419369=CARTESIAN_POINT('Ctrl Pts',(1.95243575099292,-1.93661938393808,
12.4908873016278));
#419370=CARTESIAN_POINT('Ctrl Pts',(1.95397189622228,-1.93507069301338,
12.4908873016278));
#419371=CARTESIAN_POINT('Ctrl Pts',(1.95551481836595,-1.9335114060327,12.4911020829134));
#419372=CARTESIAN_POINT('Ctrl Pts',(1.95701538486413,-1.93199140355362,
12.4915448903141));
#419373=CARTESIAN_POINT('Ctrl Pts',(1.95958267128567,-1.92939086453722,
12.4923024798169));
#419374=CARTESIAN_POINT('Ctrl Pts',(1.96208474988803,-1.92684541091315,
12.4937722312795));
#419375=CARTESIAN_POINT('Ctrl Pts',(1.9642760202528,-1.92460897749643,12.4958030942394));
#419376=CARTESIAN_POINT('Ctrl Pts',(1.9664518238919,-1.92238832958143,12.4978196226833));
#419377=CARTESIAN_POINT('Ctrl Pts',(1.96838592294445,-1.92040674778198,
12.5004326847668));
#419378=CARTESIAN_POINT('Ctrl Pts',(1.96997984158126,-1.91877028947278,
12.5033504258767));
#419379=CARTESIAN_POINT('Ctrl Pts',(1.97188429280756,-1.91681501085207,
12.5068366111226));
#419380=CARTESIAN_POINT('Ctrl Pts',(1.97336457368722,-1.9152897070531,12.5108395010833));
#419381=CARTESIAN_POINT('Ctrl Pts',(1.97444350192213,-1.91417680941899,
12.5149868989719));
#419382=CARTESIAN_POINT('Ctrl Pts',(1.97625566475848,-1.91230759173804,
12.5219528491417));
#419383=CARTESIAN_POINT('Ctrl Pts',(1.9770200939332,-1.91151551084106,12.5295503425868));
#419384=CARTESIAN_POINT('Ctrl Pts',(1.97702009390622,-1.91151551086855,
12.5369868989719));
#419385=CARTESIAN_POINT('',(1.87078946006577,-2.01560085237798,12.5369868989719));
#419386=CARTESIAN_POINT('Ctrl Pts',(1.87078946006576,-2.01560085237798,
12.5369868989719));
#419387=CARTESIAN_POINT('Ctrl Pts',(1.87078946006576,-2.01560085237798,
12.5309445149785));
#419388=CARTESIAN_POINT('Ctrl Pts',(1.87132026727296,-2.01510873201969,
12.5248274368704));
#419389=CARTESIAN_POINT('Ctrl Pts',(1.87253354338274,-2.01398066746096,
12.5190199595513));
#419390=CARTESIAN_POINT('Ctrl Pts',(1.87355261918778,-2.01303316401217,
12.5141420429941));
#419391=CARTESIAN_POINT('Ctrl Pts',(1.87508470058604,-2.01160774012995,
12.5093757677094));
#419392=CARTESIAN_POINT('Ctrl Pts',(1.87719442291575,-2.00963705642934,
12.5051960112707));
#419393=CARTESIAN_POINT('Ctrl Pts',(1.87860386287782,-2.00832050385694,
12.5024036458141));
#419394=CARTESIAN_POINT('Ctrl Pts',(1.88030517350127,-2.00672854924258,
12.4998248032393));
#419395=CARTESIAN_POINT('Ctrl Pts',(1.88223626686055,-2.00491561810338,
12.4976950015772));
#419396=CARTESIAN_POINT('Ctrl Pts',(1.88422177064409,-2.00305160587482,
12.495505190692));
#419397=CARTESIAN_POINT('Ctrl Pts',(1.88650124344871,-2.00090577551213,
12.4937456938368));
#419398=CARTESIAN_POINT('Ctrl Pts',(1.88889675008932,-1.99864180570256,
12.4925987732155));
#419399=CARTESIAN_POINT('Ctrl Pts',(1.89129169619061,-1.99637836565319,
12.4914521209692));
#419400=CARTESIAN_POINT('Ctrl Pts',(1.89386224591228,-1.99394031323696,
12.4908873016276));
#419401=CARTESIAN_POINT('Ctrl Pts',(1.89638959436514,-1.9915337070669,12.4908873016278));
#419402=CARTESIAN_POINT('',(1.87078946006577,-2.01560085237798,13.7435492065112));
#419403=CARTESIAN_POINT('',(1.87078946006577,-2.01560085237798,14.));
#419404=CARTESIAN_POINT('',(1.81463546285643,-2.0663005921075,13.7435492065112));
#419405=CARTESIAN_POINT('Origin',(0.,2.5406128344257E-15,13.7435492065112));
#419406=CARTESIAN_POINT('',(1.81463546285643,-2.0663005921075,12.5369868989719));
#419407=CARTESIAN_POINT('',(1.81463546285644,-2.06630059210751,14.));
#419408=CARTESIAN_POINT('Ctrl Pts',(1.78808672360795,-2.08931708193299,
12.4908873016278));
#419409=CARTESIAN_POINT('Ctrl Pts',(1.7897439901285,-2.08789875424664,12.4908873016278));
#419410=CARTESIAN_POINT('Ctrl Pts',(1.79140887469066,-2.08647041814326,
12.4911020829134));
#419411=CARTESIAN_POINT('Ctrl Pts',(1.79302834249066,-2.08507778344723,
12.4915448903141));
#419412=CARTESIAN_POINT('Ctrl Pts',(1.79579905455048,-2.08269515518675,
12.4923024798169));
#419413=CARTESIAN_POINT('Ctrl Pts',(1.7985002857939,-2.08036211398388,12.4937722312795));
#419414=CARTESIAN_POINT('Ctrl Pts',(1.80086655497279,-2.07831173099236,
12.4958030942394));
#419415=CARTESIAN_POINT('Ctrl Pts',(1.80321612222533,-2.07627582029587,
12.4978196226833));
#419416=CARTESIAN_POINT('Ctrl Pts',(1.8053053030356,-2.07445847907447,12.5004326847668));
#419417=CARTESIAN_POINT('Ctrl Pts',(1.80702730458398,-2.07295738511142,
12.5033504258767));
#419418=CARTESIAN_POINT('Ctrl Pts',(1.80908479226544,-2.07116384297402,
12.5068366111226));
#419419=CARTESIAN_POINT('Ctrl Pts',(1.81068447405243,-2.06976427113156,
12.5108395010833));
#419420=CARTESIAN_POINT('Ctrl Pts',(1.81185052373146,-2.06874301923995,
12.5149868989719));
#419421=CARTESIAN_POINT('Ctrl Pts',(1.81380901533943,-2.06702772932109,
12.5219528491417));
#419422=CARTESIAN_POINT('Ctrl Pts',(1.81463546288556,-2.06630059208231,
12.5295503425868));
#419423=CARTESIAN_POINT('Ctrl Pts',(1.81463546285643,-2.0663005921075,12.5369868989719));
#419424=CARTESIAN_POINT('',(1.70027438107248,-2.16138081537442,12.5369868989719));
#419425=CARTESIAN_POINT('Ctrl Pts',(1.70027438107248,-2.16138081537442,
12.5369868989719));
#419426=CARTESIAN_POINT('Ctrl Pts',(1.70027438107248,-2.16138081537442,
12.5309445149785));
#419427=CARTESIAN_POINT('Ctrl Pts',(1.70084353444031,-2.16093359822118,
12.5248274368704));
#419428=CARTESIAN_POINT('Ctrl Pts',(1.70214472120789,-2.15990818047066,
12.5190199595513));
#419429=CARTESIAN_POINT('Ctrl Pts',(1.70323763644954,-2.15904689390019,
12.5141420429941));
#419430=CARTESIAN_POINT('Ctrl Pts',(1.70488080525272,-2.15775109185545,
12.5093757677094));
#419431=CARTESIAN_POINT('Ctrl Pts',(1.70714413667196,-2.15595892739786,
12.5051960112707));
#419432=CARTESIAN_POINT('Ctrl Pts',(1.70865619809574,-2.15476163798706,
12.5024036458141));
#419433=CARTESIAN_POINT('Ctrl Pts',(1.7104816068285,-2.15331365308035,12.4998248032393));
#419434=CARTESIAN_POINT('Ctrl Pts',(1.71255404535221,-2.15166415635614,
12.4976950015772));
#419435=CARTESIAN_POINT('Ctrl Pts',(1.71468487683697,-2.14996818346538,
12.495505190692));
#419436=CARTESIAN_POINT('Ctrl Pts',(1.71713166997936,-2.14801529137137,
12.4937456938368));
#419437=CARTESIAN_POINT('Ctrl Pts',(1.71970374032639,-2.14595411076458,
12.4925987732155));
#419438=CARTESIAN_POINT('Ctrl Pts',(1.72227520881887,-2.14389341246611,
12.4914521209692));
#419439=CARTESIAN_POINT('Ctrl Pts',(1.7250359291541,-2.14167299613431,12.4908873016276));
#419440=CARTESIAN_POINT('Ctrl Pts',(1.72775102880817,-2.13948040010941,
12.4908873016278));
#419441=CARTESIAN_POINT('',(1.70027438107248,-2.16138081537442,13.7435492065112));
#419442=CARTESIAN_POINT('',(1.70027438107249,-2.16138081537442,14.));
#419443=CARTESIAN_POINT('',(1.64017473219511,-2.20733478382159,13.7435492065112));
#419444=CARTESIAN_POINT('Origin',(0.,2.5406128344257E-15,13.7435492065112));
#419445=CARTESIAN_POINT('',(1.64017473219511,-2.20733478382159,12.5369868989719));
#419446=CARTESIAN_POINT('',(1.64017473219511,-2.20733478382159,14.));
#419447=CARTESIAN_POINT('Ctrl Pts',(1.61183827409092,-2.22811071946068,
12.4908873016278));
#419448=CARTESIAN_POINT('Ctrl Pts',(1.61360563306738,-2.22683219374945,
12.4908873016278));
#419449=CARTESIAN_POINT('Ctrl Pts',(1.61538140051596,-2.22554431386447,
12.4911020829134));
#419450=CARTESIAN_POINT('Ctrl Pts',(1.61710899232677,-2.22428831470561,
12.4915448903141));
#419451=CARTESIAN_POINT('Ctrl Pts',(1.62006469139325,-2.22213945319902,
12.4923024798169));
#419452=CARTESIAN_POINT('Ctrl Pts',(1.62294709902947,-2.22003435042165,
12.4937722312795));
#419453=CARTESIAN_POINT('Ctrl Pts',(1.62547261989151,-2.21818366281583,
12.4958030942394));
#419454=CARTESIAN_POINT('Ctrl Pts',(1.62798031477508,-2.21634603798763,
12.4978196226833));
#419455=CARTESIAN_POINT('Ctrl Pts',(1.63021067418946,-2.21470503145028,
12.5004326847668));
#419456=CARTESIAN_POINT('Ctrl Pts',(1.63204929901321,-2.21334929136603,
12.5033504258767));
#419457=CARTESIAN_POINT('Ctrl Pts',(1.63424613090877,-2.21172942143895,
12.5068366111226));
#419458=CARTESIAN_POINT('Ctrl Pts',(1.63595456798473,-2.21046489547271,
12.5108395010833));
#419459=CARTESIAN_POINT('Ctrl Pts',(1.63719997923966,-2.20954208558644,
12.5149868989719));
#419460=CARTESIAN_POINT('Ctrl Pts',(1.63929176618073,-2.20799213840108,
12.5219528491417));
#419461=CARTESIAN_POINT('Ctrl Pts',(1.6401747322262,-2.20733478379885,12.5295503425868));
#419462=CARTESIAN_POINT('Ctrl Pts',(1.64017473219511,-2.20733478382159,
12.5369868989719));
#419463=CARTESIAN_POINT('',(1.51844425659869,-2.29277714564727,12.5369868989719));
#419464=CARTESIAN_POINT('Ctrl Pts',(1.51844425659869,-2.29277714564727,
12.5369868989719));
#419465=CARTESIAN_POINT('Ctrl Pts',(1.51844425659869,-2.29277714564727,
12.5309445149785));
#419466=CARTESIAN_POINT('Ctrl Pts',(1.51904796850539,-2.29237780785546,
12.5248274368704));
#419467=CARTESIAN_POINT('Ctrl Pts',(1.52042840674753,-2.2914618608991,12.5190199595513));
#419468=CARTESIAN_POINT('Ctrl Pts',(1.52158788825515,-2.29069252292696,
12.5141420429941));
#419469=CARTESIAN_POINT('Ctrl Pts',(1.52333120944598,-2.28953496606852,
12.5093757677094));
#419470=CARTESIAN_POINT('Ctrl Pts',(1.52573308785756,-2.28793324741274,
12.5051960112707));
#419471=CARTESIAN_POINT('Ctrl Pts',(1.52733770822377,-2.28686318892701,
12.5024036458141));
#419472=CARTESIAN_POINT('Ctrl Pts',(1.52927506727189,-2.28556880982862,
12.4998248032393));
#419473=CARTESIAN_POINT('Ctrl Pts',(1.53147505922358,-2.28409372464795,
12.4976950015772));
#419474=CARTESIAN_POINT('Ctrl Pts',(1.5337370380776,-2.28257707751476,12.495505190692));
#419475=CARTESIAN_POINT('Ctrl Pts',(1.53633486855308,-2.28083011986411,
12.4937456938368));
#419476=CARTESIAN_POINT('Ctrl Pts',(1.53906638590273,-2.27898544527698,
12.4925987732155));
#419477=CARTESIAN_POINT('Ctrl Pts',(1.54179726408785,-2.27714120233658,
12.4914521209692));
#419478=CARTESIAN_POINT('Ctrl Pts',(1.54472978289828,-2.27515319859355,
12.4908873016276));
#419479=CARTESIAN_POINT('Ctrl Pts',(1.54761456521333,-2.27318920407861,
12.4908873016278));
#419480=CARTESIAN_POINT('',(1.51844425659869,-2.29277714564727,13.7435492065112));
#419481=CARTESIAN_POINT('',(1.51844425659869,-2.29277714564727,14.));
#419482=CARTESIAN_POINT('',(1.45479890930081,-2.33367952673394,13.7435492065112));
#419483=CARTESIAN_POINT('Origin',(0.,2.5406128344257E-15,13.7435492065112));
#419484=CARTESIAN_POINT('',(1.45479890930082,-2.33367952673394,12.5369868989719));
#419485=CARTESIAN_POINT('',(1.45479890930082,-2.33367952673394,14.));
#419486=CARTESIAN_POINT('Ctrl Pts',(1.42486330679441,-2.35207664776276,
12.4908873016278));
#419487=CARTESIAN_POINT('Ctrl Pts',(1.42672899674439,-2.3509464324043,12.4908873016278));
#419488=CARTESIAN_POINT('Ctrl Pts',(1.42860382963999,-2.34980757936588,
12.4911020829134));
#419489=CARTESIAN_POINT('Ctrl Pts',(1.43042804862314,-2.34869657421136,
12.4915448903141));
#419490=CARTESIAN_POINT('Ctrl Pts',(1.43354906500665,-2.34679577977746,
12.4923024798169));
#419491=CARTESIAN_POINT('Ctrl Pts',(1.43659346708843,-2.34493262453724,
12.4937722312795));
#419492=CARTESIAN_POINT('Ctrl Pts',(1.43926143270895,-2.34329394833781,
12.4958030942394));
#419493=CARTESIAN_POINT('Ctrl Pts',(1.44191056692785,-2.34166683846795,
12.4978196226833));
#419494=CARTESIAN_POINT('Ctrl Pts',(1.44426726227242,-2.34021308724239,
12.5004326847668));
#419495=CARTESIAN_POINT('Ctrl Pts',(1.44621027462669,-2.33901172326352,
12.5033504258767));
#419496=CARTESIAN_POINT('Ctrl Pts',(1.44853183118254,-2.33757630551388,
12.5068366111226));
#419497=CARTESIAN_POINT('Ctrl Pts',(1.4503376541806,-2.33645524063552,12.5108395010833));
#419498=CARTESIAN_POINT('Ctrl Pts',(1.45165413900499,-2.33563701390213,
12.5149868989719));
#419499=CARTESIAN_POINT('Ctrl Pts',(1.45386530078219,-2.33426272409307,
12.5219528491417));
#419500=CARTESIAN_POINT('Ctrl Pts',(1.45479890933365,-2.33367952671381,
12.5295503425868));
#419501=CARTESIAN_POINT('Ctrl Pts',(1.45479890930082,-2.33367952673394,
12.5369868989719));
#419502=CARTESIAN_POINT('',(1.3265091361229,-2.40891542229745,12.5369868989719));
#419503=CARTESIAN_POINT('Ctrl Pts',(1.3265091361229,-2.40891542229744,12.5369868989719));
#419504=CARTESIAN_POINT('Ctrl Pts',(1.3265091361229,-2.40891542229744,12.5309445149785));
#419505=CARTESIAN_POINT('Ctrl Pts',(1.32714338896534,-2.40856662139417,
12.5248274368704));
#419506=CARTESIAN_POINT('Ctrl Pts',(1.32859389209328,-2.40776624070785,
12.5190199595513));
#419507=CARTESIAN_POINT('Ctrl Pts',(1.32981222370875,-2.40709397115132,
12.5141420429941));
#419508=CARTESIAN_POINT('Ctrl Pts',(1.33164409577233,-2.40608236282909,
12.5093757677094));
#419509=CARTESIAN_POINT('Ctrl Pts',(1.33416853707172,-2.4046817491485,12.5051960112707));
#419510=CARTESIAN_POINT('Ctrl Pts',(1.33585503789656,-2.40374604265052,
12.5024036458141));
#419511=CARTESIAN_POINT('Ctrl Pts',(1.33789145445521,-2.40261388323979,
12.4998248032393));
#419512=CARTESIAN_POINT('Ctrl Pts',(1.34020435925141,-2.40132302605116,
12.4976950015772));
#419513=CARTESIAN_POINT('Ctrl Pts',(1.34258243237862,-2.39999579771198,
12.495505190692));
#419514=CARTESIAN_POINT('Ctrl Pts',(1.34531401205399,-2.39846640021964,
12.4937456938368));
#419515=CARTESIAN_POINT('Ctrl Pts',(1.34818679860896,-2.39685050765718,
12.4925987732155));
#419516=CARTESIAN_POINT('Ctrl Pts',(1.35105891294296,-2.39523499320736,
12.4914521209692));
#419517=CARTESIAN_POINT('Ctrl Pts',(1.35414371479976,-2.39349263189001,
12.4908873016276));
#419518=CARTESIAN_POINT('Ctrl Pts',(1.35717898202543,-2.39177030894448,
12.4908873016278));
#419519=CARTESIAN_POINT('',(1.3265091361229,-2.40891542229744,13.7435492065112));
#419520=CARTESIAN_POINT('',(1.32650913612291,-2.40891542229744,14.));
#419521=CARTESIAN_POINT('',(1.25974163969005,-2.4444940174259,13.7435492065112));
#419522=CARTESIAN_POINT('Origin',(0.,2.5406128344257E-15,13.7435492065112));
#419523=CARTESIAN_POINT('',(1.25974163969005,-2.4444940174259,12.5369868989719));
#419524=CARTESIAN_POINT('',(1.25974163969005,-2.44449401742591,14.));
#419525=CARTESIAN_POINT('Ctrl Pts',(1.22840610927708,-2.46038989403931,
12.4908873016278));
#419526=CARTESIAN_POINT('Ctrl Pts',(1.23035771434178,-2.45941551043036,
12.4908873016278));
#419527=CARTESIAN_POINT('Ctrl Pts',(1.23231913598081,-2.45843326311756,
12.4911020829134));
#419528=CARTESIAN_POINT('Ctrl Pts',(1.23422784225995,-2.4574746455234,12.4915448903141));
#419529=CARTESIAN_POINT('Ctrl Pts',(1.23749340611138,-2.45583456763553,
12.4923024798169));
#419530=CARTESIAN_POINT('Ctrl Pts',(1.24067954264514,-2.45422575892319,
12.4937722312795));
#419531=CARTESIAN_POINT('Ctrl Pts',(1.24347219815314,-2.45280999924988,
12.4958030942394));
#419532=CARTESIAN_POINT('Ctrl Pts',(1.2462451421562,-2.45140423248609,12.4978196226833));
#419533=CARTESIAN_POINT('Ctrl Pts',(1.24871249001229,-2.45014741104688,
12.5004326847668));
#419534=CARTESIAN_POINT('Ctrl Pts',(1.25074695947043,-2.44910841805247,
12.5033504258767));
#419535=CARTESIAN_POINT('Ctrl Pts',(1.25317779111071,-2.44786700494856,
12.5068366111226));
#419536=CARTESIAN_POINT('Ctrl Pts',(1.25506898257676,-2.44689686165989,
12.5108395010833));
#419537=CARTESIAN_POINT('Ctrl Pts',(1.25644777998133,-2.44618866324329,
12.5149868989719));
#419538=CARTESIAN_POINT('Ctrl Pts',(1.25876360167784,-2.44499917648246,
12.5219528491417));
#419539=CARTESIAN_POINT('Ctrl Pts',(1.25974163972441,-2.44449401740852,
12.5295503425868));
#419540=CARTESIAN_POINT('Ctrl Pts',(1.25974163969005,-2.4444940174259,12.5369868989719));
#419541=CARTESIAN_POINT('',(1.12574631620482,-2.5090227642553,12.5369868989719));
#419542=CARTESIAN_POINT('Ctrl Pts',(1.12574631620482,-2.50902276425529,
12.5369868989719));
#419543=CARTESIAN_POINT('Ctrl Pts',(1.12574631620482,-2.50902276425529,
12.5309445149785));
#419544=CARTESIAN_POINT('Ctrl Pts',(1.12640688913497,-2.50872682145303,
12.5248274368704));
#419545=CARTESIAN_POINT('Ctrl Pts',(1.12791780428972,-2.50804733343815,
12.5190199595513));
#419546=CARTESIAN_POINT('Ctrl Pts',(1.12918687821715,-2.50747660614022,
12.5141420429941));
#419547=CARTESIAN_POINT('Ctrl Pts',(1.13109511034713,-2.50661767844068,
12.5093757677094));
#419548=CARTESIAN_POINT('Ctrl Pts',(1.13372531479398,-2.50542749058824,
12.5051960112707));
#419549=CARTESIAN_POINT('Ctrl Pts',(1.13548247269271,-2.50463236305038,
12.5024036458141));
#419550=CARTESIAN_POINT('Ctrl Pts',(1.13760439474569,-2.50366995766138,
12.4998248032393));
#419551=CARTESIAN_POINT('Ctrl Pts',(1.14001482038658,-2.50257191890641,
12.4976950015772));
#419552=CARTESIAN_POINT('Ctrl Pts',(1.14249316210267,-2.50144294184686,
12.495505190692));
#419553=CARTESIAN_POINT('Ctrl Pts',(1.14534031276587,-2.5001412824008,12.4937456938368));
#419554=CARTESIAN_POINT('Ctrl Pts',(1.14833525060562,-2.49876492536143,
12.4925987732155));
#419555=CARTESIAN_POINT('Ctrl Pts',(1.15132948764148,-2.49738889038429,
12.4914521209692));
#419556=CARTESIAN_POINT('Ctrl Pts',(1.15454604369723,-2.49590376661972,
12.4908873016276));
#419557=CARTESIAN_POINT('Ctrl Pts',(1.15771159663093,-2.49443457701866,
12.4908873016278));
#419558=CARTESIAN_POINT('',(1.12574631620482,-2.50902276425529,13.7435492065112));
#419559=CARTESIAN_POINT('',(1.12574631620482,-2.5090227642553,14.));
#419560=CARTESIAN_POINT('',(1.05630099730988,-2.53904080374502,13.7435492065112));
#419561=CARTESIAN_POINT('Origin',(0.,2.5406128344257E-15,13.7435492065112));
#419562=CARTESIAN_POINT('',(1.05630099730988,-2.53904080374502,12.5369868989719));
#419563=CARTESIAN_POINT('',(1.05630099730988,-2.53904080374502,14.));
#419564=CARTESIAN_POINT('Ctrl Pts',(1.02377407177525,-2.55232965150678,
12.4908873016278));
#419565=CARTESIAN_POINT('Ctrl Pts',(1.02579860434496,-2.5515175840095,12.4908873016278));
#419566=CARTESIAN_POINT('Ctrl Pts',(1.02783356179003,-2.55069847911614,
12.4911020829134));
#419567=CARTESIAN_POINT('Ctrl Pts',(1.02981405323977,-2.54989862852426,
12.4915448903141));
#419568=CARTESIAN_POINT('Ctrl Pts',(1.03320243277048,-2.54853018163017,
12.4923024798169));
#419569=CARTESIAN_POINT('Ctrl Pts',(1.03650910054327,-2.54718642580225,
12.4937722312795));
#419570=CARTESIAN_POINT('Ctrl Pts',(1.03940786127709,-2.54600300430212,
12.4958030942394));
#419571=CARTESIAN_POINT('Ctrl Pts',(1.04228616157949,-2.54482793579027,
12.4978196226833));
#419572=CARTESIAN_POINT('Ctrl Pts',(1.04484774215418,-2.54377640807673,
12.5004326847668));
#419573=CARTESIAN_POINT('Ctrl Pts',(1.04696012965761,-2.54290670039373,
12.5033504258767));
#419574=CARTESIAN_POINT('Ctrl Pts',(1.04948405959883,-2.54186755333494,
12.5068366111226));
#419575=CARTESIAN_POINT('Ctrl Pts',(1.05144803396569,-2.54105478777947,
12.5108395010833));
#419576=CARTESIAN_POINT('Ctrl Pts',(1.05287996828117,-2.54046133062329,
12.5149868989719));
#419577=CARTESIAN_POINT('Ctrl Pts',(1.0552850384857,-2.53946456274884,12.5219528491417));
#419578=CARTESIAN_POINT('Ctrl Pts',(1.05630099734555,-2.53904080373049,
12.5295503425868));
#419579=CARTESIAN_POINT('Ctrl Pts',(1.05630099730988,-2.53904080374502,
12.5369868989719));
#419580=CARTESIAN_POINT('',(0.91749184028746,-2.59243297367665,12.5369868989719));
#419581=CARTESIAN_POINT('Ctrl Pts',(0.917491840287459,-2.59243297367664,
12.5369868989719));
#419582=CARTESIAN_POINT('Ctrl Pts',(0.91749184028746,-2.59243297367664,
12.5309445149785));
#419583=CARTESIAN_POINT('Ctrl Pts',(0.918174337301462,-2.59219185842591,
12.5248274368704));
#419584=CARTESIAN_POINT('Ctrl Pts',(0.919735609591948,-2.59163778496311,
12.5190199595513));
#419585=CARTESIAN_POINT('Ctrl Pts',(0.921046980353731,-2.59117239801977,
12.5141420429941));
#419586=CARTESIAN_POINT('Ctrl Pts',(0.923018873580121,-2.59047186696506,
12.5093757677094));
#419587=CARTESIAN_POINT('Ctrl Pts',(0.925737337597789,-2.58950002544455,
12.5051960112707));
#419588=CARTESIAN_POINT('Ctrl Pts',(0.927553458974509,-2.58885076830938,
12.5024036458141));
#419589=CARTESIAN_POINT('Ctrl Pts',(0.929746765480642,-2.58806452159121,
12.4998248032393));
#419590=CARTESIAN_POINT('Ctrl Pts',(0.932238670981287,-2.58716660853665,
12.4976950015772));
#419591=CARTESIAN_POINT('Ctrl Pts',(0.934800788331022,-2.58624339591279,
12.495505190692));
#419592=CARTESIAN_POINT('Ctrl Pts',(0.937744562664136,-2.58517813684187,
12.4937456938368));
#419593=CARTESIAN_POINT('Ctrl Pts',(0.940841720971482,-2.58405047475459,
12.4925987732155));
#419594=CARTESIAN_POINT('Ctrl Pts',(0.943938154555725,-2.58292307653588,
12.4914521209692));
#419595=CARTESIAN_POINT('Ctrl Pts',(0.947265059160576,-2.58170507357772,
12.4908873016276));
#419596=CARTESIAN_POINT('Ctrl Pts',(0.950539831569806,-2.58049879453551,
12.4908873016278));
#419597=CARTESIAN_POINT('',(0.917491840287462,-2.59243297367664,13.7435492065112));
#419598=CARTESIAN_POINT('',(0.917491840287462,-2.59243297367665,14.));
#419599=CARTESIAN_POINT('',(0.845830846070012,-2.61669069242746,13.7435492065112));
#419600=CARTESIAN_POINT('Origin',(0.,2.5406128344257E-15,13.7435492065112));
#419601=CARTESIAN_POINT('',(0.845830846070013,-2.61669069242746,12.5369868989719));
#419602=CARTESIAN_POINT('',(0.845830846070013,-2.61669069242746,14.));
#419603=CARTESIAN_POINT('Ctrl Pts',(0.812328986736591,-2.62728407624823,
12.4908873016278));
#419604=CARTESIAN_POINT('Ctrl Pts',(0.814412973881085,-2.62663972903783,
12.4908873016278));
#419605=CARTESIAN_POINT('Ctrl Pts',(0.81650792482613,-2.62598921757183,
12.4911020829134));
#419606=CARTESIAN_POINT('Ctrl Pts',(0.818547021602644,-2.62535345685594,
12.4915448903141));
#419607=CARTESIAN_POINT('Ctrl Pts',(0.822035667705896,-2.62426574774394,
12.4923024798169));
#419608=CARTESIAN_POINT('Ctrl Pts',(0.825440861389251,-2.62319598727377,
12.4937722312795));
#419609=CARTESIAN_POINT('Ctrl Pts',(0.828426436574467,-2.62225277942165,
12.4958030942394));
#419610=CARTESIAN_POINT('Ctrl Pts',(0.83139093856257,-2.62131622904882,
12.4978196226833));
#419611=CARTESIAN_POINT('Ctrl Pts',(0.834029704959774,-2.62047699280439,
12.5004326847668));
#419612=CARTESIAN_POINT('Ctrl Pts',(0.83620595291819,-2.61978235819394,
12.5033504258767));
#419613=CARTESIAN_POINT('Ctrl Pts',(0.838806184822998,-2.61895239253249,
12.5068366111226));
#419614=CARTESIAN_POINT('Ctrl Pts',(0.840829872165285,-2.61830241353091,
12.5108395010833));
#419615=CARTESIAN_POINT('Ctrl Pts',(0.842305414105079,-2.6178276469946,
12.5149868989719));
#419616=CARTESIAN_POINT('Ctrl Pts',(0.844783727472212,-2.61703023133227,
12.5219528491417));
#419617=CARTESIAN_POINT('Ctrl Pts',(0.845830846106748,-2.61669069241589,
12.5295503425868));
#419618=CARTESIAN_POINT('Ctrl Pts',(0.845830846070013,-2.61669069242746,
12.5369868989719));
#419619=CARTESIAN_POINT('',(0.703131607548487,-2.65859096937951,12.5369868989719));
#419620=CARTESIAN_POINT('Ctrl Pts',(0.703131607548485,-2.65859096937951,
12.5369868989719));
#419621=CARTESIAN_POINT('Ctrl Pts',(0.703131607548487,-2.65859096937951,
12.5309445149785));
#419622=CARTESIAN_POINT('Ctrl Pts',(0.703831486741316,-2.65840628626251,
12.5248274368704));
#419623=CARTESIAN_POINT('Ctrl Pts',(0.705432726158037,-2.65798131461928,
12.5190199595513));
#419624=CARTESIAN_POINT('Ctrl Pts',(0.706777666798115,-2.65762436510386,
12.5141420429941));
#419625=CARTESIAN_POINT('Ctrl Pts',(0.708800098496836,-2.65708689261255,
12.5093757677094));
#419626=CARTESIAN_POINT('Ctrl Pts',(0.7115887311558,-2.65633986486896,12.5051960112707));
#419627=CARTESIAN_POINT('Ctrl Pts',(0.713451730022383,-2.6558407988356,
12.5024036458141));
#419628=CARTESIAN_POINT('Ctrl Pts',(0.715701824888742,-2.65523594313044,
12.4998248032393));
#419629=CARTESIAN_POINT('Ctrl Pts',(0.718258627029167,-2.65454413123952,
12.4976950015772));
#419630=CARTESIAN_POINT('Ctrl Pts',(0.720887469544312,-2.65383282687905,
12.495505190692));
#419631=CARTESIAN_POINT('Ctrl Pts',(0.723908277214839,-2.65301105730662,
12.4937456938368));
#419632=CARTESIAN_POINT('Ctrl Pts',(0.727087044912233,-2.65213959457657,
12.4925987732155));
#419633=CARTESIAN_POINT('Ctrl Pts',(0.730265068790241,-2.65126833576544,
12.4914521209692));
#419634=CARTESIAN_POINT('Ctrl Pts',(0.733680181942947,-2.65032555922241,
12.4908873016276));
#419635=CARTESIAN_POINT('Ctrl Pts',(0.737042380757624,-2.64939021832706,
12.4908873016278));
#419636=CARTESIAN_POINT('',(0.703131607548488,-2.65859096937951,13.7435492065112));
#419637=CARTESIAN_POINT('',(0.703131607548488,-2.65859096937951,14.));
#419638=CARTESIAN_POINT('',(0.629731830101817,-2.67692693627537,13.7435492065112));
#419639=CARTESIAN_POINT('Origin',(0.,2.5406128344257E-15,13.7435492065112));
#419640=CARTESIAN_POINT('',(0.629731830101817,-2.67692693627537,12.5369868989719));
#419641=CARTESIAN_POINT('',(0.629731830101817,-2.67692693627537,14.));
#419642=CARTESIAN_POINT('Ctrl Pts',(0.595477986316048,-2.6847543589336,
12.4908873016278));
#419643=CARTESIAN_POINT('Ctrl Pts',(0.597607559444711,-2.68428202003446,
12.4908873016278));
#419644=CARTESIAN_POINT('Ctrl Pts',(0.599748562336841,-2.6838044310423,
12.4911020829134));
#419645=CARTESIAN_POINT('Ctrl Pts',(0.601832694587503,-2.68333699108509,
12.4915448903141));
#419646=CARTESIAN_POINT('Ctrl Pts',(0.605398390899067,-2.68253725827985,
12.4923024798169));
#419647=CARTESIAN_POINT('Ctrl Pts',(0.60887944949084,-2.68174861224686,
12.4937722312795));
#419648=CARTESIAN_POINT('Ctrl Pts',(0.611931970617183,-2.68105189493538,
12.4958030942394));
#419649=CARTESIAN_POINT('Ctrl Pts',(0.614962946019369,-2.68036009528978,
12.4978196226833));
#419650=CARTESIAN_POINT('Ctrl Pts',(0.61766133768408,-2.67973873549321,
12.5004326847668));
#419651=CARTESIAN_POINT('Ctrl Pts',(0.619886963526366,-2.67922379663403,
12.5033504258767));
#419652=CARTESIAN_POINT('Ctrl Pts',(0.622546193280448,-2.67860853565447,
12.5068366111226));
#419653=CARTESIAN_POINT('Ctrl Pts',(0.624616126292785,-2.67812566870979,
12.5108395010833));
#419654=CARTESIAN_POINT('Ctrl Pts',(0.626125456368726,-2.67777275228632,
12.5149868989719));
#419655=CARTESIAN_POINT('Ctrl Pts',(0.628660520131902,-2.67717999550579,
12.5219528491417));
#419656=CARTESIAN_POINT('Ctrl Pts',(0.629731830139373,-2.67692693626683,
12.5295503425868));
#419657=CARTESIAN_POINT('Ctrl Pts',(0.629731830101817,-2.67692693627537,
12.5369868989719));
#419658=CARTESIAN_POINT('',(0.484092149969828,-2.70705648081779,12.5369868989719));
#419659=CARTESIAN_POINT('Ctrl Pts',(0.484092149969827,-2.70705648081778,
12.5369868989719));
#419660=CARTESIAN_POINT('Ctrl Pts',(0.484092149969828,-2.70705648081778,
12.5309445149785));
#419661=CARTESIAN_POINT('Ctrl Pts',(0.484804753760929,-2.70692945887021,
12.5248274368704));
#419662=CARTESIAN_POINT('Ctrl Pts',(0.486435304319751,-2.7066364171627,
12.5190199595513));
#419663=CARTESIAN_POINT('Ctrl Pts',(0.487804864480063,-2.70639028051533,
12.5141420429941));
#419664=CARTESIAN_POINT('Ctrl Pts',(0.489864375701838,-2.70601944337819,
12.5093757677094));
#419665=CARTESIAN_POINT('Ctrl Pts',(0.492704619111845,-2.7055022007579,
12.5051960112707));
#419666=CARTESIAN_POINT('Ctrl Pts',(0.494602097518208,-2.70515664702846,
12.5024036458141));
#419667=CARTESIAN_POINT('Ctrl Pts',(0.496894006734697,-2.70473720755122,
12.4998248032393));
#419668=CARTESIAN_POINT('Ctrl Pts',(0.499498690418499,-2.70425610071794,
12.4976950015772));
#419669=CARTESIAN_POINT('Ctrl Pts',(0.502176763585845,-2.70376143823402,
12.495505190692));
#419670=CARTESIAN_POINT('Ctrl Pts',(0.505254501617137,-2.70318862690101,
12.4937456938368));
#419671=CARTESIAN_POINT('Ctrl Pts',(0.508493724530012,-2.70257916296888,
12.4925987732155));
#419672=CARTESIAN_POINT('Ctrl Pts',(0.511732189477214,-2.70196984164896,
12.4914521209692));
#419673=CARTESIAN_POINT('Ctrl Pts',(0.515212784163198,-2.70130856554342,
12.4908873016276));
#419674=CARTESIAN_POINT('Ctrl Pts',(0.518640034504933,-2.70065038733426,
12.4908873016278));
#419675=CARTESIAN_POINT('',(0.484092149969829,-2.70705648081779,13.7435492065112));
#419676=CARTESIAN_POINT('',(0.484092149969829,-2.70705648081779,14.));
#419677=CARTESIAN_POINT('',(0.409442052702732,-2.71934867302422,13.7435492065112));
#419678=CARTESIAN_POINT('Origin',(0.,2.5406128344257E-15,13.7435492065112));
#419679=CARTESIAN_POINT('',(0.409442052702732,-2.71934867302422,12.5369868989719));
#419680=CARTESIAN_POINT('',(0.409442052702732,-2.71934867302422,14.));
#419681=CARTESIAN_POINT('Ctrl Pts',(0.374664178143524,-2.72435804431357,
12.4908873016278));
#419682=CARTESIAN_POINT('Ctrl Pts',(0.376825165298539,-2.72406085706312,
12.4908873016278));
#419683=CARTESIAN_POINT('Ctrl Pts',(0.378997972116748,-2.72375936882074,
12.4911020829134));
#419684=CARTESIAN_POINT('Ctrl Pts',(0.381113270285288,-2.723463360358,12.4915448903141));
#419685=CARTESIAN_POINT('Ctrl Pts',(0.384732287684508,-2.7229569259494,
12.4923024798169));
#419686=CARTESIAN_POINT('Ctrl Pts',(0.388266045314105,-2.72245464266283,
12.4937722312795));
#419687=CARTESIAN_POINT('Ctrl Pts',(0.391365198357109,-2.72200905243074,
12.4958030942394));
#419688=CARTESIAN_POINT('Ctrl Pts',(0.394442476532154,-2.72156660732487,
12.4978196226833));
#419689=CARTESIAN_POINT('Ctrl Pts',(0.397182536113045,-2.72116725902309,
12.5004326847668));
#419690=CARTESIAN_POINT('Ctrl Pts',(0.399442728666425,-2.72083544274834,
12.5033504258767));
#419691=CARTESIAN_POINT('Ctrl Pts',(0.402143259534509,-2.72043898091097,
12.5068366111226));
#419692=CARTESIAN_POINT('Ctrl Pts',(0.404245663154215,-2.72012643942305,
12.5108395010833));
#419693=CARTESIAN_POINT('Ctrl Pts',(0.405778737023668,-2.71989772171299,
12.5149868989719));
#419694=CARTESIAN_POINT('Ctrl Pts',(0.408353680751798,-2.71951356851282,
12.5219528491417));
#419695=CARTESIAN_POINT('Ctrl Pts',(0.409442052740859,-2.71934867301877,
12.5295503425868));
#419696=CARTESIAN_POINT('Ctrl Pts',(0.409442052702732,-2.71934867302422,
12.5369868989719));
#419697=CARTESIAN_POINT('',(0.261831139002702,-2.73750697800911,12.5369868989719));
#419698=CARTESIAN_POINT('Ctrl Pts',(0.261831139002701,-2.7375069780091,
12.5369868989719));
#419699=CARTESIAN_POINT('Ctrl Pts',(0.261831139002703,-2.7375069780091,
12.5309445149785));
#419700=CARTESIAN_POINT('Ctrl Pts',(0.262551725131416,-2.73743846254104,
12.5248274368704));
#419701=CARTESIAN_POINT('Ctrl Pts',(0.264200735787393,-2.73727930091348,
12.5190199595513));
#419702=CARTESIAN_POINT('Ctrl Pts',(0.265585801271034,-2.73714561513294,
12.5141420429941));
#419703=CARTESIAN_POINT('Ctrl Pts',(0.267668686308478,-2.73694388120992,
12.5093757677094));
#419704=CARTESIAN_POINT('Ctrl Pts',(0.270541639118242,-2.73665986587723,
12.5051960112707));
#419705=CARTESIAN_POINT('Ctrl Pts',(0.272460969658652,-2.73647012405477,
12.5024036458141));
#419706=CARTESIAN_POINT('Ctrl Pts',(0.274779440947572,-2.73623889210599,
12.4998248032393));
#419707=CARTESIAN_POINT('Ctrl Pts',(0.277414672434579,-2.73597169201693,
12.4976950015772));
#419708=CARTESIAN_POINT('Ctrl Pts',(0.280124154119048,-2.73569696330678,
12.495505190692));
#419709=CARTESIAN_POINT('Ctrl Pts',(0.283238340672297,-2.7353769221781,
12.4937456938368));
#419710=CARTESIAN_POINT('Ctrl Pts',(0.286516462306602,-2.73503351292581,
12.4925987732155));
#419711=CARTESIAN_POINT('Ctrl Pts',(0.289793816873083,-2.73469018402996,
12.4914521209692));
#419712=CARTESIAN_POINT('Ctrl Pts',(0.293316730308969,-2.73431480904527,
12.4908873016276));
#419713=CARTESIAN_POINT('Ctrl Pts',(0.296786224392195,-2.7339381735897,
12.4908873016278));
#419714=CARTESIAN_POINT('',(0.261831139002703,-2.73750697800911,13.7435492065112));
#419715=CARTESIAN_POINT('',(0.261831139002704,-2.73750697800911,14.));
#419716=CARTESIAN_POINT('',(0.186427505996095,-2.74367359301504,13.7435492065112));
#419717=CARTESIAN_POINT('Origin',(0.,2.5406128344257E-15,13.7435492065112));
#419718=CARTESIAN_POINT('',(0.186427505996095,-2.74367359301505,12.5369868989719));
#419719=CARTESIAN_POINT('',(0.186427505996095,-2.74367359301505,14.));
#419720=CARTESIAN_POINT('Ctrl Pts',(0.151357041680694,-2.74583157639606,
12.4908873016278));
#419721=CARTESIAN_POINT('Ctrl Pts',(0.153535061849082,-2.74571151852644,
12.4908873016278));
#419722=CARTESIAN_POINT('Ctrl Pts',(0.155725212922482,-2.74558813738835,
12.4911020829134));
#419723=CARTESIAN_POINT('Ctrl Pts',(0.157857600048588,-2.74546553030755,
12.4915448903141));
#419724=CARTESIAN_POINT('Ctrl Pts',(0.161505854571769,-2.74525576453302,
12.4923024798169));
#419725=CARTESIAN_POINT('Ctrl Pts',(0.165068794665194,-2.74504318660527,
12.4937722312795));
#419726=CARTESIAN_POINT('Ctrl Pts',(0.168193955272682,-2.74485168878206,
12.4958030942394));
#419727=CARTESIAN_POINT('Ctrl Pts',(0.171297057442045,-2.74466154261511,
12.4978196226833));
#419728=CARTESIAN_POINT('Ctrl Pts',(0.174060550294684,-2.74448686340517,
12.5004326847668));
#419729=CARTESIAN_POINT('Ctrl Pts',(0.176340268350619,-2.7443403778974,
12.5033504258767));
#419730=CARTESIAN_POINT('Ctrl Pts',(0.179064128745335,-2.74416535359035,
12.5068366111226));
#419731=CARTESIAN_POINT('Ctrl Pts',(0.181185011823192,-2.74402521747121,
12.5108395010833));
#419732=CARTESIAN_POINT('Ctrl Pts',(0.182731627132496,-2.74392222055319,
12.5149868989719));
#419733=CARTESIAN_POINT('Ctrl Pts',(0.185329314999907,-2.74374922740956,
12.5219528491417));
#419734=CARTESIAN_POINT('Ctrl Pts',(0.186427506034539,-2.74367359301272,
12.5295503425868));
#419735=CARTESIAN_POINT('Ctrl Pts',(0.186427505996095,-2.74367359301505,
12.5369868989719));
#419736=CARTESIAN_POINT('',(0.0378276850046104,-2.74973981791863,12.5369868989719));
#419737=CARTESIAN_POINT('Ctrl Pts',(0.0378276850046103,-2.74973981791863,
12.5369868989719));
#419738=CARTESIAN_POINT('Ctrl Pts',(0.037827685004612,-2.74973981791863,
12.5309445149785));
#419739=CARTESIAN_POINT('Ctrl Pts',(0.0385514580891393,-2.74973026488922,
12.5248274368704));
#419740=CARTESIAN_POINT('Ctrl Pts',(0.0402079549484237,-2.74970604253597,
12.5190199595513));
#419741=CARTESIAN_POINT('Ctrl Pts',(0.0415993083731197,-2.74968569727908,
12.5141420429941));
#419742=CARTESIAN_POINT('Ctrl Pts',(0.0436917059699596,-2.74965440907616,
12.5093757677094));
#419743=CARTESIAN_POINT('Ctrl Pts',(0.0465782491525343,-2.74960551110625,
12.5051960112707));
#419744=CARTESIAN_POINT('Ctrl Pts',(0.0485066589989134,-2.74957284389129,
12.5024036458141));
#419745=CARTESIAN_POINT('Ctrl Pts',(0.0508362633163583,-2.74953135828142,
12.4998248032393));
#419746=CARTESIAN_POINT('Ctrl Pts',(0.0534845055758057,-2.74947984310911,
12.4976950015772));
#419747=CARTESIAN_POINT('Ctrl Pts',(0.0562073646238211,-2.74942687644696,
12.495505190692));
#419748=CARTESIAN_POINT('Ctrl Pts',(0.0593372753013208,-2.74936173534353,
12.4937456938368));
#419749=CARTESIAN_POINT('Ctrl Pts',(0.0626324802984313,-2.74928666610298,
12.4925987732155));
#419750=CARTESIAN_POINT('Ctrl Pts',(0.0659269142302771,-2.74921161442835,
12.4914521209692));
#419751=CARTESIAN_POINT('Ctrl Pts',(0.0694687020083875,-2.74912463862312,
12.4908873016276));
#419752=CARTESIAN_POINT('Ctrl Pts',(0.0729573509224067,-2.74903205236795,
12.4908873016278));
#419753=CARTESIAN_POINT('',(0.0378276850046121,-2.74973981791863,14.));
#419754=CARTESIAN_POINT('Origin',(0.,2.60208521396521E-15,13.7435492065112));
#419755=CARTESIAN_POINT('Origin',(0.0629611349460807,-2.65846395524141,
13.7420545896477));
#419756=CARTESIAN_POINT('Origin',(-0.0636035367449967,-2.65612979764794,
13.7415084174026));
#419757=CARTESIAN_POINT('Origin',(0.,2.60208521396521E-15,13.7435492065112));
#419758=CARTESIAN_POINT('Origin',(2.18006130902264,1.51868482600949,13.7415084174033));
#419759=CARTESIAN_POINT('Origin',(2.10713407931711,1.62215309930852,13.7420545896465));
#419760=CARTESIAN_POINT('Origin',(0.,2.60208521396521E-15,13.7435492065112));
#419761=CARTESIAN_POINT('Origin',(2.23234330142418,1.44500452954644,13.742054589647));
#419762=CARTESIAN_POINT('Origin',(2.29659424696376,1.33593629214936,13.7415084174048));
#419763=CARTESIAN_POINT('Origin',(0.,2.60208521396521E-15,13.7435492065112));
#419764=CARTESIAN_POINT('Origin',(2.3426966471724,1.25823969304925,13.7420545896481));
#419765=CARTESIAN_POINT('Origin',(2.39784372909656,1.1442973226725,13.7415084174029));
#419766=CARTESIAN_POINT('Origin',(0.,2.60208521396521E-15,13.7435492065112));
#419767=CARTESIAN_POINT('Origin',(2.43745973325144,1.06310147898929,13.7420545896491));
#419768=CARTESIAN_POINT('Origin',(2.48313595683433,0.945043243314494,13.741508417404));
#419769=CARTESIAN_POINT('Origin',(0.,2.60208521396521E-15,13.7435492065112));
#419770=CARTESIAN_POINT('Origin',(2.51600192695173,0.860888499985368,13.7420545896476));
#419771=CARTESIAN_POINT('Origin',(2.55190332446211,0.739500057089027,13.7415084174023));
#419772=CARTESIAN_POINT('Origin',(0.,2.60208521396521E-15,13.7435492065112));
#419773=CARTESIAN_POINT('Origin',(2.57780054294477,0.652946450051028,13.7420545896483));
#419774=CARTESIAN_POINT('Origin',(2.60368819650721,0.529035619997232,13.7415084174039));
#419775=CARTESIAN_POINT('Origin',(0.,2.60208521396521E-15,13.7435492065112));
#419776=CARTESIAN_POINT('Origin',(2.62244432163127,0.44065914921995,13.7420545896489));
#419777=CARTESIAN_POINT('Origin',(2.63814595317993,0.315050538137071,13.7415084174041));
#419778=CARTESIAN_POINT('Origin',(0.,2.60208521396521E-15,13.7435492065112));
#419779=CARTESIAN_POINT('Origin',(2.64963616603145,0.225439334453963,13.7420545896499));
#419780=CARTESIAN_POINT('Origin',(2.65504728379398,0.0989688469239032,13.7415084174028));
#419781=CARTESIAN_POINT('Origin',(0.,2.60208521396521E-15,13.7435492065112));
#419782=CARTESIAN_POINT('Origin',(2.65919511889896,0.00871925811366688,
13.7420545896483));
#419783=CARTESIAN_POINT('Origin',(2.65427971278744,-0.117771465635996,13.7415084174022));
#419784=CARTESIAN_POINT('Origin',(0.,2.60208521396521E-15,13.7435492065112));
#419785=CARTESIAN_POINT('Origin',(2.65105756699552,-0.208058843453515,13.7420545896502));
#419786=CARTESIAN_POINT('Origin',(2.63584834821942,-0.333728028522382,13.7415084174022));
#419787=CARTESIAN_POINT('Origin',(0.,2.60208521396521E-15,13.7435492065112));
#419788=CARTESIAN_POINT('Origin',(2.62527766436935,-0.42345234774179,13.7420545896487));
#419789=CARTESIAN_POINT('Origin',(2.59987584777974,-0.547463686440066,13.7415084174026));
#419790=CARTESIAN_POINT('Origin',(0.,2.60208521396521E-15,13.7435492065112));
#419791=CARTESIAN_POINT('Origin',(2.58202697203059,-0.636027846521902,13.7420545896488));
#419792=CARTESIAN_POINT('Origin',(2.54660160252169,-0.75755606384985,13.7415084174027));
#419793=CARTESIAN_POINT('Origin',(0.,2.60208521396521E-15,13.7435492065112));
#419794=CARTESIAN_POINT('Origin',(2.52159331619725,-0.844370684920506,13.7420545896486));
#419795=CARTESIAN_POINT('Origin',(2.47638014376077,-0.96260703064293,13.7415084174038));
#419796=CARTESIAN_POINT('Origin',(0.,2.60208521396521E-15,13.7435492065112));
#419797=CARTESIAN_POINT('Origin',(2.4443788728763,-1.04709437572065,13.7420545896477));
#419798=CARTESIAN_POINT('Origin',(2.38967878371463,-1.16125200646612,13.7415084174039));
#419799=CARTESIAN_POINT('Origin',(0.,2.60208521396521E-15,13.7435492065112));
#419800=CARTESIAN_POINT('Origin',(2.35089749145357,-1.24284982621121,13.742054589648));
#419801=CARTESIAN_POINT('Origin',(2.28707450563236,-1.35216904177949,13.7415084174041));
#419802=CARTESIAN_POINT('Origin',(0.,2.60208521396521E-15,13.7435492065112));
#419803=CARTESIAN_POINT('Origin',(2.24177127509384,-1.43033431616192,13.7420545896474));
#419804=CARTESIAN_POINT('Origin',(2.16925012404985,-1.5340876152101,13.7415084174021));
#419805=CARTESIAN_POINT('Origin',(0.,2.60208521396521E-15,13.7435492065112));
#419806=CARTESIAN_POINT('Origin',(2.11772644076833,-1.60830016723173,13.7420545896489));
#419807=CARTESIAN_POINT('Origin',(2.03698974080133,-1.70579708867073,13.7415084174032));
#419808=CARTESIAN_POINT('Origin',(0.,2.60208521396521E-15,13.7435492065112));
#419809=CARTESIAN_POINT('Origin',(1.97958848637722,-1.77556304603655,13.742054589649));
#419810=CARTESIAN_POINT('Origin',(1.8911735269064,-1.86615476394301,13.7415084174042));
#419811=CARTESIAN_POINT('Origin',(0.,2.60208521396521E-15,13.7435492065112));
#419812=CARTESIAN_POINT('Origin',(1.8282766972176,-1.93100984571577,13.7420545896482));
#419813=CARTESIAN_POINT('Origin',(1.73277186520649,-2.01409348715231,13.7415084174027));
#419814=CARTESIAN_POINT('Origin',(0.,2.60208521396521E-15,13.7435492065112));
#419815=CARTESIAN_POINT('Origin',(1.66479802828494,-2.07360609347156,13.7420545896501));
#419816=CARTESIAN_POINT('Origin',(1.56283889263393,-2.14862875050822,13.7415084174026));
#419817=CARTESIAN_POINT('Origin',(0.,2.60208521396521E-15,13.7435492065112));
#419818=CARTESIAN_POINT('Origin',(1.49024040314276,-2.20240283478712,13.7420545896481));
#419819=CARTESIAN_POINT('Origin',(1.3825054850803,-2.2688652440275,13.7415084174021));
#419820=CARTESIAN_POINT('Origin',(0.,2.60208521396521E-15,13.7435492065112));
#419821=CARTESIAN_POINT('Origin',(1.30576547399232,-2.31654294861448,13.7420545896488));
#419822=CARTESIAN_POINT('Origin',(1.19297173162209,-2.37400281368525,13.7415084174022));
#419823=CARTESIAN_POINT('Origin',(0.,2.60208521396521E-15,13.7435492065112));
#419824=CARTESIAN_POINT('Origin',(1.11260089104787,-2.41526685131816,13.7420545896482));
#419825=CARTESIAN_POINT('Origin',(0.995498948118894,-2.46334178630396,13.7415084174039));
#419826=CARTESIAN_POINT('Origin',(0.,2.60208521396521E-15,13.7435492065112));
#419827=CARTESIAN_POINT('Origin',(0.912032132740323,-2.49791755162278,13.7420545896496));
#419828=CARTESIAN_POINT('Origin',(0.791401283357222,-2.53628762575223,13.7415084174029));
#419829=CARTESIAN_POINT('Origin',(0.,2.60208521396521E-15,13.7435492065112));
#419830=CARTESIAN_POINT('Origin',(0.705393951063582,-2.56394502274485,13.7420545896495));
#419831=CARTESIAN_POINT('Origin',(0.582036973629713,-2.59235488951334,13.7415084174038));
#419832=CARTESIAN_POINT('Origin',(0.,2.60208521396521E-15,13.7435492065112));
#419833=CARTESIAN_POINT('Origin',(0.494061489024843,-2.61290986275703,13.7420545896477));
#419834=CARTESIAN_POINT('Origin',(0.368799303868886,-2.6311704591873,13.7415084174023));
#419835=CARTESIAN_POINT('Origin',(0.,2.60208521396521E-15,13.7435492065112));
#419836=CARTESIAN_POINT('Origin',(0.279441129291135,-2.64448621873616,13.7420545896472));
#419837=CARTESIAN_POINT('Origin',(0.153107335591366,-2.652476023574,13.7415084174032));
#419838=CARTESIAN_POINT('Origin',(0.,2.60208521396521E-15,13.7435492065112));
#419839=CARTESIAN_POINT('Origin',(-0.153937855364234,-2.65475005273974,
13.742054589648));
#419840=CARTESIAN_POINT('Origin',(-0.279891138037187,-2.64210746615306,
13.7415084174037));
#419841=CARTESIAN_POINT('Origin',(0.,2.60208521396521E-15,13.7435492065112));
#419842=CARTESIAN_POINT('Origin',(-0.369812414643718,-2.63336922663678,
13.7420545896469));
#419843=CARTESIAN_POINT('Origin',(-0.494316109985248,-2.61050234538536,
13.7415084174037));
#419844=CARTESIAN_POINT('Origin',(0.,2.60208521396521E-15,13.7435492065112));
#419845=CARTESIAN_POINT('Origin',(-0.58322593332106,-2.59446376281132,13.7420545896483));
#419846=CARTESIAN_POINT('Origin',(-0.70545148977777,-2.56152476221158,13.7415084174036));
#419847=CARTESIAN_POINT('Origin',(0.,2.60208521396521E-15,13.7435492065112));
#419848=CARTESIAN_POINT('Origin',(-0.79275817963557,-2.53829257069669,13.7420545896477));
#419849=CARTESIAN_POINT('Origin',(-0.911892206297038,-2.4955006543659,13.7415084174031));
#419850=CARTESIAN_POINT('Origin',(0.,2.60208521396521E-15,13.7435492065112));
#419851=CARTESIAN_POINT('Origin',(-0.997014751062135,-2.4652294603152,13.7420545896484));
#419852=CARTESIAN_POINT('Origin',(-1.11226443063565,-2.41286940140007,13.7415084174049));
#419853=CARTESIAN_POINT('Origin',(0.,2.60208521396521E-15,13.7435492065112));
#419854=CARTESIAN_POINT('Origin',(-1.19463635381647,-2.37576065460941,13.7420545896491));
#419855=CARTESIAN_POINT('Origin',(-1.3052347186976,-2.31418090065322,13.7415084174027));
#419856=CARTESIAN_POINT('Origin',(0.,2.60208521396521E-15,13.7435492065112));
#419857=CARTESIAN_POINT('Origin',(-1.38430784873633,-2.2704815537189,13.7420545896491));
#419858=CARTESIAN_POINT('Origin',(-1.48951888505758,-2.20009190783617,13.7415084174049));
#419859=CARTESIAN_POINT('Origin',(0.,2.60208521396521E-15,13.7435492065112));
#419860=CARTESIAN_POINT('Origin',(-1.56476700331623,-2.15009277269043,13.7420545896486));
#419861=CARTESIAN_POINT('Origin',(-1.6638905489877,-2.07136166635204,13.7415084174028));
#419862=CARTESIAN_POINT('Origin',(0.,2.60208521396521E-15,13.7435492065112));
#419863=CARTESIAN_POINT('Origin',(-1.73481289165434,-2.01539547899836,13.7420545896465));
#419864=CARTESIAN_POINT('Origin',(-1.82718929583891,-1.92884685473472,13.7415084174032));
#419865=CARTESIAN_POINT('Origin',(0.,2.60208521396521E-15,13.7435492065112));
#419866=CARTESIAN_POINT('Origin',(-1.89331388642696,-1.8672860609137,13.7420545896469));
#419867=CARTESIAN_POINT('Origin',(-1.97832839939094,-1.77349588553556,13.7415084174032));
#419868=CARTESIAN_POINT('Origin',(0.,2.60208521396521E-15,13.7435492065112));
#419869=CARTESIAN_POINT('Origin',(-2.03921518966487,-1.70675016217609,13.7420545896489));
#419870=CARTESIAN_POINT('Origin',(-2.11630205384649,-1.60634259382475,13.7415084174034));
#419871=CARTESIAN_POINT('Origin',(0.,2.60208521396521E-15,13.7435492065112));
#419872=CARTESIAN_POINT('Origin',(-2.17154585225241,-1.53485612269886,13.7420545896468));
#419873=CARTESIAN_POINT('Origin',(-2.24019206729996,-1.42849935718093,13.7415084174041));
#419874=CARTESIAN_POINT('Origin',(0.,2.60208521396521E-15,13.7435492065112));
#419875=CARTESIAN_POINT('Origin',(-2.28942523548034,-1.35274786896119,13.7420545896478));
#419876=CARTESIAN_POINT('Origin',(-2.34917397214803,-1.24114969299734,13.741508417403));
#419877=CARTESIAN_POINT('Origin',(0.,2.60208521396521E-15,13.7435492065112));
#419878=CARTESIAN_POINT('Origin',(-2.39206887149331,-1.16163730134264,13.7420545896483));
#419879=CARTESIAN_POINT('Origin',(-2.44252251179907,-1.04554038238373,13.7415084174027));
#419880=CARTESIAN_POINT('Origin',(0.,2.60208521396521E-15,13.7435492065112));
#419881=CARTESIAN_POINT('Origin',(-2.4787936838238,-0.96279622913968,13.7420545896461));
#419882=CARTESIAN_POINT('Origin',(-2.5196164671247,-0.842973173029527,13.7415084174036));
#419883=CARTESIAN_POINT('Origin',(0.,2.60208521396521E-15,13.7435492065112));
#419884=CARTESIAN_POINT('Origin',(-2.54902253317019,-0.757547906882836,
13.7420545896479));
#419885=CARTESIAN_POINT('Origin',(-2.579942790567,-0.634796116287876,13.7415084174037));
#419886=CARTESIAN_POINT('Origin',(0.,2.60208521396521E-15,13.7435492065112));
#419887=CARTESIAN_POINT('Origin',(-2.60228805811162,-0.5472582282921,13.742054589647));
#419888=CARTESIAN_POINT('Origin',(-2.62310002039505,-0.422394596124596,
13.741508417402));
#419889=CARTESIAN_POINT('Origin',(0.,2.60208521396521E-15,13.7435492065112));
#419890=CARTESIAN_POINT('Origin',(-2.63823578537793,-0.333326636482873,
13.7420545896481));
#419891=CARTESIAN_POINT('Origin',(-2.64880095237423,-0.207182109617279,
13.741508417403));
#419892=CARTESIAN_POINT('Origin',(0.,2.60208521396521E-15,13.7435492065112));
#419893=CARTESIAN_POINT('Origin',(-2.65662648876749,-0.117176810903261,
13.7420545896479));
#419894=CARTESIAN_POINT('Origin',(-2.65687455103644,0.00940913964739448,
13.7415084174036));
#419895=CARTESIAN_POINT('Origin',(0.,2.60208521396521E-15,13.7435492065112));
#419896=CARTESIAN_POINT('Origin',(-2.65733778119037,0.0997528070212094,
13.7420545896491));
#419897=CARTESIAN_POINT('Origin',(-2.64726708791042,0.225937772641397,13.7415084174026));
#419898=CARTESIAN_POINT('Origin',(0.,2.60208521396521E-15,13.7435492065112));
#419899=CARTESIAN_POINT('Origin',(-2.64036492910454,0.316018586471474,13.7420545896483));
#419900=CARTESIAN_POINT('Origin',(-2.62004249908263,0.440962827035131,13.7415084174016));
#419901=CARTESIAN_POINT('Origin',(0.,2.60208521396521E-15,13.7435492065112));
#419902=CARTESIAN_POINT('Origin',(-2.60582088404412,0.530181314367318,13.7420545896473));
#419903=CARTESIAN_POINT('Origin',(-2.57538195971003,0.653053346567803,13.7415084174044));
#419904=CARTESIAN_POINT('Origin',(0.,2.60208521396521E-15,13.7435492065112));
#419905=CARTESIAN_POINT('Origin',(-2.55393553093483,0.740815773091958,13.7420545896478));
#419906=CARTESIAN_POINT('Origin',(-2.51358267829733,0.860797903826238,13.7415084174048));
#419907=CARTESIAN_POINT('Origin',(0.,2.60208521396521E-15,13.7435492065112));
#419908=CARTESIAN_POINT('Origin',(-2.48505415823539,0.946520225071862,13.7420545896479));
#419909=CARTESIAN_POINT('Origin',(-2.43505591886255,1.06281399305533,13.7415084174013));
#419910=CARTESIAN_POINT('Origin',(0.,2.60208521396521E-15,13.7435492065112));
#419911=CARTESIAN_POINT('Origin',(-2.39963516011764,1.14592574111846,13.7420545896477));
#419912=CARTESIAN_POINT('Origin',(-2.3403242640558,1.25775723051356,13.7415084174024));
#419913=CARTESIAN_POINT('Origin',(0.,2.60208521396521E-15,13.7435492065112));
#419914=CARTESIAN_POINT('Origin',(-2.29824698592305,1.33770531042418,13.7420545896484));
#419915=CARTESIAN_POINT('Origin',(-2.23001813739833,1.44433030111864,13.7415084174037));
#419916=CARTESIAN_POINT('Origin',(0.,2.60208521396521E-15,13.7435492065112));
#419917=CARTESIAN_POINT('Origin',(-2.18156435721672,1.52058267158977,13.7420545896466));
#419918=CARTESIAN_POINT('Origin',(-2.10487160795666,1.62129159186549,13.7415084174024));
#419919=CARTESIAN_POINT('Origin',(0.,2.60208521396521E-15,13.7435492065112));
#419920=CARTESIAN_POINT('Origin',(-2.05036377765178,1.69334080596183,13.7420545896485));
#419921=CARTESIAN_POINT('Origin',(-1.96571750525081,1.7874634545656,13.7415084174041));
#419922=CARTESIAN_POINT('Origin',(0.,2.60208521396521E-15,13.7435492065112));
#419923=CARTESIAN_POINT('Origin',(-1.90551836542749,1.85483003664387,13.7420545896466));
#419924=CARTESIAN_POINT('Origin',(-1.81348187686654,1.94174004288618,13.741508417405));
#419925=CARTESIAN_POINT('Origin',(0.,2.60208521396521E-15,13.7435492065112));
#419926=CARTESIAN_POINT('Origin',(-1.74799204287233,2.00397567946144,13.7420545896466));
#419927=CARTESIAN_POINT('Origin',(-1.6491778257871,2.08309467158083,13.7415084174022));
#419928=CARTESIAN_POINT('Origin',(0.,2.60208521396521E-15,13.7435492065112));
#419929=CARTESIAN_POINT('Origin',(-1.57883312167183,2.13978519476937,13.7420545896485));
#419930=CARTESIAN_POINT('Origin',(-1.47389876838228,2.21058664892941,13.7415084174045));
#419931=CARTESIAN_POINT('Origin',(0.,2.60208521396521E-15,13.7435492065112));
#419932=CARTESIAN_POINT('Origin',(-1.39916732653332,2.26135479263981,13.7420545896478));
#419933=CARTESIAN_POINT('Origin',(-1.28881115784196,2.32336753684382,13.7415084174024));
#419934=CARTESIAN_POINT('Origin',(0.,2.60208521396521E-15,13.7435492065112));
#419935=CARTESIAN_POINT('Origin',(-1.21019030368429,2.36787544746751,13.7420545896492));
#419936=CARTESIAN_POINT('Origin',(-1.09514672169413,2.4206867971383,13.7415084174055));
#419937=CARTESIAN_POINT('Origin',(0.,2.60208521396521E-15,13.7435492065112));
#419938=CARTESIAN_POINT('Origin',(-1.01315966403005,2.4586382818545,13.7420545896468));
#419939=CARTESIAN_POINT('Origin',(-0.894194264790857,2.50189678617287,13.7415084174032));
#419940=CARTESIAN_POINT('Origin',(0.,2.60208521396521E-15,13.7435492065112));
#419941=CARTESIAN_POINT('Origin',(-0.809386613972477,2.53303928413104,13.7420545896474));
#419942=CARTESIAN_POINT('Origin',(-0.687291092593011,2.56645706488719,13.7415084174047));
#419943=CARTESIAN_POINT('Origin',(0.,2.60208521396521E-15,13.7435492065112));
#419944=CARTESIAN_POINT('Origin',(-0.600227229537934,2.59058332789403,13.7420545896484));
#419945=CARTESIAN_POINT('Origin',(-0.475814111565582,2.61393799526496,13.7415084174039));
#419946=CARTESIAN_POINT('Origin',(0.,2.60208521396521E-15,13.7435492065112));
#419947=CARTESIAN_POINT('Origin',(2.04902042275678,1.69132676291974,13.7415084174029));
#419948=CARTESIAN_POINT('Origin',(1.96790222757021,1.78850650783342,13.7420545896482));
#419949=CARTESIAN_POINT('Origin',(0.,2.60208521396521E-15,13.7435492065112));
#419950=CARTESIAN_POINT('Origin',(1.90434364364273,1.85271319927288,13.7415084174028));
#419951=CARTESIAN_POINT('Origin',(1.81557431117862,1.94295770063162,13.7420545896495));
#419952=CARTESIAN_POINT('Origin',(0.,2.60208521396521E-15,13.7435492065112));
#419953=CARTESIAN_POINT('Origin',(1.74699377177696,2.00177013496568,13.7415084174048));
#419954=CARTESIAN_POINT('Origin',(1.65116404728956,2.08447883049457,13.7420545896484));
#419955=CARTESIAN_POINT('Origin',(0.,2.60208521396521E-15,13.7435492065112));
#419956=CARTESIAN_POINT('Origin',(1.57801794458986,2.13750562067086,13.7415084174033));
#419957=CARTESIAN_POINT('Origin',(1.47576555909092,2.21212809765666,13.7420545896483));
#419958=CARTESIAN_POINT('Origin',(0.,2.60208521396521E-15,13.7435492065112));
#419959=CARTESIAN_POINT('Origin',(1.39854066833794,2.25901635913813,13.7415084174035));
#419960=CARTESIAN_POINT('Origin',(1.29054609457721,2.32505601730086,13.7420545896465));
#419961=CARTESIAN_POINT('Origin',(0.,2.60208521396521E-15,13.7435492065112));
#419962=CARTESIAN_POINT('Origin',(1.20975633468107,2.36549371644643,13.7415084174035));
#419963=CARTESIAN_POINT('Origin',(1.09673825873626,2.422511072764,13.7420545896482));
#419964=CARTESIAN_POINT('Origin',(0.,2.60208521396521E-15,13.7435492065112));
#419965=CARTESIAN_POINT('Origin',(1.01292127221245,2.45622910334862,13.7415084174024));
#419966=CARTESIAN_POINT('Origin',(0.8956318107298,2.50384471672177,13.7420545896489));
#419967=CARTESIAN_POINT('Origin',(0.,2.60208521396521E-15,13.7435492065112));
#419968=CARTESIAN_POINT('Origin',(0.809345385797912,2.53061869082039,13.7415084174029));
#419969=CARTESIAN_POINT('Origin',(0.688565080790549,2.56851568719345,13.7420545896486));
#419970=CARTESIAN_POINT('Origin',(0.,2.60208521396521E-15,13.7435492065112));
#419971=CARTESIAN_POINT('Origin',(0.60038343937335,2.58816742842705,13.741508417403));
#419972=CARTESIAN_POINT('Origin',(0.476916063842626,2.61609360953942,13.7420545896471));
#419973=CARTESIAN_POINT('Origin',(0.,2.60208521396521E-15,13.7435492065112));
#419974=CARTESIAN_POINT('Origin',(0.387426040215676,2.62849233881714,13.741508417404));
#419975=CARTESIAN_POINT('Origin',(0.262093249178328,2.64626186054439,13.7420545896481));
#419976=CARTESIAN_POINT('Origin',(0.,2.60208521396521E-15,13.7435492065112));
#419977=CARTESIAN_POINT('Origin',(0.171890384681917,2.65132506635799,13.7415084174029));
#419978=CARTESIAN_POINT('Origin',(0.0455262471821439,2.65881967546814,13.7420545896482));
#419979=CARTESIAN_POINT('Origin',(0.,2.60208521396521E-15,13.7435492065112));
#419980=CARTESIAN_POINT('Origin',(-0.387073431921677,2.63088746702105,13.7420545896474));
#419981=CARTESIAN_POINT('Origin',(-0.261170666129395,2.64402359955241,13.7415084174024));
#419982=CARTESIAN_POINT('Origin',(0.,2.69653690488338,12.5));
#419983=CARTESIAN_POINT('',(-0.0317307692307694,2.68331575103722,12.5893111709658));
#419984=CARTESIAN_POINT('',(-0.0317307692307694,2.68331575103722,13.8235269408515));
#419985=CARTESIAN_POINT('',(-0.0317307692307694,2.68331575103722,12.5));
#419986=CARTESIAN_POINT('',(0.00111954586465913,2.66218087500164,13.8587068136939));
#419987=CARTESIAN_POINT('Ctrl Pts',(-0.0317307692368139,2.68331575103455,
13.8235269408542));
#419988=CARTESIAN_POINT('Ctrl Pts',(-0.0310568083417728,2.68169824488647,
13.8262006681044));
#419989=CARTESIAN_POINT('Ctrl Pts',(-0.0302067330691194,2.68010978649456,
13.8288634856214));
#419990=CARTESIAN_POINT('Ctrl Pts',(-0.0291938585816618,2.6785496599764,
13.8314912288862));
#419991=CARTESIAN_POINT('Ctrl Pts',(-0.0281496894582509,2.67694133045577,
13.834200161153));
#419992=CARTESIAN_POINT('Ctrl Pts',(-0.0269317626839319,2.67536105356044,
13.8368750301949));
#419993=CARTESIAN_POINT('Ctrl Pts',(-0.0255098200583974,2.67381369830471,
13.8394886372968));
#419994=CARTESIAN_POINT('Ctrl Pts',(-0.0253999999802731,2.67369419230494,
13.8396904925131));
#419995=CARTESIAN_POINT('Ctrl Pts',(-0.0252889443323249,2.67357489463028,
13.8398919674349));
#419996=CARTESIAN_POINT('Ctrl Pts',(-0.0251766301202508,2.67345581452184,
13.8400930404591));
#419997=CARTESIAN_POINT('Ctrl Pts',(-0.0234266991348905,2.67160046631923,
13.8432258934518));
#419998=CARTESIAN_POINT('Ctrl Pts',(-0.0213809904682469,2.66980662883099,
13.8462331177034));
#419999=CARTESIAN_POINT('Ctrl Pts',(-0.0190426235063883,2.66820533811557,
13.8489036603661));
#420000=CARTESIAN_POINT('Ctrl Pts',(-0.0182774826235232,2.66768137715832,
13.8497774930041));
#420001=CARTESIAN_POINT('Ctrl Pts',(-0.0174811027381851,2.66717826280278,
13.85061494757));
#420002=CARTESIAN_POINT('Ctrl Pts',(-0.0166538759919881,2.66670124117228,
13.8514076489583));
#420003=CARTESIAN_POINT('Ctrl Pts',(-0.0149041721198265,2.66569227162696,
13.8530843267192));
#420004=CARTESIAN_POINT('Ctrl Pts',(-0.0128431198768504,2.66470349169249,
13.8546805203176));
#420005=CARTESIAN_POINT('Ctrl Pts',(-0.0105313231737223,2.66391531097655,
13.8559412814273));
#420006=CARTESIAN_POINT('Ctrl Pts',(-0.010221929801502,2.66380982683545,
13.8561100121513));
#420007=CARTESIAN_POINT('Ctrl Pts',(-0.0099081113111903,2.66370789632895,
13.8562727473908));
#420008=CARTESIAN_POINT('Ctrl Pts',(-0.0095900727650585,2.66360990524316,
13.8564289040185));
#420009=CARTESIAN_POINT('Ctrl Pts',(-0.00814777158665154,2.66316551678701,
13.8571370725437));
#420010=CARTESIAN_POINT('Ctrl Pts',(-0.00659265830578076,2.66279651133532,
13.8577210840554));
#420011=CARTESIAN_POINT('Ctrl Pts',(-0.00497840473373783,2.66254578735691,
13.8581177131616));
#420012=CARTESIAN_POINT('Ctrl Pts',(-0.00452377536693578,2.66247517485494,
13.8582294175695));
#420013=CARTESIAN_POINT('Ctrl Pts',(-0.00406451623070895,2.66241377743103,
13.8583265086086));
#420014=CARTESIAN_POINT('Ctrl Pts',(-0.00360195264082081,2.66236213234807,
13.8584082369006));
#420015=CARTESIAN_POINT('Ctrl Pts',(-0.00293737280347575,2.66228793221303,
13.8585256585398));
#420016=CARTESIAN_POINT('Ctrl Pts',(-0.002257673747352,2.66223326171001,
13.8586122832068));
#420017=CARTESIAN_POINT('Ctrl Pts',(-0.00158044877125891,2.66220032816512,
13.8586682984299));
#420018=CARTESIAN_POINT('Ctrl Pts',(-0.00103873592153746,2.6621739845938,
13.8587131050557));
#420019=CARTESIAN_POINT('Ctrl Pts',(-0.000492634257675246,2.66216102405791,
13.8587357943552));
#420020=CARTESIAN_POINT('Ctrl Pts',(5.79331281739812E-5,2.66216195132077,
13.8587355499465));
#420021=CARTESIAN_POINT('Ctrl Pts',(0.000413777955724857,2.66216255063287,
13.8587353919793));
#420022=CARTESIAN_POINT('Ctrl Pts',(0.000767640276359607,2.66216890620456,
13.8587257282814));
#420023=CARTESIAN_POINT('Ctrl Pts',(0.00111954586465914,2.66218087500164,
13.8587068136939));
#420024=CARTESIAN_POINT('',(0.0317307692307694,2.68331575103722,13.8235269408515));
#420025=CARTESIAN_POINT('Ctrl Pts',(0.00111954586465914,2.66218087500164,
13.8587068136939));
#420026=CARTESIAN_POINT('Ctrl Pts',(0.00227694416047025,2.66222023972277,
13.8586446046466));
#420027=CARTESIAN_POINT('Ctrl Pts',(0.0034132030282657,2.66232024878167,
13.858482427929));
#420028=CARTESIAN_POINT('Ctrl Pts',(0.00452901854825893,2.66247648613606,
13.8582284286032));
#420029=CARTESIAN_POINT('Ctrl Pts',(0.00567371547471972,2.66263676748737,
13.8579678548414));
#420030=CARTESIAN_POINT('Ctrl Pts',(0.00679948085161418,2.66285813397142,
13.857615680862));
#420031=CARTESIAN_POINT('Ctrl Pts',(0.00786380175605046,2.66312235077613,
13.8571944833187));
#420032=CARTESIAN_POINT('Ctrl Pts',(0.0105199234229024,2.66378173083418,
13.8561433417727));
#420033=CARTESIAN_POINT('Ctrl Pts',(0.0129187674764211,2.66473417359602,
13.8546163505474));
#420034=CARTESIAN_POINT('Ctrl Pts',(0.0149915607379914,2.66578467107066,
13.8528973491086));
#420035=CARTESIAN_POINT('Ctrl Pts',(0.0153702294856515,2.66597658146062,
13.8525833129072));
#420036=CARTESIAN_POINT('Ctrl Pts',(0.0157381315426899,2.66617168202568,
13.8522628768811));
#420037=CARTESIAN_POINT('Ctrl Pts',(0.016095007457731,2.66636870368544,
13.851937733538));
#420038=CARTESIAN_POINT('Ctrl Pts',(0.0182743991566692,2.66757188762613,
13.8499521282529));
#420039=CARTESIAN_POINT('Ctrl Pts',(0.020257204092566,2.66896986054969,
13.847639871647));
#420040=CARTESIAN_POINT('Ctrl Pts',(0.0219855079307009,2.67042348860387,
13.8452109780794));
#420041=CARTESIAN_POINT('Ctrl Pts',(0.0227631076015868,2.67107750595405,
13.8441181685877));
#420042=CARTESIAN_POINT('Ctrl Pts',(0.0234898124370233,2.67174243386388,
13.8430021611332));
#420043=CARTESIAN_POINT('Ctrl Pts',(0.0241635881008166,2.67240493103305,
13.8418824960098));
#420044=CARTESIAN_POINT('Ctrl Pts',(0.0257513576580267,2.67396612252969,
13.8392439765549));
#420045=CARTESIAN_POINT('Ctrl Pts',(0.027123754201243,2.67558575023078,
13.8364981347964));
#420046=CARTESIAN_POINT('Ctrl Pts',(0.0283105152282354,2.67724597470287,
13.8336931113419));
#420047=CARTESIAN_POINT('Ctrl Pts',(0.029466345102232,2.67886292790469,
13.8309611966328));
#420048=CARTESIAN_POINT('Ctrl Pts',(0.0304467890444241,2.68052033781573,
13.8281701127185));
#420049=CARTESIAN_POINT('Ctrl Pts',(0.0312412241942218,2.68221138008974,
13.825358068512));
#420050=CARTESIAN_POINT('Ctrl Pts',(0.031413458592073,2.68257799987976,
13.8247484142932));
#420051=CARTESIAN_POINT('Ctrl Pts',(0.0315767788941016,2.68294617422922,
13.8241378483365));
#420052=CARTESIAN_POINT('Ctrl Pts',(0.0317307692307694,2.68331575103722,
13.8235269408515));
#420053=CARTESIAN_POINT('',(0.0317307692307694,2.68331575103722,12.5893111709658));
#420054=CARTESIAN_POINT('',(0.0317307692307694,2.68331575103722,12.5));
#420055=CARTESIAN_POINT('',(-0.000122408502243047,2.66216281377041,12.5969504640361));
#420056=CARTESIAN_POINT('Origin',(1.95806035357092E-7,2.69656999029512,
12.584524458991));
#420057=CARTESIAN_POINT('Origin',(1.95806035357092E-7,2.69656999029512,
12.584524458991));
#420058=CARTESIAN_POINT('Origin',(-0.1375,2.93716190488338,12.5));
#420059=CARTESIAN_POINT('',(-0.0534592077666728,2.73546400352339,13.7435492065112));
#420060=CARTESIAN_POINT('',(-0.0454872776377203,2.71633137121391,13.7902182540695));
#420061=CARTESIAN_POINT('Origin',(-0.0245384230857362,2.66605412028915,
13.7418732680451));
#420062=CARTESIAN_POINT('',(-0.0454872776377203,2.71633137121391,13.7902182540695));
#420063=CARTESIAN_POINT('',(-0.0534592077666728,2.73546400352339,12.5369868989719));
#420064=CARTESIAN_POINT('Ctrl Pts',(-0.0317307692307694,2.68331575103722,
12.5893111709658));
#420065=CARTESIAN_POINT('Ctrl Pts',(-0.0389789705363253,2.70071143417056,
12.5718848856037));
#420066=CARTESIAN_POINT('Ctrl Pts',(-0.0462216773885433,2.71809393061588,
12.5544431401645));
#420067=CARTESIAN_POINT('Ctrl Pts',(-0.0534592077666728,2.73546400352339,
12.5369868989719));
#420068=CARTESIAN_POINT('',(-0.0534592077666728,2.73546400352339,12.5));
#420069=CARTESIAN_POINT('Origin',(0.0317307692307694,2.68331575103722,12.5));
#420070=CARTESIAN_POINT('',(0.0454872776377203,2.71633137121391,13.7902182540695));
#420071=CARTESIAN_POINT('',(0.0317307692307694,2.68331575103722,13.8235269408515));
#420072=CARTESIAN_POINT('',(0.0534592077666729,2.73546400352339,13.7435492065112));
#420073=CARTESIAN_POINT('Origin',(0.0272313623171153,2.67251802140762,13.7445212918687));
#420074=CARTESIAN_POINT('',(0.0534592077666728,2.73546400352339,12.5369868989719));
#420075=CARTESIAN_POINT('',(0.0534592077666729,2.73546400352339,12.5));
#420076=CARTESIAN_POINT('Ctrl Pts',(0.0534592077666728,2.73546400352339,
12.5369868989719));
#420077=CARTESIAN_POINT('Ctrl Pts',(0.0462216773885433,2.71809393061588,
12.5544431401645));
#420078=CARTESIAN_POINT('Ctrl Pts',(0.0389789705363253,2.70071143417056,
12.5718848856037));
#420079=CARTESIAN_POINT('Ctrl Pts',(0.0317307692307694,2.68331575103722,
12.5893111709658));
#420080=CARTESIAN_POINT('Origin',(0.,1.50000000000006,11.));
#420081=CARTESIAN_POINT('Origin',(0.,1.25,12.5));
#420082=CARTESIAN_POINT('',(1.25,0.721687836487034,12.5));
#420083=CARTESIAN_POINT('',(1.25,0.721687836487034,12.5));
#420084=CARTESIAN_POINT('',(1.25,-0.721687836487026,12.5));
#420085=CARTESIAN_POINT('Origin',(0.,1.25,12.5));
#420086=CARTESIAN_POINT('',(1.25,-0.721687836487026,12.5));
#420087=CARTESIAN_POINT('',(1.25,-0.721687836487026,12.5));
#420088=CARTESIAN_POINT('',(4.15041292089432E-16,-1.44337567297406,12.5));
#420089=CARTESIAN_POINT('Origin',(0.,1.25,12.5));
#420090=CARTESIAN_POINT('',(4.15041292089432E-16,-1.44337567297406,12.5));
#420091=CARTESIAN_POINT('',(4.15041292089432E-16,-1.44337567297406,12.5));
#420092=CARTESIAN_POINT('',(-1.25,-0.721687836487026,12.5));
#420093=CARTESIAN_POINT('Origin',(0.,1.25,12.5));
#420094=CARTESIAN_POINT('',(-1.25,-0.721687836487026,12.5));
#420095=CARTESIAN_POINT('',(-1.25,-0.721687836487026,12.5));
#420096=CARTESIAN_POINT('',(-1.25,0.721687836487034,12.5));
#420097=CARTESIAN_POINT('Origin',(0.,1.25,12.5));
#420098=CARTESIAN_POINT('',(-1.25,0.721687836487034,12.5));
#420099=CARTESIAN_POINT('',(-1.25,0.721687836487034,12.5));
#420100=CARTESIAN_POINT('',(0.,1.44337567297406,12.5));
#420101=CARTESIAN_POINT('Origin',(0.,2.49354920651117,14.));
#420102=CARTESIAN_POINT('',(-2.16840434497101E-15,1.44337567297406,14.));
#420103=CARTESIAN_POINT('',(-1.25,0.721687836487034,14.));
#420104=CARTESIAN_POINT('Origin',(0.,-1.34815096107107E-30,14.));
#420105=CARTESIAN_POINT('Origin',(0.,-1.34815096107107E-30,14.));
#420106=CARTESIAN_POINT('',(1.23599047663348E-14,-1.44337567297406,14.));
#420107=CARTESIAN_POINT('Origin',(0.,-1.34815096107107E-30,14.));
#420108=CARTESIAN_POINT('',(-1.25,-0.721687836487034,14.));
#420109=CARTESIAN_POINT('Origin',(0.,-1.34815096107107E-30,14.));
#420110=CARTESIAN_POINT('Origin',(0.,-1.34815096107107E-30,14.));
#420111=CARTESIAN_POINT('Origin',(0.,2.60208521396521E-15,13.7435492065112));
#420112=CARTESIAN_POINT('Origin',(-0.171343724478305,2.65368348412408,13.7420545896475));
#420113=CARTESIAN_POINT('Origin',(-0.0447891730027414,2.65651366302394,
13.7415084174035));
#420114=CARTESIAN_POINT('Origin',(1.25,0.721687836487034,12.5));
#420115=CARTESIAN_POINT('',(1.25,0.721687836487034,12.5));
#420116=CARTESIAN_POINT('Ctrl Pts',(4.61486004131587E-15,1.44337567297406,
14.));
#420117=CARTESIAN_POINT('Ctrl Pts',(0.624999999999999,1.08253175473055,
13.6391560817565));
#420118=CARTESIAN_POINT('Ctrl Pts',(1.24999999999999,0.721687836487036,
14.));
#420119=CARTESIAN_POINT('',(0.,1.44337567297406,12.5));
#420120=CARTESIAN_POINT('',(0.,1.44337567297406,12.5));
#420121=CARTESIAN_POINT('',(1.25,0.721687836487034,12.5));
#420122=CARTESIAN_POINT('Origin',(1.25,-0.721687836487026,12.5));
#420123=CARTESIAN_POINT('',(1.25,-0.721687836487026,12.5));
#420124=CARTESIAN_POINT('Origin',(4.15041292089432E-16,-1.44337567297406,
12.5));
#420125=CARTESIAN_POINT('',(4.15041292089432E-16,-1.44337567297406,12.5));
#420126=CARTESIAN_POINT('Ctrl Pts',(1.24999999999999,-0.721687836487028,
14.));
#420127=CARTESIAN_POINT('Ctrl Pts',(0.624999999999999,-1.08253175473054,
13.6391560817565));
#420128=CARTESIAN_POINT('Ctrl Pts',(6.39603409235004E-15,-1.44337567297405,
14.));
#420129=CARTESIAN_POINT('Origin',(-1.25,-0.721687836487026,12.5));
#420130=CARTESIAN_POINT('',(-1.25,-0.721687836487026,12.5));
#420131=CARTESIAN_POINT('Ctrl Pts',(5.2220784678048E-15,-1.44337567297406,
14.));
#420132=CARTESIAN_POINT('Ctrl Pts',(-0.624999999999994,-1.08253175473054,
13.6391560817565));
#420133=CARTESIAN_POINT('Ctrl Pts',(-1.24999999999999,-0.721687836487029,
14.));
#420134=CARTESIAN_POINT('Origin',(-1.25,0.721687836487034,12.5));
#420135=CARTESIAN_POINT('',(-1.25,0.721687836487034,12.5));
#420136=CARTESIAN_POINT('Ctrl Pts',(-1.25,-0.721687836487024,14.));
#420137=CARTESIAN_POINT('Ctrl Pts',(-1.25,1.77635683940025E-15,13.6391560817565));
#420138=CARTESIAN_POINT('Ctrl Pts',(-1.25,0.721687836487028,14.));
#420139=CARTESIAN_POINT('Origin',(0.,1.44337567297406,12.5));
#420140=CARTESIAN_POINT('Ctrl Pts',(-1.24999999999999,0.721687836487037,
14.));
#420141=CARTESIAN_POINT('Ctrl Pts',(-0.624999999999999,1.08253175473055,
13.6391560817565));
#420142=CARTESIAN_POINT('Ctrl Pts',(-5.38400338153518E-15,1.44337567297406,
14.));
#420143=CARTESIAN_POINT('',(0.,1.44337567297406,12.5));
#420144=CARTESIAN_POINT('Origin',(0.,1.25,12.5));
#420145=CARTESIAN_POINT('Origin',(0.,-1.34815096107107E-30,14.));
#420146=CARTESIAN_POINT('Origin',(0.,-1.34815096107107E-30,14.));
#420147=CARTESIAN_POINT('Origin',(0.,-1.34815096107107E-30,14.));
#420148=CARTESIAN_POINT('Origin',(0.,-1.34815096107107E-30,14.));
#420149=CARTESIAN_POINT('Origin',(0.,-1.34815096107107E-30,14.));
#420150=CARTESIAN_POINT('Origin',(0.,2.54061283442571E-15,-14.));
#420151=CARTESIAN_POINT('Ctrl Pts',(0.,1.52706329386832,-13.984375));
#420152=CARTESIAN_POINT('Ctrl Pts',(-0.881650403784468,1.52706329386832,
-13.9427083333333));
#420153=CARTESIAN_POINT('Ctrl Pts',(-1.3224756056767,0.76353164693416,-13.9010416666667));
#420154=CARTESIAN_POINT('Ctrl Pts',(-1.76330080756894,2.64858386892187E-15,
-13.859375));
#420155=CARTESIAN_POINT('Ctrl Pts',(-1.3224756056767,-0.763531646934155,
-13.8177083333333));
#420156=CARTESIAN_POINT('Ctrl Pts',(-0.881650403784469,-1.52706329386831,
-13.7760416666666));
#420157=CARTESIAN_POINT('Ctrl Pts',(-1.87011317493125E-16,-1.52706329386831,
-13.734375));
#420158=CARTESIAN_POINT('Ctrl Pts',(0.881650403784467,-1.52706329386831,
-13.6927083333333));
#420159=CARTESIAN_POINT('Ctrl Pts',(1.3224756056767,-0.763531646934156,
-13.6510416666667));
#420160=CARTESIAN_POINT('Ctrl Pts',(1.76330080756894,2.21669973093722E-15,
-13.609375));
#420161=CARTESIAN_POINT('Ctrl Pts',(1.3224756056767,0.763531646934159,-13.5677083333333));
#420162=CARTESIAN_POINT('Ctrl Pts',(0.881650403784469,1.52706329386832,
-13.5260416666666));
#420163=CARTESIAN_POINT('Ctrl Pts',(0.,1.52706329386832,-13.484375));
#420164=CARTESIAN_POINT('Ctrl Pts',(-0.881650403784468,1.52706329386832,
-13.4427083333333));
#420165=CARTESIAN_POINT('Ctrl Pts',(-1.3224756056767,0.76353164693416,-13.4010416666666));
#420166=CARTESIAN_POINT('Ctrl Pts',(-1.76330080756894,2.64858386892187E-15,
-13.359375));
#420167=CARTESIAN_POINT('Ctrl Pts',(-1.3224756056767,-0.763531646934155,
-13.3177083333333));
#420168=CARTESIAN_POINT('Ctrl Pts',(-0.881650403784469,-1.52706329386831,
-13.2760416666666));
#420169=CARTESIAN_POINT('Ctrl Pts',(-1.87011317493125E-16,-1.52706329386831,
-13.234375));
#420170=CARTESIAN_POINT('Ctrl Pts',(0.881650403784467,-1.52706329386831,
-13.1927083333333));
#420171=CARTESIAN_POINT('Ctrl Pts',(1.3224756056767,-0.763531646934156,
-13.1510416666667));
#420172=CARTESIAN_POINT('Ctrl Pts',(1.76330080756894,2.21669973093722E-15,
-13.109375));
#420173=CARTESIAN_POINT('Ctrl Pts',(1.3224756056767,0.763531646934159,-13.0677083333333));
#420174=CARTESIAN_POINT('Ctrl Pts',(0.881650403784469,1.52706329386832,
-13.0260416666667));
#420175=CARTESIAN_POINT('Ctrl Pts',(0.,1.52706329386832,-12.984375));
#420176=CARTESIAN_POINT('Ctrl Pts',(-0.881650403784468,1.52706329386832,
-12.9427083333333));
#420177=CARTESIAN_POINT('Ctrl Pts',(-1.3224756056767,0.76353164693416,-12.9010416666666));
#420178=CARTESIAN_POINT('Ctrl Pts',(-1.76330080756894,2.64858386892187E-15,
-12.859375));
#420179=CARTESIAN_POINT('Ctrl Pts',(-1.3224756056767,-0.763531646934155,
-12.8177083333333));
#420180=CARTESIAN_POINT('Ctrl Pts',(-0.881650403784469,-1.52706329386831,
-12.7760416666666));
#420181=CARTESIAN_POINT('Ctrl Pts',(-1.87011317493125E-16,-1.52706329386831,
-12.734375));
#420182=CARTESIAN_POINT('Ctrl Pts',(0.881650403784467,-1.52706329386831,
-12.6927083333333));
#420183=CARTESIAN_POINT('Ctrl Pts',(1.3224756056767,-0.763531646934156,
-12.6510416666666));
#420184=CARTESIAN_POINT('Ctrl Pts',(1.76330080756894,2.21669973093722E-15,
-12.609375));
#420185=CARTESIAN_POINT('Ctrl Pts',(1.3224756056767,0.763531646934159,-12.5677083333333));
#420186=CARTESIAN_POINT('Ctrl Pts',(0.881650403784469,1.52706329386832,
-12.5260416666666));
#420187=CARTESIAN_POINT('Ctrl Pts',(0.,1.52706329386832,-12.484375));
#420188=CARTESIAN_POINT('Ctrl Pts',(-0.881650403784468,1.52706329386832,
-12.4427083333333));
#420189=CARTESIAN_POINT('Ctrl Pts',(-1.3224756056767,0.76353164693416,-12.4010416666666));
#420190=CARTESIAN_POINT('Ctrl Pts',(-1.76330080756894,2.64858386892187E-15,
-12.359375));
#420191=CARTESIAN_POINT('Ctrl Pts',(-1.3224756056767,-0.763531646934155,
-12.3177083333333));
#420192=CARTESIAN_POINT('Ctrl Pts',(-0.881650403784469,-1.52706329386831,
-12.2760416666666));
#420193=CARTESIAN_POINT('Ctrl Pts',(-1.87011317493125E-16,-1.52706329386831,
-12.234375));
#420194=CARTESIAN_POINT('Ctrl Pts',(0.881650403784467,-1.52706329386831,
-12.1927083333333));
#420195=CARTESIAN_POINT('Ctrl Pts',(1.3224756056767,-0.763531646934156,
-12.1510416666666));
#420196=CARTESIAN_POINT('Ctrl Pts',(1.76330080756894,2.21669973093722E-15,
-12.109375));
#420197=CARTESIAN_POINT('Ctrl Pts',(1.3224756056767,0.763531646934159,-12.0677083333333));
#420198=CARTESIAN_POINT('Ctrl Pts',(0.881650403784469,1.52706329386832,
-12.0260416666667));
#420199=CARTESIAN_POINT('Ctrl Pts',(0.,1.52706329386832,-11.984375));
#420200=CARTESIAN_POINT('Ctrl Pts',(-0.881650403784468,1.52706329386832,
-11.9427083333333));
#420201=CARTESIAN_POINT('Ctrl Pts',(-1.3224756056767,0.76353164693416,-11.9010416666667));
#420202=CARTESIAN_POINT('Ctrl Pts',(-1.76330080756894,2.64858386892187E-15,
-11.859375));
#420203=CARTESIAN_POINT('Ctrl Pts',(-1.3224756056767,-0.763531646934155,
-11.8177083333333));
#420204=CARTESIAN_POINT('Ctrl Pts',(-0.881650403784469,-1.52706329386831,
-11.7760416666666));
#420205=CARTESIAN_POINT('Ctrl Pts',(-1.87011317493125E-16,-1.52706329386831,
-11.734375));
#420206=CARTESIAN_POINT('Ctrl Pts',(0.881650403784467,-1.52706329386831,
-11.6927083333333));
#420207=CARTESIAN_POINT('Ctrl Pts',(1.3224756056767,-0.763531646934156,
-11.6510416666666));
#420208=CARTESIAN_POINT('Ctrl Pts',(1.76330080756894,2.21669973093722E-15,
-11.609375));
#420209=CARTESIAN_POINT('Ctrl Pts',(1.3224756056767,0.763531646934159,-11.5677083333333));
#420210=CARTESIAN_POINT('Ctrl Pts',(0.881650403784469,1.52706329386832,
-11.5260416666666));
#420211=CARTESIAN_POINT('Ctrl Pts',(0.,1.52706329386832,-11.484375));
#420212=CARTESIAN_POINT('Ctrl Pts',(-0.881650403784468,1.52706329386832,
-11.4427083333333));
#420213=CARTESIAN_POINT('Ctrl Pts',(-1.3224756056767,0.76353164693416,-11.4010416666667));
#420214=CARTESIAN_POINT('Ctrl Pts',(-1.76330080756894,2.64858386892187E-15,
-11.359375));
#420215=CARTESIAN_POINT('Ctrl Pts',(-1.3224756056767,-0.763531646934155,
-11.3177083333333));
#420216=CARTESIAN_POINT('Ctrl Pts',(-0.881650403784469,-1.52706329386831,
-11.2760416666667));
#420217=CARTESIAN_POINT('Ctrl Pts',(-1.87011317493125E-16,-1.52706329386831,
-11.234375));
#420218=CARTESIAN_POINT('Ctrl Pts',(0.881650403784467,-1.52706329386831,
-11.1927083333333));
#420219=CARTESIAN_POINT('Ctrl Pts',(1.3224756056767,-0.763531646934156,
-11.1510416666666));
#420220=CARTESIAN_POINT('Ctrl Pts',(1.76330080756894,2.21669973093722E-15,
-11.109375));
#420221=CARTESIAN_POINT('Ctrl Pts',(1.3224756056767,0.763531646934159,-11.0677083333333));
#420222=CARTESIAN_POINT('Ctrl Pts',(0.881650403784469,1.52706329386832,
-11.0260416666666));
#420223=CARTESIAN_POINT('Ctrl Pts',(0.,1.52706329386832,-10.984375));
#420224=CARTESIAN_POINT('Ctrl Pts',(-0.881650403784468,1.52706329386832,
-10.9427083333333));
#420225=CARTESIAN_POINT('Ctrl Pts',(-1.3224756056767,0.76353164693416,-10.9010416666666));
#420226=CARTESIAN_POINT('Ctrl Pts',(-1.76330080756894,2.64858386892187E-15,
-10.859375));
#420227=CARTESIAN_POINT('Ctrl Pts',(-1.3224756056767,-0.763531646934155,
-10.8177083333333));
#420228=CARTESIAN_POINT('Ctrl Pts',(-0.881650403784469,-1.52706329386831,
-10.7760416666666));
#420229=CARTESIAN_POINT('Ctrl Pts',(-1.87011317493125E-16,-1.52706329386831,
-10.734375));
#420230=CARTESIAN_POINT('Ctrl Pts',(0.881650403784467,-1.52706329386831,
-10.6927083333333));
#420231=CARTESIAN_POINT('Ctrl Pts',(1.3224756056767,-0.763531646934156,
-10.6510416666667));
#420232=CARTESIAN_POINT('Ctrl Pts',(1.76330080756894,2.21669973093722E-15,
-10.609375));
#420233=CARTESIAN_POINT('Ctrl Pts',(1.3224756056767,0.763531646934159,-10.5677083333333));
#420234=CARTESIAN_POINT('Ctrl Pts',(0.881650403784469,1.52706329386832,
-10.5260416666667));
#420235=CARTESIAN_POINT('Ctrl Pts',(0.,1.52706329386832,-10.484375));
#420236=CARTESIAN_POINT('Ctrl Pts',(-0.881650403784468,1.52706329386832,
-10.4427083333333));
#420237=CARTESIAN_POINT('Ctrl Pts',(-1.3224756056767,0.76353164693416,-10.4010416666666));
#420238=CARTESIAN_POINT('Ctrl Pts',(-1.76330080756894,2.64858386892187E-15,
-10.359375));
#420239=CARTESIAN_POINT('Ctrl Pts',(-1.3224756056767,-0.763531646934155,
-10.3177083333333));
#420240=CARTESIAN_POINT('Ctrl Pts',(-0.881650403784469,-1.52706329386831,
-10.2760416666667));
#420241=CARTESIAN_POINT('Ctrl Pts',(-1.87011317493125E-16,-1.52706329386831,
-10.234375));
#420242=CARTESIAN_POINT('Ctrl Pts',(0.881650403784467,-1.52706329386831,
-10.1927083333333));
#420243=CARTESIAN_POINT('Ctrl Pts',(1.3224756056767,-0.763531646934156,
-10.1510416666667));
#420244=CARTESIAN_POINT('Ctrl Pts',(1.76330080756894,2.21669973093722E-15,
-10.109375));
#420245=CARTESIAN_POINT('Ctrl Pts',(1.3224756056767,0.763531646934159,-10.0677083333333));
#420246=CARTESIAN_POINT('Ctrl Pts',(0.881650403784469,1.52706329386832,
-10.0260416666666));
#420247=CARTESIAN_POINT('Ctrl Pts',(0.,1.52706329386832,-9.98437499999998));
#420248=CARTESIAN_POINT('Ctrl Pts',(-0.881650403784468,1.52706329386832,
-9.94270833333331));
#420249=CARTESIAN_POINT('Ctrl Pts',(-1.3224756056767,0.76353164693416,-9.90104166666665));
#420250=CARTESIAN_POINT('Ctrl Pts',(-1.76330080756894,2.64858386892187E-15,
-9.85937499999998));
#420251=CARTESIAN_POINT('Ctrl Pts',(-1.3224756056767,-0.763531646934155,
-9.81770833333331));
#420252=CARTESIAN_POINT('Ctrl Pts',(-0.881650403784469,-1.52706329386831,
-9.77604166666665));
#420253=CARTESIAN_POINT('Ctrl Pts',(-1.87011317493125E-16,-1.52706329386831,
-9.73437499999998));
#420254=CARTESIAN_POINT('Ctrl Pts',(0.881650403784467,-1.52706329386831,
-9.69270833333331));
#420255=CARTESIAN_POINT('Ctrl Pts',(1.3224756056767,-0.763531646934156,
-9.65104166666665));
#420256=CARTESIAN_POINT('Ctrl Pts',(1.76330080756894,2.21669973093722E-15,
-9.60937499999998));
#420257=CARTESIAN_POINT('Ctrl Pts',(1.3224756056767,0.763531646934159,-9.56770833333331));
#420258=CARTESIAN_POINT('Ctrl Pts',(0.881650403784469,1.52706329386832,
-9.52604166666665));
#420259=CARTESIAN_POINT('Ctrl Pts',(0.,1.52706329386832,-9.48437499999998));
#420260=CARTESIAN_POINT('Ctrl Pts',(-0.881650403784468,1.52706329386832,
-9.44270833333331));
#420261=CARTESIAN_POINT('Ctrl Pts',(-1.3224756056767,0.76353164693416,-9.40104166666665));
#420262=CARTESIAN_POINT('Ctrl Pts',(-1.76330080756894,2.64858386892187E-15,
-9.35937499999998));
#420263=CARTESIAN_POINT('Ctrl Pts',(-1.3224756056767,-0.763531646934155,
-9.31770833333331));
#420264=CARTESIAN_POINT('Ctrl Pts',(-0.881650403784469,-1.52706329386831,
-9.27604166666665));
#420265=CARTESIAN_POINT('Ctrl Pts',(-1.87011317493125E-16,-1.52706329386831,
-9.23437499999998));
#420266=CARTESIAN_POINT('Ctrl Pts',(0.881650403784467,-1.52706329386831,
-9.19270833333332));
#420267=CARTESIAN_POINT('Ctrl Pts',(1.3224756056767,-0.763531646934156,
-9.15104166666665));
#420268=CARTESIAN_POINT('Ctrl Pts',(1.76330080756894,2.21669973093722E-15,
-9.10937499999998));
#420269=CARTESIAN_POINT('Ctrl Pts',(1.3224756056767,0.763531646934159,-9.06770833333331));
#420270=CARTESIAN_POINT('Ctrl Pts',(0.881650403784469,1.52706329386832,
-9.02604166666665));
#420271=CARTESIAN_POINT('Ctrl Pts',(0.,1.52706329386832,-8.98437499999998));
#420272=CARTESIAN_POINT('Ctrl Pts',(-0.881650403784468,1.52706329386832,
-8.94270833333331));
#420273=CARTESIAN_POINT('Ctrl Pts',(-1.3224756056767,0.76353164693416,-8.90104166666665));
#420274=CARTESIAN_POINT('Ctrl Pts',(-1.76330080756894,2.64858386892187E-15,
-8.85937499999998));
#420275=CARTESIAN_POINT('Ctrl Pts',(-1.3224756056767,-0.763531646934155,
-8.81770833333331));
#420276=CARTESIAN_POINT('Ctrl Pts',(-0.881650403784469,-1.52706329386831,
-8.77604166666665));
#420277=CARTESIAN_POINT('Ctrl Pts',(-1.87011317493125E-16,-1.52706329386831,
-8.73437499999998));
#420278=CARTESIAN_POINT('Ctrl Pts',(0.881650403784467,-1.52706329386831,
-8.69270833333331));
#420279=CARTESIAN_POINT('Ctrl Pts',(1.3224756056767,-0.763531646934156,
-8.65104166666665));
#420280=CARTESIAN_POINT('Ctrl Pts',(1.76330080756894,2.21669973093722E-15,
-8.60937499999998));
#420281=CARTESIAN_POINT('Ctrl Pts',(1.3224756056767,0.763531646934159,-8.56770833333331));
#420282=CARTESIAN_POINT('Ctrl Pts',(0.881650403784469,1.52706329386832,
-8.52604166666665));
#420283=CARTESIAN_POINT('Ctrl Pts',(0.,1.52706329386832,-8.48437499999998));
#420284=CARTESIAN_POINT('Ctrl Pts',(-0.881650403784468,1.52706329386832,
-8.44270833333332));
#420285=CARTESIAN_POINT('Ctrl Pts',(-1.3224756056767,0.76353164693416,-8.40104166666665));
#420286=CARTESIAN_POINT('Ctrl Pts',(-1.76330080756894,2.64858386892187E-15,
-8.35937499999998));
#420287=CARTESIAN_POINT('Ctrl Pts',(-1.3224756056767,-0.763531646934155,
-8.31770833333332));
#420288=CARTESIAN_POINT('Ctrl Pts',(-0.881650403784469,-1.52706329386831,
-8.27604166666665));
#420289=CARTESIAN_POINT('Ctrl Pts',(-1.87011317493125E-16,-1.52706329386831,
-8.23437499999998));
#420290=CARTESIAN_POINT('Ctrl Pts',(0.881650403784467,-1.52706329386831,
-8.19270833333332));
#420291=CARTESIAN_POINT('Ctrl Pts',(1.3224756056767,-0.763531646934156,
-8.15104166666665));
#420292=CARTESIAN_POINT('Ctrl Pts',(1.76330080756894,2.21669973093722E-15,
-8.10937499999998));
#420293=CARTESIAN_POINT('Ctrl Pts',(1.3224756056767,0.763531646934159,-8.06770833333332));
#420294=CARTESIAN_POINT('Ctrl Pts',(0.881650403784469,1.52706329386832,
-8.02604166666665));
#420295=CARTESIAN_POINT('Ctrl Pts',(0.,1.52706329386832,-7.98437499999998));
#420296=CARTESIAN_POINT('Ctrl Pts',(-0.881650403784468,1.52706329386832,
-7.94270833333332));
#420297=CARTESIAN_POINT('Ctrl Pts',(-1.3224756056767,0.76353164693416,-7.90104166666665));
#420298=CARTESIAN_POINT('Ctrl Pts',(-1.76330080756894,2.64858386892187E-15,
-7.85937499999998));
#420299=CARTESIAN_POINT('Ctrl Pts',(-1.3224756056767,-0.763531646934155,
-7.81770833333332));
#420300=CARTESIAN_POINT('Ctrl Pts',(-0.881650403784469,-1.52706329386831,
-7.77604166666665));
#420301=CARTESIAN_POINT('Ctrl Pts',(-1.87011317493125E-16,-1.52706329386831,
-7.73437499999998));
#420302=CARTESIAN_POINT('Ctrl Pts',(0.881650403784467,-1.52706329386831,
-7.69270833333331));
#420303=CARTESIAN_POINT('Ctrl Pts',(1.3224756056767,-0.763531646934156,
-7.65104166666665));
#420304=CARTESIAN_POINT('Ctrl Pts',(1.76330080756894,2.21669973093722E-15,
-7.60937499999998));
#420305=CARTESIAN_POINT('Ctrl Pts',(1.3224756056767,0.763531646934159,-7.56770833333332));
#420306=CARTESIAN_POINT('Ctrl Pts',(0.881650403784469,1.52706329386832,
-7.52604166666665));
#420307=CARTESIAN_POINT('Ctrl Pts',(0.,1.52706329386832,-7.48437499999998));
#420308=CARTESIAN_POINT('Ctrl Pts',(-0.881650403784468,1.52706329386832,
-7.44270833333332));
#420309=CARTESIAN_POINT('Ctrl Pts',(-1.3224756056767,0.76353164693416,-7.40104166666665));
#420310=CARTESIAN_POINT('Ctrl Pts',(-1.76330080756894,2.64858386892187E-15,
-7.35937499999998));
#420311=CARTESIAN_POINT('Ctrl Pts',(-1.3224756056767,-0.763531646934155,
-7.31770833333332));
#420312=CARTESIAN_POINT('Ctrl Pts',(-0.881650403784469,-1.52706329386831,
-7.27604166666665));
#420313=CARTESIAN_POINT('Ctrl Pts',(-1.87011317493125E-16,-1.52706329386831,
-7.23437499999998));
#420314=CARTESIAN_POINT('Ctrl Pts',(0.881650403784467,-1.52706329386831,
-7.19270833333332));
#420315=CARTESIAN_POINT('Ctrl Pts',(1.3224756056767,-0.763531646934156,
-7.15104166666665));
#420316=CARTESIAN_POINT('Ctrl Pts',(1.76330080756894,2.21669973093722E-15,
-7.10937499999998));
#420317=CARTESIAN_POINT('Ctrl Pts',(1.3224756056767,0.763531646934159,-7.06770833333331));
#420318=CARTESIAN_POINT('Ctrl Pts',(0.881650403784469,1.52706329386832,
-7.02604166666665));
#420319=CARTESIAN_POINT('Ctrl Pts',(0.,1.52706329386832,-6.98437499999998));
#420320=CARTESIAN_POINT('Ctrl Pts',(-0.881650403784468,1.52706329386832,
-6.94270833333332));
#420321=CARTESIAN_POINT('Ctrl Pts',(-1.3224756056767,0.76353164693416,-6.90104166666665));
#420322=CARTESIAN_POINT('Ctrl Pts',(-1.76330080756894,2.64858386892187E-15,
-6.85937499999998));
#420323=CARTESIAN_POINT('Ctrl Pts',(-1.3224756056767,-0.763531646934155,
-6.81770833333331));
#420324=CARTESIAN_POINT('Ctrl Pts',(-0.881650403784469,-1.52706329386831,
-6.77604166666665));
#420325=CARTESIAN_POINT('Ctrl Pts',(-1.87011317493125E-16,-1.52706329386831,
-6.73437499999998));
#420326=CARTESIAN_POINT('Ctrl Pts',(0.881650403784467,-1.52706329386831,
-6.69270833333332));
#420327=CARTESIAN_POINT('Ctrl Pts',(1.3224756056767,-0.763531646934156,
-6.65104166666665));
#420328=CARTESIAN_POINT('Ctrl Pts',(1.76330080756894,2.21669973093722E-15,
-6.60937499999998));
#420329=CARTESIAN_POINT('Ctrl Pts',(1.3224756056767,0.763531646934159,-6.56770833333332));
#420330=CARTESIAN_POINT('Ctrl Pts',(0.881650403784469,1.52706329386832,
-6.52604166666665));
#420331=CARTESIAN_POINT('Ctrl Pts',(0.,1.52706329386832,-6.48437499999998));
#420332=CARTESIAN_POINT('Ctrl Pts',(-0.881650403784468,1.52706329386832,
-6.44270833333332));
#420333=CARTESIAN_POINT('Ctrl Pts',(-1.3224756056767,0.76353164693416,-6.40104166666665));
#420334=CARTESIAN_POINT('Ctrl Pts',(-1.76330080756894,2.64858386892187E-15,
-6.35937499999998));
#420335=CARTESIAN_POINT('Ctrl Pts',(-1.3224756056767,-0.763531646934155,
-6.31770833333332));
#420336=CARTESIAN_POINT('Ctrl Pts',(-0.881650403784469,-1.52706329386831,
-6.27604166666665));
#420337=CARTESIAN_POINT('Ctrl Pts',(-1.87011317493125E-16,-1.52706329386831,
-6.23437499999998));
#420338=CARTESIAN_POINT('Ctrl Pts',(0.881650403784467,-1.52706329386831,
-6.19270833333332));
#420339=CARTESIAN_POINT('Ctrl Pts',(1.3224756056767,-0.763531646934156,
-6.15104166666665));
#420340=CARTESIAN_POINT('Ctrl Pts',(1.76330080756894,2.21669973093722E-15,
-6.10937499999998));
#420341=CARTESIAN_POINT('Ctrl Pts',(1.3224756056767,0.763531646934159,-6.06770833333332));
#420342=CARTESIAN_POINT('Ctrl Pts',(0.881650403784469,1.52706329386832,
-6.02604166666665));
#420343=CARTESIAN_POINT('Ctrl Pts',(0.,1.52706329386832,-5.98437499999998));
#420344=CARTESIAN_POINT('Ctrl Pts',(-0.881650403784468,1.52706329386832,
-5.94270833333331));
#420345=CARTESIAN_POINT('Ctrl Pts',(-1.3224756056767,0.76353164693416,-5.90104166666665));
#420346=CARTESIAN_POINT('Ctrl Pts',(-1.76330080756894,2.64858386892187E-15,
-5.85937499999998));
#420347=CARTESIAN_POINT('Ctrl Pts',(-1.3224756056767,-0.763531646934155,
-5.81770833333332));
#420348=CARTESIAN_POINT('Ctrl Pts',(-0.881650403784469,-1.52706329386831,
-5.77604166666665));
#420349=CARTESIAN_POINT('Ctrl Pts',(-1.87011317493125E-16,-1.52706329386831,
-5.73437499999998));
#420350=CARTESIAN_POINT('Ctrl Pts',(0.881650403784467,-1.52706329386831,
-5.69270833333332));
#420351=CARTESIAN_POINT('Ctrl Pts',(1.3224756056767,-0.763531646934156,
-5.65104166666665));
#420352=CARTESIAN_POINT('Ctrl Pts',(1.76330080756894,2.21669973093722E-15,
-5.60937499999998));
#420353=CARTESIAN_POINT('Ctrl Pts',(1.3224756056767,0.763531646934159,-5.56770833333332));
#420354=CARTESIAN_POINT('Ctrl Pts',(0.881650403784469,1.52706329386832,
-5.52604166666665));
#420355=CARTESIAN_POINT('Ctrl Pts',(0.,1.52706329386832,-5.48437499999998));
#420356=CARTESIAN_POINT('Ctrl Pts',(-0.881650403784468,1.52706329386832,
-5.44270833333332));
#420357=CARTESIAN_POINT('Ctrl Pts',(-1.3224756056767,0.76353164693416,-5.40104166666665));
#420358=CARTESIAN_POINT('Ctrl Pts',(-1.76330080756894,2.64858386892187E-15,
-5.35937499999998));
#420359=CARTESIAN_POINT('Ctrl Pts',(-1.3224756056767,-0.763531646934155,
-5.31770833333332));
#420360=CARTESIAN_POINT('Ctrl Pts',(-0.881650403784469,-1.52706329386831,
-5.27604166666665));
#420361=CARTESIAN_POINT('Ctrl Pts',(-1.87011317493125E-16,-1.52706329386831,
-5.23437499999998));
#420362=CARTESIAN_POINT('Ctrl Pts',(0.881650403784467,-1.52706329386831,
-5.19270833333331));
#420363=CARTESIAN_POINT('Ctrl Pts',(1.3224756056767,-0.763531646934156,
-5.15104166666665));
#420364=CARTESIAN_POINT('Ctrl Pts',(1.76330080756894,2.21669973093722E-15,
-5.10937499999998));
#420365=CARTESIAN_POINT('Ctrl Pts',(1.3224756056767,0.763531646934159,-5.06770833333332));
#420366=CARTESIAN_POINT('Ctrl Pts',(0.881650403784469,1.52706329386832,
-5.02604166666665));
#420367=CARTESIAN_POINT('Ctrl Pts',(0.,1.52706329386832,-4.98437499999998));
#420368=CARTESIAN_POINT('Ctrl Pts',(-0.881650403784468,1.52706329386832,
-4.94270833333331));
#420369=CARTESIAN_POINT('Ctrl Pts',(-1.3224756056767,0.76353164693416,-4.90104166666665));
#420370=CARTESIAN_POINT('Ctrl Pts',(-1.76330080756894,2.64858386892187E-15,
-4.85937499999998));
#420371=CARTESIAN_POINT('Ctrl Pts',(-1.3224756056767,-0.763531646934155,
-4.81770833333331));
#420372=CARTESIAN_POINT('Ctrl Pts',(-0.881650403784469,-1.52706329386831,
-4.77604166666665));
#420373=CARTESIAN_POINT('Ctrl Pts',(-1.87011317493125E-16,-1.52706329386831,
-4.73437499999998));
#420374=CARTESIAN_POINT('Ctrl Pts',(0.881650403784467,-1.52706329386831,
-4.69270833333331));
#420375=CARTESIAN_POINT('Ctrl Pts',(1.3224756056767,-0.763531646934156,
-4.65104166666665));
#420376=CARTESIAN_POINT('Ctrl Pts',(1.76330080756894,2.21669973093722E-15,
-4.60937499999998));
#420377=CARTESIAN_POINT('Ctrl Pts',(1.3224756056767,0.763531646934159,-4.56770833333331));
#420378=CARTESIAN_POINT('Ctrl Pts',(0.881650403784469,1.52706329386832,
-4.52604166666665));
#420379=CARTESIAN_POINT('Ctrl Pts',(0.,1.52706329386832,-4.48437499999998));
#420380=CARTESIAN_POINT('Ctrl Pts',(-0.881650403784468,1.52706329386832,
-4.44270833333331));
#420381=CARTESIAN_POINT('Ctrl Pts',(-1.3224756056767,0.76353164693416,-4.40104166666665));
#420382=CARTESIAN_POINT('Ctrl Pts',(-1.76330080756894,2.64858386892187E-15,
-4.35937499999998));
#420383=CARTESIAN_POINT('Ctrl Pts',(-1.3224756056767,-0.763531646934155,
-4.31770833333331));
#420384=CARTESIAN_POINT('Ctrl Pts',(-0.881650403784469,-1.52706329386831,
-4.27604166666665));
#420385=CARTESIAN_POINT('Ctrl Pts',(-1.87011317493125E-16,-1.52706329386831,
-4.23437499999998));
#420386=CARTESIAN_POINT('Ctrl Pts',(0.881650403784467,-1.52706329386831,
-4.19270833333332));
#420387=CARTESIAN_POINT('Ctrl Pts',(1.3224756056767,-0.763531646934156,
-4.15104166666665));
#420388=CARTESIAN_POINT('Ctrl Pts',(1.76330080756894,2.21669973093722E-15,
-4.10937499999998));
#420389=CARTESIAN_POINT('Ctrl Pts',(1.3224756056767,0.763531646934159,-4.06770833333332));
#420390=CARTESIAN_POINT('Ctrl Pts',(0.881650403784469,1.52706329386832,
-4.02604166666665));
#420391=CARTESIAN_POINT('Ctrl Pts',(0.,1.52706329386832,-3.98437499999998));
#420392=CARTESIAN_POINT('Ctrl Pts',(-0.881650403784468,1.52706329386832,
-3.94270833333332));
#420393=CARTESIAN_POINT('Ctrl Pts',(-1.3224756056767,0.76353164693416,-3.90104166666665));
#420394=CARTESIAN_POINT('Ctrl Pts',(-1.76330080756894,2.64858386892187E-15,
-3.85937499999998));
#420395=CARTESIAN_POINT('Ctrl Pts',(-1.3224756056767,-0.763531646934155,
-3.81770833333332));
#420396=CARTESIAN_POINT('Ctrl Pts',(-0.881650403784469,-1.52706329386831,
-3.77604166666665));
#420397=CARTESIAN_POINT('Ctrl Pts',(-1.87011317493125E-16,-1.52706329386831,
-3.73437499999998));
#420398=CARTESIAN_POINT('Ctrl Pts',(0.881650403784467,-1.52706329386831,
-3.69270833333332));
#420399=CARTESIAN_POINT('Ctrl Pts',(1.3224756056767,-0.763531646934156,
-3.65104166666665));
#420400=CARTESIAN_POINT('Ctrl Pts',(1.76330080756894,2.21669973093722E-15,
-3.60937499999998));
#420401=CARTESIAN_POINT('Ctrl Pts',(1.3224756056767,0.763531646934159,-3.56770833333332));
#420402=CARTESIAN_POINT('Ctrl Pts',(0.881650403784469,1.52706329386832,
-3.52604166666665));
#420403=CARTESIAN_POINT('Ctrl Pts',(0.,1.52706329386832,-3.48437499999998));
#420404=CARTESIAN_POINT('Ctrl Pts',(-0.881650403784468,1.52706329386832,
-3.44270833333332));
#420405=CARTESIAN_POINT('Ctrl Pts',(-1.3224756056767,0.76353164693416,-3.40104166666665));
#420406=CARTESIAN_POINT('Ctrl Pts',(-1.76330080756894,2.64858386892187E-15,
-3.35937499999998));
#420407=CARTESIAN_POINT('Ctrl Pts',(-1.3224756056767,-0.763531646934155,
-3.31770833333332));
#420408=CARTESIAN_POINT('Ctrl Pts',(-0.881650403784469,-1.52706329386831,
-3.27604166666665));
#420409=CARTESIAN_POINT('Ctrl Pts',(-1.87011317493125E-16,-1.52706329386831,
-3.23437499999998));
#420410=CARTESIAN_POINT('Ctrl Pts',(0.881650403784467,-1.52706329386831,
-3.19270833333331));
#420411=CARTESIAN_POINT('Ctrl Pts',(1.3224756056767,-0.763531646934156,
-3.15104166666665));
#420412=CARTESIAN_POINT('Ctrl Pts',(1.76330080756894,2.21669973093722E-15,
-3.10937499999998));
#420413=CARTESIAN_POINT('Ctrl Pts',(1.3224756056767,0.763531646934159,-3.06770833333331));
#420414=CARTESIAN_POINT('Ctrl Pts',(0.881650403784469,1.52706329386832,
-3.02604166666665));
#420415=CARTESIAN_POINT('Ctrl Pts',(0.,1.52706329386832,-2.98437499999998));
#420416=CARTESIAN_POINT('Ctrl Pts',(-0.881650403784468,1.52706329386832,
-2.94270833333331));
#420417=CARTESIAN_POINT('Ctrl Pts',(-1.3224756056767,0.76353164693416,-2.90104166666665));
#420418=CARTESIAN_POINT('Ctrl Pts',(-1.76330080756894,2.64858386892187E-15,
-2.85937499999998));
#420419=CARTESIAN_POINT('Ctrl Pts',(-1.3224756056767,-0.763531646934155,
-2.81770833333331));
#420420=CARTESIAN_POINT('Ctrl Pts',(-0.881650403784469,-1.52706329386831,
-2.77604166666665));
#420421=CARTESIAN_POINT('Ctrl Pts',(-1.87011317493125E-16,-1.52706329386831,
-2.73437499999998));
#420422=CARTESIAN_POINT('Ctrl Pts',(0.881650403784467,-1.52706329386831,
-2.69270833333331));
#420423=CARTESIAN_POINT('Ctrl Pts',(1.3224756056767,-0.763531646934156,
-2.65104166666665));
#420424=CARTESIAN_POINT('Ctrl Pts',(1.76330080756894,2.21669973093722E-15,
-2.60937499999998));
#420425=CARTESIAN_POINT('Ctrl Pts',(1.3224756056767,0.763531646934159,-2.56770833333331));
#420426=CARTESIAN_POINT('Ctrl Pts',(0.881650403784469,1.52706329386832,
-2.52604166666665));
#420427=CARTESIAN_POINT('Ctrl Pts',(0.,1.52706329386832,-2.48437499999998));
#420428=CARTESIAN_POINT('Ctrl Pts',(-0.881650403784468,1.52706329386832,
-2.44270833333331));
#420429=CARTESIAN_POINT('Ctrl Pts',(-1.3224756056767,0.76353164693416,-2.40104166666665));
#420430=CARTESIAN_POINT('Ctrl Pts',(-1.76330080756894,2.64858386892187E-15,
-2.35937499999998));
#420431=CARTESIAN_POINT('Ctrl Pts',(-1.3224756056767,-0.763531646934155,
-2.31770833333332));
#420432=CARTESIAN_POINT('Ctrl Pts',(-0.881650403784469,-1.52706329386831,
-2.27604166666665));
#420433=CARTESIAN_POINT('Ctrl Pts',(-1.87011317493125E-16,-1.52706329386831,
-2.23437499999998));
#420434=CARTESIAN_POINT('Ctrl Pts',(0.881650403784467,-1.52706329386831,
-2.19270833333332));
#420435=CARTESIAN_POINT('Ctrl Pts',(1.3224756056767,-0.763531646934156,
-2.15104166666665));
#420436=CARTESIAN_POINT('Ctrl Pts',(1.76330080756894,2.21669973093722E-15,
-2.10937499999998));
#420437=CARTESIAN_POINT('Ctrl Pts',(1.3224756056767,0.763531646934159,-2.06770833333332));
#420438=CARTESIAN_POINT('Ctrl Pts',(0.881650403784469,1.52706329386832,
-2.02604166666665));
#420439=CARTESIAN_POINT('Ctrl Pts',(0.,1.52706329386832,-1.98437499999998));
#420440=CARTESIAN_POINT('Ctrl Pts',(-0.881650403784468,1.52706329386832,
-1.94270833333332));
#420441=CARTESIAN_POINT('Ctrl Pts',(-1.3224756056767,0.76353164693416,-1.90104166666665));
#420442=CARTESIAN_POINT('Ctrl Pts',(-1.76330080756894,2.64858386892187E-15,
-1.85937499999998));
#420443=CARTESIAN_POINT('Ctrl Pts',(-1.3224756056767,-0.763531646934155,
-1.81770833333332));
#420444=CARTESIAN_POINT('Ctrl Pts',(-0.881650403784469,-1.52706329386831,
-1.77604166666665));
#420445=CARTESIAN_POINT('Ctrl Pts',(-1.87011317493125E-16,-1.52706329386831,
-1.73437499999998));
#420446=CARTESIAN_POINT('Ctrl Pts',(0.881650403784467,-1.52706329386831,
-1.69270833333332));
#420447=CARTESIAN_POINT('Ctrl Pts',(1.3224756056767,-0.763531646934156,
-1.65104166666665));
#420448=CARTESIAN_POINT('Ctrl Pts',(1.76330080756894,2.21669973093722E-15,
-1.60937499999998));
#420449=CARTESIAN_POINT('Ctrl Pts',(1.3224756056767,0.763531646934159,-1.56770833333332));
#420450=CARTESIAN_POINT('Ctrl Pts',(0.881650403784469,1.52706329386832,
-1.52604166666665));
#420451=CARTESIAN_POINT('Ctrl Pts',(0.,1.52706329386832,-1.48437499999998));
#420452=CARTESIAN_POINT('Ctrl Pts',(-0.881650403784468,1.52706329386832,
-1.44270833333332));
#420453=CARTESIAN_POINT('Ctrl Pts',(-1.3224756056767,0.76353164693416,-1.40104166666665));
#420454=CARTESIAN_POINT('Ctrl Pts',(-1.76330080756894,2.64858386892187E-15,
-1.35937499999998));
#420455=CARTESIAN_POINT('Ctrl Pts',(-1.3224756056767,-0.763531646934155,
-1.31770833333331));
#420456=CARTESIAN_POINT('Ctrl Pts',(-0.881650403784469,-1.52706329386831,
-1.27604166666665));
#420457=CARTESIAN_POINT('Ctrl Pts',(-1.87011317493125E-16,-1.52706329386831,
-1.23437499999998));
#420458=CARTESIAN_POINT('Ctrl Pts',(0.881650403784467,-1.52706329386831,
-1.19270833333331));
#420459=CARTESIAN_POINT('Ctrl Pts',(1.3224756056767,-0.763531646934156,
-1.15104166666665));
#420460=CARTESIAN_POINT('Ctrl Pts',(1.76330080756894,2.21669973093722E-15,
-1.10937499999998));
#420461=CARTESIAN_POINT('Ctrl Pts',(1.3224756056767,0.763531646934159,-1.06770833333331));
#420462=CARTESIAN_POINT('Ctrl Pts',(0.881650403784469,1.52706329386832,
-1.02604166666665));
#420463=CARTESIAN_POINT('Ctrl Pts',(0.,1.52706329386832,-0.984374999999982));
#420464=CARTESIAN_POINT('Ctrl Pts',(-0.881650403784468,1.52706329386832,
-0.942708333333315));
#420465=CARTESIAN_POINT('Ctrl Pts',(-1.3224756056767,0.76353164693416,-0.901041666666649));
#420466=CARTESIAN_POINT('Ctrl Pts',(-1.76330080756894,2.64858386892187E-15,
-0.859374999999982));
#420467=CARTESIAN_POINT('Ctrl Pts',(-1.3224756056767,-0.763531646934155,
-0.817708333333314));
#420468=CARTESIAN_POINT('Ctrl Pts',(-0.881650403784469,-1.52706329386831,
-0.776041666666649));
#420469=CARTESIAN_POINT('Ctrl Pts',(-1.87011317493125E-16,-1.52706329386831,
-0.734374999999982));
#420470=CARTESIAN_POINT('Ctrl Pts',(0.881650403784467,-1.52706329386831,
-0.692708333333314));
#420471=CARTESIAN_POINT('Ctrl Pts',(1.3224756056767,-0.763531646934156,
-0.651041666666649));
#420472=CARTESIAN_POINT('Ctrl Pts',(1.76330080756894,2.21669973093722E-15,
-0.609374999999982));
#420473=CARTESIAN_POINT('Ctrl Pts',(1.3224756056767,0.763531646934159,-0.567708333333314));
#420474=CARTESIAN_POINT('Ctrl Pts',(0.881650403784469,1.52706329386832,
-0.526041666666649));
#420475=CARTESIAN_POINT('Ctrl Pts',(0.,1.52706329386832,-0.484374999999981));
#420476=CARTESIAN_POINT('Ctrl Pts',(-0.881650403784468,1.52706329386832,
-0.442708333333316));
#420477=CARTESIAN_POINT('Ctrl Pts',(-1.3224756056767,0.76353164693416,-0.401041666666649));
#420478=CARTESIAN_POINT('Ctrl Pts',(-1.76330080756894,2.64858386892187E-15,
-0.359374999999981));
#420479=CARTESIAN_POINT('Ctrl Pts',(-1.3224756056767,-0.763531646934155,
-0.317708333333316));
#420480=CARTESIAN_POINT('Ctrl Pts',(-0.881650403784469,-1.52706329386831,
-0.276041666666648));
#420481=CARTESIAN_POINT('Ctrl Pts',(-1.87011317493125E-16,-1.52706329386831,
-0.234374999999981));
#420482=CARTESIAN_POINT('Ctrl Pts',(0.881650403784467,-1.52706329386831,
-0.192708333333316));
#420483=CARTESIAN_POINT('Ctrl Pts',(1.3224756056767,-0.763531646934156,
-0.151041666666648));
#420484=CARTESIAN_POINT('Ctrl Pts',(1.76330080756894,2.21669973093722E-15,
-0.109374999999981));
#420485=CARTESIAN_POINT('Ctrl Pts',(1.3224756056767,0.763531646934159,-0.0677083333333155));
#420486=CARTESIAN_POINT('Ctrl Pts',(0.881650403784469,1.52706329386832,
-0.0260416666666482));
#420487=CARTESIAN_POINT('Ctrl Pts',(0.,1.52706329386832,0.0156250000000191));
#420488=CARTESIAN_POINT('Ctrl Pts',(-0.881650403784468,1.52706329386832,
0.0572916666666846));
#420489=CARTESIAN_POINT('Ctrl Pts',(-1.3224756056767,0.76353164693416,0.0989583333333519));
#420490=CARTESIAN_POINT('Ctrl Pts',(-1.76330080756894,2.64858386892187E-15,
0.140625000000017));
#420491=CARTESIAN_POINT('Ctrl Pts',(-1.3224756056767,-0.763531646934155,
0.182291666666685));
#420492=CARTESIAN_POINT('Ctrl Pts',(-0.881650403784469,-1.52706329386831,
0.223958333333352));
#420493=CARTESIAN_POINT('Ctrl Pts',(-1.87011317493125E-16,-1.52706329386831,
0.265625000000018));
#420494=CARTESIAN_POINT('Ctrl Pts',(0.881650403784467,-1.52706329386831,
0.307291666666685));
#420495=CARTESIAN_POINT('Ctrl Pts',(1.3224756056767,-0.763531646934156,
0.348958333333352));
#420496=CARTESIAN_POINT('Ctrl Pts',(1.76330080756894,2.21669973093722E-15,
0.390625000000018));
#420497=CARTESIAN_POINT('Ctrl Pts',(1.3224756056767,0.763531646934159,0.432291666666685));
#420498=CARTESIAN_POINT('Ctrl Pts',(0.881650403784469,1.52706329386832,
0.473958333333352));
#420499=CARTESIAN_POINT('Ctrl Pts',(0.,1.52706329386832,0.515625000000018));
#420500=CARTESIAN_POINT('Ctrl Pts',(-0.881650403784468,1.52706329386832,
0.557291666666685));
#420501=CARTESIAN_POINT('Ctrl Pts',(-1.3224756056767,0.76353164693416,0.598958333333352));
#420502=CARTESIAN_POINT('Ctrl Pts',(-1.76330080756894,2.64858386892187E-15,
0.640625000000018));
#420503=CARTESIAN_POINT('Ctrl Pts',(-1.3224756056767,-0.763531646934155,
0.682291666666685));
#420504=CARTESIAN_POINT('Ctrl Pts',(-0.881650403784469,-1.52706329386831,
0.723958333333353));
#420505=CARTESIAN_POINT('Ctrl Pts',(-1.87011317493125E-16,-1.52706329386831,
0.765625000000018));
#420506=CARTESIAN_POINT('Ctrl Pts',(0.881650403784467,-1.52706329386831,
0.807291666666685));
#420507=CARTESIAN_POINT('Ctrl Pts',(1.3224756056767,-0.763531646934156,
0.848958333333351));
#420508=CARTESIAN_POINT('Ctrl Pts',(1.76330080756894,2.21669973093722E-15,
0.890625000000018));
#420509=CARTESIAN_POINT('Ctrl Pts',(1.3224756056767,0.763531646934159,0.932291666666685));
#420510=CARTESIAN_POINT('Ctrl Pts',(0.881650403784469,1.52706329386832,
0.973958333333351));
#420511=CARTESIAN_POINT('Ctrl Pts',(0.,1.52706329386832,1.01562500000002));
#420512=CARTESIAN_POINT('Ctrl Pts',(-0.881650403784468,1.52706329386832,
1.05729166666669));
#420513=CARTESIAN_POINT('Ctrl Pts',(-1.3224756056767,0.76353164693416,1.09895833333335));
#420514=CARTESIAN_POINT('Ctrl Pts',(-1.76330080756894,2.64858386892187E-15,
1.14062500000002));
#420515=CARTESIAN_POINT('Ctrl Pts',(-1.3224756056767,-0.763531646934155,
1.18229166666669));
#420516=CARTESIAN_POINT('Ctrl Pts',(-0.881650403784469,-1.52706329386831,
1.22395833333335));
#420517=CARTESIAN_POINT('Ctrl Pts',(-1.87011317493125E-16,-1.52706329386831,
1.26562500000002));
#420518=CARTESIAN_POINT('Ctrl Pts',(0.881650403784467,-1.52706329386831,
1.30729166666669));
#420519=CARTESIAN_POINT('Ctrl Pts',(1.3224756056767,-0.763531646934156,
1.34895833333335));
#420520=CARTESIAN_POINT('Ctrl Pts',(1.76330080756894,2.21669973093722E-15,
1.39062500000002));
#420521=CARTESIAN_POINT('Ctrl Pts',(1.3224756056767,0.763531646934159,1.43229166666668));
#420522=CARTESIAN_POINT('Ctrl Pts',(0.881650403784469,1.52706329386832,
1.47395833333335));
#420523=CARTESIAN_POINT('Ctrl Pts',(0.,1.52706329386832,1.51562500000002));
#420524=CARTESIAN_POINT('Ctrl Pts',(-0.881650403784468,1.52706329386832,
1.55729166666668));
#420525=CARTESIAN_POINT('Ctrl Pts',(-1.3224756056767,0.76353164693416,1.59895833333335));
#420526=CARTESIAN_POINT('Ctrl Pts',(-1.76330080756894,2.64858386892187E-15,
1.64062500000002));
#420527=CARTESIAN_POINT('Ctrl Pts',(-1.3224756056767,-0.763531646934155,
1.68229166666668));
#420528=CARTESIAN_POINT('Ctrl Pts',(-0.881650403784469,-1.52706329386831,
1.72395833333335));
#420529=CARTESIAN_POINT('Ctrl Pts',(-1.87011317493125E-16,-1.52706329386831,
1.76562500000002));
#420530=CARTESIAN_POINT('Ctrl Pts',(0.881650403784467,-1.52706329386831,
1.80729166666668));
#420531=CARTESIAN_POINT('Ctrl Pts',(1.3224756056767,-0.763531646934156,
1.84895833333335));
#420532=CARTESIAN_POINT('Ctrl Pts',(1.76330080756894,2.21669973093722E-15,
1.89062500000002));
#420533=CARTESIAN_POINT('Ctrl Pts',(1.3224756056767,0.763531646934159,1.93229166666668));
#420534=CARTESIAN_POINT('Ctrl Pts',(0.881650403784469,1.52706329386832,
1.97395833333335));
#420535=CARTESIAN_POINT('Ctrl Pts',(0.,1.52706329386832,2.01562500000002));
#420536=CARTESIAN_POINT('Ctrl Pts',(-0.881650403784468,1.52706329386832,
2.05729166666668));
#420537=CARTESIAN_POINT('Ctrl Pts',(-1.3224756056767,0.76353164693416,2.09895833333335));
#420538=CARTESIAN_POINT('Ctrl Pts',(-1.76330080756894,2.64858386892187E-15,
2.14062500000002));
#420539=CARTESIAN_POINT('Ctrl Pts',(-1.3224756056767,-0.763531646934155,
2.18229166666668));
#420540=CARTESIAN_POINT('Ctrl Pts',(-0.881650403784469,-1.52706329386831,
2.22395833333335));
#420541=CARTESIAN_POINT('Ctrl Pts',(-1.87011317493125E-16,-1.52706329386831,
2.26562500000002));
#420542=CARTESIAN_POINT('Ctrl Pts',(0.881650403784467,-1.52706329386831,
2.30729166666669));
#420543=CARTESIAN_POINT('Ctrl Pts',(1.3224756056767,-0.763531646934156,
2.34895833333335));
#420544=CARTESIAN_POINT('Ctrl Pts',(1.76330080756894,2.21669973093722E-15,
2.39062500000002));
#420545=CARTESIAN_POINT('Ctrl Pts',(1.3224756056767,0.763531646934159,2.43229166666669));
#420546=CARTESIAN_POINT('Ctrl Pts',(0.881650403784469,1.52706329386832,
2.47395833333335));
#420547=CARTESIAN_POINT('Ctrl Pts',(0.,1.52706329386832,2.51562500000002));
#420548=CARTESIAN_POINT('Ctrl Pts',(-0.881650403784468,1.52706329386832,
2.55729166666669));
#420549=CARTESIAN_POINT('Ctrl Pts',(-1.3224756056767,0.76353164693416,2.59895833333335));
#420550=CARTESIAN_POINT('Ctrl Pts',(-1.76330080756894,2.64858386892187E-15,
2.64062500000002));
#420551=CARTESIAN_POINT('Ctrl Pts',(-1.3224756056767,-0.763531646934155,
2.68229166666669));
#420552=CARTESIAN_POINT('Ctrl Pts',(-0.881650403784469,-1.52706329386831,
2.72395833333335));
#420553=CARTESIAN_POINT('Ctrl Pts',(-1.87011317493125E-16,-1.52706329386831,
2.76562500000002));
#420554=CARTESIAN_POINT('Ctrl Pts',(0.881650403784467,-1.52706329386831,
2.80729166666669));
#420555=CARTESIAN_POINT('Ctrl Pts',(1.3224756056767,-0.763531646934156,
2.84895833333335));
#420556=CARTESIAN_POINT('Ctrl Pts',(1.76330080756894,2.21669973093722E-15,
2.89062500000002));
#420557=CARTESIAN_POINT('Ctrl Pts',(1.3224756056767,0.763531646934159,2.93229166666669));
#420558=CARTESIAN_POINT('Ctrl Pts',(0.881650403784469,1.52706329386832,
2.97395833333335));
#420559=CARTESIAN_POINT('Ctrl Pts',(0.,1.52706329386832,3.01562500000002));
#420560=CARTESIAN_POINT('Ctrl Pts',(-0.881650403784468,1.52706329386832,
3.05729166666669));
#420561=CARTESIAN_POINT('Ctrl Pts',(-1.3224756056767,0.76353164693416,3.09895833333335));
#420562=CARTESIAN_POINT('Ctrl Pts',(-1.76330080756894,2.64858386892187E-15,
3.14062500000002));
#420563=CARTESIAN_POINT('Ctrl Pts',(-1.3224756056767,-0.763531646934155,
3.18229166666669));
#420564=CARTESIAN_POINT('Ctrl Pts',(-0.881650403784469,-1.52706329386831,
3.22395833333335));
#420565=CARTESIAN_POINT('Ctrl Pts',(-1.87011317493125E-16,-1.52706329386831,
3.26562500000002));
#420566=CARTESIAN_POINT('Ctrl Pts',(0.881650403784467,-1.52706329386831,
3.30729166666669));
#420567=CARTESIAN_POINT('Ctrl Pts',(1.3224756056767,-0.763531646934156,
3.34895833333335));
#420568=CARTESIAN_POINT('Ctrl Pts',(1.76330080756894,2.21669973093722E-15,
3.39062500000002));
#420569=CARTESIAN_POINT('Ctrl Pts',(1.3224756056767,0.763531646934159,3.43229166666669));
#420570=CARTESIAN_POINT('Ctrl Pts',(0.881650403784469,1.52706329386832,
3.47395833333335));
#420571=CARTESIAN_POINT('Ctrl Pts',(0.,1.52706329386832,3.51562500000002));
#420572=CARTESIAN_POINT('Ctrl Pts',(-0.881650403784468,1.52706329386832,
3.55729166666669));
#420573=CARTESIAN_POINT('Ctrl Pts',(-1.3224756056767,0.76353164693416,3.59895833333335));
#420574=CARTESIAN_POINT('Ctrl Pts',(-1.76330080756894,2.64858386892187E-15,
3.64062500000002));
#420575=CARTESIAN_POINT('Ctrl Pts',(-1.3224756056767,-0.763531646934155,
3.68229166666669));
#420576=CARTESIAN_POINT('Ctrl Pts',(-0.881650403784469,-1.52706329386831,
3.72395833333335));
#420577=CARTESIAN_POINT('Ctrl Pts',(-1.87011317493125E-16,-1.52706329386831,
3.76562500000002));
#420578=CARTESIAN_POINT('Ctrl Pts',(0.881650403784467,-1.52706329386831,
3.80729166666669));
#420579=CARTESIAN_POINT('Ctrl Pts',(1.3224756056767,-0.763531646934156,
3.84895833333335));
#420580=CARTESIAN_POINT('Ctrl Pts',(1.76330080756894,2.21669973093722E-15,
3.89062500000002));
#420581=CARTESIAN_POINT('Ctrl Pts',(1.3224756056767,0.763531646934159,3.93229166666669));
#420582=CARTESIAN_POINT('Ctrl Pts',(0.881650403784469,1.52706329386832,
3.97395833333335));
#420583=CARTESIAN_POINT('Ctrl Pts',(0.,1.52706329386832,4.01562500000002));
#420584=CARTESIAN_POINT('Ctrl Pts',(-0.881650403784468,1.52706329386832,
4.05729166666669));
#420585=CARTESIAN_POINT('Ctrl Pts',(-1.3224756056767,0.76353164693416,4.09895833333335));
#420586=CARTESIAN_POINT('Ctrl Pts',(-1.76330080756894,2.64858386892187E-15,
4.14062500000002));
#420587=CARTESIAN_POINT('Ctrl Pts',(-1.3224756056767,-0.763531646934155,
4.18229166666669));
#420588=CARTESIAN_POINT('Ctrl Pts',(-0.881650403784469,-1.52706329386831,
4.22395833333335));
#420589=CARTESIAN_POINT('Ctrl Pts',(-1.87011317493125E-16,-1.52706329386831,
4.26562500000002));
#420590=CARTESIAN_POINT('Ctrl Pts',(0.881650403784467,-1.52706329386831,
4.30729166666668));
#420591=CARTESIAN_POINT('Ctrl Pts',(1.3224756056767,-0.763531646934156,
4.34895833333335));
#420592=CARTESIAN_POINT('Ctrl Pts',(1.76330080756894,2.21669973093722E-15,
4.39062500000002));
#420593=CARTESIAN_POINT('Ctrl Pts',(1.3224756056767,0.763531646934159,4.43229166666668));
#420594=CARTESIAN_POINT('Ctrl Pts',(0.881650403784469,1.52706329386832,
4.47395833333335));
#420595=CARTESIAN_POINT('Ctrl Pts',(0.,1.52706329386832,4.51562500000002));
#420596=CARTESIAN_POINT('Ctrl Pts',(-0.881650403784468,1.52706329386832,
4.55729166666668));
#420597=CARTESIAN_POINT('Ctrl Pts',(-1.3224756056767,0.76353164693416,4.59895833333335));
#420598=CARTESIAN_POINT('Ctrl Pts',(-1.76330080756894,2.64858386892187E-15,
4.64062500000002));
#420599=CARTESIAN_POINT('Ctrl Pts',(-1.3224756056767,-0.763531646934155,
4.68229166666668));
#420600=CARTESIAN_POINT('Ctrl Pts',(-0.881650403784469,-1.52706329386831,
4.72395833333335));
#420601=CARTESIAN_POINT('Ctrl Pts',(-1.87011317493125E-16,-1.52706329386831,
4.76562500000002));
#420602=CARTESIAN_POINT('Ctrl Pts',(0.881650403784467,-1.52706329386831,
4.80729166666668));
#420603=CARTESIAN_POINT('Ctrl Pts',(1.3224756056767,-0.763531646934156,
4.84895833333335));
#420604=CARTESIAN_POINT('Ctrl Pts',(1.76330080756894,2.21669973093722E-15,
4.89062500000002));
#420605=CARTESIAN_POINT('Ctrl Pts',(1.3224756056767,0.763531646934159,4.93229166666668));
#420606=CARTESIAN_POINT('Ctrl Pts',(0.881650403784469,1.52706329386832,
4.97395833333335));
#420607=CARTESIAN_POINT('Ctrl Pts',(0.,1.52706329386832,5.01562500000002));
#420608=CARTESIAN_POINT('Ctrl Pts',(-0.881650403784468,1.52706329386832,
5.05729166666668));
#420609=CARTESIAN_POINT('Ctrl Pts',(-1.3224756056767,0.76353164693416,5.09895833333335));
#420610=CARTESIAN_POINT('Ctrl Pts',(-1.76330080756894,2.64858386892187E-15,
5.14062500000002));
#420611=CARTESIAN_POINT('Ctrl Pts',(-1.3224756056767,-0.763531646934155,
5.18229166666668));
#420612=CARTESIAN_POINT('Ctrl Pts',(-0.881650403784469,-1.52706329386831,
5.22395833333335));
#420613=CARTESIAN_POINT('Ctrl Pts',(-1.87011317493125E-16,-1.52706329386831,
5.26562500000002));
#420614=CARTESIAN_POINT('Ctrl Pts',(0.881650403784467,-1.52706329386831,
5.30729166666668));
#420615=CARTESIAN_POINT('Ctrl Pts',(1.3224756056767,-0.763531646934156,
5.34895833333335));
#420616=CARTESIAN_POINT('Ctrl Pts',(1.76330080756894,2.21669973093722E-15,
5.39062500000002));
#420617=CARTESIAN_POINT('Ctrl Pts',(1.3224756056767,0.763531646934159,5.43229166666668));
#420618=CARTESIAN_POINT('Ctrl Pts',(0.881650403784469,1.52706329386832,
5.47395833333335));
#420619=CARTESIAN_POINT('Ctrl Pts',(0.,1.52706329386832,5.51562500000002));
#420620=CARTESIAN_POINT('Ctrl Pts',(-0.881650403784468,1.52706329386832,
5.55729166666668));
#420621=CARTESIAN_POINT('Ctrl Pts',(-1.3224756056767,0.76353164693416,5.59895833333335));
#420622=CARTESIAN_POINT('Ctrl Pts',(-1.76330080756894,2.64858386892187E-15,
5.64062500000002));
#420623=CARTESIAN_POINT('Ctrl Pts',(-1.3224756056767,-0.763531646934155,
5.68229166666668));
#420624=CARTESIAN_POINT('Ctrl Pts',(-0.881650403784469,-1.52706329386831,
5.72395833333335));
#420625=CARTESIAN_POINT('Ctrl Pts',(-1.87011317493125E-16,-1.52706329386831,
5.76562500000002));
#420626=CARTESIAN_POINT('Ctrl Pts',(0.881650403784467,-1.52706329386831,
5.80729166666669));
#420627=CARTESIAN_POINT('Ctrl Pts',(1.3224756056767,-0.763531646934156,
5.84895833333335));
#420628=CARTESIAN_POINT('Ctrl Pts',(1.76330080756894,2.21669973093722E-15,
5.89062500000002));
#420629=CARTESIAN_POINT('Ctrl Pts',(1.3224756056767,0.763531646934159,5.93229166666668));
#420630=CARTESIAN_POINT('Ctrl Pts',(0.881650403784469,1.52706329386832,
5.97395833333335));
#420631=CARTESIAN_POINT('Ctrl Pts',(0.,1.52706329386832,6.01562500000002));
#420632=CARTESIAN_POINT('Ctrl Pts',(-0.881650403784468,1.52706329386832,
6.05729166666669));
#420633=CARTESIAN_POINT('Ctrl Pts',(-1.3224756056767,0.76353164693416,6.09895833333335));
#420634=CARTESIAN_POINT('Ctrl Pts',(-1.76330080756894,2.64858386892187E-15,
6.14062500000002));
#420635=CARTESIAN_POINT('Ctrl Pts',(-1.3224756056767,-0.763531646934155,
6.18229166666668));
#420636=CARTESIAN_POINT('Ctrl Pts',(-0.881650403784469,-1.52706329386831,
6.22395833333335));
#420637=CARTESIAN_POINT('Ctrl Pts',(-1.87011317493125E-16,-1.52706329386831,
6.26562500000002));
#420638=CARTESIAN_POINT('Ctrl Pts',(0.881650403784467,-1.52706329386831,
6.30729166666669));
#420639=CARTESIAN_POINT('Ctrl Pts',(1.3224756056767,-0.763531646934156,
6.34895833333335));
#420640=CARTESIAN_POINT('Ctrl Pts',(1.76330080756894,2.21669973093722E-15,
6.39062500000002));
#420641=CARTESIAN_POINT('Ctrl Pts',(1.3224756056767,0.763531646934159,6.43229166666669));
#420642=CARTESIAN_POINT('Ctrl Pts',(0.881650403784469,1.52706329386832,
6.47395833333335));
#420643=CARTESIAN_POINT('Ctrl Pts',(0.,1.52706329386832,6.51562500000002));
#420644=CARTESIAN_POINT('Ctrl Pts',(-0.881650403784468,1.52706329386832,
6.55729166666668));
#420645=CARTESIAN_POINT('Ctrl Pts',(-1.3224756056767,0.76353164693416,6.59895833333335));
#420646=CARTESIAN_POINT('Ctrl Pts',(-1.76330080756894,2.64858386892187E-15,
6.64062500000002));
#420647=CARTESIAN_POINT('Ctrl Pts',(-1.3224756056767,-0.763531646934155,
6.68229166666669));
#420648=CARTESIAN_POINT('Ctrl Pts',(-0.881650403784469,-1.52706329386831,
6.72395833333335));
#420649=CARTESIAN_POINT('Ctrl Pts',(-1.87011317493125E-16,-1.52706329386831,
6.76562500000002));
#420650=CARTESIAN_POINT('Ctrl Pts',(0.881650403784467,-1.52706329386831,
6.80729166666669));
#420651=CARTESIAN_POINT('Ctrl Pts',(1.3224756056767,-0.763531646934156,
6.84895833333335));
#420652=CARTESIAN_POINT('Ctrl Pts',(1.76330080756894,2.21669973093722E-15,
6.89062500000002));
#420653=CARTESIAN_POINT('Ctrl Pts',(1.3224756056767,0.763531646934159,6.93229166666669));
#420654=CARTESIAN_POINT('Ctrl Pts',(0.881650403784469,1.52706329386832,
6.97395833333335));
#420655=CARTESIAN_POINT('Ctrl Pts',(0.,1.52706329386832,7.01562500000002));
#420656=CARTESIAN_POINT('Ctrl Pts',(-0.881650403784468,1.52706329386832,
7.05729166666669));
#420657=CARTESIAN_POINT('Ctrl Pts',(-1.3224756056767,0.76353164693416,7.09895833333335));
#420658=CARTESIAN_POINT('Ctrl Pts',(-1.76330080756894,2.64858386892187E-15,
7.14062500000002));
#420659=CARTESIAN_POINT('Ctrl Pts',(-1.3224756056767,-0.763531646934155,
7.18229166666669));
#420660=CARTESIAN_POINT('Ctrl Pts',(-0.881650403784469,-1.52706329386831,
7.22395833333335));
#420661=CARTESIAN_POINT('Ctrl Pts',(-1.87011317493125E-16,-1.52706329386831,
7.26562500000002));
#420662=CARTESIAN_POINT('Ctrl Pts',(0.881650403784467,-1.52706329386831,
7.30729166666669));
#420663=CARTESIAN_POINT('Ctrl Pts',(1.3224756056767,-0.763531646934156,
7.34895833333335));
#420664=CARTESIAN_POINT('Ctrl Pts',(1.76330080756894,2.21669973093722E-15,
7.39062500000002));
#420665=CARTESIAN_POINT('Ctrl Pts',(1.3224756056767,0.763531646934159,7.43229166666669));
#420666=CARTESIAN_POINT('Ctrl Pts',(0.881650403784469,1.52706329386832,
7.47395833333335));
#420667=CARTESIAN_POINT('Ctrl Pts',(0.,1.52706329386832,7.51562500000002));
#420668=CARTESIAN_POINT('Ctrl Pts',(-0.881650403784468,1.52706329386832,
7.55729166666669));
#420669=CARTESIAN_POINT('Ctrl Pts',(-1.3224756056767,0.76353164693416,7.59895833333335));
#420670=CARTESIAN_POINT('Ctrl Pts',(-1.76330080756894,2.64858386892187E-15,
7.64062500000002));
#420671=CARTESIAN_POINT('Ctrl Pts',(-1.3224756056767,-0.763531646934155,
7.68229166666669));
#420672=CARTESIAN_POINT('Ctrl Pts',(-0.881650403784469,-1.52706329386831,
7.72395833333335));
#420673=CARTESIAN_POINT('Ctrl Pts',(-1.87011317493125E-16,-1.52706329386831,
7.76562500000002));
#420674=CARTESIAN_POINT('Ctrl Pts',(0.881650403784467,-1.52706329386831,
7.80729166666669));
#420675=CARTESIAN_POINT('Ctrl Pts',(1.3224756056767,-0.763531646934156,
7.84895833333335));
#420676=CARTESIAN_POINT('Ctrl Pts',(1.76330080756894,2.21669973093722E-15,
7.89062500000002));
#420677=CARTESIAN_POINT('Ctrl Pts',(1.3224756056767,0.763531646934159,7.93229166666669));
#420678=CARTESIAN_POINT('Ctrl Pts',(0.881650403784469,1.52706329386832,
7.97395833333335));
#420679=CARTESIAN_POINT('Ctrl Pts',(0.,1.52706329386832,8.01562500000002));
#420680=CARTESIAN_POINT('Ctrl Pts',(-0.881650403784468,1.52706329386832,
8.05729166666668));
#420681=CARTESIAN_POINT('Ctrl Pts',(-1.3224756056767,0.76353164693416,8.09895833333335));
#420682=CARTESIAN_POINT('Ctrl Pts',(-1.76330080756894,2.64858386892187E-15,
8.14062500000002));
#420683=CARTESIAN_POINT('Ctrl Pts',(-1.3224756056767,-0.763531646934155,
8.18229166666668));
#420684=CARTESIAN_POINT('Ctrl Pts',(-0.881650403784469,-1.52706329386831,
8.22395833333335));
#420685=CARTESIAN_POINT('Ctrl Pts',(-1.87011317493125E-16,-1.52706329386831,
8.26562500000002));
#420686=CARTESIAN_POINT('Ctrl Pts',(0.881650403784467,-1.52706329386831,
8.30729166666668));
#420687=CARTESIAN_POINT('Ctrl Pts',(1.3224756056767,-0.763531646934156,
8.34895833333335));
#420688=CARTESIAN_POINT('Ctrl Pts',(1.76330080756894,2.21669973093722E-15,
8.39062500000002));
#420689=CARTESIAN_POINT('Ctrl Pts',(1.3224756056767,0.763531646934159,8.43229166666669));
#420690=CARTESIAN_POINT('Ctrl Pts',(0.881650403784469,1.52706329386832,
8.47395833333335));
#420691=CARTESIAN_POINT('Ctrl Pts',(0.,1.52706329386832,8.51562500000002));
#420692=CARTESIAN_POINT('Ctrl Pts',(-0.881650403784468,1.52706329386832,
8.55729166666669));
#420693=CARTESIAN_POINT('Ctrl Pts',(-1.3224756056767,0.76353164693416,8.59895833333335));
#420694=CARTESIAN_POINT('Ctrl Pts',(-1.76330080756894,2.64858386892187E-15,
8.64062500000002));
#420695=CARTESIAN_POINT('Ctrl Pts',(-1.3224756056767,-0.763531646934155,
8.68229166666668));
#420696=CARTESIAN_POINT('Ctrl Pts',(-0.881650403784469,-1.52706329386831,
8.72395833333335));
#420697=CARTESIAN_POINT('Ctrl Pts',(-1.87011317493125E-16,-1.52706329386831,
8.76562500000002));
#420698=CARTESIAN_POINT('Ctrl Pts',(0.881650403784467,-1.52706329386831,
8.80729166666668));
#420699=CARTESIAN_POINT('Ctrl Pts',(1.3224756056767,-0.763531646934156,
8.84895833333335));
#420700=CARTESIAN_POINT('Ctrl Pts',(1.76330080756894,2.21669973093722E-15,
8.89062500000002));
#420701=CARTESIAN_POINT('Ctrl Pts',(1.3224756056767,0.763531646934159,8.93229166666668));
#420702=CARTESIAN_POINT('Ctrl Pts',(0.881650403784469,1.52706329386832,
8.97395833333335));
#420703=CARTESIAN_POINT('Ctrl Pts',(0.,1.52706329386832,9.01562500000002));
#420704=CARTESIAN_POINT('Ctrl Pts',(-0.881650403784468,1.52706329386832,
9.05729166666669));
#420705=CARTESIAN_POINT('Ctrl Pts',(-1.3224756056767,0.76353164693416,9.09895833333335));
#420706=CARTESIAN_POINT('Ctrl Pts',(-1.76330080756894,2.64858386892187E-15,
9.14062500000002));
#420707=CARTESIAN_POINT('Ctrl Pts',(-1.3224756056767,-0.763531646934155,
9.18229166666668));
#420708=CARTESIAN_POINT('Ctrl Pts',(-0.881650403784469,-1.52706329386831,
9.22395833333335));
#420709=CARTESIAN_POINT('Ctrl Pts',(-1.87011317493125E-16,-1.52706329386831,
9.26562500000002));
#420710=CARTESIAN_POINT('Ctrl Pts',(0.881650403784467,-1.52706329386831,
9.30729166666669));
#420711=CARTESIAN_POINT('Ctrl Pts',(1.3224756056767,-0.763531646934156,
9.34895833333335));
#420712=CARTESIAN_POINT('Ctrl Pts',(1.76330080756894,2.21669973093722E-15,
9.39062500000002));
#420713=CARTESIAN_POINT('Ctrl Pts',(1.3224756056767,0.763531646934159,9.43229166666668));
#420714=CARTESIAN_POINT('Ctrl Pts',(0.881650403784469,1.52706329386832,
9.47395833333335));
#420715=CARTESIAN_POINT('Ctrl Pts',(0.,1.52706329386832,9.51562500000002));
#420716=CARTESIAN_POINT('Ctrl Pts',(-0.881650403784468,1.52706329386832,
9.55729166666669));
#420717=CARTESIAN_POINT('Ctrl Pts',(-1.3224756056767,0.76353164693416,9.59895833333335));
#420718=CARTESIAN_POINT('Ctrl Pts',(-1.76330080756894,2.64858386892187E-15,
9.64062500000002));
#420719=CARTESIAN_POINT('Ctrl Pts',(-1.3224756056767,-0.763531646934155,
9.68229166666669));
#420720=CARTESIAN_POINT('Ctrl Pts',(-0.881650403784469,-1.52706329386831,
9.72395833333335));
#420721=CARTESIAN_POINT('Ctrl Pts',(-1.87011317493125E-16,-1.52706329386831,
9.76562500000002));
#420722=CARTESIAN_POINT('Ctrl Pts',(0.881650403784467,-1.52706329386831,
9.80729166666668));
#420723=CARTESIAN_POINT('Ctrl Pts',(1.3224756056767,-0.763531646934156,
9.84895833333335));
#420724=CARTESIAN_POINT('Ctrl Pts',(1.76330080756894,2.21669973093722E-15,
9.89062500000002));
#420725=CARTESIAN_POINT('Ctrl Pts',(1.3224756056767,0.763531646934159,9.93229166666669));
#420726=CARTESIAN_POINT('Ctrl Pts',(0.881650403784469,1.52706329386832,
9.97395833333335));
#420727=CARTESIAN_POINT('Ctrl Pts',(0.,1.52706329386832,10.015625));
#420728=CARTESIAN_POINT('Ctrl Pts',(-0.881650403784468,1.52706329386832,
10.0572916666667));
#420729=CARTESIAN_POINT('Ctrl Pts',(-1.3224756056767,0.76353164693416,10.0989583333333));
#420730=CARTESIAN_POINT('Ctrl Pts',(-1.76330080756894,2.64858386892187E-15,
10.140625));
#420731=CARTESIAN_POINT('Ctrl Pts',(-1.3224756056767,-0.763531646934155,
10.1822916666667));
#420732=CARTESIAN_POINT('Ctrl Pts',(-0.881650403784469,-1.52706329386831,
10.2239583333333));
#420733=CARTESIAN_POINT('Ctrl Pts',(-1.87011317493125E-16,-1.52706329386831,
10.265625));
#420734=CARTESIAN_POINT('Ctrl Pts',(0.881650403784467,-1.52706329386831,
10.3072916666667));
#420735=CARTESIAN_POINT('Ctrl Pts',(1.3224756056767,-0.763531646934156,
10.3489583333334));
#420736=CARTESIAN_POINT('Ctrl Pts',(1.76330080756894,2.21669973093722E-15,
10.390625));
#420737=CARTESIAN_POINT('Ctrl Pts',(1.3224756056767,0.763531646934159,10.4322916666667));
#420738=CARTESIAN_POINT('Ctrl Pts',(0.881650403784469,1.52706329386832,
10.4739583333334));
#420739=CARTESIAN_POINT('Ctrl Pts',(0.,1.52706329386832,10.515625));
#420740=CARTESIAN_POINT('Ctrl Pts',(-0.881650403784468,1.52706329386832,
10.5572916666667));
#420741=CARTESIAN_POINT('Ctrl Pts',(-1.3224756056767,0.76353164693416,10.5989583333334));
#420742=CARTESIAN_POINT('Ctrl Pts',(-1.76330080756894,2.64858386892187E-15,
10.640625));
#420743=CARTESIAN_POINT('Ctrl Pts',(-1.3224756056767,-0.763531646934155,
10.6822916666667));
#420744=CARTESIAN_POINT('Ctrl Pts',(-0.881650403784469,-1.52706329386831,
10.7239583333333));
#420745=CARTESIAN_POINT('Ctrl Pts',(-1.87011317493125E-16,-1.52706329386831,
10.765625));
#420746=CARTESIAN_POINT('Ctrl Pts',(0.881650403784467,-1.52706329386831,
10.8072916666667));
#420747=CARTESIAN_POINT('Ctrl Pts',(1.3224756056767,-0.763531646934156,
10.8489583333334));
#420748=CARTESIAN_POINT('Ctrl Pts',(1.76330080756894,2.21669973093722E-15,
10.890625));
#420749=CARTESIAN_POINT('Ctrl Pts',(1.3224756056767,0.763531646934159,10.9322916666667));
#420750=CARTESIAN_POINT('Ctrl Pts',(0.881650403784469,1.52706329386832,
10.9739583333334));
#420751=CARTESIAN_POINT('Ctrl Pts',(0.,1.52706329386832,11.015625));
#420752=CARTESIAN_POINT('Ctrl Pts',(-0.881650403784468,1.52706329386832,
11.0572916666667));
#420753=CARTESIAN_POINT('Ctrl Pts',(-1.3224756056767,0.76353164693416,11.0989583333334));
#420754=CARTESIAN_POINT('Ctrl Pts',(-1.76330080756894,2.64858386892187E-15,
11.140625));
#420755=CARTESIAN_POINT('Ctrl Pts',(-1.3224756056767,-0.763531646934155,
11.1822916666667));
#420756=CARTESIAN_POINT('Ctrl Pts',(-0.881650403784469,-1.52706329386831,
11.2239583333334));
#420757=CARTESIAN_POINT('Ctrl Pts',(-1.87011317493125E-16,-1.52706329386831,
11.265625));
#420758=CARTESIAN_POINT('Ctrl Pts',(0.881650403784467,-1.52706329386831,
11.3072916666667));
#420759=CARTESIAN_POINT('Ctrl Pts',(1.3224756056767,-0.763531646934156,
11.3489583333334));
#420760=CARTESIAN_POINT('Ctrl Pts',(1.76330080756894,2.21669973093722E-15,
11.390625));
#420761=CARTESIAN_POINT('Ctrl Pts',(1.3224756056767,0.763531646934159,11.4322916666667));
#420762=CARTESIAN_POINT('Ctrl Pts',(0.881650403784469,1.52706329386832,
11.4739583333334));
#420763=CARTESIAN_POINT('Ctrl Pts',(0.,1.52706329386832,11.515625));
#420764=CARTESIAN_POINT('Ctrl Pts',(0.,1.17523522336992,-14.1875030312107));
#420765=CARTESIAN_POINT('Ctrl Pts',(-0.678522372573754,1.17523522336992,
-14.145836364544));
#420766=CARTESIAN_POINT('Ctrl Pts',(-1.01778355886063,0.587617611684963,
-14.1041696978774));
#420767=CARTESIAN_POINT('Ctrl Pts',(-1.35704474514751,2.62370785959794E-15,
-14.0625030312107));
#420768=CARTESIAN_POINT('Ctrl Pts',(-1.01778355886063,-0.587617611684958,
-14.020836364544));
#420769=CARTESIAN_POINT('Ctrl Pts',(-0.678522372573755,-1.17523522336992,
-13.9791696978774));
#420770=CARTESIAN_POINT('Ctrl Pts',(-1.4392480545452E-16,-1.17523522336992,
-13.9375030312107));
#420771=CARTESIAN_POINT('Ctrl Pts',(0.678522372573754,-1.17523522336992,
-13.895836364544));
#420772=CARTESIAN_POINT('Ctrl Pts',(1.01778355886063,-0.587617611684959,
-13.8541696978774));
#420773=CARTESIAN_POINT('Ctrl Pts',(1.35704474514751,2.29132775890901E-15,
-13.8125030312107));
#420774=CARTESIAN_POINT('Ctrl Pts',(1.01778355886063,0.587617611684963,
-13.770836364544));
#420775=CARTESIAN_POINT('Ctrl Pts',(0.678522372573755,1.17523522336992,
-13.7291696978774));
#420776=CARTESIAN_POINT('Ctrl Pts',(0.,1.17523522336992,-13.6875030312107));
#420777=CARTESIAN_POINT('Ctrl Pts',(-0.678522372573754,1.17523522336992,
-13.645836364544));
#420778=CARTESIAN_POINT('Ctrl Pts',(-1.01778355886063,0.587617611684963,
-13.6041696978774));
#420779=CARTESIAN_POINT('Ctrl Pts',(-1.35704474514751,2.62370785959794E-15,
-13.5625030312107));
#420780=CARTESIAN_POINT('Ctrl Pts',(-1.01778355886063,-0.587617611684958,
-13.520836364544));
#420781=CARTESIAN_POINT('Ctrl Pts',(-0.678522372573755,-1.17523522336992,
-13.4791696978774));
#420782=CARTESIAN_POINT('Ctrl Pts',(-1.4392480545452E-16,-1.17523522336992,
-13.4375030312107));
#420783=CARTESIAN_POINT('Ctrl Pts',(0.678522372573754,-1.17523522336992,
-13.395836364544));
#420784=CARTESIAN_POINT('Ctrl Pts',(1.01778355886063,-0.587617611684959,
-13.3541696978774));
#420785=CARTESIAN_POINT('Ctrl Pts',(1.35704474514751,2.29132775890901E-15,
-13.3125030312107));
#420786=CARTESIAN_POINT('Ctrl Pts',(1.01778355886063,0.587617611684963,
-13.270836364544));
#420787=CARTESIAN_POINT('Ctrl Pts',(0.678522372573755,1.17523522336992,
-13.2291696978774));
#420788=CARTESIAN_POINT('Ctrl Pts',(0.,1.17523522336992,-13.1875030312107));
#420789=CARTESIAN_POINT('Ctrl Pts',(-0.678522372573754,1.17523522336992,
-13.145836364544));
#420790=CARTESIAN_POINT('Ctrl Pts',(-1.01778355886063,0.587617611684963,
-13.1041696978774));
#420791=CARTESIAN_POINT('Ctrl Pts',(-1.35704474514751,2.62370785959794E-15,
-13.0625030312107));
#420792=CARTESIAN_POINT('Ctrl Pts',(-1.01778355886063,-0.587617611684958,
-13.020836364544));
#420793=CARTESIAN_POINT('Ctrl Pts',(-0.678522372573755,-1.17523522336992,
-12.9791696978774));
#420794=CARTESIAN_POINT('Ctrl Pts',(-1.4392480545452E-16,-1.17523522336992,
-12.9375030312107));
#420795=CARTESIAN_POINT('Ctrl Pts',(0.678522372573754,-1.17523522336992,
-12.895836364544));
#420796=CARTESIAN_POINT('Ctrl Pts',(1.01778355886063,-0.587617611684959,
-12.8541696978774));
#420797=CARTESIAN_POINT('Ctrl Pts',(1.35704474514751,2.29132775890901E-15,
-12.8125030312107));
#420798=CARTESIAN_POINT('Ctrl Pts',(1.01778355886063,0.587617611684963,
-12.770836364544));
#420799=CARTESIAN_POINT('Ctrl Pts',(0.678522372573755,1.17523522336992,
-12.7291696978774));
#420800=CARTESIAN_POINT('Ctrl Pts',(0.,1.17523522336992,-12.6875030312107));
#420801=CARTESIAN_POINT('Ctrl Pts',(-0.678522372573754,1.17523522336992,
-12.645836364544));
#420802=CARTESIAN_POINT('Ctrl Pts',(-1.01778355886063,0.587617611684963,
-12.6041696978774));
#420803=CARTESIAN_POINT('Ctrl Pts',(-1.35704474514751,2.62370785959794E-15,
-12.5625030312107));
#420804=CARTESIAN_POINT('Ctrl Pts',(-1.01778355886063,-0.587617611684958,
-12.520836364544));
#420805=CARTESIAN_POINT('Ctrl Pts',(-0.678522372573755,-1.17523522336992,
-12.4791696978774));
#420806=CARTESIAN_POINT('Ctrl Pts',(-1.4392480545452E-16,-1.17523522336992,
-12.4375030312107));
#420807=CARTESIAN_POINT('Ctrl Pts',(0.678522372573754,-1.17523522336992,
-12.395836364544));
#420808=CARTESIAN_POINT('Ctrl Pts',(1.01778355886063,-0.587617611684959,
-12.3541696978774));
#420809=CARTESIAN_POINT('Ctrl Pts',(1.35704474514751,2.29132775890901E-15,
-12.3125030312107));
#420810=CARTESIAN_POINT('Ctrl Pts',(1.01778355886063,0.587617611684963,
-12.270836364544));
#420811=CARTESIAN_POINT('Ctrl Pts',(0.678522372573755,1.17523522336992,
-12.2291696978774));
#420812=CARTESIAN_POINT('Ctrl Pts',(0.,1.17523522336992,-12.1875030312107));
#420813=CARTESIAN_POINT('Ctrl Pts',(-0.678522372573754,1.17523522336992,
-12.145836364544));
#420814=CARTESIAN_POINT('Ctrl Pts',(-1.01778355886063,0.587617611684963,
-12.1041696978774));
#420815=CARTESIAN_POINT('Ctrl Pts',(-1.35704474514751,2.62370785959794E-15,
-12.0625030312107));
#420816=CARTESIAN_POINT('Ctrl Pts',(-1.01778355886063,-0.587617611684958,
-12.020836364544));
#420817=CARTESIAN_POINT('Ctrl Pts',(-0.678522372573755,-1.17523522336992,
-11.9791696978774));
#420818=CARTESIAN_POINT('Ctrl Pts',(-1.4392480545452E-16,-1.17523522336992,
-11.9375030312107));
#420819=CARTESIAN_POINT('Ctrl Pts',(0.678522372573754,-1.17523522336992,
-11.895836364544));
#420820=CARTESIAN_POINT('Ctrl Pts',(1.01778355886063,-0.587617611684959,
-11.8541696978774));
#420821=CARTESIAN_POINT('Ctrl Pts',(1.35704474514751,2.29132775890901E-15,
-11.8125030312107));
#420822=CARTESIAN_POINT('Ctrl Pts',(1.01778355886063,0.587617611684963,
-11.770836364544));
#420823=CARTESIAN_POINT('Ctrl Pts',(0.678522372573755,1.17523522336992,
-11.7291696978774));
#420824=CARTESIAN_POINT('Ctrl Pts',(0.,1.17523522336992,-11.6875030312107));
#420825=CARTESIAN_POINT('Ctrl Pts',(-0.678522372573754,1.17523522336992,
-11.645836364544));
#420826=CARTESIAN_POINT('Ctrl Pts',(-1.01778355886063,0.587617611684963,
-11.6041696978774));
#420827=CARTESIAN_POINT('Ctrl Pts',(-1.35704474514751,2.62370785959794E-15,
-11.5625030312107));
#420828=CARTESIAN_POINT('Ctrl Pts',(-1.01778355886063,-0.587617611684958,
-11.520836364544));
#420829=CARTESIAN_POINT('Ctrl Pts',(-0.678522372573755,-1.17523522336992,
-11.4791696978774));
#420830=CARTESIAN_POINT('Ctrl Pts',(-1.4392480545452E-16,-1.17523522336992,
-11.4375030312107));
#420831=CARTESIAN_POINT('Ctrl Pts',(0.678522372573754,-1.17523522336992,
-11.395836364544));
#420832=CARTESIAN_POINT('Ctrl Pts',(1.01778355886063,-0.587617611684959,
-11.3541696978774));
#420833=CARTESIAN_POINT('Ctrl Pts',(1.35704474514751,2.29132775890901E-15,
-11.3125030312107));
#420834=CARTESIAN_POINT('Ctrl Pts',(1.01778355886063,0.587617611684963,
-11.270836364544));
#420835=CARTESIAN_POINT('Ctrl Pts',(0.678522372573755,1.17523522336992,
-11.2291696978774));
#420836=CARTESIAN_POINT('Ctrl Pts',(0.,1.17523522336992,-11.1875030312107));
#420837=CARTESIAN_POINT('Ctrl Pts',(-0.678522372573754,1.17523522336992,
-11.145836364544));
#420838=CARTESIAN_POINT('Ctrl Pts',(-1.01778355886063,0.587617611684963,
-11.1041696978774));
#420839=CARTESIAN_POINT('Ctrl Pts',(-1.35704474514751,2.62370785959794E-15,
-11.0625030312107));
#420840=CARTESIAN_POINT('Ctrl Pts',(-1.01778355886063,-0.587617611684958,
-11.020836364544));
#420841=CARTESIAN_POINT('Ctrl Pts',(-0.678522372573755,-1.17523522336992,
-10.9791696978774));
#420842=CARTESIAN_POINT('Ctrl Pts',(-1.4392480545452E-16,-1.17523522336992,
-10.9375030312107));
#420843=CARTESIAN_POINT('Ctrl Pts',(0.678522372573754,-1.17523522336992,
-10.895836364544));
#420844=CARTESIAN_POINT('Ctrl Pts',(1.01778355886063,-0.587617611684959,
-10.8541696978774));
#420845=CARTESIAN_POINT('Ctrl Pts',(1.35704474514751,2.29132775890901E-15,
-10.8125030312107));
#420846=CARTESIAN_POINT('Ctrl Pts',(1.01778355886063,0.587617611684963,
-10.770836364544));
#420847=CARTESIAN_POINT('Ctrl Pts',(0.678522372573755,1.17523522336992,
-10.7291696978774));
#420848=CARTESIAN_POINT('Ctrl Pts',(0.,1.17523522336992,-10.6875030312107));
#420849=CARTESIAN_POINT('Ctrl Pts',(-0.678522372573754,1.17523522336992,
-10.645836364544));
#420850=CARTESIAN_POINT('Ctrl Pts',(-1.01778355886063,0.587617611684963,
-10.6041696978774));
#420851=CARTESIAN_POINT('Ctrl Pts',(-1.35704474514751,2.62370785959794E-15,
-10.5625030312107));
#420852=CARTESIAN_POINT('Ctrl Pts',(-1.01778355886063,-0.587617611684958,
-10.520836364544));
#420853=CARTESIAN_POINT('Ctrl Pts',(-0.678522372573755,-1.17523522336992,
-10.4791696978774));
#420854=CARTESIAN_POINT('Ctrl Pts',(-1.4392480545452E-16,-1.17523522336992,
-10.4375030312107));
#420855=CARTESIAN_POINT('Ctrl Pts',(0.678522372573754,-1.17523522336992,
-10.395836364544));
#420856=CARTESIAN_POINT('Ctrl Pts',(1.01778355886063,-0.587617611684959,
-10.3541696978774));
#420857=CARTESIAN_POINT('Ctrl Pts',(1.35704474514751,2.29132775890901E-15,
-10.3125030312107));
#420858=CARTESIAN_POINT('Ctrl Pts',(1.01778355886063,0.587617611684963,
-10.270836364544));
#420859=CARTESIAN_POINT('Ctrl Pts',(0.678522372573755,1.17523522336992,
-10.2291696978774));
#420860=CARTESIAN_POINT('Ctrl Pts',(0.,1.17523522336992,-10.1875030312107));
#420861=CARTESIAN_POINT('Ctrl Pts',(-0.678522372573754,1.17523522336992,
-10.145836364544));
#420862=CARTESIAN_POINT('Ctrl Pts',(-1.01778355886063,0.587617611684963,
-10.1041696978774));
#420863=CARTESIAN_POINT('Ctrl Pts',(-1.35704474514751,2.62370785959794E-15,
-10.0625030312107));
#420864=CARTESIAN_POINT('Ctrl Pts',(-1.01778355886063,-0.587617611684958,
-10.020836364544));
#420865=CARTESIAN_POINT('Ctrl Pts',(-0.678522372573755,-1.17523522336992,
-9.97916969787736));
#420866=CARTESIAN_POINT('Ctrl Pts',(-1.4392480545452E-16,-1.17523522336992,
-9.9375030312107));
#420867=CARTESIAN_POINT('Ctrl Pts',(0.678522372573754,-1.17523522336992,
-9.89583636454403));
#420868=CARTESIAN_POINT('Ctrl Pts',(1.01778355886063,-0.587617611684959,
-9.85416969787736));
#420869=CARTESIAN_POINT('Ctrl Pts',(1.35704474514751,2.29132775890901E-15,
-9.8125030312107));
#420870=CARTESIAN_POINT('Ctrl Pts',(1.01778355886063,0.587617611684963,
-9.77083636454403));
#420871=CARTESIAN_POINT('Ctrl Pts',(0.678522372573755,1.17523522336992,
-9.72916969787736));
#420872=CARTESIAN_POINT('Ctrl Pts',(0.,1.17523522336992,-9.6875030312107));
#420873=CARTESIAN_POINT('Ctrl Pts',(-0.678522372573754,1.17523522336992,
-9.64583636454403));
#420874=CARTESIAN_POINT('Ctrl Pts',(-1.01778355886063,0.587617611684963,
-9.60416969787736));
#420875=CARTESIAN_POINT('Ctrl Pts',(-1.35704474514751,2.62370785959794E-15,
-9.5625030312107));
#420876=CARTESIAN_POINT('Ctrl Pts',(-1.01778355886063,-0.587617611684958,
-9.52083636454403));
#420877=CARTESIAN_POINT('Ctrl Pts',(-0.678522372573755,-1.17523522336992,
-9.47916969787736));
#420878=CARTESIAN_POINT('Ctrl Pts',(-1.4392480545452E-16,-1.17523522336992,
-9.4375030312107));
#420879=CARTESIAN_POINT('Ctrl Pts',(0.678522372573754,-1.17523522336992,
-9.39583636454403));
#420880=CARTESIAN_POINT('Ctrl Pts',(1.01778355886063,-0.587617611684959,
-9.35416969787736));
#420881=CARTESIAN_POINT('Ctrl Pts',(1.35704474514751,2.29132775890901E-15,
-9.3125030312107));
#420882=CARTESIAN_POINT('Ctrl Pts',(1.01778355886063,0.587617611684963,
-9.27083636454403));
#420883=CARTESIAN_POINT('Ctrl Pts',(0.678522372573755,1.17523522336992,
-9.22916969787736));
#420884=CARTESIAN_POINT('Ctrl Pts',(0.,1.17523522336992,-9.1875030312107));
#420885=CARTESIAN_POINT('Ctrl Pts',(-0.678522372573754,1.17523522336992,
-9.14583636454403));
#420886=CARTESIAN_POINT('Ctrl Pts',(-1.01778355886063,0.587617611684963,
-9.10416969787736));
#420887=CARTESIAN_POINT('Ctrl Pts',(-1.35704474514751,2.62370785959794E-15,
-9.0625030312107));
#420888=CARTESIAN_POINT('Ctrl Pts',(-1.01778355886063,-0.587617611684958,
-9.02083636454403));
#420889=CARTESIAN_POINT('Ctrl Pts',(-0.678522372573755,-1.17523522336992,
-8.97916969787736));
#420890=CARTESIAN_POINT('Ctrl Pts',(-1.4392480545452E-16,-1.17523522336992,
-8.9375030312107));
#420891=CARTESIAN_POINT('Ctrl Pts',(0.678522372573754,-1.17523522336992,
-8.89583636454403));
#420892=CARTESIAN_POINT('Ctrl Pts',(1.01778355886063,-0.587617611684959,
-8.85416969787736));
#420893=CARTESIAN_POINT('Ctrl Pts',(1.35704474514751,2.29132775890901E-15,
-8.8125030312107));
#420894=CARTESIAN_POINT('Ctrl Pts',(1.01778355886063,0.587617611684963,
-8.77083636454403));
#420895=CARTESIAN_POINT('Ctrl Pts',(0.678522372573755,1.17523522336992,
-8.72916969787736));
#420896=CARTESIAN_POINT('Ctrl Pts',(0.,1.17523522336992,-8.6875030312107));
#420897=CARTESIAN_POINT('Ctrl Pts',(-0.678522372573754,1.17523522336992,
-8.64583636454403));
#420898=CARTESIAN_POINT('Ctrl Pts',(-1.01778355886063,0.587617611684963,
-8.60416969787736));
#420899=CARTESIAN_POINT('Ctrl Pts',(-1.35704474514751,2.62370785959794E-15,
-8.5625030312107));
#420900=CARTESIAN_POINT('Ctrl Pts',(-1.01778355886063,-0.587617611684958,
-8.52083636454403));
#420901=CARTESIAN_POINT('Ctrl Pts',(-0.678522372573755,-1.17523522336992,
-8.47916969787736));
#420902=CARTESIAN_POINT('Ctrl Pts',(-1.4392480545452E-16,-1.17523522336992,
-8.43750303121069));
#420903=CARTESIAN_POINT('Ctrl Pts',(0.678522372573754,-1.17523522336992,
-8.39583636454403));
#420904=CARTESIAN_POINT('Ctrl Pts',(1.01778355886063,-0.587617611684959,
-8.35416969787736));
#420905=CARTESIAN_POINT('Ctrl Pts',(1.35704474514751,2.29132775890901E-15,
-8.31250303121069));
#420906=CARTESIAN_POINT('Ctrl Pts',(1.01778355886063,0.587617611684963,
-8.27083636454403));
#420907=CARTESIAN_POINT('Ctrl Pts',(0.678522372573755,1.17523522336992,
-8.22916969787736));
#420908=CARTESIAN_POINT('Ctrl Pts',(0.,1.17523522336992,-8.1875030312107));
#420909=CARTESIAN_POINT('Ctrl Pts',(-0.678522372573754,1.17523522336992,
-8.14583636454403));
#420910=CARTESIAN_POINT('Ctrl Pts',(-1.01778355886063,0.587617611684963,
-8.10416969787736));
#420911=CARTESIAN_POINT('Ctrl Pts',(-1.35704474514751,2.62370785959794E-15,
-8.0625030312107));
#420912=CARTESIAN_POINT('Ctrl Pts',(-1.01778355886063,-0.587617611684958,
-8.02083636454403));
#420913=CARTESIAN_POINT('Ctrl Pts',(-0.678522372573755,-1.17523522336992,
-7.97916969787736));
#420914=CARTESIAN_POINT('Ctrl Pts',(-1.4392480545452E-16,-1.17523522336992,
-7.9375030312107));
#420915=CARTESIAN_POINT('Ctrl Pts',(0.678522372573754,-1.17523522336992,
-7.89583636454403));
#420916=CARTESIAN_POINT('Ctrl Pts',(1.01778355886063,-0.587617611684959,
-7.85416969787736));
#420917=CARTESIAN_POINT('Ctrl Pts',(1.35704474514751,2.29132775890901E-15,
-7.8125030312107));
#420918=CARTESIAN_POINT('Ctrl Pts',(1.01778355886063,0.587617611684963,
-7.77083636454403));
#420919=CARTESIAN_POINT('Ctrl Pts',(0.678522372573755,1.17523522336992,
-7.72916969787736));
#420920=CARTESIAN_POINT('Ctrl Pts',(0.,1.17523522336992,-7.68750303121069));
#420921=CARTESIAN_POINT('Ctrl Pts',(-0.678522372573754,1.17523522336992,
-7.64583636454403));
#420922=CARTESIAN_POINT('Ctrl Pts',(-1.01778355886063,0.587617611684963,
-7.60416969787736));
#420923=CARTESIAN_POINT('Ctrl Pts',(-1.35704474514751,2.62370785959794E-15,
-7.5625030312107));
#420924=CARTESIAN_POINT('Ctrl Pts',(-1.01778355886063,-0.587617611684958,
-7.52083636454403));
#420925=CARTESIAN_POINT('Ctrl Pts',(-0.678522372573755,-1.17523522336992,
-7.47916969787736));
#420926=CARTESIAN_POINT('Ctrl Pts',(-1.4392480545452E-16,-1.17523522336992,
-7.4375030312107));
#420927=CARTESIAN_POINT('Ctrl Pts',(0.678522372573754,-1.17523522336992,
-7.39583636454403));
#420928=CARTESIAN_POINT('Ctrl Pts',(1.01778355886063,-0.587617611684959,
-7.35416969787736));
#420929=CARTESIAN_POINT('Ctrl Pts',(1.35704474514751,2.29132775890901E-15,
-7.31250303121069));
#420930=CARTESIAN_POINT('Ctrl Pts',(1.01778355886063,0.587617611684963,
-7.27083636454403));
#420931=CARTESIAN_POINT('Ctrl Pts',(0.678522372573755,1.17523522336992,
-7.22916969787736));
#420932=CARTESIAN_POINT('Ctrl Pts',(0.,1.17523522336992,-7.1875030312107));
#420933=CARTESIAN_POINT('Ctrl Pts',(-0.678522372573754,1.17523522336992,
-7.14583636454403));
#420934=CARTESIAN_POINT('Ctrl Pts',(-1.01778355886063,0.587617611684963,
-7.10416969787736));
#420935=CARTESIAN_POINT('Ctrl Pts',(-1.35704474514751,2.62370785959794E-15,
-7.0625030312107));
#420936=CARTESIAN_POINT('Ctrl Pts',(-1.01778355886063,-0.587617611684958,
-7.02083636454403));
#420937=CARTESIAN_POINT('Ctrl Pts',(-0.678522372573755,-1.17523522336992,
-6.97916969787736));
#420938=CARTESIAN_POINT('Ctrl Pts',(-1.4392480545452E-16,-1.17523522336992,
-6.9375030312107));
#420939=CARTESIAN_POINT('Ctrl Pts',(0.678522372573754,-1.17523522336992,
-6.89583636454403));
#420940=CARTESIAN_POINT('Ctrl Pts',(1.01778355886063,-0.587617611684959,
-6.85416969787736));
#420941=CARTESIAN_POINT('Ctrl Pts',(1.35704474514751,2.29132775890901E-15,
-6.8125030312107));
#420942=CARTESIAN_POINT('Ctrl Pts',(1.01778355886063,0.587617611684963,
-6.77083636454403));
#420943=CARTESIAN_POINT('Ctrl Pts',(0.678522372573755,1.17523522336992,
-6.72916969787736));
#420944=CARTESIAN_POINT('Ctrl Pts',(0.,1.17523522336992,-6.6875030312107));
#420945=CARTESIAN_POINT('Ctrl Pts',(-0.678522372573754,1.17523522336992,
-6.64583636454403));
#420946=CARTESIAN_POINT('Ctrl Pts',(-1.01778355886063,0.587617611684963,
-6.60416969787736));
#420947=CARTESIAN_POINT('Ctrl Pts',(-1.35704474514751,2.62370785959794E-15,
-6.5625030312107));
#420948=CARTESIAN_POINT('Ctrl Pts',(-1.01778355886063,-0.587617611684958,
-6.52083636454403));
#420949=CARTESIAN_POINT('Ctrl Pts',(-0.678522372573755,-1.17523522336992,
-6.47916969787736));
#420950=CARTESIAN_POINT('Ctrl Pts',(-1.4392480545452E-16,-1.17523522336992,
-6.4375030312107));
#420951=CARTESIAN_POINT('Ctrl Pts',(0.678522372573754,-1.17523522336992,
-6.39583636454403));
#420952=CARTESIAN_POINT('Ctrl Pts',(1.01778355886063,-0.587617611684959,
-6.35416969787736));
#420953=CARTESIAN_POINT('Ctrl Pts',(1.35704474514751,2.29132775890901E-15,
-6.3125030312107));
#420954=CARTESIAN_POINT('Ctrl Pts',(1.01778355886063,0.587617611684963,
-6.27083636454403));
#420955=CARTESIAN_POINT('Ctrl Pts',(0.678522372573755,1.17523522336992,
-6.22916969787736));
#420956=CARTESIAN_POINT('Ctrl Pts',(0.,1.17523522336992,-6.18750303121069));
#420957=CARTESIAN_POINT('Ctrl Pts',(-0.678522372573754,1.17523522336992,
-6.14583636454403));
#420958=CARTESIAN_POINT('Ctrl Pts',(-1.01778355886063,0.587617611684963,
-6.10416969787736));
#420959=CARTESIAN_POINT('Ctrl Pts',(-1.35704474514751,2.62370785959794E-15,
-6.0625030312107));
#420960=CARTESIAN_POINT('Ctrl Pts',(-1.01778355886063,-0.587617611684958,
-6.02083636454403));
#420961=CARTESIAN_POINT('Ctrl Pts',(-0.678522372573755,-1.17523522336992,
-5.97916969787736));
#420962=CARTESIAN_POINT('Ctrl Pts',(-1.4392480545452E-16,-1.17523522336992,
-5.9375030312107));
#420963=CARTESIAN_POINT('Ctrl Pts',(0.678522372573754,-1.17523522336992,
-5.89583636454403));
#420964=CARTESIAN_POINT('Ctrl Pts',(1.01778355886063,-0.587617611684959,
-5.85416969787736));
#420965=CARTESIAN_POINT('Ctrl Pts',(1.35704474514751,2.29132775890901E-15,
-5.81250303121069));
#420966=CARTESIAN_POINT('Ctrl Pts',(1.01778355886063,0.587617611684963,
-5.77083636454403));
#420967=CARTESIAN_POINT('Ctrl Pts',(0.678522372573755,1.17523522336992,
-5.72916969787736));
#420968=CARTESIAN_POINT('Ctrl Pts',(0.,1.17523522336992,-5.6875030312107));
#420969=CARTESIAN_POINT('Ctrl Pts',(-0.678522372573754,1.17523522336992,
-5.64583636454403));
#420970=CARTESIAN_POINT('Ctrl Pts',(-1.01778355886063,0.587617611684963,
-5.60416969787736));
#420971=CARTESIAN_POINT('Ctrl Pts',(-1.35704474514751,2.62370785959794E-15,
-5.5625030312107));
#420972=CARTESIAN_POINT('Ctrl Pts',(-1.01778355886063,-0.587617611684958,
-5.52083636454403));
#420973=CARTESIAN_POINT('Ctrl Pts',(-0.678522372573755,-1.17523522336992,
-5.47916969787736));
#420974=CARTESIAN_POINT('Ctrl Pts',(-1.4392480545452E-16,-1.17523522336992,
-5.4375030312107));
#420975=CARTESIAN_POINT('Ctrl Pts',(0.678522372573754,-1.17523522336992,
-5.39583636454403));
#420976=CARTESIAN_POINT('Ctrl Pts',(1.01778355886063,-0.587617611684959,
-5.35416969787736));
#420977=CARTESIAN_POINT('Ctrl Pts',(1.35704474514751,2.29132775890901E-15,
-5.3125030312107));
#420978=CARTESIAN_POINT('Ctrl Pts',(1.01778355886063,0.587617611684963,
-5.27083636454403));
#420979=CARTESIAN_POINT('Ctrl Pts',(0.678522372573755,1.17523522336992,
-5.22916969787736));
#420980=CARTESIAN_POINT('Ctrl Pts',(0.,1.17523522336992,-5.1875030312107));
#420981=CARTESIAN_POINT('Ctrl Pts',(-0.678522372573754,1.17523522336992,
-5.14583636454403));
#420982=CARTESIAN_POINT('Ctrl Pts',(-1.01778355886063,0.587617611684963,
-5.10416969787736));
#420983=CARTESIAN_POINT('Ctrl Pts',(-1.35704474514751,2.62370785959794E-15,
-5.0625030312107));
#420984=CARTESIAN_POINT('Ctrl Pts',(-1.01778355886063,-0.587617611684958,
-5.02083636454403));
#420985=CARTESIAN_POINT('Ctrl Pts',(-0.678522372573755,-1.17523522336992,
-4.97916969787736));
#420986=CARTESIAN_POINT('Ctrl Pts',(-1.4392480545452E-16,-1.17523522336992,
-4.9375030312107));
#420987=CARTESIAN_POINT('Ctrl Pts',(0.678522372573754,-1.17523522336992,
-4.89583636454403));
#420988=CARTESIAN_POINT('Ctrl Pts',(1.01778355886063,-0.587617611684959,
-4.85416969787736));
#420989=CARTESIAN_POINT('Ctrl Pts',(1.35704474514751,2.29132775890901E-15,
-4.8125030312107));
#420990=CARTESIAN_POINT('Ctrl Pts',(1.01778355886063,0.587617611684963,
-4.77083636454403));
#420991=CARTESIAN_POINT('Ctrl Pts',(0.678522372573755,1.17523522336992,
-4.72916969787736));
#420992=CARTESIAN_POINT('Ctrl Pts',(0.,1.17523522336992,-4.6875030312107));
#420993=CARTESIAN_POINT('Ctrl Pts',(-0.678522372573754,1.17523522336992,
-4.64583636454403));
#420994=CARTESIAN_POINT('Ctrl Pts',(-1.01778355886063,0.587617611684963,
-4.60416969787736));
#420995=CARTESIAN_POINT('Ctrl Pts',(-1.35704474514751,2.62370785959794E-15,
-4.5625030312107));
#420996=CARTESIAN_POINT('Ctrl Pts',(-1.01778355886063,-0.587617611684958,
-4.52083636454403));
#420997=CARTESIAN_POINT('Ctrl Pts',(-0.678522372573755,-1.17523522336992,
-4.47916969787736));
#420998=CARTESIAN_POINT('Ctrl Pts',(-1.4392480545452E-16,-1.17523522336992,
-4.4375030312107));
#420999=CARTESIAN_POINT('Ctrl Pts',(0.678522372573754,-1.17523522336992,
-4.39583636454403));
#421000=CARTESIAN_POINT('Ctrl Pts',(1.01778355886063,-0.587617611684959,
-4.35416969787736));
#421001=CARTESIAN_POINT('Ctrl Pts',(1.35704474514751,2.29132775890901E-15,
-4.3125030312107));
#421002=CARTESIAN_POINT('Ctrl Pts',(1.01778355886063,0.587617611684963,
-4.27083636454403));
#421003=CARTESIAN_POINT('Ctrl Pts',(0.678522372573755,1.17523522336992,
-4.22916969787736));
#421004=CARTESIAN_POINT('Ctrl Pts',(0.,1.17523522336992,-4.1875030312107));
#421005=CARTESIAN_POINT('Ctrl Pts',(-0.678522372573754,1.17523522336992,
-4.14583636454403));
#421006=CARTESIAN_POINT('Ctrl Pts',(-1.01778355886063,0.587617611684963,
-4.10416969787736));
#421007=CARTESIAN_POINT('Ctrl Pts',(-1.35704474514751,2.62370785959794E-15,
-4.0625030312107));
#421008=CARTESIAN_POINT('Ctrl Pts',(-1.01778355886063,-0.587617611684958,
-4.02083636454403));
#421009=CARTESIAN_POINT('Ctrl Pts',(-0.678522372573755,-1.17523522336992,
-3.97916969787736));
#421010=CARTESIAN_POINT('Ctrl Pts',(-1.4392480545452E-16,-1.17523522336992,
-3.93750303121069));
#421011=CARTESIAN_POINT('Ctrl Pts',(0.678522372573754,-1.17523522336992,
-3.89583636454403));
#421012=CARTESIAN_POINT('Ctrl Pts',(1.01778355886063,-0.587617611684959,
-3.85416969787736));
#421013=CARTESIAN_POINT('Ctrl Pts',(1.35704474514751,2.29132775890901E-15,
-3.8125030312107));
#421014=CARTESIAN_POINT('Ctrl Pts',(1.01778355886063,0.587617611684963,
-3.77083636454403));
#421015=CARTESIAN_POINT('Ctrl Pts',(0.678522372573755,1.17523522336992,
-3.72916969787736));
#421016=CARTESIAN_POINT('Ctrl Pts',(0.,1.17523522336992,-3.6875030312107));
#421017=CARTESIAN_POINT('Ctrl Pts',(-0.678522372573754,1.17523522336992,
-3.64583636454403));
#421018=CARTESIAN_POINT('Ctrl Pts',(-1.01778355886063,0.587617611684963,
-3.60416969787736));
#421019=CARTESIAN_POINT('Ctrl Pts',(-1.35704474514751,2.62370785959794E-15,
-3.5625030312107));
#421020=CARTESIAN_POINT('Ctrl Pts',(-1.01778355886063,-0.587617611684958,
-3.52083636454403));
#421021=CARTESIAN_POINT('Ctrl Pts',(-0.678522372573755,-1.17523522336992,
-3.47916969787736));
#421022=CARTESIAN_POINT('Ctrl Pts',(-1.4392480545452E-16,-1.17523522336992,
-3.4375030312107));
#421023=CARTESIAN_POINT('Ctrl Pts',(0.678522372573754,-1.17523522336992,
-3.39583636454403));
#421024=CARTESIAN_POINT('Ctrl Pts',(1.01778355886063,-0.587617611684959,
-3.35416969787736));
#421025=CARTESIAN_POINT('Ctrl Pts',(1.35704474514751,2.29132775890901E-15,
-3.3125030312107));
#421026=CARTESIAN_POINT('Ctrl Pts',(1.01778355886063,0.587617611684963,
-3.27083636454403));
#421027=CARTESIAN_POINT('Ctrl Pts',(0.678522372573755,1.17523522336992,
-3.22916969787736));
#421028=CARTESIAN_POINT('Ctrl Pts',(0.,1.17523522336992,-3.1875030312107));
#421029=CARTESIAN_POINT('Ctrl Pts',(-0.678522372573754,1.17523522336992,
-3.14583636454403));
#421030=CARTESIAN_POINT('Ctrl Pts',(-1.01778355886063,0.587617611684963,
-3.10416969787736));
#421031=CARTESIAN_POINT('Ctrl Pts',(-1.35704474514751,2.62370785959794E-15,
-3.0625030312107));
#421032=CARTESIAN_POINT('Ctrl Pts',(-1.01778355886063,-0.587617611684958,
-3.02083636454403));
#421033=CARTESIAN_POINT('Ctrl Pts',(-0.678522372573755,-1.17523522336992,
-2.97916969787736));
#421034=CARTESIAN_POINT('Ctrl Pts',(-1.4392480545452E-16,-1.17523522336992,
-2.9375030312107));
#421035=CARTESIAN_POINT('Ctrl Pts',(0.678522372573754,-1.17523522336992,
-2.89583636454403));
#421036=CARTESIAN_POINT('Ctrl Pts',(1.01778355886063,-0.587617611684959,
-2.85416969787736));
#421037=CARTESIAN_POINT('Ctrl Pts',(1.35704474514751,2.29132775890901E-15,
-2.8125030312107));
#421038=CARTESIAN_POINT('Ctrl Pts',(1.01778355886063,0.587617611684963,
-2.77083636454403));
#421039=CARTESIAN_POINT('Ctrl Pts',(0.678522372573755,1.17523522336992,
-2.72916969787736));
#421040=CARTESIAN_POINT('Ctrl Pts',(0.,1.17523522336992,-2.6875030312107));
#421041=CARTESIAN_POINT('Ctrl Pts',(-0.678522372573754,1.17523522336992,
-2.64583636454403));
#421042=CARTESIAN_POINT('Ctrl Pts',(-1.01778355886063,0.587617611684963,
-2.60416969787736));
#421043=CARTESIAN_POINT('Ctrl Pts',(-1.35704474514751,2.62370785959794E-15,
-2.56250303121069));
#421044=CARTESIAN_POINT('Ctrl Pts',(-1.01778355886063,-0.587617611684958,
-2.52083636454403));
#421045=CARTESIAN_POINT('Ctrl Pts',(-0.678522372573755,-1.17523522336992,
-2.47916969787736));
#421046=CARTESIAN_POINT('Ctrl Pts',(-1.4392480545452E-16,-1.17523522336992,
-2.4375030312107));
#421047=CARTESIAN_POINT('Ctrl Pts',(0.678522372573754,-1.17523522336992,
-2.39583636454403));
#421048=CARTESIAN_POINT('Ctrl Pts',(1.01778355886063,-0.587617611684959,
-2.35416969787736));
#421049=CARTESIAN_POINT('Ctrl Pts',(1.35704474514751,2.29132775890901E-15,
-2.31250303121069));
#421050=CARTESIAN_POINT('Ctrl Pts',(1.01778355886063,0.587617611684963,
-2.27083636454403));
#421051=CARTESIAN_POINT('Ctrl Pts',(0.678522372573755,1.17523522336992,
-2.22916969787736));
#421052=CARTESIAN_POINT('Ctrl Pts',(0.,1.17523522336992,-2.1875030312107));
#421053=CARTESIAN_POINT('Ctrl Pts',(-0.678522372573754,1.17523522336992,
-2.14583636454403));
#421054=CARTESIAN_POINT('Ctrl Pts',(-1.01778355886063,0.587617611684963,
-2.10416969787736));
#421055=CARTESIAN_POINT('Ctrl Pts',(-1.35704474514751,2.62370785959794E-15,
-2.0625030312107));
#421056=CARTESIAN_POINT('Ctrl Pts',(-1.01778355886063,-0.587617611684958,
-2.02083636454403));
#421057=CARTESIAN_POINT('Ctrl Pts',(-0.678522372573755,-1.17523522336992,
-1.97916969787736));
#421058=CARTESIAN_POINT('Ctrl Pts',(-1.4392480545452E-16,-1.17523522336992,
-1.9375030312107));
#421059=CARTESIAN_POINT('Ctrl Pts',(0.678522372573754,-1.17523522336992,
-1.89583636454403));
#421060=CARTESIAN_POINT('Ctrl Pts',(1.01778355886063,-0.587617611684959,
-1.85416969787736));
#421061=CARTESIAN_POINT('Ctrl Pts',(1.35704474514751,2.29132775890901E-15,
-1.8125030312107));
#421062=CARTESIAN_POINT('Ctrl Pts',(1.01778355886063,0.587617611684963,
-1.77083636454403));
#421063=CARTESIAN_POINT('Ctrl Pts',(0.678522372573755,1.17523522336992,
-1.72916969787736));
#421064=CARTESIAN_POINT('Ctrl Pts',(0.,1.17523522336992,-1.6875030312107));
#421065=CARTESIAN_POINT('Ctrl Pts',(-0.678522372573754,1.17523522336992,
-1.64583636454403));
#421066=CARTESIAN_POINT('Ctrl Pts',(-1.01778355886063,0.587617611684963,
-1.60416969787736));
#421067=CARTESIAN_POINT('Ctrl Pts',(-1.35704474514751,2.62370785959794E-15,
-1.5625030312107));
#421068=CARTESIAN_POINT('Ctrl Pts',(-1.01778355886063,-0.587617611684958,
-1.52083636454403));
#421069=CARTESIAN_POINT('Ctrl Pts',(-0.678522372573755,-1.17523522336992,
-1.47916969787736));
#421070=CARTESIAN_POINT('Ctrl Pts',(-1.4392480545452E-16,-1.17523522336992,
-1.4375030312107));
#421071=CARTESIAN_POINT('Ctrl Pts',(0.678522372573754,-1.17523522336992,
-1.39583636454403));
#421072=CARTESIAN_POINT('Ctrl Pts',(1.01778355886063,-0.587617611684959,
-1.35416969787736));
#421073=CARTESIAN_POINT('Ctrl Pts',(1.35704474514751,2.29132775890901E-15,
-1.3125030312107));
#421074=CARTESIAN_POINT('Ctrl Pts',(1.01778355886063,0.587617611684963,
-1.27083636454403));
#421075=CARTESIAN_POINT('Ctrl Pts',(0.678522372573755,1.17523522336992,
-1.22916969787736));
#421076=CARTESIAN_POINT('Ctrl Pts',(0.,1.17523522336992,-1.1875030312107));
#421077=CARTESIAN_POINT('Ctrl Pts',(-0.678522372573754,1.17523522336992,
-1.14583636454403));
#421078=CARTESIAN_POINT('Ctrl Pts',(-1.01778355886063,0.587617611684963,
-1.10416969787736));
#421079=CARTESIAN_POINT('Ctrl Pts',(-1.35704474514751,2.62370785959794E-15,
-1.0625030312107));
#421080=CARTESIAN_POINT('Ctrl Pts',(-1.01778355886063,-0.587617611684958,
-1.02083636454403));
#421081=CARTESIAN_POINT('Ctrl Pts',(-0.678522372573755,-1.17523522336992,
-0.979169697877363));
#421082=CARTESIAN_POINT('Ctrl Pts',(-1.4392480545452E-16,-1.17523522336992,
-0.937503031210696));
#421083=CARTESIAN_POINT('Ctrl Pts',(0.678522372573754,-1.17523522336992,
-0.895836364544029));
#421084=CARTESIAN_POINT('Ctrl Pts',(1.01778355886063,-0.587617611684959,
-0.854169697877363));
#421085=CARTESIAN_POINT('Ctrl Pts',(1.35704474514751,2.29132775890901E-15,
-0.812503031210696));
#421086=CARTESIAN_POINT('Ctrl Pts',(1.01778355886063,0.587617611684963,
-0.770836364544028));
#421087=CARTESIAN_POINT('Ctrl Pts',(0.678522372573755,1.17523522336992,
-0.729169697877363));
#421088=CARTESIAN_POINT('Ctrl Pts',(0.,1.17523522336992,-0.687503031210696));
#421089=CARTESIAN_POINT('Ctrl Pts',(-0.678522372573754,1.17523522336992,
-0.64583636454403));
#421090=CARTESIAN_POINT('Ctrl Pts',(-1.01778355886063,0.587617611684963,
-0.604169697877363));
#421091=CARTESIAN_POINT('Ctrl Pts',(-1.35704474514751,2.62370785959794E-15,
-0.562503031210696));
#421092=CARTESIAN_POINT('Ctrl Pts',(-1.01778355886063,-0.587617611684958,
-0.52083636454403));
#421093=CARTESIAN_POINT('Ctrl Pts',(-0.678522372573755,-1.17523522336992,
-0.479169697877363));
#421094=CARTESIAN_POINT('Ctrl Pts',(-1.4392480545452E-16,-1.17523522336992,
-0.437503031210695));
#421095=CARTESIAN_POINT('Ctrl Pts',(0.678522372573754,-1.17523522336992,
-0.39583636454403));
#421096=CARTESIAN_POINT('Ctrl Pts',(1.01778355886063,-0.587617611684959,
-0.354169697877363));
#421097=CARTESIAN_POINT('Ctrl Pts',(1.35704474514751,2.29132775890901E-15,
-0.312503031210695));
#421098=CARTESIAN_POINT('Ctrl Pts',(1.01778355886063,0.587617611684963,
-0.27083636454403));
#421099=CARTESIAN_POINT('Ctrl Pts',(0.678522372573755,1.17523522336992,
-0.229169697877362));
#421100=CARTESIAN_POINT('Ctrl Pts',(0.,1.17523522336992,-0.187503031210695));
#421101=CARTESIAN_POINT('Ctrl Pts',(-0.678522372573754,1.17523522336992,
-0.14583636454403));
#421102=CARTESIAN_POINT('Ctrl Pts',(-1.01778355886063,0.587617611684963,
-0.104169697877362));
#421103=CARTESIAN_POINT('Ctrl Pts',(-1.35704474514751,2.62370785959794E-15,
-0.0625030312106968));
#421104=CARTESIAN_POINT('Ctrl Pts',(-1.01778355886063,-0.587617611684958,
-0.0208363645440295));
#421105=CARTESIAN_POINT('Ctrl Pts',(-0.678522372573755,-1.17523522336992,
0.0208303021226378));
#421106=CARTESIAN_POINT('Ctrl Pts',(-1.4392480545452E-16,-1.17523522336992,
0.0624969687893033));
#421107=CARTESIAN_POINT('Ctrl Pts',(0.678522372573754,-1.17523522336992,
0.104163635455971));
#421108=CARTESIAN_POINT('Ctrl Pts',(1.01778355886063,-0.587617611684959,
0.145830302122638));
#421109=CARTESIAN_POINT('Ctrl Pts',(1.35704474514751,2.29132775890901E-15,
0.187496968789303));
#421110=CARTESIAN_POINT('Ctrl Pts',(1.01778355886063,0.587617611684963,
0.229163635455971));
#421111=CARTESIAN_POINT('Ctrl Pts',(0.678522372573755,1.17523522336992,
0.270830302122638));
#421112=CARTESIAN_POINT('Ctrl Pts',(0.,1.17523522336992,0.312496968789304));
#421113=CARTESIAN_POINT('Ctrl Pts',(-0.678522372573754,1.17523522336992,
0.354163635455971));
#421114=CARTESIAN_POINT('Ctrl Pts',(-1.01778355886063,0.587617611684963,
0.395830302122638));
#421115=CARTESIAN_POINT('Ctrl Pts',(-1.35704474514751,2.62370785959794E-15,
0.437496968789304));
#421116=CARTESIAN_POINT('Ctrl Pts',(-1.01778355886063,-0.587617611684958,
0.479163635455971));
#421117=CARTESIAN_POINT('Ctrl Pts',(-0.678522372573755,-1.17523522336992,
0.520830302122638));
#421118=CARTESIAN_POINT('Ctrl Pts',(-1.4392480545452E-16,-1.17523522336992,
0.562496968789304));
#421119=CARTESIAN_POINT('Ctrl Pts',(0.678522372573754,-1.17523522336992,
0.604163635455971));
#421120=CARTESIAN_POINT('Ctrl Pts',(1.01778355886063,-0.587617611684959,
0.645830302122637));
#421121=CARTESIAN_POINT('Ctrl Pts',(1.35704474514751,2.29132775890901E-15,
0.687496968789304));
#421122=CARTESIAN_POINT('Ctrl Pts',(1.01778355886063,0.587617611684963,
0.729163635455971));
#421123=CARTESIAN_POINT('Ctrl Pts',(0.678522372573755,1.17523522336992,
0.770830302122637));
#421124=CARTESIAN_POINT('Ctrl Pts',(0.,1.17523522336992,0.812496968789304));
#421125=CARTESIAN_POINT('Ctrl Pts',(-0.678522372573754,1.17523522336992,
0.854163635455971));
#421126=CARTESIAN_POINT('Ctrl Pts',(-1.01778355886063,0.587617611684963,
0.895830302122637));
#421127=CARTESIAN_POINT('Ctrl Pts',(-1.35704474514751,2.62370785959794E-15,
0.937496968789304));
#421128=CARTESIAN_POINT('Ctrl Pts',(-1.01778355886063,-0.587617611684958,
0.979163635455971));
#421129=CARTESIAN_POINT('Ctrl Pts',(-0.678522372573755,-1.17523522336992,
1.02083030212264));
#421130=CARTESIAN_POINT('Ctrl Pts',(-1.4392480545452E-16,-1.17523522336992,
1.0624969687893));
#421131=CARTESIAN_POINT('Ctrl Pts',(0.678522372573754,-1.17523522336992,
1.10416363545597));
#421132=CARTESIAN_POINT('Ctrl Pts',(1.01778355886063,-0.587617611684959,
1.14583030212264));
#421133=CARTESIAN_POINT('Ctrl Pts',(1.35704474514751,2.29132775890901E-15,
1.1874969687893));
#421134=CARTESIAN_POINT('Ctrl Pts',(1.01778355886063,0.587617611684963,
1.22916363545597));
#421135=CARTESIAN_POINT('Ctrl Pts',(0.678522372573755,1.17523522336992,
1.27083030212264));
#421136=CARTESIAN_POINT('Ctrl Pts',(0.,1.17523522336992,1.3124969687893));
#421137=CARTESIAN_POINT('Ctrl Pts',(-0.678522372573754,1.17523522336992,
1.35416363545597));
#421138=CARTESIAN_POINT('Ctrl Pts',(-1.01778355886063,0.587617611684963,
1.39583030212264));
#421139=CARTESIAN_POINT('Ctrl Pts',(-1.35704474514751,2.62370785959794E-15,
1.4374969687893));
#421140=CARTESIAN_POINT('Ctrl Pts',(-1.01778355886063,-0.587617611684958,
1.47916363545597));
#421141=CARTESIAN_POINT('Ctrl Pts',(-0.678522372573755,-1.17523522336992,
1.52083030212264));
#421142=CARTESIAN_POINT('Ctrl Pts',(-1.4392480545452E-16,-1.17523522336992,
1.5624969687893));
#421143=CARTESIAN_POINT('Ctrl Pts',(0.678522372573754,-1.17523522336992,
1.60416363545597));
#421144=CARTESIAN_POINT('Ctrl Pts',(1.01778355886063,-0.587617611684959,
1.64583030212264));
#421145=CARTESIAN_POINT('Ctrl Pts',(1.35704474514751,2.29132775890901E-15,
1.68749696878931));
#421146=CARTESIAN_POINT('Ctrl Pts',(1.01778355886063,0.587617611684963,
1.72916363545597));
#421147=CARTESIAN_POINT('Ctrl Pts',(0.678522372573755,1.17523522336992,
1.77083030212264));
#421148=CARTESIAN_POINT('Ctrl Pts',(0.,1.17523522336992,1.8124969687893));
#421149=CARTESIAN_POINT('Ctrl Pts',(-0.678522372573754,1.17523522336992,
1.85416363545597));
#421150=CARTESIAN_POINT('Ctrl Pts',(-1.01778355886063,0.587617611684963,
1.89583030212264));
#421151=CARTESIAN_POINT('Ctrl Pts',(-1.35704474514751,2.62370785959794E-15,
1.9374969687893));
#421152=CARTESIAN_POINT('Ctrl Pts',(-1.01778355886063,-0.587617611684958,
1.97916363545597));
#421153=CARTESIAN_POINT('Ctrl Pts',(-0.678522372573755,-1.17523522336992,
2.02083030212264));
#421154=CARTESIAN_POINT('Ctrl Pts',(-1.4392480545452E-16,-1.17523522336992,
2.06249696878931));
#421155=CARTESIAN_POINT('Ctrl Pts',(0.678522372573754,-1.17523522336992,
2.10416363545597));
#421156=CARTESIAN_POINT('Ctrl Pts',(1.01778355886063,-0.587617611684959,
2.14583030212264));
#421157=CARTESIAN_POINT('Ctrl Pts',(1.35704474514751,2.29132775890901E-15,
2.18749696878931));
#421158=CARTESIAN_POINT('Ctrl Pts',(1.01778355886063,0.587617611684963,
2.22916363545597));
#421159=CARTESIAN_POINT('Ctrl Pts',(0.678522372573755,1.17523522336992,
2.27083030212264));
#421160=CARTESIAN_POINT('Ctrl Pts',(0.,1.17523522336992,2.31249696878931));
#421161=CARTESIAN_POINT('Ctrl Pts',(-0.678522372573754,1.17523522336992,
2.35416363545597));
#421162=CARTESIAN_POINT('Ctrl Pts',(-1.01778355886063,0.587617611684963,
2.39583030212264));
#421163=CARTESIAN_POINT('Ctrl Pts',(-1.35704474514751,2.62370785959794E-15,
2.43749696878931));
#421164=CARTESIAN_POINT('Ctrl Pts',(-1.01778355886063,-0.587617611684958,
2.47916363545597));
#421165=CARTESIAN_POINT('Ctrl Pts',(-0.678522372573755,-1.17523522336992,
2.52083030212264));
#421166=CARTESIAN_POINT('Ctrl Pts',(-1.4392480545452E-16,-1.17523522336992,
2.56249696878931));
#421167=CARTESIAN_POINT('Ctrl Pts',(0.678522372573754,-1.17523522336992,
2.60416363545597));
#421168=CARTESIAN_POINT('Ctrl Pts',(1.01778355886063,-0.587617611684959,
2.64583030212264));
#421169=CARTESIAN_POINT('Ctrl Pts',(1.35704474514751,2.29132775890901E-15,
2.68749696878931));
#421170=CARTESIAN_POINT('Ctrl Pts',(1.01778355886063,0.587617611684963,
2.72916363545597));
#421171=CARTESIAN_POINT('Ctrl Pts',(0.678522372573755,1.17523522336992,
2.77083030212264));
#421172=CARTESIAN_POINT('Ctrl Pts',(0.,1.17523522336992,2.8124969687893));
#421173=CARTESIAN_POINT('Ctrl Pts',(-0.678522372573754,1.17523522336992,
2.85416363545597));
#421174=CARTESIAN_POINT('Ctrl Pts',(-1.01778355886063,0.587617611684963,
2.89583030212264));
#421175=CARTESIAN_POINT('Ctrl Pts',(-1.35704474514751,2.62370785959794E-15,
2.9374969687893));
#421176=CARTESIAN_POINT('Ctrl Pts',(-1.01778355886063,-0.587617611684958,
2.97916363545597));
#421177=CARTESIAN_POINT('Ctrl Pts',(-0.678522372573755,-1.17523522336992,
3.02083030212264));
#421178=CARTESIAN_POINT('Ctrl Pts',(-1.4392480545452E-16,-1.17523522336992,
3.0624969687893));
#421179=CARTESIAN_POINT('Ctrl Pts',(0.678522372573754,-1.17523522336992,
3.10416363545597));
#421180=CARTESIAN_POINT('Ctrl Pts',(1.01778355886063,-0.587617611684959,
3.14583030212264));
#421181=CARTESIAN_POINT('Ctrl Pts',(1.35704474514751,2.29132775890901E-15,
3.1874969687893));
#421182=CARTESIAN_POINT('Ctrl Pts',(1.01778355886063,0.587617611684963,
3.22916363545597));
#421183=CARTESIAN_POINT('Ctrl Pts',(0.678522372573755,1.17523522336992,
3.27083030212264));
#421184=CARTESIAN_POINT('Ctrl Pts',(0.,1.17523522336992,3.3124969687893));
#421185=CARTESIAN_POINT('Ctrl Pts',(-0.678522372573754,1.17523522336992,
3.35416363545597));
#421186=CARTESIAN_POINT('Ctrl Pts',(-1.01778355886063,0.587617611684963,
3.39583030212264));
#421187=CARTESIAN_POINT('Ctrl Pts',(-1.35704474514751,2.62370785959794E-15,
3.4374969687893));
#421188=CARTESIAN_POINT('Ctrl Pts',(-1.01778355886063,-0.587617611684958,
3.47916363545597));
#421189=CARTESIAN_POINT('Ctrl Pts',(-0.678522372573755,-1.17523522336992,
3.52083030212264));
#421190=CARTESIAN_POINT('Ctrl Pts',(-1.4392480545452E-16,-1.17523522336992,
3.5624969687893));
#421191=CARTESIAN_POINT('Ctrl Pts',(0.678522372573754,-1.17523522336992,
3.60416363545597));
#421192=CARTESIAN_POINT('Ctrl Pts',(1.01778355886063,-0.587617611684959,
3.64583030212264));
#421193=CARTESIAN_POINT('Ctrl Pts',(1.35704474514751,2.29132775890901E-15,
3.6874969687893));
#421194=CARTESIAN_POINT('Ctrl Pts',(1.01778355886063,0.587617611684963,
3.72916363545597));
#421195=CARTESIAN_POINT('Ctrl Pts',(0.678522372573755,1.17523522336992,
3.77083030212264));
#421196=CARTESIAN_POINT('Ctrl Pts',(0.,1.17523522336992,3.8124969687893));
#421197=CARTESIAN_POINT('Ctrl Pts',(-0.678522372573754,1.17523522336992,
3.85416363545597));
#421198=CARTESIAN_POINT('Ctrl Pts',(-1.01778355886063,0.587617611684963,
3.89583030212264));
#421199=CARTESIAN_POINT('Ctrl Pts',(-1.35704474514751,2.62370785959794E-15,
3.9374969687893));
#421200=CARTESIAN_POINT('Ctrl Pts',(-1.01778355886063,-0.587617611684958,
3.97916363545597));
#421201=CARTESIAN_POINT('Ctrl Pts',(-0.678522372573755,-1.17523522336992,
4.02083030212264));
#421202=CARTESIAN_POINT('Ctrl Pts',(-1.4392480545452E-16,-1.17523522336992,
4.0624969687893));
#421203=CARTESIAN_POINT('Ctrl Pts',(0.678522372573754,-1.17523522336992,
4.10416363545597));
#421204=CARTESIAN_POINT('Ctrl Pts',(1.01778355886063,-0.587617611684959,
4.14583030212264));
#421205=CARTESIAN_POINT('Ctrl Pts',(1.35704474514751,2.29132775890901E-15,
4.1874969687893));
#421206=CARTESIAN_POINT('Ctrl Pts',(1.01778355886063,0.587617611684963,
4.22916363545597));
#421207=CARTESIAN_POINT('Ctrl Pts',(0.678522372573755,1.17523522336992,
4.27083030212264));
#421208=CARTESIAN_POINT('Ctrl Pts',(0.,1.17523522336992,4.3124969687893));
#421209=CARTESIAN_POINT('Ctrl Pts',(-0.678522372573754,1.17523522336992,
4.35416363545597));
#421210=CARTESIAN_POINT('Ctrl Pts',(-1.01778355886063,0.587617611684963,
4.39583030212264));
#421211=CARTESIAN_POINT('Ctrl Pts',(-1.35704474514751,2.62370785959794E-15,
4.4374969687893));
#421212=CARTESIAN_POINT('Ctrl Pts',(-1.01778355886063,-0.587617611684958,
4.47916363545597));
#421213=CARTESIAN_POINT('Ctrl Pts',(-0.678522372573755,-1.17523522336992,
4.52083030212264));
#421214=CARTESIAN_POINT('Ctrl Pts',(-1.4392480545452E-16,-1.17523522336992,
4.5624969687893));
#421215=CARTESIAN_POINT('Ctrl Pts',(0.678522372573754,-1.17523522336992,
4.60416363545597));
#421216=CARTESIAN_POINT('Ctrl Pts',(1.01778355886063,-0.587617611684959,
4.64583030212264));
#421217=CARTESIAN_POINT('Ctrl Pts',(1.35704474514751,2.29132775890901E-15,
4.6874969687893));
#421218=CARTESIAN_POINT('Ctrl Pts',(1.01778355886063,0.587617611684963,
4.72916363545597));
#421219=CARTESIAN_POINT('Ctrl Pts',(0.678522372573755,1.17523522336992,
4.77083030212264));
#421220=CARTESIAN_POINT('Ctrl Pts',(0.,1.17523522336992,4.8124969687893));
#421221=CARTESIAN_POINT('Ctrl Pts',(-0.678522372573754,1.17523522336992,
4.85416363545597));
#421222=CARTESIAN_POINT('Ctrl Pts',(-1.01778355886063,0.587617611684963,
4.89583030212264));
#421223=CARTESIAN_POINT('Ctrl Pts',(-1.35704474514751,2.62370785959794E-15,
4.9374969687893));
#421224=CARTESIAN_POINT('Ctrl Pts',(-1.01778355886063,-0.587617611684958,
4.97916363545597));
#421225=CARTESIAN_POINT('Ctrl Pts',(-0.678522372573755,-1.17523522336992,
5.02083030212264));
#421226=CARTESIAN_POINT('Ctrl Pts',(-1.4392480545452E-16,-1.17523522336992,
5.06249696878931));
#421227=CARTESIAN_POINT('Ctrl Pts',(0.678522372573754,-1.17523522336992,
5.10416363545597));
#421228=CARTESIAN_POINT('Ctrl Pts',(1.01778355886063,-0.587617611684959,
5.14583030212264));
#421229=CARTESIAN_POINT('Ctrl Pts',(1.35704474514751,2.29132775890901E-15,
5.1874969687893));
#421230=CARTESIAN_POINT('Ctrl Pts',(1.01778355886063,0.587617611684963,
5.22916363545597));
#421231=CARTESIAN_POINT('Ctrl Pts',(0.678522372573755,1.17523522336992,
5.27083030212264));
#421232=CARTESIAN_POINT('Ctrl Pts',(0.,1.17523522336992,5.3124969687893));
#421233=CARTESIAN_POINT('Ctrl Pts',(-0.678522372573754,1.17523522336992,
5.35416363545597));
#421234=CARTESIAN_POINT('Ctrl Pts',(-1.01778355886063,0.587617611684963,
5.39583030212264));
#421235=CARTESIAN_POINT('Ctrl Pts',(-1.35704474514751,2.62370785959794E-15,
5.4374969687893));
#421236=CARTESIAN_POINT('Ctrl Pts',(-1.01778355886063,-0.587617611684958,
5.47916363545597));
#421237=CARTESIAN_POINT('Ctrl Pts',(-0.678522372573755,-1.17523522336992,
5.52083030212264));
#421238=CARTESIAN_POINT('Ctrl Pts',(-1.4392480545452E-16,-1.17523522336992,
5.5624969687893));
#421239=CARTESIAN_POINT('Ctrl Pts',(0.678522372573754,-1.17523522336992,
5.60416363545597));
#421240=CARTESIAN_POINT('Ctrl Pts',(1.01778355886063,-0.587617611684959,
5.64583030212264));
#421241=CARTESIAN_POINT('Ctrl Pts',(1.35704474514751,2.29132775890901E-15,
5.6874969687893));
#421242=CARTESIAN_POINT('Ctrl Pts',(1.01778355886063,0.587617611684963,
5.72916363545597));
#421243=CARTESIAN_POINT('Ctrl Pts',(0.678522372573755,1.17523522336992,
5.77083030212264));
#421244=CARTESIAN_POINT('Ctrl Pts',(0.,1.17523522336992,5.81249696878931));
#421245=CARTESIAN_POINT('Ctrl Pts',(-0.678522372573754,1.17523522336992,
5.85416363545597));
#421246=CARTESIAN_POINT('Ctrl Pts',(-1.01778355886063,0.587617611684963,
5.89583030212264));
#421247=CARTESIAN_POINT('Ctrl Pts',(-1.35704474514751,2.62370785959794E-15,
5.93749696878931));
#421248=CARTESIAN_POINT('Ctrl Pts',(-1.01778355886063,-0.587617611684958,
5.97916363545597));
#421249=CARTESIAN_POINT('Ctrl Pts',(-0.678522372573755,-1.17523522336992,
6.02083030212264));
#421250=CARTESIAN_POINT('Ctrl Pts',(-1.4392480545452E-16,-1.17523522336992,
6.06249696878931));
#421251=CARTESIAN_POINT('Ctrl Pts',(0.678522372573754,-1.17523522336992,
6.10416363545597));
#421252=CARTESIAN_POINT('Ctrl Pts',(1.01778355886063,-0.587617611684959,
6.14583030212264));
#421253=CARTESIAN_POINT('Ctrl Pts',(1.35704474514751,2.29132775890901E-15,
6.18749696878931));
#421254=CARTESIAN_POINT('Ctrl Pts',(1.01778355886063,0.587617611684963,
6.22916363545597));
#421255=CARTESIAN_POINT('Ctrl Pts',(0.678522372573755,1.17523522336992,
6.27083030212264));
#421256=CARTESIAN_POINT('Ctrl Pts',(0.,1.17523522336992,6.31249696878931));
#421257=CARTESIAN_POINT('Ctrl Pts',(-0.678522372573754,1.17523522336992,
6.35416363545597));
#421258=CARTESIAN_POINT('Ctrl Pts',(-1.01778355886063,0.587617611684963,
6.39583030212264));
#421259=CARTESIAN_POINT('Ctrl Pts',(-1.35704474514751,2.62370785959794E-15,
6.43749696878931));
#421260=CARTESIAN_POINT('Ctrl Pts',(-1.01778355886063,-0.587617611684958,
6.47916363545597));
#421261=CARTESIAN_POINT('Ctrl Pts',(-0.678522372573755,-1.17523522336992,
6.52083030212264));
#421262=CARTESIAN_POINT('Ctrl Pts',(-1.4392480545452E-16,-1.17523522336992,
6.5624969687893));
#421263=CARTESIAN_POINT('Ctrl Pts',(0.678522372573754,-1.17523522336992,
6.60416363545597));
#421264=CARTESIAN_POINT('Ctrl Pts',(1.01778355886063,-0.587617611684959,
6.64583030212264));
#421265=CARTESIAN_POINT('Ctrl Pts',(1.35704474514751,2.29132775890901E-15,
6.6874969687893));
#421266=CARTESIAN_POINT('Ctrl Pts',(1.01778355886063,0.587617611684963,
6.72916363545597));
#421267=CARTESIAN_POINT('Ctrl Pts',(0.678522372573755,1.17523522336992,
6.77083030212264));
#421268=CARTESIAN_POINT('Ctrl Pts',(0.,1.17523522336992,6.8124969687893));
#421269=CARTESIAN_POINT('Ctrl Pts',(-0.678522372573754,1.17523522336992,
6.85416363545597));
#421270=CARTESIAN_POINT('Ctrl Pts',(-1.01778355886063,0.587617611684963,
6.89583030212264));
#421271=CARTESIAN_POINT('Ctrl Pts',(-1.35704474514751,2.62370785959794E-15,
6.9374969687893));
#421272=CARTESIAN_POINT('Ctrl Pts',(-1.01778355886063,-0.587617611684958,
6.97916363545597));
#421273=CARTESIAN_POINT('Ctrl Pts',(-0.678522372573755,-1.17523522336992,
7.02083030212264));
#421274=CARTESIAN_POINT('Ctrl Pts',(-1.4392480545452E-16,-1.17523522336992,
7.0624969687893));
#421275=CARTESIAN_POINT('Ctrl Pts',(0.678522372573754,-1.17523522336992,
7.10416363545597));
#421276=CARTESIAN_POINT('Ctrl Pts',(1.01778355886063,-0.587617611684959,
7.14583030212264));
#421277=CARTESIAN_POINT('Ctrl Pts',(1.35704474514751,2.29132775890901E-15,
7.1874969687893));
#421278=CARTESIAN_POINT('Ctrl Pts',(1.01778355886063,0.587617611684963,
7.22916363545597));
#421279=CARTESIAN_POINT('Ctrl Pts',(0.678522372573755,1.17523522336992,
7.27083030212264));
#421280=CARTESIAN_POINT('Ctrl Pts',(0.,1.17523522336992,7.3124969687893));
#421281=CARTESIAN_POINT('Ctrl Pts',(-0.678522372573754,1.17523522336992,
7.35416363545597));
#421282=CARTESIAN_POINT('Ctrl Pts',(-1.01778355886063,0.587617611684963,
7.39583030212264));
#421283=CARTESIAN_POINT('Ctrl Pts',(-1.35704474514751,2.62370785959794E-15,
7.4374969687893));
#421284=CARTESIAN_POINT('Ctrl Pts',(-1.01778355886063,-0.587617611684958,
7.47916363545597));
#421285=CARTESIAN_POINT('Ctrl Pts',(-0.678522372573755,-1.17523522336992,
7.52083030212264));
#421286=CARTESIAN_POINT('Ctrl Pts',(-1.4392480545452E-16,-1.17523522336992,
7.5624969687893));
#421287=CARTESIAN_POINT('Ctrl Pts',(0.678522372573754,-1.17523522336992,
7.60416363545597));
#421288=CARTESIAN_POINT('Ctrl Pts',(1.01778355886063,-0.587617611684959,
7.64583030212264));
#421289=CARTESIAN_POINT('Ctrl Pts',(1.35704474514751,2.29132775890901E-15,
7.6874969687893));
#421290=CARTESIAN_POINT('Ctrl Pts',(1.01778355886063,0.587617611684963,
7.72916363545597));
#421291=CARTESIAN_POINT('Ctrl Pts',(0.678522372573755,1.17523522336992,
7.77083030212264));
#421292=CARTESIAN_POINT('Ctrl Pts',(0.,1.17523522336992,7.8124969687893));
#421293=CARTESIAN_POINT('Ctrl Pts',(-0.678522372573754,1.17523522336992,
7.85416363545597));
#421294=CARTESIAN_POINT('Ctrl Pts',(-1.01778355886063,0.587617611684963,
7.89583030212264));
#421295=CARTESIAN_POINT('Ctrl Pts',(-1.35704474514751,2.62370785959794E-15,
7.93749696878931));
#421296=CARTESIAN_POINT('Ctrl Pts',(-1.01778355886063,-0.587617611684958,
7.97916363545597));
#421297=CARTESIAN_POINT('Ctrl Pts',(-0.678522372573755,-1.17523522336992,
8.02083030212264));
#421298=CARTESIAN_POINT('Ctrl Pts',(-1.4392480545452E-16,-1.17523522336992,
8.0624969687893));
#421299=CARTESIAN_POINT('Ctrl Pts',(0.678522372573754,-1.17523522336992,
8.10416363545597));
#421300=CARTESIAN_POINT('Ctrl Pts',(1.01778355886063,-0.587617611684959,
8.14583030212264));
#421301=CARTESIAN_POINT('Ctrl Pts',(1.35704474514751,2.29132775890901E-15,
8.1874969687893));
#421302=CARTESIAN_POINT('Ctrl Pts',(1.01778355886063,0.587617611684963,
8.22916363545597));
#421303=CARTESIAN_POINT('Ctrl Pts',(0.678522372573755,1.17523522336992,
8.27083030212264));
#421304=CARTESIAN_POINT('Ctrl Pts',(0.,1.17523522336992,8.3124969687893));
#421305=CARTESIAN_POINT('Ctrl Pts',(-0.678522372573754,1.17523522336992,
8.35416363545597));
#421306=CARTESIAN_POINT('Ctrl Pts',(-1.01778355886063,0.587617611684963,
8.39583030212264));
#421307=CARTESIAN_POINT('Ctrl Pts',(-1.35704474514751,2.62370785959794E-15,
8.4374969687893));
#421308=CARTESIAN_POINT('Ctrl Pts',(-1.01778355886063,-0.587617611684958,
8.47916363545597));
#421309=CARTESIAN_POINT('Ctrl Pts',(-0.678522372573755,-1.17523522336992,
8.52083030212264));
#421310=CARTESIAN_POINT('Ctrl Pts',(-1.4392480545452E-16,-1.17523522336992,
8.5624969687893));
#421311=CARTESIAN_POINT('Ctrl Pts',(0.678522372573754,-1.17523522336992,
8.60416363545597));
#421312=CARTESIAN_POINT('Ctrl Pts',(1.01778355886063,-0.587617611684959,
8.64583030212264));
#421313=CARTESIAN_POINT('Ctrl Pts',(1.35704474514751,2.29132775890901E-15,
8.6874969687893));
#421314=CARTESIAN_POINT('Ctrl Pts',(1.01778355886063,0.587617611684963,
8.72916363545597));
#421315=CARTESIAN_POINT('Ctrl Pts',(0.678522372573755,1.17523522336992,
8.77083030212264));
#421316=CARTESIAN_POINT('Ctrl Pts',(0.,1.17523522336992,8.8124969687893));
#421317=CARTESIAN_POINT('Ctrl Pts',(-0.678522372573754,1.17523522336992,
8.85416363545597));
#421318=CARTESIAN_POINT('Ctrl Pts',(-1.01778355886063,0.587617611684963,
8.89583030212264));
#421319=CARTESIAN_POINT('Ctrl Pts',(-1.35704474514751,2.62370785959794E-15,
8.9374969687893));
#421320=CARTESIAN_POINT('Ctrl Pts',(-1.01778355886063,-0.587617611684958,
8.97916363545597));
#421321=CARTESIAN_POINT('Ctrl Pts',(-0.678522372573755,-1.17523522336992,
9.02083030212264));
#421322=CARTESIAN_POINT('Ctrl Pts',(-1.4392480545452E-16,-1.17523522336992,
9.06249696878931));
#421323=CARTESIAN_POINT('Ctrl Pts',(0.678522372573754,-1.17523522336992,
9.10416363545597));
#421324=CARTESIAN_POINT('Ctrl Pts',(1.01778355886063,-0.587617611684959,
9.14583030212264));
#421325=CARTESIAN_POINT('Ctrl Pts',(1.35704474514751,2.29132775890901E-15,
9.1874969687893));
#421326=CARTESIAN_POINT('Ctrl Pts',(1.01778355886063,0.587617611684963,
9.22916363545597));
#421327=CARTESIAN_POINT('Ctrl Pts',(0.678522372573755,1.17523522336992,
9.27083030212264));
#421328=CARTESIAN_POINT('Ctrl Pts',(0.,1.17523522336992,9.31249696878931));
#421329=CARTESIAN_POINT('Ctrl Pts',(-0.678522372573754,1.17523522336992,
9.35416363545597));
#421330=CARTESIAN_POINT('Ctrl Pts',(-1.01778355886063,0.587617611684963,
9.39583030212263));
#421331=CARTESIAN_POINT('Ctrl Pts',(-1.35704474514751,2.62370785959794E-15,
9.4374969687893));
#421332=CARTESIAN_POINT('Ctrl Pts',(-1.01778355886063,-0.587617611684958,
9.47916363545597));
#421333=CARTESIAN_POINT('Ctrl Pts',(-0.678522372573755,-1.17523522336992,
9.52083030212264));
#421334=CARTESIAN_POINT('Ctrl Pts',(-1.4392480545452E-16,-1.17523522336992,
9.56249696878931));
#421335=CARTESIAN_POINT('Ctrl Pts',(0.678522372573754,-1.17523522336992,
9.60416363545597));
#421336=CARTESIAN_POINT('Ctrl Pts',(1.01778355886063,-0.587617611684959,
9.64583030212264));
#421337=CARTESIAN_POINT('Ctrl Pts',(1.35704474514751,2.29132775890901E-15,
9.6874969687893));
#421338=CARTESIAN_POINT('Ctrl Pts',(1.01778355886063,0.587617611684963,
9.72916363545597));
#421339=CARTESIAN_POINT('Ctrl Pts',(0.678522372573755,1.17523522336992,
9.77083030212264));
#421340=CARTESIAN_POINT('Ctrl Pts',(0.,1.17523522336992,9.8124969687893));
#421341=CARTESIAN_POINT('Ctrl Pts',(-0.678522372573754,1.17523522336992,
9.85416363545597));
#421342=CARTESIAN_POINT('Ctrl Pts',(-1.01778355886063,0.587617611684963,
9.89583030212264));
#421343=CARTESIAN_POINT('Ctrl Pts',(-1.35704474514751,2.62370785959794E-15,
9.93749696878931));
#421344=CARTESIAN_POINT('Ctrl Pts',(-1.01778355886063,-0.587617611684958,
9.97916363545597));
#421345=CARTESIAN_POINT('Ctrl Pts',(-0.678522372573755,-1.17523522336992,
10.0208303021226));
#421346=CARTESIAN_POINT('Ctrl Pts',(-1.4392480545452E-16,-1.17523522336992,
10.0624969687893));
#421347=CARTESIAN_POINT('Ctrl Pts',(0.678522372573754,-1.17523522336992,
10.104163635456));
#421348=CARTESIAN_POINT('Ctrl Pts',(1.01778355886063,-0.587617611684959,
10.1458303021226));
#421349=CARTESIAN_POINT('Ctrl Pts',(1.35704474514751,2.29132775890901E-15,
10.1874969687893));
#421350=CARTESIAN_POINT('Ctrl Pts',(1.01778355886063,0.587617611684963,
10.229163635456));
#421351=CARTESIAN_POINT('Ctrl Pts',(0.678522372573755,1.17523522336992,
10.2708303021226));
#421352=CARTESIAN_POINT('Ctrl Pts',(0.,1.17523522336992,10.3124969687893));
#421353=CARTESIAN_POINT('Ctrl Pts',(-0.678522372573754,1.17523522336992,
10.354163635456));
#421354=CARTESIAN_POINT('Ctrl Pts',(-1.01778355886063,0.587617611684963,
10.3958303021226));
#421355=CARTESIAN_POINT('Ctrl Pts',(-1.35704474514751,2.62370785959794E-15,
10.4374969687893));
#421356=CARTESIAN_POINT('Ctrl Pts',(-1.01778355886063,-0.587617611684958,
10.479163635456));
#421357=CARTESIAN_POINT('Ctrl Pts',(-0.678522372573755,-1.17523522336992,
10.5208303021226));
#421358=CARTESIAN_POINT('Ctrl Pts',(-1.4392480545452E-16,-1.17523522336992,
10.5624969687893));
#421359=CARTESIAN_POINT('Ctrl Pts',(0.678522372573754,-1.17523522336992,
10.604163635456));
#421360=CARTESIAN_POINT('Ctrl Pts',(1.01778355886063,-0.587617611684959,
10.6458303021226));
#421361=CARTESIAN_POINT('Ctrl Pts',(1.35704474514751,2.29132775890901E-15,
10.6874969687893));
#421362=CARTESIAN_POINT('Ctrl Pts',(1.01778355886063,0.587617611684963,
10.729163635456));
#421363=CARTESIAN_POINT('Ctrl Pts',(0.678522372573755,1.17523522336992,
10.7708303021226));
#421364=CARTESIAN_POINT('Ctrl Pts',(0.,1.17523522336992,10.8124969687893));
#421365=CARTESIAN_POINT('Ctrl Pts',(-0.678522372573754,1.17523522336992,
10.854163635456));
#421366=CARTESIAN_POINT('Ctrl Pts',(-1.01778355886063,0.587617611684963,
10.8958303021226));
#421367=CARTESIAN_POINT('Ctrl Pts',(-1.35704474514751,2.62370785959794E-15,
10.9374969687893));
#421368=CARTESIAN_POINT('Ctrl Pts',(-1.01778355886063,-0.587617611684958,
10.979163635456));
#421369=CARTESIAN_POINT('Ctrl Pts',(-0.678522372573755,-1.17523522336992,
11.0208303021226));
#421370=CARTESIAN_POINT('Ctrl Pts',(-1.4392480545452E-16,-1.17523522336992,
11.0624969687893));
#421371=CARTESIAN_POINT('Ctrl Pts',(0.678522372573754,-1.17523522336992,
11.104163635456));
#421372=CARTESIAN_POINT('Ctrl Pts',(1.01778355886063,-0.587617611684959,
11.1458303021226));
#421373=CARTESIAN_POINT('Ctrl Pts',(1.35704474514751,2.29132775890901E-15,
11.1874969687893));
#421374=CARTESIAN_POINT('Ctrl Pts',(1.01778355886063,0.587617611684963,
11.229163635456));
#421375=CARTESIAN_POINT('Ctrl Pts',(0.678522372573755,1.17523522336992,
11.2708303021226));
#421376=CARTESIAN_POINT('Ctrl Pts',(0.,1.17523522336992,11.3124969687893));
#421377=CARTESIAN_POINT('Ctrl Pts',(-1.43925448419923E-16,-1.17524047358087,
3.56250000000001));
#421378=CARTESIAN_POINT('Ctrl Pts',(0.678525403784459,-1.17524047358087,
3.60416666666668));
#421379=CARTESIAN_POINT('Ctrl Pts',(1.01778810567669,-0.587620236790434,
3.64583333333334));
#421380=CARTESIAN_POINT('Ctrl Pts',(1.12956523348512,-0.394016572302108,
3.65956128014086));
#421381=CARTESIAN_POINT('Ctrl Pts',(1.16245326511943,-0.172894699617312,
3.67524047358081));
#421382=CARTESIAN_POINT('Origin',(0.,-1.11022302462516E-14,-14.21875));
#421383=CARTESIAN_POINT('Ctrl Pts',(-1.43925448419923E-16,-1.17524047358087,
3.50000000000001));
#421384=CARTESIAN_POINT('Ctrl Pts',(0.678525403784459,-1.17524047358087,
3.54166666666668));
#421385=CARTESIAN_POINT('Ctrl Pts',(1.01778810567669,-0.587620236790434,
3.58333333333334));
#421386=CARTESIAN_POINT('Ctrl Pts',(1.35705080756892,2.29132664526027E-15,
3.62500000000001));
#421387=CARTESIAN_POINT('Ctrl Pts',(1.01778810567669,0.587620236790438,
3.66666666666668));
#421388=CARTESIAN_POINT('Ctrl Pts',(0.98389535208559,0.646324208018635,
3.67082921698069));
#421389=CARTESIAN_POINT('Ctrl Pts',(0.943477955796025,0.700742119234707,
3.6752404735808));
#421390=CARTESIAN_POINT('Ctrl Pts',(0.,1.17524047358087,-14.25));
#421391=CARTESIAN_POINT('Ctrl Pts',(-0.678525403784459,1.17524047358087,
-14.2083333333333));
#421392=CARTESIAN_POINT('Ctrl Pts',(-1.01778810567669,0.587620236790438,
-14.1666666666667));
#421393=CARTESIAN_POINT('Ctrl Pts',(-1.35705080756892,2.62370823081419E-15,
-14.125));
#421394=CARTESIAN_POINT('Ctrl Pts',(-1.01778810567669,-0.587620236790433,
-14.0833333333333));
#421395=CARTESIAN_POINT('Ctrl Pts',(-0.67852540378446,-1.17524047358087,
-14.0416666666667));
#421396=CARTESIAN_POINT('Ctrl Pts',(-1.43925448419923E-16,-1.17524047358087,
-14.));
#421397=CARTESIAN_POINT('Ctrl Pts',(0.678525403784459,-1.17524047358087,
-13.9583333333333));
#421398=CARTESIAN_POINT('Ctrl Pts',(1.01778810567669,-0.587620236790434,
-13.9166666666667));
#421399=CARTESIAN_POINT('Ctrl Pts',(1.35705080756892,2.29132664526027E-15,
-13.875));
#421400=CARTESIAN_POINT('Ctrl Pts',(1.01778810567669,0.587620236790438,
-13.8333333333333));
#421401=CARTESIAN_POINT('Ctrl Pts',(0.67852540378446,1.17524047358087,-13.7916666666667));
#421402=CARTESIAN_POINT('Ctrl Pts',(0.,1.17524047358087,-13.75));
#421403=CARTESIAN_POINT('Ctrl Pts',(-0.678525403784459,1.17524047358087,
-13.7083333333333));
#421404=CARTESIAN_POINT('Ctrl Pts',(-1.01778810567669,0.587620236790438,
-13.6666666666667));
#421405=CARTESIAN_POINT('Ctrl Pts',(-1.35705080756892,2.62370823081419E-15,
-13.625));
#421406=CARTESIAN_POINT('Ctrl Pts',(-1.01778810567669,-0.587620236790433,
-13.5833333333333));
#421407=CARTESIAN_POINT('Ctrl Pts',(-0.67852540378446,-1.17524047358087,
-13.5416666666667));
#421408=CARTESIAN_POINT('Ctrl Pts',(-1.43925448419923E-16,-1.17524047358087,
-13.5));
#421409=CARTESIAN_POINT('Ctrl Pts',(0.678525403784459,-1.17524047358087,
-13.4583333333333));
#421410=CARTESIAN_POINT('Ctrl Pts',(1.01778810567669,-0.587620236790434,
-13.4166666666667));
#421411=CARTESIAN_POINT('Ctrl Pts',(1.35705080756892,2.29132664526027E-15,
-13.375));
#421412=CARTESIAN_POINT('Ctrl Pts',(1.01778810567669,0.587620236790438,
-13.3333333333333));
#421413=CARTESIAN_POINT('Ctrl Pts',(0.67852540378446,1.17524047358087,-13.2916666666667));
#421414=CARTESIAN_POINT('Ctrl Pts',(0.,1.17524047358087,-13.25));
#421415=CARTESIAN_POINT('Ctrl Pts',(-0.678525403784459,1.17524047358087,
-13.2083333333333));
#421416=CARTESIAN_POINT('Ctrl Pts',(-1.01778810567669,0.587620236790438,
-13.1666666666667));
#421417=CARTESIAN_POINT('Ctrl Pts',(-1.35705080756892,2.62370823081419E-15,
-13.125));
#421418=CARTESIAN_POINT('Ctrl Pts',(-1.01778810567669,-0.587620236790433,
-13.0833333333333));
#421419=CARTESIAN_POINT('Ctrl Pts',(-0.67852540378446,-1.17524047358087,
-13.0416666666667));
#421420=CARTESIAN_POINT('Ctrl Pts',(-1.43925448419923E-16,-1.17524047358087,
-13.));
#421421=CARTESIAN_POINT('Ctrl Pts',(0.678525403784459,-1.17524047358087,
-12.9583333333333));
#421422=CARTESIAN_POINT('Ctrl Pts',(1.01778810567669,-0.587620236790434,
-12.9166666666667));
#421423=CARTESIAN_POINT('Ctrl Pts',(1.35705080756892,2.29132664526027E-15,
-12.875));
#421424=CARTESIAN_POINT('Ctrl Pts',(1.01778810567669,0.587620236790438,
-12.8333333333333));
#421425=CARTESIAN_POINT('Ctrl Pts',(0.67852540378446,1.17524047358087,-12.7916666666667));
#421426=CARTESIAN_POINT('Ctrl Pts',(0.,1.17524047358087,-12.75));
#421427=CARTESIAN_POINT('Ctrl Pts',(-0.678525403784459,1.17524047358087,
-12.7083333333333));
#421428=CARTESIAN_POINT('Ctrl Pts',(-1.01778810567669,0.587620236790438,
-12.6666666666667));
#421429=CARTESIAN_POINT('Ctrl Pts',(-1.35705080756892,2.62370823081419E-15,
-12.625));
#421430=CARTESIAN_POINT('Ctrl Pts',(-1.01778810567669,-0.587620236790433,
-12.5833333333333));
#421431=CARTESIAN_POINT('Ctrl Pts',(-0.67852540378446,-1.17524047358087,
-12.5416666666667));
#421432=CARTESIAN_POINT('Ctrl Pts',(-1.43925448419923E-16,-1.17524047358087,
-12.5));
#421433=CARTESIAN_POINT('Ctrl Pts',(0.678525403784459,-1.17524047358087,
-12.4583333333333));
#421434=CARTESIAN_POINT('Ctrl Pts',(1.01778810567669,-0.587620236790434,
-12.4166666666667));
#421435=CARTESIAN_POINT('Ctrl Pts',(1.35705080756892,2.29132664526027E-15,
-12.375));
#421436=CARTESIAN_POINT('Ctrl Pts',(1.01778810567669,0.587620236790438,
-12.3333333333333));
#421437=CARTESIAN_POINT('Ctrl Pts',(0.67852540378446,1.17524047358087,-12.2916666666667));
#421438=CARTESIAN_POINT('Ctrl Pts',(0.,1.17524047358087,-12.25));
#421439=CARTESIAN_POINT('Ctrl Pts',(-0.678525403784459,1.17524047358087,
-12.2083333333333));
#421440=CARTESIAN_POINT('Ctrl Pts',(-1.01778810567669,0.587620236790438,
-12.1666666666667));
#421441=CARTESIAN_POINT('Ctrl Pts',(-1.35705080756892,2.62370823081419E-15,
-12.125));
#421442=CARTESIAN_POINT('Ctrl Pts',(-1.01778810567669,-0.587620236790433,
-12.0833333333333));
#421443=CARTESIAN_POINT('Ctrl Pts',(-0.67852540378446,-1.17524047358087,
-12.0416666666667));
#421444=CARTESIAN_POINT('Ctrl Pts',(-1.43925448419923E-16,-1.17524047358087,
-12.));
#421445=CARTESIAN_POINT('Ctrl Pts',(0.678525403784459,-1.17524047358087,
-11.9583333333333));
#421446=CARTESIAN_POINT('Ctrl Pts',(1.01778810567669,-0.587620236790434,
-11.9166666666667));
#421447=CARTESIAN_POINT('Ctrl Pts',(1.35705080756892,2.29132664526027E-15,
-11.875));
#421448=CARTESIAN_POINT('Ctrl Pts',(1.01778810567669,0.587620236790438,
-11.8333333333333));
#421449=CARTESIAN_POINT('Ctrl Pts',(0.67852540378446,1.17524047358087,-11.7916666666667));
#421450=CARTESIAN_POINT('Ctrl Pts',(0.,1.17524047358087,-11.75));
#421451=CARTESIAN_POINT('Ctrl Pts',(-0.678525403784459,1.17524047358087,
-11.7083333333333));
#421452=CARTESIAN_POINT('Ctrl Pts',(-1.01778810567669,0.587620236790438,
-11.6666666666667));
#421453=CARTESIAN_POINT('Ctrl Pts',(-1.35705080756892,2.62370823081419E-15,
-11.625));
#421454=CARTESIAN_POINT('Ctrl Pts',(-1.01778810567669,-0.587620236790433,
-11.5833333333333));
#421455=CARTESIAN_POINT('Ctrl Pts',(-0.67852540378446,-1.17524047358087,
-11.5416666666667));
#421456=CARTESIAN_POINT('Ctrl Pts',(-1.43925448419923E-16,-1.17524047358087,
-11.5));
#421457=CARTESIAN_POINT('Ctrl Pts',(0.678525403784459,-1.17524047358087,
-11.4583333333333));
#421458=CARTESIAN_POINT('Ctrl Pts',(1.01778810567669,-0.587620236790434,
-11.4166666666667));
#421459=CARTESIAN_POINT('Ctrl Pts',(1.35705080756892,2.29132664526027E-15,
-11.375));
#421460=CARTESIAN_POINT('Ctrl Pts',(1.01778810567669,0.587620236790438,
-11.3333333333333));
#421461=CARTESIAN_POINT('Ctrl Pts',(0.67852540378446,1.17524047358087,-11.2916666666667));
#421462=CARTESIAN_POINT('Ctrl Pts',(0.,1.17524047358087,-11.25));
#421463=CARTESIAN_POINT('Ctrl Pts',(-0.678525403784459,1.17524047358087,
-11.2083333333333));
#421464=CARTESIAN_POINT('Ctrl Pts',(-1.01778810567669,0.587620236790438,
-11.1666666666667));
#421465=CARTESIAN_POINT('Ctrl Pts',(-1.35705080756892,2.62370823081419E-15,
-11.125));
#421466=CARTESIAN_POINT('Ctrl Pts',(-1.01778810567669,-0.587620236790433,
-11.0833333333333));
#421467=CARTESIAN_POINT('Ctrl Pts',(-0.67852540378446,-1.17524047358087,
-11.0416666666667));
#421468=CARTESIAN_POINT('Ctrl Pts',(-1.43925448419923E-16,-1.17524047358087,
-11.));
#421469=CARTESIAN_POINT('Ctrl Pts',(0.678525403784459,-1.17524047358087,
-10.9583333333333));
#421470=CARTESIAN_POINT('Ctrl Pts',(1.01778810567669,-0.587620236790434,
-10.9166666666667));
#421471=CARTESIAN_POINT('Ctrl Pts',(1.35705080756892,2.29132664526027E-15,
-10.875));
#421472=CARTESIAN_POINT('Ctrl Pts',(1.01778810567669,0.587620236790438,
-10.8333333333333));
#421473=CARTESIAN_POINT('Ctrl Pts',(0.67852540378446,1.17524047358087,-10.7916666666667));
#421474=CARTESIAN_POINT('Ctrl Pts',(0.,1.17524047358087,-10.75));
#421475=CARTESIAN_POINT('Ctrl Pts',(-0.678525403784459,1.17524047358087,
-10.7083333333333));
#421476=CARTESIAN_POINT('Ctrl Pts',(-1.01778810567669,0.587620236790438,
-10.6666666666667));
#421477=CARTESIAN_POINT('Ctrl Pts',(-1.35705080756892,2.62370823081419E-15,
-10.625));
#421478=CARTESIAN_POINT('Ctrl Pts',(-1.01778810567669,-0.587620236790433,
-10.5833333333333));
#421479=CARTESIAN_POINT('Ctrl Pts',(-0.67852540378446,-1.17524047358087,
-10.5416666666667));
#421480=CARTESIAN_POINT('Ctrl Pts',(-1.43925448419923E-16,-1.17524047358087,
-10.5));
#421481=CARTESIAN_POINT('Ctrl Pts',(0.678525403784459,-1.17524047358087,
-10.4583333333333));
#421482=CARTESIAN_POINT('Ctrl Pts',(1.01778810567669,-0.587620236790434,
-10.4166666666667));
#421483=CARTESIAN_POINT('Ctrl Pts',(1.35705080756892,2.29132664526027E-15,
-10.375));
#421484=CARTESIAN_POINT('Ctrl Pts',(1.01778810567669,0.587620236790438,
-10.3333333333333));
#421485=CARTESIAN_POINT('Ctrl Pts',(0.67852540378446,1.17524047358087,-10.2916666666667));
#421486=CARTESIAN_POINT('Ctrl Pts',(0.,1.17524047358087,-10.25));
#421487=CARTESIAN_POINT('Ctrl Pts',(-0.678525403784459,1.17524047358087,
-10.2083333333333));
#421488=CARTESIAN_POINT('Ctrl Pts',(-1.01778810567669,0.587620236790438,
-10.1666666666667));
#421489=CARTESIAN_POINT('Ctrl Pts',(-1.35705080756892,2.62370823081419E-15,
-10.125));
#421490=CARTESIAN_POINT('Ctrl Pts',(-1.01778810567669,-0.587620236790433,
-10.0833333333333));
#421491=CARTESIAN_POINT('Ctrl Pts',(-0.67852540378446,-1.17524047358087,
-10.0416666666667));
#421492=CARTESIAN_POINT('Ctrl Pts',(-1.43925448419923E-16,-1.17524047358087,
-9.99999999999999));
#421493=CARTESIAN_POINT('Ctrl Pts',(0.678525403784459,-1.17524047358087,
-9.95833333333332));
#421494=CARTESIAN_POINT('Ctrl Pts',(1.01778810567669,-0.587620236790434,
-9.91666666666666));
#421495=CARTESIAN_POINT('Ctrl Pts',(1.35705080756892,2.29132664526027E-15,
-9.87499999999999));
#421496=CARTESIAN_POINT('Ctrl Pts',(1.01778810567669,0.587620236790438,
-9.83333333333332));
#421497=CARTESIAN_POINT('Ctrl Pts',(0.67852540378446,1.17524047358087,-9.79166666666666));
#421498=CARTESIAN_POINT('Ctrl Pts',(0.,1.17524047358087,-9.74999999999999));
#421499=CARTESIAN_POINT('Ctrl Pts',(-0.678525403784459,1.17524047358087,
-9.70833333333332));
#421500=CARTESIAN_POINT('Ctrl Pts',(-1.01778810567669,0.587620236790438,
-9.66666666666666));
#421501=CARTESIAN_POINT('Ctrl Pts',(-1.35705080756892,2.62370823081419E-15,
-9.62499999999999));
#421502=CARTESIAN_POINT('Ctrl Pts',(-1.01778810567669,-0.587620236790433,
-9.58333333333332));
#421503=CARTESIAN_POINT('Ctrl Pts',(-0.67852540378446,-1.17524047358087,
-9.54166666666666));
#421504=CARTESIAN_POINT('Ctrl Pts',(-1.43925448419923E-16,-1.17524047358087,
-9.49999999999999));
#421505=CARTESIAN_POINT('Ctrl Pts',(0.678525403784459,-1.17524047358087,
-9.45833333333333));
#421506=CARTESIAN_POINT('Ctrl Pts',(1.01778810567669,-0.587620236790434,
-9.41666666666666));
#421507=CARTESIAN_POINT('Ctrl Pts',(1.35705080756892,2.29132664526027E-15,
-9.37499999999999));
#421508=CARTESIAN_POINT('Ctrl Pts',(1.01778810567669,0.587620236790438,
-9.33333333333332));
#421509=CARTESIAN_POINT('Ctrl Pts',(0.67852540378446,1.17524047358087,-9.29166666666666));
#421510=CARTESIAN_POINT('Ctrl Pts',(0.,1.17524047358087,-9.24999999999999));
#421511=CARTESIAN_POINT('Ctrl Pts',(-0.678525403784459,1.17524047358087,
-9.20833333333332));
#421512=CARTESIAN_POINT('Ctrl Pts',(-1.01778810567669,0.587620236790438,
-9.16666666666666));
#421513=CARTESIAN_POINT('Ctrl Pts',(-1.35705080756892,2.62370823081419E-15,
-9.12499999999999));
#421514=CARTESIAN_POINT('Ctrl Pts',(-1.01778810567669,-0.587620236790433,
-9.08333333333332));
#421515=CARTESIAN_POINT('Ctrl Pts',(-0.67852540378446,-1.17524047358087,
-9.04166666666666));
#421516=CARTESIAN_POINT('Ctrl Pts',(-1.43925448419923E-16,-1.17524047358087,
-8.99999999999999));
#421517=CARTESIAN_POINT('Ctrl Pts',(0.678525403784459,-1.17524047358087,
-8.95833333333332));
#421518=CARTESIAN_POINT('Ctrl Pts',(1.01778810567669,-0.587620236790434,
-8.91666666666666));
#421519=CARTESIAN_POINT('Ctrl Pts',(1.35705080756892,2.29132664526027E-15,
-8.87499999999999));
#421520=CARTESIAN_POINT('Ctrl Pts',(1.01778810567669,0.587620236790438,
-8.83333333333333));
#421521=CARTESIAN_POINT('Ctrl Pts',(0.67852540378446,1.17524047358087,-8.79166666666666));
#421522=CARTESIAN_POINT('Ctrl Pts',(0.,1.17524047358087,-8.74999999999999));
#421523=CARTESIAN_POINT('Ctrl Pts',(-0.678525403784459,1.17524047358087,
-8.70833333333333));
#421524=CARTESIAN_POINT('Ctrl Pts',(-1.01778810567669,0.587620236790438,
-8.66666666666666));
#421525=CARTESIAN_POINT('Ctrl Pts',(-1.35705080756892,2.62370823081419E-15,
-8.62499999999999));
#421526=CARTESIAN_POINT('Ctrl Pts',(-1.01778810567669,-0.587620236790433,
-8.58333333333333));
#421527=CARTESIAN_POINT('Ctrl Pts',(-0.67852540378446,-1.17524047358087,
-8.54166666666666));
#421528=CARTESIAN_POINT('Ctrl Pts',(-1.43925448419923E-16,-1.17524047358087,
-8.49999999999999));
#421529=CARTESIAN_POINT('Ctrl Pts',(0.678525403784459,-1.17524047358087,
-8.45833333333333));
#421530=CARTESIAN_POINT('Ctrl Pts',(1.01778810567669,-0.587620236790434,
-8.41666666666666));
#421531=CARTESIAN_POINT('Ctrl Pts',(1.35705080756892,2.29132664526027E-15,
-8.37499999999999));
#421532=CARTESIAN_POINT('Ctrl Pts',(1.01778810567669,0.587620236790438,
-8.33333333333333));
#421533=CARTESIAN_POINT('Ctrl Pts',(0.67852540378446,1.17524047358087,-8.29166666666666));
#421534=CARTESIAN_POINT('Ctrl Pts',(0.,1.17524047358087,-8.24999999999999));
#421535=CARTESIAN_POINT('Ctrl Pts',(-0.678525403784459,1.17524047358087,
-8.20833333333333));
#421536=CARTESIAN_POINT('Ctrl Pts',(-1.01778810567669,0.587620236790438,
-8.16666666666666));
#421537=CARTESIAN_POINT('Ctrl Pts',(-1.35705080756892,2.62370823081419E-15,
-8.12499999999999));
#421538=CARTESIAN_POINT('Ctrl Pts',(-1.01778810567669,-0.587620236790433,
-8.08333333333333));
#421539=CARTESIAN_POINT('Ctrl Pts',(-0.67852540378446,-1.17524047358087,
-8.04166666666666));
#421540=CARTESIAN_POINT('Ctrl Pts',(-1.43925448419923E-16,-1.17524047358087,
-7.99999999999999));
#421541=CARTESIAN_POINT('Ctrl Pts',(0.678525403784459,-1.17524047358087,
-7.95833333333333));
#421542=CARTESIAN_POINT('Ctrl Pts',(1.01778810567669,-0.587620236790434,
-7.91666666666666));
#421543=CARTESIAN_POINT('Ctrl Pts',(1.35705080756892,2.29132664526027E-15,
-7.87499999999999));
#421544=CARTESIAN_POINT('Ctrl Pts',(1.01778810567669,0.587620236790438,
-7.83333333333332));
#421545=CARTESIAN_POINT('Ctrl Pts',(0.67852540378446,1.17524047358087,-7.79166666666666));
#421546=CARTESIAN_POINT('Ctrl Pts',(0.,1.17524047358087,-7.74999999999999));
#421547=CARTESIAN_POINT('Ctrl Pts',(-0.678525403784459,1.17524047358087,
-7.70833333333332));
#421548=CARTESIAN_POINT('Ctrl Pts',(-1.01778810567669,0.587620236790438,
-7.66666666666666));
#421549=CARTESIAN_POINT('Ctrl Pts',(-1.35705080756892,2.62370823081419E-15,
-7.62499999999999));
#421550=CARTESIAN_POINT('Ctrl Pts',(-1.01778810567669,-0.587620236790433,
-7.58333333333332));
#421551=CARTESIAN_POINT('Ctrl Pts',(-0.67852540378446,-1.17524047358087,
-7.54166666666666));
#421552=CARTESIAN_POINT('Ctrl Pts',(-1.43925448419923E-16,-1.17524047358087,
-7.49999999999999));
#421553=CARTESIAN_POINT('Ctrl Pts',(0.678525403784459,-1.17524047358087,
-7.45833333333332));
#421554=CARTESIAN_POINT('Ctrl Pts',(1.01778810567669,-0.587620236790434,
-7.41666666666666));
#421555=CARTESIAN_POINT('Ctrl Pts',(1.35705080756892,2.29132664526027E-15,
-7.37499999999999));
#421556=CARTESIAN_POINT('Ctrl Pts',(1.01778810567669,0.587620236790438,
-7.33333333333332));
#421557=CARTESIAN_POINT('Ctrl Pts',(0.67852540378446,1.17524047358087,-7.29166666666666));
#421558=CARTESIAN_POINT('Ctrl Pts',(0.,1.17524047358087,-7.24999999999999));
#421559=CARTESIAN_POINT('Ctrl Pts',(-0.678525403784459,1.17524047358087,
-7.20833333333332));
#421560=CARTESIAN_POINT('Ctrl Pts',(-1.01778810567669,0.587620236790438,
-7.16666666666666));
#421561=CARTESIAN_POINT('Ctrl Pts',(-1.35705080756892,2.62370823081419E-15,
-7.12499999999999));
#421562=CARTESIAN_POINT('Ctrl Pts',(-1.01778810567669,-0.587620236790433,
-7.08333333333332));
#421563=CARTESIAN_POINT('Ctrl Pts',(-0.67852540378446,-1.17524047358087,
-7.04166666666666));
#421564=CARTESIAN_POINT('Ctrl Pts',(-1.43925448419923E-16,-1.17524047358087,
-6.99999999999999));
#421565=CARTESIAN_POINT('Ctrl Pts',(0.678525403784459,-1.17524047358087,
-6.95833333333332));
#421566=CARTESIAN_POINT('Ctrl Pts',(1.01778810567669,-0.587620236790434,
-6.91666666666666));
#421567=CARTESIAN_POINT('Ctrl Pts',(1.35705080756892,2.29132664526027E-15,
-6.87499999999999));
#421568=CARTESIAN_POINT('Ctrl Pts',(1.01778810567669,0.587620236790438,
-6.83333333333333));
#421569=CARTESIAN_POINT('Ctrl Pts',(0.67852540378446,1.17524047358087,-6.79166666666666));
#421570=CARTESIAN_POINT('Ctrl Pts',(0.,1.17524047358087,-6.74999999999999));
#421571=CARTESIAN_POINT('Ctrl Pts',(-0.678525403784459,1.17524047358087,
-6.70833333333333));
#421572=CARTESIAN_POINT('Ctrl Pts',(-1.01778810567669,0.587620236790438,
-6.66666666666666));
#421573=CARTESIAN_POINT('Ctrl Pts',(-1.35705080756892,2.62370823081419E-15,
-6.62499999999999));
#421574=CARTESIAN_POINT('Ctrl Pts',(-1.01778810567669,-0.587620236790433,
-6.58333333333332));
#421575=CARTESIAN_POINT('Ctrl Pts',(-0.67852540378446,-1.17524047358087,
-6.54166666666666));
#421576=CARTESIAN_POINT('Ctrl Pts',(-1.43925448419923E-16,-1.17524047358087,
-6.49999999999999));
#421577=CARTESIAN_POINT('Ctrl Pts',(0.678525403784459,-1.17524047358087,
-6.45833333333332));
#421578=CARTESIAN_POINT('Ctrl Pts',(1.01778810567669,-0.587620236790434,
-6.41666666666666));
#421579=CARTESIAN_POINT('Ctrl Pts',(1.35705080756892,2.29132664526027E-15,
-6.37499999999999));
#421580=CARTESIAN_POINT('Ctrl Pts',(1.01778810567669,0.587620236790438,
-6.33333333333332));
#421581=CARTESIAN_POINT('Ctrl Pts',(0.67852540378446,1.17524047358087,-6.29166666666666));
#421582=CARTESIAN_POINT('Ctrl Pts',(0.,1.17524047358087,-6.24999999999999));
#421583=CARTESIAN_POINT('Ctrl Pts',(-0.678525403784459,1.17524047358087,
-6.20833333333333));
#421584=CARTESIAN_POINT('Ctrl Pts',(-1.01778810567669,0.587620236790438,
-6.16666666666666));
#421585=CARTESIAN_POINT('Ctrl Pts',(-1.35705080756892,2.62370823081419E-15,
-6.12499999999999));
#421586=CARTESIAN_POINT('Ctrl Pts',(-1.01778810567669,-0.587620236790433,
-6.08333333333333));
#421587=CARTESIAN_POINT('Ctrl Pts',(-0.67852540378446,-1.17524047358087,
-6.04166666666666));
#421588=CARTESIAN_POINT('Ctrl Pts',(-1.43925448419923E-16,-1.17524047358087,
-5.99999999999999));
#421589=CARTESIAN_POINT('Ctrl Pts',(0.678525403784459,-1.17524047358087,
-5.95833333333332));
#421590=CARTESIAN_POINT('Ctrl Pts',(1.01778810567669,-0.587620236790434,
-5.91666666666666));
#421591=CARTESIAN_POINT('Ctrl Pts',(1.35705080756892,2.29132664526027E-15,
-5.87499999999999));
#421592=CARTESIAN_POINT('Ctrl Pts',(1.01778810567669,0.587620236790438,
-5.83333333333333));
#421593=CARTESIAN_POINT('Ctrl Pts',(0.67852540378446,1.17524047358087,-5.79166666666666));
#421594=CARTESIAN_POINT('Ctrl Pts',(0.,1.17524047358087,-5.74999999999999));
#421595=CARTESIAN_POINT('Ctrl Pts',(-0.678525403784459,1.17524047358087,
-5.70833333333332));
#421596=CARTESIAN_POINT('Ctrl Pts',(-1.01778810567669,0.587620236790438,
-5.66666666666666));
#421597=CARTESIAN_POINT('Ctrl Pts',(-1.35705080756892,2.62370823081419E-15,
-5.62499999999999));
#421598=CARTESIAN_POINT('Ctrl Pts',(-1.01778810567669,-0.587620236790433,
-5.58333333333333));
#421599=CARTESIAN_POINT('Ctrl Pts',(-0.67852540378446,-1.17524047358087,
-5.54166666666666));
#421600=CARTESIAN_POINT('Ctrl Pts',(-1.43925448419923E-16,-1.17524047358087,
-5.49999999999999));
#421601=CARTESIAN_POINT('Ctrl Pts',(0.678525403784459,-1.17524047358087,
-5.45833333333332));
#421602=CARTESIAN_POINT('Ctrl Pts',(1.01778810567669,-0.587620236790434,
-5.41666666666666));
#421603=CARTESIAN_POINT('Ctrl Pts',(1.35705080756892,2.29132664526027E-15,
-5.37499999999999));
#421604=CARTESIAN_POINT('Ctrl Pts',(1.01778810567669,0.587620236790438,
-5.33333333333332));
#421605=CARTESIAN_POINT('Ctrl Pts',(0.67852540378446,1.17524047358087,-5.29166666666666));
#421606=CARTESIAN_POINT('Ctrl Pts',(0.,1.17524047358087,-5.24999999999999));
#421607=CARTESIAN_POINT('Ctrl Pts',(-0.678525403784459,1.17524047358087,
-5.20833333333333));
#421608=CARTESIAN_POINT('Ctrl Pts',(-1.01778810567669,0.587620236790438,
-5.16666666666666));
#421609=CARTESIAN_POINT('Ctrl Pts',(-1.35705080756892,2.62370823081419E-15,
-5.12499999999999));
#421610=CARTESIAN_POINT('Ctrl Pts',(-1.01778810567669,-0.587620236790433,
-5.08333333333332));
#421611=CARTESIAN_POINT('Ctrl Pts',(-0.67852540378446,-1.17524047358087,
-5.04166666666666));
#421612=CARTESIAN_POINT('Ctrl Pts',(-1.43925448419923E-16,-1.17524047358087,
-4.99999999999999));
#421613=CARTESIAN_POINT('Ctrl Pts',(0.678525403784459,-1.17524047358087,
-4.95833333333332));
#421614=CARTESIAN_POINT('Ctrl Pts',(1.01778810567669,-0.587620236790434,
-4.91666666666666));
#421615=CARTESIAN_POINT('Ctrl Pts',(1.35705080756892,2.29132664526027E-15,
-4.87499999999999));
#421616=CARTESIAN_POINT('Ctrl Pts',(1.01778810567669,0.587620236790438,
-4.83333333333332));
#421617=CARTESIAN_POINT('Ctrl Pts',(0.67852540378446,1.17524047358087,-4.79166666666666));
#421618=CARTESIAN_POINT('Ctrl Pts',(0.,1.17524047358087,-4.74999999999999));
#421619=CARTESIAN_POINT('Ctrl Pts',(-0.678525403784459,1.17524047358087,
-4.70833333333332));
#421620=CARTESIAN_POINT('Ctrl Pts',(-1.01778810567669,0.587620236790438,
-4.66666666666666));
#421621=CARTESIAN_POINT('Ctrl Pts',(-1.35705080756892,2.62370823081419E-15,
-4.62499999999999));
#421622=CARTESIAN_POINT('Ctrl Pts',(-1.01778810567669,-0.587620236790433,
-4.58333333333332));
#421623=CARTESIAN_POINT('Ctrl Pts',(-0.67852540378446,-1.17524047358087,
-4.54166666666666));
#421624=CARTESIAN_POINT('Ctrl Pts',(-1.43925448419923E-16,-1.17524047358087,
-4.49999999999999));
#421625=CARTESIAN_POINT('Ctrl Pts',(0.678525403784459,-1.17524047358087,
-4.45833333333333));
#421626=CARTESIAN_POINT('Ctrl Pts',(1.01778810567669,-0.587620236790434,
-4.41666666666666));
#421627=CARTESIAN_POINT('Ctrl Pts',(1.35705080756892,2.29132664526027E-15,
-4.37499999999999));
#421628=CARTESIAN_POINT('Ctrl Pts',(1.01778810567669,0.587620236790438,
-4.33333333333333));
#421629=CARTESIAN_POINT('Ctrl Pts',(0.67852540378446,1.17524047358087,-4.29166666666666));
#421630=CARTESIAN_POINT('Ctrl Pts',(0.,1.17524047358087,-4.24999999999999));
#421631=CARTESIAN_POINT('Ctrl Pts',(-0.678525403784459,1.17524047358087,
-4.20833333333332));
#421632=CARTESIAN_POINT('Ctrl Pts',(-1.01778810567669,0.587620236790438,
-4.16666666666666));
#421633=CARTESIAN_POINT('Ctrl Pts',(-1.35705080756892,2.62370823081419E-15,
-4.12499999999999));
#421634=CARTESIAN_POINT('Ctrl Pts',(-1.01778810567669,-0.587620236790433,
-4.08333333333332));
#421635=CARTESIAN_POINT('Ctrl Pts',(-0.67852540378446,-1.17524047358087,
-4.04166666666666));
#421636=CARTESIAN_POINT('Ctrl Pts',(-1.43925448419923E-16,-1.17524047358087,
-3.99999999999999));
#421637=CARTESIAN_POINT('Ctrl Pts',(0.678525403784459,-1.17524047358087,
-3.95833333333332));
#421638=CARTESIAN_POINT('Ctrl Pts',(1.01778810567669,-0.587620236790434,
-3.91666666666666));
#421639=CARTESIAN_POINT('Ctrl Pts',(1.35705080756892,2.29132664526027E-15,
-3.87499999999999));
#421640=CARTESIAN_POINT('Ctrl Pts',(1.01778810567669,0.587620236790438,
-3.83333333333332));
#421641=CARTESIAN_POINT('Ctrl Pts',(0.67852540378446,1.17524047358087,-3.79166666666666));
#421642=CARTESIAN_POINT('Ctrl Pts',(0.,1.17524047358087,-3.74999999999999));
#421643=CARTESIAN_POINT('Ctrl Pts',(-0.678525403784459,1.17524047358087,
-3.70833333333332));
#421644=CARTESIAN_POINT('Ctrl Pts',(-1.01778810567669,0.587620236790438,
-3.66666666666666));
#421645=CARTESIAN_POINT('Ctrl Pts',(-1.35705080756892,2.62370823081419E-15,
-3.62499999999999));
#421646=CARTESIAN_POINT('Ctrl Pts',(-1.01778810567669,-0.587620236790433,
-3.58333333333332));
#421647=CARTESIAN_POINT('Ctrl Pts',(-0.67852540378446,-1.17524047358087,
-3.54166666666666));
#421648=CARTESIAN_POINT('Ctrl Pts',(-1.43925448419923E-16,-1.17524047358087,
-3.49999999999999));
#421649=CARTESIAN_POINT('Ctrl Pts',(0.678525403784459,-1.17524047358087,
-3.45833333333333));
#421650=CARTESIAN_POINT('Ctrl Pts',(1.01778810567669,-0.587620236790434,
-3.41666666666666));
#421651=CARTESIAN_POINT('Ctrl Pts',(1.35705080756892,2.29132664526027E-15,
-3.37499999999999));
#421652=CARTESIAN_POINT('Ctrl Pts',(1.01778810567669,0.587620236790438,
-3.33333333333332));
#421653=CARTESIAN_POINT('Ctrl Pts',(0.67852540378446,1.17524047358087,-3.29166666666666));
#421654=CARTESIAN_POINT('Ctrl Pts',(0.,1.17524047358087,-3.24999999999999));
#421655=CARTESIAN_POINT('Ctrl Pts',(-0.678525403784459,1.17524047358087,
-3.20833333333332));
#421656=CARTESIAN_POINT('Ctrl Pts',(-1.01778810567669,0.587620236790438,
-3.16666666666666));
#421657=CARTESIAN_POINT('Ctrl Pts',(-1.35705080756892,2.62370823081419E-15,
-3.12499999999999));
#421658=CARTESIAN_POINT('Ctrl Pts',(-1.01778810567669,-0.587620236790433,
-3.08333333333332));
#421659=CARTESIAN_POINT('Ctrl Pts',(-0.67852540378446,-1.17524047358087,
-3.04166666666666));
#421660=CARTESIAN_POINT('Ctrl Pts',(-1.43925448419923E-16,-1.17524047358087,
-2.99999999999999));
#421661=CARTESIAN_POINT('Ctrl Pts',(0.678525403784459,-1.17524047358087,
-2.95833333333332));
#421662=CARTESIAN_POINT('Ctrl Pts',(1.01778810567669,-0.587620236790434,
-2.91666666666666));
#421663=CARTESIAN_POINT('Ctrl Pts',(1.35705080756892,2.29132664526027E-15,
-2.87499999999999));
#421664=CARTESIAN_POINT('Ctrl Pts',(1.01778810567669,0.587620236790438,
-2.83333333333332));
#421665=CARTESIAN_POINT('Ctrl Pts',(0.67852540378446,1.17524047358087,-2.79166666666666));
#421666=CARTESIAN_POINT('Ctrl Pts',(0.,1.17524047358087,-2.74999999999999));
#421667=CARTESIAN_POINT('Ctrl Pts',(-0.678525403784459,1.17524047358087,
-2.70833333333332));
#421668=CARTESIAN_POINT('Ctrl Pts',(-1.01778810567669,0.587620236790438,
-2.66666666666666));
#421669=CARTESIAN_POINT('Ctrl Pts',(-1.35705080756892,2.62370823081419E-15,
-2.62499999999999));
#421670=CARTESIAN_POINT('Ctrl Pts',(-1.01778810567669,-0.587620236790433,
-2.58333333333332));
#421671=CARTESIAN_POINT('Ctrl Pts',(-0.67852540378446,-1.17524047358087,
-2.54166666666666));
#421672=CARTESIAN_POINT('Ctrl Pts',(-1.43925448419923E-16,-1.17524047358087,
-2.49999999999999));
#421673=CARTESIAN_POINT('Ctrl Pts',(0.678525403784459,-1.17524047358087,
-2.45833333333332));
#421674=CARTESIAN_POINT('Ctrl Pts',(1.01778810567669,-0.587620236790434,
-2.41666666666666));
#421675=CARTESIAN_POINT('Ctrl Pts',(1.35705080756892,2.29132664526027E-15,
-2.37499999999999));
#421676=CARTESIAN_POINT('Ctrl Pts',(1.01778810567669,0.587620236790438,
-2.33333333333332));
#421677=CARTESIAN_POINT('Ctrl Pts',(0.67852540378446,1.17524047358087,-2.29166666666666));
#421678=CARTESIAN_POINT('Ctrl Pts',(0.,1.17524047358087,-2.24999999999999));
#421679=CARTESIAN_POINT('Ctrl Pts',(-0.678525403784459,1.17524047358087,
-2.20833333333332));
#421680=CARTESIAN_POINT('Ctrl Pts',(-1.01778810567669,0.587620236790438,
-2.16666666666666));
#421681=CARTESIAN_POINT('Ctrl Pts',(-1.35705080756892,2.62370823081419E-15,
-2.12499999999999));
#421682=CARTESIAN_POINT('Ctrl Pts',(-1.01778810567669,-0.587620236790433,
-2.08333333333332));
#421683=CARTESIAN_POINT('Ctrl Pts',(-0.67852540378446,-1.17524047358087,
-2.04166666666666));
#421684=CARTESIAN_POINT('Ctrl Pts',(-1.43925448419923E-16,-1.17524047358087,
-1.99999999999999));
#421685=CARTESIAN_POINT('Ctrl Pts',(0.678525403784459,-1.17524047358087,
-1.95833333333332));
#421686=CARTESIAN_POINT('Ctrl Pts',(1.01778810567669,-0.587620236790434,
-1.91666666666666));
#421687=CARTESIAN_POINT('Ctrl Pts',(1.35705080756892,2.29132664526027E-15,
-1.87499999999999));
#421688=CARTESIAN_POINT('Ctrl Pts',(1.01778810567669,0.587620236790438,
-1.83333333333332));
#421689=CARTESIAN_POINT('Ctrl Pts',(0.67852540378446,1.17524047358087,-1.79166666666666));
#421690=CARTESIAN_POINT('Ctrl Pts',(0.,1.17524047358087,-1.74999999999999));
#421691=CARTESIAN_POINT('Ctrl Pts',(-0.678525403784459,1.17524047358087,
-1.70833333333332));
#421692=CARTESIAN_POINT('Ctrl Pts',(-1.01778810567669,0.587620236790438,
-1.66666666666666));
#421693=CARTESIAN_POINT('Ctrl Pts',(-1.35705080756892,2.62370823081419E-15,
-1.62499999999999));
#421694=CARTESIAN_POINT('Ctrl Pts',(-1.01778810567669,-0.587620236790433,
-1.58333333333332));
#421695=CARTESIAN_POINT('Ctrl Pts',(-0.67852540378446,-1.17524047358087,
-1.54166666666666));
#421696=CARTESIAN_POINT('Ctrl Pts',(-1.43925448419923E-16,-1.17524047358087,
-1.49999999999999));
#421697=CARTESIAN_POINT('Ctrl Pts',(0.678525403784459,-1.17524047358087,
-1.45833333333332));
#421698=CARTESIAN_POINT('Ctrl Pts',(1.01778810567669,-0.587620236790434,
-1.41666666666666));
#421699=CARTESIAN_POINT('Ctrl Pts',(1.35705080756892,2.29132664526027E-15,
-1.37499999999999));
#421700=CARTESIAN_POINT('Ctrl Pts',(1.01778810567669,0.587620236790438,
-1.33333333333332));
#421701=CARTESIAN_POINT('Ctrl Pts',(0.67852540378446,1.17524047358087,-1.29166666666666));
#421702=CARTESIAN_POINT('Ctrl Pts',(0.,1.17524047358087,-1.24999999999999));
#421703=CARTESIAN_POINT('Ctrl Pts',(-0.678525403784459,1.17524047358087,
-1.20833333333332));
#421704=CARTESIAN_POINT('Ctrl Pts',(-1.01778810567669,0.587620236790438,
-1.16666666666666));
#421705=CARTESIAN_POINT('Ctrl Pts',(-1.35705080756892,2.62370823081419E-15,
-1.12499999999999));
#421706=CARTESIAN_POINT('Ctrl Pts',(-1.01778810567669,-0.587620236790433,
-1.08333333333332));
#421707=CARTESIAN_POINT('Ctrl Pts',(-0.67852540378446,-1.17524047358087,
-1.04166666666666));
#421708=CARTESIAN_POINT('Ctrl Pts',(-1.43925448419923E-16,-1.17524047358087,
-0.99999999999999));
#421709=CARTESIAN_POINT('Ctrl Pts',(0.678525403784459,-1.17524047358087,
-0.958333333333323));
#421710=CARTESIAN_POINT('Ctrl Pts',(1.01778810567669,-0.587620236790434,
-0.916666666666658));
#421711=CARTESIAN_POINT('Ctrl Pts',(1.35705080756892,2.29132664526027E-15,
-0.87499999999999));
#421712=CARTESIAN_POINT('Ctrl Pts',(1.01778810567669,0.587620236790438,
-0.833333333333323));
#421713=CARTESIAN_POINT('Ctrl Pts',(0.67852540378446,1.17524047358087,-0.791666666666657));
#421714=CARTESIAN_POINT('Ctrl Pts',(0.,1.17524047358087,-0.74999999999999));
#421715=CARTESIAN_POINT('Ctrl Pts',(-0.678525403784459,1.17524047358087,
-0.708333333333325));
#421716=CARTESIAN_POINT('Ctrl Pts',(-1.01778810567669,0.587620236790438,
-0.666666666666658));
#421717=CARTESIAN_POINT('Ctrl Pts',(-1.35705080756892,2.62370823081419E-15,
-0.62499999999999));
#421718=CARTESIAN_POINT('Ctrl Pts',(-1.01778810567669,-0.587620236790433,
-0.583333333333325));
#421719=CARTESIAN_POINT('Ctrl Pts',(-0.67852540378446,-1.17524047358087,
-0.541666666666657));
#421720=CARTESIAN_POINT('Ctrl Pts',(-1.43925448419923E-16,-1.17524047358087,
-0.49999999999999));
#421721=CARTESIAN_POINT('Ctrl Pts',(0.678525403784459,-1.17524047358087,
-0.458333333333324));
#421722=CARTESIAN_POINT('Ctrl Pts',(1.01778810567669,-0.587620236790434,
-0.416666666666657));
#421723=CARTESIAN_POINT('Ctrl Pts',(1.35705080756892,2.29132664526027E-15,
-0.37499999999999));
#421724=CARTESIAN_POINT('Ctrl Pts',(1.01778810567669,0.587620236790438,
-0.333333333333324));
#421725=CARTESIAN_POINT('Ctrl Pts',(0.67852540378446,1.17524047358087,-0.291666666666657));
#421726=CARTESIAN_POINT('Ctrl Pts',(0.,1.17524047358087,-0.24999999999999));
#421727=CARTESIAN_POINT('Ctrl Pts',(-0.678525403784459,1.17524047358087,
-0.208333333333324));
#421728=CARTESIAN_POINT('Ctrl Pts',(-1.01778810567669,0.587620236790438,
-0.166666666666657));
#421729=CARTESIAN_POINT('Ctrl Pts',(-1.35705080756892,2.62370823081419E-15,
-0.124999999999991));
#421730=CARTESIAN_POINT('Ctrl Pts',(-1.01778810567669,-0.587620236790433,
-0.0833333333333242));
#421731=CARTESIAN_POINT('Ctrl Pts',(-0.67852540378446,-1.17524047358087,
-0.0416666666666569));
#421732=CARTESIAN_POINT('Ctrl Pts',(-1.43925448419923E-16,-1.17524047358087,
8.67361737988404E-15));
#421733=CARTESIAN_POINT('Ctrl Pts',(0.678525403784459,-1.17524047358087,
0.041666666666676));
#421734=CARTESIAN_POINT('Ctrl Pts',(1.01778810567669,-0.587620236790434,
0.0833333333333432));
#421735=CARTESIAN_POINT('Ctrl Pts',(1.35705080756892,2.29132664526027E-15,
0.125000000000009));
#421736=CARTESIAN_POINT('Ctrl Pts',(1.01778810567669,0.587620236790438,
0.166666666666676));
#421737=CARTESIAN_POINT('Ctrl Pts',(0.67852540378446,1.17524047358087,0.208333333333343));
#421738=CARTESIAN_POINT('Ctrl Pts',(0.,1.17524047358087,0.250000000000009));
#421739=CARTESIAN_POINT('Ctrl Pts',(-0.678525403784459,1.17524047358087,
0.291666666666676));
#421740=CARTESIAN_POINT('Ctrl Pts',(-1.01778810567669,0.587620236790438,
0.333333333333343));
#421741=CARTESIAN_POINT('Ctrl Pts',(-1.35705080756892,2.62370823081419E-15,
0.375000000000009));
#421742=CARTESIAN_POINT('Ctrl Pts',(-1.01778810567669,-0.587620236790433,
0.416666666666676));
#421743=CARTESIAN_POINT('Ctrl Pts',(-0.67852540378446,-1.17524047358087,
0.458333333333344));
#421744=CARTESIAN_POINT('Ctrl Pts',(-1.43925448419923E-16,-1.17524047358087,
0.500000000000009));
#421745=CARTESIAN_POINT('Ctrl Pts',(0.678525403784459,-1.17524047358087,
0.541666666666676));
#421746=CARTESIAN_POINT('Ctrl Pts',(1.01778810567669,-0.587620236790434,
0.583333333333342));
#421747=CARTESIAN_POINT('Ctrl Pts',(1.35705080756892,2.29132664526027E-15,
0.625000000000009));
#421748=CARTESIAN_POINT('Ctrl Pts',(1.01778810567669,0.587620236790438,
0.666666666666677));
#421749=CARTESIAN_POINT('Ctrl Pts',(0.67852540378446,1.17524047358087,0.708333333333342));
#421750=CARTESIAN_POINT('Ctrl Pts',(0.,1.17524047358087,0.750000000000009));
#421751=CARTESIAN_POINT('Ctrl Pts',(-0.678525403784459,1.17524047358087,
0.791666666666677));
#421752=CARTESIAN_POINT('Ctrl Pts',(-1.01778810567669,0.587620236790438,
0.833333333333342));
#421753=CARTESIAN_POINT('Ctrl Pts',(-1.35705080756892,2.62370823081419E-15,
0.87500000000001));
#421754=CARTESIAN_POINT('Ctrl Pts',(-1.01778810567669,-0.587620236790433,
0.916666666666677));
#421755=CARTESIAN_POINT('Ctrl Pts',(-0.67852540378446,-1.17524047358087,
0.958333333333342));
#421756=CARTESIAN_POINT('Ctrl Pts',(-1.43925448419923E-16,-1.17524047358087,
1.00000000000001));
#421757=CARTESIAN_POINT('Ctrl Pts',(0.678525403784459,-1.17524047358087,
1.04166666666668));
#421758=CARTESIAN_POINT('Ctrl Pts',(1.01778810567669,-0.587620236790434,
1.08333333333334));
#421759=CARTESIAN_POINT('Ctrl Pts',(1.35705080756892,2.29132664526027E-15,
1.12500000000001));
#421760=CARTESIAN_POINT('Ctrl Pts',(1.01778810567669,0.587620236790438,
1.16666666666668));
#421761=CARTESIAN_POINT('Ctrl Pts',(0.67852540378446,1.17524047358087,1.20833333333334));
#421762=CARTESIAN_POINT('Ctrl Pts',(0.,1.17524047358087,1.25000000000001));
#421763=CARTESIAN_POINT('Ctrl Pts',(-0.678525403784459,1.17524047358087,
1.29166666666668));
#421764=CARTESIAN_POINT('Ctrl Pts',(-1.01778810567669,0.587620236790438,
1.33333333333334));
#421765=CARTESIAN_POINT('Ctrl Pts',(-1.35705080756892,2.62370823081419E-15,
1.37500000000001));
#421766=CARTESIAN_POINT('Ctrl Pts',(-1.01778810567669,-0.587620236790433,
1.41666666666668));
#421767=CARTESIAN_POINT('Ctrl Pts',(-0.67852540378446,-1.17524047358087,
1.45833333333334));
#421768=CARTESIAN_POINT('Ctrl Pts',(-1.43925448419923E-16,-1.17524047358087,
1.50000000000001));
#421769=CARTESIAN_POINT('Ctrl Pts',(0.678525403784459,-1.17524047358087,
1.54166666666668));
#421770=CARTESIAN_POINT('Ctrl Pts',(1.01778810567669,-0.587620236790434,
1.58333333333334));
#421771=CARTESIAN_POINT('Ctrl Pts',(1.35705080756892,2.29132664526027E-15,
1.62500000000001));
#421772=CARTESIAN_POINT('Ctrl Pts',(1.01778810567669,0.587620236790438,
1.66666666666668));
#421773=CARTESIAN_POINT('Ctrl Pts',(0.67852540378446,1.17524047358087,1.70833333333334));
#421774=CARTESIAN_POINT('Ctrl Pts',(0.,1.17524047358087,1.75000000000001));
#421775=CARTESIAN_POINT('Ctrl Pts',(-0.678525403784459,1.17524047358087,
1.79166666666668));
#421776=CARTESIAN_POINT('Ctrl Pts',(-1.01778810567669,0.587620236790438,
1.83333333333334));
#421777=CARTESIAN_POINT('Ctrl Pts',(-1.35705080756892,2.62370823081419E-15,
1.87500000000001));
#421778=CARTESIAN_POINT('Ctrl Pts',(-1.01778810567669,-0.587620236790433,
1.91666666666668));
#421779=CARTESIAN_POINT('Ctrl Pts',(-0.67852540378446,-1.17524047358087,
1.95833333333334));
#421780=CARTESIAN_POINT('Ctrl Pts',(-1.43925448419923E-16,-1.17524047358087,
2.00000000000001));
#421781=CARTESIAN_POINT('Ctrl Pts',(0.678525403784459,-1.17524047358087,
2.04166666666668));
#421782=CARTESIAN_POINT('Ctrl Pts',(1.01778810567669,-0.587620236790434,
2.08333333333334));
#421783=CARTESIAN_POINT('Ctrl Pts',(1.35705080756892,2.29132664526027E-15,
2.12500000000001));
#421784=CARTESIAN_POINT('Ctrl Pts',(1.01778810567669,0.587620236790438,
2.16666666666668));
#421785=CARTESIAN_POINT('Ctrl Pts',(0.67852540378446,1.17524047358087,2.20833333333334));
#421786=CARTESIAN_POINT('Ctrl Pts',(0.,1.17524047358087,2.25000000000001));
#421787=CARTESIAN_POINT('Ctrl Pts',(-0.678525403784459,1.17524047358087,
2.29166666666668));
#421788=CARTESIAN_POINT('Ctrl Pts',(-1.01778810567669,0.587620236790438,
2.33333333333334));
#421789=CARTESIAN_POINT('Ctrl Pts',(-1.35705080756892,2.62370823081419E-15,
2.37500000000001));
#421790=CARTESIAN_POINT('Ctrl Pts',(-1.01778810567669,-0.587620236790433,
2.41666666666668));
#421791=CARTESIAN_POINT('Ctrl Pts',(-0.67852540378446,-1.17524047358087,
2.45833333333334));
#421792=CARTESIAN_POINT('Ctrl Pts',(-1.43925448419923E-16,-1.17524047358087,
2.50000000000001));
#421793=CARTESIAN_POINT('Ctrl Pts',(0.678525403784459,-1.17524047358087,
2.54166666666668));
#421794=CARTESIAN_POINT('Ctrl Pts',(1.01778810567669,-0.587620236790434,
2.58333333333334));
#421795=CARTESIAN_POINT('Ctrl Pts',(1.35705080756892,2.29132664526027E-15,
2.62500000000001));
#421796=CARTESIAN_POINT('Ctrl Pts',(1.01778810567669,0.587620236790438,
2.66666666666668));
#421797=CARTESIAN_POINT('Ctrl Pts',(0.67852540378446,1.17524047358087,2.70833333333334));
#421798=CARTESIAN_POINT('Ctrl Pts',(0.,1.17524047358087,2.75000000000001));
#421799=CARTESIAN_POINT('Ctrl Pts',(-0.678525403784459,1.17524047358087,
2.79166666666668));
#421800=CARTESIAN_POINT('Ctrl Pts',(-1.01778810567669,0.587620236790438,
2.83333333333334));
#421801=CARTESIAN_POINT('Ctrl Pts',(-1.35705080756892,2.62370823081419E-15,
2.87500000000001));
#421802=CARTESIAN_POINT('Ctrl Pts',(-1.01778810567669,-0.587620236790433,
2.91666666666668));
#421803=CARTESIAN_POINT('Ctrl Pts',(-0.67852540378446,-1.17524047358087,
2.95833333333334));
#421804=CARTESIAN_POINT('Ctrl Pts',(-1.43925448419923E-16,-1.17524047358087,
3.00000000000001));
#421805=CARTESIAN_POINT('Ctrl Pts',(0.678525403784459,-1.17524047358087,
3.04166666666668));
#421806=CARTESIAN_POINT('Ctrl Pts',(1.01778810567669,-0.587620236790434,
3.08333333333334));
#421807=CARTESIAN_POINT('Ctrl Pts',(1.35705080756892,2.29132664526027E-15,
3.12500000000001));
#421808=CARTESIAN_POINT('Ctrl Pts',(1.01778810567669,0.587620236790438,
3.16666666666668));
#421809=CARTESIAN_POINT('Ctrl Pts',(0.67852540378446,1.17524047358087,3.20833333333334));
#421810=CARTESIAN_POINT('Ctrl Pts',(0.,1.17524047358087,3.25000000000001));
#421811=CARTESIAN_POINT('Ctrl Pts',(-0.678525403784459,1.17524047358087,
3.29166666666668));
#421812=CARTESIAN_POINT('Ctrl Pts',(-1.01778810567669,0.587620236790438,
3.33333333333334));
#421813=CARTESIAN_POINT('Ctrl Pts',(-1.35705080756892,2.62370823081419E-15,
3.37500000000001));
#421814=CARTESIAN_POINT('Ctrl Pts',(-1.01778810567669,-0.587620236790433,
3.41666666666668));
#421815=CARTESIAN_POINT('Ctrl Pts',(-0.67852540378446,-1.17524047358087,
3.45833333333334));
#421816=CARTESIAN_POINT('Ctrl Pts',(-1.43925448419923E-16,-1.17524047358087,
3.50000000000001));
#421817=CARTESIAN_POINT('Ctrl Pts',(0.678525403784459,-1.17524047358087,
3.54166666666668));
#421818=CARTESIAN_POINT('Ctrl Pts',(1.01778810567669,-0.587620236790434,
3.58333333333334));
#421819=CARTESIAN_POINT('Ctrl Pts',(1.35705080756892,2.29132664526027E-15,
3.62500000000001));
#421820=CARTESIAN_POINT('Ctrl Pts',(1.01778810567669,0.587620236790438,
3.66666666666668));
#421821=CARTESIAN_POINT('Ctrl Pts',(0.67852540378446,1.17524047358087,3.70833333333334));
#421822=CARTESIAN_POINT('Ctrl Pts',(0.,1.17524047358087,3.75000000000001));
#421823=CARTESIAN_POINT('Ctrl Pts',(-0.678525403784459,1.17524047358087,
3.79166666666668));
#421824=CARTESIAN_POINT('Ctrl Pts',(-1.01778810567669,0.587620236790438,
3.83333333333334));
#421825=CARTESIAN_POINT('Ctrl Pts',(-1.35705080756892,2.62370823081419E-15,
3.87500000000001));
#421826=CARTESIAN_POINT('Ctrl Pts',(-1.01778810567669,-0.587620236790433,
3.91666666666668));
#421827=CARTESIAN_POINT('Ctrl Pts',(-0.67852540378446,-1.17524047358087,
3.95833333333334));
#421828=CARTESIAN_POINT('Ctrl Pts',(-1.43925448419923E-16,-1.17524047358087,
4.00000000000001));
#421829=CARTESIAN_POINT('Ctrl Pts',(0.678525403784459,-1.17524047358087,
4.04166666666667));
#421830=CARTESIAN_POINT('Ctrl Pts',(1.01778810567669,-0.587620236790434,
4.08333333333334));
#421831=CARTESIAN_POINT('Ctrl Pts',(1.35705080756892,2.29132664526027E-15,
4.12500000000001));
#421832=CARTESIAN_POINT('Ctrl Pts',(1.01778810567669,0.587620236790438,
4.16666666666667));
#421833=CARTESIAN_POINT('Ctrl Pts',(0.67852540378446,1.17524047358087,4.20833333333334));
#421834=CARTESIAN_POINT('Ctrl Pts',(0.,1.17524047358087,4.25000000000001));
#421835=CARTESIAN_POINT('Ctrl Pts',(-0.678525403784459,1.17524047358087,
4.29166666666667));
#421836=CARTESIAN_POINT('Ctrl Pts',(-1.01778810567669,0.587620236790438,
4.33333333333334));
#421837=CARTESIAN_POINT('Ctrl Pts',(-1.35705080756892,2.62370823081419E-15,
4.37500000000001));
#421838=CARTESIAN_POINT('Ctrl Pts',(-1.01778810567669,-0.587620236790433,
4.41666666666667));
#421839=CARTESIAN_POINT('Ctrl Pts',(-0.67852540378446,-1.17524047358087,
4.45833333333334));
#421840=CARTESIAN_POINT('Ctrl Pts',(-1.43925448419923E-16,-1.17524047358087,
4.50000000000001));
#421841=CARTESIAN_POINT('Ctrl Pts',(0.678525403784459,-1.17524047358087,
4.54166666666667));
#421842=CARTESIAN_POINT('Ctrl Pts',(1.01778810567669,-0.587620236790434,
4.58333333333334));
#421843=CARTESIAN_POINT('Ctrl Pts',(1.35705080756892,2.29132664526027E-15,
4.62500000000001));
#421844=CARTESIAN_POINT('Ctrl Pts',(1.01778810567669,0.587620236790438,
4.66666666666667));
#421845=CARTESIAN_POINT('Ctrl Pts',(0.67852540378446,1.17524047358087,4.70833333333334));
#421846=CARTESIAN_POINT('Ctrl Pts',(0.,1.17524047358087,4.75000000000001));
#421847=CARTESIAN_POINT('Ctrl Pts',(-0.678525403784459,1.17524047358087,
4.79166666666667));
#421848=CARTESIAN_POINT('Ctrl Pts',(-1.01778810567669,0.587620236790438,
4.83333333333334));
#421849=CARTESIAN_POINT('Ctrl Pts',(-1.35705080756892,2.62370823081419E-15,
4.87500000000001));
#421850=CARTESIAN_POINT('Ctrl Pts',(-1.01778810567669,-0.587620236790433,
4.91666666666667));
#421851=CARTESIAN_POINT('Ctrl Pts',(-0.67852540378446,-1.17524047358087,
4.95833333333334));
#421852=CARTESIAN_POINT('Ctrl Pts',(-1.43925448419923E-16,-1.17524047358087,
5.00000000000001));
#421853=CARTESIAN_POINT('Ctrl Pts',(0.678525403784459,-1.17524047358087,
5.04166666666667));
#421854=CARTESIAN_POINT('Ctrl Pts',(1.01778810567669,-0.587620236790434,
5.08333333333335));
#421855=CARTESIAN_POINT('Ctrl Pts',(1.35705080756892,2.29132664526027E-15,
5.12500000000001));
#421856=CARTESIAN_POINT('Ctrl Pts',(1.01778810567669,0.587620236790438,
5.16666666666667));
#421857=CARTESIAN_POINT('Ctrl Pts',(0.67852540378446,1.17524047358087,5.20833333333334));
#421858=CARTESIAN_POINT('Ctrl Pts',(0.,1.17524047358087,5.25000000000001));
#421859=CARTESIAN_POINT('Ctrl Pts',(-0.678525403784459,1.17524047358087,
5.29166666666668));
#421860=CARTESIAN_POINT('Ctrl Pts',(-1.01778810567669,0.587620236790438,
5.33333333333334));
#421861=CARTESIAN_POINT('Ctrl Pts',(-1.35705080756892,2.62370823081419E-15,
5.37500000000001));
#421862=CARTESIAN_POINT('Ctrl Pts',(-1.01778810567669,-0.587620236790433,
5.41666666666668));
#421863=CARTESIAN_POINT('Ctrl Pts',(-0.67852540378446,-1.17524047358087,
5.45833333333334));
#421864=CARTESIAN_POINT('Ctrl Pts',(-1.43925448419923E-16,-1.17524047358087,
5.50000000000001));
#421865=CARTESIAN_POINT('Ctrl Pts',(0.678525403784459,-1.17524047358087,
5.54166666666667));
#421866=CARTESIAN_POINT('Ctrl Pts',(1.01778810567669,-0.587620236790434,
5.58333333333334));
#421867=CARTESIAN_POINT('Ctrl Pts',(1.35705080756892,2.29132664526027E-15,
5.62500000000001));
#421868=CARTESIAN_POINT('Ctrl Pts',(1.01778810567669,0.587620236790438,
5.66666666666668));
#421869=CARTESIAN_POINT('Ctrl Pts',(0.67852540378446,1.17524047358087,5.70833333333334));
#421870=CARTESIAN_POINT('Ctrl Pts',(0.,1.17524047358087,5.75000000000001));
#421871=CARTESIAN_POINT('Ctrl Pts',(-0.678525403784459,1.17524047358087,
5.79166666666668));
#421872=CARTESIAN_POINT('Ctrl Pts',(-1.01778810567669,0.587620236790438,
5.83333333333334));
#421873=CARTESIAN_POINT('Ctrl Pts',(-1.35705080756892,2.62370823081419E-15,
5.87500000000001));
#421874=CARTESIAN_POINT('Ctrl Pts',(-1.01778810567669,-0.587620236790433,
5.91666666666668));
#421875=CARTESIAN_POINT('Ctrl Pts',(-0.67852540378446,-1.17524047358087,
5.95833333333334));
#421876=CARTESIAN_POINT('Ctrl Pts',(-1.43925448419923E-16,-1.17524047358087,
6.00000000000001));
#421877=CARTESIAN_POINT('Ctrl Pts',(0.678525403784459,-1.17524047358087,
6.04166666666668));
#421878=CARTESIAN_POINT('Ctrl Pts',(1.01778810567669,-0.587620236790434,
6.08333333333334));
#421879=CARTESIAN_POINT('Ctrl Pts',(1.35705080756892,2.29132664526027E-15,
6.12500000000001));
#421880=CARTESIAN_POINT('Ctrl Pts',(1.01778810567669,0.587620236790438,
6.16666666666668));
#421881=CARTESIAN_POINT('Ctrl Pts',(0.67852540378446,1.17524047358087,6.20833333333334));
#421882=CARTESIAN_POINT('Ctrl Pts',(0.,1.17524047358087,6.25000000000001));
#421883=CARTESIAN_POINT('Ctrl Pts',(-0.678525403784459,1.17524047358087,
6.29166666666668));
#421884=CARTESIAN_POINT('Ctrl Pts',(-1.01778810567669,0.587620236790438,
6.33333333333334));
#421885=CARTESIAN_POINT('Ctrl Pts',(-1.35705080756892,2.62370823081419E-15,
6.37500000000001));
#421886=CARTESIAN_POINT('Ctrl Pts',(-1.01778810567669,-0.587620236790433,
6.41666666666668));
#421887=CARTESIAN_POINT('Ctrl Pts',(-0.67852540378446,-1.17524047358087,
6.45833333333334));
#421888=CARTESIAN_POINT('Ctrl Pts',(-1.43925448419923E-16,-1.17524047358087,
6.50000000000001));
#421889=CARTESIAN_POINT('Ctrl Pts',(0.678525403784459,-1.17524047358087,
6.54166666666668));
#421890=CARTESIAN_POINT('Ctrl Pts',(1.01778810567669,-0.587620236790434,
6.58333333333334));
#421891=CARTESIAN_POINT('Ctrl Pts',(1.35705080756892,2.29132664526027E-15,
6.62500000000001));
#421892=CARTESIAN_POINT('Ctrl Pts',(1.01778810567669,0.587620236790438,
6.66666666666668));
#421893=CARTESIAN_POINT('Ctrl Pts',(0.67852540378446,1.17524047358087,6.70833333333334));
#421894=CARTESIAN_POINT('Ctrl Pts',(0.,1.17524047358087,6.75000000000001));
#421895=CARTESIAN_POINT('Ctrl Pts',(-0.678525403784459,1.17524047358087,
6.79166666666668));
#421896=CARTESIAN_POINT('Ctrl Pts',(-1.01778810567669,0.587620236790438,
6.83333333333334));
#421897=CARTESIAN_POINT('Ctrl Pts',(-1.35705080756892,2.62370823081419E-15,
6.87500000000001));
#421898=CARTESIAN_POINT('Ctrl Pts',(-1.01778810567669,-0.587620236790433,
6.91666666666668));
#421899=CARTESIAN_POINT('Ctrl Pts',(-0.67852540378446,-1.17524047358087,
6.95833333333334));
#421900=CARTESIAN_POINT('Ctrl Pts',(-1.43925448419923E-16,-1.17524047358087,
7.00000000000001));
#421901=CARTESIAN_POINT('Ctrl Pts',(0.678525403784459,-1.17524047358087,
7.04166666666668));
#421902=CARTESIAN_POINT('Ctrl Pts',(1.01778810567669,-0.587620236790434,
7.08333333333334));
#421903=CARTESIAN_POINT('Ctrl Pts',(1.35705080756892,2.29132664526027E-15,
7.12500000000001));
#421904=CARTESIAN_POINT('Ctrl Pts',(1.01778810567669,0.587620236790438,
7.16666666666668));
#421905=CARTESIAN_POINT('Ctrl Pts',(0.67852540378446,1.17524047358087,7.20833333333334));
#421906=CARTESIAN_POINT('Ctrl Pts',(0.,1.17524047358087,7.25000000000001));
#421907=CARTESIAN_POINT('Ctrl Pts',(-0.678525403784459,1.17524047358087,
7.29166666666668));
#421908=CARTESIAN_POINT('Ctrl Pts',(-1.01778810567669,0.587620236790438,
7.33333333333334));
#421909=CARTESIAN_POINT('Ctrl Pts',(-1.35705080756892,2.62370823081419E-15,
7.37500000000001));
#421910=CARTESIAN_POINT('Ctrl Pts',(-1.01778810567669,-0.587620236790433,
7.41666666666668));
#421911=CARTESIAN_POINT('Ctrl Pts',(-0.67852540378446,-1.17524047358087,
7.45833333333334));
#421912=CARTESIAN_POINT('Ctrl Pts',(-1.43925448419923E-16,-1.17524047358087,
7.50000000000001));
#421913=CARTESIAN_POINT('Ctrl Pts',(0.678525403784459,-1.17524047358087,
7.54166666666668));
#421914=CARTESIAN_POINT('Ctrl Pts',(1.01778810567669,-0.587620236790434,
7.58333333333334));
#421915=CARTESIAN_POINT('Ctrl Pts',(1.35705080756892,2.29132664526027E-15,
7.62500000000001));
#421916=CARTESIAN_POINT('Ctrl Pts',(1.01778810567669,0.587620236790438,
7.66666666666668));
#421917=CARTESIAN_POINT('Ctrl Pts',(0.67852540378446,1.17524047358087,7.70833333333334));
#421918=CARTESIAN_POINT('Ctrl Pts',(0.,1.17524047358087,7.75000000000001));
#421919=CARTESIAN_POINT('Ctrl Pts',(-0.678525403784459,1.17524047358087,
7.79166666666667));
#421920=CARTESIAN_POINT('Ctrl Pts',(-1.01778810567669,0.587620236790438,
7.83333333333334));
#421921=CARTESIAN_POINT('Ctrl Pts',(-1.35705080756892,2.62370823081419E-15,
7.87500000000001));
#421922=CARTESIAN_POINT('Ctrl Pts',(-1.01778810567669,-0.587620236790433,
7.91666666666667));
#421923=CARTESIAN_POINT('Ctrl Pts',(-0.67852540378446,-1.17524047358087,
7.95833333333334));
#421924=CARTESIAN_POINT('Ctrl Pts',(-1.43925448419923E-16,-1.17524047358087,
8.00000000000001));
#421925=CARTESIAN_POINT('Ctrl Pts',(0.678525403784459,-1.17524047358087,
8.04166666666667));
#421926=CARTESIAN_POINT('Ctrl Pts',(1.01778810567669,-0.587620236790434,
8.08333333333334));
#421927=CARTESIAN_POINT('Ctrl Pts',(1.35705080756892,2.29132664526027E-15,
8.12500000000001));
#421928=CARTESIAN_POINT('Ctrl Pts',(1.01778810567669,0.587620236790438,
8.16666666666667));
#421929=CARTESIAN_POINT('Ctrl Pts',(0.67852540378446,1.17524047358087,8.20833333333334));
#421930=CARTESIAN_POINT('Ctrl Pts',(0.,1.17524047358087,8.25000000000001));
#421931=CARTESIAN_POINT('Ctrl Pts',(-0.678525403784459,1.17524047358087,
8.29166666666667));
#421932=CARTESIAN_POINT('Ctrl Pts',(-1.01778810567669,0.587620236790438,
8.33333333333334));
#421933=CARTESIAN_POINT('Ctrl Pts',(-1.35705080756892,2.62370823081419E-15,
8.37500000000001));
#421934=CARTESIAN_POINT('Ctrl Pts',(-1.01778810567669,-0.587620236790433,
8.41666666666667));
#421935=CARTESIAN_POINT('Ctrl Pts',(-0.67852540378446,-1.17524047358087,
8.45833333333335));
#421936=CARTESIAN_POINT('Ctrl Pts',(-1.43925448419923E-16,-1.17524047358087,
8.50000000000001));
#421937=CARTESIAN_POINT('Ctrl Pts',(0.678525403784459,-1.17524047358087,
8.54166666666667));
#421938=CARTESIAN_POINT('Ctrl Pts',(1.01778810567669,-0.587620236790434,
8.58333333333334));
#421939=CARTESIAN_POINT('Ctrl Pts',(1.35705080756892,2.29132664526027E-15,
8.62500000000001));
#421940=CARTESIAN_POINT('Ctrl Pts',(1.01778810567669,0.587620236790438,
8.66666666666667));
#421941=CARTESIAN_POINT('Ctrl Pts',(0.67852540378446,1.17524047358087,8.70833333333334));
#421942=CARTESIAN_POINT('Ctrl Pts',(0.,1.17524047358087,8.75000000000001));
#421943=CARTESIAN_POINT('Ctrl Pts',(-0.678525403784459,1.17524047358087,
8.79166666666667));
#421944=CARTESIAN_POINT('Ctrl Pts',(-1.01778810567669,0.587620236790438,
8.83333333333334));
#421945=CARTESIAN_POINT('Ctrl Pts',(-1.35705080756892,2.62370823081419E-15,
8.87500000000001));
#421946=CARTESIAN_POINT('Ctrl Pts',(-1.01778810567669,-0.587620236790433,
8.91666666666667));
#421947=CARTESIAN_POINT('Ctrl Pts',(-0.67852540378446,-1.17524047358087,
8.95833333333334));
#421948=CARTESIAN_POINT('Ctrl Pts',(-1.43925448419923E-16,-1.17524047358087,
9.00000000000001));
#421949=CARTESIAN_POINT('Ctrl Pts',(0.678525403784459,-1.17524047358087,
9.04166666666667));
#421950=CARTESIAN_POINT('Ctrl Pts',(1.01778810567669,-0.587620236790434,
9.08333333333334));
#421951=CARTESIAN_POINT('Ctrl Pts',(1.35705080756892,2.29132664526027E-15,
9.12500000000001));
#421952=CARTESIAN_POINT('Ctrl Pts',(1.01778810567669,0.587620236790438,
9.16666666666667));
#421953=CARTESIAN_POINT('Ctrl Pts',(0.67852540378446,1.17524047358087,9.20833333333334));
#421954=CARTESIAN_POINT('Ctrl Pts',(0.,1.17524047358087,9.25000000000001));
#421955=CARTESIAN_POINT('Ctrl Pts',(-0.678525403784459,1.17524047358087,
9.29166666666668));
#421956=CARTESIAN_POINT('Ctrl Pts',(-1.01778810567669,0.587620236790438,
9.33333333333334));
#421957=CARTESIAN_POINT('Ctrl Pts',(-1.35705080756892,2.62370823081419E-15,
9.37500000000001));
#421958=CARTESIAN_POINT('Ctrl Pts',(-1.01778810567669,-0.587620236790433,
9.41666666666667));
#421959=CARTESIAN_POINT('Ctrl Pts',(-0.67852540378446,-1.17524047358087,
9.45833333333334));
#421960=CARTESIAN_POINT('Ctrl Pts',(-1.43925448419923E-16,-1.17524047358087,
9.50000000000001));
#421961=CARTESIAN_POINT('Ctrl Pts',(0.678525403784459,-1.17524047358087,
9.54166666666667));
#421962=CARTESIAN_POINT('Ctrl Pts',(1.01778810567669,-0.587620236790434,
9.58333333333334));
#421963=CARTESIAN_POINT('Ctrl Pts',(1.35705080756892,2.29132664526027E-15,
9.62500000000001));
#421964=CARTESIAN_POINT('Ctrl Pts',(1.01778810567669,0.587620236790438,
9.66666666666667));
#421965=CARTESIAN_POINT('Ctrl Pts',(0.67852540378446,1.17524047358087,9.70833333333334));
#421966=CARTESIAN_POINT('Ctrl Pts',(0.,1.17524047358087,9.75000000000001));
#421967=CARTESIAN_POINT('Ctrl Pts',(-0.678525403784459,1.17524047358087,
9.79166666666668));
#421968=CARTESIAN_POINT('Ctrl Pts',(-1.01778810567669,0.587620236790438,
9.83333333333334));
#421969=CARTESIAN_POINT('Ctrl Pts',(-1.35705080756892,2.62370823081419E-15,
9.87500000000001));
#421970=CARTESIAN_POINT('Ctrl Pts',(-1.01778810567669,-0.587620236790433,
9.91666666666668));
#421971=CARTESIAN_POINT('Ctrl Pts',(-0.67852540378446,-1.17524047358087,
9.95833333333334));
#421972=CARTESIAN_POINT('Ctrl Pts',(-1.43925448419923E-16,-1.17524047358087,
10.));
#421973=CARTESIAN_POINT('Ctrl Pts',(0.678525403784459,-1.17524047358087,
10.0416666666667));
#421974=CARTESIAN_POINT('Ctrl Pts',(1.01778810567669,-0.587620236790434,
10.0833333333333));
#421975=CARTESIAN_POINT('Ctrl Pts',(1.35705080756892,2.29132664526027E-15,
10.125));
#421976=CARTESIAN_POINT('Ctrl Pts',(1.01778810567669,0.587620236790438,
10.1666666666667));
#421977=CARTESIAN_POINT('Ctrl Pts',(0.67852540378446,1.17524047358087,10.2083333333333));
#421978=CARTESIAN_POINT('Ctrl Pts',(0.,1.17524047358087,10.25));
#421979=CARTESIAN_POINT('Ctrl Pts',(-0.678525403784459,1.17524047358087,
10.2916666666667));
#421980=CARTESIAN_POINT('Ctrl Pts',(-1.01778810567669,0.587620236790438,
10.3333333333333));
#421981=CARTESIAN_POINT('Ctrl Pts',(-1.35705080756892,2.62370823081419E-15,
10.375));
#421982=CARTESIAN_POINT('Ctrl Pts',(-1.01778810567669,-0.587620236790433,
10.4166666666667));
#421983=CARTESIAN_POINT('Ctrl Pts',(-0.67852540378446,-1.17524047358087,
10.4583333333333));
#421984=CARTESIAN_POINT('Ctrl Pts',(-1.43925448419923E-16,-1.17524047358087,
10.5));
#421985=CARTESIAN_POINT('Ctrl Pts',(0.678525403784459,-1.17524047358087,
10.5416666666667));
#421986=CARTESIAN_POINT('Ctrl Pts',(1.01778810567669,-0.587620236790434,
10.5833333333333));
#421987=CARTESIAN_POINT('Ctrl Pts',(1.35705080756892,2.29132664526027E-15,
10.625));
#421988=CARTESIAN_POINT('Ctrl Pts',(1.01778810567669,0.587620236790438,
10.6666666666667));
#421989=CARTESIAN_POINT('Ctrl Pts',(0.67852540378446,1.17524047358087,10.7083333333333));
#421990=CARTESIAN_POINT('Ctrl Pts',(0.,1.17524047358087,10.75));
#421991=CARTESIAN_POINT('Ctrl Pts',(-0.678525403784459,1.17524047358087,
10.7916666666667));
#421992=CARTESIAN_POINT('Ctrl Pts',(-1.01778810567669,0.587620236790438,
10.8333333333333));
#421993=CARTESIAN_POINT('Ctrl Pts',(-1.35705080756892,2.62370823081419E-15,
10.875));
#421994=CARTESIAN_POINT('Ctrl Pts',(-1.01778810567669,-0.587620236790433,
10.9166666666667));
#421995=CARTESIAN_POINT('Ctrl Pts',(-0.67852540378446,-1.17524047358087,
10.9583333333333));
#421996=CARTESIAN_POINT('Ctrl Pts',(-1.43925448419923E-16,-1.17524047358087,
11.));
#421997=CARTESIAN_POINT('Ctrl Pts',(0.678525403784459,-1.17524047358087,
11.0416666666667));
#421998=CARTESIAN_POINT('Ctrl Pts',(1.01778810567669,-0.587620236790434,
11.0833333333333));
#421999=CARTESIAN_POINT('Ctrl Pts',(1.35705080756892,2.29132664526027E-15,
11.125));
#422000=CARTESIAN_POINT('Ctrl Pts',(1.01778810567669,0.587620236790438,
11.1666666666667));
#422001=CARTESIAN_POINT('Ctrl Pts',(0.67852540378446,1.17524047358087,11.2083333333333));
#422002=CARTESIAN_POINT('Ctrl Pts',(0.,1.17524047358087,11.25));
#422003=CARTESIAN_POINT('Ctrl Pts',(0.,1.52706329386832,-14.453125));
#422004=CARTESIAN_POINT('Ctrl Pts',(-0.881650403784468,1.52706329386832,
-14.4114583333333));
#422005=CARTESIAN_POINT('Ctrl Pts',(-1.3224756056767,0.76353164693416,-14.3697916666667));
#422006=CARTESIAN_POINT('Ctrl Pts',(-1.76330080756894,2.64858386892187E-15,
-14.328125));
#422007=CARTESIAN_POINT('Ctrl Pts',(-1.3224756056767,-0.763531646934155,
-14.2864583333333));
#422008=CARTESIAN_POINT('Ctrl Pts',(-0.881650403784469,-1.52706329386831,
-14.2447916666667));
#422009=CARTESIAN_POINT('Ctrl Pts',(-1.87011317493125E-16,-1.52706329386831,
-14.203125));
#422010=CARTESIAN_POINT('Ctrl Pts',(0.881650403784467,-1.52706329386831,
-14.1614583333333));
#422011=CARTESIAN_POINT('Ctrl Pts',(1.3224756056767,-0.763531646934156,
-14.1197916666667));
#422012=CARTESIAN_POINT('Ctrl Pts',(1.76330080756894,2.21669973093722E-15,
-14.078125));
#422013=CARTESIAN_POINT('Ctrl Pts',(1.3224756056767,0.763531646934159,-14.0364583333333));
#422014=CARTESIAN_POINT('Ctrl Pts',(0.881650403784469,1.52706329386832,
-13.9947916666667));
#422015=CARTESIAN_POINT('Ctrl Pts',(0.,1.52706329386832,-13.953125));
#422016=CARTESIAN_POINT('Ctrl Pts',(-0.881650403784468,1.52706329386832,
-13.9114583333333));
#422017=CARTESIAN_POINT('Ctrl Pts',(-1.3224756056767,0.76353164693416,-13.8697916666667));
#422018=CARTESIAN_POINT('Ctrl Pts',(-1.76330080756894,2.64858386892187E-15,
-13.828125));
#422019=CARTESIAN_POINT('Ctrl Pts',(-1.3224756056767,-0.763531646934155,
-13.7864583333333));
#422020=CARTESIAN_POINT('Ctrl Pts',(-0.881650403784469,-1.52706329386831,
-13.7447916666667));
#422021=CARTESIAN_POINT('Ctrl Pts',(-1.87011317493125E-16,-1.52706329386831,
-13.703125));
#422022=CARTESIAN_POINT('Ctrl Pts',(0.881650403784467,-1.52706329386831,
-13.6614583333333));
#422023=CARTESIAN_POINT('Ctrl Pts',(1.3224756056767,-0.763531646934156,
-13.6197916666667));
#422024=CARTESIAN_POINT('Ctrl Pts',(1.76330080756894,2.21669973093722E-15,
-13.578125));
#422025=CARTESIAN_POINT('Ctrl Pts',(1.3224756056767,0.763531646934159,-13.5364583333333));
#422026=CARTESIAN_POINT('Ctrl Pts',(0.881650403784469,1.52706329386832,
-13.4947916666667));
#422027=CARTESIAN_POINT('Ctrl Pts',(0.,1.52706329386832,-13.453125));
#422028=CARTESIAN_POINT('Ctrl Pts',(-0.881650403784468,1.52706329386832,
-13.4114583333333));
#422029=CARTESIAN_POINT('Ctrl Pts',(-1.3224756056767,0.76353164693416,-13.3697916666667));
#422030=CARTESIAN_POINT('Ctrl Pts',(-1.76330080756894,2.64858386892187E-15,
-13.328125));
#422031=CARTESIAN_POINT('Ctrl Pts',(-1.3224756056767,-0.763531646934155,
-13.2864583333333));
#422032=CARTESIAN_POINT('Ctrl Pts',(-0.881650403784469,-1.52706329386831,
-13.2447916666667));
#422033=CARTESIAN_POINT('Ctrl Pts',(-1.87011317493125E-16,-1.52706329386831,
-13.203125));
#422034=CARTESIAN_POINT('Ctrl Pts',(0.881650403784467,-1.52706329386831,
-13.1614583333333));
#422035=CARTESIAN_POINT('Ctrl Pts',(1.3224756056767,-0.763531646934156,
-13.1197916666667));
#422036=CARTESIAN_POINT('Ctrl Pts',(1.76330080756894,2.21669973093722E-15,
-13.078125));
#422037=CARTESIAN_POINT('Ctrl Pts',(1.3224756056767,0.763531646934159,-13.0364583333333));
#422038=CARTESIAN_POINT('Ctrl Pts',(0.881650403784469,1.52706329386832,
-12.9947916666667));
#422039=CARTESIAN_POINT('Ctrl Pts',(0.,1.52706329386832,-12.953125));
#422040=CARTESIAN_POINT('Ctrl Pts',(-0.881650403784468,1.52706329386832,
-12.9114583333333));
#422041=CARTESIAN_POINT('Ctrl Pts',(-1.3224756056767,0.76353164693416,-12.8697916666667));
#422042=CARTESIAN_POINT('Ctrl Pts',(-1.76330080756894,2.64858386892187E-15,
-12.828125));
#422043=CARTESIAN_POINT('Ctrl Pts',(-1.3224756056767,-0.763531646934155,
-12.7864583333333));
#422044=CARTESIAN_POINT('Ctrl Pts',(-0.881650403784469,-1.52706329386831,
-12.7447916666667));
#422045=CARTESIAN_POINT('Ctrl Pts',(-1.87011317493125E-16,-1.52706329386831,
-12.703125));
#422046=CARTESIAN_POINT('Ctrl Pts',(0.881650403784467,-1.52706329386831,
-12.6614583333333));
#422047=CARTESIAN_POINT('Ctrl Pts',(1.3224756056767,-0.763531646934156,
-12.6197916666667));
#422048=CARTESIAN_POINT('Ctrl Pts',(1.76330080756894,2.21669973093722E-15,
-12.578125));
#422049=CARTESIAN_POINT('Ctrl Pts',(1.3224756056767,0.763531646934159,-12.5364583333333));
#422050=CARTESIAN_POINT('Ctrl Pts',(0.881650403784469,1.52706329386832,
-12.4947916666667));
#422051=CARTESIAN_POINT('Ctrl Pts',(0.,1.52706329386832,-12.453125));
#422052=CARTESIAN_POINT('Ctrl Pts',(-0.881650403784468,1.52706329386832,
-12.4114583333333));
#422053=CARTESIAN_POINT('Ctrl Pts',(-1.3224756056767,0.76353164693416,-12.3697916666667));
#422054=CARTESIAN_POINT('Ctrl Pts',(-1.76330080756894,2.64858386892187E-15,
-12.328125));
#422055=CARTESIAN_POINT('Ctrl Pts',(-1.3224756056767,-0.763531646934155,
-12.2864583333333));
#422056=CARTESIAN_POINT('Ctrl Pts',(-0.881650403784469,-1.52706329386831,
-12.2447916666667));
#422057=CARTESIAN_POINT('Ctrl Pts',(-1.87011317493125E-16,-1.52706329386831,
-12.203125));
#422058=CARTESIAN_POINT('Ctrl Pts',(0.881650403784467,-1.52706329386831,
-12.1614583333333));
#422059=CARTESIAN_POINT('Ctrl Pts',(1.3224756056767,-0.763531646934156,
-12.1197916666667));
#422060=CARTESIAN_POINT('Ctrl Pts',(1.76330080756894,2.21669973093722E-15,
-12.078125));
#422061=CARTESIAN_POINT('Ctrl Pts',(1.3224756056767,0.763531646934159,-12.0364583333333));
#422062=CARTESIAN_POINT('Ctrl Pts',(0.881650403784469,1.52706329386832,
-11.9947916666667));
#422063=CARTESIAN_POINT('Ctrl Pts',(0.,1.52706329386832,-11.953125));
#422064=CARTESIAN_POINT('Ctrl Pts',(-0.881650403784468,1.52706329386832,
-11.9114583333333));
#422065=CARTESIAN_POINT('Ctrl Pts',(-1.3224756056767,0.76353164693416,-11.8697916666667));
#422066=CARTESIAN_POINT('Ctrl Pts',(-1.76330080756894,2.64858386892187E-15,
-11.828125));
#422067=CARTESIAN_POINT('Ctrl Pts',(-1.3224756056767,-0.763531646934155,
-11.7864583333333));
#422068=CARTESIAN_POINT('Ctrl Pts',(-0.881650403784469,-1.52706329386831,
-11.7447916666667));
#422069=CARTESIAN_POINT('Ctrl Pts',(-1.87011317493125E-16,-1.52706329386831,
-11.703125));
#422070=CARTESIAN_POINT('Ctrl Pts',(0.881650403784467,-1.52706329386831,
-11.6614583333333));
#422071=CARTESIAN_POINT('Ctrl Pts',(1.3224756056767,-0.763531646934156,
-11.6197916666667));
#422072=CARTESIAN_POINT('Ctrl Pts',(1.76330080756894,2.21669973093722E-15,
-11.578125));
#422073=CARTESIAN_POINT('Ctrl Pts',(1.3224756056767,0.763531646934159,-11.5364583333333));
#422074=CARTESIAN_POINT('Ctrl Pts',(0.881650403784469,1.52706329386832,
-11.4947916666667));
#422075=CARTESIAN_POINT('Ctrl Pts',(0.,1.52706329386832,-11.453125));
#422076=CARTESIAN_POINT('Ctrl Pts',(-0.881650403784468,1.52706329386832,
-11.4114583333333));
#422077=CARTESIAN_POINT('Ctrl Pts',(-1.3224756056767,0.76353164693416,-11.3697916666667));
#422078=CARTESIAN_POINT('Ctrl Pts',(-1.76330080756894,2.64858386892187E-15,
-11.328125));
#422079=CARTESIAN_POINT('Ctrl Pts',(-1.3224756056767,-0.763531646934155,
-11.2864583333333));
#422080=CARTESIAN_POINT('Ctrl Pts',(-0.881650403784469,-1.52706329386831,
-11.2447916666667));
#422081=CARTESIAN_POINT('Ctrl Pts',(-1.87011317493125E-16,-1.52706329386831,
-11.203125));
#422082=CARTESIAN_POINT('Ctrl Pts',(0.881650403784467,-1.52706329386831,
-11.1614583333333));
#422083=CARTESIAN_POINT('Ctrl Pts',(1.3224756056767,-0.763531646934156,
-11.1197916666667));
#422084=CARTESIAN_POINT('Ctrl Pts',(1.76330080756894,2.21669973093722E-15,
-11.078125));
#422085=CARTESIAN_POINT('Ctrl Pts',(1.3224756056767,0.763531646934159,-11.0364583333333));
#422086=CARTESIAN_POINT('Ctrl Pts',(0.881650403784469,1.52706329386832,
-10.9947916666667));
#422087=CARTESIAN_POINT('Ctrl Pts',(0.,1.52706329386832,-10.953125));
#422088=CARTESIAN_POINT('Ctrl Pts',(-0.881650403784468,1.52706329386832,
-10.9114583333333));
#422089=CARTESIAN_POINT('Ctrl Pts',(-1.3224756056767,0.76353164693416,-10.8697916666667));
#422090=CARTESIAN_POINT('Ctrl Pts',(-1.76330080756894,2.64858386892187E-15,
-10.828125));
#422091=CARTESIAN_POINT('Ctrl Pts',(-1.3224756056767,-0.763531646934155,
-10.7864583333333));
#422092=CARTESIAN_POINT('Ctrl Pts',(-0.881650403784469,-1.52706329386831,
-10.7447916666667));
#422093=CARTESIAN_POINT('Ctrl Pts',(-1.87011317493125E-16,-1.52706329386831,
-10.703125));
#422094=CARTESIAN_POINT('Ctrl Pts',(0.881650403784467,-1.52706329386831,
-10.6614583333333));
#422095=CARTESIAN_POINT('Ctrl Pts',(1.3224756056767,-0.763531646934156,
-10.6197916666667));
#422096=CARTESIAN_POINT('Ctrl Pts',(1.76330080756894,2.21669973093722E-15,
-10.578125));
#422097=CARTESIAN_POINT('Ctrl Pts',(1.3224756056767,0.763531646934159,-10.5364583333333));
#422098=CARTESIAN_POINT('Ctrl Pts',(0.881650403784469,1.52706329386832,
-10.4947916666667));
#422099=CARTESIAN_POINT('Ctrl Pts',(0.,1.52706329386832,-10.453125));
#422100=CARTESIAN_POINT('Ctrl Pts',(-0.881650403784468,1.52706329386832,
-10.4114583333333));
#422101=CARTESIAN_POINT('Ctrl Pts',(-1.3224756056767,0.76353164693416,-10.3697916666667));
#422102=CARTESIAN_POINT('Ctrl Pts',(-1.76330080756894,2.64858386892187E-15,
-10.328125));
#422103=CARTESIAN_POINT('Ctrl Pts',(-1.3224756056767,-0.763531646934155,
-10.2864583333333));
#422104=CARTESIAN_POINT('Ctrl Pts',(-0.881650403784469,-1.52706329386831,
-10.2447916666667));
#422105=CARTESIAN_POINT('Ctrl Pts',(-1.87011317493125E-16,-1.52706329386831,
-10.203125));
#422106=CARTESIAN_POINT('Ctrl Pts',(0.881650403784467,-1.52706329386831,
-10.1614583333333));
#422107=CARTESIAN_POINT('Ctrl Pts',(1.3224756056767,-0.763531646934156,
-10.1197916666667));
#422108=CARTESIAN_POINT('Ctrl Pts',(1.76330080756894,2.21669973093722E-15,
-10.078125));
#422109=CARTESIAN_POINT('Ctrl Pts',(1.3224756056767,0.763531646934159,-10.0364583333333));
#422110=CARTESIAN_POINT('Ctrl Pts',(0.881650403784469,1.52706329386832,
-9.99479166666667));
#422111=CARTESIAN_POINT('Ctrl Pts',(0.,1.52706329386832,-9.953125));
#422112=CARTESIAN_POINT('Ctrl Pts',(-0.881650403784468,1.52706329386832,
-9.91145833333333));
#422113=CARTESIAN_POINT('Ctrl Pts',(-1.3224756056767,0.76353164693416,-9.86979166666667));
#422114=CARTESIAN_POINT('Ctrl Pts',(-1.76330080756894,2.64858386892187E-15,
-9.828125));
#422115=CARTESIAN_POINT('Ctrl Pts',(-1.3224756056767,-0.763531646934155,
-9.78645833333333));
#422116=CARTESIAN_POINT('Ctrl Pts',(-0.881650403784469,-1.52706329386831,
-9.74479166666667));
#422117=CARTESIAN_POINT('Ctrl Pts',(-1.87011317493125E-16,-1.52706329386831,
-9.703125));
#422118=CARTESIAN_POINT('Ctrl Pts',(0.881650403784467,-1.52706329386831,
-9.66145833333333));
#422119=CARTESIAN_POINT('Ctrl Pts',(1.3224756056767,-0.763531646934156,
-9.61979166666667));
#422120=CARTESIAN_POINT('Ctrl Pts',(1.76330080756894,2.21669973093722E-15,
-9.578125));
#422121=CARTESIAN_POINT('Ctrl Pts',(1.3224756056767,0.763531646934159,-9.53645833333333));
#422122=CARTESIAN_POINT('Ctrl Pts',(0.881650403784469,1.52706329386832,
-9.49479166666666));
#422123=CARTESIAN_POINT('Ctrl Pts',(0.,1.52706329386832,-9.453125));
#422124=CARTESIAN_POINT('Ctrl Pts',(-0.881650403784468,1.52706329386832,
-9.41145833333333));
#422125=CARTESIAN_POINT('Ctrl Pts',(-1.3224756056767,0.76353164693416,-9.36979166666666));
#422126=CARTESIAN_POINT('Ctrl Pts',(-1.76330080756894,2.64858386892187E-15,
-9.328125));
#422127=CARTESIAN_POINT('Ctrl Pts',(-1.3224756056767,-0.763531646934155,
-9.28645833333333));
#422128=CARTESIAN_POINT('Ctrl Pts',(-0.881650403784469,-1.52706329386831,
-9.24479166666667));
#422129=CARTESIAN_POINT('Ctrl Pts',(-1.87011317493125E-16,-1.52706329386831,
-9.203125));
#422130=CARTESIAN_POINT('Ctrl Pts',(0.881650403784467,-1.52706329386831,
-9.16145833333333));
#422131=CARTESIAN_POINT('Ctrl Pts',(1.3224756056767,-0.763531646934156,
-9.11979166666666));
#422132=CARTESIAN_POINT('Ctrl Pts',(1.76330080756894,2.21669973093722E-15,
-9.078125));
#422133=CARTESIAN_POINT('Ctrl Pts',(1.3224756056767,0.763531646934159,-9.03645833333333));
#422134=CARTESIAN_POINT('Ctrl Pts',(0.881650403784469,1.52706329386832,
-8.99479166666666));
#422135=CARTESIAN_POINT('Ctrl Pts',(0.,1.52706329386832,-8.953125));
#422136=CARTESIAN_POINT('Ctrl Pts',(-0.881650403784468,1.52706329386832,
-8.91145833333333));
#422137=CARTESIAN_POINT('Ctrl Pts',(-1.3224756056767,0.76353164693416,-8.86979166666666));
#422138=CARTESIAN_POINT('Ctrl Pts',(-1.76330080756894,2.64858386892187E-15,
-8.828125));
#422139=CARTESIAN_POINT('Ctrl Pts',(-1.3224756056767,-0.763531646934155,
-8.78645833333333));
#422140=CARTESIAN_POINT('Ctrl Pts',(-0.881650403784469,-1.52706329386831,
-8.74479166666666));
#422141=CARTESIAN_POINT('Ctrl Pts',(-1.87011317493125E-16,-1.52706329386831,
-8.703125));
#422142=CARTESIAN_POINT('Ctrl Pts',(0.881650403784467,-1.52706329386831,
-8.66145833333333));
#422143=CARTESIAN_POINT('Ctrl Pts',(1.3224756056767,-0.763531646934156,
-8.61979166666667));
#422144=CARTESIAN_POINT('Ctrl Pts',(1.76330080756894,2.21669973093722E-15,
-8.578125));
#422145=CARTESIAN_POINT('Ctrl Pts',(1.3224756056767,0.763531646934159,-8.53645833333333));
#422146=CARTESIAN_POINT('Ctrl Pts',(0.881650403784469,1.52706329386832,
-8.49479166666667));
#422147=CARTESIAN_POINT('Ctrl Pts',(0.,1.52706329386832,-8.453125));
#422148=CARTESIAN_POINT('Ctrl Pts',(-0.881650403784468,1.52706329386832,
-8.41145833333333));
#422149=CARTESIAN_POINT('Ctrl Pts',(-1.3224756056767,0.76353164693416,-8.36979166666667));
#422150=CARTESIAN_POINT('Ctrl Pts',(-1.76330080756894,2.64858386892187E-15,
-8.328125));
#422151=CARTESIAN_POINT('Ctrl Pts',(-1.3224756056767,-0.763531646934155,
-8.28645833333333));
#422152=CARTESIAN_POINT('Ctrl Pts',(-0.881650403784469,-1.52706329386831,
-8.24479166666667));
#422153=CARTESIAN_POINT('Ctrl Pts',(-1.87011317493125E-16,-1.52706329386831,
-8.203125));
#422154=CARTESIAN_POINT('Ctrl Pts',(0.881650403784467,-1.52706329386831,
-8.16145833333333));
#422155=CARTESIAN_POINT('Ctrl Pts',(1.3224756056767,-0.763531646934156,
-8.11979166666667));
#422156=CARTESIAN_POINT('Ctrl Pts',(1.76330080756894,2.21669973093722E-15,
-8.078125));
#422157=CARTESIAN_POINT('Ctrl Pts',(1.3224756056767,0.763531646934159,-8.03645833333333));
#422158=CARTESIAN_POINT('Ctrl Pts',(0.881650403784469,1.52706329386832,
-7.99479166666667));
#422159=CARTESIAN_POINT('Ctrl Pts',(0.,1.52706329386832,-7.953125));
#422160=CARTESIAN_POINT('Ctrl Pts',(-0.881650403784468,1.52706329386832,
-7.91145833333333));
#422161=CARTESIAN_POINT('Ctrl Pts',(-1.3224756056767,0.76353164693416,-7.86979166666667));
#422162=CARTESIAN_POINT('Ctrl Pts',(-1.76330080756894,2.64858386892187E-15,
-7.828125));
#422163=CARTESIAN_POINT('Ctrl Pts',(-1.3224756056767,-0.763531646934155,
-7.78645833333333));
#422164=CARTESIAN_POINT('Ctrl Pts',(-0.881650403784469,-1.52706329386831,
-7.74479166666667));
#422165=CARTESIAN_POINT('Ctrl Pts',(-1.87011317493125E-16,-1.52706329386831,
-7.703125));
#422166=CARTESIAN_POINT('Ctrl Pts',(0.881650403784467,-1.52706329386831,
-7.66145833333333));
#422167=CARTESIAN_POINT('Ctrl Pts',(1.3224756056767,-0.763531646934156,
-7.61979166666667));
#422168=CARTESIAN_POINT('Ctrl Pts',(1.76330080756894,2.21669973093722E-15,
-7.578125));
#422169=CARTESIAN_POINT('Ctrl Pts',(1.3224756056767,0.763531646934159,-7.53645833333333));
#422170=CARTESIAN_POINT('Ctrl Pts',(0.881650403784469,1.52706329386832,
-7.49479166666667));
#422171=CARTESIAN_POINT('Ctrl Pts',(0.,1.52706329386832,-7.453125));
#422172=CARTESIAN_POINT('Ctrl Pts',(-0.881650403784468,1.52706329386832,
-7.41145833333333));
#422173=CARTESIAN_POINT('Ctrl Pts',(-1.3224756056767,0.76353164693416,-7.36979166666667));
#422174=CARTESIAN_POINT('Ctrl Pts',(-1.76330080756894,2.64858386892187E-15,
-7.328125));
#422175=CARTESIAN_POINT('Ctrl Pts',(-1.3224756056767,-0.763531646934155,
-7.28645833333333));
#422176=CARTESIAN_POINT('Ctrl Pts',(-0.881650403784469,-1.52706329386831,
-7.24479166666667));
#422177=CARTESIAN_POINT('Ctrl Pts',(-1.87011317493125E-16,-1.52706329386831,
-7.203125));
#422178=CARTESIAN_POINT('Ctrl Pts',(0.881650403784467,-1.52706329386831,
-7.16145833333333));
#422179=CARTESIAN_POINT('Ctrl Pts',(1.3224756056767,-0.763531646934156,
-7.11979166666667));
#422180=CARTESIAN_POINT('Ctrl Pts',(1.76330080756894,2.21669973093722E-15,
-7.078125));
#422181=CARTESIAN_POINT('Ctrl Pts',(1.3224756056767,0.763531646934159,-7.03645833333333));
#422182=CARTESIAN_POINT('Ctrl Pts',(0.881650403784469,1.52706329386832,
-6.99479166666667));
#422183=CARTESIAN_POINT('Ctrl Pts',(0.,1.52706329386832,-6.953125));
#422184=CARTESIAN_POINT('Ctrl Pts',(-0.881650403784468,1.52706329386832,
-6.91145833333333));
#422185=CARTESIAN_POINT('Ctrl Pts',(-1.3224756056767,0.76353164693416,-6.86979166666667));
#422186=CARTESIAN_POINT('Ctrl Pts',(-1.76330080756894,2.64858386892187E-15,
-6.828125));
#422187=CARTESIAN_POINT('Ctrl Pts',(-1.3224756056767,-0.763531646934155,
-6.78645833333333));
#422188=CARTESIAN_POINT('Ctrl Pts',(-0.881650403784469,-1.52706329386831,
-6.74479166666667));
#422189=CARTESIAN_POINT('Ctrl Pts',(-1.87011317493125E-16,-1.52706329386831,
-6.703125));
#422190=CARTESIAN_POINT('Ctrl Pts',(0.881650403784467,-1.52706329386831,
-6.66145833333333));
#422191=CARTESIAN_POINT('Ctrl Pts',(1.3224756056767,-0.763531646934156,
-6.61979166666667));
#422192=CARTESIAN_POINT('Ctrl Pts',(1.76330080756894,2.21669973093722E-15,
-6.578125));
#422193=CARTESIAN_POINT('Ctrl Pts',(1.3224756056767,0.763531646934159,-6.53645833333333));
#422194=CARTESIAN_POINT('Ctrl Pts',(0.881650403784469,1.52706329386832,
-6.49479166666667));
#422195=CARTESIAN_POINT('Ctrl Pts',(0.,1.52706329386832,-6.453125));
#422196=CARTESIAN_POINT('Ctrl Pts',(-0.881650403784468,1.52706329386832,
-6.41145833333333));
#422197=CARTESIAN_POINT('Ctrl Pts',(-1.3224756056767,0.76353164693416,-6.36979166666667));
#422198=CARTESIAN_POINT('Ctrl Pts',(-1.76330080756894,2.64858386892187E-15,
-6.328125));
#422199=CARTESIAN_POINT('Ctrl Pts',(-1.3224756056767,-0.763531646934155,
-6.28645833333333));
#422200=CARTESIAN_POINT('Ctrl Pts',(-0.881650403784469,-1.52706329386831,
-6.24479166666667));
#422201=CARTESIAN_POINT('Ctrl Pts',(-1.87011317493125E-16,-1.52706329386831,
-6.203125));
#422202=CARTESIAN_POINT('Ctrl Pts',(0.881650403784467,-1.52706329386831,
-6.16145833333333));
#422203=CARTESIAN_POINT('Ctrl Pts',(1.3224756056767,-0.763531646934156,
-6.11979166666667));
#422204=CARTESIAN_POINT('Ctrl Pts',(1.76330080756894,2.21669973093722E-15,
-6.078125));
#422205=CARTESIAN_POINT('Ctrl Pts',(1.3224756056767,0.763531646934159,-6.03645833333333));
#422206=CARTESIAN_POINT('Ctrl Pts',(0.881650403784469,1.52706329386832,
-5.99479166666667));
#422207=CARTESIAN_POINT('Ctrl Pts',(0.,1.52706329386832,-5.953125));
#422208=CARTESIAN_POINT('Ctrl Pts',(-0.881650403784468,1.52706329386832,
-5.91145833333333));
#422209=CARTESIAN_POINT('Ctrl Pts',(-1.3224756056767,0.76353164693416,-5.86979166666667));
#422210=CARTESIAN_POINT('Ctrl Pts',(-1.76330080756894,2.64858386892187E-15,
-5.828125));
#422211=CARTESIAN_POINT('Ctrl Pts',(-1.3224756056767,-0.763531646934155,
-5.78645833333333));
#422212=CARTESIAN_POINT('Ctrl Pts',(-0.881650403784469,-1.52706329386831,
-5.74479166666667));
#422213=CARTESIAN_POINT('Ctrl Pts',(-1.87011317493125E-16,-1.52706329386831,
-5.703125));
#422214=CARTESIAN_POINT('Ctrl Pts',(0.881650403784467,-1.52706329386831,
-5.66145833333333));
#422215=CARTESIAN_POINT('Ctrl Pts',(1.3224756056767,-0.763531646934156,
-5.61979166666667));
#422216=CARTESIAN_POINT('Ctrl Pts',(1.76330080756894,2.21669973093722E-15,
-5.578125));
#422217=CARTESIAN_POINT('Ctrl Pts',(1.3224756056767,0.763531646934159,-5.53645833333333));
#422218=CARTESIAN_POINT('Ctrl Pts',(0.881650403784469,1.52706329386832,
-5.49479166666667));
#422219=CARTESIAN_POINT('Ctrl Pts',(0.,1.52706329386832,-5.453125));
#422220=CARTESIAN_POINT('Ctrl Pts',(-0.881650403784468,1.52706329386832,
-5.41145833333333));
#422221=CARTESIAN_POINT('Ctrl Pts',(-1.3224756056767,0.76353164693416,-5.36979166666667));
#422222=CARTESIAN_POINT('Ctrl Pts',(-1.76330080756894,2.64858386892187E-15,
-5.328125));
#422223=CARTESIAN_POINT('Ctrl Pts',(-1.3224756056767,-0.763531646934155,
-5.28645833333333));
#422224=CARTESIAN_POINT('Ctrl Pts',(-0.881650403784469,-1.52706329386831,
-5.24479166666667));
#422225=CARTESIAN_POINT('Ctrl Pts',(-1.87011317493125E-16,-1.52706329386831,
-5.203125));
#422226=CARTESIAN_POINT('Ctrl Pts',(0.881650403784467,-1.52706329386831,
-5.16145833333333));
#422227=CARTESIAN_POINT('Ctrl Pts',(1.3224756056767,-0.763531646934156,
-5.11979166666667));
#422228=CARTESIAN_POINT('Ctrl Pts',(1.76330080756894,2.21669973093722E-15,
-5.078125));
#422229=CARTESIAN_POINT('Ctrl Pts',(1.3224756056767,0.763531646934159,-5.03645833333333));
#422230=CARTESIAN_POINT('Ctrl Pts',(0.881650403784469,1.52706329386832,
-4.99479166666667));
#422231=CARTESIAN_POINT('Ctrl Pts',(0.,1.52706329386832,-4.953125));
#422232=CARTESIAN_POINT('Ctrl Pts',(-0.881650403784468,1.52706329386832,
-4.91145833333333));
#422233=CARTESIAN_POINT('Ctrl Pts',(-1.3224756056767,0.76353164693416,-4.86979166666667));
#422234=CARTESIAN_POINT('Ctrl Pts',(-1.76330080756894,2.64858386892187E-15,
-4.828125));
#422235=CARTESIAN_POINT('Ctrl Pts',(-1.3224756056767,-0.763531646934155,
-4.78645833333333));
#422236=CARTESIAN_POINT('Ctrl Pts',(-0.881650403784469,-1.52706329386831,
-4.74479166666667));
#422237=CARTESIAN_POINT('Ctrl Pts',(-1.87011317493125E-16,-1.52706329386831,
-4.703125));
#422238=CARTESIAN_POINT('Ctrl Pts',(0.881650403784467,-1.52706329386831,
-4.66145833333333));
#422239=CARTESIAN_POINT('Ctrl Pts',(1.3224756056767,-0.763531646934156,
-4.61979166666667));
#422240=CARTESIAN_POINT('Ctrl Pts',(1.76330080756894,2.21669973093722E-15,
-4.578125));
#422241=CARTESIAN_POINT('Ctrl Pts',(1.3224756056767,0.763531646934159,-4.53645833333333));
#422242=CARTESIAN_POINT('Ctrl Pts',(0.881650403784469,1.52706329386832,
-4.49479166666667));
#422243=CARTESIAN_POINT('Ctrl Pts',(0.,1.52706329386832,-4.453125));
#422244=CARTESIAN_POINT('Ctrl Pts',(-0.881650403784468,1.52706329386832,
-4.41145833333333));
#422245=CARTESIAN_POINT('Ctrl Pts',(-1.3224756056767,0.76353164693416,-4.36979166666667));
#422246=CARTESIAN_POINT('Ctrl Pts',(-1.76330080756894,2.64858386892187E-15,
-4.328125));
#422247=CARTESIAN_POINT('Ctrl Pts',(-1.3224756056767,-0.763531646934155,
-4.28645833333333));
#422248=CARTESIAN_POINT('Ctrl Pts',(-0.881650403784469,-1.52706329386831,
-4.24479166666667));
#422249=CARTESIAN_POINT('Ctrl Pts',(-1.87011317493125E-16,-1.52706329386831,
-4.203125));
#422250=CARTESIAN_POINT('Ctrl Pts',(0.881650403784467,-1.52706329386831,
-4.16145833333333));
#422251=CARTESIAN_POINT('Ctrl Pts',(1.3224756056767,-0.763531646934156,
-4.11979166666667));
#422252=CARTESIAN_POINT('Ctrl Pts',(1.76330080756894,2.21669973093722E-15,
-4.078125));
#422253=CARTESIAN_POINT('Ctrl Pts',(1.3224756056767,0.763531646934159,-4.03645833333333));
#422254=CARTESIAN_POINT('Ctrl Pts',(0.881650403784469,1.52706329386832,
-3.99479166666667));
#422255=CARTESIAN_POINT('Ctrl Pts',(0.,1.52706329386832,-3.953125));
#422256=CARTESIAN_POINT('Ctrl Pts',(-0.881650403784468,1.52706329386832,
-3.91145833333333));
#422257=CARTESIAN_POINT('Ctrl Pts',(-1.3224756056767,0.76353164693416,-3.86979166666667));
#422258=CARTESIAN_POINT('Ctrl Pts',(-1.76330080756894,2.64858386892187E-15,
-3.828125));
#422259=CARTESIAN_POINT('Ctrl Pts',(-1.3224756056767,-0.763531646934155,
-3.78645833333333));
#422260=CARTESIAN_POINT('Ctrl Pts',(-0.881650403784469,-1.52706329386831,
-3.74479166666667));
#422261=CARTESIAN_POINT('Ctrl Pts',(-1.87011317493125E-16,-1.52706329386831,
-3.703125));
#422262=CARTESIAN_POINT('Ctrl Pts',(0.881650403784467,-1.52706329386831,
-3.66145833333333));
#422263=CARTESIAN_POINT('Ctrl Pts',(1.3224756056767,-0.763531646934156,
-3.61979166666667));
#422264=CARTESIAN_POINT('Ctrl Pts',(1.76330080756894,2.21669973093722E-15,
-3.578125));
#422265=CARTESIAN_POINT('Ctrl Pts',(1.3224756056767,0.763531646934159,-3.53645833333333));
#422266=CARTESIAN_POINT('Ctrl Pts',(0.881650403784469,1.52706329386832,
-3.49479166666667));
#422267=CARTESIAN_POINT('Ctrl Pts',(0.,1.52706329386832,-3.453125));
#422268=CARTESIAN_POINT('Ctrl Pts',(-0.881650403784468,1.52706329386832,
-3.41145833333333));
#422269=CARTESIAN_POINT('Ctrl Pts',(-1.3224756056767,0.76353164693416,-3.36979166666667));
#422270=CARTESIAN_POINT('Ctrl Pts',(-1.76330080756894,2.64858386892187E-15,
-3.328125));
#422271=CARTESIAN_POINT('Ctrl Pts',(-1.3224756056767,-0.763531646934155,
-3.28645833333333));
#422272=CARTESIAN_POINT('Ctrl Pts',(-0.881650403784469,-1.52706329386831,
-3.24479166666667));
#422273=CARTESIAN_POINT('Ctrl Pts',(-1.87011317493125E-16,-1.52706329386831,
-3.203125));
#422274=CARTESIAN_POINT('Ctrl Pts',(0.881650403784467,-1.52706329386831,
-3.16145833333333));
#422275=CARTESIAN_POINT('Ctrl Pts',(1.3224756056767,-0.763531646934156,
-3.11979166666667));
#422276=CARTESIAN_POINT('Ctrl Pts',(1.76330080756894,2.21669973093722E-15,
-3.078125));
#422277=CARTESIAN_POINT('Ctrl Pts',(1.3224756056767,0.763531646934159,-3.03645833333333));
#422278=CARTESIAN_POINT('Ctrl Pts',(0.881650403784469,1.52706329386832,
-2.99479166666667));
#422279=CARTESIAN_POINT('Ctrl Pts',(0.,1.52706329386832,-2.953125));
#422280=CARTESIAN_POINT('Ctrl Pts',(-0.881650403784468,1.52706329386832,
-2.91145833333333));
#422281=CARTESIAN_POINT('Ctrl Pts',(-1.3224756056767,0.76353164693416,-2.86979166666667));
#422282=CARTESIAN_POINT('Ctrl Pts',(-1.76330080756894,2.64858386892187E-15,
-2.828125));
#422283=CARTESIAN_POINT('Ctrl Pts',(-1.3224756056767,-0.763531646934155,
-2.78645833333333));
#422284=CARTESIAN_POINT('Ctrl Pts',(-0.881650403784469,-1.52706329386831,
-2.74479166666667));
#422285=CARTESIAN_POINT('Ctrl Pts',(-1.87011317493125E-16,-1.52706329386831,
-2.703125));
#422286=CARTESIAN_POINT('Ctrl Pts',(0.881650403784467,-1.52706329386831,
-2.66145833333333));
#422287=CARTESIAN_POINT('Ctrl Pts',(1.3224756056767,-0.763531646934156,
-2.61979166666667));
#422288=CARTESIAN_POINT('Ctrl Pts',(1.76330080756894,2.21669973093722E-15,
-2.578125));
#422289=CARTESIAN_POINT('Ctrl Pts',(1.3224756056767,0.763531646934159,-2.53645833333333));
#422290=CARTESIAN_POINT('Ctrl Pts',(0.881650403784469,1.52706329386832,
-2.49479166666667));
#422291=CARTESIAN_POINT('Ctrl Pts',(0.,1.52706329386832,-2.453125));
#422292=CARTESIAN_POINT('Ctrl Pts',(-0.881650403784468,1.52706329386832,
-2.41145833333333));
#422293=CARTESIAN_POINT('Ctrl Pts',(-1.3224756056767,0.76353164693416,-2.36979166666667));
#422294=CARTESIAN_POINT('Ctrl Pts',(-1.76330080756894,2.64858386892187E-15,
-2.328125));
#422295=CARTESIAN_POINT('Ctrl Pts',(-1.3224756056767,-0.763531646934155,
-2.28645833333333));
#422296=CARTESIAN_POINT('Ctrl Pts',(-0.881650403784469,-1.52706329386831,
-2.24479166666667));
#422297=CARTESIAN_POINT('Ctrl Pts',(-1.87011317493125E-16,-1.52706329386831,
-2.203125));
#422298=CARTESIAN_POINT('Ctrl Pts',(0.881650403784467,-1.52706329386831,
-2.16145833333333));
#422299=CARTESIAN_POINT('Ctrl Pts',(1.3224756056767,-0.763531646934156,
-2.11979166666667));
#422300=CARTESIAN_POINT('Ctrl Pts',(1.76330080756894,2.21669973093722E-15,
-2.078125));
#422301=CARTESIAN_POINT('Ctrl Pts',(1.3224756056767,0.763531646934159,-2.03645833333333));
#422302=CARTESIAN_POINT('Ctrl Pts',(0.881650403784469,1.52706329386832,
-1.99479166666667));
#422303=CARTESIAN_POINT('Ctrl Pts',(0.,1.52706329386832,-1.953125));
#422304=CARTESIAN_POINT('Ctrl Pts',(-0.881650403784468,1.52706329386832,
-1.91145833333333));
#422305=CARTESIAN_POINT('Ctrl Pts',(-1.3224756056767,0.76353164693416,-1.86979166666667));
#422306=CARTESIAN_POINT('Ctrl Pts',(-1.76330080756894,2.64858386892187E-15,
-1.828125));
#422307=CARTESIAN_POINT('Ctrl Pts',(-1.3224756056767,-0.763531646934155,
-1.78645833333333));
#422308=CARTESIAN_POINT('Ctrl Pts',(-0.881650403784469,-1.52706329386831,
-1.74479166666667));
#422309=CARTESIAN_POINT('Ctrl Pts',(-1.87011317493125E-16,-1.52706329386831,
-1.703125));
#422310=CARTESIAN_POINT('Ctrl Pts',(0.881650403784467,-1.52706329386831,
-1.66145833333333));
#422311=CARTESIAN_POINT('Ctrl Pts',(1.3224756056767,-0.763531646934156,
-1.61979166666667));
#422312=CARTESIAN_POINT('Ctrl Pts',(1.76330080756894,2.21669973093722E-15,
-1.578125));
#422313=CARTESIAN_POINT('Ctrl Pts',(1.3224756056767,0.763531646934159,-1.53645833333333));
#422314=CARTESIAN_POINT('Ctrl Pts',(0.881650403784469,1.52706329386832,
-1.49479166666667));
#422315=CARTESIAN_POINT('Ctrl Pts',(0.,1.52706329386832,-1.453125));
#422316=CARTESIAN_POINT('Ctrl Pts',(-0.881650403784468,1.52706329386832,
-1.41145833333333));
#422317=CARTESIAN_POINT('Ctrl Pts',(-1.3224756056767,0.76353164693416,-1.36979166666667));
#422318=CARTESIAN_POINT('Ctrl Pts',(-1.76330080756894,2.64858386892187E-15,
-1.328125));
#422319=CARTESIAN_POINT('Ctrl Pts',(-1.3224756056767,-0.763531646934155,
-1.28645833333333));
#422320=CARTESIAN_POINT('Ctrl Pts',(-0.881650403784469,-1.52706329386831,
-1.24479166666667));
#422321=CARTESIAN_POINT('Ctrl Pts',(-1.87011317493125E-16,-1.52706329386831,
-1.203125));
#422322=CARTESIAN_POINT('Ctrl Pts',(0.881650403784467,-1.52706329386831,
-1.16145833333333));
#422323=CARTESIAN_POINT('Ctrl Pts',(1.3224756056767,-0.763531646934156,
-1.11979166666667));
#422324=CARTESIAN_POINT('Ctrl Pts',(1.76330080756894,2.21669973093722E-15,
-1.078125));
#422325=CARTESIAN_POINT('Ctrl Pts',(1.3224756056767,0.763531646934159,-1.03645833333333));
#422326=CARTESIAN_POINT('Ctrl Pts',(0.881650403784469,1.52706329386832,
-0.994791666666666));
#422327=CARTESIAN_POINT('Ctrl Pts',(0.,1.52706329386832,-0.953124999999999));
#422328=CARTESIAN_POINT('Ctrl Pts',(-0.881650403784468,1.52706329386832,
-0.911458333333334));
#422329=CARTESIAN_POINT('Ctrl Pts',(-1.3224756056767,0.76353164693416,-0.869791666666666));
#422330=CARTESIAN_POINT('Ctrl Pts',(-1.76330080756894,2.64858386892187E-15,
-0.828124999999999));
#422331=CARTESIAN_POINT('Ctrl Pts',(-1.3224756056767,-0.763531646934155,
-0.786458333333334));
#422332=CARTESIAN_POINT('Ctrl Pts',(-0.881650403784469,-1.52706329386831,
-0.744791666666666));
#422333=CARTESIAN_POINT('Ctrl Pts',(-1.87011317493125E-16,-1.52706329386831,
-0.703124999999999));
#422334=CARTESIAN_POINT('Ctrl Pts',(0.881650403784467,-1.52706329386831,
-0.661458333333333));
#422335=CARTESIAN_POINT('Ctrl Pts',(1.3224756056767,-0.763531646934156,
-0.619791666666666));
#422336=CARTESIAN_POINT('Ctrl Pts',(1.76330080756894,2.21669973093722E-15,
-0.578124999999999));
#422337=CARTESIAN_POINT('Ctrl Pts',(1.3224756056767,0.763531646934159,-0.536458333333333));
#422338=CARTESIAN_POINT('Ctrl Pts',(0.881650403784469,1.52706329386832,
-0.494791666666666));
#422339=CARTESIAN_POINT('Ctrl Pts',(0.,1.52706329386832,-0.453124999999999));
#422340=CARTESIAN_POINT('Ctrl Pts',(-0.881650403784468,1.52706329386832,
-0.411458333333333));
#422341=CARTESIAN_POINT('Ctrl Pts',(-1.3224756056767,0.76353164693416,-0.369791666666666));
#422342=CARTESIAN_POINT('Ctrl Pts',(-1.76330080756894,2.64858386892187E-15,
-0.328125));
#422343=CARTESIAN_POINT('Ctrl Pts',(-1.3224756056767,-0.763531646934155,
-0.286458333333333));
#422344=CARTESIAN_POINT('Ctrl Pts',(-0.881650403784469,-1.52706329386831,
-0.244791666666666));
#422345=CARTESIAN_POINT('Ctrl Pts',(-1.87011317493125E-16,-1.52706329386831,
-0.203125));
#422346=CARTESIAN_POINT('Ctrl Pts',(0.881650403784467,-1.52706329386831,
-0.161458333333333));
#422347=CARTESIAN_POINT('Ctrl Pts',(1.3224756056767,-0.763531646934156,
-0.119791666666666));
#422348=CARTESIAN_POINT('Ctrl Pts',(1.76330080756894,2.21669973093722E-15,
-0.0781250000000001));
#422349=CARTESIAN_POINT('Ctrl Pts',(1.3224756056767,0.763531646934159,-0.0364583333333328));
#422350=CARTESIAN_POINT('Ctrl Pts',(0.881650403784469,1.52706329386832,
0.00520833333333449));
#422351=CARTESIAN_POINT('Ctrl Pts',(0.,1.52706329386832,0.046875));
#422352=CARTESIAN_POINT('Ctrl Pts',(-0.881650403784468,1.52706329386832,
0.0885416666666673));
#422353=CARTESIAN_POINT('Ctrl Pts',(-1.3224756056767,0.76353164693416,0.130208333333335));
#422354=CARTESIAN_POINT('Ctrl Pts',(-1.76330080756894,2.64858386892187E-15,
0.171875));
#422355=CARTESIAN_POINT('Ctrl Pts',(-1.3224756056767,-0.763531646934155,
0.213541666666667));
#422356=CARTESIAN_POINT('Ctrl Pts',(-0.881650403784469,-1.52706329386831,
0.255208333333335));
#422357=CARTESIAN_POINT('Ctrl Pts',(-1.87011317493125E-16,-1.52706329386831,
0.296875));
#422358=CARTESIAN_POINT('Ctrl Pts',(0.881650403784467,-1.52706329386831,
0.338541666666668));
#422359=CARTESIAN_POINT('Ctrl Pts',(1.3224756056767,-0.763531646934156,
0.380208333333333));
#422360=CARTESIAN_POINT('Ctrl Pts',(1.76330080756894,2.21669973093722E-15,
0.421875));
#422361=CARTESIAN_POINT('Ctrl Pts',(1.3224756056767,0.763531646934159,0.463541666666668));
#422362=CARTESIAN_POINT('Ctrl Pts',(0.881650403784469,1.52706329386832,
0.505208333333333));
#422363=CARTESIAN_POINT('Ctrl Pts',(0.,1.52706329386832,0.546875));
#422364=CARTESIAN_POINT('Ctrl Pts',(-0.881650403784468,1.52706329386832,
0.588541666666668));
#422365=CARTESIAN_POINT('Ctrl Pts',(-1.3224756056767,0.76353164693416,0.630208333333333));
#422366=CARTESIAN_POINT('Ctrl Pts',(-1.76330080756894,2.64858386892187E-15,
0.671875000000001));
#422367=CARTESIAN_POINT('Ctrl Pts',(-1.3224756056767,-0.763531646934155,
0.713541666666668));
#422368=CARTESIAN_POINT('Ctrl Pts',(-0.881650403784469,-1.52706329386831,
0.755208333333333));
#422369=CARTESIAN_POINT('Ctrl Pts',(-1.87011317493125E-16,-1.52706329386831,
0.796875000000001));
#422370=CARTESIAN_POINT('Ctrl Pts',(0.881650403784467,-1.52706329386831,
0.838541666666668));
#422371=CARTESIAN_POINT('Ctrl Pts',(1.3224756056767,-0.763531646934156,
0.880208333333333));
#422372=CARTESIAN_POINT('Ctrl Pts',(1.76330080756894,2.21669973093722E-15,
0.921875000000001));
#422373=CARTESIAN_POINT('Ctrl Pts',(1.3224756056767,0.763531646934159,0.963541666666666));
#422374=CARTESIAN_POINT('Ctrl Pts',(0.881650403784469,1.52706329386832,
1.00520833333333));
#422375=CARTESIAN_POINT('Ctrl Pts',(0.,1.52706329386832,1.046875));
#422376=CARTESIAN_POINT('Ctrl Pts',(-0.881650403784468,1.52706329386832,
1.08854166666667));
#422377=CARTESIAN_POINT('Ctrl Pts',(-1.3224756056767,0.76353164693416,1.13020833333333));
#422378=CARTESIAN_POINT('Ctrl Pts',(-1.76330080756894,2.64858386892187E-15,
1.171875));
#422379=CARTESIAN_POINT('Ctrl Pts',(-1.3224756056767,-0.763531646934155,
1.21354166666667));
#422380=CARTESIAN_POINT('Ctrl Pts',(-0.881650403784469,-1.52706329386831,
1.25520833333333));
#422381=CARTESIAN_POINT('Ctrl Pts',(-1.87011317493125E-16,-1.52706329386831,
1.296875));
#422382=CARTESIAN_POINT('Ctrl Pts',(0.881650403784467,-1.52706329386831,
1.33854166666667));
#422383=CARTESIAN_POINT('Ctrl Pts',(1.3224756056767,-0.763531646934156,
1.38020833333333));
#422384=CARTESIAN_POINT('Ctrl Pts',(1.76330080756894,2.21669973093722E-15,
1.421875));
#422385=CARTESIAN_POINT('Ctrl Pts',(1.3224756056767,0.763531646934159,1.46354166666667));
#422386=CARTESIAN_POINT('Ctrl Pts',(0.881650403784469,1.52706329386832,
1.50520833333333));
#422387=CARTESIAN_POINT('Ctrl Pts',(0.,1.52706329386832,1.546875));
#422388=CARTESIAN_POINT('Ctrl Pts',(-0.881650403784468,1.52706329386832,
1.58854166666667));
#422389=CARTESIAN_POINT('Ctrl Pts',(-1.3224756056767,0.76353164693416,1.63020833333333));
#422390=CARTESIAN_POINT('Ctrl Pts',(-1.76330080756894,2.64858386892187E-15,
1.671875));
#422391=CARTESIAN_POINT('Ctrl Pts',(-1.3224756056767,-0.763531646934155,
1.71354166666667));
#422392=CARTESIAN_POINT('Ctrl Pts',(-0.881650403784469,-1.52706329386831,
1.75520833333333));
#422393=CARTESIAN_POINT('Ctrl Pts',(-1.87011317493125E-16,-1.52706329386831,
1.796875));
#422394=CARTESIAN_POINT('Ctrl Pts',(0.881650403784467,-1.52706329386831,
1.83854166666667));
#422395=CARTESIAN_POINT('Ctrl Pts',(1.3224756056767,-0.763531646934156,
1.88020833333333));
#422396=CARTESIAN_POINT('Ctrl Pts',(1.76330080756894,2.21669973093722E-15,
1.921875));
#422397=CARTESIAN_POINT('Ctrl Pts',(1.3224756056767,0.763531646934159,1.96354166666667));
#422398=CARTESIAN_POINT('Ctrl Pts',(0.881650403784469,1.52706329386832,
2.00520833333333));
#422399=CARTESIAN_POINT('Ctrl Pts',(0.,1.52706329386832,2.046875));
#422400=CARTESIAN_POINT('Ctrl Pts',(-0.881650403784468,1.52706329386832,
2.08854166666667));
#422401=CARTESIAN_POINT('Ctrl Pts',(-1.3224756056767,0.76353164693416,2.13020833333333));
#422402=CARTESIAN_POINT('Ctrl Pts',(-1.76330080756894,2.64858386892187E-15,
2.171875));
#422403=CARTESIAN_POINT('Ctrl Pts',(-1.3224756056767,-0.763531646934155,
2.21354166666667));
#422404=CARTESIAN_POINT('Ctrl Pts',(-0.881650403784469,-1.52706329386831,
2.25520833333333));
#422405=CARTESIAN_POINT('Ctrl Pts',(-1.87011317493125E-16,-1.52706329386831,
2.296875));
#422406=CARTESIAN_POINT('Ctrl Pts',(0.881650403784467,-1.52706329386831,
2.33854166666667));
#422407=CARTESIAN_POINT('Ctrl Pts',(1.3224756056767,-0.763531646934156,
2.38020833333333));
#422408=CARTESIAN_POINT('Ctrl Pts',(1.76330080756894,2.21669973093722E-15,
2.421875));
#422409=CARTESIAN_POINT('Ctrl Pts',(1.3224756056767,0.763531646934159,2.46354166666667));
#422410=CARTESIAN_POINT('Ctrl Pts',(0.881650403784469,1.52706329386832,
2.50520833333333));
#422411=CARTESIAN_POINT('Ctrl Pts',(0.,1.52706329386832,2.546875));
#422412=CARTESIAN_POINT('Ctrl Pts',(-0.881650403784468,1.52706329386832,
2.58854166666667));
#422413=CARTESIAN_POINT('Ctrl Pts',(-1.3224756056767,0.76353164693416,2.63020833333333));
#422414=CARTESIAN_POINT('Ctrl Pts',(-1.76330080756894,2.64858386892187E-15,
2.671875));
#422415=CARTESIAN_POINT('Ctrl Pts',(-1.3224756056767,-0.763531646934155,
2.71354166666667));
#422416=CARTESIAN_POINT('Ctrl Pts',(-0.881650403784469,-1.52706329386831,
2.75520833333333));
#422417=CARTESIAN_POINT('Ctrl Pts',(-1.87011317493125E-16,-1.52706329386831,
2.796875));
#422418=CARTESIAN_POINT('Ctrl Pts',(0.881650403784467,-1.52706329386831,
2.83854166666667));
#422419=CARTESIAN_POINT('Ctrl Pts',(1.3224756056767,-0.763531646934156,
2.88020833333333));
#422420=CARTESIAN_POINT('Ctrl Pts',(1.76330080756894,2.21669973093722E-15,
2.921875));
#422421=CARTESIAN_POINT('Ctrl Pts',(1.3224756056767,0.763531646934159,2.96354166666667));
#422422=CARTESIAN_POINT('Ctrl Pts',(0.881650403784469,1.52706329386832,
3.00520833333333));
#422423=CARTESIAN_POINT('Ctrl Pts',(0.,1.52706329386832,3.046875));
#422424=CARTESIAN_POINT('Ctrl Pts',(-0.881650403784468,1.52706329386832,
3.08854166666667));
#422425=CARTESIAN_POINT('Ctrl Pts',(-1.3224756056767,0.76353164693416,3.13020833333333));
#422426=CARTESIAN_POINT('Ctrl Pts',(-1.76330080756894,2.64858386892187E-15,
3.171875));
#422427=CARTESIAN_POINT('Ctrl Pts',(-1.3224756056767,-0.763531646934155,
3.21354166666667));
#422428=CARTESIAN_POINT('Ctrl Pts',(-0.881650403784469,-1.52706329386831,
3.25520833333333));
#422429=CARTESIAN_POINT('Ctrl Pts',(-1.87011317493125E-16,-1.52706329386831,
3.296875));
#422430=CARTESIAN_POINT('Ctrl Pts',(0.881650403784467,-1.52706329386831,
3.33854166666667));
#422431=CARTESIAN_POINT('Ctrl Pts',(1.3224756056767,-0.763531646934156,
3.38020833333333));
#422432=CARTESIAN_POINT('Ctrl Pts',(1.76330080756894,2.21669973093722E-15,
3.421875));
#422433=CARTESIAN_POINT('Ctrl Pts',(1.3224756056767,0.763531646934159,3.46354166666667));
#422434=CARTESIAN_POINT('Ctrl Pts',(0.881650403784469,1.52706329386832,
3.50520833333333));
#422435=CARTESIAN_POINT('Ctrl Pts',(0.,1.52706329386832,3.546875));
#422436=CARTESIAN_POINT('Ctrl Pts',(-0.881650403784468,1.52706329386832,
3.58854166666667));
#422437=CARTESIAN_POINT('Ctrl Pts',(-1.3224756056767,0.76353164693416,3.63020833333333));
#422438=CARTESIAN_POINT('Ctrl Pts',(-1.76330080756894,2.64858386892187E-15,
3.671875));
#422439=CARTESIAN_POINT('Ctrl Pts',(-1.3224756056767,-0.763531646934155,
3.71354166666667));
#422440=CARTESIAN_POINT('Ctrl Pts',(-0.881650403784469,-1.52706329386831,
3.75520833333333));
#422441=CARTESIAN_POINT('Ctrl Pts',(-1.87011317493125E-16,-1.52706329386831,
3.796875));
#422442=CARTESIAN_POINT('Ctrl Pts',(0.881650403784467,-1.52706329386831,
3.83854166666667));
#422443=CARTESIAN_POINT('Ctrl Pts',(1.3224756056767,-0.763531646934156,
3.88020833333333));
#422444=CARTESIAN_POINT('Ctrl Pts',(1.76330080756894,2.21669973093722E-15,
3.921875));
#422445=CARTESIAN_POINT('Ctrl Pts',(1.3224756056767,0.763531646934159,3.96354166666667));
#422446=CARTESIAN_POINT('Ctrl Pts',(0.881650403784469,1.52706329386832,
4.00520833333333));
#422447=CARTESIAN_POINT('Ctrl Pts',(0.,1.52706329386832,4.046875));
#422448=CARTESIAN_POINT('Ctrl Pts',(-0.881650403784468,1.52706329386832,
4.08854166666667));
#422449=CARTESIAN_POINT('Ctrl Pts',(-1.3224756056767,0.76353164693416,4.13020833333333));
#422450=CARTESIAN_POINT('Ctrl Pts',(-1.76330080756894,2.64858386892187E-15,
4.171875));
#422451=CARTESIAN_POINT('Ctrl Pts',(-1.3224756056767,-0.763531646934155,
4.21354166666667));
#422452=CARTESIAN_POINT('Ctrl Pts',(-0.881650403784469,-1.52706329386831,
4.25520833333333));
#422453=CARTESIAN_POINT('Ctrl Pts',(-1.87011317493125E-16,-1.52706329386831,
4.296875));
#422454=CARTESIAN_POINT('Ctrl Pts',(0.881650403784467,-1.52706329386831,
4.33854166666667));
#422455=CARTESIAN_POINT('Ctrl Pts',(1.3224756056767,-0.763531646934156,
4.38020833333334));
#422456=CARTESIAN_POINT('Ctrl Pts',(1.76330080756894,2.21669973093722E-15,
4.421875));
#422457=CARTESIAN_POINT('Ctrl Pts',(1.3224756056767,0.763531646934159,4.46354166666667));
#422458=CARTESIAN_POINT('Ctrl Pts',(0.881650403784469,1.52706329386832,
4.50520833333333));
#422459=CARTESIAN_POINT('Ctrl Pts',(0.,1.52706329386832,4.546875));
#422460=CARTESIAN_POINT('Ctrl Pts',(-0.881650403784468,1.52706329386832,
4.58854166666667));
#422461=CARTESIAN_POINT('Ctrl Pts',(-1.3224756056767,0.76353164693416,4.63020833333333));
#422462=CARTESIAN_POINT('Ctrl Pts',(-1.76330080756894,2.64858386892187E-15,
4.671875));
#422463=CARTESIAN_POINT('Ctrl Pts',(-1.3224756056767,-0.763531646934155,
4.71354166666667));
#422464=CARTESIAN_POINT('Ctrl Pts',(-0.881650403784469,-1.52706329386831,
4.75520833333333));
#422465=CARTESIAN_POINT('Ctrl Pts',(-1.87011317493125E-16,-1.52706329386831,
4.796875));
#422466=CARTESIAN_POINT('Ctrl Pts',(0.881650403784467,-1.52706329386831,
4.83854166666667));
#422467=CARTESIAN_POINT('Ctrl Pts',(1.3224756056767,-0.763531646934156,
4.88020833333334));
#422468=CARTESIAN_POINT('Ctrl Pts',(1.76330080756894,2.21669973093722E-15,
4.921875));
#422469=CARTESIAN_POINT('Ctrl Pts',(1.3224756056767,0.763531646934159,4.96354166666667));
#422470=CARTESIAN_POINT('Ctrl Pts',(0.881650403784469,1.52706329386832,
5.00520833333333));
#422471=CARTESIAN_POINT('Ctrl Pts',(0.,1.52706329386832,5.046875));
#422472=CARTESIAN_POINT('Ctrl Pts',(-0.881650403784468,1.52706329386832,
5.08854166666667));
#422473=CARTESIAN_POINT('Ctrl Pts',(-1.3224756056767,0.76353164693416,5.13020833333333));
#422474=CARTESIAN_POINT('Ctrl Pts',(-1.76330080756894,2.64858386892187E-15,
5.171875));
#422475=CARTESIAN_POINT('Ctrl Pts',(-1.3224756056767,-0.763531646934155,
5.21354166666667));
#422476=CARTESIAN_POINT('Ctrl Pts',(-0.881650403784469,-1.52706329386831,
5.25520833333333));
#422477=CARTESIAN_POINT('Ctrl Pts',(-1.87011317493125E-16,-1.52706329386831,
5.296875));
#422478=CARTESIAN_POINT('Ctrl Pts',(0.881650403784467,-1.52706329386831,
5.33854166666667));
#422479=CARTESIAN_POINT('Ctrl Pts',(1.3224756056767,-0.763531646934156,
5.38020833333333));
#422480=CARTESIAN_POINT('Ctrl Pts',(1.76330080756894,2.21669973093722E-15,
5.421875));
#422481=CARTESIAN_POINT('Ctrl Pts',(1.3224756056767,0.763531646934159,5.46354166666667));
#422482=CARTESIAN_POINT('Ctrl Pts',(0.881650403784469,1.52706329386832,
5.50520833333333));
#422483=CARTESIAN_POINT('Ctrl Pts',(0.,1.52706329386832,5.546875));
#422484=CARTESIAN_POINT('Ctrl Pts',(-0.881650403784468,1.52706329386832,
5.58854166666667));
#422485=CARTESIAN_POINT('Ctrl Pts',(-1.3224756056767,0.76353164693416,5.63020833333333));
#422486=CARTESIAN_POINT('Ctrl Pts',(-1.76330080756894,2.64858386892187E-15,
5.671875));
#422487=CARTESIAN_POINT('Ctrl Pts',(-1.3224756056767,-0.763531646934155,
5.71354166666667));
#422488=CARTESIAN_POINT('Ctrl Pts',(-0.881650403784469,-1.52706329386831,
5.75520833333333));
#422489=CARTESIAN_POINT('Ctrl Pts',(-1.87011317493125E-16,-1.52706329386831,
5.796875));
#422490=CARTESIAN_POINT('Ctrl Pts',(0.881650403784467,-1.52706329386831,
5.83854166666667));
#422491=CARTESIAN_POINT('Ctrl Pts',(1.3224756056767,-0.763531646934156,
5.88020833333333));
#422492=CARTESIAN_POINT('Ctrl Pts',(1.76330080756894,2.21669973093722E-15,
5.921875));
#422493=CARTESIAN_POINT('Ctrl Pts',(1.3224756056767,0.763531646934159,5.96354166666667));
#422494=CARTESIAN_POINT('Ctrl Pts',(0.881650403784469,1.52706329386832,
6.00520833333333));
#422495=CARTESIAN_POINT('Ctrl Pts',(0.,1.52706329386832,6.046875));
#422496=CARTESIAN_POINT('Ctrl Pts',(-0.881650403784468,1.52706329386832,
6.08854166666667));
#422497=CARTESIAN_POINT('Ctrl Pts',(-1.3224756056767,0.76353164693416,6.13020833333333));
#422498=CARTESIAN_POINT('Ctrl Pts',(-1.76330080756894,2.64858386892187E-15,
6.171875));
#422499=CARTESIAN_POINT('Ctrl Pts',(-1.3224756056767,-0.763531646934155,
6.21354166666667));
#422500=CARTESIAN_POINT('Ctrl Pts',(-0.881650403784469,-1.52706329386831,
6.25520833333333));
#422501=CARTESIAN_POINT('Ctrl Pts',(-1.87011317493125E-16,-1.52706329386831,
6.296875));
#422502=CARTESIAN_POINT('Ctrl Pts',(0.881650403784467,-1.52706329386831,
6.33854166666667));
#422503=CARTESIAN_POINT('Ctrl Pts',(1.3224756056767,-0.763531646934156,
6.38020833333333));
#422504=CARTESIAN_POINT('Ctrl Pts',(1.76330080756894,2.21669973093722E-15,
6.421875));
#422505=CARTESIAN_POINT('Ctrl Pts',(1.3224756056767,0.763531646934159,6.46354166666667));
#422506=CARTESIAN_POINT('Ctrl Pts',(0.881650403784469,1.52706329386832,
6.50520833333333));
#422507=CARTESIAN_POINT('Ctrl Pts',(0.,1.52706329386832,6.546875));
#422508=CARTESIAN_POINT('Ctrl Pts',(-0.881650403784468,1.52706329386832,
6.58854166666667));
#422509=CARTESIAN_POINT('Ctrl Pts',(-1.3224756056767,0.76353164693416,6.63020833333333));
#422510=CARTESIAN_POINT('Ctrl Pts',(-1.76330080756894,2.64858386892187E-15,
6.671875));
#422511=CARTESIAN_POINT('Ctrl Pts',(-1.3224756056767,-0.763531646934155,
6.71354166666667));
#422512=CARTESIAN_POINT('Ctrl Pts',(-0.881650403784469,-1.52706329386831,
6.75520833333333));
#422513=CARTESIAN_POINT('Ctrl Pts',(-1.87011317493125E-16,-1.52706329386831,
6.796875));
#422514=CARTESIAN_POINT('Ctrl Pts',(0.881650403784467,-1.52706329386831,
6.83854166666667));
#422515=CARTESIAN_POINT('Ctrl Pts',(1.3224756056767,-0.763531646934156,
6.88020833333333));
#422516=CARTESIAN_POINT('Ctrl Pts',(1.76330080756894,2.21669973093722E-15,
6.921875));
#422517=CARTESIAN_POINT('Ctrl Pts',(1.3224756056767,0.763531646934159,6.96354166666667));
#422518=CARTESIAN_POINT('Ctrl Pts',(0.881650403784469,1.52706329386832,
7.00520833333333));
#422519=CARTESIAN_POINT('Ctrl Pts',(0.,1.52706329386832,7.046875));
#422520=CARTESIAN_POINT('Ctrl Pts',(-0.881650403784468,1.52706329386832,
7.08854166666667));
#422521=CARTESIAN_POINT('Ctrl Pts',(-1.3224756056767,0.76353164693416,7.13020833333333));
#422522=CARTESIAN_POINT('Ctrl Pts',(-1.76330080756894,2.64858386892187E-15,
7.171875));
#422523=CARTESIAN_POINT('Ctrl Pts',(-1.3224756056767,-0.763531646934155,
7.21354166666667));
#422524=CARTESIAN_POINT('Ctrl Pts',(-0.881650403784469,-1.52706329386831,
7.25520833333333));
#422525=CARTESIAN_POINT('Ctrl Pts',(-1.87011317493125E-16,-1.52706329386831,
7.296875));
#422526=CARTESIAN_POINT('Ctrl Pts',(0.881650403784467,-1.52706329386831,
7.33854166666667));
#422527=CARTESIAN_POINT('Ctrl Pts',(1.3224756056767,-0.763531646934156,
7.38020833333333));
#422528=CARTESIAN_POINT('Ctrl Pts',(1.76330080756894,2.21669973093722E-15,
7.421875));
#422529=CARTESIAN_POINT('Ctrl Pts',(1.3224756056767,0.763531646934159,7.46354166666667));
#422530=CARTESIAN_POINT('Ctrl Pts',(0.881650403784469,1.52706329386832,
7.50520833333333));
#422531=CARTESIAN_POINT('Ctrl Pts',(0.,1.52706329386832,7.546875));
#422532=CARTESIAN_POINT('Ctrl Pts',(-0.881650403784468,1.52706329386832,
7.58854166666667));
#422533=CARTESIAN_POINT('Ctrl Pts',(-1.3224756056767,0.76353164693416,7.63020833333333));
#422534=CARTESIAN_POINT('Ctrl Pts',(-1.76330080756894,2.64858386892187E-15,
7.671875));
#422535=CARTESIAN_POINT('Ctrl Pts',(-1.3224756056767,-0.763531646934155,
7.71354166666667));
#422536=CARTESIAN_POINT('Ctrl Pts',(-0.881650403784469,-1.52706329386831,
7.75520833333334));
#422537=CARTESIAN_POINT('Ctrl Pts',(-1.87011317493125E-16,-1.52706329386831,
7.796875));
#422538=CARTESIAN_POINT('Ctrl Pts',(0.881650403784467,-1.52706329386831,
7.83854166666667));
#422539=CARTESIAN_POINT('Ctrl Pts',(1.3224756056767,-0.763531646934156,
7.88020833333333));
#422540=CARTESIAN_POINT('Ctrl Pts',(1.76330080756894,2.21669973093722E-15,
7.921875));
#422541=CARTESIAN_POINT('Ctrl Pts',(1.3224756056767,0.763531646934159,7.96354166666667));
#422542=CARTESIAN_POINT('Ctrl Pts',(0.881650403784469,1.52706329386832,
8.00520833333333));
#422543=CARTESIAN_POINT('Ctrl Pts',(0.,1.52706329386832,8.046875));
#422544=CARTESIAN_POINT('Ctrl Pts',(-0.881650403784468,1.52706329386832,
8.08854166666667));
#422545=CARTESIAN_POINT('Ctrl Pts',(-1.3224756056767,0.76353164693416,8.13020833333333));
#422546=CARTESIAN_POINT('Ctrl Pts',(-1.76330080756894,2.64858386892187E-15,
8.171875));
#422547=CARTESIAN_POINT('Ctrl Pts',(-1.3224756056767,-0.763531646934155,
8.21354166666667));
#422548=CARTESIAN_POINT('Ctrl Pts',(-0.881650403784469,-1.52706329386831,
8.25520833333334));
#422549=CARTESIAN_POINT('Ctrl Pts',(-1.87011317493125E-16,-1.52706329386831,
8.296875));
#422550=CARTESIAN_POINT('Ctrl Pts',(0.881650403784467,-1.52706329386831,
8.33854166666666));
#422551=CARTESIAN_POINT('Ctrl Pts',(1.3224756056767,-0.763531646934156,
8.38020833333334));
#422552=CARTESIAN_POINT('Ctrl Pts',(1.76330080756894,2.21669973093722E-15,
8.421875));
#422553=CARTESIAN_POINT('Ctrl Pts',(1.3224756056767,0.763531646934159,8.46354166666667));
#422554=CARTESIAN_POINT('Ctrl Pts',(0.881650403784469,1.52706329386832,
8.50520833333334));
#422555=CARTESIAN_POINT('Ctrl Pts',(0.,1.52706329386832,8.546875));
#422556=CARTESIAN_POINT('Ctrl Pts',(-0.881650403784468,1.52706329386832,
8.58854166666667));
#422557=CARTESIAN_POINT('Ctrl Pts',(-1.3224756056767,0.76353164693416,8.63020833333334));
#422558=CARTESIAN_POINT('Ctrl Pts',(-1.76330080756894,2.64858386892187E-15,
8.671875));
#422559=CARTESIAN_POINT('Ctrl Pts',(-1.3224756056767,-0.763531646934155,
8.71354166666667));
#422560=CARTESIAN_POINT('Ctrl Pts',(-0.881650403784469,-1.52706329386831,
8.75520833333334));
#422561=CARTESIAN_POINT('Ctrl Pts',(-1.87011317493125E-16,-1.52706329386831,
8.796875));
#422562=CARTESIAN_POINT('Ctrl Pts',(0.881650403784467,-1.52706329386831,
8.83854166666667));
#422563=CARTESIAN_POINT('Ctrl Pts',(1.3224756056767,-0.763531646934156,
8.88020833333333));
#422564=CARTESIAN_POINT('Ctrl Pts',(1.76330080756894,2.21669973093722E-15,
8.921875));
#422565=CARTESIAN_POINT('Ctrl Pts',(1.3224756056767,0.763531646934159,8.96354166666667));
#422566=CARTESIAN_POINT('Ctrl Pts',(0.881650403784469,1.52706329386832,
9.00520833333333));
#422567=CARTESIAN_POINT('Ctrl Pts',(0.,1.52706329386832,9.046875));
#422568=CARTESIAN_POINT('Ctrl Pts',(-0.881650403784468,1.52706329386832,
9.08854166666667));
#422569=CARTESIAN_POINT('Ctrl Pts',(-1.3224756056767,0.76353164693416,9.13020833333333));
#422570=CARTESIAN_POINT('Ctrl Pts',(-1.76330080756894,2.64858386892187E-15,
9.171875));
#422571=CARTESIAN_POINT('Ctrl Pts',(-1.3224756056767,-0.763531646934155,
9.21354166666667));
#422572=CARTESIAN_POINT('Ctrl Pts',(-0.881650403784469,-1.52706329386831,
9.25520833333333));
#422573=CARTESIAN_POINT('Ctrl Pts',(-1.87011317493125E-16,-1.52706329386831,
9.296875));
#422574=CARTESIAN_POINT('Ctrl Pts',(0.881650403784467,-1.52706329386831,
9.33854166666667));
#422575=CARTESIAN_POINT('Ctrl Pts',(1.3224756056767,-0.763531646934156,
9.38020833333333));
#422576=CARTESIAN_POINT('Ctrl Pts',(1.76330080756894,2.21669973093722E-15,
9.421875));
#422577=CARTESIAN_POINT('Ctrl Pts',(1.3224756056767,0.763531646934159,9.46354166666667));
#422578=CARTESIAN_POINT('Ctrl Pts',(0.881650403784469,1.52706329386832,
9.50520833333334));
#422579=CARTESIAN_POINT('Ctrl Pts',(0.,1.52706329386832,9.546875));
#422580=CARTESIAN_POINT('Ctrl Pts',(-0.881650403784468,1.52706329386832,
9.58854166666667));
#422581=CARTESIAN_POINT('Ctrl Pts',(-1.3224756056767,0.76353164693416,9.63020833333333));
#422582=CARTESIAN_POINT('Ctrl Pts',(-1.76330080756894,2.64858386892187E-15,
9.671875));
#422583=CARTESIAN_POINT('Ctrl Pts',(-1.3224756056767,-0.763531646934155,
9.71354166666667));
#422584=CARTESIAN_POINT('Ctrl Pts',(-0.881650403784469,-1.52706329386831,
9.75520833333333));
#422585=CARTESIAN_POINT('Ctrl Pts',(-1.87011317493125E-16,-1.52706329386831,
9.796875));
#422586=CARTESIAN_POINT('Ctrl Pts',(0.881650403784467,-1.52706329386831,
9.83854166666667));
#422587=CARTESIAN_POINT('Ctrl Pts',(1.3224756056767,-0.763531646934156,
9.88020833333333));
#422588=CARTESIAN_POINT('Ctrl Pts',(1.76330080756894,2.21669973093722E-15,
9.921875));
#422589=CARTESIAN_POINT('Ctrl Pts',(1.3224756056767,0.763531646934159,9.96354166666667));
#422590=CARTESIAN_POINT('Ctrl Pts',(0.881650403784469,1.52706329386832,
10.0052083333333));
#422591=CARTESIAN_POINT('Ctrl Pts',(0.,1.52706329386832,10.046875));
#422592=CARTESIAN_POINT('Ctrl Pts',(-0.881650403784468,1.52706329386832,
10.0885416666667));
#422593=CARTESIAN_POINT('Ctrl Pts',(-1.3224756056767,0.76353164693416,10.1302083333333));
#422594=CARTESIAN_POINT('Ctrl Pts',(-1.76330080756894,2.64858386892187E-15,
10.171875));
#422595=CARTESIAN_POINT('Ctrl Pts',(-1.3224756056767,-0.763531646934155,
10.2135416666667));
#422596=CARTESIAN_POINT('Ctrl Pts',(-0.881650403784469,-1.52706329386831,
10.2552083333333));
#422597=CARTESIAN_POINT('Ctrl Pts',(-1.87011317493125E-16,-1.52706329386831,
10.296875));
#422598=CARTESIAN_POINT('Ctrl Pts',(0.881650403784467,-1.52706329386831,
10.3385416666667));
#422599=CARTESIAN_POINT('Ctrl Pts',(1.3224756056767,-0.763531646934156,
10.3802083333333));
#422600=CARTESIAN_POINT('Ctrl Pts',(1.76330080756894,2.21669973093722E-15,
10.421875));
#422601=CARTESIAN_POINT('Ctrl Pts',(1.3224756056767,0.763531646934159,10.4635416666667));
#422602=CARTESIAN_POINT('Ctrl Pts',(0.881650403784469,1.52706329386832,
10.5052083333333));
#422603=CARTESIAN_POINT('Ctrl Pts',(0.,1.52706329386832,10.546875));
#422604=CARTESIAN_POINT('Ctrl Pts',(-0.881650403784468,1.52706329386832,
10.5885416666667));
#422605=CARTESIAN_POINT('Ctrl Pts',(-1.3224756056767,0.76353164693416,10.6302083333333));
#422606=CARTESIAN_POINT('Ctrl Pts',(-1.76330080756894,2.64858386892187E-15,
10.671875));
#422607=CARTESIAN_POINT('Ctrl Pts',(-1.3224756056767,-0.763531646934155,
10.7135416666667));
#422608=CARTESIAN_POINT('Ctrl Pts',(-0.881650403784469,-1.52706329386831,
10.7552083333333));
#422609=CARTESIAN_POINT('Ctrl Pts',(-1.87011317493125E-16,-1.52706329386831,
10.796875));
#422610=CARTESIAN_POINT('Ctrl Pts',(0.881650403784467,-1.52706329386831,
10.8385416666667));
#422611=CARTESIAN_POINT('Ctrl Pts',(1.3224756056767,-0.763531646934156,
10.8802083333333));
#422612=CARTESIAN_POINT('Ctrl Pts',(1.76330080756894,2.21669973093722E-15,
10.921875));
#422613=CARTESIAN_POINT('Ctrl Pts',(1.3224756056767,0.763531646934159,10.9635416666667));
#422614=CARTESIAN_POINT('Ctrl Pts',(0.881650403784469,1.52706329386832,
11.0052083333333));
#422615=CARTESIAN_POINT('Ctrl Pts',(0.,1.52706329386832,11.046875));
#422616=CARTESIAN_POINT('Origin',(0.,0.,12.5));
#422617=CARTESIAN_POINT('',(-0.0113570611445785,2.67622108038738,12.5737548217797));
#422618=CARTESIAN_POINT('',(0.0113570611445786,2.67622108038738,12.5737548217797));
#422619=CARTESIAN_POINT('Ctrl Pts',(-0.0113570611446294,2.67622108038736,
12.5737548217797));
#422620=CARTESIAN_POINT('Ctrl Pts',(-0.0110019926948033,2.67528393257247,
12.5746934679442));
#422621=CARTESIAN_POINT('Ctrl Pts',(-0.0104377846361818,2.67431181904781,
12.5756680099006));
#422622=CARTESIAN_POINT('Ctrl Pts',(-0.00973150788946615,2.67341366715362,
12.5765688348656));
#422623=CARTESIAN_POINT('Ctrl Pts',(-0.0095445289395165,2.6731758913825,
12.5768073183026));
#422624=CARTESIAN_POINT('Ctrl Pts',(-0.00934782754285408,2.67294319438909,
12.5770407398754));
#422625=CARTESIAN_POINT('Ctrl Pts',(-0.00914308800688213,2.67271724557782,
12.5772674179684));
#422626=CARTESIAN_POINT('Ctrl Pts',(-0.00830289231515457,2.67179001275552,
12.5781976435658));
#422627=CARTESIAN_POINT('Ctrl Pts',(-0.00727124971308708,2.67093133294071,
12.5790594849312));
#422628=CARTESIAN_POINT('Ctrl Pts',(-0.00608692606376634,2.67023630041101,
12.5797571720116));
#422629=CARTESIAN_POINT('Ctrl Pts',(-0.00531529662175078,2.66978346172677,
12.580211740231));
#422630=CARTESIAN_POINT('Ctrl Pts',(-0.0044342859023428,2.66939570266161,
12.5806009430798));
#422631=CARTESIAN_POINT('Ctrl Pts',(-0.0034987762678617,2.66911653534957,
12.5808812374708));
#422632=CARTESIAN_POINT('Ctrl Pts',(-0.00269486313975067,2.66887663801573,
12.5811221033394));
#422633=CARTESIAN_POINT('Ctrl Pts',(-0.00183421434939168,2.66871212840399,
12.581287365893));
#422634=CARTESIAN_POINT('Ctrl Pts',(-0.000963840870899584,2.66864048141248,
12.581359338449));
#422635=CARTESIAN_POINT('Ctrl Pts',(-0.000842876929915767,2.66863052396011,
12.5813693411482));
#422636=CARTESIAN_POINT('Ctrl Pts',(-0.000721709896414026,2.66862230227233,
12.5813775999465));
#422637=CARTESIAN_POINT('Ctrl Pts',(-0.000600449288197464,2.66861580422801,
12.5813841266931));
#422638=CARTESIAN_POINT('Ctrl Pts',(-0.000394716000188903,2.66860477950991,
12.5813952001081));
#422639=CARTESIAN_POINT('Ctrl Pts',(-0.000187302871016306,2.6685992504993,
12.5814007534795));
#422640=CARTESIAN_POINT('Ctrl Pts',(2.17050192878445E-5,2.66859941674402,
12.5814005856065));
#422641=CARTESIAN_POINT('Ctrl Pts',(0.000978461424311802,2.66860017774733,
12.5813998171494));
#422642=CARTESIAN_POINT('Ctrl Pts',(0.00190253100785044,2.66871988992492,
12.58127954464));
#422643=CARTESIAN_POINT('Ctrl Pts',(0.00279246900606494,2.66892852948603,
12.5810700125799));
#422644=CARTESIAN_POINT('Ctrl Pts',(0.00386741278035352,2.66918054232034,
12.5808169217085));
#422645=CARTESIAN_POINT('Ctrl Pts',(0.00488883606980967,2.66957861621199,
12.5804173076348));
#422646=CARTESIAN_POINT('Ctrl Pts',(0.00577667963579214,2.67006359989213,
12.5799304713245));
#422647=CARTESIAN_POINT('Ctrl Pts',(0.00687699751361092,2.67066464745743,
12.5793271277669));
#422648=CARTESIAN_POINT('Ctrl Pts',(0.00785584128008872,2.67140820491266,
12.5785808224116));
#422649=CARTESIAN_POINT('Ctrl Pts',(0.00869113617801994,2.67223767359591,
12.5777485681082));
#422650=CARTESIAN_POINT('Ctrl Pts',(0.00993581708932545,2.67347367280903,
12.576508418016));
#422651=CARTESIAN_POINT('Ctrl Pts',(0.0108561202078293,2.67488514781087,
12.5750928681475));
#422652=CARTESIAN_POINT('Ctrl Pts',(0.0113570611445786,2.67622108038738,
12.5737548217797));
#422653=CARTESIAN_POINT('Origin',(4.96027592420657,14.4980536550356,-1.23970454698711));
#422654=CARTESIAN_POINT('Ctrl Pts',(-0.0391405672444681,2.74327713825537,
12.5064436508398));
#422655=CARTESIAN_POINT('Ctrl Pts',(-0.0350274426582294,2.73335128343629,
12.5164271754438));
#422656=CARTESIAN_POINT('Ctrl Pts',(-0.0309128806500304,2.7234214140262,
12.5264061185523));
#422657=CARTESIAN_POINT('Ctrl Pts',(-0.02679682972068,2.71348738899688,
12.536380305637));
#422658=CARTESIAN_POINT('Ctrl Pts',(-0.0216526008840716,2.70107187254761,
12.5488460165097));
#422659=CARTESIAN_POINT('Ctrl Pts',(-0.0165060448658723,2.68864986137333,
12.5613043021964));
#422660=CARTESIAN_POINT('Ctrl Pts',(-0.0113570611445786,2.67622108038738,
12.5737548217797));
#422661=CARTESIAN_POINT('Ctrl Pts',(-0.0317307692307694,2.68331575103722,
12.5893111709658));
#422662=CARTESIAN_POINT('Ctrl Pts',(-0.0273715540959461,2.67285363471365,
12.5770542771492));
#422663=CARTESIAN_POINT('Ctrl Pts',(-0.0113570611445786,2.67622108038738,
12.5737548217797));
#422664=CARTESIAN_POINT('Ctrl Pts',(-0.0412629097345479,2.70619288824629,
12.5663937883685));
#422665=CARTESIAN_POINT('Ctrl Pts',(-0.0368981338154389,2.69571742604038,
12.5540940315304));
#422666=CARTESIAN_POINT('Ctrl Pts',(-0.0208346759798513,2.69909844921069,
12.5508374392248));
#422667=CARTESIAN_POINT('Ctrl Pts',(-0.0507854324254145,2.72904694270437,
12.5434499600945));
#422668=CARTESIAN_POINT('Ctrl Pts',(-0.0464064650654964,2.71853742104045,
12.5311293540533));
#422669=CARTESIAN_POINT('Ctrl Pts',(-0.0303041210136914,2.72195301478113,
12.5278936106989));
#422670=CARTESIAN_POINT('Ctrl Pts',(-0.0602990906798147,2.75187972251493,
12.5204817579905));
#422671=CARTESIAN_POINT('Ctrl Pts',(-0.055898450424013,2.74131818590101,
12.5081597038247));
#422672=CARTESIAN_POINT('Ctrl Pts',(-0.0397660440343088,2.74478654415416,
12.5049254088044));
#422673=CARTESIAN_POINT('Ctrl Pts',(-0.0534592077666727,2.73546400352339,
12.5369868989719));
#422674=CARTESIAN_POINT('Ctrl Pts',(-0.0538174786896658,2.73632385415953,
12.5342545179733));
#422675=CARTESIAN_POINT('Ctrl Pts',(-0.0540442458867107,2.73719243561899,
12.5314872231885));
#422676=CARTESIAN_POINT('Ctrl Pts',(-0.0540726472749342,2.73803494049807,
12.5287124745063));
#422677=CARTESIAN_POINT('Ctrl Pts',(-0.0540982610565531,2.73879475321623,
12.5262100684184));
#422678=CARTESIAN_POINT('Ctrl Pts',(-0.0539615285066121,2.73953262349448,
12.5237004536639));
#422679=CARTESIAN_POINT('Ctrl Pts',(-0.053594920915001,2.74024914247203,
12.5212220730815));
#422680=CARTESIAN_POINT('Ctrl Pts',(-0.0533142510895361,2.74079769973319,
12.5193246583486));
#422681=CARTESIAN_POINT('Ctrl Pts',(-0.0528949269479518,2.74134000950387,
12.517417831369));
#422682=CARTESIAN_POINT('Ctrl Pts',(-0.0522498055207138,2.7418329426105,
12.5155812248348));
#422683=CARTESIAN_POINT('Ctrl Pts',(-0.0519749803251656,2.74204293476346,
12.5147988205793));
#422684=CARTESIAN_POINT('Ctrl Pts',(-0.0516590665142463,2.74224439930327,
12.5140295443047));
#422685=CARTESIAN_POINT('Ctrl Pts',(-0.0512954408753555,2.74243612605565,
12.5132817086137));
#422686=CARTESIAN_POINT('Ctrl Pts',(-0.0507451426610602,2.74272627855916,
12.5121499604604));
#422687=CARTESIAN_POINT('Ctrl Pts',(-0.05007035249633,2.7429940683096,12.5110494206568));
#422688=CARTESIAN_POINT('Ctrl Pts',(-0.0492469258911254,2.74321114142987,
12.5100666561695));
#422689=CARTESIAN_POINT('Ctrl Pts',(-0.0487741162306004,2.74333578431565,
12.5095023550641));
#422690=CARTESIAN_POINT('Ctrl Pts',(-0.0482466714157864,2.74344451472892,
12.5089719619137));
#422691=CARTESIAN_POINT('Ctrl Pts',(-0.047673188284389,2.74352903919257,
12.5085043804652));
#422692=CARTESIAN_POINT('Ctrl Pts',(-0.0468339704230212,2.74365272973503,
12.5078201359221));
#422693=CARTESIAN_POINT('Ctrl Pts',(-0.0458716475248564,2.7437269769725,
12.5072563000949));
#422694=CARTESIAN_POINT('Ctrl Pts',(-0.0448507996350875,2.7437383071242,
12.5068768744332));
#422695=CARTESIAN_POINT('Ctrl Pts',(-0.0441146980311557,2.74374647694355,
12.5066032824114));
#422696=CARTESIAN_POINT('Ctrl Pts',(-0.0433352353966569,2.74372213722096,
12.5064197834844));
#422697=CARTESIAN_POINT('Ctrl Pts',(-0.0425558582720206,2.74366923074806,
12.5063282718343));
#422698=CARTESIAN_POINT('Ctrl Pts',(-0.0414182089591113,2.74359200367704,
12.5061946931565));
#422699=CARTESIAN_POINT('Ctrl Pts',(-0.0402563540000962,2.74345331865916,
12.5062515701262));
#422700=CARTESIAN_POINT('Ctrl Pts',(-0.0391405672444685,2.74327713825537,
12.5064436508398));
#422701=CARTESIAN_POINT('Origin',(-0.011423076923077,2.69177728949876,12.5893111709658));
#422702=CARTESIAN_POINT('Origin',(-0.0737669000743653,2.72700246506185,
14.));
#422703=CARTESIAN_POINT('Origin',(-0.0737669000743651,2.72700246506185,
13.7435492065112));
#422704=CARTESIAN_POINT('Origin',(-0.0737669000743653,2.72700246506185,
12.5369868989719));
#422705=CARTESIAN_POINT('Ctrl Pts',(0.0317307692307692,2.68331575103722,
12.5893111709658));
#422706=CARTESIAN_POINT('Ctrl Pts',(0.0273715540959458,2.67285363471365,
12.5770542771492));
#422707=CARTESIAN_POINT('Ctrl Pts',(0.0113570611445786,2.67622108038738,
12.5737548217797));
#422708=CARTESIAN_POINT('Ctrl Pts',(0.0276636594244307,2.67355468750201,
12.5928319619712));
#422709=CARTESIAN_POINT('Ctrl Pts',(0.0217268505389381,2.66777647699801,
12.5821634970842));
#422710=CARTESIAN_POINT('Ctrl Pts',(0.00988422427522153,2.6726617308786,
12.5773203894503));
#422711=CARTESIAN_POINT('Ctrl Pts',(0.0153590491204503,2.66218892027728,
12.5969440695591));
#422712=CARTESIAN_POINT('Ctrl Pts',(0.0113393216910521,2.6621706461079,
12.5878292599214));
#422713=CARTESIAN_POINT('Ctrl Pts',(0.00549722182757579,2.66861224243907,
12.5813877129824));
#422714=CARTESIAN_POINT('Ctrl Pts',(-0.0152378843491264,2.66213499625976,
12.596957478804));
#422715=CARTESIAN_POINT('Ctrl Pts',(-0.0112478641478143,2.66215321553576,
12.5878468778671));
#422716=CARTESIAN_POINT('Ctrl Pts',(-0.00545385531034724,2.66859890739381,
12.5814011370086));
#422717=CARTESIAN_POINT('Ctrl Pts',(-0.0276577539880537,2.67354051445456,
12.5928371701607));
#422718=CARTESIAN_POINT('Ctrl Pts',(-0.0217209762404702,2.66777078866562,
12.5821692192952));
#422719=CARTESIAN_POINT('Ctrl Pts',(-0.00987974857032336,2.67265025064741,
12.5773318885715));
#422720=CARTESIAN_POINT('Ctrl Pts',(-0.0317307692308192,2.6833157510372,
12.5893111709658));
#422721=CARTESIAN_POINT('Ctrl Pts',(-0.027371554095996,2.67285363471362,
12.5770542771492));
#422722=CARTESIAN_POINT('Ctrl Pts',(-0.0113570611446294,2.67622108038736,
12.5737548217797));
#422723=CARTESIAN_POINT('Origin',(0.0114230769230771,2.69177728949876,12.5893111709658));
#422724=CARTESIAN_POINT('Ctrl Pts',(-0.0534431697003658,2.73542540894656,
12.5369868989719));
#422725=CARTESIAN_POINT('Ctrl Pts',(-0.059315855709328,2.74959561934461,
12.5369868989719));
#422726=CARTESIAN_POINT('Ctrl Pts',(-0.0746426453864402,2.74898502792764,
12.5369868989719));
#422727=CARTESIAN_POINT('Ctrl Pts',(-0.0554284284177582,2.74021546890479,
12.5218025310015));
#422728=CARTESIAN_POINT('Ctrl Pts',(-0.0628349616649562,2.74942411315693,
12.5216901060417));
#422729=CARTESIAN_POINT('Ctrl Pts',(-0.0745959249085834,2.74898690569132,
12.5161920673678));
#422730=CARTESIAN_POINT('Ctrl Pts',(-0.0522516314408065,2.74533836185331,
12.5042015548895));
#422731=CARTESIAN_POINT('Ctrl Pts',(-0.0571442744892229,2.74951441130436,
12.4980677368514));
#422732=CARTESIAN_POINT('Ctrl Pts',(-0.0639390575126279,2.74936709060421,
12.4907278922777));
#422733=CARTESIAN_POINT('Ctrl Pts',(-0.0391402818913614,2.74325713920844,
12.506463626192));
#422734=CARTESIAN_POINT('Ctrl Pts',(-0.0392336229776118,2.74979921271597,
12.4999376786891));
#422735=CARTESIAN_POINT('Ctrl Pts',(-0.0392324829519608,2.74971931080024,
12.4906970594712));
#422736=CARTESIAN_POINT('Ctrl Pts',(-0.0439361159158126,2.71260851248741,
13.793642941384));
#422737=CARTESIAN_POINT('Ctrl Pts',(-0.0480695586587779,2.72259955197769,
13.8071662555867));
#422738=CARTESIAN_POINT('Ctrl Pts',(-0.0645921377528991,2.71847356558496,
13.8103758687955));
#422739=CARTESIAN_POINT('Ctrl Pts',(-0.0503288525022281,2.72795108802607,
13.7804579775006));
#422740=CARTESIAN_POINT('Ctrl Pts',(-0.0554385177735605,2.74027525098119,
13.7901904343352));
#422741=CARTESIAN_POINT('Ctrl Pts',(-0.0711414500059975,2.73898147995502,
13.7927914348263));
#422742=CARTESIAN_POINT('Ctrl Pts',(-0.0540924971515107,2.73698383963716,
13.7597120340895));
#422743=CARTESIAN_POINT('Ctrl Pts',(-0.0600111123098007,2.7512441721922,
13.7635825532445));
#422744=CARTESIAN_POINT('Ctrl Pts',(-0.0750279227547006,2.75106719703732,
13.7651073818884));
#422745=CARTESIAN_POINT('Ctrl Pts',(-0.0533554893522594,2.73521502004488,
13.7381884353898));
#422746=CARTESIAN_POINT('Ctrl Pts',(-0.0591347381257982,2.74914190750188,
13.7368803041982));
#422747=CARTESIAN_POINT('Ctrl Pts',(-0.0742673064063059,2.74870030320526,
13.7363986145813));
#422748=CARTESIAN_POINT('Origin',(-0.0657949699454127,2.70786983275237,
13.7902182540695));
#422749=CARTESIAN_POINT('Ctrl Pts',(0.0113570611445786,2.67622108038738,
12.5737548217797));
#422750=CARTESIAN_POINT('Ctrl Pts',(0.0273715540959461,2.67285363471365,
12.5770542771492));
#422751=CARTESIAN_POINT('Ctrl Pts',(0.0317307692307694,2.68331575103722,
12.5893111709658));
#422752=CARTESIAN_POINT('Ctrl Pts',(0.0208332521184758,2.69909501224871,
12.5508408821982));
#422753=CARTESIAN_POINT('Ctrl Pts',(0.0368967013046715,2.69571398801462,
12.55409748406));
#422754=CARTESIAN_POINT('Ctrl Pts',(0.0412614776815739,2.70618945131915,
12.5663972313419));
#422755=CARTESIAN_POINT('Ctrl Pts',(0.030301275750311,2.72194614771936,
12.52790050457));
#422756=CARTESIAN_POINT('Ctrl Pts',(0.046403605589348,2.71853055829785,
12.5311362602938));
#422757=CARTESIAN_POINT('Ctrl Pts',(0.0507825712136453,2.72904007579613,
12.5434568539655));
#422758=CARTESIAN_POINT('Ctrl Pts',(0.0397617795410514,2.74477625307133,
12.5049357605811));
#422759=CARTESIAN_POINT('Ctrl Pts',(0.0558941686815425,2.74130790971908,
12.5081700652078));
#422760=CARTESIAN_POINT('Ctrl Pts',(0.0602948028693876,2.75186943176991,
12.5204921097672));
#422761=CARTESIAN_POINT('Ctrl Pts',(0.0391405672443406,2.74327713825507,
12.5064436508395));
#422762=CARTESIAN_POINT('Ctrl Pts',(0.0403458187330792,2.74346744495352,
12.5062361689309));
#422763=CARTESIAN_POINT('Ctrl Pts',(0.0416072967527669,2.74361395374604,
12.5061871075061));
#422764=CARTESIAN_POINT('Ctrl Pts',(0.042834363742733,2.7436869143056,12.5063648335164));
#422765=CARTESIAN_POINT('Ctrl Pts',(0.0433917732582066,2.74372005749215,
12.5064455676329));
#422766=CARTESIAN_POINT('Ctrl Pts',(0.0439498697112453,2.74373826608298,
12.506574497099));
#422767=CARTESIAN_POINT('Ctrl Pts',(0.0444847578701803,2.74373970895803,
12.5067492519495));
#422768=CARTESIAN_POINT('Ctrl Pts',(0.0455596363883573,2.74374260847144,
12.5071004286051));
#422769=CARTESIAN_POINT('Ctrl Pts',(0.0465803157288013,2.74367710231937,
12.5076537929612));
#422770=CARTESIAN_POINT('Ctrl Pts',(0.0474707943411653,2.74355754611012,
12.5083435010503));
#422771=CARTESIAN_POINT('Ctrl Pts',(0.0475268552914394,2.74355001933227,
12.5083869222963));
#422772=CARTESIAN_POINT('Ctrl Pts',(0.0475824047224509,2.74354226567989,
12.5084308732336));
#422773=CARTESIAN_POINT('Ctrl Pts',(0.0476374258851168,2.7435342837174,
12.5084753333615));
#422774=CARTESIAN_POINT('Ctrl Pts',(0.0480787682303327,2.74347025784312,
12.508831962269));
#422775=CARTESIAN_POINT('Ctrl Pts',(0.0484952661504182,2.74339151902502,
12.509227847131));
#422776=CARTESIAN_POINT('Ctrl Pts',(0.0488750551274305,2.74330315989752,
12.5096423454524));
#422777=CARTESIAN_POINT('Ctrl Pts',(0.0500651456938278,2.74302628149805,
12.5109411997424));
#422778=CARTESIAN_POINT('Ctrl Pts',(0.0509701735738429,2.74264732684897,
12.5124831113042));
#422779=CARTESIAN_POINT('Ctrl Pts',(0.0516586827254371,2.74223154610909,
12.5140723025008));
#422780=CARTESIAN_POINT('Ctrl Pts',(0.0517231967870444,2.74219258699837,
12.5142212114565));
#422781=CARTESIAN_POINT('Ctrl Pts',(0.0517858370895858,2.7421533161305,
12.5143705582413));
#422782=CARTESIAN_POINT('Ctrl Pts',(0.0518466749855142,2.74211379521906,
12.5145201959299));
#422783=CARTESIAN_POINT('Ctrl Pts',(0.0526282283368708,2.74160609027122,
12.5164425148273));
#422784=CARTESIAN_POINT('Ctrl Pts',(0.0531449550363651,2.7410487292595,
12.5184635205941));
#422785=CARTESIAN_POINT('Ctrl Pts',(0.0534850107690122,2.74046085777738,
12.5205025929158));
#422786=CARTESIAN_POINT('Ctrl Pts',(0.0536822565724959,2.74011986901671,
12.5216853356836));
#422787=CARTESIAN_POINT('Ctrl Pts',(0.0538201244047732,2.73976947321855,
12.5228750347131));
#422788=CARTESIAN_POINT('Ctrl Pts',(0.053914227561147,2.73941911276914,
12.5240609649613));
#422789=CARTESIAN_POINT('Ctrl Pts',(0.0541451987100069,2.73855917184226,
12.5269717671326));
#422790=CARTESIAN_POINT('Ctrl Pts',(0.054108978580863,2.73767254503778,
12.5299036066169));
#422791=CARTESIAN_POINT('Ctrl Pts',(0.0538915946618915,2.73676966278747,
12.5328133004019));
#422792=CARTESIAN_POINT('Ctrl Pts',(0.0537872377228983,2.73633622673406,
12.5342101228451));
#422793=CARTESIAN_POINT('Ctrl Pts',(0.0536407512085802,2.73589970799702,
12.5356023438238));
#422794=CARTESIAN_POINT('Ctrl Pts',(0.0534592077666729,2.73546400352339,
12.5369868989719));
#422795=CARTESIAN_POINT('Ctrl Pts',(-0.0317292560088479,2.68331211733141,
13.8235227101244));
#422796=CARTESIAN_POINT('Ctrl Pts',(-0.0361471144551244,2.69392650450487,
13.8358800583119));
#422797=CARTESIAN_POINT('Ctrl Pts',(-0.0523410482444131,2.69040761867485,
13.8390832900376));
#422798=CARTESIAN_POINT('Ctrl Pts',(-0.0363167865314177,2.69432219058271,
13.8124254819052));
#422799=CARTESIAN_POINT('Ctrl Pts',(-0.0407432246529827,2.70495719063873,
13.8247886449158));
#422800=CARTESIAN_POINT('Ctrl Pts',(-0.0569540009528031,2.70141720294675,
13.8279860620657));
#422801=CARTESIAN_POINT('Ctrl Pts',(-0.040902261072039,2.70532732947737,
13.8013225099955));
#422802=CARTESIAN_POINT('Ctrl Pts',(-0.0453351884501785,2.71597792517399,
13.8136962257787));
#422803=CARTESIAN_POINT('Ctrl Pts',(-0.0615645680923407,2.71242179507057,
13.8168830918626));
#422804=CARTESIAN_POINT('Ctrl Pts',(-0.0454857596258171,2.71632772600364,
13.7902140179785));
#422805=CARTESIAN_POINT('Ctrl Pts',(-0.0499232224687475,2.72698922801144,
13.802602731458));
#422806=CARTESIAN_POINT('Ctrl Pts',(-0.0661728417004948,2.72342159191108,
13.8057746032558));
#422807=CARTESIAN_POINT('Origin',(-0.0520384615384617,2.67485421257569,
13.8235269408515));
#422808=CARTESIAN_POINT('Ctrl Pts',(0.0391403049721299,2.74325875688934,
12.506462012331));
#422809=CARTESIAN_POINT('Ctrl Pts',(0.0392335873299004,2.74979671424555,
12.4999388158272));
#422810=CARTESIAN_POINT('Ctrl Pts',(0.0392324836772759,2.74971936163602,
12.4907030323752));
#422811=CARTESIAN_POINT('Ctrl Pts',(0.052251582889411,2.74533793329604,
12.5042014951932));
#422812=CARTESIAN_POINT('Ctrl Pts',(0.0571414622024566,2.7495128796933,
12.4980716682127));
#422813=CARTESIAN_POINT('Ctrl Pts',(0.0639314807543423,2.74936723186163,
12.4907355092743));
#422814=CARTESIAN_POINT('Ctrl Pts',(0.0554299221525007,2.74021700947567,
12.5218047446509));
#422815=CARTESIAN_POINT('Ctrl Pts',(0.0628336980936782,2.74942043127133,
12.5216906929434));
#422816=CARTESIAN_POINT('Ctrl Pts',(0.0745888263163512,2.74898717061242,
12.5161988840776));
#422817=CARTESIAN_POINT('Ctrl Pts',(0.0534444632996223,2.73542852959617,
12.5369868989719));
#422818=CARTESIAN_POINT('Ctrl Pts',(0.0593158561893107,2.74958947155127,
12.5369868989719));
#422819=CARTESIAN_POINT('Ctrl Pts',(0.0746338391269334,2.74898537698633,
12.5369868989719));
#422820=CARTESIAN_POINT('Origin',(0.0737669000743652,2.72700246506185,12.5369868989719));
#422821=CARTESIAN_POINT('Ctrl Pts',(0.0317307692307695,2.68331575103722,
13.8235269408515));
#422822=CARTESIAN_POINT('Ctrl Pts',(0.0362721082597566,2.69421496470679,
13.8362179249168));
#422823=CARTESIAN_POINT('Ctrl Pts',(0.0528913878732058,2.69028271990423,
13.8391868794938));
#422824=CARTESIAN_POINT('Ctrl Pts',(0.0275756416919826,2.67334344494414,
13.8400110824519));
#422825=CARTESIAN_POINT('Ctrl Pts',(0.0343745296800287,2.68076617927778,
13.8494522556837));
#422826=CARTESIAN_POINT('Ctrl Pts',(0.0459495068922318,2.67391433354299,
13.85569149686));
#422827=CARTESIAN_POINT('Ctrl Pts',(0.0157029524147764,2.66218831270049,
13.8586819406588));
#422828=CARTESIAN_POINT('Ctrl Pts',(0.0200567840833213,2.66220222086172,
13.868010383617));
#422829=CARTESIAN_POINT('Ctrl Pts',(0.0261406348414864,2.65550299502995,
13.8744918421245));
#422830=CARTESIAN_POINT('Ctrl Pts',(-0.0155871213907187,2.66213559464325,
13.8587686893867));
#422831=CARTESIAN_POINT('Ctrl Pts',(-0.0199022038181156,2.66212175395646,
13.8680909899357));
#422832=CARTESIAN_POINT('Ctrl Pts',(-0.0259481535750132,2.65541780787651,
13.8745789365162));
#422833=CARTESIAN_POINT('Ctrl Pts',(-0.0275688803167364,2.67332721762648,
13.8400379222776));
#422834=CARTESIAN_POINT('Ctrl Pts',(-0.0343713127316049,2.68074322377194,
13.8494748685453));
#422835=CARTESIAN_POINT('Ctrl Pts',(-0.0459415271867833,2.67389550570487,
13.8557104837033));
#422836=CARTESIAN_POINT('Ctrl Pts',(-0.0317307692368139,2.68331575103455,
13.8235269408542));
#422837=CARTESIAN_POINT('Ctrl Pts',(-0.0362721082658378,2.69421496470408,
13.8362179249195));
#422838=CARTESIAN_POINT('Ctrl Pts',(-0.0528913878792488,2.69028271990147,
13.8391868794965));
#422839=CARTESIAN_POINT('Origin',(0.0520384615384617,2.67485421257569,13.8235269408515));
#422840=CARTESIAN_POINT('Origin',(0.0737669000743654,2.72700246506185,14.));
#422841=CARTESIAN_POINT('Origin',(0.0737669000743653,2.72700246506185,13.7435492065112));
#422842=CARTESIAN_POINT('Ctrl Pts',(0.0454857618430532,2.7163277313308,
13.7902140241682));
#422843=CARTESIAN_POINT('Ctrl Pts',(0.0499232289341833,2.72698922659215,
13.8026027327198));
#422844=CARTESIAN_POINT('Ctrl Pts',(0.0661728417005767,2.72342159191127,
13.8057746032556));
#422845=CARTESIAN_POINT('Ctrl Pts',(0.0409022632877525,2.70532733480086,
13.8013225161808));
#422846=CARTESIAN_POINT('Ctrl Pts',(0.0453351949047153,2.71597792375946,
13.8136962270464));
#422847=CARTESIAN_POINT('Ctrl Pts',(0.0615645680922413,2.71242179507032,
13.8168830918628));
#422848=CARTESIAN_POINT('Ctrl Pts',(0.0363167887449816,2.69432219590103,
13.8124254880875));
#422849=CARTESIAN_POINT('Ctrl Pts',(0.0407432310975133,2.70495718923156,
13.8247886461868));
#422850=CARTESIAN_POINT('Ctrl Pts',(0.0569540009528616,2.70141720294686,
13.8279860620656));
#422851=CARTESIAN_POINT('Ctrl Pts',(0.0317292582190083,2.68331212264155,
13.8235227163065));
#422852=CARTESIAN_POINT('Ctrl Pts',(0.0361471208901607,2.69392650310656,
13.8358800595847));
#422853=CARTESIAN_POINT('Ctrl Pts',(0.0523410482444131,2.69040761867485,
13.8390832900376));
#422854=CARTESIAN_POINT('Origin',(0.0657949699454121,2.70786983275237,13.7902182540695));
#422855=CARTESIAN_POINT('Ctrl Pts',(0.0533554409592648,2.735214891466,13.7382347919292));
#422856=CARTESIAN_POINT('Ctrl Pts',(0.0591372501192909,2.74915363429203,
13.7369371795943));
#422857=CARTESIAN_POINT('Ctrl Pts',(0.0742812611866724,2.74870340567088,
13.7364597369711));
#422858=CARTESIAN_POINT('Ctrl Pts',(0.0540829631312669,2.73696094572446,
13.7595490285574));
#422859=CARTESIAN_POINT('Ctrl Pts',(0.0600036499999177,2.75123186978083,
13.7633824266926));
#422860=CARTESIAN_POINT('Ctrl Pts',(0.0750322024404344,2.75104141808081,
13.7648920890506));
#422861=CARTESIAN_POINT('Ctrl Pts',(0.0503726399036044,2.72805616466601,
13.7803806590111));
#422862=CARTESIAN_POINT('Ctrl Pts',(0.0554888357784383,2.74040207191393,
13.7901039518744));
#422863=CARTESIAN_POINT('Ctrl Pts',(0.0712002870186107,2.73912311086945,
13.7926933640891));
#422864=CARTESIAN_POINT('Ctrl Pts',(0.0439232699567853,2.71257766735968,
13.7936647693663));
#422865=CARTESIAN_POINT('Ctrl Pts',(0.0480553632782531,2.72257262292373,
13.8072068914933));
#422866=CARTESIAN_POINT('Ctrl Pts',(0.0645931722560378,2.71843195340523,
13.8104111085397));
#422867=CARTESIAN_POINT('Origin',(-0.187089956683836,2.67697359150001,12.5));
#422868=CARTESIAN_POINT('',(-0.187089956683836,2.67697359150001,12.5893111709658));
#422869=CARTESIAN_POINT('',(-0.187089956683836,2.67697359150001,13.8235269408515));
#422870=CARTESIAN_POINT('',(-0.187089956683836,2.67697359150001,12.5));
#422871=CARTESIAN_POINT('',(-0.176070301470241,2.71100063806851,13.7902182540695));
#422872=CARTESIAN_POINT('',(-0.187089956683836,2.67697359150001,13.8235269408515));
#422873=CARTESIAN_POINT('',(-0.16968438443307,2.73071939443562,13.7435492065112));
#422874=CARTESIAN_POINT('Origin',(-0.190694276985055,2.66584504699436,13.7445212918699));
#422875=CARTESIAN_POINT('',(-0.16968438443307,2.73071939443562,12.5369868989719));
#422876=CARTESIAN_POINT('',(-0.16968438443307,2.73071939443562,12.5));
#422877=CARTESIAN_POINT('Ctrl Pts',(-0.16968438443307,2.73071939443562,
12.5369868989719));
#422878=CARTESIAN_POINT('Ctrl Pts',(-0.175482010328069,2.71281719309701,
12.5544431401645));
#422879=CARTESIAN_POINT('Ctrl Pts',(-0.1812837828392,2.69490218762818,12.5718848856037));
#422880=CARTESIAN_POINT('Ctrl Pts',(-0.187089956683836,2.67697359150001,
12.5893111709658));
#422881=CARTESIAN_POINT('Origin',(-0.376448442621724,2.91618121445596,12.5));
#422882=CARTESIAN_POINT('',(-0.276247037758877,2.72200455098751,13.7435492065112));
#422883=CARTESIAN_POINT('',(-0.266742146417875,2.703585367247,13.7902182540695));
#422884=CARTESIAN_POINT('Origin',(-0.241764934750096,2.65518293585363,13.7418732680453));
#422885=CARTESIAN_POINT('',(-0.250340332111353,2.67180088696722,13.8235269408515));
#422886=CARTESIAN_POINT('',(-0.266742146417875,2.703585367247,13.7902182540695));
#422887=CARTESIAN_POINT('',(-0.250340332111353,2.67180088696722,12.5893111709658));
#422888=CARTESIAN_POINT('',(-0.250340332111353,2.67180088696722,12.5));
#422889=CARTESIAN_POINT('',(-0.276247037758877,2.72200455098751,12.5369868989719));
#422890=CARTESIAN_POINT('Ctrl Pts',(-0.250340332111353,2.67180088696722,
12.5893111709658));
#422891=CARTESIAN_POINT('Ctrl Pts',(-0.258982325294008,2.68854789170455,
12.5718848856037));
#422892=CARTESIAN_POINT('Ctrl Pts',(-0.267617767468175,2.70528220148044,
12.5544431401645));
#422893=CARTESIAN_POINT('Ctrl Pts',(-0.276247037758877,2.72200455098751,
12.5369868989719));
#422894=CARTESIAN_POINT('',(-0.276247037758877,2.72200455098751,12.5));
#422895=CARTESIAN_POINT('Origin',(-0.21979279117526,2.68756440078102,12.5));
#422896=CARTESIAN_POINT('',(-0.215876635126138,2.65341394113584,13.8587068136939));
#422897=CARTESIAN_POINT('Ctrl Pts',(-0.250340332117159,2.67180088696406,
13.8235269408542));
#422898=CARTESIAN_POINT('Ctrl Pts',(-0.249536772004133,2.67024369700394,
13.8262006681044));
#422899=CARTESIAN_POINT('Ctrl Pts',(-0.248560051181353,2.66872981310272,
13.8288634856214));
#422900=CARTESIAN_POINT('Ctrl Pts',(-0.247423382155456,2.66725743645065,
13.8314912288862));
#422901=CARTESIAN_POINT('Ctrl Pts',(-0.24625159363173,2.66573956799097,
13.8342001611531));
#422902=CARTESIAN_POINT('Ctrl Pts',(-0.244908912170735,2.66426382167543,
13.8368750301949));
#422903=CARTESIAN_POINT('Ctrl Pts',(-0.243365577123696,2.66283751664132,
13.8394886372969));
#422904=CARTESIAN_POINT('Ctrl Pts',(-0.243246381614405,2.6627273596438,
13.8396904925131));
#422905=CARTESIAN_POINT('Ctrl Pts',(-0.243125971626977,2.6626175109886,
13.8398919674349));
#422906=CARTESIAN_POINT('Ctrl Pts',(-0.243004324996858,2.66250798176036,
13.8400930404591));
#422907=CARTESIAN_POINT('Ctrl Pts',(-0.241108988659767,2.66080144269672,
13.8432258934518));
#422908=CARTESIAN_POINT('Ctrl Pts',(-0.238923872511486,2.6591803183025,
13.8462331177034));
#422909=CARTESIAN_POINT('Ctrl Pts',(-0.236462766213828,2.65777495436557,
13.8489036603661));
#422910=CARTESIAN_POINT('Ctrl Pts',(-0.235657463591899,2.65731510293036,
13.849777493004));
#422911=CARTESIAN_POINT('Ctrl Pts',(-0.234822725104269,2.65687857500021,
13.85061494757));
#422912=CARTESIAN_POINT('Ctrl Pts',(-0.23395936919549,2.65647056727925,
13.8514076489583));
#422913=CARTESIAN_POINT('Ctrl Pts',(-0.232133246933858,2.6556075721059,
13.8530843267192));
#422914=CARTESIAN_POINT('Ctrl Pts',(-0.229998457928146,2.65479007714677,
13.8546805203176));
#422915=CARTESIAN_POINT('Ctrl Pts',(-0.227630109492369,2.65419295193012,
13.8559412814274));
#422916=CARTESIAN_POINT('Ctrl Pts',(-0.227313147664311,2.65411303721091,
13.8561100121513));
#422917=CARTESIAN_POINT('Ctrl Pts',(-0.226992065096586,2.65403702499007,
13.8562727473908));
#422918=CARTESIAN_POINT('Ctrl Pts',(-0.226667097614289,2.65396528305557,
13.8564289040185));
#422919=CARTESIAN_POINT('Ctrl Pts',(-0.225193373789397,2.65363993420106,
13.8571370725437));
#422920=CARTESIAN_POINT('Ctrl Pts',(-0.223613357649691,2.65339891275393,
13.8577210840553));
#422921=CARTESIAN_POINT('Ctrl Pts',(-0.221984039041397,2.653280599691,13.8581177131616));
#422922=CARTESIAN_POINT('Ctrl Pts',(-0.221525166841861,2.65324727866026,
13.8582294175695));
#422923=CARTESIAN_POINT('Ctrl Pts',(-0.221062431392487,2.65322351941437,
13.8583265086086));
#422924=CARTESIAN_POINT('Ctrl Pts',(-0.220597197391072,2.65320974940297,
13.8584082369006));
#422925=CARTESIAN_POINT('Ctrl Pts',(-0.219928780888465,2.65318996558916,
13.8585256585398));
#422926=CARTESIAN_POINT('Ctrl Pts',(-0.219246887321347,2.65319087878083,
13.8586122832068));
#422927=CARTESIAN_POINT('Ctrl Pts',(-0.218569231365846,2.65321325494219,
13.8586682984299));
#422928=CARTESIAN_POINT('Ctrl Pts',(-0.218027173775319,2.6532311536532,
13.8587131050557));
#422929=CARTESIAN_POINT('Ctrl Pts',(-0.217481832815699,2.65326274859779,
13.8587357943552));
#422930=CARTESIAN_POINT('Ctrl Pts',(-0.216933172977939,2.65330854912843,
13.8587355499465));
#422931=CARTESIAN_POINT('Ctrl Pts',(-0.216578561044268,2.65333815110331,
13.8587353919793));
#422932=CARTESIAN_POINT('Ctrl Pts',(-0.216226394209478,2.65337332859157,
13.8587257282814));
#422933=CARTESIAN_POINT('Ctrl Pts',(-0.215876635126138,2.65341394113584,
13.8587068136939));
#422934=CARTESIAN_POINT('Ctrl Pts',(-0.215876635126138,2.65341394113584,
13.8587068136939));
#422935=CARTESIAN_POINT('Ctrl Pts',(-0.21472629656782,2.65354751357998,
13.8586446046466));
#422936=CARTESIAN_POINT('Ctrl Pts',(-0.213601970174342,2.65373980551323,
13.858482427929));
#422937=CARTESIAN_POINT('Ctrl Pts',(-0.212502602233195,2.65398647232433,
13.8582284286032));
#422938=CARTESIAN_POINT('Ctrl Pts',(-0.211374778609438,2.65423952377902,
13.8579678548414));
#422939=CARTESIAN_POINT('Ctrl Pts',(-0.210270802547482,2.65455191401367,
13.857615680862));
#422940=CARTESIAN_POINT('Ctrl Pts',(-0.209231559205508,2.65490200369315,
13.8571944833187));
#422941=CARTESIAN_POINT('Ctrl Pts',(-0.206638021160501,2.65577568829253,
13.8561433417727));
#422942=CARTESIAN_POINT('Ctrl Pts',(-0.204324791989813,2.65692048993979,
13.8546163505474));
#422943=CARTESIAN_POINT('Ctrl Pts',(-0.202344521073351,2.65813644386444,
13.8528973491086));
#422944=CARTESIAN_POINT('Ctrl Pts',(-0.201982754793105,2.65835858070673,
13.8525833129072));
#422945=CARTESIAN_POINT('Ctrl Pts',(-0.201631979407093,2.65858301952384,
13.8522628768811));
#422946=CARTESIAN_POINT('Ctrl Pts',(-0.201292350061553,2.65880847431043,
13.851937733538));
#422947=CARTESIAN_POINT('Ctrl Pts',(-0.199218280769687,2.66018529541175,
13.8499521282529));
#422948=CARTESIAN_POINT('Ctrl Pts',(-0.197356021225063,2.66174023370548,
13.847639871647));
#422949=CARTESIAN_POINT('Ctrl Pts',(-0.195751952356615,2.66332989773982,
13.8452109780794));
#422950=CARTESIAN_POINT('Ctrl Pts',(-0.195030248570126,2.66404512049328,
13.8441181685877));
#422951=CARTESIAN_POINT('Ctrl Pts',(-0.194360159582619,2.66476706910083,
13.8430021611332));
#422952=CARTESIAN_POINT('Ctrl Pts',(-0.193742625521376,2.66548228083695,
13.8418824960098));
#422953=CARTESIAN_POINT('Ctrl Pts',(-0.192287390736757,2.66716769555671,
13.8392439765549));
#422954=CARTESIAN_POINT('Ctrl Pts',(-0.191051575423354,2.66889379713922,
13.8364981347964));
#422955=CARTESIAN_POINT('Ctrl Pts',(-0.190004086953026,2.67064522939239,
13.8336931113419));
#422956=CARTESIAN_POINT('Ctrl Pts',(-0.188983899704597,2.67235101318074,
13.8309611966328));
#422957=CARTESIAN_POINT('Ctrl Pts',(-0.188141812403136,2.67408282348032,
13.8281701127185));
#422958=CARTESIAN_POINT('Ctrl Pts',(-0.187487856314965,2.67583299279055,
13.825358068512));
#422959=CARTESIAN_POINT('Ctrl Pts',(-0.187346077929281,2.67621243138584,
13.8247484142932));
#422960=CARTESIAN_POINT('Ctrl Pts',(-0.187213310689527,2.67659269278633,
13.8241378483365));
#422961=CARTESIAN_POINT('Ctrl Pts',(-0.187089956683836,2.67697359150001,
13.8235269408515));
#422962=CARTESIAN_POINT('',(-0.217112984834088,2.65329470919124,12.5969504640361));
#422963=CARTESIAN_POINT('Origin',(-0.219795292788959,2.68759739206378,12.584524458991));
#422964=CARTESIAN_POINT('Origin',(-0.219795292788959,2.68759739206378,12.584524458991));
#422965=CARTESIAN_POINT('Ctrl Pts',(-0.250340332111353,2.67180088696722,
12.5893111709658));
#422966=CARTESIAN_POINT('Ctrl Pts',(-0.245142862299359,2.66172889897511,
12.5770542771492));
#422967=CARTESIAN_POINT('Ctrl Pts',(-0.229456134336435,2.666390469598,12.5737548217797));
#422968=CARTESIAN_POINT('Ctrl Pts',(-0.261705454267471,2.69382494444632,
12.5663937883685));
#422969=CARTESIAN_POINT('Ctrl Pts',(-0.256501354360936,2.68374010823476,
12.5540940315304));
#422970=CARTESIAN_POINT('Ctrl Pts',(-0.240766931132422,2.68841920226884,
12.5508374392248));
#422971=CARTESIAN_POINT('Ctrl Pts',(-0.273059109154684,2.71582677992147,
12.5434499600945));
#422972=CARTESIAN_POINT('Ctrl Pts',(-0.267838088866063,2.70570915431606,
12.5311293540533));
#422973=CARTESIAN_POINT('Ctrl Pts',(-0.252067726634541,2.7104258734774,
12.5278936106989));
#422974=CARTESIAN_POINT('Ctrl Pts',(-0.284402195019786,2.73780813407251,
12.5204817579905));
#422975=CARTESIAN_POINT('Ctrl Pts',(-0.279155334248852,2.72764043313481,
12.5081597038247));
#422976=CARTESIAN_POINT('Ctrl Pts',(-0.263359310506878,2.7324121915987,
12.5049254088044));
#422977=CARTESIAN_POINT('Ctrl Pts',(-0.276247037758876,2.72200455098751,
12.5369868989719));
#422978=CARTESIAN_POINT('Ctrl Pts',(-0.276674202374231,2.72283233813534,
12.5342545179733));
#422979=CARTESIAN_POINT('Ctrl Pts',(-0.276971012474594,2.72367954582987,
12.5314872231885));
#422980=CARTESIAN_POINT('Ctrl Pts',(-0.277067991328621,2.72451693236666,
12.5287124745063));
#422981=CARTESIAN_POINT('Ctrl Pts',(-0.277155451672784,2.72527212910971,
12.5262100684184));
#422982=CARTESIAN_POINT('Ctrl Pts',(-0.277079317366856,2.72601868915766,
12.5237004536639));
#422983=CARTESIAN_POINT('Ctrl Pts',(-0.276772332580271,2.72676270589956,
12.5212220730815));
#422984=CARTESIAN_POINT('Ctrl Pts',(-0.276537309169838,2.72733231507807,
12.5193246583486));
#422985=CARTESIAN_POINT('Ctrl Pts',(-0.276163583575611,2.72790699916809,
12.517417831369));
#422986=CARTESIAN_POINT('Ctrl Pts',(-0.275560787361057,2.72845087546581,
12.5155812248347));
#422987=CARTESIAN_POINT('Ctrl Pts',(-0.275303992933616,2.72868256969198,
12.5147988205793));
#422988=CARTESIAN_POINT('Ctrl Pts',(-0.275005551530144,2.72890911378354,
12.5140295443047));
#422989=CARTESIAN_POINT('Ctrl Pts',(-0.274658763335797,2.72912984144627,
12.5132817086137));
#422990=CARTESIAN_POINT('Ctrl Pts',(-0.274133946316095,2.72946388290445,
12.5121499604604));
#422991=CARTESIAN_POINT('Ctrl Pts',(-0.273483228810673,2.72978578326946,
12.5110494206568));
#422992=CARTESIAN_POINT('Ctrl Pts',(-0.272680235564079,2.73006925100947,
12.5100666561695));
#422993=CARTESIAN_POINT('Ctrl Pts',(-0.272219158691014,2.73023201753301,
12.5095023550641));
#422994=CARTESIAN_POINT('Ctrl Pts',(-0.271702331443396,2.73038337780377,
12.5089719619137));
#422995=CARTESIAN_POINT('Ctrl Pts',(-0.271137646058283,2.7305143652184,
12.5085043804652));
#422996=CARTESIAN_POINT('Ctrl Pts',(-0.270311302552617,2.73070604823741,
12.5078201359221));
#422997=CARTESIAN_POINT('Ctrl Pts',(-0.26935823354364,2.73085848667329,
12.5072563000949));
#422998=CARTESIAN_POINT('Ctrl Pts',(-0.268341705953558,2.73095298770495,
12.5068768744332));
#422999=CARTESIAN_POINT('Ctrl Pts',(-0.267608719583111,2.73102112945426,
12.5066032824114));
#423000=CARTESIAN_POINT('Ctrl Pts',(-0.266829866632878,2.73106040416098,
12.5064197834844));
#423001=CARTESIAN_POINT('Ctrl Pts',(-0.266048770452628,2.73107120020104,
12.5063282718343));
#423002=CARTESIAN_POINT('Ctrl Pts',(-0.264908611850729,2.73108695907716,
12.5061946931565));
#423003=CARTESIAN_POINT('Ctrl Pts',(-0.263739318751798,2.73104343748753,
12.5062515701262));
#423004=CARTESIAN_POINT('Ctrl Pts',(-0.262612884346067,2.73095879028853,
12.5064436508398));
#423005=CARTESIAN_POINT('',(-0.229456134336435,2.666390469598,12.5737548217797));
#423006=CARTESIAN_POINT('Origin',(-0.230789905912253,2.68188953580805,12.5893111709658));
#423007=CARTESIAN_POINT('Ctrl Pts',(-0.262612884346068,2.73095879028853,
12.5064436508398));
#423008=CARTESIAN_POINT('Ctrl Pts',(-0.257704396527699,2.72140122077071,
12.5164271754438));
#423009=CARTESIAN_POINT('Ctrl Pts',(-0.252794148843822,2.71183976718331,
12.5264061185523));
#423010=CARTESIAN_POINT('Ctrl Pts',(-0.247882078471508,2.70227429316508,
12.536380305637));
#423011=CARTESIAN_POINT('Ctrl Pts',(-0.241742986781333,2.69031939072946,
12.5488460165097));
#423012=CARTESIAN_POINT('Ctrl Pts',(-0.235601046272685,2.6783582048664,
12.5613043021964));
#423013=CARTESIAN_POINT('Ctrl Pts',(-0.229456134336435,2.666390469598,12.5737548217797));
#423014=CARTESIAN_POINT('Ctrl Pts',(-0.187089956683836,2.67697359150001,
12.5893111709658));
#423015=CARTESIAN_POINT('Ctrl Pts',(-0.190581907283988,2.66619097050297,
12.5770542771492));
#423016=CARTESIAN_POINT('Ctrl Pts',(-0.206817591415412,2.66824188143219,
12.5737548217797));
#423017=CARTESIAN_POINT('Ctrl Pts',(-0.190347916222393,2.66691349989206,
12.5928319619712));
#423018=CARTESIAN_POINT('Ctrl Pts',(-0.195793993067713,2.66067061086804,
12.5821634970842));
#423019=CARTESIAN_POINT('Ctrl Pts',(-0.207995407513229,2.66457432548726,
12.5773203894503));
#423020=CARTESIAN_POINT('Ctrl Pts',(-0.201685168407197,2.65458261134995,
12.5969440695591));
#423021=CARTESIAN_POINT('Ctrl Pts',(-0.205690031010724,2.65423675288354,
12.5878292599214));
#423022=CARTESIAN_POINT('Ctrl Pts',(-0.212037741670697,2.66018072996003,
12.5813877129824));
#423023=CARTESIAN_POINT('Ctrl Pts',(-0.232175897796688,2.65203493263431,
12.596957478804));
#423024=CARTESIAN_POINT('Ctrl Pts',(-0.228200639098576,2.65237831497512,
12.5878468778671));
#423025=CARTESIAN_POINT('Ctrl Pts',(-0.222951293072859,2.65927482483445,
12.5814011370086));
#423026=CARTESIAN_POINT('Ctrl Pts',(-0.245484096960501,2.6623901652322,
12.5928371701607));
#423027=CARTESIAN_POINT('Ctrl Pts',(-0.239096787135805,2.65712354023063,
12.5821692192952));
#423028=CARTESIAN_POINT('Ctrl Pts',(-0.227692681624127,2.66295193618891,
12.5773318885715));
#423029=CARTESIAN_POINT('Ctrl Pts',(-0.2503403321114,2.67180088696719,12.5893111709658));
#423030=CARTESIAN_POINT('Ctrl Pts',(-0.245142862299407,2.66172889897508,
12.5770542771492));
#423031=CARTESIAN_POINT('Ctrl Pts',(-0.229456134336484,2.66639046959797,
12.5737548217797));
#423032=CARTESIAN_POINT('',(-0.206817591415412,2.66824188143219,12.5737548217797));
#423033=CARTESIAN_POINT('Origin',(-0.208019770758347,2.68375170943985,12.5893111709658));
#423034=CARTESIAN_POINT('Ctrl Pts',(-0.229456134336484,2.66639046959797,
12.5737548217797));
#423035=CARTESIAN_POINT('Ctrl Pts',(-0.229025861100665,2.66548538144008,
12.5746934679442));
#423036=CARTESIAN_POINT('Ctrl Pts',(-0.228384294120895,2.66456249073761,
12.5756680099006));
#423037=CARTESIAN_POINT('Ctrl Pts',(-0.227607159734381,2.66372489548137,
12.5765688348656));
#423038=CARTESIAN_POINT('Ctrl Pts',(-0.227401422008713,2.66350315140976,
12.5768073183026));
#423039=CARTESIAN_POINT('Ctrl Pts',(-0.227186408154502,2.66328726168631,
12.5770407398754));
#423040=CARTESIAN_POINT('Ctrl Pts',(-0.22696393294672,2.66307875287396,
12.5772674179684));
#423041=CARTESIAN_POINT('Ctrl Pts',(-0.226050954853818,2.66222308909126,
12.5781976435658));
#423042=CARTESIAN_POINT('Ctrl Pts',(-0.224952754580903,2.66145135491207,
12.5790594849312));
#423043=CARTESIAN_POINT('Ctrl Pts',(-0.223715720067288,2.66085516841792,
12.5797571720116));
#423044=CARTESIAN_POINT('Ctrl Pts',(-0.222909747601871,2.66046673148003,
12.580211740231));
#423045=CARTESIAN_POINT('Ctrl Pts',(-0.222000062409363,2.6601520732037,
12.5806009430798));
#423046=CARTESIAN_POINT('Ctrl Pts',(-0.221044910878422,2.65995008751792,
12.5808812374708));
#423047=CARTESIAN_POINT('Ctrl Pts',(-0.220224118845122,2.65977651480578,
12.5811221033394));
#423048=CARTESIAN_POINT('Ctrl Pts',(-0.219352924732026,2.65968270345249,
12.581287365893));
#423049=CARTESIAN_POINT('Ctrl Pts',(-0.218479607454537,2.65968223837908,
12.581359338449));
#423050=CARTESIAN_POINT('Ctrl Pts',(-0.218358234386279,2.65968217374348,
12.5813693411482));
#423051=CARTESIAN_POINT('Ctrl Pts',(-0.218236800382204,2.65968385565078,
12.5813775999465));
#423052=CARTESIAN_POINT('Ctrl Pts',(-0.21811541360772,2.65968726309347,
12.5813841266931));
#423053=CARTESIAN_POINT('Ctrl Pts',(-0.217909466263382,2.65969304423211,
12.5813952001081));
#423054=CARTESIAN_POINT('Ctrl Pts',(-0.217702292618593,2.65970443971438,
12.5814007534795));
#423055=CARTESIAN_POINT('Ctrl Pts',(-0.217493993735289,2.65972164148933,
12.5814005856065));
#423056=CARTESIAN_POINT('Ctrl Pts',(-0.216540482887111,2.65980038448957,
12.5813998171494));
#423057=CARTESIAN_POINT('Ctrl Pts',(-0.215629245722708,2.65999501858446,
12.58127954464));
#423058=CARTESIAN_POINT('Ctrl Pts',(-0.214759274980914,2.66027550212328,
12.5810700125799));
#423059=CARTESIAN_POINT('Ctrl Pts',(-0.213708449378927,2.66061429430257,
12.5808169217085));
#423060=CARTESIAN_POINT('Ctrl Pts',(-0.212722871508912,2.66109429911671,
12.5804173076348));
#423061=CARTESIAN_POINT('Ctrl Pts',(-0.211877512841454,2.66165003654662,
12.5799304713245));
#423062=CARTESIAN_POINT('Ctrl Pts',(-0.210829847137029,2.66233877029763,
12.5793271277669));
#423063=CARTESIAN_POINT('Ctrl Pts',(-0.209914867227887,2.66315963848088,
12.5785808224116));
#423064=CARTESIAN_POINT('Ctrl Pts',(-0.209149961102918,2.66405443146419,
12.5777485681082));
#423065=CARTESIAN_POINT('Ctrl Pts',(-0.208010167174992,2.66538777104121,
12.576508418016));
#423066=CARTESIAN_POINT('Ctrl Pts',(-0.20720797460534,2.66686956272427,
12.5750928681475));
#423067=CARTESIAN_POINT('Ctrl Pts',(-0.206817591415412,2.66824188143219,
12.5737548217797));
#423068=CARTESIAN_POINT('Ctrl Pts',(-0.206817591415412,2.66824188143219,
12.5737548217797));
#423069=CARTESIAN_POINT('Ctrl Pts',(-0.190581907283988,2.66619097050297,
12.5770542771492));
#423070=CARTESIAN_POINT('Ctrl Pts',(-0.187089956683836,2.67697359150001,
12.5893111709658));
#423071=CARTESIAN_POINT('Ctrl Pts',(-0.199237369483173,2.69181209970925,
12.5508408821982));
#423072=CARTESIAN_POINT('Ctrl Pts',(-0.182951785236016,2.68975164578888,
12.55409748406));
#423073=CARTESIAN_POINT('Ctrl Pts',(-0.179455379801222,2.70054802264873,
12.5663972313419));
#423074=CARTESIAN_POINT('Ctrl Pts',(-0.191663429599364,2.71535893173455,
12.52790050457));
#423075=CARTESIAN_POINT('Ctrl Pts',(-0.175336276687888,2.71326719677367,
12.5311362602938));
#423076=CARTESIAN_POINT('Ctrl Pts',(-0.17182850495217,2.72409867107017,
12.5434568539655));
#423077=CARTESIAN_POINT('Ctrl Pts',(-0.184095270385093,2.73888419068029,
12.5049357605811));
#423078=CARTESIAN_POINT('Ctrl Pts',(-0.167733858256901,2.73674232743516,
12.5081700652078));
#423079=CARTESIAN_POINT('Ctrl Pts',(-0.164208728911819,2.74762739943244,
12.5204921097672));
#423080=CARTESIAN_POINT('Ctrl Pts',(-0.184592223874505,2.73733942947567,
12.5064436508395));
#423081=CARTESIAN_POINT('Ctrl Pts',(-0.183406494523313,2.73762734212962,
12.5062361689309));
#423082=CARTESIAN_POINT('Ctrl Pts',(-0.182161155794383,2.73787618559581,
12.5061871075061));
#423083=CARTESIAN_POINT('Ctrl Pts',(-0.180944118731537,2.73804892073635,
12.5063648335164));
#423084=CARTESIAN_POINT('Ctrl Pts',(-0.180391265427633,2.73812738769193,
12.5064455676329));
#423085=CARTESIAN_POINT('Ctrl Pts',(-0.179836510163696,2.73819102573722,
12.506574497099));
#423086=CARTESIAN_POINT('Ctrl Pts',(-0.179303519408695,2.73823606216183,
12.5067492519495));
#423087=CARTESIAN_POINT('Ctrl Pts',(-0.178232453797269,2.73832656460527,
12.5071004286051));
#423088=CARTESIAN_POINT('Ctrl Pts',(-0.177209831323526,2.73834447126128,
12.5076537929613));
#423089=CARTESIAN_POINT('Ctrl Pts',(-0.176312570764263,2.73829789513915,
12.5083435010505));
#423090=CARTESIAN_POINT('Ctrl Pts',(-0.176256082849997,2.73829496289392,
12.5083869222964));
#423091=CARTESIAN_POINT('Ctrl Pts',(-0.176200086260576,2.73829176283551,
12.5084308732337));
#423092=CARTESIAN_POINT('Ctrl Pts',(-0.176144597572335,2.7382882921679,
12.5084753333615));
#423093=CARTESIAN_POINT('Ctrl Pts',(-0.175699505054222,2.73826045283278,
12.5088319622689));
#423094=CARTESIAN_POINT('Ctrl Pts',(-0.175277975051939,2.73821592445867,
12.509227847131));
#423095=CARTESIAN_POINT('Ctrl Pts',(-0.17489224770224,2.7381588156663,12.5096423454524));
#423096=CARTESIAN_POINT('Ctrl Pts',(-0.173683548904055,2.73797986198629,
12.5109411997424));
#423097=CARTESIAN_POINT('Ctrl Pts',(-0.172750644107707,2.73767593645163,
12.5124831113042));
#423098=CARTESIAN_POINT('Ctrl Pts',(-0.172030535923296,2.73731765907553,
12.5140723025008));
#423099=CARTESIAN_POINT('Ctrl Pts',(-0.171963060997705,2.73728408809298,
12.5142212114565));
#423100=CARTESIAN_POINT('Ctrl Pts',(-0.171897428185298,2.73725005366185,
12.5143705582413));
#423101=CARTESIAN_POINT('Ctrl Pts',(-0.171833571401274,2.7372156231063,
12.5145201959299));
#423102=CARTESIAN_POINT('Ctrl Pts',(-0.171013235937672,2.73677331135852,
12.5164425148273));
#423103=CARTESIAN_POINT('Ctrl Pts',(-0.170452798506902,2.73625992294265,
12.518463520594));
#423104=CARTESIAN_POINT('Ctrl Pts',(-0.170065957298328,2.73570172525353,
12.5205025929157));
#423105=CARTESIAN_POINT('Ctrl Pts',(-0.169841574064402,2.73537794846895,
12.5216853356836));
#423106=CARTESIAN_POINT('Ctrl Pts',(-0.169675604465496,2.73503995609214,
12.5228750347131));
#423107=CARTESIAN_POINT('Ctrl Pts',(-0.169553256800397,2.73469843171908,
12.5240609649613));
#423108=CARTESIAN_POINT('Ctrl Pts',(-0.169252961020137,2.73386017846754,
12.5269717671326));
#423109=CARTESIAN_POINT('Ctrl Pts',(-0.169216792314183,2.73297354956384,
12.5299036066169));
#423110=CARTESIAN_POINT('Ctrl Pts',(-0.169359859620749,2.73205595277224,
12.5328133004019));
#423111=CARTESIAN_POINT('Ctrl Pts',(-0.169428540258459,2.73161545288222,
12.5342101228451));
#423112=CARTESIAN_POINT('Ctrl Pts',(-0.169538959021474,2.73116844661443,
12.5356023438238));
#423113=CARTESIAN_POINT('Ctrl Pts',(-0.16968438443307,2.73071939443562,
12.5369868989719));
#423114=CARTESIAN_POINT('Origin',(3.76220301131683,14.8546061023375,-1.24025450174292));
#423115=CARTESIAN_POINT('Ctrl Pts',(-0.276227907241606,2.72196739208225,
12.5369868989719));
#423116=CARTESIAN_POINT('Ctrl Pts',(-0.283236056069593,2.73561177384507,
12.5369868989719));
#423117=CARTESIAN_POINT('Ctrl Pts',(-0.298462078249489,2.73375393847501,
12.5369868989719));
#423118=CARTESIAN_POINT('Ctrl Pts',(-0.27859699452973,2.7265796964954,12.5218025310015));
#423119=CARTESIAN_POINT('Ctrl Pts',(-0.286729473143964,2.7351539985249,
12.5216901060417));
#423120=CARTESIAN_POINT('Ctrl Pts',(-0.298415666285335,2.73375961814326,
12.5161920673678));
#423121=CARTESIAN_POINT('Ctrl Pts',(-0.275848331416576,2.73194448188581,
12.5042015548895));
#423122=CARTESIAN_POINT('Ctrl Pts',(-0.281065081397688,2.7357078400473,
12.4980677368514));
#423123=CARTESIAN_POINT('Ctrl Pts',(-0.287825247336383,2.73500717164852,
12.4907278922777));
#423124=CARTESIAN_POINT('Ctrl Pts',(-0.262610969834461,2.73093888104572,
12.506463626192));
#423125=CARTESIAN_POINT('Ctrl Pts',(-0.263237240060458,2.73745157817826,
12.4999376786891));
#423126=CARTESIAN_POINT('Ctrl Pts',(-0.263229591080243,2.73737203505225,
12.4906970594712));
#423127=CARTESIAN_POINT('Origin',(-0.295797463957976,2.71191590214668,12.5369868989719));
#423128=CARTESIAN_POINT('Origin',(-0.295797463957976,2.71191590214668,14.));
#423129=CARTESIAN_POINT('Origin',(-0.295797463957976,2.71191590214668,13.7435492065112));
#423130=CARTESIAN_POINT('Ctrl Pts',(-0.264892698511088,2.70000133010642,
13.793642941384));
#423131=CARTESIAN_POINT('Ctrl Pts',(-0.269826750035054,2.70962221128044,
13.8071662555867));
#423132=CARTESIAN_POINT('Ctrl Pts',(-0.285958045415463,2.70416321018274,
13.8103758687955));
#423133=CARTESIAN_POINT('Ctrl Pts',(-0.272514726133809,2.7147717871116,
13.7804579775006));
#423134=CARTESIAN_POINT('Ctrl Pts',(-0.27861192310825,2.72663845727571,
13.7901904343351));
#423135=CARTESIAN_POINT('Ctrl Pts',(-0.294157150779669,2.72406905641006,
13.7927914348262));
#423136=CARTESIAN_POINT('Ctrl Pts',(-0.277002100678258,2.72346771100792,
13.7597120340895));
#423137=CARTESIAN_POINT('Ctrl Pts',(-0.284063371622543,2.73719817140167,
13.7635825532445));
#423138=CARTESIAN_POINT('Ctrl Pts',(-0.299015789751427,2.73579777565649,
13.7651073818885));
#423139=CARTESIAN_POINT('Ctrl Pts',(-0.276123369993984,2.72176484999464,
13.7381884353898));
#423140=CARTESIAN_POINT('Ctrl Pts',(-0.283018559412648,2.73517433445553,
13.7368803041982));
#423141=CARTESIAN_POINT('Ctrl Pts',(-0.298064780470721,2.73350075476201,
13.7363986145813));
#423142=CARTESIAN_POINT('Origin',(-0.286292572616974,2.69349671840617,13.7902182540695));
#423143=CARTESIAN_POINT('Ctrl Pts',(-0.25033852774379,2.67179738869388,
13.8235227101244));
#423144=CARTESIAN_POINT('Ctrl Pts',(-0.255606857224329,2.6820163608929,
13.8358800583119));
#423145=CARTESIAN_POINT('Ctrl Pts',(-0.27146008517196,2.67718922792421,
13.8390832900376));
#423146=CARTESIAN_POINT('Ctrl Pts',(-0.25580821681952,2.6823969005086,13.8124254819053));
#423147=CARTESIAN_POINT('Ctrl Pts',(-0.261086777568463,2.69263571767931,
13.8247886449158));
#423148=CARTESIAN_POINT('Ctrl Pts',(-0.276955071986918,2.68778618024237,
13.8279860620657));
#423149=CARTESIAN_POINT('Ctrl Pts',(-0.261275454558501,2.69299166196687,
13.8013225099955));
#423150=CARTESIAN_POINT('Ctrl Pts',(-0.266561754161049,2.70324549395033,
13.8136962257787));
#423151=CARTESIAN_POINT('Ctrl Pts',(-0.282447274264371,2.69837835146943,
13.8168830918626));
#423152=CARTESIAN_POINT('Ctrl Pts',(-0.26674033633855,2.70358185789793,
13.7902140179785));
#423153=CARTESIAN_POINT('Ctrl Pts',(-0.27203204528012,2.71384619022022,
13.802602731458));
#423154=CARTESIAN_POINT('Ctrl Pts',(-0.287936799781886,2.70896593031318,
13.8057746032558));
#423155=CARTESIAN_POINT('Origin',(-0.269890758310452,2.66171223812639,13.8235269408515));
#423156=CARTESIAN_POINT('Ctrl Pts',(-0.187089956683836,2.67697359150001,
13.8235269408515));
#423157=CARTESIAN_POINT('Ctrl Pts',(-0.183452115683267,2.68820670022581,
13.8362179249168));
#423158=CARTESIAN_POINT('Ctrl Pts',(-0.166567620895153,2.68564216521781,
13.8391868794938));
#423159=CARTESIAN_POINT('Ctrl Pts',(-0.190418422853553,2.66669578596405,
13.8400110824519));
#423160=CARTESIAN_POINT('Ctrl Pts',(-0.184247179361899,2.67464799425036,
13.8494522556837));
#423161=CARTESIAN_POINT('Ctrl Pts',(-0.172152227894695,2.66876241556666,
13.85569149686));
#423162=CARTESIAN_POINT('Ctrl Pts',(-0.201342359899562,2.65461003710596,
13.8586819406588));
#423163=CARTESIAN_POINT('Ctrl Pts',(-0.197004148890986,2.65497877668892,
13.868010383617));
#423164=CARTESIAN_POINT('Ctrl Pts',(-0.19039449254647,2.64879773229496,
13.8744918421245));
#423165=CARTESIAN_POINT('Ctrl Pts',(-0.232524021554646,2.65200706296568,
13.8587686893867));
#423166=CARTESIAN_POINT('Ctrl Pts',(-0.236823617756771,2.65164154905553,
13.8680909899357));
#423167=CARTESIAN_POINT('Ctrl Pts',(-0.242303016272693,2.64446710877009,
13.8745789365163));
#423168=CARTESIAN_POINT('Ctrl Pts',(-0.245378133337349,2.66218482216098,
13.8400379222776));
#423169=CARTESIAN_POINT('Ctrl Pts',(-0.252762404567227,2.66902169076523,
13.8494748685453));
#423170=CARTESIAN_POINT('Ctrl Pts',(-0.263735967494693,2.66125367802444,
13.8557104837033));
#423171=CARTESIAN_POINT('Ctrl Pts',(-0.250340332117159,2.67180088696406,
13.8235269408542));
#423172=CARTESIAN_POINT('Ctrl Pts',(-0.255754947312626,2.68229367310862,
13.8362179249195));
#423173=CARTESIAN_POINT('Ctrl Pts',(-0.271998413187523,2.67701988695185,
13.8391868794965));
#423174=CARTESIAN_POINT('Origin',(-0.166160142609325,2.67019547356017,13.8235269408515));
#423175=CARTESIAN_POINT('Ctrl Pts',(-0.176071515536958,2.71099688674549,
13.7902140241682));
#423176=CARTESIAN_POINT('Ctrl Pts',(-0.172517824591793,2.72198460152422,
13.8026027327198));
#423177=CARTESIAN_POINT('Ctrl Pts',(-0.156031485724598,2.71975333214794,
13.8057746032556));
#423178=CARTESIAN_POINT('Ctrl Pts',(-0.17974312843904,2.69965949544416,
13.8013225161808));
#423179=CARTESIAN_POINT('Ctrl Pts',(-0.176193068911704,2.71063597052669,
13.8136962270464));
#423180=CARTESIAN_POINT('Ctrl Pts',(-0.159727840122992,2.70841451914335,
13.8168830918628));
#423181=CARTESIAN_POINT('Ctrl Pts',(-0.183416324206491,2.68831721649143,
13.8124254880875));
#423182=CARTESIAN_POINT('Ctrl Pts',(-0.179871461162618,2.69927761890379,
13.8247886461867));
#423183=CARTESIAN_POINT('Ctrl Pts',(-0.16342608956085,2.69707073986811,
13.8279860620656));
#423184=CARTESIAN_POINT('Ctrl Pts',(-0.187091166919895,2.67696985201606,
13.8235227163065));
#423185=CARTESIAN_POINT('Ctrl Pts',(-0.183553174869323,2.68790901082681,
13.8358800595848));
#423186=CARTESIAN_POINT('Ctrl Pts',(-0.167126309723535,2.68572179060922,
13.8390832900376));
#423187=CARTESIAN_POINT('Origin',(-0.15514048739573,2.70422252012867,13.7902182540695));
#423188=CARTESIAN_POINT('Ctrl Pts',(-0.169767501019668,2.73046265331991,
13.7382347919292));
#423189=CARTESIAN_POINT('Ctrl Pts',(-0.165141067293955,2.74482628725131,
13.7369371795942));
#423190=CARTESIAN_POINT('Ctrl Pts',(-0.150010748861761,2.74561193422088,
13.7364597369711));
#423191=CARTESIAN_POINT('Ctrl Pts',(-0.169184719249316,2.73226219753788,
13.7595490285574));
#423192=CARTESIAN_POINT('Ctrl Pts',(-0.164446945773195,2.74696822721648,
13.7633824266926));
#423193=CARTESIAN_POINT('Ctrl Pts',(-0.149452876019529,2.74800337577097,
13.7648920890506));
#423194=CARTESIAN_POINT('Ctrl Pts',(-0.172156874358305,2.72308462061578,
13.780380659011));
#423195=CARTESIAN_POINT('Ctrl Pts',(-0.168064008257698,2.73580646533606,
13.7901039518743));
#423196=CARTESIAN_POINT('Ctrl Pts',(-0.152300588377005,2.73581238906302,
13.7926933640892));
#423197=CARTESIAN_POINT('Ctrl Pts',(-0.177323143332834,2.70713194320866,
13.7936647693663));
#423198=CARTESIAN_POINT('Ctrl Pts',(-0.174019480878138,2.71743044534879,
13.8072068914933));
#423199=CARTESIAN_POINT('Ctrl Pts',(-0.157199197089587,2.71465153852775,
13.8104111085397));
#423200=CARTESIAN_POINT('Origin',(-0.148754570358559,2.72394127649578,13.7435492065112));
#423201=CARTESIAN_POINT('Origin',(-0.148754570358559,2.72394127649578,14.));
#423202=CARTESIAN_POINT('Origin',(-0.148754570358559,2.72394127649578,12.5369868989719));
#423203=CARTESIAN_POINT('Ctrl Pts',(-0.184590987022074,2.73732108789479,
12.506462012331));
#423204=CARTESIAN_POINT('Ctrl Pts',(-0.18503091927362,2.7438448941154,12.4999388158272));
#423205=CARTESIAN_POINT('Ctrl Pts',(-0.185025714298148,2.74376770893236,
12.4907030323752));
#423206=CARTESIAN_POINT('Ctrl Pts',(-0.171692807979739,2.74046203688297,
12.5042014951932));
#423207=CARTESIAN_POINT('Ctrl Pts',(-0.167159496226433,2.74502166204993,
12.4980716682127));
#423208=CARTESIAN_POINT('Ctrl Pts',(-0.160380199250707,2.74542994839683,
12.4907355092744));
#423209=CARTESIAN_POINT('Ctrl Pts',(-0.168107641546659,2.73561721667034,
12.5218047446509));
#423210=CARTESIAN_POINT('Ctrl Pts',(-0.161478665375871,2.74539349131174,
12.5216906929434));
#423211=CARTESIAN_POINT('Ctrl Pts',(-0.149727336606756,2.74591982437135,
12.5161988840775));
#423212=CARTESIAN_POINT('Ctrl Pts',(-0.169696188384732,2.73068283673402,
12.5369868989719));
#423213=CARTESIAN_POINT('Ctrl Pts',(-0.164998580303643,2.74527523235082,
12.5369868989719));
#423214=CARTESIAN_POINT('Ctrl Pts',(-0.149682327375411,2.74592170567534,
12.5369868989719));
#423215=CARTESIAN_POINT('Origin',(-4.19924629559645E-32,-1.71423978068635E-33,
12.5));
#423216=CARTESIAN_POINT('Origin',(0.250340332111317,2.67180088696722,12.5));
#423217=CARTESIAN_POINT('',(0.250340332111317,2.67180088696722,12.5893111709658));
#423218=CARTESIAN_POINT('',(0.250340332111317,2.67180088696722,13.8235269408515));
#423219=CARTESIAN_POINT('',(0.250340332111317,2.67180088696722,12.5));
#423220=CARTESIAN_POINT('',(0.266742146417839,2.703585367247,13.7902182540695));
#423221=CARTESIAN_POINT('',(0.250340332111317,2.67180088696722,13.8235269408515));
#423222=CARTESIAN_POINT('',(0.276247037758841,2.72200455098751,13.7435492065112));
#423223=CARTESIAN_POINT('Origin',(0.24497578139935,2.66140582933077,13.7445212918703));
#423224=CARTESIAN_POINT('',(0.276247037758841,2.72200455098751,12.5369868989719));
#423225=CARTESIAN_POINT('',(0.276247037758841,2.72200455098751,12.5));
#423226=CARTESIAN_POINT('Ctrl Pts',(0.276247037758841,2.72200455098751,
12.5369868989719));
#423227=CARTESIAN_POINT('Ctrl Pts',(0.267617767468139,2.70528220148044,
12.5544431401645));
#423228=CARTESIAN_POINT('Ctrl Pts',(0.258982325293973,2.68854789170455,
12.5718848856037));
#423229=CARTESIAN_POINT('Ctrl Pts',(0.250340332111317,2.67180088696722,
12.5893111709658));
#423230=CARTESIAN_POINT('Origin',(0.102363482435782,2.9385962674314,12.5));
#423231=CARTESIAN_POINT('',(0.169684384433034,2.73071939443562,13.7435492065112));
#423232=CARTESIAN_POINT('',(0.176070301470205,2.71100063806852,13.7902182540695));
#423233=CARTESIAN_POINT('Origin',(0.192851387736352,2.6591831544195,13.7418732680435));
#423234=CARTESIAN_POINT('',(0.187089956683801,2.67697359150002,13.8235269408515));
#423235=CARTESIAN_POINT('',(0.176070301470205,2.71100063806852,13.7902182540695));
#423236=CARTESIAN_POINT('',(0.187089956683801,2.67697359150002,12.5893111709658));
#423237=CARTESIAN_POINT('',(0.187089956683801,2.67697359150002,12.5));
#423238=CARTESIAN_POINT('',(0.169684384433034,2.73071939443562,12.5369868989719));
#423239=CARTESIAN_POINT('Ctrl Pts',(0.187089956683801,2.67697359150002,
12.5893111709658));
#423240=CARTESIAN_POINT('Ctrl Pts',(0.181283782839164,2.69490218762819,
12.5718848856037));
#423241=CARTESIAN_POINT('Ctrl Pts',(0.175482010328033,2.71281719309701,
12.5544431401645));
#423242=CARTESIAN_POINT('Ctrl Pts',(0.169684384433034,2.73071939443562,
12.5369868989719));
#423243=CARTESIAN_POINT('',(0.169684384433034,2.73071939443562,12.5));
#423244=CARTESIAN_POINT('Origin',(0.219792791175224,2.68756440078102,12.5));
#423245=CARTESIAN_POINT('',(0.2181082764625,2.6532314343732,13.8587068136939));
#423246=CARTESIAN_POINT('Ctrl Pts',(0.187089956677558,2.67697359149784,
13.8235269408542));
#423247=CARTESIAN_POINT('Ctrl Pts',(0.187629833256057,2.67530653339834,
13.8262006681044));
#423248=CARTESIAN_POINT('Ctrl Pts',(0.1883476058679,2.67365407144425,13.8288634856214));
#423249=CARTESIAN_POINT('Ctrl Pts',(0.189229945304323,2.67201657744458,
13.8314912288862));
#423250=CARTESIAN_POINT('Ctrl Pts',(0.190139546254182,2.67032849003059,
13.8342001611531));
#423251=CARTESIAN_POINT('Ctrl Pts',(0.191224613240091,2.66865419903748,
13.8368750301949));
#423252=CARTESIAN_POINT('Ctrl Pts',(0.192515700650559,2.66699609095406,
13.8394886372969));
#423253=CARTESIAN_POINT('Ctrl Pts',(0.192615414463006,2.66686803124477,
13.8396904925131));
#423254=CARTESIAN_POINT('Ctrl Pts',(0.192716376714451,2.66674007845698,
13.8398919674349));
#423255=CARTESIAN_POINT('Ctrl Pts',(0.19281861107592,2.66661223992683,13.8400930404591));
#423256=CARTESIAN_POINT('Ctrl Pts',(0.194411491207561,2.66462042962144,
13.8432258934518));
#423257=CARTESIAN_POINT('Ctrl Pts',(0.196304178538909,2.66266581673169,
13.8462331177034));
#423258=CARTESIAN_POINT('Ctrl Pts',(0.198504244718641,2.6608792555633,13.8489036603661));
#423259=CARTESIAN_POINT('Ctrl Pts',(0.199224131976106,2.66029467195774,
13.8497774930041));
#423260=CARTESIAN_POINT('Ctrl Pts',(0.199976853482409,2.65972831931982,
13.85061494757));
#423261=CARTESIAN_POINT('Ctrl Pts',(0.20076244600851,2.65918545828004,13.8514076489583));
#423262=CARTESIAN_POINT('Ctrl Pts',(0.202424087500611,2.65803722888861,
13.8530843267192));
#423263=CARTESIAN_POINT('Ctrl Pts',(0.204397687018218,2.65688374414613,
13.8546805203176));
#423264=CARTESIAN_POINT('Ctrl Pts',(0.206637547363053,2.65590975314353,
13.8559412814273));
#423265=CARTESIAN_POINT('Ctrl Pts',(0.206937313317593,2.6557794015601,13.8561100121513));
#423266=CARTESIAN_POINT('Ctrl Pts',(0.207241779320219,2.65565223109864,
13.8562727473908));
#423267=CARTESIAN_POINT('Ctrl Pts',(0.207550772436138,2.65552864297606,
13.8564289040185));
#423268=CARTESIAN_POINT('Ctrl Pts',(0.20895205269168,2.65496817225013,13.8571370725437));
#423269=CARTESIAN_POINT('Ctrl Pts',(0.210471914091406,2.65447363846428,
13.8577210840554));
#423270=CARTESIAN_POINT('Ctrl Pts',(0.212060360036008,2.65409217209711,
13.8581177131616));
#423271=CARTESIAN_POINT('Ctrl Pts',(0.212507721086649,2.65398473803844,
13.8582294175695));
#423272=CARTESIAN_POINT('Ctrl Pts',(0.21296044761595,2.65388611102624,13.8583265086086));
#423273=CARTESIAN_POINT('Ctrl Pts',(0.213417262509939,2.65379693456122,
13.8584082369006));
#423274=CARTESIAN_POINT('Ctrl Pts',(0.214073583012853,2.65366881189461,
13.8585256585398));
#423275=CARTESIAN_POINT('Ctrl Pts',(0.214746564272907,2.65355892152009,
13.8586122832068));
#423276=CARTESIAN_POINT('Ctrl Pts',(0.21541885144911,2.65347089743625,13.8586682984299));
#423277=CARTESIAN_POINT('Ctrl Pts',(0.215956614548388,2.65340048689472,
13.8587131050557));
#423278=CARTESIAN_POINT('Ctrl Pts',(0.216499842700019,2.65334305712858,
13.8587357943552));
#423279=CARTESIAN_POINT('Ctrl Pts',(0.217048653698843,2.65329910495289,
13.8587355499465));
#423280=CARTESIAN_POINT('Ctrl Pts',(0.217403363331688,2.65327069761387,
13.8587353919793));
#423281=CARTESIAN_POINT('Ctrl Pts',(0.217756566242839,2.65324818897368,
13.8587257282814));
#423282=CARTESIAN_POINT('Ctrl Pts',(0.2181082764625,2.6532314343732,13.8587068136939));
#423283=CARTESIAN_POINT('Ctrl Pts',(0.2181082764625,2.6532314343732,13.8587068136939));
#423284=CARTESIAN_POINT('Ctrl Pts',(0.219265032201073,2.65317632940561,
13.8586446046466));
#423285=CARTESIAN_POINT('Ctrl Pts',(0.220405661927858,2.65318339004639,
13.858482427929));
#423286=CARTESIAN_POINT('Ctrl Pts',(0.221530499458477,2.65324815821025,
13.8582284286032));
#423287=CARTESIAN_POINT('Ctrl Pts',(0.222684451918457,2.65331460281224,
13.8579678548414));
#423288=CARTESIAN_POINT('Ctrl Pts',(0.223824514827443,2.65344347238825,
13.857615680862));
#423289=CARTESIAN_POINT('Ctrl Pts',(0.224906830414324,2.65362005799896,
13.8571944833187));
#423290=CARTESIAN_POINT('Ctrl Pts',(0.227607859651537,2.65406074545018,
13.8561433417727));
#423291=CARTESIAN_POINT('Ctrl Pts',(0.230076354676476,2.65481449097715,
13.8546163505475));
#423292=CARTESIAN_POINT('Ctrl Pts',(0.232227876185974,2.65569254111439,
13.8528973491086));
#423293=CARTESIAN_POINT('Ctrl Pts',(0.232620927423026,2.65585294792005,
13.8525833129072));
#423294=CARTESIAN_POINT('Ctrl Pts',(0.233003507823617,2.656017411871,13.8522628768812));
#423295=CARTESIAN_POINT('Ctrl Pts',(0.23337525535784,2.6561846892573,13.851937733538));
#423296=CARTESIAN_POINT('Ctrl Pts',(0.235645465971667,2.65720622904672,
13.8499521282529));
#423297=CARTESIAN_POINT('Ctrl Pts',(0.237735621059127,2.65843793332097,
13.847639871647));
#423298=CARTESIAN_POINT('Ctrl Pts',(0.239576658290055,2.65974585174012,
13.8452109780794));
#423299=CARTESIAN_POINT('Ctrl Pts',(0.240404979047825,2.66033431130946,
13.8441181685877));
#423300=CARTESIAN_POINT('Ctrl Pts',(0.241183463630411,2.66093779353603,
13.8430021611332));
#423301=CARTESIAN_POINT('Ctrl Pts',(0.241908997030878,2.6615431673289,13.8418824960098));
#423302=CARTESIAN_POINT('Ctrl Pts',(0.243618735016232,2.66296974613057,
13.8392439765549));
#423303=CARTESIAN_POINT('Ctrl Pts',(0.245118579716688,2.66447212159511,
13.8364981347964));
#423304=CARTESIAN_POINT('Ctrl Pts',(0.246436715601507,2.66603008976617,
13.8336931113419));
#423305=CARTESIAN_POINT('Ctrl Pts',(0.247720496243951,2.66754745182466,
13.8309611966328));
#423306=CARTESIAN_POINT('Ctrl Pts',(0.248832772134196,2.66911943155766,
13.8281701127186));
#423307=CARTESIAN_POINT('Ctrl Pts',(0.249762399510772,2.67074009318812,
13.8253580685121));
#423308=CARTESIAN_POINT('Ctrl Pts',(0.2499639437293,2.67109145437867,13.8247484142933));
#423309=CARTESIAN_POINT('Ctrl Pts',(0.250156730223949,2.67144509153756,
13.8241378483365));
#423310=CARTESIAN_POINT('Ctrl Pts',(0.250340332111317,2.67180088696722,
13.8235269408515));
#423311=CARTESIAN_POINT('',(0.216868982438032,2.65331466404988,12.5969504640361));
#423312=CARTESIAN_POINT('Origin',(0.219795683097938,2.68759736014377,12.584524458991));
#423313=CARTESIAN_POINT('Origin',(0.219795683097938,2.68759736014377,12.584524458991));
#423314=CARTESIAN_POINT('Ctrl Pts',(0.187089956683801,2.67697359150002,
12.5893111709658));
#423315=CARTESIAN_POINT('Ctrl Pts',(0.190581907283952,2.66619097050298,
12.5770542771492));
#423316=CARTESIAN_POINT('Ctrl Pts',(0.206817591415377,2.66824188143219,
12.5737548217797));
#423317=CARTESIAN_POINT('Ctrl Pts',(0.179454232654721,2.70055156486539,
12.5663937883685));
#423318=CARTESIAN_POINT('Ctrl Pts',(0.182950637722834,2.68975518913778,
12.5540940315304));
#423319=CARTESIAN_POINT('Ctrl Pts',(0.199236230503856,2.69181564129295,
12.5508374392248));
#423320=CARTESIAN_POINT('Ctrl Pts',(0.171826212977586,2.72410574834465,
12.5434499600945));
#423321=CARTESIAN_POINT('Ctrl Pts',(0.175333986103709,2.71327426975484,
12.5311293540532));
#423322=CARTESIAN_POINT('Ctrl Pts',(0.191661153532608,2.71536600786211,
12.5278936106989));
#423323=CARTESIAN_POINT('Ctrl Pts',(0.164205294159946,2.74763800543221,
12.5204817579905));
#423324=CARTESIAN_POINT('Ctrl Pts',(0.167730428365766,2.73675291842571,
12.5081597038247));
#423325=CARTESIAN_POINT('Ctrl Pts',(0.184091858900337,2.73889479511617,
12.5049254088044));
#423326=CARTESIAN_POINT('Ctrl Pts',(0.169684384433034,2.73071939443562,
12.5369868989719));
#423327=CARTESIAN_POINT('Ctrl Pts',(0.169397391436294,2.73160558639595,
12.5342545179733));
#423328=CARTESIAN_POINT('Ctrl Pts',(0.169242176240853,2.73248976135401,
12.5314872231885));
#423329=CARTESIAN_POINT('Ctrl Pts',(0.169282541324984,2.73333177784442,
12.5287124745063));
#423330=CARTESIAN_POINT('Ctrl Pts',(0.169318944561396,2.73409115010943,
12.5262100684184));
#423331=CARTESIAN_POINT('Ctrl Pts',(0.169515365422786,2.73481542021301,
12.5237004536639));
#423332=CARTESIAN_POINT('Ctrl Pts',(0.169939156106387,2.73549967311065,
12.5212220730815));
#423333=CARTESIAN_POINT('Ctrl Pts',(0.170263604535504,2.73602352789638,
12.5193246583486));
#423334=CARTESIAN_POINT('Ctrl Pts',(0.170725736691472,2.73652985436569,
12.517417831369));
#423335=CARTESIAN_POINT('Ctrl Pts',(0.171408890154744,2.73696856389274,
12.5155812248347));
#423336=CARTESIAN_POINT('Ctrl Pts',(0.171699917202061,2.73715545650933,
12.5147988205793));
#423337=CARTESIAN_POINT('Ctrl Pts',(0.172031201066131,2.73733050078412,
12.5140295443047));
#423338=CARTESIAN_POINT('Ctrl Pts',(0.172409244280923,2.73749195071623,
12.5132817086137));
#423339=CARTESIAN_POINT('Ctrl Pts',(0.172981361545988,2.73773628334805,
12.5121499604604));
#423340=CARTESIAN_POINT('Ctrl Pts',(0.17367573375281,2.73794818038731,12.5110494206568));
#423341=CARTESIAN_POINT('Ctrl Pts',(0.174514113948424,2.73809741430203,
12.5100666561695));
#423342=CARTESIAN_POINT('Ctrl Pts',(0.174995509926128,2.73818310407221,
12.5095023550641));
#423343=CARTESIAN_POINT('Ctrl Pts',(0.175530062249885,2.73824848104504,
12.5089719619137));
#423344=CARTESIAN_POINT('Ctrl Pts',(0.176108526691945,2.73828598006134,
12.5085043804652));
#423345=CARTESIAN_POINT('Ctrl Pts',(0.176955034052607,2.73834085498711,
12.5078201359221));
#423346=CARTESIAN_POINT('Ctrl Pts',(0.177920206739881,2.73833641692304,
12.5072563000949));
#423347=CARTESIAN_POINT('Ctrl Pts',(0.178938581355058,2.73826450079449,
12.5068768744332));
#423348=CARTESIAN_POINT('Ctrl Pts',(0.179672899557749,2.73821264431509,
12.5066032824114));
#423349=CARTESIAN_POINT('Ctrl Pts',(0.180447784681282,2.73812485214003,
12.5064197834844));
#423350=CARTESIAN_POINT('Ctrl Pts',(0.181220256124129,2.73800859523801,
12.5063282718343));
#423351=CARTESIAN_POINT('Ctrl Pts',(0.18234782527957,2.73783889615328,12.5061946931565));
#423352=CARTESIAN_POINT('Ctrl Pts',(0.183494510145609,2.73760597063306,
12.5062515701262));
#423353=CARTESIAN_POINT('Ctrl Pts',(0.184592223874365,2.73733942947598,
12.5064436508398));
#423354=CARTESIAN_POINT('',(0.206817591415377,2.66824188143219,12.5737548217797));
#423355=CARTESIAN_POINT('Origin',(0.208019770758312,2.68375170943986,12.5893111709658));
#423356=CARTESIAN_POINT('Ctrl Pts',(0.184592223874365,2.73733942947598,
12.5064436508398));
#423357=CARTESIAN_POINT('Ctrl Pts',(0.187882613062957,2.72711134428183,
12.5164271754438));
#423358=CARTESIAN_POINT('Ctrl Pts',(0.191174107664169,2.71687914069164,
12.5264061185523));
#423359=CARTESIAN_POINT('Ctrl Pts',(0.194466747510725,2.70664267394882,
12.536380305637));
#423360=CARTESIAN_POINT('Ctrl Pts',(0.198581879499603,2.69384916669944,
12.5488460165097));
#423361=CARTESIAN_POINT('Ctrl Pts',(0.202698801546182,2.68104899664882,
12.5613043021964));
#423362=CARTESIAN_POINT('Ctrl Pts',(0.206817591415376,2.66824188143219,
12.5737548217797));
#423363=CARTESIAN_POINT('Ctrl Pts',(0.250340332111317,2.67180088696722,
12.5893111709658));
#423364=CARTESIAN_POINT('Ctrl Pts',(0.245142862299324,2.66172889897511,
12.5770542771492));
#423365=CARTESIAN_POINT('Ctrl Pts',(0.2294561343364,2.666390469598,12.5737548217797));
#423366=CARTESIAN_POINT('Ctrl Pts',(0.245491137981933,2.66240380977211,
12.5928319619712));
#423367=CARTESIAN_POINT('Ctrl Pts',(0.23910310553989,2.65712873082571,12.5821634970843));
#423368=CARTESIAN_POINT('Ctrl Pts',(0.227698078181869,2.66296301340908,
12.5773203894503));
#423369=CARTESIAN_POINT('Ctrl Pts',(0.23230105471023,2.65207880117041,12.5969440695591));
#423370=CARTESIAN_POINT('Ctrl Pts',(0.228293213077796,2.65238823290965,
12.5878292599214));
#423371=CARTESIAN_POINT('Ctrl Pts',(0.222995602221529,2.6592845807347,12.5813877129824));
#423372=CARTESIAN_POINT('Ctrl Pts',(0.20180153470467,2.65451899070645,12.596957478804));
#423373=CARTESIAN_POINT('Ctrl Pts',(0.205779763483049,2.65421192567137,
12.5878468778671));
#423374=CARTESIAN_POINT('Ctrl Pts',(0.212079876959397,2.66016390451229,
12.5814011370086));
#423375=CARTESIAN_POINT('Ctrl Pts',(0.190352646773942,2.66689889265637,
12.5928371701607));
#423376=CARTESIAN_POINT('Ctrl Pts',(0.195799384167996,2.66066446265324,
12.5821692192952));
#423377=CARTESIAN_POINT('Ctrl Pts',(0.207998932580136,2.6645625186441,12.5773318885715));
#423378=CARTESIAN_POINT('Ctrl Pts',(0.187089956683749,2.67697359149999,
12.5893111709658));
#423379=CARTESIAN_POINT('Ctrl Pts',(0.190581907283901,2.66619097050295,
12.5770542771492));
#423380=CARTESIAN_POINT('Ctrl Pts',(0.206817591415324,2.66824188143217,
12.5737548217797));
#423381=CARTESIAN_POINT('',(0.2294561343364,2.666390469598,12.5737548217797));
#423382=CARTESIAN_POINT('Origin',(0.230789905912218,2.68188953580805,12.5893111709658));
#423383=CARTESIAN_POINT('Ctrl Pts',(0.206817591415324,2.66824188143217,
12.5737548217797));
#423384=CARTESIAN_POINT('Ctrl Pts',(0.207095092157204,2.66727891052437,
12.5746934679442));
#423385=CARTESIAN_POINT('Ctrl Pts',(0.20757818658313,2.66626404343265,12.5756680099006));
#423386=CARTESIAN_POINT('Ctrl Pts',(0.208208905534819,2.66531131195319,
12.5765688348656));
#423387=CARTESIAN_POINT('Ctrl Pts',(0.208375881394991,2.66505908684108,
12.5768073183026));
#423388=CARTESIAN_POINT('Ctrl Pts',(0.208552961318769,2.66481113113779,
12.5770407398754));
#423389=CARTESIAN_POINT('Ctrl Pts',(0.208738602675104,2.66456924597966,
12.5772674179684));
#423390=CARTESIAN_POINT('Ctrl Pts',(0.209500424601951,2.66357661469922,
12.5781976435658));
#423391=CARTESIAN_POINT('Ctrl Pts',(0.210458644121863,2.66263670362128,
12.5790594849312));
#423392=CARTESIAN_POINT('Ctrl Pts',(0.211582375428402,2.66184745038285,
12.5797571720116));
#423393=CARTESIAN_POINT('Ctrl Pts',(0.21231452678039,2.66133322351899,12.580211740231));
#423394=CARTESIAN_POINT('Ctrl Pts',(0.213161000045717,2.66087494413759,
12.5806009430798));
#423395=CARTESIAN_POINT('Ctrl Pts',(0.214070642121469,2.66052045301169,
12.5808812374708));
#423396=CARTESIAN_POINT('Ctrl Pts',(0.214852326435155,2.66021582753334,
12.5811221033394));
#423397=CARTESIAN_POINT('Ctrl Pts',(0.21569670242707,2.65998171444748,12.581287365893));
#423398=CARTESIAN_POINT('Ctrl Pts',(0.216558339914664,2.65983936233677,
12.581359338449));
#423399=CARTESIAN_POINT('Ctrl Pts',(0.216678089733308,2.65981957833284,
12.5813693411482));
#423400=CARTESIAN_POINT('Ctrl Pts',(0.216798183449623,2.65980150776395,
12.5813775999465));
#423401=CARTESIAN_POINT('Ctrl Pts',(0.216918510922236,2.65978514747604,
12.5813841266931));
#423402=CARTESIAN_POINT('Ctrl Pts',(0.217122661032826,2.65975739026887,
12.5813952001081));
#423403=CARTESIAN_POINT('Ctrl Pts',(0.217328933346229,2.65973497356003,
12.5814007534795));
#423404=CARTESIAN_POINT('Ctrl Pts',(0.217537259330507,2.65971810316819,
12.5814005856065));
#423405=CARTESIAN_POINT('Ctrl Pts',(0.218490894236355,2.65964087711022,
12.5813998171494));
#423406=CARTESIAN_POINT('Ctrl Pts',(0.219421646708412,2.65968487070571,
12.58127954464));
#423407=CARTESIAN_POINT('Ctrl Pts',(0.220325629572498,2.65982027782726,
12.5810700125799));
#423408=CARTESIAN_POINT('Ctrl Pts',(0.221417537945624,2.65998383421276,
12.5808169217085));
#423409=CARTESIAN_POINT('Ctrl Pts',(0.222468009251053,2.66029732806586,
12.5804173076348));
#423410=CARTESIAN_POINT('Ctrl Pts',(0.223392429263112,2.66070833050984,
12.5799304713245));
#423411=CARTESIAN_POINT('Ctrl Pts',(0.224538076880387,2.66121769201706,
12.5793271277669));
#423412=CARTESIAN_POINT('Ctrl Pts',(0.225574270460432,2.66187899049208,
12.5785808224116));
#423413=CARTESIAN_POINT('Ctrl Pts',(0.226474395381594,2.66263761489803,
12.5777485681082));
#423414=CARTESIAN_POINT('Ctrl Pts',(0.227815680130172,2.6637680483764,12.576508418016));
#423415=CARTESIAN_POINT('Ctrl Pts',(0.228847969332114,2.66509981356379,
12.5750928681475));
#423416=CARTESIAN_POINT('Ctrl Pts',(0.2294561343364,2.666390469598,12.5737548217797));
#423417=CARTESIAN_POINT('Ctrl Pts',(0.2294561343364,2.666390469598,12.5737548217797));
#423418=CARTESIAN_POINT('Ctrl Pts',(0.245142862299325,2.66172889897512,
12.5770542771492));
#423419=CARTESIAN_POINT('Ctrl Pts',(0.250340332111317,2.67180088696722,
12.5893111709658));
#423420=CARTESIAN_POINT('Ctrl Pts',(0.24076523186447,2.68841589280098,12.5508408821982));
#423421=CARTESIAN_POINT('Ctrl Pts',(0.256499646385662,2.68373679841165,
12.5540974840599));
#423422=CARTESIAN_POINT('Ctrl Pts',(0.261703746838024,2.69382163568088,
12.5663972313419));
#423423=CARTESIAN_POINT('Ctrl Pts',(0.252064331109194,2.71041926118062,
12.52790050457));
#423424=CARTESIAN_POINT('Ctrl Pts',(0.267834679527419,2.70570254748252,
12.5311362602938));
#423425=CARTESIAN_POINT('Ctrl Pts',(0.27305569774653,2.71582016907758,12.5434568539655));
#423426=CARTESIAN_POINT('Ctrl Pts',(0.263354221384546,2.7324022823544,12.5049357605811));
#423427=CARTESIAN_POINT('Ctrl Pts',(0.279150229149263,2.72763054014779,
12.5081700652078));
#423428=CARTESIAN_POINT('Ctrl Pts',(0.284397082685404,2.73779822706545,
12.5204921097672));
#423429=CARTESIAN_POINT('Ctrl Pts',(0.262612884345878,2.73095879028825,
12.5064436508395));
#423430=CARTESIAN_POINT('Ctrl Pts',(0.263829637222359,2.73105022457152,
12.5062361689309));
#423431=CARTESIAN_POINT('Ctrl Pts',(0.265098859604712,2.73109342369852,
12.5061871075062));
#423432=CARTESIAN_POINT('Ctrl Pts',(0.266327790593432,2.73106612413663,
12.5063648335164));
#423433=CARTESIAN_POINT('Ctrl Pts',(0.266886046852116,2.73105372299171,
12.5064455676329));
#423434=CARTESIAN_POINT('Ctrl Pts',(0.26744377045444,2.73102638095292,12.506574497099));
#423435=CARTESIAN_POINT('Ctrl Pts',(0.267976996424862,2.7309842206763,12.5067492519495));
#423436=CARTESIAN_POINT('Ctrl Pts',(0.269048534710697,2.7308994979639,12.5071004286051));
#423437=CARTESIAN_POINT('Ctrl Pts',(0.270060478465309,2.73075101493638,
12.5076537929612));
#423438=CARTESIAN_POINT('Ctrl Pts',(0.270938249142587,2.73055927426686,
12.5083435010503));
#423439=CARTESIAN_POINT('Ctrl Pts',(0.270993510052408,2.73054720304584,
12.5083869222963));
#423440=CARTESIAN_POINT('Ctrl Pts',(0.271048242652624,2.73053494739878,
12.5084308732336));
#423441=CARTESIAN_POINT('Ctrl Pts',(0.27110243013287,2.73052250726006,12.5084753333615));
#423442=CARTESIAN_POINT('Ctrl Pts',(0.271537085244699,2.73042272092823,
12.508831962269));
#423443=CARTESIAN_POINT('Ctrl Pts',(0.271945779357663,2.73031029565999,
12.509227847131));
#423444=CARTESIAN_POINT('Ctrl Pts',(0.272317102529008,2.73019127421278,
12.5096423454524));
#423445=CARTESIAN_POINT('Ctrl Pts',(0.273480665007251,2.72981831367392,
12.5109411997424));
#423446=CARTESIAN_POINT('Ctrl Pts',(0.274351793159712,2.72936685179109,
12.5124831113042));
#423447=CARTESIAN_POINT('Ctrl Pts',(0.275004121363683,2.72889633463966,
12.5140723025008));
#423448=CARTESIAN_POINT('Ctrl Pts',(0.27506524523087,2.72885224666723,12.5142212114565));
#423449=CARTESIAN_POINT('Ctrl Pts',(0.275124476162666,2.72880800070374,
12.5143705582413));
#423450=CARTESIAN_POINT('Ctrl Pts',(0.275181890304338,2.72876365244157,
12.5145201959299));
#423451=CARTESIAN_POINT('Ctrl Pts',(0.275919460434837,2.72819393298635,
12.5164425148273));
#423452=CARTESIAN_POINT('Ctrl Pts',(0.276389037672122,2.72759630852435,
12.518463520594));
#423453=CARTESIAN_POINT('Ctrl Pts',(0.276680044914046,2.72698267543696,
12.5205025929157));
#423454=CARTESIAN_POINT('Ctrl Pts',(0.276848840648812,2.72662674392413,
12.5216853356836));
#423455=CARTESIAN_POINT('Ctrl Pts',(0.276957689226786,2.72626627653085,
12.5228750347131));
#423456=CARTESIAN_POINT('Ctrl Pts',(0.277022921633456,2.72590941159608,
12.5240609649613));
#423457=CARTESIAN_POINT('Ctrl Pts',(0.27718303107603,2.72503350575881,12.5269717671327));
#423458=CARTESIAN_POINT('Ctrl Pts',(0.27707466315077,2.72415278140866,12.5299036066169));
#423459=CARTESIAN_POINT('Ctrl Pts',(0.276784409273502,2.72327062223204,
12.532813300402));
#423460=CARTESIAN_POINT('Ctrl Pts',(0.276645070511438,2.72284713446068,
12.5342101228452));
#423461=CARTESIAN_POINT('Ctrl Pts',(0.276463491089403,2.72242400821456,
12.5356023438238));
#423462=CARTESIAN_POINT('Ctrl Pts',(0.276247037758841,2.72200455098751,
12.5369868989719));
#423463=CARTESIAN_POINT('Origin',(6.12570493509179,14.0459053753743,-1.24019187649867));
#423464=CARTESIAN_POINT('Ctrl Pts',(0.1696972233177,2.73067962102774,12.5369868989719));
#423465=CARTESIAN_POINT('Ctrl Pts',(0.164999081884238,2.74528135964877,
12.5369868989719));
#423466=CARTESIAN_POINT('Ctrl Pts',(0.149673521966447,2.74592207557002,
12.5369868989719));
#423467=CARTESIAN_POINT('Ctrl Pts',(0.168109004740274,2.7356155594723,12.5218025310016));
#423468=CARTESIAN_POINT('Ctrl Pts',(0.161477706116907,2.74539726393894,
12.5216901060418));
#423469=CARTESIAN_POINT('Ctrl Pts',(0.149720240040939,2.74592013893292,
12.5161920673678));
#423470=CARTESIAN_POINT('Ctrl Pts',(0.171692794521266,2.74046246797167,
12.5042015548894));
#423471=CARTESIAN_POINT('Ctrl Pts',(0.167156818137774,2.74502341779219,
12.4980677368513));
#423472=CARTESIAN_POINT('Ctrl Pts',(0.160372636189632,2.74543042518558,
12.4907278922777));
#423473=CARTESIAN_POINT('Ctrl Pts',(0.184590878169996,2.7373194737153,12.506463626192));
#423474=CARTESIAN_POINT('Ctrl Pts',(0.185031087393022,2.74384738717799,
12.4999376786891));
#423475=CARTESIAN_POINT('Ctrl Pts',(0.185025710877426,2.74376765820662,
12.4906970594712));
#423476=CARTESIAN_POINT('Origin',(0.148754570358523,2.72394127649578,12.5369868989719));
#423477=CARTESIAN_POINT('Origin',(0.148754570358523,2.72394127649578,14.));
#423478=CARTESIAN_POINT('Origin',(0.148754570358523,2.72394127649578,13.7435492065112));
#423479=CARTESIAN_POINT('Ctrl Pts',(0.177312854281905,2.7071637327667,13.793642941384));
#423480=CARTESIAN_POINT('Ctrl Pts',(0.174007527699429,2.71745844185384,
13.8071662555867));
#423481=CARTESIAN_POINT('Ctrl Pts',(0.157203619929424,2.71469292792477,
13.8103758687955));
#423482=CARTESIAN_POINT('Ctrl Pts',(0.172191951339028,2.72297632453001,
13.7804579775006));
#423483=CARTESIAN_POINT('Ctrl Pts',(0.16810382175015,2.735675965005,13.7901904343351));
#423484=CARTESIAN_POINT('Ctrl Pts',(0.152347685379907,2.73566643365103,
13.7927914348263));
#423485=CARTESIAN_POINT('Ctrl Pts',(0.169177083019134,2.7322857923841,13.7597120340895));
#423486=CARTESIAN_POINT('Ctrl Pts',(0.164440511054253,2.7469810969401,13.7635825532445));
#423487=CARTESIAN_POINT('Ctrl Pts',(0.149459242689212,2.74802872011601,
13.7651073818884));
#423488=CARTESIAN_POINT('Ctrl Pts',(0.16976746326803,2.73046278541545,13.7381884353898));
#423489=CARTESIAN_POINT('Ctrl Pts',(0.165142615086688,2.74481439473029,
13.7368803041982));
#423490=CARTESIAN_POINT('Ctrl Pts',(0.150024404328957,2.7456077046343,13.7363986145813));
#423491=CARTESIAN_POINT('Origin',(0.155140487395694,2.70422252012868,13.7902182540695));
#423492=CARTESIAN_POINT('Ctrl Pts',(0.187091168689846,2.67696984654341,
13.8235227101244));
#423493=CARTESIAN_POINT('Ctrl Pts',(0.183553181396909,2.68790901169596,
13.8358800583119));
#423494=CARTESIAN_POINT('Ctrl Pts',(0.1671263097235,2.68572179060922,13.8390832900376));
#423495=CARTESIAN_POINT('Ctrl Pts',(0.18341632597915,2.68831721101041,13.8124254819053));
#423496=CARTESIAN_POINT('Ctrl Pts',(0.179871467700373,2.69927761978102,
13.8247886449158));
#423497=CARTESIAN_POINT('Ctrl Pts',(0.163426089560844,2.69707073986799,
13.8279860620657));
#423498=CARTESIAN_POINT('Ctrl Pts',(0.179743130213438,2.69965948995776,
13.8013225099955));
#423499=CARTESIAN_POINT('Ctrl Pts',(0.176193075460045,2.71063597141044,
13.8136962257787));
#423500=CARTESIAN_POINT('Ctrl Pts',(0.159727840122876,2.7084145191436,13.8168830918626));
#423501=CARTESIAN_POINT('Ctrl Pts',(0.176071517312574,2.71099688125532,
13.7902140179785));
#423502=CARTESIAN_POINT('Ctrl Pts',(0.172517831151386,2.7219846024118,13.802602731458));
#423503=CARTESIAN_POINT('Ctrl Pts',(0.156031485724627,2.71975333214774,
13.8057746032558));
#423504=CARTESIAN_POINT('Origin',(0.16616014260929,2.67019547356017,13.8235269408515));
#423505=CARTESIAN_POINT('Ctrl Pts',(0.250340332111317,2.67180088696722,
13.8235269408515));
#423506=CARTESIAN_POINT('Ctrl Pts',(0.255754947306752,2.68229367311183,
13.8362179249168));
#423507=CARTESIAN_POINT('Ctrl Pts',(0.271998413181692,2.6770198869551,13.8391868794938));
#423508=CARTESIAN_POINT('Ctrl Pts',(0.245386194891663,2.6622004443687,13.8400110824519));
#423509=CARTESIAN_POINT('Ctrl Pts',(0.252767481898282,2.66904430767732,
13.8494522556836));
#423510=CARTESIAN_POINT('Ctrl Pts',(0.263745455291886,2.66127179279442,
13.85569149686));
#423511=CARTESIAN_POINT('Ctrl Pts',(0.232643764171567,2.65205016430416,
13.8586819406588));
#423512=CARTESIAN_POINT('Ctrl Pts',(0.236984242468656,2.65170914848714,
13.868010383617));
#423513=CARTESIAN_POINT('Ctrl Pts',(0.242501800617441,2.64453632346018,
13.8744918421245));
#423514=CARTESIAN_POINT('Ctrl Pts',(0.201453508494333,2.65454805315992,
13.8587686893867));
#423515=CARTESIAN_POINT('Ctrl Pts',(0.197151656003279,2.65488597780398,
13.8680909899357));
#423516=CARTESIAN_POINT('Ctrl Pts',(0.190579389803528,2.64869713958462,
13.8745789365163));
#423517=CARTESIAN_POINT('Ctrl Pts',(0.190423839053807,2.66667906152662,
13.8400379222776));
#423518=CARTESIAN_POINT('Ctrl Pts',(0.184248514519325,2.67462485291589,
13.8494748685453));
#423519=CARTESIAN_POINT('Ctrl Pts',(0.172158646404701,2.66874299995655,
13.8557104837033));
#423520=CARTESIAN_POINT('Ctrl Pts',(0.187089956677558,2.67697359149784,
13.8235269408542));
#423521=CARTESIAN_POINT('Ctrl Pts',(0.18345211567695,2.68820670022361,13.8362179249195));
#423522=CARTESIAN_POINT('Ctrl Pts',(0.166567620888867,2.68564216521555,
13.8391868794965));
#423523=CARTESIAN_POINT('Origin',(0.269890758310417,2.66171223812639,13.8235269408515));
#423524=CARTESIAN_POINT('Ctrl Pts',(0.266740338982597,2.70358186302666,
13.7902140241683));
#423525=CARTESIAN_POINT('Ctrl Pts',(0.27203205160835,2.71384618827866,13.8026027327198));
#423526=CARTESIAN_POINT('Ctrl Pts',(0.287936799781948,2.70896593031337,
13.8057746032556));
#423527=CARTESIAN_POINT('Ctrl Pts',(0.26127545720074,2.69299166709209,13.8013225161808));
#423528=CARTESIAN_POINT('Ctrl Pts',(0.26656176047881,2.7032454920144,13.8136962270464));
#423529=CARTESIAN_POINT('Ctrl Pts',(0.282447274264215,2.69837835146919,
13.8168830918628));
#423530=CARTESIAN_POINT('Ctrl Pts',(0.255808219459156,2.68239690562876,
13.8124254880875));
#423531=CARTESIAN_POINT('Ctrl Pts',(0.261086783876821,2.69263571575147,
13.8247886461868));
#423532=CARTESIAN_POINT('Ctrl Pts',(0.27695507198693,2.68778618024249,13.8279860620656));
#423533=CARTESIAN_POINT('Ctrl Pts',(0.250338530379399,2.67179739380624,
13.8235227163066));
#423534=CARTESIAN_POINT('Ctrl Pts',(0.25560686352397,2.68201635897472,13.8358800595847));
#423535=CARTESIAN_POINT('Ctrl Pts',(0.271460085171925,2.67718922792421,
13.8390832900376));
#423536=CARTESIAN_POINT('Origin',(0.286292572616938,2.69349671840617,13.7902182540695));
#423537=CARTESIAN_POINT('Ctrl Pts',(0.276123311281598,2.72176472578806,
13.7382347919292));
#423538=CARTESIAN_POINT('Ctrl Pts',(0.283022018889911,2.73518581747498,
13.7369371795942));
#423539=CARTESIAN_POINT('Ctrl Pts',(0.298078941697422,2.73350270946029,
13.7364597369711));
#423540=CARTESIAN_POINT('Ctrl Pts',(0.27699073231523,2.72344567038401,13.7595490285574));
#423541=CARTESIAN_POINT('Ctrl Pts',(0.284054931382105,2.73718651817309,
13.7633824266926));
#423542=CARTESIAN_POINT('Ctrl Pts',(0.299017953972554,2.73577173364322,
13.7648920890506));
#423543=CARTESIAN_POINT('Ctrl Pts',(0.272566932557813,2.71487294503796,
13.7803806590111));
#423544=CARTESIAN_POINT('Ctrl Pts',(0.278672410767457,2.72676075483776,
13.7901039518744));
#423545=CARTESIAN_POINT('Ctrl Pts',(0.29422733625131,2.72420542029655,13.7926933640892));
#423546=CARTESIAN_POINT('Ctrl Pts',(0.264877381131631,2.69997163467822,
13.7936647693663));
#423547=CARTESIAN_POINT('Ctrl Pts',(0.269810406920547,2.70959652888598,
13.8072068914933));
#423548=CARTESIAN_POINT('Ctrl Pts',(0.285955684697386,2.70412165214251,
13.8104111085397));
#423549=CARTESIAN_POINT('Origin',(0.29579746395794,2.71191590214668,13.7435492065112));
#423550=CARTESIAN_POINT('Origin',(0.29579746395794,2.71191590214668,14.));
#423551=CARTESIAN_POINT('Origin',(0.29579746395794,2.71191590214668,12.5369868989719));
#423552=CARTESIAN_POINT('Ctrl Pts',(0.262611124694406,2.73094049146263,
12.506462012331));
#423553=CARTESIAN_POINT('Ctrl Pts',(0.263237000882791,2.73744909092692,
12.4999388158272));
#423554=CARTESIAN_POINT('Ctrl Pts',(0.263229595946696,2.73737208565975,
12.4907030323752));
#423555=CARTESIAN_POINT('Ctrl Pts',(0.275848248095312,2.73194405871191,
12.5042014951932));
#423556=CARTESIAN_POINT('Ctrl Pts',(0.281062153627983,2.73570654276002,
12.4980716682129));
#423557=CARTESIAN_POINT('Ctrl Pts',(0.287817707302887,2.73500793001206,
12.4907355092744));
#423558=CARTESIAN_POINT('Ctrl Pts',(0.278598608864998,2.72658111018693,
12.5218047446509));
#423559=CARTESIAN_POINT('Ctrl Pts',(0.28672791366929,2.73515043188327,12.5216906929433));
#423560=CARTESIAN_POINT('Ctrl Pts',(0.298408612906582,2.73376046078403,
12.5161988840775));
#423561=CARTESIAN_POINT('Ctrl Pts',(0.276229450898405,2.72197039690782,
12.5369868989719));
#423562=CARTESIAN_POINT('Ctrl Pts',(0.283235555445726,2.73560564646888,
12.5369868989719));
#423563=CARTESIAN_POINT('Ctrl Pts',(0.298453329743572,2.73375500416414,
12.5369868989719));
#423564=CARTESIAN_POINT('Origin',(4.19924629559577E-32,-1.71423978068577E-33,
12.5));
#423565=CARTESIAN_POINT('Origin',(0.467283921384947,2.64250562881057,12.5));
#423566=CARTESIAN_POINT('',(0.467283921384947,2.64250562881057,12.5893111709658));
#423567=CARTESIAN_POINT('',(0.467283921384947,2.64250562881057,13.8235269408515));
#423568=CARTESIAN_POINT('',(0.467283921384947,2.64250562881057,12.5));
#423569=CARTESIAN_POINT('',(0.486221890222939,2.67284744872126,13.7902182540695));
#423570=CARTESIAN_POINT('',(0.467283921384947,2.64250562881057,13.8235269408515));
#423571=CARTESIAN_POINT('',(0.497196489292313,2.69043060726395,13.7435492065112));
#423572=CARTESIAN_POINT('Origin',(0.461089927072368,2.63258242055567,13.7445212918703));
#423573=CARTESIAN_POINT('',(0.497196489292313,2.69043060726395,12.5369868989719));
#423574=CARTESIAN_POINT('',(0.497196489292313,2.69043060726395,12.5));
#423575=CARTESIAN_POINT('Ctrl Pts',(0.497196489292313,2.69043060726395,
12.5369868989719));
#423576=CARTESIAN_POINT('Ctrl Pts',(0.487232905459094,2.6744672656343,12.5544431401645));
#423577=CARTESIAN_POINT('Ctrl Pts',(0.477262195405901,2.65849250659843,
12.5718848856037));
#423578=CARTESIAN_POINT('Ctrl Pts',(0.467283921384947,2.64250562881057,
12.5893111709658));
#423579=CARTESIAN_POINT('Origin',(0.341545752784778,2.92047475665393,12.5));
#423580=CARTESIAN_POINT('',(0.391698755050327,2.70780229831487,13.7435492065112));
#423581=CARTESIAN_POINT('',(0.396456161771436,2.6876286429604,13.7902182540695));
#423582=CARTESIAN_POINT('Origin',(0.40895780438952,2.63461576339665,13.7418732680443));
#423583=CARTESIAN_POINT('',(0.404665629804346,2.65281661438093,13.8235269408515));
#423584=CARTESIAN_POINT('',(0.396456161771436,2.6876286429604,13.7902182540695));
#423585=CARTESIAN_POINT('',(0.404665629804346,2.65281661438093,12.5893111709658));
#423586=CARTESIAN_POINT('',(0.404665629804346,2.65281661438093,12.5));
#423587=CARTESIAN_POINT('',(0.391698755050327,2.70780229831487,12.5369868989719));
#423588=CARTESIAN_POINT('Ctrl Pts',(0.404665629804346,2.65281661438093,
12.5893111709658));
#423589=CARTESIAN_POINT('Ctrl Pts',(0.400340122549613,2.67115881165471,
12.5718848856037));
#423590=CARTESIAN_POINT('Ctrl Pts',(0.396017894218406,2.68948710474141,
12.5544431401645));
#423591=CARTESIAN_POINT('Ctrl Pts',(0.391698755050327,2.70780229831487,
12.5369868989719));
#423592=CARTESIAN_POINT('',(0.391698755050327,2.70780229831487,12.5));
#423593=CARTESIAN_POINT('Origin',(0.438122897588471,2.66070659900838,12.5));
#423594=CARTESIAN_POINT('',(0.433645532464802,2.62662517630146,13.8587068136939));
#423595=CARTESIAN_POINT('Ctrl Pts',(0.404665629797947,2.65281661437927,
13.8235269408542));
#423596=CARTESIAN_POINT('Ctrl Pts',(0.405067829270345,2.65111109832496,
13.8262006681044));
#423597=CARTESIAN_POINT('Ctrl Pts',(0.405648522563066,2.64940562967036,
13.8288634856214));
#423598=CARTESIAN_POINT('Ctrl Pts',(0.406394455125075,2.64770166544159,
13.8314912288862));
#423599=CARTESIAN_POINT('Ctrl Pts',(0.40716343465713,2.64594505407748,13.8342001611531));
#423600=CARTESIAN_POINT('Ctrl Pts',(0.408108420912855,2.6441878911169,13.8368750301949));
#423601=CARTESIAN_POINT('Ctrl Pts',(0.409260061134546,2.64243006464152,
13.8394886372969));
#423602=CARTESIAN_POINT('Ctrl Pts',(0.409349005102356,2.64229430343894,
13.8396904925131));
#423603=CARTESIAN_POINT('Ctrl Pts',(0.40943920207018,2.64215854704271,13.8398919674349));
#423604=CARTESIAN_POINT('Ctrl Pts',(0.409530676228246,2.64202280083516,
13.8400930404591));
#423605=CARTESIAN_POINT('Ctrl Pts',(0.410955905151698,2.63990778359594,
13.8432258934518));
#423606=CARTESIAN_POINT('Ctrl Pts',(0.412682975625832,2.63780540293098,
13.8462331177034));
#423607=CARTESIAN_POINT('Ctrl Pts',(0.414730099945994,2.63584546057943,
13.8489036603661));
#423608=CARTESIAN_POINT('Ctrl Pts',(0.415399942847134,2.63520414463301,
13.8497774930041));
#423609=CARTESIAN_POINT('Ctrl Pts',(0.416103996736968,2.63457832269608,
13.85061494757));
#423610=CARTESIAN_POINT('Ctrl Pts',(0.416842727054327,2.63397323489766,
13.8514076489583));
#423611=CARTESIAN_POINT('Ctrl Pts',(0.418405248216396,2.63269338693728,
13.8530843267192));
#423612=CARTESIAN_POINT('Ctrl Pts',(0.420278261029477,2.63138287363743,
13.8546805203176));
#423613=CARTESIAN_POINT('Ctrl Pts',(0.422431279114987,2.63022955409759,
13.8559412814273));
#423614=CARTESIAN_POINT('Ctrl Pts',(0.422719422758868,2.63007520254012,
13.8561100121513));
#423615=CARTESIAN_POINT('Ctrl Pts',(0.423012510102785,2.62992363842213,
13.8562727473908));
#423616=CARTESIAN_POINT('Ctrl Pts',(0.423310401490274,2.62977527572134,
13.8564289040185));
#423617=CARTESIAN_POINT('Ctrl Pts',(0.424661335534045,2.62910245256584,
13.8571370725437));
#423618=CARTESIAN_POINT('Ctrl Pts',(0.42613583062577,2.62848568148658,13.8577210840554));
#423619=CARTESIAN_POINT('Ctrl Pts',(0.427687898097245,2.62797601132638,
13.8581177131616));
#423620=CARTESIAN_POINT('Ctrl Pts',(0.428125013717743,2.62783247066695,
13.8582294175695));
#423621=CARTESIAN_POINT('Ctrl Pts',(0.428568194819761,2.62769727041296,
13.8583265086086));
#423622=CARTESIAN_POINT('Ctrl Pts',(0.4290162209901,2.62757115602055,13.8584082369006));
#423623=CARTESIAN_POINT('Ctrl Pts',(0.429659914453921,2.62738996345757,
13.8585256585398));
#423624=CARTESIAN_POINT('Ctrl Pts',(0.430321699338655,2.62722558451386,
13.8586122832068));
#423625=CARTESIAN_POINT('Ctrl Pts',(0.430984574754729,2.62708305567682,
13.8586682984299));
#423626=CARTESIAN_POINT('Ctrl Pts',(0.431514809378862,2.62696904673562,
13.8587131050557));
#423627=CARTESIAN_POINT('Ctrl Pts',(0.43205154892454,2.62686752992485,13.8587357943552));
#423628=CARTESIAN_POINT('Ctrl Pts',(0.432594951289688,2.62677899080508,
13.8587355499465));
#423629=CARTESIAN_POINT('Ctrl Pts',(0.432946165193391,2.62672176586114,
13.8587353919793));
#423630=CARTESIAN_POINT('Ctrl Pts',(0.43329635818761,2.62667054280039,13.8587257282814));
#423631=CARTESIAN_POINT('Ctrl Pts',(0.433645532464802,2.62662517630146,
13.8587068136939));
#423632=CARTESIAN_POINT('Ctrl Pts',(0.433645532464802,2.62662517630146,
13.8587068136939));
#423633=CARTESIAN_POINT('Ctrl Pts',(0.434793947627904,2.62647596835956,
13.8586446046467));
#423634=CARTESIAN_POINT('Ctrl Pts',(0.435931357511387,2.62639003359478,
13.858482427929));
#423635=CARTESIAN_POINT('Ctrl Pts',(0.43705773144479,2.62636290154669,13.8582284286032));
#423636=CARTESIAN_POINT('Ctrl Pts',(0.438213260075057,2.62633506722148,
13.8579678548414));
#423637=CARTESIAN_POINT('Ctrl Pts',(0.439360033585576,2.62637058228371,
13.857615680862));
#423638=CARTESIAN_POINT('Ctrl Pts',(0.44045314122324,2.6264583615523,13.8571944833187));
#423639=CARTESIAN_POINT('Ctrl Pts',(0.443181103126918,2.62667742369442,
13.8561433417727));
#423640=CARTESIAN_POINT('Ctrl Pts',(0.445702821696192,2.62722745593441,
13.8546163505474));
#423641=CARTESIAN_POINT('Ctrl Pts',(0.447918753432971,2.62792721545549,
13.8528973491086));
#423642=CARTESIAN_POINT('Ctrl Pts',(0.448323571468247,2.62805505119599,
13.8525833129072));
#423643=CARTESIAN_POINT('Ctrl Pts',(0.448718284202914,2.62818778405236,
13.8522628768812));
#423644=CARTESIAN_POINT('Ctrl Pts',(0.449102429437782,2.62832420396178,
13.851937733538));
#423645=CARTESIAN_POINT('Ctrl Pts',(0.45144835108942,2.62915730142119,13.8499521282529));
#423646=CARTESIAN_POINT('Ctrl Pts',(0.453631946691186,2.63021454025739,
13.847639871647));
#423647=CARTESIAN_POINT('Ctrl Pts',(0.455573465515885,2.63136804506022,
13.8452109780794));
#423648=CARTESIAN_POINT('Ctrl Pts',(0.456446995022561,2.63188703074737,
13.8441181685877));
#423649=CARTESIAN_POINT('Ctrl Pts',(0.457272078665843,2.63242505121604,
13.8430021611332));
#423650=CARTESIAN_POINT('Ctrl Pts',(0.458044541497908,2.63296927296989,
13.8418824960098));
#423651=CARTESIAN_POINT('Ctrl Pts',(0.459864869887205,2.63425174543004,
13.8392439765549));
#423652=CARTESIAN_POINT('Ctrl Pts',(0.461482181525879,2.6356268705972,13.8364981347964));
#423653=CARTESIAN_POINT('Ctrl Pts',(0.462922920291689,2.6370722144461,13.8336931113419));
#423654=CARTESIAN_POINT('Ctrl Pts',(0.464326108354215,2.63847988756711,
13.8309611966328));
#423655=CARTESIAN_POINT('Ctrl Pts',(0.465562814179977,2.63995597585631,
13.8281701127186));
#423656=CARTESIAN_POINT('Ctrl Pts',(0.466621447266517,2.64149547160745,
13.8253580685121));
#423657=CARTESIAN_POINT('Ctrl Pts',(0.466850960062196,2.64182923594778,
13.8247484142933));
#423658=CARTESIAN_POINT('Ctrl Pts',(0.467071929787148,2.64216598251914,
13.8241378483365));
#423659=CARTESIAN_POINT('Ctrl Pts',(0.467283921384947,2.64250562881057,
13.8235269408515));
#423660=CARTESIAN_POINT('',(0.432417146080976,2.62680914300621,12.5969504640361));
#423661=CARTESIAN_POINT('Origin',(0.438128466382594,2.66073921298301,12.584524458991));
#423662=CARTESIAN_POINT('Origin',(0.438128466382594,2.66073921298301,12.584524458991));
#423663=CARTESIAN_POINT('Ctrl Pts',(0.404665629804346,2.65281661438093,
12.5893111709658));
#423664=CARTESIAN_POINT('Ctrl Pts',(0.407267077514713,2.64178524527415,
12.5770542771492));
#423665=CARTESIAN_POINT('Ctrl Pts',(0.423615907026998,2.64250597298499,
12.5737548217797));
#423666=CARTESIAN_POINT('Ctrl Pts',(0.398977136733573,2.67693851637994,
12.5663937883685));
#423667=CARTESIAN_POINT('Ctrl Pts',(0.401581902951781,2.66589307522986,
12.5540940315304));
#423668=CARTESIAN_POINT('Ctrl Pts',(0.417981252745244,2.66661924440073,
12.5508374392248));
#423669=CARTESIAN_POINT('Ctrl Pts',(0.39329438328257,2.70103607967557,12.5434499600945));
#423670=CARTESIAN_POINT('Ctrl Pts',(0.39590761852335,2.6899547258629,12.5311293540533));
#423671=CARTESIAN_POINT('Ctrl Pts',(0.412350954724039,2.69070868816462,
12.5278936106989));
#423672=CARTESIAN_POINT('Ctrl Pts',(0.387616919859073,2.72511121075171,
12.5204817579905));
#423673=CARTESIAN_POINT('Ctrl Pts',(0.39024308882838,2.71397501181074,12.5081597038247));
#423674=CARTESIAN_POINT('Ctrl Pts',(0.406724660887055,2.71477615310253,
12.5049254088044));
#423675=CARTESIAN_POINT('Ctrl Pts',(0.391698755050328,2.70780229831487,
12.5369868989719));
#423676=CARTESIAN_POINT('Ctrl Pts',(0.391484949870882,2.7087089341381,12.5342545179733));
#423677=CARTESIAN_POINT('Ctrl Pts',(0.391402319608562,2.70960281855631,
12.5314872231885));
#423678=CARTESIAN_POINT('Ctrl Pts',(0.391511182542072,2.71043874317721,
12.5287124745063));
#423679=CARTESIAN_POINT('Ctrl Pts',(0.391609360538986,2.71119262149194,
12.5262100684184));
#423680=CARTESIAN_POINT('Ctrl Pts',(0.3918641625634,2.71189847152282,12.5237004536639));
#423681=CARTESIAN_POINT('Ctrl Pts',(0.392342316081914,2.71254590475039,
12.5212220730815));
#423682=CARTESIAN_POINT('Ctrl Pts',(0.392708383963915,2.71304157089353,
12.5193246583486));
#423683=CARTESIAN_POINT('Ctrl Pts',(0.393210248721006,2.71350854454234,
12.517417831369));
#423684=CARTESIAN_POINT('Ctrl Pts',(0.393926887946714,2.71389011095029,
12.5155812248348));
#423685=CARTESIAN_POINT('Ctrl Pts',(0.39423218010882,2.714052660291,12.5147988205793));
#423686=CARTESIAN_POINT('Ctrl Pts',(0.394576629386592,2.71420011940999,
12.5140295443047));
#423687=CARTESIAN_POINT('Ctrl Pts',(0.394966574362074,2.71433021809919,
12.5132817086137));
#423688=CARTESIAN_POINT('Ctrl Pts',(0.395556703331901,2.71452710486594,
12.5121499604604));
#423689=CARTESIAN_POINT('Ctrl Pts',(0.396266036648342,2.7146816990542,12.5110494206568));
#423690=CARTESIAN_POINT('Ctrl Pts',(0.397113791152486,2.71476210063629,
12.5100666561695));
#423691=CARTESIAN_POINT('Ctrl Pts',(0.397600569836561,2.71480826703958,
12.5095023550641));
#423692=CARTESIAN_POINT('Ctrl Pts',(0.398138672311807,2.71482985549899,
12.5089719619137));
#423693=CARTESIAN_POINT('Ctrl Pts',(0.398718268479109,2.71482007951818,
12.5085043804652));
#423694=CARTESIAN_POINT('Ctrl Pts',(0.399566431972245,2.71480577364368,
12.5078201359221));
#423695=CARTESIAN_POINT('Ctrl Pts',(0.400528031383566,2.71472267981267,
12.5072563000949));
#423696=CARTESIAN_POINT('Ctrl Pts',(0.401537155609109,2.71456799599384,
12.5068768744332));
#423697=CARTESIAN_POINT('Ctrl Pts',(0.402264803644073,2.714456458312,12.5066032824114));
#423698=CARTESIAN_POINT('Ctrl Pts',(0.403029954523992,2.71430579792691,
12.5064197834844));
#423699=CARTESIAN_POINT('Ctrl Pts',(0.403790379615045,2.71412696426627,
12.5063282718343));
#423700=CARTESIAN_POINT('Ctrl Pts',(0.404900364826325,2.71386592248724,
12.5061946931565));
#423701=CARTESIAN_POINT('Ctrl Pts',(0.406024248600795,2.71354030654559,
12.5062515701262));
#423702=CARTESIAN_POINT('Ctrl Pts',(0.407096584198923,2.71318517842265,
12.5064436508398));
#423703=CARTESIAN_POINT('',(0.423615907026998,2.64250597298499,12.5737548217797));
#423704=CARTESIAN_POINT('Origin',(0.426078281186186,2.65786620454249,12.5893111709658));
#423705=CARTESIAN_POINT('Ctrl Pts',(0.407096584198923,2.71318517842265,
12.5064436508398));
#423706=CARTESIAN_POINT('Ctrl Pts',(0.409542340992688,2.70272292907287,
12.5164271754438));
#423707=CARTESIAN_POINT('Ctrl Pts',(0.411988863833398,2.69225648492929,
12.5264061185523));
#423708=CARTESIAN_POINT('Ctrl Pts',(0.414436180622228,2.68178569847023,
12.536380305637));
#423709=CARTESIAN_POINT('Ctrl Pts',(0.417494830238938,2.66869933910072,
12.5488460165097));
#423710=CARTESIAN_POINT('Ctrl Pts',(0.420554720876929,2.65560619319357,
12.5613043021964));
#423711=CARTESIAN_POINT('Ctrl Pts',(0.423615907026998,2.64250597298499,
12.5737548217797));
#423712=CARTESIAN_POINT('Ctrl Pts',(0.467283921384947,2.64250562881057,
12.5893111709658));
#423713=CARTESIAN_POINT('Ctrl Pts',(0.46128278519986,2.63289079656826,12.5770542771492));
#423714=CARTESIAN_POINT('Ctrl Pts',(0.446028214811845,2.63881547015691,
12.5737548217797));
#423715=CARTESIAN_POINT('Ctrl Pts',(0.461684913519388,2.63353507395389,
12.5928319619712));
#423716=CARTESIAN_POINT('Ctrl Pts',(0.454888168822745,2.62879823134515,
12.5821634970842));
#423717=CARTESIAN_POINT('Ctrl Pts',(0.443996638945792,2.63554271644331,
12.5773203894503));
#423718=CARTESIAN_POINT('Ctrl Pts',(0.447697135107924,2.62431953520396,
12.5969440695591));
#423719=CARTESIAN_POINT('Ctrl Pts',(0.443727850797269,2.62495461363464,
12.5878292599214));
#423720=CARTESIAN_POINT('Ctrl Pts',(0.439009983674417,2.63225981889662,
12.5813877129824));
#423721=CARTESIAN_POINT('Ctrl Pts',(0.417497997839952,2.62923759923481,
12.596957478804));
#423722=CARTESIAN_POINT('Ctrl Pts',(0.42143796073924,2.62860729335578,12.5878468778671));
#423723=CARTESIAN_POINT('Ctrl Pts',(0.428202252638728,2.63402594974239,
12.5814011370086));
#423724=CARTESIAN_POINT('Ctrl Pts',(0.407096282077668,2.64250949873489,
12.5928371701607));
#423725=CARTESIAN_POINT('Ctrl Pts',(0.412016731979506,2.63585185362063,
12.5821692192951));
#423726=CARTESIAN_POINT('Ctrl Pts',(0.424493415151723,2.63874256270109,
12.5773318885715));
#423727=CARTESIAN_POINT('Ctrl Pts',(0.404665629804292,2.65281661438091,
12.5893111709658));
#423728=CARTESIAN_POINT('Ctrl Pts',(0.40726707751466,2.64178524527414,12.5770542771492));
#423729=CARTESIAN_POINT('Ctrl Pts',(0.423615907026944,2.64250597298498,
12.5737548217797));
#423730=CARTESIAN_POINT('',(0.446028214811845,2.63881547015691,12.5737548217797));
#423731=CARTESIAN_POINT('Origin',(0.448620866155203,2.65415424973717,12.5893111709658));
#423732=CARTESIAN_POINT('Ctrl Pts',(0.423615907026944,2.64250597298498,
12.5737548217797));
#423733=CARTESIAN_POINT('Ctrl Pts',(0.423813993339227,2.64152358739678,
12.5746934679442));
#423734=CARTESIAN_POINT('Ctrl Pts',(0.424212759218763,2.64047272051103,
12.5756680099006));
#423735=CARTESIAN_POINT('Ctrl Pts',(0.424763723044868,2.6394717497171,12.5765688348656));
#423736=CARTESIAN_POINT('Ctrl Pts',(0.424909584618459,2.63920675378052,
12.5768073183026));
#423737=CARTESIAN_POINT('Ctrl Pts',(0.425065864631672,2.63894518947167,
12.5770407398754));
#423738=CARTESIAN_POINT('Ctrl Pts',(0.425231172395766,2.6386889776725,12.5772674179684));
#423739=CARTESIAN_POINT('Ctrl Pts',(0.425909550758503,2.6376375537313,12.5781976435658));
#423740=CARTESIAN_POINT('Ctrl Pts',(0.426787970403449,2.63662266634339,
12.5790594849312));
#423741=CARTESIAN_POINT('Ctrl Pts',(0.427843631120765,2.6357444447463,12.5797571720116));
#423742=CARTESIAN_POINT('Ctrl Pts',(0.428531432036273,2.63517225179777,
12.580211740231));
#423743=CARTESIAN_POINT('Ctrl Pts',(0.429337734707596,2.63464650187381,
12.5806009430798));
#423744=CARTESIAN_POINT('Ctrl Pts',(0.430215455706686,2.63421904601401,
12.5808812374708));
#423745=CARTESIAN_POINT('Ctrl Pts',(0.430969709225813,2.63385171962343,
12.5811221033394));
#423746=CARTESIAN_POINT('Ctrl Pts',(0.431792193236375,2.6335495610474,12.581287365893));
#423747=CARTESIAN_POINT('Ctrl Pts',(0.432639360677754,2.63333745114731,
12.581359338449));
#423748=CARTESIAN_POINT('Ctrl Pts',(0.432757099458768,2.6333079722511,12.5813693411482));
#423749=CARTESIAN_POINT('Ctrl Pts',(0.432875320654025,2.63328017305776,
12.5813775999465));
#423750=CARTESIAN_POINT('Ctrl Pts',(0.432993914231552,2.63325405940128,
12.5813841266931));
#423751=CARTESIAN_POINT('Ctrl Pts',(0.43319512257942,2.63320975442467,12.5813952001081));
#423752=CARTESIAN_POINT('Ctrl Pts',(0.433398881368839,2.6331705991971,12.5814007534795));
#423753=CARTESIAN_POINT('Ctrl Pts',(0.433605139072039,2.63313680443837,
12.5814005856065));
#423754=CARTESIAN_POINT('Ctrl Pts',(0.434549306195751,2.63298210524581,
12.5813998171494));
#423755=CARTESIAN_POINT('Ctrl Pts',(0.435480547552188,2.63295008748908,
12.58127954464));
#423756=CARTESIAN_POINT('Ctrl Pts',(0.436392559425332,2.63301136105901,
12.5810700125799));
#423757=CARTESIAN_POINT('Ctrl Pts',(0.437494165927224,2.63308537255494,
12.5808169217085));
#423758=CARTESIAN_POINT('Ctrl Pts',(0.438566694535404,2.6333122001196,12.5804173076348));
#423759=CARTESIAN_POINT('Ctrl Pts',(0.439521539130877,2.63364648617398,
12.5799304713245));
#423760=CARTESIAN_POINT('Ctrl Pts',(0.440704892391735,2.63406077190632,
12.5793271277669));
#423761=CARTESIAN_POINT('Ctrl Pts',(0.441791540088032,2.6346354105689,12.5785808224116));
#423762=CARTESIAN_POINT('Ctrl Pts',(0.442750504849584,2.63531814217729,
12.5777485681082));
#423763=CARTESIAN_POINT('Ctrl Pts',(0.44417946740673,2.63633548707263,12.576508418016));
#423764=CARTESIAN_POINT('Ctrl Pts',(0.445316872977787,2.63757867976795,
12.5750928681475));
#423765=CARTESIAN_POINT('Ctrl Pts',(0.446028214811845,2.63881547015691,
12.5737548217797));
#423766=CARTESIAN_POINT('Ctrl Pts',(0.446028214811845,2.63881547015691,
12.5737548217797));
#423767=CARTESIAN_POINT('Ctrl Pts',(0.461282785199861,2.63289079656826,
12.5770542771492));
#423768=CARTESIAN_POINT('Ctrl Pts',(0.467283921384947,2.64250562881057,
12.5893111709658));
#423769=CARTESIAN_POINT('Ctrl Pts',(0.459094958715932,2.65984580914408,
12.5508408821982));
#423770=CARTESIAN_POINT('Ctrl Pts',(0.474395628639503,2.65389978320067,
12.55409748406));
#423771=CARTESIAN_POINT('Ctrl Pts',(0.480404420737386,2.66352688150644,
12.5663972313419));
#423772=CARTESIAN_POINT('Ctrl Pts',(0.472149939932253,2.6808549816464,12.52790050457));
#423773=CARTESIAN_POINT('Ctrl Pts',(0.487483357862869,2.6748685326232,12.5311362602938));
#423774=CARTESIAN_POINT('Ctrl Pts',(0.49351168366197,2.68452692721261,12.5434568539655));
#423775=CARTESIAN_POINT('Ctrl Pts',(0.48519408433515,2.70184462526304,12.5049357605811));
#423776=CARTESIAN_POINT('Ctrl Pts',(0.500548590898578,2.69580123935917,
12.5081700652078));
#423777=CARTESIAN_POINT('Ctrl Pts',(0.506606746838401,2.70550742686479,
12.5204921097672));
#423778=CARTESIAN_POINT('Ctrl Pts',(0.484337556030204,2.70046636214855,
12.5064436508395));
#423779=CARTESIAN_POINT('Ctrl Pts',(0.485557713004785,2.70045831553657,
12.5062361689309));
#423780=CARTESIAN_POINT('Ctrl Pts',(0.486826233284257,2.70039791751499,
12.5061871075061));
#423781=CARTESIAN_POINT('Ctrl Pts',(0.48804884993876,2.70027053950571,12.5063648335164));
#423782=CARTESIAN_POINT('Ctrl Pts',(0.488604237837358,2.7002126765569,12.5064455676329));
#423783=CARTESIAN_POINT('Ctrl Pts',(0.489157877030412,2.70013996584525,
12.506574497099));
#423784=CARTESIAN_POINT('Ctrl Pts',(0.489685892281465,2.70005448298666,
12.5067492519495));
#423785=CARTESIAN_POINT('Ctrl Pts',(0.490746959424457,2.69988270186413,
12.5071004286051));
#423786=CARTESIAN_POINT('Ctrl Pts',(0.491743433274509,2.6996522300912,12.5076537929612));
#423787=CARTESIAN_POINT('Ctrl Pts',(0.492602654597667,2.69938958096391,
12.5083435010503));
#423788=CARTESIAN_POINT('Ctrl Pts',(0.492656747714796,2.69937304563172,
12.5083869222963));
#423789=CARTESIAN_POINT('Ctrl Pts',(0.492710299247793,2.69935636954928,
12.5084308732336));
#423790=CARTESIAN_POINT('Ctrl Pts',(0.492763292436878,2.69933955402141,
12.5084753333615));
#423791=CARTESIAN_POINT('Ctrl Pts',(0.493188367757264,2.69920467129361,
12.508831962269));
#423792=CARTESIAN_POINT('Ctrl Pts',(0.493586538271215,2.69905930774684,
12.509227847131));
#423793=CARTESIAN_POINT('Ctrl Pts',(0.49394692454245,2.69891041604802,12.5096423454524));
#423794=CARTESIAN_POINT('Ctrl Pts',(0.495076215616221,2.69844385536062,
12.5109411997424));
#423795=CARTESIAN_POINT('Ctrl Pts',(0.495907646827,2.69792289064837,12.5124831113042));
#423796=CARTESIAN_POINT('Ctrl Pts',(0.496519452946775,2.6974007682994,12.5140723025008));
#423797=CARTESIAN_POINT('Ctrl Pts',(0.49657677985029,2.69735184486344,12.5142212114565));
#423798=CARTESIAN_POINT('Ctrl Pts',(0.496632207239263,2.69730291825394,
12.5143705582413));
#423799=CARTESIAN_POINT('Ctrl Pts',(0.496685815545039,2.6972540377714,12.5145201959299));
#423800=CARTESIAN_POINT('Ctrl Pts',(0.497374494047155,2.69662609519776,
12.5164425148273));
#423801=CARTESIAN_POINT('Ctrl Pts',(0.497793796863192,2.69599218437767,
12.518463520594));
#423802=CARTESIAN_POINT('Ctrl Pts',(0.498033819009212,2.69535687331197,
12.5205025929157));
#423803=CARTESIAN_POINT('Ctrl Pts',(0.498173041367493,2.69498836771248,
12.5216853356836));
#423804=CARTESIAN_POINT('Ctrl Pts',(0.498252146321835,2.69462022757511,
12.5228750347131));
#423805=CARTESIAN_POINT('Ctrl Pts',(0.498288073867896,2.69425923303223,
12.5240609649613));
#423806=CARTESIAN_POINT('Ctrl Pts',(0.498376256102257,2.69337319129344,
12.5269717671326));
#423807=CARTESIAN_POINT('Ctrl Pts',(0.498196461551548,2.69250423047285,
12.5299036066169));
#423808=CARTESIAN_POINT('Ctrl Pts',(0.497835269307655,2.69164866499371,
12.5328133004019));
#423809=CARTESIAN_POINT('Ctrl Pts',(0.497661875998992,2.69123794374564,
12.5342101228451));
#423810=CARTESIAN_POINT('Ctrl Pts',(0.497446412050331,2.69083102582579,
12.5356023438238));
#423811=CARTESIAN_POINT('Ctrl Pts',(0.497196489292312,2.69043060726395,
12.5369868989719));
#423812=CARTESIAN_POINT('Origin',(7.25027860668965,13.5000022643794,-1.24036406790302));
#423813=CARTESIAN_POINT('Ctrl Pts',(0.391708309312677,2.70776161076147,
12.5369868989719));
#423814=CARTESIAN_POINT('Ctrl Pts',(0.388215977810789,2.72269770544401,
12.5369868989719));
#423815=CARTESIAN_POINT('Ctrl Pts',(0.372993636725075,2.72458546484474,
12.5369868989719));
#423816=CARTESIAN_POINT('Ctrl Pts',(0.390527700207791,2.71281057983639,
12.5218025310015));
#423817=CARTESIAN_POINT('Ctrl Pts',(0.384715766406483,2.72310024888808,
12.5216901060417));
#423818=CARTESIAN_POINT('Ctrl Pts',(0.373040041495134,2.72457972669485,
12.5161920673678));
#423819=CARTESIAN_POINT('Ctrl Pts',(0.394494633263108,2.71734924851006,
12.5042015548895));
#423820=CARTESIAN_POINT('Ctrl Pts',(0.390345509719021,2.72226474633153,
12.4980677368514));
#423821=CARTESIAN_POINT('Ctrl Pts',(0.3836170764577,2.72322337325147,12.4907278922777));
#423822=CARTESIAN_POINT('Ctrl Pts',(0.407093616392521,2.71316539875053,
12.506463626192));
#423823=CARTESIAN_POINT('Ctrl Pts',(0.408064446405071,2.71963570998129,
12.4999376786891));
#423824=CARTESIAN_POINT('Ctrl Pts',(0.408052589128054,2.71955668453743,
12.4906970594712));
#423825=CARTESIAN_POINT('Origin',(0.370286103668487,2.7027527081533,12.5369868989719));
#423826=CARTESIAN_POINT('Origin',(0.370286103668487,2.7027527081533,14.));
#423827=CARTESIAN_POINT('Origin',(0.370286103668487,2.7027527081533,13.7435492065112));
#423828=CARTESIAN_POINT('Ctrl Pts',(0.39738183668897,2.683703225055,13.793642941384));
#423829=CARTESIAN_POINT('Ctrl Pts',(0.394926622670047,2.69423309414853,
13.8071662555867));
#423830=CARTESIAN_POINT('Ctrl Pts',(0.377953213457921,2.69284645672205,
13.8103758687955));
#423831=CARTESIAN_POINT('Ctrl Pts',(0.393566846153838,2.69988060285367,
13.7804579775006));
#423832=CARTESIAN_POINT('Ctrl Pts',(0.390527458075338,2.71287120683648,
13.7901904343351));
#423833=CARTESIAN_POINT('Ctrl Pts',(0.37482297205525,2.71414597858428,13.7927914348262));
#423834=CARTESIAN_POINT('Ctrl Pts',(0.391320817614566,2.70940483397817,
13.7597120340895));
#423835=CARTESIAN_POINT('Ctrl Pts',(0.38779780994803,2.72443731570785,13.7635825532445));
#423836=CARTESIAN_POINT('Ctrl Pts',(0.372951781532102,2.72670256545515,
13.7651073818884));
#423837=CARTESIAN_POINT('Ctrl Pts',(0.391760641429967,2.70753977144373,
13.7381884353898));
#423838=CARTESIAN_POINT('Ctrl Pts',(0.388320971442423,2.72222059502428,
13.7368803041982));
#423839=CARTESIAN_POINT('Ctrl Pts',(0.373317727405731,2.7242435397824,13.7363986145813));
#423840=CARTESIAN_POINT('Origin',(0.375043510389596,2.68257905279884,13.7902182540695));
#423841=CARTESIAN_POINT('Ctrl Pts',(0.404666532528808,2.65281278309563,
13.8235227101244));
#423842=CARTESIAN_POINT('Ctrl Pts',(0.402031961110901,2.66400392788798,
13.8358800583119));
#423843=CARTESIAN_POINT('Ctrl Pts',(0.385481469674138,2.66316292713999,
13.8390832900376));
#423844=CARTESIAN_POINT('Ctrl Pts',(0.401928833101939,2.66442192393992,
13.8124254819052));
#423845=CARTESIAN_POINT('Ctrl Pts',(0.39928914511293,2.67563480171307,13.8247886449158));
#423846=CARTESIAN_POINT('Ctrl Pts',(0.382718606411933,2.67477571600075,
13.8279860620657));
#423847=CARTESIAN_POINT('Ctrl Pts',(0.399192360622903,2.67602586194496,
13.8013225099955));
#423848=CARTESIAN_POINT('Ctrl Pts',(0.396548803522908,2.68725518248059,
13.8136962257787));
#423849=CARTESIAN_POINT('Ctrl Pts',(0.379957285915346,2.68638319144869,
13.8168830918626));
#423850=CARTESIAN_POINT('Ctrl Pts',(0.396457067353036,2.68762479954526,
13.7902140179785));
#423851=CARTESIAN_POINT('Ctrl Pts',(0.393810807068658,2.69886561837895,
13.802602731458));
#423852=CARTESIAN_POINT('Ctrl Pts',(0.377197449355671,2.69798556268668,
13.8057746032558));
#423853=CARTESIAN_POINT('Origin',(0.383252978422506,2.64776702421936,13.8235269408515));
#423854=CARTESIAN_POINT('Ctrl Pts',(0.467283921384947,2.64250562881057,
13.8235269408515));
#423855=CARTESIAN_POINT('Ctrl Pts',(0.473535779376053,2.65252215966961,
13.8362179249168));
#423856=CARTESIAN_POINT('Ctrl Pts',(0.489295333927072,2.64594192833548,
13.8391868794938));
#423857=CARTESIAN_POINT('Ctrl Pts',(0.461563743450256,2.63334093906817,
13.8400110824519));
#423858=CARTESIAN_POINT('Ctrl Pts',(0.469478308228246,2.63956038657065,
13.8494522556836));
#423859=CARTESIAN_POINT('Ctrl Pts',(0.479786221201546,2.63091892734374,
13.85569149686));
#423860=CARTESIAN_POINT('Ctrl Pts',(0.448036370061348,2.62426305962186,
13.8586819406588));
#423861=CARTESIAN_POINT('Ctrl Pts',(0.452334609820048,2.6235693892306,13.868010383617));
#423862=CARTESIAN_POINT('Ctrl Pts',(0.457249156920298,2.61597069897555,
13.8744918421245));
#423863=CARTESIAN_POINT('Ctrl Pts',(0.417153498517881,2.62929493235242,
13.8587686893867));
#423864=CARTESIAN_POINT('Ctrl Pts',(0.412893504081745,2.62998237349456,
13.8680909899357));
#423865=CARTESIAN_POINT('Ctrl Pts',(0.40583865878635,2.62434982883307,13.8745789365163));
#423866=CARTESIAN_POINT('Ctrl Pts',(0.407149319193208,2.64228459624337,
13.8400379222776));
#423867=CARTESIAN_POINT('Ctrl Pts',(0.401642198305064,2.65070729494577,
13.8494748685453));
#423868=CARTESIAN_POINT('Ctrl Pts',(0.389113132608578,2.64583044985511,
13.8557104837033));
#423869=CARTESIAN_POINT('Ctrl Pts',(0.404665629797947,2.65281661437927,
13.8235269408542));
#423870=CARTESIAN_POINT('Ctrl Pts',(0.401955496057409,2.66430886367604,
13.8362179249195));
#423871=CARTESIAN_POINT('Ctrl Pts',(0.384918149621722,2.66312910501989,
13.8391868794965));
#423872=CARTESIAN_POINT('Origin',(0.485946976614692,2.63085700788398,13.8235269408515));
#423873=CARTESIAN_POINT('Ctrl Pts',(0.4862198031753,2.67284410348367,13.7902140241683));
#423874=CARTESIAN_POINT('Ctrl Pts',(0.492330545861212,2.68264295133528,
13.8026027327198));
#423875=CARTESIAN_POINT('Ctrl Pts',(0.507784585967035,2.67648254739715,
13.8057746032556));
#423876=CARTESIAN_POINT('Ctrl Pts',(0.479909906053499,2.66273458415115,
13.8013225161808));
#423877=CARTESIAN_POINT('Ctrl Pts',(0.486014401516539,2.67252340752409,
13.8136962270464));
#423878=CARTESIAN_POINT('Ctrl Pts',(0.501450340426531,2.66637764514013,
13.8168830918628));
#423879=CARTESIAN_POINT('Ctrl Pts',(0.47359728867826,2.65262070651389,13.8124254880875));
#423880=CARTESIAN_POINT('Ctrl Pts',(0.479692847185781,2.66239519583671,
13.8247886461867));
#423881=CARTESIAN_POINT('Ctrl Pts',(0.495113052711343,2.6562683839621,13.8279860620656));
#423882=CARTESIAN_POINT('Ctrl Pts',(0.467281840923095,2.64250229413067,
13.8235227163066));
#423883=CARTESIAN_POINT('Ctrl Pts',(0.473365584653211,2.65225783847546,
13.8358800595847));
#423884=CARTESIAN_POINT('Ctrl Pts',(0.488772600020414,2.64615458456687,
13.8390832900376));
#423885=CARTESIAN_POINT('Origin',(0.504884945452683,2.66119882779466,13.7902182540695));
#423886=CARTESIAN_POINT('Ctrl Pts',(0.497053626524536,2.69020166491958,
13.7382347919292));
#423887=CARTESIAN_POINT('Ctrl Pts',(0.505023322820197,2.70301579031652,
13.7369371795943));
#423888=CARTESIAN_POINT('Ctrl Pts',(0.519892956030771,2.70011100371444,
13.7364597369712));
#423889=CARTESIAN_POINT('Ctrl Pts',(0.498055173875918,2.69180631344405,
13.7595490285574));
#423890=CARTESIAN_POINT('Ctrl Pts',(0.506215874061809,2.70492564189087,
13.7633824266926));
#423891=CARTESIAN_POINT('Ctrl Pts',(0.521013790355526,2.70229593968879,
13.7648920890506));
#423892=CARTESIAN_POINT('Ctrl Pts',(0.49294733724627,2.6836226938832,13.780380659011));
#423893=CARTESIAN_POINT('Ctrl Pts',(0.500001466840538,2.69497329482198,
13.7901039518744));
#423894=CARTESIAN_POINT('Ctrl Pts',(0.515296351105374,2.69115859211384,
13.7926933640892));
#423895=CARTESIAN_POINT('Ctrl Pts',(0.484068777036776,2.66939773623195,
13.7936647693663));
#423896=CARTESIAN_POINT('Ctrl Pts',(0.489769906820424,2.67858851700046,
13.8072068914933));
#423897=CARTESIAN_POINT('Ctrl Pts',(0.50541520923648,2.67181586743344,13.8104111085397));
#423898=CARTESIAN_POINT('Origin',(0.515859544522057,2.67878198633736,13.7435492065112));
#423899=CARTESIAN_POINT('Origin',(0.515859544522058,2.67878198633736,14.));
#423900=CARTESIAN_POINT('Origin',(0.515859544522057,2.67878198633736,12.5369868989719));
#423901=CARTESIAN_POINT('Ctrl Pts',(0.48433431070966,2.70044826763868,12.506462012331));
#423902=CARTESIAN_POINT('Ctrl Pts',(0.48548861562589,2.70688419555548,12.4999388158272));
#423903=CARTESIAN_POINT('Ctrl Pts',(0.485474958684953,2.70680805008802,
12.4907030323752));
#423904=CARTESIAN_POINT('Ctrl Pts',(0.497609188721907,2.70036954715612,
12.5042014951932));
#423905=CARTESIAN_POINT('Ctrl Pts',(0.503112422793168,2.70369453014448,
12.4980716682127));
#423906=CARTESIAN_POINT('Ctrl Pts',(0.509788554495942,2.7024476016328,12.4907355092743));
#423907=CARTESIAN_POINT('Ctrl Pts',(0.499913267801054,2.69480026346409,
12.5218047446509));
#423908=CARTESIAN_POINT('Ctrl Pts',(0.508714002286156,2.70267845763908,
12.5216906929434));
#423909=CARTESIAN_POINT('Ctrl Pts',(0.520242539411905,2.70034102612785,
12.5161988840776));
#423910=CARTESIAN_POINT('Ctrl Pts',(0.49717617707613,2.69039800032153,12.5369868989719));
#423911=CARTESIAN_POINT('Ctrl Pts',(0.505270368811235,2.7034168171524,12.5369868989719));
#423912=CARTESIAN_POINT('Ctrl Pts',(0.520286662692129,2.70033194282706,
12.5369868989719));
#423913=CARTESIAN_POINT('Origin',(8.3705472999219E-32,-6.84555113983343E-33,
12.5));
#423914=CARTESIAN_POINT('Origin',(0.68111781325818,2.59562493167692,12.5));
#423915=CARTESIAN_POINT('',(0.68111781325818,2.59562493167692,12.5893111709658));
#423916=CARTESIAN_POINT('',(0.68111781325818,2.59562493167692,13.8235269408515));
#423917=CARTESIAN_POINT('',(0.68111781325818,2.59562493167692,12.5));
#423918=CARTESIAN_POINT('',(0.702465907569571,2.62432217141306,13.7902182540695));
#423919=CARTESIAN_POINT('',(0.68111781325818,2.59562493167692,13.8235269408515));
#423920=CARTESIAN_POINT('',(0.714837180221191,2.64095229173885,13.7435492065112));
#423921=CARTESIAN_POINT('Origin',(0.674135595355062,2.58623961011718,13.74452129187));
#423922=CARTESIAN_POINT('',(0.714837180221191,2.64095229173885,12.5369868989719));
#423923=CARTESIAN_POINT('',(0.714837180221191,2.64095229173885,12.5));
#423924=CARTESIAN_POINT('Ctrl Pts',(0.714837180221191,2.64095229173885,
12.5369868989719));
#423925=CARTESIAN_POINT('Ctrl Pts',(0.703605588851989,2.62585419139139,
12.5544431401645));
#423926=CARTESIAN_POINT('Ctrl Pts',(0.692365964350122,2.61074529248129,
12.5718848856037));
#423927=CARTESIAN_POINT('Ctrl Pts',(0.68111781325818,2.59562493167692,12.5893111709658));
#423928=CARTESIAN_POINT('Origin',(0.578455092500073,2.88291796821534,12.5));
#423929=CARTESIAN_POINT('',(0.611106435078506,2.66686522465476,13.7435492065112));
#423930=CARTESIAN_POINT('',(0.614203671726741,2.6463709226609,13.7902182540695));
#423931=CARTESIAN_POINT('Origin',(0.622342674328417,2.59251543914704,13.741873268044));
#423932=CARTESIAN_POINT('',(0.619548319923672,2.61100558037707,13.8235269408515));
#423933=CARTESIAN_POINT('',(0.614203671726741,2.6463709226609,13.7902182540695));
#423934=CARTESIAN_POINT('',(0.619548319923672,2.61100558037707,12.5893111709658));
#423935=CARTESIAN_POINT('',(0.619548319923672,2.61100558037707,12.5));
#423936=CARTESIAN_POINT('',(0.611106435078506,2.66686522465476,12.5369868989719));
#423937=CARTESIAN_POINT('Ctrl Pts',(0.619548319923672,2.61100558037707,
12.5893111709658));
#423938=CARTESIAN_POINT('Ctrl Pts',(0.616732264795966,2.62963931449986,
12.5718848856037));
#423939=CARTESIAN_POINT('Ctrl Pts',(0.613918344361108,2.64825892343789,
12.5544431401645));
#423940=CARTESIAN_POINT('Ctrl Pts',(0.611106435078506,2.66686522465476,
12.5369868989719));
#423941=CARTESIAN_POINT('',(0.611106435078506,2.66686522465476,12.5));
#423942=CARTESIAN_POINT('Origin',(0.653537368403456,2.61614223380502,12.5));
#423943=CARTESIAN_POINT('',(0.646296948995977,2.58253916104401,13.8587068136939));
#423944=CARTESIAN_POINT('Ctrl Pts',(0.619548319917159,2.61100558037594,
13.8235269408542));
#423945=CARTESIAN_POINT('Ctrl Pts',(0.619810165712327,2.60927295629476,
13.8262006681044));
#423946=CARTESIAN_POINT('Ctrl Pts',(0.620249915267873,2.60752583055217,
13.8288634856214));
#423947=CARTESIAN_POINT('Ctrl Pts',(0.620854476897341,2.60576673569509,
13.8314912288862));
#423948=CARTESIAN_POINT('Ctrl Pts',(0.621477717579682,2.60395329033967,
13.8342001611531));
#423949=CARTESIAN_POINT('Ctrl Pts',(0.622276334377607,2.60212494904122,
13.8368750301949));
#423950=CARTESIAN_POINT('Ctrl Pts',(0.623280863434857,2.60027910221905,
13.8394886372969));
#423951=CARTESIAN_POINT('Ctrl Pts',(0.623358445650594,2.60013654299158,
13.8396904925131));
#423952=CARTESIAN_POINT('Ctrl Pts',(0.623437277088852,2.59999388642334,
13.8398919674349));
#423953=CARTESIAN_POINT('Ctrl Pts',(0.623517382298079,2.59985113590701,
13.8400930404591));
#423954=CARTESIAN_POINT('Ctrl Pts',(0.624765475350002,2.59762698682474,
13.8432258934518));
#423955=CARTESIAN_POINT('Ctrl Pts',(0.626315435597862,2.59539082938103,
13.8462331177034));
#423956=CARTESIAN_POINT('Ctrl Pts',(0.628195994783854,2.5932705489393,13.8489036603661));
#423957=CARTESIAN_POINT('Ctrl Pts',(0.62881133563468,2.59257676850382,13.849777493004));
#423958=CARTESIAN_POINT('Ctrl Pts',(0.62946203654557,2.59189564200963,13.85061494757));
#423959=CARTESIAN_POINT('Ctrl Pts',(0.630148988525808,2.59123235421203,
13.8514076489583));
#423960=CARTESIAN_POINT('Ctrl Pts',(0.631601991037305,2.58982940485971,
13.8530843267192));
#423961=CARTESIAN_POINT('Ctrl Pts',(0.63336195255461,2.5883705842523,13.8546805203176));
#423962=CARTESIAN_POINT('Ctrl Pts',(0.635413800400653,2.58704561132647,
13.8559412814273));
#423963=CARTESIAN_POINT('Ctrl Pts',(0.635688404185469,2.5868682869791,13.8561100121513));
#423964=CARTESIAN_POINT('Ctrl Pts',(0.635968162422763,2.58669333783879,
13.8562727473908));
#423965=CARTESIAN_POINT('Ctrl Pts',(0.636252969663793,2.58652118788908,
13.8564289040185));
#423966=CARTESIAN_POINT('Ctrl Pts',(0.637544567252616,2.5857404898311,13.8571370725437));
#423967=CARTESIAN_POINT('Ctrl Pts',(0.638963883514774,2.58500558596821,
13.8577210840554));
#423968=CARTESIAN_POINT('Ctrl Pts',(0.640469243760167,2.5843711037858,13.8581177131616));
#423969=CARTESIAN_POINT('Ctrl Pts',(0.640893205018191,2.58419241176502,
13.8582294175695));
#423970=CARTESIAN_POINT('Ctrl Pts',(0.641323891395816,2.58402153800461,
13.8583265086086));
#423971=CARTESIAN_POINT('Ctrl Pts',(0.641760147302266,2.58385932495528,
13.8584082369006));
#423972=CARTESIAN_POINT('Ctrl Pts',(0.642386930053195,2.58362626830254,
13.8585256585398));
#423973=CARTESIAN_POINT('Ctrl Pts',(0.643033114493385,2.5834084947044,13.8586122832068));
#423974=CARTESIAN_POINT('Ctrl Pts',(0.643682166822805,2.58321240962006,
13.8586682984299));
#423975=CARTESIAN_POINT('Ctrl Pts',(0.644201344347852,2.58305556098988,
13.8587131050557));
#423976=CARTESIAN_POINT('Ctrl Pts',(0.644728023374455,2.5829106327121,13.8587357943552));
#423977=CARTESIAN_POINT('Ctrl Pts',(0.645262400852843,2.58277809586149,
13.8587355499465));
#423978=CARTESIAN_POINT('Ctrl Pts',(0.645607781757141,2.58269243413515,
13.8587353919793));
#423979=CARTESIAN_POINT('Ctrl Pts',(0.645952634358145,2.58261283753483,
13.8587257282814));
#423980=CARTESIAN_POINT('Ctrl Pts',(0.646296948995977,2.58253916104401,
13.8587068136939));
#423981=CARTESIAN_POINT('Ctrl Pts',(0.646296948995977,2.58253916104401,
13.8587068136939));
#423982=CARTESIAN_POINT('Ctrl Pts',(0.647429381069848,2.58229684308209,
13.8586446046467));
#423983=CARTESIAN_POINT('Ctrl Pts',(0.648556001834598,2.58211848479346,
13.858482427929));
#423984=CARTESIAN_POINT('Ctrl Pts',(0.649676416337789,2.58199963309271,
13.8582284286032));
#423985=CARTESIAN_POINT('Ctrl Pts',(0.650825831285958,2.58187770507316,
13.8579678548414));
#423986=CARTESIAN_POINT('Ctrl Pts',(0.6519716838095,2.58181962927471,13.857615680862));
#423987=CARTESIAN_POINT('Ctrl Pts',(0.653068309046968,2.58181801804464,
13.8571944833187));
#423988=CARTESIAN_POINT('Ctrl Pts',(0.655805049480698,2.58181399705524,
13.8561433417727));
#423989=CARTESIAN_POINT('Ctrl Pts',(0.658363209973259,2.58215665563443,
13.8546163505474));
#423990=CARTESIAN_POINT('Ctrl Pts',(0.660628805277197,2.58267346775518,
13.8528973491086));
#423991=CARTESIAN_POINT('Ctrl Pts',(0.661042696113486,2.58276788170478,
13.8525833129072));
#423992=CARTESIAN_POINT('Ctrl Pts',(0.661446914434123,2.58286800015131,
13.8522628768812));
#423993=CARTESIAN_POINT('Ctrl Pts',(0.661840900946499,2.58297265473186,
13.851937733538));
#423994=CARTESIAN_POINT('Ctrl Pts',(0.664246921914411,2.58361176573513,
13.8499521282529));
#423995=CARTESIAN_POINT('Ctrl Pts',(0.666509426562027,2.58448750338326,
13.847639871647));
#423996=CARTESIAN_POINT('Ctrl Pts',(0.66853850649305,2.58547891818562,13.8452109780794));
#423997=CARTESIAN_POINT('Ctrl Pts',(0.66945143155388,2.58592497622647,13.8441181685877));
#423998=CARTESIAN_POINT('Ctrl Pts',(0.670317623462334,2.58639395449978,
13.8430021611332));
#423999=CARTESIAN_POINT('Ctrl Pts',(0.671131875113294,2.58687340250863,
13.8418824960098));
#424000=CARTESIAN_POINT('Ctrl Pts',(0.673050679921444,2.58800323398464,
13.8392439765549));
#424001=CARTESIAN_POINT('Ctrl Pts',(0.674774695556229,2.5892419576233,13.8364981347964));
#424002=CARTESIAN_POINT('Ctrl Pts',(0.676328449324258,2.59056505862521,
13.8336931113419));
#424003=CARTESIAN_POINT('Ctrl Pts',(0.67784170682183,2.59185367497638,13.8309611966328));
#424004=CARTESIAN_POINT('Ctrl Pts',(0.679194612509888,2.59322404869775,
13.8281701127185));
#424005=CARTESIAN_POINT('Ctrl Pts',(0.680375206277863,2.59467213347936,
13.825358068512));
#424006=CARTESIAN_POINT('Ctrl Pts',(0.680631160280891,2.59498607982283,
13.8247484142932));
#424007=CARTESIAN_POINT('Ctrl Pts',(0.680878842719071,2.59530369481378,
13.8241378483365));
#424008=CARTESIAN_POINT('Ctrl Pts',(0.68111781325818,2.59562493167692,13.8235269408515));
#424009=CARTESIAN_POINT('',(0.645087644960638,2.58282264050882,12.5969504640361));
#424010=CARTESIAN_POINT('Origin',(0.653545577009588,2.61617428535095,12.584524458991));
#424011=CARTESIAN_POINT('Origin',(0.653545577009588,2.61617428535095,12.584524458991));
#424012=CARTESIAN_POINT('Ctrl Pts',(0.619548319923672,2.61100558037707,
12.5893111709658));
#424013=CARTESIAN_POINT('Ctrl Pts',(0.62124195253895,2.59979887510191,12.5770542771492));
#424014=CARTESIAN_POINT('Ctrl Pts',(0.63759512866906,2.59918462327037,12.5737548217797));
#424015=CARTESIAN_POINT('Ctrl Pts',(0.615844913794055,2.63551088373177,
12.5663937883685));
#424016=CARTESIAN_POINT('Ctrl Pts',(0.617540706872934,2.62428988274767,
12.5540940315304));
#424017=CARTESIAN_POINT('Ctrl Pts',(0.633944678711678,2.6236769363982,12.5508374392248));
#424018=CARTESIAN_POINT('Ctrl Pts',(0.612145244355821,2.65999146153581,
12.5434499600945));
#424019=CARTESIAN_POINT('Ctrl Pts',(0.613846551061904,2.64873397708158,
12.5311293540533));
#424020=CARTESIAN_POINT('Ctrl Pts',(0.630296628344904,2.64814514608311,
12.5278936106989));
#424021=CARTESIAN_POINT('Ctrl Pts',(0.608449018908829,2.68444925057535,
12.5204817579905));
#424022=CARTESIAN_POINT('Ctrl Pts',(0.610158745920418,2.67313604926652,
12.5081597038247));
#424023=CARTESIAN_POINT('Ctrl Pts',(0.626650777360416,2.67259112369652,
12.5049254088044));
#424024=CARTESIAN_POINT('Ctrl Pts',(0.611106435078507,2.66686522465476,
12.5369868989719));
#424025=CARTESIAN_POINT('Ctrl Pts',(0.610967240554547,2.66778627082908,
12.5342545179733));
#424026=CARTESIAN_POINT('Ctrl Pts',(0.610957745116111,2.66868391605411,
12.5314872231885));
#424027=CARTESIAN_POINT('Ctrl Pts',(0.611134381434141,2.66950818586508,
12.5287124745063));
#424028=CARTESIAN_POINT('Ctrl Pts',(0.611293680833185,2.67025155329372,
12.5262100684184));
#424029=CARTESIAN_POINT('Ctrl Pts',(0.611605168355191,2.67093428593639,
12.5237004536639));
#424030=CARTESIAN_POINT('Ctrl Pts',(0.612134502675841,2.67154059093258,
12.5212220730815));
#424031=CARTESIAN_POINT('Ctrl Pts',(0.612539753889369,2.67200476985674,
12.5193246583486));
#424032=CARTESIAN_POINT('Ctrl Pts',(0.613078011420432,2.67242928305247,
12.517417831369));
#424033=CARTESIAN_POINT('Ctrl Pts',(0.613823367292772,2.67275116707981,
12.5155812248347));
#424034=CARTESIAN_POINT('Ctrl Pts',(0.614140892900696,2.6728882914056,12.5147988205793));
#424035=CARTESIAN_POINT('Ctrl Pts',(0.614496215339052,2.67300718405268,
12.5140295443047));
#424036=CARTESIAN_POINT('Ctrl Pts',(0.614895467055743,2.67310506571365,
12.5132817086137));
#424037=CARTESIAN_POINT('Ctrl Pts',(0.615499680519403,2.6732531963664,12.5121499604604));
#424038=CARTESIAN_POINT('Ctrl Pts',(0.616219254449275,2.67334945890483,
12.5110494206568));
#424039=CARTESIAN_POINT('Ctrl Pts',(0.617070741595595,2.67336049309504,
12.5100666561695));
#424040=CARTESIAN_POINT('Ctrl Pts',(0.61755966355421,2.67336682890164,12.5095023550641));
#424041=CARTESIAN_POINT('Ctrl Pts',(0.618097735197687,2.67334448518002,
12.5089719619137));
#424042=CARTESIAN_POINT('Ctrl Pts',(0.618674605973363,2.67328749925963,
12.5085043804652));
#424043=CARTESIAN_POINT('Ctrl Pts',(0.619518781210861,2.67320410778808,
12.5078201359221));
#424044=CARTESIAN_POINT('Ctrl Pts',(0.62047040806087,2.67304291116586,12.5072563000949));
#424045=CARTESIAN_POINT('Ctrl Pts',(0.621463566341549,2.67280648905205,
12.5068768744332));
#424046=CARTESIAN_POINT('Ctrl Pts',(0.622179701831168,2.67263601243263,
12.5066032824114));
#424047=CARTESIAN_POINT('Ctrl Pts',(0.622930026514607,2.67242348645752,
12.5064197834844));
#424048=CARTESIAN_POINT('Ctrl Pts',(0.623673344750348,2.67218326614677,
12.5063282718343));
#424049=CARTESIAN_POINT('Ctrl Pts',(0.624758359249019,2.6718326188634,12.5061946931565));
#424050=CARTESIAN_POINT('Ctrl Pts',(0.625851962670828,2.67141647942069,
12.5062515701262));
#424051=CARTESIAN_POINT('Ctrl Pts',(0.626891783921846,2.67097512765096,
12.5064436508398));
#424052=CARTESIAN_POINT('',(0.63759512866906,2.59918462327037,12.5737548217797));
#424053=CARTESIAN_POINT('Origin',(0.641301310950734,2.61429303857096,12.5893111709658));
#424054=CARTESIAN_POINT('Ctrl Pts',(0.626891783921846,2.67097512765096,
12.5064436508398));
#424055=CARTESIAN_POINT('Ctrl Pts',(0.628476632212847,2.66034833868883,
12.5164271754438));
#424056=CARTESIAN_POINT('Ctrl Pts',(0.6300619020872,2.64971730645078,12.5264061185523));
#424057=CARTESIAN_POINT('Ctrl Pts',(0.631647609328853,2.63908188163182,
12.536380305637));
#424058=CARTESIAN_POINT('Ctrl Pts',(0.633629421764836,2.62578975770468,
12.5488460165097));
#424059=CARTESIAN_POINT('Ctrl Pts',(0.635611917926886,2.6124907686668,12.5613043021964));
#424060=CARTESIAN_POINT('Ctrl Pts',(0.63759512866906,2.59918462327037,12.5737548217797));
#424061=CARTESIAN_POINT('Ctrl Pts',(0.68111781325818,2.59562493167692,12.5893111709658));
#424062=CARTESIAN_POINT('Ctrl Pts',(0.674352947271195,2.58653124030665,
12.5770542771492));
#424063=CARTESIAN_POINT('Ctrl Pts',(0.659632051107192,2.59367958913582,
12.5737548217797));
#424064=CARTESIAN_POINT('Ctrl Pts',(0.67480625213002,2.58714059672121,12.5928319619712));
#424065=CARTESIAN_POINT('Ctrl Pts',(0.66764602639335,2.58297351335615,12.5821634970842));
#424066=CARTESIAN_POINT('Ctrl Pts',(0.657340475331822,2.59058331753354,
12.5773203894503));
#424067=CARTESIAN_POINT('Ctrl Pts',(0.660113864936306,2.57909585571297,
12.5969440695591));
#424068=CARTESIAN_POINT('Ctrl Pts',(0.656209552879632,2.58005235449292,
12.5878292599214));
#424069=CARTESIAN_POINT('Ctrl Pts',(0.652102826117502,2.58771780225609,
12.5813877129824));
#424070=CARTESIAN_POINT('Ctrl Pts',(0.630416080681929,2.58645906533392,
12.596957478804));
#424071=CARTESIAN_POINT('Ctrl Pts',(0.634291557899078,2.58550971319259,
12.5878468778671));
#424072=CARTESIAN_POINT('Ctrl Pts',(0.641475012975146,2.59035898686064,
12.5814011370086));
#424073=CARTESIAN_POINT('Ctrl Pts',(0.621130758790323,2.60053464008273,
12.5928371701607));
#424074=CARTESIAN_POINT('Ctrl Pts',(0.625492176417632,2.59349808538714,
12.5821692192952));
#424075=CARTESIAN_POINT('Ctrl Pts',(0.63816296408195,2.59536221036517,12.5773318885715));
#424076=CARTESIAN_POINT('Ctrl Pts',(0.619548319923617,2.61100558037706,
12.5893111709658));
#424077=CARTESIAN_POINT('Ctrl Pts',(0.621241952538896,2.5997988751019,12.5770542771492));
#424078=CARTESIAN_POINT('Ctrl Pts',(0.637595128669005,2.59918462327036,
12.5737548217797));
#424079=CARTESIAN_POINT('',(0.659632051107192,2.59367958913582,12.5737548217797));
#424080=CARTESIAN_POINT('Origin',(0.663466328551157,2.6087560050389,12.5893111709658));
#424081=CARTESIAN_POINT('Ctrl Pts',(0.637595128669005,2.59918462327036,
12.5737548217797));
#424082=CARTESIAN_POINT('Ctrl Pts',(0.637712482319963,2.59818936061577,
12.5746934679442));
#424083=CARTESIAN_POINT('Ctrl Pts',(0.638024265931971,2.59710948728175,
12.5756680099006));
#424084=CARTESIAN_POINT('Ctrl Pts',(0.638491808059133,2.59606693846884,
12.5765688348656));
#424085=CARTESIAN_POINT('Ctrl Pts',(0.638615584661436,2.59579093521201,
12.5768073183026));
#424086=CARTESIAN_POINT('Ctrl Pts',(0.63875002474638,2.59551750296491,12.5770407398754));
#424087=CARTESIAN_POINT('Ctrl Pts',(0.638893898822339,2.59524866957195,
12.5772674179684));
#424088=CARTESIAN_POINT('Ctrl Pts',(0.639484319124885,2.59414545002286,
12.5781976435658));
#424089=CARTESIAN_POINT('Ctrl Pts',(0.640277093157057,2.5930623402331,12.5790594849312));
#424090=CARTESIAN_POINT('Ctrl Pts',(0.641257658037249,2.59210099469719,
12.5797571720116));
#424091=CARTESIAN_POINT('Ctrl Pts',(0.641896531314664,2.59147464351364,
12.580211740231));
#424092=CARTESIAN_POINT('Ctrl Pts',(0.642657297580737,2.59088492182612,
12.5806009430798));
#424093=CARTESIAN_POINT('Ctrl Pts',(0.643497256414729,2.59038734588064,
12.5808812374708));
#424094=CARTESIAN_POINT('Ctrl Pts',(0.64421905970657,2.58995976307438,12.5811221033394));
#424095=CARTESIAN_POINT('Ctrl Pts',(0.645014178240386,2.58959156982365,
12.581287365893));
#424096=CARTESIAN_POINT('Ctrl Pts',(0.645841237876002,2.58931111369056,
12.581359338449));
#424097=CARTESIAN_POINT('Ctrl Pts',(0.645956182087224,2.58927213607926,
12.5813693411482));
#424098=CARTESIAN_POINT('Ctrl Pts',(0.646071744018875,2.58923479326052,
12.5813775999465));
#424099=CARTESIAN_POINT('Ctrl Pts',(0.646187814480624,2.58919910001754,
12.5813841266931));
#424100=CARTESIAN_POINT('Ctrl Pts',(0.646384742057413,2.58913854211381,
12.5813952001081));
#424101=CARTESIAN_POINT('Ctrl Pts',(0.646584631341723,2.58908290893908,
12.5814007534795));
#424102=CARTESIAN_POINT('Ctrl Pts',(0.646787448152858,2.58903241471201,
12.5814005856065));
#424103=CARTESIAN_POINT('Ctrl Pts',(0.647715864218004,2.58880127188245,
12.5813998171494));
#424104=CARTESIAN_POINT('Ctrl Pts',(0.648641397201237,2.58869345584639,
12.58127954464));
#424105=CARTESIAN_POINT('Ctrl Pts',(0.649555368794894,2.58868018809921,
12.5810700125799));
#424106=CARTESIAN_POINT('Ctrl Pts',(0.650659342416034,2.58866416217127,
12.5808169217085));
#424107=CARTESIAN_POINT('Ctrl Pts',(0.651746790826033,2.58880281394749,
12.5804173076348));
#424108=CARTESIAN_POINT('Ctrl Pts',(0.652725705671675,2.58905815899372,
12.5799304713245));
#424109=CARTESIAN_POINT('Ctrl Pts',(0.653938889555404,2.58937461194798,
12.5793271277669));
#424110=CARTESIAN_POINT('Ctrl Pts',(0.655068759906819,2.58985876667262,
12.5785808224116));
#424111=CARTESIAN_POINT('Ctrl Pts',(0.656080182756492,2.59046106201725,
12.5777485681082));
#424112=CARTESIAN_POINT('Ctrl Pts',(0.65758731361215,2.59135854806713,12.576508418016));
#424113=CARTESIAN_POINT('Ctrl Pts',(0.658822266305905,2.59250489502811,
12.5750928681475));
#424114=CARTESIAN_POINT('Ctrl Pts',(0.659632051107192,2.59367958913582,
12.5737548217797));
#424115=CARTESIAN_POINT('Ctrl Pts',(0.659632051107192,2.59367958913582,
12.5737548217797));
#424116=CARTESIAN_POINT('Ctrl Pts',(0.674352947271195,2.58653124030665,
12.5770542771492));
#424117=CARTESIAN_POINT('Ctrl Pts',(0.68111781325818,2.59562493167692,12.5893111709658));
#424118=CARTESIAN_POINT('Ctrl Pts',(0.674369484362452,2.61357489047098,
12.5508408821982));
#424119=CARTESIAN_POINT('Ctrl Pts',(0.689134586254481,2.60640150279514,
12.55409748406));
#424120=CARTESIAN_POINT('Ctrl Pts',(0.695908082477892,2.61550679538659,
12.5663972313419));
#424121=CARTESIAN_POINT('Ctrl Pts',(0.689093468804328,2.63345005451928,
12.52790050457));
#424122=CARTESIAN_POINT('Ctrl Pts',(0.703887914880779,2.62623370900147,
12.5311362602938));
#424123=CARTESIAN_POINT('Ctrl Pts',(0.710683430746334,2.6353686015628,12.5434568539655));
#424124=CARTESIAN_POINT('Ctrl Pts',(0.703805060705893,2.65330663796353,
12.5049357605811));
#424125=CARTESIAN_POINT('Ctrl Pts',(0.718615884360165,2.64603182609852,
12.5081700652078));
#424126=CARTESIAN_POINT('Ctrl Pts',(0.725445026675419,2.65521192111564,
12.5204921097672));
#424127=CARTESIAN_POINT('Ctrl Pts',(0.702839041189222,2.65200277591434,
12.5064436508395));
#424128=CARTESIAN_POINT('Ctrl Pts',(0.704054482318549,2.65189530195598,
12.5062361689309));
#424129=CARTESIAN_POINT('Ctrl Pts',(0.705313858701969,2.65173170872469,
12.5061871075061));
#424130=CARTESIAN_POINT('Ctrl Pts',(0.706522024710137,2.65150509994767,
12.5063648335164));
#424131=CARTESIAN_POINT('Ctrl Pts',(0.707070848233817,2.65140216026334,
12.5064455676329));
#424132=CARTESIAN_POINT('Ctrl Pts',(0.707616718640117,2.65128456475662,
12.506574497099));
#424133=CARTESIAN_POINT('Ctrl Pts',(0.70813600931742,2.65115632819037,12.5067492519495));
#424134=CARTESIAN_POINT('Ctrl Pts',(0.709179544090808,2.65089863183273,
12.5071004286051));
#424135=CARTESIAN_POINT('Ctrl Pts',(0.710153916667244,2.65058770506602,
12.5076537929612));
#424136=CARTESIAN_POINT('Ctrl Pts',(0.710988870660144,2.65025589536758,
12.5083435010503));
#424137=CARTESIAN_POINT('Ctrl Pts',(0.711041436003802,2.65023500596412,
12.5083869222963));
#424138=CARTESIAN_POINT('Ctrl Pts',(0.711093450092954,2.65021402042289,
12.5084308732336));
#424139=CARTESIAN_POINT('Ctrl Pts',(0.711144896329939,2.65019294141042,
12.5084753333615));
#424140=CARTESIAN_POINT('Ctrl Pts',(0.711557563052756,2.65002385990895,
12.508831962269));
#424141=CARTESIAN_POINT('Ctrl Pts',(0.711942560208617,2.64984652545407,
12.509227847131));
#424142=CARTESIAN_POINT('Ctrl Pts',(0.712289611268568,2.64966875435332,
12.5096423454524));
#424143=CARTESIAN_POINT('Ctrl Pts',(0.713377115692091,2.64911169840178,
12.5109411997424));
#424144=CARTESIAN_POINT('Ctrl Pts',(0.714163316923655,2.64852469779433,
12.5124831113042));
#424145=CARTESIAN_POINT('Ctrl Pts',(0.71473052949045,2.64795444488592,12.5140723025008));
#424146=CARTESIAN_POINT('Ctrl Pts',(0.714783677929208,2.64790101156382,
12.5142212114565));
#424147=CARTESIAN_POINT('Ctrl Pts',(0.714834932915229,2.6478477299068,12.5143705582413));
#424148=CARTESIAN_POINT('Ctrl Pts',(0.714884378630678,2.64779464249544,
12.5145201959299));
#424149=CARTESIAN_POINT('Ctrl Pts',(0.715519582462606,2.64711265565761,
12.5164425148273));
#424150=CARTESIAN_POINT('Ctrl Pts',(0.715885820466335,2.64644667705136,
12.5184635205941));
#424151=CARTESIAN_POINT('Ctrl Pts',(0.716073260208669,2.64579391589766,
12.5205025929158));
#424152=CARTESIAN_POINT('Ctrl Pts',(0.71618198268864,2.64541528855548,12.5216853356836));
#424153=CARTESIAN_POINT('Ctrl Pts',(0.716230817588929,2.64504192558589,
12.5228750347131));
#424154=CARTESIAN_POINT('Ctrl Pts',(0.71623720118249,2.64467920379404,12.5240609649613));
#424155=CARTESIAN_POINT('Ctrl Pts',(0.716252869370419,2.6437889226153,12.5269717671326));
#424156=CARTESIAN_POINT('Ctrl Pts',(0.716002844697329,2.64293750811518,
12.5299036066169));
#424157=CARTESIAN_POINT('Ctrl Pts',(0.715573117761601,2.64211422998061,
12.5328133004019));
#424158=CARTESIAN_POINT('Ctrl Pts',(0.7153668238102,2.64171900853796,12.5342101228451));
#424159=CARTESIAN_POINT('Ctrl Pts',(0.715118909211944,2.64133100691601,
12.5356023438238));
#424160=CARTESIAN_POINT('Ctrl Pts',(0.714837180221191,2.64095229173885,
12.5369868989719));
#424161=CARTESIAN_POINT('Origin',(8.32709028079248,12.8648684166111,-1.24137497597455));
#424162=CARTESIAN_POINT('Ctrl Pts',(0.611112641136512,2.66682389372473,
12.5369868989719));
#424163=CARTESIAN_POINT('Ctrl Pts',(0.608849360456181,2.68199494722301,
12.5369868989719));
#424164=CARTESIAN_POINT('Ctrl Pts',(0.593831540370921,2.68511718737588,
12.5369868989719));
#424165=CARTESIAN_POINT('Ctrl Pts',(0.610347498262984,2.67195229337386,
12.5218025310016));
#424166=CARTESIAN_POINT('Ctrl Pts',(0.605393606744313,2.68268145096083,
12.5216901060418));
#424167=CARTESIAN_POINT('Ctrl Pts',(0.593877323020444,2.68510768589965,
12.5161920673678));
#424168=CARTESIAN_POINT('Ctrl Pts',(0.614671175307676,2.67615251813078,
12.5042015548894));
#424169=CARTESIAN_POINT('Ctrl Pts',(0.61093651633559,2.68138985212617,12.4980677368513));
#424170=CARTESIAN_POINT('Ctrl Pts',(0.604308608374317,2.68289371906861,
12.4907278922777));
#424171=CARTESIAN_POINT('Ctrl Pts',(0.626887213763669,2.67095565569782,
12.506463626192));
#424172=CARTESIAN_POINT('Ctrl Pts',(0.628382203852189,2.67732530584298,
12.4999376786891));
#424173=CARTESIAN_POINT('Ctrl Pts',(0.628363944721972,2.67724750982792,
12.4906970594712));
#424174=CARTESIAN_POINT('Origin',(0.589353444051444,2.66357776646088,12.5369868989719));
#424175=CARTESIAN_POINT('Origin',(0.589353444051444,2.66357776646088,14.));
#424176=CARTESIAN_POINT('Origin',(0.589353444051445,2.66357776646088,13.7435492065112));
#424177=CARTESIAN_POINT('Ctrl Pts',(0.614806308536257,2.64238311516042,
13.793642941384));
#424178=CARTESIAN_POINT('Ctrl Pts',(0.613217546125108,2.65307806971884,
13.8071662555867));
#424179=CARTESIAN_POINT('Ctrl Pts',(0.596187590708747,2.65307953663824,
13.8103758687955));
#424180=CARTESIAN_POINT('Ctrl Pts',(0.612322618541459,2.65881762121425,
13.7804579775005));
#424181=CARTESIAN_POINT('Ctrl Pts',(0.610352198599527,2.67201273837864,
13.7901904343351));
#424182=CARTESIAN_POINT('Ctrl Pts',(0.594803873693005,2.67456332983262,
13.7927914348263));
#424183=CARTESIAN_POINT('Ctrl Pts',(0.61086037673216,2.66849323342245,13.7597120340895));
#424184=CARTESIAN_POINT('Ctrl Pts',(0.608574378398752,2.68376285364013,
13.7635825532445));
#424185=CARTESIAN_POINT('Ctrl Pts',(0.593962387801594,2.68723065509545,
13.7651073818884));
#424186=CARTESIAN_POINT('Ctrl Pts',(0.611146717159145,2.66659852700566,
13.7381884353898));
#424187=CARTESIAN_POINT('Ctrl Pts',(0.608915115801662,2.68151086639315,
13.7368803041982));
#424188=CARTESIAN_POINT('Ctrl Pts',(0.594126682599713,2.68474998364179,
13.7363986145813));
#424189=CARTESIAN_POINT('Origin',(0.592450680699679,2.64308346446701,13.7902182540695));
#424190=CARTESIAN_POINT('Ctrl Pts',(0.619548907359073,2.61100168825963,
13.8235227101244));
#424191=CARTESIAN_POINT('Ctrl Pts',(0.617835284454321,2.62237033746962,
13.8358800583119));
#424192=CARTESIAN_POINT('Ctrl Pts',(0.601271314044061,2.6228811537816,13.8390832900376));
#424193=CARTESIAN_POINT('Ctrl Pts',(0.617766570154019,2.6227953485643,13.8124254819053));
#424194=CARTESIAN_POINT('Ctrl Pts',(0.61604961914282,2.63418607548845,13.8247886449158));
#424195=CARTESIAN_POINT('Ctrl Pts',(0.599464194081463,2.63468050105046,
13.8279860620657));
#424196=CARTESIAN_POINT('Ctrl Pts',(0.615985031734527,2.63458372333411,
13.8013225099955));
#424197=CARTESIAN_POINT('Ctrl Pts',(0.61426556472429,2.64599115367724,13.8136962257787));
#424198=CARTESIAN_POINT('Ctrl Pts',(0.597658178658591,2.6464744268367,13.8168830918626));
#424199=CARTESIAN_POINT('Ctrl Pts',(0.614204261021079,2.6463670182211,13.7902140179785));
#424200=CARTESIAN_POINT('Ctrl Pts',(0.612483037039116,2.65778612893728,
13.802602731458));
#424201=CARTESIAN_POINT('Ctrl Pts',(0.595853226194451,2.65826314444222,
13.8057746032558));
#424202=CARTESIAN_POINT('Origin',(0.59779532889661,2.60771812218318,13.8235269408515));
#424203=CARTESIAN_POINT('Ctrl Pts',(0.68111781325818,2.59562493167692,13.8235269408515));
#424204=CARTESIAN_POINT('Ctrl Pts',(0.688165308961509,2.60509854889014,
13.8362179249168));
#424205=CARTESIAN_POINT('Ctrl Pts',(0.70333607495321,2.59725566273247,13.8391868794938));
#424206=CARTESIAN_POINT('Ctrl Pts',(0.674669661448873,2.58695698428885,
13.8400110824519));
#424207=CARTESIAN_POINT('Ctrl Pts',(0.683064833875491,2.59251062658824,
13.8494522556837));
#424208=CARTESIAN_POINT('Ctrl Pts',(0.692634088968283,2.58305773050263,
13.85569149686));
#424209=CARTESIAN_POINT('Ctrl Pts',(0.660447367829172,2.57901191725071,
13.8586819406588));
#424210=CARTESIAN_POINT('Ctrl Pts',(0.664674764973042,2.5779702085472,13.868010383617));
#424211=CARTESIAN_POINT('Ctrl Pts',(0.668953595524655,2.56999622109403,
13.8744918421245));
#424212=CARTESIAN_POINT('Ctrl Pts',(0.630077400834271,2.58654428757324,
13.8587686893867));
#424213=CARTESIAN_POINT('Ctrl Pts',(0.625887614013172,2.5875766704061,13.8680909899357));
#424214=CARTESIAN_POINT('Ctrl Pts',(0.618397138453611,2.58253790295787,
13.8745789365163));
#424215=CARTESIAN_POINT('Ctrl Pts',(0.621165287788283,2.6003061629184,13.8400379222776));
#424216=CARTESIAN_POINT('Ctrl Pts',(0.616363019527336,2.60914971726367,
13.8494748685453));
#424217=CARTESIAN_POINT('Ctrl Pts',(0.603478135114092,2.60531033464119,
13.8557104837033));
#424218=CARTESIAN_POINT('Ctrl Pts',(0.619548319917159,2.61100558037594,
13.8235269408542));
#424219=CARTESIAN_POINT('Ctrl Pts',(0.617783928929597,2.62268049122072,
13.8362179249195));
#424220=CARTESIAN_POINT('Ctrl Pts',(0.600707111575873,2.62289336001569,
13.8391868794965));
#424221=CARTESIAN_POINT('Origin',(0.698769297965203,2.58249385831494,13.8235269408515));
#424222=CARTESIAN_POINT('Ctrl Pts',(0.702463554798479,2.62431900742022,
13.7902140241682));
#424223=CARTESIAN_POINT('Ctrl Pts',(0.709352661560167,2.63358716815571,
13.8026027327198));
#424224=CARTESIAN_POINT('Ctrl Pts',(0.72425314951107,2.62618761471654,13.8057746032556));
#424225=CARTESIAN_POINT('Ctrl Pts',(0.695350633661023,2.61475744187296,
13.8013225161808));
#424226=CARTESIAN_POINT('Ctrl Pts',(0.702232696898884,2.62401612069207,
13.8136962270464));
#424227=CARTESIAN_POINT('Ctrl Pts',(0.717116337306784,2.61663263550401,
13.8168830918628));
#424228=CARTESIAN_POINT('Ctrl Pts',(0.688234646079274,2.60519175424879,
13.8124254880875));
#424229=CARTESIAN_POINT('Ctrl Pts',(0.695106633740426,2.61443687515799,
13.8247886461868));
#424230=CARTESIAN_POINT('Ctrl Pts',(0.709976137757868,2.60707355983987,
13.8279860620656));
#424231=CARTESIAN_POINT('Ctrl Pts',(0.681115467911512,2.59562177766984,
13.8235227163065));
#424232=CARTESIAN_POINT('Ctrl Pts',(0.687974135916385,2.60484897965289,
13.8358800595847));
#424233=CARTESIAN_POINT('Ctrl Pts',(0.702832413857569,2.59751021903401,
13.8390832900376));
#424234=CARTESIAN_POINT('Origin',(0.720117392276593,2.61119109805108,13.7902182540695));
#424235=CARTESIAN_POINT('Ctrl Pts',(0.714676131891023,2.64073575582309,
13.7382347919292));
#424236=CARTESIAN_POINT('Ctrl Pts',(0.723663779860099,2.65285763903972,
13.7369371795942));
#424237=CARTESIAN_POINT('Ctrl Pts',(0.738247168518024,2.64875050472583,
13.7364597369711));
#424238=CARTESIAN_POINT('Ctrl Pts',(0.715805140427811,2.64225342960495,
13.7595490285574));
#424239=CARTESIAN_POINT('Ctrl Pts',(0.725008033619357,2.65466393174321,
13.7633824266926));
#424240=CARTESIAN_POINT('Ctrl Pts',(0.739542365924913,2.65083681210318,
13.7648920890506));
#424241=CARTESIAN_POINT('Ctrl Pts',(0.710047258735931,2.63451337646721,
13.780380659011));
#424242=CARTESIAN_POINT('Ctrl Pts',(0.718003095646263,2.64525123216844,
13.7901039518744));
#424243=CARTESIAN_POINT('Ctrl Pts',(0.732936153760743,2.64020254751053,
13.7926933640891));
#424244=CARTESIAN_POINT('Ctrl Pts',(0.70003877509647,2.62105943627068,13.7936647693663));
#424245=CARTESIAN_POINT('Ctrl Pts',(0.706470068796747,2.62975494047029,
13.8072068914933));
#424246=CARTESIAN_POINT('Ctrl Pts',(0.721511278945734,2.6217295889452,13.8104111085397));
#424247=CARTESIAN_POINT('Origin',(0.732488664928214,2.62782121837687,13.7435492065112));
#424248=CARTESIAN_POINT('Origin',(0.732488664928214,2.62782121837687,14.));
#424249=CARTESIAN_POINT('Origin',(0.732488664928214,2.62782121837687,12.5369868989719));
#424250=CARTESIAN_POINT('Ctrl Pts',(0.702834331796678,2.6519850061362,12.506462012331));
#424251=CARTESIAN_POINT('Ctrl Pts',(0.704509383731982,2.65830543246707,
12.4999388158272));
#424252=CARTESIAN_POINT('Ctrl Pts',(0.704489565670892,2.65823065353485,
12.4907030323752));
#424253=CARTESIAN_POINT('Ctrl Pts',(0.716058622297308,2.65082452179361,
12.5042014951932));
#424254=CARTESIAN_POINT('Ctrl Pts',(0.721814561792379,2.65368987650902,
12.4980716682127));
#424255=CARTESIAN_POINT('Ctrl Pts',(0.72836684296802,2.65190293033714,12.4907355092743));
#424256=CARTESIAN_POINT('Ctrl Pts',(0.717901086419768,2.64508596559864,
12.5218047446509));
#424257=CARTESIAN_POINT('Ctrl Pts',(0.727314683149728,2.65222060416988,
12.5216906929434));
#424258=CARTESIAN_POINT('Ctrl Pts',(0.738614337651426,2.64895126746769,
12.5161988840776));
#424259=CARTESIAN_POINT('Ctrl Pts',(0.714814277823711,2.64092144892752,
12.5369868989719));
#424260=CARTESIAN_POINT('Ctrl Pts',(0.723942691236055,2.65323719495015,
12.5369868989719));
#424261=CARTESIAN_POINT('Ctrl Pts',(0.738657573741734,2.64893861793388,
12.5369868989719));
#424262=CARTESIAN_POINT('Origin',(1.24861436930101E-31,-1.53597860469545E-32,
12.5));
#424263=CARTESIAN_POINT('Origin',(0.890418978460709,2.53147077887094,12.5));
#424264=CARTESIAN_POINT('',(0.890418978460709,2.53147077887094,12.5893111709658));
#424265=CARTESIAN_POINT('',(0.890418978460709,2.53147077887094,13.8235269408515));
#424266=CARTESIAN_POINT('',(0.890418978460709,2.53147077887094,12.5));
#424267=CARTESIAN_POINT('',(0.914035130200043,2.55833246303679,13.7902182540695));
#424268=CARTESIAN_POINT('',(0.890418978460709,2.53147077887094,13.8235269408515));
#424269=CARTESIAN_POINT('',(0.92772074765553,2.57389887443869,13.7435492065112));
#424270=CARTESIAN_POINT('Origin',(0.882695002474742,2.52268580177247,13.7445212918696));
#424271=CARTESIAN_POINT('',(0.92772074765553,2.57389887443869,12.5369868989719));
#424272=CARTESIAN_POINT('',(0.92772074765553,2.57389887443869,12.5));
#424273=CARTESIAN_POINT('Ctrl Pts',(0.92772074765553,2.57389887443869,12.5369868989719));
#424274=CARTESIAN_POINT('Ctrl Pts',(0.915295893137825,2.55976649074023,
12.5544431401645));
#424275=CARTESIAN_POINT('Ctrl Pts',(0.902862152033936,2.54562399918533,
12.5718848856037));
#424276=CARTESIAN_POINT('Ctrl Pts',(0.890418978460709,2.53147077887094,
12.5893111709658));
#424277=CARTESIAN_POINT('Origin',(0.811514909013153,2.82617583634627,12.5));
#424278=CARTESIAN_POINT('',(0.826447302606703,2.60818060292637,13.7435492065112));
#424279=CARTESIAN_POINT('',(0.827863757583178,2.58750204049156,13.7902182540695));
#424280=CARTESIAN_POINT('Origin',(0.831585956448851,2.53316235238502,13.7418732680438));
#424281=CARTESIAN_POINT('',(0.830308018192183,2.5518187350214,13.8235269408515));
#424282=CARTESIAN_POINT('',(0.827863757583178,2.58750204049156,13.7902182540695));
#424283=CARTESIAN_POINT('',(0.830308018192183,2.5518187350214,12.5893111709658));
#424284=CARTESIAN_POINT('',(0.830308018192183,2.5518187350214,12.5));
#424285=CARTESIAN_POINT('',(0.826447302606703,2.60818060292637,12.5369868989719));
#424286=CARTESIAN_POINT('Ctrl Pts',(0.830308018192183,2.5518187350214,12.5893111709658));
#424287=CARTESIAN_POINT('Ctrl Pts',(0.829020155573762,2.57062000156696,
12.5718848856037));
#424288=CARTESIAN_POINT('Ctrl Pts',(0.827733269211485,2.58940701593086,
12.5544431401645));
#424289=CARTESIAN_POINT('Ctrl Pts',(0.826447302606703,2.60818060292637,
12.5369868989719));
#424290=CARTESIAN_POINT('',(0.826447302606703,2.60818060292637,12.5));
#424291=CARTESIAN_POINT('Origin',(0.864602655857793,2.55416787366878,12.5));
#424292=CARTESIAN_POINT('',(0.854647365963043,2.52126677375875,13.8587068136939));
#424293=CARTESIAN_POINT('Ctrl Pts',(0.830308018185601,2.5518187350208,13.8235269408542));
#424294=CARTESIAN_POINT('Ctrl Pts',(0.830427767762972,2.55007053324016,
13.8262006681044));
#424295=CARTESIAN_POINT('Ctrl Pts',(0.830723647120603,2.54829337724314,
13.8288634856214));
#424296=CARTESIAN_POINT('Ctrl Pts',(0.831182814559629,2.54649085824381,
13.8314912288862));
#424297=CARTESIAN_POINT('Ctrl Pts',(0.831656168828339,2.54463264707671,
13.8342001611531));
#424298=CARTESIAN_POINT('Ctrl Pts',(0.832303101505432,2.54274529475008,
13.8368750301949));
#424299=CARTESIAN_POINT('Ctrl Pts',(0.833153834423097,2.54082371138719,
13.8394886372969));
#424300=CARTESIAN_POINT('Ctrl Pts',(0.833219538589919,2.54067530284296,
13.8396904925131));
#424301=CARTESIAN_POINT('Ctrl Pts',(0.833286479888402,2.54052669545863,
13.8398919674349));
#424302=CARTESIAN_POINT('Ctrl Pts',(0.833354683061843,2.54037789061465,
13.8400930404591));
#424303=CARTESIAN_POINT('Ctrl Pts',(0.834417334388897,2.5380594110345,13.8432258934518));
#424304=CARTESIAN_POINT('Ctrl Pts',(0.835779869680757,2.53570435807089,
13.8462331177034));
#424305=CARTESIAN_POINT('Ctrl Pts',(0.837481348921467,2.53343784965551,
13.8489036603661));
#424306=CARTESIAN_POINT('Ctrl Pts',(0.83803809273014,2.53269622172531,13.849777493004));
#424307=CARTESIAN_POINT('Ctrl Pts',(0.838631110354884,2.53196432345828,
13.85061494757));
#424308=CARTESIAN_POINT('Ctrl Pts',(0.839261712445912,2.53124724973237,
13.8514076489583));
#424309=CARTESIAN_POINT('Ctrl Pts',(0.840595526814868,2.52973053538457,
13.8530843267192));
#424310=CARTESIAN_POINT('Ctrl Pts',(0.842230724782893,2.52813311568002,
13.8546805203176));
#424311=CARTESIAN_POINT('Ctrl Pts',(0.844167747680612,2.52664530684441,
13.8559412814274));
#424312=CARTESIAN_POINT('Ctrl Pts',(0.844426984163462,2.52644618977143,
13.8561100121513));
#424313=CARTESIAN_POINT('Ctrl Pts',(0.8446915515492,2.52624901986648,13.8562727473908));
#424314=CARTESIAN_POINT('Ctrl Pts',(0.844961379298549,2.52605422829737,
13.8564289040185));
#424315=CARTESIAN_POINT('Ctrl Pts',(0.846185045063571,2.52517085075368,
13.8571370725437));
#424316=CARTESIAN_POINT('Ctrl Pts',(0.847539737180612,2.52432270477111,
13.8577210840554));
#424317=CARTESIAN_POINT('Ctrl Pts',(0.848988372275861,2.52356763294074,
13.8581177131616));
#424318=CARTESIAN_POINT('Ctrl Pts',(0.849396357779184,2.52335497872453,
13.8582294175695));
#424319=CARTESIAN_POINT('Ctrl Pts',(0.849811683285629,2.52314956859438,
13.8583265086086));
#424320=CARTESIAN_POINT('Ctrl Pts',(0.850233265717106,2.52295233638922,
13.8584082369006));
#424321=CARTESIAN_POINT('Ctrl Pts',(0.850838966619347,2.5226689666003,13.8585256585398));
#424322=CARTESIAN_POINT('Ctrl Pts',(0.851465250364158,2.52239924759507,
13.8586122832068));
#424323=CARTESIAN_POINT('Ctrl Pts',(0.852096160270757,2.52215091117732,
13.8586682984299));
#424324=CARTESIAN_POINT('Ctrl Pts',(0.852600825655947,2.52195226665992,
13.8587131050557));
#424325=CARTESIAN_POINT('Ctrl Pts',(0.85311393920145,2.52176489138891,13.8587357943552));
#424326=CARTESIAN_POINT('Ctrl Pts',(0.853635735599124,2.52158923881833,
13.8587355499465));
#424327=CARTESIAN_POINT('Ctrl Pts',(0.853972985051072,2.52147571037424,
13.8587353919793));
#424328=CARTESIAN_POINT('Ctrl Pts',(0.854310202321688,2.52136826993659,
13.8587257282814));
#424329=CARTESIAN_POINT('Ctrl Pts',(0.854647365963043,2.52126677375875,
13.8587068136939));
#424330=CARTESIAN_POINT('Ctrl Pts',(0.854647365963043,2.52126677375875,
13.8587068136939));
#424331=CARTESIAN_POINT('Ctrl Pts',(0.855756278799083,2.52093295836288,
13.8586446046466));
#424332=CARTESIAN_POINT('Ctrl Pts',(0.856864612969799,2.5206633634954,13.858482427929));
#424333=CARTESIAN_POINT('Ctrl Pts',(0.857971611869124,2.52045358308046,
13.8582284286032));
#424334=CARTESIAN_POINT('Ctrl Pts',(0.859107263968355,2.5202383727774,13.8579678548414));
#424335=CARTESIAN_POINT('Ctrl Pts',(0.860244570045428,2.52008709260314,
13.857615680862));
#424336=CARTESIAN_POINT('Ctrl Pts',(0.861337415022675,2.51999610159688,
13.8571944833187));
#424337=CARTESIAN_POINT('Ctrl Pts',(0.864064721430431,2.51976902423498,
13.8561433417727));
#424338=CARTESIAN_POINT('Ctrl Pts',(0.866642299710296,2.51990202881707,
13.8546163505474));
#424339=CARTESIAN_POINT('Ctrl Pts',(0.86894248141846,2.52023245423809,13.8528973491086));
#424340=CARTESIAN_POINT('Ctrl Pts',(0.869362690680508,2.52029281808754,
13.8525833129072));
#424341=CARTESIAN_POINT('Ctrl Pts',(0.869773724580859,2.52035965585248,
13.8522628768812));
#424342=CARTESIAN_POINT('Ctrl Pts',(0.870174930455481,2.52043184864519,
13.851937733538));
#424343=CARTESIAN_POINT('Ctrl Pts',(0.872625039067083,2.52087272001402,
13.8499521282529));
#424344=CARTESIAN_POINT('Ctrl Pts',(0.874951396165398,2.52156112858452,
13.847639871647));
#424345=CARTESIAN_POINT('Ctrl Pts',(0.877054534010571,2.52238385568447,
13.8452109780794));
#424346=CARTESIAN_POINT('Ctrl Pts',(0.878000779259908,2.52275401763635,
13.8441181685877));
#424347=CARTESIAN_POINT('Ctrl Pts',(0.878902315069305,2.52315083274127,
13.8430021611332));
#424348=CARTESIAN_POINT('Ctrl Pts',(0.879752936828771,2.52356231635773,
13.8418824960098));
#424349=CARTESIAN_POINT('Ctrl Pts',(0.881757448726344,2.52453198800752,
13.8392439765549));
#424350=CARTESIAN_POINT('Ctrl Pts',(0.88357669531762,2.52562606661625,13.8364981347964));
#424351=CARTESIAN_POINT('Ctrl Pts',(0.885233124112882,2.52681811975228,
13.8336931113419));
#424352=CARTESIAN_POINT('Ctrl Pts',(0.886846380566513,2.52797910380439,
13.8309611966328));
#424353=CARTESIAN_POINT('Ctrl Pts',(0.888306482752718,2.52923464334691,
13.8281701127186));
#424354=CARTESIAN_POINT('Ctrl Pts',(0.889601180545386,2.53058168039367,
13.8253580685121));
#424355=CARTESIAN_POINT('Ctrl Pts',(0.88988187242412,2.53087371947918,13.8247484142933));
#424356=CARTESIAN_POINT('Ctrl Pts',(0.890154619289783,2.53117008921438,
13.8241378483365));
#424357=CARTESIAN_POINT('Ctrl Pts',(0.890418978460709,2.53147077887094,
13.8235269408515));
#424358=CARTESIAN_POINT('',(0.853465191995009,2.5216478794746,12.5969504640361));
#424359=CARTESIAN_POINT('Origin',(0.864613449649006,2.55419914948822,12.584524458991));
#424360=CARTESIAN_POINT('Origin',(0.864613449649006,2.55419914948822,12.584524458991));
#424361=CARTESIAN_POINT('Ctrl Pts',(0.830308018192183,2.5518187350214,12.5893111709658));
#424362=CARTESIAN_POINT('Ctrl Pts',(0.831082564866749,2.5405112723525,12.5770542771492));
#424363=CARTESIAN_POINT('Ctrl Pts',(0.847331259925621,2.53856612872316,
12.5737548217797));
#424364=CARTESIAN_POINT('Ctrl Pts',(0.828614344560504,2.57654436098097,
12.5663937883685));
#424365=CARTESIAN_POINT('Ctrl Pts',(0.829389879276917,2.56522247407308,
12.5540940315303));
#424366=CARTESIAN_POINT('Ctrl Pts',(0.845689307434817,2.56327449126019,
12.5508374392248));
#424367=CARTESIAN_POINT('Ctrl Pts',(0.826922379824748,2.60124503908716,
12.5434499600944));
#424368=CARTESIAN_POINT('Ctrl Pts',(0.827700436080648,2.58988634069314,
12.5311293540533));
#424369=CARTESIAN_POINT('Ctrl Pts',(0.844047781895784,2.58795863496758,
12.5278936106989));
#424370=CARTESIAN_POINT('Ctrl Pts',(0.825231990124768,2.62592272353936,
12.5204817579905));
#424371=CARTESIAN_POINT('Ctrl Pts',(0.826013897227463,2.61450780735084,
12.5081597038247));
#424372=CARTESIAN_POINT('Ctrl Pts',(0.842406636300544,2.61262044130881,
12.5049254088044));
#424373=CARTESIAN_POINT('Ctrl Pts',(0.826447302606703,2.60818060292637,
12.5369868989719));
#424374=CARTESIAN_POINT('Ctrl Pts',(0.826383645054817,2.60910993004145,
12.5342545179733));
#424375=CARTESIAN_POINT('Ctrl Pts',(0.826447347630837,2.61000536239243,
12.5314872231885));
#424376=CARTESIAN_POINT('Ctrl Pts',(0.826690581847834,2.61081249201388,
12.5287124745062));
#424377=CARTESIAN_POINT('Ctrl Pts',(0.826909942537789,2.61154040156883,
12.5262100684184));
#424378=CARTESIAN_POINT('Ctrl Pts',(0.827276042659319,2.61219547335019,
12.5237004536639));
#424379=CARTESIAN_POINT('Ctrl Pts',(0.827853035149533,2.61275661525529,
12.5212220730815));
#424380=CARTESIAN_POINT('Ctrl Pts',(0.828294772814625,2.6131862179263,12.5193246583486));
#424381=CARTESIAN_POINT('Ctrl Pts',(0.828865841104599,2.61356544560367,
12.517417831369));
#424382=CARTESIAN_POINT('Ctrl Pts',(0.829634953403218,2.61382550516533,
12.5155812248348));
#424383=CARTESIAN_POINT('Ctrl Pts',(0.829962599376427,2.61393629193642,
12.5147988205793));
#424384=CARTESIAN_POINT('Ctrl Pts',(0.830326430363164,2.61402582690065,
12.5140295443047));
#424385=CARTESIAN_POINT('Ctrl Pts',(0.830732331866762,2.61409084014709,
12.5132817086137));
#424386=CARTESIAN_POINT('Ctrl Pts',(0.831346608883344,2.61418922890078,
12.5121499604604));
#424387=CARTESIAN_POINT('Ctrl Pts',(0.832071634780866,2.61422651917806,
12.5110494206568));
#424388=CARTESIAN_POINT('Ctrl Pts',(0.832921188062887,2.61416811254567,
12.5100666561695));
#424389=CARTESIAN_POINT('Ctrl Pts',(0.833408999601075,2.61413457559184,
12.5095023550641));
#424390=CARTESIAN_POINT('Ctrl Pts',(0.833943459634806,2.61406844838295,
12.5089719619137));
#424391=CARTESIAN_POINT('Ctrl Pts',(0.834513766039022,2.61396463175489,
12.5085043804652));
#424392=CARTESIAN_POINT('Ctrl Pts',(0.835348335173957,2.61381270964279,
12.5078201359221));
#424393=CARTESIAN_POINT('Ctrl Pts',(0.836283656542937,2.61357448296628,
12.5072563000949));
#424394=CARTESIAN_POINT('Ctrl Pts',(0.837254239574256,2.61325789590764,
12.5068768744332));
#424395=CARTESIAN_POINT('Ctrl Pts',(0.837954096755,2.61302961484443,12.5066032824114));
#424396=CARTESIAN_POINT('Ctrl Pts',(0.838684601954986,2.61275663760459,
12.5064197834844));
#424397=CARTESIAN_POINT('Ctrl Pts',(0.839405866675194,2.61245662927027,
12.5063282718343));
#424398=CARTESIAN_POINT('Ctrl Pts',(0.840458689868784,2.61201870998238,
12.5061946931565));
#424399=CARTESIAN_POINT('Ctrl Pts',(0.841514735187592,2.61151481637794,
12.5062515701262));
#424400=CARTESIAN_POINT('Ctrl Pts',(0.842515122252634,2.61099017808463,
12.5064436508398));
#424401=CARTESIAN_POINT('',(0.847331259925621,2.53856612872316,12.5737548217797));
#424402=CARTESIAN_POINT('Origin',(0.852256586298173,2.55332218375572,12.5893111709658));
#424403=CARTESIAN_POINT('Ctrl Pts',(0.842515122252634,2.61099017808463,
12.5064436508398));
#424404=CARTESIAN_POINT('Ctrl Pts',(0.843228515136987,2.60026956903739,
12.5164271754438));
#424405=CARTESIAN_POINT('Ctrl Pts',(0.843941982335526,2.58954469647043,
12.5264061185523));
#424406=CARTESIAN_POINT('Ctrl Pts',(0.844655527409933,2.57881541028901,
12.536380305637));
#424407=CARTESIAN_POINT('Ctrl Pts',(0.845547314030407,2.56540597869594,
12.5488460165097));
#424408=CARTESIAN_POINT('Ctrl Pts',(0.846439222531624,2.55198964910518,
12.5613043021964));
#424409=CARTESIAN_POINT('Ctrl Pts',(0.847331259925621,2.53856612872316,
12.5737548217797));
#424410=CARTESIAN_POINT('Ctrl Pts',(0.890418978460709,2.53147077887094,
12.5893111709658));
#424411=CARTESIAN_POINT('Ctrl Pts',(0.882935401738845,2.52295874538841,
12.5770542771492));
#424412=CARTESIAN_POINT('Ctrl Pts',(0.868846144934049,2.53128319837605,
12.5737548217797));
#424413=CARTESIAN_POINT('Ctrl Pts',(0.883436866467923,2.5235291256655,12.5928319619712));
#424414=CARTESIAN_POINT('Ctrl Pts',(0.875960809812146,2.51995953279641,
12.5821634970842));
#424415=CARTESIAN_POINT('Ctrl Pts',(0.86630981930806,2.52838401406174,12.5773203894503));
#424416=CARTESIAN_POINT('Ctrl Pts',(0.868137645904655,2.51670871882308,
12.5969440695591));
#424417=CARTESIAN_POINT('Ctrl Pts',(0.864324288654534,2.51798027261073,
12.5878292599214));
#424418=CARTESIAN_POINT('Ctrl Pts',(0.860856031842167,2.52595495058492,
12.5813877129824));
#424419=CARTESIAN_POINT('Ctrl Pts',(0.839138848518301,2.52646807308894,
12.596957478804));
#424420=CARTESIAN_POINT('Ctrl Pts',(0.842924049391841,2.52520599246717,
12.5878468778671));
#424421=CARTESIAN_POINT('Ctrl Pts',(0.850478862936143,2.52945361230049,
12.5814011370086));
#424422=CARTESIAN_POINT('Ctrl Pts',(0.831031712782593,2.54125365245881,
12.5928371701607));
#424423=CARTESIAN_POINT('Ctrl Pts',(0.834805073620663,2.53388501529245,
12.5821692192952));
#424424=CARTESIAN_POINT('Ctrl Pts',(0.847585643775695,2.5347101507239,12.5773318885715));
#424425=CARTESIAN_POINT('Ctrl Pts',(0.830308018192128,2.55181873502139,
12.5893111709658));
#424426=CARTESIAN_POINT('Ctrl Pts',(0.831082564866694,2.54051127235249,
12.5770542771492));
#424427=CARTESIAN_POINT('Ctrl Pts',(0.847331259925566,2.53856612872316,
12.5737548217797));
#424428=CARTESIAN_POINT('',(0.868846144934049,2.53128319837605,12.5737548217797));
#424429=CARTESIAN_POINT('Origin',(0.873896531994843,2.54599691954156,12.5893111709658));
#424430=CARTESIAN_POINT('Ctrl Pts',(0.847331259925566,2.53856612872316,
12.5737548217797));
#424431=CARTESIAN_POINT('Ctrl Pts',(0.847367099946014,2.53756461231094,
12.5746934679442));
#424432=CARTESIAN_POINT('Ctrl Pts',(0.847589826421995,2.53646291890752,
12.5756680099006));
#424433=CARTESIAN_POINT('Ctrl Pts',(0.847970835434494,2.53538573006596,
12.5765688348656));
#424434=CARTESIAN_POINT('Ctrl Pts',(0.848071703352644,2.53510055624503,
12.5768073183026));
#424435=CARTESIAN_POINT('Ctrl Pts',(0.848183408832736,2.53481707570617,
12.5770407398754));
#424436=CARTESIAN_POINT('Ctrl Pts',(0.848304891762323,2.5345374097613,12.5772674179684));
#424437=CARTESIAN_POINT('Ctrl Pts',(0.848803424854977,2.5333897363484,12.5781976435658));
#424438=CARTESIAN_POINT('Ctrl Pts',(0.849505277493991,2.53224561207373,
12.5790594849312));
#424439=CARTESIAN_POINT('Ctrl Pts',(0.850404221039561,2.53120754019494,
12.5797571720116));
#424440=CARTESIAN_POINT('Ctrl Pts',(0.850989915082629,2.53053119904016,
12.580211740231));
#424441=CARTESIAN_POINT('Ctrl Pts',(0.851700082169469,2.52988143008961,
12.5806009430798));
#424442=CARTESIAN_POINT('Ctrl Pts',(0.852496689050906,2.52931704534428,
12.5808812374708));
#424443=CARTESIAN_POINT('Ctrl Pts',(0.853181238633642,2.52883205161534,
12.5811221033394));
#424444=CARTESIAN_POINT('Ctrl Pts',(0.853943700308057,2.52840027395526,
12.581287365893));
#424445=CARTESIAN_POINT('Ctrl Pts',(0.854745148192489,2.52805333797847,
12.581359338449));
#424446=CARTESIAN_POINT('Ctrl Pts',(0.854856532899159,2.52800512104164,
12.5813693411482));
#424447=CARTESIAN_POINT('Ctrl Pts',(0.854968666521613,2.5279584831078,12.5813775999465));
#424448=CARTESIAN_POINT('Ctrl Pts',(0.855081441437813,2.52791344781096,
12.5813841266931));
#424449=CARTESIAN_POINT('Ctrl Pts',(0.855272777722989,2.52783703998297,
12.5813952001081));
#424450=CARTESIAN_POINT('Ctrl Pts',(0.855467467271982,2.52776529909069,
12.5814007534795));
#424451=CARTESIAN_POINT('Ctrl Pts',(0.855665493478638,2.52769844142603,
12.5814005856065));
#424452=CARTESIAN_POINT('Ctrl Pts',(0.85657198002948,2.52739239317685,12.5813998171494));
#424453=CARTESIAN_POINT('Ctrl Pts',(0.857485645370209,2.5272094963594,12.58127954464));
#424454=CARTESIAN_POINT('Ctrl Pts',(0.858395494354219,2.52712177558977,
12.5810700125799));
#424455=CARTESIAN_POINT('Ctrl Pts',(0.8594944883323,2.52701581888787,12.5808169217085));
#424456=CARTESIAN_POINT('Ctrl Pts',(0.860589619754366,2.52706537217095,
12.5804173076348));
#424457=CARTESIAN_POINT('Ctrl Pts',(0.86158609033339,2.52724007692988,12.5799304713245));
#424458=CARTESIAN_POINT('Ctrl Pts',(0.862821031301405,2.52745659116387,
12.5793271277669));
#424459=CARTESIAN_POINT('Ctrl Pts',(0.863986605207165,2.52784703998076,
12.5785808224116));
#424460=CARTESIAN_POINT('Ctrl Pts',(0.865043755292766,2.52836489088548,
12.5777485681082));
#424461=CARTESIAN_POINT('Ctrl Pts',(0.86661902473975,2.5291365454683,12.576508418016));
#424462=CARTESIAN_POINT('Ctrl Pts',(0.867943306149779,2.53017841794506,
12.5750928681475));
#424463=CARTESIAN_POINT('Ctrl Pts',(0.868846144934049,2.53128319837605,
12.5737548217797));
#424464=CARTESIAN_POINT('Ctrl Pts',(0.868846144934049,2.53128319837605,
12.5737548217797));
#424465=CARTESIAN_POINT('Ctrl Pts',(0.882935401738845,2.52295874538841,
12.5770542771492));
#424466=CARTESIAN_POINT('Ctrl Pts',(0.890418978460709,2.53147077887094,
12.5893111709658));
#424467=CARTESIAN_POINT('Ctrl Pts',(0.885156192353693,2.54991106211131,
12.5508408821982));
#424468=CARTESIAN_POINT('Ctrl Pts',(0.899287466897137,2.54155805041447,
12.55409748406));
#424469=CARTESIAN_POINT('Ctrl Pts',(0.906780590746262,2.55008094307168,
12.5663972313419));
#424470=CARTESIAN_POINT('Ctrl Pts',(0.901451194333948,2.56851995176799,
12.52790050457));
#424471=CARTESIAN_POINT('Ctrl Pts',(0.915608213958567,2.56012173334445,
12.5311362602938));
#424472=CARTESIAN_POINT('Ctrl Pts',(0.923125696853579,2.56867233267479,
12.5434568539655));
#424473=CARTESIAN_POINT('Ctrl Pts',(0.9177323305173,2.58711133275317,12.5049357605811));
#424474=CARTESIAN_POINT('Ctrl Pts',(0.931900907674612,2.5786535075997,12.5081700652078));
#424475=CARTESIAN_POINT('Ctrl Pts',(0.939455589549916,2.5872464181106,12.5204921097672));
#424476=CARTESIAN_POINT('Ctrl Pts',(0.916663248489405,2.58589054875607,
12.5064436508395));
#424477=CARTESIAN_POINT('Ctrl Pts',(0.917865885213295,2.5856843626728,12.5062361689309));
#424478=CARTESIAN_POINT('Ctrl Pts',(0.919107736758615,2.58541866291777,
12.5061871075061));
#424479=CARTESIAN_POINT('Ctrl Pts',(0.920293411974997,2.58509433141703,
12.5063648335164));
#424480=CARTESIAN_POINT('Ctrl Pts',(0.920832018793759,2.58494700004379,
12.5064455676329));
#424481=CARTESIAN_POINT('Ctrl Pts',(0.921366487735811,2.58478530232069,
12.506574497099));
#424482=CARTESIAN_POINT('Ctrl Pts',(0.921873598045585,2.58461516543998,
12.5067492519495));
#424483=CARTESIAN_POINT('Ctrl Pts',(0.922892655897611,2.58427326877398,
12.5071004286051));
#424484=CARTESIAN_POINT('Ctrl Pts',(0.923838442911685,2.58388395617983,
12.5076537929612));
#424485=CARTESIAN_POINT('Ctrl Pts',(0.924643573093256,2.58348519404902,
12.5083435010503));
#424486=CARTESIAN_POINT('Ctrl Pts',(0.924694260849764,2.58346008958983,
12.5083869222963));
#424487=CARTESIAN_POINT('Ctrl Pts',(0.924744391349898,2.58343493424511,
12.5084308732336));
#424488=CARTESIAN_POINT('Ctrl Pts',(0.924793948268574,2.5834097320254,12.5084753333616));
#424489=CARTESIAN_POINT('Ctrl Pts',(0.925191460164867,2.58320757695976,
12.508831962269));
#424490=CARTESIAN_POINT('Ctrl Pts',(0.925560721870087,2.58299945172831,
12.509227847131));
#424491=CARTESIAN_POINT('Ctrl Pts',(0.925892128151208,2.58279398426298,
12.5096423454524));
#424492=CARTESIAN_POINT('Ctrl Pts',(0.926930608761967,2.58215014016275,
12.5109411997424));
#424493=CARTESIAN_POINT('Ctrl Pts',(0.927666347974835,2.58150101005229,
12.5124831113042));
#424494=CARTESIAN_POINT('Ctrl Pts',(0.9281851922826,2.58088642152345,12.5140723025008));
#424495=CARTESIAN_POINT('Ctrl Pts',(0.928233808562511,2.58082883390516,
12.5142212114565));
#424496=CARTESIAN_POINT('Ctrl Pts',(0.928280550052106,2.58077155178127,
12.5143705582413));
#424497=CARTESIAN_POINT('Ctrl Pts',(0.928325504124151,2.58071461072905,
12.5145201959299));
#424498=CARTESIAN_POINT('Ctrl Pts',(0.928903006109187,2.57998311813691,
12.5164425148273));
#424499=CARTESIAN_POINT('Ctrl Pts',(0.929213742047119,2.57928950372225,
12.5184635205941));
#424500=CARTESIAN_POINT('Ctrl Pts',(0.929347352005207,2.57862363649833,
12.5205025929157));
#424501=CARTESIAN_POINT('Ctrl Pts',(0.929424851076703,2.57823740711595,
12.5216853356836));
#424502=CARTESIAN_POINT('Ctrl Pts',(0.929443090934737,2.57786130598311,
12.5228750347131));
#424503=CARTESIAN_POINT('Ctrl Pts',(0.929419888094036,2.57749927079595,
12.5240609649613));
#424504=CARTESIAN_POINT('Ctrl Pts',(0.929362937966327,2.57661067485162,
12.5269717671326));
#424505=CARTESIAN_POINT('Ctrl Pts',(0.929044347043804,2.57578247269498,
12.5299036066169));
#424506=CARTESIAN_POINT('Ctrl Pts',(0.928548945178096,2.57499696068514,
12.5328133004019));
#424507=CARTESIAN_POINT('Ctrl Pts',(0.928311123436168,2.57461986918142,
12.5342101228451));
#424508=CARTESIAN_POINT('Ctrl Pts',(0.928032408019065,2.57425336594414,
12.5356023438238));
#424509=CARTESIAN_POINT('Ctrl Pts',(0.927720747655529,2.57389887443869,
12.5369868989719));
#424510=CARTESIAN_POINT('Origin',(9.34773057027711,12.1430337570218,-1.24095417635099));
#424511=CARTESIAN_POINT('Ctrl Pts',(0.826450119160066,2.60813890367028,
12.5369868989719));
#424512=CARTESIAN_POINT('Ctrl Pts',(0.825430951060778,2.62344395512627,
12.5369868989719));
#424513=CARTESIAN_POINT('Ctrl Pts',(0.8107175930909,2.62777989803818,12.5369868989719));
#424514=CARTESIAN_POINT('Ctrl Pts',(0.826105534417468,2.61331260524006,
12.5218025310015));
#424515=CARTESIAN_POINT('Ctrl Pts',(0.822042652512112,2.62440985058867,
12.5216901060418));
#424516=CARTESIAN_POINT('Ctrl Pts',(0.810762448943919,2.62776669646636,
12.5161920673677));
#424517=CARTESIAN_POINT('Ctrl Pts',(0.83075718209413,2.61714643427736,12.5042015548895));
#424518=CARTESIAN_POINT('Ctrl Pts',(0.827461841233387,2.62267075085312,
12.4980677368513));
#424519=CARTESIAN_POINT('Ctrl Pts',(0.820978566206095,2.62470984983164,
12.4907278922778));
#424520=CARTESIAN_POINT('Ctrl Pts',(0.842508980156334,2.61097114343314,
12.506463626192));
#424521=CARTESIAN_POINT('Ctrl Pts',(0.844518181408437,2.61719774352186,
12.4999376786891));
#424522=CARTESIAN_POINT('Ctrl Pts',(0.844493641936519,2.61712169465524,
12.4906970594712));
#424523=CARTESIAN_POINT('Origin',(0.804498734500713,2.60667715419205,12.5369868989719));
#424524=CARTESIAN_POINT('Origin',(0.804498734500713,2.60667715419205,14.));
#424525=CARTESIAN_POINT('Origin',(0.804498734500713,2.60667715419205,13.7435492065112));
#424526=CARTESIAN_POINT('Ctrl Pts',(0.828139345836136,2.58347838159699,
13.793642941384));
#424527=CARTESIAN_POINT('Ctrl Pts',(0.827427607984465,2.59426724846225,
13.8071662555867));
#424528=CARTESIAN_POINT('Ctrl Pts',(0.810454437907433,2.59565680996541,
13.8103758687955));
#424529=CARTESIAN_POINT('Ctrl Pts',(0.827003484928802,2.60006064697971,
13.7804579775005));
#424530=CARTESIAN_POINT('Ctrl Pts',(0.826115145943083,2.61337246599799,
13.790190434335));
#424531=CARTESIAN_POINT('Ctrl Pts',(0.810826453687069,2.61718190339281,
13.7927914348263));
#424532=CARTESIAN_POINT('Ctrl Pts',(0.826334760827468,2.60982325066871,
13.7597120340895));
#424533=CARTESIAN_POINT('Ctrl Pts',(0.825300984768903,2.6252283925711,13.7635825532445));
#424534=CARTESIAN_POINT('Ctrl Pts',(0.811020272377169,2.62987566808793,
13.7651073818884));
#424535=CARTESIAN_POINT('Ctrl Pts',(0.826465712317739,2.60791150932817,
13.7381884353898));
#424536=CARTESIAN_POINT('Ctrl Pts',(0.825457030529163,2.62295612536434,
13.7368803041981));
#424537=CARTESIAN_POINT('Ctrl Pts',(0.810981822744995,2.62738985931261,
13.7363986145813));
#424538=CARTESIAN_POINT('Origin',(0.805915189477188,2.58599859175724,13.7902182540695));
#424539=CARTESIAN_POINT('Ctrl Pts',(0.830308286429238,2.55181480797322,
13.8235227101244));
#424540=CARTESIAN_POINT('Ctrl Pts',(0.829527015915338,2.56328530511605,
13.8358800583119));
#424541=CARTESIAN_POINT('Ctrl Pts',(0.813059797021804,2.56514453908973,
13.8390832900376));
#424542=CARTESIAN_POINT('Ctrl Pts',(0.829493172606032,2.56371450287475,
13.8124254819052));
#424543=CARTESIAN_POINT('Ctrl Pts',(0.828710384598348,2.57520727554153,
13.8247886449157));
#424544=CARTESIAN_POINT('Ctrl Pts',(0.812220446444013,2.57705192205735,
13.8279860620657));
#424545=CARTESIAN_POINT('Ctrl Pts',(0.828678424090336,2.57560886472017,
13.8013225099955));
#424546=CARTESIAN_POINT('Ctrl Pts',(0.827894489939108,2.58711849030397,
13.8136962257787));
#424547=CARTESIAN_POINT('Ctrl Pts',(0.811381754829519,2.58895381155168,
13.8168830918626));
#424548=CARTESIAN_POINT('Ctrl Pts',(0.827864026668595,2.5874981010105,13.7902140179785));
#424549=CARTESIAN_POINT('Ctrl Pts',(0.827079293450659,2.59901951131138,
13.802602731458));
#424550=CARTESIAN_POINT('Ctrl Pts',(0.810543698121769,2.60085042355405,
13.8057746032558));
#424551=CARTESIAN_POINT('Origin',(0.808359450086194,2.55031528628708,13.8235269408515));
#424552=CARTESIAN_POINT('Ctrl Pts',(0.890418978460709,2.53147077887094,
13.8235269408515));
#424553=CARTESIAN_POINT('Ctrl Pts',(0.898215211955112,2.54033843707882,
13.8362179249168));
#424554=CARTESIAN_POINT('Ctrl Pts',(0.912696230442824,2.531285089211,13.8391868794938));
#424555=CARTESIAN_POINT('Ctrl Pts',(0.883285764163169,2.5233572575969,13.8400110824519));
#424556=CARTESIAN_POINT('Ctrl Pts',(0.892105675750976,2.52820813611993,
13.8494522556837));
#424557=CARTESIAN_POINT('Ctrl Pts',(0.90087259114951,2.51800671063957,13.85569149686));
#424558=CARTESIAN_POINT('Ctrl Pts',(0.868463197330234,2.51659787607726,
13.8586819406588));
#424559=CARTESIAN_POINT('Ctrl Pts',(0.872591619228754,2.51521506146106,
13.868010383617));
#424560=CARTESIAN_POINT('Ctrl Pts',(0.876206258320368,2.50691884238066,
13.8744918421245));
#424561=CARTESIAN_POINT('Ctrl Pts',(0.838808242003569,2.52658061731002,
13.8587686893867));
#424562=CARTESIAN_POINT('Ctrl Pts',(0.834716545137537,2.52795107149618,
13.8680909899357));
#424563=CARTESIAN_POINT('Ctrl Pts',(0.826840287192812,2.52353961342725,
13.8745789365163));
#424564=CARTESIAN_POINT('Ctrl Pts',(0.83104750387819,2.54102312109951,13.8400379222776));
#424565=CARTESIAN_POINT('Ctrl Pts',(0.826982046547405,2.5502286786926,13.8494748685453));
#424566=CARTESIAN_POINT('Ctrl Pts',(0.813827090197301,2.54745230899619,
13.8557104837033));
#424567=CARTESIAN_POINT('Ctrl Pts',(0.830308018185601,2.5518187350208,13.8235269408542));
#424568=CARTESIAN_POINT('Ctrl Pts',(0.829501111681931,2.56359861280815,
13.8362179249195));
#424569=CARTESIAN_POINT('Ctrl Pts',(0.812498466812179,2.56520269244754,
13.8391868794965));
#424570=CARTESIAN_POINT('Origin',(0.906941424926576,2.51694463820032,13.8235269408515));
#424571=CARTESIAN_POINT('Ctrl Pts',(0.914032527362825,2.55832950134457,
13.7902140241683));
#424572=CARTESIAN_POINT('Ctrl Pts',(0.92165415233143,2.56700529688334,13.8026027327198));
#424573=CARTESIAN_POINT('Ctrl Pts',(0.935901927838467,2.55841583675045,
13.8057746032556));
#424574=CARTESIAN_POINT('Ctrl Pts',(0.906163917526332,2.54937952022373,
13.8013225161808));
#424575=CARTESIAN_POINT('Ctrl Pts',(0.913777749543641,2.558046439509,13.8136962270464));
#424576=CARTESIAN_POINT('Ctrl Pts',(0.928010043278109,2.54947436739259,
13.8168830918628));
#424577=CARTESIAN_POINT('Ctrl Pts',(0.898291915461332,2.54042568068552,
13.8124254880875));
#424578=CARTESIAN_POINT('Ctrl Pts',(0.905894600332056,2.54907990842673,
13.8247886461867));
#424579=CARTESIAN_POINT('Ctrl Pts',(0.920114448745435,2.5405290913138,13.8279860620656));
#424580=CARTESIAN_POINT('Ctrl Pts',(0.890416383837143,2.53146782652609,
13.8235227163066));
#424581=CARTESIAN_POINT('Ctrl Pts',(0.898004332812819,2.54010528064054,
13.8358800595847));
#424582=CARTESIAN_POINT('Ctrl Pts',(0.912214993939689,2.5315798515525,13.8390832900376));
#424583=CARTESIAN_POINT('Origin',(0.930557576665909,2.54380632236618,13.7902182540695));
#424584=CARTESIAN_POINT('Ctrl Pts',(0.927542585513044,2.57369618596234,
13.7382347919292));
#424585=CARTESIAN_POINT('Ctrl Pts',(0.937488373841171,2.58504515786582,
13.7369371795942));
#424586=CARTESIAN_POINT('Ctrl Pts',(0.951688467901028,2.57976300814133,
13.7364597369711));
#424587=CARTESIAN_POINT('Ctrl Pts',(0.928791541869654,2.5751167851329,13.7595490285574));
#424588=CARTESIAN_POINT('Ctrl Pts',(0.938975384331029,2.58673587111851,
13.7633824266926));
#424589=CARTESIAN_POINT('Ctrl Pts',(0.953149409064946,2.58173680289031,
13.7648920890506));
#424590=CARTESIAN_POINT('Ctrl Pts',(0.922421932868273,2.56787180719496,
13.780380659011));
#424591=CARTESIAN_POINT('Ctrl Pts',(0.93122653231263,2.5779254590006,13.7901039518744));
#424592=CARTESIAN_POINT('Ctrl Pts',(0.945698387238799,2.57167639055629,
13.7926933640892));
#424593=CARTESIAN_POINT('Ctrl Pts',(0.911350130606159,2.55527841820539,
13.7936647693663));
#424594=CARTESIAN_POINT('Ctrl Pts',(0.918468789024592,2.56342077869032,
13.8072068914933));
#424595=CARTESIAN_POINT('Ctrl Pts',(0.932805810134608,2.55419613259745,
13.8104111085397));
#424596=CARTESIAN_POINT('Origin',(0.944243194121396,2.55937273376807,13.7435492065112));
#424597=CARTESIAN_POINT('Origin',(0.944243194121396,2.55937273376807,14.));
#424598=CARTESIAN_POINT('Origin',(0.944243194121396,2.55937273376807,12.5369868989719));
#424599=CARTESIAN_POINT('Ctrl Pts',(0.916657106365097,2.58587322196464,
12.506462012331));
#424600=CARTESIAN_POINT('Ctrl Pts',(0.918841758125204,2.59203608531513,
12.4999388158272));
#424601=CARTESIAN_POINT('Ctrl Pts',(0.918815910829888,2.59196317055959,
12.4907030323752));
#424602=CARTESIAN_POINT('Ctrl Pts',(0.929742803882678,2.58363869659378,
12.5042014951932));
#424603=CARTESIAN_POINT('Ctrl Pts',(0.93571314397386,2.58602535457338,12.4980716682128));
#424604=CARTESIAN_POINT('Ctrl Pts',(0.942097970272217,2.58371028257328,
12.4907355092744));
#424605=CARTESIAN_POINT('Ctrl Pts',(0.931111391753753,2.57776905704064,
12.5218047446509));
#424606=CARTESIAN_POINT('Ctrl Pts',(0.941075204795464,2.58411266016551,
12.5216906929433));
#424607=CARTESIAN_POINT('Ctrl Pts',(0.952070779336664,2.57993317516873,
12.5161988840775));
#424608=CARTESIAN_POINT('Ctrl Pts',(0.927695407488456,2.5738700010123,12.5369868989719));
#424609=CARTESIAN_POINT('Ctrl Pts',(0.937797294492868,2.58540071696883,
12.5369868989719));
#424610=CARTESIAN_POINT('Ctrl Pts',(0.952112840508009,2.57991704358246,
12.5369868989719));
#424611=CARTESIAN_POINT('Origin',(1.65186468598901E-31,-2.72002836734922E-32,
12.5));
#424612=CARTESIAN_POINT('Origin',(1.09379455227037,2.45047010569484,12.5));
#424613=CARTESIAN_POINT('',(1.09379455227037,2.45047010569484,12.5893111709658));
#424614=CARTESIAN_POINT('',(1.09379455227037,2.45047010569484,13.8235269408515));
#424615=CARTESIAN_POINT('',(1.09379455227037,2.45047010569484,12.5));
#424616=CARTESIAN_POINT('',(1.11952159984422,2.47531747421416,13.7902182540695));
#424617=CARTESIAN_POINT('',(1.09379455227037,2.45047010569484,13.8235269408515));
#424618=CARTESIAN_POINT('',(1.13443048657737,2.48971658479255,13.7435492065112));
#424619=CARTESIAN_POINT('Origin',(1.08538021998782,2.4423439356315,13.7445212918694));
#424620=CARTESIAN_POINT('',(1.13443048657737,2.48971658479255,12.5369868989719));
#424621=CARTESIAN_POINT('',(1.13443048657737,2.48971658479255,12.5));
#424622=CARTESIAN_POINT('Ctrl Pts',(1.13443048657737,2.48971658479255,12.5369868989719));
#424623=CARTESIAN_POINT('Ctrl Pts',(1.12089505426802,2.47664396642493,12.5544431401645));
#424624=CARTESIAN_POINT('Ctrl Pts',(1.10734994105773,2.46356199817319,12.5718848856037));
#424625=CARTESIAN_POINT('Ctrl Pts',(1.09379455227037,2.45047010569484,12.5893111709658));
#424626=CARTESIAN_POINT('Origin',(1.03917422769729,2.7506259705725,12.5));
#424627=CARTESIAN_POINT('',(1.03628829969026,2.53213896960501,13.7435492065112));
#424628=CARTESIAN_POINT('',(1.0360145467208,2.51141375915053,13.7902182540695));
#424629=CARTESIAN_POINT('Origin',(1.03529517123111,2.45695148811307,13.7418732680447));
#424630=CARTESIAN_POINT('',(1.03554215359081,2.47564995700462,13.8235269408515));
#424631=CARTESIAN_POINT('',(1.0360145467208,2.51141375915053,13.7902182540695));
#424632=CARTESIAN_POINT('',(1.03554215359081,2.47564995700462,12.5893111709658));
#424633=CARTESIAN_POINT('',(1.03554215359081,2.47564995700462,12.5));
#424634=CARTESIAN_POINT('',(1.03628829969026,2.53213896960501,12.5369868989719));
#424635=CARTESIAN_POINT('Ctrl Pts',(1.03554215359081,2.47564995700462,12.5893111709658));
#424636=CARTESIAN_POINT('Ctrl Pts',(1.03579105399491,2.49449363664608,12.5718848856037));
#424637=CARTESIAN_POINT('Ctrl Pts',(1.03603976572164,2.5133230319549,12.5544431401645));
#424638=CARTESIAN_POINT('Ctrl Pts',(1.03628829969026,2.53213896960501,12.5369868989719));
#424639=CARTESIAN_POINT('',(1.03628829969026,2.53213896960501,12.5));
#424640=CARTESIAN_POINT('Origin',(1.06991415528679,2.47519594774131,12.5));
#424641=CARTESIAN_POINT('',(1.05731024571616,2.44321577207398,13.8587068136939));
#424642=CARTESIAN_POINT('Ctrl Pts',(1.0355421535842,2.47564995700456,13.8235269408542));
#424643=CARTESIAN_POINT('Ctrl Pts',(1.03551901003009,2.47389781151887,13.8262006681044));
#424644=CARTESIAN_POINT('Ctrl Pts',(1.0356690501615,2.47210245194736,13.8288634856214));
#424645=CARTESIAN_POINT('Ctrl Pts',(1.03597976772654,2.47026850427233,13.8314912288862));
#424646=CARTESIAN_POINT('Ctrl Pts',(1.03630008548706,2.46837789338229,13.8342001611531));
#424647=CARTESIAN_POINT('Ctrl Pts',(1.03679102881309,2.46644409004582,13.8368750301949));
#424648=CARTESIAN_POINT('Ctrl Pts',(1.03748230410397,2.46445955796243,13.8394886372968));
#424649=CARTESIAN_POINT('Ctrl Pts',(1.03753569297148,2.46430628773583,13.8396904925131));
#424650=CARTESIAN_POINT('Ctrl Pts',(1.03759029864689,2.46415271849303,13.8398919674349));
#424651=CARTESIAN_POINT('Ctrl Pts',(1.03764614590368,2.46399884959309,13.8400930404591));
#424652=CARTESIAN_POINT('Ctrl Pts',(1.03851628373661,2.46160146861416,13.8432258934518));
#424653=CARTESIAN_POINT('Ctrl Pts',(1.03968232662491,2.45914319261956,13.8462331177034));
#424654=CARTESIAN_POINT('Ctrl Pts',(1.04119340285672,2.45674553947007,13.8489036603661));
#424655=CARTESIAN_POINT('Ctrl Pts',(1.04168784458504,2.45596099945666,13.849777493004));
#424656=CARTESIAN_POINT('Ctrl Pts',(1.04221923248918,2.45518320007902,13.85061494757));
#424657=CARTESIAN_POINT('Ctrl Pts',(1.04278928813813,2.45441711243214,13.8514076489583));
#424658=CARTESIAN_POINT('Ctrl Pts',(1.04399503804997,2.4527967265726,13.8530843267192));
#424659=CARTESIAN_POINT('Ctrl Pts',(1.04549459049601,2.45107133833551,13.8546805203176));
#424660=CARTESIAN_POINT('Ctrl Pts',(1.04730389787759,2.44943059471246,13.8559412814274));
#424661=CARTESIAN_POINT('Ctrl Pts',(1.04754604188247,2.44921101000513,13.8561100121513));
#424662=CARTESIAN_POINT('Ctrl Pts',(1.04779365776436,2.44899293146871,13.8562727473908));
#424663=CARTESIAN_POINT('Ctrl Pts',(1.04804671036289,2.44877679458595,13.8564289040185));
#424664=CARTESIAN_POINT('Ctrl Pts',(1.04919430101033,2.44779661628836,13.8571370725437));
#424665=CARTESIAN_POINT('Ctrl Pts',(1.05047535372972,2.4468408724577,13.8577210840553));
#424666=CARTESIAN_POINT('Ctrl Pts',(1.05185762324726,2.44597023585783,13.8581177131616));
#424667=CARTESIAN_POINT('Ctrl Pts',(1.05224691791968,2.4457250346249,13.8582294175695));
#424668=CARTESIAN_POINT('Ctrl Pts',(1.05264411863223,2.44548645509554,13.8583265086086));
#424669=CARTESIAN_POINT('Ctrl Pts',(1.05304822202721,2.44525551628232,13.8584082369006));
#424670=CARTESIAN_POINT('Ctrl Pts',(1.0536288102412,2.44492371913641,13.8585256585398));
#424671=CARTESIAN_POINT('Ctrl Pts',(1.05423102547564,2.44460384965959,13.8586122832068));
#424672=CARTESIAN_POINT('Ctrl Pts',(1.05483959435808,2.44430491454631,13.8586682984299));
#424673=CARTESIAN_POINT('Ctrl Pts',(1.05532638913854,2.44406579608818,13.8587131050557));
#424674=CARTESIAN_POINT('Ctrl Pts',(1.05582252251695,2.44383722077545,13.8587357943552));
#424675=CARTESIAN_POINT('Ctrl Pts',(1.05632826536498,2.44361962142378,13.8587355499465));
#424676=CARTESIAN_POINT('Ctrl Pts',(1.05665513902499,2.44347898177504,13.8587353919793));
#424677=CARTESIAN_POINT('Ctrl Pts',(1.0569824768398,2.44334441249848,13.8587257282814));
#424678=CARTESIAN_POINT('Ctrl Pts',(1.05731024571616,2.44321577207398,13.8587068136939));
#424679=CARTESIAN_POINT('Ctrl Pts',(1.05731024571616,2.44321577207398,13.8587068136939));
#424680=CARTESIAN_POINT('Ctrl Pts',(1.05838825968252,2.44279268073048,13.8586446046466));
#424681=CARTESIAN_POINT('Ctrl Pts',(1.05947093147828,2.44243364339347,13.858482427929));
#424682=CARTESIAN_POINT('Ctrl Pts',(1.06055714787882,2.44213433031837,13.8582284286032));
#424683=CARTESIAN_POINT('Ctrl Pts',(1.06167147955176,2.44182726992088,13.8579678548414));
#424684=CARTESIAN_POINT('Ctrl Pts',(1.06279267059807,2.4415837921154,13.857615680862));
#424685=CARTESIAN_POINT('Ctrl Pts',(1.06387446261208,2.44140402686309,13.8571944833187));
#424686=CARTESIAN_POINT('Ctrl Pts',(1.06657418521963,2.44095540429107,13.8561433417727));
#424687=CARTESIAN_POINT('Ctrl Pts',(1.06915402792857,2.44087786975251,13.8546163505475));
#424688=CARTESIAN_POINT('Ctrl Pts',(1.07147348871116,2.44101970954713,13.8528973491086));
#424689=CARTESIAN_POINT('Ctrl Pts',(1.07189721997571,2.44104562158495,13.8525833129073));
#424690=CARTESIAN_POINT('Ctrl Pts',(1.07231233409303,2.44107873387402,13.8522628768812));
#424691=CARTESIAN_POINT('Ctrl Pts',(1.07271808937104,2.44111798444778,13.851937733538));
#424692=CARTESIAN_POINT('Ctrl Pts',(1.07519598055777,2.44135768225595,13.8499521282529));
#424693=CARTESIAN_POINT('Ctrl Pts',(1.07757070858412,2.44185418050337,13.847639871647));
#424694=CARTESIAN_POINT('Ctrl Pts',(1.07973390830809,2.4425027447878,13.8452109780794));
#424695=CARTESIAN_POINT('Ctrl Pts',(1.08070717663991,2.44279454728398,13.8441181685877));
#424696=CARTESIAN_POINT('Ctrl Pts',(1.08163805677817,2.44311655848146,13.8430021611332));
#424697=CARTESIAN_POINT('Ctrl Pts',(1.08251938789867,2.44345733934995,13.8418824960098));
#424698=CARTESIAN_POINT('Ctrl Pts',(1.08459626718971,2.44426039816869,13.8392439765549));
#424699=CARTESIAN_POINT('Ctrl Pts',(1.08649863795158,2.44520255083485,13.8364981347964));
#424700=CARTESIAN_POINT('Ctrl Pts',(1.08824671851374,2.44625562318806,13.8336931113419));
#424701=CARTESIAN_POINT('Ctrl Pts',(1.0899492379679,2.4472812487838,13.8309611966328));
#424702=CARTESIAN_POINT('Ctrl Pts',(1.09150681991311,2.44841359873896,13.8281701127186));
#424703=CARTESIAN_POINT('Ctrl Pts',(1.09290700573027,2.44965062374159,13.8253580685121));
#424704=CARTESIAN_POINT('Ctrl Pts',(1.09321056752656,2.4499188120972,13.8247484142933));
#424705=CARTESIAN_POINT('Ctrl Pts',(1.0935065637343,2.45019196428493,13.8241378483365));
#424706=CARTESIAN_POINT('Ctrl Pts',(1.09379455227037,2.45047010569484,13.8235269408515));
#424707=CARTESIAN_POINT('',(1.05616306898853,2.44369196784508,12.5969504640361));
#424708=CARTESIAN_POINT('Origin',(1.06992746243219,2.47522623969885,12.584524458991));
#424709=CARTESIAN_POINT('Origin',(1.06992746243219,2.47522623969885,12.584524458991));
#424710=CARTESIAN_POINT('Ctrl Pts',(1.03554215359081,2.47564995700462,12.5893111709658));
#424711=CARTESIAN_POINT('Ctrl Pts',(1.03539245984433,2.46431698624043,12.5770542771492));
#424712=CARTESIAN_POINT('Ctrl Pts',(1.05142854144719,2.46105389542323,12.5737548217797));
#424713=CARTESIAN_POINT('Ctrl Pts',(1.03586948357564,2.50043136060788,12.5663937883685));
#424714=CARTESIAN_POINT('Ctrl Pts',(1.03571959887401,2.48908393306558,12.5540940315304));
#424715=CARTESIAN_POINT('Ctrl Pts',(1.05180601334584,2.48581387729336,12.5508374392248));
#424716=CARTESIAN_POINT('Ctrl Pts',(1.03619648328852,2.52518776007868,12.5434499600945));
#424717=CARTESIAN_POINT('Ctrl Pts',(1.03604611125831,2.51380343800857,12.5311293540533));
#424718=CARTESIAN_POINT('Ctrl Pts',(1.0521819367162,2.51054968611948,12.5278936106989));
#424719=CARTESIAN_POINT('Ctrl Pts',(1.03652317860012,2.54992111402498,12.5204817579905));
#424720=CARTESIAN_POINT('Ctrl Pts',(1.03637206233116,2.53848044734067,12.5081597038247));
#424721=CARTESIAN_POINT('Ctrl Pts',(1.0525564180634,2.53526320093622,12.5049254088044));
#424722=CARTESIAN_POINT('Ctrl Pts',(1.03628829969026,2.53213896960501,12.5369868989719));
#424723=CARTESIAN_POINT('Ctrl Pts',(1.03630060274096,2.53307039314223,12.5342545179733));
#424724=CARTESIAN_POINT('Ctrl Pts',(1.03643707940131,2.53395765366459,12.5314872231885));
#424725=CARTESIAN_POINT('Ctrl Pts',(1.03674529283368,2.53474227178204,12.5287124745063));
#424726=CARTESIAN_POINT('Ctrl Pts',(1.03702325500535,2.53544987934533,12.5262100684184));
#424727=CARTESIAN_POINT('Ctrl Pts',(1.0374415313905,2.53607293087077,12.5237004536639));
#424728=CARTESIAN_POINT('Ctrl Pts',(1.03806234226045,2.53658517537798,12.5212220730815));
#424729=CARTESIAN_POINT('Ctrl Pts',(1.03853762668583,2.53697734286094,12.5193246583486));
#424730=CARTESIAN_POINT('Ctrl Pts',(1.03913770536946,2.53730876132232,12.517417831369));
#424731=CARTESIAN_POINT('Ctrl Pts',(1.0399254557789,2.53750526576482,12.5155812248348));
#424732=CARTESIAN_POINT('Ctrl Pts',(1.0402610416875,2.53758897771353,12.5147988205793));
#424733=CARTESIAN_POINT('Ctrl Pts',(1.04063095998743,2.5376485591545,12.5140295443047));
#424734=CARTESIAN_POINT('Ctrl Pts',(1.0410408100704,2.53768027133397,12.5132817086137));
#424735=CARTESIAN_POINT('Ctrl Pts',(1.04166106272771,2.53772826342768,12.5121499604604));
#424736=CARTESIAN_POINT('Ctrl Pts',(1.04238671566515,2.53770633328319,12.5110494206568));
#424737=CARTESIAN_POINT('Ctrl Pts',(1.04322868144594,2.53757887451469,12.5100666561695));
#424738=CARTESIAN_POINT('Ctrl Pts',(1.0437121362584,2.53750568798333,12.5095023550641));
#424739=CARTESIAN_POINT('Ctrl Pts',(1.04423942793907,2.53739621735281,12.5089719619137));
#424740=CARTESIAN_POINT('Ctrl Pts',(1.0447993746768,2.53724626089961,12.5085043804652));
#424741=CARTESIAN_POINT('Ctrl Pts',(1.04561878378927,2.53702681916354,12.5078201359221));
#424742=CARTESIAN_POINT('Ctrl Pts',(1.0465315752678,2.536713147792,12.5072563000949));
#424743=CARTESIAN_POINT('Ctrl Pts',(1.04747312397982,2.53631850262317,12.5068768744332));
#424744=CARTESIAN_POINT('Ctrl Pts',(1.04815204541762,2.53603393628898,12.5066032824114));
#424745=CARTESIAN_POINT('Ctrl Pts',(1.04885786974257,2.53570232440291,12.5064197834844));
#424746=CARTESIAN_POINT('Ctrl Pts',(1.04955228104954,2.53534452455097,12.5063282718343));
#424747=CARTESIAN_POINT('Ctrl Pts',(1.0505659065734,2.53482224753919,12.5061946931565));
#424748=CARTESIAN_POINT('Ctrl Pts',(1.05157736598184,2.53423395310182,12.5062515701262));
#424749=CARTESIAN_POINT('Ctrl Pts',(1.05253166145004,2.5336295196662,12.5064436508398));
#424750=CARTESIAN_POINT('',(1.05142854144719,2.46105389542323,12.5737548217797));
#424751=CARTESIAN_POINT('Origin',(1.05754023467624,2.4753593910761,12.5893111709658));
#424752=CARTESIAN_POINT('Ctrl Pts',(1.05253166145004,2.5336295196662,12.5064436508398));
#424753=CARTESIAN_POINT('Ctrl Pts',(1.05236885141579,2.52288643441829,12.5164271754438));
#424754=CARTESIAN_POINT('Ctrl Pts',(1.05220576793201,2.51213909377987,12.5264061185523));
#424755=CARTESIAN_POINT('Ctrl Pts',(1.05204240231442,2.50138734786532,12.536380305637));
#424756=CARTESIAN_POINT('Ctrl Pts',(1.05183822842656,2.48794984616116,12.5488460165097));
#424757=CARTESIAN_POINT('Ctrl Pts',(1.05163361376306,2.47450545947743,12.5613043021964));
#424758=CARTESIAN_POINT('Ctrl Pts',(1.05142854144719,2.46105389542323,12.5737548217797));
#424759=CARTESIAN_POINT('Ctrl Pts',(1.09379455227037,2.45047010569484,12.5893111709658));
#424760=CARTESIAN_POINT('Ctrl Pts',(1.08564206678201,2.4425963762785,12.5770542771492));
#424761=CARTESIAN_POINT('Ctrl Pts',(1.07227821101589,2.45204153556342,12.5737548217797));
#424762=CARTESIAN_POINT('Ctrl Pts',(1.0861883542163,2.44312398463148,12.5928319619712));
#424763=CARTESIAN_POINT('Ctrl Pts',(1.07844621856501,2.44017563730997,12.5821634970843));
#424764=CARTESIAN_POINT('Ctrl Pts',(1.06951401436786,2.44935873213036,12.5773203894503));
#424765=CARTESIAN_POINT('Ctrl Pts',(1.07038411407214,2.43757330063713,12.5969440695591));
#424766=CARTESIAN_POINT('Ctrl Pts',(1.06668708889191,2.43915144745181,12.5878292599214));
#424767=CARTESIAN_POINT('Ctrl Pts',(1.06388038270617,2.44738228547084,12.5813877129824));
#424768=CARTESIAN_POINT('Ctrl Pts',(1.04227728576595,2.44966385265545,12.596957478804));
#424769=CARTESIAN_POINT('Ctrl Pts',(1.04594702040858,2.44809744249155,12.5878468778671));
#424770=CARTESIAN_POINT('Ctrl Pts',(1.05382291638343,2.45171514128095,12.5814011370086));
#424771=CARTESIAN_POINT('Ctrl Pts',(1.03540228783687,2.46506104105513,12.5928371701607));
#424772=CARTESIAN_POINT('Ctrl Pts',(1.03856248079188,2.45740935848259,12.5821692192952));
#424773=CARTESIAN_POINT('Ctrl Pts',(1.0513677808519,2.45719001322731,12.5773318885715));
#424774=CARTESIAN_POINT('Ctrl Pts',(1.03554215359075,2.47564995700461,12.5893111709658));
#424775=CARTESIAN_POINT('Ctrl Pts',(1.03539245984427,2.46431698624042,12.5770542771492));
#424776=CARTESIAN_POINT('Ctrl Pts',(1.05142854144714,2.46105389542323,12.5737548217797));
#424777=CARTESIAN_POINT('',(1.07227821101589,2.45204153556342,12.5737548217797));
#424778=CARTESIAN_POINT('Origin',(1.07851109820088,2.46629464460458,12.5893111709658));
#424779=CARTESIAN_POINT('Ctrl Pts',(1.05142854144714,2.46105389542323,12.5737548217797));
#424780=CARTESIAN_POINT('Ctrl Pts',(1.05138262932765,2.46005279017987,12.5746934679442));
#424781=CARTESIAN_POINT('Ctrl Pts',(1.05151481645966,2.45893660829488,12.5756680099006));
#424782=CARTESIAN_POINT('Ctrl Pts',(1.05180675680538,2.4578319479387,12.5765688348656));
#424783=CARTESIAN_POINT('Ctrl Pts',(1.05188404478002,2.45753950133839,12.5768073183026));
#424784=CARTESIAN_POINT('Ctrl Pts',(1.05197227227372,2.45724785902399,12.5770407398754));
#424785=CARTESIAN_POINT('Ctrl Pts',(1.05207055560808,2.45695922165792,12.5772674179684));
#424786=CARTESIAN_POINT('Ctrl Pts',(1.05247388383537,2.45577473195842,12.5781976435658));
#424787=CARTESIAN_POINT('Ctrl Pts',(1.05308014436771,2.45457720715713,12.5790594849312));
#424788=CARTESIAN_POINT('Ctrl Pts',(1.05389148425767,2.45346931713253,12.5797571720116));
#424789=CARTESIAN_POINT('Ctrl Pts',(1.05442010136917,2.45274748694532,12.580211740231));
#424790=CARTESIAN_POINT('Ctrl Pts',(1.05507494323198,2.45204199483691,12.5806009430798));
#424791=CARTESIAN_POINT('Ctrl Pts',(1.0558228968735,2.45141455717908,12.5808812374708));
#424792=CARTESIAN_POINT('Ctrl Pts',(1.0564656371826,2.45087538008073,12.5811221033394));
#424793=CARTESIAN_POINT('Ctrl Pts',(1.05719036794097,2.45038289142037,12.581287365893));
#424794=CARTESIAN_POINT('Ctrl Pts',(1.05796087057078,2.44997178440156,12.581359338449));
#424795=CARTESIAN_POINT('Ctrl Pts',(1.05806795452605,2.44991464901498,12.5813693411482));
#424796=CARTESIAN_POINT('Ctrl Pts',(1.05817591360855,2.44985902633379,12.5813775999465));
#424797=CARTESIAN_POINT('Ctrl Pts',(1.05828464248074,2.44980494868556,12.5813841266931));
#424798=CARTESIAN_POINT('Ctrl Pts',(1.05846911416289,2.44971319941479,12.5813952001081));
#424799=CARTESIAN_POINT('Ctrl Pts',(1.05865730834974,2.44962582822876,12.5814007534795));
#424800=CARTESIAN_POINT('Ctrl Pts',(1.05884922612019,2.44954305205324,12.5814005856065));
#424801=CARTESIAN_POINT('Ctrl Pts',(1.05972775063829,2.44916413508506,12.5813998171494));
#424802=CARTESIAN_POINT('Ctrl Pts',(1.06062346804441,2.44890737463436,12.58127954464));
#424803=CARTESIAN_POINT('Ctrl Pts',(1.0615231395239,2.44874578460953,12.5810700125799));
#424804=CARTESIAN_POINT('Ctrl Pts',(1.06260984023532,2.44855060225803,12.5808169217085));
#424805=CARTESIAN_POINT('Ctrl Pts',(1.06370536675053,2.44851072727905,12.5804173076348));
#424806=CARTESIAN_POINT('Ctrl Pts',(1.06471276171563,2.44860362911934,12.5799304713245));
#424807=CARTESIAN_POINT('Ctrl Pts',(1.06596124143954,2.44871876376655,12.5793271277669));
#424808=CARTESIAN_POINT('Ctrl Pts',(1.06715476219761,2.44901290830323,12.5785808224116));
#424809=CARTESIAN_POINT('Ctrl Pts',(1.06825060435974,2.4494428685557,12.5777485681082));
#424810=CARTESIAN_POINT('Ctrl Pts',(1.06988352923978,2.45008355643754,12.576508418016));
#424811=CARTESIAN_POINT('Ctrl Pts',(1.07128832649179,2.45101402094063,12.5750928681475));
#424812=CARTESIAN_POINT('Ctrl Pts',(1.07227821101589,2.45204153556342,12.5737548217797));
#424813=CARTESIAN_POINT('Ctrl Pts',(1.07227821101589,2.45204153556342,12.5737548217797));
#424814=CARTESIAN_POINT('Ctrl Pts',(1.08564206678201,2.4425963762785,12.5770542771492));
#424815=CARTESIAN_POINT('Ctrl Pts',(1.09379455227037,2.45047010569484,12.5893111709658));
#424816=CARTESIAN_POINT('Ctrl Pts',(1.0900523319253,2.46927799633899,12.5508408821982));
#424817=CARTESIAN_POINT('Ctrl Pts',(1.10345573781959,2.45980094853584,12.55409748406));
#424818=CARTESIAN_POINT('Ctrl Pts',(1.11161862379148,2.46768472281437,12.5663972313419));
#424819=CARTESIAN_POINT('Ctrl Pts',(1.10780991089423,2.48649677251367,12.52790050457));
#424820=CARTESIAN_POINT('Ctrl Pts',(1.12123529143713,2.47697256994233,12.5311362602938));
#424821=CARTESIAN_POINT('Ctrl Pts',(1.1294247137533,2.48488197321396,12.5434568539655));
#424822=CARTESIAN_POINT('Ctrl Pts',(1.12555224308429,2.50369922846665,12.5049357605811));
#424823=CARTESIAN_POINT('Ctrl Pts',(1.13898428420131,2.49411467545568,12.5081700652078));
#424824=CARTESIAN_POINT('Ctrl Pts',(1.14721423047522,2.50206321705864,12.5204921097672));
#424825=CARTESIAN_POINT('Ctrl Pts',(1.12438721310968,2.50256964663775,12.5064436508395));
#424826=CARTESIAN_POINT('Ctrl Pts',(1.12556904207916,2.50226612056393,12.5062361689309));
#424827=CARTESIAN_POINT('Ctrl Pts',(1.12678510446924,2.50190008247318,12.5061871075061));
#424828=CARTESIAN_POINT('Ctrl Pts',(1.12794039842089,2.50148018662134,12.5063648335164));
#424829=CARTESIAN_POINT('Ctrl Pts',(1.12846520419522,2.50128944402519,12.5064455676329));
#424830=CARTESIAN_POINT('Ctrl Pts',(1.12898471487039,2.50108472015738,12.506574497099));
#424831=CARTESIAN_POINT('Ctrl Pts',(1.12947627007719,2.50087381519507,12.5067492519495));
#424832=CARTESIAN_POINT('Ctrl Pts',(1.1304640693461,2.50044999348656,12.5071004286051));
#424833=CARTESIAN_POINT('Ctrl Pts',(1.13137497674137,2.49998488587599,12.5076537929613));
#424834=CARTESIAN_POINT('Ctrl Pts',(1.13214492510314,2.49952182500897,12.5083435010505));
#424835=CARTESIAN_POINT('Ctrl Pts',(1.13219339795375,2.49949267256013,12.5083869222964));
#424836=CARTESIAN_POINT('Ctrl Pts',(1.13224131125456,2.49946351481665,12.5084308732337));
#424837=CARTESIAN_POINT('Ctrl Pts',(1.13228864906172,2.49943435710636,12.5084753333615));
#424838=CARTESIAN_POINT('Ctrl Pts',(1.13266836075541,2.49920047378516,12.5088319622689));
#424839=CARTESIAN_POINT('Ctrl Pts',(1.13301942963428,2.4989629428162,12.509227847131));
#424840=CARTESIAN_POINT('Ctrl Pts',(1.13333298568245,2.49873114633838,12.5096423454524));
#424841=CARTESIAN_POINT('Ctrl Pts',(1.13431553156332,2.49800479876572,12.5109411997424));
#424842=CARTESIAN_POINT('Ctrl Pts',(1.13499591253442,2.49729785900603,12.5124831113042));
#424843=CARTESIAN_POINT('Ctrl Pts',(1.13546293575989,2.49664302484202,12.5140723025008));
#424844=CARTESIAN_POINT('Ctrl Pts',(1.13550669634763,2.49658166616364,12.5142212114565));
#424845=CARTESIAN_POINT('Ctrl Pts',(1.1355486132839,2.49652076477596,12.5143705582413));
#424846=CARTESIAN_POINT('Ctrl Pts',(1.1355887765506,2.49646034901619,12.5145201959299));
#424847=CARTESIAN_POINT('Ctrl Pts',(1.13610473350832,2.49568421863226,12.5164425148273));
#424848=CARTESIAN_POINT('Ctrl Pts',(1.13635789948406,2.49496758429867,12.5184635205941));
#424849=CARTESIAN_POINT('Ctrl Pts',(1.13643679050567,2.49429304224105,12.5205025929158));
#424850=CARTESIAN_POINT('Ctrl Pts',(1.13648255042516,2.49390178111128,12.5216853356836));
#424851=CARTESIAN_POINT('Ctrl Pts',(1.13647007385769,2.49352544470617,12.5228750347131));
#424852=CARTESIAN_POINT('Ctrl Pts',(1.1364174389938,2.49316650540816,12.5240609649613));
#424853=CARTESIAN_POINT('Ctrl Pts',(1.13628824954416,2.49228550815763,12.5269717671326));
#424854=CARTESIAN_POINT('Ctrl Pts',(1.13590321254223,2.49148602989319,12.5299036066169));
#424855=CARTESIAN_POINT('Ctrl Pts',(1.13534543256422,2.4907435114609,12.5328133004019));
#424856=CARTESIAN_POINT('Ctrl Pts',(1.13507766569622,2.49038705937785,12.5342101228451));
#424857=CARTESIAN_POINT('Ctrl Pts',(1.13477000426539,2.49004449354382,12.5356023438238));
#424858=CARTESIAN_POINT('Ctrl Pts',(1.13443048657737,2.48971658479255,12.5369868989719));
#424859=CARTESIAN_POINT('Origin',(10.3056869474636,11.3400187595675,-1.23989184831316));
#424860=CARTESIAN_POINT('Ctrl Pts',(1.03628770799528,2.53209717952451,12.5369868989719));
#424861=CARTESIAN_POINT('Ctrl Pts',(1.0365194348726,2.54743437634594,12.5369868989719));
#424862=CARTESIAN_POINT('Ctrl Pts',(1.02220845398785,2.5529551670322,12.5369868989719));
#424863=CARTESIAN_POINT('Ctrl Pts',(1.03636597453823,2.53728175288462,12.5218025310015));
#424864=CARTESIAN_POINT('Ctrl Pts',(1.03322114005496,2.54867323565804,12.5216901060417));
#424865=CARTESIAN_POINT('Ctrl Pts',(1.02225208453606,2.55293835321908,12.5161920673678));
#424866=CARTESIAN_POINT('Ctrl Pts',(1.04131463689905,2.54072367270261,12.5042015548895));
#424867=CARTESIAN_POINT('Ctrl Pts',(1.03848054409933,2.54649820844322,12.4980677368514));
#424868=CARTESIAN_POINT('Ctrl Pts',(1.03218504713171,2.5490589695907,12.4907278922777));
#424869=CARTESIAN_POINT('Ctrl Pts',(1.05252398829026,2.53361104898882,12.506463626192));
#424870=CARTESIAN_POINT('Ctrl Pts',(1.0550340298031,2.53965316202484,12.4999376786891));
#424871=CARTESIAN_POINT('Ctrl Pts',(1.05500337329562,2.53957936639933,12.4906970594712));
#424872=CARTESIAN_POINT('Origin',(1.01429021860483,2.53242953553353,12.5369868989719));
#424873=CARTESIAN_POINT('Origin',(1.01429021860483,2.53242953553353,14.));
#424874=CARTESIAN_POINT('Origin',(1.01429021860483,2.53242953553353,13.7435492065112));
#424875=CARTESIAN_POINT('Ctrl Pts',(1.03596125242285,2.50738102564795,13.793642941384));
#424876=CARTESIAN_POINT('Ctrl Pts',(1.03613127562864,2.5181920066911,13.8071662555867));
#424877=CARTESIAN_POINT('Ctrl Pts',(1.01932784453742,2.52096041547549,13.8103758687955));
#424878=CARTESIAN_POINT('Ctrl Pts',(1.03618077956992,2.5240006981193,13.7804579775006));
#424879=CARTESIAN_POINT('Ctrl Pts',(1.03638043328978,2.53734063103223,13.7901904343351));
#424880=CARTESIAN_POINT('Ctrl Pts',(1.02145311740879,2.54238356319055,13.7927914348262));
#424881=CARTESIAN_POINT('Ctrl Pts',(1.03631002342511,2.53378532477233,13.7597120340895));
#424882=CARTESIAN_POINT('Ctrl Pts',(1.03653534925048,2.54922346968174,13.7635825532445));
#424883=CARTESIAN_POINT('Ctrl Pts',(1.02268095084899,2.55501929240823,13.7651073818885));
#424884=CARTESIAN_POINT('Ctrl Pts',(1.0362847145181,2.5318692708312,13.7381884353898));
#424885=CARTESIAN_POINT('Ctrl Pts',(1.03650566490932,2.54694604407851,13.7368803041982));
#424886=CARTESIAN_POINT('Ctrl Pts',(1.02244001266249,2.55254488895851,13.7363986145813));
#424887=CARTESIAN_POINT('Origin',(1.01401646563537,2.51170432507905,13.7902182540695));
#424888=CARTESIAN_POINT('Ctrl Pts',(1.03554210084444,2.47564602115955,13.8235227101244));
#424889=CARTESIAN_POINT('Ctrl Pts',(1.03569838194778,2.48714203196923,13.8358800583119));
#424890=CARTESIAN_POINT('Ctrl Pts',(1.01943750119579,2.49033731070927,13.8390832900376));
#424891=CARTESIAN_POINT('Ctrl Pts',(1.03569963485109,2.48757256015172,13.8124254819053));
#424892=CARTESIAN_POINT('Ctrl Pts',(1.03585621917197,2.49909089605522,13.8247886449158));
#424893=CARTESIAN_POINT('Ctrl Pts',(1.01957150574241,2.5022734877066,13.8279860620657));
#424894=CARTESIAN_POINT('Ctrl Pts',(1.03585709825614,2.49949375405706,13.8013225099955));
#424895=CARTESIAN_POINT('Ctrl Pts',(1.03601391391637,2.51102898022224,13.8136962257787));
#424896=CARTESIAN_POINT('Ctrl Pts',(1.01970571929062,2.51420413579808,13.8168830918626));
#424897=CARTESIAN_POINT('Ctrl Pts',(1.03601449380658,2.5114098108448,13.7902140179785));
#424898=CARTESIAN_POINT('Ctrl Pts',(1.03617147362278,2.52295684764573,13.802602731458));
#424899=CARTESIAN_POINT('Ctrl Pts',(1.01984013546838,2.52612947220724,13.8057746032558));
#424900=CARTESIAN_POINT('Origin',(1.01354407250538,2.47594052293313,13.8235269408515));
#424901=CARTESIAN_POINT('Ctrl Pts',(1.09379455227037,2.45047010569484,13.8235269408515));
#424902=CARTESIAN_POINT('Ctrl Pts',(1.10228764090823,2.45867279209507,13.8362179249168));
#424903=CARTESIAN_POINT('Ctrl Pts',(1.11598254310312,2.44846923105347,13.8391868794938));
#424904=CARTESIAN_POINT('Ctrl Pts',(1.08602374584887,2.44296500468032,13.8400110824519));
#424905=CARTESIAN_POINT('Ctrl Pts',(1.09520970154143,2.44708083763075,13.8494522556837));
#424906=CARTESIAN_POINT('Ctrl Pts',(1.10311593487012,2.43619877155908,13.85569149686));
#424907=CARTESIAN_POINT('Ctrl Pts',(1.07069954753941,2.43743629124795,13.8586819406588));
#424908=CARTESIAN_POINT('Ctrl Pts',(1.07470152022599,2.43572157312218,13.868010383617));
#424909=CARTESIAN_POINT('Ctrl Pts',(1.07762791303082,2.42715833238374,13.8744918421245));
#424910=CARTESIAN_POINT('Ctrl Pts',(1.04195695271595,2.44980296989507,13.8587686893867));
#424911=CARTESIAN_POINT('Ctrl Pts',(1.03799057537254,2.45150237528801,13.8680909899357));
#424912=CARTESIAN_POINT('Ctrl Pts',(1.02978095023979,2.447747584124,13.8745789365163));
#424913=CARTESIAN_POINT('Ctrl Pts',(1.03539923594297,2.46482998964901,13.8400379222776));
#424914=CARTESIAN_POINT('Ctrl Pts',(1.03209764449017,2.47433628902295,13.8494748685453));
#424915=CARTESIAN_POINT('Ctrl Pts',(1.01876016026727,2.47264140853484,13.8557104837033));
#424916=CARTESIAN_POINT('Ctrl Pts',(1.0355421535842,2.47564995700456,13.8235269408542));
#424917=CARTESIAN_POINT('Ctrl Pts',(1.03569810139407,2.48745640859135,13.8362179249195));
#424918=CARTESIAN_POINT('Ctrl Pts',(1.01888277880466,2.4904410241898,13.8391868794965));
#424919=CARTESIAN_POINT('Origin',(1.10907800633986,2.43464556678511,13.8235269408515));
#424920=CARTESIAN_POINT('Ctrl Pts',(1.11951876426231,2.47531473453212,13.7902140241682));
#424921=CARTESIAN_POINT('Ctrl Pts',(1.12782218678114,2.48334042888628,13.8026027327198));
#424922=CARTESIAN_POINT('Ctrl Pts',(1.14132243324905,2.47361822349969,13.8057746032556));
#424923=CARTESIAN_POINT('Ctrl Pts',(1.11094683002701,2.46703589848542,13.8013225161808));
#424924=CARTESIAN_POINT('Ctrl Pts',(1.11924176202788,2.47505338131897,13.8136962270464));
#424925=CARTESIAN_POINT('Ctrl Pts',(1.13272799552232,2.46534976799986,13.8168830918628));
#424926=CARTESIAN_POINT('Ctrl Pts',(1.10237120035374,2.45875349335803,13.8124254880875));
#424927=CARTESIAN_POINT('Ctrl Pts',(1.11065398782056,2.46675923547352,13.8247886461867));
#424928=CARTESIAN_POINT('Ctrl Pts',(1.12412954988478,2.4570778208428,13.8279860620656));
#424929=CARTESIAN_POINT('Ctrl Pts',(1.09379172563669,2.45046737465958,13.8235227163065));
#424930=CARTESIAN_POINT('Ctrl Pts',(1.10205845903465,2.45845760007342,13.8358800595848));
#424931=CARTESIAN_POINT('Ctrl Pts',(1.11552693374202,2.44880223784019,13.8390832900376));
#424932=CARTESIAN_POINT('Origin',(1.13480505391371,2.45949293530442,13.7902182540695));
#424933=CARTESIAN_POINT('Ctrl Pts',(1.13423639626223,2.48952909261398,13.7382347919292));
#424934=CARTESIAN_POINT('Ctrl Pts',(1.145074137369,2.50002962766872,13.7369371795943));
#424935=CARTESIAN_POINT('Ctrl Pts',(1.15879643754766,2.4936076143686,13.7364597369711));
#424936=CARTESIAN_POINT('Ctrl Pts',(1.13559698884022,2.49084316332022,13.7595490285573));
#424937=CARTESIAN_POINT('Ctrl Pts',(1.14669400878008,2.50159351005293,13.7633824266925));
#424938=CARTESIAN_POINT('Ctrl Pts',(1.16041340014625,2.4954557612108,13.7648920890506));
#424939=CARTESIAN_POINT('Ctrl Pts',(1.12865804122628,2.48414147471485,13.7803806590111));
#424940=CARTESIAN_POINT('Ctrl Pts',(1.13825281004802,2.49344401723081,13.7901039518744));
#424941=CARTESIAN_POINT('Ctrl Pts',(1.15216715397904,2.48603615151962,13.7926933640892));
#424942=CARTESIAN_POINT('Ctrl Pts',(1.11659660135886,2.47249244385822,13.7936647693663));
#424943=CARTESIAN_POINT('Ctrl Pts',(1.12435525099816,2.48002747456282,13.8072068914933));
#424944=CARTESIAN_POINT('Ctrl Pts',(1.13789267255913,2.46966492239998,13.8104111085397));
#424945=CARTESIAN_POINT('Origin',(1.14971394064686,2.47389204588282,13.7435492065112));
#424946=CARTESIAN_POINT('Origin',(1.14971394064686,2.47389204588282,14.));
#424947=CARTESIAN_POINT('Origin',(1.14971394064686,2.47389204588282,12.5369868989719));
#424948=CARTESIAN_POINT('Ctrl Pts',(1.12437967912842,2.50255287813992,12.506462012331));
#424949=CARTESIAN_POINT('Ctrl Pts',(1.12705939221632,2.50851716567126,12.4999388158272));
#424950=CARTESIAN_POINT('Ctrl Pts',(1.12702768769627,2.50844660032808,12.4907030323752));
#424951=CARTESIAN_POINT('Ctrl Pts',(1.13723970050497,2.49925918213859,12.5042014951932));
#424952=CARTESIAN_POINT('Ctrl Pts',(1.14338470956401,2.50115126056727,12.4980716682127));
#424953=CARTESIAN_POINT('Ctrl Pts',(1.14955959101947,2.49832346916108,12.4907355092743));
#424954=CARTESIAN_POINT('Ctrl Pts',(1.13812530439812,2.49329752070994,12.5218047446509));
#424955=CARTESIAN_POINT('Ctrl Pts',(1.14857302621971,2.49880787275631,12.5216906929434));
#424956=CARTESIAN_POINT('Ctrl Pts',(1.15919134706604,2.49374605324804,12.5161988840776));
#424957=CARTESIAN_POINT('Ctrl Pts',(1.13440287727529,2.48968987289895,12.5369868989719));
#424958=CARTESIAN_POINT('Ctrl Pts',(1.14541101148044,2.50035882377718,12.5369868989719));
#424959=CARTESIAN_POINT('Ctrl Pts',(1.15923195340826,2.49372654696235,12.5369868989719));
#424960=CARTESIAN_POINT('Origin',(2.04412211573024E-31,-4.22882474612863E-32,
12.5));
#424961=CARTESIAN_POINT('Origin',(1.28989110379808,2.35316195826446,12.5));
#424962=CARTESIAN_POINT('',(1.28989110379808,2.35316195826446,12.5893111709658));
#424963=CARTESIAN_POINT('',(1.28989110379808,2.35316195826446,13.8235269408515));
#424964=CARTESIAN_POINT('',(1.28989110379808,2.35316195826446,12.5));
#424965=CARTESIAN_POINT('',(1.31755783794949,2.37582965599927,13.7902182540695));
#424966=CARTESIAN_POINT('',(1.28989110379808,2.35316195826446,13.8235269408515));
#424967=CARTESIAN_POINT('',(1.33359077777889,2.38896564204895,13.7435492065112));
#424968=CARTESIAN_POINT('Origin',(1.28084241121639,2.34574867356094,13.7445212918716));
#424969=CARTESIAN_POINT('',(1.33359077777889,2.38896564204895,12.5369868989719));
#424970=CARTESIAN_POINT('',(1.33359077777889,2.38896564204895,12.5));
#424971=CARTESIAN_POINT('Ctrl Pts',(1.33359077777889,2.38896564204895,12.5369868989719));
#424972=CARTESIAN_POINT('Ctrl Pts',(1.31903484374673,2.37703978513056,12.5544431401645));
#424973=CARTESIAN_POINT('Ctrl Pts',(1.30446849892367,2.36510539852233,12.5718848856037));
#424974=CARTESIAN_POINT('Ctrl Pts',(1.28989110379808,2.35316195826446,12.5893111709658));
#424975=CARTESIAN_POINT('Origin',(1.25991801334777,2.65677114278591,12.5));
#424976=CARTESIAN_POINT('',(1.23923296911491,2.43924636921446,13.7435492065112));
#424977=CARTESIAN_POINT('',(1.23727082998037,2.41861243359646,13.7902182540695));
#424978=CARTESIAN_POINT('Origin',(1.23211466746072,2.3643900170544,13.7418732680449));
#424979=CARTESIAN_POINT('',(1.23388492680971,2.38300613697746,13.8235269408515));
#424980=CARTESIAN_POINT('',(1.23727082998037,2.41861243359646,13.7902182540695));
#424981=CARTESIAN_POINT('',(1.23388492680971,2.38300613697746,12.5893111709658));
#424982=CARTESIAN_POINT('',(1.23388492680971,2.38300613697746,12.5));
#424983=CARTESIAN_POINT('',(1.23923296911491,2.43924636921446,12.5369868989719));
#424984=CARTESIAN_POINT('Ctrl Pts',(1.23388492680971,2.38300613697746,12.5893111709658));
#424985=CARTESIAN_POINT('Ctrl Pts',(1.23566893384522,2.4017668281358,12.5718848856037));
#424986=CARTESIAN_POINT('Ctrl Pts',(1.23745158852544,2.42051329787039,12.5544431401645));
#424987=CARTESIAN_POINT('Ctrl Pts',(1.23923296911491,2.43924636921446,12.5369868989719));
#424988=CARTESIAN_POINT('',(1.23923296911491,2.43924636921446,12.5));
#424989=CARTESIAN_POINT('Origin',(1.26810555253577,2.3797520011602,12.5));
#424990=CARTESIAN_POINT('',(1.25293690022837,2.3489055725281,13.8587068136939));
#424991=CARTESIAN_POINT('Ctrl Pts',(1.23388492680312,2.38300613697794,13.8235269408542));
#424992=CARTESIAN_POINT('Ctrl Pts',(1.23371904413407,2.38126170802633,13.8262006681044));
#424993=CARTESIAN_POINT('Ctrl Pts',(1.23372224654694,2.37946009270208,13.8288634856214));
#424994=CARTESIAN_POINT('Ctrl Pts',(1.23388244646385,2.37760692097054,13.8314912288862));
#424995=CARTESIAN_POINT('Ctrl Pts',(1.23404759605434,2.37569649206111,13.834200161153));
#424996=CARTESIAN_POINT('Ctrl Pts',(1.23437928288247,2.37372910685695,13.8368750301949));
#424997=CARTESIAN_POINT('Ctrl Pts',(1.23490650022355,2.37169483278667,13.8394886372968));
#424998=CARTESIAN_POINT('Ctrl Pts',(1.23494721849766,2.37153772086575,13.839690492513));
#424999=CARTESIAN_POINT('Ctrl Pts',(1.23498912515823,2.37138021174245,13.8398919674349));
#425000=CARTESIAN_POINT('Ctrl Pts',(1.23503224484409,2.37122230275869,13.8400930404591));
#425001=CARTESIAN_POINT('Ctrl Pts',(1.23570407855918,2.36876197455584,13.8432258934518));
#425002=CARTESIAN_POINT('Ctrl Pts',(1.23666586922088,2.36621683495141,13.8462331177034));
#425003=CARTESIAN_POINT('Ctrl Pts',(1.23797648648077,2.36370399305394,13.8489036603661));
#425004=CARTESIAN_POINT('Ctrl Pts',(1.23840533570063,2.36288176194168,13.849777493004));
#425005=CARTESIAN_POINT('Ctrl Pts',(1.23887155758534,2.36206323757994,13.85061494757));
#425006=CARTESIAN_POINT('Ctrl Pts',(1.2393772731659,2.36125323419899,13.8514076489583));
#425007=CARTESIAN_POINT('Ctrl Pts',(1.24044693455389,2.3595399602283,13.8530843267192));
#425008=CARTESIAN_POINT('Ctrl Pts',(1.24180086220381,2.35769808563273,13.8546805203176));
#425009=CARTESIAN_POINT('Ctrl Pts',(1.24347041342712,2.35591532610035,13.8559412814273));
#425010=CARTESIAN_POINT('Ctrl Pts',(1.24369385352563,2.35567673505865,13.8561100121513));
#425011=CARTESIAN_POINT('Ctrl Pts',(1.24392287006086,2.35543919916743,13.8562727473908));
#425012=CARTESIAN_POINT('Ctrl Pts',(1.2441574634853,2.35520315532629,13.8564289040185));
#425013=CARTESIAN_POINT('Ctrl Pts',(1.24522134198875,2.35413269919965,13.8571370725437));
#425014=CARTESIAN_POINT('Ctrl Pts',(1.246420230116,2.3530757178384,13.8577210840554));
#425015=CARTESIAN_POINT('Ctrl Pts',(1.24772693528028,2.35209531041194,13.8581177131616));
#425016=CARTESIAN_POINT('Ctrl Pts',(1.24809494842996,2.35181919393605,13.8582294175695));
#425017=CARTESIAN_POINT('Ctrl Pts',(1.2484713810434,2.3515490327149,13.8583265086086));
#425018=CARTESIAN_POINT('Ctrl Pts',(1.24885531616046,2.35128592415332,13.8584082369006));
#425019=CARTESIAN_POINT('Ctrl Pts',(1.24940692796741,2.35090790770569,13.8585256585398));
#425020=CARTESIAN_POINT('Ctrl Pts',(1.24998106704845,2.35054001643586,13.8586122832068));
#425021=CARTESIAN_POINT('Ctrl Pts',(1.25056324498123,2.35019247199092,13.8586682984299));
#425022=CARTESIAN_POINT('Ctrl Pts',(1.25102892961801,2.34991447088594,13.8587131050557));
#425023=CARTESIAN_POINT('Ctrl Pts',(1.25150478114356,2.34964621666249,13.8587357943552));
#425024=CARTESIAN_POINT('Ctrl Pts',(1.25199110480672,2.34938811861751,13.8587355499465));
#425025=CARTESIAN_POINT('Ctrl Pts',(1.25230542738467,2.34922130369772,13.8587353919793));
#425026=CARTESIAN_POINT('Ctrl Pts',(1.25262070736467,2.34906050111852,13.8587257282814));
#425027=CARTESIAN_POINT('Ctrl Pts',(1.25293690022837,2.3489055725281,13.8587068136939));
#425028=CARTESIAN_POINT('Ctrl Pts',(1.25293690022837,2.3489055725281,13.8587068136939));
#425029=CARTESIAN_POINT('Ctrl Pts',(1.25397684131982,2.34839602084015,13.8586446046466));
#425030=CARTESIAN_POINT('Ctrl Pts',(1.25502664573831,2.34794993036791,13.858482427929));
#425031=CARTESIAN_POINT('Ctrl Pts',(1.256084851049,2.34756307651182,13.8582284286032));
#425032=CARTESIAN_POINT('Ctrl Pts',(1.25717044660222,2.34716620945617,13.8579678548414));
#425033=CARTESIAN_POINT('Ctrl Pts',(1.25826806127632,2.3468321543241,13.857615680862));
#425034=CARTESIAN_POINT('Ctrl Pts',(1.25933160117973,2.34656481113383,13.8571944833187));
#425035=CARTESIAN_POINT('Ctrl Pts',(1.26198577377861,2.34589762886089,13.8561433417727));
#425036=CARTESIAN_POINT('Ctrl Pts',(1.26455071248909,2.34561007118124,13.8546163505474));
#425037=CARTESIAN_POINT('Ctrl Pts',(1.26687401671733,2.34556238142904,13.8528973491086));
#425038=CARTESIAN_POINT('Ctrl Pts',(1.26729845012266,2.34555366921491,13.8525833129072));
#425039=CARTESIAN_POINT('Ctrl Pts',(1.26771488194094,2.34555283567127,13.8522628768812));
#425040=CARTESIAN_POINT('Ctrl Pts',(1.26812248638786,2.34555888281998,13.851937733538));
#425041=CARTESIAN_POINT('Ctrl Pts',(1.27061167019269,2.34559581191813,13.8499521282529));
#425042=CARTESIAN_POINT('Ctrl Pts',(1.27301896572387,2.34589709572854,13.847639871647));
#425043=CARTESIAN_POINT('Ctrl Pts',(1.27522783158936,2.34636718110915,13.8452109780794));
#425044=CARTESIAN_POINT('Ctrl Pts',(1.2762216460635,2.34657868225217,13.8441181685877));
#425045=CARTESIAN_POINT('Ctrl Pts',(1.27717567567689,2.34682374661082,13.8430021611332));
#425046=CARTESIAN_POINT('Ctrl Pts',(1.27808185104523,2.34709155689088,13.8418824960098));
#425047=CARTESIAN_POINT('Ctrl Pts',(1.28021727644072,2.34772265865462,13.8392439765549));
#425048=CARTESIAN_POINT('Ctrl Pts',(1.28219011140962,2.34850661550767,13.8364981347964));
#425049=CARTESIAN_POINT('Ctrl Pts',(1.28401821055095,2.34941369905528,13.8336931113419));
#425050=CARTESIAN_POINT('Ctrl Pts',(1.28579866301958,2.35029714082553,13.8309611966328));
#425051=CARTESIAN_POINT('Ctrl Pts',(1.28744335927292,2.35129876559121,13.8281701127186));
#425052=CARTESIAN_POINT('Ctrl Pts',(1.28893971510898,2.3524175463524,13.8253580685121));
#425053=CARTESIAN_POINT('Ctrl Pts',(1.28926412666915,2.35266009922885,13.8247484142933));
#425054=CARTESIAN_POINT('Ctrl Pts',(1.28958140241306,2.35290821608639,13.8241378483365));
#425055=CARTESIAN_POINT('Ctrl Pts',(1.28989110379808,2.35316195826446,13.8235269408515));
#425056=CARTESIAN_POINT('',(1.25183235501256,2.34947368935035,12.5969504640361));
#425057=CARTESIAN_POINT('Origin',(1.2681212844785,2.37978110766788,12.584524458991));
#425058=CARTESIAN_POINT('Origin',(1.2681212844785,2.37978110766788,12.584524458991));
#425059=CARTESIAN_POINT('Ctrl Pts',(1.23388492680971,2.38300613697746,12.5893111709658));
#425060=CARTESIAN_POINT('Ctrl Pts',(1.23281198882938,2.37172307716861,12.5770542771492));
#425061=CARTESIAN_POINT('Ctrl Pts',(1.24852873949894,2.36716375449457,12.5737548217797));
#425062=CARTESIAN_POINT('Ctrl Pts',(1.23623108208401,2.40767840207199,12.5663937883685));
#425063=CARTESIAN_POINT('Ctrl Pts',(1.23515677542226,2.3963809491534,12.5540940315304));
#425064=CARTESIAN_POINT('Ctrl Pts',(1.25092312377384,2.39181058210357,12.5508374392248));
#425065=CARTESIAN_POINT('Ctrl Pts',(1.2385748701164,2.4323257731535,12.5434499600944));
#425066=CARTESIAN_POINT('Ctrl Pts',(1.23749707050107,2.42099158819238,12.5311293540533));
#425067=CARTESIAN_POINT('Ctrl Pts',(1.25331399434559,2.41643344332179,12.5278936106989));
#425068=CARTESIAN_POINT('Ctrl Pts',(1.24091647633618,2.45695020020412,12.5204817579905));
#425069=CARTESIAN_POINT('Ctrl Pts',(1.2398333423494,2.44555991877323,12.5081597038247));
#425070=CARTESIAN_POINT('Ctrl Pts',(1.25570161052364,2.44103420225039,12.5049254088044));
#425071=CARTESIAN_POINT('Ctrl Pts',(1.23923296911491,2.43924636921446,12.5369868989719));
#425072=CARTESIAN_POINT('Ctrl Pts',(1.23932115089342,2.44017369070384,12.5342545179733));
#425073=CARTESIAN_POINT('Ctrl Pts',(1.23952949340843,2.4410468748252,12.5314872231885));
#425074=CARTESIAN_POINT('Ctrl Pts',(1.23990063494665,2.44180375993454,12.5287124745063));
#425075=CARTESIAN_POINT('Ctrl Pts',(1.24023534880764,2.44248635649457,12.5262100684184));
#425076=CARTESIAN_POINT('Ctrl Pts',(1.24070301789607,2.44307324145897,12.5237004536639));
#425077=CARTESIAN_POINT('Ctrl Pts',(1.24136351575186,2.44353317966562,12.5212220730815));
#425078=CARTESIAN_POINT('Ctrl Pts',(1.24186918399808,2.44388530215064,12.5193246583486));
#425079=CARTESIAN_POINT('Ctrl Pts',(1.24249427965073,2.44416670586086,12.517417831369));
#425080=CARTESIAN_POINT('Ctrl Pts',(1.24329542582199,2.44429834747954,12.5155812248348));
#425081=CARTESIAN_POINT('Ctrl Pts',(1.24363671839713,2.44435442751668,12.5147988205793));
#425082=CARTESIAN_POINT('Ctrl Pts',(1.244010262265,2.44438365892971,12.5140295443047));
#425083=CARTESIAN_POINT('Ctrl Pts',(1.24442133344266,2.4443818590029,12.5132817086137));
#425084=CARTESIAN_POINT('Ctrl Pts',(1.24504343406159,2.44437913505716,12.5121499604604));
#425085=CARTESIAN_POINT('Ctrl Pts',(1.24576488493838,2.44429813043238,12.5110494206568));
#425086=CARTESIAN_POINT('Ctrl Pts',(1.2465936600746,2.44410246774485,12.5100666561695));
#425087=CARTESIAN_POINT('Ctrl Pts',(1.24706954084931,2.44399011868025,12.5095023550641));
#425088=CARTESIAN_POINT('Ctrl Pts',(1.24758615513775,2.44383803313712,12.5089719619137));
#425089=CARTESIAN_POINT('Ctrl Pts',(1.24813201585584,2.44364293479422,12.5085043804652));
#425090=CARTESIAN_POINT('Ctrl Pts',(1.2489308119134,2.44335743378275,12.5078201359221));
#425091=CARTESIAN_POINT('Ctrl Pts',(1.24981499902482,2.44297040514737,12.5072563000949));
#425092=CARTESIAN_POINT('Ctrl Pts',(1.25072124756621,2.44250032816684,12.5068768744332));
#425093=CARTESIAN_POINT('Ctrl Pts',(1.25137471515091,2.44216137030367,12.5066032824114));
#425094=CARTESIAN_POINT('Ctrl Pts',(1.25205116145639,2.44177333059376,12.5064197834844));
#425095=CARTESIAN_POINT('Ctrl Pts',(1.25271409815743,2.4413601203232,12.5063282718343));
#425096=CARTESIAN_POINT('Ctrl Pts',(1.25368178050094,2.44075696125485,12.5061946931565));
#425097=CARTESIAN_POINT('Ctrl Pts',(1.25464192290353,2.44008818098697,12.5062515701262));
#425098=CARTESIAN_POINT('Ctrl Pts',(1.255543776096,2.43940797481384,12.5064436508398));
#425099=CARTESIAN_POINT('',(1.24852873949894,2.36716375449457,12.5737548217797));
#425100=CARTESIAN_POINT('Origin',(1.25578612727439,2.38092349005441,12.5893111709658));
#425101=CARTESIAN_POINT('Ctrl Pts',(1.255543776096,2.43940797481384,12.5064436508398));
#425102=CARTESIAN_POINT('Ctrl Pts',(1.25450584661706,2.4287139068251,12.5164271754438));
#425103=CARTESIAN_POINT('Ctrl Pts',(1.25346729774465,2.41801561989398,12.5264061185523));
#425104=CARTESIAN_POINT('Ctrl Pts',(1.2524281086063,2.40731296534145,12.536380305637));
#425105=CARTESIAN_POINT('Ctrl Pts',(1.25112933295363,2.39393681788302,12.5488460165097));
#425106=CARTESIAN_POINT('Ctrl Pts',(1.24982955680223,2.38055384428151,12.5613043021964));
#425107=CARTESIAN_POINT('Ctrl Pts',(1.24852873949894,2.36716375449458,12.5737548217797));
#425108=CARTESIAN_POINT('Ctrl Pts',(1.28989110379807,2.35316195826446,12.5893111709658));
#425109=CARTESIAN_POINT('Ctrl Pts',(1.28112396298907,2.3459789312845,12.5770542771492));
#425110=CARTESIAN_POINT('Ctrl Pts',(1.26857444251688,2.35648194088999,12.5737548217797));
#425111=CARTESIAN_POINT('Ctrl Pts',(1.28171143767584,2.34646025656683,12.5928319619712));
#425112=CARTESIAN_POINT('Ctrl Pts',(1.27375474566441,2.34415277555787,12.5821634970843));
#425113=CARTESIAN_POINT('Ctrl Pts',(1.26560077011944,2.3540333719524,12.5773203894503));
#425114=CARTESIAN_POINT('Ctrl Pts',(1.26550735256142,2.34221623430672,12.5969440695591));
#425115=CARTESIAN_POINT('Ctrl Pts',(1.26195126254369,2.34409047184176,12.5878292599214));
#425116=CARTESIAN_POINT('Ctrl Pts',(1.25982478515117,2.35252269503661,12.5813877129824));
#425117=CARTESIAN_POINT('Ctrl Pts',(1.23847953964047,2.35655752344862,12.596957478804));
#425118=CARTESIAN_POINT('Ctrl Pts',(1.24200938657361,2.35469720794379,12.5878468778671));
#425119=CARTESIAN_POINT('Ctrl Pts',(1.25015395219074,2.35766091050071,12.5814011370086));
#425120=CARTESIAN_POINT('Ctrl Pts',(1.23288243149495,2.37246385512966,12.5928371701607));
#425121=CARTESIAN_POINT('Ctrl Pts',(1.2354084260042,2.36458004783603,12.5821692192951));
#425122=CARTESIAN_POINT('Ctrl Pts',(1.24815323881001,2.3633176816005,12.5773318885715));
#425123=CARTESIAN_POINT('Ctrl Pts',(1.23388492680966,2.38300613697746,12.5893111709658));
#425124=CARTESIAN_POINT('Ctrl Pts',(1.23281198882932,2.37172307716861,12.5770542771492));
#425125=CARTESIAN_POINT('Ctrl Pts',(1.24852873949888,2.36716375449458,12.5737548217797));
#425126=CARTESIAN_POINT('',(1.26857444251688,2.35648194088999,12.5737548217797));
#425127=CARTESIAN_POINT('Origin',(1.2759483509902,2.37017958571773,12.5893111709658));
#425128=CARTESIAN_POINT('Ctrl Pts',(1.24852873949888,2.36716375449458,12.5737548217797));
#425129=CARTESIAN_POINT('Ctrl Pts',(1.24840138077704,2.36616972261029,12.5746934679442));
#425130=CARTESIAN_POINT('Ctrl Pts',(1.24844214888152,2.36504648025003,12.5756680099006));
#425131=CARTESIAN_POINT('Ctrl Pts',(1.24864307774563,2.36392169971164,12.5765688348656));
#425132=CARTESIAN_POINT('Ctrl Pts',(1.24869627143804,2.36362392651583,12.5768073183026));
#425133=CARTESIAN_POINT('Ctrl Pts',(1.24876043380594,2.36332606325736,12.5770407398754));
#425134=CARTESIAN_POINT('Ctrl Pts',(1.2488348634857,2.36303037530415,12.5772674179684));
#425135=CARTESIAN_POINT('Ctrl Pts',(1.2491403027648,2.36181695190157,12.5781976435658));
#425136=CARTESIAN_POINT('Ctrl Pts',(1.24964693662665,2.36057399590364,12.5790594849312));
#425137=CARTESIAN_POINT('Ctrl Pts',(1.25036527352791,2.35940366055855,12.5797571720116));
#425138=CARTESIAN_POINT('Ctrl Pts',(1.25083329584817,2.35864114499971,12.580211740231));
#425139=CARTESIAN_POINT('Ctrl Pts',(1.25142845462241,2.35788462466702,12.5806009430798));
#425140=CARTESIAN_POINT('Ctrl Pts',(1.25212277751592,2.35719830959079,12.5808812374708));
#425141=CARTESIAN_POINT('Ctrl Pts',(1.25271943122067,2.35660853725765,12.5811221033394));
#425142=CARTESIAN_POINT('Ctrl Pts',(1.25340160809937,2.35605861502781,12.581287365893));
#425143=CARTESIAN_POINT('Ctrl Pts',(1.25413603790667,2.35558607281637,12.581359338449));
#425144=CARTESIAN_POINT('Ctrl Pts',(1.25423810848449,2.3555203992066,12.5813693411482));
#425145=CARTESIAN_POINT('Ctrl Pts',(1.25434117457716,2.35545616193782,12.5813775999465));
#425146=CARTESIAN_POINT('Ctrl Pts',(1.25444513383263,2.35539340181603,12.5813841266931));
#425147=CARTESIAN_POINT('Ctrl Pts',(1.25462151328316,2.35528692167874,12.5813952001081));
#425148=CARTESIAN_POINT('Ctrl Pts',(1.2548019597066,2.35518450163979,12.5814007534795));
#425149=CARTESIAN_POINT('Ctrl Pts',(1.25498649185973,2.35508635781519,12.5814005856065));
#425150=CARTESIAN_POINT('Ctrl Pts',(1.25583120790937,2.35463709375792,12.5813998171494));
#425151=CARTESIAN_POINT('Ctrl Pts',(1.25670301652934,2.3543081783724,12.58127954464));
#425152=CARTESIAN_POINT('Ctrl Pts',(1.25758652333905,2.35407379444733,12.5810700125799));
#425153=CARTESIAN_POINT('Ctrl Pts',(1.25865369896987,2.35379068535259,12.5808169217085));
#425154=CARTESIAN_POINT('Ctrl Pts',(1.25974233003,2.35366164747295,12.5804173076348));
#425155=CARTESIAN_POINT('Ctrl Pts',(1.2607539453339,2.35367212814817,12.5799304713245));
#425156=CARTESIAN_POINT('Ctrl Pts',(1.26200765538713,2.35368511700652,12.5793271277669));
#425157=CARTESIAN_POINT('Ctrl Pts',(1.26322118031378,2.35388099977963,12.5785808224116));
#425158=CARTESIAN_POINT('Ctrl Pts',(1.26434842190364,2.35422020806532,12.5777485681082));
#425159=CARTESIAN_POINT('Ctrl Pts',(1.26602813537108,2.35472566557403,12.576508418016));
#425160=CARTESIAN_POINT('Ctrl Pts',(1.26750409977113,2.3555385300157,12.5750928681475));
#425161=CARTESIAN_POINT('Ctrl Pts',(1.26857444251688,2.35648194088999,12.5737548217797));
#425162=CARTESIAN_POINT('Ctrl Pts',(1.26857444251688,2.35648194088999,12.5737548217797));
#425163=CARTESIAN_POINT('Ctrl Pts',(1.28112396298907,2.3459789312845,12.5770542771492));
#425164=CARTESIAN_POINT('Ctrl Pts',(1.28989110379808,2.35316195826446,12.5893111709658));
#425165=CARTESIAN_POINT('Ctrl Pts',(1.28769435307392,2.37221229290324,12.5508408821982));
#425166=CARTESIAN_POINT('Ctrl Pts',(1.30028069286421,2.36167427718335,12.55409748406));
#425167=CARTESIAN_POINT('Ctrl Pts',(1.30905901829952,2.36886646786604,12.5663972313419));
#425168=CARTESIAN_POINT('Ctrl Pts',(1.30679633527328,2.38792636748136,12.52790050457));
#425169=CARTESIAN_POINT('Ctrl Pts',(1.31940073304203,2.37733956275899,12.5311362602938));
#425170=CARTESIAN_POINT('Ctrl Pts',(1.32820759552495,2.38455513419804,12.5434568539655));
#425171=CARTESIAN_POINT('Ctrl Pts',(1.3258817911766,2.40362541889598,12.5049357605811));
#425172=CARTESIAN_POINT('Ctrl Pts',(1.33848790823583,2.39297792164647,12.5081700652078));
#425173=CARTESIAN_POINT('Ctrl Pts',(1.34733834997374,2.40022919810854,12.5204921097672));
#425174=CARTESIAN_POINT('Ctrl Pts',(1.32462856633754,2.40259455641597,12.5064436508395));
#425175=CARTESIAN_POINT('Ctrl Pts',(1.3257817226758,2.40219571026755,12.5062361689309));
#425176=CARTESIAN_POINT('Ctrl Pts',(1.32696390321607,2.40173176976419,12.5061871075061));
#425177=CARTESIAN_POINT('Ctrl Pts',(1.32808112761236,2.40121910389888,12.5063648335164));
#425178=CARTESIAN_POINT('Ctrl Pts',(1.32858863984641,2.40098621944031,12.5064455676329));
#425179=CARTESIAN_POINT('Ctrl Pts',(1.32908973499688,2.40073983183135,12.506574497099));
#425180=CARTESIAN_POINT('Ctrl Pts',(1.32956246388191,2.40048956232518,12.5067492519495));
#425181=CARTESIAN_POINT('Ctrl Pts',(1.33051243092642,2.39998663603774,12.5071004286051));
#425182=CARTESIAN_POINT('Ctrl Pts',(1.33138239676436,2.39944882862522,12.5076537929613));
#425183=CARTESIAN_POINT('Ctrl Pts',(1.33211203942697,2.39892455061569,12.5083435010505));
#425184=CARTESIAN_POINT('Ctrl Pts',(1.33215797479295,2.39889154418189,12.5083869222964));
#425185=CARTESIAN_POINT('Ctrl Pts',(1.33220335203943,2.39885857807958,12.5084308732337));
#425186=CARTESIAN_POINT('Ctrl Pts',(1.33224815570986,2.39882565891842,12.5084753333615));
#425187=CARTESIAN_POINT('Ctrl Pts',(1.33260754028227,2.39856160379656,12.5088319622689));
#425188=CARTESIAN_POINT('Ctrl Pts',(1.33293808002931,2.39829624781952,12.509227847131));
#425189=CARTESIAN_POINT('Ctrl Pts',(1.33323169918076,2.39803966489652,12.5096423454524));
#425190=CARTESIAN_POINT('Ctrl Pts',(1.33415177165101,2.39723564757469,12.5109411997424));
#425191=CARTESIAN_POINT('Ctrl Pts',(1.33477226655723,2.39647560273324,12.5124831113042));
#425192=CARTESIAN_POINT('Ctrl Pts',(1.33518436073789,2.39578488074739,12.5140723025007));
#425193=CARTESIAN_POINT('Ctrl Pts',(1.33522297441397,2.39572015934078,12.5142212114565));
#425194=CARTESIAN_POINT('Ctrl Pts',(1.33525978784662,2.39565604397801,12.5143705582413));
#425195=CARTESIAN_POINT('Ctrl Pts',(1.33529489302807,2.3955925555676,12.5145201959299));
#425196=CARTESIAN_POINT('Ctrl Pts',(1.33574587135004,2.39477695241153,12.5164425148273));
#425197=CARTESIAN_POINT('Ctrl Pts',(1.33593978258578,2.39404206724226,12.518463520594));
#425198=CARTESIAN_POINT('Ctrl Pts',(1.33596342966419,2.39336333931705,12.5205025929157));
#425199=CARTESIAN_POINT('Ctrl Pts',(1.33597714590695,2.39296965021816,12.5216853356836));
#425200=CARTESIAN_POINT('Ctrl Pts',(1.33593403594348,2.39259558299747,12.5228750347131));
#425201=CARTESIAN_POINT('Ctrl Pts',(1.33585231933275,2.39224212827041,12.5240609649613));
#425202=CARTESIAN_POINT('Ctrl Pts',(1.33565175029564,2.39137459260503,12.5269717671327));
#425203=CARTESIAN_POINT('Ctrl Pts',(1.33520282957202,2.39060915862872,12.5299036066169));
#425204=CARTESIAN_POINT('Ctrl Pts',(1.33458638341544,2.38991457511165,12.532813300402));
#425205=CARTESIAN_POINT('Ctrl Pts',(1.33429045336569,2.38958113457907,12.5342101228452));
#425206=CARTESIAN_POINT('Ctrl Pts',(1.3339558933572,2.3892647858674,12.5356023438238));
#425207=CARTESIAN_POINT('Ctrl Pts',(1.33359077777889,2.38896564204895,12.5369868989719));
#425208=CARTESIAN_POINT('Origin',(11.1950251471808,10.4617154507776,-1.23893508993275));
#425209=CARTESIAN_POINT('Ctrl Pts',(1.23922897310923,2.4392047664156,12.5369868989719));
#425210=CARTESIAN_POINT('Ctrl Pts',(1.24071005285903,2.45447204208811,12.5369868989719));
#425211=CARTESIAN_POINT('Ctrl Pts',(1.22689668627604,2.46114094059758,12.5369868989719));
#425212=CARTESIAN_POINT('Ctrl Pts',(1.23972957008679,2.44436570908569,12.5218025310016));
#425213=CARTESIAN_POINT('Ctrl Pts',(1.23752371138027,2.45597562084555,12.5216901060418));
#425214=CARTESIAN_POINT('Ctrl Pts',(1.22693880116534,2.46112062643631,12.5161920673678));
#425215=CARTESIAN_POINT('Ctrl Pts',(1.24494231460027,2.44739281427596,12.5042015548894));
#425216=CARTESIAN_POINT('Ctrl Pts',(1.24258833028154,2.45337914059885,12.4980677368513));
#425217=CARTESIAN_POINT('Ctrl Pts',(1.2365225068672,2.45644452247225,12.4907278922777));
#425218=CARTESIAN_POINT('Ctrl Pts',(1.25553462293633,2.43939019102985,12.506463626192));
#425219=CARTESIAN_POINT('Ctrl Pts',(1.25852880079779,2.44520760774782,12.4999376786891));
#425220=CARTESIAN_POINT('Ctrl Pts',(1.25849223126875,2.44513655646112,12.4906970594712));
#425221=CARTESIAN_POINT('Origin',(1.21733176865023,2.4413290161375,12.5369868989719));
#425222=CARTESIAN_POINT('Origin',(1.21733176865023,2.4413290161375,14.));
#425223=CARTESIAN_POINT('Origin',(1.21733176865023,2.4413290161375,13.7435492065112));
#425224=CARTESIAN_POINT('Ctrl Pts',(1.23688900779627,2.41459746266198,13.793642941384));
#425225=CARTESIAN_POINT('Ctrl Pts',(1.23793966058313,2.42535861258785,13.8071662555867));
#425226=CARTESIAN_POINT('Ctrl Pts',(1.22141779253926,2.42948744534977,13.8103758687955));
#425227=CARTESIAN_POINT('Ctrl Pts',(1.23846246208079,2.43114394104373,13.7804579775006));
#425228=CARTESIAN_POINT('Ctrl Pts',(1.23974877984366,2.44442321279872,13.7901904343351));
#425229=CARTESIAN_POINT('Ctrl Pts',(1.22528217916204,2.45066607983901,13.7927914348262));
#425230=CARTESIAN_POINT('Ctrl Pts',(1.23938881379597,2.44088547558468,13.7597120340895));
#425231=CARTESIAN_POINT('Ctrl Pts',(1.24087174199913,2.45625388519388,13.7635825532445));
#425232=CARTESIAN_POINT('Ctrl Pts',(1.22753585632341,2.46315968488607,13.7651073818884));
#425233=CARTESIAN_POINT('Ctrl Pts',(1.23920741291829,2.43897786006587,13.7381884353898));
#425234=CARTESIAN_POINT('Ctrl Pts',(1.2406565251009,2.45398645708587,13.7368803041982));
#425235=CARTESIAN_POINT('Ctrl Pts',(1.22709403298645,2.46071315350867,13.7363986145813));
#425236=CARTESIAN_POINT('Origin',(1.2153696295157,2.42069508051951,13.7902182540695));
#425237=CARTESIAN_POINT('Ctrl Pts',(1.23388455343094,2.38300221852792,13.8235227101244));
#425238=CARTESIAN_POINT('Ctrl Pts',(1.23497734612654,2.39444723894921,13.8358800583119));
#425239=CARTESIAN_POINT('Ctrl Pts',(1.21903101699467,2.39895729840277,13.8390832900376));
#425240=CARTESIAN_POINT('Ctrl Pts',(1.23501368690463,2.39487623246143,13.8124254819052));
#425241=CARTESIAN_POINT('Ctrl Pts',(1.23610860151124,2.40634347897658,13.8247886449157));
#425242=CARTESIAN_POINT('Ctrl Pts',(1.22013748488756,2.41084283614122,13.8279860620657));
#425243=CARTESIAN_POINT('Ctrl Pts',(1.23614231433744,2.40674492484817,13.8013225099955));
#425244=CARTESIAN_POINT('Ctrl Pts',(1.23723883622677,2.41822898656775,13.8136962257787));
#425245=CARTESIAN_POINT('Ctrl Pts',(1.22124371042945,2.42272284633523,13.8168830918626));
#425246=CARTESIAN_POINT('Ctrl Pts',(1.23727045541865,2.4186085027414,13.7902140179785));
#425247=CARTESIAN_POINT('Ctrl Pts',(1.23836810359418,2.43010432241759,13.802602731458));
#425248=CARTESIAN_POINT('Ctrl Pts',(1.22234970497524,2.43459754600491,13.8057746032558));
#425249=CARTESIAN_POINT('Origin',(1.21198372634504,2.3850887839005,13.8235269408515));
#425250=CARTESIAN_POINT('Ctrl Pts',(1.28989110379808,2.35316195826446,13.8235269408515));
#425251=CARTESIAN_POINT('Ctrl Pts',(1.29902452747577,2.36064508533239,13.8362179249168));
#425252=CARTESIAN_POINT('Ctrl Pts',(1.31184217606322,2.34935921413227,13.8391868794938));
#425253=CARTESIAN_POINT('Ctrl Pts',(1.28153441868724,2.34631522271842,13.8400110824519));
#425254=CARTESIAN_POINT('Ctrl Pts',(1.29102528746501,2.34966861990706,13.8494522556837));
#425255=CARTESIAN_POINT('Ctrl Pts',(1.29801822404552,2.33817833159836,13.85569149686));
#425256=CARTESIAN_POINT('Ctrl Pts',(1.2658105689127,2.34205397004906,13.8586819406588));
#425257=CARTESIAN_POINT('Ctrl Pts',(1.26965945991938,2.34001875957994,13.868010383617));
#425258=CARTESIAN_POINT('Ctrl Pts',(1.27187813177613,2.33124548413774,13.8744918421245));
#425259=CARTESIAN_POINT('Ctrl Pts',(1.2381716118188,2.3567222879045,13.8587686893867));
#425260=CARTESIAN_POINT('Ctrl Pts',(1.23435694958484,2.35873933524174,13.8680909899357));
#425261=CARTESIAN_POINT('Ctrl Pts',(1.22586859096482,2.35566619849833,13.8745789365163));
#425262=CARTESIAN_POINT('Ctrl Pts',(1.2328605569214,2.37223382128573,13.8400379222776));
#425263=CARTESIAN_POINT('Ctrl Pts',(1.23034480289294,2.38197759958659,13.8494748685453));
#425264=CARTESIAN_POINT('Ctrl Pts',(1.21691354955425,2.38137548745683,13.8557104837033));
#425265=CARTESIAN_POINT('Ctrl Pts',(1.23388492680312,2.38300613697794,13.8235269408542));
#425266=CARTESIAN_POINT('Ctrl Pts',(1.23500269111959,2.39476059237678,13.8362179249195));
#425267=CARTESIAN_POINT('Ctrl Pts',(1.21848659400803,2.39910588180992,13.8391868794965));
#425268=CARTESIAN_POINT('Origin',(1.30383385660595,2.33614433081118,13.8235269408515));
#425269=CARTESIAN_POINT('Ctrl Pts',(1.31755478849323,2.37582715655954,13.7902140241682));
#425270=CARTESIAN_POINT('Ctrl Pts',(1.32648475065538,2.38314934005731,13.8026027327198));
#425271=CARTESIAN_POINT('Ctrl Pts',(1.33914762617131,2.37235908908981,13.8057746032556));
#425272=CARTESIAN_POINT('Ctrl Pts',(1.3083365746672,2.36827455987497,13.8013225161808));
#425273=CARTESIAN_POINT('Ctrl Pts',(1.31725740524774,2.37558925123131,13.8136962270464));
#425274=CARTESIAN_POINT('Ctrl Pts',(1.32990782984329,2.36481867265513,13.8168830918628));
#425275=CARTESIAN_POINT('Ctrl Pts',(1.29911438678623,2.36071870719801,13.8124254880875));
#425276=CARTESIAN_POINT('Ctrl Pts',(1.30802215626515,2.36802268679485,13.8247886461868));
#425277=CARTESIAN_POINT('Ctrl Pts',(1.32066375433798,2.35727510286342,13.8279860620656));
#425278=CARTESIAN_POINT('Ctrl Pts',(1.28988806396505,2.35315946671338,13.8235227163065));
#425279=CARTESIAN_POINT('Ctrl Pts',(1.29877856803845,2.36044928979476,13.8358800595847));
#425280=CARTESIAN_POINT('Ctrl Pts',(1.31141522584929,2.34972824925897,13.8390832900376));
#425281=CARTESIAN_POINT('Origin',(1.33150059075736,2.35881202854599,13.7902182540695));
#425282=CARTESIAN_POINT('Ctrl Pts',(1.33338205093011,2.38879459389766,13.7382347919292));
#425283=CARTESIAN_POINT('Ctrl Pts',(1.34503962143658,2.39837681277536,13.7369371795943));
#425284=CARTESIAN_POINT('Ctrl Pts',(1.35819280809039,2.39085767333853,13.7364597369711));
#425285=CARTESIAN_POINT('Ctrl Pts',(1.33484522521034,2.38999339121579,13.7595490285574));
#425286=CARTESIAN_POINT('Ctrl Pts',(1.34678157379184,2.3998034569118,13.7633824266926));
#425287=CARTESIAN_POINT('Ctrl Pts',(1.35995503150433,2.39256787316164,13.7648920890506));
#425288=CARTESIAN_POINT('Ctrl Pts',(1.32738311653536,2.38387959057498,13.780380659011));
#425289=CARTESIAN_POINT('Ctrl Pts',(1.33770420313101,2.39236911691569,13.7901039518744));
#425290=CARTESIAN_POINT('Ctrl Pts',(1.35096843840372,2.38385175206171,13.7926933640892));
#425291=CARTESIAN_POINT('Ctrl Pts',(1.31441230595499,2.37325244022971,13.7936647693663));
#425292=CARTESIAN_POINT('Ctrl Pts',(1.32275931428189,2.38012999676785,13.8072068914933));
#425293=CARTESIAN_POINT('Ctrl Pts',(1.33540704698687,2.36869849960996,13.8104111085397));
#425294=CARTESIAN_POINT('Origin',(1.34753353058677,2.37194801459568,13.7435492065112));
#425295=CARTESIAN_POINT('Origin',(1.34753353058677,2.37194801459568,14.));
#425296=CARTESIAN_POINT('Origin',(1.34753353058677,2.37194801459568,12.5369868989719));
#425297=CARTESIAN_POINT('Ctrl Pts',(1.32461969063675,2.40257845780336,12.506462012331));
#425298=CARTESIAN_POINT('Ctrl Pts',(1.32777663200395,2.40830447816604,12.4999388158272));
#425299=CARTESIAN_POINT('Ctrl Pts',(1.3277392812475,2.40823673183594,12.4907030323752));
#425300=CARTESIAN_POINT('Ctrl Pts',(1.33716845455174,2.39824751017493,12.5042014951932));
#425301=CARTESIAN_POINT('Ctrl Pts',(1.3434472385572,2.39963241758292,12.4980716682127));
#425302=CARTESIAN_POINT('Ctrl Pts',(1.34937108235248,2.39631072525598,12.4907355092744));
#425303=CARTESIAN_POINT('Ctrl Pts',(1.33756518091922,2.39223350074408,12.5218047446509));
#425304=CARTESIAN_POINT('Ctrl Pts',(1.3484272836557,2.39687393122821,12.5216906929434));
#425305=CARTESIAN_POINT('Ctrl Pts',(1.35859768763379,2.39096346278212,12.5161988840775));
#425306=CARTESIAN_POINT('Ctrl Pts',(1.33356108307719,2.38894126945141,12.5369868989719));
#425307=CARTESIAN_POINT('Ctrl Pts',(1.34540220716617,2.39867745514345,12.5369868989719));
#425308=CARTESIAN_POINT('Ctrl Pts',(1.35863656891839,2.39094071160812,12.5369868989719));
#425309=CARTESIAN_POINT('Origin',(2.42277625004769E-31,-6.05232695006679E-32,
12.5));
#425310=CARTESIAN_POINT('Origin',(1.47740364284705,2.24019390624622,12.5));
#425311=CARTESIAN_POINT('',(1.47740364284705,2.24019390624622,12.5893111709658));
#425312=CARTESIAN_POINT('',(1.47740364284705,2.24019390624622,13.8235269408515));
#425313=CARTESIAN_POINT('',(1.47740364284705,2.24019390624622,12.5));
#425314=CARTESIAN_POINT('',(1.50682594602495,2.260531083408,13.7902182540695));
#425315=CARTESIAN_POINT('',(1.47740364284705,2.24019390624622,13.8235269408515));
#425316=CARTESIAN_POINT('',(1.52387624238129,2.2723165271091,13.7435492065112));
#425317=CARTESIAN_POINT('Origin',(1.46778080751396,2.2335428410822,13.7445212918695));
#425318=CARTESIAN_POINT('',(1.52387624238129,2.2723165271091,12.5369868989719));
#425319=CARTESIAN_POINT('',(1.52387624238129,2.2723165271091,12.5));
#425320=CARTESIAN_POINT('Ctrl Pts',(1.52387624238129,2.2723165271091,12.5369868989719));
#425321=CARTESIAN_POINT('Ctrl Pts',(1.50839667396574,2.26161679625011,12.5544431401645));
#425322=CARTESIAN_POINT('Ctrl Pts',(1.49290603415143,2.25090941265923,12.5718848856037));
#425323=CARTESIAN_POINT('Ctrl Pts',(1.47740364284705,2.24019390624622,12.5893111709658));
#425324=CARTESIAN_POINT('Origin',(1.47227725249127,2.54523594138047,12.5));
#425325=CARTESIAN_POINT('',(1.43393074758915,2.3301209866841,13.7435492065112));
#425326=CARTESIAN_POINT('',(1.43029328000174,2.30971564133977,13.7902182540695));
#425327=CARTESIAN_POINT('Origin',(1.4207346438628,2.25609392052757,13.7418732680446));
#425328=CARTESIAN_POINT('',(1.42401639941738,2.27450380427705,13.8235269408515));
#425329=CARTESIAN_POINT('',(1.43029328000174,2.30971564133977,13.7902182540695));
#425330=CARTESIAN_POINT('',(1.42401639941738,2.27450380427705,12.5893111709658));
#425331=CARTESIAN_POINT('',(1.42401639941738,2.27450380427705,12.5));
#425332=CARTESIAN_POINT('',(1.43393074758915,2.3301209866841,12.5369868989719));
#425333=CARTESIAN_POINT('Ctrl Pts',(1.42401639941738,2.27450380427705,12.5893111709658));
#425334=CARTESIAN_POINT('Ctrl Pts',(1.42732364081181,2.2930566576479,12.5718848856037));
#425335=CARTESIAN_POINT('Ctrl Pts',(1.43062837517274,2.31159544714513,12.5544431401645));
#425336=CARTESIAN_POINT('Ctrl Pts',(1.43393074758915,2.3301209866841,12.5369868989719));
#425337=CARTESIAN_POINT('',(1.43393074758915,2.3301209866841,12.5));
#425338=CARTESIAN_POINT('Origin',(1.45785791655531,2.26847119764282,12.5));
#425339=CARTESIAN_POINT('',(1.44022546638962,2.23896379393913,13.8587068136939));
#425340=CARTESIAN_POINT('Ctrl Pts',(1.42401639941085,2.27450380427807,13.8235269408542));
#425341=CARTESIAN_POINT('Ctrl Pts',(1.42370888154866,2.27277870074739,13.8262006681044));
#425342=CARTESIAN_POINT('Ctrl Pts',(1.42356522493145,2.27098281912313,13.8288634856214));
#425343=CARTESIAN_POINT('Ctrl Pts',(1.42357384109623,2.26912275588719,13.8314912288862));
#425344=CARTESIAN_POINT('Ctrl Pts',(1.4235827234734,2.26720522254756,13.8342001611531));
#425345=CARTESIAN_POINT('Ctrl Pts',(1.42375294648253,2.26521734809964,13.8368750301949));
#425346=CARTESIAN_POINT('Ctrl Pts',(1.42411259732939,2.26314686980077,13.8394886372968));
#425347=CARTESIAN_POINT('Ctrl Pts',(1.42414037403668,2.26298696173946,13.8396904925131));
#425348=CARTESIAN_POINT('Ctrl Pts',(1.42416930280051,2.26282656093291,13.8398919674349));
#425349=CARTESIAN_POINT('Ctrl Pts',(1.42419940796103,2.26266566272357,13.8400930404591));
#425350=CARTESIAN_POINT('Ctrl Pts',(1.42466846661575,2.26015876037508,13.8432258934518));
#425351=CARTESIAN_POINT('Ctrl Pts',(1.42541960449268,2.25754369464496,13.8462331177034));
#425352=CARTESIAN_POINT('Ctrl Pts',(1.42652104083903,2.25493238654776,13.8489036603661));
#425353=CARTESIAN_POINT('Ctrl Pts',(1.42688144362962,2.25407793614903,13.849777493004));
#425354=CARTESIAN_POINT('Ctrl Pts',(1.42727939686518,2.25322413394779,13.85061494757));
#425355=CARTESIAN_POINT('Ctrl Pts',(1.42771740692362,2.2523756052716,13.8514076489583));
#425356=CARTESIAN_POINT('Ctrl Pts',(1.42864386136771,2.25058084474533,13.8530843267192));
#425357=CARTESIAN_POINT('Ctrl Pts',(1.42984315405642,2.24863474116279,13.8546805203176));
#425358=CARTESIAN_POINT('Ctrl Pts',(1.43136183853355,2.24672182969162,13.8559412814274));
#425359=CARTESIAN_POINT('Ctrl Pts',(1.43156508776869,2.2464658200996,13.8561100121513));
#425360=CARTESIAN_POINT('Ctrl Pts',(1.43177398088997,2.24621040761577,13.8562727473908));
#425361=CARTESIAN_POINT('Ctrl Pts',(1.43198855395975,2.24595602764911,13.8564289040185));
#425362=CARTESIAN_POINT('Ctrl Pts',(1.43296164038328,2.24480241740233,13.8571370725437));
#425363=CARTESIAN_POINT('Ctrl Pts',(1.43407038551572,2.24365123254706,13.8577210840554));
#425364=CARTESIAN_POINT('Ctrl Pts',(1.43529283041943,2.24256757874369,13.8581177131616));
#425365=CARTESIAN_POINT('Ctrl Pts',(1.4356371129796,2.24226238453443,13.8582294175695));
#425366=CARTESIAN_POINT('Ctrl Pts',(1.43599027239699,2.24196243949982,13.8583265086086));
#425367=CARTESIAN_POINT('Ctrl Pts',(1.43635148421128,2.24166891213396,13.8584082369006));
#425368=CARTESIAN_POINT('Ctrl Pts',(1.43687044872563,2.24124719202169,13.8585256585398));
#425369=CARTESIAN_POINT('Ctrl Pts',(1.43741269085242,2.24083372721456,13.8586122832068));
#425370=CARTESIAN_POINT('Ctrl Pts',(1.43796460353744,2.24043988628889,13.8586682984299));
#425371=CARTESIAN_POINT('Ctrl Pts',(1.43840607897612,2.24012485258855,13.8587131050557));
#425372=CARTESIAN_POINT('Ctrl Pts',(1.43885848193541,2.23981870464198,13.8587357943552));
#425373=CARTESIAN_POINT('Ctrl Pts',(1.43932215000997,2.2395218255036,13.8587355499465));
#425374=CARTESIAN_POINT('Ctrl Pts',(1.43962182974097,2.2393299454385,13.8587353919793));
#425375=CARTESIAN_POINT('Ctrl Pts',(1.4399229537499,2.23914397967128,13.8587257282814));
#425376=CARTESIAN_POINT('Ctrl Pts',(1.44022546638962,2.23896379393913,13.8587068136939));
#425377=CARTESIAN_POINT('Ctrl Pts',(1.44022546638962,2.23896379393913,13.8587068136939));
#425378=CARTESIAN_POINT('Ctrl Pts',(1.44122041396978,2.23837117288915,13.8586446046466));
#425379=CARTESIAN_POINT('Ctrl Pts',(1.44223036473579,2.2378409979402,13.858482427929));
#425380=CARTESIAN_POINT('Ctrl Pts',(1.44325351677486,2.23736917775172,13.8582284286032));
#425381=CARTESIAN_POINT('Ctrl Pts',(1.44430315174906,2.2368851451227,13.8579678548414));
#425382=CARTESIAN_POINT('Ctrl Pts',(1.4453698856064,2.23646273574583,13.857615680862));
#425383=CARTESIAN_POINT('Ctrl Pts',(1.44640809571661,2.23610959374242,13.8571944833187));
#425384=CARTESIAN_POINT('Ctrl Pts',(1.44899905522606,2.23522829175651,13.8561433417727));
#425385=CARTESIAN_POINT('Ctrl Pts',(1.45153202069412,2.23473262458468,13.8546163505474));
#425386=CARTESIAN_POINT('Ctrl Pts',(1.45384370716165,2.23449572265309,13.8528973491086));
#425387=CARTESIAN_POINT('Ctrl Pts',(1.45426601817352,2.23445244416535,13.8525833129072));
#425388=CARTESIAN_POINT('Ctrl Pts',(1.45468099640773,2.23441767033611,13.8522628768812));
#425389=CARTESIAN_POINT('Ctrl Pts',(1.45508773748325,2.23439047381699,13.851937733538));
#425390=CARTESIAN_POINT('Ctrl Pts',(1.45757164879865,2.23422438844806,13.8499521282529));
#425391=CARTESIAN_POINT('Ctrl Pts',(1.45999549168006,2.23432845282741,13.847639871647));
#425392=CARTESIAN_POINT('Ctrl Pts',(1.46223532404918,2.23461693096355,13.8452109780794));
#425393=CARTESIAN_POINT('Ctrl Pts',(1.46324307099428,2.2347467232482,13.8441181685877));
#425394=CARTESIAN_POINT('Ctrl Pts',(1.46421390117313,2.23491320990514,13.8430021611332));
#425395=CARTESIAN_POINT('Ctrl Pts',(1.46513889034174,2.23510626736355,13.8418824960098));
#425396=CARTESIAN_POINT('Ctrl Pts',(1.467318650938,2.23556121219418,13.8392439765549));
#425397=CARTESIAN_POINT('Ctrl Pts',(1.46934882122271,2.23618175613059,13.8364981347964));
#425398=CARTESIAN_POINT('Ctrl Pts',(1.47124477324504,2.23693681438127,13.8336931113419));
#425399=CARTESIAN_POINT('Ctrl Pts',(1.4730913101107,2.2376721931668,13.8309611966328));
#425400=CARTESIAN_POINT('Ctrl Pts',(1.47481217548998,2.23853642709544,13.8281701127186));
#425401=CARTESIAN_POINT('Ctrl Pts',(1.47639474334372,2.23952951831381,13.8253580685121));
#425402=CARTESIAN_POINT('Ctrl Pts',(1.47673784576237,2.23974482156173,13.8247484142933));
#425403=CARTESIAN_POINT('Ctrl Pts',(1.47707428962471,2.23996625191232,13.8241378483365));
#425404=CARTESIAN_POINT('Ctrl Pts',(1.47740364284705,2.24019390624622,13.8235269408515));
#425405=CARTESIAN_POINT('',(1.43917090325177,2.23962005108887,12.5969504640361));
#425406=CARTESIAN_POINT('Origin',(1.45787596860187,2.26849892500159,12.584524458991));
#425407=CARTESIAN_POINT('Origin',(1.45787596860187,2.26849892500159,12.584524458991));
#425408=CARTESIAN_POINT('Ctrl Pts',(1.42401639941738,2.27450380427705,12.5893111709658));
#425409=CARTESIAN_POINT('Ctrl Pts',(1.42202735742843,2.263345742325,12.5770542771492));
#425410=CARTESIAN_POINT('Ctrl Pts',(1.43732018478205,2.25752052933428,12.5737548217797));
#425411=CARTESIAN_POINT('Ctrl Pts',(1.42836576670489,2.29890274100932,12.5663937883685));
#425412=CARTESIAN_POINT('Ctrl Pts',(1.42637418741666,2.28773044539962,12.5540940315304));
#425413=CARTESIAN_POINT('Ctrl Pts',(1.44171554720094,2.28189018211084,12.5508374392248));
#425414=CARTESIAN_POINT('Ctrl Pts',(1.43271074553412,2.32327705951349,12.5434499600945));
#425415=CARTESIAN_POINT('Ctrl Pts',(1.43071269091247,2.31206843879219,12.5311293540532));
#425416=CARTESIAN_POINT('Ctrl Pts',(1.44610545412486,2.30623623464224,12.5278936106989));
#425417=CARTESIAN_POINT('Ctrl Pts',(1.43705167965902,2.34762868816916,12.5204817579905));
#425418=CARTESIAN_POINT('Ctrl Pts',(1.4350437360324,2.33636459243535,12.5081597038247));
#425419=CARTESIAN_POINT('Ctrl Pts',(1.45049031594202,2.33056052369087,12.5049254088044));
#425420=CARTESIAN_POINT('Ctrl Pts',(1.43393074758915,2.3301209866841,12.5369868989719));
#425421=CARTESIAN_POINT('Ctrl Pts',(1.43409422126029,2.33103803495414,12.5342545179733));
#425422=CARTESIAN_POINT('Ctrl Pts',(1.43437304314491,2.33189133177823,12.5314872231885));
#425423=CARTESIAN_POINT('Ctrl Pts',(1.43480464290327,2.33261544693394,12.5287124745063));
#425424=CARTESIAN_POINT('Ctrl Pts',(1.43519388098805,2.33326848992322,12.5262100684184));
#425425=CARTESIAN_POINT('Ctrl Pts',(1.43570783051915,2.33381530270399,12.5237004536639));
#425426=CARTESIAN_POINT('Ctrl Pts',(1.4364036198565,2.33421987379719,12.5212220730815));
#425427=CARTESIAN_POINT('Ctrl Pts',(1.43693630678483,2.33452960796722,12.5193246583486));
#425428=CARTESIAN_POINT('Ctrl Pts',(1.43758225949808,2.33475912423101,12.517417831369));
#425429=CARTESIAN_POINT('Ctrl Pts',(1.43839146993557,2.33482502697263,12.5155812248347));
#425430=CARTESIAN_POINT('Ctrl Pts',(1.43873619793146,2.33485310189479,12.5147988205793));
#425431=CARTESIAN_POINT('Ctrl Pts',(1.43911088149446,2.33485178874967,12.5140295443047));
#425432=CARTESIAN_POINT('Ctrl Pts',(1.43952043815593,2.33481648869479,12.5132817086137));
#425433=CARTESIAN_POINT('Ctrl Pts',(1.44014024675951,2.33476306683701,12.5121499604604));
#425434=CARTESIAN_POINT('Ctrl Pts',(1.44085269443909,2.33462352680435,12.5110494206568));
#425435=CARTESIAN_POINT('Ctrl Pts',(1.44166276356893,2.3343609623007,12.5100666561695));
#425436=CARTESIAN_POINT('Ctrl Pts',(1.44212790339786,2.33421019836734,12.5095023550641));
#425437=CARTESIAN_POINT('Ctrl Pts',(1.44263040231119,2.33401651001581,12.5089719619137));
#425438=CARTESIAN_POINT('Ctrl Pts',(1.44315854439662,2.33377756813051,12.5085043804652));
#425439=CARTESIAN_POINT('Ctrl Pts',(1.44393141154329,2.33342790780574,12.5078201359221));
#425440=CARTESIAN_POINT('Ctrl Pts',(1.44478111016828,2.33297009751822,12.5072563000949));
#425441=CARTESIAN_POINT('Ctrl Pts',(1.44564602760451,2.33242771701075,12.5068768744332));
#425442=CARTESIAN_POINT('Ctrl Pts',(1.44626969261716,2.33203662332726,12.5066032824114));
#425443=CARTESIAN_POINT('Ctrl Pts',(1.44691225926462,2.33159473813375,12.5064197834844));
#425444=CARTESIAN_POINT('Ctrl Pts',(1.44753930962537,2.33112886729074,12.5063282718343));
#425445=CARTESIAN_POINT('Ctrl Pts',(1.44845460902218,2.33044884008991,12.5061946931565));
#425446=CARTESIAN_POINT('Ctrl Pts',(1.44935704482965,2.32970402461386,12.5062515701262));
#425447=CARTESIAN_POINT('Ctrl Pts',(1.45020045406218,2.32895257236308,12.5064436508398));
#425448=CARTESIAN_POINT('',(1.43732018478205,2.25752052933428,12.5737548217797));
#425449=CARTESIAN_POINT('Origin',(1.44567497038565,2.27064293603114,12.5893111709658));
#425450=CARTESIAN_POINT('Ctrl Pts',(1.45020045406218,2.32895257236308,12.5064436508398));
#425451=CARTESIAN_POINT('Ctrl Pts',(1.448294312388,2.31837868889157,12.5164271754438));
#425452=CARTESIAN_POINT('Ctrl Pts',(1.44638720949835,2.30780065100219,12.5264061185523));
#425453=CARTESIAN_POINT('Ctrl Pts',(1.4444791124715,2.29721831221191,12.536380305637));
#425454=CARTESIAN_POINT('Ctrl Pts',(1.44209437819172,2.28399253505363,12.5488460165097));
#425455=CARTESIAN_POINT('Ctrl Pts',(1.43970809034824,2.27076003601564,12.5613043021964));
#425456=CARTESIAN_POINT('Ctrl Pts',(1.43732018478205,2.25752052933428,12.5737548217797));
#425457=CARTESIAN_POINT('Ctrl Pts',(1.47740364284705,2.24019390624622,12.5893111709658));
#425458=CARTESIAN_POINT('Ctrl Pts',(1.46808019059302,2.23374938356208,12.5770542771492));
#425459=CARTESIAN_POINT('Ctrl Pts',(1.45642852040297,2.24524034769209,12.5737548217797));
#425460=CARTESIAN_POINT('Ctrl Pts',(1.46870494298515,2.23418122263341,12.5928319619712));
#425461=CARTESIAN_POINT('Ctrl Pts',(1.46058664508617,2.23252996384242,12.5821634970842));
#425462=CARTESIAN_POINT('Ctrl Pts',(1.45326516155529,2.24304230807227,12.5773203894503));
#425463=CARTESIAN_POINT('Ctrl Pts',(1.45220884841342,2.23127210537548,12.5969440695591));
#425464=CARTESIAN_POINT('Ctrl Pts',(1.44881735875055,2.23342996088931,12.5878292599214));
#425465=CARTESIAN_POINT('Ctrl Pts',(1.44738526150745,2.24200745420583,12.5813877129824));
#425466=CARTESIAN_POINT('Ctrl Pts',(1.42643991651343,2.24776869272787,12.596957478804));
#425467=CARTESIAN_POINT('Ctrl Pts',(1.42980638518812,2.24562685197486,12.5878468778671));
#425468=CARTESIAN_POINT('Ctrl Pts',(1.43816541970709,2.24791683534776,12.5814011370086));
#425469=CARTESIAN_POINT('Ctrl Pts',(1.42215794598272,2.2640783136773,12.5928371701607));
#425470=CARTESIAN_POINT('Ctrl Pts',(1.42403293196948,2.25601484709938,12.5821692192952));
#425471=CARTESIAN_POINT('Ctrl Pts',(1.43663244289462,2.25371786072261,12.5773318885715));
#425472=CARTESIAN_POINT('Ctrl Pts',(1.42401639941733,2.27450380427706,12.5893111709658));
#425473=CARTESIAN_POINT('Ctrl Pts',(1.42202735742837,2.26334574232501,12.5770542771492));
#425474=CARTESIAN_POINT('Ctrl Pts',(1.437320184782,2.25752052933429,12.5737548217797));
#425475=CARTESIAN_POINT('',(1.45642852040297,2.24524034769209,12.5737548217797));
#425476=CARTESIAN_POINT('Origin',(1.46489437802034,2.25829137274004,12.5893111709658));
#425477=CARTESIAN_POINT('Ctrl Pts',(1.437320184782,2.25752052933429,12.5737548217797));
#425478=CARTESIAN_POINT('Ctrl Pts',(1.43711222700909,2.25654018592726,12.5746934679442));
#425479=CARTESIAN_POINT('Ctrl Pts',(1.43706130478103,2.2554173580843,12.5756680099006));
#425480=CARTESIAN_POINT('Ctrl Pts',(1.43716988501508,2.25427994259259,12.5765688348656));
#425481=CARTESIAN_POINT('Ctrl Pts',(1.43719863043003,2.25397882443277,12.5768073183026));
#425482=CARTESIAN_POINT('Ctrl Pts',(1.43723830068214,2.2536767224611,12.5770407398754));
#425483=CARTESIAN_POINT('Ctrl Pts',(1.43728838139006,2.25337595167529,12.5772674179684));
#425484=CARTESIAN_POINT('Ctrl Pts',(1.43749389907298,2.25214166970218,12.5781976435658));
#425485=CARTESIAN_POINT('Ctrl Pts',(1.43789753469957,2.25086155417469,12.5790594849312));
#425486=CARTESIAN_POINT('Ctrl Pts',(1.43851808819857,2.24963656189775,12.5797571720116));
#425487=CARTESIAN_POINT('Ctrl Pts',(1.43892240111627,2.24883843538253,12.580211740231));
#425488=CARTESIAN_POINT('Ctrl Pts',(1.43945391611847,2.24803592134354,12.5806009430798));
#425489=CARTESIAN_POINT('Ctrl Pts',(1.44008998765969,2.24729529616251,12.5808812374708));
#425490=CARTESIAN_POINT('Ctrl Pts',(1.44063658412813,2.24665885343216,12.5811221033394));
#425491=CARTESIAN_POINT('Ctrl Pts',(1.44127166735258,2.24605515727454,12.581287365893));
#425492=CARTESIAN_POINT('Ctrl Pts',(1.44196513682819,2.24552432456091,12.581359338449));
#425493=CARTESIAN_POINT('Ctrl Pts',(1.4420615147657,2.24545054977499,12.5813693411482));
#425494=CARTESIAN_POINT('Ctrl Pts',(1.44215900198069,2.24537812540706,12.5813775999465));
#425495=CARTESIAN_POINT('Ctrl Pts',(1.44225749978775,2.24530710046997,12.5813841266931));
#425496=CARTESIAN_POINT('Ctrl Pts',(1.4424246132305,2.24518659807391,12.5813952001081));
#425497=CARTESIAN_POINT('Ctrl Pts',(1.44259611104936,2.24506981077049,12.5814007534795));
#425498=CARTESIAN_POINT('Ctrl Pts',(1.44277202955414,2.24495695242778,12.5814005856065));
#425499=CARTESIAN_POINT('Ctrl Pts',(1.44357731568938,2.24444033105959,12.5813998171494));
#425500=CARTESIAN_POINT('Ctrl Pts',(1.44441941378067,2.24404144961688,12.58127954464));
#425501=CARTESIAN_POINT('Ctrl Pts',(1.44528087632854,2.24373583157791,12.5810700125799));
#425502=CARTESIAN_POINT('Ctrl Pts',(1.446321425001,2.24336667978424,12.5808169217085));
#425503=CARTESIAN_POINT('Ctrl Pts',(1.44739591594597,2.24314933772975,12.5804173076348));
#425504=CARTESIAN_POINT('Ctrl Pts',(1.44840501945573,2.24307732749274,12.5799304713245));
#425505=CARTESIAN_POINT('Ctrl Pts',(1.44965561660472,2.24298808412352,12.5793271277669));
#425506=CARTESIAN_POINT('Ctrl Pts',(1.45088106989178,2.24308440156553,12.5785808224116));
#425507=CARTESIAN_POINT('Ctrl Pts',(1.45203220930258,2.24333060050925,12.5777485681082));
#425508=CARTESIAN_POINT('Ctrl Pts',(1.45374753314142,2.2436974639085,12.576508418016));
#425509=CARTESIAN_POINT('Ctrl Pts',(1.45528484238996,2.24438731881001,12.5750928681475));
#425510=CARTESIAN_POINT('Ctrl Pts',(1.45642852040297,2.24524034769209,12.5737548217797));
#425511=CARTESIAN_POINT('Ctrl Pts',(1.45642852040297,2.24524034769209,12.5737548217797));
#425512=CARTESIAN_POINT('Ctrl Pts',(1.46808019059302,2.23374938356208,12.5770542771492));
#425513=CARTESIAN_POINT('Ctrl Pts',(1.47740364284705,2.24019390624622,12.5893111709658));
#425514=CARTESIAN_POINT('Ctrl Pts',(1.47676698075747,2.25935990804567,12.5508408821982));
#425515=CARTESIAN_POINT('Ctrl Pts',(1.48845249442907,2.24783105316495,12.55409748406));
#425516=CARTESIAN_POINT('Ctrl Pts',(1.49778784102034,2.25428379740954,12.5663972313419));
#425517=CARTESIAN_POINT('Ctrl Pts',(1.49708624564732,2.27346470645356,12.52790050457));
#425518=CARTESIAN_POINT('Ctrl Pts',(1.50878578045427,2.26188575301888,12.5311362602938));
#425519=CARTESIAN_POINT('Ctrl Pts',(1.51815147488721,2.26835947418794,12.5434568539655));
#425520=CARTESIAN_POINT('Ctrl Pts',(1.51738781470373,2.28755587873285,12.5049357605811));
#425521=CARTESIAN_POINT('Ctrl Pts',(1.529084116076,2.27591629458227,12.5081700652078));
#425522=CARTESIAN_POINT('Ctrl Pts',(1.53849615504836,2.28242204985496,12.5204921097672));
#425523=CARTESIAN_POINT('Ctrl Pts',(1.51605473500476,2.28663059582145,12.5064436508395));
#425524=CARTESIAN_POINT('Ctrl Pts',(1.51717154464663,2.28613908385374,12.5062361689309));
#425525=CARTESIAN_POINT('Ctrl Pts',(1.51831197612063,2.28558032838526,12.5061871075061));
#425526=CARTESIAN_POINT('Ctrl Pts',(1.51938369601753,2.28497830421322,12.5063648335164));
#425527=CARTESIAN_POINT('Ctrl Pts',(1.51987053730112,2.28470482769989,12.5064455676329));
#425528=CARTESIAN_POINT('Ctrl Pts',(1.52034988222133,2.28441841601867,12.506574497099));
#425529=CARTESIAN_POINT('Ctrl Pts',(1.52080063885185,2.28413044747091,12.5067492519495));
#425530=CARTESIAN_POINT('Ctrl Pts',(1.52170645179803,2.28355176349601,12.5071004286051));
#425531=CARTESIAN_POINT('Ctrl Pts',(1.52252968659954,2.28294483530112,12.5076537929613));
#425532=CARTESIAN_POINT('Ctrl Pts',(1.52321416791145,2.28236282913274,12.5083435010505));
#425533=CARTESIAN_POINT('Ctrl Pts',(1.5232572601005,2.28232618836636,12.5083869222964));
#425534=CARTESIAN_POINT('Ctrl Pts',(1.52329979931455,2.28228963328919,12.5084308732337));
#425535=CARTESIAN_POINT('Ctrl Pts',(1.52334177068723,2.28225317174875,12.5084753333615));
#425536=CARTESIAN_POINT('Ctrl Pts',(1.52367843649331,2.28196070206952,12.5088319622689));
#425537=CARTESIAN_POINT('Ctrl Pts',(1.52398624742104,2.28166928698463,12.509227847131));
#425538=CARTESIAN_POINT('Ctrl Pts',(1.52425797568876,2.28138962513347,12.5096423454524));
#425539=CARTESIAN_POINT('Ctrl Pts',(1.5251094518179,2.28051328866509,12.5109411997424));
#425540=CARTESIAN_POINT('Ctrl Pts',(1.52566593136802,2.27970519671489,12.5124831113042));
#425541=CARTESIAN_POINT('Ctrl Pts',(1.5260203540851,2.27898318354805,12.5140723025008));
#425542=CARTESIAN_POINT('Ctrl Pts',(1.52605356388188,2.27891553012351,12.5142212114565));
#425543=CARTESIAN_POINT('Ctrl Pts',(1.52608502882357,2.2788486274628,12.5143705582413));
#425544=CARTESIAN_POINT('Ctrl Pts',(1.52611484230059,2.27878248890665,12.5145201959299));
#425545=CARTESIAN_POINT('Ctrl Pts',(1.52649784080049,2.27793284068288,12.5164425148273));
#425546=CARTESIAN_POINT('Ctrl Pts',(1.52663120684895,2.2771845952175,12.5184635205941));
#425547=CARTESIAN_POINT('Ctrl Pts',(1.52659945261675,2.27650619824704,12.5205025929157));
#425548=CARTESIAN_POINT('Ctrl Pts',(1.52658103390345,2.27611270111503,12.5216853356836));
#425549=CARTESIAN_POINT('Ctrl Pts',(1.52650757743367,2.27574339243439,12.5228750347131));
#425550=CARTESIAN_POINT('Ctrl Pts',(1.52639732288665,2.27539777446118,12.5240609649613));
#425551=CARTESIAN_POINT('Ctrl Pts',(1.52612670901593,2.27454947368767,12.5269717671327));
#425552=CARTESIAN_POINT('Ctrl Pts',(1.52561689206398,2.27382317783633,12.5299036066169));
#425553=CARTESIAN_POINT('Ctrl Pts',(1.52494588207629,2.27318115157318,12.5328133004019));
#425554=CARTESIAN_POINT('Ctrl Pts',(1.52462375821045,2.2728729415828,12.5342101228451));
#425555=CARTESIAN_POINT('Ctrl Pts',(1.52426452606594,2.27258491524197,12.5356023438238));
#425556=CARTESIAN_POINT('Ctrl Pts',(1.52387624238129,2.2723165271091,12.5369868989719));
#425557=CARTESIAN_POINT('Origin',(12.0106235946827,9.5144905286836,-1.23909490405968));
#425558=CARTESIAN_POINT('Ctrl Pts',(1.43392337386552,2.33007984802669,12.5369868989719));
#425559=CARTESIAN_POINT('Ctrl Pts',(1.43664395014642,2.34517560134957,12.5369868989719));
#425560=CARTESIAN_POINT('Ctrl Pts',(1.42342012354076,2.35294822726294,12.5369868989719));
#425561=CARTESIAN_POINT('Ctrl Pts',(1.43484296988741,2.33518281478483,12.5218025310016));
#425562=CARTESIAN_POINT('Ctrl Pts',(1.43359076658335,2.34693389348384,12.5216901060418));
#425563=CARTESIAN_POINT('Ctrl Pts',(1.4234604425035,2.35292454794093,12.5161920673678));
#425564=CARTESIAN_POINT('Ctrl Pts',(1.44028510659882,2.33777496046166,12.5042015548894));
#425565=CARTESIAN_POINT('Ctrl Pts',(1.43842689613838,2.34393323935284,12.4980677368514));
#425566=CARTESIAN_POINT('Ctrl Pts',(1.43263111333136,2.34748284234156,12.4907278922777));
#425567=CARTESIAN_POINT('Ctrl Pts',(1.4501898818154,2.32893559382066,12.506463626192));
#425568=CARTESIAN_POINT('Ctrl Pts',(1.45364827026581,2.33448960027209,12.4999376786891));
#425569=CARTESIAN_POINT('Ctrl Pts',(1.45360603107938,2.3344217661588,12.4906970594712));
#425570=CARTESIAN_POINT('Origin',(1.41227217662088,2.33398185493001,12.5369868989719));
#425571=CARTESIAN_POINT('Origin',(1.41227217662088,2.33398185493001,14.));
#425572=CARTESIAN_POINT('Origin',(1.41227217662088,2.33398185493001,13.7435492065112));
#425573=CARTESIAN_POINT('Ctrl Pts',(1.42958547089512,2.30574515194253,13.793642941384));
#425574=CARTESIAN_POINT('Ctrl Pts',(1.43150976134211,2.31638485707385,13.8071662555867));
#425575=CARTESIAN_POINT('Ctrl Pts',(1.41537940665151,2.32184663711247,13.8103758687955));
#425576=CARTESIAN_POINT('Ctrl Pts',(1.43250238123844,2.32210832215104,13.7804579775005));
#425577=CARTESIAN_POINT('Ctrl Pts',(1.43486680281184,2.33523856138542,13.7901904343351));
#425578=CARTESIAN_POINT('Ctrl Pts',(1.42095719017033,2.34263981805758,13.7927914348262));
#425579=CARTESIAN_POINT('Ctrl Pts',(1.43421967609579,2.33174193627479,13.7597120340895));
#425580=CARTESIAN_POINT('Ctrl Pts',(1.43695033803418,2.34693833635346,13.7635825532446));
#425581=CARTESIAN_POINT('Ctrl Pts',(1.42422171320313,2.35490815605373,13.7651073818884));
#425582=CARTESIAN_POINT('Ctrl Pts',(1.43388339044034,2.32985545404484,13.7381884353898));
#425583=CARTESIAN_POINT('Ctrl Pts',(1.43655102081185,2.34469599510058,13.7368803041981));
#425584=CARTESIAN_POINT('Ctrl Pts',(1.42358194497715,2.35250577801131,13.7363986145813));
#425585=CARTESIAN_POINT('Origin',(1.40863470903346,2.31357650958568,13.7902182540695));
#425586=CARTESIAN_POINT('Ctrl Pts',(1.42401570789099,2.27449992929967,13.8235227101244));
#425587=CARTESIAN_POINT('Ctrl Pts',(1.42603773982375,2.28581779460998,13.8358800583119));
#425588=CARTESIAN_POINT('Ctrl Pts',(1.41051208250141,2.2916126210755,13.8390832900376));
#425589=CARTESIAN_POINT('Ctrl Pts',(1.42610892663473,2.28624239857086,13.8124254819053));
#425590=CARTESIAN_POINT('Ctrl Pts',(1.42813488505102,2.2975822430641,13.8247886449157));
#425591=CARTESIAN_POINT('Ctrl Pts',(1.4125836503793,2.30336842326239,13.8279860620657));
#425592=CARTESIAN_POINT('Ctrl Pts',(1.42820120726595,2.29797960524938,13.8013225099955));
#425593=CARTESIAN_POINT('Ctrl Pts',(1.43023013821212,2.30933607798735,13.8136962257787));
#425594=CARTESIAN_POINT('Ctrl Pts',(1.4146545261664,2.31511873605116,13.8168830918626));
#425595=CARTESIAN_POINT('Ctrl Pts',(1.43029258628516,2.30971175409457,13.7902140179785));
#425596=CARTESIAN_POINT('Ctrl Pts',(1.43232359815253,2.32107985386274,13.802602731458));
#425597=CARTESIAN_POINT('Ctrl Pts',(1.41672473886898,2.32686377481425,13.8057746032558));
#425598=CARTESIAN_POINT('Origin',(1.40235782844911,2.27836467252297,13.8235269408515));
#425599=CARTESIAN_POINT('Ctrl Pts',(1.47740364284705,2.24019390624622,13.8235269408515));
#425600=CARTESIAN_POINT('Ctrl Pts',(1.48711662013691,2.24690767500585,13.8362179249168));
#425601=CARTESIAN_POINT('Ctrl Pts',(1.49897171578034,2.23461459925801,13.8391868794938));
#425602=CARTESIAN_POINT('Ctrl Pts',(1.46851669140757,2.23405110006411,13.8400110824519));
#425603=CARTESIAN_POINT('Ctrl Pts',(1.4782493131047,2.23661974518589,13.8494522556836));
#425604=CARTESIAN_POINT('Ctrl Pts',(1.48428241609783,2.2245977006131,13.85569149686));
#425605=CARTESIAN_POINT('Ctrl Pts',(1.45249782979392,2.2310856660912,13.8586819406588));
#425606=CARTESIAN_POINT('Ctrl Pts',(1.45616802538609,2.22874350726861,13.868010383617));
#425607=CARTESIAN_POINT('Ctrl Pts',(1.45766421139961,2.21981858182324,13.8744918421245));
#425608=CARTESIAN_POINT('Ctrl Pts',(1.42614644312893,2.24795800791975,13.8587686893867));
#425609=CARTESIAN_POINT('Ctrl Pts',(1.4225088819522,2.25027927408403,13.8680909899357));
#425610=CARTESIAN_POINT('Ctrl Pts',(1.41379827847105,2.24790824297923,13.8745789365163));
#425611=CARTESIAN_POINT('Ctrl Pts',(1.4221173943012,2.26385082823282,13.8400379222776));
#425612=CARTESIAN_POINT('Ctrl Pts',(1.42040421962509,2.27376724222361,13.8494748685453));
#425613=CARTESIAN_POINT('Ctrl Pts',(1.40696857994555,2.27426190540908,13.8557104837033));
#425614=CARTESIAN_POINT('Ctrl Pts',(1.42401639941085,2.27450380427807,13.8235269408542));
#425615=CARTESIAN_POINT('Ctrl Pts',(1.42608854169682,2.28612803952764,13.8362179249195));
#425616=CARTESIAN_POINT('Ctrl Pts',(1.40998158196441,2.2918050856112,13.8391868794965));
#425617=CARTESIAN_POINT('Origin',(1.48991290767377,2.2220964397524,13.8235269408515));
#425618=CARTESIAN_POINT('Ctrl Pts',(1.50682270298796,2.26052884084395,13.7902140241682));
#425619=CARTESIAN_POINT('Ctrl Pts',(1.51631977736859,2.26709878556223,13.8026027327198));
#425620=CARTESIAN_POINT('Ctrl Pts',(1.5280610125852,2.25531229635374,13.8057746032556));
#425621=CARTESIAN_POINT('Ctrl Pts',(1.4970195552633,2.25375274480634,13.8013225161808));
#425622=CARTESIAN_POINT('Ctrl Pts',(1.50650691776783,2.26031596662135,13.8136962270464));
#425623=CARTESIAN_POINT('Ctrl Pts',(1.51823734697599,2.24855009921154,13.8168830918628));
#425624=CARTESIAN_POINT('Ctrl Pts',(1.48721218131346,2.24697372753278,13.8124254880875));
#425625=CARTESIAN_POINT('Ctrl Pts',(1.49668565306825,2.25352733783179,13.8247886461867));
#425626=CARTESIAN_POINT('Ctrl Pts',(1.50840915940023,2.24178510799748,13.8279860620656));
#425627=CARTESIAN_POINT('Ctrl Pts',(1.47740041004428,2.24019167076019,13.8235227163065));
#425628=CARTESIAN_POINT('Ctrl Pts',(1.48685551995534,2.24673257893923,13.8358800595847));
#425629=CARTESIAN_POINT('Ctrl Pts',(1.49857626599681,2.23501720685682,13.8390832900376));
#425630=CARTESIAN_POINT('Origin',(1.51933521085166,2.24243361691417,13.7902182540695));
#425631=CARTESIAN_POINT('Ctrl Pts',(1.52365426804161,2.27216306128232,13.7382347919292));
#425632=CARTESIAN_POINT('Ctrl Pts',(1.53605408873942,2.28076319589732,13.7369371795942));
#425633=CARTESIAN_POINT('Ctrl Pts',(1.54855062958131,2.27219696895615,13.7364597369711));
#425634=CARTESIAN_POINT('Ctrl Pts',(1.52521028684062,2.27323860741397,13.7595490285574));
#425635=CARTESIAN_POINT('Ctrl Pts',(1.53790652963333,2.28204310770456,13.7633824266926));
#425636=CARTESIAN_POINT('Ctrl Pts',(1.55044638650451,2.27375784066251,13.7648920890506));
#425637=CARTESIAN_POINT('Ctrl Pts',(1.51727467620672,2.2677533810723,13.780380659011));
#425638=CARTESIAN_POINT('Ctrl Pts',(1.52825339544785,2.27537339484063,13.7901039518744));
#425639=CARTESIAN_POINT('Ctrl Pts',(1.54077925076494,2.26580321250166,13.7926933640892));
#425640=CARTESIAN_POINT('Ctrl Pts',(1.50348081351774,2.25821883317055,13.7936647693663));
#425641=CARTESIAN_POINT('Ctrl Pts',(1.51236063256899,2.26439314653818,13.8072068914933));
#425642=CARTESIAN_POINT('Ctrl Pts',(1.52403450784357,2.25196877911278,13.8104111085397));
#425643=CARTESIAN_POINT('Origin',(1.53638550720801,2.25421906061527,13.7435492065112));
#425644=CARTESIAN_POINT('Origin',(1.53638550720801,2.25421906061527,14.));
#425645=CARTESIAN_POINT('Origin',(1.53638550720801,2.25421906061527,12.5369868989719));
#425646=CARTESIAN_POINT('Ctrl Pts',(1.51604457665074,2.28661527422765,12.506462012331));
#425647=CARTESIAN_POINT('Ctrl Pts',(1.51965773737332,2.29206492170091,12.4999388158272));
#425648=CARTESIAN_POINT('Ctrl Pts',(1.5196149889436,2.29200044522452,12.4907030323752));
#425649=CARTESIAN_POINT('Ctrl Pts',(1.52819857315075,2.28127589671409,12.5042014951932));
#425650=CARTESIAN_POINT('Ctrl Pts',(1.534569347831,2.28214441677112,12.4980716682127));
#425651=CARTESIAN_POINT('Ctrl Pts',(1.54020273176299,2.27835092883773,12.4907355092743));
#425652=CARTESIAN_POINT('Ctrl Pts',(1.52810378184397,2.27524956152149,12.5218047446509));
#425653=CARTESIAN_POINT('Ctrl Pts',(1.53930797999379,2.27898918914412,12.5216906929434));
#425654=CARTESIAN_POINT('Ctrl Pts',(1.54896278474319,2.27226940495258,12.5161988840776));
#425655=CARTESIAN_POINT('Ctrl Pts',(1.52384465989328,2.27229465600322,12.5369868989719));
#425656=CARTESIAN_POINT('Ctrl Pts',(1.53643997313891,2.28103328379968,12.5369868989719));
#425657=CARTESIAN_POINT('Ctrl Pts',(1.54899968222163,2.27224356029559,12.5369868989719));
#425658=CARTESIAN_POINT('Origin',(2.78530720815102E-31,-8.17839987285318E-32,
12.5));
#425659=CARTESIAN_POINT('Origin',(1.65508430440733,2.11231773338789,12.5));
#425660=CARTESIAN_POINT('',(1.65508430440733,2.11231773338789,12.5893111709658));
#425661=CARTESIAN_POINT('',(1.65508430440733,2.11231773338789,13.8235269408515));
#425662=CARTESIAN_POINT('',(1.65508430440733,2.11231773338789,12.5));
#425663=CARTESIAN_POINT('',(1.68606637603839,2.13018904941803,13.7902182540695));
#425664=CARTESIAN_POINT('',(1.65508430440733,2.11231773338789,13.8235269408515));
#425665=CARTESIAN_POINT('',(1.70402056201252,2.14054552058717,13.7435492065112));
#425666=CARTESIAN_POINT('Origin',(1.64495136471449,2.10647314951159,13.7445212918719));
#425667=CARTESIAN_POINT('',(1.70402056201252,2.14054552058717,12.5369868989719));
#425668=CARTESIAN_POINT('',(1.70402056201252,2.14054552058717,12.5));
#425669=CARTESIAN_POINT('Ctrl Pts',(1.70402056201252,2.14054552058717,12.5369868989719));
#425670=CARTESIAN_POINT('Ctrl Pts',(1.68772037318743,2.13114312073112,12.5544431401645));
#425671=CARTESIAN_POINT('Ctrl Pts',(1.67140852603406,2.12173399602879,12.5718848856037));
#425672=CARTESIAN_POINT('Ctrl Pts',(1.65508430440733,2.11231773338789,12.5893111709658));
#425673=CARTESIAN_POINT('Origin',(1.67483872942809,2.41676261471951,12.5));
#425674=CARTESIAN_POINT('',(1.6190859535201,2.20548903343026,13.7435492065112));
#425675=CARTESIAN_POINT('',(1.61379736422647,2.18544807256622,13.7902182540695));
#425676=CARTESIAN_POINT('Origin',(1.59989986561444,2.13278389118854,13.7418732680441));
#425677=CARTESIAN_POINT('',(1.6046712778331,2.1508650240259,13.8235269408515));
#425678=CARTESIAN_POINT('',(1.61379736422647,2.18544807256622,13.7902182540695));
#425679=CARTESIAN_POINT('',(1.6046712778331,2.1508650240259,12.5893111709658));
#425680=CARTESIAN_POINT('',(1.6046712778331,2.1508650240259,12.5));
#425681=CARTESIAN_POINT('',(1.6190859535201,2.20548903343026,12.5369868989719));
#425682=CARTESIAN_POINT('Ctrl Pts',(1.6046712778331,2.1508650240259,12.5893111709658));
#425683=CARTESIAN_POINT('Ctrl Pts',(1.60947974444063,2.16908657343108,12.5718848856037));
#425684=CARTESIAN_POINT('Ctrl Pts',(1.61428456602034,2.18729431010553,12.5544431401645));
#425685=CARTESIAN_POINT('Ctrl Pts',(1.6190859535201,2.20548903343026,12.5369868989719));
#425686=CARTESIAN_POINT('',(1.6190859535201,2.20548903343026,12.5));
#425687=CARTESIAN_POINT('Origin',(1.6379084766698,2.14209409257653,12.5));
#425688=CARTESIAN_POINT('',(1.61792956969214,2.11412208070473,13.8587068136939));
#425689=CARTESIAN_POINT('Ctrl Pts',(1.60467127782667,2.15086502402745,13.8235269408542));
#425690=CARTESIAN_POINT('Ctrl Pts',(1.60422417125196,2.14917072619708,13.8262006681044));
#425691=CARTESIAN_POINT('Ctrl Pts',(1.60393461161577,2.14739252956872,13.8288634856214));
#425692=CARTESIAN_POINT('Ctrl Pts',(1.60379158668926,2.14553795324233,13.8314912288862));
#425693=CARTESIAN_POINT('Ctrl Pts',(1.60364414274236,2.1436260763405,13.8342001611531));
#425694=CARTESIAN_POINT('Ctrl Pts',(1.60365176912644,2.14163094162529,13.8368750301949));
#425695=CARTESIAN_POINT('Ctrl Pts',(1.60384146006204,2.1395380377893,13.8394886372969));
#425696=CARTESIAN_POINT('Ctrl Pts',(1.60385611035312,2.13937639774937,13.8396904925131));
#425697=CARTESIAN_POINT('Ctrl Pts',(1.60387186870404,2.13921417270046,13.8398919674349));
#425698=CARTESIAN_POINT('Ctrl Pts',(1.60388875899436,2.13905135601658,13.8400930404591));
#425699=CARTESIAN_POINT('Ctrl Pts',(1.60415192108076,2.13651456254395,13.8432258934518));
#425700=CARTESIAN_POINT('Ctrl Pts',(1.60468740747428,2.13384697351913,13.8462331177034));
#425701=CARTESIAN_POINT('Ctrl Pts',(1.60557233302992,2.13115457704674,13.8489036603661));
#425702=CARTESIAN_POINT('Ctrl Pts',(1.60586189097013,2.13027359358798,13.8497774930041));
#425703=CARTESIAN_POINT('Ctrl Pts',(1.60618892724341,2.12939019546001,13.85061494757));
#425704=CARTESIAN_POINT('Ctrl Pts',(1.60655631689504,2.12850878830696,13.8514076489583));
#425705=CARTESIAN_POINT('Ctrl Pts',(1.60733339899377,2.12664448506031,13.8530843267192));
#425706=CARTESIAN_POINT('Ctrl Pts',(1.60837007562625,2.12460710348909,13.8546805203176));
#425707=CARTESIAN_POINT('Ctrl Pts',(1.60972778676256,2.12257677018939,13.8559412814273));
#425708=CARTESIAN_POINT('Ctrl Pts',(1.60990949254421,2.12230504574861,13.8561100121513));
#425709=CARTESIAN_POINT('Ctrl Pts',(1.61009687210231,2.12203345640009,13.8562727473908));
#425710=CARTESIAN_POINT('Ctrl Pts',(1.61028999686907,2.12176243316459,13.8564289040185));
#425711=CARTESIAN_POINT('Ctrl Pts',(1.61116581548311,2.12053334588351,13.8571370725437));
#425712=CARTESIAN_POINT('Ctrl Pts',(1.6121770391048,2.11929561847949,13.8577210840554));
#425713=CARTESIAN_POINT('Ctrl Pts',(1.61330708857883,2.11811592983647,13.8581177131616));
#425714=CARTESIAN_POINT('Ctrl Pts',(1.61362534940583,2.11778368891096,13.8582294175695));
#425715=CARTESIAN_POINT('Ctrl Pts',(1.61395288540951,2.11745595614763,13.8583265086086));
#425716=CARTESIAN_POINT('Ctrl Pts',(1.61428897011599,2.11713396335368,13.8584082369006));
#425717=CARTESIAN_POINT('Ctrl Pts',(1.61477183371452,2.11667134605454,13.8585256585398));
#425718=CARTESIAN_POINT('Ctrl Pts',(1.61527857035516,2.11621505925019,13.8586122832068));
#425719=CARTESIAN_POINT('Ctrl Pts',(1.61579654490457,2.11577754279017,13.8586682984299));
#425720=CARTESIAN_POINT('Ctrl Pts',(1.61621087319893,2.11542757299177,13.8587131050557));
#425721=CARTESIAN_POINT('Ctrl Pts',(1.61663681692492,2.11508556868615,13.8587357943552));
#425722=CARTESIAN_POINT('Ctrl Pts',(1.61707474377634,2.11475188413605,13.8587355499465));
#425723=CARTESIAN_POINT('Ctrl Pts',(1.61735778634109,2.1145362158559,13.8587353919793));
#425724=CARTESIAN_POINT('Ctrl Pts',(1.61764275044824,2.11432632447222,13.8587257282814));
#425725=CARTESIAN_POINT('Ctrl Pts',(1.61792956969214,2.11412208070473,13.8587068136939));
#425726=CARTESIAN_POINT('Ctrl Pts',(1.61792956969214,2.11412208070473,13.8587068136939));
#425727=CARTESIAN_POINT('Ctrl Pts',(1.61887290254913,2.11345033408795,13.8586446046466));
#425728=CARTESIAN_POINT('Ctrl Pts',(1.61983627860707,2.11283960288903,13.858482427929));
#425729=CARTESIAN_POINT('Ctrl Pts',(1.62081756846665,2.11228595625362,13.8582284286032));
#425730=CARTESIAN_POINT('Ctrl Pts',(1.62182425771426,2.11171797920851,13.8579678548414));
#425731=CARTESIAN_POINT('Ctrl Pts',(1.62285301181702,2.11121002665154,13.857615680862));
#425732=CARTESIAN_POINT('Ctrl Pts',(1.62385898301704,2.11077343593676,13.8571944833187));
#425733=CARTESIAN_POINT('Ctrl Pts',(1.62636948702899,2.1096838791572,13.8561433417727));
#425734=CARTESIAN_POINT('Ctrl Pts',(1.62885362278733,2.10898340107645,13.8546163505475));
#425735=CARTESIAN_POINT('Ctrl Pts',(1.63113830760212,2.10855886350875,13.8528973491086));
#425736=CARTESIAN_POINT('Ctrl Pts',(1.63155568581042,2.10848130675859,13.8525833129073));
#425737=CARTESIAN_POINT('Ctrl Pts',(1.6319664488489,2.10841282405783,13.8522628768812));
#425738=CARTESIAN_POINT('Ctrl Pts',(1.63236961975827,2.10835256485923,13.851937733538));
#425739=CARTESIAN_POINT('Ctrl Pts',(1.63483172856425,2.10798457029395,13.8499521282529));
#425740=CARTESIAN_POINT('Ctrl Pts',(1.63725598852144,2.10789072271098,13.847639871647));
#425741=CARTESIAN_POINT('Ctrl Pts',(1.63951188167932,2.10799567382824,13.8452109780794));
#425742=CARTESIAN_POINT('Ctrl Pts',(1.64052685470572,2.10804289350828,13.8441181685877));
#425743=CARTESIAN_POINT('Ctrl Pts',(1.64150802473536,2.10812969452228,13.8430021611332));
#425744=CARTESIAN_POINT('Ctrl Pts',(1.64244567205393,2.10824671439349,13.8418824960098));
#425745=CARTESIAN_POINT('Ctrl Pts',(1.64465526190383,2.10852247470822,13.8392439765549));
#425746=CARTESIAN_POINT('Ctrl Pts',(1.64672925705608,2.1089754761105,13.8364981347964));
#425747=CARTESIAN_POINT('Ctrl Pts',(1.64868044471151,2.10957348427616,13.8336931113419));
#425748=CARTESIAN_POINT('Ctrl Pts',(1.65058077757604,2.11015590625249,13.8309611966327));
#425749=CARTESIAN_POINT('Ctrl Pts',(1.65236636000607,2.11087699800988,13.8281701127185));
#425750=CARTESIAN_POINT('Ctrl Pts',(1.65402460814955,2.11173779082723,13.825358068512));
#425751=CARTESIAN_POINT('Ctrl Pts',(1.65438411813667,2.11192441163902,13.8247484142932));
#425752=CARTESIAN_POINT('Ctrl Pts',(1.65473749113902,2.11211768190021,13.8241378483365));
#425753=CARTESIAN_POINT('Ctrl Pts',(1.65508430440733,2.11231773338789,13.8235269408515));
#425754=CARTESIAN_POINT('',(1.61693200657635,2.11486211089867,12.5969504640361));
#425755=CARTESIAN_POINT('Origin',(1.63792872868682,2.14212025626543,12.584524458991));
#425756=CARTESIAN_POINT('Origin',(1.63792872868682,2.14212025626543,12.584524458991));
#425757=CARTESIAN_POINT('Ctrl Pts',(1.6046712778331,2.1508650240259,12.5893111709658));
#425758=CARTESIAN_POINT('Ctrl Pts',(1.60177936858179,2.13990621499198,12.5770542771492));
#425759=CARTESIAN_POINT('Ctrl Pts',(1.61654650137658,2.13285387751594,12.5737548217797));
#425760=CARTESIAN_POINT('Ctrl Pts',(1.61099491281211,2.17482826149746,12.5663937883686));
#425761=CARTESIAN_POINT('Ctrl Pts',(1.60809931452895,2.1638554729807,12.5540940315304));
#425762=CARTESIAN_POINT('Ctrl Pts',(1.62291359152771,2.15678417944156,12.5508374392248));
#425763=CARTESIAN_POINT('Ctrl Pts',(1.61731216732095,2.19876732035617,12.5434499600944));
#425764=CARTESIAN_POINT('Ctrl Pts',(1.61440715441655,2.18775885539644,12.5311293540533));
#425765=CARTESIAN_POINT('Ctrl Pts',(1.62927332069752,2.18069140432334,12.5278936106989));
#425766=CARTESIAN_POINT('Ctrl Pts',(1.62362354115058,2.2226840945459,12.5204817579905));
#425767=CARTESIAN_POINT('Ctrl Pts',(1.62070415041766,2.21162114520783,12.5081597038247));
#425768=CARTESIAN_POINT('Ctrl Pts',(1.63562624762186,2.20457734936162,12.5049254088044));
#425769=CARTESIAN_POINT('Ctrl Pts',(1.6190859535201,2.20548903343026,12.5369868989719));
#425770=CARTESIAN_POINT('Ctrl Pts',(1.61932363119355,2.20638970567602,12.5342545179733));
#425771=CARTESIAN_POINT('Ctrl Pts',(1.61967107693414,2.20721743665328,12.5314872231885));
#425772=CARTESIAN_POINT('Ctrl Pts',(1.62016026268745,2.20790396298846,12.5287124745063));
#425773=CARTESIAN_POINT('Ctrl Pts',(1.6206014346808,2.20852310651364,12.5262100684184));
#425774=CARTESIAN_POINT('Ctrl Pts',(1.62115824440522,2.20902620816193,12.5237004536639));
#425775=CARTESIAN_POINT('Ctrl Pts',(1.6218846948609,2.2093727197878,12.5212220730815));
#425776=CARTESIAN_POINT('Ctrl Pts',(1.62244085552771,2.20963800441305,12.5193246583486));
#425777=CARTESIAN_POINT('Ctrl Pts',(1.62310336659281,2.20981410583755,12.517417831369));
#425778=CARTESIAN_POINT('Ctrl Pts',(1.62391525613458,2.20981383113023,12.5155812248348));
#425779=CARTESIAN_POINT('Ctrl Pts',(1.6242611254433,2.20981371410344,12.5147988205793));
#425780=CARTESIAN_POINT('Ctrl Pts',(1.62463445524413,2.20978186513892,12.5140295443047));
#425781=CARTESIAN_POINT('Ctrl Pts',(1.62503977185742,2.20971329987201,12.5132817086137));
#425782=CARTESIAN_POINT('Ctrl Pts',(1.62565316372165,2.20960953561584,12.5121499604604));
#425783=CARTESIAN_POINT('Ctrl Pts',(1.62635186698226,2.20941238879121,12.5110494206568));
#425784=CARTESIAN_POINT('Ctrl Pts',(1.62713783922933,2.20908466979489,12.5100666561695));
#425785=CARTESIAN_POINT('Ctrl Pts',(1.62758914268366,2.20889649430187,12.5095023550641));
#425786=CARTESIAN_POINT('Ctrl Pts',(1.62807418217456,2.20866249210592,12.5089719619137));
#425787=CARTESIAN_POINT('Ctrl Pts',(1.62858109092889,2.20838129679704,12.5085043804652));
#425788=CARTESIAN_POINT('Ctrl Pts',(1.62932288586133,2.20796980409075,12.5078201359221));
#425789=CARTESIAN_POINT('Ctrl Pts',(1.63013244139569,2.20744425880307,12.5072563000949));
#425790=CARTESIAN_POINT('Ctrl Pts',(1.63095027184392,2.20683318422143,12.5068768744332));
#425791=CARTESIAN_POINT('Ctrl Pts',(1.63153998389674,2.20639255738156,12.5066032824114));
#425792=CARTESIAN_POINT('Ctrl Pts',(1.63214439471116,2.20589976737752,12.5064197834844));
#425793=CARTESIAN_POINT('Ctrl Pts',(1.63273138581492,2.20538433625565,12.5063282718343));
#425794=CARTESIAN_POINT('Ctrl Pts',(1.63358821109856,2.20463196639117,12.5061946931565));
#425795=CARTESIAN_POINT('Ctrl Pts',(1.63442693474951,2.20381607233106,12.5062515701262));
#425796=CARTESIAN_POINT('Ctrl Pts',(1.63520628727281,2.20299837479338,12.5064436508398));
#425797=CARTESIAN_POINT('',(1.61654650137658,2.13285387751594,12.5737548217797));
#425798=CARTESIAN_POINT('Origin',(1.62594308508859,2.1452516278983,12.5893111709658));
#425799=CARTESIAN_POINT('Ctrl Pts',(1.63520628727281,2.20299837479338,12.5064436508398));
#425800=CARTESIAN_POINT('Ctrl Pts',(1.63244461846173,2.19261504328903,12.5164271754438));
#425801=CARTESIAN_POINT('Ctrl Pts',(1.62968165300992,2.18222764953829,12.5264061185523));
#425802=CARTESIAN_POINT('Ctrl Pts',(1.62691734616548,2.17183605022895,12.536380305637));
#425803=CARTESIAN_POINT('Ctrl Pts',(1.62346252327176,2.15884865873571,12.5488460165097));
#425804=CARTESIAN_POINT('Ctrl Pts',(1.6200056040881,2.14585469435912,12.5613043021964));
#425805=CARTESIAN_POINT('Ctrl Pts',(1.61654650137658,2.13285387751594,12.5737548217797));
#425806=CARTESIAN_POINT('Ctrl Pts',(1.65508430440733,2.11231773338789,12.5893111709658));
#425807=CARTESIAN_POINT('Ctrl Pts',(1.64526658674475,2.10665460223475,12.5770542771492));
#425808=CARTESIAN_POINT('Ctrl Pts',(1.63459030677956,2.11905705041888,12.5737548217797));
#425809=CARTESIAN_POINT('Ctrl Pts',(1.64592445921814,2.10703408127733,12.5928319619712));
#425810=CARTESIAN_POINT('Ctrl Pts',(1.63769858136471,2.1060500335591,12.5821634970842));
#425811=CARTESIAN_POINT('Ctrl Pts',(1.63125831311288,2.11712416770785,12.5773203894503));
#425812=CARTESIAN_POINT('Ctrl Pts',(1.62924613397682,2.10547922871696,12.5969440695591));
#425813=CARTESIAN_POINT('Ctrl Pts',(1.62604181447296,2.10790634203715,12.5878292599214));
#425814=CARTESIAN_POINT('Ctrl Pts',(1.62531362775016,2.1165720236725,12.5813877129824));
#425815=CARTESIAN_POINT('Ctrl Pts',(1.604907571088,2.12402133221274,12.596957478804));
#425816=CARTESIAN_POINT('Ctrl Pts',(1.60808825821064,2.12161221980839,12.5878468778671));
#425817=CARTESIAN_POINT('Ctrl Pts',(1.61660613363589,2.12321324453574,12.5814011370086));
#425818=CARTESIAN_POINT('Ctrl Pts',(1.60196923397952,2.14062570459404,12.5928371701607));
#425819=CARTESIAN_POINT('Ctrl Pts',(1.60318073372141,2.13243623977153,12.5821692192952));
#425820=CARTESIAN_POINT('Ctrl Pts',(1.61555109509945,2.12911991931888,12.5773318885715));
#425821=CARTESIAN_POINT('Ctrl Pts',(1.60467127783304,2.15086502402591,12.5893111709658));
#425822=CARTESIAN_POINT('Ctrl Pts',(1.60177936858174,2.13990621499199,12.5770542771492));
#425823=CARTESIAN_POINT('Ctrl Pts',(1.61654650137653,2.13285387751595,12.5737548217797));
#425824=CARTESIAN_POINT('',(1.63459030677956,2.11905705041888,12.5737548217797));
#425825=CARTESIAN_POINT('Origin',(1.64409177465531,2.13137460326862,12.5893111709658));
#425826=CARTESIAN_POINT('Ctrl Pts',(1.61654650137653,2.13285387751595,12.5737548217797));
#425827=CARTESIAN_POINT('Ctrl Pts',(1.61625932847722,2.13189374660982,12.5746934679442));
#425828=CARTESIAN_POINT('Ctrl Pts',(1.61611705479564,2.13077880551821,12.5756680099006));
#425829=CARTESIAN_POINT('Ctrl Pts',(1.6161325638161,2.12963632438565,12.5765688348656));
#425830=CARTESIAN_POINT('Ctrl Pts',(1.61613666965758,2.12933386515348,12.5768073183026));
#425831=CARTESIAN_POINT('Ctrl Pts',(1.61615158379493,2.12902953490736,12.5770407398754));
#425832=CARTESIAN_POINT('Ctrl Pts',(1.61617698225217,2.1287256828689,12.5772674179684));
#425833=CARTESIAN_POINT('Ctrl Pts',(1.61628121065262,2.12747875626814,12.5781976435658));
#425834=CARTESIAN_POINT('Ctrl Pts',(1.61657916191547,2.12617000016873,12.5790594849312));
#425835=CARTESIAN_POINT('Ctrl Pts',(1.61709780233104,2.12489850308143,12.5797571720116));
#425836=CARTESIAN_POINT('Ctrl Pts',(1.61743571521043,2.1240700770101,12.580211740231));
#425837=CARTESIAN_POINT('Ctrl Pts',(1.61790004929595,2.12322690986335,12.5806009430798));
#425838=CARTESIAN_POINT('Ctrl Pts',(1.61847363653371,2.12243690331591,12.5808812374708));
#425839=CARTESIAN_POINT('Ctrl Pts',(1.61896653825652,2.12175802560971,12.5811221033394));
#425840=CARTESIAN_POINT('Ctrl Pts',(1.61955030145264,2.12110457302263,12.581287365893));
#425841=CARTESIAN_POINT('Ctrl Pts',(1.62019819567159,2.12051898241095,12.581359338449));
#425842=CARTESIAN_POINT('Ctrl Pts',(1.62028823958953,2.12043759740791,12.5813693411482));
#425843=CARTESIAN_POINT('Ctrl Pts',(1.62037949916551,2.12035746791303,12.5813775999465));
#425844=CARTESIAN_POINT('Ctrl Pts',(1.62047188003752,2.12027865081987,12.5813841266931));
#425845=CARTESIAN_POINT('Ctrl Pts',(1.6206286153601,2.12014492808861,12.5813952001081));
#425846=CARTESIAN_POINT('Ctrl Pts',(1.62079002328469,2.12001455072096,12.5814007534795));
#425847=CARTESIAN_POINT('Ctrl Pts',(1.6209561574325,2.11988772891379,12.5814005856065));
#425848=CARTESIAN_POINT('Ctrl Pts',(1.62171665460697,2.11930718826465,12.5813998171494));
#425849=CARTESIAN_POINT('Ctrl Pts',(1.62252343814571,2.11884099525493,12.58127954464));
#425850=CARTESIAN_POINT('Ctrl Pts',(1.62335712354063,2.1184661769397,12.5810700125799));
#425851=CARTESIAN_POINT('Ctrl Pts',(1.624364120575,2.11801343909139,12.5808169217085));
#425852=CARTESIAN_POINT('Ctrl Pts',(1.62541732084484,2.11770923923754,12.5804173076348));
#425853=CARTESIAN_POINT('Ctrl Pts',(1.62641719714309,2.11755521730455,12.5799304713245));
#425854=CARTESIAN_POINT('Ctrl Pts',(1.62765635887015,2.11736433560767,12.5793271277669));
#425855=CARTESIAN_POINT('Ctrl Pts',(1.62888558532817,2.11736044674188,12.5785808224116));
#425856=CARTESIAN_POINT('Ctrl Pts',(1.63005296191707,2.11751199793029,12.5777485681082));
#425857=CARTESIAN_POINT('Ctrl Pts',(1.63179248093017,2.11773782580469,12.576508418016));
#425858=CARTESIAN_POINT('Ctrl Pts',(1.63338090448777,2.11830008029549,12.5750928681475));
#425859=CARTESIAN_POINT('Ctrl Pts',(1.63459030677956,2.11905705041888,12.5737548217797));
#425860=CARTESIAN_POINT('Ctrl Pts',(1.63459030677956,2.11905705041888,12.5737548217797));
#425861=CARTESIAN_POINT('Ctrl Pts',(1.64526658674475,2.10665460223475,12.5770542771492));
#425862=CARTESIAN_POINT('Ctrl Pts',(1.65508430440733,2.11231773338789,12.5893111709658));
#425863=CARTESIAN_POINT('Ctrl Pts',(1.65601196783346,2.13147185576822,12.5508408821982));
#425864=CARTESIAN_POINT('Ctrl Pts',(1.66671889022083,2.11902888435382,12.5540974840599));
#425865=CARTESIAN_POINT('Ctrl Pts',(1.67654913277672,2.1246992402119,12.5663972313419));
#425866=CARTESIAN_POINT('Ctrl Pts',(1.67741329405842,2.1438735128996,12.52790050457));
#425867=CARTESIAN_POINT('Ctrl Pts',(1.68813010742981,2.13137946677734,12.5311362602938));
#425868=CARTESIAN_POINT('Ctrl Pts',(1.69799230666146,2.1370682561301,12.5434568539655));
#425869=CARTESIAN_POINT('Ctrl Pts',(1.69879587267538,2.15626303161689,12.5049357605811));
#425870=CARTESIAN_POINT('Ctrl Pts',(1.70950452140481,2.14370882007737,12.5081700652078));
#425871=CARTESIAN_POINT('Ctrl Pts',(1.71941552204513,2.14942575943273,12.5204921097672));
#425872=CARTESIAN_POINT('Ctrl Pts',(1.69739180954195,2.15544948587923,12.5064436508395));
#425873=CARTESIAN_POINT('Ctrl Pts',(1.69846484030352,2.15486857902327,12.5062361689309));
#425874=CARTESIAN_POINT('Ctrl Pts',(1.69955593332796,2.15421872701515,12.5061871075061));
#425875=CARTESIAN_POINT('Ctrl Pts',(1.70057501660636,2.15353135090792,12.5063648335164));
#425876=CARTESIAN_POINT('Ctrl Pts',(1.70103794709108,2.1532191022809,12.5064455676329));
#425877=CARTESIAN_POINT('Ctrl Pts',(1.70149235181968,2.1528945725499,12.506574497099));
#425878=CARTESIAN_POINT('Ctrl Pts',(1.70191813648468,2.15257082134372,12.5067492519495));
#425879=CARTESIAN_POINT('Ctrl Pts',(1.70277376729671,2.15192023072781,12.5071004286051));
#425880=CARTESIAN_POINT('Ctrl Pts',(1.70354479256992,2.15124822075764,12.5076537929612));
#425881=CARTESIAN_POINT('Ctrl Pts',(1.70417955742088,2.15061235958551,12.5083435010503));
#425882=CARTESIAN_POINT('Ctrl Pts',(1.7042195196617,2.15057232832472,12.5083869222963));
#425883=CARTESIAN_POINT('Ctrl Pts',(1.70425893775195,2.15053242754061,12.5084308732336));
#425884=CARTESIAN_POINT('Ctrl Pts',(1.70429779751439,2.15049266626635,12.5084753333615));
#425885=CARTESIAN_POINT('Ctrl Pts',(1.70460950409876,2.15017372836719,12.508831962269));
#425886=CARTESIAN_POINT('Ctrl Pts',(1.70489253777622,2.14985819349379,12.509227847131));
#425887=CARTESIAN_POINT('Ctrl Pts',(1.70514056685342,2.14955731381794,12.5096423454524));
#425888=CARTESIAN_POINT('Ctrl Pts',(1.7059177802083,2.14861449007762,12.5109411997424));
#425889=CARTESIAN_POINT('Ctrl Pts',(1.70640654112272,2.14776372873729,12.5124831113042));
#425890=CARTESIAN_POINT('Ctrl Pts',(1.70670093375151,2.14701522926795,12.5140723025008));
#425891=CARTESIAN_POINT('Ctrl Pts',(1.70672851866326,2.14694509404787,12.5142212114565));
#425892=CARTESIAN_POINT('Ctrl Pts',(1.70675442572002,2.14687584931539,12.5143705582413));
#425893=CARTESIAN_POINT('Ctrl Pts',(1.70677874908882,2.14680750075468,12.5145201959299));
#425894=CARTESIAN_POINT('Ctrl Pts',(1.70709121897482,2.14592946173196,12.5164425148273));
#425895=CARTESIAN_POINT('Ctrl Pts',(1.70716315230696,2.14517283542057,12.5184635205941));
#425896=CARTESIAN_POINT('Ctrl Pts',(1.70707620808332,2.14449928402478,12.5205025929157));
#425897=CARTESIAN_POINT('Ctrl Pts',(1.70702577698747,2.14410859751815,12.5216853356836));
#425898=CARTESIAN_POINT('Ctrl Pts',(1.70692246285206,2.1437465050659,12.5228750347131));
#425899=CARTESIAN_POINT('Ctrl Pts',(1.70678440409457,2.14341102387711,12.5240609649613));
#425900=CARTESIAN_POINT('Ctrl Pts',(1.70644554628091,2.14258760329718,12.5269717671326));
#425901=CARTESIAN_POINT('Ctrl Pts',(1.70587822584832,2.14190527894986,12.5299036066169));
#425902=CARTESIAN_POINT('Ctrl Pts',(1.70515711749028,2.14132008251949,12.5328133004019));
#425903=CARTESIAN_POINT('Ctrl Pts',(1.70481094348954,2.14103915415795,12.5342101228451));
#425904=CARTESIAN_POINT('Ctrl Pts',(1.70442942983967,2.14078136695572,12.5356023438238));
#425905=CARTESIAN_POINT('Ctrl Pts',(1.70402056201252,2.14054552058717,12.5369868989719));
#425906=CARTESIAN_POINT('Origin',(12.7471961618985,8.5044392418344,-1.24036033660154));
#425907=CARTESIAN_POINT('Ctrl Pts',(1.61907525114944,2.20544863268529,12.5369868989719));
#425908=CARTESIAN_POINT('Ctrl Pts',(1.62301721897513,2.2202724039108,12.5369868989719));
#425909=CARTESIAN_POINT('Ctrl Pts',(1.61047093473111,2.22909703168501,12.5369868989719));
#425910=CARTESIAN_POINT('Ctrl Pts',(1.62040772645585,2.2104596641296,12.5218025310015));
#425911=CARTESIAN_POINT('Ctrl Pts',(1.62011751176063,2.22227370827781,12.5216901060417));
#425912=CARTESIAN_POINT('Ctrl Pts',(1.61050918945125,2.22907014478422,12.5161920673677));
#425913=CARTESIAN_POINT('Ctrl Pts',(1.62604303884323,2.21259959999119,12.5042015548895));
#425914=CARTESIAN_POINT('Ctrl Pts',(1.62469296832513,2.2188888491207,12.4980677368514));
#425915=CARTESIAN_POINT('Ctrl Pts',(1.61920579610378,2.22289905120251,12.4907278922778));
#425916=CARTESIAN_POINT('Ctrl Pts',(1.63519436629549,2.20298231448191,12.506463626192));
#425917=CARTESIAN_POINT('Ctrl Pts',(1.63909395033029,2.20823594967023,12.4999376786891));
#425918=CARTESIAN_POINT('Ctrl Pts',(1.6390463225813,2.20817178415518,12.4906970594712));
#425919=CARTESIAN_POINT('Origin',(1.59781414626462,2.21110242955786,12.5369868989719));
#425920=CARTESIAN_POINT('Origin',(1.59781414626462,2.21110242955786,14.));
#425921=CARTESIAN_POINT('Origin',(1.59781414626462,2.21110242955786,13.7435492065112));
#425922=CARTESIAN_POINT('Ctrl Pts',(1.61276827855017,2.18154848765808,13.793642941384));
#425923=CARTESIAN_POINT('Ctrl Pts',(1.61555340082184,2.19199594251261,13.8071662555867));
#425924=CARTESIAN_POINT('Ctrl Pts',(1.59992190433366,2.19875432258291,13.8103758687955));
#425925=CARTESIAN_POINT('Ctrl Pts',(1.61700923339519,2.1976194554953,13.7804579775006));
#425926=CARTESIAN_POINT('Ctrl Pts',(1.62043602394366,2.21051328263337,13.7901904343352));
#425927=CARTESIAN_POINT('Ctrl Pts',(1.60717596551943,2.21902367479535,13.7927914348262));
#425928=CARTESIAN_POINT('Ctrl Pts',(1.61950604308078,2.20708103908937,13.7597120340895));
#425929=CARTESIAN_POINT('Ctrl Pts',(1.62346626664974,2.22200430010217,13.7635825532445));
#425930=CARTESIAN_POINT('Ctrl Pts',(1.61142960956155,2.23098510197535,13.7651073818884));
#425931=CARTESIAN_POINT('Ctrl Pts',(1.61901711057312,2.20522824437622,13.7381884353898));
#425932=CARTESIAN_POINT('Ctrl Pts',(1.62288550649353,2.21980196811551,13.7368803041982));
#425933=CARTESIAN_POINT('Ctrl Pts',(1.61059615399851,2.22864286469742,13.7363986145813));
#425934=CARTESIAN_POINT('Origin',(1.59252555697098,2.19106146869382,13.7902182540695));
#425935=CARTESIAN_POINT('Ctrl Pts',(1.60467027276106,2.15086121830799,13.8235227101244));
#425936=CARTESIAN_POINT('Ctrl Pts',(1.60760808764213,2.16197660998099,13.8358800583119));
#425937=CARTESIAN_POINT('Ctrl Pts',(1.59260642281721,2.16901763984444,13.8390832900376));
#425938=CARTESIAN_POINT('Ctrl Pts',(1.6077136467495,2.1623939987213,13.8124254819053));
#425939=CARTESIAN_POINT('Ctrl Pts',(1.61065716655649,2.17353097639845,13.8247886449158));
#425940=CARTESIAN_POINT('Ctrl Pts',(1.59562930473764,2.18056547355579,13.8279860620657));
#425941=CARTESIAN_POINT('Ctrl Pts',(1.61075565679672,2.17392161051757,13.8013225099955));
#425942=CARTESIAN_POINT('Ctrl Pts',(1.61370349459905,2.18507491882158,13.8136962257787));
#425943=CARTESIAN_POINT('Ctrl Pts',(1.59865104943327,2.19210789254638,13.8168830918626));
#425944=CARTESIAN_POINT('Ctrl Pts',(1.6137963559716,2.18544425479983,13.7902140179785));
#425945=CARTESIAN_POINT('Ctrl Pts',(1.61674721548195,2.19660898183165,13.802602731458));
#425946=CARTESIAN_POINT('Ctrl Pts',(1.60167170336868,2.20364510910769,13.8057746032558));
#425947=CARTESIAN_POINT('Origin',(1.58339947057761,2.1564784201535,13.8235269408515));
#425948=CARTESIAN_POINT('Ctrl Pts',(1.65508430440733,2.11231773338789,13.8235269408515));
#425949=CARTESIAN_POINT('Ctrl Pts',(1.66531219704801,2.11821746481581,13.8362179249168));
#425950=CARTESIAN_POINT('Ctrl Pts',(1.67612584604187,2.10499899291114,13.8391868794938));
#425951=CARTESIAN_POINT('Ctrl Pts',(1.6457262278348,2.10691973593138,13.8400110824519));
#425952=CARTESIAN_POINT('Ctrl Pts',(1.65563583345973,2.10868653507685,13.8494522556837));
#425953=CARTESIAN_POINT('Ctrl Pts',(1.66066895356037,2.09621273896306,13.85569149686));
#425954=CARTESIAN_POINT('Ctrl Pts',(1.62951895726314,2.10526985512872,13.8586819406588));
#425955=CARTESIAN_POINT('Ctrl Pts',(1.63298603289465,2.10263633463321,13.868010383617));
#425956=CARTESIAN_POINT('Ctrl Pts',(1.63374977619388,2.09361915309099,13.8744918421245));
#425957=CARTESIAN_POINT('Ctrl Pts',(1.60463050515763,2.12423393827925,13.8587686893867));
#425958=CARTESIAN_POINT('Ctrl Pts',(1.60119425240762,2.12684397562723,13.8680909899357));
#425959=CARTESIAN_POINT('Ctrl Pts',(1.59231937169436,2.12519082898184,13.8745789365163));
#425960=CARTESIAN_POINT('Ctrl Pts',(1.60191027505477,2.14040228142712,13.8400379222776));
#425961=CARTESIAN_POINT('Ctrl Pts',(1.60101108062577,2.15042533900887,13.8494748685453));
#425962=CARTESIAN_POINT('Ctrl Pts',(1.5876604665708,2.15201348560764,13.8557104837033));
#425963=CARTESIAN_POINT('Ctrl Pts',(1.60467127782667,2.15086502402745,13.8235269408542));
#425964=CARTESIAN_POINT('Ctrl Pts',(1.60768400831709,2.16228168176001,13.8362179249195));
#425965=CARTESIAN_POINT('Ctrl Pts',(1.5920933751234,2.16925270468897,13.8391868794965));
#425966=CARTESIAN_POINT('Origin',(1.66607683415935,2.09326086350716,13.8235269408515));
#425967=CARTESIAN_POINT('Ctrl Pts',(1.68606296100254,2.13018707865354,13.7902140241682));
#425968=CARTESIAN_POINT('Ctrl Pts',(1.69606394613856,2.13596106269421,13.8026027327198));
#425969=CARTESIAN_POINT('Ctrl Pts',(1.70680540507266,2.12325677238577,13.8057746032556));
#425970=CARTESIAN_POINT('Ctrl Pts',(1.67574011770996,2.12423257706404,13.8013225161808));
#425971=CARTESIAN_POINT('Ctrl Pts',(1.68573087530632,2.13000065217942,13.8136962270464));
#425972=CARTESIAN_POINT('Ctrl Pts',(1.6964632450561,2.11731779584232,13.8168830918628));
#425973=CARTESIAN_POINT('Ctrl Pts',(1.6654128241468,2.11827550843538,13.8124254880875));
#425974=CARTESIAN_POINT('Ctrl Pts',(1.67538895378594,2.12403513624135,13.8247886461868));
#425975=CARTESIAN_POINT('Ctrl Pts',(1.68611635037669,2.11137640310633,13.8279860620656));
#425976=CARTESIAN_POINT('Ctrl Pts',(1.65508090014856,2.11231576884368,13.8235227163065));
#425977=CARTESIAN_POINT('Ctrl Pts',(1.6650376937008,2.11806423345566,13.8358800595847));
#425978=CARTESIAN_POINT('Ctrl Pts',(1.6757645283418,2.10543249369491,13.8390832900376));
#425979=CARTESIAN_POINT('Origin',(1.69705890579041,2.1111321795373,13.7902182540695));
#425980=CARTESIAN_POINT('Ctrl Pts',(1.70378681738456,2.14041065837467,13.7382347919292));
#425981=CARTESIAN_POINT('Ctrl Pts',(1.71684636951277,2.14797147624999,13.7369371795943));
#425982=CARTESIAN_POINT('Ctrl Pts',(1.72860310212523,2.13841516863148,13.7364597369711));
#425983=CARTESIAN_POINT('Ctrl Pts',(1.70542532565402,2.14135579573781,13.7595490285574));
#425984=CARTESIAN_POINT('Ctrl Pts',(1.71879697125689,2.14909613812624,13.7633824266925));
#425985=CARTESIAN_POINT('Ctrl Pts',(1.73061977660815,2.13981632487743,13.7648920890506));
#425986=CARTESIAN_POINT('Ctrl Pts',(1.69706902324063,2.13653564697155,13.7803806590111));
#425987=CARTESIAN_POINT('Ctrl Pts',(1.70863231356203,2.14323543823304,13.7901039518745));
#425988=CARTESIAN_POINT('Ctrl Pts',(1.72033643142302,2.13267612639362,13.7926933640892));
#425989=CARTESIAN_POINT('Ctrl Pts',(1.68254390432342,2.12815715235653,13.7936647693663));
#425990=CARTESIAN_POINT('Ctrl Pts',(1.6918974403683,2.13358713351688,13.8072068914932));
#425991=CARTESIAN_POINT('Ctrl Pts',(1.70251977049854,2.12025257793931,13.8104111085397));
#425992=CARTESIAN_POINT('Origin',(1.71501309176454,2.12148865070644,13.7435492065112));
#425993=CARTESIAN_POINT('Origin',(1.71501309176454,2.12148865070644,14.));
#425994=CARTESIAN_POINT('Origin',(1.71501309176454,2.12148865070644,12.5369868989719));
#425995=CARTESIAN_POINT('Ctrl Pts',(1.69738043613688,2.15543504326693,12.506462012331));
#425996=CARTESIAN_POINT('Ctrl Pts',(1.70142577122634,2.16057205134594,12.4999388158272));
#425997=CARTESIAN_POINT('Ctrl Pts',(1.70137790960711,2.1605112738036,12.4907030323752));
#425998=CARTESIAN_POINT('Ctrl Pts',(1.70905878238044,2.14912276854463,12.5042014951932));
#425999=CARTESIAN_POINT('Ctrl Pts',(1.71547915128111,2.14946912139297,12.4980716682127));
#426000=CARTESIAN_POINT('Ctrl Pts',(1.72078458610918,2.14522908288952,12.4907355092743));
#426001=CARTESIAN_POINT('Ctrl Pts',(1.70847310421998,2.14312421185675,12.5218047446509));
#426002=CARTESIAN_POINT('Ctrl Pts',(1.71994483569297,2.14593815001309,12.5216906929434));
#426003=CARTESIAN_POINT('Ctrl Pts',(1.72901979008099,2.13845376913115,12.5161988840776));
#426004=CARTESIAN_POINT('Ctrl Pts',(1.70398730191446,2.14052629652156,12.5369868989719));
#426005=CARTESIAN_POINT('Ctrl Pts',(1.71725298458519,2.14820921229621,12.5369868989719));
#426006=CARTESIAN_POINT('Ctrl Pts',(1.72905445820664,2.13842500298309,12.5369868989719));
#426007=CARTESIAN_POINT('Origin',(3.12930240632745E-31,-1.0592894849964E-31,
12.5));
#426008=CARTESIAN_POINT('Origin',(1.82175065299146,1.97038443452176,12.5));
#426009=CARTESIAN_POINT('',(1.82175065299146,1.97038443452176,12.5893111709658));
#426010=CARTESIAN_POINT('',(1.82175065299146,1.97038443452176,13.8235269408515));
#426011=CARTESIAN_POINT('',(1.82175065299146,1.97038443452176,12.5));
#426012=CARTESIAN_POINT('',(1.85408631250068,1.98567095876063,13.7902182540695));
#426013=CARTESIAN_POINT('',(1.82175065299146,1.97038443452176,13.8235269408515));
#426014=CARTESIAN_POINT('',(1.87282490594716,1.99452953679089,13.7435492065112));
#426015=CARTESIAN_POINT('Origin',(1.81117504197252,1.96538522666951,13.7445212918709));
#426016=CARTESIAN_POINT('',(1.87282490594716,1.99452953679089,12.5369868989719));
#426017=CARTESIAN_POINT('',(1.87282490594716,1.99452953679089,12.5));
#426018=CARTESIAN_POINT('Ctrl Pts',(1.87282490594716,1.99452953679089,12.5369868989719));
#426019=CARTESIAN_POINT('Ctrl Pts',(1.85581257177983,1.98648703935753,12.5544431401645));
#426020=CARTESIAN_POINT('Ctrl Pts',(1.83878806993894,1.97843878971625,12.5718848856037));
#426021=CARTESIAN_POINT('Ctrl Pts',(1.82175065299146,1.97038443452176,12.5893111709658));
#426022=CARTESIAN_POINT('Origin',(1.8662544309495,2.27220613159535,12.5));
#426023=CARTESIAN_POINT('',(1.79346640956076,2.06617991453902,13.7435492065112));
#426024=CARTESIAN_POINT('',(1.7865618932501,2.04663670744329,13.7902182540695));
#426025=CARTESIAN_POINT('Origin',(1.76841801772587,1.99528053694052,13.7418732680445));
#426026=CARTESIAN_POINT('',(1.77464733364696,2.0129125919076,13.8235269408515));
#426027=CARTESIAN_POINT('',(1.7865618932501,2.04663670744329,13.7902182540695));
#426028=CARTESIAN_POINT('',(1.77464733364696,2.0129125919076,12.5893111709658));
#426029=CARTESIAN_POINT('',(1.77464733364696,2.0129125919076,12.5));
#426030=CARTESIAN_POINT('',(1.79346640956076,2.06617991453902,12.5369868989719));
#426031=CARTESIAN_POINT('Ctrl Pts',(1.77464733364696,2.0129125919076,12.5893111709658));
#426032=CARTESIAN_POINT('Ctrl Pts',(1.78092502591566,2.03068157594217,12.5718848856037));
#426033=CARTESIAN_POINT('Ctrl Pts',(1.78719795941929,2.04843709031033,12.5544431401645));
#426034=CARTESIAN_POINT('Ctrl Pts',(1.79346640956076,2.06617991453902,12.5369868989719));
#426035=CARTESIAN_POINT('',(1.79346640956076,2.06617991453902,12.5));
#426036=CARTESIAN_POINT('Origin',(1.80705902610793,2.00146170474478,12.5));
#426037=CARTESIAN_POINT('',(1.78486661864788,1.97521123382891,13.8587068136939));
#426038=CARTESIAN_POINT('Ctrl Pts',(1.77464733364068,2.01291259190967,13.8235269408542));
#426039=CARTESIAN_POINT('Ctrl Pts',(1.77406361377395,2.01126037505213,13.8262006681044));
#426040=CARTESIAN_POINT('Ctrl Pts',(1.77363007809038,2.00951169702485,13.8288634856214));
#426041=CARTESIAN_POINT('Ctrl Pts',(1.77333636387986,2.00767494950749,13.8314912288862));
#426042=CARTESIAN_POINT('Ctrl Pts',(1.77303357482403,2.00578145226881,13.8342001611531));
#426043=CARTESIAN_POINT('Ctrl Pts',(1.77287855383073,2.00379233457868,13.8368750301949));
#426044=CARTESIAN_POINT('Ctrl Pts',(1.77289702249318,2.00169093313529,13.8394886372969));
#426045=CARTESIAN_POINT('Ctrl Pts',(1.77289844887278,2.00152863680453,13.8396904925131));
#426046=CARTESIAN_POINT('Ctrl Pts',(1.77290093194159,2.00136566709419,13.8398919674349));
#426047=CARTESIAN_POINT('Ctrl Pts',(1.7729044949596,2.00120201545393,13.8400930404591));
#426048=CARTESIAN_POINT('Ctrl Pts',(1.7729600091774,1.99865221279919,13.8432258934518));
#426049=CARTESIAN_POINT('Ctrl Pts',(1.77327628051391,1.9959498528445,13.8462331177034));
#426050=CARTESIAN_POINT('Ctrl Pts',(1.77393880624529,1.99319428545123,13.8489036603661));
#426051=CARTESIAN_POINT('Ctrl Pts',(1.77415559237479,1.992292631732,13.8497774930041));
#426052=CARTESIAN_POINT('Ctrl Pts',(1.77440953531336,1.99138551654611,13.85061494757));
#426053=CARTESIAN_POINT('Ctrl Pts',(1.77470385964067,1.99047709653535,13.8514076489583));
#426054=CARTESIAN_POINT('Ctrl Pts',(1.77532639804086,1.98855565719886,13.8530843267192));
#426055=CARTESIAN_POINT('Ctrl Pts',(1.77619355970518,1.98644055607719,13.8546805203176));
#426056=CARTESIAN_POINT('Ctrl Pts',(1.77738126215705,1.98430631248208,13.8559412814273));
#426057=CARTESIAN_POINT('Ctrl Pts',(1.77754021526322,1.98402068147387,13.8561100121513));
#426058=CARTESIAN_POINT('Ctrl Pts',(1.77770483427809,1.98373472264295,13.8562727473908));
#426059=CARTESIAN_POINT('Ctrl Pts',(1.77787522552839,1.98344885975351,13.8564289040185));
#426060=CARTESIAN_POINT('Ctrl Pts',(1.77864794790453,1.98215247481122,13.8571370725437));
#426061=CARTESIAN_POINT('Ctrl Pts',(1.77955492048912,1.98083644173013,13.8577210840554));
#426062=CARTESIAN_POINT('Ctrl Pts',(1.78058505424064,1.97956856888076,13.8581177131616));
#426063=CARTESIAN_POINT('Ctrl Pts',(1.78087517536119,1.97921149224752,13.8582294175695));
#426064=CARTESIAN_POINT('Ctrl Pts',(1.78117490825311,1.97885815276292,13.8583265086086));
#426065=CARTESIAN_POINT('Ctrl Pts',(1.7814836292635,1.97850983734979,13.8584082369006));
#426066=CARTESIAN_POINT('Ctrl Pts',(1.78192717856864,1.97800940150559,13.8585256585398));
#426067=CARTESIAN_POINT('Ctrl Pts',(1.78239503747439,1.97751332921741,13.8586122832068));
#426068=CARTESIAN_POINT('Ctrl Pts',(1.78287562685303,1.97703504882291,13.8586682984299));
#426069=CARTESIAN_POINT('Ctrl Pts',(1.78326005071664,1.97665247191771,13.8587131050557));
#426070=CARTESIAN_POINT('Ctrl Pts',(1.78365670062409,1.97627688723527,13.8587357943552));
#426071=CARTESIAN_POINT('Ctrl Pts',(1.78406597192143,1.97590861788907,13.8587355499465));
#426072=CARTESIAN_POINT('Ctrl Pts',(1.78433049371834,1.97567059663072,13.8587353919793));
#426073=CARTESIAN_POINT('Ctrl Pts',(1.78459740153457,1.97543817642315,13.8587257282814));
#426074=CARTESIAN_POINT('Ctrl Pts',(1.78486661864788,1.97521123382891,13.8587068136939));
#426075=CARTESIAN_POINT('Ctrl Pts',(1.78486661864788,1.97521123382891,13.8587068136939));
#426076=CARTESIAN_POINT('Ctrl Pts',(1.78575205905721,1.97446483200821,13.8586446046466));
#426077=CARTESIAN_POINT('Ctrl Pts',(1.78666244929838,1.97377760887465,13.858482427929));
#426078=CARTESIAN_POINT('Ctrl Pts',(1.78759534665637,1.9731458202193,13.8582284286032));
#426079=CARTESIAN_POINT('Ctrl Pts',(1.78855239082654,1.97249767855163,13.8579678548414));
#426080=CARTESIAN_POINT('Ctrl Pts',(1.78953631898589,1.97190756315503,13.857615680862));
#426081=CARTESIAN_POINT('Ctrl Pts',(1.79050335670337,1.97139042916805,13.8571944833187));
#426082=CARTESIAN_POINT('Ctrl Pts',(1.79291669822787,1.97009986841542,13.8561433417727));
#426083=CARTESIAN_POINT('Ctrl Pts',(1.79533547276294,1.96919924099179,13.8546163505474));
#426084=CARTESIAN_POINT('Ctrl Pts',(1.79757795172452,1.96858989301544,13.8528973491086));
#426085=CARTESIAN_POINT('Ctrl Pts',(1.79798761954609,1.96847857413025,13.8525833129072));
#426086=CARTESIAN_POINT('Ctrl Pts',(1.79839143382854,1.96837683829907,13.8522628768811));
#426087=CARTESIAN_POINT('Ctrl Pts',(1.79878835153583,1.96828391743601,13.851937733538));
#426088=CARTESIAN_POINT('Ctrl Pts',(1.8012122729045,1.96771646261751,13.8499521282529));
#426089=CARTESIAN_POINT('Ctrl Pts',(1.80362081688741,1.96742532761238,13.847639871647));
#426090=CARTESIAN_POINT('Ctrl Pts',(1.80587775823729,1.9673460532784,13.8452109780794));
#426091=CARTESIAN_POINT('Ctrl Pts',(1.80689320286696,1.96731038611465,13.8441181685877));
#426092=CARTESIAN_POINT('Ctrl Pts',(1.80787818322274,1.96731692383928,13.8430021611332));
#426093=CARTESIAN_POINT('Ctrl Pts',(1.80882224880307,1.96735712737537,13.8418824960098));
#426094=CARTESIAN_POINT('Ctrl Pts',(1.81104696345071,1.9674518680348,13.8392439765549));
#426095=CARTESIAN_POINT('Ctrl Pts',(1.81315098137492,1.96773431225335,13.8364981347964));
#426096=CARTESIAN_POINT('Ctrl Pts',(1.81514441983153,1.96817129068831,13.8336931113419));
#426097=CARTESIAN_POINT('Ctrl Pts',(1.81708590229323,1.96859687993326,13.8309611966327));
#426098=CARTESIAN_POINT('Ctrl Pts',(1.81892431901754,1.96917003077274,13.8281701127185));
#426099=CARTESIAN_POINT('Ctrl Pts',(1.82064721208293,1.96989279675487,13.825358068512));
#426100=CARTESIAN_POINT('Ctrl Pts',(1.8210207371589,1.97004949319983,13.8247484142932));
#426101=CARTESIAN_POINT('Ctrl Pts',(1.82138868766226,1.97021331718992,13.8241378483365));
#426102=CARTESIAN_POINT('Ctrl Pts',(1.82175065299146,1.97038443452176,13.8235269408515));
#426103=CARTESIAN_POINT('',(1.78393269417216,1.97603011228814,12.5969504640361));
#426104=CARTESIAN_POINT('Origin',(1.80708134332157,2.00148613064876,12.584524458991));
#426105=CARTESIAN_POINT('Origin',(1.80708134332157,2.00148613064876,12.584524458991));
#426106=CARTESIAN_POINT('Ctrl Pts',(1.77464733364696,2.0129125919076,12.5893111709658));
#426107=CARTESIAN_POINT('Ctrl Pts',(1.77087180231224,2.00222596485786,12.5770542771492));
#426108=CARTESIAN_POINT('Ctrl Pts',(1.78501496771585,1.99399343503885,12.5737548217797));
#426109=CARTESIAN_POINT('Ctrl Pts',(1.78290315357002,2.03628065872676,12.5663937883685));
#426110=CARTESIAN_POINT('Ctrl Pts',(1.77912280602073,2.02558039940009,12.5540940315304));
#426111=CARTESIAN_POINT('Ctrl Pts',(1.79331141366479,2.0173251339024,12.5508374392248));
#426112=CARTESIAN_POINT('Ctrl Pts',(1.79115064347199,2.05962514745298,12.5434499600945));
#426113=CARTESIAN_POINT('Ctrl Pts',(1.78735800466664,2.04889009777273,12.5311293540533));
#426114=CARTESIAN_POINT('Ctrl Pts',(1.80159864213211,2.04063443249746,12.5278936106989));
#426115=CARTESIAN_POINT('Ctrl Pts',(1.79939045585481,2.0829479049905,12.5204817579905));
#426116=CARTESIAN_POINT('Ctrl Pts',(1.79557904607925,2.07215972415076,12.5081597038247));
#426117=CARTESIAN_POINT('Ctrl Pts',(1.80987735648312,2.06392307650201,12.5049254088044));
#426118=CARTESIAN_POINT('Ctrl Pts',(1.79346640956076,2.06617991453902,12.5369868989719));
#426119=CARTESIAN_POINT('Ctrl Pts',(1.79377670953082,2.0670582169353,12.5342545179733));
#426120=CARTESIAN_POINT('Ctrl Pts',(1.7941904669333,2.06785487365262,12.5314872231885));
#426121=CARTESIAN_POINT('Ctrl Pts',(1.79473398323109,2.06849924244778,12.5287124745063));
#426122=CARTESIAN_POINT('Ctrl Pts',(1.79522415320617,2.06908036621086,12.5262100684184));
#426123=CARTESIAN_POINT('Ctrl Pts',(1.79582011764708,2.06953640866822,12.5237004536639));
#426124=CARTESIAN_POINT('Ctrl Pts',(1.79657239481317,2.06982255484906,12.5212220730815));
#426125=CARTESIAN_POINT('Ctrl Pts',(1.79714832806097,2.07004162450412,12.5193246583486));
#426126=CARTESIAN_POINT('Ctrl Pts',(1.7978229885761,2.0701631391634,12.517417831369));
#426127=CARTESIAN_POINT('Ctrl Pts',(1.7986321542312,2.07009668883528,12.5155812248348));
#426128=CARTESIAN_POINT('Ctrl Pts',(1.79897686314955,2.07006838063833,12.5147988205793));
#426129=CARTESIAN_POINT('Ctrl Pts',(1.79934635473999,2.07000620780402,12.5140295443047));
#426130=CARTESIAN_POINT('Ctrl Pts',(1.7997447339899,2.06990483361562,12.5132817086137));
#426131=CARTESIAN_POINT('Ctrl Pts',(1.80034762709312,2.06975141749507,12.5121499604604));
#426132=CARTESIAN_POINT('Ctrl Pts',(1.80102793617984,2.06949797585804,12.5110494206568));
#426133=CARTESIAN_POINT('Ctrl Pts',(1.8017845810285,2.0691072832849,12.5100666561695));
#426134=CARTESIAN_POINT('Ctrl Pts',(1.8022190447582,2.06888294850909,12.5095023550641));
#426135=CARTESIAN_POINT('Ctrl Pts',(1.80268339696886,2.06861018971475,12.5089719619137));
#426136=CARTESIAN_POINT('Ctrl Pts',(1.80316569899797,2.06828861229067,12.5085043804652));
#426137=CARTESIAN_POINT('Ctrl Pts',(1.8038714851933,2.06781802561894,12.5078201359221));
#426138=CARTESIAN_POINT('Ctrl Pts',(1.80463551017852,2.06722824274825,12.5072563000949));
#426139=CARTESIAN_POINT('Ctrl Pts',(1.80540081111206,2.06655254069297,12.5068768744332));
#426140=CARTESIAN_POINT('Ctrl Pts',(1.80595264576864,2.06606531299563,12.5066032824114));
#426141=CARTESIAN_POINT('Ctrl Pts',(1.80651487849577,2.06552489761722,12.5064197834844));
#426142=CARTESIAN_POINT('Ctrl Pts',(1.8070579040136,2.06496333632558,12.5063282718343));
#426143=CARTESIAN_POINT('Ctrl Pts',(1.80785055315317,2.06414363069476,12.5061946931565));
#426144=CARTESIAN_POINT('Ctrl Pts',(1.80861998308007,2.06326208769095,12.5062515701262));
#426145=CARTESIAN_POINT('Ctrl Pts',(1.80933009243168,2.06238358650856,12.5064436508398));
#426146=CARTESIAN_POINT('',(1.78501496771585,1.99399343503885,12.5737548217797));
#426147=CARTESIAN_POINT('Origin',(1.79539081682198,2.0055840241234,12.5893111709658));
#426148=CARTESIAN_POINT('Ctrl Pts',(1.80933009243168,2.06238358650856,12.5064436508398));
#426149=CARTESIAN_POINT('Ctrl Pts',(1.80573127493399,2.05225990632942,12.5164271754438));
#426150=CARTESIAN_POINT('Ctrl Pts',(1.80213083399926,2.04213228310893,12.5264061185523));
#426151=CARTESIAN_POINT('Ctrl Pts',(1.79852871334319,2.03200057765943,12.536380305637));
#426152=CARTESIAN_POINT('Ctrl Pts',(1.79402679311189,2.01933800077885,12.5488460165097));
#426153=CARTESIAN_POINT('Ctrl Pts',(1.78952224781487,2.00666904375274,12.5613043021964));
#426154=CARTESIAN_POINT('Ctrl Pts',(1.78501496771585,1.99399343503885,12.5737548217797));
#426155=CARTESIAN_POINT('Ctrl Pts',(1.82175065299146,1.97038443452176,12.5893111709658));
#426156=CARTESIAN_POINT('Ctrl Pts',(1.81150400521158,1.9655403821031,12.5770542771492));
#426157=CARTESIAN_POINT('Ctrl Pts',(1.80187416435296,1.97877177809493,12.5737548217797));
#426158=CARTESIAN_POINT('Ctrl Pts',(1.81219061973347,1.96586497574649,12.5928319619712));
#426159=CARTESIAN_POINT('Ctrl Pts',(1.80391190378551,1.96555468777625,12.5821634970843));
#426160=CARTESIAN_POINT('Ctrl Pts',(1.79839570973538,1.97711691530823,12.5773203894503));
#426161=CARTESIAN_POINT('Ctrl Pts',(1.79544105532531,1.96567473517094,12.5969440695591));
#426162=CARTESIAN_POINT('Ctrl Pts',(1.79244523019807,1.96835495425879,12.5878292599214));
#426163=CARTESIAN_POINT('Ctrl Pts',(1.79242579995806,1.97705115553144,12.5813877129824));
#426164=CARTESIAN_POINT('Ctrl Pts',(1.7726948305681,1.98613896017059,12.596957478804));
#426165=CARTESIAN_POINT('Ctrl Pts',(1.77566856919067,1.98347860836047,12.5878468778671));
#426166=CARTESIAN_POINT('Ctrl Pts',(1.78428860046658,1.98438001988686,12.5814011370086));
#426167=CARTESIAN_POINT('Ctrl Pts',(1.7711196810305,2.00292758462508,12.5928371701607));
#426168=CARTESIAN_POINT('Ctrl Pts',(1.77165963219662,1.9946666210952,12.5821692192952));
#426169=CARTESIAN_POINT('Ctrl Pts',(1.78371852131355,1.99035303613215,12.5773318885715));
#426170=CARTESIAN_POINT('Ctrl Pts',(1.7746473336469,2.01291259190762,12.5893111709658));
#426171=CARTESIAN_POINT('Ctrl Pts',(1.77087180231219,2.00222596485788,12.5770542771492));
#426172=CARTESIAN_POINT('Ctrl Pts',(1.7850149677158,1.99399343503886,12.5737548217797));
#426173=CARTESIAN_POINT('',(1.80187416435296,1.97877177809493,12.5737548217797));
#426174=CARTESIAN_POINT('Origin',(1.812348011786,1.99027388746449,12.5893111709658));
#426175=CARTESIAN_POINT('Ctrl Pts',(1.7850149677158,1.99399343503886,12.5737548217797));
#426176=CARTESIAN_POINT('Ctrl Pts',(1.78465049077835,1.99305990614639,12.5746934679442));
#426177=CARTESIAN_POINT('Ctrl Pts',(1.78441781245114,1.99196027155514,12.5756680099006));
#426178=CARTESIAN_POINT('Ctrl Pts',(1.78434014704803,1.99082032780515,12.5765688348656));
#426179=CARTESIAN_POINT('Ctrl Pts',(1.78431958599235,1.99051854031693,12.5768073183026));
#426180=CARTESIAN_POINT('Ctrl Pts',(1.78430964476381,1.99021400706395,12.5770407398754));
#426181=CARTESIAN_POINT('Ctrl Pts',(1.78431019194782,1.98990909585803,12.5772674179684));
#426182=CARTESIAN_POINT('Ctrl Pts',(1.78431243744301,1.98865782272043,12.5781976435658));
#426183=CARTESIAN_POINT('Ctrl Pts',(1.7845027215256,1.98732913560501,12.5790594849312));
#426184=CARTESIAN_POINT('Ctrl Pts',(1.78491599739136,1.98601959531068,12.5797571720116));
#426185=CARTESIAN_POINT('Ctrl Pts',(1.78518526147797,1.98516638272206,12.580211740231));
#426186=CARTESIAN_POINT('Ctrl Pts',(1.78557932458009,1.9842881736058,12.5806009430798));
#426187=CARTESIAN_POINT('Ctrl Pts',(1.78608661038595,1.98345404305517,12.5808812374708));
#426188=CARTESIAN_POINT('Ctrl Pts',(1.78652253718349,1.98273724819225,12.5811221033394));
#426189=CARTESIAN_POINT('Ctrl Pts',(1.78705109550353,1.98203838779487,12.581287365893));
#426190=CARTESIAN_POINT('Ctrl Pts',(1.78764910283671,1.98140193629404,12.581359338449));
#426191=CARTESIAN_POINT('Ctrl Pts',(1.78773221350764,1.98131348267764,12.5813693411482));
#426192=CARTESIAN_POINT('Ctrl Pts',(1.7878166381272,1.9812261813044,12.5813775999465));
#426193=CARTESIAN_POINT('Ctrl Pts',(1.78790228728468,1.98114009656993,12.5813841266931));
#426194=CARTESIAN_POINT('Ctrl Pts',(1.78804760143938,1.98099404340616,12.5813952001081));
#426195=CARTESIAN_POINT('Ctrl Pts',(1.78819784532659,1.98085094361417,12.5814007534795));
#426196=CARTESIAN_POINT('Ctrl Pts',(1.78835308952209,1.98071100232073,12.5814005856065));
#426197=CARTESIAN_POINT('Ctrl Pts',(1.78906373675257,1.98007040579288,12.5813998171494));
#426198=CARTESIAN_POINT('Ctrl Pts',(1.78982983672742,1.97954000365373,12.58127954464));
#426199=CARTESIAN_POINT('Ctrl Pts',(1.79063019693062,1.97909847941628,12.5810700125799));
#426200=CARTESIAN_POINT('Ctrl Pts',(1.79159694092779,1.978565168409,12.5808169217085));
#426201=CARTESIAN_POINT('Ctrl Pts',(1.79262184164847,1.97817613515564,12.5804173076348));
#426202=CARTESIAN_POINT('Ctrl Pts',(1.79360583672341,1.97794112651723,12.5799304713245));
#426203=CARTESIAN_POINT('Ctrl Pts',(1.79482531661169,1.97764987677887,12.5793271277669));
#426204=CARTESIAN_POINT('Ctrl Pts',(1.79605013594142,1.97754580748505,12.5785808224116));
#426205=CARTESIAN_POINT('Ctrl Pts',(1.7972259810098,1.97760170236999,12.5777485681082));
#426206=CARTESIAN_POINT('Ctrl Pts',(1.79897811898514,1.97768499187229,12.576508418016));
#426207=CARTESIAN_POINT('Ctrl Pts',(1.8006070861551,1.97811590424151,12.5750928681475));
#426208=CARTESIAN_POINT('Ctrl Pts',(1.80187416435296,1.97877177809493,12.5737548217797));
#426209=CARTESIAN_POINT('Ctrl Pts',(1.80187416435296,1.97877177809493,12.5737548217797));
#426210=CARTESIAN_POINT('Ctrl Pts',(1.81150400521158,1.9655403821031,12.5770542771492));
#426211=CARTESIAN_POINT('Ctrl Pts',(1.82175065299146,1.97038443452176,12.5893111709658));
#426212=CARTESIAN_POINT('Ctrl Pts',(1.82423646848627,1.98939920995872,12.5508408821982));
#426213=CARTESIAN_POINT('Ctrl Pts',(1.83389354678749,1.97612492793244,12.55409748406));
#426214=CARTESIAN_POINT('Ctrl Pts',(1.84415326666565,1.98097516012137,12.5663972313419));
#426215=CARTESIAN_POINT('Ctrl Pts',(1.84657743375127,2.00001519483152,12.52790050457));
#426216=CARTESIAN_POINT('Ctrl Pts',(1.8562402070622,1.98668920183727,12.5311362602938));
#426217=CARTESIAN_POINT('Ctrl Pts',(1.86653327978389,1.99155520141915,12.5434568539655));
#426218=CARTESIAN_POINT('Ctrl Pts',(1.86889872439596,2.01062060978389,12.5049357605811));
#426219=CARTESIAN_POINT('Ctrl Pts',(1.87854845619206,1.99723531706192,12.5081700652078));
#426220=CARTESIAN_POINT('Ctrl Pts',(1.88889246242629,2.00212539521176,12.5204921097672));
#426221=CARTESIAN_POINT('Ctrl Pts',(1.86743302163657,2.00992421523262,12.5064436508395));
#426222=CARTESIAN_POINT('Ctrl Pts',(1.86845513267516,2.0092577793277,12.5062361689309));
#426223=CARTESIAN_POINT('Ctrl Pts',(1.86948962620598,2.00852115543782,12.5061871075061));
#426224=CARTESIAN_POINT('Ctrl Pts',(1.87044929103482,2.00775300176998,12.5063648335164));
#426225=CARTESIAN_POINT('Ctrl Pts',(1.87088522999466,2.00740405899237,12.5064455676329));
#426226=CARTESIAN_POINT('Ctrl Pts',(1.87131167054314,2.00704357090341,12.506574497099));
#426227=CARTESIAN_POINT('Ctrl Pts',(1.87170964971593,2.00668619154967,12.5067492519495));
#426228=CARTESIAN_POINT('Ctrl Pts',(1.87250940431204,2.00596802386589,12.5071004286051));
#426229=CARTESIAN_POINT('Ctrl Pts',(1.87322308901106,2.00523540423583,12.5076537929612));
#426230=CARTESIAN_POINT('Ctrl Pts',(1.87380391314577,2.00454991961107,12.5083435010503));
#426231=CARTESIAN_POINT('Ctrl Pts',(1.87384047949614,2.00450676425739,12.5083869222963));
#426232=CARTESIAN_POINT('Ctrl Pts',(1.87387651414162,2.00446378329956,12.5084308732336));
#426233=CARTESIAN_POINT('Ctrl Pts',(1.87391200368841,2.00442098689627,12.5084753333615));
#426234=CARTESIAN_POINT('Ctrl Pts',(1.87419667669519,2.0040777032563,12.508831962269));
#426235=CARTESIAN_POINT('Ctrl Pts',(1.87445304957996,2.00374014842688,12.509227847131));
#426236=CARTESIAN_POINT('Ctrl Pts',(1.87467572887406,2.00342005323096,12.5096423454524));
#426237=CARTESIAN_POINT('Ctrl Pts',(1.87537350722804,2.00241701655513,12.5109411997424));
#426238=CARTESIAN_POINT('Ctrl Pts',(1.87579129688352,2.00152924750102,12.5124831113042));
#426239=CARTESIAN_POINT('Ctrl Pts',(1.87602370028963,2.00075924286967,12.5140723025008));
#426240=CARTESIAN_POINT('Ctrl Pts',(1.87604547674333,2.00068709259235,12.5142212114565));
#426241=CARTESIAN_POINT('Ctrl Pts',(1.87606565350796,2.00061596660036,12.5143705582413));
#426242=CARTESIAN_POINT('Ctrl Pts',(1.87608432490054,2.00054586288349,12.5145201959299));
#426243=CARTESIAN_POINT('Ctrl Pts',(1.8763241867371,1.99964527626665,12.5164425148273));
#426244=CARTESIAN_POINT('Ctrl Pts',(1.87633420864846,1.99888530433253,12.518463520594));
#426245=CARTESIAN_POINT('Ctrl Pts',(1.87619265303285,1.99822108088482,12.5205025929157));
#426246=CARTESIAN_POINT('Ctrl Pts',(1.87611054516506,1.9978358049578,12.5216853356836));
#426247=CARTESIAN_POINT('Ctrl Pts',(1.87597806090256,1.99748333839948,12.5228750347131));
#426248=CARTESIAN_POINT('Ctrl Pts',(1.87581311669285,1.99716022656708,12.5240609649613));
#426249=CARTESIAN_POINT('Ctrl Pts',(1.87540826997908,1.99636716590881,12.5269717671327));
#426250=CARTESIAN_POINT('Ctrl Pts',(1.87478722148973,1.99573335382147,12.5299036066169));
#426251=CARTESIAN_POINT('Ctrl Pts',(1.87402081361849,1.99520888160956,12.532813300402));
#426252=CARTESIAN_POINT('Ctrl Pts',(1.8736528932137,1.99495710440875,12.5342101228452));
#426253=CARTESIAN_POINT('Ctrl Pts',(1.87325163696887,1.99473127187644,12.5356023438238));
#426254=CARTESIAN_POINT('Ctrl Pts',(1.87282490594716,1.99452953679089,12.5369868989719));
#426255=CARTESIAN_POINT('Origin',(13.3982603696714,7.43726248417796,-1.24070444298747));
#426256=CARTESIAN_POINT('Ctrl Pts',(1.79345244976558,2.06614052056676,12.5369868989719));
#426257=CARTESIAN_POINT('Ctrl Pts',(1.79858957599058,2.08059365994316,12.5369868989719));
#426258=CARTESIAN_POINT('Ctrl Pts',(1.78680432755982,2.09041156313634,12.5369868989719));
#426259=CARTESIAN_POINT('Ctrl Pts',(1.79518893695318,2.07102626910976,12.5218025310015));
#426260=CARTESIAN_POINT('Ctrl Pts',(1.79586264219775,2.08282465819253,12.5216901060418));
#426261=CARTESIAN_POINT('Ctrl Pts',(1.78684026345852,2.09038164758466,12.5161920673677));
#426262=CARTESIAN_POINT('Ctrl Pts',(1.8009799229424,2.07269975423603,12.5042015548895));
#426263=CARTESIAN_POINT('Ctrl Pts',(1.8001469768632,2.07907811968861,12.4980677368513));
#426264=CARTESIAN_POINT('Ctrl Pts',(1.79500493145329,2.08352223363022,12.4907278922778));
#426265=CARTESIAN_POINT('Ctrl Pts',(1.80931690205595,2.06236855130678,12.506463626192));
#426266=CARTESIAN_POINT('Ctrl Pts',(1.81363173058679,2.06728685315659,12.4999376786891));
#426267=CARTESIAN_POINT('Ctrl Pts',(1.81357903123004,2.0672267832507,12.4906970594712));
#426268=CARTESIAN_POINT('Origin',(1.77272292638574,2.07350848232323,12.5369868989719));
#426269=CARTESIAN_POINT('Origin',(1.77272292638574,2.07350848232323,14.));
#426270=CARTESIAN_POINT('Origin',(1.77272292638574,2.07350848232323,13.7435492065112));
#426271=CARTESIAN_POINT('Ctrl Pts',(1.7852183793995,2.04283397811842,13.793642941384));
#426272=CARTESIAN_POINT('Ctrl Pts',(1.78884579896665,2.05301965660783,13.8071662555867));
#426273=CARTESIAN_POINT('Ctrl Pts',(1.77381718571099,2.06102966080549,13.8103758687955));
#426274=CARTESIAN_POINT('Ctrl Pts',(1.79075515589145,2.05850579394497,13.7804579775006));
#426275=CARTESIAN_POINT('Ctrl Pts',(1.79522151068929,2.07107740269442,13.7901904343351));
#426276=CARTESIAN_POINT('Ctrl Pts',(1.78269924998341,2.08064029509048,13.7927914348262));
#426277=CARTESIAN_POINT('Ctrl Pts',(1.79401486454876,2.06773238173152,13.7597120340895));
#426278=CARTESIAN_POINT('Ctrl Pts',(1.79917829511383,2.08228319183858,13.7635825532445));
#426279=CARTESIAN_POINT('Ctrl Pts',(1.7879137077355,2.09221521012996,13.7651073818885));
#426280=CARTESIAN_POINT('Ctrl Pts',(1.79337653895405,2.06592560457833,13.7381884353898));
#426281=CARTESIAN_POINT('Ctrl Pts',(1.79841995688676,2.08013552527418,13.7368803041982));
#426282=CARTESIAN_POINT('Ctrl Pts',(1.78689211134467,2.08994870081916,13.7363986145813));
#426283=CARTESIAN_POINT('Origin',(1.76581841007508,2.05396527522749,13.7902182540695));
#426284=CARTESIAN_POINT('Ctrl Pts',(1.77464602171788,2.01290888077561,13.8235227101244));
#426285=CARTESIAN_POINT('Ctrl Pts',(1.77848006887388,2.02374782771363,13.8358800583119));
#426286=CARTESIAN_POINT('Ctrl Pts',(1.76410223015073,2.03198820408293,13.8390832900376));
#426287=CARTESIAN_POINT('Ctrl Pts',(1.77861929779921,2.02415522358009,13.8124254819052));
#426288=CARTESIAN_POINT('Ctrl Pts',(1.78246079035821,2.03501521969218,13.8247886449157));
#426289=CARTESIAN_POINT('Ctrl Pts',(1.7680563093333,2.04325122039067,13.8279860620657));
#426290=CARTESIAN_POINT('Ctrl Pts',(1.78259079318749,2.03539652613963,13.8013225099955));
#426291=CARTESIAN_POINT('Ctrl Pts',(1.78643792047172,2.04627244658305,13.8136962257787));
#426292=CARTESIAN_POINT('Ctrl Pts',(1.77200881372502,2.05450893268902,13.8168830918626));
#426293=CARTESIAN_POINT('Ctrl Pts',(1.78656057716672,2.04663298456234,13.7902140179785));
#426294=CARTESIAN_POINT('Ctrl Pts',(1.79041164683682,2.05752003944145,13.802602731458));
#426295=CARTESIAN_POINT('Ctrl Pts',(1.7759598069397,2.06576154877587,13.8057746032558));
#426296=CARTESIAN_POINT('Origin',(1.75390385047194,2.0202411596918,13.8235269408515));
#426297=CARTESIAN_POINT('Ctrl Pts',(1.82175065299146,1.97038443452176,13.8235269408515));
#426298=CARTESIAN_POINT('Ctrl Pts',(1.83242539604493,1.97543086687871,13.8362179249168));
#426299=CARTESIAN_POINT('Ctrl Pts',(1.84212563533929,1.96137496556683,13.8391868794938));
#426300=CARTESIAN_POINT('Ctrl Pts',(1.81198372774147,1.96576716857329,13.8400110824519));
#426301=CARTESIAN_POINT('Ctrl Pts',(1.82200437050368,1.96672036398564,13.8494522556837));
#426302=CARTESIAN_POINT('Ctrl Pts',(1.82600401312805,1.95387782738599,13.85569149686));
#426303=CARTESIAN_POINT('Ctrl Pts',(1.79569590492346,1.96544382062545,13.8586819406588));
#426304=CARTESIAN_POINT('Ctrl Pts',(1.79893678777804,1.96253646410141,13.868010383617));
#426305=CARTESIAN_POINT('Ctrl Pts',(1.79896300577732,1.95348703431776,13.8744918421245));
#426306=CARTESIAN_POINT('Ctrl Pts',(1.77243601591992,1.98637344225342,13.8587686893867));
#426307=CARTESIAN_POINT('Ctrl Pts',(1.76922393929173,1.98925488141718,13.8680909899357));
#426308=CARTESIAN_POINT('Ctrl Pts',(1.76024384221326,1.98833062064939,13.8745789365163));
#426309=CARTESIAN_POINT('Ctrl Pts',(1.77104270722445,2.00270971058003,13.8400379222776));
#426310=CARTESIAN_POINT('Ctrl Pts',(1.77096347703319,2.01277270995821,13.8494748685453));
#426311=CARTESIAN_POINT('Ctrl Pts',(1.75778673473655,2.01544377111672,13.8557104837033));
#426312=CARTESIAN_POINT('Ctrl Pts',(1.77464733364068,2.01291259190967,13.8235269408542));
#426313=CARTESIAN_POINT('Ctrl Pts',(1.77858060311121,2.02404569615164,13.8362179249195));
#426314=CARTESIAN_POINT('Ctrl Pts',(1.76361004954787,2.03226430491853,13.8391868794965));
#426315=CARTESIAN_POINT('Origin',(1.83115329419692,1.95049498157902,13.8235269408515));
#426316=CARTESIAN_POINT('Ctrl Pts',(1.85408274819248,1.98566927291083,13.7902140241682));
#426317=CARTESIAN_POINT('Ctrl Pts',(1.86452108917785,1.99060887136271,13.8026027327198));
#426318=CARTESIAN_POINT('Ctrl Pts',(1.87419128919243,1.97707132491028,13.8057746032556));
#426319=CARTESIAN_POINT('Ctrl Pts',(1.84330890615097,1.98057599199512,13.8013225161807));
#426320=CARTESIAN_POINT('Ctrl Pts',(1.85373657199566,1.98551053482259,13.8136962270464));
#426321=CARTESIAN_POINT('Ctrl Pts',(1.86339946013712,1.97199509187463,13.8168830918628));
#426322=CARTESIAN_POINT('Ctrl Pts',(1.83253041940917,1.97548051532018,13.8124254880875));
#426323=CARTESIAN_POINT('Ctrl Pts',(1.8429428174359,1.98040783126028,13.8247886461867));
#426324=CARTESIAN_POINT('Ctrl Pts',(1.85260271523098,1.96691683660509,13.8279860620656));
#426325=CARTESIAN_POINT('Ctrl Pts',(1.82174709993151,1.9703827539931,13.8235227163065));
#426326=CARTESIAN_POINT('Ctrl Pts',(1.8321393163066,1.97530051995441,13.8358800595847));
#426327=CARTESIAN_POINT('Ctrl Pts',(1.84180085423237,1.96183647465937,13.8390832900376));
#426328=CARTESIAN_POINT('Origin',(1.86348895370614,1.96578150581789,13.7902182540695));
#426329=CARTESIAN_POINT('Ctrl Pts',(1.87258094656285,1.99441417567843,13.7382347919292));
#426330=CARTESIAN_POINT('Ctrl Pts',(1.88621332095675,2.00088536081857,13.7369371795943));
#426331=CARTESIAN_POINT('Ctrl Pts',(1.89715200622395,1.99040256817324,13.7364597369711));
#426332=CARTESIAN_POINT('Ctrl Pts',(1.87429104030055,1.99522261453984,13.7595490285573));
#426333=CARTESIAN_POINT('Ctrl Pts',(1.88824910261822,2.00184728832458,13.7633824266925));
#426334=CARTESIAN_POINT('Ctrl Pts',(1.89927617763065,1.9916346844951,13.7648920890506));
#426335=CARTESIAN_POINT('Ctrl Pts',(1.86556965592157,1.99109962064379,13.7803806590111));
#426336=CARTESIAN_POINT('Ctrl Pts',(1.87764056553396,1.99683460339297,13.7901039518744));
#426337=CARTESIAN_POINT('Ctrl Pts',(1.88844505696549,1.98535643253125,13.7926933640892));
#426338=CARTESIAN_POINT('Ctrl Pts',(1.85040994304603,1.98393293681479,13.7936647693663));
#426339=CARTESIAN_POINT('Ctrl Pts',(1.86017494984539,1.98858245013912,13.8072068914933));
#426340=CARTESIAN_POINT('Ctrl Pts',(1.86967504497685,1.97442644567669,13.8104111085397));
#426341=CARTESIAN_POINT('Origin',(1.88222754715262,1.97464008384815,13.7435492065112));
#426342=CARTESIAN_POINT('Origin',(1.88222754715262,1.97464008384815,14.));
#426343=CARTESIAN_POINT('Origin',(1.88222754715262,1.97464008384815,12.5369868989719));
#426344=CARTESIAN_POINT('Ctrl Pts',(1.86742050886859,2.00991074771501,12.506462012331));
#426345=CARTESIAN_POINT('Ctrl Pts',(1.87187109728735,2.01470093045857,12.4999388158272));
#426346=CARTESIAN_POINT('Ctrl Pts',(1.87181844098977,2.01464425631477,12.4907030323752));
#426347=CARTESIAN_POINT('Ctrl Pts',(1.87854548738825,2.00266758293081,12.5042014951932));
#426348=CARTESIAN_POINT('Ctrl Pts',(1.88497272401356,2.00248946364943,12.4980716682127));
#426349=CARTESIAN_POINT('Ctrl Pts',(1.88991490294428,1.99783109133255,12.4907355092743));
#426350=CARTESIAN_POINT('Ctrl Pts',(1.87747281996563,1.99673672415271,12.5218047446509));
#426351=CARTESIAN_POINT('Ctrl Pts',(1.88913574228157,1.99860624654853,12.5216906929434));
#426352=CARTESIAN_POINT('Ctrl Pts',(1.89757045398399,1.99040707629619,12.5161988840776));
#426353=CARTESIAN_POINT('Ctrl Pts',(1.87279018957953,1.99451308769853,12.5369868989719));
#426354=CARTESIAN_POINT('Ctrl Pts',(1.88663796074585,2.00108916291449,12.5369868989719));
#426355=CARTESIAN_POINT('Ctrl Pts',(1.89760266204618,1.99037558009103,12.5369868989719));
#426356=CARTESIAN_POINT('Origin',(3.45247261328832E-31,-1.32797438156902E-31,
12.5));
#426357=CARTESIAN_POINT('Origin',(1.97629355154764,1.81533855233443,12.5));
#426358=CARTESIAN_POINT('',(1.97629355154764,1.81533855233443,12.5893111709658));
#426359=CARTESIAN_POINT('',(1.97629355154764,1.81533855233443,13.8235269408515));
#426360=CARTESIAN_POINT('',(1.97629355154764,1.81533855233443,12.5));
#426361=CARTESIAN_POINT('',(2.00976761045597,1.82793855548533,13.7902182540695));
#426362=CARTESIAN_POINT('',(1.97629355154764,1.81533855233443,13.8235269408515));
#426363=CARTESIAN_POINT('',(2.02916590912708,1.83524028800147,13.7435492065112));
#426364=CARTESIAN_POINT('Origin',(1.96534564815276,1.81121798941157,13.7445212918713));
#426365=CARTESIAN_POINT('',(2.02916590912708,1.83524028800147,12.5369868989719));
#426366=CARTESIAN_POINT('',(2.02916590912708,1.83524028800147,12.5));
#426367=CARTESIAN_POINT('Ctrl Pts',(2.02916590912708,1.83524028800147,12.5369868989719));
#426368=CARTESIAN_POINT('Ctrl Pts',(2.01155464389455,1.82861121448431,12.5544431401645));
#426369=CARTESIAN_POINT('Ctrl Pts',(1.99393078261705,1.82197739967757,12.5718848856037));
#426370=CARTESIAN_POINT('Ctrl Pts',(1.97629355154764,1.81533855233443,12.5893111709658));
#426371=CARTESIAN_POINT('Origin',(2.04525051714325,2.11252849155305,12.5));
#426372=CARTESIAN_POINT('',(1.95591164254692,1.91312070921222,13.7435492065112));
#426373=CARTESIAN_POINT('',(1.94743714763612,1.89420531270362,13.7902182540695));
#426374=CARTESIAN_POINT('Origin',(1.92516763969895,1.84449891991954,13.7418732680457));
#426375=CARTESIAN_POINT('',(1.9328134042516,1.86156455859736,13.8235269408515));
#426376=CARTESIAN_POINT('',(1.94743714763612,1.89420531270362,13.7902182540695));
#426377=CARTESIAN_POINT('',(1.9328134042516,1.86156455859736,12.5893111709658));
#426378=CARTESIAN_POINT('',(1.9328134042516,1.86156455859736,12.5));
#426379=CARTESIAN_POINT('',(1.95591164254692,1.91312070921222,12.5369868989719));
#426380=CARTESIAN_POINT('Ctrl Pts',(1.9328134042516,1.86156455859736,12.5893111709658));
#426381=CARTESIAN_POINT('Ctrl Pts',(1.94051854517517,1.87876272760424,12.5718848856037));
#426382=CARTESIAN_POINT('Ctrl Pts',(1.9482178452652,1.89594785964745,12.5544431401645));
#426383=CARTESIAN_POINT('Ctrl Pts',(1.95591164254692,1.91312070921222,12.5369868989719));
#426384=CARTESIAN_POINT('',(1.95591164254692,1.91312070921222,12.5));
#426385=CARTESIAN_POINT('Origin',(1.96418389587106,1.8475099194859,12.5));
#426386=CARTESIAN_POINT('',(1.93992567473915,1.82315568207856,13.8587068136939));
#426387=CARTESIAN_POINT('Ctrl Pts',(1.93281340424551,1.86156455859993,13.8235269408542));
#426388=CARTESIAN_POINT('Ctrl Pts',(1.93209695564616,1.85996541794582,13.8262006681044));
#426389=CARTESIAN_POINT('Ctrl Pts',(1.93152232902365,1.85825789568338,13.8288634856214));
#426390=CARTESIAN_POINT('Ctrl Pts',(1.93107988014874,1.85645120022672,13.8314912288862));
#426391=CARTESIAN_POINT('Ctrl Pts',(1.9306237609952,1.85458868356291,13.8342001611531));
#426392=CARTESIAN_POINT('Ctrl Pts',(1.93030712426365,1.85261882014791,13.8368750301949));
#426393=CARTESIAN_POINT('Ctrl Pts',(1.93015424774706,1.85052290557702,13.8394886372969));
#426394=CARTESIAN_POINT('Ctrl Pts',(1.93014244072286,1.85036103301074,13.8396904925131));
#426395=CARTESIAN_POINT('Ctrl Pts',(1.93013163198512,1.8501984031755,13.8398919674349));
#426396=CARTESIAN_POINT('Ctrl Pts',(1.93012184401954,1.85003500565352,13.8400930404591));
#426397=CARTESIAN_POINT('Ctrl Pts',(1.92996934093079,1.84748916233266,13.8432258934518));
#426398=CARTESIAN_POINT('Ctrl Pts',(1.93006429247672,1.84477001520775,13.8462331177034));
#426399=CARTESIAN_POINT('Ctrl Pts',(1.93050000938439,1.84196961473997,13.8489036603661));
#426400=CARTESIAN_POINT('Ctrl Pts',(1.93064258102727,1.84105329111701,13.849777493004));
#426401=CARTESIAN_POINT('Ctrl Pts',(1.93082174068276,1.84012849557507,13.85061494757));
#426402=CARTESIAN_POINT('Ctrl Pts',(1.93104104100592,1.83919910809192,13.8514076489583));
#426403=CARTESIAN_POINT('Ctrl Pts',(1.93150489281725,1.83723331952729,13.8530843267192));
#426404=CARTESIAN_POINT('Ctrl Pts',(1.93219676869563,1.83505457450409,13.8546805203176));
#426405=CARTESIAN_POINT('Ctrl Pts',(1.93320655849924,1.83283062365253,13.8559412814274));
#426406=CARTESIAN_POINT('Ctrl Pts',(1.93334170112321,1.83253298690417,13.8561100121513));
#426407=CARTESIAN_POINT('Ctrl Pts',(1.93348246408243,1.83223456159975,13.8562727473908));
#426408=CARTESIAN_POINT('Ctrl Pts',(1.93362898789057,1.8319357614268,13.8564289040185));
#426409=CARTESIAN_POINT('Ctrl Pts',(1.93429347168891,1.8305807060512,13.8571370725437));
#426410=CARTESIAN_POINT('Ctrl Pts',(1.93509015748347,1.82919512527606,13.8577210840553));
#426411=CARTESIAN_POINT('Ctrl Pts',(1.93601352014234,1.82784750570495,13.8581177131616));
#426412=CARTESIAN_POINT('Ctrl Pts',(1.93627357084825,1.82746796965008,13.8582294175695));
#426413=CARTESIAN_POINT('Ctrl Pts',(1.93654350595545,1.82709137486019,13.8583265086086));
#426414=CARTESIAN_POINT('Ctrl Pts',(1.93682280878238,1.82671905480949,13.8584082369006));
#426415=CARTESIAN_POINT('Ctrl Pts',(1.93722409204667,1.8261841307382,13.8585256585398));
#426416=CARTESIAN_POINT('Ctrl Pts',(1.93764995969372,1.82565157424543,13.8586122832068));
#426417=CARTESIAN_POINT('Ctrl Pts',(1.93808996565855,1.82513571279355,13.8586682984299));
#426418=CARTESIAN_POINT('Ctrl Pts',(1.93844192681403,1.82472307476775,13.8587131050557));
#426419=CARTESIAN_POINT('Ctrl Pts',(1.93880664326325,1.82431640916258,13.8587357943552));
#426420=CARTESIAN_POINT('Ctrl Pts',(1.93918453537355,1.82391600579203,13.8587355499465));
#426421=CARTESIAN_POINT('Ctrl Pts',(1.93942877605383,1.82365721554756,13.8587353919793));
#426422=CARTESIAN_POINT('Ctrl Pts',(1.93967585135178,1.82340381323412,13.8587257282814));
#426423=CARTESIAN_POINT('Ctrl Pts',(1.93992567473915,1.82315568207856,13.8587068136939));
#426424=CARTESIAN_POINT('Ctrl Pts',(1.93992567473915,1.82315568207856,13.8587068136939));
#426425=CARTESIAN_POINT('Ctrl Pts',(1.94074733024086,1.82233959223502,13.8586446046466));
#426426=CARTESIAN_POINT('Ctrl Pts',(1.94159867616829,1.82158045052351,13.858482427929));
#426427=CARTESIAN_POINT('Ctrl Pts',(1.94247697274657,1.82087472429757,13.8582284286032));
#426428=CARTESIAN_POINT('Ctrl Pts',(1.94337800286824,1.82015073128319,13.8579678548414));
#426429=CARTESIAN_POINT('Ctrl Pts',(1.94431055720462,1.81948238016756,13.857615680862));
#426430=CARTESIAN_POINT('Ctrl Pts',(1.9452322259631,1.81888814434975,13.8571944833187));
#426431=CARTESIAN_POINT('Ctrl Pts',(1.9475323446104,1.81740516809297,13.8561433417727));
#426432=CARTESIAN_POINT('Ctrl Pts',(1.94986966137666,1.81631038485339,13.8546163505475));
#426433=CARTESIAN_POINT('Ctrl Pts',(1.95205501115748,1.81552028157863,13.8528973491087));
#426434=CARTESIAN_POINT('Ctrl Pts',(1.95245424232062,1.81537594136721,13.8525833129073));
#426435=CARTESIAN_POINT('Ctrl Pts',(1.95284842052968,1.81524162944075,13.8522628768812));
#426436=CARTESIAN_POINT('Ctrl Pts',(1.9532364436131,1.81511666528624,13.851937733538));
#426437=CARTESIAN_POINT('Ctrl Pts',(1.95560604674767,1.8143535265327,13.8499521282529));
#426438=CARTESIAN_POINT('Ctrl Pts',(1.95798284629349,1.81386704156084,13.847639871647));
#426439=CARTESIAN_POINT('Ctrl Pts',(1.96022581626304,1.81360406933324,13.8452109780794));
#426440=CARTESIAN_POINT('Ctrl Pts',(1.96123497487951,1.81348575268478,13.8441181685877));
#426441=CARTESIAN_POINT('Ctrl Pts',(1.96221721067966,1.81341198361257,13.8430021611332));
#426442=CARTESIAN_POINT('Ctrl Pts',(1.96316141192108,1.81337510326563,13.8418824960098));
#426443=CARTESIAN_POINT('Ctrl Pts',(1.96538644625752,1.81328819378631,13.8392439765549));
#426444=CARTESIAN_POINT('Ctrl Pts',(1.96750648506154,1.81339820120145,13.8364981347964));
#426445=CARTESIAN_POINT('Ctrl Pts',(1.96952890831528,1.81367124188632,13.833693111342));
#426446=CARTESIAN_POINT('Ctrl Pts',(1.97149862012867,1.8139371661737,13.8309611966328));
#426447=CARTESIAN_POINT('Ctrl Pts',(1.97337763678728,1.81435856187097,13.8281701127186));
#426448=CARTESIAN_POINT('Ctrl Pts',(1.9751537092055,1.81493849112953,13.8253580685121));
#426449=CARTESIAN_POINT('Ctrl Pts',(1.97553876362257,1.81506422041867,13.8247484142933));
#426450=CARTESIAN_POINT('Ctrl Pts',(1.97591884297707,1.81519750791604,13.8241378483365));
#426451=CARTESIAN_POINT('Ctrl Pts',(1.97629355154764,1.81533855233443,13.8235269408515));
#426452=CARTESIAN_POINT('',(1.93906160401641,1.82404795930237,12.5969504640361));
#426453=CARTESIAN_POINT('Origin',(1.96420812976395,1.84753244505461,12.584524458991));
#426454=CARTESIAN_POINT('Origin',(1.96420812976395,1.84753244505461,12.584524458991));
#426455=CARTESIAN_POINT('Ctrl Pts',(1.9328134042516,1.86156455859736,12.5893111709658));
#426456=CARTESIAN_POINT('Ctrl Pts',(1.92817937637158,1.85122123127164,12.5770542771492));
#426457=CARTESIAN_POINT('Ctrl Pts',(1.94160445395171,1.84186329523733,12.5737548217797));
#426458=CARTESIAN_POINT('Ctrl Pts',(1.94294646799923,1.88418194413488,12.5663937883685));
#426459=CARTESIAN_POINT('Ctrl Pts',(1.93830652877308,1.8738254224587,12.5540940315304));
#426460=CARTESIAN_POINT('Ctrl Pts',(1.95177504421946,1.86444112243238,12.5508374392248));
#426461=CARTESIAN_POINT('Ctrl Pts',(1.95306930760976,1.90677650900767,12.5434499600945));
#426462=CARTESIAN_POINT('Ctrl Pts',(1.94841428228888,1.89638631459144,12.5311293540533));
#426463=CARTESIAN_POINT('Ctrl Pts',(1.96193462184618,1.88699737520424,12.5278936106989));
#426464=CARTESIAN_POINT('Ctrl Pts',(1.96318272395384,1.9293500407896,12.5204817579905));
#426465=CARTESIAN_POINT('Ctrl Pts',(1.95850465943888,1.91890842201175,12.5081597038247));
#426466=CARTESIAN_POINT('Ctrl Pts',(1.97208403014572,1.90953373609163,12.5049254088044));
#426467=CARTESIAN_POINT('Ctrl Pts',(1.95591164254692,1.91312070921222,12.5369868989719));
#426468=CARTESIAN_POINT('Ctrl Pts',(1.95629249981849,1.91397079680149,12.5342545179733));
#426469=CARTESIAN_POINT('Ctrl Pts',(1.9567698153956,1.91473107763987,12.5314872231885));
#426470=CARTESIAN_POINT('Ctrl Pts',(1.95736404522658,1.91532900072698,12.5287124745063));
#426471=CARTESIAN_POINT('Ctrl Pts',(1.95789995118309,1.9158682374452,12.5262100684184));
#426472=CARTESIAN_POINT('Ctrl Pts',(1.95853110429545,1.91627418582429,12.5237004536639));
#426473=CARTESIAN_POINT('Ctrl Pts',(1.95930420189151,1.91649806230449,12.5212220730815));
#426474=CARTESIAN_POINT('Ctrl Pts',(1.95989607497958,1.91666945911695,12.5193246583486));
#426475=CARTESIAN_POINT('Ctrl Pts',(1.96057839519032,1.91673557835099,12.517417831369));
#426476=CARTESIAN_POINT('Ctrl Pts',(1.96137945209482,1.91660339461804,12.5155812248347));
#426477=CARTESIAN_POINT('Ctrl Pts',(1.96172070664183,1.91654708363731,12.5147988205793));
#426478=CARTESIAN_POINT('Ctrl Pts',(1.9620839011163,1.91645500068317,12.5140295443047));
#426479=CARTESIAN_POINT('Ctrl Pts',(1.96247269185465,1.91632149220178,12.5132817086137));
#426480=CARTESIAN_POINT('Ctrl Pts',(1.96306107404274,1.91611944517581,12.5121499604604));
#426481=CARTESIAN_POINT('Ctrl Pts',(1.96371846161084,1.91581139533868,12.5110494206568));
#426482=CARTESIAN_POINT('Ctrl Pts',(1.96444074371445,1.91536032918333,12.5100666561695));
#426483=CARTESIAN_POINT('Ctrl Pts',(1.96485547643508,1.91510132803565,12.5095023550641));
#426484=CARTESIAN_POINT('Ctrl Pts',(1.96529605117817,1.91479162780768,12.5089719619137));
#426485=CARTESIAN_POINT('Ctrl Pts',(1.96575053684161,1.91443180831311,12.5085043804652));
#426486=CARTESIAN_POINT('Ctrl Pts',(1.96641561740914,1.91390525935259,12.5078201359221));
#426487=CARTESIAN_POINT('Ctrl Pts',(1.96712902738502,1.91325516380659,12.5072563000949));
#426488=CARTESIAN_POINT('Ctrl Pts',(1.96783670585242,1.91251933096337,12.5068768744332));
#426489=CARTESIAN_POINT('Ctrl Pts',(1.96834699074417,1.91198874482851,12.5066032824114));
#426490=CARTESIAN_POINT('Ctrl Pts',(1.96886330381797,1.91140430045091,12.5064197834844));
#426491=CARTESIAN_POINT('Ctrl Pts',(1.96935875000463,1.91080034608724,12.5063282718343));
#426492=CARTESIAN_POINT('Ctrl Pts',(1.97008194805089,1.90991875969581,12.5061946931565));
#426493=CARTESIAN_POINT('Ctrl Pts',(1.97077696382452,1.90897743427154,12.5062515701262));
#426494=CARTESIAN_POINT('Ctrl Pts',(1.97141310434388,1.90804397572488,12.5064436508398));
#426495=CARTESIAN_POINT('',(1.94160445395171,1.84186329523733,12.5737548217797));
#426496=CARTESIAN_POINT('Origin',(1.95289051888806,1.85256958956603,12.5893111709658));
#426497=CARTESIAN_POINT('Ctrl Pts',(1.97141310434388,1.90804397572488,12.5064436508398));
#426498=CARTESIAN_POINT('Ctrl Pts',(1.96700108769627,1.89824731829224,12.5164271754438));
#426499=CARTESIAN_POINT('Ctrl Pts',(1.96258713161899,1.88844686326359,12.5264061185523));
#426500=CARTESIAN_POINT('Ctrl Pts',(1.95817116866995,1.8786424765021,12.536380305637));
#426501=CARTESIAN_POINT('Ctrl Pts',(1.95265211063745,1.86638898159414,12.5488460165097));
#426502=CARTESIAN_POINT('Ctrl Pts',(1.94712991623282,1.85412934173728,12.5613043021964));
#426503=CARTESIAN_POINT('Ctrl Pts',(1.94160445395171,1.84186329523733,12.5737548217797));
#426504=CARTESIAN_POINT('Ctrl Pts',(1.97629355154764,1.81533855233443,12.5893111709658));
#426505=CARTESIAN_POINT('Ctrl Pts',(1.96568616340084,1.81134581501989,12.5770542771492));
#426506=CARTESIAN_POINT('Ctrl Pts',(1.9571668466509,1.82531810606213,12.5737548217797));
#426507=CARTESIAN_POINT('Ctrl Pts',(1.96639695066487,1.81161336314696,12.5928319619712));
#426508=CARTESIAN_POINT('Ctrl Pts',(1.95812049011114,1.81197889983995,12.5821634970843));
#426509=CARTESIAN_POINT('Ctrl Pts',(1.95356507962399,1.82395227603856,12.5773203894503));
#426510=CARTESIAN_POINT('Ctrl Pts',(1.94968761267752,1.81278900057586,12.5969440695591));
#426511=CARTESIAN_POINT('Ctrl Pts',(1.94692021864885,1.81570448901556,12.5878292599214));
#426512=CARTESIAN_POINT('Ctrl Pts',(1.94760967419668,1.8243733381408,12.5813877129824));
#426513=CARTESIAN_POINT('Ctrl Pts',(1.92868509842483,1.83503916103836,12.596957478804));
#426514=CARTESIAN_POINT('Ctrl Pts',(1.93143209880742,1.83214527402485,12.5878468778671));
#426515=CARTESIAN_POINT('Ctrl Pts',(1.94009692104806,1.83234107360529,12.5814011370086));
#426516=CARTESIAN_POINT('Ctrl Pts',(1.9284836188184,1.85190031204024,12.5928371701607));
#426517=CARTESIAN_POINT('Ctrl Pts',(1.92834842812283,1.84362282515232,12.5821692192952));
#426518=CARTESIAN_POINT('Ctrl Pts',(1.94001559506115,1.83834068187509,12.5773318885715));
#426519=CARTESIAN_POINT('Ctrl Pts',(1.93281340425155,1.86156455859738,12.5893111709658));
#426520=CARTESIAN_POINT('Ctrl Pts',(1.92817937637153,1.85122123127166,12.5770542771492));
#426521=CARTESIAN_POINT('Ctrl Pts',(1.94160445395166,1.84186329523735,12.5737548217797));
#426522=CARTESIAN_POINT('',(1.9571668466509,1.82531810606213,12.5737548217797));
#426523=CARTESIAN_POINT('Origin',(1.96854337191463,1.83592822731137,12.5893111709658));
#426524=CARTESIAN_POINT('Ctrl Pts',(1.94160445395166,1.84186329523735,12.5737548217797));
#426525=CARTESIAN_POINT('Ctrl Pts',(1.94116509850996,1.8409625808393,12.5746934679442));
#426526=CARTESIAN_POINT('Ctrl Pts',(1.94084356397299,1.83988557063518,12.5756680099006));
#426527=CARTESIAN_POINT('Ctrl Pts',(1.94067324099676,1.83875575040534,12.5765688348656));
#426528=CARTESIAN_POINT('Ctrl Pts',(1.94062814987434,1.83845664300701,12.5768073183026));
#426529=CARTESIAN_POINT('Ctrl Pts',(1.94059341943716,1.83815393336573,12.5770407398754));
#426530=CARTESIAN_POINT('Ctrl Pts',(1.94056911170652,1.83784999212612,12.5772674179684));
#426531=CARTESIAN_POINT('Ctrl Pts',(1.94046935935304,1.83660269946795,12.5781976435658));
#426532=CARTESIAN_POINT('Ctrl Pts',(1.94055070994621,1.83526292353006,12.5790594849312));
#426533=CARTESIAN_POINT('Ctrl Pts',(1.94085587097945,1.83392405480331,12.5797571720116));
#426534=CARTESIAN_POINT('Ctrl Pts',(1.94105469436521,1.8330517336864,12.580211740231));
#426535=CARTESIAN_POINT('Ctrl Pts',(1.941375864059,1.83214432693741,12.5806009430798));
#426536=CARTESIAN_POINT('Ctrl Pts',(1.94181347252961,1.83127162338478,12.5808812374708));
#426537=CARTESIAN_POINT('Ctrl Pts',(1.94218952338097,1.83052168151669,12.5811221033394));
#426538=CARTESIAN_POINT('Ctrl Pts',(1.94265935935651,1.82978206410965,12.581287365893));
#426539=CARTESIAN_POINT('Ctrl Pts',(1.94320350016378,1.8290989871994,12.581359338449));
#426540=CARTESIAN_POINT('Ctrl Pts',(1.94327912449992,1.82900405361388,12.5813693411482));
#426541=CARTESIAN_POINT('Ctrl Pts',(1.94335615233113,1.8289101613385,12.5813775999465));
#426542=CARTESIAN_POINT('Ctrl Pts',(1.94343449979307,1.82881738184242,12.5813841266931));
#426543=CARTESIAN_POINT('Ctrl Pts',(1.94356742573818,1.82865997020587,12.5813952001081));
#426544=CARTESIAN_POINT('Ctrl Pts',(1.94370550573972,1.82850510029502,12.5814007534795));
#426545=CARTESIAN_POINT('Ctrl Pts',(1.9438488268584,1.82835297080154,12.5814005856065));
#426546=CARTESIAN_POINT('Ctrl Pts',(1.94450489490482,1.82765658145918,12.5813998171494));
#426547=CARTESIAN_POINT('Ctrl Pts',(1.94522521304684,1.82706549992931,12.58127954464));
#426548=CARTESIAN_POINT('Ctrl Pts',(1.94598692179323,1.8265602080406,12.5810700125799));
#426549=CARTESIAN_POINT('Ctrl Pts',(1.94690697923139,1.82594987297112,12.5808169217085));
#426550=CARTESIAN_POINT('Ctrl Pts',(1.94789675985771,1.82547859527038,12.5804173076348));
#426551=CARTESIAN_POINT('Ctrl Pts',(1.94885832538448,1.82516416387024,12.5799304713245));
#426552=CARTESIAN_POINT('Ctrl Pts',(1.95005000799652,1.82477448430937,12.5793271277669));
#426553=CARTESIAN_POINT('Ctrl Pts',(1.95126226922739,1.8245709271515,12.5785808224116));
#426554=CARTESIAN_POINT('Ctrl Pts',(1.95243875772033,1.82453079376174,12.5777485681082));
#426555=CARTESIAN_POINT('Ctrl Pts',(1.95419185446875,1.82447099061405,12.576508418016));
#426556=CARTESIAN_POINT('Ctrl Pts',(1.95585052474333,1.82476769321095,12.5750928681475));
#426557=CARTESIAN_POINT('Ctrl Pts',(1.9571668466509,1.82531810606213,12.5737548217797));
#426558=CARTESIAN_POINT('Ctrl Pts',(1.9571668466509,1.82531810606213,12.5737548217797));
#426559=CARTESIAN_POINT('Ctrl Pts',(1.96568616340084,1.81134581501989,12.5770542771492));
#426560=CARTESIAN_POINT('Ctrl Pts',(1.97629355154764,1.81533855233443,12.5893111709658));
#426561=CARTESIAN_POINT('Ctrl Pts',(1.98032097641911,1.83408744063474,12.5508408821982));
#426562=CARTESIAN_POINT('Ctrl Pts',(1.98886394437141,1.82007018615336,12.55409748406));
#426563=CARTESIAN_POINT('Ctrl Pts',(1.99948486482878,1.82406801717812,12.5663972313419));
#426564=CARTESIAN_POINT('Ctrl Pts',(2.00345290528634,1.84284710562112,12.52790050457));
#426565=CARTESIAN_POINT('Ctrl Pts',(2.01199733437468,1.82877784803957,12.5311362602938));
#426566=CARTESIAN_POINT('Ctrl Pts',(2.02265278188567,1.83278867542623,12.5434568539655));
#426567=CARTESIAN_POINT('Ctrl Pts',(2.02656436345227,1.85159783952182,12.5049357605811));
#426568=CARTESIAN_POINT('Ctrl Pts',(2.03509096094202,1.83747054253206,12.5081700652078));
#426569=CARTESIAN_POINT('Ctrl Pts',(2.04579913511532,1.8415012168131,12.5204921097672));
#426570=CARTESIAN_POINT('Ctrl Pts',(2.02504677507696,1.85102323054778,12.5064436508395));
#426571=CARTESIAN_POINT('Ctrl Pts',(2.02601116441225,1.8502757006149,12.5062361689309));
#426572=CARTESIAN_POINT('Ctrl Pts',(2.02698217406567,1.84945720695371,12.5061871075061));
#426573=CARTESIAN_POINT('Ctrl Pts',(2.02787603403384,1.8486133876612,12.5063648335164));
#426574=CARTESIAN_POINT('Ctrl Pts',(2.02828208036695,1.8482300728896,12.5064455676329));
#426575=CARTESIAN_POINT('Ctrl Pts',(2.02867771884383,1.84783602543144,12.506574497099));
#426576=CARTESIAN_POINT('Ctrl Pts',(2.02904524403868,1.84744739623077,12.5067492519495));
#426577=CARTESIAN_POINT('Ctrl Pts',(2.02978380018397,1.84666643076658,12.5071004286051));
#426578=CARTESIAN_POINT('Ctrl Pts',(2.03043539485487,1.84587807693941,12.5076537929612));
#426579=CARTESIAN_POINT('Ctrl Pts',(2.03095841298454,1.8451475306491,12.5083435010503));
#426580=CARTESIAN_POINT('Ctrl Pts',(2.03099134010144,1.84510153839428,12.5083869222963));
#426581=CARTESIAN_POINT('Ctrl Pts',(2.03102375149753,1.8450557632939,12.5084308732336));
#426582=CARTESIAN_POINT('Ctrl Pts',(2.03105563465161,1.84501021656458,12.5084753333615));
#426583=CARTESIAN_POINT('Ctrl Pts',(2.03131137962889,1.84464487167977,12.508831962269));
#426584=CARTESIAN_POINT('Ctrl Pts',(2.03153938560174,1.84428754326604,12.509227847131));
#426585=CARTESIAN_POINT('Ctrl Pts',(2.03173523321877,1.84395036273076,12.5096423454524));
#426586=CARTESIAN_POINT('Ctrl Pts',(2.03234893297202,1.84289378816302,12.5109411997424));
#426587=CARTESIAN_POINT('Ctrl Pts',(2.03269297104733,1.84197491935171,12.5124831113042));
#426588=CARTESIAN_POINT('Ctrl Pts',(2.03286183862445,1.84118853381212,12.5140723025008));
#426589=CARTESIAN_POINT('Ctrl Pts',(2.03287766170138,1.84111484862576,12.5142212114565));
#426590=CARTESIAN_POINT('Ctrl Pts',(2.03289197390084,1.84104231470602,12.5143705582413));
#426591=CARTESIAN_POINT('Ctrl Pts',(2.03290486906217,1.84097092236164,12.5145201959299));
#426592=CARTESIAN_POINT('Ctrl Pts',(2.03307052660835,1.84005378140603,12.5164425148273));
#426593=CARTESIAN_POINT('Ctrl Pts',(2.03301857040475,1.83929552133701,12.518463520594));
#426594=CARTESIAN_POINT('Ctrl Pts',(2.03282334542645,1.83864504613485,12.5205025929157));
#426595=CARTESIAN_POINT('Ctrl Pts',(2.03271010720103,1.83826774473516,12.5216853356836));
#426596=CARTESIAN_POINT('Ctrl Pts',(2.03254933447234,1.83792724967755,12.5228750347131));
#426597=CARTESIAN_POINT('Ctrl Pts',(2.03235860248692,1.83761865745748,12.5240609649613));
#426598=CARTESIAN_POINT('Ctrl Pts',(2.03189046106112,1.83686123440871,12.5269717671326));
#426599=CARTESIAN_POINT('Ctrl Pts',(2.03121981749025,1.83628015249623,12.5299036066169));
#426600=CARTESIAN_POINT('Ctrl Pts',(2.03041321042375,1.83581989477883,12.5328133004019));
#426601=CARTESIAN_POINT('Ctrl Pts',(2.0300259920645,1.83559894427448,12.5342101228451));
#426602=CARTESIAN_POINT('Ctrl Pts',(2.02960766351881,1.83540656929033,12.5356023438238));
#426603=CARTESIAN_POINT('Ctrl Pts',(2.02916590912708,1.83524028800147,12.5369868989719));
#426604=CARTESIAN_POINT('Origin',(13.9600593447379,6.32049840735972,-1.24090551502508));
#426605=CARTESIAN_POINT('Ctrl Pts',(1.95589451822736,1.91308258417306,12.5369868989719));
#426606=CARTESIAN_POINT('Ctrl Pts',(1.96219261612419,1.9270689084424,12.5369868989719));
#426607=CARTESIAN_POINT('Ctrl Pts',(1.95124683239059,1.93781475052863,12.5369868989719));
#426608=CARTESIAN_POINT('Ctrl Pts',(1.95802346126042,1.91781053596428,12.5218025310015));
#426609=CARTESIAN_POINT('Ctrl Pts',(1.95965660304747,1.92951475364883,12.5216901060418));
#426610=CARTESIAN_POINT('Ctrl Pts',(1.95128021032037,1.93778200540912,12.5161920673677));
#426611=CARTESIAN_POINT('Ctrl Pts',(1.96393158279513,1.91900643358783,12.5042015548895));
#426612=CARTESIAN_POINT('Ctrl Pts',(1.96362130427354,1.92543146839368,12.4980677368512));
#426613=CARTESIAN_POINT('Ctrl Pts',(1.95885860513893,1.93027991935011,12.4907278922778));
#426614=CARTESIAN_POINT('Ctrl Pts',(1.97139873234952,1.90803006568957,12.506463626192));
#426615=CARTESIAN_POINT('Ctrl Pts',(1.97610009090441,1.91258030371353,12.4999376786891));
#426616=CARTESIAN_POINT('Ctrl Pts',(1.97604267064543,1.9125247291721,12.4906970594712));
#426617=CARTESIAN_POINT('Origin',(1.93583452791047,1.92211567824355,12.5369868989719));
#426618=CARTESIAN_POINT('Origin',(1.93583452791047,1.92211567824355,14.));
#426619=CARTESIAN_POINT('Origin',(1.93583452791047,1.92211567824355,13.7435492065112));
#426620=CARTESIAN_POINT('Ctrl Pts',(1.94578814647423,1.89052474549827,13.793642941384));
#426621=CARTESIAN_POINT('Ctrl Pts',(1.95023372345813,1.90038086361272,13.8071662555867));
#426622=CARTESIAN_POINT('Ctrl Pts',(1.93590800637666,1.90958918668137,13.8103758687955));
#426623=CARTESIAN_POINT('Ctrl Pts',(1.95258389827906,1.90569311596547,13.7804579775006));
#426624=CARTESIAN_POINT('Ctrl Pts',(1.95806009447194,1.91785884434426,13.7901904343351));
#426625=CARTESIAN_POINT('Ctrl Pts',(1.94635896506339,1.92841059750327,13.7927914348263));
#426626=CARTESIAN_POINT('Ctrl Pts',(1.95658481308477,1.91462330652505,13.7597120340895));
#426627=CARTESIAN_POINT('Ctrl Pts',(1.96291708886745,1.92870483248585,13.7635825532445));
#426628=CARTESIAN_POINT('Ctrl Pts',(1.95249953516948,1.93952197125236,13.7651073818884));
#426629=CARTESIAN_POINT('Ctrl Pts',(1.95580134235455,1.91287457073571,13.7381884353898));
#426630=CARTESIAN_POINT('Ctrl Pts',(1.96198621918532,1.92662612371035,13.7368803041982));
#426631=CARTESIAN_POINT('Ctrl Pts',(1.95129659650628,1.93734627315421,13.7363986145813));
#426632=CARTESIAN_POINT('Origin',(1.92736003299966,1.90320028173495,13.7902182540695));
#426633=CARTESIAN_POINT('Ctrl Pts',(1.93281179419615,1.86156096674826,13.8235227101244));
#426634=CARTESIAN_POINT('Ctrl Pts',(1.93751655867584,1.87205133754772,13.8358800583119));
#426635=CARTESIAN_POINT('Ctrl Pts',(1.92385822819898,1.88143622207771,13.8390832900376));
#426636=CARTESIAN_POINT('Ctrl Pts',(1.93768853087362,1.8724460293881,13.8124254819052));
#426637=CARTESIAN_POINT('Ctrl Pts',(1.94240243168542,1.88295677245277,13.8247886449158));
#426638=CARTESIAN_POINT('Ctrl Pts',(1.92871719089907,1.89233946746655,13.8279860620657));
#426639=CARTESIAN_POINT('Ctrl Pts',(1.94256308195636,1.88332621369697,13.8013225099955));
#426640=CARTESIAN_POINT('Ctrl Pts',(1.94728389672519,1.89385236882366,13.8136962257787));
#426641=CARTESIAN_POINT('Ctrl Pts',(1.93357415172232,1.90323755485475,13.8168830918626));
#426642=CARTESIAN_POINT('Ctrl Pts',(1.94743553248254,1.89420170948327,13.7902140179785));
#426643=CARTESIAN_POINT('Ctrl Pts',(1.95216118407913,1.90473864065568,13.802602731458));
#426644=CARTESIAN_POINT('Ctrl Pts',(1.93842919100827,1.91413068616362,13.8057746032558));
#426645=CARTESIAN_POINT('Origin',(1.91273628961514,1.87055952762869,13.8235269408515));
#426646=CARTESIAN_POINT('Ctrl Pts',(1.97629355154764,1.81533855233443,13.8235269408515));
#426647=CARTESIAN_POINT('Ctrl Pts',(1.98734410636009,1.81949810244568,13.8362179249168));
#426648=CARTESIAN_POINT('Ctrl Pts',(1.99586638246287,1.80469831143077,13.8391868794938));
#426649=CARTESIAN_POINT('Ctrl Pts',(1.96618277489624,1.81153274503707,13.8400110824519));
#426650=CARTESIAN_POINT('Ctrl Pts',(1.97624776907141,1.81166599335812,13.8494522556836));
#426651=CARTESIAN_POINT('Ctrl Pts',(1.97918731725781,1.79854018123482,13.85569149686));
#426652=CARTESIAN_POINT('Ctrl Pts',(1.9499227926055,1.81253808177131,13.8586819406588));
#426653=CARTESIAN_POINT('Ctrl Pts',(1.95291591514243,1.80937623719673,13.868010383617));
#426654=CARTESIAN_POINT('Ctrl Pts',(1.95220443336531,1.80035478163383,13.8744918421245));
#426655=CARTESIAN_POINT('Ctrl Pts',(1.92844625742762,1.83529395869795,13.8587686893867));
#426656=CARTESIAN_POINT('Ctrl Pts',(1.92547973276126,1.83842762417526,13.8680909899357));
#426657=CARTESIAN_POINT('Ctrl Pts',(1.91645418038201,1.83823840008797,13.8745789365162));
#426658=CARTESIAN_POINT('Ctrl Pts',(1.92838914237902,1.85168943703289,13.8400379222776));
#426659=CARTESIAN_POINT('Ctrl Pts',(1.92913040368935,1.86172541060687,13.8494748685453));
#426660=CARTESIAN_POINT('Ctrl Pts',(1.91621522219703,1.86546161085383,13.8557104837033));
#426661=CARTESIAN_POINT('Ctrl Pts',(1.93281340424551,1.86156455859993,13.8235269408542));
#426662=CARTESIAN_POINT('Ctrl Pts',(1.93764103743677,1.87234002037941,13.8362179249195));
#426663=CARTESIAN_POINT('Ctrl Pts',(1.92339019006777,1.88175152149887,13.8391868794965));
#426664=CARTESIAN_POINT('Origin',(1.98404373118065,1.79474887735749,13.8235269408515));
#426665=CARTESIAN_POINT('Ctrl Pts',(2.00976392059532,1.82793716576927,13.7902140241683));
#426666=CARTESIAN_POINT('Ctrl Pts',(2.02057015199298,1.83200950641964,13.8026027327198));
#426667=CARTESIAN_POINT('Ctrl Pts',(2.02910473950242,1.81772879396133,13.8057746032556));
#426668=CARTESIAN_POINT('Ctrl Pts',(1.99861077794605,1.82373900047149,13.8013225161808));
#426669=CARTESIAN_POINT('Ctrl Pts',(2.0094059576434,1.8278071724427,13.8136962270464));
#426670=CARTESIAN_POINT('Ctrl Pts',(2.01793505925016,1.8135490859268,13.8168830918628));
#426671=CARTESIAN_POINT('Ctrl Pts',(1.98745282707664,1.81953902530688,13.8124254880875));
#426672=CARTESIAN_POINT('Ctrl Pts',(1.99823220069998,1.82360123890651,13.8247886461867));
#426673=CARTESIAN_POINT('Ctrl Pts',(2.00676031467335,1.80936776307468,13.8279860620656));
#426674=CARTESIAN_POINT('Ctrl Pts',(1.97628987333152,1.81533716700497,13.8235227163066));
#426675=CARTESIAN_POINT('Ctrl Pts',(1.98704835404407,1.81939150739452,13.8358800595847));
#426676=CARTESIAN_POINT('Ctrl Pts',(1.99558029931377,1.80518475756521,13.8390832900376));
#426677=CARTESIAN_POINT('Origin',(2.01751779008898,1.80734888050839,13.7902182540695));
#426678=CARTESIAN_POINT('Ctrl Pts',(2.02891335849587,1.83514519569823,13.7382347919292));
#426679=CARTESIAN_POINT('Ctrl Pts',(2.04302783395304,1.84048368343377,13.7369371795943));
#426680=CARTESIAN_POINT('Ctrl Pts',(2.05307567672931,1.8291441670171,13.7364597369711));
#426681=CARTESIAN_POINT('Ctrl Pts',(2.03068365731009,1.83581155603065,13.7595490285574));
#426682=CARTESIAN_POINT('Ctrl Pts',(2.0451352477408,1.84127647510066,13.7633824266926));
#426683=CARTESIAN_POINT('Ctrl Pts',(2.0552932090495,1.83019904388407,13.7648920890506));
#426684=CARTESIAN_POINT('Ctrl Pts',(2.02165523033963,1.83241315484894,13.7803806590111));
#426685=CARTESIAN_POINT('Ctrl Pts',(2.03415342933113,1.83714516372188,13.7901039518744));
#426686=CARTESIAN_POINT('Ctrl Pts',(2.04398639222538,1.82482451917112,13.7926933640891));
#426687=CARTESIAN_POINT('Ctrl Pts',(2.00596180889381,1.82650597490444,13.7936647693663));
#426688=CARTESIAN_POINT('Ctrl Pts',(2.01607330193851,1.8303440786487,13.8072068914933));
#426689=CARTESIAN_POINT('Ctrl Pts',(2.0243879405055,1.81546083117553,13.8104111085397));
#426690=CARTESIAN_POINT('Origin',(2.03691608876009,1.81465061302453,13.7435492065112));
#426691=CARTESIAN_POINT('Origin',(2.03691608876009,1.81465061302453,14.));
#426692=CARTESIAN_POINT('Origin',(2.03691608876009,1.81465061302453,12.5369868989719));
#426693=CARTESIAN_POINT('Ctrl Pts',(2.02503320621647,1.85101082774899,12.506462012331));
#426694=CARTESIAN_POINT('Ctrl Pts',(2.02985943003291,1.85542230728125,12.4999388158272));
#426695=CARTESIAN_POINT('Ctrl Pts',(2.02980232947595,1.85537011369308,12.4907030323752));
#426696=CARTESIAN_POINT('Ctrl Pts',(2.03553078211568,1.84288497496945,12.5042014951932));
#426697=CARTESIAN_POINT('Ctrl Pts',(2.04192211426631,1.84218356891276,12.4980716682127));
#426698=CARTESIAN_POINT('Ctrl Pts',(2.04646814791431,1.8371378634817,12.4907355092744));
#426699=CARTESIAN_POINT('Ctrl Pts',(2.03397826385555,1.83706128298778,12.5218047446509));
#426700=CARTESIAN_POINT('Ctrl Pts',(2.04575476219069,1.83797394826004,12.5216906929434));
#426701=CARTESIAN_POINT('Ctrl Pts',(2.0534930995928,1.82911455276253,12.5161988840775));
#426702=CARTESIAN_POINT('Ctrl Pts',(2.02912996752156,1.83522672334837,12.5369868989719));
#426703=CARTESIAN_POINT('Ctrl Pts',(2.0434676725511,1.84065219531004,12.5369868989719));
#426704=CARTESIAN_POINT('Ctrl Pts',(2.05352263325222,1.82908053610232,12.5369868989719));
#426705=CARTESIAN_POINT('Origin',(3.75266718462565E-31,-1.62210662334638E-31,
12.5));
#426706=CARTESIAN_POINT('Origin',(2.11768454258375,1.6482118915911,12.5));
#426707=CARTESIAN_POINT('',(2.11768454258375,1.6482118915911,12.5893111709658));
#426708=CARTESIAN_POINT('',(2.11768454258375,1.6482118915911,13.8235269408515));
#426709=CARTESIAN_POINT('',(2.11768454258375,1.6482118915911,12.5));
#426710=CARTESIAN_POINT('',(2.152074236552,1.65804152271191,13.7902182540695));
#426711=CARTESIAN_POINT('',(2.11768454258375,1.6482118915911,13.8235269408515));
#426712=CARTESIAN_POINT('',(2.17200314797058,1.66373781788874,13.7435492065112));
#426713=CARTESIAN_POINT('Origin',(2.10643720329692,1.64499739526187,13.7445212918691));
#426714=CARTESIAN_POINT('',(2.17200314797058,1.66373781788874,12.5369868989719));
#426715=CARTESIAN_POINT('',(2.17200314797058,1.66373781788874,12.5));
#426716=CARTESIAN_POINT('Ctrl Pts',(2.17200314797058,1.66373781788874,12.5369868989719));
#426717=CARTESIAN_POINT('Ctrl Pts',(2.15391015173731,1.6585662836783,12.5544431401645));
#426718=CARTESIAN_POINT('Ctrl Pts',(2.13580421491226,1.65339105064915,12.5718848856037));
#426719=CARTESIAN_POINT('Ctrl Pts',(2.11768454258375,1.6482118915911,12.5893111709658));
#426720=CARTESIAN_POINT('Origin',(2.210635798588,1.93879232294214,12.5));
#426721=CARTESIAN_POINT('',(2.10534060625464,1.74733000120831,13.7435492065112));
#426722=CARTESIAN_POINT('',(2.09535252910913,1.72916829412978,13.7902182540695));
#426723=CARTESIAN_POINT('Origin',(2.06910558865603,1.68144246689875,13.7418732680435));
#426724=CARTESIAN_POINT('',(2.07811692054271,1.69782812028618,13.8235269408515));
#426725=CARTESIAN_POINT('',(2.09535252910913,1.72916829412978,13.7902182540695));
#426726=CARTESIAN_POINT('',(2.07811692054271,1.69782812028618,12.5893111709658));
#426727=CARTESIAN_POINT('',(2.07811692054271,1.69782812028618,12.5));
#426728=CARTESIAN_POINT('',(2.10534060625464,1.74733000120831,12.5369868989719));
#426729=CARTESIAN_POINT('Ctrl Pts',(2.07811692054271,1.69782812028618,12.5893111709658));
#426730=CARTESIAN_POINT('Ctrl Pts',(2.08719823367956,1.71434102328813,12.5718848856037));
#426731=CARTESIAN_POINT('Ctrl Pts',(2.09627266278419,1.73084140878799,12.5544431401645));
#426732=CARTESIAN_POINT('Ctrl Pts',(2.10534060625464,1.74733000120831,12.5369868989719));
#426733=CARTESIAN_POINT('',(2.10534060625464,1.74733000120831,12.5));
#426734=CARTESIAN_POINT('Origin',(2.10823744587471,1.68126326053052,12.5));
#426735=CARTESIAN_POINT('',(2.08207484552998,1.65896733006374,13.8587068136939));
#426736=CARTESIAN_POINT('Ctrl Pts',(2.07811692053685,1.69782812028924,13.8235269408542));
#426737=CARTESIAN_POINT('Ctrl Pts',(2.07727251105211,1.69629269785577,13.8262006681044));
#426738=CARTESIAN_POINT('Ctrl Pts',(2.07656061753603,1.69463769463711,13.8288634856214));
#426739=CARTESIAN_POINT('Ctrl Pts',(2.07597237842099,1.69287307450134,13.8314912288862));
#426740=CARTESIAN_POINT('Ctrl Pts',(2.07536596456744,1.69105393315349,13.8342001611531));
#426741=CARTESIAN_POINT('Ctrl Pts',(2.07488981926285,1.68911643312964,13.8368750301949));
#426742=CARTESIAN_POINT('Ctrl Pts',(2.07456661493521,1.68703995339693,13.8394886372969));
#426743=CARTESIAN_POINT('Ctrl Pts',(2.074541653081,1.68687958183033,13.8396904925131));
#426744=CARTESIAN_POINT('Ctrl Pts',(2.0745176244671,1.68671837414493,13.8398919674349));
#426745=CARTESIAN_POINT('Ctrl Pts',(2.07449455065522,1.68655631812479,13.8400930404591));
#426746=CARTESIAN_POINT('Ctrl Pts',(2.0741350451428,1.68403137630506,13.8432258934518));
#426747=CARTESIAN_POINT('Ctrl Pts',(2.07400804501129,1.68131353748541,13.8462331177034));
#426748=CARTESIAN_POINT('Ctrl Pts',(2.07421405347112,1.67848694014619,13.8489036603661));
#426749=CARTESIAN_POINT('Ctrl Pts',(2.07428146183661,1.67756204460203,13.8497774930041));
#426750=CARTESIAN_POINT('Ctrl Pts',(2.07438464593108,1.67662572306582,13.85061494757));
#426751=CARTESIAN_POINT('Ctrl Pts',(2.07452746284261,1.67568155303062,13.8514076489583));
#426752=CARTESIAN_POINT('Ctrl Pts',(2.0748295412078,1.67368449723647,13.8530843267192));
#426753=CARTESIAN_POINT('Ctrl Pts',(2.07534152698039,1.67145660750048,13.8546805203176));
#426754=CARTESIAN_POINT('Ctrl Pts',(2.07616668415117,1.6691577494185,13.8559412814273));
#426755=CARTESIAN_POINT('Ctrl Pts',(2.0762771169411,1.6688500876534,13.8561100121513));
#426756=CARTESIAN_POINT('Ctrl Pts',(2.07639308709043,1.66854118184659,13.8562727473908));
#426757=CARTESIAN_POINT('Ctrl Pts',(2.07651476836467,1.66823143285592,13.8564289040185));
#426758=CARTESIAN_POINT('Ctrl Pts',(2.07706659155516,1.66682672471698,13.8571370725437));
#426759=CARTESIAN_POINT('Ctrl Pts',(2.07774768874718,1.66538081705924,13.8577210840554));
#426760=CARTESIAN_POINT('Ctrl Pts',(2.07855813548723,1.66396241895231,13.8581177131616));
#426761=CARTESIAN_POINT('Ctrl Pts',(2.07878638518395,1.66356294922562,13.8582294175695));
#426762=CARTESIAN_POINT('Ctrl Pts',(2.07902472613285,1.66316560530663,13.8583265086086));
#426763=CARTESIAN_POINT('Ctrl Pts',(2.07927275206209,1.66277175834687,13.8584082369006));
#426764=CARTESIAN_POINT('Ctrl Pts',(2.07962909881161,1.66220590587992,13.8585256585398));
#426765=CARTESIAN_POINT('Ctrl Pts',(2.08001014112102,1.66164040925815,13.8586122832068));
#426766=CARTESIAN_POINT('Ctrl Pts',(2.08040663550495,1.66109039972175,13.8586682984299));
#426767=CARTESIAN_POINT('Ctrl Pts',(2.08072379170887,1.66065044661331,13.8587131050557));
#426768=CARTESIAN_POINT('Ctrl Pts',(2.08105414757208,1.66021540637792,13.8587357943552));
#426769=CARTESIAN_POINT('Ctrl Pts',(2.08139814568569,1.65978553360139,13.8587355499465));
#426770=CARTESIAN_POINT('Ctrl Pts',(2.08162047986781,1.65950769657728,13.8587353919793));
#426771=CARTESIAN_POINT('Ctrl Pts',(2.08184607840205,1.65923499850864,13.8587257282814));
#426772=CARTESIAN_POINT('Ctrl Pts',(2.08207484552998,1.65896733006374,13.8587068136939));
#426773=CARTESIAN_POINT('Ctrl Pts',(2.08207484552998,1.65896733006374,13.8587068136939));
#426774=CARTESIAN_POINT('Ctrl Pts',(2.08282724814235,1.65808698314053,13.8586446046466));
#426775=CARTESIAN_POINT('Ctrl Pts',(2.08361388418944,1.65726097481382,13.858482427929));
#426776=CARTESIAN_POINT('Ctrl Pts',(2.08443173506927,1.65648600750882,13.8582284286032));
#426777=CARTESIAN_POINT('Ctrl Pts',(2.08527075493565,1.6556909812018,13.8579678548414));
#426778=CARTESIAN_POINT('Ctrl Pts',(2.08614572945382,1.65494884213355,13.857615680862));
#426779=CARTESIAN_POINT('Ctrl Pts',(2.08701589569976,1.65428145902623,13.8571944833187));
#426780=CARTESIAN_POINT('Ctrl Pts',(2.08918748455982,1.65261593622757,13.8561433417727));
#426781=CARTESIAN_POINT('Ctrl Pts',(2.09142778909988,1.65133428277386,13.8546163505474));
#426782=CARTESIAN_POINT('Ctrl Pts',(2.09354146655774,1.65036868220764,13.8528973491086));
#426783=CARTESIAN_POINT('Ctrl Pts',(2.09392760424489,1.65019228123029,13.8525833129072));
#426784=CARTESIAN_POINT('Ctrl Pts',(2.09430952318956,1.65002628703228,13.8522628768812));
#426785=CARTESIAN_POINT('Ctrl Pts',(2.09468606941946,1.64987011120217,13.851937733538));
#426786=CARTESIAN_POINT('Ctrl Pts',(2.09698558500203,1.64891636707609,13.8499521282529));
#426787=CARTESIAN_POINT('Ctrl Pts',(2.09931482290192,1.64823776961473,13.847639871647));
#426788=CARTESIAN_POINT('Ctrl Pts',(2.10152889489607,1.64779284953028,13.8452109780794));
#426789=CARTESIAN_POINT('Ctrl Pts',(2.10252505171524,1.6475926707749,13.8441181685877));
#426790=CARTESIAN_POINT('Ctrl Pts',(2.10349800634257,1.64743908582684,13.8430021611332));
#426791=CARTESIAN_POINT('Ctrl Pts',(2.1044360597416,1.64732536702951,13.8418824960098));
#426792=CARTESIAN_POINT('Ctrl Pts',(2.10664660653044,1.64705738577968,13.8392439765549));
#426793=CARTESIAN_POINT('Ctrl Pts',(2.10876855770583,1.6469942243102,13.8364981347964));
#426794=CARTESIAN_POINT('Ctrl Pts',(2.11080650686364,1.64710151020428,13.8336931113419));
#426795=CARTESIAN_POINT('Ctrl Pts',(2.11279133992161,1.64720599985183,13.8309611966328));
#426796=CARTESIAN_POINT('Ctrl Pts',(2.11469845196866,1.64747283608806,13.8281701127186));
#426797=CARTESIAN_POINT('Ctrl Pts',(2.1165158842708,1.64790606928952,13.8253580685121));
#426798=CARTESIAN_POINT('Ctrl Pts',(2.11690990555534,1.64799999471516,13.8247484142933));
#426799=CARTESIAN_POINT('Ctrl Pts',(2.11729958439555,1.6481018587135,13.8241378483365));
#426800=CARTESIAN_POINT('Ctrl Pts',(2.11768454258375,1.6482118915911,13.8235269408515));
#426801=CARTESIAN_POINT('',(2.08128637880857,1.65992706809418,12.5969504640361));
#426802=CARTESIAN_POINT('Origin',(2.10826343517428,1.68128373586001,12.584524458991));
#426803=CARTESIAN_POINT('Origin',(2.10826343517428,1.68128373586001,12.584524458991));
#426804=CARTESIAN_POINT('Ctrl Pts',(2.07811692054271,1.69782812028618,12.5893111709658));
#426805=CARTESIAN_POINT('Ctrl Pts',(2.07265523480837,1.68789692582132,12.5770542771492));
#426806=CARTESIAN_POINT('Ctrl Pts',(2.08527288288871,1.67747585909206,12.5737548217797));
#426807=CARTESIAN_POINT('Ctrl Pts',(2.09005979424748,1.71954430957288,12.5663937883685));
#426808=CARTESIAN_POINT('Ctrl Pts',(2.08459114137447,1.70960044649025,12.5540940315303));
#426809=CARTESIAN_POINT('Ctrl Pts',(2.09724993387507,1.69914956290367,12.5508374392248));
#426810=CARTESIAN_POINT('Ctrl Pts',(2.10199061773916,1.74123858749091,12.5434499600945));
#426811=CARTESIAN_POINT('Ctrl Pts',(2.09650418432823,1.73126239336826,12.5311293540533));
#426812=CARTESIAN_POINT('Ctrl Pts',(2.1092142503483,1.72080266171172,12.5278936106989));
#426813=CARTESIAN_POINT('Ctrl Pts',(2.11391033492732,1.7629126703876,12.5204817579905));
#426814=CARTESIAN_POINT('Ctrl Pts',(2.10839674742046,1.75288710092186,12.5081597038247));
#426815=CARTESIAN_POINT('Ctrl Pts',(2.12116680995867,1.74243676371845,12.5049254088044));
#426816=CARTESIAN_POINT('Ctrl Pts',(2.10534060625464,1.74733000120831,12.5369868989719));
#426817=CARTESIAN_POINT('Ctrl Pts',(2.10578948628541,1.74814621679791,12.5342545179733));
#426818=CARTESIAN_POINT('Ctrl Pts',(2.10632718358074,1.7488650622138,12.5314872231885));
#426819=CARTESIAN_POINT('Ctrl Pts',(2.10696817244343,1.74941256051339,12.5287124745063));
#426820=CARTESIAN_POINT('Ctrl Pts',(2.10754624801564,1.74990632165534,12.5262100684184));
#426821=CARTESIAN_POINT('Ctrl Pts',(2.10820838957962,1.7502594744367,12.5237004536639));
#426822=CARTESIAN_POINT('Ctrl Pts',(2.10899716276871,1.75041959135521,12.5212220730815));
#426823=CARTESIAN_POINT('Ctrl Pts',(2.10960103687929,1.75054217470755,12.5193246583486));
#426824=CARTESIAN_POINT('Ctrl Pts',(2.1102864760572,1.75055245850377,12.5174178313691));
#426825=CARTESIAN_POINT('Ctrl Pts',(2.11107409330956,1.75035542102692,12.5155812248348));
#426826=CARTESIAN_POINT('Ctrl Pts',(2.11140962249253,1.7502714820027,12.5147988205794));
#426827=CARTESIAN_POINT('Ctrl Pts',(2.11176410285173,1.75015010172559,12.5140295443047));
#426828=CARTESIAN_POINT('Ctrl Pts',(2.11214071774031,1.74998534742812,12.5132817086137));
#426829=CARTESIAN_POINT('Ctrl Pts',(2.11271067342687,1.74973601408637,12.5121499604604));
#426830=CARTESIAN_POINT('Ctrl Pts',(2.11334076467055,1.74937540606996,12.5110494206568));
#426831=CARTESIAN_POINT('Ctrl Pts',(2.1140238773609,1.74886696810325,12.5100666561695));
#426832=CARTESIAN_POINT('Ctrl Pts',(2.11441611909463,1.7485750241936,12.5095023550641));
#426833=CARTESIAN_POINT('Ctrl Pts',(2.1148299844179,1.74823044353594,12.5089719619137));
#426834=CARTESIAN_POINT('Ctrl Pts',(2.11525362918859,1.74783477651024,12.5085043804652));
#426835=CARTESIAN_POINT('Ctrl Pts',(2.11587357812687,1.74725576935739,12.5078201359221));
#426836=CARTESIAN_POINT('Ctrl Pts',(2.11653162546771,1.74654968741468,12.5072563000949));
#426837=CARTESIAN_POINT('Ctrl Pts',(2.11717697198553,1.74575862062969,12.5068768744332));
#426838=CARTESIAN_POINT('Ctrl Pts',(2.11764231125069,1.74518820702048,12.5066032824114));
#426839=CARTESIAN_POINT('Ctrl Pts',(2.11810926869283,1.74456362302461,12.5064197834844));
#426840=CARTESIAN_POINT('Ctrl Pts',(2.1185538384357,1.74392129480555,12.5063282718343));
#426841=CARTESIAN_POINT('Ctrl Pts',(2.11920277262498,1.7429836944655,12.5061946931565));
#426842=CARTESIAN_POINT('Ctrl Pts',(2.11981874903004,1.74198885098616,12.5062515701262));
#426843=CARTESIAN_POINT('Ctrl Pts',(2.12037668730694,1.74100664708784,12.5064436508398));
#426844=CARTESIAN_POINT('',(2.08527288288871,1.67747585909206,12.5737548217797));
#426845=CARTESIAN_POINT('Origin',(2.09739405675519,1.68722661004256,12.5893111709658));
#426846=CARTESIAN_POINT('Ctrl Pts',(2.12037668730694,1.74100664708784,12.5064436508398));
#426847=CARTESIAN_POINT('Ctrl Pts',(2.11518083275227,1.73160220754059,12.5164271754438));
#426848=CARTESIAN_POINT('Ctrl Pts',(2.10998273568189,1.72219414111502,12.5264061185523));
#426849=CARTESIAN_POINT('Ctrl Pts',(2.10478231794473,1.71278231961782,12.536380305637));
#426850=CARTESIAN_POINT('Ctrl Pts',(2.09828285053164,1.70101945166941,12.5488460165097));
#426851=CARTESIAN_POINT('Ctrl Pts',(2.09177975631206,1.68925071486236,12.5613043021964));
#426852=CARTESIAN_POINT('Ctrl Pts',(2.08527288288871,1.67747585909206,12.5737548217797));
#426853=CARTESIAN_POINT('Ctrl Pts',(2.11768454258375,1.6482118915911,12.5893111709658));
#426854=CARTESIAN_POINT('Ctrl Pts',(2.10678700448806,1.64509704038874,12.5770542771492));
#426855=CARTESIAN_POINT('Ctrl Pts',(2.09943490649417,1.65971724318977,12.5737548217797));
#426856=CARTESIAN_POINT('Ctrl Pts',(2.10751723432225,1.64530576251085,12.5928319619712));
#426857=CARTESIAN_POINT('Ctrl Pts',(2.09929810764222,1.64634469128069,12.5821634970843));
#426858=CARTESIAN_POINT('Ctrl Pts',(2.09573379622326,1.6586495353028,12.5773203894503));
#426859=CARTESIAN_POINT('Ctrl Pts',(2.09095932064318,1.64783945427108,12.5969440695591));
#426860=CARTESIAN_POINT('Ctrl Pts',(2.08843877426376,1.65097080996808,12.5878292599214));
#426861=CARTESIAN_POINT('Ctrl Pts',(2.0898325273865,1.65955461718524,12.5813877129824));
#426862=CARTESIAN_POINT('Ctrl Pts',(2.07184028516219,1.67172747904958,12.596957478804));
#426863=CARTESIAN_POINT('Ctrl Pts',(2.07434226647048,1.66861931517329,12.5878468778671));
#426864=CARTESIAN_POINT('Ctrl Pts',(2.08299421671343,1.66810819979388,12.5814011370086));
#426865=CARTESIAN_POINT('Ctrl Pts',(2.07301381630046,1.68854894842081,12.5928371701607));
#426866=CARTESIAN_POINT('Ctrl Pts',(2.07220438341499,1.68031002348439,12.5821692192951));
#426867=CARTESIAN_POINT('Ctrl Pts',(2.08340218510367,1.67409447368502,12.5773318885715));
#426868=CARTESIAN_POINT('Ctrl Pts',(2.07811692054266,1.69782812028621,12.5893111709658));
#426869=CARTESIAN_POINT('Ctrl Pts',(2.07265523480832,1.68789692582134,12.5770542771492));
#426870=CARTESIAN_POINT('Ctrl Pts',(2.08527288288866,1.67747585909209,12.5737548217797));
#426871=CARTESIAN_POINT('',(2.09943490649417,1.65971724318977,12.5737548217797));
#426872=CARTESIAN_POINT('Origin',(2.11163840068996,1.66936476771233,12.5893111709658));
#426873=CARTESIAN_POINT('Ctrl Pts',(2.08527288288866,1.67747585909209,12.5737548217797));
#426874=CARTESIAN_POINT('Ctrl Pts',(2.08476157278068,1.67661395329417,12.5746934679442));
#426875=CARTESIAN_POINT('Ctrl Pts',(2.08435332179325,1.6755667348024,12.5756680099006));
#426876=CARTESIAN_POINT('Ctrl Pts',(2.0840914747152,1.67445455685994,12.5765688348656));
#426877=CARTESIAN_POINT('Ctrl Pts',(2.08402215360003,1.67416012006189,12.5768073183026));
#426878=CARTESIAN_POINT('Ctrl Pts',(2.08396286507953,1.67386124851501,12.5770407398754));
#426879=CARTESIAN_POINT('Ctrl Pts',(2.08391386419817,1.67356029992052,12.5772674179684));
#426880=CARTESIAN_POINT('Ctrl Pts',(2.08371277783148,1.67232528826864,12.5781976435658));
#426881=CARTESIAN_POINT('Ctrl Pts',(2.08368465356045,1.67098333949609,12.5790594849312));
#426882=CARTESIAN_POINT('Ctrl Pts',(2.08387966896484,1.66962405228739,12.5797571720116));
#426883=CARTESIAN_POINT('Ctrl Pts',(2.08400672851294,1.66873842779531,12.580211740231));
#426884=CARTESIAN_POINT('Ctrl Pts',(2.08425286746706,1.66780786205578,12.5806009430798));
#426885=CARTESIAN_POINT('Ctrl Pts',(2.08461788639027,1.66690239319932,12.5808812374708));
#426886=CARTESIAN_POINT('Ctrl Pts',(2.08493155873907,1.66612429506545,12.5811221033394));
#426887=CARTESIAN_POINT('Ctrl Pts',(2.08533954568921,1.66534884268058,12.581287365893));
#426888=CARTESIAN_POINT('Ctrl Pts',(2.08582619880327,1.66462368612505,12.581359338449));
#426889=CARTESIAN_POINT('Ctrl Pts',(2.08589383353713,1.66452290433774,12.5813693411482));
#426890=CARTESIAN_POINT('Ctrl Pts',(2.08596295197249,1.66442304599782,12.5813775999465));
#426891=CARTESIAN_POINT('Ctrl Pts',(2.08603347634946,1.66432418917237,12.5813841266931));
#426892=CARTESIAN_POINT('Ctrl Pts',(2.08615312948473,1.66415646661151,12.5813952001081));
#426893=CARTESIAN_POINT('Ctrl Pts',(2.08627812670098,1.66399085721551,12.5814007534795));
#426894=CARTESIAN_POINT('Ctrl Pts',(2.08640857096445,1.66382755191868,12.5814005856065));
#426895=CARTESIAN_POINT('Ctrl Pts',(2.0870056938022,1.66308000411798,12.5813998171494));
#426896=CARTESIAN_POINT('Ctrl Pts',(2.08767543651301,1.66243217674746,12.58127954464));
#426897=CARTESIAN_POINT('Ctrl Pts',(2.08839342475655,1.66186647984163,12.5810700125799));
#426898=CARTESIAN_POINT('Ctrl Pts',(2.08926067280524,1.66118318238914,12.5808169217085));
#426899=CARTESIAN_POINT('Ctrl Pts',(2.09020874651044,1.66063279651635,12.5804173076348));
#426900=CARTESIAN_POINT('Ctrl Pts',(2.09114148342909,1.66024103484359,12.5799304713245));
#426901=CARTESIAN_POINT('Ctrl Pts',(2.09229743831373,1.65975551871339,12.5793271277669));
#426902=CARTESIAN_POINT('Ctrl Pts',(2.09348907404726,1.65945382833077,12.5785808224116));
#426903=CARTESIAN_POINT('Ctrl Pts',(2.09465837662795,1.65931793374739,12.5777485681082));
#426904=CARTESIAN_POINT('Ctrl Pts',(2.09640076557984,1.65911543592979,12.576508418016));
#426905=CARTESIAN_POINT('Ctrl Pts',(2.09807810078201,1.65927595424756,12.5750928681475));
#426906=CARTESIAN_POINT('Ctrl Pts',(2.09943490649417,1.65971724318977,12.5737548217797));
#426907=CARTESIAN_POINT('Ctrl Pts',(2.09943490649417,1.65971724318977,12.5737548217797));
#426908=CARTESIAN_POINT('Ctrl Pts',(2.10678700448806,1.64509704038875,12.5770542771492));
#426909=CARTESIAN_POINT('Ctrl Pts',(2.11768454258375,1.6482118915911,12.5893111709658));
#426910=CARTESIAN_POINT('Ctrl Pts',(2.12322677498387,1.66657012199645,12.5508408821982));
#426911=CARTESIAN_POINT('Ctrl Pts',(2.13059878054495,1.65190317757585,12.55409748406));
#426912=CARTESIAN_POINT('Ctrl Pts',(2.14151022110824,1.65502200253059,12.5663972313419));
#426913=CARTESIAN_POINT('Ctrl Pts',(2.14699572828318,1.67341517297119,12.52790050457));
#426914=CARTESIAN_POINT('Ctrl Pts',(2.15436495138303,1.65869627939029,12.5311362602937));
#426915=CARTESIAN_POINT('Ctrl Pts',(2.16531186343821,1.66182524318719,12.5434568539655));
#426916=CARTESIAN_POINT('Ctrl Pts',(2.17074355102939,1.68025299112988,12.5049357605811));
#426917=CARTESIAN_POINT('Ctrl Pts',(2.1780902711133,1.66547770470294,12.5081700652078));
#426918=CARTESIAN_POINT('Ctrl Pts',(2.18909135209325,1.66862215164286,12.5204921097672));
#426919=CARTESIAN_POINT('Ctrl Pts',(2.16918417633841,1.67980399166099,12.5064436508395));
#426920=CARTESIAN_POINT('Ctrl Pts',(2.17008442611849,1.67898034238851,12.5062361689309));
#426921=CARTESIAN_POINT('Ctrl Pts',(2.17098548998548,1.67808542589629,12.5061871075061));
#426922=CARTESIAN_POINT('Ctrl Pts',(2.17180759660236,1.67717155645727,12.5063648335164));
#426923=CARTESIAN_POINT('Ctrl Pts',(2.17218104813739,1.67675642058825,12.5064455676329));
#426924=CARTESIAN_POINT('Ctrl Pts',(2.17254325163388,1.67633143608171,12.506574497099));
#426925=CARTESIAN_POINT('Ctrl Pts',(2.17287787703125,1.67591414329733,12.5067492519495));
#426926=CARTESIAN_POINT('Ctrl Pts',(2.1735503197565,1.67507557724895,12.5071004286051));
#426927=CARTESIAN_POINT('Ctrl Pts',(2.17413548814429,1.67423673558925,12.5076537929613));
#426928=CARTESIAN_POINT('Ctrl Pts',(2.17459721966958,1.67346598929836,12.5083435010505));
#426929=CARTESIAN_POINT('Ctrl Pts',(2.17462628842842,1.67341746621334,12.5083869222964));
#426930=CARTESIAN_POINT('Ctrl Pts',(2.17465486088258,1.67336920159624,12.5084308732337));
#426931=CARTESIAN_POINT('Ctrl Pts',(2.17468292546678,1.67332120764692,12.5084753333615));
#426932=CARTESIAN_POINT('Ctrl Pts',(2.17490804047394,1.67293623282721,12.5088319622689));
#426933=CARTESIAN_POINT('Ctrl Pts',(2.17510616219274,1.6725615087908,12.509227847131));
#426934=CARTESIAN_POINT('Ctrl Pts',(2.17527387479912,1.67220948679698,12.5096423454524));
#426935=CARTESIAN_POINT('Ctrl Pts',(2.17579941188104,1.67110640566676,12.5109411997424));
#426936=CARTESIAN_POINT('Ctrl Pts',(2.17606740885955,1.67016255201858,12.5124831113042));
#426937=CARTESIAN_POINT('Ctrl Pts',(2.17617161682182,1.66936501883677,12.5140723025008));
#426938=CARTESIAN_POINT('Ctrl Pts',(2.17618138122202,1.66929028910413,12.5142212114565));
#426939=CARTESIAN_POINT('Ctrl Pts',(2.17618973361099,1.6692168299579,12.5143705582413));
#426940=CARTESIAN_POINT('Ctrl Pts',(2.17619676672589,1.66914462409029,12.5145201959299));
#426941=CARTESIAN_POINT('Ctrl Pts',(2.17628711755804,1.66821703221765,12.5164425148273));
#426942=CARTESIAN_POINT('Ctrl Pts',(2.17617352899946,1.66746553010939,12.5184635205941));
#426943=CARTESIAN_POINT('Ctrl Pts',(2.17592593384847,1.66683313195791,12.5205025929157));
#426944=CARTESIAN_POINT('Ctrl Pts',(2.17578231884714,1.66646631596413,12.5216853356836));
#426945=CARTESIAN_POINT('Ctrl Pts',(2.17559432756824,1.66614005834567,12.5228750347131));
#426946=CARTESIAN_POINT('Ctrl Pts',(2.175379077097,1.66584803936824,12.5240609649613));
#426947=CARTESIAN_POINT('Ctrl Pts',(2.17485075636314,1.6651312944544,12.5269717671326));
#426948=CARTESIAN_POINT('Ctrl Pts',(2.17413498073306,1.66460680972102,12.5299036066169));
#426949=CARTESIAN_POINT('Ctrl Pts',(2.17329354230824,1.66421382943731,12.5328133004019));
#426950=CARTESIAN_POINT('Ctrl Pts',(2.17288960286883,1.66402517601857,12.5342101228451));
#426951=CARTESIAN_POINT('Ctrl Pts',(2.17245698592973,1.66386753880635,12.5356023438238));
#426952=CARTESIAN_POINT('Ctrl Pts',(2.17200314797057,1.66373781788874,12.5369868989719));
#426953=CARTESIAN_POINT('Origin',(14.4283934060731,5.16148105026723,-1.24046354638259));
#426954=CARTESIAN_POINT('Ctrl Pts',(2.10532043137021,1.74729339881809,12.5369868989719));
#426955=CARTESIAN_POINT('Ctrl Pts',(2.11273758813649,1.76071983129993,12.5369868989719));
#426956=CARTESIAN_POINT('Ctrl Pts',(2.10270411148486,1.77232210047308,12.5369868989719));
#426957=CARTESIAN_POINT('Ctrl Pts',(2.1078276624841,1.75183209011841,12.5218025310015));
#426958=CARTESIAN_POINT('Ctrl Pts',(2.11040937252457,1.76336424676715,12.5216901060418));
#426959=CARTESIAN_POINT('Ctrl Pts',(2.10273470932111,1.7722867436991,12.5161920673677));
#426960=CARTESIAN_POINT('Ctrl Pts',(2.11381360199028,1.75254244173787,12.5042015548895));
#426961=CARTESIAN_POINT('Ctrl Pts',(2.11402805587868,1.75897138835048,12.4980677368513));
#426962=CARTESIAN_POINT('Ctrl Pts',(2.10967639799629,1.76419191068048,12.4907278922778));
#426963=CARTESIAN_POINT('Ctrl Pts',(2.12036122933718,1.74099395478799,12.506463626192));
#426964=CARTESIAN_POINT('Ctrl Pts',(2.12541783115062,1.74514584790279,12.4999376786891));
#426965=CARTESIAN_POINT('Ctrl Pts',(2.12535607211176,1.74509513856523,12.4906970594712));
#426966=CARTESIAN_POINT('Origin',(2.08606347004216,1.75793151145193,12.5369868989719));
#426967=CARTESIAN_POINT('Origin',(2.08606347004216,1.75793151145193,14.));
#426968=CARTESIAN_POINT('Origin',(2.08606347004216,1.75793151145193,13.7435492065112));
#426969=CARTESIAN_POINT('Ctrl Pts',(2.09340901446662,1.72563438261146,13.793642941384));
#426970=CARTESIAN_POINT('Ctrl Pts',(2.0986431642859,1.73509534951103,13.8071662555867));
#426971=CARTESIAN_POINT('Ctrl Pts',(2.08511567866223,1.74544071157992,13.8103758687955));
#426972=CARTESIAN_POINT('Ctrl Pts',(2.10141851697729,1.74019836471646,13.7804579775006));
#426973=CARTESIAN_POINT('Ctrl Pts',(2.10786811138308,1.75187725180944,13.7901904343352));
#426974=CARTESIAN_POINT('Ctrl Pts',(2.0970659823575,1.76334764555504,13.7927914348263));
#426975=CARTESIAN_POINT('Ctrl Pts',(2.10613401250348,1.74877272910428,13.7597120340895));
#426976=CARTESIAN_POINT('Ctrl Pts',(2.11359299325318,1.76229126068683,13.7635825532444));
#426977=CARTESIAN_POINT('Ctrl Pts',(2.10409180033665,1.77392153365468,13.7651073818884));
#426978=CARTESIAN_POINT('Ctrl Pts',(2.10521061050618,1.74709367222693,13.7381884353898));
#426979=CARTESIAN_POINT('Ctrl Pts',(2.11249578690014,1.76029534316416,13.7368803041982));
#426980=CARTESIAN_POINT('Ctrl Pts',(2.10271552475942,1.77185112568106,13.7363986145813));
#426981=CARTESIAN_POINT('Origin',(2.07607539289665,1.7397698043734,13.7902182540695));
#426982=CARTESIAN_POINT('Ctrl Pts',(2.07811502307555,1.69782467162314,13.8235227101244));
#426983=CARTESIAN_POINT('Ctrl Pts',(2.08365919544754,1.70789665459716,13.8358800583119));
#426984=CARTESIAN_POINT('Ctrl Pts',(2.07081126715283,1.71836359242969,13.8390832900376));
#426985=CARTESIAN_POINT('Ctrl Pts',(2.08386276647115,1.70827601580236,13.8124254819053));
#426986=CARTESIAN_POINT('Ctrl Pts',(2.08941770530363,1.71836755855869,13.8247886449157));
#426987=CARTESIAN_POINT('Ctrl Pts',(2.07654277777535,1.72883450760048,13.8279860620657));
#426988=CARTESIAN_POINT('Ctrl Pts',(2.08960793391517,1.71872267602913,13.8013225099955));
#426989=CARTESIAN_POINT('Ctrl Pts',(2.09517101992517,1.7288290160134,13.8136962257787));
#426990=CARTESIAN_POINT('Ctrl Pts',(2.0822718727572,1.73930044510501,13.8168830918626));
#426991=CARTESIAN_POINT('Ctrl Pts',(2.09535062563393,1.72916483454887,13.7902140179785));
#426992=CARTESIAN_POINT('Ctrl Pts',(2.10091941072531,1.73928152047611,13.802602731458));
#426993=CARTESIAN_POINT('Ctrl Pts',(2.08799864862899,1.74976159964428,13.8057746032558));
#426994=CARTESIAN_POINT('Origin',(2.05883978433024,1.70842963052981,13.8235269408515));
#426995=CARTESIAN_POINT('Ctrl Pts',(2.11768454258375,1.6482118915911,13.8235269408515));
#426996=CARTESIAN_POINT('Ctrl Pts',(2.12903736953611,1.65145687833693,13.8362179249168));
#426997=CARTESIAN_POINT('Ctrl Pts',(2.13632496810593,1.6360116877864,13.8391868794938));
#426998=CARTESIAN_POINT('Ctrl Pts',(2.10729720008146,1.64524286996452,13.8400110824519));
#426999=CARTESIAN_POINT('Ctrl Pts',(2.11733956479398,1.64455528444865,13.8494522556836));
#427000=CARTESIAN_POINT('Ctrl Pts',(2.11919945633416,1.63123354691577,13.85569149686));
#427001=CARTESIAN_POINT('Ctrl Pts',(2.09117326581736,1.64757020103072,13.8586819406588));
#427002=CARTESIAN_POINT('Ctrl Pts',(2.09389870930001,1.64417490995957,13.868010383617));
#427003=CARTESIAN_POINT('Ctrl Pts',(2.09245426254032,1.63524146491575,13.8744918421245));
#427004=CARTESIAN_POINT('Ctrl Pts',(2.07162300726337,1.67200089664954,13.8587686893867));
#427005=CARTESIAN_POINT('Ctrl Pts',(2.06892177629104,1.67536593441366,13.8680909899357));
#427006=CARTESIAN_POINT('Ctrl Pts',(2.059910832173,1.67591300626196,13.8745789365163));
#427007=CARTESIAN_POINT('Ctrl Pts',(2.07290246595287,1.68834647578953,13.8400379222776));
#427008=CARTESIAN_POINT('Ctrl Pts',(2.07445928579305,1.69828863581103,13.8494748685453));
#427009=CARTESIAN_POINT('Ctrl Pts',(2.06189161350704,1.70306511135021,13.8557104837033));
#427010=CARTESIAN_POINT('Ctrl Pts',(2.07811692053685,1.69782812028924,13.8235269408542));
#427011=CARTESIAN_POINT('Ctrl Pts',(2.08380679034645,1.70817423068592,13.8362179249195));
#427012=CARTESIAN_POINT('Ctrl Pts',(2.07037048620981,1.71871599217078,13.8391868794965));
#427013=CARTESIAN_POINT('Origin',(2.12373068447753,1.62705901546987,13.8235269408515));
#427014=CARTESIAN_POINT('Ctrl Pts',(2.15207044569429,1.65804043837791,13.7902140241683));
#427015=CARTESIAN_POINT('Ctrl Pts',(2.1631726538172,1.66121842047165,13.8026027327198));
#427016=CARTESIAN_POINT('Ctrl Pts',(2.17051483254974,1.6462895777927,13.8057746032556));
#427017=CARTESIAN_POINT('Ctrl Pts',(2.14061222476149,1.65476532679547,13.8013225161808));
#427018=CARTESIAN_POINT('Ctrl Pts',(2.15170307817164,1.65794005489717,13.8136962270464));
#427019=CARTESIAN_POINT('Ctrl Pts',(2.15904163347975,1.64303421002668,13.8168830918628));
#427020=CARTESIAN_POINT('Ctrl Pts',(2.12914906408654,1.65148880328298,13.8124254880875));
#427021=CARTESIAN_POINT('Ctrl Pts',(2.1402236783535,1.65465888118083,13.8247886461868));
#427022=CARTESIAN_POINT('Ctrl Pts',(2.14756325531373,1.6397776456057,13.8279860620656));
#427023=CARTESIAN_POINT('Ctrl Pts',(2.11768076368937,1.64821081067997,13.8235227163066));
#427024=CARTESIAN_POINT('Ctrl Pts',(2.12873391282528,1.6513747445314,13.8358800595848));
#427025=CARTESIAN_POINT('Ctrl Pts',(2.13607948675081,1.63651983374397,13.8390832900376));
#427026=CARTESIAN_POINT('Origin',(2.15812037844579,1.63688864659068,13.7902182540695));
#427027=CARTESIAN_POINT('Ctrl Pts',(2.17174368677524,1.6636636272183,13.7382347919292));
#427028=CARTESIAN_POINT('Ctrl Pts',(2.18624633379024,1.66783389079414,13.7369371795942));
#427029=CARTESIAN_POINT('Ctrl Pts',(2.19533646733967,1.65571311321701,13.7364597369711));
#427030=CARTESIAN_POINT('Ctrl Pts',(2.17356240961947,1.66418347450367,13.7595490285574));
#427031=CARTESIAN_POINT('Ctrl Pts',(2.18841135521326,1.66845227072419,13.7633824266926));
#427032=CARTESIAN_POINT('Ctrl Pts',(2.19763260326166,1.65658373059756,13.7648920890506));
#427033=CARTESIAN_POINT('Ctrl Pts',(2.16428702274945,1.66153228183547,13.780380659011));
#427034=CARTESIAN_POINT('Ctrl Pts',(2.17712933766779,1.66522982609384,13.7901039518744));
#427035=CARTESIAN_POINT('Ctrl Pts',(2.185925335279,1.65214869971078,13.7926933640892));
#427036=CARTESIAN_POINT('Ctrl Pts',(2.14816432986381,1.65692391708338,13.7936647693663));
#427037=CARTESIAN_POINT('Ctrl Pts',(2.15855501883592,1.65992506930038,13.8072068914933));
#427038=CARTESIAN_POINT('Ctrl Pts',(2.1656288682906,1.64441362437285,13.8104111085397));
#427039=CARTESIAN_POINT('Origin',(2.17804928986436,1.64258494176751,13.7435492065112));
#427040=CARTESIAN_POINT('Origin',(2.17804928986436,1.64258494176751,14.));
#427041=CARTESIAN_POINT('Origin',(2.17804928986436,1.64258494176751,12.5369868989719));
#427042=CARTESIAN_POINT('Ctrl Pts',(2.16916964168394,1.67979273611958,12.506462012331));
#427043=CARTESIAN_POINT('Ctrl Pts',(2.17433938317482,1.6837961547721,12.4999388158272));
#427044=CARTESIAN_POINT('Ctrl Pts',(2.17427821835328,1.68374878907928,12.4907030323752));
#427045=CARTESIAN_POINT('Ctrl Pts',(2.17896995532707,1.67083827155431,12.5042014951932));
#427046=CARTESIAN_POINT('Ctrl Pts',(2.18528284974206,1.66961824646391,12.4980716682127));
#427047=CARTESIAN_POINT('Ctrl Pts',(2.18940248500344,1.66421878625579,12.4907355092743));
#427048=CARTESIAN_POINT('Ctrl Pts',(2.17694791798238,1.66516050207837,12.5218047446509));
#427049=CARTESIAN_POINT('Ctrl Pts',(2.18875962168325,1.66511023659022,12.5216906929434));
#427050=CARTESIAN_POINT('Ctrl Pts',(2.19575008742635,1.65564957366289,12.5161988840776));
#427051=CARTESIAN_POINT('Ctrl Pts',(2.17196622031264,1.66372722794542,12.5369868989719));
#427052=CARTESIAN_POINT('Ctrl Pts',(2.18669844414395,1.66796599103203,12.5369868989719));
#427053=CARTESIAN_POINT('Ctrl Pts',(2.19577675014134,1.6556132629229,12.5369868989719));
#427054=CARTESIAN_POINT('Origin',(4.02788837499579E-31,-1.93972880878785E-31,
12.5));
#427055=CARTESIAN_POINT('Origin',(-0.404665629804381,2.65281661438092,12.5));
#427056=CARTESIAN_POINT('',(-0.404665629804381,2.65281661438092,12.5893111709658));
#427057=CARTESIAN_POINT('',(-0.404665629804381,2.65281661438092,13.8235269408515));
#427058=CARTESIAN_POINT('',(-0.404665629804381,2.65281661438092,12.5));
#427059=CARTESIAN_POINT('',(-0.396456161771472,2.6876286429604,13.7902182540695));
#427060=CARTESIAN_POINT('',(-0.404665629804381,2.65281661438092,13.8235269408515));
#427061=CARTESIAN_POINT('',(-0.391698755050363,2.70780229831486,13.7435492065112));
#427062=CARTESIAN_POINT('Origin',(-0.407350877337861,2.64143131362234,13.7445212918694));
#427063=CARTESIAN_POINT('',(-0.391698755050363,2.70780229831486,12.5369868989719));
#427064=CARTESIAN_POINT('',(-0.391698755050363,2.70780229831486,12.5));
#427065=CARTESIAN_POINT('Ctrl Pts',(-0.391698755050363,2.70780229831486,
12.5369868989719));
#427066=CARTESIAN_POINT('Ctrl Pts',(-0.396017894218442,2.6894871047414,
12.5544431401645));
#427067=CARTESIAN_POINT('Ctrl Pts',(-0.400340122549649,2.67115881165471,
12.5718848856037));
#427068=CARTESIAN_POINT('Ctrl Pts',(-0.404665629804381,2.65281661438092,
12.5893111709658));
#427069=CARTESIAN_POINT('Origin',(-0.612891682967421,2.87579381918237,12.5));
#427070=CARTESIAN_POINT('',(-0.497196489292348,2.69043060726394,13.7435492065112));
#427071=CARTESIAN_POINT('',(-0.486221890222975,2.67284744872125,13.7902182540695));
#427072=CARTESIAN_POINT('Origin',(-0.45738254066051,2.62664194705149,13.7418732680444));
#427073=CARTESIAN_POINT('',(-0.467283921384982,2.64250562881056,13.8235269408515));
#427074=CARTESIAN_POINT('',(-0.486221890222975,2.67284744872125,13.7902182540695));
#427075=CARTESIAN_POINT('',(-0.467283921384982,2.64250562881056,12.5893111709658));
#427076=CARTESIAN_POINT('',(-0.467283921384982,2.64250562881056,12.5));
#427077=CARTESIAN_POINT('',(-0.497196489292348,2.69043060726394,12.5369868989719));
#427078=CARTESIAN_POINT('Ctrl Pts',(-0.467283921384982,2.64250562881056,
12.5893111709658));
#427079=CARTESIAN_POINT('Ctrl Pts',(-0.477262195405936,2.65849250659842,
12.5718848856037));
#427080=CARTESIAN_POINT('Ctrl Pts',(-0.487232905459129,2.67446726563429,
12.5544431401645));
#427081=CARTESIAN_POINT('Ctrl Pts',(-0.497196489292348,2.69043060726394,
12.5369868989719));
#427082=CARTESIAN_POINT('',(-0.497196489292348,2.69043060726394,12.5));
#427083=CARTESIAN_POINT('Origin',(-0.438122897588506,2.66070659900837,12.5));
#427084=CARTESIAN_POINT('',(-0.431436192726697,2.62698897527435,13.8587068136939));
#427085=CARTESIAN_POINT('Ctrl Pts',(-0.467283921390512,2.64250562880694,
13.8235269408542));
#427086=CARTESIAN_POINT('Ctrl Pts',(-0.466356109619478,2.64101911787706,
13.8262006681044));
#427087=CARTESIAN_POINT('Ctrl Pts',(-0.465259243162499,2.63958988311412,
13.8288634856214));
#427088=CARTESIAN_POINT('Ctrl Pts',(-0.464006343942995,2.63821505475183,
13.8314912288862));
#427089=CARTESIAN_POINT('Ctrl Pts',(-0.462714734078248,2.63679774851727,
13.8342001611531));
#427090=CARTESIAN_POINT('Ctrl Pts',(-0.461256233254173,2.63543635362977,
13.8368750301949));
#427091=CARTESIAN_POINT('Ctrl Pts',(-0.459601776425736,2.63414059064196,
13.8394886372969));
#427092=CARTESIAN_POINT('Ctrl Pts',(-0.459473998711725,2.63404051572332,
13.8396904925131));
#427093=CARTESIAN_POINT('Ctrl Pts',(-0.459345035693413,2.63394084711228,
13.8398919674349));
#427094=CARTESIAN_POINT('Ctrl Pts',(-0.4592148661835,2.63384159766317,13.8400930404591));
#427095=CARTESIAN_POINT('Ctrl Pts',(-0.457186737645295,2.6322952244744,
13.8432258934518));
#427096=CARTESIAN_POINT('Ctrl Pts',(-0.454876755602826,2.63085760148959,
13.8462331177034));
#427097=CARTESIAN_POINT('Ctrl Pts',(-0.452309288225724,2.62965751679628,
13.8489036603661));
#427098=CARTESIAN_POINT('Ctrl Pts',(-0.451469183020814,2.62926483511854,
13.8497774930041));
#427099=CARTESIAN_POINT('Ctrl Pts',(-0.450601640977806,2.62889779863514,
13.85061494757));
#427100=CARTESIAN_POINT('Ctrl Pts',(-0.449707901397574,2.62856152004778,
13.8514076489583));
#427101=CARTESIAN_POINT('Ctrl Pts',(-0.447817513288837,2.62785024233689,
13.8530843267192));
#427102=CARTESIAN_POINT('Ctrl Pts',(-0.445623194189009,2.62720947264718,
13.8546805203176));
#427103=CARTESIAN_POINT('Ctrl Pts',(-0.443214054988678,2.62680737669962,
13.8559412814274));
#427104=CARTESIAN_POINT('Ctrl Pts',(-0.442891634033449,2.62675356322156,
13.8561100121513));
#427105=CARTESIAN_POINT('Ctrl Pts',(-0.442565424139822,2.62670397513517,
13.8562727473908));
#427106=CARTESIAN_POINT('Ctrl Pts',(-0.442235690326336,2.62665895978269,
13.8564289040185));
#427107=CARTESIAN_POINT('Ctrl Pts',(-0.440740351243861,2.62645481567278,
13.8571370725437));
#427108=CARTESIAN_POINT('Ctrl Pts',(-0.439145946992039,2.62634338218817,
13.8577210840554));
#427109=CARTESIAN_POINT('Ctrl Pts',(-0.437512406194008,2.62635826739462,
13.8581177131616));
#427110=CARTESIAN_POINT('Ctrl Pts',(-0.437052344880522,2.62636245958109,
13.8582294175695));
#427111=CARTESIAN_POINT('Ctrl Pts',(-0.436589212546076,2.62637649662708,
13.8583265086086));
#427112=CARTESIAN_POINT('Ctrl Pts',(-0.43612440418866,2.6264006933244,13.8584082369006));
#427113=CARTESIAN_POINT('Ctrl Pts',(-0.435456599222336,2.62643545748983,
13.8585256585398));
#427114=CARTESIAN_POINT('Ctrl Pts',(-0.434777049033409,2.62649194829904,
13.8586122832068));
#427115=CARTESIAN_POINT('Ctrl Pts',(-0.434103471787078,2.62656948525699,
13.8586682984299));
#427116=CARTESIAN_POINT('Ctrl Pts',(-0.433564676759578,2.62663150713736,
13.8587131050557));
#427117=CARTESIAN_POINT('Ctrl Pts',(-0.433023725658311,2.62670744730329,
13.8587357943552));
#427118=CARTESIAN_POINT('Ctrl Pts',(-0.432480624609339,2.62679781630673,
13.8587355499465));
#427119=CARTESIAN_POINT('Ctrl Pts',(-0.432129605453252,2.62685622394815,
13.8587353919793));
#427120=CARTESIAN_POINT('Ctrl Pts',(-0.431781477716286,2.62691998925264,
13.8587257282814));
#427121=CARTESIAN_POINT('Ctrl Pts',(-0.431436192726697,2.62698897527435,
13.8587068136939));
#427122=CARTESIAN_POINT('Ctrl Pts',(-0.431436192726697,2.62698897527435,
13.8587068136939));
#427123=CARTESIAN_POINT('Ctrl Pts',(-0.4303005692194,2.62721586653891,13.8586446046466));
#427124=CARTESIAN_POINT('Ctrl Pts',(-0.42919565750709,2.6274991616754,13.858482427929));
#427125=CARTESIAN_POINT('Ctrl Pts',(-0.428120053257249,2.62783461641623,
13.8582284286032));
#427126=CARTESIAN_POINT('Ctrl Pts',(-0.427016608416334,2.62817875395862,
13.8579678548414));
#427127=CARTESIAN_POINT('Ctrl Pts',(-0.425941768447865,2.62858008903839,
13.857615680862));
#427128=CARTESIAN_POINT('Ctrl Pts',(-0.424934518661332,2.62901372180358,
13.8571944833187));
#427129=CARTESIAN_POINT('Ctrl Pts',(-0.422420823805986,2.63009589671742,
13.8561433417727));
#427130=CARTESIAN_POINT('Ctrl Pts',(-0.420208603676628,2.63142543878401,
13.8546163505474));
#427131=CARTESIAN_POINT('Ctrl Pts',(-0.418334033481517,2.63279875718589,
13.8528973491086));
#427132=CARTESIAN_POINT('Ctrl Pts',(-0.417991577163569,2.6330496421965,
13.8525833129072));
#427133=CARTESIAN_POINT('Ctrl Pts',(-0.417660262800879,2.63330192566237,
13.8522628768812));
#427134=CARTESIAN_POINT('Ctrl Pts',(-0.417340140202077,2.6335543132114,
13.851937733538));
#427135=CARTESIAN_POINT('Ctrl Pts',(-0.41538519590622,2.6350956089561,13.8499521282529));
#427136=CARTESIAN_POINT('Ctrl Pts',(-0.413655874782884,2.63679716476219,
13.847639871647));
#427137=CARTESIAN_POINT('Ctrl Pts',(-0.412186715697788,2.63851228582483,
13.8452109780794));
#427138=CARTESIAN_POINT('Ctrl Pts',(-0.411525710615326,2.63928395429214,
13.8441181685877));
#427139=CARTESIAN_POINT('Ctrl Pts',(-0.410916696807409,2.64005811914853,
13.8430021611332));
#427140=CARTESIAN_POINT('Ctrl Pts',(-0.410359513936009,2.6408212858355,
13.8418824960098));
#427141=CARTESIAN_POINT('Ctrl Pts',(-0.409046498271374,2.64261970762151,
13.8392439765549));
#427142=CARTESIAN_POINT('Ctrl Pts',(-0.407955488334797,2.64444079616419,
13.8364981347964));
#427143=CARTESIAN_POINT('Ctrl Pts',(-0.407054243284078,2.64627178070576,
13.8336931113419));
#427144=CARTESIAN_POINT('Ctrl Pts',(-0.406176487839031,2.64805504337099,
13.8309611966327));
#427145=CARTESIAN_POINT('Ctrl Pts',(-0.405478361130355,2.64984972914729,
13.8281701127185));
#427146=CARTESIAN_POINT('Ctrl Pts',(-0.404969236073682,2.65164737840573,
13.825358068512));
#427147=CARTESIAN_POINT('Ctrl Pts',(-0.404858857211935,2.65203711070503,
13.8247484142932));
#427148=CARTESIAN_POINT('Ctrl Pts',(-0.404757526578536,2.65242692857967,
13.8241378483365));
#427149=CARTESIAN_POINT('Ctrl Pts',(-0.404665629804381,2.65281661438092,
13.8235269408515));
#427150=CARTESIAN_POINT('',(-0.432658710073015,2.62676936608522,12.5969504640361));
#427151=CARTESIAN_POINT('Origin',(-0.438128079974114,2.66073927661063,12.584524458991));
#427152=CARTESIAN_POINT('Origin',(-0.438128079974114,2.66073927661063,12.584524458991));
#427153=CARTESIAN_POINT('Ctrl Pts',(-0.467283921384982,2.64250562881056,
12.5893111709658));
#427154=CARTESIAN_POINT('Ctrl Pts',(-0.461282785199896,2.63289079656825,
12.5770542771492));
#427155=CARTESIAN_POINT('Ctrl Pts',(-0.44602821481188,2.6388154701569,12.5737548217797));
#427156=CARTESIAN_POINT('Ctrl Pts',(-0.480406392180606,2.6635300400909,
12.5663937883685));
#427157=CARTESIAN_POINT('Ctrl Pts',(-0.474397600712889,2.65390294279477,
12.5540940315304));
#427158=CARTESIAN_POINT('Ctrl Pts',(-0.459096922082043,2.65984896909383,
12.5508374392248));
#427159=CARTESIAN_POINT('Ctrl Pts',(-0.493515622564045,2.68453323799796,
12.5434499600945));
#427160=CARTESIAN_POINT('Ctrl Pts',(-0.487487294375404,2.67487483958022,
12.5311293540532));
#427161=CARTESIAN_POINT('Ctrl Pts',(-0.472153863122835,2.6808612951745,
12.5278936106989));
#427162=CARTESIAN_POINT('Ctrl Pts',(-0.506612649674959,2.70551688420438,
12.5204817579905));
#427163=CARTESIAN_POINT('Ctrl Pts',(-0.500554485381652,2.69581068331508,
12.5081597038247));
#427164=CARTESIAN_POINT('Ctrl Pts',(-0.48519996421925,2.70185408672443,
12.5049254088044));
#427165=CARTESIAN_POINT('Ctrl Pts',(-0.497196489292348,2.69043060726394,
12.5369868989719));
#427166=CARTESIAN_POINT('Ctrl Pts',(-0.497689704890034,2.69122082213657,
12.5342545179733));
#427167=CARTESIAN_POINT('Ctrl Pts',(-0.498054582671471,2.69204101803876,
12.5314872231885));
#427168=CARTESIAN_POINT('Ctrl Pts',(-0.498219493613029,2.69286771356402,
12.5287124745063));
#427169=CARTESIAN_POINT('Ctrl Pts',(-0.498368218485575,2.6936132686222,
12.5262100684185));
#427170=CARTESIAN_POINT('Ctrl Pts',(-0.498353189084903,2.69436355020591,
12.5237004536639));
#427171=CARTESIAN_POINT('Ctrl Pts',(-0.49810787003645,2.6951301134035,12.5212220730815));
#427172=CARTESIAN_POINT('Ctrl Pts',(-0.497920057083069,2.69571698384426,
12.5193246583486));
#427173=CARTESIAN_POINT('Ctrl Pts',(-0.497594417118367,2.69632021782581,
12.517417831369));
#427174=CARTESIAN_POINT('Ctrl Pts',(-0.497037957625851,2.69691141790759,
12.5155812248347));
#427175=CARTESIAN_POINT('Ctrl Pts',(-0.496800902891061,2.69716327232013,
12.5147988205793));
#427176=CARTESIAN_POINT('Ctrl Pts',(-0.496521919973337,2.6974133883499,
12.5140295443047));
#427177=CARTESIAN_POINT('Ctrl Pts',(-0.496194277041749,2.6976616480168,
12.5132817086137));
#427178=CARTESIAN_POINT('Ctrl Pts',(-0.495698433787316,2.69803735543885,
12.5121499604604));
#427179=CARTESIAN_POINT('Ctrl Pts',(-0.495076119358838,2.69841122422461,
12.5110494206568));
#427180=CARTESIAN_POINT('Ctrl Pts',(-0.494298903258426,2.69875920015332,
12.5100666561695));
#427181=CARTESIAN_POINT('Ctrl Pts',(-0.49385262756334,2.69895900713027,
12.509502355064));
#427182=CARTESIAN_POINT('Ctrl Pts',(-0.493349857282979,2.69915198998088,
12.5089719619137));
#427183=CARTESIAN_POINT('Ctrl Pts',(-0.492797727532223,2.69932856864687,
12.5085043804652));
#427184=CARTESIAN_POINT('Ctrl Pts',(-0.49198975756195,2.69958696852355,
12.5078201359221));
#427185=CARTESIAN_POINT('Ctrl Pts',(-0.491052284959171,2.69981658370521,
12.5072563000949));
#427186=CARTESIAN_POINT('Ctrl Pts',(-0.490046842492173,2.69999362672806,
12.5068768744332));
#427187=CARTESIAN_POINT('Ctrl Pts',(-0.489321849258572,2.70012128693521,
12.5066032824114));
#427188=CARTESIAN_POINT('Ctrl Pts',(-0.488548789130486,2.70022391470455,
12.5064197834843));
#427189=CARTESIAN_POINT('Ctrl Pts',(-0.487771171960831,2.70029834141171,
12.5063282718343));
#427190=CARTESIAN_POINT('Ctrl Pts',(-0.486636091637325,2.70040698136224,
12.5061946931564));
#427191=CARTESIAN_POINT('Ctrl Pts',(-0.485467141851131,2.70045891282986,
12.5062515701262));
#427192=CARTESIAN_POINT('Ctrl Pts',(-0.484337556030415,2.70046636214881,
12.5064436508398));
#427193=CARTESIAN_POINT('',(-0.44602821481188,2.6388154701569,12.5737548217797));
#427194=CARTESIAN_POINT('Origin',(-0.448620866155238,2.65415424973716,12.5893111709658));
#427195=CARTESIAN_POINT('Ctrl Pts',(-0.484337556030415,2.70046636214881,
12.5064436508398));
#427196=CARTESIAN_POINT('Ctrl Pts',(-0.478666370156481,2.69134068198049,
12.5164271754438));
#427197=CARTESIAN_POINT('Ctrl Pts',(-0.472993113685128,2.6822112741119,
12.5264061185523));
#427198=CARTESIAN_POINT('Ctrl Pts',(-0.467317712887747,2.67307800775614,
12.536380305637));
#427199=CARTESIAN_POINT('Ctrl Pts',(-0.460224612986331,2.66166327723746,
12.5488460165097));
#427200=CARTESIAN_POINT('Ctrl Pts',(-0.45312816158799,2.65024251640408,
12.5613043021964));
#427201=CARTESIAN_POINT('Ctrl Pts',(-0.44602821481188,2.6388154701569,12.5737548217797));
#427202=CARTESIAN_POINT('Ctrl Pts',(-0.404665629804381,2.65281661438092,
12.5893111709658));
#427203=CARTESIAN_POINT('Ctrl Pts',(-0.407267077514747,2.64178524527415,
12.5770542771492));
#427204=CARTESIAN_POINT('Ctrl Pts',(-0.423615907027033,2.64250597298498,
12.5737548217797));
#427205=CARTESIAN_POINT('Ctrl Pts',(-0.407092757891956,2.64252444295008,
12.5928319619712));
#427206=CARTESIAN_POINT('Ctrl Pts',(-0.412011859954225,2.63585842080247,
12.5821634970842));
#427207=CARTESIAN_POINT('Ctrl Pts',(-0.424490864181512,2.63875461758363,
12.5773203894503));
#427208=CARTESIAN_POINT('Ctrl Pts',(-0.417387204414804,2.6293104931194,
12.5969440695591));
#427209=CARTESIAN_POINT('Ctrl Pts',(-0.42135055049259,2.62863935198698,
12.5878292599214));
#427210=CARTESIAN_POINT('Ctrl Pts',(-0.428161628981916,2.63404615362204,
12.5813877129824));
#427211=CARTESIAN_POINT('Ctrl Pts',(-0.44756881895074,2.62428601408715,
12.596957478804));
#427212=CARTESIAN_POINT('Ctrl Pts',(-0.443634776446592,2.62495227433994,
12.5878468778671));
#427213=CARTESIAN_POINT('Ctrl Pts',(-0.438965026764344,2.63225370706529,
12.5814011370086));
#427214=CARTESIAN_POINT('Ctrl Pts',(-0.461676783769701,2.63352204872367,
12.5928371701607));
#427215=CARTESIAN_POINT('Ctrl Pts',(-0.454881448360943,2.62879357302993,
12.5821692192952));
#427216=CARTESIAN_POINT('Ctrl Pts',(-0.443990357448371,2.63553211595122,
12.5773318885715));
#427217=CARTESIAN_POINT('Ctrl Pts',(-0.467283921385027,2.64250562881053,
12.5893111709658));
#427218=CARTESIAN_POINT('Ctrl Pts',(-0.461282785199942,2.63289079656822,
12.5770542771492));
#427219=CARTESIAN_POINT('Ctrl Pts',(-0.446028214811926,2.63881547015687,
12.5737548217797));
#427220=CARTESIAN_POINT('',(-0.423615907027033,2.64250597298498,12.5737548217797));
#427221=CARTESIAN_POINT('Origin',(-0.426078281186221,2.65786620454249,12.5893111709658));
#427222=CARTESIAN_POINT('Ctrl Pts',(-0.446028214811926,2.63881547015687,
12.5737548217797));
#427223=CARTESIAN_POINT('Ctrl Pts',(-0.445525600187509,2.63794846486834,
12.5746934679442));
#427224=CARTESIAN_POINT('Ctrl Pts',(-0.44481094380899,2.63708093867342,
12.5756680099006));
#427225=CARTESIAN_POINT('Ctrl Pts',(-0.443968123483801,2.63630947411337,
12.5765688348656));
#427226=CARTESIAN_POINT('Ctrl Pts',(-0.443744996133033,2.63610523741148,
12.5768073183026));
#427227=CARTESIAN_POINT('Ctrl Pts',(-0.443513100702999,2.63590759166848,
12.5770407398754));
#427228=CARTESIAN_POINT('Ctrl Pts',(-0.443274370359209,2.6357179104468,
12.5772674179684));
#427229=CARTESIAN_POINT('Ctrl Pts',(-0.442294685583711,2.63493951000499,
12.5781976435658));
#427230=CARTESIAN_POINT('Ctrl Pts',(-0.441137235981574,2.63425985722505,
12.5790594849312));
#427231=CARTESIAN_POINT('Ctrl Pts',(-0.439855722864257,2.63376648428921,
12.5797571720116));
#427232=CARTESIAN_POINT('Ctrl Pts',(-0.43902077098922,2.6334450340814,12.580211740231));
#427233=CARTESIAN_POINT('Ctrl Pts',(-0.438088465128481,2.63320557059283,
12.5806009430798));
#427234=CARTESIAN_POINT('Ctrl Pts',(-0.43712002807693,2.63308211071472,
12.5808812374708));
#427235=CARTESIAN_POINT('Ctrl Pts',(-0.436287819373999,2.63297601772203,
12.5811221033394));
#427236=CARTESIAN_POINT('Ctrl Pts',(-0.43541187759125,2.63295352892627,
12.581287365893));
#427237=CARTESIAN_POINT('Ctrl Pts',(-0.434541428297158,2.63302424886595,
12.581359338449));
#427238=CARTESIAN_POINT('Ctrl Pts',(-0.434420453819371,2.63303407747726,
12.5813693411482));
#427239=CARTESIAN_POINT('Ctrl Pts',(-0.434299560967986,2.63304565178682,
12.5813775999465));
#427240=CARTESIAN_POINT('Ctrl Pts',(-0.434178855836194,2.63305894204054,
12.5813841266931));
#427241=CARTESIAN_POINT('Ctrl Pts',(-0.433974064981122,2.6330814905634,
12.5813952001081));
#427242=CARTESIAN_POINT('Ctrl Pts',(-0.433768509527142,2.63310973470351,
12.5814007534795));
#427243=CARTESIAN_POINT('Ctrl Pts',(-0.433562305845541,2.63314385753371,
12.5814005856065));
#427244=CARTESIAN_POINT('Ctrl Pts',(-0.432618386011585,2.6333000585092,
12.5813998171494));
#427245=CARTESIAN_POINT('Ctrl Pts',(-0.431726045399303,2.63356831926361,
12.58127954464));
#427246=CARTESIAN_POINT('Ctrl Pts',(-0.430881831425681,2.63391878020847,
12.5810700125799));
#427247=CARTESIAN_POINT('Ctrl Pts',(-0.429862117067003,2.63434209712668,
12.5808169217085));
#427248=CARTESIAN_POINT('Ctrl Pts',(-0.428918943474546,2.63490083851046,
12.5804173076348));
#427249=CARTESIAN_POINT('Ctrl Pts',(-0.428121695428069,2.63552363134925,
12.5799304713245));
#427250=CARTESIAN_POINT('Ctrl Pts',(-0.427133653939449,2.63629546787648,
12.5793271277669));
#427251=CARTESIAN_POINT('Ctrl Pts',(-0.426288626927976,2.63718818404541,
12.5785808224116));
#427252=CARTESIAN_POINT('Ctrl Pts',(-0.425599199900031,2.63814234662912,
12.5777485681082));
#427253=CARTESIAN_POINT('Ctrl Pts',(-0.424571878096021,2.63956415341515,
12.576508418016));
#427254=CARTESIAN_POINT('Ctrl Pts',(-0.423893134534421,2.64110640070023,
12.5750928681475));
#427255=CARTESIAN_POINT('Ctrl Pts',(-0.423615907027033,2.64250597298498,
12.5737548217797));
#427256=CARTESIAN_POINT('Ctrl Pts',(-0.423615907027033,2.64250597298498,
12.5737548217797));
#427257=CARTESIAN_POINT('Ctrl Pts',(-0.407267077514747,2.64178524527415,
12.5770542771492));
#427258=CARTESIAN_POINT('Ctrl Pts',(-0.404665629804381,2.65281661438092,
12.5893111709658));
#427259=CARTESIAN_POINT('Ctrl Pts',(-0.417982099262763,2.66661562176396,
12.5508408821982));
#427260=CARTESIAN_POINT('Ctrl Pts',(-0.401582757830894,2.66588945013814,
12.55409748406));
#427261=CARTESIAN_POINT('Ctrl Pts',(-0.398977991339499,2.67693489244663,
12.5663972313419));
#427262=CARTESIAN_POINT('Ctrl Pts',(-0.412352646447294,2.69070145006173,
12.52790050457));
#427263=CARTESIAN_POINT('Ctrl Pts',(-0.395909324972191,2.6899474897126,
12.5311362602938));
#427264=CARTESIAN_POINT('Ctrl Pts',(-0.393296090767228,2.7010288391329,
12.5434568539655));
#427265=CARTESIAN_POINT('Ctrl Pts',(-0.406727196660406,2.71476530588435,
12.5049357605811));
#427266=CARTESIAN_POINT('Ctrl Pts',(-0.390245644042783,2.71396417649287,
12.5081700652078));
#427267=CARTESIAN_POINT('Ctrl Pts',(-0.38761947869465,2.72510036007836,
12.5204921097672));
#427268=CARTESIAN_POINT('Ctrl Pts',(-0.407096584199038,2.71318517842233,
12.5064436508395));
#427269=CARTESIAN_POINT('Ctrl Pts',(-0.405938267818595,2.71356878102058,
12.5062361689309));
#427270=CARTESIAN_POINT('Ctrl Pts',(-0.404717355904196,2.71391830314823,
12.5061871075061));
#427271=CARTESIAN_POINT('Ctrl Pts',(-0.403518447949327,2.71418966334587,
12.5063648335164));
#427272=CARTESIAN_POINT('Ctrl Pts',(-0.402973830004515,2.71431293188584,
12.5064455676329));
#427273=CARTESIAN_POINT('Ctrl Pts',(-0.402426107734433,2.71442157588489,
12.506574497099));
#427274=CARTESIAN_POINT('Ctrl Pts',(-0.401898561348905,2.71450990614909,
12.5067492519495));
#427275=CARTESIAN_POINT('Ctrl Pts',(-0.400838436409385,2.71468740924372,
12.5071004286051));
#427276=CARTESIAN_POINT('Ctrl Pts',(-0.399820676186354,2.71478860954198,
12.5076537929612));
#427277=CARTESIAN_POINT('Ctrl Pts',(-0.398922604801309,2.71481532346341,
12.5083435010503));
#427278=CARTESIAN_POINT('Ctrl Pts',(-0.39886606584061,2.71481700526441,
12.5083869222963));
#427279=CARTESIAN_POINT('Ctrl Pts',(-0.398809994740654,2.71481838009582,
12.5084308732336));
#427280=CARTESIAN_POINT('Ctrl Pts',(-0.398754407794718,2.71481944381979,
12.5084753333615));
#427281=CARTESIAN_POINT('Ctrl Pts',(-0.398308527120983,2.71482797629003,
12.508831962269));
#427282=CARTESIAN_POINT('Ctrl Pts',(-0.397884770249155,2.71481795468889,
12.509227847131));
#427283=CARTESIAN_POINT('Ctrl Pts',(-0.397495671478641,2.71479247628123,
12.5096423454524));
#427284=CARTESIAN_POINT('Ctrl Pts',(-0.396276408139752,2.71471263822789,
12.5109411997424));
#427285=CARTESIAN_POINT('Ctrl Pts',(-0.395321834754573,2.71448576438194,
12.5124831113042));
#427286=CARTESIAN_POINT('Ctrl Pts',(-0.394574919738505,2.71418737464644,
12.5140723025008));
#427287=CARTESIAN_POINT('Ctrl Pts',(-0.394504932983426,2.71415941520141,
12.5142212114565));
#427288=CARTESIAN_POINT('Ctrl Pts',(-0.394436744436691,2.71413084370056,
12.5143705582413));
#427289=CARTESIAN_POINT('Ctrl Pts',(-0.394370293720933,2.71410173263056,
12.5145201959299));
#427290=CARTESIAN_POINT('Ctrl Pts',(-0.393516635342246,2.71372775759454,
12.5164425148273));
#427291=CARTESIAN_POINT('Ctrl Pts',(-0.392916216798835,2.71326175828972,
12.5184635205941));
#427292=CARTESIAN_POINT('Ctrl Pts',(-0.392485164478752,2.71273694910712,
12.5205025929158));
#427293=CARTESIAN_POINT('Ctrl Pts',(-0.392235137047787,2.71243253897973,
12.5216853356836));
#427294=CARTESIAN_POINT('Ctrl Pts',(-0.392042170182552,2.71210919930776,
12.5228750347131));
#427295=CARTESIAN_POINT('Ctrl Pts',(-0.391892392212254,2.7117787837994,
12.5240609649613));
#427296=CARTESIAN_POINT('Ctrl Pts',(-0.391524770219468,2.71096779666032,
12.5269717671326));
#427297=CARTESIAN_POINT('Ctrl Pts',(-0.391416453375186,2.71008706602646,
12.5299036066169));
#427298=CARTESIAN_POINT('Ctrl Pts',(-0.391484251980021,2.70916086114884,
12.5328133004019));
#427299=CARTESIAN_POINT('Ctrl Pts',(-0.391516799258136,2.70871622887628,
12.5342101228451));
#427300=CARTESIAN_POINT('Ctrl Pts',(-0.391590415451197,2.70826170983071,
12.5356023438238));
#427301=CARTESIAN_POINT('Ctrl Pts',(-0.391698755050363,2.70780229831486,
12.5369868989719));
#427302=CARTESIAN_POINT('Origin',(2.53877470614877,15.1113213650641,-1.23968739425757));
#427303=CARTESIAN_POINT('Ctrl Pts',(-0.49717439363454,2.69039513131661,
12.5369868989719));
#427304=CARTESIAN_POINT('Ctrl Pts',(-0.50527136720736,2.70342288333476,
12.5369868989719));
#427305=CARTESIAN_POINT('Ctrl Pts',(-0.520295295224563,2.70033016759948,
12.5369868989719));
#427306=CARTESIAN_POINT('Ctrl Pts',(-0.499911543608354,2.6947989860598,
12.5218025310016));
#427307=CARTESIAN_POINT('Ctrl Pts',(-0.508715847286229,2.70268188530136,
12.5216901060418));
#427308=CARTESIAN_POINT('Ctrl Pts',(-0.520249500638078,2.70033961137504,
12.5161920673678));
#427309=CARTESIAN_POINT('Ctrl Pts',(-0.497609306258535,2.70036996213051,
12.5042015548894));
#427310=CARTESIAN_POINT('Ctrl Pts',(-0.503115446561909,2.70369558447474,
12.4980677368513));
#427311=CARTESIAN_POINT('Ctrl Pts',(-0.509796007626935,2.70244623120992,
12.4907278922777));
#427312=CARTESIAN_POINT('Ctrl Pts',(-0.48433402510107,2.70044667520282,
12.506463626192));
#427313=CARTESIAN_POINT('Ctrl Pts',(-0.485489056741789,2.7068866550355,
12.4999376786891));
#427314=CARTESIAN_POINT('Ctrl Pts',(-0.485474949709712,2.70680800004557,
12.4906970594712));
#427315=CARTESIAN_POINT('Origin',(-0.515859544522093,2.67878198633735,12.5369868989719));
#427316=CARTESIAN_POINT('Origin',(-0.515859544522093,2.67878198633735,14.));
#427317=CARTESIAN_POINT('Origin',(-0.515859544522093,2.67878198633735,13.7435492065112));
#427318=CARTESIAN_POINT('Ctrl Pts',(-0.484086463901995,2.66942608434243,
13.793642941384));
#427319=CARTESIAN_POINT('Ctrl Pts',(-0.489788288908134,2.67861278182332,
13.8071662555867));
#427320=CARTESIAN_POINT('Ctrl Pts',(-0.505420949465545,2.67185709477229,
13.8103758687955));
#427321=CARTESIAN_POINT('Ctrl Pts',(-0.492887059224724,2.68352612785969,
13.7804579775006));
#427322=CARTESIAN_POINT('Ctrl Pts',(-0.499931212062378,2.69485633450072,
13.7901904343351));
#427323=CARTESIAN_POINT('Ctrl Pts',(-0.515215284247408,2.69102840273443,
13.7927914348263));
#427324=CARTESIAN_POINT('Ctrl Pts',(-0.498068300927142,2.69182735410252,
13.7597120340895));
#427325=CARTESIAN_POINT('Ctrl Pts',(-0.506225236064354,2.70493656838637,
13.7635825532445));
#427326=CARTESIAN_POINT('Ctrl Pts',(-0.521013756001522,2.70232207145352,
13.7651073818884));
#427327=CARTESIAN_POINT('Ctrl Pts',(-0.497053695165545,2.69020178392726,
13.7381884353898));
#427328=CARTESIAN_POINT('Ctrl Pts',(-0.505018938881371,2.70300462748538,
13.7368803041982));
#427329=CARTESIAN_POINT('Ctrl Pts',(-0.519878682598321,2.70011020979169,
13.7363986145813));
#427330=CARTESIAN_POINT('Origin',(-0.504884945452719,2.66119882779466,13.7902182540695));
#427331=CARTESIAN_POINT('Ctrl Pts',(-0.467281837879557,2.64250228925016,
13.8235227101244));
#427332=CARTESIAN_POINT('Ctrl Pts',(-0.47336557853089,2.65225784090073,
13.8358800583119));
#427333=CARTESIAN_POINT('Ctrl Pts',(-0.488772600020449,2.64615458456686,
13.8390832900376));
#427334=CARTESIAN_POINT('Ctrl Pts',(-0.473597285630048,2.65262070162588,
13.8124254819053));
#427335=CARTESIAN_POINT('Ctrl Pts',(-0.479692841055534,2.66239519827228,
13.8247886449158));
#427336=CARTESIAN_POINT('Ctrl Pts',(-0.495113052711319,2.656268383962,13.8279860620657));
#427337=CARTESIAN_POINT('Ctrl Pts',(-0.479909903002316,2.66273457925838,
13.8013225099955));
#427338=CARTESIAN_POINT('Ctrl Pts',(-0.486014395377619,2.67252340996857,
13.8136962257787));
#427339=CARTESIAN_POINT('Ctrl Pts',(-0.501450340426691,2.66637764514034,
13.8168830918626));
#427340=CARTESIAN_POINT('Ctrl Pts',(-0.486219800122016,2.67284409858753,
13.7902140179785));
#427341=CARTESIAN_POINT('Ctrl Pts',(-0.492330539712305,2.68264295378619,
13.802602731458));
#427342=CARTESIAN_POINT('Ctrl Pts',(-0.507784585966958,2.67648254739697,
13.8057746032558));
#427343=CARTESIAN_POINT('Origin',(-0.485946976614727,2.63085700788397,13.8235269408515));
#427344=CARTESIAN_POINT('Ctrl Pts',(-0.404665629804381,2.65281661438092,
13.8235269408515));
#427345=CARTESIAN_POINT('Ctrl Pts',(-0.401955496063886,2.66430886367772,
13.8362179249168));
#427346=CARTESIAN_POINT('Ctrl Pts',(-0.384918149628171,2.66312910502163,
13.8391868794938));
#427347=CARTESIAN_POINT('Ctrl Pts',(-0.407145284211823,2.64230170650223,
13.8400110824519));
#427348=CARTESIAN_POINT('Ctrl Pts',(-0.401642753823838,2.65073046810706,
13.8494522556837));
#427349=CARTESIAN_POINT('Ctrl Pts',(-0.389108318008103,2.64585032402954,
13.85569149686));
#427350=CARTESIAN_POINT('Ctrl Pts',(-0.417047772027924,2.62936576969432,
13.8586819406588));
#427351=CARTESIAN_POINT('Ctrl Pts',(-0.412754051757822,2.6300868867979,
13.868010383617));
#427352=CARTESIAN_POINT('Ctrl Pts',(-0.40566257599941,2.62446515767242,
13.8744918421245));
#427353=CARTESIAN_POINT('Ctrl Pts',(-0.447913512718888,2.62422986183445,
13.8587686893867));
#427354=CARTESIAN_POINT('Ctrl Pts',(-0.4521690095924,2.62351510713571,13.8680909899357));
#427355=CARTESIAN_POINT('Ctrl Pts',(-0.457045392374262,2.61591791736115,
13.8745789365163));
#427356=CARTESIAN_POINT('Ctrl Pts',(-0.461554435365154,2.6333260259336,
13.8400379222776));
#427357=CARTESIAN_POINT('Ctrl Pts',(-0.469471404303291,2.63953825876411,
13.8494748685453));
#427358=CARTESIAN_POINT('Ctrl Pts',(-0.479775288452308,2.63090164619271,
13.8557104837033));
#427359=CARTESIAN_POINT('Ctrl Pts',(-0.467283921390512,2.64250562880694,
13.8235269408542));
#427360=CARTESIAN_POINT('Ctrl Pts',(-0.473535779381647,2.65252215966594,
13.8362179249195));
#427361=CARTESIAN_POINT('Ctrl Pts',(-0.489295333932619,2.64594192833176,
13.8391868794965));
#427362=CARTESIAN_POINT('Origin',(-0.383252978422541,2.64776702421936,13.8235269408515));
#427363=CARTESIAN_POINT('Ctrl Pts',(-0.39645706603083,2.68762480516188,
13.7902140241682));
#427364=CARTESIAN_POINT('Ctrl Pts',(-0.393810800458559,2.698865618029,13.8026027327198));
#427365=CARTESIAN_POINT('Ctrl Pts',(-0.377197449355658,2.69798556268688,
13.8057746032556));
#427366=CARTESIAN_POINT('Ctrl Pts',(-0.399192359301602,2.67602586755773,
13.8013225161808));
#427367=CARTESIAN_POINT('Ctrl Pts',(-0.396548796924342,2.68725518213354,
13.8136962270464));
#427368=CARTESIAN_POINT('Ctrl Pts',(-0.379957285915439,2.68638319144844,
13.8168830918628));
#427369=CARTESIAN_POINT('Ctrl Pts',(-0.401928831781928,2.66442192954721,
13.8124254880875));
#427370=CARTESIAN_POINT('Ctrl Pts',(-0.399289138525419,2.67563480137168,
13.8247886461867));
#427371=CARTESIAN_POINT('Ctrl Pts',(-0.382718606411943,2.67477571600085,
13.8279860620656));
#427372=CARTESIAN_POINT('Ctrl Pts',(-0.404666531210821,2.65281278869432,
13.8235227163065));
#427373=CARTESIAN_POINT('Ctrl Pts',(-0.402031954534204,2.66400392755378,
13.8358800595848));
#427374=CARTESIAN_POINT('Ctrl Pts',(-0.385481469674173,2.66316292713999,
13.8390832900376));
#427375=CARTESIAN_POINT('Origin',(-0.375043510389632,2.68257905279883,13.7902182540695));
#427376=CARTESIAN_POINT('Ctrl Pts',(-0.391760668288975,2.70753963671063,
13.7382347919292));
#427377=CARTESIAN_POINT('Ctrl Pts',(-0.388320398150704,2.72223257413337,
13.7369371795943));
#427378=CARTESIAN_POINT('Ctrl Pts',(-0.373304462126552,2.72424886834272,
13.7364597369711));
#427379=CARTESIAN_POINT('Ctrl Pts',(-0.391326505236804,2.70938069521824,
13.7595490285573));
#427380=CARTESIAN_POINT('Ctrl Pts',(-0.387803174254,2.72442396431789,13.7633824266925));
#427381=CARTESIAN_POINT('Ctrl Pts',(-0.372943370247577,2.72667782438402,
13.7648920890506));
#427382=CARTESIAN_POINT('Ctrl Pts',(-0.393540713025231,2.69999139769274,
13.7803806590111));
#427383=CARTESIAN_POINT('Ctrl Pts',(-0.390498414047488,2.71300451810768,
13.7901039518745));
#427384=CARTESIAN_POINT('Ctrl Pts',(-0.374787928484793,2.71429528718463,
13.7926933640892));
#427385=CARTESIAN_POINT('Ctrl Pts',(-0.39738950035983,2.68367070262093,
13.7936647693663));
#427386=CARTESIAN_POINT('Ctrl Pts',(-0.394936254100455,2.69420421650451,
13.8072068914932));
#427387=CARTESIAN_POINT('Ctrl Pts',(-0.377945431714628,2.69280556554734,
13.8104111085397));
#427388=CARTESIAN_POINT('Origin',(-0.370286103668523,2.7027527081533,13.7435492065112));
#427389=CARTESIAN_POINT('Origin',(-0.370286103668523,2.7027527081533,14.));
#427390=CARTESIAN_POINT('Origin',(-0.370286103668523,2.7027527081533,12.5369868989719));
#427391=CARTESIAN_POINT('Ctrl Pts',(-0.407093856453013,2.71316699868649,
12.506462012331));
#427392=CARTESIAN_POINT('Ctrl Pts',(-0.408064075637327,2.71963323891745,
12.4999388158272));
#427393=CARTESIAN_POINT('Ctrl Pts',(-0.408052596672013,2.71955673481557,
12.4907030323752));
#427394=CARTESIAN_POINT('Ctrl Pts',(-0.394494611539127,2.71734881775887,
12.5042014951931));
#427395=CARTESIAN_POINT('Ctrl Pts',(-0.390348035787285,2.72226277814235,
12.4980716682126));
#427396=CARTESIAN_POINT('Ctrl Pts',(-0.383624575490615,2.72322228158951,
12.4907355092743));
#427397=CARTESIAN_POINT('Ctrl Pts',(-0.390526476627142,2.71281234263312,
12.521804744651));
#427398=CARTESIAN_POINT('Ctrl Pts',(-0.38471641496952,2.72309641062548,
12.5216906929435));
#427399=CARTESIAN_POINT('Ctrl Pts',(-0.373047088808023,2.72457883474397,
12.5161988840776));
#427400=CARTESIAN_POINT('Ctrl Pts',(-0.391707539933291,2.70776490012432,
12.5369868989719));
#427401=CARTESIAN_POINT('Ctrl Pts',(-0.388214978467543,2.7226916394176,
12.5369868989719));
#427402=CARTESIAN_POINT('Ctrl Pts',(-0.373002382684925,2.72458437845827,
12.5369868989719));
#427403=CARTESIAN_POINT('Origin',(-8.37054729992257E-32,-6.84555113983452E-33,
12.5));
#427404=CARTESIAN_POINT('Origin',(-0.619548319923707,2.61100558037706,12.5));
#427405=CARTESIAN_POINT('',(-0.619548319923707,2.61100558037706,12.5893111709658));
#427406=CARTESIAN_POINT('',(-0.619548319923707,2.61100558037706,13.8235269408515));
#427407=CARTESIAN_POINT('',(-0.619548319923707,2.61100558037706,12.5));
#427408=CARTESIAN_POINT('',(-0.614203671726777,2.64637092266089,13.7902182540695));
#427409=CARTESIAN_POINT('',(-0.619548319923707,2.61100558037706,13.8235269408515));
#427410=CARTESIAN_POINT('',(-0.611106435078542,2.66686522465476,13.7435492065112));
#427411=CARTESIAN_POINT('Origin',(-0.621296624808806,2.59943929067106,13.7445212918714));
#427412=CARTESIAN_POINT('',(-0.611106435078542,2.66686522465476,12.5369868989719));
#427413=CARTESIAN_POINT('',(-0.611106435078542,2.66686522465476,12.5));
#427414=CARTESIAN_POINT('Ctrl Pts',(-0.611106435078542,2.66686522465476,
12.5369868989719));
#427415=CARTESIAN_POINT('Ctrl Pts',(-0.613918344361144,2.64825892343788,
12.5544431401645));
#427416=CARTESIAN_POINT('Ctrl Pts',(-0.616732264796001,2.62963931449985,
12.5718848856037));
#427417=CARTESIAN_POINT('Ctrl Pts',(-0.619548319923707,2.61100558037706,
12.5893111709658));
#427418=CARTESIAN_POINT('Origin',(-0.845256230282979,2.8162684905147,12.5));
#427419=CARTESIAN_POINT('',(-0.714837180221226,2.64095229173884,13.7435492065112));
#427420=CARTESIAN_POINT('',(-0.702465907569606,2.62432217141305,13.7902182540695));
#427421=CARTESIAN_POINT('Origin',(-0.669956341227117,2.58062108945978,13.7418732680448));
#427422=CARTESIAN_POINT('',(-0.681117813258215,2.59562493167691,13.8235269408515));
#427423=CARTESIAN_POINT('',(-0.702465907569606,2.62432217141305,13.7902182540695));
#427424=CARTESIAN_POINT('',(-0.681117813258215,2.59562493167691,12.5893111709658));
#427425=CARTESIAN_POINT('',(-0.681117813258215,2.59562493167691,12.5));
#427426=CARTESIAN_POINT('',(-0.714837180221226,2.64095229173884,12.5369868989719));
#427427=CARTESIAN_POINT('Ctrl Pts',(-0.681117813258215,2.59562493167691,
12.5893111709658));
#427428=CARTESIAN_POINT('Ctrl Pts',(-0.692365964350157,2.61074529248128,
12.5718848856037));
#427429=CARTESIAN_POINT('Ctrl Pts',(-0.703605588852024,2.62585419139138,
12.5544431401645));
#427430=CARTESIAN_POINT('Ctrl Pts',(-0.714837180221226,2.64095229173884,
12.5369868989719));
#427431=CARTESIAN_POINT('',(-0.714837180221226,2.64095229173884,12.5));
#427432=CARTESIAN_POINT('Origin',(-0.653537368403491,2.61614223380501,12.5));
#427433=CARTESIAN_POINT('',(-0.644124613647114,2.58308183120501,13.8587068136939));
#427434=CARTESIAN_POINT('Ctrl Pts',(-0.681117813263431,2.59562493167285,
13.8235269408542));
#427435=CARTESIAN_POINT('Ctrl Pts',(-0.680071924268647,2.59421899225819,
13.8262006681044));
#427436=CARTESIAN_POINT('Ctrl Pts',(-0.678862211642773,2.59288391795508,
13.8288634856214));
#427437=CARTESIAN_POINT('Ctrl Pts',(-0.677501420067256,2.59161578713848,
13.8314912288862));
#427438=CARTESIAN_POINT('Ctrl Pts',(-0.676098584312039,2.5903084750682,
13.8342001611531));
#427439=CARTESIAN_POINT('Ctrl Pts',(-0.674533970207235,2.58907049146711,
13.8368750301949));
#427440=CARTESIAN_POINT('Ctrl Pts',(-0.672779401734628,2.58791389361448,
13.8394886372968));
#427441=CARTESIAN_POINT('Ctrl Pts',(-0.672643892155498,2.58782456675681,
13.8396904925131));
#427442=CARTESIAN_POINT('Ctrl Pts',(-0.672507234333911,2.58773574146807,
13.8398919674349));
#427443=CARTESIAN_POINT('Ctrl Pts',(-0.672369408200813,2.58764743228681,
13.8400930404591));
#427444=CARTESIAN_POINT('Ctrl Pts',(-0.670221984322296,2.58627151583134,
13.8432258934518));
#427445=CARTESIAN_POINT('Ctrl Pts',(-0.667802508935009,2.5850269613997,
13.8462331177034));
#427446=CARTESIAN_POINT('Ctrl Pts',(-0.665145766550256,2.58404014231565,
13.8489036603661));
#427447=CARTESIAN_POINT('Ctrl Pts',(-0.664276449523898,2.58371724362716,
13.8497774930041));
#427448=CARTESIAN_POINT('Ctrl Pts',(-0.663381877274673,2.58342214115775,
13.85061494757));
#427449=CARTESIAN_POINT('Ctrl Pts',(-0.662463701712439,2.58315982958252,
13.8514076489583));
#427450=CARTESIAN_POINT('Ctrl Pts',(-0.660521627977569,2.5826050027699,
13.8530843267192));
#427451=CARTESIAN_POINT('Ctrl Pts',(-0.658282381615198,2.58214522256617,
13.8546805203176));
#427452=CARTESIAN_POINT('Ctrl Pts',(-0.655848484074212,2.58194083176989,
13.8559412814274));
#427453=CARTESIAN_POINT('Ctrl Pts',(-0.655522749650073,2.5819134776528,
13.8561100121513));
#427454=CARTESIAN_POINT('Ctrl Pts',(-0.655193583303564,2.58189064370139,
13.8562727473908));
#427455=CARTESIAN_POINT('Ctrl Pts',(-0.654861277483013,2.58187265450069,
13.8564289040185));
#427456=CARTESIAN_POINT('Ctrl Pts',(-0.65335427437784,2.58179107368073,
13.8571370725437));
#427457=CARTESIAN_POINT('Ctrl Pts',(-0.651756092511145,2.58180996973009,
13.8577210840554));
#427458=CARTESIAN_POINT('Ctrl Pts',(-0.650129200467877,2.58195795414735,
13.8581177131616));
#427459=CARTESIAN_POINT('Ctrl Pts',(-0.649671011672573,2.58199963165271,
13.8582294175695));
#427460=CARTESIAN_POINT('Ctrl Pts',(-0.649210564522325,2.58205137157636,
13.8583265086086));
#427461=CARTESIAN_POINT('Ctrl Pts',(-0.648749275031835,2.58211337395736,
13.8584082369006));
#427462=CARTESIAN_POINT('Ctrl Pts',(-0.648086525733664,2.58220245475225,
13.8585256585398));
#427463=CARTESIAN_POINT('Ctrl Pts',(-0.647413841217318,2.58231414724199,
13.8586122832068));
#427464=CARTESIAN_POINT('Ctrl Pts',(-0.646748825225599,2.58244632900087,
13.8586682984299));
#427465=CARTESIAN_POINT('Ctrl Pts',(-0.646216878353138,2.58255206130522,
13.8587131050557));
#427466=CARTESIAN_POINT('Ctrl Pts',(-0.645683917050552,2.58267184132321,
13.8587357943552));
#427467=CARTESIAN_POINT('Ctrl Pts',(-0.645149989038243,2.58280617740864,
13.8587355499465));
#427468=CARTESIAN_POINT('Ctrl Pts',(-0.644804898634477,2.58289300202337,
13.8587353919793));
#427469=CARTESIAN_POINT('Ctrl Pts',(-0.644463126728151,2.58298493079649,
13.8587257282814));
#427470=CARTESIAN_POINT('Ctrl Pts',(-0.644124613647114,2.58308183120501,
13.8587068136939));
#427471=CARTESIAN_POINT('Ctrl Pts',(-0.644124613647114,2.58308183120501,
13.8587068136939));
#427472=CARTESIAN_POINT('Ctrl Pts',(-0.643011262577741,2.58340053136607,
13.8586446046466));
#427473=CARTESIAN_POINT('Ctrl Pts',(-0.641933118551584,2.58377294442342,
13.858482427929));
#427474=CARTESIAN_POINT('Ctrl Pts',(-0.640888435961713,2.58419495469807,
13.8582284286032));
#427475=CARTESIAN_POINT('Ctrl Pts',(-0.639816713147,2.5846278881496,13.8579678548414));
#427476=CARTESIAN_POINT('Ctrl Pts',(-0.638778162154673,2.58511549725576,
13.857615680862));
#427477=CARTESIAN_POINT('Ctrl Pts',(-0.637809609004724,2.58562978735214,
13.8571944833187));
#427478=CARTESIAN_POINT('Ctrl Pts',(-0.63539248556353,2.58691325088495,
13.8561433417727));
#427479=CARTESIAN_POINT('Ctrl Pts',(-0.633295996435442,2.58841868548779,
13.8546163505474));
#427480=CARTESIAN_POINT('Ctrl Pts',(-0.631539601917027,2.58994022915956,
13.8528973491086));
#427481=CARTESIAN_POINT('Ctrl Pts',(-0.631218734551702,2.5902181927401,
13.8525833129072));
#427482=CARTESIAN_POINT('Ctrl Pts',(-0.630909086054786,2.59049664194987,
13.8522628768812));
#427483=CARTESIAN_POINT('Ctrl Pts',(-0.630610600565828,2.59077428266382,
13.851937733538));
#427484=CARTESIAN_POINT('Ctrl Pts',(-0.62878779109773,2.59246979598301,
13.8499521282529));
#427485=CARTESIAN_POINT('Ctrl Pts',(-0.627202916742444,2.5943066457283,
13.847639871647));
#427486=CARTESIAN_POINT('Ctrl Pts',(-0.625878444452019,2.59613580997153,
13.8452109780794));
#427487=CARTESIAN_POINT('Ctrl Pts',(-0.625282536953345,2.59695878882638,
13.8441181685877));
#427488=CARTESIAN_POINT('Ctrl Pts',(-0.624738651211423,2.59778001799223,
13.8430021611332));
#427489=CARTESIAN_POINT('Ctrl Pts',(-0.624245527489944,2.59858606088166,
13.8418824960098));
#427490=CARTESIAN_POINT('Ctrl Pts',(-0.623083468847915,2.60048552153364,
13.8392439765549));
#427491=CARTESIAN_POINT('Ctrl Pts',(-0.622144524779294,2.60238947799269,
13.8364981347964));
#427492=CARTESIAN_POINT('Ctrl Pts',(-0.621395520785306,2.60428782992262,
13.8336931113419));
#427493=CARTESIAN_POINT('Ctrl Pts',(-0.620666038461315,2.60613670414588,
13.8309611966328));
#427494=CARTESIAN_POINT('Ctrl Pts',(-0.620116518263491,2.60798232206115,
13.8281701127186));
#427495=CARTESIAN_POINT('Ctrl Pts',(-0.619755612381567,2.60981548820858,
13.8253580685121));
#427496=CARTESIAN_POINT('Ctrl Pts',(-0.619677367596864,2.61021292060776,
13.8247484142933));
#427497=CARTESIAN_POINT('Ctrl Pts',(-0.619608147908461,2.61060970078293,
13.8241378483365));
#427498=CARTESIAN_POINT('Ctrl Pts',(-0.619548319923707,2.61100558037706,
13.8235269408515));
#427499=CARTESIAN_POINT('',(-0.645325162980033,2.58276330623435,12.5969504640361));
#427500=CARTESIAN_POINT('Origin',(-0.653545197073089,2.61617438026271,12.584524458991));
#427501=CARTESIAN_POINT('Origin',(-0.653545197073089,2.61617438026271,12.584524458991));
#427502=CARTESIAN_POINT('Ctrl Pts',(-0.681117813258215,2.59562493167691,
12.5893111709658));
#427503=CARTESIAN_POINT('Ctrl Pts',(-0.67435294727123,2.58653124030664,
12.5770542771492));
#427504=CARTESIAN_POINT('Ctrl Pts',(-0.659632051107227,2.59367958913581,
12.5737548217797));
#427505=CARTESIAN_POINT('Ctrl Pts',(-0.695910304815245,2.61550978277018,
12.5663937883685));
#427506=CARTESIAN_POINT('Ctrl Pts',(-0.689136809302223,2.60640449113366,
12.5540940315304));
#427507=CARTESIAN_POINT('Ctrl Pts',(-0.674371698760894,2.61357787987369,
12.5508374392248));
#427508=CARTESIAN_POINT('Ctrl Pts',(-0.710687870929649,2.63537457029247,
12.5434499600945));
#427509=CARTESIAN_POINT('Ctrl Pts',(-0.703892352370572,2.62623967411034,
12.5311293540533));
#427510=CARTESIAN_POINT('Ctrl Pts',(-0.689097893551968,2.63345602726317,
12.5278936106989));
#427511=CARTESIAN_POINT('Ctrl Pts',(-0.725451680731751,2.65522086585074,
12.5204817579905));
#427512=CARTESIAN_POINT('Ctrl Pts',(-0.718622528999914,2.64604075817535,
12.5081597038247));
#427513=CARTESIAN_POINT('Ctrl Pts',(-0.703811692222104,2.65331558867755,
12.5049254088044));
#427514=CARTESIAN_POINT('Ctrl Pts',(-0.714837180221225,2.64095229173884,
12.5369868989719));
#427515=CARTESIAN_POINT('Ctrl Pts',(-0.715393164532816,2.64169967558667,
12.5342545179733));
#427516=CARTESIAN_POINT('Ctrl Pts',(-0.715823681793893,2.64248740142811,
12.5314872231885));
#427517=CARTESIAN_POINT('Ctrl Pts',(-0.716055427367871,2.64329790441951,
12.5287124745063));
#427518=CARTESIAN_POINT('Ctrl Pts',(-0.716264427029309,2.64402885624694,
12.5262100684184));
#427519=CARTESIAN_POINT('Ctrl Pts',(-0.716310602552072,2.64477786636624,
12.5237004536639));
#427520=CARTESIAN_POINT('Ctrl Pts',(-0.716128581799546,2.64556187466791,
12.5212220730815));
#427521=CARTESIAN_POINT('Ctrl Pts',(-0.715989229167435,2.64616210084496,
12.5193246583486));
#427522=CARTESIAN_POINT('Ctrl Pts',(-0.7157138419125,2.64678987029541,12.517417831369));
#427523=CARTESIAN_POINT('Ctrl Pts',(-0.715207422288142,2.64742445982225,
12.5155812248347));
#427524=CARTESIAN_POINT('Ctrl Pts',(-0.71499168480615,2.64769479837161,
12.5147988205793));
#427525=CARTESIAN_POINT('Ctrl Pts',(-0.714734016959458,2.64796682185866,
12.5140295443047));
#427526=CARTESIAN_POINT('Ctrl Pts',(-0.714427699700277,2.64824096140262,
12.5132817086137));
#427527=CARTESIAN_POINT('Ctrl Pts',(-0.713964129966165,2.64865583451764,
12.5121499604604));
#427528=CARTESIAN_POINT('Ctrl Pts',(-0.713374360014477,2.64907918368906,
12.5110494206568));
#427529=CARTESIAN_POINT('Ctrl Pts',(-0.712628093305165,2.64948935208408,
12.5100666561695));
#427530=CARTESIAN_POINT('Ctrl Pts',(-0.712199588679178,2.64972486983197,
12.5095023550641));
#427531=CARTESIAN_POINT('Ctrl Pts',(-0.711714221219373,2.6499581909934,
12.5089719619137));
#427532=CARTESIAN_POINT('Ctrl Pts',(-0.711178321435369,2.65017918580885,
12.5085043804652));
#427533=CARTESIAN_POINT('Ctrl Pts',(-0.710394101907337,2.65050258293467,
12.5078201359221));
#427534=CARTESIAN_POINT('Ctrl Pts',(-0.709478464436223,2.65080784681095,
12.5072563000949));
#427535=CARTESIAN_POINT('Ctrl Pts',(-0.70849079814604,2.65106625363288,
12.5068768744332));
#427536=CARTESIAN_POINT('Ctrl Pts',(-0.707778622759639,2.65125258274028,
12.5066032824114));
#427537=CARTESIAN_POINT('Ctrl Pts',(-0.707016500041307,2.65141788060135,
12.5064197834844));
#427538=CARTESIAN_POINT('Ctrl Pts',(-0.706247536796213,2.65155544267816,
12.5063282718343));
#427539=CARTESIAN_POINT('Ctrl Pts',(-0.705125088523378,2.65175624072215,
12.5061946931565));
#427540=CARTESIAN_POINT('Ctrl Pts',(-0.703964261217886,2.65190327965168,
12.5062515701262));
#427541=CARTESIAN_POINT('Ctrl Pts',(-0.702839041189455,2.65200277591458,
12.5064436508398));
#427542=CARTESIAN_POINT('',(-0.659632051107227,2.59367958913581,12.5737548217797));
#427543=CARTESIAN_POINT('Origin',(-0.663466328551192,2.6087560050389,12.5893111709658));
#427544=CARTESIAN_POINT('Ctrl Pts',(-0.702839041189455,2.65200277591458,
12.5064436508398));
#427545=CARTESIAN_POINT('Ctrl Pts',(-0.696442898066279,2.64336971499165,
12.5164271754438));
#427546=CARTESIAN_POINT('Ctrl Pts',(-0.690044387393246,2.63473310754498,
12.5264061185523));
#427547=CARTESIAN_POINT('Ctrl Pts',(-0.68364342502673,2.62609282923241,
12.536380305637));
#427548=CARTESIAN_POINT('Ctrl Pts',(-0.675643520323638,2.61529423377897,
12.5488460165097));
#427549=CARTESIAN_POINT('Ctrl Pts',(-0.66763978374881,2.60448990125433,
12.5613043021964));
#427550=CARTESIAN_POINT('Ctrl Pts',(-0.659632051107227,2.59367958913581,
12.5737548217797));
#427551=CARTESIAN_POINT('Ctrl Pts',(-0.619548319923707,2.61100558037706,
12.5893111709658));
#427552=CARTESIAN_POINT('Ctrl Pts',(-0.621241952538985,2.59979887510191,
12.5770542771492));
#427553=CARTESIAN_POINT('Ctrl Pts',(-0.637595128669095,2.59918462327036,
12.5737548217797));
#427554=CARTESIAN_POINT('Ctrl Pts',(-0.621128464423323,2.60054982182612,
12.5928319619712));
#427555=CARTESIAN_POINT('Ctrl Pts',(-0.625487855889913,2.59350502783251,
12.5821634970842));
#427556=CARTESIAN_POINT('Ctrl Pts',(-0.638161404184726,2.59537443306385,
12.5773203894503));
#427557=CARTESIAN_POINT('Ctrl Pts',(-0.630311597441073,2.58654074736283,
12.5969440695591));
#427558=CARTESIAN_POINT('Ctrl Pts',(-0.634207051578876,2.58554878989792,
12.5878292599214));
#427559=CARTESIAN_POINT('Ctrl Pts',(-0.641436171293958,2.59038243471871,
12.5813877129824));
#427560=CARTESIAN_POINT('Ctrl Pts',(-0.659983243458332,2.57907290509295,
12.596957478804));
#427561=CARTESIAN_POINT('Ctrl Pts',(-0.656116597551942,2.58005760940567,
12.5878468778671));
#427562=CARTESIAN_POINT('Ctrl Pts',(-0.652057520626844,2.58771537516689,
12.5814011370086));
#427563=CARTESIAN_POINT('Ctrl Pts',(-0.674797087754222,2.58712827748144,
12.5928371701607));
#427564=CARTESIAN_POINT('Ctrl Pts',(-0.667638948597393,2.58296941832113,
12.5821692192952));
#427565=CARTESIAN_POINT('Ctrl Pts',(-0.657333350697047,2.59057326431407,
12.5773318885715));
#427566=CARTESIAN_POINT('Ctrl Pts',(-0.681117813258257,2.59562493167688,
12.5893111709658));
#427567=CARTESIAN_POINT('Ctrl Pts',(-0.674352947271273,2.5865312403066,
12.5770542771492));
#427568=CARTESIAN_POINT('Ctrl Pts',(-0.659632051107271,2.59367958913578,
12.5737548217797));
#427569=CARTESIAN_POINT('',(-0.637595128669095,2.59918462327036,12.5737548217797));
#427570=CARTESIAN_POINT('Origin',(-0.641301310950769,2.61429303857095,12.5893111709658));
#427571=CARTESIAN_POINT('Ctrl Pts',(-0.659632051107271,2.59367958913578,
12.5737548217797));
#427572=CARTESIAN_POINT('Ctrl Pts',(-0.65906043991165,2.59285643649376,
12.5746934679442));
#427573=CARTESIAN_POINT('Ctrl Pts',(-0.658277450054665,2.59205004805008,
12.5756680099006));
#427574=CARTESIAN_POINT('Ctrl Pts',(-0.657374552621003,2.59134984815557,
12.5765688348656));
#427575=CARTESIAN_POINT('Ctrl Pts',(-0.657135520520848,2.59116447798497,
12.5768073183026));
#427576=CARTESIAN_POINT('Ctrl Pts',(-0.656888286740824,2.59098639152223,
12.5770407398754));
#427577=CARTESIAN_POINT('Ctrl Pts',(-0.656634889972081,2.59081680018845,
12.5772674179684));
#427578=CARTESIAN_POINT('Ctrl Pts',(-0.655595018154532,2.59012084321406,
12.5781976435658));
#427579=CARTESIAN_POINT('Ctrl Pts',(-0.654386021859309,2.58953779481049,
12.5790594849312));
#427580=CARTESIAN_POINT('Ctrl Pts',(-0.653068558396651,2.58915051874844,
12.5797571720116));
#427581=CARTESIAN_POINT('Ctrl Pts',(-0.652210183578965,2.58889819446881,
12.580211740231));
#427582=CARTESIAN_POINT('Ctrl Pts',(-0.651261461391678,2.58873551935799,
12.5806009430798));
#427583=CARTESIAN_POINT('Ctrl Pts',(-0.650286183608314,2.58869140689267,
12.5808812374708));
#427584=CARTESIAN_POINT('Ctrl Pts',(-0.649448096447365,2.58865349965081,
12.5811221033394));
#427585=CARTESIAN_POINT('Ctrl Pts',(-0.648573236243005,2.5887024830718,
12.581287365893));
#427586=CARTESIAN_POINT('Ctrl Pts',(-0.647711447628746,2.58884391739505,
12.581359338449));
#427587=CARTESIAN_POINT('Ctrl Pts',(-0.647591676806622,2.58886357384547,
12.5813693411482));
#427588=CARTESIAN_POINT('Ctrl Pts',(-0.647472129629909,2.58888496353217,
12.5813775999465));
#427589=CARTESIAN_POINT('Ctrl Pts',(-0.647352909413546,2.58890804815248,
12.5813841266931));
#427590=CARTESIAN_POINT('Ctrl Pts',(-0.647150637897095,2.58894721400287,
12.5813952001081));
#427591=CARTESIAN_POINT('Ctrl Pts',(-0.646948068571554,2.58899211884071,
12.5814007534795));
#427592=CARTESIAN_POINT('Ctrl Pts',(-0.646745332343135,2.58904293564436,
12.5814005856065));
#427593=CARTESIAN_POINT('Ctrl Pts',(-0.645817285154161,2.58927555510339,
12.5813998171494));
#427594=CARTESIAN_POINT('Ctrl Pts',(-0.64494977947355,2.58961565728625,
12.58127954464));
#427595=CARTESIAN_POINT('Ctrl Pts',(-0.644136940372809,2.59003376337738,
12.5810700125799));
#427596=CARTESIAN_POINT('Ctrl Pts',(-0.643155123288255,2.59053878793026,
12.5808169217085));
#427597=CARTESIAN_POINT('Ctrl Pts',(-0.642260630638001,2.59117254755197,
12.5804173076348));
#427598=CARTESIAN_POINT('Ctrl Pts',(-0.641516798766718,2.59185825121603,
12.5799304713245));
#427599=CARTESIAN_POINT('Ctrl Pts',(-0.640594956746993,2.59270805407474,
12.5793271277669));
#427600=CARTESIAN_POINT('Ctrl Pts',(-0.639825506148532,2.59366667735055,
12.5785808224116));
#427601=CARTESIAN_POINT('Ctrl Pts',(-0.639216146240733,2.59467385974008,
12.5777485681082));
#427602=CARTESIAN_POINT('Ctrl Pts',(-0.638308133217751,2.59617467184554,
12.576508418016));
#427603=CARTESIAN_POINT('Ctrl Pts',(-0.637757355590619,2.59776711133143,
12.5750928681475));
#427604=CARTESIAN_POINT('Ctrl Pts',(-0.637595128669095,2.59918462327036,
12.5737548217797));
#427605=CARTESIAN_POINT('Ctrl Pts',(-0.637595128669095,2.59918462327036,
12.5737548217797));
#427606=CARTESIAN_POINT('Ctrl Pts',(-0.621241952538985,2.59979887510191,
12.5770542771492));
#427607=CARTESIAN_POINT('Ctrl Pts',(-0.619548319923707,2.61100558037706,
12.5893111709658));
#427608=CARTESIAN_POINT('Ctrl Pts',(-0.633945227133948,2.62367325681644,
12.5508408821982));
#427609=CARTESIAN_POINT('Ctrl Pts',(-0.617541263428884,2.62428620003755,
12.55409748406));
#427610=CARTESIAN_POINT('Ctrl Pts',(-0.615845470172143,2.63550720219847,
12.5663972313419));
#427611=CARTESIAN_POINT('Ctrl Pts',(-0.630297724466514,2.64813779417324,
12.52790050457));
#427612=CARTESIAN_POINT('Ctrl Pts',(-0.613847662019243,2.64872662591756,
12.5311362602938));
#427613=CARTESIAN_POINT('Ctrl Pts',(-0.612146355987524,2.65998410590958,
12.5434568539655));
#427614=CARTESIAN_POINT('Ctrl Pts',(-0.626652420547208,2.6725801058825,
12.5049357605811));
#427615=CARTESIAN_POINT('Ctrl Pts',(-0.61016040945356,2.67312504172859,
12.5081700652078));
#427616=CARTESIAN_POINT('Ctrl Pts',(-0.608450684799481,2.68443822743786,
12.5204921097672));
#427617=CARTESIAN_POINT('Ctrl Pts',(-0.626891783921935,2.67097512765063,
12.5064436508395));
#427618=CARTESIAN_POINT('Ctrl Pts',(-0.625768588916643,2.67145186738117,
12.5062361689309));
#427619=CARTESIAN_POINT('Ctrl Pts',(-0.62458022878413,2.67189974215819,
12.5061871075061));
#427620=CARTESIAN_POINT('Ctrl Pts',(-0.623407428471871,2.67226792155561,
12.5063648335164));
#427621=CARTESIAN_POINT('Ctrl Pts',(-0.62287467022872,2.67243517134816,
12.5064455676329));
#427622=CARTESIAN_POINT('Ctrl Pts',(-0.622337625953831,2.67258809829308,
12.506574497099));
#427623=CARTESIAN_POINT('Ctrl Pts',(-0.621819034671932,2.67271913457354,
12.5067492519495));
#427624=CARTESIAN_POINT('Ctrl Pts',(-0.620776905360758,2.67298245706555,
12.5071004286051));
#427625=CARTESIAN_POINT('Ctrl Pts',(-0.619770780414712,2.67316627753478,
12.5076537929612));
#427626=CARTESIAN_POINT('Ctrl Pts',(-0.618877874720707,2.673266103723,12.5083435010503));
#427627=CARTESIAN_POINT('Ctrl Pts',(-0.618821660971136,2.67327238837813,
12.5083869222963));
#427628=CARTESIAN_POINT('Ctrl Pts',(-0.618765888504668,2.67327832895009,
12.5084308732336));
#427629=CARTESIAN_POINT('Ctrl Pts',(-0.618710573223093,2.67328391998674,
12.5084753333615));
#427630=CARTESIAN_POINT('Ctrl Pts',(-0.618266871656053,2.67332876748015,
12.508831962269));
#427631=CARTESIAN_POINT('Ctrl Pts',(-0.61784370794673,2.67335331934408,
12.509227847131));
#427632=CARTESIAN_POINT('Ctrl Pts',(-0.617453827143522,2.67335964087574,
12.5096423454524));
#427633=CARTESIAN_POINT('Ctrl Pts',(-0.616232113260281,2.67337944975814,
12.5109411997424));
#427634=CARTESIAN_POINT('Ctrl Pts',(-0.615262223814655,2.67323113740892,
12.5124831113042));
#427635=CARTESIAN_POINT('Ctrl Pts',(-0.614493472563127,2.67299462104848,
12.5140723025008));
#427636=CARTESIAN_POINT('Ctrl Pts',(-0.614421439728871,2.67297245920645,
12.5142212114565));
#427637=CARTESIAN_POINT('Ctrl Pts',(-0.614351149231337,2.67294954077451,
12.5143705582413));
#427638=CARTESIAN_POINT('Ctrl Pts',(-0.614282546802396,2.67292594291943,
12.5145201959299));
#427639=CARTESIAN_POINT('Ctrl Pts',(-0.613401246464292,2.67262279333733,
12.5164425148273));
#427640=CARTESIAN_POINT('Ctrl Pts',(-0.612764842494584,2.67220728429206,
12.5184635205941));
#427641=CARTESIAN_POINT('Ctrl Pts',(-0.612292447645065,2.6717193561345,
12.5205025929158));
#427642=CARTESIAN_POINT('Ctrl Pts',(-0.612018439908361,2.67143633846346,
12.5216853356836));
#427643=CARTESIAN_POINT('Ctrl Pts',(-0.611799759939447,2.67112980326851,
12.5228750347131));
#427644=CARTESIAN_POINT('Ctrl Pts',(-0.61162354841163,2.67081269548555,
12.5240609649613));
#427645=CARTESIAN_POINT('Ctrl Pts',(-0.611191046670025,2.67003437144451,
12.5269717671326));
#427646=CARTESIAN_POINT('Ctrl Pts',(-0.611011302518143,2.66916540019756,
12.5299036066169));
#427647=CARTESIAN_POINT('Ctrl Pts',(-0.611003381232721,2.66823675097456,
12.5328133004019));
#427648=CARTESIAN_POINT('Ctrl Pts',(-0.610999578554476,2.66779094527389,
12.5342101228451));
#427649=CARTESIAN_POINT('Ctrl Pts',(-0.611035902273964,2.66733193819979,
12.5356023438238));
#427650=CARTESIAN_POINT('Ctrl Pts',(-0.611106435078542,2.66686522465476,
12.5369868989719));
#427651=CARTESIAN_POINT('Origin',(1.29852573867523,15.2673948607278,-1.23905631314464));
#427652=CARTESIAN_POINT('Ctrl Pts',(-0.714812266465859,2.64091873483605,
12.5369868989719));
#427653=CARTESIAN_POINT('Ctrl Pts',(-0.723944180760299,2.65324315956923,
12.5369868989719));
#427654=CARTESIAN_POINT('Ctrl Pts',(-0.738666032852597,2.64893614498169,
12.5369868989719));
#427655=CARTESIAN_POINT('Ctrl Pts',(-0.717899263843912,2.64508483298256,
12.5218025310015));
#427656=CARTESIAN_POINT('Ctrl Pts',(-0.727316801397066,2.65222387004222,
12.5216901060417));
#427657=CARTESIAN_POINT('Ctrl Pts',(-0.738621160399221,2.6489492900178,
12.5161920673678));
#427658=CARTESIAN_POINT('Ctrl Pts',(-0.716058773267108,2.65082492580684,
12.5042015548895));
#427659=CARTESIAN_POINT('Ctrl Pts',(-0.721817661437463,2.65369068086588,
12.4980677368514));
#427660=CARTESIAN_POINT('Ctrl Pts',(-0.728374159597134,2.65190095697487,
12.4907278922777));
#427661=CARTESIAN_POINT('Ctrl Pts',(-0.702833917340125,2.65198344227881,
12.506463626192));
#427662=CARTESIAN_POINT('Ctrl Pts',(-0.704510023850558,2.65830784780834,
12.4999376786891));
#427663=CARTESIAN_POINT('Ctrl Pts',(-0.70448955264659,2.65823060439047,
12.4906970594712));
#427664=CARTESIAN_POINT('Origin',(-0.732488664928249,2.62782121837686,12.5369868989719));
#427665=CARTESIAN_POINT('Origin',(-0.732488664928249,2.62782121837686,14.));
#427666=CARTESIAN_POINT('Origin',(-0.732488664928249,2.62782121837686,13.7435492065112));
#427667=CARTESIAN_POINT('Ctrl Pts',(-0.700058713744277,2.62108624841145,
13.793642941384));
#427668=CARTESIAN_POINT('Ctrl Pts',(-0.706490367527905,2.62977762624316,
13.8071662555867));
#427669=CARTESIAN_POINT('Ctrl Pts',(-0.721520360485517,2.62177021122151,
13.8103758687955));
#427670=CARTESIAN_POINT('Ctrl Pts',(-0.709979310257147,2.63442204497754,
13.7804579775006));
#427671=CARTESIAN_POINT('Ctrl Pts',(-0.717923541283087,2.64514038743966,
13.7901904343351));
#427672=CARTESIAN_POINT('Ctrl Pts',(-0.732844745003035,2.64007939902705,
13.7927914348262));
#427673=CARTESIAN_POINT('Ctrl Pts',(-0.715819938808819,2.64227333027577,
13.7597120340895));
#427674=CARTESIAN_POINT('Ctrl Pts',(-0.725018255081397,2.65467405879156,
13.7635825532445));
#427675=CARTESIAN_POINT('Ctrl Pts',(-0.739544461666612,2.65086285971679,
13.7651073818885));
#427676=CARTESIAN_POINT('Ctrl Pts',(-0.714676210003871,2.64073586883991,
13.7381884353898));
#427677=CARTESIAN_POINT('Ctrl Pts',(-0.723658500634108,2.65284687068369,
13.7368803041982));
#427678=CARTESIAN_POINT('Ctrl Pts',(-0.738232877867184,2.64875087686204,
13.7363986145813));
#427679=CARTESIAN_POINT('Origin',(-0.720117392276629,2.61119109805107,13.7902182540695));
#427680=CARTESIAN_POINT('Ctrl Pts',(-0.681115464480307,2.59562177305366,
13.8235227101244));
#427681=CARTESIAN_POINT('Ctrl Pts',(-0.68797413001214,2.60484898256911,
13.8358800583119));
#427682=CARTESIAN_POINT('Ctrl Pts',(-0.702832413857604,2.597510219034,13.8390832900376));
#427683=CARTESIAN_POINT('Ctrl Pts',(-0.688234642642779,2.60519174962549,
13.8124254819053));
#427684=CARTESIAN_POINT('Ctrl Pts',(-0.69510662782911,2.61443687808509,
13.8247886449157));
#427685=CARTESIAN_POINT('Ctrl Pts',(-0.709976137757826,2.60707355983978,
13.8279860620657));
#427686=CARTESIAN_POINT('Ctrl Pts',(-0.695350630221196,2.61475743724518,
13.8013225099955));
#427687=CARTESIAN_POINT('Ctrl Pts',(-0.702232690979661,2.62401612362875,
13.8136962257787));
#427688=CARTESIAN_POINT('Ctrl Pts',(-0.717116337306965,2.6166326355042,
13.8168830918626));
#427689=CARTESIAN_POINT('Ctrl Pts',(-0.702463551356287,2.62431900278925,
13.7902140179785));
#427690=CARTESIAN_POINT('Ctrl Pts',(-0.709352655631513,2.63358717109964,
13.802602731458));
#427691=CARTESIAN_POINT('Ctrl Pts',(-0.724253149510978,2.62618761471636,
13.8057746032558));
#427692=CARTESIAN_POINT('Origin',(-0.698769297965238,2.58249385831493,13.8235269408515));
#427693=CARTESIAN_POINT('Ctrl Pts',(-0.619548319923707,2.61100558037706,
13.8235269408515));
#427694=CARTESIAN_POINT('Ctrl Pts',(-0.617783928936189,2.62268049122187,
13.8362179249168));
#427695=CARTESIAN_POINT('Ctrl Pts',(-0.600707111582438,2.6228933600169,
13.8391868794938));
#427696=CARTESIAN_POINT('Ctrl Pts',(-0.621162660877916,2.60032354513268,
13.8400110824519));
#427697=CARTESIAN_POINT('Ctrl Pts',(-0.616365462025495,2.6091727680382,
13.8494522556837));
#427698=CARTESIAN_POINT('Ctrl Pts',(-0.603474956463533,2.60533053512058,
13.85569149686));
#427699=CARTESIAN_POINT('Ctrl Pts',(-0.629977800041478,2.58662350690017,
13.8586819406588));
#427700=CARTESIAN_POINT('Ctrl Pts',(-0.625757144509834,2.58769220260906,
13.868010383617));
#427701=CARTESIAN_POINT('Ctrl Pts',(-0.618231041938688,2.58266720043183,
13.8744918421245));
#427702=CARTESIAN_POINT('Ctrl Pts',(-0.660322213356513,2.57898884394015,
13.8587686893867));
#427703=CARTESIAN_POINT('Ctrl Pts',(-0.664505291271827,2.57792960502741,
13.8680909899357));
#427704=CARTESIAN_POINT('Ctrl Pts',(-0.66874620679676,2.56996022380826,
13.8745789365163));
#427705=CARTESIAN_POINT('Ctrl Pts',(-0.674659168776717,2.58694287947182,
13.8400379222776));
#427706=CARTESIAN_POINT('Ctrl Pts',(-0.683056149301072,2.59248913514406,
13.8494748685453));
#427707=CARTESIAN_POINT('Ctrl Pts',(-0.692621784022613,2.58304139797377,
13.8557104837033));
#427708=CARTESIAN_POINT('Ctrl Pts',(-0.681117813263431,2.59562493167285,
13.8235269408542));
#427709=CARTESIAN_POINT('Ctrl Pts',(-0.688165308966787,2.60509854888603,
13.8362179249195));
#427710=CARTESIAN_POINT('Ctrl Pts',(-0.703336074958441,2.59725566272831,
13.8391868794965));
#427711=CARTESIAN_POINT('Origin',(-0.597795328896645,2.60771812218317,13.8235269408515));
#427712=CARTESIAN_POINT('Ctrl Pts',(-0.614204260161081,2.64636702392679,
13.7902140241682));
#427713=CARTESIAN_POINT('Ctrl Pts',(-0.612483030422494,2.65778612912728,
13.8026027327198));
#427714=CARTESIAN_POINT('Ctrl Pts',(-0.595853226194454,2.65826314444243,
13.8057746032556));
#427715=CARTESIAN_POINT('Ctrl Pts',(-0.615985030875118,2.63458372903589,
13.8013225161807));
#427716=CARTESIAN_POINT('Ctrl Pts',(-0.614265558119394,2.64599115386919,
13.8136962270464));
#427717=CARTESIAN_POINT('Ctrl Pts',(-0.597658178658661,2.64647442683644,
13.8168830918628));
#427718=CARTESIAN_POINT('Ctrl Pts',(-0.617766569295444,2.62279535426053,
13.8124254880876));
#427719=CARTESIAN_POINT('Ctrl Pts',(-0.616049612549406,2.63418607568515,
13.8247886461868));
#427720=CARTESIAN_POINT('Ctrl Pts',(-0.599464194081469,2.63468050105057,
13.8279860620656));
#427721=CARTESIAN_POINT('Ctrl Pts',(-0.619548906501818,2.61100169394711,
13.8235227163065));
#427722=CARTESIAN_POINT('Ctrl Pts',(-0.617835277872275,2.62237033767259,
13.8358800595847));
#427723=CARTESIAN_POINT('Ctrl Pts',(-0.601271314044096,2.62288115378159,
13.8390832900376));
#427724=CARTESIAN_POINT('Origin',(-0.592450680699715,2.643083464467,13.7902182540695));
#427725=CARTESIAN_POINT('Ctrl Pts',(-0.611146732946785,2.6665983905316,
13.7382347919292));
#427726=CARTESIAN_POINT('Ctrl Pts',(-0.608915520826138,2.68152285237136,
13.7369371795942));
#427727=CARTESIAN_POINT('Ctrl Pts',(-0.594113895786784,2.68475637571517,
13.7364597369711));
#427728=CARTESIAN_POINT('Ctrl Pts',(-0.61086407789628,2.66846871138821,
13.7595490285574));
#427729=CARTESIAN_POINT('Ctrl Pts',(-0.608578636593199,2.68374910943501,
13.7633824266926));
#427730=CARTESIAN_POINT('Ctrl Pts',(-0.593951987877943,2.68720668194595,
13.7648920890506));
#427731=CARTESIAN_POINT('Ctrl Pts',(-0.612305603176639,2.6589301774852,
13.780380659011));
#427732=CARTESIAN_POINT('Ctrl Pts',(-0.610334117319525,2.67214797342552,
13.7901039518743));
#427733=CARTESIAN_POINT('Ctrl Pts',(-0.594781116764188,2.67471499799725,
13.7926933640891));
#427734=CARTESIAN_POINT('Ctrl Pts',(-0.614811295826587,2.64235007628175,
13.7936647693663));
#427735=CARTESIAN_POINT('Ctrl Pts',(-0.613224791711657,2.65304850311181,
13.8072068914933));
#427736=CARTESIAN_POINT('Ctrl Pts',(-0.596176501848199,2.65303941580986,
13.8104111085397));
#427737=CARTESIAN_POINT('Origin',(-0.58935344405148,2.66357776646087,13.7435492065112));
#427738=CARTESIAN_POINT('Origin',(-0.58935344405148,2.66357776646087,14.));
#427739=CARTESIAN_POINT('Origin',(-0.58935344405148,2.66357776646087,12.5369868989719));
#427740=CARTESIAN_POINT('Ctrl Pts',(-0.626887583435017,2.67095723074299,
12.506462012331));
#427741=CARTESIAN_POINT('Ctrl Pts',(-0.628381632903502,2.67732287322241,
12.4999388158272));
#427742=CARTESIAN_POINT('Ctrl Pts',(-0.628363956338964,2.67724755932385,
12.4907030323752));
#427743=CARTESIAN_POINT('Ctrl Pts',(-0.614671118545729,2.67615209058353,
12.5042014951932));
#427744=CARTESIAN_POINT('Ctrl Pts',(-0.610938873572858,2.68138768458791,
12.4980716682126));
#427745=CARTESIAN_POINT('Ctrl Pts',(-0.604315993474235,2.68289201979826,
12.4907355092743));
#427746=CARTESIAN_POINT('Ctrl Pts',(-0.610346422437987,2.67195415003824,
12.521804744651));
#427747=CARTESIAN_POINT('Ctrl Pts',(-0.605393940295253,2.68267757260581,
12.5216906929435));
#427748=CARTESIAN_POINT('Ctrl Pts',(-0.593884274181701,2.68510622249523,
12.5161988840776));
#427749=CARTESIAN_POINT('Ctrl Pts',(-0.61111214243078,2.6668272348541,12.5369868989719));
#427750=CARTESIAN_POINT('Ctrl Pts',(-0.608847870000681,2.68198898283656,
12.5369868989719));
#427751=CARTESIAN_POINT('Ctrl Pts',(-0.593840168678727,2.68511539172735,
12.5369868989719));
#427752=CARTESIAN_POINT('Origin',(-1.24861436930108E-31,-1.53597860469562E-32,
12.5));
#427753=CARTESIAN_POINT('Origin',(-0.830308018192218,2.55181873502139,12.5));
#427754=CARTESIAN_POINT('',(-0.830308018192218,2.55181873502139,12.5893111709658));
#427755=CARTESIAN_POINT('',(-0.830308018192218,2.55181873502139,13.8235269408515));
#427756=CARTESIAN_POINT('',(-0.830308018192218,2.55181873502139,12.5));
#427757=CARTESIAN_POINT('',(-0.827863757583213,2.58750204049155,13.7902182540695));
#427758=CARTESIAN_POINT('',(-0.830308018192218,2.55181873502139,13.8235269408515));
#427759=CARTESIAN_POINT('',(-0.826447302606738,2.60818060292636,13.7435492065112));
#427760=CARTESIAN_POINT('Origin',(-0.831107745750198,2.54014842810589,13.7445212918695));
#427761=CARTESIAN_POINT('',(-0.826447302606738,2.60818060292636,12.5369868989719));
#427762=CARTESIAN_POINT('',(-0.826447302606738,2.60818060292636,12.5));
#427763=CARTESIAN_POINT('Ctrl Pts',(-0.826447302606738,2.60818060292636,
12.5369868989719));
#427764=CARTESIAN_POINT('Ctrl Pts',(-0.82773326921152,2.58940701593085,
12.5544431401645));
#427765=CARTESIAN_POINT('Ctrl Pts',(-0.829020155573796,2.57062000156695,
12.5718848856037));
#427766=CARTESIAN_POINT('Ctrl Pts',(-0.830308018192218,2.55181873502139,
12.5893111709658));
#427767=CARTESIAN_POINT('Origin',(-1.07199573684347,2.73800135969425,12.5));
#427768=CARTESIAN_POINT('',(-0.927720747655564,2.57389887443867,13.7435492065112));
#427769=CARTESIAN_POINT('',(-0.914035130200078,2.55833246303678,13.7902182540695));
#427770=CARTESIAN_POINT('Origin',(-0.878071692878184,2.5174266242904,13.7418732680452));
#427771=CARTESIAN_POINT('',(-0.890418978460743,2.53147077887092,13.8235269408515));
#427772=CARTESIAN_POINT('',(-0.914035130200078,2.55833246303678,13.7902182540695));
#427773=CARTESIAN_POINT('',(-0.890418978460743,2.53147077887092,12.5893111709658));
#427774=CARTESIAN_POINT('',(-0.890418978460743,2.53147077887092,12.5));
#427775=CARTESIAN_POINT('',(-0.927720747655564,2.57389887443867,12.5369868989719));
#427776=CARTESIAN_POINT('Ctrl Pts',(-0.890418978460743,2.53147077887092,
12.5893111709658));
#427777=CARTESIAN_POINT('Ctrl Pts',(-0.90286215203397,2.54562399918532,
12.5718848856037));
#427778=CARTESIAN_POINT('Ctrl Pts',(-0.915295893137859,2.55976649074021,
12.5544431401645));
#427779=CARTESIAN_POINT('Ctrl Pts',(-0.927720747655564,2.57389887443867,
12.5369868989719));
#427780=CARTESIAN_POINT('',(-0.927720747655564,2.57389887443867,12.5));
#427781=CARTESIAN_POINT('Origin',(-0.864602655857827,2.55416787366877,12.5));
#427782=CARTESIAN_POINT('',(-0.852526491536523,2.52198470372759,13.8587068136939));
#427783=CARTESIAN_POINT('Ctrl Pts',(-0.890418978465611,2.53147077886645,
13.8235269408542));
#427784=CARTESIAN_POINT('Ctrl Pts',(-0.889261972465776,2.53015476726184,
13.8262006681044));
#427785=CARTESIAN_POINT('Ctrl Pts',(-0.88794746410894,2.52892273811777,
13.8288634856214));
#427786=CARTESIAN_POINT('Ctrl Pts',(-0.886487836020826,2.52776974404823,
13.8314912288862));
#427787=CARTESIAN_POINT('Ctrl Pts',(-0.884983110015638,2.52658112608835,
13.8342001611531));
#427788=CARTESIAN_POINT('Ctrl Pts',(-0.883322794878828,2.52547479235028,
13.8368750301949));
#427789=CARTESIAN_POINT('Ctrl Pts',(-0.881479791125753,2.52446505660073,
13.8394886372969));
#427790=CARTESIAN_POINT('Ctrl Pts',(-0.881337451475401,2.52438707225952,
13.8396904925131));
#427791=CARTESIAN_POINT('Ctrl Pts',(-0.881194008285796,2.52430968141073,
13.8398919674349));
#427792=CARTESIAN_POINT('Ctrl Pts',(-0.881049442739693,2.52423290018035,
13.8400930404591));
#427793=CARTESIAN_POINT('Ctrl Pts',(-0.878797014272475,2.52303659695519,
13.8432258934518));
#427794=CARTESIAN_POINT('Ctrl Pts',(-0.876284146749888,2.52199339338113,
13.8462331177034));
#427795=CARTESIAN_POINT('Ctrl Pts',(-0.873555809539721,2.52122640702453,
13.8489036603661));
#427796=CARTESIAN_POINT('Ctrl Pts',(-0.872663065853298,2.52097544016277,
13.8497774930041));
#427797=CARTESIAN_POINT('Ctrl Pts',(-0.871747416628582,2.52075423556561,
13.85061494757));
#427798=CARTESIAN_POINT('Ctrl Pts',(-0.870810915391224,2.52056763664275,
13.8514076489583));
#427799=CARTESIAN_POINT('Ctrl Pts',(-0.868830080210522,2.52017295300931,
13.8530843267192));
#427800=CARTESIAN_POINT('Ctrl Pts',(-0.866560808400721,2.51989722205296,
13.8546805203176));
#427801=CARTESIAN_POINT('Ctrl Pts',(-0.864118349705672,2.51989189659498,
13.8559412814273));
#427802=CARTESIAN_POINT('Ctrl Pts',(-0.863791469521455,2.519891183876,13.8561100121513));
#427803=CARTESIAN_POINT('Ctrl Pts',(-0.863461537269772,2.51989525601575,
13.8562727473908));
#427804=CARTESIAN_POINT('Ctrl Pts',(-0.863128870882547,2.51990441268198,
13.8564289040185));
#427805=CARTESIAN_POINT('Ctrl Pts',(-0.861620232611703,2.51994593805888,
13.8571370725437));
#427806=CARTESIAN_POINT('Ctrl Pts',(-0.860028908766775,2.52009503789213,
13.8577210840553));
#427807=CARTESIAN_POINT('Ctrl Pts',(-0.8584194921764,2.5203751367083,13.8581177131616));
#427808=CARTESIAN_POINT('Ctrl Pts',(-0.857966225070116,2.52045402217564,
13.8582294175695));
#427809=CARTESIAN_POINT('Ctrl Pts',(-0.857511527303881,2.52054312065629,
13.8583265086086));
#427810=CARTESIAN_POINT('Ctrl Pts',(-0.857056826485769,2.52064251610535,
13.8584082369006));
#427811=CARTESIAN_POINT('Ctrl Pts',(-0.856403543342984,2.52078532071172,
13.8585256585398));
#427812=CARTESIAN_POINT('Ctrl Pts',(-0.85574220110369,2.52095147158689,
13.8586122832068));
#427813=CARTESIAN_POINT('Ctrl Pts',(-0.855090171938288,2.52113741849891,
13.8586682984299));
#427814=CARTESIAN_POINT('Ctrl Pts',(-0.854568613239538,2.52128615759619,
13.8587131050557));
#427815=CARTESIAN_POINT('Ctrl Pts',(-0.854047188505169,2.52144898034998,
13.8587357943552));
#427816=CARTESIAN_POINT('Ctrl Pts',(-0.853525986732354,2.52162638953292,
13.8587355499465));
#427817=CARTESIAN_POINT('Ctrl Pts',(-0.853189121600519,2.5217410533175,
13.8587353919793));
#427818=CARTESIAN_POINT('Ctrl Pts',(-0.852855979960392,2.52186053378845,
13.8587257282814));
#427819=CARTESIAN_POINT('Ctrl Pts',(-0.852526491536523,2.52198470372759,
13.8587068136939));
#427820=CARTESIAN_POINT('Ctrl Pts',(-0.852526491536523,2.52198470372759,
13.8587068136939));
#427821=CARTESIAN_POINT('Ctrl Pts',(-0.851442822072846,2.52239309188814,
13.8586446046466));
#427822=CARTESIAN_POINT('Ctrl Pts',(-0.850398620603542,2.52285214451888,
13.858482427929));
#427823=CARTESIAN_POINT('Ctrl Pts',(-0.849391811864,2.52335790191855,13.8582284286032));
#427824=CARTESIAN_POINT('Ctrl Pts',(-0.848358943213999,2.52387675017852,
13.8579678548414));
#427825=CARTESIAN_POINT('Ctrl Pts',(-0.847363592583318,2.52444738835292,
13.857615680862));
#427826=CARTESIAN_POINT('Ctrl Pts',(-0.846440181631368,2.52503891326476,
13.8571944833187));
#427827=CARTESIAN_POINT('Ctrl Pts',(-0.84413571516204,2.52651512417848,
13.8561433417727));
#427828=CARTESIAN_POINT('Ctrl Pts',(-0.842168908824479,2.52818643289867,
13.8546163505474));
#427829=CARTESIAN_POINT('Ctrl Pts',(-0.8405423784985,2.52984607621821,13.8528973491086));
#427830=CARTESIAN_POINT('Ctrl Pts',(-0.840245235405169,2.53014926856692,
13.8525833129072));
#427831=CARTESIAN_POINT('Ctrl Pts',(-0.839959313433678,2.53045203048706,
13.8522628768812));
#427832=CARTESIAN_POINT('Ctrl Pts',(-0.839684451426241,2.53075307671278,
13.851937733538));
#427833=CARTESIAN_POINT('Ctrl Pts',(-0.838005907282168,2.53259152424506,
13.8499521282529));
#427834=CARTESIAN_POINT('Ctrl Pts',(-0.836576026772279,2.53455144399757,
13.847639871647));
#427835=CARTESIAN_POINT('Ctrl Pts',(-0.835405055421095,2.53648247863514,
13.8452109780794));
#427836=CARTESIAN_POINT('Ctrl Pts',(-0.834878211172296,2.53735129108902,
13.8441181685877));
#427837=CARTESIAN_POINT('Ctrl Pts',(-0.83440307296625,2.53821411941972,
13.8430021611332));
#427838=CARTESIAN_POINT('Ctrl Pts',(-0.8339772900517,2.53905767442917,13.8418824960098));
#427839=CARTESIAN_POINT('Ctrl Pts',(-0.832973921740808,2.54104553334987,
13.8392439765549));
#427840=CARTESIAN_POINT('Ctrl Pts',(-0.832193292058001,2.54301968720919,
13.8364981347964));
#427841=CARTESIAN_POINT('Ctrl Pts',(-0.831601513618745,2.5449727733086,
13.8336931113419));
#427842=CARTESIAN_POINT('Ctrl Pts',(-0.831025159000315,2.54687495513699,
13.8309611966328));
#427843=CARTESIAN_POINT('Ctrl Pts',(-0.830627902279593,2.54875922290853,
13.8281701127186));
#427844=CARTESIAN_POINT('Ctrl Pts',(-0.830417617341518,2.55061570652669,
13.8253580685121));
#427845=CARTESIAN_POINT('Ctrl Pts',(-0.830372027339997,2.55101819417869,
13.8247484142933));
#427846=CARTESIAN_POINT('Ctrl Pts',(-0.8303353792422,2.55141929614777,13.8241378483365));
#427847=CARTESIAN_POINT('Ctrl Pts',(-0.830308018192218,2.55181873502139,
13.8235269408515));
#427848=CARTESIAN_POINT('',(-0.853697083398605,2.52156938270644,12.5969504640361));
#427849=CARTESIAN_POINT('Origin',(-0.864613078712907,2.55419927505252,12.584524458991));
#427850=CARTESIAN_POINT('Origin',(-0.864613078712907,2.55419927505252,12.584524458991));
#427851=CARTESIAN_POINT('Ctrl Pts',(-0.890418978460743,2.53147077887093,
12.5893111709658));
#427852=CARTESIAN_POINT('Ctrl Pts',(-0.882935401738879,2.5229587453884,
12.5770542771492));
#427853=CARTESIAN_POINT('Ctrl Pts',(-0.868846144934083,2.53128319837604,
12.5737548217797));
#427854=CARTESIAN_POINT('Ctrl Pts',(-0.906783049188463,2.55008373937387,
12.5663937883685));
#427855=CARTESIAN_POINT('Ctrl Pts',(-0.899289926125211,2.54156084761049,
12.5540940315304));
#427856=CARTESIAN_POINT('Ctrl Pts',(-0.885158643047976,2.54991386107299,
12.5508374392248));
#427857=CARTESIAN_POINT('Ctrl Pts',(-0.923130608769454,2.56867791962787,
12.5434499600945));
#427858=CARTESIAN_POINT('Ctrl Pts',(-0.915613122894688,2.56012731690829,
12.5311293540533));
#427859=CARTESIAN_POINT('Ctrl Pts',(-0.90145609119268,2.56852554398007,
12.5278936106989));
#427860=CARTESIAN_POINT('Ctrl Pts',(-0.939462950544374,2.58725479071547,
12.5204817579905));
#427861=CARTESIAN_POINT('Ctrl Pts',(-0.931908258252054,2.57866186835596,
12.5081597038247));
#427862=CARTESIAN_POINT('Ctrl Pts',(-0.917739669533975,2.58711971315429,
12.5049254088044));
#427863=CARTESIAN_POINT('Ctrl Pts',(-0.927720747655562,2.57389887443867,
12.5369868989719));
#427864=CARTESIAN_POINT('Ctrl Pts',(-0.928335800697191,2.5745984535455,
12.5342545179733));
#427865=CARTESIAN_POINT('Ctrl Pts',(-0.928829092416563,2.57534846714068,
12.5314872231885));
#427866=CARTESIAN_POINT('Ctrl Pts',(-0.929126130394403,2.57613738383454,
12.5287124745063));
#427867=CARTESIAN_POINT('Ctrl Pts',(-0.929394013986471,2.57684886806739,
12.5262100684184));
#427868=CARTESIAN_POINT('Ctrl Pts',(-0.929501087142187,2.57759162218354,
12.5237004536639));
#427869=CARTESIAN_POINT('Ctrl Pts',(-0.929383576003663,2.57838785814339,
12.5212220730815));
#427870=CARTESIAN_POINT('Ctrl Pts',(-0.929293611061598,2.57899744565056,
12.5193246583486));
#427871=CARTESIAN_POINT('Ctrl Pts',(-0.929070309173177,2.57964557286779,
12.517417831369));
#427872=CARTESIAN_POINT('Ctrl Pts',(-0.928617299556025,2.58031932875108,
12.5155812248347));
#427873=CARTESIAN_POINT('Ctrl Pts',(-0.928424315024181,2.58060635237881,
12.5147988205793));
#427874=CARTESIAN_POINT('Ctrl Pts',(-0.928189676985529,2.58089847305173,
12.5140295443047));
#427875=CARTESIAN_POINT('Ctrl Pts',(-0.927906723889576,2.58119666811931,
12.5132817086137));
#427876=CARTESIAN_POINT('Ctrl Pts',(-0.92747851265588,2.58164794601516,
12.5121499604604));
#427877=CARTESIAN_POINT('Ctrl Pts',(-0.926925212002706,2.58211795825336,
12.5110494206568));
#427878=CARTESIAN_POINT('Ctrl Pts',(-0.926214860966318,2.58258758951169,
12.5100666561695));
#427879=CARTESIAN_POINT('Ctrl Pts',(-0.925806979037018,2.58285725069876,
12.5095023550641));
#427880=CARTESIAN_POINT('Ctrl Pts',(-0.925342244438101,2.58312935745719,
12.5089719619137));
#427881=CARTESIAN_POINT('Ctrl Pts',(-0.924826140945495,2.58339329773807,
12.5085043804652));
#427882=CARTESIAN_POINT('Ctrl Pts',(-0.924070890711275,2.5837795399585,
12.5078201359221));
#427883=CARTESIAN_POINT('Ctrl Pts',(-0.923183181789113,2.58415842104837,
12.5072563000953));
#427884=CARTESIAN_POINT('Ctrl Pts',(-0.922219864431952,2.58449647201457,
12.5068768744336));
#427885=CARTESIAN_POINT('Ctrl Pts',(-0.921525246302446,2.58474023003271,
12.5066032824118));
#427886=CARTESIAN_POINT('Ctrl Pts',(-0.920779132793865,2.58496709795591,
12.5064197834844));
#427887=CARTESIAN_POINT('Ctrl Pts',(-0.920023940796857,2.58516687994944,
12.5063282718343));
#427888=CARTESIAN_POINT('Ctrl Pts',(-0.918921594282759,2.58545849980904,
12.5061946931565));
#427889=CARTESIAN_POINT('Ctrl Pts',(-0.917776614572163,2.58569966768065,
12.5062515701262));
#427890=CARTESIAN_POINT('Ctrl Pts',(-0.916663248489658,2.5858905487563,
12.5064436508398));
#427891=CARTESIAN_POINT('',(-0.868846144934083,2.53128319837604,12.5737548217797));
#427892=CARTESIAN_POINT('Origin',(-0.873896531994877,2.54599691954154,12.5893111709658));
#427893=CARTESIAN_POINT('Ctrl Pts',(-0.916663248489658,2.5858905487563,
12.5064436508398));
#427894=CARTESIAN_POINT('Ctrl Pts',(-0.909584713394436,2.57780755867484,
12.5164271754438));
#427895=CARTESIAN_POINT('Ctrl Pts',(-0.902503529552574,2.5697212268477,
12.5264061185523));
#427896=CARTESIAN_POINT('Ctrl Pts',(-0.895419602965386,2.56163143620496,
12.536380305637));
#427897=CARTESIAN_POINT('Ctrl Pts',(-0.886566131506523,2.55152083868786,
12.5488460165097));
#427898=CARTESIAN_POINT('Ctrl Pts',(-0.877708373301593,2.54140483552231,
12.5613043021964));
#427899=CARTESIAN_POINT('Ctrl Pts',(-0.868846144934083,2.53128319837604,
12.5737548217797));
#427900=CARTESIAN_POINT('Ctrl Pts',(-0.830308018192218,2.55181873502139,
12.5893111709658));
#427901=CARTESIAN_POINT('Ctrl Pts',(-0.831082564866783,2.54051127235248,
12.5770542771492));
#427902=CARTESIAN_POINT('Ctrl Pts',(-0.847331259925655,2.53856612872315,
12.5737548217797));
#427903=CARTESIAN_POINT('Ctrl Pts',(-0.831030663502936,2.54126897069842,
12.5928319619712));
#427904=CARTESIAN_POINT('Ctrl Pts',(-0.834801333342892,2.53389228680053,
12.5821634970842));
#427905=CARTESIAN_POINT('Ctrl Pts',(-0.847585085332313,2.53472245989866,
12.5773203894503));
#427906=CARTESIAN_POINT('Ctrl Pts',(-0.839041370780464,2.52655799968174,
12.5969440695591));
#427907=CARTESIAN_POINT('Ctrl Pts',(-0.842843009373702,2.5252518271976,
12.5878292599214));
#427908=CARTESIAN_POINT('Ctrl Pts',(-0.850442061715556,2.52948014809535,
12.5813877129824));
#427909=CARTESIAN_POINT('Ctrl Pts',(-0.868005588370279,2.51669649143244,
12.596957478804));
#427910=CARTESIAN_POINT('Ctrl Pts',(-0.864232070952202,2.51799308676035,
12.5878468778671));
#427911=CARTESIAN_POINT('Ctrl Pts',(-0.860810679271491,2.52595622438975,
12.5814011370086));
#427912=CARTESIAN_POINT('Ctrl Pts',(-0.883426728453422,2.52351759439869,
12.5928371701607));
#427913=CARTESIAN_POINT('Ctrl Pts',(-0.875953421783604,2.51995602829336,
12.5821692192952));
#427914=CARTESIAN_POINT('Ctrl Pts',(-0.866301898949204,2.52837457501741,
12.5773318885715));
#427915=CARTESIAN_POINT('Ctrl Pts',(-0.890418978460782,2.53147077887088,
12.5893111709658));
#427916=CARTESIAN_POINT('Ctrl Pts',(-0.882935401738917,2.52295874538836,
12.5770542771492));
#427917=CARTESIAN_POINT('Ctrl Pts',(-0.868846144934124,2.531283198376,12.5737548217797));
#427918=CARTESIAN_POINT('',(-0.847331259925655,2.53856612872315,12.5737548217797));
#427919=CARTESIAN_POINT('Origin',(-0.852256586298207,2.55332218375571,12.5893111709658));
#427920=CARTESIAN_POINT('Ctrl Pts',(-0.868846144934124,2.531283198376,12.5737548217797));
#427921=CARTESIAN_POINT('Ctrl Pts',(-0.868209341145503,2.53050937632552,
12.5746934679442));
#427922=CARTESIAN_POINT('Ctrl Pts',(-0.867363228478373,2.52976949201513,
12.5756680099006));
#427923=CARTESIAN_POINT('Ctrl Pts',(-0.866406262569698,2.52914521650094,
12.5765688348656));
#427924=CARTESIAN_POINT('Ctrl Pts',(-0.866152916439339,2.52897994646952,
12.5768073183026));
#427925=CARTESIAN_POINT('Ctrl Pts',(-0.865891989609333,2.52882260442307,
12.5770407398754));
#427926=CARTESIAN_POINT('Ctrl Pts',(-0.865625612729321,2.52867423157954,
12.5772674179684));
#427927=CARTESIAN_POINT('Ctrl Pts',(-0.864532474045098,2.5280653495514,
12.5781976435658));
#427928=CARTESIAN_POINT('Ctrl Pts',(-0.863279976727664,2.52758278561512,
12.5790594849312));
#427929=CARTESIAN_POINT('Ctrl Pts',(-0.861935330421642,2.52730418368516,
12.5797571720116));
#427930=CARTESIAN_POINT('Ctrl Pts',(-0.861059245004097,2.52712266451016,
12.580211740231));
#427931=CARTESIAN_POINT('Ctrl Pts',(-0.860100420079891,2.52703786035313,
12.5806009430798));
#427932=CARTESIAN_POINT('Ctrl Pts',(-0.859124791877453,2.52707338886178,
12.5808812374708));
#427933=CARTESIAN_POINT('Ctrl Pts',(-0.858286403590271,2.52710391963717,
12.5811221033394));
#427934=CARTESIAN_POINT('Ctrl Pts',(-0.857418447014624,2.52722404929833,
12.581287365893));
#427935=CARTESIAN_POINT('Ctrl Pts',(-0.856571054141246,2.52743525678305,
12.581359338449));
#427936=CARTESIAN_POINT('Ctrl Pts',(-0.85645328402984,2.52746461026216,
12.5813693411482));
#427937=CARTESIAN_POINT('Ctrl Pts',(-0.856335878094531,2.52749567298117,
12.5813775999465));
#427938=CARTESIAN_POINT('Ctrl Pts',(-0.856218936184463,2.52752839834373,
12.5813841266931));
#427939=CARTESIAN_POINT('Ctrl Pts',(-0.856020530090201,2.52758392087937,
12.5813952001081));
#427940=CARTESIAN_POINT('Ctrl Pts',(-0.855822294958541,2.52764518758066,
12.5814007534795));
#427941=CARTESIAN_POINT('Ctrl Pts',(-0.855624375359456,2.52771236018032,
12.5814005856065));
#427942=CARTESIAN_POINT('Ctrl Pts',(-0.854718376816389,2.52801985007875,
12.5813998171494));
#427943=CARTESIAN_POINT('Ctrl Pts',(-0.853881479174623,2.52842953036616,
12.58127954464));
#427944=CARTESIAN_POINT('Ctrl Pts',(-0.853105424256869,2.5289124991765,
12.5810700125799));
#427945=CARTESIAN_POINT('Ctrl Pts',(-0.85216803827715,2.52949587050898,
12.5808169217085));
#427946=CARTESIAN_POINT('Ctrl Pts',(-0.851328179270106,2.53020043080289,
12.5804173076348));
#427947=CARTESIAN_POINT('Ctrl Pts',(-0.850642713652396,2.53094448204749,
12.5799304713245));
#427948=CARTESIAN_POINT('Ctrl Pts',(-0.849793205808115,2.53186659593986,
12.5793271277669));
#427949=CARTESIAN_POINT('Ctrl Pts',(-0.849104452189448,2.53288474684281,
12.5785808224116));
#427950=CARTESIAN_POINT('Ctrl Pts',(-0.848579214591445,2.53393824640552,
12.5777485681082));
#427951=CARTESIAN_POINT('Ctrl Pts',(-0.847796553026346,2.53550807617347,
12.576508418016));
#427952=CARTESIAN_POINT('Ctrl Pts',(-0.847377406667919,2.53714011043811,
12.5750928681475));
#427953=CARTESIAN_POINT('Ctrl Pts',(-0.847331259925655,2.53856612872315,
12.5737548217797));
#427954=CARTESIAN_POINT('Ctrl Pts',(-0.847331259925655,2.53856612872315,
12.5737548217797));
#427955=CARTESIAN_POINT('Ctrl Pts',(-0.831082564866783,2.54051127235248,
12.5770542771492));
#427956=CARTESIAN_POINT('Ctrl Pts',(-0.830308018192218,2.55181873502139,
12.5893111709658));
#427957=CARTESIAN_POINT('Ctrl Pts',(-0.845689554112151,2.56327077922043,
12.5508408821982));
#427958=CARTESIAN_POINT('Ctrl Pts',(-0.829390133805893,2.56521875825246,
12.55409748406));
#427959=CARTESIAN_POINT('Ctrl Pts',(-0.828614599008143,2.57654064634775,
12.5663972313419));
#427960=CARTESIAN_POINT('Ctrl Pts',(-0.844048275121227,2.5879512181765,
12.52790050457));
#427961=CARTESIAN_POINT('Ctrl Pts',(-0.827700944153361,2.58987892343607,
12.5311362602937));
#427962=CARTESIAN_POINT('Ctrl Pts',(-0.826922888205761,2.60123761732792,
12.5434568539655));
#427963=CARTESIAN_POINT('Ctrl Pts',(-0.84240737596564,2.61260932622068,
12.5049357605811));
#427964=CARTESIAN_POINT('Ctrl Pts',(-0.826014658008805,2.61449670084619,
12.5081700652078));
#427965=CARTESIAN_POINT('Ctrl Pts',(-0.825232751984268,2.6259116012949,
12.5204921097672));
#427966=CARTESIAN_POINT('Ctrl Pts',(-0.842515122252696,2.61099017808429,
12.5064436508395));
#427967=CARTESIAN_POINT('Ctrl Pts',(-0.841434523300001,2.61155688232287,
12.5062361689309));
#427968=CARTESIAN_POINT('Ctrl Pts',(-0.84028662328999,2.61210012921652,
12.5061871075061));
#427969=CARTESIAN_POINT('Ctrl Pts',(-0.839147735412921,2.61256267764056,
12.5063648335164));
#427970=CARTESIAN_POINT('Ctrl Pts',(-0.838630382289638,2.61277279566592,
12.5064455676329));
#427971=CARTESIAN_POINT('Ctrl Pts',(-0.838107589950988,2.61296898785313,
12.506574497099));
#427972=CARTESIAN_POINT('Ctrl Pts',(-0.837601404912136,2.61314185812502,
12.5067492519495));
#427973=CARTESIAN_POINT('Ctrl Pts',(-0.836584206427947,2.61348924764668,
12.5071004286051));
#427974=CARTESIAN_POINT('Ctrl Pts',(-0.835596412354412,2.61375446499197,
12.5076537929612));
#427975=CARTESIAN_POINT('Ctrl Pts',(-0.834714614491528,2.61392673912018,
12.5083435010503));
#427976=CARTESIAN_POINT('Ctrl Pts',(-0.834659100046304,2.61393758480609,
12.5083869222963));
#427977=CARTESIAN_POINT('Ctrl Pts',(-0.834603997369877,2.61394805158507,
12.5084308732336));
#427978=CARTESIAN_POINT('Ctrl Pts',(-0.834549321866726,2.61395813272698,
12.5084753333615));
#427979=CARTESIAN_POINT('Ctrl Pts',(-0.834110752167104,2.61403899679089,
12.508831962269));
#427980=CARTESIAN_POINT('Ctrl Pts',(-0.833690997704952,2.61409795873129,
12.509227847131));
#427981=CARTESIAN_POINT('Ctrl Pts',(-0.83330292946147,2.61413603813351,
12.5096423454524));
#427982=CARTESIAN_POINT('Ctrl Pts',(-0.832086895338208,2.61425536212681,
12.5109411997424));
#427983=CARTESIAN_POINT('Ctrl Pts',(-0.831108144286379,2.61418659826853,
12.5124831113042));
#427984=CARTESIAN_POINT('Ctrl Pts',(-0.830322672712138,2.61401352926051,
12.5140723025007));
#427985=CARTESIAN_POINT('Ctrl Pts',(-0.830249073165328,2.6139973125049,
12.5142212114565));
#427986=CARTESIAN_POINT('Ctrl Pts',(-0.830177148488656,2.61398019966024,
12.5143705582413));
#427987=CARTESIAN_POINT('Ctrl Pts',(-0.830106850884374,2.6139622720599,
12.5145201959299));
#427988=CARTESIAN_POINT('Ctrl Pts',(-0.829203773495196,2.61373196534218,
12.5164425148273));
#427989=CARTESIAN_POINT('Ctrl Pts',(-0.82853561926261,2.6133697117006,12.5184635205941));
#427990=CARTESIAN_POINT('Ctrl Pts',(-0.828025025593438,2.61292191164947,
12.5205025929158));
#427991=CARTESIAN_POINT('Ctrl Pts',(-0.827728861027278,2.61266216987068,
12.5216853356836));
#427992=CARTESIAN_POINT('Ctrl Pts',(-0.827485923233799,2.6123744790939,
12.5228750347131));
#427993=CARTESIAN_POINT('Ctrl Pts',(-0.827284450807109,2.61207278933631,
12.5240609649613));
#427994=CARTESIAN_POINT('Ctrl Pts',(-0.826789947544418,2.61133230801141,
12.5269717671326));
#427995=CARTESIAN_POINT('Ctrl Pts',(-0.826539972252611,2.61048087901163,
12.5299036066169));
#427996=CARTESIAN_POINT('Ctrl Pts',(-0.82645638379178,2.60955596545061,
12.5328133004019));
#427997=CARTESIAN_POINT('Ctrl Pts',(-0.826416256463371,2.60911195308521,
12.5342101228451));
#427998=CARTESIAN_POINT('Ctrl Pts',(-0.826415045980927,2.60865151259894,
12.5356023438238));
#427999=CARTESIAN_POINT('Ctrl Pts',(-0.826447302606738,2.60818060292636,
12.5369868989719));
#428000=CARTESIAN_POINT('Origin',(0.0498110926827573,15.3230129328841,-1.23968016501985));
#428001=CARTESIAN_POINT('Ctrl Pts',(-0.927693181599444,2.57386745989593,
12.5369868989719));
#428002=CARTESIAN_POINT('Ctrl Pts',(-0.937799265232525,2.58540654033113,
12.5369868989719));
#428003=CARTESIAN_POINT('Ctrl Pts',(-0.952121069903317,2.57991388936274,
12.5369868989719));
#428004=CARTESIAN_POINT('Ctrl Pts',(-0.931109482923459,2.57776807674996,
12.5218025310015));
#428005=CARTESIAN_POINT('Ctrl Pts',(-0.941077582193263,2.58411574251414,
12.5216901060418));
#428006=CARTESIAN_POINT('Ctrl Pts',(-0.952077418201794,2.57993064818136,
12.5161920673677));
#428007=CARTESIAN_POINT('Ctrl Pts',(-0.929742987280898,2.58363908695726,
12.5042015548896));
#428008=CARTESIAN_POINT('Ctrl Pts',(-0.935716298867672,2.586025903604,12.4980677368514));
#428009=CARTESIAN_POINT('Ctrl Pts',(-0.942105101708514,2.58370771940401,
12.4907278922778));
#428010=CARTESIAN_POINT('Ctrl Pts',(-0.916656565818685,2.58587169709282,
12.5064636261921));
#428011=CARTESIAN_POINT('Ctrl Pts',(-0.918842592986576,2.59203844044394,
12.4999376786892));
#428012=CARTESIAN_POINT('Ctrl Pts',(-0.918815893843201,2.59196312264034,
12.4906970594712));
#428013=CARTESIAN_POINT('Origin',(-0.94424319412143,2.55937273376805,12.5369868989719));
#428014=CARTESIAN_POINT('Origin',(-0.944243194121431,2.55937273376806,14.));
#428015=CARTESIAN_POINT('Origin',(-0.944243194121431,2.55937273376806,13.7435492065112));
#428016=CARTESIAN_POINT('Ctrl Pts',(-0.911372188348151,2.55530351594609,
13.793642941384));
#428017=CARTESIAN_POINT('Ctrl Pts',(-0.918490869314486,2.56344173444312,
13.8071662555867));
#428018=CARTESIAN_POINT('Ctrl Pts',(-0.93281817254894,2.5542358794767,13.8103758687955));
#428019=CARTESIAN_POINT('Ctrl Pts',(-0.922346766118139,2.5677863180351,
13.7804579775006));
#428020=CARTESIAN_POINT('Ctrl Pts',(-0.931138207785595,2.5778214675176,
13.7901904343351));
#428021=CARTESIAN_POINT('Ctrl Pts',(-0.945597244891531,2.57156110250158,
13.7927914348262));
#428022=CARTESIAN_POINT('Ctrl Pts',(-0.92880791309972,2.57513541338049,
13.7597120340895));
#428023=CARTESIAN_POINT('Ctrl Pts',(-0.938986397230478,2.58674513132594,
13.7635825532445));
#428024=CARTESIAN_POINT('Ctrl Pts',(-0.953153620955572,2.58176259301024,
13.7651073818884));
#428025=CARTESIAN_POINT('Ctrl Pts',(-0.927542672577892,2.57369629223617,
13.7381884353898));
#428026=CARTESIAN_POINT('Ctrl Pts',(-0.937482234460371,2.58503485564652,
13.7368803041982));
#428027=CARTESIAN_POINT('Ctrl Pts',(-0.951674255133689,2.57976454386001,
13.7363986145813));
#428028=CARTESIAN_POINT('Origin',(-0.930557576665944,2.54380632236616,13.7902182540695));
#428029=CARTESIAN_POINT('Ctrl Pts',(-0.890416380041073,2.53146782220492,
13.8235227101244));
#428030=CARTESIAN_POINT('Ctrl Pts',(-0.898004327165888,2.54010528402833,
13.8358800583119));
#428031=CARTESIAN_POINT('Ctrl Pts',(-0.912214993939723,2.53157985155249,
13.8390832900376));
#428032=CARTESIAN_POINT('Ctrl Pts',(-0.898291911659455,2.54042567635774,
13.8124254819053));
#428033=CARTESIAN_POINT('Ctrl Pts',(-0.905894594678995,2.54907991182599,
13.8247886449158));
#428034=CARTESIAN_POINT('Ctrl Pts',(-0.920114448745398,2.5405290913137,
13.8279860620657));
#428035=CARTESIAN_POINT('Ctrl Pts',(-0.906163913720722,2.54937951589171,
13.8013225099954));
#428036=CARTESIAN_POINT('Ctrl Pts',(-0.913777743883447,2.55804644291841,
13.8136962257787));
#428037=CARTESIAN_POINT('Ctrl Pts',(-0.928010043278306,2.54947436739277,
13.8168830918626));
#428038=CARTESIAN_POINT('Ctrl Pts',(-0.9140325235546,2.55832949700957,13.7902140179785));
#428039=CARTESIAN_POINT('Ctrl Pts',(-0.921654146662431,2.56700530030073,
13.802602731458));
#428040=CARTESIAN_POINT('Ctrl Pts',(-0.935901927838362,2.55841583675028,
13.8057746032558));
#428041=CARTESIAN_POINT('Origin',(-0.906941424926609,2.51694463820031,13.8235269408515));
#428042=CARTESIAN_POINT('Ctrl Pts',(-0.830308018192218,2.55181873502139,
13.8235269408515));
#428043=CARTESIAN_POINT('Ctrl Pts',(-0.829501111688596,2.56359861280876,
13.8362179249168));
#428044=CARTESIAN_POINT('Ctrl Pts',(-0.812498466818824,2.56520269244821,
13.8391868794938));
#428045=CARTESIAN_POINT('Ctrl Pts',(-0.831046302520483,2.54104065959348,
13.8400110824519));
#428046=CARTESIAN_POINT('Ctrl Pts',(-0.826986359770495,2.55025145368134,
13.8494522556837));
#428047=CARTESIAN_POINT('Ctrl Pts',(-0.813825568650046,2.54747270134967,
13.85569149686));
#428048=CARTESIAN_POINT('Ctrl Pts',(-0.838715429734773,2.52666769143045,
13.8586819406588));
#428049=CARTESIAN_POINT('Ctrl Pts',(-0.834595926707794,2.528076853751,13.868010383617));
#428050=CARTESIAN_POINT('Ctrl Pts',(-0.826685282294806,2.52368201908246,
13.8744918421245));
#428051=CARTESIAN_POINT('Ctrl Pts',(-0.868336578609752,2.51658508079264,
13.8587686893867));
#428052=CARTESIAN_POINT('Ctrl Pts',(-0.872419399873498,2.51518840672611,
13.8680909899357));
#428053=CARTESIAN_POINT('Ctrl Pts',(-0.875996625548385,2.50689986897952,
13.8745789365163));
#428054=CARTESIAN_POINT('Ctrl Pts',(-0.883274156730999,2.52334405496269,
13.8400379222776));
#428055=CARTESIAN_POINT('Ctrl Pts',(-0.892095268321583,2.52818742406021,
13.8494748685453));
#428056=CARTESIAN_POINT('Ctrl Pts',(-0.900858995894796,2.51799143542316,
13.8557104837033));
#428057=CARTESIAN_POINT('Ctrl Pts',(-0.890418978465611,2.53147077886645,
13.8235269408542));
#428058=CARTESIAN_POINT('Ctrl Pts',(-0.898215211960036,2.54033843707429,
13.8362179249195));
#428059=CARTESIAN_POINT('Ctrl Pts',(-0.912696230447696,2.53128508920643,
13.8391868794965));
#428060=CARTESIAN_POINT('Origin',(-0.808359450086228,2.55031528628707,13.8235269408515));
#428061=CARTESIAN_POINT('Ctrl Pts',(-0.827864026276527,2.58749810676731,
13.7902140241682));
#428062=CARTESIAN_POINT('Ctrl Pts',(-0.827079286871544,2.59901951204006,
13.8026027327198));
#428063=CARTESIAN_POINT('Ctrl Pts',(-0.810543698121789,2.60085042355425,
13.8057746032556));
#428064=CARTESIAN_POINT('Ctrl Pts',(-0.828678423698535,2.57560887047302,
13.8013225161808));
#428065=CARTESIAN_POINT('Ctrl Pts',(-0.82789448337184,2.58711849103363,
13.8136962270464));
#428066=CARTESIAN_POINT('Ctrl Pts',(-0.811381754829571,2.58895381155141,
13.8168830918628));
#428067=CARTESIAN_POINT('Ctrl Pts',(-0.82949317221461,2.56371450862203,
13.8124254880875));
#428068=CARTESIAN_POINT('Ctrl Pts',(-0.82871037804292,2.57520727627501,
13.8247886461868));
#428069=CARTESIAN_POINT('Ctrl Pts',(-0.812220446444029,2.57705192205747,
13.8279860620656));
#428070=CARTESIAN_POINT('Ctrl Pts',(-0.830308286038418,2.55181481371165,
13.8235227163065));
#428071=CARTESIAN_POINT('Ctrl Pts',(-0.829527009371742,2.56328530585484,
13.8358800595847));
#428072=CARTESIAN_POINT('Ctrl Pts',(-0.813059797021839,2.56514453908972,
13.8390832900376));
#428073=CARTESIAN_POINT('Origin',(-0.805915189477223,2.58599859175722,13.7902182540695));
#428074=CARTESIAN_POINT('Ctrl Pts',(-0.826465716928943,2.60791137202139,
13.7382347919292));
#428075=CARTESIAN_POINT('Ctrl Pts',(-0.82545841117444,2.62296803844693,
13.7369371795943));
#428076=CARTESIAN_POINT('Ctrl Pts',(-0.810969599492456,2.62739727236085,
13.7364597369712));
#428077=CARTESIAN_POINT('Ctrl Pts',(-0.826336450902827,2.60979850855029,
13.7595490285573));
#428078=CARTESIAN_POINT('Ctrl Pts',(-0.825304108514234,2.62521434701637,
13.7633824266925));
#428079=CARTESIAN_POINT('Ctrl Pts',(-0.811007953024174,2.62985262239744,
13.7648920890506));
#428080=CARTESIAN_POINT('Ctrl Pts',(-0.826995700562206,2.6001742156392,
13.7803806590111));
#428081=CARTESIAN_POINT('Ctrl Pts',(-0.826108147738794,2.6135087248536,
13.7901039518745));
#428082=CARTESIAN_POINT('Ctrl Pts',(-0.81081613484347,2.61733492179509,
13.7926933640892));
#428083=CARTESIAN_POINT('Ctrl Pts',(-0.828141623556339,2.583445046142,13.7936647693663));
#428084=CARTESIAN_POINT('Ctrl Pts',(-0.827432419508959,2.59423718965308,
13.8072068914933));
#428085=CARTESIAN_POINT('Ctrl Pts',(-0.810440115724187,2.59561772648085,
13.8104111085397));
#428086=CARTESIAN_POINT('Origin',(-0.804498734500748,2.60667715419204,13.7435492065112));
#428087=CARTESIAN_POINT('Origin',(-0.804498734500748,2.60667715419204,14.));
#428088=CARTESIAN_POINT('Origin',(-0.804498734500748,2.60667715419204,12.5369868989719));
#428089=CARTESIAN_POINT('Ctrl Pts',(-0.842509476978436,2.61097268310583,
12.506462012331));
#428090=CARTESIAN_POINT('Ctrl Pts',(-0.844517414078375,2.61719536553326,
12.4999388158272));
#428091=CARTESIAN_POINT('Ctrl Pts',(-0.844493657549235,2.61712174303959,
12.4907030323752));
#428092=CARTESIAN_POINT('Ctrl Pts',(-0.830757090671982,2.61714601277937,
12.5042014951932));
#428093=CARTESIAN_POINT('Ctrl Pts',(-0.827464013952634,2.62266839839037,
12.4980716682127));
#428094=CARTESIAN_POINT('Ctrl Pts',(-0.820985788226397,2.62470755426128,
12.4907355092743));
#428095=CARTESIAN_POINT('Ctrl Pts',(-0.826104613507571,2.61331454341629,
12.5218047446509));
#428096=CARTESIAN_POINT('Ctrl Pts',(-0.822042668831244,2.6244059579511,
12.5216906929434));
#428097=CARTESIAN_POINT('Ctrl Pts',(-0.810769257694715,2.62776467134713,
12.5161988840776));
#428098=CARTESIAN_POINT('Ctrl Pts',(-0.826449894446796,2.60814227433147,
12.5369868989719));
#428099=CARTESIAN_POINT('Ctrl Pts',(-0.825428979411771,2.62343813207178,
12.5369868989719));
#428100=CARTESIAN_POINT('Ctrl Pts',(-0.810726046326702,2.62777740507733,
12.5369868989719));
#428101=CARTESIAN_POINT('Origin',(-1.65186468598908E-31,-2.72002836734944E-32,
12.5));
#428102=CARTESIAN_POINT('Origin',(-1.03554215359084,2.4756499570046,12.5));
#428103=CARTESIAN_POINT('',(-1.03554215359084,2.4756499570046,12.5893111709658));
#428104=CARTESIAN_POINT('',(-1.03554215359084,2.4756499570046,13.8235269408515));
#428105=CARTESIAN_POINT('',(-1.03554215359084,2.4756499570046,12.5));
#428106=CARTESIAN_POINT('',(-1.03601454672084,2.51141375915052,13.7902182540695));
#428107=CARTESIAN_POINT('',(-1.03554215359084,2.4756499570046,13.8235269408515));
#428108=CARTESIAN_POINT('',(-1.03628829969029,2.532138969605,13.7435492065112));
#428109=CARTESIAN_POINT('Origin',(-1.03538798176588,2.46395329685158,13.7445212918692));
#428110=CARTESIAN_POINT('',(-1.03628829969029,2.532138969605,12.5369868989719));
#428111=CARTESIAN_POINT('',(-1.03628829969029,2.532138969605,12.5));
#428112=CARTESIAN_POINT('Ctrl Pts',(-1.03628829969029,2.532138969605,12.5369868989719));
#428113=CARTESIAN_POINT('Ctrl Pts',(-1.03603976572167,2.51332303195488,
12.5544431401645));
#428114=CARTESIAN_POINT('Ctrl Pts',(-1.03579105399495,2.49449363664606,
12.5718848856037));
#428115=CARTESIAN_POINT('Ctrl Pts',(-1.03554215359084,2.4756499570046,12.5893111709658));
#428116=CARTESIAN_POINT('Origin',(-1.29160128864211,2.64151328156347,12.5));
#428117=CARTESIAN_POINT('',(-1.1344304865774,2.48971658479254,13.7435492065112));
#428118=CARTESIAN_POINT('',(-1.11952159984425,2.47531747421414,13.7902182540695));
#428119=CARTESIAN_POINT('Origin',(-1.08034362228217,2.43747910027977,13.7418732680441));
#428120=CARTESIAN_POINT('',(-1.09379455227041,2.45047010569483,13.8235269408515));
#428121=CARTESIAN_POINT('',(-1.11952159984425,2.47531747421414,13.7902182540695));
#428122=CARTESIAN_POINT('',(-1.09379455227041,2.45047010569483,12.5893111709658));
#428123=CARTESIAN_POINT('',(-1.09379455227041,2.45047010569483,12.5));
#428124=CARTESIAN_POINT('',(-1.1344304865774,2.48971658479254,12.5369868989719));
#428125=CARTESIAN_POINT('Ctrl Pts',(-1.09379455227041,2.45047010569483,
12.5893111709658));
#428126=CARTESIAN_POINT('Ctrl Pts',(-1.10734994105777,2.46356199817318,
12.5718848856037));
#428127=CARTESIAN_POINT('Ctrl Pts',(-1.12089505426805,2.47664396642491,
12.5544431401645));
#428128=CARTESIAN_POINT('Ctrl Pts',(-1.1344304865774,2.48971658479254,12.5369868989719));
#428129=CARTESIAN_POINT('',(-1.1344304865774,2.48971658479254,12.5));
#428130=CARTESIAN_POINT('Origin',(-1.06991415528683,2.47519594774129,12.5));
#428131=CARTESIAN_POINT('',(-1.05525494628247,2.44410418414473,13.8587068136939));
#428132=CARTESIAN_POINT('Ctrl Pts',(-1.09379455227489,2.45047010568997,
13.8235269408542));
#428133=CARTESIAN_POINT('Ctrl Pts',(-1.09253412895405,2.44925277973552,
13.8262006681044));
#428134=CARTESIAN_POINT('Ctrl Pts',(-1.09112357270249,2.44813199470117,
13.8288634856214));
#428135=CARTESIAN_POINT('Ctrl Pts',(-1.08957482168588,2.44710181036399,
13.8314912288862));
#428136=CARTESIAN_POINT('Ctrl Pts',(-1.08797821913402,2.44603979657094,
13.8342001611531));
#428137=CARTESIAN_POINT('Ctrl Pts',(-1.08623325208851,2.44507247516437,
13.8368750301949));
#428138=CARTESIAN_POINT('Ctrl Pts',(-1.08431407794086,2.44421632114273,
13.8394886372969));
#428139=CARTESIAN_POINT('Ctrl Pts',(-1.08416585546618,2.4441501982909,13.8396904925131));
#428140=CARTESIAN_POINT('Ctrl Pts',(-1.08401658149932,2.44408475690539,
13.8398919674349));
#428141=CARTESIAN_POINT('Ctrl Pts',(-1.08386623860007,2.44402001459231,
13.8400930404591));
#428142=CARTESIAN_POINT('Ctrl Pts',(-1.08152379508397,2.44301128579805,
13.8432258934518));
#428143=CARTESIAN_POINT('Ctrl Pts',(-1.07893425814486,2.44217637542924,
13.8462331177034));
#428144=CARTESIAN_POINT('Ctrl Pts',(-1.07615248274327,2.44163432596774,
13.8489036603661));
#428145=CARTESIAN_POINT('Ctrl Pts',(-1.07524225345872,2.44145696107579,
13.849777493004));
#428146=CARTESIAN_POINT('Ctrl Pts',(-1.07431162075303,2.44131112643096,
13.85061494757));
#428147=CARTESIAN_POINT('Ctrl Pts',(-1.07336302610177,2.44120148194552,
13.8514076489583));
#428148=CARTESIAN_POINT('Ctrl Pts',(-1.07135661160652,2.44096956804571,
13.8530843267192));
#428149=CARTESIAN_POINT('Ctrl Pts',(-1.06907241597874,2.44087972128076,
13.8546805203176));
#428150=CARTESIAN_POINT('Ctrl Pts',(-1.06663765028923,2.44107349660114,
13.8559412814274));
#428151=CARTESIAN_POINT('Ctrl Pts',(-1.06631179967866,2.44109943002329,
13.8561100121513));
#428152=CARTESIAN_POINT('Ctrl Pts',(-1.06598329716654,2.44113038115478,
13.8562727473908));
#428153=CARTESIAN_POINT('Ctrl Pts',(-1.0656524840526,2.44116662275184,13.8564289040185));
#428154=CARTESIAN_POINT('Ctrl Pts',(-1.06415225035486,2.44133097798106,
13.8571370725437));
#428155=CARTESIAN_POINT('Ctrl Pts',(-1.06257837452934,2.44160928936341,
13.8577210840553));
#428156=CARTESIAN_POINT('Ctrl Pts',(-1.06099714379373,2.44201963856708,
13.8581177131616));
#428157=CARTESIAN_POINT('Ctrl Pts',(-1.06055181479428,2.44213520702663,
13.8582294175695));
#428158=CARTESIAN_POINT('Ctrl Pts',(-1.06010589235067,2.44226107112859,
13.8583265086086));
#428159=CARTESIAN_POINT('Ctrl Pts',(-1.05966080616386,2.44239719818541,
13.8584082369006));
#428160=CARTESIAN_POINT('Ctrl Pts',(-1.059021336668,2.44259277626215,13.8585256585398));
#428161=CARTESIAN_POINT('Ctrl Pts',(-1.05837573782924,2.44281227981609,
13.8586122832068));
#428162=CARTESIAN_POINT('Ctrl Pts',(-1.05774103463668,2.44305075443522,
13.8586682984299));
#428163=CARTESIAN_POINT('Ctrl Pts',(-1.05723333499873,2.4432415104913,13.8587131050557));
#428164=CARTESIAN_POINT('Ctrl Pts',(-1.05672691682815,2.44344629242233,
13.8587357943552));
#428165=CARTESIAN_POINT('Ctrl Pts',(-1.05622190980664,2.44366559407393,
13.8587355499465));
#428166=CARTESIAN_POINT('Ctrl Pts',(-1.05589551172886,2.44380733395969,
13.8587353919793));
#428167=CARTESIAN_POINT('Ctrl Pts',(-1.05557321735783,2.44395357100555,
13.8587257282814));
#428168=CARTESIAN_POINT('Ctrl Pts',(-1.05525494628247,2.44410418414473,
13.8587068136939));
#428169=CARTESIAN_POINT('Ctrl Pts',(-1.05525494628247,2.44410418414473,
13.8587068136939));
#428170=CARTESIAN_POINT('Ctrl Pts',(-1.05420817006571,2.44459954254902,
13.8586446046467));
#428171=CARTESIAN_POINT('Ctrl Pts',(-1.05320486014151,2.44514217983373,
13.858482427929));
#428172=CARTESIAN_POINT('Ctrl Pts',(-1.05224262539812,2.44572831862652,
13.8582284286032));
#428173=CARTESIAN_POINT('Ctrl Pts',(-1.05125548448328,2.44632962884536,
13.8579678548414));
#428174=CARTESIAN_POINT('Ctrl Pts',(-1.05030995810848,2.44697949858509,
13.857615680862));
#428175=CARTESIAN_POINT('Ctrl Pts',(-1.04943783450206,2.4476443218117,13.8571944833187));
#428176=CARTESIAN_POINT('Ctrl Pts',(-1.04726136084877,2.44930345616624,
13.8561433417727));
#428177=CARTESIAN_POINT('Ctrl Pts',(-1.04543732607343,2.45112951671997,
13.8546163505475));
#428178=CARTESIAN_POINT('Ctrl Pts',(-1.04395148423086,2.45291621503479,
13.8528973491086));
#428179=CARTESIAN_POINT('Ctrl Pts',(-1.04368004284776,2.45324261845664,
13.8525833129073));
#428180=CARTESIAN_POINT('Ctrl Pts',(-1.04341975016522,2.45356767825653,
13.8522628768812));
#428181=CARTESIAN_POINT('Ctrl Pts',(-1.0431703408006,2.45389012658109,13.851937733538));
#428182=CARTESIAN_POINT('Ctrl Pts',(-1.04164723241489,2.45585927376145,
13.8499521282529));
#428183=CARTESIAN_POINT('Ctrl Pts',(-1.04038186136928,2.45792922057858,
13.847639871647));
#428184=CARTESIAN_POINT('Ctrl Pts',(-1.03937218357848,2.45994927489359,
13.8452109780794));
#428185=CARTESIAN_POINT('Ctrl Pts',(-1.03891790864111,2.46085813914296,
13.8441181685877));
#428186=CARTESIAN_POINT('Ctrl Pts',(-1.03851467993731,2.46175682465833,
13.8430021611332));
#428187=CARTESIAN_POINT('Ctrl Pts',(-1.03815907134473,2.46263227806838,
13.8418824960098));
#428188=CARTESIAN_POINT('Ctrl Pts',(-1.03732107061554,2.46469530638467,
13.8392439765549));
#428189=CARTESIAN_POINT('Ctrl Pts',(-1.03670395028029,2.46672651997604,
13.8364981347964));
#428190=CARTESIAN_POINT('Ctrl Pts',(-1.03627333558364,2.46872134277917,
13.833693111342));
#428191=CARTESIAN_POINT('Ctrl Pts',(-1.03585394421567,2.47066417350646,
13.8309611966328));
#428192=CARTESIAN_POINT('Ctrl Pts',(-1.03561159464998,2.47257455164312,
13.8281701127186));
#428193=CARTESIAN_POINT('Ctrl Pts',(-1.03555333006732,2.47444199813983,
13.8253580685121));
#428194=CARTESIAN_POINT('Ctrl Pts',(-1.03554069824292,2.47484686255574,
13.8247484142933));
#428195=CARTESIAN_POINT('Ctrl Pts',(-1.03553686562278,2.4752496170513,13.8241378483365));
#428196=CARTESIAN_POINT('Ctrl Pts',(-1.03554215359084,2.4756499570046,13.8235269408515));
#428197=CARTESIAN_POINT('',(-1.05638779057725,2.44359483096628,12.5969504640361));
#428198=CARTESIAN_POINT('Origin',(-1.06992710296501,2.47522639508009,12.584524458991));
#428199=CARTESIAN_POINT('Origin',(-1.06992710296501,2.47522639508009,12.584524458991));
#428200=CARTESIAN_POINT('Ctrl Pts',(-1.09379455227041,2.45047010569483,
12.5893111709658));
#428201=CARTESIAN_POINT('Ctrl Pts',(-1.08564206678204,2.44259637627849,
12.5770542771492));
#428202=CARTESIAN_POINT('Ctrl Pts',(-1.07227821101593,2.4520415355634,12.5737548217797));
#428203=CARTESIAN_POINT('Ctrl Pts',(-1.11162130197801,2.46768730942624,
12.5663937883685));
#428204=CARTESIAN_POINT('Ctrl Pts',(-1.10345841686222,2.45980353597454,
12.5540940315304));
#428205=CARTESIAN_POINT('Ctrl Pts',(-1.09005500260645,2.46928058623304,
12.5508374392248));
#428206=CARTESIAN_POINT('Ctrl Pts',(-1.1294300647137,2.48488714121014,12.5434499600945));
#428207=CARTESIAN_POINT('Ctrl Pts',(-1.12124063915155,2.47697773480345,
12.5311293540533));
#428208=CARTESIAN_POINT('Ctrl Pts',(-1.10781524727627,2.48650194697867,
12.5278936106989));
#428209=CARTESIAN_POINT('Ctrl Pts',(-1.1472222494216,2.50207096181498,12.5204817579905));
#428210=CARTESIAN_POINT('Ctrl Pts',(-1.13899229179957,2.49412240925192,
12.5081597038247));
#428211=CARTESIAN_POINT('Ctrl Pts',(-1.12556024076148,2.50370698278469,
12.5049254088044));
#428212=CARTESIAN_POINT('Ctrl Pts',(-1.1344304865774,2.48971658479254,12.5369868989719));
#428213=CARTESIAN_POINT('Ctrl Pts',(-1.13510051527256,2.49036370357483,
12.5342545179733));
#428214=CARTESIAN_POINT('Ctrl Pts',(-1.13565329867523,2.49107101370702,
12.5314872231885));
#428215=CARTESIAN_POINT('Ctrl Pts',(-1.1360136523182,2.49183309399291,12.5287124745063));
#428216=CARTESIAN_POINT('Ctrl Pts',(-1.13633863711978,2.492520375821,12.5262100684184));
#428217=CARTESIAN_POINT('Ctrl Pts',(-1.13650589535426,2.49325193102789,
12.5237004536639));
#428218=CARTESIAN_POINT('Ctrl Pts',(-1.13645367584698,2.49405509582697,
12.5212220730815));
#428219=CARTESIAN_POINT('Ctrl Pts',(-1.1364136972968,2.49466998795997,12.5193246583486));
#428220=CARTESIAN_POINT('Ctrl Pts',(-1.13624396681212,2.4953341597643,12.517417831369));
#428221=CARTESIAN_POINT('Ctrl Pts',(-1.13584738190643,2.4960425982698,12.5155812248347));
#428222=CARTESIAN_POINT('Ctrl Pts',(-1.13567843460495,2.49634439688102,
12.5147988205793));
#428223=CARTESIAN_POINT('Ctrl Pts',(-1.13546838785177,2.49665467072492,
12.5140295443047));
#428224=CARTESIAN_POINT('Ctrl Pts',(-1.13521068192522,2.49697493687713,
12.5132817086137));
#428225=CARTESIAN_POINT('Ctrl Pts',(-1.13482067886705,2.49745961637389,
12.5121499604604));
#428226=CARTESIAN_POINT('Ctrl Pts',(-1.13430752963695,2.49797316382496,
12.5110494206568));
#428227=CARTESIAN_POINT('Ctrl Pts',(-1.13363782154244,2.49849913262807,
12.5100666561695));
#428228=CARTESIAN_POINT('Ctrl Pts',(-1.13325327669677,2.49880114270361,
12.5095023550641));
#428229=CARTESIAN_POINT('Ctrl Pts',(-1.13281226769082,2.49911022423344,
12.5089719619137));
#428230=CARTESIAN_POINT('Ctrl Pts',(-1.1323193950732,2.49941535350073,12.5085043804652));
#428231=CARTESIAN_POINT('Ctrl Pts',(-1.13159814019849,2.49986187043752,
12.5078201359222));
#428232=CARTESIAN_POINT('Ctrl Pts',(-1.1307442673798,2.50031184735045,12.5072563000949));
#428233=CARTESIAN_POINT('Ctrl Pts',(-1.12981170967374,2.5007272927876,12.5068768744332));
#428234=CARTESIAN_POINT('Ctrl Pts',(-1.12913927137018,2.50102685754714,
12.5066032824114));
#428235=CARTESIAN_POINT('Ctrl Pts',(-1.12841413233554,2.50131378576313,
12.5064197834844));
#428236=CARTESIAN_POINT('Ctrl Pts',(-1.12767773726476,2.50157445815717,
12.5063282718343));
#428237=CARTESIAN_POINT('Ctrl Pts',(-1.12660282844358,2.50195495915033,
12.5061946931565));
#428238=CARTESIAN_POINT('Ctrl Pts',(-1.12548131597894,2.50228865103162,
12.5062515701262));
#428239=CARTESIAN_POINT('Ctrl Pts',(-1.12438721310995,2.50256964663795,
12.5064436508398));
#428240=CARTESIAN_POINT('',(-1.07227821101593,2.4520415355634,12.5737548217797));
#428241=CARTESIAN_POINT('Origin',(-1.07851109820091,2.46629464460456,12.5893111709658));
#428242=CARTESIAN_POINT('Ctrl Pts',(-1.12438721310995,2.50256964663795,
12.5064436508398));
#428243=CARTESIAN_POINT('Ctrl Pts',(-1.11667339252586,2.49509051836337,
12.5164271754438));
#428244=CARTESIAN_POINT('Ctrl Pts',(-1.10895665962532,2.48760827535993,
12.5264061185523));
#428245=CARTESIAN_POINT('Ctrl Pts',(-1.10123691118013,2.48012280860901,
12.536380305637));
#428246=CARTESIAN_POINT('Ctrl Pts',(-1.09158879135733,2.4707674933866,12.5488460165097));
#428247=CARTESIAN_POINT('Ctrl Pts',(-1.08193595844174,2.46140713991218,
12.5613043021964));
#428248=CARTESIAN_POINT('Ctrl Pts',(-1.07227821101593,2.4520415355634,12.5737548217797));
#428249=CARTESIAN_POINT('Ctrl Pts',(-1.03554215359084,2.4756499570046,12.5893111709658));
#428250=CARTESIAN_POINT('Ctrl Pts',(-1.03539245984436,2.46431698624041,
12.5770542771492));
#428251=CARTESIAN_POINT('Ctrl Pts',(-1.05142854144723,2.46105389542322,
12.5737548217797));
#428252=CARTESIAN_POINT('Ctrl Pts',(-1.03540249062735,2.46507639385059,
12.5928319619712));
#428253=CARTESIAN_POINT('Ctrl Pts',(-1.038559345655,2.45741691066269,12.5821634970843));
#428254=CARTESIAN_POINT('Ctrl Pts',(-1.0513682275787,2.45720232696262,12.5773203894503));
#428255=CARTESIAN_POINT('Ctrl Pts',(-1.04218746222939,2.44976142536551,
12.5969440695591));
#428256=CARTESIAN_POINT('Ctrl Pts',(-1.04586998600045,2.44814973022451,
12.5878292599214));
#428257=CARTESIAN_POINT('Ctrl Pts',(-1.0537884005295,2.45174458842127,12.5813877129824));
#428258=CARTESIAN_POINT('Ctrl Pts',(-1.07025149930247,2.43757187784713,
12.596957478804));
#428259=CARTESIAN_POINT('Ctrl Pts',(-1.06659622250853,2.43917173556225,
12.5878468778671));
#428260=CARTESIAN_POINT('Ctrl Pts',(-1.06383528486935,2.44738725169273,
12.5814011370086));
#428261=CARTESIAN_POINT('Ctrl Pts',(-1.08617731002991,2.4431133180763,12.5928371701607));
#428262=CARTESIAN_POINT('Ctrl Pts',(-1.07843856946996,2.44017274666077,
12.5821692192951));
#428263=CARTESIAN_POINT('Ctrl Pts',(-1.0695053509936,2.44934997007645,12.5773318885715));
#428264=CARTESIAN_POINT('Ctrl Pts',(-1.09379455227044,2.45047010569479,
12.5893111709658));
#428265=CARTESIAN_POINT('Ctrl Pts',(-1.08564206678208,2.44259637627845,
12.5770542771492));
#428266=CARTESIAN_POINT('Ctrl Pts',(-1.07227821101596,2.45204153556336,
12.5737548217797));
#428267=CARTESIAN_POINT('',(-1.05142854144723,2.46105389542322,12.5737548217797));
#428268=CARTESIAN_POINT('Origin',(-1.05754023467627,2.47535939107608,12.5893111709658));
#428269=CARTESIAN_POINT('Ctrl Pts',(-1.07227821101596,2.45204153556336,
12.5737548217797));
#428270=CARTESIAN_POINT('Ctrl Pts',(-1.07158045245849,2.45132219376248,
12.5746934679442));
#428271=CARTESIAN_POINT('Ctrl Pts',(-1.07067684772141,2.4506537373934,12.5756680099006));
#428272=CARTESIAN_POINT('Ctrl Pts',(-1.06967218178794,2.45010954071008,
12.5765688348656));
#428273=CARTESIAN_POINT('Ctrl Pts',(-1.06940620760409,2.44996547066263,
12.5768073183026));
#428274=CARTESIAN_POINT('Ctrl Pts',(-1.06913332414911,2.44982992011784,
12.5770407398754));
#428275=CARTESIAN_POINT('Ctrl Pts',(-1.06885573985202,2.44970375316135,
12.5772674179684));
#428276=CARTESIAN_POINT('Ctrl Pts',(-1.06771660895871,2.44918599808889,
12.5781976435658));
#428277=CARTESIAN_POINT('Ctrl Pts',(-1.06642894578207,2.44880713000329,
12.5790594849312));
#428278=CARTESIAN_POINT('Ctrl Pts',(-1.065066065032,2.4486390562553,12.5797571720116));
#428279=CARTESIAN_POINT('Ctrl Pts',(-1.0641780992185,2.44852955016509,12.580211740231));
#428280=CARTESIAN_POINT('Ctrl Pts',(-1.06321555237905,2.44852318131952,
12.5806009430798));
#428281=CARTESIAN_POINT('Ctrl Pts',(-1.06224606640226,2.44863811436578,
12.5808812374708));
#428282=CARTESIAN_POINT('Ctrl Pts',(-1.06141295632457,2.44873687998115,
12.5811221033394));
#428283=CARTESIAN_POINT('Ctrl Pts',(-1.06055767948544,2.44892735643941,
12.581287365893));
#428284=CARTESIAN_POINT('Ctrl Pts',(-1.0597303216127,2.44920693153464,12.581359338449));
#428285=CARTESIAN_POINT('Ctrl Pts',(-1.05961533595268,2.44924578669987,
12.5813693411482));
#428286=CARTESIAN_POINT('Ctrl Pts',(-1.05950085257591,2.44928631573391,
12.5813775999465));
#428287=CARTESIAN_POINT('Ctrl Pts',(-1.05938696720125,2.44932846405683,
12.5813841266931));
#428288=CARTESIAN_POINT('Ctrl Pts',(-1.059193746889,2.44939997378441,12.5813952001081));
#428289=CARTESIAN_POINT('Ctrl Pts',(-1.05900116517332,2.44947719462936,
12.5814007534795));
#428290=CARTESIAN_POINT('Ctrl Pts',(-1.05880937932584,2.44956027600246,
12.5814005856065));
#428291=CARTESIAN_POINT('Ctrl Pts',(-1.05793145869951,2.44994059004576,
12.5813998171494));
#428292=CARTESIAN_POINT('Ctrl Pts',(-1.05713073851232,2.45041712208299,
12.58127954464));
#428293=CARTESIAN_POINT('Ctrl Pts',(-1.05639663229499,2.4509617395348,12.5810700125799));
#428294=CARTESIAN_POINT('Ctrl Pts',(-1.05550991556914,2.45161957540691,
12.5808169217085));
#428295=CARTESIAN_POINT('Ctrl Pts',(-1.05473027932843,2.4523902476405,12.5804173076348));
#428296=CARTESIAN_POINT('Ctrl Pts',(-1.05410774162489,2.45318769492736,
12.5799304713245));
#428297=CARTESIAN_POINT('Ctrl Pts',(-1.05333622129059,2.45417598333758,
12.5793271277669));
#428298=CARTESIAN_POINT('Ctrl Pts',(-1.05273274819342,2.45524688624139,
12.5785808224116));
#428299=CARTESIAN_POINT('Ctrl Pts',(-1.05229512827477,2.45633969211152,
12.5777485681082));
#428300=CARTESIAN_POINT('Ctrl Pts',(-1.05164302665113,2.45796809258384,
12.576508418016));
#428301=CARTESIAN_POINT('Ctrl Pts',(-1.05135830091127,2.45962886070849,
12.5750928681475));
#428302=CARTESIAN_POINT('Ctrl Pts',(-1.05142854144723,2.46105389542322,
12.5737548217797));
#428303=CARTESIAN_POINT('Ctrl Pts',(-1.05142854144723,2.46105389542322,
12.5737548217797));
#428304=CARTESIAN_POINT('Ctrl Pts',(-1.03539245984436,2.46431698624041,
12.5770542771492));
#428305=CARTESIAN_POINT('Ctrl Pts',(-1.03554215359084,2.4756499570046,12.5893111709658));
#428306=CARTESIAN_POINT('Ctrl Pts',(-1.0518059566367,2.48581015749861,12.5508408821982));
#428307=CARTESIAN_POINT('Ctrl Pts',(-1.03571954968216,2.4890802088625,12.55409748406));
#428308=CARTESIAN_POINT('Ctrl Pts',(-1.03586943439953,2.50042763759486,
12.5663972313419));
#428309=CARTESIAN_POINT('Ctrl Pts',(-1.05218182376314,2.51054225380471,
12.52790050457));
#428310=CARTESIAN_POINT('Ctrl Pts',(-1.03604601306511,2.51379600401922,
12.5311362602938));
#428311=CARTESIAN_POINT('Ctrl Pts',(-1.03619638503566,2.52518032157695,
12.5434568539655));
#428312=CARTESIAN_POINT('Ctrl Pts',(-1.05255624928446,2.53525206254306,
12.5049357605811));
#428313=CARTESIAN_POINT('Ctrl Pts',(-1.03637191529783,2.53846931578125,
12.5081700652078));
#428314=CARTESIAN_POINT('Ctrl Pts',(-1.03652303135842,2.54990996669025,
12.5204921097672));
#428315=CARTESIAN_POINT('Ctrl Pts',(-1.05253166145008,2.53362951966586,
12.5064436508395));
#428316=CARTESIAN_POINT('Ctrl Pts',(-1.05150084975772,2.53428241708927,
12.5062361689309));
#428317=CARTESIAN_POINT('Ctrl Pts',(-1.05040104895539,2.53491742088109,
12.5061871075061));
#428318=CARTESIAN_POINT('Ctrl Pts',(-1.04930365262443,2.53547126014831,
12.5063648335164));
#428319=CARTESIAN_POINT('Ctrl Pts',(-1.04880514752069,2.5357228481057,12.5064455676329));
#428320=CARTESIAN_POINT('Ctrl Pts',(-1.04830008621504,2.53596099990856,
12.506574497099));
#428321=CARTESIAN_POINT('Ctrl Pts',(-1.04780967599716,2.53617455374873,
12.5067492519495));
#428322=CARTESIAN_POINT('Ctrl Pts',(-1.04682417762803,2.53660369848009,
12.5071004286051));
#428323=CARTESIAN_POINT('Ctrl Pts',(-1.04586128803358,2.53694854772377,
12.5076537929612));
#428324=CARTESIAN_POINT('Ctrl Pts',(-1.04499646622111,2.53719212333607,
12.5083435010503));
#428325=CARTESIAN_POINT('Ctrl Pts',(-1.04494202051971,2.53720745787651,
12.5083869222963));
#428326=CARTESIAN_POINT('Ctrl Pts',(-1.04488795433255,2.53722238120782,
12.5084308732336));
#428327=CARTESIAN_POINT('Ctrl Pts',(-1.04483428246428,2.53723688536665,
12.5084753333615));
#428328=CARTESIAN_POINT('Ctrl Pts',(-1.04440376324107,2.53735322786407,
12.508831962269));
#428329=CARTESIAN_POINT('Ctrl Pts',(-1.04399021142279,2.53744620749895,
12.509227847131));
#428330=CARTESIAN_POINT('Ctrl Pts',(-1.04360653826916,2.53751579135959,
12.5096423454524));
#428331=CARTESIAN_POINT('Ctrl Pts',(-1.04240427641233,2.5377338363823,12.5109411997424));
#428332=CARTESIAN_POINT('Ctrl Pts',(-1.04142317718106,2.5377450786271,12.5124831113042));
#428333=CARTESIAN_POINT('Ctrl Pts',(-1.04062621246784,2.53763660871718,
12.5140723025008));
#428334=CARTESIAN_POINT('Ctrl Pts',(-1.04055153600132,2.53762644496782,
12.5142212114565));
#428335=CARTESIAN_POINT('Ctrl Pts',(-1.04047845579237,2.5376152515936,12.5143705582413));
#428336=CARTESIAN_POINT('Ctrl Pts',(-1.04040693083171,2.53760311355324,
12.5145201959299));
#428337=CARTESIAN_POINT('Ctrl Pts',(-1.03948808622249,2.5374471823531,12.5164425148273));
#428338=CARTESIAN_POINT('Ctrl Pts',(-1.03879262818321,2.53714059485342,
12.5184635205941));
#428339=CARTESIAN_POINT('Ctrl Pts',(-1.03824723361101,2.53673590294418,
12.5205025929158));
#428340=CARTESIAN_POINT('Ctrl Pts',(-1.03793088314171,2.53650116559633,
12.5216853356836));
#428341=CARTESIAN_POINT('Ctrl Pts',(-1.0376653042346,2.53623423377237,12.5228750347131));
#428342=CARTESIAN_POINT('Ctrl Pts',(-1.03743991167479,2.53594996973572,
12.5240609649613));
#428343=CARTESIAN_POINT('Ctrl Pts',(-1.03688669772864,2.53525225890799,
12.5269717671327));
#428344=CARTESIAN_POINT('Ctrl Pts',(-1.03656815484123,2.53442403827491,
12.5299036066169));
#428345=CARTESIAN_POINT('Ctrl Pts',(-1.03640945547241,2.53350901552302,
12.5328133004019));
#428346=CARTESIAN_POINT('Ctrl Pts',(-1.03633327053459,2.53306975132193,
12.5342101228451));
#428347=CARTESIAN_POINT('Ctrl Pts',(-1.03629453390577,2.53261094157895,
12.5356023438238));
#428348=CARTESIAN_POINT('Ctrl Pts',(-1.03628829969029,2.532138969605,12.5369868989719));
#428349=CARTESIAN_POINT('Origin',(-1.19934860600709,15.2783548945013,-1.24212577218808));
#428350=CARTESIAN_POINT('Ctrl Pts',(-1.13440045166831,2.4896875216687,12.5369868989719));
#428351=CARTESIAN_POINT('Ctrl Pts',(-1.14541345032086,2.50036446712909,
12.5369868989719));
#428352=CARTESIAN_POINT('Ctrl Pts',(-1.15923989832276,2.49372273246592,
12.5369868989719));
#428353=CARTESIAN_POINT('Ctrl Pts',(-1.13812332201667,2.49329669926858,
12.5218025310015));
#428354=CARTESIAN_POINT('Ctrl Pts',(-1.14857564694703,2.49881075106864,
12.5216901060418));
#428355=CARTESIAN_POINT('Ctrl Pts',(-1.15919775786794,2.49374299353988,
12.5161920673677));
#428356=CARTESIAN_POINT('Ctrl Pts',(-1.13723991511127,2.49925955625448,
12.5042015548895));
#428357=CARTESIAN_POINT('Ctrl Pts',(-1.14338789871131,2.50115155061784,
12.4980677368513));
#428358=CARTESIAN_POINT('Ctrl Pts',(-1.14956648980444,2.49832033324227,
12.4907278922778));
#428359=CARTESIAN_POINT('Ctrl Pts',(-1.12437901608947,2.50255140240162,
12.506463626192));
#428360=CARTESIAN_POINT('Ctrl Pts',(-1.12706041626462,2.50851944491462,
12.4999376786891));
#428361=CARTESIAN_POINT('Ctrl Pts',(-1.12702766686024,2.50844655395285,
12.4906970594712));
#428362=CARTESIAN_POINT('Origin',(-1.1497139406469,2.4738920458828,12.5369868989719));
#428363=CARTESIAN_POINT('Origin',(-1.1497139406469,2.4738920458828,14.));
#428364=CARTESIAN_POINT('Origin',(-1.1497139406469,2.4738920458828,13.7435492065112));
#428365=CARTESIAN_POINT('Ctrl Pts',(-1.11662063140439,2.4725156601775,13.793642941384));
#428366=CARTESIAN_POINT('Ctrl Pts',(-1.12437896590609,2.48004656083848,
13.8071662555867));
#428367=CARTESIAN_POINT('Ctrl Pts',(-1.13790823357821,2.46970352937323,
13.8103758687955));
#428368=CARTESIAN_POINT('Ctrl Pts',(-1.12857615642712,2.48406239680105,
13.7804579775006));
#428369=CARTESIAN_POINT('Ctrl Pts',(-1.13815630314232,2.49334757103985,
13.7901904343351));
#428370=CARTESIAN_POINT('Ctrl Pts',(-1.15205695112785,2.48592949111667,
13.7927914348263));
#428371=CARTESIAN_POINT('Ctrl Pts',(-1.13561482397145,2.49086039517658,
13.7597120340895));
#428372=CARTESIAN_POINT('Ctrl Pts',(-1.14670573982784,2.50160184179418,
13.7635825532445));
#428373=CARTESIAN_POINT('Ctrl Pts',(-1.16041970015636,2.49548112220804,
13.7651073818884));
#428374=CARTESIAN_POINT('Ctrl Pts',(-1.13423649169967,2.4895291914376,13.7381884353898));
#428375=CARTESIAN_POINT('Ctrl Pts',(-1.14506717868998,2.50001986014577,
13.7368803041982));
#428376=CARTESIAN_POINT('Ctrl Pts',(-1.15878239724748,2.49361030344978,
13.7363986145813));
#428377=CARTESIAN_POINT('Origin',(-1.13480505391374,2.45949293530441,13.7902182540695));
#428378=CARTESIAN_POINT('Ctrl Pts',(-1.09379172150105,2.45046737066223,
13.8235227101244));
#428379=CARTESIAN_POINT('Ctrl Pts',(-1.10205845368266,2.45845760391019,
13.8358800583119));
#428380=CARTESIAN_POINT('Ctrl Pts',(-1.11552693374205,2.44880223784017,
13.8390832900376));
#428381=CARTESIAN_POINT('Ctrl Pts',(-1.10237119621174,2.45875348935453,
13.8124254819053));
#428382=CARTESIAN_POINT('Ctrl Pts',(-1.11065398246338,2.4667592393222,13.8247886449157));
#428383=CARTESIAN_POINT('Ctrl Pts',(-1.12412954988472,2.4570778208427,13.8279860620657));
#428384=CARTESIAN_POINT('Ctrl Pts',(-1.11094682588098,2.46703589447802,
13.8013225099955));
#428385=CARTESIAN_POINT('Ctrl Pts',(-1.11924175666444,2.47505338517836,
13.8136962257787));
#428386=CARTESIAN_POINT('Ctrl Pts',(-1.13272799552254,2.46534976800002,
13.8168830918626));
#428387=CARTESIAN_POINT('Ctrl Pts',(-1.11951876011343,2.47531473052196,
13.7902140179785));
#428388=CARTESIAN_POINT('Ctrl Pts',(-1.12782218140957,2.48334043275437,
13.802602731458));
#428389=CARTESIAN_POINT('Ctrl Pts',(-1.14132243324893,2.47361822349952,
13.8057746032558));
#428390=CARTESIAN_POINT('Origin',(-1.1090780063399,2.43464556678509,13.8235269408515));
#428391=CARTESIAN_POINT('Ctrl Pts',(-1.03554215359084,2.4756499570046,13.8235269408515));
#428392=CARTESIAN_POINT('Ctrl Pts',(-1.03569810140076,2.48745640859141,
13.8362179249168));
#428393=CARTESIAN_POINT('Ctrl Pts',(-1.01888277881134,2.49044102418992,
13.8391868794938));
#428394=CARTESIAN_POINT('Ctrl Pts',(-1.03539946813276,2.4648475677069,13.8400110824519));
#428395=CARTESIAN_POINT('Ctrl Pts',(-1.03210379973435,2.47435863666198,
13.8494522556836));
#428396=CARTESIAN_POINT('Ctrl Pts',(-1.01876030594897,2.47266185705468,
13.85569149686));
#428397=CARTESIAN_POINT('Ctrl Pts',(-1.0418715466215,2.44989731934508,13.8586819406588));
#428398=CARTESIAN_POINT('Ctrl Pts',(-1.03788061071216,2.45163757053456,
13.868010383617));
#428399=CARTESIAN_POINT('Ctrl Pts',(-1.02963806849073,2.44790215027432,
13.8744918421245));
#428400=CARTESIAN_POINT('Ctrl Pts',(-1.07057230719779,2.43743385913977,
13.8587686893867));
#428401=CARTESIAN_POINT('Ctrl Pts',(-1.07452770130807,2.43570904455491,
13.8680909899357));
#428402=CARTESIAN_POINT('Ctrl Pts',(-1.07741743128625,2.42715650913208,
13.8745789365162));
#428403=CARTESIAN_POINT('Ctrl Pts',(-1.08601110090223,2.44295279209027,
13.8400379222776));
#428404=CARTESIAN_POINT('Ctrl Pts',(-1.09519764051676,2.4470610427908,13.8494748685452));
#428405=CARTESIAN_POINT('Ctrl Pts',(-1.10310113978058,2.43618465530915,
13.8557104837033));
#428406=CARTESIAN_POINT('Ctrl Pts',(-1.09379455227489,2.45047010568997,
13.8235269408542));
#428407=CARTESIAN_POINT('Ctrl Pts',(-1.10228764091277,2.45867279209016,
13.8362179249195));
#428408=CARTESIAN_POINT('Ctrl Pts',(-1.1159825431076,2.44846923104852,13.8391868794965));
#428409=CARTESIAN_POINT('Origin',(-1.01354407250541,2.47594052293312,13.8235269408515));
#428410=CARTESIAN_POINT('Ctrl Pts',(-1.03601449388505,2.51140981661443,
13.7902140241683));
#428411=CARTESIAN_POINT('Ctrl Pts',(-1.03617146712492,2.52295684890825,
13.8026027327198));
#428412=CARTESIAN_POINT('Ctrl Pts',(-1.01984013546842,2.52612947220744,
13.8057746032556));
#428413=CARTESIAN_POINT('Ctrl Pts',(-1.03585709833455,2.49949375982273,
13.8013225161808));
#428414=CARTESIAN_POINT('Ctrl Pts',(-1.0360139074304,2.51102898148478,13.8136962270464));
#428415=CARTESIAN_POINT('Ctrl Pts',(-1.01970571929065,2.51420413579781,
13.8168830918628));
#428416=CARTESIAN_POINT('Ctrl Pts',(-1.03569963492943,2.48757256591174,
13.8124254880875));
#428417=CARTESIAN_POINT('Ctrl Pts',(-1.03585621269812,2.49909089732053,
13.8247886461867));
#428418=CARTESIAN_POINT('Ctrl Pts',(-1.01957150574246,2.5022734877067,13.8279860620656));
#428419=CARTESIAN_POINT('Ctrl Pts',(-1.03554210092266,2.47564602691076,
13.8235227163066));
#428420=CARTESIAN_POINT('Ctrl Pts',(-1.03569837548615,2.48714203323894,
13.8358800595848));
#428421=CARTESIAN_POINT('Ctrl Pts',(-1.01943750119583,2.49033731070925,
13.8390832900376));
#428422=CARTESIAN_POINT('Origin',(-1.01401646563541,2.51170432507903,13.7902182540695));
#428423=CARTESIAN_POINT('Ctrl Pts',(-1.03628470792219,2.53186913360543,
13.7382347919292));
#428424=CARTESIAN_POINT('Ctrl Pts',(-1.03650801198745,2.54695780498591,
13.7369371795942));
#428425=CARTESIAN_POINT('Ctrl Pts',(-1.02242843431407,2.55255327364901,
13.7364597369711));
#428426=CARTESIAN_POINT('Ctrl Pts',(-1.03630969116454,2.53376052722437,
13.7595490285574));
#428427=CARTESIAN_POINT('Ctrl Pts',(-1.03653731775874,2.54920921624813,
13.7633824266926));
#428428=CARTESIAN_POINT('Ctrl Pts',(-1.0226667940499,2.55499732754202,13.7648920890506));
#428429=CARTESIAN_POINT('Ctrl Pts',(-1.03618227800523,2.52411452338656,
13.780380659011));
#428430=CARTESIAN_POINT('Ctrl Pts',(-1.03638456473314,2.53747700691635,
13.7901039518744));
#428431=CARTESIAN_POINT('Ctrl Pts',(-1.02145530532064,2.54253691351826,
13.7926933640892));
#428432=CARTESIAN_POINT('Ctrl Pts',(-1.03596080541507,2.50734761545859,
13.7936647693663));
#428433=CARTESIAN_POINT('Ctrl Pts',(-1.0361336210712,2.51816165571623,13.8072068914933));
#428434=CARTESIAN_POINT('Ctrl Pts',(-1.01931038434322,2.52092262942891,
13.8104111085397));
#428435=CARTESIAN_POINT('Origin',(-1.01429021860486,2.53242953553352,13.7435492065112));
#428436=CARTESIAN_POINT('Origin',(-1.01429021860486,2.53242953553352,14.));
#428437=CARTESIAN_POINT('Origin',(-1.01429021860486,2.53242953553352,12.5369868989719));
#428438=CARTESIAN_POINT('Ctrl Pts',(-1.05252460895684,2.53361254304276,
12.506462012331));
#428439=CARTESIAN_POINT('Ctrl Pts',(-1.05503307119812,2.53965085449332,
12.4999388158272));
#428440=CARTESIAN_POINT('Ctrl Pts',(-1.05500339280016,2.5395794133501,12.4907030323752));
#428441=CARTESIAN_POINT('Ctrl Pts',(-1.04131451142509,2.54072326005886,
12.5042014951932));
#428442=CARTESIAN_POINT('Ctrl Pts',(-1.03848251784149,2.54649568671134,
12.4980716682128));
#428443=CARTESIAN_POINT('Ctrl Pts',(-1.03219205801105,2.54905609299695,
12.4907355092743));
#428444=CARTESIAN_POINT('Ctrl Pts',(-1.03636521467194,2.53728375967444,
12.5218047446509));
#428445=CARTESIAN_POINT('Ctrl Pts',(-1.03322083903367,2.54866935464272,
12.5216906929433));
#428446=CARTESIAN_POINT('Ctrl Pts',(-1.02225870556527,2.55293577986187,
12.5161988840776));
#428447=CARTESIAN_POINT('Ctrl Pts',(-1.03628775876991,2.53210055728633,
12.5369868989719));
#428448=CARTESIAN_POINT('Ctrl Pts',(-1.03651699515108,2.54742873337489,
12.5369868989719));
#428449=CARTESIAN_POINT('Ctrl Pts',(-1.02221667589676,2.55295199334928,
12.5369868989719));
#428450=CARTESIAN_POINT('Origin',(-2.0441221157303E-31,-4.22882474612891E-32,
12.5));
#428451=CARTESIAN_POINT('Origin',(-1.23388492680974,2.38300613697744,12.5));
#428452=CARTESIAN_POINT('',(-1.23388492680974,2.38300613697744,12.5893111709658));
#428453=CARTESIAN_POINT('',(-1.23388492680974,2.38300613697744,13.8235269408515));
#428454=CARTESIAN_POINT('',(-1.23388492680974,2.38300613697744,12.5));
#428455=CARTESIAN_POINT('',(-1.2372708299804,2.41861243359644,13.7902182540695));
#428456=CARTESIAN_POINT('',(-1.23388492680974,2.38300613697744,13.8235269408515));
#428457=CARTESIAN_POINT('',(-1.23923296911494,2.43924636921444,13.7435492065112));
#428458=CARTESIAN_POINT('Origin',(-1.23277788158981,2.37136096293081,13.7445212918691));
#428459=CARTESIAN_POINT('',(-1.23923296911494,2.43924636921444,12.5369868989719));
#428460=CARTESIAN_POINT('',(-1.23923296911494,2.43924636921444,12.5));
#428461=CARTESIAN_POINT('Ctrl Pts',(-1.23923296911494,2.43924636921444,
12.5369868989719));
#428462=CARTESIAN_POINT('Ctrl Pts',(-1.23745158852547,2.42051329787037,
12.5544431401645));
#428463=CARTESIAN_POINT('Ctrl Pts',(-1.23566893384525,2.40176682813578,
12.5718848856037));
#428464=CARTESIAN_POINT('Ctrl Pts',(-1.23388492680974,2.38300613697744,
12.5893111709658));
#428465=CARTESIAN_POINT('Origin',(-1.50261144696405,2.52744636836289,12.5));
#428466=CARTESIAN_POINT('',(-1.33359077777893,2.38896564204893,13.7435492065112));
#428467=CARTESIAN_POINT('',(-1.31755783794952,2.37582965599925,13.7902182540695));
#428468=CARTESIAN_POINT('Origin',(-1.27542604312872,2.34131055501697,13.7418732680455));
#428469=CARTESIAN_POINT('',(-1.28989110379811,2.35316195826444,13.8235269408515));
#428470=CARTESIAN_POINT('',(-1.31755783794952,2.37582965599925,13.7902182540695));
#428471=CARTESIAN_POINT('',(-1.28989110379811,2.35316195826444,12.5893111709658));
#428472=CARTESIAN_POINT('',(-1.28989110379811,2.35316195826444,12.5));
#428473=CARTESIAN_POINT('',(-1.33359077777893,2.38896564204893,12.5369868989719));
#428474=CARTESIAN_POINT('Ctrl Pts',(-1.28989110379811,2.35316195826444,
12.5893111709658));
#428475=CARTESIAN_POINT('Ctrl Pts',(-1.30446849892371,2.36510539852232,
12.5718848856037));
#428476=CARTESIAN_POINT('Ctrl Pts',(-1.31903484374676,2.37703978513054,
12.5544431401645));
#428477=CARTESIAN_POINT('Ctrl Pts',(-1.33359077777893,2.38896564204893,
12.5369868989719));
#428478=CARTESIAN_POINT('',(-1.33359077777893,2.38896564204893,12.5));
#428479=CARTESIAN_POINT('Origin',(-1.2681055525358,2.37975200116018,12.5));
#428480=CARTESIAN_POINT('',(-1.25096085346492,2.34995855446554,13.8587068136939));
#428481=CARTESIAN_POINT('Ctrl Pts',(-1.28989110380218,2.35316195825924,
13.8235269408542));
#428482=CARTESIAN_POINT('Ctrl Pts',(-1.28853565106957,2.35205141905832,
13.8262006681044));
#428483=CARTESIAN_POINT('Ctrl Pts',(-1.28703843394242,2.35104933677319,
13.8288634856214));
#428484=CARTESIAN_POINT('Ctrl Pts',(-1.28541086667981,2.35014881787516,
13.8314912288862));
#428485=CARTESIAN_POINT('Ctrl Pts',(-1.28373301270785,2.34922047577551,
13.834200161153));
#428486=CARTESIAN_POINT('Ctrl Pts',(-1.28191500622142,2.34839860406482,
13.8368750301949));
#428487=CARTESIAN_POINT('Ctrl Pts',(-1.27993243346653,2.34770172933483,
13.8394886372968));
#428488=CARTESIAN_POINT('Ctrl Pts',(-1.27977931456361,2.34764790800905,
13.8396904925131));
#428489=CARTESIAN_POINT('Ctrl Pts',(-1.27962520321311,2.34759485158844,
13.8398919674349));
#428490=CARTESIAN_POINT('Ctrl Pts',(-1.2794700834679,2.34754257904207,13.8400930404591));
#428491=CARTESIAN_POINT('Ctrl Pts',(-1.27705321347805,2.3467281376024,13.8432258934518));
#428492=CARTESIAN_POINT('Ctrl Pts',(-1.27440424006349,2.3461070766296,13.8462331177034));
#428493=CARTESIAN_POINT('Ctrl Pts',(-1.27158753872682,2.34579357131293,
13.8489036603661));
#428494=CARTESIAN_POINT('Ctrl Pts',(-1.27066588126985,2.34569098872488,
13.8497774930041));
#428495=CARTESIAN_POINT('Ctrl Pts',(-1.2697264582903,2.34562149453788,13.85061494757));
#428496=CARTESIAN_POINT('Ctrl Pts',(-1.26877208296604,2.34558953415582,
13.8514076489583));
#428497=CARTESIAN_POINT('Ctrl Pts',(-1.26675344151369,2.34552193333839,
13.8530843267192));
#428498=CARTESIAN_POINT('Ctrl Pts',(-1.26446952301299,2.34561856868024,
13.8546805203176));
#428499=CARTESIAN_POINT('Ctrl Pts',(-1.26205865329298,2.34601015523619,
13.8559412814274));
#428500=CARTESIAN_POINT('Ctrl Pts',(-1.2617360007381,2.34606256221682,13.8561100121513));
#428501=CARTESIAN_POINT('Ctrl Pts',(-1.26141111409554,2.34612018636539,
13.8562727473908));
#428502=CARTESIAN_POINT('Ctrl Pts',(-1.26108435576156,2.34618327171143,
13.8564289040185));
#428503=CARTESIAN_POINT('Ctrl Pts',(-1.25960251044468,2.34646936303604,
13.8571370725437));
#428504=CARTESIAN_POINT('Ctrl Pts',(-1.25805655652251,2.34687503385115,
13.8577210840553));
#428505=CARTESIAN_POINT('Ctrl Pts',(-1.25651403447133,2.34741290263608,
13.8581177131616));
#428506=CARTESIAN_POINT('Ctrl Pts',(-1.25607960716972,2.3475643849988,13.8582294175695));
#428507=CARTESIAN_POINT('Ctrl Pts',(-1.25564542758903,2.34772617711724,
13.8583265086086));
#428508=CARTESIAN_POINT('Ctrl Pts',(-1.25521291800866,2.34789812987871,
13.8584082369006));
#428509=CARTESIAN_POINT('Ctrl Pts',(-1.2545915177237,2.34814517988599,13.8585256585398));
#428510=CARTESIAN_POINT('Ctrl Pts',(-1.25396595863925,2.34841657535878,
13.8586122832068));
#428511=CARTESIAN_POINT('Ctrl Pts',(-1.25335280526454,2.34870599067578,
13.8586682984299));
#428512=CARTESIAN_POINT('Ctrl Pts',(-1.25286234334472,2.34893749424056,
13.8587131050557));
#428513=CARTESIAN_POINT('Ctrl Pts',(-1.25237430186731,2.34918287255886,
13.8587357943552));
#428514=CARTESIAN_POINT('Ctrl Pts',(-1.2518888503355,2.34944260726282,13.8587355499465));
#428515=CARTESIAN_POINT('Ctrl Pts',(-1.25157509143687,2.34961047999432,
13.8587353919793));
#428516=CARTESIAN_POINT('Ctrl Pts',(-1.25126578915053,2.34978250043178,
13.8587257282814));
#428517=CARTESIAN_POINT('Ctrl Pts',(-1.25096085346492,2.34995855446554,
13.8587068136939));
#428518=CARTESIAN_POINT('Ctrl Pts',(-1.25096085346492,2.34995855446554,
13.8587068136939));
#428519=CARTESIAN_POINT('Ctrl Pts',(-1.24995793661838,2.35053758658503,
13.8586446046466));
#428520=CARTESIAN_POINT('Ctrl Pts',(-1.24900219510156,2.35116019736199,
13.858482427929));
#428521=CARTESIAN_POINT('Ctrl Pts',(-1.24809093786802,2.35182281689079,
13.8582284286032));
#428522=CARTESIAN_POINT('Ctrl Pts',(-1.24715609394828,2.35250258744822,
13.8579678548414));
#428523=CARTESIAN_POINT('Ctrl Pts',(-1.24626668415136,2.35322736397738,
13.857615680862));
#428524=CARTESIAN_POINT('Ctrl Pts',(-1.24545165172919,2.35396106122987,
13.8571944833187));
#428525=CARTESIAN_POINT('Ctrl Pts',(-1.24341765496499,2.35579207775985,
13.8561433417727));
#428526=CARTESIAN_POINT('Ctrl Pts',(-1.24174853040234,2.35776073801542,
13.8546163505475));
#428527=CARTESIAN_POINT('Ctrl Pts',(-1.24041326507549,2.35966260114303,
13.8528973491087));
#428528=CARTESIAN_POINT('Ctrl Pts',(-1.24016933180026,2.3600100434771,13.8525833129073));
#428529=CARTESIAN_POINT('Ctrl Pts',(-1.23993640061154,2.36035523793739,
13.8522628768812));
#428530=CARTESIAN_POINT('Ctrl Pts',(-1.23971410366792,2.36069694252038,
13.851937733538));
#428531=CARTESIAN_POINT('Ctrl Pts',(-1.23835656707558,2.36278368499922,
13.8499521282529));
#428532=CARTESIAN_POINT('Ctrl Pts',(-1.23726412632978,2.36494988372643,
13.847639871647));
#428533=CARTESIAN_POINT('Ctrl Pts',(-1.23642246133848,2.36704551459069,
13.8452109780794));
#428534=CARTESIAN_POINT('Ctrl Pts',(-1.2360437788373,2.36798838229392,13.8441181685877));
#428535=CARTESIAN_POINT('Ctrl Pts',(-1.23571514305624,2.36891694439013,
13.8430021611332));
#428536=CARTESIAN_POINT('Ctrl Pts',(-1.23543207530215,2.36981847020278,
13.8418824960098));
#428537=CARTESIAN_POINT('Ctrl Pts',(-1.23476501891126,2.37194293880158,
13.8392439765549));
#428538=CARTESIAN_POINT('Ctrl Pts',(-1.23431551475758,2.37401769473368,
13.8364981347964));
#428539=CARTESIAN_POINT('Ctrl Pts',(-1.23404892947329,2.37604097902391,
13.8336931113419));
#428540=CARTESIAN_POINT('Ctrl Pts',(-1.23378929233613,2.37801152943216,
13.8309611966328));
#428541=CARTESIAN_POINT('Ctrl Pts',(-1.23370346272186,2.37993530468263,
13.8281701127186));
#428542=CARTESIAN_POINT('Ctrl Pts',(-1.2337976062358,2.38180128650958,13.8253580685121));
#428543=CARTESIAN_POINT('Ctrl Pts',(-1.23381801665123,2.38220583338349,
13.8247484142933));
#428544=CARTESIAN_POINT('Ctrl Pts',(-1.23384702501419,2.3826075601408,13.8241378483365));
#428545=CARTESIAN_POINT('Ctrl Pts',(-1.23388492680974,2.38300613697744,
13.8235269408515));
#428546=CARTESIAN_POINT('',(-1.25204841130135,2.3493585587908,12.5969504640361));
#428547=CARTESIAN_POINT('Origin',(-1.26812093887242,2.379781291832,12.584524458991));
#428548=CARTESIAN_POINT('Origin',(-1.26812093887242,2.379781291832,12.584524458991));
#428549=CARTESIAN_POINT('Ctrl Pts',(-1.28989110379811,2.35316195826444,
12.5893111709658));
#428550=CARTESIAN_POINT('Ctrl Pts',(-1.2811239629891,2.34597893128448,12.5770542771492));
#428551=CARTESIAN_POINT('Ctrl Pts',(-1.26857444251691,2.35648194088997,
12.5737548217797));
#428552=CARTESIAN_POINT('Ctrl Pts',(-1.3090618984075,2.36886882757411,12.5663937883685));
#428553=CARTESIAN_POINT('Ctrl Pts',(-1.30028357389284,2.36167663764567,
12.5540940315304));
#428554=CARTESIAN_POINT('Ctrl Pts',(-1.28769722596902,2.37221465649431,
12.5508374392248));
#428555=CARTESIAN_POINT('Ctrl Pts',(-1.32821334992012,2.38455984884519,
12.5434499600945));
#428556=CARTESIAN_POINT('Ctrl Pts',(-1.31940648394648,2.37734427454605,
12.5311293540533));
#428557=CARTESIAN_POINT('Ctrl Pts',(-1.30680207566588,2.38793108976406,
12.5278936106989));
#428558=CARTESIAN_POINT('Ctrl Pts',(-1.34734697350727,2.40023626347626,
12.5204817579905));
#428559=CARTESIAN_POINT('Ctrl Pts',(-1.33849651956565,2.39298497701554,
12.5081597038247));
#428560=CARTESIAN_POINT('Ctrl Pts',(-1.32589039429109,2.40363249552723,
12.5049254088044));
#428561=CARTESIAN_POINT('Ctrl Pts',(-1.33359077777893,2.38896564204893,
12.5369868989719));
#428562=CARTESIAN_POINT('Ctrl Pts',(-1.33431132319719,2.38955599403796,
12.5342545179733));
#428563=CARTESIAN_POINT('Ctrl Pts',(-1.33491991960081,2.39021589367493,
12.5314872231885));
#428564=CARTESIAN_POINT('Ctrl Pts',(-1.33534119081486,2.39094606603426,
12.5287124745063));
#428565=CARTESIAN_POINT('Ctrl Pts',(-1.33572111410573,2.39160457171043,
12.5262100684184));
#428566=CARTESIAN_POINT('Ctrl Pts',(-1.33594744434302,2.39232005962886,
12.5237004536639));
#428567=CARTESIAN_POINT('Ctrl Pts',(-1.33596086397918,2.39312480833795,
12.5212220730815));
#428568=CARTESIAN_POINT('Ctrl Pts',(-1.33597113787156,2.39374091309109,
12.5193246583486));
#428569=CARTESIAN_POINT('Ctrl Pts',(-1.33585610831898,2.39441670952873,
12.517417831369));
#428570=CARTESIAN_POINT('Ctrl Pts',(-1.33551858733187,2.39515511611507,
12.5155812248348));
#428571=CARTESIAN_POINT('Ctrl Pts',(-1.33537480157718,2.39546968128981,
12.5147988205793));
#428572=CARTESIAN_POINT('Ctrl Pts',(-1.33519074393596,2.39579604348345,
12.5140295443047));
#428573=CARTESIAN_POINT('Ctrl Pts',(-1.33496000016923,2.39613624940191,
12.5132817086137));
#428574=CARTESIAN_POINT('Ctrl Pts',(-1.3346108006926,2.39665110503747,12.5121499604604));
#428575=CARTESIAN_POINT('Ctrl Pts',(-1.33414121780903,2.39720477012786,
12.5110494206568));
#428576=CARTESIAN_POINT('Ctrl Pts',(-1.33351660945326,2.39778357624014,
12.5100666561695));
#428577=CARTESIAN_POINT('Ctrl Pts',(-1.33315796077373,2.39811592537693,
12.5095023550641));
#428578=CARTESIAN_POINT('Ctrl Pts',(-1.33274361220289,2.39845992479159,
12.5089719619137));
#428579=CARTESIAN_POINT('Ctrl Pts',(-1.33227725044621,2.39880421246036,
12.5085043804652));
#428580=CARTESIAN_POINT('Ctrl Pts',(-1.33159479076321,2.39930803261697,
12.5078201359221));
#428581=CARTESIAN_POINT('Ctrl Pts',(-1.3307804364317,2.39982611083052,12.5072563000949));
#428582=CARTESIAN_POINT('Ctrl Pts',(-1.32988484439441,2.40031618601774,
12.5068768744332));
#428583=CARTESIAN_POINT('Ctrl Pts',(-1.32923906088276,2.40066956396461,
12.5066032824114));
#428584=CARTESIAN_POINT('Ctrl Pts',(-1.32853972200176,2.40101464301381,
12.5064197834844));
#428585=CARTESIAN_POINT('Ctrl Pts',(-1.3278270244449,2.40133447107659,12.5063282718343));
#428586=CARTESIAN_POINT('Ctrl Pts',(-1.32678670665749,2.40180132103198,
12.5061946931565));
#428587=CARTESIAN_POINT('Ctrl Pts',(-1.32569612491923,2.40222531625855,
12.5062515701262));
#428588=CARTESIAN_POINT('Ctrl Pts',(-1.32462856633783,2.40259455641616,
12.5064436508398));
#428589=CARTESIAN_POINT('',(-1.26857444251691,2.35648194088997,12.5737548217797));
#428590=CARTESIAN_POINT('Origin',(-1.27594835099023,2.37017958571772,12.5893111709658));
#428591=CARTESIAN_POINT('Ctrl Pts',(-1.32462856633783,2.40259455641616,
12.5064436508398));
#428592=CARTESIAN_POINT('Ctrl Pts',(-1.31633079446817,2.39576906231314,
12.5164271754438));
#428593=CARTESIAN_POINT('Ctrl Pts',(-1.30802986609324,2.3889407012261,12.5264061185523));
#428594=CARTESIAN_POINT('Ctrl Pts',(-1.29972566944228,2.38210937291322,
12.536380305637));
#428595=CARTESIAN_POINT('Ctrl Pts',(-1.28934710790115,2.37357159806479,
12.5488460165097));
#428596=CARTESIAN_POINT('Ctrl Pts',(-1.27896343828533,2.36502918588953,
12.5613043021964));
#428597=CARTESIAN_POINT('Ctrl Pts',(-1.26857444251691,2.35648194088997,
12.5737548217797));
#428598=CARTESIAN_POINT('Ctrl Pts',(-1.23388492680974,2.38300613697744,
12.5893111709658));
#428599=CARTESIAN_POINT('Ctrl Pts',(-1.23281198882941,2.37172307716859,
12.5770542771492));
#428600=CARTESIAN_POINT('Ctrl Pts',(-1.24852873949897,2.36716375449456,
12.5737548217797));
#428601=CARTESIAN_POINT('Ctrl Pts',(-1.23288388500602,2.37247914031066,
12.5928319619712));
#428602=CARTESIAN_POINT('Ctrl Pts',(-1.235405916872,2.36458783042964,12.5821634970842));
#428603=CARTESIAN_POINT('Ctrl Pts',(-1.24815468773411,2.3633299179505,12.5773203894503));
#428604=CARTESIAN_POINT('Ctrl Pts',(-1.23839796806602,2.35666209294564,
12.5969440695591));
#428605=CARTESIAN_POINT('Ctrl Pts',(-1.24193687042678,2.35475560071305,
12.5878292599214));
#428606=CARTESIAN_POINT('Ctrl Pts',(-1.25012195140077,2.35769307302062,
12.5813877129824));
#428607=CARTESIAN_POINT('Ctrl Pts',(-1.26537506308586,2.34222562558581,
12.596957478804));
#428608=CARTESIAN_POINT('Ctrl Pts',(-1.26186235218005,2.344118098899,12.5878468778671));
#428609=CARTESIAN_POINT('Ctrl Pts',(-1.25978024216687,2.35253132062618,
12.5814011370086));
#428610=CARTESIAN_POINT('Ctrl Pts',(-1.2816995608148,2.34645052570746,12.5928371701607));
#428611=CARTESIAN_POINT('Ctrl Pts',(-1.27374688640638,2.34415051799933,
12.5821692192952));
#428612=CARTESIAN_POINT('Ctrl Pts',(-1.26559142138311,2.35402534519893,
12.5773318885715));
#428613=CARTESIAN_POINT('Ctrl Pts',(-1.28989110379814,2.3531619582644,12.5893111709658));
#428614=CARTESIAN_POINT('Ctrl Pts',(-1.28112396298914,2.34597893128444,
12.5770542771492));
#428615=CARTESIAN_POINT('Ctrl Pts',(-1.26857444251695,2.35648194088993,
12.5737548217797));
#428616=CARTESIAN_POINT('',(-1.24852873949897,2.36716375449456,12.5737548217797));
#428617=CARTESIAN_POINT('Origin',(-1.25578612727442,2.3809234900544,12.5893111709658));
#428618=CARTESIAN_POINT('Ctrl Pts',(-1.26857444251695,2.35648194088993,
12.5737548217797));
#428619=CARTESIAN_POINT('Ctrl Pts',(-1.26782037265869,2.35582186643966,
12.5746934679442));
#428620=CARTESIAN_POINT('Ctrl Pts',(-1.26686528919211,2.35522928647873,
12.5756680099006));
#428621=CARTESIAN_POINT('Ctrl Pts',(-1.2658196091199,2.35476879016542,12.5765688348656));
#428622=CARTESIAN_POINT('Ctrl Pts',(-1.26554277689685,2.35464687886433,
12.5768073183026));
#428623=CARTESIAN_POINT('Ctrl Pts',(-1.26525975281126,2.3545340218877,12.5770407398754));
#428624=CARTESIAN_POINT('Ctrl Pts',(-1.26497280837479,2.35443090043853,
12.5772674179684));
#428625=CARTESIAN_POINT('Ctrl Pts',(-1.26379526600055,2.35400771789635,
12.5781976435658));
#428626=CARTESIAN_POINT('Ctrl Pts',(-1.26248100615068,2.35373506696603,
12.5790594849312));
#428627=CARTESIAN_POINT('Ctrl Pts',(-1.2611089607031,2.35367863990307,12.5797571720116));
#428628=CARTESIAN_POINT('Ctrl Pts',(-1.26021502375964,2.35364187564261,
12.580211740231));
#428629=CARTESIAN_POINT('Ctrl Pts',(-1.25925516059535,2.35371398449211,
12.5806009430798));
#428630=CARTESIAN_POINT('Ctrl Pts',(-1.25829826861342,2.35390755721551,
12.5808812374708));
#428631=CARTESIAN_POINT('Ctrl Pts',(-1.25747598095534,2.354073900402,12.5811221033394));
#428632=CARTESIAN_POINT('Ctrl Pts',(-1.25663907557899,2.35433345606794,
12.581287365893));
#428633=CARTESIAN_POINT('Ctrl Pts',(-1.25583725863703,2.35467953824755,
12.581359338449));
#428634=CARTESIAN_POINT('Ctrl Pts',(-1.25572582263898,2.35472763652419,
12.5813693411482));
#428635=CARTESIAN_POINT('Ctrl Pts',(-1.25561502368873,2.35477736215924,
12.5813775999465));
#428636=CARTESIAN_POINT('Ctrl Pts',(-1.25550495273787,2.35482865295239,
12.5813841266931));
#428637=CARTESIAN_POINT('Ctrl Pts',(-1.25531820405693,2.35491567398647,
12.5813952001081));
#428638=CARTESIAN_POINT('Ctrl Pts',(-1.25513255735676,2.3550083350831,12.5814007534795));
#428639=CARTESIAN_POINT('Ctrl Pts',(-1.25494818156407,2.3551067723368,12.5814005856065));
#428640=CARTESIAN_POINT('Ctrl Pts',(-1.25410418127139,2.35555737959776,
12.5813998171494));
#428641=CARTESIAN_POINT('Ctrl Pts',(-1.25334496719951,2.35609759214273,
12.58127954464));
#428642=CARTESIAN_POINT('Ctrl Pts',(-1.25265769503836,2.35670023389671,
12.5810700125799));
#428643=CARTESIAN_POINT('Ctrl Pts',(-1.2518275485199,2.35742815651926,12.5808169217085));
#428644=CARTESIAN_POINT('Ctrl Pts',(-1.25111332339607,2.35825981199598,
12.5804173076348));
#428645=CARTESIAN_POINT('Ctrl Pts',(-1.2505578564924,2.35910534844497,12.5799304713245));
#428646=CARTESIAN_POINT('Ctrl Pts',(-1.24986945800863,2.36015323447673,
12.5793271277669));
#428647=CARTESIAN_POINT('Ctrl Pts',(-1.24935528144683,2.36126976269925,
12.5785808224116));
#428648=CARTESIAN_POINT('Ctrl Pts',(-1.24900819149589,2.36239460243404,
12.5777485681082));
#428649=CARTESIAN_POINT('Ctrl Pts',(-1.24849098944245,2.36407073687427,
12.576508418016));
#428650=CARTESIAN_POINT('Ctrl Pts',(-1.24834257912397,2.36574918672104,
12.5750928681475));
#428651=CARTESIAN_POINT('Ctrl Pts',(-1.24852873949897,2.36716375449456,
12.5737548217797));
#428652=CARTESIAN_POINT('Ctrl Pts',(-1.24852873949897,2.36716375449456,
12.5737548217797));
#428653=CARTESIAN_POINT('Ctrl Pts',(-1.23281198882941,2.37172307716859,
12.5770542771492));
#428654=CARTESIAN_POINT('Ctrl Pts',(-1.23388492680974,2.38300613697744,
12.5893111709658));
#428655=CARTESIAN_POINT('Ctrl Pts',(-1.25092276405561,2.39180687930844,
12.5508408821982));
#428656=CARTESIAN_POINT('Ctrl Pts',(-1.23515642283701,2.39637724135191,
12.55409748406));
#428657=CARTESIAN_POINT('Ctrl Pts',(-1.23623072961141,2.40767469545534,
12.5663972313419));
#428658=CARTESIAN_POINT('Ctrl Pts',(-1.25331327596572,2.41642604494416,
12.52790050457));
#428659=CARTESIAN_POINT('Ctrl Pts',(-1.23749636669548,2.42098418694264,
12.5311362602938));
#428660=CARTESIAN_POINT('Ctrl Pts',(-1.23857416588352,2.4323183674113,12.5434568539655));
#428661=CARTESIAN_POINT('Ctrl Pts',(-1.25570053442384,2.44102311467636,
12.5049357605811));
#428662=CARTESIAN_POINT('Ctrl Pts',(-1.23983228847987,2.44554883623774,
12.5081700652078));
#428663=CARTESIAN_POINT('Ctrl Pts',(-1.24091542097314,2.45693910196279,
12.5204921097672));
#428664=CARTESIAN_POINT('Ctrl Pts',(-1.25554377609601,2.4394079748135,12.5064436508395));
#428665=CARTESIAN_POINT('Ctrl Pts',(-1.25456961154573,2.44014272049711,
12.5062361689309));
#428666=CARTESIAN_POINT('Ctrl Pts',(-1.25352522894396,2.44086525534164,
12.5061871075061));
#428667=CARTESIAN_POINT('Ctrl Pts',(-1.25247662715064,2.44150669974309,
12.5063648335164));
#428668=CARTESIAN_POINT('Ctrl Pts',(-1.25200028753567,2.44179808335616,
12.5064455676329));
#428669=CARTESIAN_POINT('Ctrl Pts',(-1.25151631836267,2.44207660991371,
12.506574497099));
#428670=CARTESIAN_POINT('Ctrl Pts',(-1.25104494656484,2.4423294261566,12.5067492519495));
#428671=CARTESIAN_POINT('Ctrl Pts',(-1.25009770663982,2.44283747021027,
12.5071004286051));
#428672=CARTESIAN_POINT('Ctrl Pts',(-1.24916612939584,2.44325965643752,
12.5076537929612));
#428673=CARTESIAN_POINT('Ctrl Pts',(-1.24832403888024,2.4435729125784,12.5083435010503));
#428674=CARTESIAN_POINT('Ctrl Pts',(-1.24827102424984,2.44359263392453,
12.5083869222963));
#428675=CARTESIAN_POINT('Ctrl Pts',(-1.24821835435351,2.44361191449586,
12.5084308732336));
#428676=CARTESIAN_POINT('Ctrl Pts',(-1.24816604329756,2.44363074514883,
12.5084753333615));
#428677=CARTESIAN_POINT('Ctrl Pts',(-1.24774643958516,2.44378179183962,
12.508831962269));
#428678=CARTESIAN_POINT('Ctrl Pts',(-1.24734184252986,2.44390817040486,
12.509227847131));
#428679=CARTESIAN_POINT('Ctrl Pts',(-1.24696511774763,2.44400879565481,
12.5096423454524));
#428680=CARTESIAN_POINT('Ctrl Pts',(-1.24578462901153,2.44432411065328,
12.5109411997424));
#428681=CARTESIAN_POINT('Ctrl Pts',(-1.24480771065434,2.44441528418586,
12.5124831113042));
#428682=CARTESIAN_POINT('Ctrl Pts',(-1.24400455647081,2.44437213522341,
12.5140723025008));
#428683=CARTESIAN_POINT('Ctrl Pts',(-1.24392930004414,2.44436809211837,
12.5142212114565));
#428684=CARTESIAN_POINT('Ctrl Pts',(-1.24385555063965,2.44436289270466,
12.5143705582413));
#428685=CARTESIAN_POINT('Ctrl Pts',(-1.24378327430942,2.44435662500092,
12.5145201959299));
#428686=CARTESIAN_POINT('Ctrl Pts',(-1.24285477723943,2.44427610701477,
12.5164425148273));
#428687=CARTESIAN_POINT('Ctrl Pts',(-1.24213664355196,2.44402722594623,
12.5184635205941));
#428688=CARTESIAN_POINT('Ctrl Pts',(-1.24156007758763,2.44366833533676,
12.5205025929157));
#428689=CARTESIAN_POINT('Ctrl Pts',(-1.24122564647538,2.44346016455818,
12.5216853356836));
#428690=CARTESIAN_POINT('Ctrl Pts',(-1.24093919383844,2.44321576807429,
12.5228750347131));
#428691=CARTESIAN_POINT('Ctrl Pts',(-1.24069138109582,2.44295082148883,
12.5240609649613));
#428692=CARTESIAN_POINT('Ctrl Pts',(-1.24008313801374,2.44230052430872,
12.5269717671327));
#428693=CARTESIAN_POINT('Ctrl Pts',(-1.2396981473811,2.44150102371401,12.5299036066169));
#428694=CARTESIAN_POINT('Ctrl Pts',(-1.23946539322239,2.44060198109668,
12.5328133004019));
#428695=CARTESIAN_POINT('Ctrl Pts',(-1.23935365767335,2.44017038829069,
12.5342101228451));
#428696=CARTESIAN_POINT('Ctrl Pts',(-1.23927765268403,2.43971626259414,
12.5356023438238));
#428697=CARTESIAN_POINT('Ctrl Pts',(-1.23923296911494,2.43924636921444,
12.5369868989719));
#428698=CARTESIAN_POINT('Origin',(-2.44055823560797,15.1283953684929,-1.24064857945397));
#428699=CARTESIAN_POINT('Ctrl Pts',(-1.33355847389414,2.38893912375418,
12.5369868989719));
#428700=CARTESIAN_POINT('Ctrl Pts',(-1.34540509787711,2.39868288092943,
12.5369868989719));
#428701=CARTESIAN_POINT('Ctrl Pts',(-1.35864417647996,2.39093626221983,
12.5369868989719));
#428702=CARTESIAN_POINT('Ctrl Pts',(-1.33756313817891,2.39223284361851,
12.5218025310015));
#428703=CARTESIAN_POINT('Ctrl Pts',(-1.34843013027199,2.39687658634958,
12.5216901060417));
#428704=CARTESIAN_POINT('Ctrl Pts',(-1.35860382770967,2.390959890715,12.5161920673677));
#428705=CARTESIAN_POINT('Ctrl Pts',(-1.33716869893787,2.39824786555357,
12.5042015548895));
#428706=CARTESIAN_POINT('Ctrl Pts',(-1.34345044073467,2.39963244672326,
12.4980677368515));
#428707=CARTESIAN_POINT('Ctrl Pts',(-1.3493777025758,2.39630703745667,12.4907278922778));
#428708=CARTESIAN_POINT('Ctrl Pts',(-1.32461890951763,2.40257704101929,
12.506463626192));
#428709=CARTESIAN_POINT('Ctrl Pts',(-1.32777783842431,2.40830666635597,
12.4999376786891));
#428710=CARTESIAN_POINT('Ctrl Pts',(-1.32773925670079,2.40823668731335,
12.4906970594712));
#428711=CARTESIAN_POINT('Origin',(-1.3475335305868,2.37194801459566,12.5369868989719));
#428712=CARTESIAN_POINT('Origin',(-1.3475335305868,2.37194801459566,14.));
#428713=CARTESIAN_POINT('Origin',(-1.3475335305868,2.37194801459566,13.7435492065112));
#428714=CARTESIAN_POINT('Ctrl Pts',(-1.31443814838807,2.3732736206268,13.793642941384));
#428715=CARTESIAN_POINT('Ctrl Pts',(-1.32278450598908,2.38014708655031,
13.8071662555867));
#428716=CARTESIAN_POINT('Ctrl Pts',(-1.33542570305467,2.36873570975417,
13.8103758687955));
#428717=CARTESIAN_POINT('Ctrl Pts',(-1.32729505861706,2.38380745015776,
13.7804579775006));
#428718=CARTESIAN_POINT('Ctrl Pts',(-1.33760015608416,2.39228085785026,
13.7901904343351));
#428719=CARTESIAN_POINT('Ctrl Pts',(-1.3508499084304,2.38375442911789,13.7927914348262));
#428720=CARTESIAN_POINT('Ctrl Pts',(-1.3348644055529,2.3900091120058,13.7597120340895));
#428721=CARTESIAN_POINT('Ctrl Pts',(-1.34679394491978,2.39981080474053,
13.7635825532445));
#428722=CARTESIAN_POINT('Ctrl Pts',(-1.35996337770837,2.39259263626295,
13.7651073818885));
#428723=CARTESIAN_POINT('Ctrl Pts',(-1.33338215410505,2.38879468461343,
13.7381884353898));
#428724=CARTESIAN_POINT('Ctrl Pts',(-1.3450318897682,2.39836764494998,13.7368803041982));
#428725=CARTESIAN_POINT('Ctrl Pts',(-1.35817903369322,2.39086149788683,
13.7363986145813));
#428726=CARTESIAN_POINT('Origin',(-1.3315005907574,2.35881202854597,13.7902182540695));
#428727=CARTESIAN_POINT('Ctrl Pts',(-1.28988805951734,2.35315946306641,
13.8235227101244));
#428728=CARTESIAN_POINT('Ctrl Pts',(-1.29877856301699,2.36044929405501,
13.8358800583119));
#428729=CARTESIAN_POINT('Ctrl Pts',(-1.31141522584932,2.34972824925896,
13.8390832900376));
#428730=CARTESIAN_POINT('Ctrl Pts',(-1.2991143823317,2.36071870354545,13.8124254819053));
#428731=CARTESIAN_POINT('Ctrl Pts',(-1.30802215123948,2.36802269106741,
13.8247886449158));
#428732=CARTESIAN_POINT('Ctrl Pts',(-1.32066375433791,2.35727510286332,
13.8279860620657));
#428733=CARTESIAN_POINT('Ctrl Pts',(-1.30833657020832,2.36827455621884,
13.8013225099955));
#428734=CARTESIAN_POINT('Ctrl Pts',(-1.31725740021674,2.37558925551505,
13.8136962257787));
#428735=CARTESIAN_POINT('Ctrl Pts',(-1.32990782984351,2.3648186726553,13.8168830918626));
#428736=CARTESIAN_POINT('Ctrl Pts',(-1.31755478403128,2.37582715290089,
13.7902140179785));
#428737=CARTESIAN_POINT('Ctrl Pts',(-1.32648474561696,2.38314934435037,
13.802602731458));
#428738=CARTESIAN_POINT('Ctrl Pts',(-1.33914762617117,2.37235908908966,
13.8057746032558));
#428739=CARTESIAN_POINT('Origin',(-1.30383385660598,2.33614433081117,13.8235269408515));
#428740=CARTESIAN_POINT('Ctrl Pts',(-1.23388492680974,2.38300613697744,
13.8235269408515));
#428741=CARTESIAN_POINT('Ctrl Pts',(-1.23500269112627,2.3947605923763,13.8362179249168));
#428742=CARTESIAN_POINT('Ctrl Pts',(-1.2184865940147,2.3991058818095,13.8391868794938));
#428743=CARTESIAN_POINT('Ctrl Pts',(-1.23286222111351,2.37225132192846,
13.8400110824519));
#428744=CARTESIAN_POINT('Ctrl Pts',(-1.2303527591961,2.38199937115624,13.8494522556837));
#428745=CARTESIAN_POINT('Ctrl Pts',(-1.21691536149542,2.38139585606149,
13.85569149686));
#428746=CARTESIAN_POINT('Ctrl Pts',(-1.23809418026215,2.35682328480407,
13.8586819406588));
#428747=CARTESIAN_POINT('Ctrl Pts',(-1.23425837049046,2.35888304377793,
13.868010383617));
#428748=CARTESIAN_POINT('Ctrl Pts',(-1.22573878321916,2.35583189653154,
13.8744918421245));
#428749=CARTESIAN_POINT('Ctrl Pts',(-1.26568355371342,2.34206191730261,
13.8587686893867));
#428750=CARTESIAN_POINT('Ctrl Pts',(-1.26948519817504,2.34002044055592,
13.8680909899357));
#428751=CARTESIAN_POINT('Ctrl Pts',(-1.27166820178028,2.33126082316899,
13.8745789365163));
#428752=CARTESIAN_POINT('Ctrl Pts',(-1.28152082037615,2.3463040814453,13.8400379222776));
#428753=CARTESIAN_POINT('Ctrl Pts',(-1.29101165310921,2.34964987401829,
13.8494748685453));
#428754=CARTESIAN_POINT('Ctrl Pts',(-1.29800232757999,2.33816546825623,
13.8557104837033));
#428755=CARTESIAN_POINT('Ctrl Pts',(-1.28989110380218,2.35316195825924,
13.8235269408542));
#428756=CARTESIAN_POINT('Ctrl Pts',(-1.29902452747989,2.36064508532712,
13.8362179249195));
#428757=CARTESIAN_POINT('Ctrl Pts',(-1.31184217606728,2.34935921412697,
13.8391868794965));
#428758=CARTESIAN_POINT('Origin',(-1.21198372634507,2.38508878390049,13.8235269408515));
#428759=CARTESIAN_POINT('Ctrl Pts',(-1.23727045596713,2.41860850848543,
13.7902140241683));
#428760=CARTESIAN_POINT('Ctrl Pts',(-1.23836809722087,2.43010432420553,
13.8026027327198));
#428761=CARTESIAN_POINT('Ctrl Pts',(-1.22234970497529,2.43459754600511,
13.8057746032556));
#428762=CARTESIAN_POINT('Ctrl Pts',(-1.23614231488555,2.40674493058826,
13.8013225161808));
#428763=CARTESIAN_POINT('Ctrl Pts',(-1.2372388298653,2.41822898835476,13.8136962270464));
#428764=CARTESIAN_POINT('Ctrl Pts',(-1.22124371042945,2.42272284633497,
13.8168830918628));
#428765=CARTESIAN_POINT('Ctrl Pts',(-1.2350136874522,2.3948762381959,13.8124254880875));
#428766=CARTESIAN_POINT('Ctrl Pts',(-1.23610859516207,2.40634348076539,
13.8247886461867));
#428767=CARTESIAN_POINT('Ctrl Pts',(-1.22013748488761,2.41084283614132,
13.8279860620656));
#428768=CARTESIAN_POINT('Ctrl Pts',(-1.23388455397768,2.38300222425361,
13.8235227163065));
#428769=CARTESIAN_POINT('Ctrl Pts',(-1.23497733978991,2.39444724074138,
13.8358800595847));
#428770=CARTESIAN_POINT('Ctrl Pts',(-1.2190310169947,2.39895729840275,13.8390832900376));
#428771=CARTESIAN_POINT('Origin',(-1.21536962951573,2.42069508051949,13.7902182540695));
#428772=CARTESIAN_POINT('Ctrl Pts',(-1.23920739515915,2.43897772383434,
13.7382347919292));
#428773=CARTESIAN_POINT('Ctrl Pts',(-1.24065982299245,2.45399798755115,
13.7369371795942));
#428774=CARTESIAN_POINT('Ctrl Pts',(-1.22708317659414,2.46072245404268,
13.7364597369712));
#428775=CARTESIAN_POINT('Ctrl Pts',(-1.23938646141061,2.44086078763087,
13.7595490285574));
#428776=CARTESIAN_POINT('Ctrl Pts',(-1.24087254217017,2.45623951873574,
13.7633824266926));
#428777=CARTESIAN_POINT('Ctrl Pts',(-1.22751995628939,2.46313894701669,
13.7648920890506));
#428778=CARTESIAN_POINT('Ctrl Pts',(-1.23847323334616,2.43125726543041,
13.7803806590111));
#428779=CARTESIAN_POINT('Ctrl Pts',(-1.2397640134406,2.44455879815232,13.7901039518744));
#428780=CARTESIAN_POINT('Ctrl Pts',(-1.22529685926915,2.45081874157102,
13.7926933640892));
#428781=CARTESIAN_POINT('Ctrl Pts',(-1.23688583903527,2.41456420007755,
13.7936647693663));
#428782=CARTESIAN_POINT('Ctrl Pts',(-1.23793952433521,2.42532817142801,
13.8072068914933));
#428783=CARTESIAN_POINT('Ctrl Pts',(-1.22139731052884,2.42945120820106,
13.8104111085397));
#428784=CARTESIAN_POINT('Origin',(-1.21733176865027,2.44132901613749,13.7435492065112));
#428785=CARTESIAN_POINT('Origin',(-1.21733176865027,2.44132901613749,14.));
#428786=CARTESIAN_POINT('Origin',(-1.21733176865027,2.44132901613749,12.5369868989719));
#428787=CARTESIAN_POINT('Ctrl Pts',(-1.25553536331697,2.43939162952238,
12.506462012331));
#428788=CARTESIAN_POINT('Ctrl Pts',(-1.25852765729725,2.44520538602962,
12.4999388158272));
#428789=CARTESIAN_POINT('Ctrl Pts',(-1.25849225453531,2.44513660166587,
12.4907030323752));
#428790=CARTESIAN_POINT('Ctrl Pts',(-1.2449421559095,2.44739241323252,12.5042014951932));
#428791=CARTESIAN_POINT('Ctrl Pts',(-1.24259009191169,2.45337646637956,
12.4980716682127));
#428792=CARTESIAN_POINT('Ctrl Pts',(-1.23652925994931,2.45644108399838,
12.4907355092744));
#428793=CARTESIAN_POINT('Ctrl Pts',(-1.2397289763209,2.44436777113429,12.5218047446509));
#428794=CARTESIAN_POINT('Ctrl Pts',(-1.23752309502183,2.45597177728004,
12.5216906929434));
#428795=CARTESIAN_POINT('Ctrl Pts',(-1.22694519041112,2.46111752196638,
12.5161988840775));
#428796=CARTESIAN_POINT('Ctrl Pts',(-1.23922929903385,2.43920812879961,
12.5369868989719));
#428797=CARTESIAN_POINT('Ctrl Pts',(-1.24070716130095,2.45446661675355,
12.5369868989719));
#428798=CARTESIAN_POINT('Ctrl Pts',(-1.22690462214259,2.46113710731293,
12.5369868989719));
#428799=CARTESIAN_POINT('Origin',(-2.42277625004775E-31,-6.05232695006712E-32,
12.5));
#428800=CARTESIAN_POINT('Origin',(-1.42401639941741,2.27450380427704,12.5));
#428801=CARTESIAN_POINT('',(-1.42401639941741,2.27450380427704,12.5893111709658));
#428802=CARTESIAN_POINT('',(-1.42401639941741,2.27450380427704,13.8235269408515));
#428803=CARTESIAN_POINT('',(-1.42401639941741,2.27450380427704,12.5));
#428804=CARTESIAN_POINT('',(-1.43029328000177,2.30971564133975,13.7902182540695));
#428805=CARTESIAN_POINT('',(-1.42401639941741,2.27450380427704,13.8235269408515));
#428806=CARTESIAN_POINT('',(-1.43393074758918,2.33012098668408,13.7435492065112));
#428807=CARTESIAN_POINT('Origin',(-1.42196384800666,2.26298761305396,13.7445212918707));
#428808=CARTESIAN_POINT('',(-1.43393074758918,2.33012098668408,12.5369868989719));
#428809=CARTESIAN_POINT('',(-1.43393074758918,2.33012098668408,12.5));
#428810=CARTESIAN_POINT('Ctrl Pts',(-1.43393074758918,2.33012098668408,
12.5369868989719));
#428811=CARTESIAN_POINT('Ctrl Pts',(-1.43062837517278,2.31159544714511,
12.5544431401645));
#428812=CARTESIAN_POINT('Ctrl Pts',(-1.42732364081185,2.29305665764788,
12.5718848856037));
#428813=CARTESIAN_POINT('Ctrl Pts',(-1.42401639941741,2.27450380427704,
12.5893111709658));
#428814=CARTESIAN_POINT('Origin',(-1.70362197401988,2.39655971658016,12.5));
#428815=CARTESIAN_POINT('',(-1.52387624238132,2.27231652710908,13.7435492065112));
#428816=CARTESIAN_POINT('',(-1.50682594602498,2.26053108340798,13.7902182540695));
#428817=CARTESIAN_POINT('Origin',(-1.46202071408172,2.22956097429398,13.7418732680435));
#428818=CARTESIAN_POINT('',(-1.47740364284708,2.2401939062462,13.8235269408515));
#428819=CARTESIAN_POINT('',(-1.50682594602498,2.26053108340798,13.7902182540695));
#428820=CARTESIAN_POINT('',(-1.47740364284708,2.2401939062462,12.5893111709658));
#428821=CARTESIAN_POINT('',(-1.47740364284708,2.2401939062462,12.5));
#428822=CARTESIAN_POINT('',(-1.52387624238132,2.27231652710908,12.5369868989719));
#428823=CARTESIAN_POINT('Ctrl Pts',(-1.47740364284708,2.2401939062462,12.5893111709658));
#428824=CARTESIAN_POINT('Ctrl Pts',(-1.49290603415146,2.25090941265921,
12.5718848856037));
#428825=CARTESIAN_POINT('Ctrl Pts',(-1.50839667396577,2.26161679625009,
12.5544431401645));
#428826=CARTESIAN_POINT('Ctrl Pts',(-1.52387624238132,2.27231652710908,
12.5369868989719));
#428827=CARTESIAN_POINT('',(-1.52387624238132,2.27231652710908,12.5));
#428828=CARTESIAN_POINT('Origin',(-1.45785791655534,2.2684711976428,12.5));
#428829=CARTESIAN_POINT('',(-1.43834182256171,2.2401743383222,13.8587068136939));
#428830=CARTESIAN_POINT('Ctrl Pts',(-1.47740364285072,2.24019390624068,
13.8235269408542));
#428831=CARTESIAN_POINT('Ctrl Pts',(-1.47596218102064,2.23919754424846,
13.8262006681044));
#428832=CARTESIAN_POINT('Ctrl Pts',(-1.47438826675084,2.23832083340481,
13.8288634856214));
#428833=CARTESIAN_POINT('Ctrl Pts',(-1.47269271443384,2.23755597275063,
13.8314912288862));
#428834=CARTESIAN_POINT('Ctrl Pts',(-1.47094477488312,2.23676748030788,
13.8342001611531));
#428835=CARTESIAN_POINT('Ctrl Pts',(-1.46906582748899,2.2360965277137,13.8368750301949));
#428836=CARTESIAN_POINT('Ctrl Pts',(-1.46703304982142,2.23556356986172,
13.8394886372969));
#428837=CARTESIAN_POINT('Ctrl Pts',(-1.46687605347133,2.23552240823403,
13.8396904925131));
#428838=CARTESIAN_POINT('Ctrl Pts',(-1.46671813032281,2.23548208986005,
13.8398919674349));
#428839=CARTESIAN_POINT('Ctrl Pts',(-1.46655926602795,2.23544263494557,
13.8400930404591));
#428840=CARTESIAN_POINT('Ctrl Pts',(-1.46408405343539,2.23482790083391,
13.8432258934518));
#428841=CARTESIAN_POINT('Ctrl Pts',(-1.4613932720264,2.23442482231541,13.8462331177034));
#428842=CARTESIAN_POINT('Ctrl Pts',(-1.45856038943732,2.23434194746974,
13.8489036603661));
#428843=CARTESIAN_POINT('Ctrl Pts',(-1.45763343728625,2.23431482985578,
13.849777493004));
#428844=CARTESIAN_POINT('Ctrl Pts',(-1.45669147573778,2.23432213859897,
13.85061494757));
#428845=CARTESIAN_POINT('Ctrl Pts',(-1.45573767095083,2.23436807501136,
13.8514076489583));
#428846=CARTESIAN_POINT('Ctrl Pts',(-1.45372023626719,2.23446523714859,
13.8530843267192));
#428847=CARTESIAN_POINT('Ctrl Pts',(-1.45145179399437,2.23474771150499,
13.8546805203176));
#428848=CARTESIAN_POINT('Ctrl Pts',(-1.44908086418411,2.23533450335257,
13.8559412814274));
#428849=CARTESIAN_POINT('Ctrl Pts',(-1.44876355688443,2.23541303513189,
13.8561100121513));
#428850=CARTESIAN_POINT('Ctrl Pts',(-1.44844444817843,2.23549694881832,
13.8562727473908));
#428851=CARTESIAN_POINT('Ctrl Pts',(-1.4481239191472,2.23558645809077,13.8564289040185));
#428852=CARTESIAN_POINT('Ctrl Pts',(-1.44667032364727,2.2359923816202,13.8571370725437));
#428853=CARTESIAN_POINT('Ctrl Pts',(-1.44516257969674,2.23652271219574,
13.8577210840554));
#428854=CARTESIAN_POINT('Ctrl Pts',(-1.44366903155974,2.2371845211339,13.8581177131616));
#428855=CARTESIAN_POINT('Ctrl Pts',(-1.44324839699799,2.23737090930966,
13.8582294175695));
#428856=CARTESIAN_POINT('Ctrl Pts',(-1.4428288496737,2.23756755274473,13.8583265086086));
#428857=CARTESIAN_POINT('Ctrl Pts',(-1.44241179497967,2.2377741868936,13.8584082369006));
#428858=CARTESIAN_POINT('Ctrl Pts',(-1.44181259922199,2.23807106475438,
13.8585256585398));
#428859=CARTESIAN_POINT('Ctrl Pts',(-1.44121124288433,2.23839254605391,
13.8586122832068));
#428860=CARTESIAN_POINT('Ctrl Pts',(-1.44062371976203,2.23873097605759,
13.8586682984299));
#428861=CARTESIAN_POINT('Ctrl Pts',(-1.44015375950349,2.23900168651305,
13.8587131050557));
#428862=CARTESIAN_POINT('Ctrl Pts',(-1.43968734255476,2.23928602826641,
13.8587357943552));
#428863=CARTESIAN_POINT('Ctrl Pts',(-1.43922467711251,2.23958446753113,
13.8587355499465));
#428864=CARTESIAN_POINT('Ctrl Pts',(-1.43892564540677,2.23977735594301,
13.8587353919793));
#428865=CARTESIAN_POINT('Ctrl Pts',(-1.43863139356086,2.23997401500444,
13.8587257282814));
#428866=CARTESIAN_POINT('Ctrl Pts',(-1.43834182256171,2.2401743383222,13.8587068136939));
#428867=CARTESIAN_POINT('Ctrl Pts',(-1.43834182256171,2.2401743383222,13.8587068136939));
#428868=CARTESIAN_POINT('Ctrl Pts',(-1.43738943933149,2.24083319079368,
13.8586446046466));
#428869=CARTESIAN_POINT('Ctrl Pts',(-1.43648762652411,2.24153163169092,
13.858482427929));
#428870=CARTESIAN_POINT('Ctrl Pts',(-1.43563341106693,2.24226632233211,
13.8582284286032));
#428871=CARTESIAN_POINT('Ctrl Pts',(-1.43475708537432,2.24302002946721,
13.8579678548414));
#428872=CARTESIAN_POINT('Ctrl Pts',(-1.43392971103076,2.24381488951759,
13.857615680862));
#428873=CARTESIAN_POINT('Ctrl Pts',(-1.43317719369912,2.2446125781618,13.8571944833187));
#428874=CARTESIAN_POINT('Ctrl Pts',(-1.43129920973686,2.24660329175433,
13.8561433417727));
#428875=CARTESIAN_POINT('Ctrl Pts',(-1.42979610313547,2.24870145060258,
13.8546163505474));
#428876=CARTESIAN_POINT('Ctrl Pts',(-1.42862030029477,2.25070582195769,
13.8528973491086));
#428877=CARTESIAN_POINT('Ctrl Pts',(-1.42840549846313,2.25107199103252,
13.8525833129072));
#428878=CARTESIAN_POINT('Ctrl Pts',(-1.42820147888688,2.25143502294101,
13.8522628768812));
#428879=CARTESIAN_POINT('Ctrl Pts',(-1.42800777371376,2.25179370979477,
13.851937733538));
#428880=CARTESIAN_POINT('Ctrl Pts',(-1.42682484309684,2.25398416064518,
13.8499521282529));
#428881=CARTESIAN_POINT('Ctrl Pts',(-1.42591260266378,2.25623219558733,
13.847639871647));
#428882=CARTESIAN_POINT('Ctrl Pts',(-1.42524455161363,2.25838945692319,
13.8452109780794));
#428883=CARTESIAN_POINT('Ctrl Pts',(-1.4249439816182,2.25936005345129,13.8441181685877));
#428884=CARTESIAN_POINT('Ctrl Pts',(-1.42469212577678,2.26031231270079,
13.8430021611332));
#428885=CARTESIAN_POINT('Ctrl Pts',(-1.42448348263038,2.26123391141051,
13.8418824960098));
#428886=CARTESIAN_POINT('Ctrl Pts',(-1.42399180972801,2.26340568230381,
13.8392439765549));
#428887=CARTESIAN_POINT('Ctrl Pts',(-1.42371291313188,2.26551017341821,
13.8364981347964));
#428888=CARTESIAN_POINT('Ctrl Pts',(-1.42361213134105,2.2675484545724,13.8336931113419));
#428889=CARTESIAN_POINT('Ctrl Pts',(-1.42351397627701,2.26953361097376,
13.8309611966328));
#428890=CARTESIAN_POINT('Ctrl Pts',(-1.42358523779606,2.27145798093114,
13.8281701127186));
#428891=CARTESIAN_POINT('Ctrl Pts',(-1.42383116289706,2.27331008028712,
13.8253580685121));
#428892=CARTESIAN_POINT('Ctrl Pts',(-1.42388447972437,2.27371161742634,
13.8247484142933));
#428893=CARTESIAN_POINT('Ctrl Pts',(-1.42394613602456,2.27410964302014,
13.8241378483365));
#428894=CARTESIAN_POINT('Ctrl Pts',(-1.42401639941741,2.27450380427704,
13.8235269408515));
#428895=CARTESIAN_POINT('',(-1.43937685642172,2.23948769302342,12.5969504640361));
#428896=CARTESIAN_POINT('Origin',(-1.45787563915687,2.26849913672305,12.584524458991));
#428897=CARTESIAN_POINT('Origin',(-1.45787563915687,2.26849913672305,12.584524458991));
#428898=CARTESIAN_POINT('Ctrl Pts',(-1.47740364284708,2.2401939062462,12.5893111709658));
#428899=CARTESIAN_POINT('Ctrl Pts',(-1.46808019059305,2.23374938356206,
12.5770542771492));
#428900=CARTESIAN_POINT('Ctrl Pts',(-1.456428520403,2.24524034769207,12.5737548217797));
#428901=CARTESIAN_POINT('Ctrl Pts',(-1.49779090388309,2.25428591451033,
12.5663937883685));
#428902=CARTESIAN_POINT('Ctrl Pts',(-1.4884555582709,2.2478331709425,12.5540940315304));
#428903=CARTESIAN_POINT('Ctrl Pts',(-1.47677003674784,2.25936202960448,
12.5508374392248));
#428904=CARTESIAN_POINT('Ctrl Pts',(-1.51815759442263,2.26836370411087,
12.5434499600945));
#428905=CARTESIAN_POINT('Ctrl Pts',(-1.50879189627741,2.26188998037585,
12.5311293540533));
#428906=CARTESIAN_POINT('Ctrl Pts',(-1.49709235184912,2.273468945128,12.5278936106989));
#428907=CARTESIAN_POINT('Ctrl Pts',(-1.53850532578086,2.28242838881521,
12.5204817579905));
#428908=CARTESIAN_POINT('Ctrl Pts',(-1.52909327383041,2.27592262457185,
12.5081597038247));
#428909=CARTESIAN_POINT('Ctrl Pts',(-1.51739696600321,2.28756223058349,
12.5049254088044));
#428910=CARTESIAN_POINT('Ctrl Pts',(-1.52387624238132,2.27231652710908,
12.5369868989719));
#428911=CARTESIAN_POINT('Ctrl Pts',(-1.52464250941181,2.27284618360976,
12.5342545179733));
#428912=CARTESIAN_POINT('Ctrl Pts',(-1.52530286870771,2.27345428122829,
12.5314872231885));
#428913=CARTESIAN_POINT('Ctrl Pts',(-1.52578225400243,2.2741476864845,12.5287124745063));
#428914=CARTESIAN_POINT('Ctrl Pts',(-1.52621458745577,2.27477303376212,
12.5262100684184));
#428915=CARTESIAN_POINT('Ctrl Pts',(-1.52649848350549,2.27546769293803,
12.5237004536639));
#428916=CARTESIAN_POINT('Ctrl Pts',(-1.52657745297963,2.27626867008726,
12.5212220730815));
#428917=CARTESIAN_POINT('Ctrl Pts',(-1.5266379109435,2.27688188738504,12.5193246583486));
#428918=CARTESIAN_POINT('Ctrl Pts',(-1.52657834782572,2.27756481114221,
12.517417831369));
#428919=CARTESIAN_POINT('Ctrl Pts',(-1.52630213690367,2.27832827183539,
12.5155812248347));
#428920=CARTESIAN_POINT('Ctrl Pts',(-1.52618446956624,2.27865351019431,
12.5147988205793));
#428921=CARTESIAN_POINT('Ctrl Pts',(-1.52602762591022,2.27899378885114,
12.5140295443047));
#428922=CARTESIAN_POINT('Ctrl Pts',(-1.52582537986502,2.27935167052157,
12.5132817086137));
#428923=CARTESIAN_POINT('Ctrl Pts',(-1.52551930783482,2.27989327601663,
12.5121499604604));
#428924=CARTESIAN_POINT('Ctrl Pts',(-1.5250964162944,2.28048337419652,12.5110494206568));
#428925=CARTESIAN_POINT('Ctrl Pts',(-1.52452106434293,2.28111116575878,
12.5100666561695));
#428926=CARTESIAN_POINT('Ctrl Pts',(-1.52419069857732,2.28147164222815,
12.5095023550641));
#428927=CARTESIAN_POINT('Ctrl Pts',(-1.523805767863,2.28184827026828,12.5089719619137));
#428928=CARTESIAN_POINT('Ctrl Pts',(-1.52336902052781,2.28222942516089,
12.5085043804652));
#428929=CARTESIAN_POINT('Ctrl Pts',(-1.52272989769311,2.28278719569731,
12.5078201359221));
#428930=CARTESIAN_POINT('Ctrl Pts',(-1.52196048124246,2.28336992748646,
12.5072563000949));
#428931=CARTESIAN_POINT('Ctrl Pts',(-1.52110781489119,2.28393137105423,
12.5068768744332));
#428932=CARTESIAN_POINT('Ctrl Pts',(-1.52049298375417,2.2843362105165,12.5066032824114));
#428933=CARTESIAN_POINT('Ctrl Pts',(-1.51982409901167,2.28473714395477,
12.5064197834844));
#428934=CARTESIAN_POINT('Ctrl Pts',(-1.5191398418534,2.2851139992833,12.5063282718343));
#428935=CARTESIAN_POINT('Ctrl Pts',(-1.51814103824299,2.28566409139149,
12.5061946931565));
#428936=CARTESIAN_POINT('Ctrl Pts',(-1.51708864487265,2.28617556834506,
12.5062515701262));
#428937=CARTESIAN_POINT('Ctrl Pts',(-1.51605473500506,2.28663059582161,
12.5064436508398));
#428938=CARTESIAN_POINT('',(-1.456428520403,2.24524034769207,12.5737548217797));
#428939=CARTESIAN_POINT('Origin',(-1.46489437802037,2.25829137274002,12.5893111709658));
#428940=CARTESIAN_POINT('Ctrl Pts',(-1.51605473500506,2.28663059582161,
12.5064436508398));
#428941=CARTESIAN_POINT('Ctrl Pts',(-1.50722823215259,2.2805041584273,12.5164271754438));
#428942=CARTESIAN_POINT('Ctrl Pts',(-1.49839834961203,2.27437512087309,
12.5264061185523));
#428943=CARTESIAN_POINT('Ctrl Pts',(-1.48956496781393,2.26824339236108,
12.536380305637));
#428944=CARTESIAN_POINT('Ctrl Pts',(-1.47852503216917,2.2605799753696,12.5488460165097));
#428945=CARTESIAN_POINT('Ctrl Pts',(-1.46747962746124,2.25291235283713,
12.5613043021964));
#428946=CARTESIAN_POINT('Ctrl Pts',(-1.456428520403,2.24524034769207,12.5737548217797));
#428947=CARTESIAN_POINT('Ctrl Pts',(-1.42401639941741,2.27450380427703,
12.5893111709658));
#428948=CARTESIAN_POINT('Ctrl Pts',(-1.42202735742846,2.26334574232498,
12.5770542771492));
#428949=CARTESIAN_POINT('Ctrl Pts',(-1.43732018478208,2.25752052933426,
12.5737548217797));
#428950=CARTESIAN_POINT('Ctrl Pts',(-1.42216064054149,2.26409342952347,
12.5928319619712));
#428951=CARTESIAN_POINT('Ctrl Pts',(-1.42403106553985,2.25602280831461,
12.5821634970843));
#428952=CARTESIAN_POINT('Ctrl Pts',(-1.43663488437367,2.25372993825639,
12.5773203894503));
#428953=CARTESIAN_POINT('Ctrl Pts',(-1.42636713974644,2.24787956311911,
12.5969440695591));
#428954=CARTESIAN_POINT('Ctrl Pts',(-1.42973886988556,2.24569096118618,
12.5878292599214));
#428955=CARTESIAN_POINT('Ctrl Pts',(-1.43813614694107,2.247951499211,12.5813877129824));
#428956=CARTESIAN_POINT('Ctrl Pts',(-1.45207776459661,2.23129224822624,
12.596957478804));
#428957=CARTESIAN_POINT('Ctrl Pts',(-1.44873099609045,2.23346474303984,
12.5878468778671));
#428958=CARTESIAN_POINT('Ctrl Pts',(-1.44734156980188,2.2420196817612,12.5814011370086));
#428959=CARTESIAN_POINT('Ctrl Pts',(-1.468692312488,2.23417249222711,12.5928371701607));
#428960=CARTESIAN_POINT('Ctrl Pts',(-1.46057862796719,2.2325283543982,12.5821692192952));
#428961=CARTESIAN_POINT('Ctrl Pts',(-1.45325518967119,2.24303507003596,
12.5773318885715));
#428962=CARTESIAN_POINT('Ctrl Pts',(-1.47740364284711,2.24019390624615,
12.5893111709658));
#428963=CARTESIAN_POINT('Ctrl Pts',(-1.46808019059308,2.23374938356201,
12.5770542771492));
#428964=CARTESIAN_POINT('Ctrl Pts',(-1.45642852040303,2.24524034769202,
12.5737548217797));
#428965=CARTESIAN_POINT('',(-1.43732018478208,2.25752052933426,12.5737548217797));
#428966=CARTESIAN_POINT('Origin',(-1.44567497038569,2.27064293603112,12.5893111709658));
#428967=CARTESIAN_POINT('Ctrl Pts',(-1.45642852040303,2.24524034769202,
12.5737548217797));
#428968=CARTESIAN_POINT('Ctrl Pts',(-1.45562315745449,2.24464393327892,
12.5746934679442));
#428969=CARTESIAN_POINT('Ctrl Pts',(-1.45462295118129,2.24413117324802,
12.5756680099006));
#428970=CARTESIAN_POINT('Ctrl Pts',(-1.45354321579869,2.24375744183171,
12.5765688348656));
#428971=CARTESIAN_POINT('Ctrl Pts',(-1.45325736780921,2.24365850057658,
12.5768073183026));
#428972=CARTESIAN_POINT('Ctrl Pts',(-1.45296608657162,2.24356908821268,
12.5770407398754));
#428973=CARTESIAN_POINT('Ctrl Pts',(-1.45267169156365,2.24348969852705,
12.5772674179684));
#428974=CARTESIAN_POINT('Ctrl Pts',(-1.45146357405869,2.24316390472514,
12.5781976435658));
#428975=CARTESIAN_POINT('Ctrl Pts',(-1.45013146371807,2.24299928539706,
12.5790594849312));
#428976=CARTESIAN_POINT('Ctrl Pts',(-1.44875938430905,2.24305488053192,
12.5797571720116));
#428977=CARTESIAN_POINT('Ctrl Pts',(-1.44786542523849,2.2430911027613,12.580211740231));
#428978=CARTESIAN_POINT('Ctrl Pts',(-1.44691463348036,2.24324120943337,
12.5806009430798));
#428979=CARTESIAN_POINT('Ctrl Pts',(-1.44597670345157,2.24351213363939,
12.5808812374708));
#428980=CARTESIAN_POINT('Ctrl Pts',(-1.44517071040179,2.24374494741053,
12.5811221033394));
#428981=CARTESIAN_POINT('Ctrl Pts',(-1.4443577459554,2.24407185498403,12.581287365893));
#428982=CARTESIAN_POINT('Ctrl Pts',(-1.44358680590368,2.24448214112821,
12.581359338449));
#428983=CARTESIAN_POINT('Ctrl Pts',(-1.44347966115579,2.24453916243017,
12.5813693411482));
#428984=CARTESIAN_POINT('Ctrl Pts',(-1.44337328398079,2.24459775375031,
12.5813775999465));
#428985=CARTESIAN_POINT('Ctrl Pts',(-1.44326775995774,2.24465784568193,
12.5813841266931));
#428986=CARTESIAN_POINT('Ctrl Pts',(-1.44308872568978,2.24475979891188,
12.5813952001081));
#428987=CARTESIAN_POINT('Ctrl Pts',(-1.44291124945329,2.24486728361588,
12.5814007534795));
#428988=CARTESIAN_POINT('Ctrl Pts',(-1.44273551070586,2.2449804216665,12.5814005856065));
#428989=CARTESIAN_POINT('Ctrl Pts',(-1.44193104742953,2.24549832342815,
12.5813998171494));
#428990=CARTESIAN_POINT('Ctrl Pts',(-1.44121839191735,2.24609862145549,
12.58127954464));
#428991=CARTESIAN_POINT('Ctrl Pts',(-1.44058252749522,2.24675527703021,
12.5810700125799));
#428992=CARTESIAN_POINT('Ctrl Pts',(-1.43981447567226,2.24754844219824,
12.5808169217085));
#428993=CARTESIAN_POINT('Ctrl Pts',(-1.43917041471568,2.2484355463881,12.5804173076348));
#428994=CARTESIAN_POINT('Ctrl Pts',(-1.43868571515248,2.24932354509367,
12.5799304713245));
#428995=CARTESIAN_POINT('Ctrl Pts',(-1.43808501969756,2.2504240552383,12.5793271277669));
#428996=CARTESIAN_POINT('Ctrl Pts',(-1.43766356143134,2.25157877846844,
12.5785808224116));
#428997=CARTESIAN_POINT('Ctrl Pts',(-1.43740931127446,2.25272816644503,
12.5777485681082));
#428998=CARTESIAN_POINT('Ctrl Pts',(-1.43703045068553,2.25444088045501,
12.576508418016));
#428999=CARTESIAN_POINT('Ctrl Pts',(-1.43701934343463,2.25612584221711,
12.5750928681475));
#429000=CARTESIAN_POINT('Ctrl Pts',(-1.43732018478208,2.25752052933426,
12.5737548217797));
#429001=CARTESIAN_POINT('Ctrl Pts',(-1.43732018478208,2.25752052933426,
12.5737548217797));
#429002=CARTESIAN_POINT('Ctrl Pts',(-1.42202735742846,2.26334574232498,
12.5770542771492));
#429003=CARTESIAN_POINT('Ctrl Pts',(-1.42401639941741,2.27450380427704,
12.5893111709658));
#429004=CARTESIAN_POINT('Ctrl Pts',(-1.44171488686745,2.28188652095685,
12.5508408821982));
#429005=CARTESIAN_POINT('Ctrl Pts',(-1.42637353378435,2.2877267786745,12.55409748406));
#429006=CARTESIAN_POINT('Ctrl Pts',(-1.42836511328145,2.2988990754559,12.5663972313419));
#429007=CARTESIAN_POINT('Ctrl Pts',(-1.44610413509887,2.30622891943672,
12.52790050457));
#429008=CARTESIAN_POINT('Ctrl Pts',(-1.43071138617805,2.31206111953635,
12.5311362602938));
#429009=CARTESIAN_POINT('Ctrl Pts',(-1.43270944000778,2.32326973581482,
12.5434568539655));
#429010=CARTESIAN_POINT('Ctrl Pts',(-1.45048833968264,2.33054956072195,
12.5049357605811));
#429011=CARTESIAN_POINT('Ctrl Pts',(-1.43504178234001,2.33635363267623,
12.5081700652078));
#429012=CARTESIAN_POINT('Ctrl Pts',(-1.43704972319792,2.3476177128782,12.5204921097672));
#429013=CARTESIAN_POINT('Ctrl Pts',(-1.45020045406216,2.32895257236274,
12.5064436508395));
#429014=CARTESIAN_POINT('Ctrl Pts',(-1.44928941955832,2.32976427669525,
12.5062361689309));
#429015=CARTESIAN_POINT('Ctrl Pts',(-1.44830740535102,2.33056953424231,
12.5061871075062));
#429016=CARTESIAN_POINT('Ctrl Pts',(-1.44731457636726,2.33129431507133,
12.5063648335164));
#429017=CARTESIAN_POINT('Ctrl Pts',(-1.4468635722026,2.3316235552302,12.5064455676329));
#429018=CARTESIAN_POINT('Ctrl Pts',(-1.44640391589726,2.33194060299416,
12.506574497099));
#429019=CARTESIAN_POINT('Ctrl Pts',(-1.44595471942102,2.33223099918938,
12.5067492519495));
#429020=CARTESIAN_POINT('Ctrl Pts',(-1.44505204166545,2.33281456161607,
12.5071004286051));
#429021=CARTESIAN_POINT('Ctrl Pts',(-1.44415797626474,2.33331127524723,
12.5076537929613));
#429022=CARTESIAN_POINT('Ctrl Pts',(-1.44334422101941,2.33369212724876,
12.5083435010505));
#429023=CARTESIAN_POINT('Ctrl Pts',(-1.44329299026369,2.33371610415824,
12.5083869222964));
#429024=CARTESIAN_POINT('Ctrl Pts',(-1.44324206716773,2.33373961366055,
12.5084308732337));
#429025=CARTESIAN_POINT('Ctrl Pts',(-1.44319146504562,2.33376264549273,
12.5084753333615));
#429026=CARTESIAN_POINT('Ctrl Pts',(-1.4427855692375,2.33394739118608,12.5088319622689));
#429027=CARTESIAN_POINT('Ctrl Pts',(-1.44239261947182,2.33410632765318,
12.509227847131));
#429028=CARTESIAN_POINT('Ctrl Pts',(-1.44202535010225,2.33423732464801,
12.5096423454524));
#429029=CARTESIAN_POINT('Ctrl Pts',(-1.44087449044466,2.33464781125296,
12.5109411997424));
#429030=CARTESIAN_POINT('Ctrl Pts',(-1.43990825419202,2.3348183093285,12.5124831113042));
#429031=CARTESIAN_POINT('Ctrl Pts',(-1.43910425539677,2.33484076846274,
12.5140723025008));
#429032=CARTESIAN_POINT('Ctrl Pts',(-1.43902891982906,2.33484287290822,
12.5142212114565));
#429033=CARTESIAN_POINT('Ctrl Pts',(-1.43895499201914,2.33484370205625,
12.5143705582413));
#429034=CARTESIAN_POINT('Ctrl Pts',(-1.4388824453064,2.33484334639968,12.5145201959299));
#429035=CARTESIAN_POINT('Ctrl Pts',(-1.43795047477045,2.33483877746143,
12.5164425148273));
#429036=CARTESIAN_POINT('Ctrl Pts',(-1.437214444496,2.33464925908648,12.518463520594));
#429037=CARTESIAN_POINT('Ctrl Pts',(-1.4366105440909,2.33433855813458,12.5205025929157));
#429038=CARTESIAN_POINT('Ctrl Pts',(-1.43626025791957,2.33415833926744,
12.5216853356836));
#429039=CARTESIAN_POINT('Ctrl Pts',(-1.43595483784785,2.33393810454189,
12.5228750347131));
#429040=CARTESIAN_POINT('Ctrl Pts',(-1.43568625407533,2.33369423858345,
12.5240609649613));
#429041=CARTESIAN_POINT('Ctrl Pts',(-1.43502702961469,2.3330956826714,12.5269717671326));
#429042=CARTESIAN_POINT('Ctrl Pts',(-1.43457815328594,2.33233022265961,
12.5299036066169));
#429043=CARTESIAN_POINT('Ctrl Pts',(-1.43427289327788,2.33145314315715,
12.5328133004019));
#429044=CARTESIAN_POINT('Ctrl Pts',(-1.43412635069925,2.33103209392516,
12.5342101228451));
#429045=CARTESIAN_POINT('Ctrl Pts',(-1.43401358315011,2.33058567440663,
12.5356023438238));
#429046=CARTESIAN_POINT('Ctrl Pts',(-1.43393074758918,2.33012098668408,
12.5369868989719));
#429047=CARTESIAN_POINT('Origin',(-3.66550788035654,14.8789346212549,-1.24043609528171));
#429048=CARTESIAN_POINT('Ctrl Pts',(-1.52384188449782,2.27229273011825,
12.5369868989719));
#429049=CARTESIAN_POINT('Ctrl Pts',(-1.53644329648318,2.28103845591202,
12.5369868989719));
#429050=CARTESIAN_POINT('Ctrl Pts',(-1.54900690180321,2.27223850562538,
12.5369868989719));
#429051=CARTESIAN_POINT('Ctrl Pts',(-1.52810169233888,2.27524907308474,
12.5218025310015));
#429052=CARTESIAN_POINT('Ctrl Pts',(-1.53931103355524,2.27899160340515,
12.5216901060417));
#429053=CARTESIAN_POINT('Ctrl Pts',(-1.54896861323185,2.27226534429804,
12.5161920673678));
#429054=CARTESIAN_POINT('Ctrl Pts',(-1.52819884569036,2.28127623099051,
12.5042015548895));
#429055=CARTESIAN_POINT('Ctrl Pts',(-1.53457254172868,2.28214418480728,
12.4980677368514));
#429056=CARTESIAN_POINT('Ctrl Pts',(-1.54020902936817,2.27834671369962,
12.4907278922777));
#429057=CARTESIAN_POINT('Ctrl Pts',(-1.51604368264968,2.28661392582627,
12.506463626192));
#429058=CARTESIAN_POINT('Ctrl Pts',(-1.51965911813721,2.29206700427535,
12.4999376786891));
#429059=CARTESIAN_POINT('Ctrl Pts',(-1.51961496084956,2.29200040285086,
12.4906970594712));
#429060=CARTESIAN_POINT('Origin',(-1.53638550720804,2.25421906061525,12.5369868989719));
#429061=CARTESIAN_POINT('Origin',(-1.53638550720804,2.25421906061525,14.));
#429062=CARTESIAN_POINT('Origin',(-1.53638550720804,2.25421906061525,13.7435492065112));
#429063=CARTESIAN_POINT('Ctrl Pts',(-1.50350829636126,2.25823783669342,
13.793642941384));
#429064=CARTESIAN_POINT('Ctrl Pts',(-1.51238713342879,2.26440812609782,
13.8071662555867));
#429065=CARTESIAN_POINT('Ctrl Pts',(-1.52405613480702,2.25200434480059,
13.8103758687955));
#429066=CARTESIAN_POINT('Ctrl Pts',(-1.51718103118014,2.26768865823418,
13.7804579775006));
#429067=CARTESIAN_POINT('Ctrl Pts',(-1.52814250067577,2.27529391025014,
13.7901904343351));
#429068=CARTESIAN_POINT('Ctrl Pts',(-1.54065318246692,2.26571587468511,
13.7927914348262));
#429069=CARTESIAN_POINT('Ctrl Pts',(-1.52523068475255,2.27325271251839,
13.7597120340895));
#429070=CARTESIAN_POINT('Ctrl Pts',(-1.53791945851365,2.28204942272231,
13.7635825532445));
#429071=CARTESIAN_POINT('Ctrl Pts',(-1.5504567233599,2.27378184107353,13.7651073818884));
#429072=CARTESIAN_POINT('Ctrl Pts',(-1.52365437826742,2.27216314328652,
13.7381884353898));
#429073=CARTESIAN_POINT('Ctrl Pts',(-1.53604563553464,2.28075468877985,
13.7368803041982));
#429074=CARTESIAN_POINT('Ctrl Pts',(-1.54853721275351,2.27220190351982,
13.7363986145813));
#429075=CARTESIAN_POINT('Origin',(-1.5193352108517,2.24243361691415,13.7902182540695));
#429076=CARTESIAN_POINT('Ctrl Pts',(-1.47740040531412,2.24019166748788,
13.8235227101244));
#429077=CARTESIAN_POINT('Ctrl Pts',(-1.48685551529785,2.24673258359459,
13.8358800583119));
#429078=CARTESIAN_POINT('Ctrl Pts',(-1.49857626599684,2.2350172068568,13.8390832900376));
#429079=CARTESIAN_POINT('Ctrl Pts',(-1.48721217657602,2.24697372425544,
13.8124254819053));
#429080=CARTESIAN_POINT('Ctrl Pts',(-1.49668564840759,2.25352734249975,
13.8247886449157));
#429081=CARTESIAN_POINT('Ctrl Pts',(-1.50840915940017,2.24178510799739,
13.8279860620657));
#429082=CARTESIAN_POINT('Ctrl Pts',(-1.49701955052126,2.25375274152581,
13.8013225099955));
#429083=CARTESIAN_POINT('Ctrl Pts',(-1.50650691310271,2.26031597130091,
13.8136962257787));
#429084=CARTESIAN_POINT('Ctrl Pts',(-1.51823734697624,2.24855009921166,
13.8168830918626));
#429085=CARTESIAN_POINT('Ctrl Pts',(-1.50682269824265,2.26052883756116,
13.7902140179785));
#429086=CARTESIAN_POINT('Ctrl Pts',(-1.51631977269687,2.26709879025167,
13.802602731458));
#429087=CARTESIAN_POINT('Ctrl Pts',(-1.52806101258505,2.2553122963536,13.8057746032558));
#429088=CARTESIAN_POINT('Origin',(-1.4899129076738,2.22209643975238,13.8235269408515));
#429089=CARTESIAN_POINT('Ctrl Pts',(-1.42401639941741,2.27450380427704,
13.8235269408515));
#429090=CARTESIAN_POINT('Ctrl Pts',(-1.42608854170343,2.28612803952662,
13.8362179249168));
#429091=CARTESIAN_POINT('Ctrl Pts',(-1.40998158197101,2.29180508561024,
13.8391868794938));
#429092=CARTESIAN_POINT('Ctrl Pts',(-1.42212047942069,2.2638681349965,13.8400110824519));
#429093=CARTESIAN_POINT('Ctrl Pts',(-1.42041392403934,2.27378829283754,
13.8494522556836));
#429094=CARTESIAN_POINT('Ctrl Pts',(-1.406972046088,2.27428205854887,13.85569149686));
#429095=CARTESIAN_POINT('Ctrl Pts',(-1.42607750140433,2.24806498015116,
13.8586819406588));
#429096=CARTESIAN_POINT('Ctrl Pts',(-1.42242234445147,2.25043053955327,
13.868010383617));
#429097=CARTESIAN_POINT('Ctrl Pts',(-1.41368240857793,2.24808397020224,
13.8744918421245));
#429098=CARTESIAN_POINT('Ctrl Pts',(-1.45237188500218,2.23110393981881,
13.8587686893867));
#429099=CARTESIAN_POINT('Ctrl Pts',(-1.45599448049846,2.22875938660122,
13.8680909899357));
#429100=CARTESIAN_POINT('Ctrl Pts',(-1.45745623020193,2.21985098105868,
13.8745789365163));
#429101=CARTESIAN_POINT('Ctrl Pts',(-1.46850223022654,2.23404110425126,
13.8400379222776));
#429102=CARTESIAN_POINT('Ctrl Pts',(-1.47823419615212,2.23660217299914,
13.8494748685453));
#429103=CARTESIAN_POINT('Ctrl Pts',(-1.48426552404467,2.22458617578222,
13.8557104837033));
#429104=CARTESIAN_POINT('Ctrl Pts',(-1.47740364285072,2.24019390624068,
13.8235269408542));
#429105=CARTESIAN_POINT('Ctrl Pts',(-1.48711662014059,2.24690767500026,
13.8362179249195));
#429106=CARTESIAN_POINT('Ctrl Pts',(-1.49897171578396,2.23461459925239,
13.8391868794965));
#429107=CARTESIAN_POINT('Origin',(-1.40235782844914,2.27836467252295,13.8235269408515));
#429108=CARTESIAN_POINT('Ctrl Pts',(-1.43029258730001,2.30971175977477,
13.7902140241683));
#429109=CARTESIAN_POINT('Ctrl Pts',(-1.43232359194615,2.32107985616422,
13.8026027327198));
#429110=CARTESIAN_POINT('Ctrl Pts',(-1.41672473886905,2.32686377481444,
13.8057746032556));
#429111=CARTESIAN_POINT('Ctrl Pts',(-1.4282012082801,2.29797961092568,13.8013225161808));
#429112=CARTESIAN_POINT('Ctrl Pts',(-1.43023013201747,2.30933608028693,
13.8136962270464));
#429113=CARTESIAN_POINT('Ctrl Pts',(-1.41465452616637,2.3151187360509,13.8168830918628));
#429114=CARTESIAN_POINT('Ctrl Pts',(-1.4261089276479,2.28624240424164,13.8124254880875));
#429115=CARTESIAN_POINT('Ctrl Pts',(-1.42813487886878,2.29758224536448,
13.8247886461867));
#429116=CARTESIAN_POINT('Ctrl Pts',(-1.41258365037936,2.30336842326249,
13.8279860620656));
#429117=CARTESIAN_POINT('Ctrl Pts',(-1.4240157089026,2.27449993496174,13.8235227163066));
#429118=CARTESIAN_POINT('Ctrl Pts',(-1.42603773365429,2.28581779691267,
13.8358800595848));
#429119=CARTESIAN_POINT('Ctrl Pts',(-1.41051208250144,2.29161262107548,
13.8390832900376));
#429120=CARTESIAN_POINT('Origin',(-1.4086347090335,2.31357650958566,13.7902182540695));
#429121=CARTESIAN_POINT('Ctrl Pts',(-1.43388336163615,2.32985531971413,
13.7382347919292));
#429122=CARTESIAN_POINT('Ctrl Pts',(-1.43655524756991,2.34470721839042,
13.7369371795942));
#429123=CARTESIAN_POINT('Ctrl Pts',(-1.42357188278845,2.35251593249532,
13.7364597369711));
#429124=CARTESIAN_POINT('Ctrl Pts',(-1.43421531924036,2.33171752220937,
13.7595490285574));
#429125=CARTESIAN_POINT('Ctrl Pts',(-1.43694996454301,2.34692395247711,
13.7633824266926));
#429126=CARTESIAN_POINT('Ctrl Pts',(-1.42420417574629,2.35488878318828,
13.7648920890506));
#429127=CARTESIAN_POINT('Ctrl Pts',(-1.43252235365287,2.32222039150202,
13.780380659011));
#429128=CARTESIAN_POINT('Ctrl Pts',(-1.43489303718528,2.3353724539104,13.7901039518744));
#429129=CARTESIAN_POINT('Ctrl Pts',(-1.42098426477899,2.34279077525527,
13.7926933640891));
#429130=CARTESIAN_POINT('Ctrl Pts',(-1.42957960146849,2.30571225832004,
13.7936647693663));
#429131=CARTESIAN_POINT('Ctrl Pts',(-1.43150714431042,2.31635452830992,
13.8072068914933));
#429132=CARTESIAN_POINT('Ctrl Pts',(-1.41535603912925,2.32181219001387,
13.8104111085397));
#429133=CARTESIAN_POINT('Origin',(-1.41227217662091,2.33398185492999,13.7435492065112));
#429134=CARTESIAN_POINT('Origin',(-1.41227217662091,2.33398185492999,14.));
#429135=CARTESIAN_POINT('Origin',(-1.41227217662091,2.33398185492999,12.5369868989719));
#429136=CARTESIAN_POINT('Ctrl Pts',(-1.45019073698299,2.32893696717882,
12.506462012331));
#429137=CARTESIAN_POINT('Ctrl Pts',(-1.45364694947951,2.33448747915239,
12.4999388158272));
#429138=CARTESIAN_POINT('Ctrl Pts',(-1.45360605795313,2.33442180931669,
12.4907030323752));
#429139=CARTESIAN_POINT('Ctrl Pts',(-1.44028491574729,2.33777457368743,
12.5042014951932));
#429140=CARTESIAN_POINT('Ctrl Pts',(-1.43842843393313,2.34393043044257,
12.4980716682127));
#429141=CARTESIAN_POINT('Ctrl Pts',(-1.4326375636756,2.34747886487005,12.4907355092743));
#429142=CARTESIAN_POINT('Ctrl Pts',(-1.43484254617332,2.33518491836954,
12.5218047446509));
#429143=CARTESIAN_POINT('Ctrl Pts',(-1.43358983898951,2.34693011294637,
12.5216906929434));
#429144=CARTESIAN_POINT('Ctrl Pts',(-1.42346655744649,2.35292093301802,
12.5161988840776));
#429145=CARTESIAN_POINT('Ctrl Pts',(-1.43392397277117,2.33008317265677,
12.5369868989719));
#429146=CARTESIAN_POINT('Ctrl Pts',(-1.43664062599462,2.34517042975619,
12.5369868989719));
#429147=CARTESIAN_POINT('Ctrl Pts',(-1.42342772055309,2.35294375988644,
12.5369868989719));
#429148=CARTESIAN_POINT('Origin',(-2.78530720815108E-31,-8.17839987285357E-32,
12.5));
#429149=CARTESIAN_POINT('Origin',(-1.60467127783313,2.15086502402588,12.5));
#429150=CARTESIAN_POINT('',(-1.60467127783313,2.15086502402588,12.5893111709658));
#429151=CARTESIAN_POINT('',(-1.60467127783313,2.15086502402588,13.8235269408515));
#429152=CARTESIAN_POINT('',(-1.60467127783313,2.15086502402588,12.5));
#429153=CARTESIAN_POINT('',(-1.6137973642265,2.1854480725662,13.7902182540695));
#429154=CARTESIAN_POINT('',(-1.60467127783313,2.15086502402588,13.8235269408515));
#429155=CARTESIAN_POINT('',(-1.61908595352014,2.20548903343024,13.7435492065112));
#429156=CARTESIAN_POINT('Origin',(-1.60168687962198,2.13955445397357,13.7445212918705));
#429157=CARTESIAN_POINT('',(-1.61908595352014,2.20548903343024,12.5369868989719));
#429158=CARTESIAN_POINT('',(-1.61908595352014,2.20548903343024,12.5));
#429159=CARTESIAN_POINT('Ctrl Pts',(-1.61908595352014,2.20548903343024,
12.5369868989719));
#429160=CARTESIAN_POINT('Ctrl Pts',(-1.61428456602037,2.1872943101055,12.5544431401645));
#429161=CARTESIAN_POINT('Ctrl Pts',(-1.60947974444066,2.16908657343106,
12.5718848856037));
#429162=CARTESIAN_POINT('Ctrl Pts',(-1.60467127783313,2.15086502402588,
12.5893111709658));
#429163=CARTESIAN_POINT('Origin',(-1.89329517791645,2.2497243552881,12.5));
#429164=CARTESIAN_POINT('',(-1.70402056201255,2.14054552058715,13.7435492065112));
#429165=CARTESIAN_POINT('',(-1.68606637603842,2.130189049418,13.7902182540695));
#429166=CARTESIAN_POINT('Origin',(-1.63888587840916,2.10297403314562,13.7418732680461));
#429167=CARTESIAN_POINT('',(-1.65508430440736,2.11231773338787,13.8235269408515));
#429168=CARTESIAN_POINT('',(-1.68606637603842,2.130189049418,13.7902182540695));
#429169=CARTESIAN_POINT('',(-1.65508430440736,2.11231773338787,12.5893111709658));
#429170=CARTESIAN_POINT('',(-1.65508430440736,2.11231773338787,12.5));
#429171=CARTESIAN_POINT('',(-1.70402056201255,2.14054552058715,12.5369868989719));
#429172=CARTESIAN_POINT('Ctrl Pts',(-1.65508430440736,2.11231773338787,
12.5893111709658));
#429173=CARTESIAN_POINT('Ctrl Pts',(-1.67140852603409,2.12173399602877,
12.5718848856037));
#429174=CARTESIAN_POINT('Ctrl Pts',(-1.68772037318746,2.1311431207311,12.5544431401645));
#429175=CARTESIAN_POINT('Ctrl Pts',(-1.70402056201255,2.14054552058715,
12.5369868989719));
#429176=CARTESIAN_POINT('',(-1.70402056201255,2.14054552058715,12.5));
#429177=CARTESIAN_POINT('Origin',(-1.63790847666983,2.1420940925765,12.5));
#429178=CARTESIAN_POINT('',(-1.61615086413916,2.11548213156001,13.8587068136939));
#429179=CARTESIAN_POINT('Ctrl Pts',(-1.65508430441053,2.11231773338207,
13.8235269408542));
#429180=CARTESIAN_POINT('Ctrl Pts',(-1.65356642617364,2.11144217922321,
13.8262006681044));
#429181=CARTESIAN_POINT('Ctrl Pts',(-1.65192628890099,2.11069667418707,
13.8288634856214));
#429182=CARTESIAN_POINT('Ctrl Pts',(-1.65017403515052,2.11007256179819,
13.8314912288862));
#429183=CARTESIAN_POINT('Ctrl Pts',(-1.64836764227037,2.10942916629946,
13.8342001611531));
#429184=CARTESIAN_POINT('Ctrl Pts',(-1.64644025805345,2.10891359790061,
13.8368750301949));
#429185=CARTESIAN_POINT('Ctrl Pts',(-1.6443708032732,2.10854810367321,13.8394886372969));
#429186=CARTESIAN_POINT('Ctrl Pts',(-1.64421097426073,2.10851987566746,
13.8396904925131));
#429187=CARTESIAN_POINT('Ctrl Pts',(-1.64405029026668,2.10849256365223,
13.8398919674349));
#429188=CARTESIAN_POINT('Ctrl Pts',(-1.64388873863784,2.10846618893557,
13.8400930404591));
#429189=CARTESIAN_POINT('Ctrl Pts',(-1.64137165557397,2.108055253106,13.8432258934518));
#429190=CARTESIAN_POINT('Ctrl Pts',(-1.6386569728769,2.10787283946285,13.8462331177034));
#429191=CARTESIAN_POINT('Ctrl Pts',(-1.63582676140163,2.10802114660661,
13.8489036603661));
#429192=CARTESIAN_POINT('Ctrl Pts',(-1.6349006832701,2.10806967442998,13.8497774930041));
#429193=CARTESIAN_POINT('Ctrl Pts',(-1.63396245175139,2.10815373746488,
13.85061494757));
#429194=CARTESIAN_POINT('Ctrl Pts',(-1.63301556491525,2.10827726497248,
13.8514076489583));
#429195=CARTESIAN_POINT('Ctrl Pts',(-1.63101276269529,2.10853854346638,
13.8530843267192));
#429196=CARTESIAN_POINT('Ctrl Pts',(-1.62877489275942,2.10900497701708,
13.8546805203176));
#429197=CARTESIAN_POINT('Ctrl Pts',(-1.6264596810056,2.10978306915337,13.8559412814273));
#429198=CARTESIAN_POINT('Ctrl Pts',(-1.62614983058885,2.10988720311533,
13.8561100121513));
#429199=CARTESIAN_POINT('Ctrl Pts',(-1.6258386234352,2.1099968479079,13.8562727473908));
#429200=CARTESIAN_POINT('Ctrl Pts',(-1.62552645677455,2.11011218543732,
13.8564289040185));
#429201=CARTESIAN_POINT('Ctrl Pts',(-1.6241107845298,2.11063523981746,13.8571370725437));
#429202=CARTESIAN_POINT('Ctrl Pts',(-1.62265128433814,2.11128670089093,
13.8577210840553));
#429203=CARTESIAN_POINT('Ctrl Pts',(-1.62121664943176,2.11206804575303,
13.8581177131616));
#429204=CARTESIAN_POINT('Ctrl Pts',(-1.62081260686348,2.11228809935928,
13.8582294175695));
#429205=CARTESIAN_POINT('Ctrl Pts',(-1.6204104838138,2.11251828548136,13.8583265086086));
#429206=CARTESIAN_POINT('Ctrl Pts',(-1.62001165943628,2.11275822590146,
13.8584082369006));
#429207=CARTESIAN_POINT('Ctrl Pts',(-1.61943865575479,2.11310295594257,
13.8585256585398));
#429208=CARTESIAN_POINT('Ctrl Pts',(-1.61886550409113,2.11347238366383,
13.8586122832068));
#429209=CARTESIAN_POINT('Ctrl Pts',(-1.61830752109069,2.11385757615836,
13.8586682984299));
#429210=CARTESIAN_POINT('Ctrl Pts',(-1.61786119000141,2.11416569197108,
13.8587131050557));
#429211=CARTESIAN_POINT('Ctrl Pts',(-1.6174195015092,2.11448710491203,13.8587357943552));
#429212=CARTESIAN_POINT('Ctrl Pts',(-1.61698270111869,2.11482226267343,
13.8587355499465));
#429213=CARTESIAN_POINT('Ctrl Pts',(-1.61670038661254,2.11503888312512,
13.8587353919793));
#429214=CARTESIAN_POINT('Ctrl Pts',(-1.61642314340459,2.11525887207689,
13.8587257282814));
#429215=CARTESIAN_POINT('Ctrl Pts',(-1.61615086413916,2.11548213156001,
13.8587068136939));
#429216=CARTESIAN_POINT('Ctrl Pts',(-1.61615086413916,2.11548213156001,
13.8587068136939));
#429217=CARTESIAN_POINT('Ctrl Pts',(-1.61525535247848,2.11621641982901,
13.8586446046466));
#429218=CARTESIAN_POINT('Ctrl Pts',(-1.61441346979595,2.11698604283761,
13.858482427929));
#429219=CARTESIAN_POINT('Ctrl Pts',(-1.61362198077802,2.11778791534621,
13.8582284286032));
#429220=CARTESIAN_POINT('Ctrl Pts',(-1.61281000511545,2.11861054326235,
13.8579678548414));
#429221=CARTESIAN_POINT('Ctrl Pts',(-1.61205017226499,2.11947019717145,
13.857615680862));
#429222=CARTESIAN_POINT('Ctrl Pts',(-1.61136517790258,2.12032656872106,
13.8571944833187));
#429223=CARTESIAN_POINT('Ctrl Pts',(-1.6096557044157,2.12246373150562,13.8561433417727));
#429224=CARTESIAN_POINT('Ctrl Pts',(-1.60832861870202,2.12467742604556,
13.8546163505474));
#429225=CARTESIAN_POINT('Ctrl Pts',(-1.60732010312139,2.12677096686748,
13.8528973491086));
#429226=CARTESIAN_POINT('Ctrl Pts',(-1.60713586220407,2.12715342588832,
13.8525833129072));
#429227=CARTESIAN_POINT('Ctrl Pts',(-1.6069621119569,2.12753187932757,13.8522628768811));
#429228=CARTESIAN_POINT('Ctrl Pts',(-1.60679828763023,2.12790516145029,
13.851937733538));
#429229=CARTESIAN_POINT('Ctrl Pts',(-1.60579783519682,2.13018474358327,
13.8499521282529));
#429230=CARTESIAN_POINT('Ctrl Pts',(-1.60507186588607,2.13249965443872,
13.847639871647));
#429231=CARTESIAN_POINT('Ctrl Pts',(-1.60458187454659,2.13470419002792,
13.8452109780794));
#429232=CARTESIAN_POINT('Ctrl Pts',(-1.60436141730064,2.13569605622112,
13.8441181685877));
#429233=CARTESIAN_POINT('Ctrl Pts',(-1.60418801745794,2.13666567549571,
13.8430021611332));
#429234=CARTESIAN_POINT('Ctrl Pts',(-1.60405518740495,2.13760121401513,
13.8418824960098));
#429235=CARTESIAN_POINT('Ctrl Pts',(-1.60374216999313,2.13980583442596,
13.8392439765549));
#429236=CARTESIAN_POINT('Ctrl Pts',(-1.60363573696538,2.14192605568153,
13.8364981347964));
#429237=CARTESIAN_POINT('Ctrl Pts',(-1.60370142935419,2.1439657692749,13.8336931113419));
#429238=CARTESIAN_POINT('Ctrl Pts',(-1.60376540956904,2.14595232078104,
13.8309611966328));
#429239=CARTESIAN_POINT('Ctrl Pts',(-1.60399328798778,2.14786447908079,
13.8281701127185));
#429240=CARTESIAN_POINT('Ctrl Pts',(-1.60438935808485,2.14969037055016,
13.825358068512));
#429241=CARTESIAN_POINT('Ctrl Pts',(-1.60447522650935,2.15008622579127,
13.8247484142932));
#429242=CARTESIAN_POINT('Ctrl Pts',(-1.60456912043427,2.15047790142687,
13.8241378483365));
#429243=CARTESIAN_POINT('Ctrl Pts',(-1.60467127783313,2.15086502402588,
13.8235269408515));
#429244=CARTESIAN_POINT('',(-1.61712648604294,2.11471340614851,12.5969504640361));
#429245=CARTESIAN_POINT('Origin',(-1.63792841759527,2.14212049413521,12.584524458991));
#429246=CARTESIAN_POINT('Origin',(-1.63792841759527,2.14212049413521,12.584524458991));
#429247=CARTESIAN_POINT('Ctrl Pts',(-1.65508430440736,2.11231773338787,
12.5893111709658));
#429248=CARTESIAN_POINT('Ctrl Pts',(-1.64526658674478,2.10665460223473,
12.5770542771492));
#429249=CARTESIAN_POINT('Ctrl Pts',(-1.63459030677959,2.11905705041885,
12.5737548217797));
#429250=CARTESIAN_POINT('Ctrl Pts',(-1.67655235801145,2.12470110061648,
12.5663937883685));
#429251=CARTESIAN_POINT('Ctrl Pts',(-1.66672211648652,2.11903074535306,
12.5540940315304));
#429252=CARTESIAN_POINT('Ctrl Pts',(-1.65601518658201,2.13147372117614,
12.5508374392248));
#429253=CARTESIAN_POINT('Ctrl Pts',(-1.69799875061259,2.13707197317934,
12.5434499600945));
#429254=CARTESIAN_POINT('Ctrl Pts',(-1.68813654747176,2.13138318157174,
12.5311293540532));
#429255=CARTESIAN_POINT('Ctrl Pts',(-1.67741972543363,2.14387723975807,
12.5278936106989));
#429256=CARTESIAN_POINT('Ctrl Pts',(-1.71942517894689,2.14943132980078,
12.5204817579905));
#429257=CARTESIAN_POINT('Ctrl Pts',(-1.70951416464046,2.14371438256243,
12.5081597038247));
#429258=CARTESIAN_POINT('Ctrl Pts',(-1.69880551125946,2.15626861641641,
12.5049254088044));
#429259=CARTESIAN_POINT('Ctrl Pts',(-1.70402056201255,2.14054552058714,
12.5369868989719));
#429260=CARTESIAN_POINT('Ctrl Pts',(-1.7048274512746,2.14101095682285,12.5342545179733));
#429261=CARTESIAN_POINT('Ctrl Pts',(-1.70553517888064,2.14156320563363,
12.5314872231885));
#429262=CARTESIAN_POINT('Ctrl Pts',(-1.70606948802598,2.14221522928913,
12.5287124745063));
#429263=CARTESIAN_POINT('Ctrl Pts',(-1.70655135453398,2.14280325658524,
12.5262100684185));
#429264=CARTESIAN_POINT('Ctrl Pts',(-1.70689092711476,2.14347246417644,
12.5237004536639));
#429265=CARTESIAN_POINT('Ctrl Pts',(-1.70703492089806,2.14426433939502,
12.5212220730815));
#429266=CARTESIAN_POINT('Ctrl Pts',(-1.70714516059564,2.14487058837751,
12.5193246583486));
#429267=CARTESIAN_POINT('Ctrl Pts',(-1.70714146029539,2.14555609470927,
12.517417831369));
#429268=CARTESIAN_POINT('Ctrl Pts',(-1.70692839757651,2.14633952880434,
12.5155812248347));
#429269=CARTESIAN_POINT('Ctrl Pts',(-1.70683763171305,2.14667327593982,
12.5147988205793));
#429270=CARTESIAN_POINT('Ctrl Pts',(-1.70670904581089,2.14702520656152,
12.5140295443047));
#429271=CARTESIAN_POINT('Ctrl Pts',(-1.70653664340126,2.14739838234046,
12.5132817086137));
#429272=CARTESIAN_POINT('Ctrl Pts',(-1.70627573567636,2.14796313339982,
12.5121499604604));
#429273=CARTESIAN_POINT('Ctrl Pts',(-1.70590234975253,2.14858573766316,
12.5110494206568));
#429274=CARTESIAN_POINT('Ctrl Pts',(-1.70538008307767,2.14925833682614,
12.5100666561695));
#429275=CARTESIAN_POINT('Ctrl Pts',(-1.70508019875564,2.14964454171666,
12.5095023550641));
#429276=CARTESIAN_POINT('Ctrl Pts',(-1.70472724754823,2.1500512919848,12.5089719619137));
#429277=CARTESIAN_POINT('Ctrl Pts',(-1.70432302111599,2.15046677757833,
12.5085043804652));
#429278=CARTESIAN_POINT('Ctrl Pts',(-1.70373148838661,2.15107478662366,
12.5078201359221));
#429279=CARTESIAN_POINT('Ctrl Pts',(-1.70301213015636,2.15171829400449,
12.5072563000949));
#429280=CARTESIAN_POINT('Ctrl Pts',(-1.70220806384499,2.1523473696385,12.5068768744332));
#429281=CARTESIAN_POINT('Ctrl Pts',(-1.70162827668238,2.15280097647633,
12.5066032824114));
#429282=CARTESIAN_POINT('Ctrl Pts',(-1.70099429739599,2.15325509615781,
12.5064197834844));
#429283=CARTESIAN_POINT('Ctrl Pts',(-1.7003430342548,2.15368647084205,12.5063282718343));
#429284=CARTESIAN_POINT('Ctrl Pts',(-1.69939239169463,2.15431614433082,
12.5061946931565));
#429285=CARTESIAN_POINT('Ctrl Pts',(-1.69838519019644,2.15491169921664,
12.5062515701262));
#429286=CARTESIAN_POINT('Ctrl Pts',(-1.69739180954226,2.15544948587937,
12.5064436508398));
#429287=CARTESIAN_POINT('',(-1.63459030677959,2.11905705041885,12.5737548217797));
#429288=CARTESIAN_POINT('Origin',(-1.64409177465534,2.13137460326859,12.5893111709658));
#429289=CARTESIAN_POINT('Ctrl Pts',(-1.69739180954226,2.15544948587937,
12.5064436508398));
#429290=CARTESIAN_POINT('Ctrl Pts',(-1.68809531462718,2.15006287562382,
12.5164271754438));
#429291=CARTESIAN_POINT('Ctrl Pts',(-1.67879523933249,2.14467394933615,
12.5264061185523));
#429292=CARTESIAN_POINT('Ctrl Pts',(-1.66949145708569,2.13928262626659,
12.536380305637));
#429293=CARTESIAN_POINT('Ctrl Pts',(-1.65786361628756,2.13254456590778,
12.5488460165097));
#429294=CARTESIAN_POINT('Ctrl Pts',(-1.6462299818335,2.12580275978098,12.5613043021964));
#429295=CARTESIAN_POINT('Ctrl Pts',(-1.63459030677959,2.11905705041885,
12.5737548217797));
#429296=CARTESIAN_POINT('Ctrl Pts',(-1.60467127783313,2.15086502402588,
12.5893111709658));
#429297=CARTESIAN_POINT('Ctrl Pts',(-1.60177936858182,2.13990621499196,
12.5770542771492));
#429298=CARTESIAN_POINT('Ctrl Pts',(-1.61654650137661,2.13285387751592,
12.5737548217797));
#429299=CARTESIAN_POINT('Ctrl Pts',(-1.60197315165416,2.14064055051192,
12.5928319619712));
#429300=CARTESIAN_POINT('Ctrl Pts',(-1.60317952241511,2.1324443266278,12.5821634970842));
#429301=CARTESIAN_POINT('Ctrl Pts',(-1.6155545128858,2.12913175766246,12.5773203894503));
#429302=CARTESIAN_POINT('Ctrl Pts',(-1.60484407344586,2.12413776567403,
12.5969440695591));
#429303=CARTESIAN_POINT('Ctrl Pts',(-1.60802619305558,2.12168161882553,
12.5878292599214));
#429304=CARTESIAN_POINT('Ctrl Pts',(-1.61657978369924,2.12325017906002,
12.5813877129824));
#429305=CARTESIAN_POINT('Ctrl Pts',(-1.62911712815993,2.10550998909203,
12.596957478804));
#429306=CARTESIAN_POINT('Ctrl Pts',(-1.62595857424566,2.10794804781149,
12.5878468778671));
#429307=CARTESIAN_POINT('Ctrl Pts',(-1.62527107808441,2.11658777182131,
12.5814011370086));
#429308=CARTESIAN_POINT('Ctrl Pts',(-1.64591115913877,2.1070264094235,12.5928371701607));
#429309=CARTESIAN_POINT('Ctrl Pts',(-1.63769045973738,2.1060490829398,12.5821692192952));
#429310=CARTESIAN_POINT('Ctrl Pts',(-1.63124778444224,2.11711776655663,
12.5773318885715));
#429311=CARTESIAN_POINT('Ctrl Pts',(-1.65508430440738,2.11231773338782,
12.5893111709658));
#429312=CARTESIAN_POINT('Ctrl Pts',(-1.6452665867448,2.10665460223468,12.5770542771492));
#429313=CARTESIAN_POINT('Ctrl Pts',(-1.63459030677962,2.11905705041881,
12.5737548217797));
#429314=CARTESIAN_POINT('',(-1.61654650137661,2.13285387751592,12.5737548217797));
#429315=CARTESIAN_POINT('Origin',(-1.62594308508861,2.14525162789828,12.5893111709658));
#429316=CARTESIAN_POINT('Ctrl Pts',(-1.63459030677962,2.11905705041881,
12.5737548217797));
#429317=CARTESIAN_POINT('Ctrl Pts',(-1.63373901029835,2.1185282650824,12.5746934679442));
#429318=CARTESIAN_POINT('Ctrl Pts',(-1.63270033742626,2.11809873731492,
12.5756680099006));
#429319=CARTESIAN_POINT('Ctrl Pts',(-1.63159373219408,2.11781425791652,
12.5765688348656));
#429320=CARTESIAN_POINT('Ctrl Pts',(-1.63130077070939,2.11773894514509,
12.5768073183026));
#429321=CARTESIAN_POINT('Ctrl Pts',(-1.63100317074836,2.11767357241844,
12.5770407398754));
#429322=CARTESIAN_POINT('Ctrl Pts',(-1.6307032843191,2.11761844282163,12.5772674179684));
#429323=CARTESIAN_POINT('Ctrl Pts',(-1.62947263150611,2.11739220586398,
12.5781976435658));
#429324=CARTESIAN_POINT('Ctrl Pts',(-1.62813153564926,2.1173367136526,12.5790594849312));
#429325=CARTESIAN_POINT('Ctrl Pts',(-1.6267685532409,2.11750396100884,12.5797571720116));
#429326=CARTESIAN_POINT('Ctrl Pts',(-1.62588052119337,2.1176129286751,12.580211740231));
#429327=CARTESIAN_POINT('Ctrl Pts',(-1.62494512820368,2.11784003423461,
12.5806009430798));
#429328=CARTESIAN_POINT('Ctrl Pts',(-1.62403240189761,2.11818650696735,
12.5808812374708));
#429329=CARTESIAN_POINT('Ctrl Pts',(-1.62324806720689,2.1184842419859,12.5811221033394));
#429330=CARTESIAN_POINT('Ctrl Pts',(-1.62246445383474,2.118876325951,12.581287365893));
#429331=CARTESIAN_POINT('Ctrl Pts',(-1.6217295211521,2.11934808567315,12.581359338449));
#429332=CARTESIAN_POINT('Ctrl Pts',(-1.62162738068499,2.11941365053306,
12.5813693411482));
#429333=CARTESIAN_POINT('Ctrl Pts',(-1.6215261332078,2.11948071762274,12.5813775999465));
#429334=CARTESIAN_POINT('Ctrl Pts',(-1.62142585835752,2.11954921079093,
12.5813841266931));
#429335=CARTESIAN_POINT('Ctrl Pts',(-1.62125572994604,2.11966541773483,
12.5813952001081));
#429336=CARTESIAN_POINT('Ctrl Pts',(-1.62108760524831,2.11978701075322,
12.5814007534795));
#429337=CARTESIAN_POINT('Ctrl Pts',(-1.62092167305851,2.11991409668571,
12.5814005856065));
#429338=CARTESIAN_POINT('Ctrl Pts',(-1.62016210036891,2.12049584639726,
12.5813998171494));
#429339=CARTESIAN_POINT('Ctrl Pts',(-1.61950074602127,2.12115223502266,
12.58127954464));
#429340=CARTESIAN_POINT('Ctrl Pts',(-1.61892052091099,2.1218585344836,12.5810700125799));
#429341=CARTESIAN_POINT('Ctrl Pts',(-1.61821967504169,2.12271166381379,
12.5808169217085));
#429342=CARTESIAN_POINT('Ctrl Pts',(-1.61765006437176,2.12364831318477,
12.5804173076348));
#429343=CARTESIAN_POINT('Ctrl Pts',(-1.61723935774465,2.12457286466203,
12.5799304713245));
#429344=CARTESIAN_POINT('Ctrl Pts',(-1.61673036284773,2.1257186752061,12.5793271277669));
#429345=CARTESIAN_POINT('Ctrl Pts',(-1.61640442761231,2.12690390895128,
12.5785808224116));
#429346=CARTESIAN_POINT('Ctrl Pts',(-1.61624470924234,2.12807019618232,
12.5777485681082));
#429347=CARTESIAN_POINT('Ctrl Pts',(-1.61600671137264,2.12980809193288,
12.576508418016));
#429348=CARTESIAN_POINT('Ctrl Pts',(-1.61613298110624,2.13148835246778,
12.5750928681475));
#429349=CARTESIAN_POINT('Ctrl Pts',(-1.61654650137661,2.13285387751592,
12.5737548217797));
#429350=CARTESIAN_POINT('Ctrl Pts',(-1.61654650137661,2.13285387751592,
12.5737548217797));
#429351=CARTESIAN_POINT('Ctrl Pts',(-1.60177936858182,2.13990621499196,
12.5770542771492));
#429352=CARTESIAN_POINT('Ctrl Pts',(-1.60467127783313,2.15086502402588,
12.5893111709658));
#429353=CARTESIAN_POINT('Ctrl Pts',(-1.62291263497338,2.15678058429305,
12.5508408821982));
#429354=CARTESIAN_POINT('Ctrl Pts',(-1.60809836419938,2.16385187173341,
12.55409748406));
#429355=CARTESIAN_POINT('Ctrl Pts',(-1.61099396278624,2.17482466140095,
12.5663972313419));
#429356=CARTESIAN_POINT('Ctrl Pts',(-1.62927140980334,2.18068422097144,
12.52790050457));
#429357=CARTESIAN_POINT('Ctrl Pts',(-1.61440525743634,2.18775166684268,
12.5311362602938));
#429358=CARTESIAN_POINT('Ctrl Pts',(-1.6173102691892,2.198760127439,12.5434568539654));
#429359=CARTESIAN_POINT('Ctrl Pts',(-1.63562338435458,2.20456658395455,
12.5049357605811));
#429360=CARTESIAN_POINT('Ctrl Pts',(-1.62070130990391,2.21161038116047,
12.5081700652078));
#429361=CARTESIAN_POINT('Ctrl Pts',(-1.62362069661134,2.22267331524406,
12.5204921097672));
#429362=CARTESIAN_POINT('Ctrl Pts',(-1.63520628727276,2.20299837479304,
12.5064436508395));
#429363=CARTESIAN_POINT('Ctrl Pts',(-1.63436444559968,2.20388163601603,
12.5062361689309));
#429364=CARTESIAN_POINT('Ctrl Pts',(-1.63345133492937,2.2047642574095,12.5061871075061));
#429365=CARTESIAN_POINT('Ctrl Pts',(-1.63252088586825,2.20556755136925,
12.5063648335164));
#429366=CARTESIAN_POINT('Ctrl Pts',(-1.63209821851221,2.205932457035,12.5064455676329));
#429367=CARTESIAN_POINT('Ctrl Pts',(-1.63166593401139,2.20628591610481,
12.506574497099));
#429368=CARTESIAN_POINT('Ctrl Pts',(-1.6312419021852,2.20661195971359,12.5067492519495));
#429369=CARTESIAN_POINT('Ctrl Pts',(-1.63038979377069,2.20726715700158,
12.5071004286051));
#429370=CARTESIAN_POINT('Ctrl Pts',(-1.62953919007105,2.20783509248937,
12.5076537929613));
#429371=CARTESIAN_POINT('Ctrl Pts',(-1.62875918550295,2.20828100584431,
12.5083435010505));
#429372=CARTESIAN_POINT('Ctrl Pts',(-1.62871007955406,2.20830907875479,
12.5083869222964));
#429373=CARTESIAN_POINT('Ctrl Pts',(-1.62866124214319,2.20833666073623,
12.5084308732337));
#429374=CARTESIAN_POINT('Ctrl Pts',(-1.6286126857036,2.20836374047461,12.5084753333615));
#429375=CARTESIAN_POINT('Ctrl Pts',(-1.62822319896941,2.20858095571843,
12.5088319622689));
#429376=CARTESIAN_POINT('Ctrl Pts',(-1.62784451150921,2.20877139239141,
12.509227847131));
#429377=CARTESIAN_POINT('Ctrl Pts',(-1.62748914166938,2.20893188936773,
12.5096423454524));
#429378=CARTESIAN_POINT('Ctrl Pts',(-1.62637556987143,2.20943481585851,
12.5109411997424));
#429379=CARTESIAN_POINT('Ctrl Pts',(-1.6254264458662,2.20968350384047,12.5124831113042));
#429380=CARTESIAN_POINT('Ctrl Pts',(-1.62462695293855,2.20977142160957,
12.5140723025008));
#429381=CARTESIAN_POINT('Ctrl Pts',(-1.62455203957557,2.20977965960083,
12.5142212114565));
#429382=CARTESIAN_POINT('Ctrl Pts',(-1.6244784253376,2.20978651179276,12.5143705582413));
#429383=CARTESIAN_POINT('Ctrl Pts',(-1.62440609102875,2.20979207055018,
12.5145201959299));
#429384=CARTESIAN_POINT('Ctrl Pts',(-1.623476849137,2.20986348106537,12.5164425148273));
#429385=CARTESIAN_POINT('Ctrl Pts',(-1.62272782043561,2.20973458659751,
12.518463520594));
#429386=CARTESIAN_POINT('Ctrl Pts',(-1.6221006044473,2.20947414296675,12.5205025929157));
#429387=CARTESIAN_POINT('Ctrl Pts',(-1.62173679431356,2.20932307533789,
12.5216853356836));
#429388=CARTESIAN_POINT('Ctrl Pts',(-1.62141443932725,2.20912846799645,
12.5228750347131));
#429389=CARTESIAN_POINT('Ctrl Pts',(-1.62112687190551,2.20890730555274,
12.5240609649613));
#429390=CARTESIAN_POINT('Ctrl Pts',(-1.62042105309633,2.2083644741996,12.5269717671327));
#429391=CARTESIAN_POINT('Ctrl Pts',(-1.61991127826939,2.2076381487808,12.5299036066169));
#429392=CARTESIAN_POINT('Ctrl Pts',(-1.61953554386697,2.20678886921258,
12.532813300402));
#429393=CARTESIAN_POINT('Ctrl Pts',(-1.61935516947545,2.20638116556777,
12.5342101228452));
#429394=CARTESIAN_POINT('Ctrl Pts',(-1.6192063898159,2.2059454230755,12.5356023438238));
#429395=CARTESIAN_POINT('Ctrl Pts',(-1.61908595352013,2.20548903343024,
12.5369868989719));
#429396=CARTESIAN_POINT('Origin',(-4.86600595941219,14.5303612090825,-1.24011047643264));
#429397=CARTESIAN_POINT('Ctrl Pts',(-1.70398437877637,2.1405246032653,12.5369868989719));
#429398=CARTESIAN_POINT('Ctrl Pts',(-1.71725671844646,2.14821409631539,
12.5369868989719));
#429399=CARTESIAN_POINT('Ctrl Pts',(-1.72906124176311,2.13841937666895,
12.5369868989719));
#429400=CARTESIAN_POINT('Ctrl Pts',(-1.70847098185535,2.14312389535928,
12.5218025310016));
#429401=CARTESIAN_POINT('Ctrl Pts',(-1.7199480758786,2.14594030734725,12.5216901060418));
#429402=CARTESIAN_POINT('Ctrl Pts',(-1.72902526819479,2.13844924691217,
12.5161920673678));
#429403=CARTESIAN_POINT('Ctrl Pts',(-1.70905908125986,2.14912307949432,
12.5042015548894));
#429404=CARTESIAN_POINT('Ctrl Pts',(-1.71548231564416,2.14946862986869,
12.4980677368513));
#429405=CARTESIAN_POINT('Ctrl Pts',(-1.72079051918672,2.14522436846363,
12.4907278922777));
#429406=CARTESIAN_POINT('Ctrl Pts',(-1.69737943520329,2.15543377222162,
12.506463626192));
#429407=CARTESIAN_POINT('Ctrl Pts',(-1.70142731714501,2.16057401444572,
12.4999376786891));
#429408=CARTESIAN_POINT('Ctrl Pts',(-1.7013778781527,2.16051123386085,12.4906970594712));
#429409=CARTESIAN_POINT('Origin',(-1.71501309176457,2.12148865070642,12.5369868989719));
#429410=CARTESIAN_POINT('Origin',(-1.71501309176457,2.12148865070642,14.));
#429411=CARTESIAN_POINT('Origin',(-1.71501309176457,2.12148865070642,13.7435492065112));
#429412=CARTESIAN_POINT('Ctrl Pts',(-1.68257284468358,2.12817385253986,
13.793642941384));
#429413=CARTESIAN_POINT('Ctrl Pts',(-1.69192507402185,2.13359990316717,
13.8071662555867));
#429414=CARTESIAN_POINT('Ctrl Pts',(-1.70254422443381,2.12028626248691,
13.8103758687955));
#429415=CARTESIAN_POINT('Ctrl Pts',(-1.69697041429798,2.13647877243237,
13.7804579775006));
#429416=CARTESIAN_POINT('Ctrl Pts',(-1.7085153090511,2.14316525707442,13.7901904343351));
#429417=CARTESIAN_POINT('Ctrl Pts',(-1.72020366376397,2.13259935492315,
13.7927914348262));
#429418=CARTESIAN_POINT('Ctrl Pts',(-1.70544680539051,2.14136819128946,
13.7597120340895));
#429419=CARTESIAN_POINT('Ctrl Pts',(-1.71881037184997,2.14910137830751,
13.7635825532445));
#429420=CARTESIAN_POINT('Ctrl Pts',(-1.73063203532483,2.13983940287936,
13.7651073818885));
#429421=CARTESIAN_POINT('Ctrl Pts',(-1.7037869339277,2.14041073112157,13.7381884353898));
#429422=CARTESIAN_POINT('Ctrl Pts',(-1.71683725102629,2.14796368645392,
13.7368803041982));
#429423=CARTESIAN_POINT('Ctrl Pts',(-1.72859013215357,2.13842118037182,
13.7363986145813));
#429424=CARTESIAN_POINT('Origin',(-1.69705890579044,2.11113217953728,13.7902182540695));
#429425=CARTESIAN_POINT('Ctrl Pts',(-1.65508089516743,2.11231576596783,
13.8235227101244));
#429426=CARTESIAN_POINT('Ctrl Pts',(-1.66503768943828,2.11806423847515,
13.8358800583119));
#429427=CARTESIAN_POINT('Ctrl Pts',(-1.67576452834183,2.10543249369488,
13.8390832900376));
#429428=CARTESIAN_POINT('Ctrl Pts',(-1.66541281915797,2.11827550555509,
13.8124254819052));
#429429=CARTESIAN_POINT('Ctrl Pts',(-1.67538894952124,2.12403514127364,
13.8247886449157));
#429430=CARTESIAN_POINT('Ctrl Pts',(-1.68611635037659,2.11137640310625,
13.8279860620657));
#429431=CARTESIAN_POINT('Ctrl Pts',(-1.67574011271632,2.12423257418097,
13.8013225099955));
#429432=CARTESIAN_POINT('Ctrl Pts',(-1.68573087103815,2.13000065722366,
13.8136962257787));
#429433=CARTESIAN_POINT('Ctrl Pts',(-1.69646324505636,2.11731779584243,
13.8168830918626));
#429434=CARTESIAN_POINT('Ctrl Pts',(-1.68606295600545,2.13018707576847,
13.7902140179785));
#429435=CARTESIAN_POINT('Ctrl Pts',(-1.69606394186462,2.13596106774883,
13.802602731458));
#429436=CARTESIAN_POINT('Ctrl Pts',(-1.7068054050725,2.12325677238564,13.8057746032558));
#429437=CARTESIAN_POINT('Origin',(-1.66607683415938,2.09326086350714,13.8235269408515));
#429438=CARTESIAN_POINT('Ctrl Pts',(-1.60467127783313,2.15086502402588,
13.8235269408515));
#429439=CARTESIAN_POINT('Ctrl Pts',(-1.6076840083236,2.16228168175845,13.8362179249168));
#429440=CARTESIAN_POINT('Ctrl Pts',(-1.59209337512992,2.16925270468747,
13.8391868794938));
#429441=CARTESIAN_POINT('Ctrl Pts',(-1.6019147605707,2.14041927913812,13.8400110824519));
#429442=CARTESIAN_POINT('Ctrl Pts',(-1.60102246856986,2.15044552857883,
13.8494522556837));
#429443=CARTESIAN_POINT('Ctrl Pts',(-1.58766556384792,2.15203328916674,
13.85569149686));
#429444=CARTESIAN_POINT('Ctrl Pts',(-1.60457051206087,2.12434617395997,
13.8586819406588));
#429445=CARTESIAN_POINT('Ctrl Pts',(-1.6011203323933,2.12700179138279,13.868010383617));
#429446=CARTESIAN_POINT('Ctrl Pts',(-1.5922182107488,2.125375415959,13.8744918421245));
#429447=CARTESIAN_POINT('Ctrl Pts',(-1.62939492102075,2.10529833372175,
13.8587686893867));
#429448=CARTESIAN_POINT('Ctrl Pts',(-1.63281435977636,2.1026663066481,13.8680909899357));
#429449=CARTESIAN_POINT('Ctrl Pts',(-1.63354512787496,2.09366839691907,
13.8745789365162));
#429450=CARTESIAN_POINT('Ctrl Pts',(-1.64571100002057,2.10691095209924,
13.8400379222776));
#429451=CARTESIAN_POINT('Ctrl Pts',(-1.65561933451111,2.10867025353205,
13.8494748685452));
#429452=CARTESIAN_POINT('Ctrl Pts',(-1.66065117833342,2.09620262933925,
13.8557104837033));
#429453=CARTESIAN_POINT('Ctrl Pts',(-1.65508430441053,2.11231773338207,
13.8235269408542));
#429454=CARTESIAN_POINT('Ctrl Pts',(-1.66531219705122,2.11821746480994,
13.8362179249195));
#429455=CARTESIAN_POINT('Ctrl Pts',(-1.67612584604502,2.10499899290525,
13.8391868794965));
#429456=CARTESIAN_POINT('Origin',(-1.58339947057764,2.15647842015348,13.8235269408515));
#429457=CARTESIAN_POINT('Ctrl Pts',(-1.61379635744607,2.18544426037843,
13.7902140241682));
#429458=CARTESIAN_POINT('Ctrl Pts',(-1.6167472094838,2.19660898463136,13.8026027327198));
#429459=CARTESIAN_POINT('Ctrl Pts',(-1.60167170336877,2.20364510910788,
13.8057746032556));
#429460=CARTESIAN_POINT('Ctrl Pts',(-1.61075565827017,2.17392161609233,
13.8013225161808));
#429461=CARTESIAN_POINT('Ctrl Pts',(-1.61370348861245,2.18507492161842,
13.8136962270464));
#429462=CARTESIAN_POINT('Ctrl Pts',(-1.59865104943324,2.1921078925461,13.8168830918628));
#429463=CARTESIAN_POINT('Ctrl Pts',(-1.60771364822151,2.1623940042906,13.8124254880875));
#429464=CARTESIAN_POINT('Ctrl Pts',(-1.61065716058229,2.17353097919505,
13.8247886461867));
#429465=CARTESIAN_POINT('Ctrl Pts',(-1.59562930473771,2.18056547355589,
13.8279860620656));
#429466=CARTESIAN_POINT('Ctrl Pts',(-1.60467027423082,2.15086122386878,
13.8235227163065));
#429467=CARTESIAN_POINT('Ctrl Pts',(-1.60760808168087,2.1619766127789,13.8358800595847));
#429468=CARTESIAN_POINT('Ctrl Pts',(-1.59260642281724,2.16901763984442,
13.8390832900376));
#429469=CARTESIAN_POINT('Origin',(-1.59252555697101,2.1910614686938,13.7902182540695));
#429470=CARTESIAN_POINT('Ctrl Pts',(-1.61901707091557,2.2052281128403,13.7382347919292));
#429471=CARTESIAN_POINT('Ctrl Pts',(-1.62289063398972,2.21981280954076,
13.7369371795943));
#429472=CARTESIAN_POINT('Ctrl Pts',(-1.61058695297563,2.22865380555502,
13.7364597369711));
#429473=CARTESIAN_POINT('Ctrl Pts',(-1.61949971074945,2.20705706138388,
13.7595490285574));
#429474=CARTESIAN_POINT('Ctrl Pts',(-1.62346472198187,2.22198999452996,
13.7633824266926));
#429475=CARTESIAN_POINT('Ctrl Pts',(-1.61141055139078,2.23096722303704,
13.7648920890506));
#429476=CARTESIAN_POINT('Ctrl Pts',(-1.61703827404558,2.1977295240076,13.7803806590111));
#429477=CARTESIAN_POINT('Ctrl Pts',(-1.62047308450817,2.21064459129706,
13.7901039518744));
#429478=CARTESIAN_POINT('Ctrl Pts',(-1.60721525445259,2.21917192286346,
13.7926933640892));
#429479=CARTESIAN_POINT('Ctrl Pts',(-1.61275974751797,2.18151618189917,
13.7936647693663));
#429480=CARTESIAN_POINT('Ctrl Pts',(-1.61554832042228,2.19196592797752,
13.8072068914933));
#429481=CARTESIAN_POINT('Ctrl Pts',(-1.59989580680658,2.19872189477419,
13.8104111085397));
#429482=CARTESIAN_POINT('Origin',(-1.59781414626465,2.21110242955784,13.7435492065112));
#429483=CARTESIAN_POINT('Origin',(-1.59781414626465,2.21110242955784,14.));
#429484=CARTESIAN_POINT('Origin',(-1.59781414626465,2.21110242955784,12.5369868989719));
#429485=CARTESIAN_POINT('Ctrl Pts',(-1.63519533055901,2.20298361356624,
12.506462012331));
#429486=CARTESIAN_POINT('Ctrl Pts',(-1.63909246104785,2.20823394326472,
12.4999388158272));
#429487=CARTESIAN_POINT('Ctrl Pts',(-1.6390463528834,2.20817182497901,12.4907030323752));
#429488=CARTESIAN_POINT('Ctrl Pts',(-1.6260428171011,2.21259923006011,12.5042014951932));
#429489=CARTESIAN_POINT('Ctrl Pts',(-1.62469427205075,2.21888592421232,
12.4980716682127));
#429490=CARTESIAN_POINT('Ctrl Pts',(-1.61921190078417,2.22289456120277,
12.4907355092744));
#429491=CARTESIAN_POINT('Ctrl Pts',(-1.62040747561331,2.21046179525144,
12.5218047446509));
#429492=CARTESIAN_POINT('Ctrl Pts',(-1.6201162791044,2.22227001592727,12.5216906929434));
#429493=CARTESIAN_POINT('Ctrl Pts',(-1.6105149893975,2.22906604346504,12.5161988840775));
#429494=CARTESIAN_POINT('Ctrl Pts',(-1.61907611905049,2.20545189743654,
12.5369868989719));
#429495=CARTESIAN_POINT('Ctrl Pts',(-1.62301348435132,2.2202675204747,12.5369868989719));
#429496=CARTESIAN_POINT('Ctrl Pts',(-1.61047814233234,2.2290919599463,12.5369868989719));
#429497=CARTESIAN_POINT('Origin',(-3.12930240632751E-31,-1.05928948499644E-31,
12.5));
#429498=CARTESIAN_POINT('Origin',(-1.77464733364699,2.01291259190758,12.5));
#429499=CARTESIAN_POINT('',(-1.77464733364699,2.01291259190758,12.5893111709658));
#429500=CARTESIAN_POINT('',(-1.77464733364699,2.01291259190758,13.8235269408515));
#429501=CARTESIAN_POINT('',(-1.77464733364699,2.01291259190758,12.5));
#429502=CARTESIAN_POINT('',(-1.78656189325013,2.04663670744327,13.7902182540695));
#429503=CARTESIAN_POINT('',(-1.77464733364699,2.01291259190758,13.8235269408515));
#429504=CARTESIAN_POINT('',(-1.79346640956079,2.066179914539,13.7435492065112));
#429505=CARTESIAN_POINT('Origin',(-1.77075094931264,2.00188291300246,13.7445212918702));
#429506=CARTESIAN_POINT('',(-1.79346640956079,2.066179914539,12.5369868989719));
#429507=CARTESIAN_POINT('',(-1.79346640956079,2.066179914539,12.5));
#429508=CARTESIAN_POINT('Ctrl Pts',(-1.79346640956079,2.066179914539,12.5369868989719));
#429509=CARTESIAN_POINT('Ctrl Pts',(-1.78719795941931,2.04843709031031,
12.5544431401645));
#429510=CARTESIAN_POINT('Ctrl Pts',(-1.78092502591569,2.03068157594215,
12.5718848856037));
#429511=CARTESIAN_POINT('Ctrl Pts',(-1.77464733364699,2.01291259190758,
12.5893111709658));
#429512=CARTESIAN_POINT('Origin',(-2.0703688147757,2.08791744959,12.5));
#429513=CARTESIAN_POINT('',(-1.87282490594719,1.99452953679086,13.7435492065112));
#429514=CARTESIAN_POINT('',(-1.8540863125007,1.98567095876061,13.7902182540695));
#429515=CARTESIAN_POINT('Origin',(-1.80484452760419,1.96239214676757,13.7418732680449));
#429516=CARTESIAN_POINT('',(-1.82175065299149,1.97038443452173,13.8235269408515));
#429517=CARTESIAN_POINT('',(-1.8540863125007,1.98567095876061,13.7902182540695));
#429518=CARTESIAN_POINT('',(-1.82175065299149,1.97038443452173,12.5893111709658));
#429519=CARTESIAN_POINT('',(-1.82175065299149,1.97038443452173,12.5));
#429520=CARTESIAN_POINT('',(-1.87282490594719,1.99452953679086,12.5369868989719));
#429521=CARTESIAN_POINT('Ctrl Pts',(-1.82175065299149,1.97038443452173,
12.5893111709658));
#429522=CARTESIAN_POINT('Ctrl Pts',(-1.83878806993896,1.97843878971623,
12.5718848856037));
#429523=CARTESIAN_POINT('Ctrl Pts',(-1.85581257177986,1.9864870393575,12.5544431401645));
#429524=CARTESIAN_POINT('Ctrl Pts',(-1.87282490594719,1.99452953679086,
12.5369868989719));
#429525=CARTESIAN_POINT('',(-1.87282490594719,1.99452953679086,12.5));
#429526=CARTESIAN_POINT('Origin',(-1.80705902610795,2.00146170474476,12.5));
#429527=CARTESIAN_POINT('',(-1.78320468836154,1.97671174024261,13.8587068136939));
#429528=CARTESIAN_POINT('Ctrl Pts',(-1.82175065299418,1.9703844345157,13.8235269408542));
#429529=CARTESIAN_POINT('Ctrl Pts',(-1.82016645957971,1.96963551485868,
13.8262006681044));
#429530=CARTESIAN_POINT('Ctrl Pts',(-1.81847101414716,1.96902617684305,
13.8288634856214));
#429531=CARTESIAN_POINT('Ctrl Pts',(-1.81667371992282,1.96854696608446,
13.8314912288862));
#429532=CARTESIAN_POINT('Ctrl Pts',(-1.81482089495982,1.96805294922064,
13.8342001611531));
#429533=CARTESIAN_POINT('Ctrl Pts',(-1.81285790034408,1.96769619603974,
13.8368750301949));
#429534=CARTESIAN_POINT('Ctrl Pts',(-1.81076554033127,1.9675005977407,13.8394886372969));
#429535=CARTESIAN_POINT('Ctrl Pts',(-1.81060394229213,1.96748549120961,
13.8396904925131));
#429536=CARTESIAN_POINT('Ctrl Pts',(-1.81044156677802,1.9674713673101,13.8398919674349));
#429537=CARTESIAN_POINT('Ctrl Pts',(-1.81027840291465,1.96745824831066,
13.8400930404591));
#429538=CARTESIAN_POINT('Ctrl Pts',(-1.80773620015197,1.96725384547332,
13.8432258934518));
#429539=CARTESIAN_POINT('Ctrl Pts',(-1.80501568193227,1.96729331063822,
13.8462331177034));
#429540=CARTESIAN_POINT('Ctrl Pts',(-1.80220697616124,1.96767181281182,
13.8489036603661));
#429541=CARTESIAN_POINT('Ctrl Pts',(-1.80128793494641,1.96779566312788,
13.8497774930041));
#429542=CARTESIAN_POINT('Ctrl Pts',(-1.80035967723343,1.96795592102885,
13.85061494757));
#429543=CARTESIAN_POINT('Ctrl Pts',(-1.79942600972377,1.96815621757647,
13.8514076489583));
#429544=CARTESIAN_POINT('Ctrl Pts',(-1.79745116828584,1.96857987366177,
13.8530843267192));
#429545=CARTESIAN_POINT('Ctrl Pts',(-1.79525876334212,1.96922716236845,
13.8546805203176));
#429546=CARTESIAN_POINT('Ctrl Pts',(-1.793014676997,1.97019137671864,13.8559412814273));
#429547=CARTESIAN_POINT('Ctrl Pts',(-1.79271434546656,1.97032041986892,
13.8561100121513));
#429548=CARTESIAN_POINT('Ctrl Pts',(-1.79241311089752,1.97045506609962,
13.8562727473908));
#429549=CARTESIAN_POINT('Ctrl Pts',(-1.79211138402505,1.97059546433379,
13.8564289040185));
#429550=CARTESIAN_POINT('Ctrl Pts',(-1.79074305610068,1.97123216872404,
13.8571370725437));
#429551=CARTESIAN_POINT('Ctrl Pts',(-1.78934151240086,1.9720004249295,13.8577210840554));
#429552=CARTESIAN_POINT('Ctrl Pts',(-1.78797533798368,1.97289610599441,
13.8581177131616));
#429553=CARTESIAN_POINT('Ctrl Pts',(-1.78759057624551,1.97314836061069,
13.8582294175695));
#429554=CARTESIAN_POINT('Ctrl Pts',(-1.78720855353301,1.97341055756911,
13.8583265086086));
#429555=CARTESIAN_POINT('Ctrl Pts',(-1.78683061358246,1.97368220749652,
13.8584082369006));
#429556=CARTESIAN_POINT('Ctrl Pts',(-1.78628761522211,1.9740724955964,13.8585256585398));
#429557=CARTESIAN_POINT('Ctrl Pts',(-1.78574648246221,1.97448741125886,
13.8586122832068));
#429558=CARTESIAN_POINT('Ctrl Pts',(-1.78522175286843,1.97491680285174,
13.8586682984299));
#429559=CARTESIAN_POINT('Ctrl Pts',(-1.78480202120818,1.97526027356182,
13.8587131050557));
#429560=CARTESIAN_POINT('Ctrl Pts',(-1.78438800053653,1.97561661874028,
13.8587357943552));
#429561=CARTESIAN_POINT('Ctrl Pts',(-1.78397997203229,1.97598626457877,
13.8587355499465));
#429562=CARTESIAN_POINT('Ctrl Pts',(-1.78371625348208,1.97622517549701,
13.8587353919793));
#429563=CARTESIAN_POINT('Ctrl Pts',(-1.78345786391976,1.97646703034904,
13.8587257282814));
#429564=CARTESIAN_POINT('Ctrl Pts',(-1.78320468836154,1.97671174024261,
13.8587068136939));
#429565=CARTESIAN_POINT('Ctrl Pts',(-1.78320468836154,1.97671174024261,
13.8587068136939));
#429566=CARTESIAN_POINT('Ctrl Pts',(-1.78237200775288,1.97751657774173,
13.8586446046466));
#429567=CARTESIAN_POINT('Ctrl Pts',(-1.78159565778567,1.97835226114744,
13.858482427929));
#429568=CARTESIAN_POINT('Ctrl Pts',(-1.78087216243592,1.97921597919409,
13.8582284286032));
#429569=CARTESIAN_POINT('Ctrl Pts',(-1.78012994036745,1.98010205343822,
13.8579678548414));
#429570=CARTESIAN_POINT('Ctrl Pts',(-1.77944270557235,1.98102078035111,
13.857615680862));
#429571=CARTESIAN_POINT('Ctrl Pts',(-1.77882979270363,1.98193013579475,
13.8571944833187));
#429572=CARTESIAN_POINT('Ctrl Pts',(-1.77730020595615,1.98419952530559,
13.8561433417727));
#429573=CARTESIAN_POINT('Ctrl Pts',(-1.77615797266665,1.9865140237653,13.8546163505474));
#429574=CARTESIAN_POINT('Ctrl Pts',(-1.77532345585089,1.98868280188526,
13.8528973491086));
#429575=CARTESIAN_POINT('Ctrl Pts',(-1.7751710019408,1.98907900565043,13.8525833129072));
#429576=CARTESIAN_POINT('Ctrl Pts',(-1.77502867730194,1.98947036207524,
13.8522628768812));
#429577=CARTESIAN_POINT('Ctrl Pts',(-1.77489582404558,1.989855755336,13.851937733538));
#429578=CARTESIAN_POINT('Ctrl Pts',(-1.77408450764156,1.99220929850855,
13.8499521282529));
#429579=CARTESIAN_POINT('Ctrl Pts',(-1.7735496406591,1.99457567992749,13.847639871647));
#429580=CARTESIAN_POINT('Ctrl Pts',(-1.77324096984181,1.9968128189494,13.8452109780794));
#429581=CARTESIAN_POINT('Ctrl Pts',(-1.77310209245195,1.99781935410184,
13.8441181685877));
#429582=CARTESIAN_POINT('Ctrl Pts',(-1.7730083025553,1.99879988074523,13.8430021611332));
#429583=CARTESIAN_POINT('Ctrl Pts',(-1.7729521695578,1.99974313321985,13.8418824960098));
#429584=CARTESIAN_POINT('Ctrl Pts',(-1.77281989071578,2.0019659317631,13.8392439765549));
#429585=CARTESIAN_POINT('Ctrl Pts',(-1.77288662955065,2.00408777343718,
13.8364981347964));
#429586=CARTESIAN_POINT('Ctrl Pts',(-1.77311835894709,2.00611534551228,
13.8336931113419));
#429587=CARTESIAN_POINT('Ctrl Pts',(-1.77334404866305,2.00809007195069,
13.8309611966328));
#429588=CARTESIAN_POINT('Ctrl Pts',(-1.77372702748818,2.00997729349478,
13.8281701127186));
#429589=CARTESIAN_POINT('Ctrl Pts',(-1.77427060680018,2.01176482607106,
13.8253580685121));
#429590=CARTESIAN_POINT('Ctrl Pts',(-1.77438845538168,2.01215236506277,
13.8247484142933));
#429591=CARTESIAN_POINT('Ctrl Pts',(-1.77451396208275,2.01253508420346,
13.8241378483365));
#429592=CARTESIAN_POINT('Ctrl Pts',(-1.77464733364699,2.01291259190758,
13.8235269408515));
#429593=CARTESIAN_POINT('',(-1.78411440570672,1.97586605045878,12.5969504640361));
#429594=CARTESIAN_POINT('Origin',(-1.80708105265376,2.00148639308392,12.584524458991));
#429595=CARTESIAN_POINT('Origin',(-1.80708105265376,2.00148639308392,12.584524458991));
#429596=CARTESIAN_POINT('Ctrl Pts',(-1.82175065299149,1.97038443452173,
12.5893111709658));
#429597=CARTESIAN_POINT('Ctrl Pts',(-1.8115040052116,1.96554038210308,12.5770542771492));
#429598=CARTESIAN_POINT('Ctrl Pts',(-1.80187416435298,1.97877177809491,
12.5737548217797));
#429599=CARTESIAN_POINT('Ctrl Pts',(-1.8441566328089,1.98097675144902,12.5663937883685));
#429600=CARTESIAN_POINT('Ctrl Pts',(-1.83389691400673,1.97612651976878,
12.5540940315304));
#429601=CARTESIAN_POINT('Ctrl Pts',(-1.82423982857276,1.98940080680176,
12.5508374392248));
#429602=CARTESIAN_POINT('Ctrl Pts',(-1.86654000526735,1.99155838085839,
12.5434499600945));
#429603=CARTESIAN_POINT('Ctrl Pts',(-1.85624692846577,1.98669237934775,
12.5311293540533));
#429604=CARTESIAN_POINT('Ctrl Pts',(-1.84658414750019,2.00001838507236,
12.5278936106989));
#429605=CARTESIAN_POINT('Ctrl Pts',(-1.88890254123221,2.00213015991773,
12.5204817579905));
#429606=CARTESIAN_POINT('Ctrl Pts',(-1.87855852073481,1.99724007502505,
12.5081597038247));
#429607=CARTESIAN_POINT('Ctrl Pts',(-1.86890878612145,2.01062539036636,
12.5049254088044));
#429608=CARTESIAN_POINT('Ctrl Pts',(-1.87282490594719,1.99452953679086,
12.5369868989719));
#429609=CARTESIAN_POINT('Ctrl Pts',(-1.8736670477259,1.99492765536024,12.5342545179733));
#429610=CARTESIAN_POINT('Ctrl Pts',(-1.87441743383162,1.99542038023855,
12.5314872231885));
#429611=CARTESIAN_POINT('Ctrl Pts',(-1.87500311108837,1.9960266831835,12.5287124745063));
#429612=CARTESIAN_POINT('Ctrl Pts',(-1.87553130390893,1.99657347727345,
12.5262100684184));
#429613=CARTESIAN_POINT('Ctrl Pts',(-1.87592429322125,1.99721277981382,
12.5237004536639));
#429614=CARTESIAN_POINT('Ctrl Pts',(-1.87613235305885,1.99799028330282,
12.5212220730815));
#429615=CARTESIAN_POINT('Ctrl Pts',(-1.87629164086314,1.99858552948307,
12.5193246583486));
#429616=CARTESIAN_POINT('Ctrl Pts',(-1.8763438280053,1.99926905645787,12.517417831369));
#429617=CARTESIAN_POINT('Ctrl Pts',(-1.87619533138684,2.00006725033019,
12.5155812248348));
#429618=CARTESIAN_POINT('Ctrl Pts',(-1.8761320710292,2.00040728521011,12.5147988205793));
#429619=CARTESIAN_POINT('Ctrl Pts',(-1.87603259859886,2.00076852575646,
12.5140295443047));
#429620=CARTESIAN_POINT('Ctrl Pts',(-1.8758911871344,2.00115451222068,12.5132817086137));
#429621=CARTESIAN_POINT('Ctrl Pts',(-1.87567718001267,2.0017386505192,12.5121499604604));
#429622=CARTESIAN_POINT('Ctrl Pts',(-1.87535578452713,2.00238961753736,
12.5110494206568));
#429623=CARTESIAN_POINT('Ctrl Pts',(-1.87489007872744,2.00310254826459,
12.5100666561695));
#429624=CARTESIAN_POINT('Ctrl Pts',(-1.87462267152968,2.00351191144643,
12.5095023550641));
#429625=CARTESIAN_POINT('Ctrl Pts',(-1.87430404866123,2.00394607708666,
12.5089719619137));
#429626=CARTESIAN_POINT('Ctrl Pts',(-1.87393503319215,2.00439312839303,
12.5085043804652));
#429627=CARTESIAN_POINT('Ctrl Pts',(-1.8733950271208,2.00504732974738,12.5078201359221));
#429628=CARTESIAN_POINT('Ctrl Pts',(-1.87273051432205,2.00574733028379,
12.5072563000953));
#429629=CARTESIAN_POINT('Ctrl Pts',(-1.87198039897921,2.00643985158945,
12.5068768744336));
#429630=CARTESIAN_POINT('Ctrl Pts',(-1.8714395141789,2.00693920712416,12.5066032824118));
#429631=CARTESIAN_POINT('Ctrl Pts',(-1.87084465937544,2.007443490958,12.5064197834844));
#429632=CARTESIAN_POINT('Ctrl Pts',(-1.87023072430008,2.0079265142706,12.5063282718343));
#429633=CARTESIAN_POINT('Ctrl Pts',(-1.86933456915955,2.00863157876677,
12.5061946931565));
#429634=CARTESIAN_POINT('Ctrl Pts',(-1.86837926229331,2.00930724826534,
12.5062515701262));
#429635=CARTESIAN_POINT('Ctrl Pts',(-1.86743302163689,2.00992421523273,
12.5064436508398));
#429636=CARTESIAN_POINT('',(-1.80187416435298,1.97877177809491,12.5737548217797));
#429637=CARTESIAN_POINT('Origin',(-1.81234801178603,1.99027388746447,12.5893111709658));
#429638=CARTESIAN_POINT('Ctrl Pts',(-1.86743302163689,2.00992421523273,
12.5064436508398));
#429639=CARTESIAN_POINT('Ctrl Pts',(-1.85772840129906,2.00531327911846,
12.5164271754438));
#429640=CARTESIAN_POINT('Ctrl Pts',(-1.84802002371692,2.00070032651266,
12.5264061185523));
#429641=CARTESIAN_POINT('Ctrl Pts',(-1.83830775615727,1.99608528725107,
12.536380305637));
#429642=CARTESIAN_POINT('Ctrl Pts',(-1.82616939156783,1.99031742420491,
12.5488460165097));
#429643=CARTESIAN_POINT('Ctrl Pts',(-1.81402494728548,1.98454630009124,
12.5613043021964));
#429644=CARTESIAN_POINT('Ctrl Pts',(-1.80187416435298,1.97877177809491,
12.5737548217797));
#429645=CARTESIAN_POINT('Ctrl Pts',(-1.77464733364699,2.01291259190758,
12.5893111709658));
#429646=CARTESIAN_POINT('Ctrl Pts',(-1.77087180231227,2.00222596485784,
12.5770542771492));
#429647=CARTESIAN_POINT('Ctrl Pts',(-1.78501496771588,1.99399343503882,
12.5737548217797));
#429648=CARTESIAN_POINT('Ctrl Pts',(-1.77112479574953,2.00294206181754,
12.5928319619712));
#429649=CARTESIAN_POINT('Ctrl Pts',(-1.77165908407471,1.99467477977585,
12.5821634970842));
#429650=CARTESIAN_POINT('Ctrl Pts',(-1.78372289266241,1.9903645565033,12.5773203894503));
#429651=CARTESIAN_POINT('Ctrl Pts',(-1.77264103461714,1.98626018185646,
12.5969440695591));
#429652=CARTESIAN_POINT('Ctrl Pts',(-1.77561236721645,1.98355283534443,
12.5878292599214));
#429653=CARTESIAN_POINT('Ctrl Pts',(-1.78426534871378,1.98441897927902,
12.5813877129824));
#429654=CARTESIAN_POINT('Ctrl Pts',(-1.79531498602076,1.9657159083651,12.596957478804));
#429655=CARTESIAN_POINT('Ctrl Pts',(-1.79236566635355,1.9684033061119,12.5878468778671));
#429656=CARTESIAN_POINT('Ctrl Pts',(-1.79238467549314,1.97707031947235,
12.5814011370086));
#429657=CARTESIAN_POINT('Ctrl Pts',(-1.81217673858171,1.96585841350007,
12.5928371701607));
#429658=CARTESIAN_POINT('Ctrl Pts',(-1.80390373169794,1.96555440230808,
12.5821692192952));
#429659=CARTESIAN_POINT('Ctrl Pts',(-1.79838469434477,1.97711139364071,
12.5773318885715));
#429660=CARTESIAN_POINT('Ctrl Pts',(-1.82175065299151,1.97038443452168,
12.5893111709658));
#429661=CARTESIAN_POINT('Ctrl Pts',(-1.81150400521162,1.96554038210303,
12.5770542771492));
#429662=CARTESIAN_POINT('Ctrl Pts',(-1.80187416435301,1.97877177809486,
12.5737548217797));
#429663=CARTESIAN_POINT('',(-1.78501496771588,1.99399343503882,12.5737548217797));
#429664=CARTESIAN_POINT('Origin',(-1.79539081682201,2.00558402412337,12.5893111709658));
#429665=CARTESIAN_POINT('Ctrl Pts',(-1.80187416435301,1.97877177809486,
12.5737548217797));
#429666=CARTESIAN_POINT('Ctrl Pts',(-1.80098259957663,1.97831414081431,
12.5746934679442));
#429667=CARTESIAN_POINT('Ctrl Pts',(-1.79991237230225,1.97797070374669,
12.5756680099006));
#429668=CARTESIAN_POINT('Ctrl Pts',(-1.79878626149575,1.97777736952967,
12.5765688348656));
#429669=CARTESIAN_POINT('Ctrl Pts',(-1.79848813612619,1.97772618643599,
12.5768073183026));
#429670=CARTESIAN_POINT('Ctrl Pts',(-1.79818619792037,1.9776852883913,12.5770407398754));
#429671=CARTESIAN_POINT('Ctrl Pts',(-1.79788281576452,1.97765478576167,
12.5772674179684));
#429672=CARTESIAN_POINT('Ctrl Pts',(-1.79663781743491,1.97752961121792,
12.5781976435658));
#429673=CARTESIAN_POINT('Ctrl Pts',(-1.7952966608335,1.97758361541476,12.5790594849312));
#429674=CARTESIAN_POINT('Ctrl Pts',(-1.79395184584885,1.9778614019888,12.5797571720116));
#429675=CARTESIAN_POINT('Ctrl Pts',(-1.79307565053111,1.97804238993011,
12.580211740231));
#429676=CARTESIAN_POINT('Ctrl Pts',(-1.79216188119587,1.97834498302703,
12.5806009430798));
#429677=CARTESIAN_POINT('Ctrl Pts',(-1.7912804326555,1.97876469856761,12.5808812374708));
#429678=CARTESIAN_POINT('Ctrl Pts',(-1.79052297594182,1.97912537345615,
12.5811221033394));
#429679=CARTESIAN_POINT('Ctrl Pts',(-1.7897739284616,1.97958002455874,12.581287365893));
#429680=CARTESIAN_POINT('Ctrl Pts',(-1.7890798940038,1.98011011837575,12.581359338449));
#429681=CARTESIAN_POINT('Ctrl Pts',(-1.78898343754543,1.98018379047029,
12.5813693411482));
#429682=CARTESIAN_POINT('Ctrl Pts',(-1.78888799355128,1.9802588870091,12.5813775999465));
#429683=CARTESIAN_POINT('Ctrl Pts',(-1.78879363518637,1.98033532560312,
12.5813841266931));
#429684=CARTESIAN_POINT('Ctrl Pts',(-1.78863354480788,1.98046501292293,
12.5813952001081));
#429685=CARTESIAN_POINT('Ctrl Pts',(-1.78847589049102,1.98059990507425,
12.5814007534795));
#429686=CARTESIAN_POINT('Ctrl Pts',(-1.78832086911021,1.98074009315269,
12.5814005856065));
#429687=CARTESIAN_POINT('Ctrl Pts',(-1.78761124183826,1.9813818193658,12.5813998171494));
#429688=CARTESIAN_POINT('Ctrl Pts',(-1.78700558985925,1.98208993043124,
12.58127954464));
#429689=CARTESIAN_POINT('Ctrl Pts',(-1.78648486536318,1.98284117347202,
12.5810700125799));
#429690=CARTESIAN_POINT('Ctrl Pts',(-1.78585588946117,1.98374858952942,
12.5808169217085));
#429691=CARTESIAN_POINT('Ctrl Pts',(-1.78536451974292,1.9847285508345,12.5804173076348));
#429692=CARTESIAN_POINT('Ctrl Pts',(-1.78503053923674,1.98568350234591,
12.5799304713245));
#429693=CARTESIAN_POINT('Ctrl Pts',(-1.78461663217488,1.9868669881093,12.5793271277669));
#429694=CARTESIAN_POINT('Ctrl Pts',(-1.78438838901547,1.98807484483448,
12.5785808224116));
#429695=CARTESIAN_POINT('Ctrl Pts',(-1.78432426533182,1.98925026987088,
12.5777485681082));
#429696=CARTESIAN_POINT('Ctrl Pts',(-1.78422871401791,1.99100178195255,
12.576508418016));
#429697=CARTESIAN_POINT('Ctrl Pts',(-1.78449152043175,1.99266615940361,
12.5750928681475));
#429698=CARTESIAN_POINT('Ctrl Pts',(-1.78501496771588,1.99399343503882,
12.5737548217797));
#429699=CARTESIAN_POINT('Ctrl Pts',(-1.78501496771588,1.99399343503882,
12.5737548217797));
#429700=CARTESIAN_POINT('Ctrl Pts',(-1.77087180231227,2.00222596485784,
12.5770542771492));
#429701=CARTESIAN_POINT('Ctrl Pts',(-1.77464733364699,2.01291259190758,
12.5893111709658));
#429702=CARTESIAN_POINT('Ctrl Pts',(-1.79331016725534,2.01732162868452,
12.5508408821982));
#429703=CARTESIAN_POINT('Ctrl Pts',(-1.77912156531826,2.02557688759631,
12.55409748406));
#429704=CARTESIAN_POINT('Ctrl Pts',(-1.78290191326399,2.03627714804518,
12.5663972313419));
#429705=CARTESIAN_POINT('Ctrl Pts',(-1.80159615208642,2.04062742880315,
12.52790050457));
#429706=CARTESIAN_POINT('Ctrl Pts',(-1.78735552806453,2.04888308775984,
12.5311362602938));
#429707=CARTESIAN_POINT('Ctrl Pts',(-1.79114816536659,2.05961813318499,
12.5434568539655));
#429708=CARTESIAN_POINT('Ctrl Pts',(-1.8098736252625,2.06391258029882,12.5049357605811));
#429709=CARTESIAN_POINT('Ctrl Pts',(-1.79557533764729,2.07214922744812,
12.5081700652078));
#429710=CARTESIAN_POINT('Ctrl Pts',(-1.79938674216736,2.08293739341225,
12.5204921097672));
#429711=CARTESIAN_POINT('Ctrl Pts',(-1.80933009243161,2.06238358650823,
12.5064436508395));
#429712=CARTESIAN_POINT('Ctrl Pts',(-1.80856304590672,2.063332526664,12.5062361689309));
#429713=CARTESIAN_POINT('Ctrl Pts',(-1.80772491537427,2.06428663820413,
12.5061871075061));
#429714=CARTESIAN_POINT('Ctrl Pts',(-1.80686303822078,2.06516309950585,
12.5063648335164));
#429715=CARTESIAN_POINT('Ctrl Pts',(-1.80647152045487,2.06556124229146,
12.5064455676329));
#429716=CARTESIAN_POINT('Ctrl Pts',(-1.80606948454061,2.06594876045532,
12.506574497099));
#429717=CARTESIAN_POINT('Ctrl Pts',(-1.8056734392263,2.06630828171125,12.5067492519495));
#429718=CARTESIAN_POINT('Ctrl Pts',(-1.80487757079387,2.0670307536306,12.5071004286051));
#429719=CARTESIAN_POINT('Ctrl Pts',(-1.80407608942265,2.06766613145799,
12.5076537929612));
#429720=CARTESIAN_POINT('Ctrl Pts',(-1.80333502633357,2.06817413868651,
12.5083435010503));
#429721=CARTESIAN_POINT('Ctrl Pts',(-1.8032883719834,2.06820612077748,12.5083869222963));
#429722=CARTESIAN_POINT('Ctrl Pts',(-1.80324194526245,2.06823759168458,
12.5084308732336));
#429723=CARTESIAN_POINT('Ctrl Pts',(-1.8031957576404,2.06826853911802,12.5084753333615));
#429724=CARTESIAN_POINT('Ctrl Pts',(-1.80282527195008,2.06851677838069,
12.508831962269));
#429725=CARTESIAN_POINT('Ctrl Pts',(-1.80246336689796,2.06873744793491,
12.509227847131));
#429726=CARTESIAN_POINT('Ctrl Pts',(-1.8021222615155,2.06892637681182,12.5096423454524));
#429727=CARTESIAN_POINT('Ctrl Pts',(-1.80105338821379,2.06951839629562,
12.5109411997424));
#429728=CARTESIAN_POINT('Ctrl Pts',(-1.80012769271963,2.0698436192065,12.5124831113042));
#429729=CARTESIAN_POINT('Ctrl Pts',(-1.79933802615312,2.0699964105322,12.5140723025008));
#429730=CARTESIAN_POINT('Ctrl Pts',(-1.79926403353094,2.07001072724677,
12.5142212114565));
#429731=CARTESIAN_POINT('Ctrl Pts',(-1.79919122275552,2.07002355688239,
12.5143705582413));
#429732=CARTESIAN_POINT('Ctrl Pts',(-1.79911958222345,2.0700349930612,12.5145201959299));
#429733=CARTESIAN_POINT('Ctrl Pts',(-1.79819925292737,2.07018190780463,
12.5164425148273));
#429734=CARTESIAN_POINT('Ctrl Pts',(-1.79744221046146,2.07011449501529,
12.518463520594));
#429735=CARTESIAN_POINT('Ctrl Pts',(-1.79679585290887,2.06990604191506,
12.5205025929157));
#429736=CARTESIAN_POINT('Ctrl Pts',(-1.79642093990914,2.06978513085462,
12.5216853356836));
#429737=CARTESIAN_POINT('Ctrl Pts',(-1.79608379522748,2.06961744597704,
12.5228750347131));
#429738=CARTESIAN_POINT('Ctrl Pts',(-1.79577915787028,2.06942045884763,
12.5240609649613));
#429739=CARTESIAN_POINT('Ctrl Pts',(-1.79503144182028,2.06893696450648,
12.5269717671327));
#429740=CARTESIAN_POINT('Ctrl Pts',(-1.79446416096251,2.06825460725651,
12.5299036066169));
#429741=CARTESIAN_POINT('Ctrl Pts',(-1.79402045261618,2.06743877943794,
12.532813300402));
#429742=CARTESIAN_POINT('Ctrl Pts',(-1.79380744677358,2.0670471345808,12.5342101228452));
#429743=CARTESIAN_POINT('Ctrl Pts',(-1.79362364510772,2.06662496890918,
12.5356023438238));
#429744=CARTESIAN_POINT('Ctrl Pts',(-1.79346640956079,2.066179914539,12.5369868989719));
#429745=CARTESIAN_POINT('Origin',(-6.03418914296824,14.0854309020258,-1.24015958218552));
#429746=CARTESIAN_POINT('Ctrl Pts',(-1.8727871381517,1.99451163833927,12.5369868989719));
#429747=CARTESIAN_POINT('Ctrl Pts',(-1.88664208027583,2.00109372633821,
12.5369868989719));
#429748=CARTESIAN_POINT('Ctrl Pts',(-1.8976089644341,1.99036941957516,12.5369868989719));
#429749=CARTESIAN_POINT('Ctrl Pts',(-1.87747067886539,1.99673658170076,
12.5218025310016));
#429750=CARTESIAN_POINT('Ctrl Pts',(-1.88913914752845,1.9986081325992,12.5216901060418));
#429751=CARTESIAN_POINT('Ctrl Pts',(-1.89757554526698,1.99040212260739,
12.5161920673678));
#429752=CARTESIAN_POINT('Ctrl Pts',(-1.87854581061836,2.00266786848435,
12.5042015548895));
#429753=CARTESIAN_POINT('Ctrl Pts',(-1.88497583778361,2.00248871583569,
12.4980677368514));
#429754=CARTESIAN_POINT('Ctrl Pts',(-1.88992043201053,1.99782590899263,
12.4907278922777));
#429755=CARTESIAN_POINT('Ctrl Pts',(-1.86741940766348,2.00990956248433,
12.5064636261921));
#429756=CARTESIAN_POINT('Ctrl Pts',(-1.87187279807295,2.01470276101957,
12.4999376786892));
#429757=CARTESIAN_POINT('Ctrl Pts',(-1.87181840638433,2.01464421906876,
12.4906970594712));
#429758=CARTESIAN_POINT('Origin',(-1.88222754715265,1.97464008384812,12.5369868989719));
#429759=CARTESIAN_POINT('Origin',(-1.88222754715265,1.97464008384812,14.));
#429760=CARTESIAN_POINT('Origin',(-1.88222754715265,1.97464008384812,13.7435492065112));
#429761=CARTESIAN_POINT('Ctrl Pts',(-1.8504401483295,1.98394722252162,13.793642941384));
#429762=CARTESIAN_POINT('Ctrl Pts',(-1.86020353239528,1.98859292490015,
13.8071662555867));
#429763=CARTESIAN_POINT('Ctrl Pts',(-1.86970216314701,1.97445802491901,
13.8103758687955));
#429764=CARTESIAN_POINT('Ctrl Pts',(-1.86546673928909,1.9910509728942,13.7804579775006));
#429765=CARTESIAN_POINT('Ctrl Pts',(-1.87751822992994,1.99677419271026,
13.7901904343352));
#429766=CARTESIAN_POINT('Ctrl Pts',(-1.88830647349234,1.98529073830824,
13.7927914348262));
#429767=CARTESIAN_POINT('Ctrl Pts',(-1.87431345891751,1.99523321804838,
13.7597120340895));
#429768=CARTESIAN_POINT('Ctrl Pts',(-1.88826288574537,2.00185141879679,
13.7635825532445));
#429769=CARTESIAN_POINT('Ctrl Pts',(-1.89929027662885,1.99165668650768,
13.7651073818884));
#429770=CARTESIAN_POINT('Ctrl Pts',(-1.87258106864775,1.99441423868393,
13.7381884353898));
#429771=CARTESIAN_POINT('Ctrl Pts',(-1.88620359787057,2.00087834018372,
13.7368803041982));
#429772=CARTESIAN_POINT('Ctrl Pts',(-1.89713956942145,1.9904096170831,13.7363986145813));
#429773=CARTESIAN_POINT('Origin',(-1.86348895370616,1.96578150581787,13.7902182540695));
#429774=CARTESIAN_POINT('Ctrl Pts',(-1.82174709473251,1.97038275153282,
13.8235227101244));
#429775=CARTESIAN_POINT('Ctrl Pts',(-1.83213931246737,1.97530052530466,
13.8358800583119));
#429776=CARTESIAN_POINT('Ctrl Pts',(-1.84180085423239,1.96183647465935,
13.8390832900376));
#429777=CARTESIAN_POINT('Ctrl Pts',(-1.83253041420221,1.97548051285612,
13.8124254819053));
#429778=CARTESIAN_POINT('Ctrl Pts',(-1.84294281359559,1.9804078366235,13.8247886449158));
#429779=CARTESIAN_POINT('Ctrl Pts',(-1.85260271523091,1.966916836605,13.8279860620657));
#429780=CARTESIAN_POINT('Ctrl Pts',(-1.8433089009389,1.98057598952865,13.8013225099954));
#429781=CARTESIAN_POINT('Ctrl Pts',(-1.85373656815285,1.98551054019794,
13.8136962257787));
#429782=CARTESIAN_POINT('Ctrl Pts',(-1.86339946013736,1.97199509187472,
13.8168830918626));
#429783=CARTESIAN_POINT('Ctrl Pts',(-1.85408274297684,1.98566927044266,
13.7902140179785));
#429784=CARTESIAN_POINT('Ctrl Pts',(-1.86452108533012,1.99060887674889,
13.802602731458));
#429785=CARTESIAN_POINT('Ctrl Pts',(-1.87419128919226,1.97707132491017,
13.8057746032558));
#429786=CARTESIAN_POINT('Origin',(-1.83115329419695,1.950494981579,13.8235269408515));
#429787=CARTESIAN_POINT('Ctrl Pts',(-1.77464733364699,2.01291259190758,
13.8235269408515));
#429788=CARTESIAN_POINT('Ctrl Pts',(-1.77858060311757,2.02404569614956,
13.8362179249168));
#429789=CARTESIAN_POINT('Ctrl Pts',(-1.76361004955423,2.03226430491651,
13.8391868794938));
#429790=CARTESIAN_POINT('Ctrl Pts',(-1.77104856328642,2.00272628612134,
13.8400110824519));
#429791=CARTESIAN_POINT('Ctrl Pts',(-1.77097647272219,2.0127919041258,13.8494522556836));
#429792=CARTESIAN_POINT('Ctrl Pts',(-1.75779342922683,2.0154630933057,13.85569149686));
#429793=CARTESIAN_POINT('Ctrl Pts',(-1.77238537069517,1.9864901944735,13.8586819406588));
#429794=CARTESIAN_POINT('Ctrl Pts',(-1.76916312868933,1.98941819722124,
13.868010383617));
#429795=CARTESIAN_POINT('Ctrl Pts',(-1.76015806342466,1.98852283898479,
13.8744918421245));
#429796=CARTESIAN_POINT('Ctrl Pts',(-1.79557460267115,1.96548231456356,
13.8587686893867));
#429797=CARTESIAN_POINT('Ctrl Pts',(-1.79876812888534,1.96258032933977,
13.8680909899357));
#429798=CARTESIAN_POINT('Ctrl Pts',(-1.79876305223794,1.95355279502892,
13.8745789365163));
#429799=CARTESIAN_POINT('Ctrl Pts',(-1.81196783463268,1.96575965517686,
13.8400379222776));
#429800=CARTESIAN_POINT('Ctrl Pts',(-1.82198659935692,1.9667054814338,13.8494748685453));
#429801=CARTESIAN_POINT('Ctrl Pts',(-1.82598547301851,1.95386920024712,
13.8557104837033));
#429802=CARTESIAN_POINT('Ctrl Pts',(-1.82175065299418,1.9703844345157,13.8235269408542));
#429803=CARTESIAN_POINT('Ctrl Pts',(-1.83242539604766,1.9754308668726,13.8362179249195));
#429804=CARTESIAN_POINT('Ctrl Pts',(-1.84212563534195,1.9613749655607,13.8391868794965));
#429805=CARTESIAN_POINT('Origin',(-1.75390385047197,2.02024115969178,13.8235269408515));
#429806=CARTESIAN_POINT('Ctrl Pts',(-1.78656057909098,2.04663299000219,
13.7902140241682));
#429807=CARTESIAN_POINT('Ctrl Pts',(-1.79041164108685,2.05752004272074,
13.8026027327198));
#429808=CARTESIAN_POINT('Ctrl Pts',(-1.7759598069398,2.06576154877605,13.8057746032556));
#429809=CARTESIAN_POINT('Ctrl Pts',(-1.78259079511043,2.03539653157572,
13.8013225161808));
#429810=CARTESIAN_POINT('Ctrl Pts',(-1.78643791473303,2.04627244985853,
13.8136962270464));
#429811=CARTESIAN_POINT('Ctrl Pts',(-1.77200881372497,2.05450893268876,
13.8168830918628));
#429812=CARTESIAN_POINT('Ctrl Pts',(-1.77861929972028,2.0241552290109,13.8124254880875));
#429813=CARTESIAN_POINT('Ctrl Pts',(-1.78246078463185,2.03501522296646,
13.8247886461867));
#429814=CARTESIAN_POINT('Ctrl Pts',(-1.76805630933336,2.04325122039075,
13.8279860620656));
#429815=CARTESIAN_POINT('Ctrl Pts',(-1.774646023636,2.01290888619809,13.8235227163065));
#429816=CARTESIAN_POINT('Ctrl Pts',(-1.77848006316053,2.02374783098812,
13.8358800595847));
#429817=CARTESIAN_POINT('Ctrl Pts',(-1.76410223015076,2.03198820408291,
13.8390832900376));
#429818=CARTESIAN_POINT('Origin',(-1.76581841007511,2.05396527522747,13.7902182540695));
#429819=CARTESIAN_POINT('Ctrl Pts',(-1.79337648870707,2.06592547671255,
13.7382347919292));
#429820=CARTESIAN_POINT('Ctrl Pts',(-1.79842595099843,2.08014591268695,
13.7369371795942));
#429821=CARTESIAN_POINT('Ctrl Pts',(-1.7868838327189,2.08996035524074,13.7364597369711));
#429822=CARTESIAN_POINT('Ctrl Pts',(-1.79400659888214,2.06770899995365,
13.7595490285574));
#429823=CARTESIAN_POINT('Ctrl Pts',(-1.79917558954875,2.08226905977173,
13.7633824266926));
#429824=CARTESIAN_POINT('Ctrl Pts',(-1.78789325567977,2.09219894410019,
13.7648920890506));
#429825=CARTESIAN_POINT('Ctrl Pts',(-1.79079307151705,2.05861312913077,
13.7803806590111));
#429826=CARTESIAN_POINT('Ctrl Pts',(-1.79526915081292,2.07120525365933,
13.7901039518744));
#429827=CARTESIAN_POINT('Ctrl Pts',(-1.78275049177969,2.08078484746259,
13.7926933640892));
#429828=CARTESIAN_POINT('Ctrl Pts',(-1.78520724353435,2.04280247521258,
13.7936647693663));
#429829=CARTESIAN_POINT('Ctrl Pts',(-1.78883828900845,2.05299015604334,
13.8072068914933));
#429830=CARTESIAN_POINT('Ctrl Pts',(-1.77378853185383,2.06099946808836,
13.8104111085397));
#429831=CARTESIAN_POINT('Origin',(-1.77272292638577,2.0735084823232,13.7435492065112));
#429832=CARTESIAN_POINT('Origin',(-1.77272292638577,2.0735084823232,14.));
#429833=CARTESIAN_POINT('Origin',(-1.77272292638577,2.0735084823232,12.5369868989719));
#429834=CARTESIAN_POINT('Ctrl Pts',(-1.8093179689984,2.06236976747208,12.506462012331));
#429835=CARTESIAN_POINT('Ctrl Pts',(-1.81363008271914,2.06728497481759,
12.4999388158272));
#429836=CARTESIAN_POINT('Ctrl Pts',(-1.81357906475883,2.06722682146879,
12.4907030323752));
#429837=CARTESIAN_POINT('Ctrl Pts',(-1.80097967178528,2.07269940360991,
12.5042014951932));
#429838=CARTESIAN_POINT('Ctrl Pts',(-1.80014803784357,2.07907509824681,
12.4980716682127));
#429839=CARTESIAN_POINT('Ctrl Pts',(-1.79501064984419,2.08351726098247,
12.4907355092744));
#429840=CARTESIAN_POINT('Ctrl Pts',(-1.79518886065152,2.07102841358646,
12.5218047446509));
#429841=CARTESIAN_POINT('Ctrl Pts',(-1.7958611126822,2.08282107860093,12.5216906929434));
#429842=CARTESIAN_POINT('Ctrl Pts',(-1.78684570981034,2.09037708716282,
12.5161988840775));
#429843=CARTESIAN_POINT('Ctrl Pts',(-1.7934535808863,2.06614370371284,12.5369868989719));
#429844=CARTESIAN_POINT('Ctrl Pts',(-1.79858545574804,2.0805890971628,12.5369868989719));
#429845=CARTESIAN_POINT('Ctrl Pts',(-1.78681109778457,2.09040592078701,
12.5369868989719));
#429846=CARTESIAN_POINT('Origin',(-3.45247261328837E-31,-1.32797438156907E-31,
12.5));
#429847=CARTESIAN_POINT('Origin',(-1.93281340425162,1.86156455859733,12.5));
#429848=CARTESIAN_POINT('',(-1.93281340425162,1.86156455859733,12.5893111709658));
#429849=CARTESIAN_POINT('',(-1.93281340425162,1.86156455859733,13.8235269408515));
#429850=CARTESIAN_POINT('',(-1.93281340425162,1.86156455859733,12.5));
#429851=CARTESIAN_POINT('',(-1.94743714763615,1.89420531270359,13.7902182540695));
#429852=CARTESIAN_POINT('',(-1.93281340425162,1.86156455859733,13.8235269408515));
#429853=CARTESIAN_POINT('',(-1.95591164254695,1.91312070921219,13.7435492065112));
#429854=CARTESIAN_POINT('Origin',(-1.92803096359008,1.85088917153589,13.7445212918708));
#429855=CARTESIAN_POINT('',(-1.95591164254695,1.91312070921219,12.5369868989719));
#429856=CARTESIAN_POINT('',(-1.95591164254695,1.91312070921219,12.5));
#429857=CARTESIAN_POINT('Ctrl Pts',(-1.95591164254695,1.91312070921219,
12.5369868989719));
#429858=CARTESIAN_POINT('Ctrl Pts',(-1.94821784526522,1.89594785964742,
12.5544431401645));
#429859=CARTESIAN_POINT('Ctrl Pts',(-1.94051854517519,1.87876272760421,
12.5718848856037));
#429860=CARTESIAN_POINT('Ctrl Pts',(-1.93281340425162,1.86156455859733,
12.5893111709658));
#429861=CARTESIAN_POINT('Origin',(-2.23366448875944,1.912215797747,12.5));
#429862=CARTESIAN_POINT('',(-2.02916590912711,1.83524028800144,13.7435492065112));
#429863=CARTESIAN_POINT('',(-2.009767610456,1.82793855548531,13.7902182540695));
#429864=CARTESIAN_POINT('Origin',(-1.9587922342461,1.80875086442513,13.7418732680437));
#429865=CARTESIAN_POINT('',(-1.97629355154766,1.8153385523344,13.8235269408515));
#429866=CARTESIAN_POINT('',(-2.009767610456,1.82793855548531,13.7902182540695));
#429867=CARTESIAN_POINT('',(-1.97629355154766,1.8153385523344,12.5893111709658));
#429868=CARTESIAN_POINT('',(-1.97629355154766,1.8153385523344,12.5));
#429869=CARTESIAN_POINT('',(-2.02916590912711,1.83524028800144,12.5369868989719));
#429870=CARTESIAN_POINT('Ctrl Pts',(-1.97629355154766,1.8153385523344,12.5893111709658));
#429871=CARTESIAN_POINT('Ctrl Pts',(-1.99393078261707,1.82197739967754,
12.5718848856037));
#429872=CARTESIAN_POINT('Ctrl Pts',(-2.01155464389458,1.82861121448428,
12.5544431401645));
#429873=CARTESIAN_POINT('Ctrl Pts',(-2.02916590912711,1.83524028800144,
12.5369868989719));
#429874=CARTESIAN_POINT('',(-2.02916590912711,1.83524028800144,12.5));
#429875=CARTESIAN_POINT('Origin',(-1.96418389587109,1.84750991948588,12.5));
#429876=CARTESIAN_POINT('',(-1.93839157959151,1.82478665842783,13.8587068136939));
#429877=CARTESIAN_POINT('Ctrl Pts',(-1.97629355154985,1.81533855232817,
13.8235269408542));
#429878=CARTESIAN_POINT('Ctrl Pts',(-1.9746535855036,1.81472125110974,13.8262006681044));
#429879=CARTESIAN_POINT('Ctrl Pts',(-1.97291411482078,1.8142521351586,13.8288634856214));
#429880=CARTESIAN_POINT('Ctrl Pts',(-1.9710837408191,1.81392101509882,13.8314912288862));
#429881=CARTESIAN_POINT('Ctrl Pts',(-1.96919681401769,1.81357966447064,
13.8342001611531));
#429882=CARTESIAN_POINT('Ctrl Pts',(-1.96721127240841,1.81338410064125,
13.8368750301949));
#429883=CARTESIAN_POINT('Ctrl Pts',(-1.96510993147372,1.81335969994498,
13.8394886372969));
#429884=CARTESIAN_POINT('Ctrl Pts',(-1.9649476398162,1.81335781542002,13.8396904925131));
#429885=CARTESIAN_POINT('Ctrl Pts',(-1.96478465336429,1.81335697362844,
13.8398919674349));
#429886=CARTESIAN_POINT('Ctrl Pts',(-1.96462096309497,1.81335719765099,
13.8400930404591));
#429887=CARTESIAN_POINT('Ctrl Pts',(-1.96207055857344,1.81336068807305,
13.8432258934518));
#429888=CARTESIAN_POINT('Ctrl Pts',(-1.959362309431,1.81362176941183,13.8462331177034));
#429889=CARTESIAN_POINT('Ctrl Pts',(-1.95659380083772,1.81422794774577,
13.8489036603661));
#429890=CARTESIAN_POINT('Ctrl Pts',(-1.95568791260724,1.81442629635108,
13.849777493004));
#429891=CARTESIAN_POINT('Ctrl Pts',(-1.95477580610192,1.81466168262824,
13.85061494757));
#429892=CARTESIAN_POINT('Ctrl Pts',(-1.95386157132197,1.81493741527541,
13.8514076489583));
#429893=CARTESIAN_POINT('Ctrl Pts',(-1.95192783290997,1.81552062959076,
13.8530843267192));
#429894=CARTESIAN_POINT('Ctrl Pts',(-1.94979548305156,1.81634446585388,
13.8546805203176));
#429895=CARTESIAN_POINT('Ctrl Pts',(-1.94763745613948,1.81748838573059,
13.8559412814273));
#429896=CARTESIAN_POINT('Ctrl Pts',(-1.94734864215218,1.81764147930829,
13.8561100121513));
#429897=CARTESIAN_POINT('Ctrl Pts',(-1.94705938483413,1.81780023092866,
13.8562727473908));
#429898=CARTESIAN_POINT('Ctrl Pts',(-1.94677010569243,1.81796475554049,
13.8564289040185));
#429899=CARTESIAN_POINT('Ctrl Pts',(-1.94545822808503,1.81871087277817,
13.8571370725437));
#429900=CARTESIAN_POINT('Ctrl Pts',(-1.94412396791914,1.81959081149731,
13.8577210840554));
#429901=CARTESIAN_POINT('Ctrl Pts',(-1.94283534565652,1.82059486815531,
13.8581177131616));
#429902=CARTESIAN_POINT('Ctrl Pts',(-1.94247242527434,1.82087764506878,
13.8582294175695));
#429903=CARTESIAN_POINT('Ctrl Pts',(-1.94211304519712,1.82117010798605,
13.8583265086086));
#429904=CARTESIAN_POINT('Ctrl Pts',(-1.94175850480154,1.82147165963533,
13.8584082369006));
#429905=CARTESIAN_POINT('Ctrl Pts',(-1.94124912532684,1.82190490849107,
13.8585256585398));
#429906=CARTESIAN_POINT('Ctrl Pts',(-1.94074361261994,1.82236255089946,
13.8586122832068));
#429907=CARTESIAN_POINT('Ctrl Pts',(-1.94025562842169,1.82283328406048,
13.8586682984299));
#429908=CARTESIAN_POINT('Ctrl Pts',(-1.93986528943541,1.82320982392702,
13.8587131050557));
#429909=CARTESIAN_POINT('Ctrl Pts',(-1.93948169182359,1.82359872992462,
13.8587357943552));
#429910=CARTESIAN_POINT('Ctrl Pts',(-1.939105150568,1.82400040390811,13.8587355499465));
#429911=CARTESIAN_POINT('Ctrl Pts',(-1.93886178297736,1.82426001537999,
13.8587353919793));
#429912=CARTESIAN_POINT('Ctrl Pts',(-1.93862396660077,1.82452212662797,
13.8587257282814));
#429913=CARTESIAN_POINT('Ctrl Pts',(-1.93839157959151,1.82478665842783,
13.8587068136939));
#429914=CARTESIAN_POINT('Ctrl Pts',(-1.93839157959151,1.82478665842783,
13.8587068136939));
#429915=CARTESIAN_POINT('Ctrl Pts',(-1.93762727138672,1.82565668909649,
13.8586446046466));
#429916=CARTESIAN_POINT('Ctrl Pts',(-1.93692162061559,1.82655287156429,
13.858482427929));
#429917=CARTESIAN_POINT('Ctrl Pts',(-1.93627093367604,1.82747268724808,
13.8582284286032));
#429918=CARTESIAN_POINT('Ctrl Pts',(-1.93560340456708,1.82841631114229,
13.8579678548414));
#429919=CARTESIAN_POINT('Ctrl Pts',(-1.93499334126151,1.82938799708295,
13.857615680862));
#429920=CARTESIAN_POINT('Ctrl Pts',(-1.9344565887205,1.83034428481017,13.8571944833187));
#429921=CARTESIAN_POINT('Ctrl Pts',(-1.93311706785987,1.83273079863454,
13.8561433417727));
#429922=CARTESIAN_POINT('Ctrl Pts',(-1.93216728836863,1.83513069840862,
13.8546163505474));
#429923=CARTESIAN_POINT('Ctrl Pts',(-1.93151232388946,1.83736028096605,
13.8528973491086));
#429924=CARTESIAN_POINT('Ctrl Pts',(-1.93139267154222,1.83776759280487,
13.8525833129072));
#429925=CARTESIAN_POINT('Ctrl Pts',(-1.93128271965864,1.83816924780281,
13.8522628768812));
#429926=CARTESIAN_POINT('Ctrl Pts',(-1.9311817215891,1.83856418747303,13.851937733538));
#429927=CARTESIAN_POINT('Ctrl Pts',(-1.93056494039128,1.84097602924366,
13.8499521282529));
#429928=CARTESIAN_POINT('Ctrl Pts',(-1.93022473518864,1.84337813334817,
13.847639871647));
#429929=CARTESIAN_POINT('Ctrl Pts',(-1.9300994390469,1.84563298801171,13.8452109780794));
#429930=CARTESIAN_POINT('Ctrl Pts',(-1.93004306571924,1.846647493798,13.8441181685877));
#429931=CARTESIAN_POINT('Ctrl Pts',(-1.93002950992493,1.84763240256716,
13.8430021611332));
#429932=CARTESIAN_POINT('Ctrl Pts',(-1.93005044753876,1.84857709180739,
13.8418824960098));
#429933=CARTESIAN_POINT('Ctrl Pts',(-1.93009978756041,1.8508032761255,13.8392439765549));
#429934=CARTESIAN_POINT('Ctrl Pts',(-1.93033925412197,1.85291261771184,
13.8364981347964));
#429935=CARTESIAN_POINT('Ctrl Pts',(-1.93073547840514,1.85491455511104,
13.8336931113419));
#429936=CARTESIAN_POINT('Ctrl Pts',(-1.93112137569438,1.85686431500308,
13.8309611966328));
#429937=CARTESIAN_POINT('Ctrl Pts',(-1.93165690626502,1.85871404064352,
13.8281701127186));
#429938=CARTESIAN_POINT('Ctrl Pts',(-1.93234437736132,1.86045131859234,
13.8253580685121));
#429939=CARTESIAN_POINT('Ctrl Pts',(-1.93249342183694,1.86082796232657,
13.8247484142933));
#429940=CARTESIAN_POINT('Ctrl Pts',(-1.93264970608777,1.86119917803961,
13.8241378483365));
#429941=CARTESIAN_POINT('Ctrl Pts',(-1.93281340425162,1.86156455859733,
13.8235269408515));
#429942=CARTESIAN_POINT('',(-1.93922933835866,1.82386963219822,12.5969504640361));
#429943=CARTESIAN_POINT('Origin',(-1.96420786145421,1.84753273030865,12.584524458991));
#429944=CARTESIAN_POINT('Origin',(-1.96420786145421,1.84753273030865,12.584524458991));
#429945=CARTESIAN_POINT('Ctrl Pts',(-1.97629355154766,1.8153385523344,12.5893111709658));
#429946=CARTESIAN_POINT('Ctrl Pts',(-1.96568616340087,1.81134581501986,
12.5770542771492));
#429947=CARTESIAN_POINT('Ctrl Pts',(-1.95716684665092,1.8253181060621,12.5737548217797));
#429948=CARTESIAN_POINT('Ctrl Pts',(-1.99948834947938,1.82406932883881,
12.5663937883685));
#429949=CARTESIAN_POINT('Ctrl Pts',(-1.98886743013587,1.82007149823336,
12.5540940315303));
#429950=CARTESIAN_POINT('Ctrl Pts',(-1.98032445548272,1.8340887582862,12.5508374392248));
#429951=CARTESIAN_POINT('Ctrl Pts',(-2.02265974414446,1.83279129609681,
12.5434499600945));
#429952=CARTESIAN_POINT('Ctrl Pts',(-2.01200429240993,1.82878046712038,
12.5311293540533));
#429953=CARTESIAN_POINT('Ctrl Pts',(-2.00345985673006,1.84284973801384,
12.5278936106989));
#429954=CARTESIAN_POINT('Ctrl Pts',(-2.04580956875261,1.84150514414865,
12.5204817579905));
#429955=CARTESIAN_POINT('Ctrl Pts',(-2.03510137981401,1.83747446430979,
12.5081597038247));
#429956=CARTESIAN_POINT('Ctrl Pts',(-2.02657478136005,1.85160178407327,
12.5049254088044));
#429957=CARTESIAN_POINT('Ctrl Pts',(-2.02916590912711,1.83524028800144,
12.5369868989719));
#429958=CARTESIAN_POINT('Ctrl Pts',(-2.03003769910788,1.8355684394911,12.5342545179733));
#429959=CARTESIAN_POINT('Ctrl Pts',(-2.03082575001755,1.83599836143416,
12.5314872231885));
#429960=CARTESIAN_POINT('Ctrl Pts',(-2.0314588978002,1.83655490882249,12.5287124745063));
#429961=CARTESIAN_POINT('Ctrl Pts',(-2.03202990189724,1.83705683088183,
12.5262100684184));
#429962=CARTESIAN_POINT('Ctrl Pts',(-2.03247369266208,1.83766197391845,
12.5237004536639));
#429963=CARTESIAN_POINT('Ctrl Pts',(-2.03274443395007,1.83841993152044,
12.5212220730815));
#429964=CARTESIAN_POINT('Ctrl Pts',(-2.03295170982702,1.83900021363332,
12.5193246583486));
#429965=CARTESIAN_POINT('Ctrl Pts',(-2.03305943711478,1.83967721249193,
12.5174178313691));
#429966=CARTESIAN_POINT('Ctrl Pts',(-2.03297649481723,1.84048485429296,
12.5155812248348));
#429967=CARTESIAN_POINT('Ctrl Pts',(-2.03294116095266,1.84082891404129,
12.5147988205794));
#429968=CARTESIAN_POINT('Ctrl Pts',(-2.03287146396674,1.84119706051606,
12.5140295443047));
#429969=CARTESIAN_POINT('Ctrl Pts',(-2.03276198451743,1.84159328898931,
12.5132817086137));
#429970=CARTESIAN_POINT('Ctrl Pts',(-2.03259630218093,1.842192927183,12.5121499604604));
#429971=CARTESIAN_POINT('Ctrl Pts',(-2.03232903596763,1.84286792487787,
12.5110494206568));
#429972=CARTESIAN_POINT('Ctrl Pts',(-2.03192299023836,1.843616442733,12.5100666561695));
#429973=CARTESIAN_POINT('Ctrl Pts',(-2.03168983971566,1.84404623996173,
12.5095023550641));
#429974=CARTESIAN_POINT('Ctrl Pts',(-2.03140766556882,1.84450493167331,
12.5089719619137));
#429975=CARTESIAN_POINT('Ctrl Pts',(-2.03107631679997,1.84498057363984,
12.5085043804652));
#429976=CARTESIAN_POINT('Ctrl Pts',(-2.03059143103796,1.84567661370114,
12.5078201359221));
#429977=CARTESIAN_POINT('Ctrl Pts',(-2.0299861858922,1.84642844900638,12.5072563000949));
#429978=CARTESIAN_POINT('Ctrl Pts',(-2.02929501341177,1.84717980736874,
12.5068768744332));
#429979=CARTESIAN_POINT('Ctrl Pts',(-2.0287966304729,1.84772158847168,12.5066032824114));
#429980=CARTESIAN_POINT('Ctrl Pts',(-2.02824485881439,1.84827268053072,
12.5064197834844));
#429981=CARTESIAN_POINT('Ctrl Pts',(-2.0276723374415,1.84880413803124,12.5063282718343));
#429982=CARTESIAN_POINT('Ctrl Pts',(-2.0268366334852,1.84957990144691,12.5061946931565));
#429983=CARTESIAN_POINT('Ctrl Pts',(-2.0259395786605,1.8503311890892,12.5062515701262));
#429984=CARTESIAN_POINT('Ctrl Pts',(-2.02504677507729,1.85102323054787,
12.5064436508398));
#429985=CARTESIAN_POINT('',(-1.95716684665092,1.8253181060621,12.5737548217797));
#429986=CARTESIAN_POINT('Origin',(-1.96854337191465,1.83592822731135,12.5893111709658));
#429987=CARTESIAN_POINT('Ctrl Pts',(-2.02504677507729,1.85102323054787,
12.5064436508398));
#429988=CARTESIAN_POINT('Ctrl Pts',(-2.0149986119639,1.84721865359398,12.5164271754438));
#429989=CARTESIAN_POINT('Ctrl Pts',(-2.00494653974534,1.84341237310856,
12.5264061185523));
#429990=CARTESIAN_POINT('Ctrl Pts',(-1.99489042041103,1.83960432997982,
12.536380305637));
#429991=CARTESIAN_POINT('Ctrl Pts',(-1.98232231084392,1.83484504842325,
12.5488460165097));
#429992=CARTESIAN_POINT('Ctrl Pts',(-1.96974787600632,1.8300830122015,12.5613043021964));
#429993=CARTESIAN_POINT('Ctrl Pts',(-1.95716684665092,1.8253181060621,12.5737548217797));
#429994=CARTESIAN_POINT('Ctrl Pts',(-1.93281340425162,1.86156455859733,
12.5893111709658));
#429995=CARTESIAN_POINT('Ctrl Pts',(-1.9281793763716,1.85122123127162,12.5770542771492));
#429996=CARTESIAN_POINT('Ctrl Pts',(-1.94160445395174,1.84186329523731,
12.5737548217797));
#429997=CARTESIAN_POINT('Ctrl Pts',(-1.92848989654421,1.85191432416395,
12.5928319619712));
#429998=CARTESIAN_POINT('Ctrl Pts',(-1.92834854683296,1.84363100136265,
12.5821634970843));
#429999=CARTESIAN_POINT('Ctrl Pts',(-1.94002089088191,1.83835180760764,
12.5773203894503));
#430000=CARTESIAN_POINT('Ctrl Pts',(-1.92864136216822,1.8351643642385,12.5969440695591));
#430001=CARTESIAN_POINT('Ctrl Pts',(-1.93138213402892,1.8322238350073,12.5878292599214));
#430002=CARTESIAN_POINT('Ctrl Pts',(-1.9400769222157,1.832381798597,12.5813877129824));
#430003=CARTESIAN_POINT('Ctrl Pts',(-1.94956531885574,1.81284031258831,
12.596957478804));
#430004=CARTESIAN_POINT('Ctrl Pts',(-1.94684486067137,1.81575916517382,
12.5878468778671));
#430005=CARTESIAN_POINT('Ctrl Pts',(-1.94757024860912,1.82439579034094,
12.5814011370086));
#430006=CARTESIAN_POINT('Ctrl Pts',(-1.96638258081749,1.8116079541786,12.5928371701607));
#430007=CARTESIAN_POINT('Ctrl Pts',(-1.9581123219472,1.81197928142266,12.5821692192952));
#430008=CARTESIAN_POINT('Ctrl Pts',(-1.95355365081902,1.82394767060053,
12.5773318885715));
#430009=CARTESIAN_POINT('Ctrl Pts',(-1.97629355154768,1.81533855233435,
12.5893111709658));
#430010=CARTESIAN_POINT('Ctrl Pts',(-1.96568616340088,1.81134581501981,
12.5770542771492));
#430011=CARTESIAN_POINT('Ctrl Pts',(-1.95716684665094,1.82531810606205,
12.5737548217797));
#430012=CARTESIAN_POINT('',(-1.94160445395174,1.84186329523731,12.5737548217797));
#430013=CARTESIAN_POINT('Origin',(-1.95289051888808,1.852569589566,12.5893111709658));
#430014=CARTESIAN_POINT('Ctrl Pts',(-1.95716684665094,1.82531810606205,
12.5737548217797));
#430015=CARTESIAN_POINT('Ctrl Pts',(-1.95624094679594,1.82493466233796,
12.5746934679442));
#430016=CARTESIAN_POINT('Ctrl Pts',(-1.95514628730521,1.82467960148722,
12.5756680099006));
#430017=CARTESIAN_POINT('Ctrl Pts',(-1.954008165006,1.82457869905889,12.5765688348656));
#430018=CARTESIAN_POINT('Ctrl Pts',(-1.95370685972672,1.82455198625801,
12.5768073183026));
#430019=CARTESIAN_POINT('Ctrl Pts',(-1.95340259262505,1.82453583506502,
12.5770407398754));
#430020=CARTESIAN_POINT('Ctrl Pts',(-1.95309773370081,1.82453016239254,
12.5772674179684));
#430021=CARTESIAN_POINT('Ctrl Pts',(-1.95184667511306,1.82450688327862,
12.5781976435658));
#430022=CARTESIAN_POINT('Ctrl Pts',(-1.950514382943,1.82467002449465,12.5790594849312));
#430023=CARTESIAN_POINT('Ctrl Pts',(-1.94919668490389,1.82505650166269,
12.5797571720116));
#430024=CARTESIAN_POINT('Ctrl Pts',(-1.94833815725122,1.82530830543415,
12.580211740231));
#430025=CARTESIAN_POINT('Ctrl Pts',(-1.9474520925546,1.82568437236135,12.5806009430798));
#430026=CARTESIAN_POINT('Ctrl Pts',(-1.94660778767454,1.8261745375721,12.5808812374708));
#430027=CARTESIAN_POINT('Ctrl Pts',(-1.94588224968734,1.82659575209876,
12.5811221033394));
#430028=CARTESIAN_POINT('Ctrl Pts',(-1.94517275288646,1.82710994471076,
12.581287365893));
#430029=CARTESIAN_POINT('Ctrl Pts',(-1.9445242353383,1.82769484493574,12.581359338449));
#430030=CARTESIAN_POINT('Ctrl Pts',(-1.94443410479048,1.82777613398928,
12.5813693411482));
#430031=CARTESIAN_POINT('Ctrl Pts',(-1.94434509944343,1.82785876022213,
12.5813775999465));
#430032=CARTESIAN_POINT('Ctrl Pts',(-1.94425728550322,1.82794263555575,
12.5813841266931));
#430033=CARTESIAN_POINT('Ctrl Pts',(-1.94410829853279,1.82808494020376,
12.5813952001081));
#430034=CARTESIAN_POINT('Ctrl Pts',(-1.94396216376027,1.82823223380299,
12.5814007534795));
#430035=CARTESIAN_POINT('Ctrl Pts',(-1.94381908483015,1.82838459109884,
12.5814005856065));
#430036=CARTESIAN_POINT('Ctrl Pts',(-1.94316412542827,1.82908202323144,
12.5813998171494));
#430037=CARTESIAN_POINT('Ctrl Pts',(-1.94261820633187,1.82983714437461,
12.58127954464));
#430038=CARTESIAN_POINT('Ctrl Pts',(-1.94216044778564,1.83062833159675,
12.5810700125799));
#430039=CARTESIAN_POINT('Ctrl Pts',(-1.94160752758177,1.83158399567722,
12.5808169217085));
#430040=CARTESIAN_POINT('Ctrl Pts',(-1.9411976687996,1.83260074743558,12.5804173076348));
#430041=CARTESIAN_POINT('Ctrl Pts',(-1.94094263699953,1.8335797439364,12.5799304713245));
#430042=CARTESIAN_POINT('Ctrl Pts',(-1.94062657225593,1.83479302901661,
12.5793271277669));
#430043=CARTESIAN_POINT('Ctrl Pts',(-1.9404975400931,1.83601547063458,12.5785808224116));
#430044=CARTESIAN_POINT('Ctrl Pts',(-1.9405294378283,1.83719221121665,12.5777485681082));
#430045=CARTESIAN_POINT('Ctrl Pts',(-1.9405769689484,1.83894568360549,12.576508418016));
#430046=CARTESIAN_POINT('Ctrl Pts',(-1.94097456310917,1.84058310181538,
12.5750928681475));
#430047=CARTESIAN_POINT('Ctrl Pts',(-1.94160445395174,1.84186329523731,
12.5737548217797));
#430048=CARTESIAN_POINT('Ctrl Pts',(-1.94160445395174,1.84186329523731,
12.5737548217797));
#430049=CARTESIAN_POINT('Ctrl Pts',(-1.9281793763716,1.85122123127162,12.5770542771492));
#430050=CARTESIAN_POINT('Ctrl Pts',(-1.93281340425162,1.86156455859733,
12.5893111709658));
#430051=CARTESIAN_POINT('Ctrl Pts',(-1.95177351624953,1.86443773047174,
12.5508408821982));
#430052=CARTESIAN_POINT('Ctrl Pts',(-1.9383050059543,1.87382202346895,12.55409748406));
#430053=CARTESIAN_POINT('Ctrl Pts',(-1.94294494566708,1.88417854623126,
12.5663972313419));
#430054=CARTESIAN_POINT('Ctrl Pts',(-1.96193156921978,1.88699059777604,
12.52790050457));
#430055=CARTESIAN_POINT('Ctrl Pts',(-1.94841124254629,1.89637952976981,
12.5311362602938));
#430056=CARTESIAN_POINT('Ctrl Pts',(-1.9530662660221,1.90676972006767,12.5434568539655));
#430057=CARTESIAN_POINT('Ctrl Pts',(-1.97207945580243,1.90952357894281,
12.5049357605811));
#430058=CARTESIAN_POINT('Ctrl Pts',(-1.9585001077677,1.91889826250765,12.5081700652078));
#430059=CARTESIAN_POINT('Ctrl Pts',(-1.96317816583218,1.92933986688776,
12.5204921097672));
#430060=CARTESIAN_POINT('Ctrl Pts',(-1.97141310434378,1.90804397572455,
12.5064436508395));
#430061=CARTESIAN_POINT('Ctrl Pts',(-1.97072595753515,1.90905227977293,
12.5062361689309));
#430062=CARTESIAN_POINT('Ctrl Pts',(-1.96996838476096,1.91007153200484,
12.5061871075061));
#430063=CARTESIAN_POINT('Ctrl Pts',(-1.96918081516536,1.91101532794316,
12.5063648335164));
#430064=CARTESIAN_POINT('Ctrl Pts',(-1.96882305247573,1.9114440582741,12.5064455676329));
#430065=CARTESIAN_POINT('Ctrl Pts',(-1.96845394063071,1.91186305666257,
12.506574497099));
#430066=CARTESIAN_POINT('Ctrl Pts',(-1.96808851744449,1.912253663011,12.5067492519495));
#430067=CARTESIAN_POINT('Ctrl Pts',(-1.96735418536714,1.91303860163037,
12.5071004286051));
#430068=CARTESIAN_POINT('Ctrl Pts',(-1.96660716005056,1.9137371934628,12.5076537929612));
#430069=CARTESIAN_POINT('Ctrl Pts',(-1.965909970093,1.91430391386063,12.5083435010503));
#430070=CARTESIAN_POINT('Ctrl Pts',(-1.96586607781866,1.91433959229648,
12.5083869222963));
#430071=CARTESIAN_POINT('Ctrl Pts',(-1.96582237074989,1.91437474269549,
12.5084308732336));
#430072=CARTESIAN_POINT('Ctrl Pts',(-1.96577885931647,1.91440935187388,
12.5084753333615));
#430073=CARTESIAN_POINT('Ctrl Pts',(-1.96542984019117,1.91468696316406,
12.508831962269));
#430074=CARTESIAN_POINT('Ctrl Pts',(-1.96508712596552,1.91493639708005,
12.509227847131));
#430075=CARTESIAN_POINT('Ctrl Pts',(-1.96476255504048,1.91515250056705,
12.5096423454524));
#430076=CARTESIAN_POINT('Ctrl Pts',(-1.96374549341047,1.91582967325188,
12.5109411997424));
#430077=CARTESIAN_POINT('Ctrl Pts',(-1.96284938677816,1.91622926678686,
12.5124831113042));
#430078=CARTESIAN_POINT('Ctrl Pts',(-1.9620748016735,1.91644591486811,12.5140723025008));
#430079=CARTESIAN_POINT('Ctrl Pts',(-1.96200222220081,1.91646621503062,
12.5142212114565));
#430080=CARTESIAN_POINT('Ctrl Pts',(-1.96193069943166,1.91648493673082,
12.5143705582413));
#430081=CARTESIAN_POINT('Ctrl Pts',(-1.96186022943228,1.91650217422513,
12.5145201959299));
#430082=CARTESIAN_POINT('Ctrl Pts',(-1.96095493737149,1.91672361550343,
12.5164425148273));
#430083=CARTESIAN_POINT('Ctrl Pts',(-1.96019491913377,1.91671813301359,
12.5184635205941));
#430084=CARTESIAN_POINT('Ctrl Pts',(-1.95953372141976,1.91656305766488,
12.5205025929157));
#430085=CARTESIAN_POINT('Ctrl Pts',(-1.95915020053821,1.91647310781602,
12.5216853356836));
#430086=CARTESIAN_POINT('Ctrl Pts',(-1.95880050980342,1.91633346131749,
12.5228750347131));
#430087=CARTESIAN_POINT('Ctrl Pts',(-1.95848082982212,1.91616196041923,
12.5240609649613));
#430088=CARTESIAN_POINT('Ctrl Pts',(-1.95769619245825,1.91574102066515,
12.5269717671326));
#430089=CARTESIAN_POINT('Ctrl Pts',(-1.95707518073017,1.91510717255893,
12.5299036066169));
#430090=CARTESIAN_POINT('Ctrl Pts',(-1.95656645124578,1.91433022568954,
12.5328133004019));
#430091=CARTESIAN_POINT('Ctrl Pts',(-1.95632223147083,1.91395724595197,
12.5342101228451));
#430092=CARTESIAN_POINT('Ctrl Pts',(-1.95610463096842,1.9135514665439,12.5356023438238));
#430093=CARTESIAN_POINT('Ctrl Pts',(-1.95591164254695,1.91312070921219,
12.5369868989719));
#430094=CARTESIAN_POINT('Origin',(-7.16189571922773,13.5460285809191,-1.23934284754315));
#430095=CARTESIAN_POINT('Ctrl Pts',(-2.02912680811102,1.83522552753148,
12.5369868989719));
#430096=CARTESIAN_POINT('Ctrl Pts',(-2.04347215033515,1.84065640776932,
12.5369868989719));
#430097=CARTESIAN_POINT('Ctrl Pts',(-2.05352841253022,1.82907388238194,
12.5369868989719));
#430098=CARTESIAN_POINT('Ctrl Pts',(-2.03397611826865,1.83706131552939,
12.5218025310016));
#430099=CARTESIAN_POINT('Ctrl Pts',(-2.04575830983759,1.83797555047574,
12.5216901060418));
#430100=CARTESIAN_POINT('Ctrl Pts',(-2.05349777016335,1.82910920056989,
12.5161920673678));
#430101=CARTESIAN_POINT('Ctrl Pts',(-2.03553112754562,1.8428852332266,12.5042015548895));
#430102=CARTESIAN_POINT('Ctrl Pts',(-2.04192515672187,1.84218256978616,
12.4980677368513));
#430103=CARTESIAN_POINT('Ctrl Pts',(-2.04647323617422,1.83713224771536,
12.4907278922777));
#430104=CARTESIAN_POINT('Ctrl Pts',(-2.02503201206828,1.85100973622055,
12.506463626192));
#430105=CARTESIAN_POINT('Ctrl Pts',(-2.029861274367,1.85542399312139,12.4999376786891));
#430106=CARTESIAN_POINT('Ctrl Pts',(-2.02980229194976,1.85537007939167,
12.4906970594712));
#430107=CARTESIAN_POINT('Origin',(-2.03691608876012,1.8146506130245,12.5369868989719));
#430108=CARTESIAN_POINT('Origin',(-2.03691608876012,1.8146506130245,14.));
#430109=CARTESIAN_POINT('Origin',(-2.03691608876012,1.8146506130245,13.7435492065112));
#430110=CARTESIAN_POINT('Ctrl Pts',(-2.00599307808942,1.82651775106574,
13.793642941384));
#430111=CARTESIAN_POINT('Ctrl Pts',(-2.01610264317258,1.83035218881266,
13.8071662555867));
#430112=CARTESIAN_POINT('Ctrl Pts',(-2.0244175424436,1.8154900949579,13.8103758687955));
#430113=CARTESIAN_POINT('Ctrl Pts',(-2.02154869091056,1.83237305763171,
13.7804579775006));
#430114=CARTESIAN_POINT('Ctrl Pts',(-2.03402657675728,1.83709492553815,
13.7901904343351));
#430115=CARTESIAN_POINT('Ctrl Pts',(-2.04384291518824,1.82477033937984,
13.7927914348262));
#430116=CARTESIAN_POINT('Ctrl Pts',(-2.03070686561534,1.83582029693149,
13.7597120340895));
#430117=CARTESIAN_POINT('Ctrl Pts',(-2.04514932167757,1.84127946837625,
13.7635825532445));
#430118=CARTESIAN_POINT('Ctrl Pts',(-2.05530905450276,1.83021982348751,
13.7651073818884));
#430119=CARTESIAN_POINT('Ctrl Pts',(-2.02891348531008,1.83514524854303,
13.7381884353898));
#430120=CARTESIAN_POINT('Ctrl Pts',(-2.04301757097271,1.84047747868129,
13.7368803041982));
#430121=CARTESIAN_POINT('Ctrl Pts',(-2.05306385586082,1.82915220618717,
13.7363986145813));
#430122=CARTESIAN_POINT('Origin',(-2.01751779008901,1.80734888050836,13.7902182540695));
#430123=CARTESIAN_POINT('Ctrl Pts',(-1.97628986794929,1.81533716497664,
13.8235227101244));
#430124=CARTESIAN_POINT('Ctrl Pts',(-1.98704835065372,1.8193915130399,13.8358800583119));
#430125=CARTESIAN_POINT('Ctrl Pts',(-1.99558029931379,1.80518475756518,
13.8390832900376));
#430126=CARTESIAN_POINT('Ctrl Pts',(-1.98745282168616,1.81953902327544,
13.8124254819052));
#430127=CARTESIAN_POINT('Ctrl Pts',(-1.99823219730958,1.82360124456487,
13.8247886449157));
#430128=CARTESIAN_POINT('Ctrl Pts',(-2.00676031467326,1.80936776307462,
13.8279860620657));
#430129=CARTESIAN_POINT('Ctrl Pts',(-1.9986107725503,1.82373899843805,13.8013225099955));
#430130=CARTESIAN_POINT('Ctrl Pts',(-2.00940595425151,1.8278071781134,13.8136962257787));
#430131=CARTESIAN_POINT('Ctrl Pts',(-2.01793505925043,1.81354908592687,
13.8168830918626));
#430132=CARTESIAN_POINT('Ctrl Pts',(-2.00976391519586,1.82793716373444,
13.7902140179785));
#430133=CARTESIAN_POINT('Ctrl Pts',(-2.02057014859708,1.83200951210152,
13.802602731458));
#430134=CARTESIAN_POINT('Ctrl Pts',(-2.02910473950224,1.81772879396123,
13.8057746032558));
#430135=CARTESIAN_POINT('Origin',(-1.98404373118067,1.79474887735746,13.8235269408515));
#430136=CARTESIAN_POINT('Ctrl Pts',(-1.93281340425162,1.86156455859733,
13.8235269408515));
#430137=CARTESIAN_POINT('Ctrl Pts',(-1.93764103744294,1.87234002037682,
13.8362179249168));
#430138=CARTESIAN_POINT('Ctrl Pts',(-1.92339019007394,1.88175152149634,
13.8391868794938));
#430139=CARTESIAN_POINT('Ctrl Pts',(-1.92839633001593,1.85170548009703,
13.8400110824519));
#430140=CARTESIAN_POINT('Ctrl Pts',(-1.92914492063915,1.8617434816382,13.8494522556837));
#430141=CARTESIAN_POINT('Ctrl Pts',(-1.91622346934972,1.8654803230867,13.85569149686));
#430142=CARTESIAN_POINT('Ctrl Pts',(-1.92840529711048,1.83541445049064,
13.8586819406588));
#430143=CARTESIAN_POINT('Ctrl Pts',(-1.92543243625529,1.83859535318809,
13.868010383617));
#430144=CARTESIAN_POINT('Ctrl Pts',(-1.91638435459405,1.83843697060033,
13.8744918421245));
#430145=CARTESIAN_POINT('Ctrl Pts',(-1.94980503158974,1.8125863348837,13.8587686893867));
#430146=CARTESIAN_POINT('Ctrl Pts',(-1.95275139287244,1.80943370374263,
13.8680909899357));
#430147=CARTESIAN_POINT('Ctrl Pts',(-1.95201050526329,1.80043662160138,
13.8745789365163));
#430148=CARTESIAN_POINT('Ctrl Pts',(-1.96616632225896,1.81152655207678,
13.8400379222776));
#430149=CARTESIAN_POINT('Ctrl Pts',(-1.97622884399063,1.81165260884018,
13.8494748685453));
#430150=CARTESIAN_POINT('Ctrl Pts',(-1.97916813564705,1.79853309399309,
13.8557104837033));
#430151=CARTESIAN_POINT('Ctrl Pts',(-1.97629355154985,1.81533855232817,
13.8235269408542));
#430152=CARTESIAN_POINT('Ctrl Pts',(-1.98734410636231,1.81949810243936,
13.8362179249195));
#430153=CARTESIAN_POINT('Ctrl Pts',(-1.99586638246502,1.80469831142444,
13.8391868794965));
#430154=CARTESIAN_POINT('Origin',(-1.91273628961517,1.87055952762867,13.8235269408515));
#430155=CARTESIAN_POINT('Ctrl Pts',(-1.9474355348438,1.89420171474816,13.7902140241683));
#430156=CARTESIAN_POINT('Ctrl Pts',(-1.95216117861558,1.90473864439274,
13.8026027327198));
#430157=CARTESIAN_POINT('Ctrl Pts',(-1.93842919100838,1.91413068616379,
13.8057746032556));
#430158=CARTESIAN_POINT('Ctrl Pts',(-1.942563084316,1.88332621895825,13.8013225161808));
#430159=CARTESIAN_POINT('Ctrl Pts',(-1.94728389127257,1.89385237255602,
13.8136962270464));
#430160=CARTESIAN_POINT('Ctrl Pts',(-1.93357415172225,1.90323755485449,
13.8168830918628));
#430161=CARTESIAN_POINT('Ctrl Pts',(-1.93768853323095,1.87244603464424,
13.8124254880875));
#430162=CARTESIAN_POINT('Ctrl Pts',(-1.94240242624502,1.88295677618289,
13.8247886461867));
#430163=CARTESIAN_POINT('Ctrl Pts',(-1.92871719089915,1.89233946746664,
13.8279860620656));
#430164=CARTESIAN_POINT('Ctrl Pts',(-1.93281179654987,1.86156097199635,
13.8235227163065));
#430165=CARTESIAN_POINT('Ctrl Pts',(-1.9375165532484,1.872051341277,13.8358800595847));
#430166=CARTESIAN_POINT('Ctrl Pts',(-1.92385822819901,1.88143622207769,
13.8390832900376));
#430167=CARTESIAN_POINT('Origin',(-1.92736003299969,1.90320028173492,13.7902182540695));
#430168=CARTESIAN_POINT('Ctrl Pts',(-1.95580128185251,1.91287444739099,
13.7382347919292));
#430169=CARTESIAN_POINT('Ctrl Pts',(-1.96199304002264,1.92663598798411,
13.7369371795942));
#430170=CARTESIAN_POINT('Ctrl Pts',(-1.9512892953705,1.93735856358153,13.7364597369711));
#430171=CARTESIAN_POINT('Ctrl Pts',(-1.95657466908952,1.9146006762767,13.7595490285574));
#430172=CARTESIAN_POINT('Ctrl Pts',(-1.9629132404103,1.92869096797099,13.7633824266926));
#430173=CARTESIAN_POINT('Ctrl Pts',(-1.95247782533384,1.93950742637888,
13.7648920890506));
#430174=CARTESIAN_POINT('Ctrl Pts',(-1.95263043655764,1.90579700352681,
13.780380659011));
#430175=CARTESIAN_POINT('Ctrl Pts',(-1.95811799711753,1.91798238678324,
13.7901039518744));
#430176=CARTESIAN_POINT('Ctrl Pts',(-1.94642181871712,1.92855049220719,
13.7926933640892));
#430177=CARTESIAN_POINT('Ctrl Pts',(-1.94577447988346,1.89049425509214,
13.7936647693663));
#430178=CARTESIAN_POINT('Ctrl Pts',(-1.95022383391882,1.90035207334026,
13.8072068914933));
#430179=CARTESIAN_POINT('Ctrl Pts',(-1.93587698687609,1.90956142998339,
13.8104111085397));
#430180=CARTESIAN_POINT('Origin',(-1.93583452791049,1.92211567824353,13.7435492065112));
#430181=CARTESIAN_POINT('Origin',(-1.93583452791049,1.92211567824353,14.));
#430182=CARTESIAN_POINT('Origin',(-1.93583452791049,1.92211567824353,12.5369868989719));
#430183=CARTESIAN_POINT('Ctrl Pts',(-1.97139989487055,1.90803119084247,
12.506462012331));
#430184=CARTESIAN_POINT('Ctrl Pts',(-1.97609829541783,1.91257856594105,
12.4999388158272));
#430185=CARTESIAN_POINT('Ctrl Pts',(-1.97604270717779,1.91252476453011,
12.4907030323752));
#430186=CARTESIAN_POINT('Ctrl Pts',(-1.96393130389444,1.91900610460002,
12.5042014951932));
#430187=CARTESIAN_POINT('Ctrl Pts',(-1.96362211544802,1.92542837052573,
12.4980716682127));
#430188=CARTESIAN_POINT('Ctrl Pts',(-1.95886389918542,1.93027449714647,
12.4907355092744));
#430189=CARTESIAN_POINT('Ctrl Pts',(-1.9580235600074,1.91781267952468,12.5218047446509));
#430190=CARTESIAN_POINT('Ctrl Pts',(-1.95965478685134,1.92951131063775,
12.5216906929434));
#430191=CARTESIAN_POINT('Ctrl Pts',(-1.95128526683317,1.93777701623348,
12.5161988840775));
#430192=CARTESIAN_POINT('Ctrl Pts',(-1.95589590504031,1.91308566453063,
12.5369868989719));
#430193=CARTESIAN_POINT('Ctrl Pts',(-1.96218813768246,1.92706469668231,
12.5369868989719));
#430194=CARTESIAN_POINT('Ctrl Pts',(-1.95125312018413,1.93780857511758,
12.5369868989719));
#430195=CARTESIAN_POINT('Origin',(-3.7526671846257E-31,-1.62210662334643E-31,
12.5));
#430196=CARTESIAN_POINT('Origin',(-2.07811692054273,1.69782812028616,12.5));
#430197=CARTESIAN_POINT('',(-2.07811692054273,1.69782812028616,12.5893111709658));
#430198=CARTESIAN_POINT('',(-2.07811692054273,1.69782812028616,13.8235269408515));
#430199=CARTESIAN_POINT('',(-2.07811692054273,1.69782812028616,12.5));
#430200=CARTESIAN_POINT('',(-2.09535252910915,1.72916829412975,13.7902182540695));
#430201=CARTESIAN_POINT('',(-2.07811692054273,1.69782812028616,13.8235269408515));
#430202=CARTESIAN_POINT('',(-2.10534060625466,1.74733000120828,13.7435492065112));
#430203=CARTESIAN_POINT('Origin',(-2.07248024990848,1.68757806800912,13.7445212918717));
#430204=CARTESIAN_POINT('',(-2.10534060625466,1.74733000120828,12.5369868989719));
#430205=CARTESIAN_POINT('',(-2.10534060625466,1.74733000120828,12.5));
#430206=CARTESIAN_POINT('Ctrl Pts',(-2.10534060625466,1.74733000120828,
12.5369868989719));
#430207=CARTESIAN_POINT('Ctrl Pts',(-2.09627266278421,1.73084140878796,
12.5544431401645));
#430208=CARTESIAN_POINT('Ctrl Pts',(-2.08719823367958,1.71434102328811,
12.5718848856037));
#430209=CARTESIAN_POINT('Ctrl Pts',(-2.07811692054273,1.69782812028616,
12.5893111709658));
#430210=CARTESIAN_POINT('Origin',(-2.38209549409917,1.7237886652634,12.5));
#430211=CARTESIAN_POINT('',(-2.1720031479706,1.66373781788871,13.7435492065112));
#430212=CARTESIAN_POINT('',(-2.15207423655202,1.65804152271188,13.7902182540695));
#430213=CARTESIAN_POINT('Origin',(-2.09970450175266,1.643072643505,13.7418732680448));
#430214=CARTESIAN_POINT('',(-2.11768454258377,1.64821189159107,13.8235269408515));
#430215=CARTESIAN_POINT('',(-2.15207423655202,1.65804152271188,13.7902182540695));
#430216=CARTESIAN_POINT('',(-2.11768454258377,1.64821189159107,12.5893111709658));
#430217=CARTESIAN_POINT('',(-2.11768454258377,1.64821189159107,12.5));
#430218=CARTESIAN_POINT('',(-2.1720031479706,1.66373781788871,12.5369868989719));
#430219=CARTESIAN_POINT('Ctrl Pts',(-2.11768454258377,1.64821189159107,
12.5893111709658));
#430220=CARTESIAN_POINT('Ctrl Pts',(-2.13580421491228,1.65339105064912,
12.5718848856037));
#430221=CARTESIAN_POINT('Ctrl Pts',(-2.15391015173733,1.65856628367827,
12.5544431401645));
#430222=CARTESIAN_POINT('Ctrl Pts',(-2.1720031479706,1.66373781788871,12.5369868989719));
#430223=CARTESIAN_POINT('',(-2.1720031479706,1.66373781788871,12.5));
#430224=CARTESIAN_POINT('Origin',(-2.10823744587473,1.6812632605305,12.5));
#430225=CARTESIAN_POINT('',(-2.08067879467115,1.66071792247006,13.8587068136939));
#430226=CARTESIAN_POINT('Ctrl Pts',(-2.11768454258545,1.64821189158468,
13.8235269408542));
#430227=CARTESIAN_POINT('Ctrl Pts',(-2.11599971761088,1.6477303168426,13.8262006681044));
#430228=CARTESIAN_POINT('Ctrl Pts',(-2.11422779756818,1.64740454484519,
13.8288634856214));
#430229=CARTESIAN_POINT('Ctrl Pts',(-2.11237652462616,1.6472237190336,13.8314912288862));
#430230=CARTESIAN_POINT('Ctrl Pts',(-2.11046805317288,1.64703730627316,
13.8342001611531));
#430231=CARTESIAN_POINT('Ctrl Pts',(-2.1084731780219,1.64700423324031,13.8368750301949));
#430232=CARTESIAN_POINT('Ctrl Pts',(-2.10637684024255,1.64715119252942,
13.8394886372968));
#430233=CARTESIAN_POINT('Ctrl Pts',(-2.10621493499085,1.64716254255179,
13.8396904925131));
#430234=CARTESIAN_POINT('Ctrl Pts',(-2.10605242224907,1.64717498847012,
13.8398919674349));
#430235=CARTESIAN_POINT('Ctrl Pts',(-2.10588929490553,1.64718855402383,
13.8400930404591));
#430236=CARTESIAN_POINT('Ctrl Pts',(-2.10334766114646,1.64739991447711,
13.8432258934518));
#430237=CARTESIAN_POINT('Ctrl Pts',(-2.1006697040325,1.64788087453654,13.8462331177034));
#430238=CARTESIAN_POINT('Ctrl Pts',(-2.09795981658488,1.648710695014,13.8489036603661));
#430239=CARTESIAN_POINT('Ctrl Pts',(-2.09707310987547,1.64898222193134,
13.8497774930041));
#430240=CARTESIAN_POINT('Ctrl Pts',(-2.09618322449611,1.64929117012785,
13.85061494757));
#430241=CARTESIAN_POINT('Ctrl Pts',(-2.09529450652748,1.64964050391928,
13.8514076489583));
#430242=CARTESIAN_POINT('Ctrl Pts',(-2.09341473985153,1.65037939526964,
13.8530843267192));
#430243=CARTESIAN_POINT('Ctrl Pts',(-2.09135663551493,1.65137429659479,
13.8546805203176));
#430244=CARTESIAN_POINT('Ctrl Pts',(-2.08929902934897,1.65269030939996,
13.8559412814274));
#430245=CARTESIAN_POINT('Ctrl Pts',(-2.08902365491422,1.65286643459259,
13.8561100121513));
#430246=CARTESIAN_POINT('Ctrl Pts',(-2.08874829980687,1.65304823513679,
13.8562727473908));
#430247=CARTESIAN_POINT('Ctrl Pts',(-2.08847339350089,1.65323579124213,
13.8564289040185));
#430248=CARTESIAN_POINT('Ctrl Pts',(-2.08722669653949,1.65408635604014,
13.8571370725437));
#430249=CARTESIAN_POINT('Ctrl Pts',(-2.0859685991888,1.65507212142597,13.8577210840553));
#430250=CARTESIAN_POINT('Ctrl Pts',(-2.08476610464929,1.65617787184565,
13.8581177131616));
#430251=CARTESIAN_POINT('Ctrl Pts',(-2.08442744079835,1.65648928922261,
13.8582294175695));
#430252=CARTESIAN_POINT('Ctrl Pts',(-2.08409309497155,1.65681007180626,
13.8583265086086));
#430253=CARTESIAN_POINT('Ctrl Pts',(-2.08376431353877,1.65713951840094,
13.8584082369006));
#430254=CARTESIAN_POINT('Ctrl Pts',(-2.08329194278608,1.65761284481289,
13.8585256585398));
#430255=CARTESIAN_POINT('Ctrl Pts',(-2.08282541423584,1.65811016843248,
13.8586122832068));
#430256=CARTESIAN_POINT('Ctrl Pts',(-2.08237742288745,1.65861911051012,
13.8586682984299));
#430257=CARTESIAN_POINT('Ctrl Pts',(-2.08201907421669,1.65902621372243,
13.8587131050557));
#430258=CARTESIAN_POINT('Ctrl Pts',(-2.08166845244351,1.65944509243391,
13.8587357943552));
#430259=CARTESIAN_POINT('Ctrl Pts',(-2.0813259042565,1.65987612148833,13.8587355499465));
#430260=CARTESIAN_POINT('Ctrl Pts',(-2.08110450719651,1.6601547058424,13.8587353919793));
#430261=CARTESIAN_POINT('Ctrl Pts',(-2.08088884663434,1.66043532917931,
13.8587257282814));
#430262=CARTESIAN_POINT('Ctrl Pts',(-2.08067879467115,1.66071792247006,
13.8587068136939));
#430263=CARTESIAN_POINT('Ctrl Pts',(-2.08067879467115,1.66071792247006,
13.8587068136939));
#430264=CARTESIAN_POINT('Ctrl Pts',(-2.07998794521534,1.66164735639762,
13.8586446046466));
#430265=CARTESIAN_POINT('Ctrl Pts',(-2.07935768962981,1.66259807398097,
13.858482427929));
#430266=CARTESIAN_POINT('Ctrl Pts',(-2.07878414131476,1.66356786608021,
13.8582284286032));
#430267=CARTESIAN_POINT('Ctrl Pts',(-2.0781957474614,1.66456275996318,13.8579678548414));
#430268=CARTESIAN_POINT('Ctrl Pts',(-2.07766691551601,1.66558093852198,
13.857615680862));
#430269=CARTESIAN_POINT('Ctrl Pts',(-2.07720989530231,1.66657779459574,
13.8571944833187));
#430270=CARTESIAN_POINT('Ctrl Pts',(-2.07606935461884,1.66906555087786,
13.8561433417727));
#430271=CARTESIAN_POINT('Ctrl Pts',(-2.07531834955168,1.67153488102927,
13.8546163505475));
#430272=CARTESIAN_POINT('Ctrl Pts',(-2.07484729608965,1.6738104305201,13.8528973491086));
#430273=CARTESIAN_POINT('Ctrl Pts',(-2.07476124157188,1.67422613983949,
13.8525833129073));
#430274=CARTESIAN_POINT('Ctrl Pts',(-2.07468439415524,1.67463542046283,
13.8522628768812));
#430275=CARTESIAN_POINT('Ctrl Pts',(-2.07461592339801,1.67503727828417,
13.851937733538));
#430276=CARTESIAN_POINT('Ctrl Pts',(-2.07419778198349,1.67749136824381,
13.8499521282529));
#430277=CARTESIAN_POINT('Ctrl Pts',(-2.07405450257017,1.6799132094274,13.847639871647));
#430278=CARTESIAN_POINT('Ctrl Pts',(-2.07411341492913,1.6821707740468,13.8452109780794));
#430279=CARTESIAN_POINT('Ctrl Pts',(-2.07413992081886,1.68318649909833,
13.8441181685877));
#430280=CARTESIAN_POINT('Ctrl Pts',(-2.07420668933847,1.68416923558789,
13.8430021611332));
#430281=CARTESIAN_POINT('Ctrl Pts',(-2.07430455822727,1.6851090748427,13.8418824960098));
#430282=CARTESIAN_POINT('Ctrl Pts',(-2.07453518876287,1.68732383004633,
13.8392439765549));
#430283=CARTESIAN_POINT('Ctrl Pts',(-2.07494578944066,1.68940663422467,
13.8364981347964));
#430284=CARTESIAN_POINT('Ctrl Pts',(-2.07550387180333,1.69136961438488,
13.8336931113419));
#430285=CARTESIAN_POINT('Ctrl Pts',(-2.07604740858306,1.69328143240015,
13.8309611966328));
#430286=CARTESIAN_POINT('Ctrl Pts',(-2.07673192703162,1.69508135251798,
13.8281701127186));
#430287=CARTESIAN_POINT('Ctrl Pts',(-2.07755871490548,1.69675681454122,
13.8253580685121));
#430288=CARTESIAN_POINT('Ctrl Pts',(-2.07773796340883,1.69712005651608,
13.8247484142933));
#430289=CARTESIAN_POINT('Ctrl Pts',(-2.07792398516354,1.69747729842215,
13.8241378483365));
#430290=CARTESIAN_POINT('Ctrl Pts',(-2.07811692054273,1.69782812028616,
13.8235269408515));
#430291=CARTESIAN_POINT('',(-2.08143901971418,1.65973566245264,12.5969504640361));
#430292=CARTESIAN_POINT('Origin',(-2.10826319100818,1.68128404203464,12.584524458991));
#430293=CARTESIAN_POINT('Origin',(-2.10826319100818,1.68128404203464,12.584524458991));
#430294=CARTESIAN_POINT('Ctrl Pts',(-2.11768454258377,1.64821189159107,
12.5893111709658));
#430295=CARTESIAN_POINT('Ctrl Pts',(-2.10678700448808,1.64509704038872,
12.5770542771492));
#430296=CARTESIAN_POINT('Ctrl Pts',(-2.09943490649419,1.65971724318974,
12.5737548217797));
#430297=CARTESIAN_POINT('Ctrl Pts',(-2.14151380107655,1.65502302579549,
12.5663937883685));
#430298=CARTESIAN_POINT('Ctrl Pts',(-2.13060236165761,1.65190420116785,
12.5540940315304));
#430299=CARTESIAN_POINT('Ctrl Pts',(-2.12323034987202,1.66657115168753,
12.5508374392248));
#430300=CARTESIAN_POINT('Ctrl Pts',(-2.16531901613962,1.66182728764898,
12.5434499600944));
#430301=CARTESIAN_POINT('Ctrl Pts',(-2.15437209974549,1.65869832261179,
12.5311293540533));
#430302=CARTESIAN_POINT('Ctrl Pts',(-2.14700287116098,1.67341722999765,
12.5278936106989));
#430303=CARTESIAN_POINT('Ctrl Pts',(-2.18910207112778,1.66862521547222,
12.5204817579905));
#430304=CARTESIAN_POINT('Ctrl Pts',(-2.17810097497864,1.66548076419649,
12.5081597038247));
#430305=CARTESIAN_POINT('Ctrl Pts',(-2.17075425579,1.68025607339996,12.5049254088044));
#430306=CARTESIAN_POINT('Ctrl Pts',(-2.1720031479706,1.66373781788871,12.5369868989719));
#430307=CARTESIAN_POINT('Ctrl Pts',(-2.17289878453494,1.66399381850462,
12.5342545179733));
#430308=CARTESIAN_POINT('Ctrl Pts',(-2.17371925589978,1.66435807645283,
12.5314872231885));
#430309=CARTESIAN_POINT('Ctrl Pts',(-2.1743956607143,1.66486116455349,12.5287124745063));
#430310=CARTESIAN_POINT('Ctrl Pts',(-2.17500567614977,1.66531487437373,
12.5262100684184));
#430311=CARTESIAN_POINT('Ctrl Pts',(-2.1754973150128,1.66588183077953,12.5237004536639));
#430312=CARTESIAN_POINT('Ctrl Pts',(-2.17582893601259,1.66661519841171,
12.5212220730815));
#430313=CARTESIAN_POINT('Ctrl Pts',(-2.17608282057543,1.66717665477551,
12.5193246583486));
#430314=CARTESIAN_POINT('Ctrl Pts',(-2.17624537110145,1.66784262020223,
12.517417831369));
#430315=CARTESIAN_POINT('Ctrl Pts',(-2.17622853509212,1.66865433520904,
12.5155812248347));
#430316=CARTESIAN_POINT('Ctrl Pts',(-2.17622136286165,1.66900013016493,
12.5147988205793));
#430317=CARTESIAN_POINT('Ctrl Pts',(-2.1761819051421,1.66937273261406,12.5140295443047));
#430318=CARTESIAN_POINT('Ctrl Pts',(-2.1761050862756,1.66977656626123,12.5132817086137));
#430319=CARTESIAN_POINT('Ctrl Pts',(-2.17598883131297,1.67038771385684,
12.5121499604604));
#430320=CARTESIAN_POINT('Ctrl Pts',(-2.17577747298445,1.67108225023013,
12.5110494206568));
#430321=CARTESIAN_POINT('Ctrl Pts',(-2.17543378949294,1.67186137395032,
12.5100666561695));
#430322=CARTESIAN_POINT('Ctrl Pts',(-2.17523644722355,1.67230874499629,
12.5095023550641));
#430323=CARTESIAN_POINT('Ctrl Pts',(-2.17499259962067,1.67278891026161,
12.5089719619137));
#430324=CARTESIAN_POINT('Ctrl Pts',(-2.17470112262343,1.67328997756949,
12.5085043804652));
#430325=CARTESIAN_POINT('Ctrl Pts',(-2.17427458400551,1.67402322430597,
12.5078201359221));
#430326=CARTESIAN_POINT('Ctrl Pts',(-2.17373263432014,1.67482189103943,
12.5072563000949));
#430327=CARTESIAN_POINT('Ctrl Pts',(-2.17310500434093,1.6756270862925,12.5068768744332));
#430328=CARTESIAN_POINT('Ctrl Pts',(-2.17265243991971,1.6762076874998,12.5066032824114));
#430329=CARTESIAN_POINT('Ctrl Pts',(-2.17214742335478,1.67680192035804,
12.5064197834844));
#430330=CARTESIAN_POINT('Ctrl Pts',(-2.17162012571962,1.67737827528449,
12.5063282718343));
#430331=CARTESIAN_POINT('Ctrl Pts',(-2.17085043441952,1.67821957504213,
12.5061946931565));
#430332=CARTESIAN_POINT('Ctrl Pts',(-2.17001760138821,1.67904148113283,
12.5062515701262));
#430333=CARTESIAN_POINT('Ctrl Pts',(-2.16918417633874,1.67980399166105,
12.5064436508398));
#430334=CARTESIAN_POINT('',(-2.09943490649419,1.65971724318974,12.5737548217797));
#430335=CARTESIAN_POINT('Origin',(-2.11163840068998,1.6693647677123,12.5893111709658));
#430336=CARTESIAN_POINT('Ctrl Pts',(-2.16918417633874,1.67980399166105,
12.5064436508398));
#430337=CARTESIAN_POINT('Ctrl Pts',(-2.15885933931749,1.67683109269946,
12.5164271754438));
#430338=CARTESIAN_POINT('Ctrl Pts',(-2.14853046734465,1.67385681450306,
12.5264061185523));
#430339=CARTESIAN_POINT('Ctrl Pts',(-2.13819741805072,1.67088110940588,
12.536380305637));
#430340=CARTESIAN_POINT('Ctrl Pts',(-2.12528320220153,1.66716208157243,
12.5488460165097));
#430341=CARTESIAN_POINT('Ctrl Pts',(-2.11236245759787,1.66344082380799,
12.5613043021964));
#430342=CARTESIAN_POINT('Ctrl Pts',(-2.09943490649419,1.65971724318974,
12.5737548217797));
#430343=CARTESIAN_POINT('Ctrl Pts',(-2.07811692054273,1.69782812028616,
12.5893111709658));
#430344=CARTESIAN_POINT('Ctrl Pts',(-2.07265523480839,1.68789692582129,
12.5770542771492));
#430345=CARTESIAN_POINT('Ctrl Pts',(-2.08527288288873,1.67747585909204,
12.5737548217797));
#430346=CARTESIAN_POINT('Ctrl Pts',(-2.07302121525583,1.68856240222741,
12.5928319619712));
#430347=CARTESIAN_POINT('Ctrl Pts',(-2.07220516816716,1.6803181628131,12.5821634970842));
#430348=CARTESIAN_POINT('Ctrl Pts',(-2.08340837015351,1.67410513073906,
12.5773203894503));
#430349=CARTESIAN_POINT('Ctrl Pts',(-2.0718068996575,1.67185583055733,12.5969440695591));
#430350=CARTESIAN_POINT('Ctrl Pts',(-2.07429887139505,1.66870168734384,
12.5878292599214));
#430351=CARTESIAN_POINT('Ctrl Pts',(-2.08297760389043,1.66815041936703,
12.5813877129824));
#430352=CARTESIAN_POINT('Ctrl Pts',(-2.09084161614938,1.64790056362884,
12.596957478804));
#430353=CARTESIAN_POINT('Ctrl Pts',(-2.08836812364821,1.65103144657069,
12.5878468778671));
#430354=CARTESIAN_POINT('Ctrl Pts',(-2.08979506304708,1.65958020822894,
12.5814011370086));
#430355=CARTESIAN_POINT('Ctrl Pts',(-2.10750247140822,1.64530154281635,
12.5928371701607));
#430356=CARTESIAN_POINT('Ctrl Pts',(-2.0992899977597,1.6463457373749,12.5821692192952));
#430357=CARTESIAN_POINT('Ctrl Pts',(-2.09572203006074,1.65864587674269,
12.5773318885715));
#430358=CARTESIAN_POINT('Ctrl Pts',(-2.11768454258378,1.64821189159102,
12.5893111709658));
#430359=CARTESIAN_POINT('Ctrl Pts',(-2.10678700448809,1.64509704038866,
12.5770542771492));
#430360=CARTESIAN_POINT('Ctrl Pts',(-2.09943490649421,1.65971724318969,
12.5737548217797));
#430361=CARTESIAN_POINT('',(-2.08527288288873,1.67747585909204,12.5737548217797));
#430362=CARTESIAN_POINT('Origin',(-2.09739405675521,1.68722661004253,12.5893111709658));
#430363=CARTESIAN_POINT('Ctrl Pts',(-2.09943490649421,1.65971724318969,
12.5737548217797));
#430364=CARTESIAN_POINT('Ctrl Pts',(-2.09848083327137,1.65941054477678,
12.5746934679442));
#430365=CARTESIAN_POINT('Ctrl Pts',(-2.09736902634259,1.6592455575308,12.5756680099006));
#430366=CARTESIAN_POINT('Ctrl Pts',(-2.09622646656681,1.65923775838016,
12.5765688348656));
#430367=CARTESIAN_POINT('Ctrl Pts',(-2.09592398651472,1.65923569364137,
12.5768073183026));
#430368=CARTESIAN_POINT('Ctrl Pts',(-2.09561941536456,1.65924439678361,
12.5770407398754));
#430369=CARTESIAN_POINT('Ctrl Pts',(-2.09531510845777,1.65926359181898,
12.5772674179684));
#430370=CARTESIAN_POINT('Ctrl Pts',(-2.09406631520036,1.65934236305355,
12.5781976435658));
#430371=CARTESIAN_POINT('Ctrl Pts',(-2.09275175364623,1.6596135556109,12.5790594849312));
#430372=CARTESIAN_POINT('Ctrl Pts',(-2.09146994161572,1.66010615143115,
12.5797571720116));
#430373=CARTESIAN_POINT('Ctrl Pts',(-2.09063479498799,1.6604270953202,12.580211740231));
#430374=CARTESIAN_POINT('Ctrl Pts',(-2.08978233154435,1.66087413341432,
12.5806009430798));
#430375=CARTESIAN_POINT('Ctrl Pts',(-2.08898078903428,1.66143148632664,
12.5808812374708));
#430376=CARTESIAN_POINT('Ctrl Pts',(-2.08829199810917,1.66191043737823,
12.5811221033394));
#430377=CARTESIAN_POINT('Ctrl Pts',(-2.08762677357178,1.66248074963265,
12.581287365893));
#430378=CARTESIAN_POINT('Ctrl Pts',(-2.08702808871054,1.6631165638511,12.581359338449));
#430379=CARTESIAN_POINT('Ctrl Pts',(-2.0869448838772,1.6632049288984,12.5813693411482));
#430380=CARTESIAN_POINT('Ctrl Pts',(-2.08686290949314,1.66329453496134,
12.5813775999465));
#430381=CARTESIAN_POINT('Ctrl Pts',(-2.08678222436493,1.66338528885807,
12.5813841266931));
#430382=CARTESIAN_POINT('Ctrl Pts',(-2.08664533228625,1.66353926382032,
12.5813952001081));
#430383=CARTESIAN_POINT('Ctrl Pts',(-2.08651168956088,1.66369797865285,
12.5814007534795));
#430384=CARTESIAN_POINT('Ctrl Pts',(-2.08638150524812,1.66386149125346,
12.5814005856065));
#430385=CARTESIAN_POINT('Ctrl Pts',(-2.08578557236308,1.66460998800977,
12.5813998171494));
#430386=CARTESIAN_POINT('Ctrl Pts',(-2.0853030191508,1.66540709402405,12.58127954464));
#430387=CARTESIAN_POINT('Ctrl Pts',(-2.084911272862,1.66623296020712,12.5810700125799));
#430388=CARTESIAN_POINT('Ctrl Pts',(-2.08443808794901,1.66723051252387,
12.5808169217085));
#430389=CARTESIAN_POINT('Ctrl Pts',(-2.08411246764549,1.66827728842033,
12.5804173076348));
#430390=CARTESIAN_POINT('Ctrl Pts',(-2.08393808174607,1.66927381485035,
12.5799304713245));
#430391=CARTESIAN_POINT('Ctrl Pts',(-2.08372196267946,1.67050882503535,
12.5793271277669));
#430392=CARTESIAN_POINT('Ctrl Pts',(-2.08369300020097,1.67173771639883,
12.5785808224116));
#430393=CARTESIAN_POINT('Ctrl Pts',(-2.08382070708085,1.67290794151214,
12.5777485681082));
#430394=CARTESIAN_POINT('Ctrl Pts',(-2.0840110043232,1.67465170513872,12.576508418016));
#430395=CARTESIAN_POINT('Ctrl Pts',(-2.08454074030736,1.67625126735941,
12.5750928681475));
#430396=CARTESIAN_POINT('Ctrl Pts',(-2.08527288288873,1.67747585909204,
12.5737548217797));
#430397=CARTESIAN_POINT('Ctrl Pts',(-2.08527288288873,1.67747585909204,
12.5737548217797));
#430398=CARTESIAN_POINT('Ctrl Pts',(-2.07265523480839,1.68789692582129,
12.5770542771492));
#430399=CARTESIAN_POINT('Ctrl Pts',(-2.07811692054273,1.69782812028616,
12.5893111709658));
#430400=CARTESIAN_POINT('Ctrl Pts',(-2.09724813451306,1.69914630677325,
12.5508408821982));
#430401=CARTESIAN_POINT('Ctrl Pts',(-2.08458934657359,1.70959718293428,
12.55409748406));
#430402=CARTESIAN_POINT('Ctrl Pts',(-2.09005800002012,1.71954104705978,
12.5663972313419));
#430403=CARTESIAN_POINT('Ctrl Pts',(-2.10921065545595,1.72079615565222,
12.52790050457));
#430404=CARTESIAN_POINT('Ctrl Pts',(-2.09650060167422,1.73125587888978,
12.5311362602938));
#430405=CARTESIAN_POINT('Ctrl Pts',(-2.10198703291048,1.74123206905817,
12.5434568539655));
#430406=CARTESIAN_POINT('Ctrl Pts',(-2.12116142293421,1.74242701321815,
12.5049357605811));
#430407=CARTESIAN_POINT('Ctrl Pts',(-2.10839138280069,1.75287734622613,
12.5081700652078));
#430408=CARTESIAN_POINT('Ctrl Pts',(-2.11390496270498,1.76290290186781,
12.5204921097672));
#430409=CARTESIAN_POINT('Ctrl Pts',(-2.12037668730681,1.74100664708752,
12.5064436508395));
#430410=CARTESIAN_POINT('Ctrl Pts',(-2.11977401306308,1.74206760493142,
12.5062361689309));
#430411=CARTESIAN_POINT('Ctrl Pts',(-2.11910203956898,1.74314521489967,
12.5061871075061));
#430412=CARTESIAN_POINT('Ctrl Pts',(-2.11839401867698,1.74415006466835,
12.5063648335164));
#430413=CARTESIAN_POINT('Ctrl Pts',(-2.1180723919153,1.74460652941499,12.5064455676329));
#430414=CARTESIAN_POINT('Ctrl Pts',(-2.11773866051794,1.74505421966292,
12.506574497099));
#430415=CARTESIAN_POINT('Ctrl Pts',(-2.11740629129084,1.74547331168305,
12.5067492519495));
#430416=CARTESIAN_POINT('Ctrl Pts',(-2.11673838242732,1.74631549336552,
12.5071004286051));
#430417=CARTESIAN_POINT('Ctrl Pts',(-2.11605078449554,1.74707265018967,
12.5076537929613));
#430418=CARTESIAN_POINT('Ctrl Pts',(-2.11540210735358,1.7476943123261,12.5083435010505));
#430419=CARTESIAN_POINT('Ctrl Pts',(-2.11536126925098,1.74773344967266,
12.5083869222964));
#430420=CARTESIAN_POINT('Ctrl Pts',(-2.11532057269779,1.74777204564341,
12.5084308732337));
#430421=CARTESIAN_POINT('Ctrl Pts',(-2.11528002701449,1.74781008624831,
12.5084753333615));
#430422=CARTESIAN_POINT('Ctrl Pts',(-2.1149547971189,1.74811522210867,12.5088319622689));
#430423=CARTESIAN_POINT('Ctrl Pts',(-2.11463355442634,1.7483917604449,12.509227847131));
#430424=CARTESIAN_POINT('Ctrl Pts',(-2.11432767792467,1.74863360040892,
12.5096423454524));
#430425=CARTESIAN_POINT('Ctrl Pts',(-2.11336919634372,1.7493914198223,12.5109411997424));
#430426=CARTESIAN_POINT('Ctrl Pts',(-2.11250864201505,1.74986272475234,
12.5124831113042));
#430427=CARTESIAN_POINT('Ctrl Pts',(-2.11175429310831,1.7501417878319,12.5140723025008));
#430428=CARTESIAN_POINT('Ctrl Pts',(-2.11168360978953,1.7501679363481,12.5142212114565));
#430429=CARTESIAN_POINT('Ctrl Pts',(-2.11161385099886,1.75019242552307,
12.5143705582413));
#430430=CARTESIAN_POINT('Ctrl Pts',(-2.11154502049841,1.75021534962019,
12.5145201959299));
#430431=CARTESIAN_POINT('Ctrl Pts',(-2.11066079024221,1.75050984377818,
12.5164425148273));
#430432=CARTESIAN_POINT('Ctrl Pts',(-2.10990285402866,1.75056632807291,
12.518463520594));
#430433=CARTESIAN_POINT('Ctrl Pts',(-2.10923121631493,1.75046566247659,
12.5205025929157));
#430434=CARTESIAN_POINT('Ctrl Pts',(-2.10884163981974,1.75040727244071,
12.5216853356836));
#430435=CARTESIAN_POINT('Ctrl Pts',(-2.10848173016598,1.75029659364564,
12.5228750347131));
#430436=CARTESIAN_POINT('Ctrl Pts',(-2.10814913497809,1.75015172028871,
12.5240609649613));
#430437=CARTESIAN_POINT('Ctrl Pts',(-2.10733279793255,1.74979613640631,
12.5269717671327));
#430438=CARTESIAN_POINT('Ctrl Pts',(-2.10666218806475,1.7492150155984,12.5299036066169));
#430439=CARTESIAN_POINT('Ctrl Pts',(-2.10609182295306,1.74848212013141,
12.5328133004019));
#430440=CARTESIAN_POINT('Ctrl Pts',(-2.10581801448809,1.74813028763204,
12.5342101228451));
#430441=CARTESIAN_POINT('Ctrl Pts',(-2.10556806324457,1.74774359488252,
12.5356023438238));
#430442=CARTESIAN_POINT('Ctrl Pts',(-2.10534060625466,1.74733000120828,
12.5369868989719));
#430443=CARTESIAN_POINT('Origin',(-8.24240891046344,12.9175899459587,-1.23982923200078));
#430444=CARTESIAN_POINT('Ctrl Pts',(-2.17196297394457,1.6637262936288,12.5369868989719));
#430445=CARTESIAN_POINT('Ctrl Pts',(-2.18670325038309,1.66796982449374,
12.5369868989719));
#430446=CARTESIAN_POINT('Ctrl Pts',(-2.1957819678493,1.65560616027741,12.5369868989719));
#430447=CARTESIAN_POINT('Ctrl Pts',(-2.17694578218716,1.66516070939695,
12.5218025310016));
#430448=CARTESIAN_POINT('Ctrl Pts',(-2.1887632881211,1.66511154430852,12.5216901060418));
#430449=CARTESIAN_POINT('Ctrl Pts',(-2.19575430620257,1.65564385858438,
12.5161920673678));
#430450=CARTESIAN_POINT('Ctrl Pts',(-2.17897032065797,1.67083850079639,
12.5042015548895));
#430451=CARTESIAN_POINT('Ctrl Pts',(-2.18528580063597,1.66961700267343,
12.4980677368513));
#430452=CARTESIAN_POINT('Ctrl Pts',(-2.1894070985955,1.66421277443503,12.4907278922777));
#430453=CARTESIAN_POINT('Ctrl Pts',(-2.16916836253948,1.67979174555728,
12.506463626192));
#430454=CARTESIAN_POINT('Ctrl Pts',(-2.17434135878366,1.6837976846724,12.4999376786891));
#430455=CARTESIAN_POINT('Ctrl Pts',(-2.17427817815607,1.68374875795074,
12.4906970594712));
#430456=CARTESIAN_POINT('Origin',(-2.17804928986438,1.64258494176748,12.5369868989719));
#430457=CARTESIAN_POINT('Origin',(-2.17804928986438,1.64258494176748,14.));
#430458=CARTESIAN_POINT('Origin',(-2.17804928986438,1.64258494176748,13.7435492065112));
#430459=CARTESIAN_POINT('Ctrl Pts',(-2.14819645488023,1.65693310533074,
13.793642941384));
#430460=CARTESIAN_POINT('Ctrl Pts',(-2.15858492349311,1.65993076089547,
13.8071662555867));
#430461=CARTESIAN_POINT('Ctrl Pts',(-2.16566075700062,1.64444037794964,
13.8103758687955));
#430462=CARTESIAN_POINT('Ctrl Pts',(-2.1641775695261,1.66150100199096,13.7804579775006));
#430463=CARTESIAN_POINT('Ctrl Pts',(-2.17699881230708,1.66519009473591,
13.7901904343353));
#430464=CARTESIAN_POINT('Ctrl Pts',(-2.1857779194939,1.65210639490877,13.7927914348263));
#430465=CARTESIAN_POINT('Ctrl Pts',(-2.1735862531656,1.66419029462756,13.7597120340895));
#430466=CARTESIAN_POINT('Ctrl Pts',(-2.18842562629994,1.66845410688339,
13.7635825532444));
#430467=CARTESIAN_POINT('Ctrl Pts',(-2.19765008972107,1.65660314950704,
13.7651073818884));
#430468=CARTESIAN_POINT('Ctrl Pts',(-2.17174381747484,1.66366366955073,
13.7381884353898));
#430469=CARTESIAN_POINT('Ctrl Pts',(-2.1862355992142,1.66782854321562,13.7368803041982));
#430470=CARTESIAN_POINT('Ctrl Pts',(-2.19532534107114,1.65572208914794,
13.7363986145813));
#430471=CARTESIAN_POINT('Origin',(-2.15812037844581,1.63688864659065,13.7902182540695));
#430472=CARTESIAN_POINT('Ctrl Pts',(-2.11768075815972,1.64821080909709,
13.8235227101244));
#430473=CARTESIAN_POINT('Ctrl Pts',(-2.12873390990635,1.65137475043435,
13.8358800583119));
#430474=CARTESIAN_POINT('Ctrl Pts',(-2.13607948675083,1.63651983374394,
13.8390832900376));
#430475=CARTESIAN_POINT('Ctrl Pts',(-2.12914905854842,1.65148880169767,
13.8124254819053));
#430476=CARTESIAN_POINT('Ctrl Pts',(-2.14022367543563,1.65465888709674,
13.8247886449158));
#430477=CARTESIAN_POINT('Ctrl Pts',(-2.14756325531363,1.63977764560561,
13.8279860620657));
#430478=CARTESIAN_POINT('Ctrl Pts',(-2.14061221921795,1.65476532520861,
13.8013225099954));
#430479=CARTESIAN_POINT('Ctrl Pts',(-2.15170307525326,1.65794006082546,
13.8136962257787));
#430480=CARTESIAN_POINT('Ctrl Pts',(-2.15904163348003,1.64303421002671,
13.8168830918626));
#430481=CARTESIAN_POINT('Ctrl Pts',(-2.15207044014693,1.65804043678995,
13.7902140179785));
#430482=CARTESIAN_POINT('Ctrl Pts',(-2.16317265089572,1.66121842641144,
13.802602731458));
#430483=CARTESIAN_POINT('Ctrl Pts',(-2.17051483254955,1.64628957779261,
13.8057746032558));
#430484=CARTESIAN_POINT('Origin',(-2.12373068447755,1.62705901546984,13.8235269408515));
#430485=CARTESIAN_POINT('Ctrl Pts',(-2.07811692054273,1.69782812028616,
13.8235269408515));
#430486=CARTESIAN_POINT('Ctrl Pts',(-2.08380679035239,1.70817423068283,
13.8362179249168));
#430487=CARTESIAN_POINT('Ctrl Pts',(-2.07037048621576,1.71871599216776,
13.8391868794938));
#430488=CARTESIAN_POINT('Ctrl Pts',(-2.07291093733218,1.68836187961257,
13.8400110824519));
#430489=CARTESIAN_POINT('Ctrl Pts',(-2.07447522739571,1.69830546344632,
13.8494522556837));
#430490=CARTESIAN_POINT('Ctrl Pts',(-2.06190135843871,1.70308308910016,
13.85569149686));
#430491=CARTESIAN_POINT('Ctrl Pts',(-2.07159200443801,1.67212432616183,
13.8586819406588));
#430492=CARTESIAN_POINT('Ctrl Pts',(-2.06888830863196,1.67553696042635,
13.868010383617));
#430493=CARTESIAN_POINT('Ctrl Pts',(-2.05985742406479,1.67611660749727,
13.8744918421245));
#430494=CARTESIAN_POINT('Ctrl Pts',(-2.09105982971829,1.64762789220088,
13.8587686893867));
#430495=CARTESIAN_POINT('Ctrl Pts',(-2.09373941852129,1.64424559538263,
13.8680909899357));
#430496=CARTESIAN_POINT('Ctrl Pts',(-2.09226765043519,1.63533883950822,
13.8745789365163));
#430497=CARTESIAN_POINT('Ctrl Pts',(-2.1072802974052,1.64523803865347,13.8400379222776));
#430498=CARTESIAN_POINT('Ctrl Pts',(-2.11731961172237,1.64454348703638,
13.8494748685453));
#430499=CARTESIAN_POINT('Ctrl Pts',(-2.11917976087262,1.6312280467356,13.8557104837033));
#430500=CARTESIAN_POINT('Ctrl Pts',(-2.11768454258545,1.64821189158468,
13.8235269408542));
#430501=CARTESIAN_POINT('Ctrl Pts',(-2.12903736953781,1.65145687833045,
13.8362179249195));
#430502=CARTESIAN_POINT('Ctrl Pts',(-2.13632496810756,1.63601168777992,
13.8391868794965));
#430503=CARTESIAN_POINT('Origin',(-2.05883978433026,1.70842963052978,13.8235269408515));
#430504=CARTESIAN_POINT('Ctrl Pts',(-2.09535062841647,1.72916483960377,
13.7902140241683));
#430505=CARTESIAN_POINT('Ctrl Pts',(-2.10091940558456,1.73928152464605,
13.8026027327198));
#430506=CARTESIAN_POINT('Ctrl Pts',(-2.08799864862912,1.74976159964444,
13.8057746032556));
#430507=CARTESIAN_POINT('Ctrl Pts',(-2.0896079366958,1.71872268108058,13.8013225161808));
#430508=CARTESIAN_POINT('Ctrl Pts',(-2.09517101479492,1.7288290201778,13.8136962270464));
#430509=CARTESIAN_POINT('Ctrl Pts',(-2.08227187275708,1.73930044510477,
13.8168830918628));
#430510=CARTESIAN_POINT('Ctrl Pts',(-2.08386276924907,1.70827602084888,
13.8124254880875));
#430511=CARTESIAN_POINT('Ctrl Pts',(-2.08941770018537,1.71836756271985,
13.8247886461867));
#430512=CARTESIAN_POINT('Ctrl Pts',(-2.07654277777542,1.72883450760057,
13.8279860620656));
#430513=CARTESIAN_POINT('Ctrl Pts',(-2.0781150258492,1.69782467666191,13.8235227163065));
#430514=CARTESIAN_POINT('Ctrl Pts',(-2.08365919034214,1.70789665875641,
13.8358800595848));
#430515=CARTESIAN_POINT('Ctrl Pts',(-2.07081126715285,1.71836359242966,
13.8390832900376));
#430516=CARTESIAN_POINT('Origin',(-2.07607539289668,1.73976980437337,13.7902182540695));
#430517=CARTESIAN_POINT('Ctrl Pts',(-2.10521054015172,1.7470935542241,13.7382347919292));
#430518=CARTESIAN_POINT('Ctrl Pts',(-2.11250338907157,1.76030461865379,
13.7369371795942));
#430519=CARTESIAN_POINT('Ctrl Pts',(-2.10270924970151,1.77186397032332,
13.7364597369711));
#430520=CARTESIAN_POINT('Ctrl Pts',(-2.10612205768621,1.74875100098601,
13.7595490285574));
#430521=CARTESIAN_POINT('Ctrl Pts',(-2.1135880275148,1.76227775599,13.7633824266926));
#430522=CARTESIAN_POINT('Ctrl Pts',(-2.10406897719646,1.77390880673123,
13.7648920890506));
#430523=CARTESIAN_POINT('Ctrl Pts',(-2.10147336820428,1.74029811329877,
13.780380659011));
#430524=CARTESIAN_POINT('Ctrl Pts',(-2.10793589121805,1.75199566356795,
13.7901039518744));
#430525=CARTESIAN_POINT('Ctrl Pts',(-2.09714002958799,1.76348195161457,
13.7926933640892));
#430526=CARTESIAN_POINT('Ctrl Pts',(-2.09339290809914,1.72560510761366,
13.7936647693663));
#430527=CARTESIAN_POINT('Ctrl Pts',(-2.09863096097873,1.73506746112509,
13.8072068914933));
#430528=CARTESIAN_POINT('Ctrl Pts',(-2.08508249994794,1.74541557561732,
13.8104111085397));
#430529=CARTESIAN_POINT('Origin',(-2.08606347004218,1.7579315114519,13.7435492065112));
#430530=CARTESIAN_POINT('Origin',(-2.08606347004219,1.7579315114519,14.));
#430531=CARTESIAN_POINT('Origin',(-2.08606347004219,1.7579315114519,12.5369868989719));
#430532=CARTESIAN_POINT('Ctrl Pts',(-2.12036247970043,1.74099498144077,
12.506462012331));
#430533=CARTESIAN_POINT('Ctrl Pts',(-2.12541589999379,1.74514426226142,
12.4999388158272));
#430534=CARTESIAN_POINT('Ctrl Pts',(-2.12535611140457,1.74509517082787,
12.4907030323752));
#430535=CARTESIAN_POINT('Ctrl Pts',(-2.11381329720205,1.75254213657774,
12.5042014951932));
#430536=CARTESIAN_POINT('Ctrl Pts',(-2.11402861184905,1.75896823467215,
12.4980716682127));
#430537=CARTESIAN_POINT('Ctrl Pts',(-2.10968123246735,1.76418607500484,
12.4907355092743));
#430538=CARTESIAN_POINT('Ctrl Pts',(-2.10782793562257,1.75183421849748,
12.5218047446509));
#430539=CARTESIAN_POINT('Ctrl Pts',(-2.11040728173428,1.76336096324925,
12.5216906929434));
#430540=CARTESIAN_POINT('Ctrl Pts',(-2.10273934234465,1.7722813589718,12.5161988840776));
#430541=CARTESIAN_POINT('Ctrl Pts',(-2.10532206464639,1.74729635588789,
12.5369868989719));
#430542=CARTESIAN_POINT('Ctrl Pts',(-2.11273278129887,1.7607159985887,12.5369868989719));
#430543=CARTESIAN_POINT('Ctrl Pts',(-2.10270987500295,1.77231543309665,
12.5369868989719));
#430544=CARTESIAN_POINT('Origin',(-4.02788837499584E-31,-1.9397288087879E-31,
12.5));
#430545=CARTESIAN_POINT('Origin',(-2.20959091159279,1.5227929159564,12.5));
#430546=CARTESIAN_POINT('',(-2.20959091159279,1.5227929159564,12.5893111709658));
#430547=CARTESIAN_POINT('',(-2.20959091159279,1.5227929159564,13.8235269408515));
#430548=CARTESIAN_POINT('',(-2.20959091159279,1.5227929159564,12.5));
#430549=CARTESIAN_POINT('',(-2.22932368520977,1.55262394585116,13.7902182540695));
#430550=CARTESIAN_POINT('',(-2.20959091159279,1.5227929159564,13.8235269408515));
#430551=CARTESIAN_POINT('',(-2.2407588755845,1.56991110033548,13.7435492065112));
#430552=CARTESIAN_POINT('Origin',(-2.20313752209684,1.51303641086648,13.7445212918712));
#430553=CARTESIAN_POINT('',(-2.2407588755845,1.56991110033548,12.5369868989719));
#430554=CARTESIAN_POINT('',(-2.2407588755845,1.56991110033548,12.5));
#430555=CARTESIAN_POINT('Ctrl Pts',(-2.2407588755845,1.56991110033548,12.5369868989719));
#430556=CARTESIAN_POINT('Ctrl Pts',(-2.23037713159302,1.55421649392175,
12.5544431401645));
#430557=CARTESIAN_POINT('Ctrl Pts',(-2.2199879623023,1.53851066230838,12.5718848856037));
#430558=CARTESIAN_POINT('Ctrl Pts',(-2.20959091159279,1.5227929159564,12.5893111709658));
#430559=CARTESIAN_POINT('Origin',(-2.51467404694377,1.52389000361758,12.5));
#430560=CARTESIAN_POINT('',(-2.30038606421963,1.48116344709534,13.7435492065112));
#430561=CARTESIAN_POINT('',(-2.28005916367105,1.47711049716241,13.7902182540695));
#430562=CARTESIAN_POINT('Origin',(-2.22664358222596,1.46646004522961,13.7418732680453));
#430563=CARTESIAN_POINT('',(-2.24498269238234,1.47011665264502,13.8235269408515));
#430564=CARTESIAN_POINT('',(-2.28005916367105,1.47711049716241,13.7902182540695));
#430565=CARTESIAN_POINT('',(-2.24498269238234,1.47011665264502,12.5893111709658));
#430566=CARTESIAN_POINT('',(-2.24498269238234,1.47011665264502,12.5));
#430567=CARTESIAN_POINT('',(-2.30038606421963,1.48116344709534,12.5369868989719));
#430568=CARTESIAN_POINT('Ctrl Pts',(-2.24498269238234,1.47011665264502,
12.5893111709658));
#430569=CARTESIAN_POINT('Ctrl Pts',(-2.26346422254014,1.47380165696895,
12.5718848856037));
#430570=CARTESIAN_POINT('Ctrl Pts',(-2.28193174289044,1.47748386789857,
12.5544431401645));
#430571=CARTESIAN_POINT('Ctrl Pts',(-2.30038606421963,1.48116344709534,
12.5369868989719));
#430572=CARTESIAN_POINT('',(-2.30038606421963,1.48116344709534,12.5));
#430573=CARTESIAN_POINT('Origin',(-2.23826102351077,1.5038280719652,12.5));
#430574=CARTESIAN_POINT('',(-2.20911943565999,1.48559738273759,13.8587068136939));
#430575=CARTESIAN_POINT('Ctrl Pts',(-2.24498269238349,1.47011665263851,
13.8235269408542));
#430576=CARTESIAN_POINT('Ctrl Pts',(-2.24326422071284,1.46977400917324,
13.8262006681044));
#430577=CARTESIAN_POINT('Ctrl Pts',(-2.2414716431458,1.46959374908846,13.8288634856214));
#430578=CARTESIAN_POINT('Ctrl Pts',(-2.23961179117942,1.46956442089099,
13.8314912288862));
#430579=CARTESIAN_POINT('Ctrl Pts',(-2.23769447563692,1.46953418654446,
13.834200161153));
#430580=CARTESIAN_POINT('Ctrl Pts',(-2.23570354250922,1.46966382440372,
13.8368750301949));
#430581=CARTESIAN_POINT('Ctrl Pts',(-2.23362615866727,1.46998116568839,
13.8394886372968));
#430582=CARTESIAN_POINT('Ctrl Pts',(-2.23346571727412,1.47000567472556,
13.8396904925131));
#430583=CARTESIAN_POINT('Ctrl Pts',(-2.23330475973798,1.47003132552828,
13.8398919674349));
#430584=CARTESIAN_POINT('Ctrl Pts',(-2.23314328090578,1.47005814233663,
13.8400930404591));
#430585=CARTESIAN_POINT('Ctrl Pts',(-2.23062733206249,1.47047596625217,
13.8432258934518));
#430586=CARTESIAN_POINT('Ctrl Pts',(-2.22799748833976,1.47117360432241,
13.8462331177034));
#430587=CARTESIAN_POINT('Ctrl Pts',(-2.22536425589166,1.47222154462504,
13.8489036603661));
#430588=CARTESIAN_POINT('Ctrl Pts',(-2.22450263159018,1.47256444288756,
13.8497774930041));
#430589=CARTESIAN_POINT('Ctrl Pts',(-2.22364088937716,1.47294489700414,
13.85061494757));
#430590=CARTESIAN_POINT('Ctrl Pts',(-2.22278360249132,1.4733655071811,13.8514076489583));
#430591=CARTESIAN_POINT('Ctrl Pts',(-2.2209703170885,1.47425515836644,13.8530843267192));
#430592=CARTESIAN_POINT('Ctrl Pts',(-2.21900015461852,1.47541450384944,
13.8546805203176));
#430593=CARTESIAN_POINT('Ctrl Pts',(-2.21705666222821,1.47689385173497,
13.8559412814273));
#430594=CARTESIAN_POINT('Ctrl Pts',(-2.21679655991744,1.47709183645844,
13.8561100121513));
#430595=CARTESIAN_POINT('Ctrl Pts',(-2.2165369394636,1.47729547607385,13.8562727473908));
#430596=CARTESIAN_POINT('Ctrl Pts',(-2.21627823544945,1.47750481551776,
13.8564289040185));
#430597=CARTESIAN_POINT('Ctrl Pts',(-2.21510501569664,1.4784541675077,13.8571370725437));
#430598=CARTESIAN_POINT('Ctrl Pts',(-2.21393145359144,1.47953919945421,
13.8577210840553));
#430599=CARTESIAN_POINT('Ctrl Pts',(-2.2128230891778,1.48073928504898,13.8581177131616));
#430600=CARTESIAN_POINT('Ctrl Pts',(-2.21251093561018,1.48107727045816,
13.8582294175695));
#430601=CARTESIAN_POINT('Ctrl Pts',(-2.2122038490501,1.48142423795302,13.8583265086086));
#430602=CARTESIAN_POINT('Ctrl Pts',(-2.21190301456631,1.48177938708036,
13.8584082369006));
#430603=CARTESIAN_POINT('Ctrl Pts',(-2.21147079608506,1.48228964113935,
13.8585256585398));
#430604=CARTESIAN_POINT('Ctrl Pts',(-2.211046356362,1.4828233363635,13.8586122832068));
#430605=CARTESIAN_POINT('Ctrl Pts',(-2.21064133917199,1.48336710043221,
13.8586682984299));
#430606=CARTESIAN_POINT('Ctrl Pts',(-2.21031736556804,1.48380205778557,
13.8587131050557));
#430607=CARTESIAN_POINT('Ctrl Pts',(-2.21000205296354,1.48424812164223,
13.8587357943552));
#430608=CARTESIAN_POINT('Ctrl Pts',(-2.20969577744678,1.48470563734033,
13.8587355499465));
#430609=CARTESIAN_POINT('Ctrl Pts',(-2.20949782427831,1.48500134064375,
13.8587353919793));
#430610=CARTESIAN_POINT('Ctrl Pts',(-2.20930575471597,1.48529860856762,
13.8587257282814));
#430611=CARTESIAN_POINT('Ctrl Pts',(-2.20911943565999,1.48559738273759,
13.8587068136939));
#430612=CARTESIAN_POINT('Ctrl Pts',(-2.20911943565999,1.48559738273759,
13.8587068136939));
#430613=CARTESIAN_POINT('Ctrl Pts',(-2.20850664244234,1.48658003469455,
13.8586446046466));
#430614=CARTESIAN_POINT('Ctrl Pts',(-2.20795597628939,1.48757896052475,
13.858482427929));
#430615=CARTESIAN_POINT('Ctrl Pts',(-2.20746338346827,1.48859227523296,
13.8582284286032));
#430616=CARTESIAN_POINT('Ctrl Pts',(-2.20695804053452,1.48963181825003,
13.8579678548414));
#430617=CARTESIAN_POINT('Ctrl Pts',(-2.20651395923866,1.49068971361666,
13.857615680862));
#430618=CARTESIAN_POINT('Ctrl Pts',(-2.20613971274639,1.49172050412425,
13.8571944833187));
#430619=CARTESIAN_POINT('Ctrl Pts',(-2.20520574235014,1.49429294725656,
13.8561433417727));
#430620=CARTESIAN_POINT('Ctrl Pts',(-2.20465850952187,1.49681527480058,
13.8546163505474));
#430621=CARTESIAN_POINT('Ctrl Pts',(-2.20437450186005,1.49912164781843,
13.8528973491086));
#430622=CARTESIAN_POINT('Ctrl Pts',(-2.20432261785038,1.49954298814142,
13.8525833129072));
#430623=CARTESIAN_POINT('Ctrl Pts',(-2.20427938630757,1.49995717069509,
13.8522628768812));
#430624=CARTESIAN_POINT('Ctrl Pts',(-2.20424389852424,1.50036327237003,
13.851937733538));
#430625=CARTESIAN_POINT('Ctrl Pts',(-2.20402717955515,1.50284327895489,
13.8499521282529));
#430626=CARTESIAN_POINT('Ctrl Pts',(-2.20408177943199,1.50526874026406,
13.847639871647));
#430627=CARTESIAN_POINT('Ctrl Pts',(-2.20432450823963,1.50751399111926,
13.8452109780794));
#430628=CARTESIAN_POINT('Ctrl Pts',(-2.20443371695443,1.50852417595339,
13.8441181685877));
#430629=CARTESIAN_POINT('Ctrl Pts',(-2.20458036545448,1.50949820021415,
13.8430021611332));
#430630=CARTESIAN_POINT('Ctrl Pts',(-2.20475451431693,1.51042693500837,
13.8418824960098));
#430631=CARTESIAN_POINT('Ctrl Pts',(-2.20516490055834,1.51261552226703,
13.8392439765549));
#430632=CARTESIAN_POINT('Ctrl Pts',(-2.20574390287259,1.51465792831923,
13.8364981347964));
#430633=CARTESIAN_POINT('Ctrl Pts',(-2.20646012936871,1.51656888793135,
13.8336931113419));
#430634=CARTESIAN_POINT('Ctrl Pts',(-2.20715768849135,1.5184300412364,13.8309611966328));
#430635=CARTESIAN_POINT('Ctrl Pts',(-2.20798663946049,1.52016817766021,
13.8281701127186));
#430636=CARTESIAN_POINT('Ctrl Pts',(-2.20894724197503,1.52177067383454,
13.8253580685121));
#430637=CARTESIAN_POINT('Ctrl Pts',(-2.20915550163689,1.5221180967346,13.8247484142932));
#430638=CARTESIAN_POINT('Ctrl Pts',(-2.20937002295136,1.52245898744773,
13.8241378483365));
#430639=CARTESIAN_POINT('Ctrl Pts',(-2.20959091159279,1.5227929159564,13.8235269408515));
#430640=CARTESIAN_POINT('',(-2.20979706780673,1.48455642571058,12.5969504640361));
#430641=CARTESIAN_POINT('Origin',(-2.23828837686492,1.50384668585321,12.584524458991));
#430642=CARTESIAN_POINT('Origin',(-2.23828837686492,1.50384668585321,12.584524458991));
#430643=CARTESIAN_POINT('Ctrl Pts',(-2.24498269238234,1.47011665264502,
12.5893111709658));
#430644=CARTESIAN_POINT('Ctrl Pts',(-2.23386752565582,1.46790041637569,
12.5770542771492));
#430645=CARTESIAN_POINT('Ctrl Pts',(-2.22773157341713,1.48307123589803,
12.5737548217797));
#430646=CARTESIAN_POINT('Ctrl Pts',(-2.26928783165239,1.47496281757504,
12.5663937883685));
#430647=CARTESIAN_POINT('Ctrl Pts',(-2.25815848598708,1.47274375418857,
12.5540940315304));
#430648=CARTESIAN_POINT('Ctrl Pts',(-2.25200649659126,1.48796278903927,
12.5508374392248));
#430649=CARTESIAN_POINT('Ctrl Pts',(-2.2935684473349,1.47980409278406,12.5434499600944));
#430650=CARTESIAN_POINT('Ctrl Pts',(-2.28240291620359,1.47757781443226,
12.5311293540533));
#430651=CARTESIAN_POINT('Ctrl Pts',(-2.27625793571488,1.4928484064102,12.5278936106989));
#430652=CARTESIAN_POINT('Ctrl Pts',(-2.31782646039602,1.48464086129061,
12.5204817579905));
#430653=CARTESIAN_POINT('Ctrl Pts',(-2.30660566751615,1.48240356438245,
12.5081597038247));
#430654=CARTESIAN_POINT('Ctrl Pts',(-2.30048771879692,1.4977285357809,12.5049254088044));
#430655=CARTESIAN_POINT('Ctrl Pts',(-2.30038606421963,1.48116344709534,
12.5369868989719));
#430656=CARTESIAN_POINT('Ctrl Pts',(-2.30129958705399,1.48134559319564,
12.5342545179733));
#430657=CARTESIAN_POINT('Ctrl Pts',(-2.30214701877243,1.48164176307246,
12.5314872231885));
#430658=CARTESIAN_POINT('Ctrl Pts',(-2.30286217925637,1.48208804391716,
12.5287124745063));
#430659=CARTESIAN_POINT('Ctrl Pts',(-2.30350714647819,1.4824905221343,12.5262100684184));
#430660=CARTESIAN_POINT('Ctrl Pts',(-2.3040433616639,1.48301551890794,12.5237004536639));
#430661=CARTESIAN_POINT('Ctrl Pts',(-2.30443365549245,1.48371941612972,
12.5212220730815));
#430662=CARTESIAN_POINT('Ctrl Pts',(-2.3047324591813,1.48425831034496,12.5193246583486));
#430663=CARTESIAN_POINT('Ctrl Pts',(-2.30494875119866,1.48490881044974,
12.517417831369));
#430664=CARTESIAN_POINT('Ctrl Pts',(-2.30499813351841,1.48571919683289,
12.5155812248348));
#430665=CARTESIAN_POINT('Ctrl Pts',(-2.30501917065206,1.48606442578796,
12.5147988205793));
#430666=CARTESIAN_POINT('Ctrl Pts',(-2.30501021478349,1.48643900460363,
12.5140295443047));
#430667=CARTESIAN_POINT('Ctrl Pts',(-2.30496656771668,1.48684775597842,
12.5132817086137));
#430668=CARTESIAN_POINT('Ctrl Pts',(-2.30490051378551,1.48746634588954,
12.5121499604604));
#430669=CARTESIAN_POINT('Ctrl Pts',(-2.30474646989657,1.48817579891627,
12.5110494206568));
#430670=CARTESIAN_POINT('Ctrl Pts',(-2.30446743579976,1.48898034356171,
12.5100666561695));
#430671=CARTESIAN_POINT('Ctrl Pts',(-2.30430721506393,1.48944231124443,
12.5095023550641));
#430672=CARTESIAN_POINT('Ctrl Pts',(-2.30410331677059,1.48994075464284,
12.5089719619137));
#430673=CARTESIAN_POINT('Ctrl Pts',(-2.30385365127628,1.4904639127718,12.5085043804652));
#430674=CARTESIAN_POINT('Ctrl Pts',(-2.30348829834658,1.49122948654741,
12.5078201359221));
#430675=CARTESIAN_POINT('Ctrl Pts',(-2.30301325070733,1.49206966971377,
12.5072563000949));
#430676=CARTESIAN_POINT('Ctrl Pts',(-2.30245334000328,1.492923343416,12.5068768744332));
#430677=CARTESIAN_POINT('Ctrl Pts',(-2.30204960584128,1.49353890092241,
12.5066032824114));
#430678=CARTESIAN_POINT('Ctrl Pts',(-2.30159470517184,1.49417232005823,
12.5064197834844));
#430679=CARTESIAN_POINT('Ctrl Pts',(-2.30111614035319,1.49478973686366,
12.5063282718343));
#430680=CARTESIAN_POINT('Ctrl Pts',(-2.30041758387788,1.49569097425218,
12.5061946931565));
#430681=CARTESIAN_POINT('Ctrl Pts',(-2.29965451500638,1.49657802914186,
12.5062515701262));
#430682=CARTESIAN_POINT('Ctrl Pts',(-2.29888601479686,1.49740593435787,
12.5064436508398));
#430683=CARTESIAN_POINT('',(-2.22773157341713,1.48307123589803,12.5737548217797));
#430684=CARTESIAN_POINT('Origin',(-2.24068082430453,1.49169196100993,12.5893111709658));
#430685=CARTESIAN_POINT('Ctrl Pts',(-2.29888601479686,1.49740593435787,
12.5064436508398));
#430686=CARTESIAN_POINT('Ctrl Pts',(-2.28835321395465,1.49528449754067,
12.5164271754438));
#430687=CARTESIAN_POINT('Ctrl Pts',(-2.27781627916637,1.49316201496396,
12.5264061185523));
#430688=CARTESIAN_POINT('Ctrl Pts',(-2.26727506465103,1.49103845072481,
12.536380305637));
#430689=CARTESIAN_POINT('Ctrl Pts',(-2.25410068449553,1.48838442613112,
12.5488460165097));
#430690=CARTESIAN_POINT('Ctrl Pts',(-2.24091961554937,1.48572871118047,
12.5613043021964));
#430691=CARTESIAN_POINT('Ctrl Pts',(-2.22773157341713,1.48307123589803,
12.5737548217797));
#430692=CARTESIAN_POINT('Ctrl Pts',(-2.20959091159279,1.5227929159564,12.5893111709658));
#430693=CARTESIAN_POINT('Ctrl Pts',(-2.20333791462157,1.51333994481301,
12.5770542771492));
#430694=CARTESIAN_POINT('Ctrl Pts',(-2.21506416483591,1.50192509786855,
12.5737548217797));
#430695=CARTESIAN_POINT('Ctrl Pts',(-2.20375691980434,1.51397337609722,
12.5928319619712));
#430696=CARTESIAN_POINT('Ctrl Pts',(-2.20227160599699,1.505823084123,12.5821634970843));
#430697=CARTESIAN_POINT('Ctrl Pts',(-2.21293111045991,1.49871756043331,
12.5773203894503));
#430698=CARTESIAN_POINT('Ctrl Pts',(-2.20118490405364,1.49742137216061,
12.5969440695591));
#430699=CARTESIAN_POINT('Ctrl Pts',(-2.20341149200726,1.49407460526751,
12.5878292599214));
#430700=CARTESIAN_POINT('Ctrl Pts',(-2.21201641327838,1.49281777432162,
12.5813877129824));
#430701=CARTESIAN_POINT('Ctrl Pts',(-2.21820370745212,1.47199430830287,
12.596957478804));
#430702=CARTESIAN_POINT('Ctrl Pts',(-2.21599364131866,1.47531638609164,
12.5878468778671));
#430703=CARTESIAN_POINT('Ctrl Pts',(-2.21811263613238,1.48372039364263,
12.5814011370086));
#430704=CARTESIAN_POINT('Ctrl Pts',(-2.23459728076517,1.46804592114231,
12.5928371701607));
#430705=CARTESIAN_POINT('Ctrl Pts',(-2.22649724499558,1.46975603407284,
12.5821692192952));
#430706=CARTESIAN_POINT('Ctrl Pts',(-2.2239437249622,1.48230606823244,12.5773318885715));
#430707=CARTESIAN_POINT('Ctrl Pts',(-2.24498269238234,1.47011665264496,
12.5893111709658));
#430708=CARTESIAN_POINT('Ctrl Pts',(-2.23386752565583,1.46790041637563,
12.5770542771492));
#430709=CARTESIAN_POINT('Ctrl Pts',(-2.22773157341714,1.48307123589797,
12.5737548217797));
#430710=CARTESIAN_POINT('',(-2.21506416483591,1.50192509786855,12.5737548217797));
#430711=CARTESIAN_POINT('Origin',(-2.22793978322029,1.51065541580203,12.5893111709658));
#430712=CARTESIAN_POINT('Ctrl Pts',(-2.22773157341714,1.48307123589797,
12.5737548217797));
#430713=CARTESIAN_POINT('Ctrl Pts',(-2.22675567602634,1.48284332382357,
12.5746934679442));
#430714=CARTESIAN_POINT('Ctrl Pts',(-2.22563412055118,1.48276950814525,
12.5756680099006));
#430715=CARTESIAN_POINT('Ctrl Pts',(-2.22449472684561,1.48285486417438,
12.5765688348656));
#430716=CARTESIAN_POINT('Ctrl Pts',(-2.22419308497557,1.48287746123817,
12.5768073183026));
#430717=CARTESIAN_POINT('Ctrl Pts',(-2.22389023664768,1.48291096079766,
12.5770407398754));
#430718=CARTESIAN_POINT('Ctrl Pts',(-2.22358850687059,1.48295489580108,
12.5772674179684));
#430719=CARTESIAN_POINT('Ctrl Pts',(-2.22235028945663,1.48313519317458,
12.5781976435658));
#430720=CARTESIAN_POINT('Ctrl Pts',(-2.22106220670867,1.48351263233153,
12.5790594849312));
#430721=CARTESIAN_POINT('Ctrl Pts',(-2.21982481093434,1.48410806866006,
12.5797571720116));
#430722=CARTESIAN_POINT('Ctrl Pts',(-2.21901860309458,1.48449601683809,
12.580211740231));
#430723=CARTESIAN_POINT('Ctrl Pts',(-2.2182054139075,1.48501105113437,12.5806009430798));
#430724=CARTESIAN_POINT('Ctrl Pts',(-2.21745196790057,1.48563188265658,
12.5808812374708));
#430725=CARTESIAN_POINT('Ctrl Pts',(-2.21680450782752,1.48616538289287,
12.5811221033394));
#430726=CARTESIAN_POINT('Ctrl Pts',(-2.21618798251315,1.48678801945575,
12.581287365893));
#430727=CARTESIAN_POINT('Ctrl Pts',(-2.21564311448782,1.48747051642895,
12.581359338449));
#430728=CARTESIAN_POINT('Ctrl Pts',(-2.21556738908339,1.4875653694152,12.5813693411482));
#430729=CARTESIAN_POINT('Ctrl Pts',(-2.21549299118832,1.48766135899467,
12.5813775999465));
#430730=CARTESIAN_POINT('Ctrl Pts',(-2.21541997181832,1.48775838750229,
12.5813841266931));
#430731=CARTESIAN_POINT('Ctrl Pts',(-2.2152960856256,1.48792300810081,12.5813952001081));
#430732=CARTESIAN_POINT('Ctrl Pts',(-2.21517582431766,1.48809208794563,
12.5814007534795));
#430733=CARTESIAN_POINT('Ctrl Pts',(-2.21505940097739,1.48826566770161,
12.5814005856065));
#430734=CARTESIAN_POINT('Ctrl Pts',(-2.2145264604442,1.48906024795921,12.5813998171494));
#430735=CARTESIAN_POINT('Ctrl Pts',(-2.21411048442807,1.48989403423559,
12.58127954464));
#430736=CARTESIAN_POINT('Ctrl Pts',(-2.21378735740361,1.4907490833764,12.5810700125799));
#430737=CARTESIAN_POINT('Ctrl Pts',(-2.21339705674902,1.49178188538335,
12.5808169217085));
#430738=CARTESIAN_POINT('Ctrl Pts',(-2.21315784187356,1.49285171929701,
12.5804173076348));
#430739=CARTESIAN_POINT('Ctrl Pts',(-2.21306526238418,1.49385914393727,
12.5799304713245));
#430740=CARTESIAN_POINT('Ctrl Pts',(-2.21295052723128,1.49510766043804,
12.5793271277669));
#430741=CARTESIAN_POINT('Ctrl Pts',(-2.21302182717764,1.49633482347775,
12.5785808224116));
#430742=CARTESIAN_POINT('Ctrl Pts',(-2.21324449333399,1.49749074546726,
12.5777485681082));
#430743=CARTESIAN_POINT('Ctrl Pts',(-2.21357629030185,1.49921319587233,
12.576508418016));
#430744=CARTESIAN_POINT('Ctrl Pts',(-2.21423464280381,1.50076425728114,
12.5750928681475));
#430745=CARTESIAN_POINT('Ctrl Pts',(-2.21506416483591,1.50192509786855,
12.5737548217797));
#430746=CARTESIAN_POINT('Ctrl Pts',(-2.21506416483591,1.50192509786855,
12.5737548217797));
#430747=CARTESIAN_POINT('Ctrl Pts',(-2.20333791462157,1.51333994481301,
12.5770542771492));
#430748=CARTESIAN_POINT('Ctrl Pts',(-2.20959091159279,1.5227929159564,12.5893111709658));
#430749=CARTESIAN_POINT('Ctrl Pts',(-2.22876591246297,1.5225473447426,12.5508408821982));
#430750=CARTESIAN_POINT('Ctrl Pts',(-2.21700108902443,1.53399525521084,
12.55409748406));
#430751=CARTESIAN_POINT('Ctrl Pts',(-2.22326206321831,1.54346028592439,
12.5663972313419));
#430752=CARTESIAN_POINT('Ctrl Pts',(-2.2424532927753,1.54315009902394,12.52790050457));
#430753=CARTESIAN_POINT('Ctrl Pts',(-2.23063809519623,1.55461100577294,
12.5311362602938));
#430754=CARTESIAN_POINT('Ctrl Pts',(-2.2369194228983,1.56410680591216,12.5434568539655));
#430755=CARTESIAN_POINT('Ctrl Pts',(-2.25612741076335,1.56373488320074,
12.5049357605811));
#430756=CARTESIAN_POINT('Ctrl Pts',(-2.24425166104124,1.57519132040988,
12.5081700652078));
#430757=CARTESIAN_POINT('Ctrl Pts',(-2.25056407082075,1.58473410889444,
12.5204921097672));
#430758=CARTESIAN_POINT('Ctrl Pts',(-2.25522951325334,1.56238320646001,
12.5064436508395));
#430759=CARTESIAN_POINT('Ctrl Pts',(-2.25471532227217,1.56348975760002,
12.5062361689309));
#430760=CARTESIAN_POINT('Ctrl Pts',(-2.25413341993089,1.56461855398806,
12.5061871075061));
#430761=CARTESIAN_POINT('Ctrl Pts',(-2.25350965950472,1.56567777047767,
12.5063648335164));
#430762=CARTESIAN_POINT('Ctrl Pts',(-2.25322630904402,1.56615893194244,
12.5064455676329));
#430763=CARTESIAN_POINT('Ctrl Pts',(-2.25293017902171,1.5666323347451,12.506574497099));
#430764=CARTESIAN_POINT('Ctrl Pts',(-2.2526330756161,1.56707712344868,12.5067492519495));
#430765=CARTESIAN_POINT('Ctrl Pts',(-2.25203603478978,1.56797094361401,
12.5071004286051));
#430766=CARTESIAN_POINT('Ctrl Pts',(-2.25141244009367,1.56878162667607,
12.5076537929613));
#430767=CARTESIAN_POINT('Ctrl Pts',(-2.25081659260674,1.56945409349212,
12.5083435010505));
#430768=CARTESIAN_POINT('Ctrl Pts',(-2.25077908044664,1.56949642929687,
12.5083869222964));
#430769=CARTESIAN_POINT('Ctrl Pts',(-2.25074166523779,1.56953821398961,
12.5084308732337));
#430770=CARTESIAN_POINT('Ctrl Pts',(-2.25070435512934,1.56957943286714,
12.5084753333615));
#430771=CARTESIAN_POINT('Ctrl Pts',(-2.25040507881477,1.56991006266887,
12.5088319622689));
#430772=CARTESIAN_POINT('Ctrl Pts',(-2.25010744547243,1.57021186510831,
12.509227847131));
#430773=CARTESIAN_POINT('Ctrl Pts',(-2.24982229895179,1.57047783214431,
12.5096423454524));
#430774=CARTESIAN_POINT('Ctrl Pts',(-2.24892877595666,1.57131125512306,
12.5109411997424));
#430775=CARTESIAN_POINT('Ctrl Pts',(-2.24810950077872,1.57185113499161,
12.5124831113042));
#430776=CARTESIAN_POINT('Ctrl Pts',(-2.24738040813741,1.57219075595073,
12.5140723025008));
#430777=CARTESIAN_POINT('Ctrl Pts',(-2.24731209135837,1.57222257880657,
12.5142212114565));
#430778=CARTESIAN_POINT('Ctrl Pts',(-2.24724456077942,1.57225267248488,
12.5143705582413));
#430779=CARTESIAN_POINT('Ctrl Pts',(-2.24717782783351,1.57228113062874,
12.5145201959299));
#430780=CARTESIAN_POINT('Ctrl Pts',(-2.24632054378837,1.57264671785638,
12.5164425148273));
#430781=CARTESIAN_POINT('Ctrl Pts',(-2.24556973353945,1.57276479304203,
12.518463520594));
#430782=CARTESIAN_POINT('Ctrl Pts',(-2.24489212546417,1.57271920711102,
12.5205025929157));
#430783=CARTESIAN_POINT('Ctrl Pts',(-2.24449908592263,1.57269276546418,
12.5216853356836));
#430784=CARTESIAN_POINT('Ctrl Pts',(-2.24413135248927,1.57261179092169,
12.5228750347131));
#430785=CARTESIAN_POINT('Ctrl Pts',(-2.24378805546091,1.57249450921438,
12.5240609649613));
#430786=CARTESIAN_POINT('Ctrl Pts',(-2.24294545132205,1.57220664755573,
12.5269717671326));
#430787=CARTESIAN_POINT('Ctrl Pts',(-2.24222970611256,1.57168212130923,
12.5299036066169));
#430788=CARTESIAN_POINT('Ctrl Pts',(-2.2416015010593,1.57099815454307,12.5328133004019));
#430789=CARTESIAN_POINT('Ctrl Pts',(-2.24129992605445,1.57066981066912,
12.5342101228451));
#430790=CARTESIAN_POINT('Ctrl Pts',(-2.24101928745411,1.57030477795461,
12.5356023438238));
#430791=CARTESIAN_POINT('Ctrl Pts',(-2.2407588755845,1.56991110033548,12.5369868989719));
#430792=CARTESIAN_POINT('Origin',(-9.26738283409461,12.2020107234904,-1.2388424640659));
#430793=CARTESIAN_POINT('Ctrl Pts',(-2.30034508453518,1.48115523573753,
12.5369868989719));
#430794=CARTESIAN_POINT('Ctrl Pts',(-2.31538220108036,1.48418317723182,
12.5369868989719));
#430795=CARTESIAN_POINT('Ctrl Pts',(-2.32342295645086,1.47112065233202,
12.5369868989719));
#430796=CARTESIAN_POINT('Ctrl Pts',(-2.30542823109593,1.48217873347564,
12.5218025310016));
#430797=CARTESIAN_POINT('Ctrl Pts',(-2.31720240784264,1.48116649553802,
12.5216901060418));
#430798=CARTESIAN_POINT('Ctrl Pts',(-2.32339845960796,1.471160479882,12.5161920673678));
#430799=CARTESIAN_POINT('Ctrl Pts',(-2.30790882579116,1.48767261381232,
12.5042015548894));
#430800=CARTESIAN_POINT('Ctrl Pts',(-2.31410372809367,1.48594040987532,
12.4980677368513));
#430801=CARTESIAN_POINT('Ctrl Pts',(-2.31777081800236,1.48021823971661,
12.4907278922777));
#430802=CARTESIAN_POINT('Ctrl Pts',(-2.29886925544556,1.49739501797345,
12.506463626192));
#430803=CARTESIAN_POINT('Ctrl Pts',(-2.3043515601987,1.50096598043898,12.4999376786891));
#430804=CARTESIAN_POINT('Ctrl Pts',(-2.3042846018174,1.50092236632464,12.4906970594712));
#430805=CARTESIAN_POINT('Origin',(-2.30468793229744,1.45958813873043,12.5369868989719));
#430806=CARTESIAN_POINT('Origin',(-2.30468793229744,1.45958813873043,14.));
#430807=CARTESIAN_POINT('Origin',(-2.30468793229744,1.45958813873043,13.7435492065112));
#430808=CARTESIAN_POINT('Ctrl Pts',(-2.27610393869126,1.47632184315448,
13.793642941384));
#430809=CARTESIAN_POINT('Ctrl Pts',(-2.28670217728922,1.47846276763383,
13.8071662555867));
#430810=CARTESIAN_POINT('Ctrl Pts',(-2.29249185652868,1.46244718153968,
13.8103758687955));
#430811=CARTESIAN_POINT('Ctrl Pts',(-2.29240420348061,1.47957193131032,
13.7804579775005));
#430812=CARTESIAN_POINT('Ctrl Pts',(-2.30548347994049,1.48220369859024,
13.7901904343351));
#430813=CARTESIAN_POINT('Ctrl Pts',(-2.31316693237331,1.46844795495796,
13.7927914348262));
#430814=CARTESIAN_POINT('Ctrl Pts',(-2.30200078281746,1.48148538048494,
13.7597120340895));
#430815=CARTESIAN_POINT('Ctrl Pts',(-2.31713831944396,1.48452545858477,
13.7635825532445));
#430816=CARTESIAN_POINT('Ctrl Pts',(-2.325366126179,1.47196205488693,13.7651073818884));
#430817=CARTESIAN_POINT('Ctrl Pts',(-2.3001215528468,1.48111068332275,13.7381884353898));
#430818=CARTESIAN_POINT('Ctrl Pts',(-2.31490459024643,1.48408048396722,
13.7368803041982));
#430819=CARTESIAN_POINT('Ctrl Pts',(-2.32297729833982,1.47127341478032,
13.7363986145813));
#430820=CARTESIAN_POINT('Origin',(-2.28436103174886,1.45553518879749,13.7902182540695));
#430821=CARTESIAN_POINT('Ctrl Pts',(-2.24497883231734,1.47011588221864,
13.8235227101244));
#430822=CARTESIAN_POINT('Ctrl Pts',(-2.25625309620494,1.4723683613223,13.8358800583119));
#430823=CARTESIAN_POINT('Ctrl Pts',(-2.26236341763185,1.4569641404359,13.8390832900376));
#430824=CARTESIAN_POINT('Ctrl Pts',(-2.25667615971092,1.47244819462107,
13.8124254819053));
#430825=CARTESIAN_POINT('Ctrl Pts',(-2.26797231811368,1.47470504773445,
13.8247886449158));
#430826=CARTESIAN_POINT('Ctrl Pts',(-2.27407451681287,1.45927507844938,
13.8279860620657));
#430827=CARTESIAN_POINT('Ctrl Pts',(-2.26836824474284,1.47477946175696,
13.8013225099954));
#430828=CARTESIAN_POINT('Ctrl Pts',(-2.2796809672952,1.47703962597359,13.8136962257787));
#430829=CARTESIAN_POINT('Ctrl Pts',(-2.28578014185561,1.4615852125404,13.8168830918626));
#430830=CARTESIAN_POINT('Ctrl Pts',(-2.28005529138546,1.47710972429605,
13.7902140179785));
#430831=CARTESIAN_POINT('Ctrl Pts',(-2.29137959610102,1.47937220617531,
13.802602731458));
#430832=CARTESIAN_POINT('Ctrl Pts',(-2.29748050749599,1.46389457610245,
13.8057746032558));
#430833=CARTESIAN_POINT('Origin',(-2.24928456046014,1.4485413442801,13.8235269408515));
#430834=CARTESIAN_POINT('Ctrl Pts',(-2.20959091159279,1.5227929159564,13.8235269408515));
#430835=CARTESIAN_POINT('Ctrl Pts',(-2.21610515287597,1.53264082331256,
13.8362179249168));
#430836=CARTESIAN_POINT('Ctrl Pts',(-2.20357280835889,1.54424269147948,
13.8391868794938));
#430837=CARTESIAN_POINT('Ctrl Pts',(-2.20363066436673,1.5137825093794,13.8400110824519));
#430838=CARTESIAN_POINT('Ctrl Pts',(-2.20600024377829,1.52356550259586,
13.8494522556837));
#430839=CARTESIAN_POINT('Ctrl Pts',(-2.19385763417706,1.5293521181446,13.85569149686));
#430840=CARTESIAN_POINT('Ctrl Pts',(-2.20099260876462,1.49770649032351,
13.8586819406588));
#430841=CARTESIAN_POINT('Ctrl Pts',(-2.19857607065724,1.50132814563712,
13.868010383617));
#430842=CARTESIAN_POINT('Ctrl Pts',(-2.18962248223092,1.50264196491109,
13.8744918421245));
#430843=CARTESIAN_POINT('Ctrl Pts',(-2.21839896968065,1.47170475773493,
13.8587686893867));
#430844=CARTESIAN_POINT('Ctrl Pts',(-2.22079395378256,1.4681153038668,13.8680909899357));
#430845=CARTESIAN_POINT('Ctrl Pts',(-2.2186010995933,1.45935814725004,13.8745789365163));
#430846=CARTESIAN_POINT('Ctrl Pts',(-2.23437066984899,1.4680007375281,13.8400379222776));
#430847=CARTESIAN_POINT('Ctrl Pts',(-2.24431996677128,1.46649019965689,
13.8494748685453));
#430848=CARTESIAN_POINT('Ctrl Pts',(-2.24508859442963,1.45306744596076,
13.8557104837033));
#430849=CARTESIAN_POINT('Ctrl Pts',(-2.24498269238349,1.47011665263851,
13.8235269408542));
#430850=CARTESIAN_POINT('Ctrl Pts',(-2.25656224028548,1.47242548116746,
13.8362179249195));
#430851=CARTESIAN_POINT('Ctrl Pts',(-2.26256666355615,1.45643767627614,
13.8391868794965));
#430852=CARTESIAN_POINT('Origin',(-2.19124203996528,1.53493041611077,13.8235269408515));
#430853=CARTESIAN_POINT('Ctrl Pts',(-2.22932150926554,1.55262065774392,
13.7902140241682));
#430854=CARTESIAN_POINT('Ctrl Pts',(-2.23569636053668,1.56224977331409,
13.8026027327198));
#430855=CARTESIAN_POINT('Ctrl Pts',(-2.22367281973875,1.5737481383698,13.8057746032556));
#430856=CARTESIAN_POINT('Ctrl Pts',(-2.22274679301792,1.54268132732958,
13.8013225161807));
#430857=CARTESIAN_POINT('Ctrl Pts',(-2.22911512089271,1.552300595907,13.8136962270464));
#430858=CARTESIAN_POINT('Ctrl Pts',(-2.21711241802939,1.56378857785723,
13.8168830918628));
#430859=CARTESIAN_POINT('Ctrl Pts',(-2.216169242351,1.53273771198048,13.8124254880875));
#430860=CARTESIAN_POINT('Ctrl Pts',(-2.22252824406069,1.54234289663759,
13.8247886461868));
#430861=CARTESIAN_POINT('Ctrl Pts',(-2.21054931507107,1.55382443932404,
13.8279860620656));
#430862=CARTESIAN_POINT('Ctrl Pts',(-2.20958874251634,1.52278963822562,
13.8235227163065));
#430863=CARTESIAN_POINT('Ctrl Pts',(-2.21593541930373,1.5323762057549,13.8358800595847));
#430864=CARTESIAN_POINT('Ctrl Pts',(-2.20398339878361,1.54385553658406,
13.8390832900376));
#430865=CARTESIAN_POINT('Origin',(-2.21097481358226,1.56476144600553,13.7902182540695));
#430866=CARTESIAN_POINT('Ctrl Pts',(-2.24060996964151,1.56968604170401,
13.7382347919292));
#430867=CARTESIAN_POINT('Ctrl Pts',(-2.24895537660476,1.58225871251618,
13.7369371795943));
#430868=CARTESIAN_POINT('Ctrl Pts',(-2.24013602089833,1.59457791467962,
13.7364597369711));
#430869=CARTESIAN_POINT('Ctrl Pts',(-2.24165355147467,1.57126367630735,
13.7595490285574));
#430870=CARTESIAN_POINT('Ctrl Pts',(-2.25019723501361,1.58413687629824,
13.7633824266925));
#430871=CARTESIAN_POINT('Ctrl Pts',(-2.24165789716282,1.59650511664909,
13.7648920890506));
#430872=CARTESIAN_POINT('Ctrl Pts',(-2.23633134130424,1.56321782625572,
13.7803806590111));
#430873=CARTESIAN_POINT('Ctrl Pts',(-2.24372581974754,1.57434969827063,
13.7901039518745));
#430874=CARTESIAN_POINT('Ctrl Pts',(-2.23390211956567,1.58667772958803,
13.7926933640892));
#430875=CARTESIAN_POINT('Ctrl Pts',(-2.22708015189695,1.54923234284881,
13.7936647693663));
#430876=CARTESIAN_POINT('Ctrl Pts',(-2.23307204524306,1.55823626122213,
13.8072068914933));
#430877=CARTESIAN_POINT('Ctrl Pts',(-2.22041213299701,1.56965426856883,
13.8104111085397));
#430878=CARTESIAN_POINT('Origin',(-2.22241000395699,1.58204860048985,13.7435492065112));
#430879=CARTESIAN_POINT('Origin',(-2.22241000395699,1.58204860048985,14.));
#430880=CARTESIAN_POINT('Origin',(-2.22241000395699,1.58204860048985,12.5369868989719));
#430881=CARTESIAN_POINT('Ctrl Pts',(-2.2552144020631,1.56237273768155,12.506462012331));
#430882=CARTESIAN_POINT('Ctrl Pts',(-2.26058921242423,1.56609631144499,
12.4999388158272));
#430883=CARTESIAN_POINT('Ctrl Pts',(-2.26052562136902,1.5660522566842,12.4907030323752));
#430884=CARTESIAN_POINT('Ctrl Pts',(-2.24962821177142,1.57441528978563,
12.5042014951932));
#430885=CARTESIAN_POINT('Ctrl Pts',(-2.25036659662837,1.58080245542613,
12.4980716682127));
#430886=CARTESIAN_POINT('Ctrl Pts',(-2.24645898522011,1.58635728560428,
12.4907355092743));
#430887=CARTESIAN_POINT('Ctrl Pts',(-2.24360506409332,1.57419758977853,
12.5218047446509));
#430888=CARTESIAN_POINT('Ctrl Pts',(-2.24711536434996,1.58547573958442,
12.5216906929434));
#430889=CARTESIAN_POINT('Ctrl Pts',(-2.2402000344604,1.59499146167199,12.5161988840776));
#430890=CARTESIAN_POINT('Ctrl Pts',(-2.24073765326595,1.56987907828033,
12.5369868989719));
#430891=CARTESIAN_POINT('Ctrl Pts',(-2.24921753683209,1.58265002602219,
12.5369868989719));
#430892=CARTESIAN_POINT('Ctrl Pts',(-2.24017344252634,1.59502782427993,
12.5369868989719));
#430893=CARTESIAN_POINT('Origin',(-4.27630463278518E-31,-2.27872721465334E-31,
12.5));
#430894=CARTESIAN_POINT('Origin',(-2.32636043968303,1.3376237760141,12.5));
#430895=CARTESIAN_POINT('',(-2.32636043968303,1.3376237760141,12.5893111709658));
#430896=CARTESIAN_POINT('',(-2.32636043968303,1.3376237760141,13.8235269408515));
#430897=CARTESIAN_POINT('',(-2.32636043968303,1.3376237760141,12.5));
#430898=CARTESIAN_POINT('',(-2.34845905999784,1.36574714137786,13.7902182540695));
#430899=CARTESIAN_POINT('',(-2.32636043968303,1.3376237760141,13.8235269408515));
#430900=CARTESIAN_POINT('',(-2.36126526429652,1.38204470010705,13.7435492065112));
#430901=CARTESIAN_POINT('Origin',(-2.31913327757043,1.3284257460468,13.7445212918724));
#430902=CARTESIAN_POINT('',(-2.36126526429652,1.38204470010705,12.5369868989719));
#430903=CARTESIAN_POINT('',(-2.36126526429652,1.38204470010705,12.5));
#430904=CARTESIAN_POINT('Ctrl Pts',(-2.36126526429652,1.38204470010705,
12.5369868989719));
#430905=CARTESIAN_POINT('Ctrl Pts',(-2.34963880857739,1.36724852471616,
12.5544431401645));
#430906=CARTESIAN_POINT('Ctrl Pts',(-2.33800403730813,1.35244176670738,
12.5718848856037));
#430907=CARTESIAN_POINT('Ctrl Pts',(-2.32636043968303,1.3376237760141,12.5893111709658));
#430908=CARTESIAN_POINT('Origin',(-2.63051785889797,1.31385010542184,12.5));
#430909=CARTESIAN_POINT('',(-2.41346029074828,1.28873217793633,13.7435492065112));
#430910=CARTESIAN_POINT('',(-2.39287067323913,1.28634954496039,13.7902182540695));
#430911=CARTESIAN_POINT('Origin',(-2.3387647170221,1.28008839730092,13.741873268043));
#430912=CARTESIAN_POINT('',(-2.35734085275917,1.28223802992779,13.8235269408515));
#430913=CARTESIAN_POINT('',(-2.39287067323913,1.28634954496039,13.7902182540695));
#430914=CARTESIAN_POINT('',(-2.35734085275917,1.28223802992779,12.5893111709658));
#430915=CARTESIAN_POINT('',(-2.35734085275917,1.28223802992779,12.5));
#430916=CARTESIAN_POINT('',(-2.41346029074828,1.28873217793633,12.5369868989719));
#430917=CARTESIAN_POINT('Ctrl Pts',(-2.35734085275917,1.28223802992779,
12.5893111709658));
#430918=CARTESIAN_POINT('Ctrl Pts',(-2.37606124921231,1.28440435642181,
12.5718848856037));
#430919=CARTESIAN_POINT('Ctrl Pts',(-2.39476745478685,1.28656904074567,
12.5544431401645));
#430920=CARTESIAN_POINT('Ctrl Pts',(-2.41346029074828,1.28873217793633,
12.5369868989719));
#430921=CARTESIAN_POINT('',(-2.41346029074828,1.28873217793633,12.5));
#430922=CARTESIAN_POINT('Origin',(-2.35338934332242,1.31638515569514,12.5));
#430923=CARTESIAN_POINT('',(-2.32285875128382,1.30059043752891,13.8587068136939));
#430924=CARTESIAN_POINT('Ctrl Pts',(-2.35734085275979,1.28223802992121,
13.8235269408542));
#430925=CARTESIAN_POINT('Ctrl Pts',(-2.35560017053849,1.28203659796847,
13.8262006681044));
#430926=CARTESIAN_POINT('Ctrl Pts',(-2.35379886475506,1.28200304939745,
13.8288634856214));
#430927=CARTESIAN_POINT('Ctrl Pts',(-2.35194281077231,1.28212541398842,
13.8314912288862));
#430928=CARTESIAN_POINT('Ctrl Pts',(-2.35002941055919,1.28225155926039,
13.8342001611531));
#430929=CARTESIAN_POINT('Ctrl Pts',(-2.34805566878626,1.28254304529319,
13.8368750301949));
#430930=CARTESIAN_POINT('Ctrl Pts',(-2.34601106352842,1.28302865671952,
13.8394886372969));
#430931=CARTESIAN_POINT('Ctrl Pts',(-2.34585315370484,1.2830661616679,13.8396904925131));
#430932=CARTESIAN_POINT('Ctrl Pts',(-2.34569482252017,1.28310484665314,
13.8398919674349));
#430933=CARTESIAN_POINT('Ctrl Pts',(-2.3455360668143,1.28314473625469,13.8400930404591));
#430934=CARTESIAN_POINT('Ctrl Pts',(-2.34306254611124,1.28376624308328,
13.8432258934518));
#430935=CARTESIAN_POINT('Ctrl Pts',(-2.34049831695584,1.28467591649807,
13.8462331177034));
#430936=CARTESIAN_POINT('Ctrl Pts',(-2.33795926323475,1.28593500275606,
13.8489036603661));
#430937=CARTESIAN_POINT('Ctrl Pts',(-2.33712845530876,1.28634699043239,
13.8497774930041));
#430938=CARTESIAN_POINT('Ctrl Pts',(-2.33630059101433,1.28679641860967,
13.85061494757));
#430939=CARTESIAN_POINT('Ctrl Pts',(-2.33548044031406,1.28728550608083,
13.8514076489583));
#430940=CARTESIAN_POINT('Ctrl Pts',(-2.33374570329957,1.28831999661928,
13.8530843267192));
#430941=CARTESIAN_POINT('Ctrl Pts',(-2.3318765938024,1.2896360710072,13.8546805203176));
#430942=CARTESIAN_POINT('Ctrl Pts',(-2.33006014880899,1.29126890915697,
13.8559412814273));
#430943=CARTESIAN_POINT('Ctrl Pts',(-2.32981704956014,1.29148743585562,
13.8561100121513));
#430944=CARTESIAN_POINT('Ctrl Pts',(-2.32957489149108,1.29171155935421,
13.8562727473908));
#430945=CARTESIAN_POINT('Ctrl Pts',(-2.32933411140126,1.29194128901726,
13.8564289040185));
#430946=CARTESIAN_POINT('Ctrl Pts',(-2.32824217644093,1.29298311041826,
13.8571370725437));
#430947=CARTESIAN_POINT('Ctrl Pts',(-2.32716095944341,1.29416018821688,
13.8577210840554));
#430948=CARTESIAN_POINT('Ctrl Pts',(-2.32615410113795,1.2954466226151,13.8581177131616));
#430949=CARTESIAN_POINT('Ctrl Pts',(-2.32587053518412,1.29580892681936,
13.8582294175695));
#430950=CARTESIAN_POINT('Ctrl Pts',(-2.32559275150116,1.296179770214,13.8583265086086));
#430951=CARTESIAN_POINT('Ctrl Pts',(-2.32532186597022,1.29655825841516,
13.8584082369006));
#430952=CARTESIAN_POINT('Ctrl Pts',(-2.32493267610309,1.2971020444646,13.8585256585398));
#430953=CARTESIAN_POINT('Ctrl Pts',(-2.32455314978355,1.29766855963966,
13.8586122832068));
#430954=CARTESIAN_POINT('Ctrl Pts',(-2.32419380207448,1.29824352703926,
13.8586682984299));
#430955=CARTESIAN_POINT('Ctrl Pts',(-2.32390635952822,1.29870344396426,
13.8587131050557));
#430956=CARTESIAN_POINT('Ctrl Pts',(-2.32362845444578,1.29917372448472,
13.8587357943552));
#430957=CARTESIAN_POINT('Ctrl Pts',(-2.32336048981229,1.29965468213501,
13.8587355499465));
#430958=CARTESIAN_POINT('Ctrl Pts',(-2.32318729788112,1.29996553653094,
13.8587353919793));
#430959=CARTESIAN_POINT('Ctrl Pts',(-2.32302009750993,1.30027747077265,
13.8587257282814));
#430960=CARTESIAN_POINT('Ctrl Pts',(-2.32285875128382,1.30059043752891,
13.8587068136939));
#430961=CARTESIAN_POINT('Ctrl Pts',(-2.32285875128382,1.30059043752891,
13.8587068136939));
#430962=CARTESIAN_POINT('Ctrl Pts',(-2.32232809234198,1.30161976812876,
13.8586446046466));
#430963=CARTESIAN_POINT('Ctrl Pts',(-2.32186068021392,1.30266025451934,
13.858482427929));
#430964=CARTESIAN_POINT('Ctrl Pts',(-2.32145232101062,1.30371034839446,
13.8582284286032));
#430965=CARTESIAN_POINT('Ctrl Pts',(-2.32103339197034,1.30478762255838,
13.8579678548414));
#430966=CARTESIAN_POINT('Ctrl Pts',(-2.32067701661175,1.30587819461371,
13.857615680862));
#430967=CARTESIAN_POINT('Ctrl Pts',(-2.32038803438958,1.30693605981437,
13.8571944833187));
#430968=CARTESIAN_POINT('Ctrl Pts',(-2.31966684969946,1.30957607061221,
13.8561433417727));
#430969=CARTESIAN_POINT('Ctrl Pts',(-2.31932703085426,1.31213460987516,
13.8546163505474));
#430970=CARTESIAN_POINT('Ctrl Pts',(-2.31923195901678,1.31445645788808,
13.8528973491086));
#430971=CARTESIAN_POINT('Ctrl Pts',(-2.31921459079473,1.31488062526437,
13.8525833129072));
#430972=CARTESIAN_POINT('Ctrl Pts',(-2.31920526282451,1.31529695343186,
13.8522628768812));
#430973=CARTESIAN_POINT('Ctrl Pts',(-2.31920299418043,1.31570459642078,
13.851937733538));
#430974=CARTESIAN_POINT('Ctrl Pts',(-2.31918913988576,1.31819401559622,
13.8499521282529));
#430975=CARTESIAN_POINT('Ctrl Pts',(-2.31944125569959,1.32060695598612,
13.847639871647));
#430976=CARTESIAN_POINT('Ctrl Pts',(-2.31986618563574,1.32282495130311,
13.8452109780794));
#430977=CARTESIAN_POINT('Ctrl Pts',(-2.32005737040963,1.32382287330644,
13.8441181685877));
#430978=CARTESIAN_POINT('Ctrl Pts',(-2.32028292296854,1.32478170336765,
13.8430021611332));
#430979=CARTESIAN_POINT('Ctrl Pts',(-2.3205321928727,1.32569315312445,13.8418824960098));
#430980=CARTESIAN_POINT('Ctrl Pts',(-2.32111960376718,1.32784100775104,
13.8392439765549));
#430981=CARTESIAN_POINT('Ctrl Pts',(-2.32186315455302,1.32982942380178,
13.8364981347964));
#430982=CARTESIAN_POINT('Ctrl Pts',(-2.32273275881343,1.33167564574487,
13.8336931113419));
#430983=CARTESIAN_POINT('Ctrl Pts',(-2.32357969813809,1.3334737486715,13.8309611966328));
#430984=CARTESIAN_POINT('Ctrl Pts',(-2.32454756509587,1.33513853439016,
13.8281701127186));
#430985=CARTESIAN_POINT('Ctrl Pts',(-2.32563558959985,1.33665740036793,
13.8253580685121));
#430986=CARTESIAN_POINT('Ctrl Pts',(-2.32587147448655,1.33698669215113,
13.8247484142933));
#430987=CARTESIAN_POINT('Ctrl Pts',(-2.32611306775684,1.3373089630999,13.8241378483365));
#430988=CARTESIAN_POINT('Ctrl Pts',(-2.32636043968303,1.3376237760141,13.8235269408515));
#430989=CARTESIAN_POINT('',(-2.3234492810039,1.29949771088997,12.5969504640361));
#430990=CARTESIAN_POINT('Origin',(-2.35341812286521,1.31640147809467,12.584524458991));
#430991=CARTESIAN_POINT('Origin',(-2.35341812286521,1.31640147809467,12.584524458991));
#430992=CARTESIAN_POINT('Ctrl Pts',(-2.35734085275917,1.28223802992779,
12.5893111709658));
#430993=CARTESIAN_POINT('Ctrl Pts',(-2.34608202700252,1.2809351572782,12.5770542771492));
#430994=CARTESIAN_POINT('Ctrl Pts',(-2.34120305426881,1.29655563422094,
12.5737548217797));
#430995=CARTESIAN_POINT('Ctrl Pts',(-2.38196012611476,1.28508697515537,
12.5663937883685));
#430996=CARTESIAN_POINT('Ctrl Pts',(-2.37068693816224,1.28378244051078,
12.5540940315304));
#430997=CARTESIAN_POINT('Ctrl Pts',(-2.36579591163059,1.29945227952655,
12.5508374392248));
#430998=CARTESIAN_POINT('Ctrl Pts',(-2.40655455892536,1.28793304583215,
12.5434499600945));
#430999=CARTESIAN_POINT('Ctrl Pts',(-2.3952447178243,1.28662426968091,12.5311293540533));
#431000=CARTESIAN_POINT('Ctrl Pts',(-2.39036487926272,1.30234492298075,
12.5278936106989));
#431001=CARTESIAN_POINT('Ctrl Pts',(-2.43112609698477,1.29077646712561,
12.5204817579905));
#431002=CARTESIAN_POINT('Ctrl Pts',(-2.41976027989949,1.28946121342681,
12.5081597038247));
#431003=CARTESIAN_POINT('Ctrl Pts',(-2.41491181558899,1.30523386186405,
12.5049254088044));
#431004=CARTESIAN_POINT('Ctrl Pts',(-2.41346029074828,1.28873217793633,
12.5369868989719));
#431005=CARTESIAN_POINT('Ctrl Pts',(-2.41438562050889,1.28883925736877,
12.5342545179733));
#431006=CARTESIAN_POINT('Ctrl Pts',(-2.41525437306266,1.28906536821254,
12.5314872231885));
#431007=CARTESIAN_POINT('Ctrl Pts',(-2.416003529941,1.28945187187587,12.5287124745063));
#431008=CARTESIAN_POINT('Ctrl Pts',(-2.41667915679872,1.28980044006379,
12.5262100684184));
#431009=CARTESIAN_POINT('Ctrl Pts',(-2.41725637988353,1.29027998343836,
12.5237004536639));
#431010=CARTESIAN_POINT('Ctrl Pts',(-2.41770274919979,1.29094972592987,
12.5212220730815));
#431011=CARTESIAN_POINT('Ctrl Pts',(-2.41804448352542,1.29146247174446,
12.5193246583486));
#431012=CARTESIAN_POINT('Ctrl Pts',(-2.41831307764641,1.29209317755643,
12.517417831369));
#431013=CARTESIAN_POINT('Ctrl Pts',(-2.41842834966406,1.29289684232824,
12.5155812248348));
#431014=CARTESIAN_POINT('Ctrl Pts',(-2.41847745616316,1.29323920784074,
12.5147988205794));
#431015=CARTESIAN_POINT('Ctrl Pts',(-2.41849906174541,1.29361327026274,
12.5140295443047));
#431016=CARTESIAN_POINT('Ctrl Pts',(-2.41848887694232,1.29402421919219,
12.5132817086137));
#431017=CARTESIAN_POINT('Ctrl Pts',(-2.41847346362062,1.29464613480501,
12.5121499604604));
#431018=CARTESIAN_POINT('Ctrl Pts',(-2.41837775930793,1.29536578319234,
12.5110494206568));
#431019=CARTESIAN_POINT('Ctrl Pts',(-2.41816523153169,1.29619039465117,
12.5100666561695));
#431020=CARTESIAN_POINT('Ctrl Pts',(-2.41804319857198,1.29666388465191,
12.5095023550641));
#431021=CARTESIAN_POINT('Ctrl Pts',(-2.41788060649771,1.29717728912481,
12.5089719619137));
#431022=CARTESIAN_POINT('Ctrl Pts',(-2.41767441398901,1.29771905654383,
12.5085043804652));
#431023=CARTESIAN_POINT('Ctrl Pts',(-2.41737267811099,1.29851186259139,
12.5078201359221));
#431024=CARTESIAN_POINT('Ctrl Pts',(-2.41696769388149,1.29938797091034,
12.5072563000949));
#431025=CARTESIAN_POINT('Ctrl Pts',(-2.41647922856598,1.30028444200408,
12.5068768744332));
#431026=CARTESIAN_POINT('Ctrl Pts',(-2.41612701144742,1.30093085937595,
12.5066032824114));
#431027=CARTESIAN_POINT('Ctrl Pts',(-2.41572525396238,1.3015992494895,12.5064197834844));
#431028=CARTESIAN_POINT('Ctrl Pts',(-2.41529860673015,1.30225361936695,
12.5063282718343));
#431029=CARTESIAN_POINT('Ctrl Pts',(-2.41467583385773,1.30320879680022,
12.5061946931565));
#431030=CARTESIAN_POINT('Ctrl Pts',(-2.41398760724347,1.30415509728495,
12.5062515701262));
#431031=CARTESIAN_POINT('Ctrl Pts',(-2.41328914611601,1.30504288761613,
12.5064436508398));
#431032=CARTESIAN_POINT('',(-2.34120305426881,1.29655563422094,12.5737548217797));
#431033=CARTESIAN_POINT('Origin',(-2.35481188671965,1.30409219041889,12.5893111709658));
#431034=CARTESIAN_POINT('Ctrl Pts',(-2.41328914611601,1.30504288761613,
12.5064436508398));
#431035=CARTESIAN_POINT('Ctrl Pts',(-2.40261847550464,1.30378703075533,
12.5164271754438));
#431036=CARTESIAN_POINT('Ctrl Pts',(-2.39194359946346,1.30253046856967,
12.5264061185523));
#431037=CARTESIAN_POINT('Ctrl Pts',(-2.38126436977013,1.30127317715821,
12.536380305637));
#431038=CARTESIAN_POINT('Ctrl Pts',(-2.36791749863464,1.29970181790006,
12.5488460165097));
#431039=CARTESIAN_POINT('Ctrl Pts',(-2.35456382318511,1.29812931910801,
12.5613043021964));
#431040=CARTESIAN_POINT('Ctrl Pts',(-2.34120305426881,1.29655563422094,
12.5737548217797));
#431041=CARTESIAN_POINT('Ctrl Pts',(-2.32636043968303,1.33762377601409,
12.5893111709658));
#431042=CARTESIAN_POINT('Ctrl Pts',(-2.31935774413811,1.32871193615552,
12.5770542771492));
#431043=CARTESIAN_POINT('Ctrl Pts',(-2.33011456022597,1.31637927291894,
12.5737548217797));
#431044=CARTESIAN_POINT('Ctrl Pts',(-2.31982698564585,1.32930910693714,
12.5928319619712));
#431045=CARTESIAN_POINT('Ctrl Pts',(-2.31768228963815,1.32130700125139,
12.5821634970842));
#431046=CARTESIAN_POINT('Ctrl Pts',(-2.32772715933415,1.31335627203387,
12.5773203894503));
#431047=CARTESIAN_POINT('Ctrl Pts',(-2.31591438608324,1.31302182158929,
12.5969440695591));
#431048=CARTESIAN_POINT('Ctrl Pts',(-2.31786077267748,1.30950470319809,
12.5878292599214));
#431049=CARTESIAN_POINT('Ctrl Pts',(-2.32633461839298,1.3075506732857,12.5813877129824));
#431050=CARTESIAN_POINT('Ctrl Pts',(-2.33080401905962,1.28629217371711,
12.596957478804));
#431051=CARTESIAN_POINT('Ctrl Pts',(-2.32887208691935,1.28978333847323,
12.5878468778671));
#431052=CARTESIAN_POINT('Ctrl Pts',(-2.33166903558704,1.29798666463326,
12.5814011370086));
#431053=CARTESIAN_POINT('Ctrl Pts',(-2.34682121390122,1.28102069607358,
12.5928371701607));
#431054=CARTESIAN_POINT('Ctrl Pts',(-2.3388875204122,1.2833853468567,12.5821692192952));
#431055=CARTESIAN_POINT('Ctrl Pts',(-2.33736544129892,1.29610175740138,
12.5773318885715));
#431056=CARTESIAN_POINT('Ctrl Pts',(-2.35734085275918,1.28223802992773,
12.5893111709658));
#431057=CARTESIAN_POINT('Ctrl Pts',(-2.34608202700252,1.28093515727815,
12.5770542771492));
#431058=CARTESIAN_POINT('Ctrl Pts',(-2.34120305426881,1.29655563422088,
12.5737548217797));
#431059=CARTESIAN_POINT('',(-2.33011456022597,1.31637927291894,12.5737548217797));
#431060=CARTESIAN_POINT('Origin',(-2.34365893801224,1.32403105900996,12.5893111709658));
#431061=CARTESIAN_POINT('Ctrl Pts',(-2.34120305426881,1.29655563422088,
12.5737548217797));
#431062=CARTESIAN_POINT('Ctrl Pts',(-2.34021182714618,1.29640802520225,
12.5746934679442));
#431063=CARTESIAN_POINT('Ctrl Pts',(-2.33908798689128,1.29642587232275,
12.5756680099006));
#431064=CARTESIAN_POINT('Ctrl Pts',(-2.33795934173306,1.29660381550135,
12.5765688348656));
#431065=CARTESIAN_POINT('Ctrl Pts',(-2.33766054542194,1.29665092398799,
12.5768073183026));
#431066=CARTESIAN_POINT('Ctrl Pts',(-2.33736143532197,1.29670899703069,
12.5770407398754));
#431067=CARTESIAN_POINT('Ctrl Pts',(-2.33706429063648,1.29677737962196,
12.5772674179684));
#431068=CARTESIAN_POINT('Ctrl Pts',(-2.33584488919855,1.29705800328511,
12.5781976435658));
#431069=CARTESIAN_POINT('Ctrl Pts',(-2.33459185723495,1.29753917724634,
12.5790594849312));
#431070=CARTESIAN_POINT('Ctrl Pts',(-2.33340711238151,1.29823349155264,
12.5797571720116));
#431071=CARTESIAN_POINT('Ctrl Pts',(-2.33263520850987,1.29868586228851,
12.580211740231));
#431072=CARTESIAN_POINT('Ctrl Pts',(-2.33186670521922,1.29926546531869,
12.5806009430798));
#431073=CARTESIAN_POINT('Ctrl Pts',(-2.33116636977431,1.29994564391944,
12.5808812374708));
#431074=CARTESIAN_POINT('Ctrl Pts',(-2.33056454929326,1.30053014298438,
12.5811221033394));
#431075=CARTESIAN_POINT('Ctrl Pts',(-2.33000082607617,1.30120096031213,
12.581287365893));
#431076=CARTESIAN_POINT('Ctrl Pts',(-2.32951340089355,1.30192559813532,
12.581359338449));
#431077=CARTESIAN_POINT('Ctrl Pts',(-2.32944565885811,1.30202630782955,
12.5813693411482));
#431078=CARTESIAN_POINT('Ctrl Pts',(-2.32937933255776,1.30212804213074,
12.5813775999465));
#431079=CARTESIAN_POINT('Ctrl Pts',(-2.32931446487782,1.30223069954053,
12.5813841266931));
#431080=CARTESIAN_POINT('Ctrl Pts',(-2.32920440901323,1.3024048702524,12.5813952001081));
#431081=CARTESIAN_POINT('Ctrl Pts',(-2.32909832944188,1.30258318991104,
12.5814007534795));
#431082=CARTESIAN_POINT('Ctrl Pts',(-2.32899644185222,1.30276568167775,
12.5814005856065));
#431083=CARTESIAN_POINT('Ctrl Pts',(-2.32853004030221,1.30360105763613,
12.5813998171494));
#431084=CARTESIAN_POINT('Ctrl Pts',(-2.32818340973398,1.30446597546451,
12.58127954464));
#431085=CARTESIAN_POINT('Ctrl Pts',(-2.3279310523309,1.30534451735209,12.5810700125799));
#431086=CARTESIAN_POINT('Ctrl Pts',(-2.32762623332117,1.30640569592229,
12.5808169217085));
#431087=CARTESIAN_POINT('Ctrl Pts',(-2.32747501580929,1.30749146828497,
12.5804173076348));
#431088=CARTESIAN_POINT('Ctrl Pts',(-2.32746485883118,1.30850308689069,
12.5799304713245));
#431089=CARTESIAN_POINT('Ctrl Pts',(-2.32745227113552,1.30975680103591,
12.5793271277669));
#431090=CARTESIAN_POINT('Ctrl Pts',(-2.32762335901736,1.3109740691843,12.5785808224116));
#431091=CARTESIAN_POINT('Ctrl Pts',(-2.32793950264364,1.31210799557987,
12.5777485681082));
#431092=CARTESIAN_POINT('Ctrl Pts',(-2.32841059128292,1.31379767014018,
12.576508418016));
#431093=CARTESIAN_POINT('Ctrl Pts',(-2.32919317907541,1.31528990867935,
12.5750928681475));
#431094=CARTESIAN_POINT('Ctrl Pts',(-2.33011456022597,1.31637927291894,
12.5737548217797));
#431095=CARTESIAN_POINT('Ctrl Pts',(-2.33011456022597,1.31637927291894,
12.5737548217797));
#431096=CARTESIAN_POINT('Ctrl Pts',(-2.31935774413811,1.32871193615552,
12.5770542771492));
#431097=CARTESIAN_POINT('Ctrl Pts',(-2.32636043968303,1.3376237760141,12.5893111709658));
#431098=CARTESIAN_POINT('Ctrl Pts',(-2.34545162098595,1.33581608133531,
12.5508408821982));
#431099=CARTESIAN_POINT('Ctrl Pts',(-2.33465905500726,1.3481848421554,12.55409748406));
#431100=CARTESIAN_POINT('Ctrl Pts',(-2.3416706841982,1.35710805123919,12.5663972313419));
#431101=CARTESIAN_POINT('Ctrl Pts',(-2.36077277340999,1.35523463308848,
12.52790050457));
#431102=CARTESIAN_POINT('Ctrl Pts',(-2.34993106022407,1.36762045290534,
12.5311362602938));
#431103=CARTESIAN_POINT('Ctrl Pts',(-2.35696548319246,1.37657267003228,
12.5434568539655));
#431104=CARTESIAN_POINT('Ctrl Pts',(-2.37607924290869,1.37463635553372,
12.5049357605811));
#431105=CARTESIAN_POINT('Ctrl Pts',(-2.36517681475302,1.38702265624458,
12.5081700652078));
#431106=CARTESIAN_POINT('Ctrl Pts',(-2.37224604636214,1.39601917188909,
12.5204921097672));
#431107=CARTESIAN_POINT('Ctrl Pts',(-2.37507415887584,1.37336236336858,
12.5064436508395));
#431108=CARTESIAN_POINT('Ctrl Pts',(-2.37465187301338,1.37450714388944,
12.5062361689309));
#431109=CARTESIAN_POINT('Ctrl Pts',(-2.374163914289,1.37567961474355,12.5061871075061));
#431110=CARTESIAN_POINT('Ctrl Pts',(-2.37362856535138,1.37678614904312,
12.5063648335164));
#431111=CARTESIAN_POINT('Ctrl Pts',(-2.37338537684222,1.37728880517584,
12.5064455676329));
#431112=CARTESIAN_POINT('Ctrl Pts',(-2.37312881889141,1.37778477011569,
12.506574497099));
#431113=CARTESIAN_POINT('Ctrl Pts',(-2.37286895848143,1.37825229550728,
12.5067492519495));
#431114=CARTESIAN_POINT('Ctrl Pts',(-2.37234675890051,1.37919180592974,
12.5071004286051));
#431115=CARTESIAN_POINT('Ctrl Pts',(-2.37179131735987,1.3800506202677,12.5076537929613));
#431116=CARTESIAN_POINT('Ctrl Pts',(-2.37125226479469,1.38076941660765,
12.5083435010505));
#431117=CARTESIAN_POINT('Ctrl Pts',(-2.37121832821432,1.3808146691328,12.5083869222964));
#431118=CARTESIAN_POINT('Ctrl Pts',(-2.37118444334185,1.38085936447729,
12.5084308732337));
#431119=CARTESIAN_POINT('Ctrl Pts',(-2.3711506171009,1.38090348732261,12.5084753333615));
#431120=CARTESIAN_POINT('Ctrl Pts',(-2.37087928600183,1.38125741077894,
12.5088319622689));
#431121=CARTESIAN_POINT('Ctrl Pts',(-2.3706072427105,1.38158246887616,12.509227847131));
#431122=CARTESIAN_POINT('Ctrl Pts',(-2.37034472377393,1.38187079301739,
12.5096423454524));
#431123=CARTESIAN_POINT('Ctrl Pts',(-2.36952210561275,1.38277427326909,
12.5109411997424));
#431124=CARTESIAN_POINT('Ctrl Pts',(-2.36874956172666,1.3833791352647,12.5124831113042));
#431125=CARTESIAN_POINT('Ctrl Pts',(-2.36805057734202,1.38377705398192,
12.5140723025008));
#431126=CARTESIAN_POINT('Ctrl Pts',(-2.36798508173961,1.38381433940156,
12.5142212114565));
#431127=CARTESIAN_POINT('Ctrl Pts',(-2.36792022877725,1.38384983731474,
12.5143705582413));
#431128=CARTESIAN_POINT('Ctrl Pts',(-2.36785603748264,1.38388364012108,
12.5145201959299));
#431129=CARTESIAN_POINT('Ctrl Pts',(-2.36703140473243,1.3843178874957,12.5164425148273));
#431130=CARTESIAN_POINT('Ctrl Pts',(-2.36629271696646,1.38449676780137,
12.5184635205941));
#431131=CARTESIAN_POINT('Ctrl Pts',(-2.36561364789958,1.38450656490253,
12.5205025929158));
#431132=CARTESIAN_POINT('Ctrl Pts',(-2.365219760925,1.38451224760952,12.5216853356836));
#431133=CARTESIAN_POINT('Ctrl Pts',(-2.36484665091736,1.38446151619183,
12.5228750347131));
#431134=CARTESIAN_POINT('Ctrl Pts',(-2.3644949366336,1.38437260662455,12.5240609649613));
#431135=CARTESIAN_POINT('Ctrl Pts',(-2.36363167279295,1.3841543828615,12.5269717671326));
#431136=CARTESIAN_POINT('Ctrl Pts',(-2.36287555540805,1.38368994181205,
12.5299036066169));
#431137=CARTESIAN_POINT('Ctrl Pts',(-2.36219369101421,1.3830594554327,12.5328133004019));
#431138=CARTESIAN_POINT('Ctrl Pts',(-2.36186635640138,1.38275678525848,
12.5342101228451));
#431139=CARTESIAN_POINT('Ctrl Pts',(-2.3615568980478,1.38241584181146,12.5356023438238));
#431140=CARTESIAN_POINT('Ctrl Pts',(-2.36126526429652,1.38204470010705,
12.5369868989719));
#431141=CARTESIAN_POINT('Origin',(-10.2316378295468,11.4066885757328,-1.23974187479773));
#431142=CARTESIAN_POINT('Ctrl Pts',(-2.41341877811849,1.28872733412586,
12.5369868989719));
#431143=CARTESIAN_POINT('Ctrl Pts',(-2.42865266524063,1.29051953579836,
12.5369868989719));
#431144=CARTESIAN_POINT('Ctrl Pts',(-2.43560194861504,1.27684507916319,
12.5369868989719));
#431145=CARTESIAN_POINT('Ctrl Pts',(-2.41856843549576,1.28933310262533,
12.5218025310015));
#431146=CARTESIAN_POINT('Ctrl Pts',(-2.43022092785154,1.28736452811494,
12.5216901060417));
#431147=CARTESIAN_POINT('Ctrl Pts',(-2.43558077959844,1.27688677091039,
12.5161920673678));
#431148=CARTESIAN_POINT('Ctrl Pts',(-2.42148857846681,1.29460651103199,
12.5042015548895));
#431149=CARTESIAN_POINT('Ctrl Pts',(-2.42752167704109,1.2923751288124,12.4980677368514));
#431150=CARTESIAN_POINT('Ctrl Pts',(-2.43071015502069,1.2863730968317,12.4907278922777));
#431151=CARTESIAN_POINT('Ctrl Pts',(-2.4132715527434,1.3050333735978,12.506463626192));
#431152=CARTESIAN_POINT('Ctrl Pts',(-2.41902668217186,1.30814559524769,
12.4999376786891));
#431153=CARTESIAN_POINT('Ctrl Pts',(-2.41895639163384,1.30810758398541,
12.4906970594712));
#431154=CARTESIAN_POINT('Origin',(-2.4159892567878,1.26687801744522,12.5369868989719));
#431155=CARTESIAN_POINT('Origin',(-2.4159892567878,1.26687801744522,14.));
#431156=CARTESIAN_POINT('Origin',(-2.4159892567878,1.26687801744522,13.7435492065112));
#431157=CARTESIAN_POINT('Ctrl Pts',(-2.38886432632103,1.28588590268799,
13.793642941384));
#431158=CARTESIAN_POINT('Ctrl Pts',(-2.3996018053748,1.28715584858276,13.8071662555867));
#431159=CARTESIAN_POINT('Ctrl Pts',(-2.40406680098607,1.27072164042337,
13.8103758687955));
#431160=CARTESIAN_POINT('Ctrl Pts',(-2.40537526568099,1.287796553539,13.7804579775006));
#431161=CARTESIAN_POINT('Ctrl Pts',(-2.41862553539282,1.28935348137683,
13.7901904343351));
#431162=CARTESIAN_POINT('Ctrl Pts',(-2.42516220096345,1.27501723614377,
13.7927914348262));
#431163=CARTESIAN_POINT('Ctrl Pts',(-2.41509587706315,1.28892142556309,
13.7597120340895));
#431164=CARTESIAN_POINT('Ctrl Pts',(-2.43043083937317,1.29071753828875,
13.7635825532445));
#431165=CARTESIAN_POINT('Ctrl Pts',(-2.43760723472565,1.27752529564813,
13.7651073818884));
#431166=CARTESIAN_POINT('Ctrl Pts',(-2.41319235877791,1.28870114986332,
13.7381884353898));
#431167=CARTESIAN_POINT('Ctrl Pts',(-2.42816827316289,1.29045611395404,
13.7368803041982));
#431168=CARTESIAN_POINT('Ctrl Pts',(-2.43517022495231,1.27703365858039,
13.7363986145813));
#431169=CARTESIAN_POINT('Origin',(-2.39539963927866,1.26449538446929,13.7902182540695));
#431170=CARTESIAN_POINT('Ctrl Pts',(-2.35733694274133,1.28223757669607,
13.8235227101244));
#431171=CARTESIAN_POINT('Ctrl Pts',(-2.36875729040384,1.28356360368931,
13.8358800583119));
#431172=CARTESIAN_POINT('Ctrl Pts',(-2.37359169323221,1.26771259115543,
13.8390832900376));
#431173=CARTESIAN_POINT('Ctrl Pts',(-2.36918545335587,1.28360868774612,
13.8124254819053));
#431174=CARTESIAN_POINT('Ctrl Pts',(-2.38062797920374,1.28493728958868,
13.8247886449157));
#431175=CARTESIAN_POINT('Ctrl Pts',(-2.38545218759861,1.26906127640952,
13.8279860620657));
#431176=CARTESIAN_POINT('Ctrl Pts',(-2.38102865385343,1.28497918430881,
13.8013225099955));
#431177=CARTESIAN_POINT('Ctrl Pts',(-2.39248795862072,1.28630973610524,
13.8136962257787));
#431178=CARTESIAN_POINT('Ctrl Pts',(-2.39730716051433,1.27040960660921,
13.8168830918626));
#431179=CARTESIAN_POINT('Ctrl Pts',(-2.39286675084249,1.28634909029291,
13.7902140179785));
#431180=CARTESIAN_POINT('Ctrl Pts',(-2.4043377881453,1.28768100798631,13.802602731458));
#431181=CARTESIAN_POINT('Ctrl Pts',(-2.40915682872264,1.27175759753393,
13.8057746032558));
#431182=CARTESIAN_POINT('Origin',(-2.3598698187987,1.26038386943668,13.8235269408515));
#431183=CARTESIAN_POINT('Ctrl Pts',(-2.32636043968303,1.3376237760141,13.8235269408515));
#431184=CARTESIAN_POINT('Ctrl Pts',(-2.33365570123877,1.34690794413108,
13.8362179249168));
#431185=CARTESIAN_POINT('Ctrl Pts',(-2.32211071702631,1.35949271046151,
13.8391868794938));
#431186=CARTESIAN_POINT('Ctrl Pts',(-2.31968559290336,1.32912916630282,
13.8400110824519));
#431187=CARTESIAN_POINT('Ctrl Pts',(-2.32284469250289,1.33868646469628,
13.8494522556836));
#431188=CARTESIAN_POINT('Ctrl Pts',(-2.31121414932101,1.34544356116811,
13.85569149686));
#431189=CARTESIAN_POINT('Ctrl Pts',(-2.31574597041812,1.31332166489626,
13.8586819406588));
#431190=CARTESIAN_POINT('Ctrl Pts',(-2.31363267167181,1.31712823974037,
13.868010383617));
#431191=CARTESIAN_POINT('Ctrl Pts',(-2.30481596404009,1.3191674879669,13.8744918421245));
#431192=CARTESIAN_POINT('Ctrl Pts',(-2.33097503050985,1.28598767092046,
13.8587686893867));
#431193=CARTESIAN_POINT('Ctrl Pts',(-2.33306947168661,1.2822149472257,13.8680909899357));
#431194=CARTESIAN_POINT('Ctrl Pts',(-2.33017012447703,1.27366566729906,
13.8745789365163));
#431195=CARTESIAN_POINT('Ctrl Pts',(-2.34659167413014,1.28099413369755,
13.8400379222776));
#431196=CARTESIAN_POINT('Ctrl Pts',(-2.35638474272802,1.2786776619526,13.8494748685453));
#431197=CARTESIAN_POINT('Ctrl Pts',(-2.35605673380427,1.26523692107231,
13.8557104837033));
#431198=CARTESIAN_POINT('Ctrl Pts',(-2.35734085275979,1.28223802992121,
13.8235269408542));
#431199=CARTESIAN_POINT('Ctrl Pts',(-2.36907006163061,1.2835953353604,13.8362179249195));
#431200=CARTESIAN_POINT('Ctrl Pts',(-2.37375135115599,1.26717131233205,
13.8391868794965));
#431201=CARTESIAN_POINT('Origin',(-2.30906194135383,1.35121649301823,13.8235269408515));
#431202=CARTESIAN_POINT('Ctrl Pts',(-2.34845662328262,1.36574404157119,
13.7902140241682));
#431203=CARTESIAN_POINT('Ctrl Pts',(-2.35559512507335,1.37482150749381,
13.8026027327198));
#431204=CARTESIAN_POINT('Ctrl Pts',(-2.34454881511321,1.38726164288447,
13.8057746032556));
#431205=CARTESIAN_POINT('Ctrl Pts',(-2.34109363615993,1.35637368386972,
13.8013225161808));
#431206=CARTESIAN_POINT('Ctrl Pts',(-2.34822483363906,1.36544186728202,
13.8136962270464));
#431207=CARTESIAN_POINT('Ctrl Pts',(-2.33719844595753,1.37786995563101,
13.8168830918628));
#431208=CARTESIAN_POINT('Ctrl Pts',(-2.33372747478725,1.34699928652274,
13.8124254880875));
#431209=CARTESIAN_POINT('Ctrl Pts',(-2.34084822916302,1.35605419304686,
13.8247886461867));
#431210=CARTESIAN_POINT('Ctrl Pts',(-2.32984501138987,1.36847392576679,
13.8279860620656));
#431211=CARTESIAN_POINT('Ctrl Pts',(-2.32635801065852,1.33762068598958,
13.8235227163065));
#431212=CARTESIAN_POINT('Ctrl Pts',(-2.33346496365344,1.3466580419284,13.8358800595848));
#431213=CARTESIAN_POINT('Ctrl Pts',(-2.32248838452712,1.35907337686072,
13.8390832900376));
#431214=CARTESIAN_POINT('Origin',(-2.33116056166863,1.37933985838199,13.7902182540695));
#431215=CARTESIAN_POINT('Ctrl Pts',(-2.36109850945796,1.38183252755633,
13.7382347919292));
#431216=CARTESIAN_POINT('Ctrl Pts',(-2.37044093715816,1.39368313570106,
13.7369371795942));
#431217=CARTESIAN_POINT('Ctrl Pts',(-2.36265505647251,1.40668020610054,
13.7364597369711));
#431218=CARTESIAN_POINT('Ctrl Pts',(-2.36226721072488,1.38331985110314,
13.7595490285574));
#431219=CARTESIAN_POINT('Ctrl Pts',(-2.37183175116987,1.39545382705888,
13.7633824266926));
#431220=CARTESIAN_POINT('Ctrl Pts',(-2.36432895367105,1.4084769484205,13.7648920890506));
#431221=CARTESIAN_POINT('Ctrl Pts',(-2.35630689829647,1.37573458249166,
13.780380659011));
#431222=CARTESIAN_POINT('Ctrl Pts',(-2.36458412313523,1.38622669548064,
13.7901039518744));
#431223=CARTESIAN_POINT('Ctrl Pts',(-2.35579795950558,1.39931442905445,
13.7926933640892));
#431224=CARTESIAN_POINT('Ctrl Pts',(-2.34594654472624,1.36254969244765,
13.7936647693663));
#431225=CARTESIAN_POINT('Ctrl Pts',(-2.35265240347727,1.37103525609161,
13.8072068914933));
#431226=CARTESIAN_POINT('Ctrl Pts',(-2.34096528964321,1.38344717133773,
13.8104111085397));
#431227=CARTESIAN_POINT('Origin',(-2.34396676596731,1.39563741711118,13.7435492065112));
#431228=CARTESIAN_POINT('Origin',(-2.34396676596731,1.39563741711118,14.));
#431229=CARTESIAN_POINT('Origin',(-2.34396676596731,1.39563741711118,12.5369868989719));
#431230=CARTESIAN_POINT('Ctrl Pts',(-2.37505824466421,1.37335316112641,
12.506462012331));
#431231=CARTESIAN_POINT('Ctrl Pts',(-2.38071867661695,1.37662624806359,
12.4999388158272));
#431232=CARTESIAN_POINT('Ctrl Pts',(-2.38065170628375,1.37658752315273,
12.4907030323752));
#431233=CARTESIAN_POINT('Ctrl Pts',(-2.37047222175398,1.38581096900024,
12.5042014951932));
#431234=CARTESIAN_POINT('Ctrl Pts',(-2.37172876299148,1.39211669665329,
12.4980716682127));
#431235=CARTESIAN_POINT('Ctrl Pts',(-2.36828692406589,1.39797155019853,
12.4907355092744));
#431236=CARTESIAN_POINT('Ctrl Pts',(-2.3644513710313,1.38608493582388,12.5218047446509));
#431237=CARTESIAN_POINT('Ctrl Pts',(-2.36886926496384,1.39703943645774,
12.5216906929434));
#431238=CARTESIAN_POINT('Ctrl Pts',(-2.36275256495378,1.40708715934986,
12.5161988840775));
#431239=CARTESIAN_POINT('Ctrl Pts',(-2.36124150249871,1.38201451441863,
12.5369868989719));
#431240=CARTESIAN_POINT('Ctrl Pts',(-2.37073412075248,1.39405177865136,
12.5369868989719));
#431241=CARTESIAN_POINT('Ctrl Pts',(-2.36272902539233,1.40712556845369,
12.5369868989719));
#431242=CARTESIAN_POINT('Origin',(-4.49626278878395E-31,-2.63684586248252E-31,
12.5));
#431243=CARTESIAN_POINT('Origin',(-2.42764842286964,1.14355297053481,12.5));
#431244=CARTESIAN_POINT('',(-2.42764842286964,1.14355297053481,12.5893111709658));
#431245=CARTESIAN_POINT('',(-2.42764842286964,1.14355297053481,13.8235269408515));
#431246=CARTESIAN_POINT('',(-2.42764842286964,1.14355297053481,12.5));
#431247=CARTESIAN_POINT('',(-2.45196582721009,1.1697815150111,13.7902182540695));
#431248=CARTESIAN_POINT('',(-2.42764842286964,1.14355297053481,13.8235269408515));
#431249=CARTESIAN_POINT('',(-2.46605782225598,1.18498102042073,13.7435492065112));
#431250=CARTESIAN_POINT('Origin',(-2.41969558370818,1.13497462705725,13.7445212918713));
#431251=CARTESIAN_POINT('',(-2.46605782225598,1.18498102042073,12.5369868989719));
#431252=CARTESIAN_POINT('',(-2.46605782225598,1.18498102042073,12.5));
#431253=CARTESIAN_POINT('Ctrl Pts',(-2.46605782225598,1.18498102042073,
12.5369868989719));
#431254=CARTESIAN_POINT('Ctrl Pts',(-2.4532640269538,1.17118174215871,12.5544431401645));
#431255=CARTESIAN_POINT('Ctrl Pts',(-2.44046108118918,1.15737259428612,
12.5718848856037));
#431256=CARTESIAN_POINT('Ctrl Pts',(-2.42764842286964,1.14355297053481,
12.5893111709658));
#431257=CARTESIAN_POINT('Origin',(-2.72885600850611,1.09506675154452,12.5));
#431258=CARTESIAN_POINT('',(-2.51047333723491,1.08772460875899,13.7435492065112));
#431259=CARTESIAN_POINT('',(-2.48975802327268,1.08702814876941,13.7902182540695));
#431260=CARTESIAN_POINT('Origin',(-2.4353217585087,1.08519797228937,13.7418732680457));
#431261=CARTESIAN_POINT('',(-2.45401129869476,1.08582632467577,13.8235269408515));
#431262=CARTESIAN_POINT('',(-2.48975802327268,1.08702814876941,13.7902182540695));
#431263=CARTESIAN_POINT('',(-2.45401129869476,1.08582632467577,12.5893111709658));
#431264=CARTESIAN_POINT('',(-2.45401129869476,1.08582632467577,12.5));
#431265=CARTESIAN_POINT('',(-2.51047333723491,1.08772460875899,12.5369868989719));
#431266=CARTESIAN_POINT('Ctrl Pts',(-2.45401129869476,1.08582632467577,
12.5893111709658));
#431267=CARTESIAN_POINT('Ctrl Pts',(-2.47284598029348,1.08645955679448,
12.5718848856037));
#431268=CARTESIAN_POINT('Ctrl Pts',(-2.49166638438046,1.08709230889557,
12.5544431401645));
#431269=CARTESIAN_POINT('Ctrl Pts',(-2.51047333723491,1.08772460875899,
12.5369868989719));
#431270=CARTESIAN_POINT('',(-2.51047333723491,1.08772460875899,12.5));
#431271=CARTESIAN_POINT('Origin',(-2.45285624533617,1.12018191340219,12.5));
#431272=CARTESIAN_POINT('',(-2.42113982516251,1.10692827754081,13.8587068136939));
#431273=CARTESIAN_POINT('Ctrl Pts',(-2.45401129869484,1.08582632466916,
13.8235269408542));
#431274=CARTESIAN_POINT('Ctrl Pts',(-2.45225998987588,1.08576744472537,
13.8262006681044));
#431275=CARTESIAN_POINT('Ctrl Pts',(-2.45046194326886,1.08588083092831,
13.8288634856214));
#431276=CARTESIAN_POINT('Ctrl Pts',(-2.44862203900277,1.08615407399156,
13.8314912288862));
#431277=CARTESIAN_POINT('Ctrl Pts',(-2.44672528748175,1.08643575940605,
13.8342001611531));
#431278=CARTESIAN_POINT('Ctrl Pts',(-2.44478187198945,1.08688715382095,
13.8368750301949));
#431279=CARTESIAN_POINT('Ctrl Pts',(-2.44278365182638,1.08753780372501,
13.8394886372968));
#431280=CARTESIAN_POINT('Ctrl Pts',(-2.44262932443618,1.08758805499536,
13.8396904925131));
#431281=CARTESIAN_POINT('Ctrl Pts',(-2.4424746732709,1.08763951672092,13.8398919674349));
#431282=CARTESIAN_POINT('Ctrl Pts',(-2.44231969718439,1.08769221365696,
13.8400930404591));
#431283=CARTESIAN_POINT('Ctrl Pts',(-2.43990506549373,1.0885132673732,13.8432258934518));
#431284=CARTESIAN_POINT('Ctrl Pts',(-2.43742351542761,1.08962892240605,
13.8462331177034));
#431285=CARTESIAN_POINT('Ctrl Pts',(-2.43499553741713,1.09109077560807,
13.8489036603661));
#431286=CARTESIAN_POINT('Ctrl Pts',(-2.43420107475631,1.09156911098822,
13.8497774930041));
#431287=CARTESIAN_POINT('Ctrl Pts',(-2.43341259768076,1.09208452235582,
13.85061494757));
#431288=CARTESIAN_POINT('Ctrl Pts',(-2.43263504113365,1.09263883232474,
13.8514076489583));
#431289=CARTESIAN_POINT('Ctrl Pts',(-2.4309903968961,1.09381127785246,13.8530843267192));
#431290=CARTESIAN_POINT('Ctrl Pts',(-2.42923477898703,1.09527532288743,
13.8546805203176));
#431291=CARTESIAN_POINT('Ctrl Pts',(-2.42755746953222,1.09705078503298,
13.8559412814273));
#431292=CARTESIAN_POINT('Ctrl Pts',(-2.42733299113072,1.09728839944766,
13.8561100121513));
#431293=CARTESIAN_POINT('Ctrl Pts',(-2.42710990696846,1.09753151532451,
13.8562727473908));
#431294=CARTESIAN_POINT('Ctrl Pts',(-2.42688865315478,1.09778010639366,
13.8564289040185));
#431295=CARTESIAN_POINT('Ctrl Pts',(-2.42588526963393,1.09890746405619,
13.8571370725437));
#431296=CARTESIAN_POINT('Ctrl Pts',(-2.42490359306482,1.10016875444836,
13.8577210840554));
#431297=CARTESIAN_POINT('Ctrl Pts',(-2.42400494134343,1.10153297664135,
13.8581177131616));
#431298=CARTESIAN_POINT('Ctrl Pts',(-2.42375185008804,1.101917188566,13.8582294175695));
#431299=CARTESIAN_POINT('Ctrl Pts',(-2.42350521788678,1.10230943995882,
13.8583265086086));
#431300=CARTESIAN_POINT('Ctrl Pts',(-2.42326608400721,1.10270874845725,
13.8584082369006));
#431301=CARTESIAN_POINT('Ctrl Pts',(-2.42292251274854,1.10328244769071,
13.8585256585398));
#431302=CARTESIAN_POINT('Ctrl Pts',(-2.42259042551756,1.10387801275165,
13.8586122832068));
#431303=CARTESIAN_POINT('Ctrl Pts',(-2.42227913868915,1.10448035716898,
13.8586682984299));
#431304=CARTESIAN_POINT('Ctrl Pts',(-2.4220301400833,1.10496217299436,13.8587131050557));
#431305=CARTESIAN_POINT('Ctrl Pts',(-2.42179149193538,1.10545354053934,
13.8587357943552));
#431306=CARTESIAN_POINT('Ctrl Pts',(-2.4215636214456,1.10595473944802,13.8587355499465));
#431307=CARTESIAN_POINT('Ctrl Pts',(-2.42141634331542,1.10627867625174,
13.8587353919793));
#431308=CARTESIAN_POINT('Ctrl Pts',(-2.42127512482626,1.10660320094039,
13.8587257282814));
#431309=CARTESIAN_POINT('Ctrl Pts',(-2.42113982516251,1.10692827754081,
13.8587068136939));
#431310=CARTESIAN_POINT('Ctrl Pts',(-2.42113982516251,1.10692827754081,
13.8587068136939));
#431311=CARTESIAN_POINT('Ctrl Pts',(-2.42069483194421,1.10799743675823,
13.8586446046466));
#431312=CARTESIAN_POINT('Ctrl Pts',(-2.42031378439166,1.10907255944393,
13.858482427929));
#431313=CARTESIAN_POINT('Ctrl Pts',(-2.41999237636932,1.11015244428447,
13.8582284286032));
#431314=CARTESIAN_POINT('Ctrl Pts',(-2.41966264912614,1.1112602805134,13.8579678548414));
#431315=CARTESIAN_POINT('Ctrl Pts',(-2.41939635132405,1.11237627168034,
13.857615680862));
#431316=CARTESIAN_POINT('Ctrl Pts',(-2.41919455650097,1.1134541716557,13.8571944833187));
#431317=CARTESIAN_POINT('Ctrl Pts',(-2.41869095688211,1.1161441812828,13.8561433417727));
#431318=CARTESIAN_POINT('Ctrl Pts',(-2.41856081345834,1.11872190560802,
13.8546163505474));
#431319=CARTESIAN_POINT('Ctrl Pts',(-2.41865531013259,1.12104377710058,
13.8528973491086));
#431320=CARTESIAN_POINT('Ctrl Pts',(-2.41867257328081,1.12146794876624,
13.8525833129072));
#431321=CARTESIAN_POINT('Ctrl Pts',(-2.4186972109593,1.12188365195227,13.8522628768812));
#431322=CARTESIAN_POINT('Ctrl Pts',(-2.41872817655191,1.12229012345833,
13.851937733538));
#431323=CARTESIAN_POINT('Ctrl Pts',(-2.4189172791297,1.12477238855045,13.8499521282529));
#431324=CARTESIAN_POINT('Ctrl Pts',(-2.41936523309139,1.12715675030091,
13.847639871647));
#431325=CARTESIAN_POINT('Ctrl Pts',(-2.41996953631742,1.1293327296868,13.8452109780794));
#431326=CARTESIAN_POINT('Ctrl Pts',(-2.42024142484727,1.13031174785304,
13.8441181685877));
#431327=CARTESIAN_POINT('Ctrl Pts',(-2.42054438044999,1.13124900285884,
13.8430021611332));
#431328=CARTESIAN_POINT('Ctrl Pts',(-2.42086711254577,1.13213710203047,
13.8418824960098));
#431329=CARTESIAN_POINT('Ctrl Pts',(-2.42162763897073,1.13422993040682,
13.8392439765549));
#431330=CARTESIAN_POINT('Ctrl Pts',(-2.42253079002036,1.13615112387534,
13.8364981347964));
#431331=CARTESIAN_POINT('Ctrl Pts',(-2.42354798497218,1.13792032184698,
13.8336931113419));
#431332=CARTESIAN_POINT('Ctrl Pts',(-2.4245386682574,1.1396434083169,13.8309611966328));
#431333=CARTESIAN_POINT('Ctrl Pts',(-2.4256390102089,1.1412237644561,13.8281701127186));
#431334=CARTESIAN_POINT('Ctrl Pts',(-2.42684721607875,1.14264889243483,
13.8253580685121));
#431335=CARTESIAN_POINT('Ctrl Pts',(-2.42710915641527,1.14295786171868,
13.8247484142933));
#431336=CARTESIAN_POINT('Ctrl Pts',(-2.42737621387803,1.14325936824308,
13.8241378483365));
#431337=CARTESIAN_POINT('Ctrl Pts',(-2.42764842286964,1.14355297053481,
13.8235269408515));
#431338=CARTESIAN_POINT('',(-2.4216393225781,1.10579105320548,12.5969504640361));
#431339=CARTESIAN_POINT('Origin',(-2.45288625954449,1.12019583569037,12.584524458991));
#431340=CARTESIAN_POINT('Origin',(-2.45288625954449,1.12019583569037,12.584524458991));
#431341=CARTESIAN_POINT('Ctrl Pts',(-2.45401129869476,1.08582632467577,
12.5893111709658));
#431342=CARTESIAN_POINT('Ctrl Pts',(-2.44268373953581,1.08544548604845,
12.5770542771492));
#431343=CARTESIAN_POINT('Ctrl Pts',(-2.43909421506564,1.10141166871473,
12.5737548217797));
#431344=CARTESIAN_POINT('Ctrl Pts',(-2.47878086893348,1.08665909094047,
12.5663937883685));
#431345=CARTESIAN_POINT('Ctrl Pts',(-2.46743885989968,1.08627776650061,
12.5540940315303));
#431346=CARTESIAN_POINT('Ctrl Pts',(-2.46384134520686,1.10229412948815,
12.5508374392248));
#431347=CARTESIAN_POINT('Ctrl Pts',(-2.50352544697966,1.08749101695422,
12.5434499600945));
#431348=CARTESIAN_POINT('Ctrl Pts',(-2.49214656103544,1.0871084526928,12.5311293540533));
#431349=CARTESIAN_POINT('Ctrl Pts',(-2.48856433892152,1.10317454896066,
12.5278936106989));
#431350=CARTESIAN_POINT('Ctrl Pts',(-2.52824699050566,1.08832216853502,
12.5204817579905));
#431351=CARTESIAN_POINT('Ctrl Pts',(-2.51681178685245,1.08793771084195,
12.5081597038247));
#431352=CARTESIAN_POINT('Ctrl Pts',(-2.51326507268073,1.10405307194491,
12.5049254088044));
#431353=CARTESIAN_POINT('Ctrl Pts',(-2.51047333723491,1.08772460875899,
12.5369868989719));
#431354=CARTESIAN_POINT('Ctrl Pts',(-2.5114043160049,1.08775590892762,12.5342545179733));
#431355=CARTESIAN_POINT('Ctrl Pts',(-2.5122886079891,1.08791045600796,12.5314872231885));
#431356=CARTESIAN_POINT('Ctrl Pts',(-2.51306677574641,1.08823461037182,
12.5287124745063));
#431357=CARTESIAN_POINT('Ctrl Pts',(-2.51376856605476,1.08852694886673,
12.5262100684184));
#431358=CARTESIAN_POINT('Ctrl Pts',(-2.51438295571426,1.0889578475602,12.5237004536639));
#431359=CARTESIAN_POINT('Ctrl Pts',(-2.51488243000409,1.08958897829564,
12.5212220730815));
#431360=CARTESIAN_POINT('Ctrl Pts',(-2.51526482078093,1.09007216347079,
12.5193246583486));
#431361=CARTESIAN_POINT('Ctrl Pts',(-2.51558392955601,1.09067887774684,
12.517417831369));
#431362=CARTESIAN_POINT('Ctrl Pts',(-2.51576432415528,1.09147047265085,
12.5155812248347));
#431363=CARTESIAN_POINT('Ctrl Pts',(-2.5158411732242,1.0918076963348,12.5147988205793));
#431364=CARTESIAN_POINT('Ctrl Pts',(-2.51589319647567,1.09217875303941,
12.5140295443047));
#431365=CARTESIAN_POINT('Ctrl Pts',(-2.51591654171449,1.0925891647262,12.5132817086137));
#431366=CARTESIAN_POINT('Ctrl Pts',(-2.51595187157537,1.09321026729493,
12.5121499604604));
#431367=CARTESIAN_POINT('Ctrl Pts',(-2.51591514373557,1.0939353219013,12.511049420657));
#431368=CARTESIAN_POINT('Ctrl Pts',(-2.51577053661718,1.09477451252028,
12.5100666561697));
#431369=CARTESIAN_POINT('Ctrl Pts',(-2.5156875035428,1.09525637384121,12.5095023550643));
#431370=CARTESIAN_POINT('Ctrl Pts',(-2.51556729971076,1.09578132276691,
12.5089719619137));
#431371=CARTESIAN_POINT('Ctrl Pts',(-2.5154059523648,1.09633809410319,12.5085043804652));
#431372=CARTESIAN_POINT('Ctrl Pts',(-2.51516984154096,1.09715285642926,
12.5078201359221));
#431373=CARTESIAN_POINT('Ctrl Pts',(-2.51483761582447,1.09805905954442,
12.5072563000949));
#431374=CARTESIAN_POINT('Ctrl Pts',(-2.51442384655357,1.09899236216246,
12.5068768744332));
#431375=CARTESIAN_POINT('Ctrl Pts',(-2.51412549042528,1.09966533759884,
12.5066032824114));
#431376=CARTESIAN_POINT('Ctrl Pts',(-2.51377954975441,1.10036425066418,
12.5064197834844));
#431377=CARTESIAN_POINT('Ctrl Pts',(-2.51340765937553,1.10105121889007,
12.5063282718343));
#431378=CARTESIAN_POINT('Ctrl Pts',(-2.51286481455672,1.10205397981988,
12.5061946931565));
#431379=CARTESIAN_POINT('Ctrl Pts',(-2.51225601023427,1.10305322842605,
12.5062515701262));
#431380=CARTESIAN_POINT('Ctrl Pts',(-2.51163223633243,1.10399499577423,
12.5064436508398));
#431381=CARTESIAN_POINT('',(-2.43909421506564,1.10141166871474,12.5737548217797));
#431382=CARTESIAN_POINT('Origin',(-2.45327206454526,1.10781390146068,12.5893111709658));
#431383=CARTESIAN_POINT('Ctrl Pts',(-2.51163223633243,1.10399499577423,
12.5064436508398));
#431384=CARTESIAN_POINT('Ctrl Pts',(-2.50089470750429,1.10361307639003,
12.5164271754438));
#431385=CARTESIAN_POINT('Ctrl Pts',(-2.49015292974903,1.10323079680946,
12.5264061185523));
#431386=CARTESIAN_POINT('Ctrl Pts',(-2.47940675338938,1.1028481452926,12.536380305637));
#431387=CARTESIAN_POINT('Ctrl Pts',(-2.46597621249922,1.10236990850661,
12.5488460165097));
#431388=CARTESIAN_POINT('Ctrl Pts',(-2.45253879705324,1.10189109059316,
12.5613043021964));
#431389=CARTESIAN_POINT('Ctrl Pts',(-2.43909421506564,1.10141166871473,
12.5737548217797));
#431390=CARTESIAN_POINT('Ctrl Pts',(-2.42764842286964,1.14355297053481,
12.5893111709658));
#431391=CARTESIAN_POINT('Ctrl Pts',(-2.41994263053451,1.13524156878495,
12.5770542771492));
#431392=CARTESIAN_POINT('Ctrl Pts',(-2.42965842765956,1.12207316109535,
12.5737548217797));
#431393=CARTESIAN_POINT('Ctrl Pts',(-2.4204589856424,1.13579850499095,12.5928319619712));
#431394=CARTESIAN_POINT('Ctrl Pts',(-2.41766918003243,1.12799783828675,
12.5821634970842));
#431395=CARTESIAN_POINT('Ctrl Pts',(-2.42703256801096,1.11925481433258,
12.5773203894503));
#431396=CARTESIAN_POINT('Ctrl Pts',(-2.41523183997244,1.11988432742864,
12.5969440695591));
#431397=CARTESIAN_POINT('Ctrl Pts',(-2.41688507232563,1.11622026338195,
12.5878292599214));
#431398=CARTESIAN_POINT('Ctrl Pts',(-2.42517145044037,1.11358203824974,
12.5813877129824));
#431399=CARTESIAN_POINT('Ctrl Pts',(-2.42789321447587,1.09202997693854,
12.596957478804));
#431400=CARTESIAN_POINT('Ctrl Pts',(-2.42625227301845,1.09566699553654,
12.5878468778671));
#431401=CARTESIAN_POINT('Ctrl Pts',(-2.42970856230818,1.10361504852349,
12.5814011370086));
#431402=CARTESIAN_POINT('Ctrl Pts',(-2.443427439057,1.08547048962603,12.5928371701607));
#431403=CARTESIAN_POINT('Ctrl Pts',(-2.43571288526976,1.08847394190091,
12.5821692192952));
#431404=CARTESIAN_POINT('Ctrl Pts',(-2.43523237626195,1.10127210321656,
12.5773318885715));
#431405=CARTESIAN_POINT('Ctrl Pts',(-2.45401129869476,1.08582632467571,
12.5893111709658));
#431406=CARTESIAN_POINT('Ctrl Pts',(-2.4426837395358,1.0854454860484,12.5770542771492));
#431407=CARTESIAN_POINT('Ctrl Pts',(-2.43909421506564,1.10141166871468,
12.5737548217797));
#431408=CARTESIAN_POINT('',(-2.42965842765956,1.12207316109535,12.5737548217797));
#431409=CARTESIAN_POINT('Origin',(-2.44378142924822,1.12859549396993,12.5893111709658));
#431410=CARTESIAN_POINT('Ctrl Pts',(-2.43909421506564,1.10141166871468,
12.5737548217797));
#431411=CARTESIAN_POINT('Ctrl Pts',(-2.43809425466414,1.10134534506547,
12.5746934679442));
#431412=CARTESIAN_POINT('Ctrl Pts',(-2.43697560860098,1.10145473621515,
12.5756680099006));
#431413=CARTESIAN_POINT('Ctrl Pts',(-2.43586522293742,1.10172408236073,
12.5765688348656));
#431414=CARTESIAN_POINT('Ctrl Pts',(-2.43557126062537,1.10179538877101,
12.5768073183026));
#431415=CARTESIAN_POINT('Ctrl Pts',(-2.43527787928168,1.1018776488304,12.5770407398754));
#431416=CARTESIAN_POINT('Ctrl Pts',(-2.43498729713664,1.10197002393467,
12.5772674179684));
#431417=CARTESIAN_POINT('Ctrl Pts',(-2.43379482659014,1.10234910638329,
12.5781976435658));
#431418=CARTESIAN_POINT('Ctrl Pts',(-2.43258518413186,1.10293081301547,
12.5790594849312));
#431419=CARTESIAN_POINT('Ctrl Pts',(-2.43146097448086,1.10371938475238,
12.5797571720116));
#431420=CARTESIAN_POINT('Ctrl Pts',(-2.43072851147025,1.1042331675935,12.580211740231));
#431421=CARTESIAN_POINT('Ctrl Pts',(-2.43000980833863,1.10487348219503,
12.5806009430798));
#431422=CARTESIAN_POINT('Ctrl Pts',(-2.42936724407257,1.10560848139795,
12.5808812374708));
#431423=CARTESIAN_POINT('Ctrl Pts',(-2.42881506819955,1.10624008954671,
12.5811221033394));
#431424=CARTESIAN_POINT('Ctrl Pts',(-2.42830789856473,1.10695462346068,
12.581287365893));
#431425=CARTESIAN_POINT('Ctrl Pts',(-2.427881159959,1.10771657978872,12.581359338449));
#431426=CARTESIAN_POINT('Ctrl Pts',(-2.42782185210462,1.10782247598452,
12.5813693411482));
#431427=CARTESIAN_POINT('Ctrl Pts',(-2.42776403878955,1.10792927798243,
12.5813775999465));
#431428=CARTESIAN_POINT('Ctrl Pts',(-2.4277077544834,1.10803688112628,12.5813841266931));
#431429=CARTESIAN_POINT('Ctrl Pts',(-2.42761226135055,1.10821944287415,
12.5813952001081));
#431430=CARTESIAN_POINT('Ctrl Pts',(-2.42752106945785,1.10840581565869,
12.5814007534795));
#431431=CARTESIAN_POINT('Ctrl Pts',(-2.42743439566389,1.10859600498354,
12.5814005856065));
#431432=CARTESIAN_POINT('Ctrl Pts',(-2.42703763692243,1.10946661735351,
12.5813998171494));
#431433=CARTESIAN_POINT('Ctrl Pts',(-2.42676265857133,1.11035691084844,
12.58127954464));
#431434=CARTESIAN_POINT('Ctrl Pts',(-2.42658275018652,1.11125309893149,
12.5810700125799));
#431435=CARTESIAN_POINT('Ctrl Pts',(-2.42636544134188,1.11233559209663,
12.5808169217085));
#431436=CARTESIAN_POINT('Ctrl Pts',(-2.42630322752117,1.1134300772724,12.5804173076348));
#431437=CARTESIAN_POINT('Ctrl Pts',(-2.42637556064734,1.11443915768868,
12.5799304713245));
#431438=CARTESIAN_POINT('Ctrl Pts',(-2.42646520417795,1.11568972621756,
12.5793271277669));
#431439=CARTESIAN_POINT('Ctrl Pts',(-2.42673494143363,1.11688899875593,
12.5785808224116));
#431440=CARTESIAN_POINT('Ctrl Pts',(-2.42714245864617,1.11799338346448,
12.5777485681082));
#431441=CARTESIAN_POINT('Ctrl Pts',(-2.4277497039397,1.1196390376746,12.576508418016));
#431442=CARTESIAN_POINT('Ctrl Pts',(-2.42865131903009,1.12106252274286,
12.5750928681475));
#431443=CARTESIAN_POINT('Ctrl Pts',(-2.42965842765956,1.12207316109535,
12.5737548217797));
#431444=CARTESIAN_POINT('Ctrl Pts',(-2.42965842765956,1.12207316109535,
12.5737548217797));
#431445=CARTESIAN_POINT('Ctrl Pts',(-2.41994263053451,1.13524156878495,
12.5770542771492));
#431446=CARTESIAN_POINT('Ctrl Pts',(-2.42764842286964,1.14355297053481,
12.5893111709658));
#431447=CARTESIAN_POINT('Ctrl Pts',(-2.44652873594355,1.14019518230089,
12.5508408821982));
#431448=CARTESIAN_POINT('Ctrl Pts',(-2.43678025017059,1.15340248141025,
12.55409748406));
#431449=CARTESIAN_POINT('Ctrl Pts',(-2.44449587312322,1.16172448638006,
12.5663972313419));
#431450=CARTESIAN_POINT('Ctrl Pts',(-2.46338170073771,1.15830030426781,
12.52790050457));
#431451=CARTESIAN_POINT('Ctrl Pts',(-2.45358562175745,1.1715286115652,12.5311362602938));
#431452=CARTESIAN_POINT('Ctrl Pts',(-2.4613263270679,1.17987767015181,12.5434568539655));
#431453=CARTESIAN_POINT('Ctrl Pts',(-2.48021865971795,1.17638984971966,
12.5049357605811));
#431454=CARTESIAN_POINT('Ctrl Pts',(-2.47036210698932,1.18962358514459,
12.5081700652078));
#431455=CARTESIAN_POINT('Ctrl Pts',(-2.47814111585804,1.19801395762177,
12.5204921097672));
#431456=CARTESIAN_POINT('Ctrl Pts',(-2.47911307783068,1.17520202033778,
12.5064436508395));
#431457=CARTESIAN_POINT('Ctrl Pts',(-2.47878550732966,1.176377411914,12.5062361689309));
#431458=CARTESIAN_POINT('Ctrl Pts',(-2.47839473950699,1.17758575463409,
12.5061871075061));
#431459=CARTESIAN_POINT('Ctrl Pts',(-2.47795136471677,1.1787322429404,12.5063648335164));
#431460=CARTESIAN_POINT('Ctrl Pts',(-2.47774995653857,1.17925304864746,
12.5064455676329));
#431461=CARTESIAN_POINT('Ctrl Pts',(-2.47753467801008,1.17976827515964,
12.506574497099));
#431462=CARTESIAN_POINT('Ctrl Pts',(-2.47731378992389,1.1802554259349,12.5067492519495));
#431463=CARTESIAN_POINT('Ctrl Pts',(-2.47686990674041,1.18123437432765,
12.5071004286051));
#431464=CARTESIAN_POINT('Ctrl Pts',(-2.47638631472707,1.18213560467378,
12.5076537929613));
#431465=CARTESIAN_POINT('Ctrl Pts',(-2.47590764438951,1.18289594706659,
12.5083435010505));
#431466=CARTESIAN_POINT('Ctrl Pts',(-2.47587750923121,1.18294381516405,
12.5083869222964));
#431467=CARTESIAN_POINT('Ctrl Pts',(-2.47584738019338,1.18299112372014,
12.5084308732337));
#431468=CARTESIAN_POINT('Ctrl Pts',(-2.47581726292796,1.18303785690299,
12.5084753333615));
#431469=CARTESIAN_POINT('Ctrl Pts',(-2.4755756827081,1.18341271871171,12.5088319622689));
#431470=CARTESIAN_POINT('Ctrl Pts',(-2.47533103987099,1.18375886925869,
12.509227847131));
#431471=CARTESIAN_POINT('Ctrl Pts',(-2.47509289553871,1.18406763175556,
12.5096423454524));
#431472=CARTESIAN_POINT('Ctrl Pts',(-2.47434665659961,1.18503515676821,
12.5109411997424));
#431473=CARTESIAN_POINT('Ctrl Pts',(-2.47362598515748,1.18570097563409,
12.5124831113042));
#431474=CARTESIAN_POINT('Ctrl Pts',(-2.47296176065527,1.18615454402601,
12.5140723025008));
#431475=CARTESIAN_POINT('Ctrl Pts',(-2.47289952209191,1.18619704388111,
12.5142212114565));
#431476=CARTESIAN_POINT('Ctrl Pts',(-2.47283777833191,1.18623770979641,
12.5143705582413));
#431477=CARTESIAN_POINT('Ctrl Pts',(-2.47277655587106,1.18627663231314,
12.5145201959299));
#431478=CARTESIAN_POINT('Ctrl Pts',(-2.47199006221069,1.18677664999011,
12.5164425148273));
#431479=CARTESIAN_POINT('Ctrl Pts',(-2.47126841277287,1.18701514499689,
12.5184635205941));
#431480=CARTESIAN_POINT('Ctrl Pts',(-2.47059240180699,1.18708025993212,
12.5205025929158));
#431481=CARTESIAN_POINT('Ctrl Pts',(-2.4702002886522,1.18711802917547,12.5216853356836));
#431482=CARTESIAN_POINT('Ctrl Pts',(-2.46982428505582,1.18709787849179,
12.5228750347131));
#431483=CARTESIAN_POINT('Ctrl Pts',(-2.4694664941172,1.18703793274305,12.5240609649613));
#431484=CARTESIAN_POINT('Ctrl Pts',(-2.46858831545318,1.18689079911873,
12.5269717671326));
#431485=CARTESIAN_POINT('Ctrl Pts',(-2.46779685772931,1.18648953404488,
12.5299036066169));
#431486=CARTESIAN_POINT('Ctrl Pts',(-2.46706587168992,1.18591672383515,
12.5328133004019));
#431487=CARTESIAN_POINT('Ctrl Pts',(-2.46671495582697,1.18564174158075,
12.5342101228451));
#431488=CARTESIAN_POINT('Ctrl Pts',(-2.46637873711443,1.18532715632361,
12.5356023438238));
#431489=CARTESIAN_POINT('Ctrl Pts',(-2.46605782225598,1.18498102042073,
12.5369868989719));
#431490=CARTESIAN_POINT('Origin',(-11.1269742283812,10.5343602107449,-1.23915455685045));
#431491=CARTESIAN_POINT('Ctrl Pts',(-2.51043156791945,1.08772316473061,
12.5369868989719));
#431492=CARTESIAN_POINT('Ctrl Pts',(-2.5257608466132,1.08826769977493,12.5369868989719));
#431493=CARTESIAN_POINT('Ctrl Pts',(-2.53157241165723,1.07407231265713,
12.5369868989719));
#431494=CARTESIAN_POINT('Ctrl Pts',(-2.51561346599296,1.08790717270204,
12.5218025310015));
#431495=CARTESIAN_POINT('Ctrl Pts',(-2.52706672854372,1.08499536215749,
12.5216901060418));
#431496=CARTESIAN_POINT('Ctrl Pts',(-2.53155471134322,1.07411559114987,
12.5161920673677));
#431497=CARTESIAN_POINT('Ctrl Pts',(-2.5189537241703,1.09292501551582,12.5042015548895));
#431498=CARTESIAN_POINT('Ctrl Pts',(-2.52478486974079,1.09020930449414,
12.4980677368513));
#431499=CARTESIAN_POINT('Ctrl Pts',(-2.5274735169963,1.08396735322399,12.4907278922778));
#431500=CARTESIAN_POINT('Ctrl Pts',(-2.5116139260195,1.10398694743621,12.506463626192));
#431501=CARTESIAN_POINT('Ctrl Pts',(-2.51760358068647,1.10661971694886,
12.4999376786891));
#431502=CARTESIAN_POINT('Ctrl Pts',(-2.51753042576366,1.10658756149731,
12.4906970594712));
#431503=CARTESIAN_POINT('Origin',(-2.51121257138441,1.06573703197408,12.5369868989719));
#431504=CARTESIAN_POINT('Origin',(-2.51121257138441,1.06573703197408,14.));
#431505=CARTESIAN_POINT('Origin',(-2.51121257138441,1.06573703197408,13.7435492065112));
#431506=CARTESIAN_POINT('Ctrl Pts',(-2.48572721599399,1.08689260369535,
13.793642941384));
#431507=CARTESIAN_POINT('Ctrl Pts',(-2.49653247935202,1.08728311972515,
13.8071662555867));
#431508=CARTESIAN_POINT('Ctrl Pts',(-2.499643077526,1.07053965644437,13.8103758687955));
#431509=CARTESIAN_POINT('Ctrl Pts',(-2.50233895234728,1.08745110217535,
13.7804579775006));
#431510=CARTESIAN_POINT('Ctrl Pts',(-2.51567203695235,1.08792282947323,
13.7901904343351));
#431511=CARTESIAN_POINT('Ctrl Pts',(-2.52101841522977,1.07310148798607,
13.7927914348263));
#431512=CARTESIAN_POINT('Ctrl Pts',(-2.51211890670968,1.08777991121118,
13.7597120340895));
#431513=CARTESIAN_POINT('Ctrl Pts',(-2.52754924305908,1.08832010572878,
13.7635825532445));
#431514=CARTESIAN_POINT('Ctrl Pts',(-2.53362646930207,1.07458681634366,
13.7651073818884));
#431515=CARTESIAN_POINT('Ctrl Pts',(-2.51020376771007,1.08771552287228,
13.7381884353898));
#431516=CARTESIAN_POINT('Ctrl Pts',(-2.52527289684106,1.08824397141278,
13.7368803041982));
#431517=CARTESIAN_POINT('Ctrl Pts',(-2.53115749549256,1.07429545407832,
13.7363986145813));
#431518=CARTESIAN_POINT('Origin',(-2.49049725742218,1.0650405719845,13.7902182540695));
#431519=CARTESIAN_POINT('Ctrl Pts',(-2.45400736474459,1.0858261916549,13.8235227101244));
#431520=CARTESIAN_POINT('Ctrl Pts',(-2.46549779565255,1.08621694204688,
13.8358800583119));
#431521=CARTESIAN_POINT('Ctrl Pts',(-2.46902410772919,1.07002462373867,
13.8390832900376));
#431522=CARTESIAN_POINT('Ctrl Pts',(-2.46592820869684,1.08622697683474,
13.8124254819052));
#431523=CARTESIAN_POINT('Ctrl Pts',(-2.47744095386821,1.08661848578045,
13.8247886449157));
#431524=CARTESIAN_POINT('Ctrl Pts',(-2.48095506764779,1.07040208095551,
13.8279860620657));
#431525=CARTESIAN_POINT('Ctrl Pts',(-2.47784371011467,1.08662758239573,
13.8013225099955));
#431526=CARTESIAN_POINT('Ctrl Pts',(-2.48937333731432,1.08701966716926,
13.8136962257787));
#431527=CARTESIAN_POINT('Ctrl Pts',(-2.49288049554766,1.07077963434886,
13.8168830918626));
#431528=CARTESIAN_POINT('Ctrl Pts',(-2.48975407686786,1.08702801532653,
13.7902140179785));
#431529=CARTESIAN_POINT('Ctrl Pts',(-2.50129550889728,1.08742050514159,
13.802602731458));
#431530=CARTESIAN_POINT('Ctrl Pts',(-2.50480060873704,1.07115728197905,
13.8057746032558));
#431531=CARTESIAN_POINT('Origin',(-2.45475053284426,1.06383874789086,13.8235269408515));
#431532=CARTESIAN_POINT('Ctrl Pts',(-2.42764842286964,1.14355297053481,
13.8235269408515));
#431533=CARTESIAN_POINT('Ctrl Pts',(-2.43567615593591,1.15221161480558,
13.8362179249168));
#431534=CARTESIAN_POINT('Ctrl Pts',(-2.42519536199323,1.16569552975593,
13.8391868794938));
#431535=CARTESIAN_POINT('Ctrl Pts',(-2.42030339654042,1.13563068791539,
13.8400110824519));
#431536=CARTESIAN_POINT('Ctrl Pts',(-2.42423099304139,1.14489868924187,
13.8494522556837));
#431537=CARTESIAN_POINT('Ctrl Pts',(-2.41318991562471,1.15258129927463,
13.85569149686));
#431538=CARTESIAN_POINT('Ctrl Pts',(-2.41508842470968,1.12019690047195,
13.8586819406589));
#431539=CARTESIAN_POINT('Ctrl Pts',(-2.41329242897892,1.12416306271903,
13.868010383617));
#431540=CARTESIAN_POINT('Ctrl Pts',(-2.40467127587644,1.1269141690376,13.8744918421245));
#431541=CARTESIAN_POINT('Ctrl Pts',(-2.42803883709481,1.09171254832903,
13.8587686893867));
#431542=CARTESIAN_POINT('Ctrl Pts',(-2.42981879718596,1.08778166166139,
13.8680909899357));
#431543=CARTESIAN_POINT('Ctrl Pts',(-2.42623225163339,1.07949715247226,
13.8745789365162));
#431544=CARTESIAN_POINT('Ctrl Pts',(-2.44319649798033,1.08546272525639,
13.8400379222776));
#431545=CARTESIAN_POINT('Ctrl Pts',(-2.45276816699803,1.08235573537491,
13.8494748685453));
#431546=CARTESIAN_POINT('Ctrl Pts',(-2.45134570433742,1.06898645322352,
13.8557104837033));
#431547=CARTESIAN_POINT('Ctrl Pts',(-2.45401129869484,1.08582632466916,
13.8235269408542));
#431548=CARTESIAN_POINT('Ctrl Pts',(-2.46581211258463,1.08622307437485,
13.8362179249195));
#431549=CARTESIAN_POINT('Ctrl Pts',(-2.4691391151553,1.06947213237294,13.8391868794965));
#431550=CARTESIAN_POINT('Origin',(-2.41151541649107,1.15851044709968,13.8235269408515));
#431551=CARTESIAN_POINT('Ctrl Pts',(-2.45196314593983,1.16977862413369,
13.7902140241683));
#431552=CARTESIAN_POINT('Ctrl Pts',(-2.4598177926985,1.17824403137073,13.8026027327198));
#431553=CARTESIAN_POINT('Ctrl Pts',(-2.44982222494642,1.19154315004781,
13.8057746032556));
#431554=CARTESIAN_POINT('Ctrl Pts',(-2.44386088740655,1.16103959732961,
13.8013225161808));
#431555=CARTESIAN_POINT('Ctrl Pts',(-2.45170749754734,1.16949634831233,
13.8136962270464));
#431556=CARTESIAN_POINT('Ctrl Pts',(-2.44173080383841,1.18278183618263,
13.8168830918628));
#431557=CARTESIAN_POINT('Ctrl Pts',(-2.43575513591674,1.15229680305245,
13.8124254880875));
#431558=CARTESIAN_POINT('Ctrl Pts',(-2.44359025551311,1.1607411725346,13.8247886461867));
#431559=CARTESIAN_POINT('Ctrl Pts',(-2.43363597355523,1.17401644401586,
13.8279860620656));
#431560=CARTESIAN_POINT('Ctrl Pts',(-2.42764575006183,1.14355008878014,
13.8235227163065));
#431561=CARTESIAN_POINT('Ctrl Pts',(-2.43546568366467,1.15197809101578,
13.8358800595848));
#431562=CARTESIAN_POINT('Ctrl Pts',(-2.42553759325522,1.16524680804569,
13.8390832900376));
#431563=CARTESIAN_POINT('Origin',(-2.43583282083151,1.18473899157597,13.7902182540695));
#431564=CARTESIAN_POINT('Ctrl Pts',(-2.46587432824779,1.18478314592408,
13.7382347919292));
#431565=CARTESIAN_POINT('Ctrl Pts',(-2.47615160437,1.19583282755939,13.7369371795942));
#431566=CARTESIAN_POINT('Ctrl Pts',(-2.46945101245651,1.20942127283577,
13.7364597369711));
#431567=CARTESIAN_POINT('Ctrl Pts',(-2.46716037143437,1.18617026052154,
13.7595490285574));
#431568=CARTESIAN_POINT('Ctrl Pts',(-2.47768211834678,1.19748426283415,
13.7633824266927));
#431569=CARTESIAN_POINT('Ctrl Pts',(-2.47126579107942,1.2110755984825,13.7648920890506));
#431570=CARTESIAN_POINT('Ctrl Pts',(-2.46060162164384,1.17909605206138,
13.780380659011));
#431571=CARTESIAN_POINT('Ctrl Pts',(-2.46970650931237,1.18887858274357,
13.7901039518743));
#431572=CARTESIAN_POINT('Ctrl Pts',(-2.46201635270427,1.20263892186614,
13.7926933640892));
#431573=CARTESIAN_POINT('Ctrl Pts',(-2.44920105035431,1.16679949864812,
13.7936647693663));
#431574=CARTESIAN_POINT('Ctrl Pts',(-2.45657624812666,1.17471023753671,
13.8072068914933));
#431575=CARTESIAN_POINT('Ctrl Pts',(-2.44593970851891,1.18803346143411,
13.8104111085397));
#431576=CARTESIAN_POINT('Origin',(-2.44992481587741,1.1999384969856,13.7435492065112));
#431577=CARTESIAN_POINT('Origin',(-2.44992481587741,1.1999384969856,14.));
#431578=CARTESIAN_POINT('Origin',(-2.44992481587741,1.1999384969856,12.5369868989719));
#431579=CARTESIAN_POINT('Ctrl Pts',(-2.47909646650412,1.1751941458713,12.506462012331));
#431580=CARTESIAN_POINT('Ctrl Pts',(-2.48500485080772,1.17799496412867,
12.4999388158272));
#431581=CARTESIAN_POINT('Ctrl Pts',(-2.48493494687304,1.17796182677563,
12.4907030323752));
#431582=CARTESIAN_POINT('Ctrl Pts',(-2.47554113020114,1.18798430485887,
12.5042014951932));
#431583=CARTESIAN_POINT('Ctrl Pts',(-2.47730746574457,1.19416663094731,
12.4980716682127));
#431584=CARTESIAN_POINT('Ctrl Pts',(-2.47435430417184,1.20028254477528,
12.4907355092743));
#431585=CARTESIAN_POINT('Ctrl Pts',(-2.46956264420209,1.18874811530927,
12.5218047446509));
#431586=CARTESIAN_POINT('Ctrl Pts',(-2.47485873145528,1.19930606637672,
12.5216906929434));
#431587=CARTESIAN_POINT('Ctrl Pts',(-2.46958136695414,1.20981892413528,
12.5161988840776));
#431588=CARTESIAN_POINT('Ctrl Pts',(-2.46603167910977,1.18495287197982,
12.5369868989719));
#431589=CARTESIAN_POINT('Ctrl Pts',(-2.47647386024285,1.19617634669597,
12.5369868989719));
#431590=CARTESIAN_POINT('Ctrl Pts',(-2.46956103641718,1.20985912412876,
12.5369868989719));
#431591=CARTESIAN_POINT('Origin',(-4.6862990577545E-31,-3.01170153175954E-31,
12.5));
#431592=CARTESIAN_POINT('Origin',(-2.51278080633585,0.94187200870957,12.5));
#431593=CARTESIAN_POINT('',(-2.51278080633585,0.94187200870957,12.5893111709658));
#431594=CARTESIAN_POINT('',(-2.51278080633585,0.94187200870957,13.8235269408515));
#431595=CARTESIAN_POINT('',(-2.51278080633585,0.94187200870957,12.5));
#431596=CARTESIAN_POINT('',(-2.53915516638814,0.966031185662302,13.7902182540695));
#431597=CARTESIAN_POINT('',(-2.51278080633585,0.94187200870957,13.8235269408515));
#431598=CARTESIAN_POINT('',(-2.55443917227924,0.980031487551614,13.7435492065112));
#431599=CARTESIAN_POINT('Origin',(-2.50415521495494,0.933970439180074,13.7445212918689));
#431600=CARTESIAN_POINT('',(-2.55443917227924,0.980031487551614,12.5369868989719));
#431601=CARTESIAN_POINT('',(-2.55443917227924,0.980031487551614,12.5));
#431602=CARTESIAN_POINT('Ctrl Pts',(-2.55443917227924,0.980031487551614,
12.5369868989719));
#431603=CARTESIAN_POINT('Ctrl Pts',(-2.54056317799091,0.967320938338584,
12.5544431401645));
#431604=CARTESIAN_POINT('Ctrl Pts',(-2.52667725922266,0.954601298202932,
12.5718848856037));
#431605=CARTESIAN_POINT('Ctrl Pts',(-2.51278080633585,0.94187200870957,
12.5893111709658));
#431606=CARTESIAN_POINT('Origin',(-2.80903407160718,0.868995909108973,12.5));
#431607=CARTESIAN_POINT('',(-2.59077959786119,0.879478411772282,13.7435492065112));
#431608=CARTESIAN_POINT('',(-2.5700764444425,0.880472759595378,13.7902182540695));
#431609=CARTESIAN_POINT('Origin',(-2.51567213548189,0.883085733816646,13.7418732680441));
#431610=CARTESIAN_POINT('',(-2.5343507043209,0.88218862438177,13.8235269408515));
#431611=CARTESIAN_POINT('',(-2.5700764444425,0.880472759595378,13.7902182540695));
#431612=CARTESIAN_POINT('',(-2.5343507043209,0.88218862438177,12.5893111709658));
#431613=CARTESIAN_POINT('',(-2.5343507043209,0.88218862438177,12.5));
#431614=CARTESIAN_POINT('',(-2.59077959786119,0.879478411772282,12.5369868989719));
#431615=CARTESIAN_POINT('Ctrl Pts',(-2.5343507043209,0.88218862438177,12.5893111709658));
#431616=CARTESIAN_POINT('Ctrl Pts',(-2.55317432936666,0.881284548069891,
12.5718848856037));
#431617=CARTESIAN_POINT('Ctrl Pts',(-2.57198368528205,0.880381157087365,
12.5544431401645));
#431618=CARTESIAN_POINT('Ctrl Pts',(-2.59077959786119,0.879478411772282,
12.5369868989719));
#431619=CARTESIAN_POINT('',(-2.59077959786119,0.879478411772282,12.5));
#431620=CARTESIAN_POINT('Origin',(-2.53599979373,0.916524045292556,12.5));
#431621=CARTESIAN_POINT('',(-2.50330861296455,0.90589969249633,13.8587068136939));
#431622=CARTESIAN_POINT('Ctrl Pts',(-2.53435070432044,0.882188624375176,
13.8235269408542));
#431623=CARTESIAN_POINT('Ctrl Pts',(-2.53260042357507,0.882272688276647,
13.8262006681044));
#431624=CARTESIAN_POINT('Ctrl Pts',(-2.53081760184798,0.882532254687068,
13.8288634856214));
#431625=CARTESIAN_POINT('Ctrl Pts',(-2.52900609155787,0.882954557835087,
13.8314912288862));
#431626=CARTESIAN_POINT('Ctrl Pts',(-2.52713861129738,0.883389908822146,
13.8342001611531));
#431627=CARTESIAN_POINT('Ctrl Pts',(-2.52523845519516,0.88399820766378,
13.8368750301949));
#431628=CARTESIAN_POINT('Ctrl Pts',(-2.52329991795237,0.884809566077829,
13.8394886372969));
#431629=CARTESIAN_POINT('Ctrl Pts',(-2.52315020001887,0.884872229256226,
13.8396904925131));
#431630=CARTESIAN_POINT('Ctrl Pts',(-2.52300025805097,0.884936125252825,
13.8398919674349));
#431631=CARTESIAN_POINT('Ctrl Pts',(-2.5228500929241,0.885001278833934,
13.8400930404591));
#431632=CARTESIAN_POINT('Ctrl Pts',(-2.52051041922137,0.886016415460797,
13.8432258934518));
#431633=CARTESIAN_POINT('Ctrl Pts',(-2.51812806255079,0.887330627611538,
13.8462331177034));
#431634=CARTESIAN_POINT('Ctrl Pts',(-2.515827318044,0.888985519365726,13.8489036603661));
#431635=CARTESIAN_POINT('Ctrl Pts',(-2.51507448766627,0.889527019206639,
13.8497774930041));
#431636=CARTESIAN_POINT('Ctrl Pts',(-2.51433064499445,0.890104983786962,
13.85061494757));
#431637=CARTESIAN_POINT('Ctrl Pts',(-2.51360085711104,0.890720827412258,
13.8514076489583));
#431638=CARTESIAN_POINT('Ctrl Pts',(-2.51205725048647,0.892023425497699,
13.8530843267192));
#431639=CARTESIAN_POINT('Ctrl Pts',(-2.51042680751305,0.893625698201537,
13.8546805203176));
#431640=CARTESIAN_POINT('Ctrl Pts',(-2.50889979581452,0.895531968935214,
13.8559412814273));
#431641=CARTESIAN_POINT('Ctrl Pts',(-2.50869543212709,0.895787089781212,
13.8561100121513));
#431642=CARTESIAN_POINT('Ctrl Pts',(-2.50849290645992,0.896047580140268,
13.8562727473908));
#431643=CARTESIAN_POINT('Ctrl Pts',(-2.50829265133,0.896313378282975,13.8564289040185));
#431644=CARTESIAN_POINT('Ctrl Pts',(-2.50738449660041,0.89751876982779,
13.8571370725437));
#431645=CARTESIAN_POINT('Ctrl Pts',(-2.50650889335531,0.898855879134049,
13.8577210840554));
#431646=CARTESIAN_POINT('Ctrl Pts',(-2.50572442859695,0.900288810448204,
13.8581177131616));
#431647=CARTESIAN_POINT('Ctrl Pts',(-2.50550349632054,0.900692373226265,
13.8582294175695));
#431648=CARTESIAN_POINT('Ctrl Pts',(-2.50528965689758,0.90110342224896,
13.8583265086086));
#431649=CARTESIAN_POINT('Ctrl Pts',(-2.50508386606588,0.901520893712507,
13.8584082369006));
#431650=CARTESIAN_POINT('Ctrl Pts',(-2.50478819982573,0.902120688256229,
13.8585256585398));
#431651=CARTESIAN_POINT('Ctrl Pts',(-2.50450576166904,0.902741339815834,
13.8586122832068));
#431652=CARTESIAN_POINT('Ctrl Pts',(-2.50424460728378,0.903367052748162,
13.8586682984299));
#431653=CARTESIAN_POINT('Ctrl Pts',(-2.50403570966297,0.903867561069096,
13.8587131050557));
#431654=CARTESIAN_POINT('Ctrl Pts',(-2.50383790661363,0.904376745668662,
13.8587357943552));
#431655=CARTESIAN_POINT('Ctrl Pts',(-2.50365164670807,0.904894850439687,
13.8587355499465));
#431656=CARTESIAN_POINT('Ctrl Pts',(-2.50353126249048,0.905229713905339,
13.8587353919793));
#431657=CARTESIAN_POINT('Ctrl Pts',(-2.50341696566905,0.905564669382782,
13.8587257282814));
#431658=CARTESIAN_POINT('Ctrl Pts',(-2.50330861296455,0.90589969249633,
13.8587068136939));
#431659=CARTESIAN_POINT('Ctrl Pts',(-2.50330861296455,0.90589969249633,
13.8587068136939));
#431660=CARTESIAN_POINT('Ctrl Pts',(-2.50295224682631,0.907001565253013,
13.8586446046466));
#431661=CARTESIAN_POINT('Ctrl Pts',(-2.50266009965791,0.908104169469626,
13.858482427929));
#431662=CARTESIAN_POINT('Ctrl Pts',(-2.50242778173392,0.909206658820027,
13.8582284286032));
#431663=CARTESIAN_POINT('Ctrl Pts',(-2.50218945056825,0.910337684646655,
13.8579678548414));
#431664=CARTESIAN_POINT('Ctrl Pts',(-2.50201500249059,0.911471668188101,
13.857615680862));
#431665=CARTESIAN_POINT('Ctrl Pts',(-2.50190173797787,0.912562429691672,
13.8571944833187));
#431666=CARTESIAN_POINT('Ctrl Pts',(-2.50161907480263,0.915284536577744,
13.8561433417727));
#431667=CARTESIAN_POINT('Ctrl Pts',(-2.50169947288329,0.91786429163513,
13.8546163505475));
#431668=CARTESIAN_POINT('Ctrl Pts',(-2.5019829092095,0.920170734935598,
13.8528973491087));
#431669=CARTESIAN_POINT('Ctrl Pts',(-2.50203468884459,0.920592088098222,
13.8525833129073));
#431670=CARTESIAN_POINT('Ctrl Pts',(-2.50209312821209,0.921004399866691,
13.8522628768812));
#431671=CARTESIAN_POINT('Ctrl Pts',(-2.50215712197049,0.921406994889097,
13.851937733538));
#431672=CARTESIAN_POINT('Ctrl Pts',(-2.50254792297429,0.923865586833268,
13.8499521282529));
#431673=CARTESIAN_POINT('Ctrl Pts',(-2.50318873402412,0.926205502410216,
13.847639871647));
#431674=CARTESIAN_POINT('Ctrl Pts',(-2.50396838900178,0.928324985081203,
13.8452109780794));
#431675=CARTESIAN_POINT('Ctrl Pts',(-2.50431917191428,0.929278584205991,
13.8441181685877));
#431676=CARTESIAN_POINT('Ctrl Pts',(-2.50469751444125,0.930188026878953,
13.8430021611332));
#431677=CARTESIAN_POINT('Ctrl Pts',(-2.5050915609998,0.931046865311944,
13.8418824960098));
#431678=CARTESIAN_POINT('Ctrl Pts',(-2.50602014177737,0.933070740010502,
13.8392439765549));
#431679=CARTESIAN_POINT('Ctrl Pts',(-2.50707688276956,0.934911925671254,
13.8364981347964));
#431680=CARTESIAN_POINT('Ctrl Pts',(-2.50823489914821,0.936592325950845,
13.8336931113419));
#431681=CARTESIAN_POINT('Ctrl Pts',(-2.50936273356018,0.938228929107881,
13.8309611966328));
#431682=CARTESIAN_POINT('Ctrl Pts',(-2.51058822791128,0.939714338658285,
13.8281701127186));
#431683=CARTESIAN_POINT('Ctrl Pts',(-2.51190857473627,0.941036244646406,
13.8253580685121));
#431684=CARTESIAN_POINT('Ctrl Pts',(-2.5121948273529,0.941322835291278,
13.8247484142933));
#431685=CARTESIAN_POINT('Ctrl Pts',(-2.51248557178476,0.941601570915133,
13.8241378483365));
#431686=CARTESIAN_POINT('Ctrl Pts',(-2.51278080633585,0.94187200870957,
13.8235269408515));
#431687=CARTESIAN_POINT('',(-2.50371375400294,0.904725538504549,12.5969504640361));
#431688=CARTESIAN_POINT('Origin',(-2.53603084286427,0.916535474818858,12.584524458991));
#431689=CARTESIAN_POINT('Origin',(-2.53603084286427,0.916535474818858,12.584524458991));
#431690=CARTESIAN_POINT('Ctrl Pts',(-2.5343507043209,0.88218862438177,12.5893111709658));
#431691=CARTESIAN_POINT('Ctrl Pts',(-2.52302979479693,0.882732354194952,
12.5770542771492));
#431692=CARTESIAN_POINT('Ctrl Pts',(-2.52075360628343,0.898937990273366,
12.5737548217797));
#431693=CARTESIAN_POINT('Ctrl Pts',(-2.5591057340396,0.880999669761492,
12.5663937883685));
#431694=CARTESIAN_POINT('Ctrl Pts',(-2.54777038312331,0.881544093177552,
12.5540940315303));
#431695=CARTESIAN_POINT('Ctrl Pts',(-2.545490321136,0.897800393883671,12.5508374392248));
#431696=CARTESIAN_POINT('Ctrl Pts',(-2.58383578623695,0.879811914781843,
12.5434499600945));
#431697=CARTESIAN_POINT('Ctrl Pts',(-2.57246358005819,0.88035810831233,
12.5311293540533));
#431698=CARTESIAN_POINT('Ctrl Pts',(-2.57020281348901,0.896662730328217,
12.5278936106989));
#431699=CARTESIAN_POINT('Ctrl Pts',(-2.60854281743612,0.878625265473343,
12.5204817579905));
#431700=CARTESIAN_POINT('Ctrl Pts',(-2.59711432660861,0.87917416228852,
12.5081597038247));
#431701=CARTESIAN_POINT('Ctrl Pts',(-2.59489296537332,0.895524990987918,
12.5049254088044));
#431702=CARTESIAN_POINT('Ctrl Pts',(-2.59077959786119,0.879478411772282,
12.5369868989719));
#431703=CARTESIAN_POINT('Ctrl Pts',(-2.59171003013044,0.879433724379648,
12.5342545179733));
#431704=CARTESIAN_POINT('Ctrl Pts',(-2.5926039767278,0.879515679211253,
12.5314872231885));
#431705=CARTESIAN_POINT('Ctrl Pts',(-2.59340597678606,0.879775327081827,
12.5287124745063));
#431706=CARTESIAN_POINT('Ctrl Pts',(-2.59412926024632,0.880009490419281,
12.5262100684184));
#431707=CARTESIAN_POINT('Ctrl Pts',(-2.5947767278187,0.880388876871923,
12.5237004536639));
#431708=CARTESIAN_POINT('Ctrl Pts',(-2.5953259831631,0.880977195780399,
12.5212220730815));
#431709=CARTESIAN_POINT('Ctrl Pts',(-2.59574648564362,0.881427604798481,
12.5193246583486));
#431710=CARTESIAN_POINT('Ctrl Pts',(-2.59611398545653,0.882006289955195,
12.5174178313691));
#431711=CARTESIAN_POINT('Ctrl Pts',(-2.59635830214115,0.882780547057912,
12.5155812248348));
#431712=CARTESIAN_POINT('Ctrl Pts',(-2.596462382362,0.883110384745324,12.5147988205794));
#431713=CARTESIAN_POINT('Ctrl Pts',(-2.59654447707654,0.883475966411407,
12.5140295443047));
#431714=CARTESIAN_POINT('Ctrl Pts',(-2.59660119699856,0.883883109633485,
12.5132817086137));
#431715=CARTESIAN_POINT('Ctrl Pts',(-2.59668703492763,0.884499265823006,
12.5121499604604));
#431716=CARTESIAN_POINT('Ctrl Pts',(-2.59670952797798,0.885224901530192,
12.5110494206568));
#431717=CARTESIAN_POINT('Ctrl Pts',(-2.59663380385397,0.886073086634248,
12.5100666561695));
#431718=CARTESIAN_POINT('Ctrl Pts',(-2.59659032323634,0.8865601125678,12.5095023550641));
#431719=CARTESIAN_POINT('Ctrl Pts',(-2.59651330758367,0.88709311249712,
12.5089719619137));
#431720=CARTESIAN_POINT('Ctrl Pts',(-2.59639787914041,0.88766118252928,
12.5085043804652));
#431721=CARTESIAN_POINT('Ctrl Pts',(-2.59622896464932,0.88849247902502,
12.5078201359221));
#431722=CARTESIAN_POINT('Ctrl Pts',(-2.59597170835315,0.88942274630422,
12.5072563000949));
#431723=CARTESIAN_POINT('Ctrl Pts',(-2.59563538869309,0.890386669471616,
12.5068768744332));
#431724=CARTESIAN_POINT('Ctrl Pts',(-2.59539287906586,0.891081724432006,
12.5066032824114));
#431725=CARTESIAN_POINT('Ctrl Pts',(-2.59510505738726,0.891806509298019,
12.5064197834844));
#431726=CARTESIAN_POINT('Ctrl Pts',(-2.59479039873085,0.892521504212145,
12.5063282718343));
#431727=CARTESIAN_POINT('Ctrl Pts',(-2.59433109450834,0.893565175429939,
12.5061946931565));
#431728=CARTESIAN_POINT('Ctrl Pts',(-2.59380576397003,0.894610722322953,
12.5062515701262));
#431729=CARTESIAN_POINT('Ctrl Pts',(-2.59326082840621,0.895600199381803,
12.5064436508398));
#431730=CARTESIAN_POINT('',(-2.52075360628343,0.898937990273366,12.5737548217797));
#431731=CARTESIAN_POINT('Origin',(-2.53540612154272,0.904163293764673,12.5893111709658));
#431732=CARTESIAN_POINT('Ctrl Pts',(-2.59326082840621,0.895600199381803,
12.5064436508398));
#431733=CARTESIAN_POINT('Ctrl Pts',(-2.58252789784408,0.896094759084691,
12.5164271754438));
#431734=CARTESIAN_POINT('Ctrl Pts',(-2.57179070313345,0.89658930611674,
12.5264061185523));
#431735=CARTESIAN_POINT('Ctrl Pts',(-2.56104909413815,0.897083840977176,
12.536380305637));
#431736=CARTESIAN_POINT('Ctrl Pts',(-2.54762426152707,0.897701909250244,
12.5488460165097));
#431737=CARTESIAN_POINT('Ctrl Pts',(-2.53419252986739,0.898319958669642,
12.5613043021964));
#431738=CARTESIAN_POINT('Ctrl Pts',(-2.52075360628343,0.898937990273366,
12.5737548217797));
#431739=CARTESIAN_POINT('Ctrl Pts',(-2.51278080633585,0.941872008709569,
12.5893111709658));
#431740=CARTESIAN_POINT('Ctrl Pts',(-2.50442319798712,0.934216356075794,
12.5770542771492));
#431741=CARTESIAN_POINT('Ctrl Pts',(-2.51303331912251,0.920299837513707,
12.5737548217797));
#431742=CARTESIAN_POINT('Ctrl Pts',(-2.50498323043713,0.934729351387608,
12.5928319619712));
#431743=CARTESIAN_POINT('Ctrl Pts',(-2.50156688092093,0.927182035814867,
12.5821634970842));
#431744=CARTESIAN_POINT('Ctrl Pts',(-2.51018647537985,0.91770490050594,
12.5773203894503));
#431745=CARTESIAN_POINT('Ctrl Pts',(-2.49847632445183,0.919294187836864,
12.5969440695591));
#431746=CARTESIAN_POINT('Ctrl Pts',(-2.49982540057543,0.915507561876375,
12.5878292599214));
#431747=CARTESIAN_POINT('Ctrl Pts',(-2.50786916661021,0.912202698477325,
12.5813877129824));
#431748=CARTESIAN_POINT('Ctrl Pts',(-2.50882518112397,0.890500500835704,
12.596957478804));
#431749=CARTESIAN_POINT('Ctrl Pts',(-2.50748615054405,0.89425916951689,
12.5878468778671));
#431750=CARTESIAN_POINT('Ctrl Pts',(-2.51157877942085,0.901899056349452,
12.5814011370086));
#431751=CARTESIAN_POINT('Ctrl Pts',(-2.52377305774301,0.882696656160039,
12.5928371701607));
#431752=CARTESIAN_POINT('Ctrl Pts',(-2.51632898274018,0.886318922447337,
12.5821692192951));
#431753=CARTESIAN_POINT('Ctrl Pts',(-2.51689324154602,0.899113664881937,
12.5773318885715));
#431754=CARTESIAN_POINT('Ctrl Pts',(-2.53435070432089,0.882188624381715,
12.5893111709658));
#431755=CARTESIAN_POINT('Ctrl Pts',(-2.52302979479692,0.882732354194897,
12.5770542771492));
#431756=CARTESIAN_POINT('Ctrl Pts',(-2.52075360628343,0.898937990273311,
12.5737548217797));
#431757=CARTESIAN_POINT('',(-2.51303331912251,0.920299837513707,12.5737548217797));
#431758=CARTESIAN_POINT('Origin',(-2.52764095826811,0.925649312122681,12.5893111709658));
#431759=CARTESIAN_POINT('Ctrl Pts',(-2.52075360628343,0.898937990273311,
12.5737548217797));
#431760=CARTESIAN_POINT('Ctrl Pts',(-2.51975156717454,0.898953393366479,
12.5746934679442));
#431761=CARTESIAN_POINT('Ctrl Pts',(-2.51864555970812,0.899153600565276,
12.5756680099006));
#431762=CARTESIAN_POINT('Ctrl Pts',(-2.5175608229726,0.899512557223679,
12.5765688348656));
#431763=CARTESIAN_POINT('Ctrl Pts',(-2.51727365093031,0.899607587025209,
12.5768073183026));
#431764=CARTESIAN_POINT('Ctrl Pts',(-2.51698795074734,0.899713486674167,
12.5770407398754));
#431765=CARTESIAN_POINT('Ctrl Pts',(-2.51670586491899,0.899829239550346,
12.5772674179684));
#431766=CARTESIAN_POINT('Ctrl Pts',(-2.51554826095865,0.900304258053291,
12.5781976435658));
#431767=CARTESIAN_POINT('Ctrl Pts',(-2.51439005797669,0.900982626194758,
12.5790594849312));
#431768=CARTESIAN_POINT('Ctrl Pts',(-2.51333386495786,0.901860207547482,
12.5797571720116));
#431769=CARTESIAN_POINT('Ctrl Pts',(-2.51264571722877,0.902431983353795,
12.580211740231));
#431770=CARTESIAN_POINT('Ctrl Pts',(-2.51198159710695,0.903128748338649,
12.5806009430798));
#431771=CARTESIAN_POINT('Ctrl Pts',(-2.51140108017891,0.903913676845319,
12.5808812374708));
#431772=CARTESIAN_POINT('Ctrl Pts',(-2.51090222355325,0.904588190829869,
12.5811221033394));
#431773=CARTESIAN_POINT('Ctrl Pts',(-2.51045498263095,0.905341686224759,
12.581287365893));
#431774=CARTESIAN_POINT('Ctrl Pts',(-2.51009177047712,0.906135890363982,
12.581359338449));
#431775=CARTESIAN_POINT('Ctrl Pts',(-2.51004129148778,0.906246268339646,
12.5813693411482));
#431776=CARTESIAN_POINT('Ctrl Pts',(-2.50999237589608,0.906357427284618,
12.5813775999465));
#431777=CARTESIAN_POINT('Ctrl Pts',(-2.50994504952647,0.906469260081351,
12.5813841266931));
#431778=CARTESIAN_POINT('Ctrl Pts',(-2.50986475461642,0.906658997946903,
12.5813952001081));
#431779=CARTESIAN_POINT('Ctrl Pts',(-2.50978905726936,0.906852183577215,
12.5814007534795));
#431780=CARTESIAN_POINT('Ctrl Pts',(-2.50971817407091,0.907048804781627,
12.5814005856065));
#431781=CARTESIAN_POINT('Ctrl Pts',(-2.50939369850195,0.907948859781517,
12.5813998171494));
#431782=CARTESIAN_POINT('Ctrl Pts',(-2.50919220230355,0.908858604186674,
12.58127954464));
#431783=CARTESIAN_POINT('Ctrl Pts',(-2.50908594019762,0.909766474481359,
12.5810700125799));
#431784=CARTESIAN_POINT('Ctrl Pts',(-2.50895758767257,0.910863078428028,
12.5808169217085));
#431785=CARTESIAN_POINT('Ctrl Pts',(-2.50898479156574,0.911958992798614,
12.5804173076348));
#431786=CARTESIAN_POINT('Ctrl Pts',(-2.50913913343118,0.912958819761757,
12.5799304713245));
#431787=CARTESIAN_POINT('Ctrl Pts',(-2.50933041162515,0.914197920347066,
12.5793271277669));
#431788=CARTESIAN_POINT('Ctrl Pts',(-2.50969700319774,0.915371216314544,
12.5785808224116));
#431789=CARTESIAN_POINT('Ctrl Pts',(-2.51019318203673,0.916438709838056,
12.5777485681082));
#431790=CARTESIAN_POINT('Ctrl Pts',(-2.51093254286728,0.918029392140734,
12.576508418016));
#431791=CARTESIAN_POINT('Ctrl Pts',(-2.51194718515588,0.919374650679806,
12.5750928681475));
#431792=CARTESIAN_POINT('Ctrl Pts',(-2.51303331912251,0.920299837513707,
12.5737548217797));
#431793=CARTESIAN_POINT('Ctrl Pts',(-2.51303331912251,0.920299837513707,
12.5737548217797));
#431794=CARTESIAN_POINT('Ctrl Pts',(-2.50442319798712,0.934216356075795,
12.5770542771492));
#431795=CARTESIAN_POINT('Ctrl Pts',(-2.51278080633585,0.94187200870957,
12.5893111709658));
#431796=CARTESIAN_POINT('Ctrl Pts',(-2.53132460581228,0.936986472447185,
12.5508408821982));
#431797=CARTESIAN_POINT('Ctrl Pts',(-2.52268507480955,0.950944417449307,
12.55409748406));
#431798=CARTESIAN_POINT('Ctrl Pts',(-2.53105334532603,0.958609836735127,
12.5663972313419));
#431799=CARTESIAN_POINT('Ctrl Pts',(-2.54959722927643,0.953657678028315,
12.52790050457));
#431800=CARTESIAN_POINT('Ctrl Pts',(-2.54091197579121,0.967640440603685,
12.5311362602938));
#431801=CARTESIAN_POINT('Ctrl Pts',(-2.54930745032697,0.97533077904262,
12.5434568539655));
#431802=CARTESIAN_POINT('Ctrl Pts',(-2.56785263055407,0.970314663546385,
12.5049357605811));
#431803=CARTESIAN_POINT('Ctrl Pts',(-2.55910754698467,0.984307765359549,
12.5081700652078));
#431804=CARTESIAN_POINT('Ctrl Pts',(-2.5675445650924,0.992036158124872,
12.5204921097672));
#431805=CARTESIAN_POINT('Ctrl Pts',(-2.56665390827743,0.969220901756311,
12.5064436508395));
#431806=CARTESIAN_POINT('Ctrl Pts',(-2.56642323306549,0.970419082350872,
12.5062361689309));
#431807=CARTESIAN_POINT('Ctrl Pts',(-2.5661322566399,0.971655255615505,
12.5061871075061));
#431808=CARTESIAN_POINT('Ctrl Pts',(-2.56578380658317,0.972834068238053,
12.5063648335164));
#431809=CARTESIAN_POINT('Ctrl Pts',(-2.56562551907411,0.973369557643392,
12.5064455676329));
#431810=CARTESIAN_POINT('Ctrl Pts',(-2.56545295261105,0.973900616980473,
12.506574497099));
#431811=CARTESIAN_POINT('Ctrl Pts',(-2.56527250682241,0.974404151231364,
12.5067492519495));
#431812=CARTESIAN_POINT('Ctrl Pts',(-2.56490989400573,0.975416022854365,
12.5071004286051));
#431813=CARTESIAN_POINT('Ctrl Pts',(-2.56450136974474,0.976353671669394,
12.5076537929613));
#431814=CARTESIAN_POINT('Ctrl Pts',(-2.56408626710693,0.977150500161891,
12.5083435010505));
#431815=CARTESIAN_POINT('Ctrl Pts',(-2.56406013391521,0.977200665277364,
12.5083869222964));
#431816=CARTESIAN_POINT('Ctrl Pts',(-2.56403396121578,0.977250272214424,
12.5084308732337));
#431817=CARTESIAN_POINT('Ctrl Pts',(-2.56400775335133,0.977299304733193,
12.5084753333615));
#431818=CARTESIAN_POINT('Ctrl Pts',(-2.56379753168718,0.977692610250802,
12.5088319622689));
#431819=CARTESIAN_POINT('Ctrl Pts',(-2.56358191736201,0.978057549672773,
12.509227847131));
#431820=CARTESIAN_POINT('Ctrl Pts',(-2.56336973244526,0.978384695761815,
12.5096423454524));
#431821=CARTESIAN_POINT('Ctrl Pts',(-2.56270483882527,0.979409826816081,
12.5109411997424));
#431822=CARTESIAN_POINT('Ctrl Pts',(-2.56204083577664,0.980132171637527,
12.5124831113042));
#431823=CARTESIAN_POINT('Ctrl Pts',(-2.56141579146133,0.980638371281332,
12.5140723025008));
#431824=CARTESIAN_POINT('Ctrl Pts',(-2.5613572241244,0.980685802742381,
12.5142212114565));
#431825=CARTESIAN_POINT('Ctrl Pts',(-2.56129900046128,0.980731366034844,
12.5143705582413));
#431826=CARTESIAN_POINT('Ctrl Pts',(-2.56124115425957,0.980775149239031,
12.5145201959299));
#431827=CARTESIAN_POINT('Ctrl Pts',(-2.56049803367459,0.981337609683192,
12.5164425148273));
#431828=CARTESIAN_POINT('Ctrl Pts',(-2.55979822502288,0.981634132246162,
12.5184635205941));
#431829=CARTESIAN_POINT('Ctrl Pts',(-2.55912977089943,0.981754131686319,
12.5205025929158));
#431830=CARTESIAN_POINT('Ctrl Pts',(-2.55874204101279,0.981823736117943,
12.5216853356836));
#431831=CARTESIAN_POINT('Ctrl Pts',(-2.55836564606957,0.981834300267755,
12.5228750347131));
#431832=CARTESIAN_POINT('Ctrl Pts',(-2.55800415951575,0.98180371726661,
12.5240609649613));
#431833=CARTESIAN_POINT('Ctrl Pts',(-2.55711691016249,0.981728652931021,
12.5269717671326));
#431834=CARTESIAN_POINT('Ctrl Pts',(-2.55629537912022,0.98139323418563,
12.5299036066169));
#431835=CARTESIAN_POINT('Ctrl Pts',(-2.55552013602678,0.980881912102984,
12.5328133004019));
#431836=CARTESIAN_POINT('Ctrl Pts',(-2.55514797420086,0.980636447729916,
12.5342101228451));
#431837=CARTESIAN_POINT('Ctrl Pts',(-2.55478723260943,0.980350314175644,
12.5356023438238));
#431838=CARTESIAN_POINT('Ctrl Pts',(-2.55443917227924,0.980031487551613,
12.5369868989719));
#431839=CARTESIAN_POINT('Origin',(-11.9498738845008,9.59352869647897,-1.24102268496923));
#431840=CARTESIAN_POINT('Ctrl Pts',(-2.59073784982797,0.879480377135765,
12.5369868989719));
#431841=CARTESIAN_POINT('Ctrl Pts',(-2.60606050627276,0.878773621761026,
12.5369868989719));
#431842=CARTESIAN_POINT('Ctrl Pts',(-2.61069567797988,0.864151772119807,
12.5369868989719));
#431843=CARTESIAN_POINT('Ctrl Pts',(-2.59591750392105,0.879241400036461,
12.5218025310015));
#431844=CARTESIAN_POINT('Ctrl Pts',(-2.6070953170942,0.875405731076495,
12.5216901060418));
#431845=CARTESIAN_POINT('Ctrl Pts',(-2.61068156416115,0.864196349346829,
12.5161920673677));
#431846=CARTESIAN_POINT('Ctrl Pts',(-2.59965564843752,0.88397028434133,
12.5042015548895));
#431847=CARTESIAN_POINT('Ctrl Pts',(-2.60524603569246,0.880788317126344,
12.4980677368513));
#431848=CARTESIAN_POINT('Ctrl Pts',(-2.60741695972008,0.874347985722612,
12.4907278922778));
#431849=CARTESIAN_POINT('Ctrl Pts',(-2.59324192300507,0.895593670284452,
12.506463626192));
#431850=CARTESIAN_POINT('Ctrl Pts',(-2.59942624274697,0.897729467013142,
12.4999376786891));
#431851=CARTESIAN_POINT('Ctrl Pts',(-2.59935071027332,0.897703381361547,
12.4906970594712));
#431852=CARTESIAN_POINT('Origin',(-2.58972418063936,0.857503742389379,12.5369868989719));
#431853=CARTESIAN_POINT('Origin',(-2.58972418063936,0.857503742389379,14.));
#431854=CARTESIAN_POINT('Origin',(-2.58972418063936,0.857503742389379,13.7435492065112));
#431855=CARTESIAN_POINT('Ctrl Pts',(-2.56604800116064,0.880666213749779,
13.793642941384));
#431856=CARTESIAN_POINT('Ctrl Pts',(-2.576849141578,0.880174701094858,13.8071662555867));
#431857=CARTESIAN_POINT('Ctrl Pts',(-2.57858464179707,0.863233407678336,
13.8103758687955));
#431858=CARTESIAN_POINT('Ctrl Pts',(-2.58264998614256,0.879868843143524,
13.7804579775005));
#431859=CARTESIAN_POINT('Ctrl Pts',(-2.59597715616263,0.879252230634105,
13.7901904343351));
#431860=CARTESIAN_POINT('Ctrl Pts',(-2.60009766788152,0.864044426475094,
13.7927914348262));
#431861=CARTESIAN_POINT('Ctrl Pts',(-2.59242419950251,0.879399401021213,
13.7597120340895));
#431862=CARTESIAN_POINT('Ctrl Pts',(-2.60784722354869,0.878680082425412,
13.7635825532445));
#431863=CARTESIAN_POINT('Ctrl Pts',(-2.61278483774422,0.864497139070781,
13.7651073818884));
#431864=CARTESIAN_POINT('Ctrl Pts',(-2.59051018472259,0.879491328536952,
13.7381884353898));
#431865=CARTESIAN_POINT('Ctrl Pts',(-2.60557224603145,0.878789744789382,
13.7368803041982));
#431866=CARTESIAN_POINT('Ctrl Pts',(-2.6103003305119,0.864407990575627,
13.7363986145813));
#431867=CARTESIAN_POINT('Origin',(-2.56902102722068,0.858498090212475,13.7902182540695));
#431868=CARTESIAN_POINT('Ctrl Pts',(-2.53434677261819,0.882188812456973,
13.8235227101244));
#431869=CARTESIAN_POINT('Ctrl Pts',(-2.54583081984969,0.881641685868309,
13.8358800583119));
#431870=CARTESIAN_POINT('Ctrl Pts',(-2.54802557414952,0.865215818992561,
13.8390832900376));
#431871=CARTESIAN_POINT('Ctrl Pts',(-2.54626061865845,0.881616604607372,
13.8124254819053));
#431872=CARTESIAN_POINT('Ctrl Pts',(-2.55776696773367,0.881068415228781,
13.8247886449158));
#431873=CARTESIAN_POINT('Ctrl Pts',(-2.55994760105056,0.864619536256662,
13.8279860620657));
#431874=CARTESIAN_POINT('Ctrl Pts',(-2.55816912530053,0.881044653202725,
13.8013225099955));
#431875=CARTESIAN_POINT('Ctrl Pts',(-2.56969234716577,0.880495661693927,
13.8136962257787));
#431876=CARTESIAN_POINT('Ctrl Pts',(-2.57186412217945,0.864023800288131,
13.8168830918626));
#431877=CARTESIAN_POINT('Ctrl Pts',(-2.57007250029219,0.880472948265155,
13.7902140179785));
#431878=CARTESIAN_POINT('Ctrl Pts',(-2.58160752072225,0.879923398246903,
13.802602731458));
#431879=CARTESIAN_POINT('Ctrl Pts',(-2.58377535396331,0.863428591441119,
13.8057746032558));
#431880=CARTESIAN_POINT('Origin',(-2.53329528709908,0.860213954998868,13.8235269408515));
#431881=CARTESIAN_POINT('Ctrl Pts',(-2.51278080633585,0.94187200870957,
13.8235269408515));
#431882=CARTESIAN_POINT('Ctrl Pts',(-2.52148758767358,0.94984750728508,
13.8362179249168));
#431883=CARTESIAN_POINT('Ctrl Pts',(-2.51214073195516,0.964140837626054,
13.8391868794938));
#431884=CARTESIAN_POINT('Ctrl Pts',(-2.50481448039544,0.934574774665753,
13.8400110824519));
#431885=CARTESIAN_POINT('Ctrl Pts',(-2.50948443629105,0.943491801905506,
13.8494522556836));
#431886=CARTESIAN_POINT('Ctrl Pts',(-2.49910630118824,0.952048798996971,
13.85569149686));
#431887=CARTESIAN_POINT('Ctrl Pts',(-2.49835886399634,0.919617410494477,
13.8586819406588));
#431888=CARTESIAN_POINT('Ctrl Pts',(-2.49689212333642,0.923716765989122,
13.868010383617));
#431889=CARTESIAN_POINT('Ctrl Pts',(-2.48852389711468,0.927161422241115,
13.8744918421245));
#431890=CARTESIAN_POINT('Ctrl Pts',(-2.50894444581712,0.890172258848369,
13.8587686893867));
#431891=CARTESIAN_POINT('Ctrl Pts',(-2.51039807948191,0.886109368610075,
13.8680909899357));
#431892=CARTESIAN_POINT('Ctrl Pts',(-2.50614820345524,0.878144762200234,
13.8745789365163));
#431893=CARTESIAN_POINT('Ctrl Pts',(-2.52354225223554,0.882707741467401,
13.8400379222776));
#431894=CARTESIAN_POINT('Ctrl Pts',(-2.53282882379497,0.878830909954466,
13.8494748685453));
#431895=CARTESIAN_POINT('Ctrl Pts',(-2.5303213736518,0.865622056898879,
13.8557104837033));
#431896=CARTESIAN_POINT('Ctrl Pts',(-2.53435070432044,0.882188624375176,
13.8235269408542));
#431897=CARTESIAN_POINT('Ctrl Pts',(-2.54614459075977,0.881622178043516,
13.8362179249195));
#431898=CARTESIAN_POINT('Ctrl Pts',(-2.54809516572253,0.864655791823373,
13.8391868794965));
#431899=CARTESIAN_POINT('Origin',(-2.49792065440359,0.958094705296459,13.8235269408515));
#431900=CARTESIAN_POINT('Ctrl Pts',(-2.53915225840624,0.966028522952471,
13.7902140241683));
#431901=CARTESIAN_POINT('Ctrl Pts',(-2.54767077875461,0.973825535615466,
13.8026027327198));
#431902=CARTESIAN_POINT('Ctrl Pts',(-2.53879247206483,0.98789513413836,
13.8057746032556));
#431903=CARTESIAN_POINT('Ctrl Pts',(-2.53036464765615,0.957978983827332,
13.8013225161808));
#431904=CARTESIAN_POINT('Ctrl Pts',(-2.53887445256273,0.965768024097925,
13.8136962270464));
#431905=CARTESIAN_POINT('Ctrl Pts',(-2.53001384607697,0.97982249875968,
13.8168830918628));
#431906=CARTESIAN_POINT('Ctrl Pts',(-2.521573248488,0.949925974473432,13.8124254880875));
#431907=CARTESIAN_POINT('Ctrl Pts',(-2.53007059187678,0.957703611027938,
13.8247886461867));
#431908=CARTESIAN_POINT('Ctrl Pts',(-2.52123148983828,0.971746076529088,
13.8279860620656));
#431909=CARTESIAN_POINT('Ctrl Pts',(-2.51277790753183,0.941869354402355,
13.8235227163066));
#431910=CARTESIAN_POINT('Ctrl Pts',(-2.52125878137466,0.949631915970467,
13.8358800595848));
#431911=CARTESIAN_POINT('Ctrl Pts',(-2.51244524948573,0.963665713975314,
13.8390832900376));
#431912=CARTESIAN_POINT('Origin',(-2.52429501445589,0.98225388224919,13.7902182540695));
#431913=CARTESIAN_POINT('Ctrl Pts',(-2.55424016022377,0.97984922793118,
13.7382347919292));
#431914=CARTESIAN_POINT('Ctrl Pts',(-2.56538389119101,0.990024449248841,
13.7369371795942));
#431915=CARTESIAN_POINT('Ctrl Pts',(-2.55981317938335,1.00411384054075,
13.7364597369711));
#431916=CARTESIAN_POINT('Ctrl Pts',(-2.55563498692476,0.981126902560485,
13.7595490285574));
#431917=CARTESIAN_POINT('Ctrl Pts',(-2.56704391981487,0.991545638411246,
13.7633824266926));
#431918=CARTESIAN_POINT('Ctrl Pts',(-2.56175676237833,1.00561474025,13.7648920890506));
#431919=CARTESIAN_POINT('Ctrl Pts',(-2.54852144716987,0.974610831941804,
13.780380659011));
#431920=CARTESIAN_POINT('Ctrl Pts',(-2.55839340614298,0.983618679189502,
13.7901039518744));
#431921=CARTESIAN_POINT('Ctrl Pts',(-2.55185043327982,0.997960051074283,
13.7926933640892));
#431922=CARTESIAN_POINT('Ctrl Pts',(-2.53615652708199,0.963284446693457,
13.7936647693663));
#431923=CARTESIAN_POINT('Ctrl Pts',(-2.54415198315131,0.970567716164538,
13.8072068914933));
#431924=CARTESIAN_POINT('Ctrl Pts',(-2.53463680218607,0.984713584856361,
13.8104111085397));
#431925=CARTESIAN_POINT('Origin',(-2.53957902034698,0.996254184138503,13.7435492065112));
#431926=CARTESIAN_POINT('Origin',(-2.53957902034698,0.996254184138503,14.));
#431927=CARTESIAN_POINT('Origin',(-2.53957902034698,0.996254184138503,12.5369868989719));
#431928=CARTESIAN_POINT('Ctrl Pts',(-2.56663671038155,0.969214407468799,
12.506462012331));
#431929=CARTESIAN_POINT('Ctrl Pts',(-2.5727537277133,0.971524318062958,
12.4999388158272));
#431930=CARTESIAN_POINT('Ctrl Pts',(-2.57268135537629,0.971496988791367,
12.4907030323752));
#431931=CARTESIAN_POINT('Ctrl Pts',(-2.56413572086239,0.982251801172283,
12.5042014951932));
#431932=CARTESIAN_POINT('Ctrl Pts',(-2.56640009604014,0.988269583336049,
12.4980716682127));
#431933=CARTESIAN_POINT('Ctrl Pts',(-2.56395526462324,0.994605857049262,
12.4907355092743));
#431934=CARTESIAN_POINT('Ctrl Pts',(-2.55823938542484,0.983500372216855,
12.5218047446509));
#431935=CARTESIAN_POINT('Ctrl Pts',(-2.56437842141187,0.993591512295486,
12.5216906929434));
#431936=CARTESIAN_POINT('Ctrl Pts',(-2.55997551240968,1.00449954358663,
12.5161988840776));
#431937=CARTESIAN_POINT('Ctrl Pts',(-2.55441082176292,0.980005563681427,
12.5369868989719));
#431938=CARTESIAN_POINT('Ctrl Pts',(-2.56573307478275,0.990340558508506,
12.5369868989719));
#431939=CARTESIAN_POINT('Ctrl Pts',(-2.55995852619355,1.00454126694547,
12.5369868989719));
#431940=CARTESIAN_POINT('Origin',(-4.84514877968061E-31,-3.40079961985221E-31,
12.5));
#431941=CARTESIAN_POINT('Origin',(-2.58119104811554,0.733923044064313,12.5));
#431942=CARTESIAN_POINT('',(-2.58119104811554,0.733923044064313,12.5893111709658));
#431943=CARTESIAN_POINT('',(-2.58119104811554,0.733923044064313,13.8235269408515));
#431944=CARTESIAN_POINT('',(-2.58119104811554,0.733923044064313,12.5));
#431945=CARTESIAN_POINT('',(-2.609446846865,0.755852078156851,13.7902182540695));
#431946=CARTESIAN_POINT('',(-2.58119104811554,0.733923044064313,13.8235269408515));
#431947=CARTESIAN_POINT('',(-2.62582115106377,0.768560006826658,13.7435492065112));
#431948=CARTESIAN_POINT('Origin',(-2.57195010640843,0.726750832130225,13.7445212918697));
#431949=CARTESIAN_POINT('',(-2.62582115106377,0.768560006826658,12.5369868989719));
#431950=CARTESIAN_POINT('',(-2.62582115106377,0.768560006826658,12.5));
#431951=CARTESIAN_POINT('Ctrl Pts',(-2.62582115106377,0.768560006826658,
12.5369868989719));
#431952=CARTESIAN_POINT('Ctrl Pts',(-2.6109553002419,0.757022773270534,
12.5544431401645));
#431953=CARTESIAN_POINT('Ctrl Pts',(-2.59607881696842,0.745477287978329,
12.5718848856037));
#431954=CARTESIAN_POINT('Ctrl Pts',(-2.58119104811554,0.733923044064313,
12.5893111709658));
#431955=CARTESIAN_POINT('Origin',(-2.87051847641971,0.637142042272538,12.5));
#431956=CARTESIAN_POINT('',(-2.65384464771224,0.665379431058958,13.7435492065112));
#431957=CARTESIAN_POINT('',(-2.63329143090733,0.668057969474022,13.7902182540695));
#431958=CARTESIAN_POINT('Origin',(-2.57928112945653,0.675096705483978,13.7418732680456));
#431959=CARTESIAN_POINT('',(-2.59782442414822,0.672680104343387,13.8235269408515));
#431960=CARTESIAN_POINT('',(-2.63329143090733,0.668057969474022,13.7902182540695));
#431961=CARTESIAN_POINT('',(-2.59782442414822,0.672680104343387,12.5893111709658));
#431962=CARTESIAN_POINT('',(-2.59782442414822,0.672680104343387,12.5));
#431963=CARTESIAN_POINT('',(-2.65384464771224,0.665379431058958,12.5369868989719));
#431964=CARTESIAN_POINT('Ctrl Pts',(-2.59782442414822,0.672680104343387,
12.5893111709658));
#431965=CARTESIAN_POINT('Ctrl Pts',(-2.61651172452203,0.670244736079616,
12.5718848856037));
#431966=CARTESIAN_POINT('Ctrl Pts',(-2.63518485910551,0.667811213931415,
12.5544431401645));
#431967=CARTESIAN_POINT('Ctrl Pts',(-2.65384464771224,0.665379431058958,
12.5369868989719));
#431968=CARTESIAN_POINT('',(-2.65384464771224,0.665379431058958,12.5));
#431969=CARTESIAN_POINT('Origin',(-2.60226668190707,0.706766860877324,12.5));
#431970=CARTESIAN_POINT('',(-2.56881829496413,0.698842494461434,13.8587068136939));
#431971=CARTESIAN_POINT('Ctrl Pts',(-2.59782442414722,0.672680104336852,
13.8235269408542));
#431972=CARTESIAN_POINT('Ctrl Pts',(-2.59608681930503,0.672906552652186,
13.8262006681044));
#431973=CARTESIAN_POINT('Ctrl Pts',(-2.5943310868423,0.673310571898458,
13.8288634856214));
#431974=CARTESIAN_POINT('Ctrl Pts',(-2.59256002583027,0.673879124773476,
13.8314912288862));
#431975=CARTESIAN_POINT('Ctrl Pts',(-2.59073424460335,0.67446524414411,
13.8342001611531));
#431976=CARTESIAN_POINT('Ctrl Pts',(-2.58888999311657,0.67522639928405,
13.8368750301949));
#431977=CARTESIAN_POINT('Ctrl Pts',(-2.58702403943955,0.6761930667517,13.8394886372969));
#431978=CARTESIAN_POINT('Ctrl Pts',(-2.58687992731091,0.676267724825033,
13.8396904925131));
#431979=CARTESIAN_POINT('Ctrl Pts',(-2.58673569237944,0.67634362987535,
13.8398919674349));
#431980=CARTESIAN_POINT('Ctrl Pts',(-2.58659133753637,0.676420806515196,
13.8400930404591));
#431981=CARTESIAN_POINT('Ctrl Pts',(-2.58434219196403,0.677623270485919,
13.8432258934518));
#431982=CARTESIAN_POINT('Ctrl Pts',(-2.58207488287958,0.679127293889516,
13.8462331177034));
#431983=CARTESIAN_POINT('Ctrl Pts',(-2.57991668295157,0.680964211164284,
13.8489036603661));
#431984=CARTESIAN_POINT('Ctrl Pts',(-2.57921049481889,0.681565271873869,
13.8497774930041));
#431985=CARTESIAN_POINT('Ctrl Pts',(-2.57851623670105,0.682201943407981,
13.85061494757));
#431986=CARTESIAN_POINT('Ctrl Pts',(-2.5778390740993,0.682875222351935,
13.8514076489583));
#431987=CARTESIAN_POINT('Ctrl Pts',(-2.57640677753513,0.684299304419751,
13.8530843267192));
#431988=CARTESIAN_POINT('Ctrl Pts',(-2.57491235982633,0.686029141931973,
13.8546805203176));
#431989=CARTESIAN_POINT('Ctrl Pts',(-2.57354580789501,0.688053535336556,
13.8559412814273));
#431990=CARTESIAN_POINT('Ctrl Pts',(-2.57336291892827,0.68832446482673,
13.8561100121513));
#431991=CARTESIAN_POINT('Ctrl Pts',(-2.57318229953109,0.688600596147636,
13.8562727473908));
#431992=CARTESIAN_POINT('Ctrl Pts',(-2.57300437574977,0.688881832521115,
13.8564289040185));
#431993=CARTESIAN_POINT('Ctrl Pts',(-2.57219749343134,0.690157236266359,
13.8571370725437));
#431994=CARTESIAN_POINT('Ctrl Pts',(-2.57143379050539,0.691561266244882,
13.8577210840554));
#431995=CARTESIAN_POINT('Ctrl Pts',(-2.57076873319358,0.693053370758716,
13.8581177131616));
#431996=CARTESIAN_POINT('Ctrl Pts',(-2.570581430164,0.69347359874649,13.8582294175695));
#431997=CARTESIAN_POINT('Ctrl Pts',(-2.57040180658542,0.693900709935634,
13.8583265086086));
#431998=CARTESIAN_POINT('Ctrl Pts',(-2.57023072830563,0.69433356616058,
13.8584082369006));
#431999=CARTESIAN_POINT('Ctrl Pts',(-2.56998493469404,0.694955464480841,
13.8585256585398));
#432000=CARTESIAN_POINT('Ctrl Pts',(-2.56975402519097,0.69559707220538,
13.8586122832068));
#432001=CARTESIAN_POINT('Ctrl Pts',(-2.5695447411882,0.696241989636382,
13.8586682984299));
#432002=CARTESIAN_POINT('Ctrl Pts',(-2.56937733473164,0.696757859652574,
13.8587131050557));
#432003=CARTESIAN_POINT('Ctrl Pts',(-2.56922169312754,0.697281472767224,
13.8587357943552));
#432004=CARTESIAN_POINT('Ctrl Pts',(-2.56907828333514,0.697813035498819,
13.8587355499465));
#432005=CARTESIAN_POINT('Ctrl Pts',(-2.56898559416724,0.698156597165358,
13.8587353919793));
#432006=CARTESIAN_POINT('Ctrl Pts',(-2.56889897964001,0.698499754358227,
13.8587257282814));
#432007=CARTESIAN_POINT('Ctrl Pts',(-2.56881829496413,0.698842494461434,
13.8587068136939));
#432008=CARTESIAN_POINT('Ctrl Pts',(-2.56881829496413,0.698842494461434,
13.8587068136939));
#432009=CARTESIAN_POINT('Ctrl Pts',(-2.56855292746382,0.699969747975907,
13.8586446046466));
#432010=CARTESIAN_POINT('Ctrl Pts',(-2.56835162487077,0.701092496074216,
13.858482427929));
#432011=CARTESIAN_POINT('Ctrl Pts',(-2.5682099430826,0.702210253049674,
13.8582284286032));
#432012=CARTESIAN_POINT('Ctrl Pts',(-2.56806459404903,0.703356941683728,
13.8579678548414));
#432013=CARTESIAN_POINT('Ctrl Pts',(-2.56798315661897,0.704501371126314,
13.857615680862));
#432014=CARTESIAN_POINT('Ctrl Pts',(-2.56795917617325,0.705597735320246,
13.8571944833187));
#432015=CARTESIAN_POINT('Ctrl Pts',(-2.56789933051843,0.708333824293116,
13.8561433417727));
#432016=CARTESIAN_POINT('Ctrl Pts',(-2.56818973506757,0.710898442238415,
13.8546163505475));
#432017=CARTESIAN_POINT('Ctrl Pts',(-2.56866022482375,0.713174108347192,
13.8528973491087));
#432018=CARTESIAN_POINT('Ctrl Pts',(-2.56874617636078,0.713589838970963,
13.8525833129073));
#432019=CARTESIAN_POINT('Ctrl Pts',(-2.56883802851296,0.713996015455054,
13.8522628768812));
#432020=CARTESIAN_POINT('Ctrl Pts',(-2.56893462456924,0.714392054790332,
13.851937733538));
#432021=CARTESIAN_POINT('Ctrl Pts',(-2.56952452328284,0.716810612062803,
13.8499521282529));
#432022=CARTESIAN_POINT('Ctrl Pts',(-2.570353926929,0.719090509714142,13.847639871647));
#432023=CARTESIAN_POINT('Ctrl Pts',(-2.57130374518305,0.721139390862746,
13.8452109780794));
#432024=CARTESIAN_POINT('Ctrl Pts',(-2.5717310880758,0.722061224901229,
13.8441181685877));
#432025=CARTESIAN_POINT('Ctrl Pts',(-2.57218229971992,0.722936803050407,
13.8430021611332));
#432026=CARTESIAN_POINT('Ctrl Pts',(-2.57264503842641,0.723760665316686,
13.8418824960098));
#432027=CARTESIAN_POINT('Ctrl Pts',(-2.57373549400471,0.725702117785256,
13.8392439765549));
#432028=CARTESIAN_POINT('Ctrl Pts',(-2.57493879250251,0.727451042851449,
13.8364981347964));
#432029=CARTESIAN_POINT('Ctrl Pts',(-2.57622992390006,0.72903146265238,
13.8336931113419));
#432030=CARTESIAN_POINT('Ctrl Pts',(-2.57748740388685,0.730570691172548,
13.8309611966328));
#432031=CARTESIAN_POINT('Ctrl Pts',(-2.57882989517482,0.731951268978667,
13.8281701127185));
#432032=CARTESIAN_POINT('Ctrl Pts',(-2.58025359626469,0.733161155909921,
13.825358068512));
#432033=CARTESIAN_POINT('Ctrl Pts',(-2.58056225619747,0.733423460702361,
13.8247484142932));
#432034=CARTESIAN_POINT('Ctrl Pts',(-2.58087475274221,0.733677570486074,
13.8241378483365));
#432035=CARTESIAN_POINT('Ctrl Pts',(-2.58119104811554,0.733923044064313,
13.8235269408515));
#432036=CARTESIAN_POINT('',(-2.56912638347858,0.697639224614051,12.5969504640361));
#432037=CARTESIAN_POINT('Origin',(-2.60229855934039,0.706775721580128,12.584524458991));
#432038=CARTESIAN_POINT('Origin',(-2.60229855934039,0.706775721580128,12.584524458991));
#432039=CARTESIAN_POINT('Ctrl Pts',(-2.59782442414822,0.672680104343387,
12.5893111709658));
#432040=CARTESIAN_POINT('Ctrl Pts',(-2.58658550304429,0.674144784164871,
12.5770542771492));
#432041=CARTESIAN_POINT('Ctrl Pts',(-2.58563779814648,0.690482027821057,
12.5737548217797));
#432042=CARTESIAN_POINT('Ctrl Pts',(-2.62240017270848,0.669477341134959,
12.5663937883685));
#432043=CARTESIAN_POINT('Ctrl Pts',(-2.61114691479985,0.67094388935897,
12.5540940315304));
#432044=CARTESIAN_POINT('Ctrl Pts',(-2.61019947895433,0.687331944784543,
12.5508374392248));
#432045=CARTESIAN_POINT('Ctrl Pts',(-2.6469511246397,0.666277809475349,
12.5434499600945));
#432046=CARTESIAN_POINT('Ctrl Pts',(-2.63566127838219,0.667749125969949,
12.5311293540532));
#432047=CARTESIAN_POINT('Ctrl Pts',(-2.63473701238633,0.6841837691644,12.5278936106989));
#432048=CARTESIAN_POINT('Ctrl Pts',(-2.67147922229582,0.663081256232907,
12.5204817579905));
#432049=CARTESIAN_POINT('Ctrl Pts',(-2.6601334990149,0.664559854738586,
12.5081597038247));
#432050=CARTESIAN_POINT('Ctrl Pts',(-2.65925227350856,0.681037338967124,
12.5049254088044));
#432051=CARTESIAN_POINT('Ctrl Pts',(-2.65384464771224,0.665379431058958,
12.5369868989719));
#432052=CARTESIAN_POINT('Ctrl Pts',(-2.65476834160751,0.665259053492282,
12.5342545179733));
#432053=CARTESIAN_POINT('Ctrl Pts',(-2.65566599375092,0.665267870679265,
12.5314872231885));
#432054=CARTESIAN_POINT('Ctrl Pts',(-2.65648648893205,0.665461284142814,
12.5287124745063));
#432055=CARTESIAN_POINT('Ctrl Pts',(-2.65722645221213,0.665635714004431,
12.5262100684184));
#432056=CARTESIAN_POINT('Ctrl Pts',(-2.65790268890752,0.665961063462004,
12.5237004536639));
#432057=CARTESIAN_POINT('Ctrl Pts',(-2.65849807010281,0.66650265537824,
12.5212220730815));
#432058=CARTESIAN_POINT('Ctrl Pts',(-2.65895388591238,0.666917290841554,
12.5193246583486));
#432059=CARTESIAN_POINT('Ctrl Pts',(-2.6593673311125,0.667464095824692,
12.5174178313691));
#432060=CARTESIAN_POINT('Ctrl Pts',(-2.65967394399523,0.66821586257285,
12.5155812248348));
#432061=CARTESIAN_POINT('Ctrl Pts',(-2.65980456273132,0.668536119248333,
12.5147988205794));
#432062=CARTESIAN_POINT('Ctrl Pts',(-2.65991618258215,0.668893792990215,
12.5140295443047));
#432063=CARTESIAN_POINT('Ctrl Pts',(-2.66000589972564,0.669294958276603,
12.5132817086137));
#432064=CARTESIAN_POINT('Ctrl Pts',(-2.66014167448565,0.669902067669133,
12.5121499604604));
#432065=CARTESIAN_POINT('Ctrl Pts',(-2.66022323873884,0.670623455490945,
12.5110494206568));
#432066=CARTESIAN_POINT('Ctrl Pts',(-2.66021690154075,0.671474990548134,
12.5100666561695));
#432067=CARTESIAN_POINT('Ctrl Pts',(-2.6602132627362,0.67196394001706,12.5095023550641));
#432068=CARTESIAN_POINT('Ctrl Pts',(-2.66017994778913,0.672501443923755,
12.5089719619137));
#432069=CARTESIAN_POINT('Ctrl Pts',(-2.66011120640582,0.673077032239456,
12.5085043804652));
#432070=CARTESIAN_POINT('Ctrl Pts',(-2.66001061234554,0.673919330763834,
12.5078201359221));
#432071=CARTESIAN_POINT('Ctrl Pts',(-2.65983003746791,0.674867471431794,
12.5072563000949));
#432072=CARTESIAN_POINT('Ctrl Pts',(-2.65957340557055,0.675855600398903,
12.5068768744332));
#432073=CARTESIAN_POINT('Ctrl Pts',(-2.65938835630595,0.676568109407218,
12.5066032824114));
#432074=CARTESIAN_POINT('Ctrl Pts',(-2.65916056902539,0.677313942750192,
12.5064197834844));
#432075=CARTESIAN_POINT('Ctrl Pts',(-2.65890523609289,0.67805220617937,
12.5063282718343));
#432076=CARTESIAN_POINT('Ctrl Pts',(-2.65853252906052,0.67912984222539,
12.5061946931565));
#432077=CARTESIAN_POINT('Ctrl Pts',(-2.6580941682944,0.680214729463172,
12.5062515701262));
#432078=CARTESIAN_POINT('Ctrl Pts',(-2.65763169752486,0.681245331426123,
12.5064436508398));
#432079=CARTESIAN_POINT('',(-2.58563779814648,0.690482027821057,12.5737548217797));
#432080=CARTESIAN_POINT('Origin',(-2.60066746911388,0.694495628525106,12.5893111709658));
#432081=CARTESIAN_POINT('Ctrl Pts',(-2.65763169752486,0.681245331426123,
12.5064436508398));
#432082=CARTESIAN_POINT('Ctrl Pts',(-2.64697479111083,0.682613079002884,
12.5164271754438));
#432083=CARTESIAN_POINT('Ctrl Pts',(-2.6363136337041,0.683981161518646,
12.5264061185523));
#432084=CARTESIAN_POINT('Ctrl Pts',(-2.62564807570878,0.685349591708476,
12.536380305637));
#432085=CARTESIAN_POINT('Ctrl Pts',(-2.61231829142286,0.687059851898216,
12.5488460165097));
#432086=CARTESIAN_POINT('Ctrl Pts',(-2.59898162950762,0.688770655633538,
12.5613043021964));
#432087=CARTESIAN_POINT('Ctrl Pts',(-2.58563779814648,0.690482027821057,
12.5737548217797));
#432088=CARTESIAN_POINT('Ctrl Pts',(-2.58119104811554,0.733923044064313,
12.5893111709658));
#432089=CARTESIAN_POINT('Ctrl Pts',(-2.57223724225788,0.726974087651802,
12.5770542771492));
#432090=CARTESIAN_POINT('Ctrl Pts',(-2.57968438846801,0.712402070352199,
12.5737548217797));
#432091=CARTESIAN_POINT('Ctrl Pts',(-2.57283722512644,0.727439728170275,
12.5928319619712));
#432092=CARTESIAN_POINT('Ctrl Pts',(-2.56881706694639,0.720195989868897,
12.5821634970842));
#432093=CARTESIAN_POINT('Ctrl Pts',(-2.57663550590669,0.710047811977098,
12.5773203894503));
#432094=CARTESIAN_POINT('Ctrl Pts',(-2.56509386121157,0.712586297097903,
12.5969440695591));
#432095=CARTESIAN_POINT('Ctrl Pts',(-2.56612980322656,0.708702308594637,
12.5878292599214));
#432096=CARTESIAN_POINT('Ctrl Pts',(-2.57387742724554,0.7047528002494,12.5813877129824));
#432097=CARTESIAN_POINT('Ctrl Pts',(-2.57306133011871,0.683044890822048,
12.596957478804));
#432098=CARTESIAN_POINT('Ctrl Pts',(-2.57203312144387,0.686900196266482,
12.5878468778671));
#432099=CARTESIAN_POINT('Ctrl Pts',(-2.57673485413781,0.694181074758283,
12.5814011370086));
#432100=CARTESIAN_POINT('Ctrl Pts',(-2.58732338312299,0.674048622082001,
12.5928371701607));
#432101=CARTESIAN_POINT('Ctrl Pts',(-2.58019932599553,0.678265596797179,
12.5821692192952));
#432102=CARTESIAN_POINT('Ctrl Pts',(-2.58180459756576,0.690971773450833,
12.5773318885715));
#432103=CARTESIAN_POINT('Ctrl Pts',(-2.5978244241482,0.672680104343332,
12.5893111709658));
#432104=CARTESIAN_POINT('Ctrl Pts',(-2.58658550304428,0.674144784164816,
12.5770542771492));
#432105=CARTESIAN_POINT('Ctrl Pts',(-2.58563779814647,0.690482027821002,
12.5737548217797));
#432106=CARTESIAN_POINT('',(-2.57968438846801,0.712402070352199,12.5737548217797));
#432107=CARTESIAN_POINT('Origin',(-2.59467945374212,0.71654308682464,12.5893111709658));
#432108=CARTESIAN_POINT('Ctrl Pts',(-2.58563779814647,0.690482027821002,
12.5737548217797));
#432109=CARTESIAN_POINT('Ctrl Pts',(-2.58464034873514,0.6905790551515,12.5746934679442));
#432110=CARTESIAN_POINT('Ctrl Pts',(-2.58355434016266,0.690868746053545,
12.5756680099006));
#432111=CARTESIAN_POINT('Ctrl Pts',(-2.5825024710992,0.691314924427426,
12.5765688348656));
#432112=CARTESIAN_POINT('Ctrl Pts',(-2.58222400040923,0.691433045212554,
12.5768073183026));
#432113=CARTESIAN_POINT('Ctrl Pts',(-2.58194788267456,0.691561879706389,
12.5770407398754));
#432114=CARTESIAN_POINT('Ctrl Pts',(-2.58167617039754,0.691700240038191,
12.5772674179684));
#432115=CARTESIAN_POINT('Ctrl Pts',(-2.58056113668672,0.692268033425692,
12.5781976435658));
#432116=CARTESIAN_POINT('Ctrl Pts',(-2.57946208083084,0.69303854864839,
12.5790594849312));
#432117=CARTESIAN_POINT('Ctrl Pts',(-2.57848093323446,0.693999299457811,
12.5797571720116));
#432118=CARTESIAN_POINT('Ctrl Pts',(-2.5778416802965,0.694625263155669,
12.580211740231));
#432119=CARTESIAN_POINT('Ctrl Pts',(-2.57723656279431,0.695373841667835,
12.5806009430798));
#432120=CARTESIAN_POINT('Ctrl Pts',(-2.57672195644868,0.696203475908542,
12.5808812374708));
#432121=CARTESIAN_POINT('Ctrl Pts',(-2.5762797388789,0.696916406949604,
12.5811221033394));
#432122=CARTESIAN_POINT('Ctrl Pts',(-2.57589540298367,0.697703849437877,
12.581287365893));
#432123=CARTESIAN_POINT('Ctrl Pts',(-2.5755981343987,0.698525016090779,
12.581359338449));
#432124=CARTESIAN_POINT('Ctrl Pts',(-2.57555682020375,0.698639141299089,
12.5813693411482));
#432125=CARTESIAN_POINT('Ctrl Pts',(-2.57551712786061,0.698753917446674,
12.5813775999465));
#432126=CARTESIAN_POINT('Ctrl Pts',(-2.57547907437673,0.698869235667479,
12.5813841266931));
#432127=CARTESIAN_POINT('Ctrl Pts',(-2.57541451203886,0.699064886976527,
12.5813952001081));
#432128=CARTESIAN_POINT('Ctrl Pts',(-2.57535481299079,0.699263599834116,
12.5814007534795));
#432129=CARTESIAN_POINT('Ctrl Pts',(-2.57530019210384,0.699465344436412,
12.5814005856065));
#432130=CARTESIAN_POINT('Ctrl Pts',(-2.57505015903876,0.700388852348694,
12.5813998171494));
#432131=CARTESIAN_POINT('Ctrl Pts',(-2.57492348591701,0.70131199346516,
12.58127954464));
#432132=CARTESIAN_POINT('Ctrl Pts',(-2.57489157724675,0.702225504244456,
12.5810700125799));
#432133=CARTESIAN_POINT('Ctrl Pts',(-2.57485303520616,0.703328921254315,
12.5808169217085));
#432134=CARTESIAN_POINT('Ctrl Pts',(-2.5749694757758,0.704418971690396,
12.5804173076348));
#432135=CARTESIAN_POINT('Ctrl Pts',(-2.57520479926084,0.705402891516927,
12.5799304713245));
#432136=CARTESIAN_POINT('Ctrl Pts',(-2.57549643919336,0.706622278148708,
12.5793271277669));
#432137=CARTESIAN_POINT('Ctrl Pts',(-2.57595744547643,0.707761789454208,
12.5785808224116));
#432138=CARTESIAN_POINT('Ctrl Pts',(-2.57653898395356,0.708785287799404,
12.5777485681082));
#432139=CARTESIAN_POINT('Ctrl Pts',(-2.57740553999678,0.710310412466362,
12.576508418016));
#432140=CARTESIAN_POINT('Ctrl Pts',(-2.57852645720657,0.711568492002621,
12.5750928681475));
#432141=CARTESIAN_POINT('Ctrl Pts',(-2.57968438846801,0.712402070352199,
12.5737548217797));
#432142=CARTESIAN_POINT('Ctrl Pts',(-2.57968438846801,0.712402070352199,
12.5737548217797));
#432143=CARTESIAN_POINT('Ctrl Pts',(-2.57223724225788,0.726974087651802,
12.5770542771492));
#432144=CARTESIAN_POINT('Ctrl Pts',(-2.58119104811554,0.733923044064313,
12.5893111709658));
#432145=CARTESIAN_POINT('Ctrl Pts',(-2.59927492806847,0.727542272211241,
12.5508408821982));
#432146=CARTESIAN_POINT('Ctrl Pts',(-2.59180184648936,0.74215797528504,
12.55409748406));
#432147=CARTESIAN_POINT('Ctrl Pts',(-2.60076707511013,0.749115796786229,
12.5663972313419));
#432148=CARTESIAN_POINT('Ctrl Pts',(-2.61884560890822,0.742668617284018,
12.52790050457));
#432149=CARTESIAN_POINT('Ctrl Pts',(-2.611328979847,0.757312782159411,12.5311362602938));
#432150=CARTESIAN_POINT('Ctrl Pts',(-2.62032335311021,0.764293222517126,
12.5434568539655));
#432151=CARTESIAN_POINT('Ctrl Pts',(-2.63839796579971,0.757782193377856,
12.5049357605811));
#432152=CARTESIAN_POINT('Ctrl Pts',(-2.63082254847786,0.772441539795387,
12.5081700652078));
#432153=CARTESIAN_POINT('Ctrl Pts',(-2.63986142886112,0.779456521670096,
12.5204921097672));
#432154=CARTESIAN_POINT('Ctrl Pts',(-2.63711408043268,0.756789777983852,
12.5064436508395));
#432155=CARTESIAN_POINT('Ctrl Pts',(-2.6369818356153,0.758002773902584,
12.5062361689309));
#432156=CARTESIAN_POINT('Ctrl Pts',(-2.6367925869869,0.759258551182633,
12.5061871075061));
#432157=CARTESIAN_POINT('Ctrl Pts',(-2.63654138054129,0.760461843317901,
12.5063648335164));
#432158=CARTESIAN_POINT('Ctrl Pts',(-2.63642726707863,0.761008452827877,
12.5064455676329));
#432159=CARTESIAN_POINT('Ctrl Pts',(-2.63629856108233,0.761551810877591,
12.506574497099));
#432160=CARTESIAN_POINT('Ctrl Pts',(-2.6361597584282,0.762068377666752,
12.5067492519495));
#432161=CARTESIAN_POINT('Ctrl Pts',(-2.63588082910678,0.763106438681291,
12.5071004286051));
#432162=CARTESIAN_POINT('Ctrl Pts',(-2.6355500912597,0.764074266067061,
12.5076537929613));
#432163=CARTESIAN_POINT('Ctrl Pts',(-2.63520131876121,0.764902277897087,
12.5083435010505));
#432164=CARTESIAN_POINT('Ctrl Pts',(-2.63517936144816,0.764954406190012,
12.5083869222964));
#432165=CARTESIAN_POINT('Ctrl Pts',(-2.63515731926212,0.765005981382064,
12.5084308732337));
#432166=CARTESIAN_POINT('Ctrl Pts',(-2.63513519520765,0.765056986933429,
12.5084753333615));
#432167=CARTESIAN_POINT('Ctrl Pts',(-2.6349577310897,0.765466118776604,
12.5088319622689));
#432168=CARTESIAN_POINT('Ctrl Pts',(-2.63477258015423,0.765847418461921,
12.509227847131));
#432169=CARTESIAN_POINT('Ctrl Pts',(-2.63458776670862,0.766190771039883,
12.5096423454524));
#432170=CARTESIAN_POINT('Ctrl Pts',(-2.63400864316508,0.767266686057732,
12.5109411997424));
#432171=CARTESIAN_POINT('Ctrl Pts',(-2.63340572734068,0.768040749749141,
12.5124831113042));
#432172=CARTESIAN_POINT('Ctrl Pts',(-2.63282402277907,0.768596211969716,
12.5140723025008));
#432173=CARTESIAN_POINT('Ctrl Pts',(-2.63276951642453,0.768648259388164,
12.5142212114565));
#432174=CARTESIAN_POINT('Ctrl Pts',(-2.63271520032718,0.768698416841596,
12.5143705582413));
#432175=CARTESIAN_POINT('Ctrl Pts',(-2.63266111534153,0.768746769363242,
12.5145201959299));
#432176=CARTESIAN_POINT('Ctrl Pts',(-2.63196631317682,0.769367929493147,
12.5164425148273));
#432177=CARTESIAN_POINT('Ctrl Pts',(-2.63129300242233,0.769720506303571,
12.5184635205941));
#432178=CARTESIAN_POINT('Ctrl Pts',(-2.63063655359323,0.769894591672177,
12.5205025929158));
#432179=CARTESIAN_POINT('Ctrl Pts',(-2.63025578725315,0.769995568086067,
12.5216853356836));
#432180=CARTESIAN_POINT('Ctrl Pts',(-2.62988150580933,0.770036776766694,
12.5228750347131));
#432181=CARTESIAN_POINT('Ctrl Pts',(-2.62951872927369,0.770035760037976,
12.5240609649613));
#432182=CARTESIAN_POINT('Ctrl Pts',(-2.62862831372925,0.770033264531883,
12.5269717671326));
#432183=CARTESIAN_POINT('Ctrl Pts',(-2.62778217652212,0.769765924271362,
12.5299036066169));
#432184=CARTESIAN_POINT('Ctrl Pts',(-2.6269678354895,0.769319493079882,
12.5328133004019));
#432185=CARTESIAN_POINT('Ctrl Pts',(-2.62657690437617,0.769105180113062,
12.5342101228451));
#432186=CARTESIAN_POINT('Ctrl Pts',(-2.62619404058162,0.768849402433252,
12.5356023438238));
#432187=CARTESIAN_POINT('Ctrl Pts',(-2.62582115106377,0.768560006826658,
12.5369868989719));
#432188=CARTESIAN_POINT('Origin',(-12.6912014024061,8.58690233099497,-1.23983103325459));
#432189=CARTESIAN_POINT('Ctrl Pts',(-2.65380319878753,0.665384792735134,
12.5369868989719));
#432190=CARTESIAN_POINT('Ctrl Pts',(-2.6690172632328,0.66343145028175,12.5369868989719));
#432191=CARTESIAN_POINT('Ctrl Pts',(-2.67244519530005,0.648480444114029,
12.5369868989719));
#432192=CARTESIAN_POINT('Ctrl Pts',(-2.65894613915679,0.664724420918261,
12.5218025310015));
#432193=CARTESIAN_POINT('Ctrl Pts',(-2.66977411644987,0.659990419286952,
12.5216901060417));
#432194=CARTESIAN_POINT('Ctrl Pts',(-2.67243476190172,0.64852602342125,
12.5161920673678));
#432195=CARTESIAN_POINT('Ctrl Pts',(-2.66305729327739,0.669132876769389,
12.5042015548895));
#432196=CARTESIAN_POINT('Ctrl Pts',(-2.66836971911194,0.665505828827929,
12.4980677368514));
#432197=CARTESIAN_POINT('Ctrl Pts',(-2.67000847277043,0.658909976633512,
12.4907278922777));
#432198=CARTESIAN_POINT('Ctrl Pts',(-2.65761232284785,0.681240365019505,
12.506463626192));
#432199=CARTESIAN_POINT('Ctrl Pts',(-2.66395015203713,0.682864975589384,
12.4999376786891));
#432200=CARTESIAN_POINT('Ctrl Pts',(-2.66387274466878,0.682845133333455,
12.4906970594712));
#432201=CARTESIAN_POINT('Origin',(-2.65100160274658,0.643563906877238,12.5369868989719));
#432202=CARTESIAN_POINT('Origin',(-2.65100160274658,0.643563906877238,14.));
#432203=CARTESIAN_POINT('Origin',(-2.65100160274658,0.643563906877238,13.7435492065112));
#432204=CARTESIAN_POINT('Ctrl Pts',(-2.6292921602477,0.668579135451396,
13.793642941384));
#432205=CARTESIAN_POINT('Ctrl Pts',(-2.640017297917,0.667208865047367,13.8071662555867));
#432206=CARTESIAN_POINT('Ctrl Pts',(-2.6403661507135,0.650182483007689,
13.8103758687955));
#432207=CARTESIAN_POINT('Ctrl Pts',(-2.64577391038728,0.666431202128725,
13.7804579775006));
#432208=CARTESIAN_POINT('Ctrl Pts',(-2.65900647570461,0.664730353266513,
13.7901904343351));
#432209=CARTESIAN_POINT('Ctrl Pts',(-2.66187369953941,0.649237291863243,
13.7927914348263));
#432210=CARTESIAN_POINT('Ctrl Pts',(-2.65547733696763,0.665166632908131,
13.7597120340895));
#432211=CARTESIAN_POINT('Ctrl Pts',(-2.67079041103023,0.663192588145461,
13.7635825532445));
#432212=CARTESIAN_POINT('Ctrl Pts',(-2.67455555417036,0.648654375969331,
13.7651073818884));
#432213=CARTESIAN_POINT('Ctrl Pts',(-2.65357718385987,0.665414264516065,
13.7381884353898));
#432214=CARTESIAN_POINT('Ctrl Pts',(-2.66853194181363,0.663487317404509,
13.7368803041982));
#432215=CARTESIAN_POINT('Ctrl Pts',(-2.67207204750091,0.648768034512946,
13.7363986145813));
#432216=CARTESIAN_POINT('Origin',(-2.63044838594166,0.646242445292302,13.7902182540695));
#432217=CARTESIAN_POINT('Ctrl Pts',(-2.59782052085778,0.672680612263058,
13.8235227101244));
#432218=CARTESIAN_POINT('Ctrl Pts',(-2.60922175997325,0.671199249730936,
13.8358800583119));
#432219=CARTESIAN_POINT('Ctrl Pts',(-2.61007035076852,0.654649145721622,
13.8390832900376));
#432220=CARTESIAN_POINT('Ctrl Pts',(-2.60964808430635,0.671139219332836,
13.8124254819053));
#432221=CARTESIAN_POINT('Ctrl Pts',(-2.62107146443071,0.669654979739829,
13.8247886449158));
#432222=CARTESIAN_POINT('Ctrl Pts',(-2.62190410552995,0.653083091196193,
13.8279860620657));
#432223=CARTESIAN_POINT('Ctrl Pts',(-2.6214703470257,0.669598517204799,
13.8013225099955));
#432224=CARTESIAN_POINT('Ctrl Pts',(-2.63291047841627,0.668112102861582,
13.8136962257787));
#432225=CARTESIAN_POINT('Ctrl Pts',(-2.63373241740585,0.651518030390368,
13.8168830918626));
#432226=CARTESIAN_POINT('Ctrl Pts',(-2.63328751525918,0.668058479000884,
13.7902140179785));
#432227=CARTESIAN_POINT('Ctrl Pts',(-2.64473936043208,0.666570546314042,
13.802602731458));
#432228=CARTESIAN_POINT('Ctrl Pts',(-2.64555550050187,0.649953926082836,
13.8057746032558));
#432229=CARTESIAN_POINT('Origin',(-2.59498137918255,0.650864580161667,13.8235269408515));
#432230=CARTESIAN_POINT('Ctrl Pts',(-2.58119104811554,0.733923044064314,
13.8235269408515));
#432231=CARTESIAN_POINT('Ctrl Pts',(-2.59051893553145,0.741162321317405,
13.8362179249168));
#432232=CARTESIAN_POINT('Ctrl Pts',(-2.58236821981996,0.756169947293812,
13.8391868794938));
#432233=CARTESIAN_POINT('Ctrl Pts',(-2.57265643714878,0.727299420484737,
13.8400110824519));
#432234=CARTESIAN_POINT('Ctrl Pts',(-2.57803767465309,0.735806132292735,
13.8494522556837));
#432235=CARTESIAN_POINT('Ctrl Pts',(-2.56839154664088,0.745180571039019,
13.85569149686));
#432236=CARTESIAN_POINT('Ctrl Pts',(-2.5650031372433,0.71291801837636,13.8586819406588));
#432237=CARTESIAN_POINT('Ctrl Pts',(-2.56387541257129,0.71712328658411,
13.868010383617));
#432238=CARTESIAN_POINT('Ctrl Pts',(-2.55581580239515,0.721238569150482,
13.8744918421245));
#432239=CARTESIAN_POINT('Ctrl Pts',(-2.57315344319922,0.682708019853152,
13.8587686893867));
#432240=CARTESIAN_POINT('Ctrl Pts',(-2.57427107674546,0.678540163908405,
13.8680909899357));
#432241=CARTESIAN_POINT('Ctrl Pts',(-2.56938615246847,0.670948463419457,
13.8745789365163));
#432242=CARTESIAN_POINT('Ctrl Pts',(-2.58709424915727,0.674078483295469,
13.8400379222776));
#432243=CARTESIAN_POINT('Ctrl Pts',(-2.59603392265685,0.669457609825165,
13.8494748685453));
#432244=CARTESIAN_POINT('Ctrl Pts',(-2.59245817169815,0.656497088603161,
13.8557104837033));
#432245=CARTESIAN_POINT('Ctrl Pts',(-2.59782442414722,0.672680104336852,
13.8235269408542));
#432246=CARTESIAN_POINT('Ctrl Pts',(-2.60953289676769,0.671154231574727,
13.8362179249195));
#432247=CARTESIAN_POINT('Ctrl Pts',(-2.61009406336799,0.654085309637386,
13.8391868794965));
#432248=CARTESIAN_POINT('Origin',(-2.56770264248896,0.751303001303987,13.8235269408515));
#432249=CARTESIAN_POINT('Ctrl Pts',(-2.60944373152358,0.755849661334478,
13.7902140241682));
#432250=CARTESIAN_POINT('Ctrl Pts',(-2.61856943611421,0.762926391590561,
13.8026027327198));
#432251=CARTESIAN_POINT('Ctrl Pts',(-2.61086747415291,0.777672839102445,
13.8057746032556));
#432252=CARTESIAN_POINT('Ctrl Pts',(-2.60002924865636,0.748543178243071,
13.8013225161807));
#432253=CARTESIAN_POINT('Ctrl Pts',(-2.60914561698112,0.755612673023652,
13.8136962270464));
#432254=CARTESIAN_POINT('Ctrl Pts',(-2.6014600635928,0.770342604266843,
13.8168830918628));
#432255=CARTESIAN_POINT('Ctrl Pts',(-2.5906107071209,0.741233545261063,
13.8124254880875));
#432256=CARTESIAN_POINT('Ctrl Pts',(-2.5997137258838,0.748292689999847,
13.8247886461868));
#432257=CARTESIAN_POINT('Ctrl Pts',(-2.59204862653035,0.763008899229835,
13.8279860620656));
#432258=CARTESIAN_POINT('Ctrl Pts',(-2.58118794260636,0.733920634868514,
13.8235227163065));
#432259=CARTESIAN_POINT('Ctrl Pts',(-2.59027331787303,0.740966097202585,
13.8358800595847));
#432260=CARTESIAN_POINT('Ctrl Pts',(-2.58263299710521,0.755671583572082,
13.8390832900376));
#432261=CARTESIAN_POINT('Origin',(-2.59595844123842,0.773232035396524,13.7902182540695));
#432262=CARTESIAN_POINT('Ctrl Pts',(-2.62560794535342,0.768394574990138,
13.7382347919292));
#432263=CARTESIAN_POINT('Ctrl Pts',(-2.63754397147469,0.777627621571077,
13.7369371795943));
#432264=CARTESIAN_POINT('Ctrl Pts',(-2.63314021194084,0.792124196304043,
13.7364597369711));
#432265=CARTESIAN_POINT('Ctrl Pts',(-2.62710227322728,0.769554306937452,
13.7595490285574));
#432266=CARTESIAN_POINT('Ctrl Pts',(-2.63932246752902,0.779008441358257,
13.7633824266926));
#432267=CARTESIAN_POINT('Ctrl Pts',(-2.63519966508372,0.793461681835887,
13.7648920890506));
#432268=CARTESIAN_POINT('Ctrl Pts',(-2.61948128294142,0.763639737535113,
13.780380659011));
#432269=CARTESIAN_POINT('Ctrl Pts',(-2.63005461696086,0.771812955611082,
13.7901039518744));
#432270=CARTESIAN_POINT('Ctrl Pts',(-2.62470237024758,0.78663992079435,
13.7926933640892));
#432271=CARTESIAN_POINT('Ctrl Pts',(-2.60623430055833,0.7533588956768,13.7936647693663));
#432272=CARTESIAN_POINT('Ctrl Pts',(-2.61479680648362,0.759966226773704,
13.8072068914933));
#432273=CARTESIAN_POINT('Ctrl Pts',(-2.60646630612032,0.774840601837694,
13.8104111085397));
#432274=CARTESIAN_POINT('Origin',(-2.61233274543719,0.785939964066332,13.7435492065112));
#432275=CARTESIAN_POINT('Origin',(-2.61233274543719,0.785939964066332,14.));
#432276=CARTESIAN_POINT('Origin',(-2.61233274543719,0.785939964066332,12.5369868989719));
#432277=CARTESIAN_POINT('Ctrl Pts',(-2.63709641041666,0.756784707093716,
12.506462012331));
#432278=CARTESIAN_POINT('Ctrl Pts',(-2.64338135303544,0.75858833795077,
12.4999388158272));
#432279=CARTESIAN_POINT('Ctrl Pts',(-2.64330699392206,0.758566998632415,
12.4907030323752));
#432280=CARTESIAN_POINT('Ctrl Pts',(-2.63566641135388,0.769982573809021,
12.5042014951932));
#432281=CARTESIAN_POINT('Ctrl Pts',(-2.63841375712275,0.775795764700635,
12.4980716682127));
#432282=CARTESIAN_POINT('Ctrl Pts',(-2.63649352581143,0.78231023144297,
12.4907355092743));
#432283=CARTESIAN_POINT('Ctrl Pts',(-2.62989146561741,0.771707596413527,
12.5218047446509));
#432284=CARTESIAN_POINT('Ctrl Pts',(-2.63683259606657,0.78126477063104,
12.5216906929434));
#432285=CARTESIAN_POINT('Ctrl Pts',(-2.63333344319635,0.792495384306188,
12.5161988840776));
#432286=CARTESIAN_POINT('Ctrl Pts',(-2.62579078184538,0.768536480046287,
12.5369868989719));
#432287=CARTESIAN_POINT('Ctrl Pts',(-2.63791775902611,0.77791421729887,
12.5369868989719));
#432288=CARTESIAN_POINT('Ctrl Pts',(-2.63331991434154,0.792538353368299,
12.5369868989719));
#432289=CARTESIAN_POINT('Origin',(-4.97175483587123E-31,-3.80155074318093E-31,
12.5));
#432290=CARTESIAN_POINT('Origin',(-2.63242388933657,0.521089942649588,12.5));
#432291=CARTESIAN_POINT('',(-2.63242388933657,0.521089942649588,12.5893111709658));
#432292=CARTESIAN_POINT('',(-2.63242388933657,0.521089942649588,13.8235269408515));
#432293=CARTESIAN_POINT('',(-2.63242388933657,0.521089942649588,12.5));
#432294=CARTESIAN_POINT('',(-2.66237308910439,0.540642899778083,13.7902182540695));
#432295=CARTESIAN_POINT('',(-2.63242388933657,0.521089942649588,13.8235269408515));
#432296=CARTESIAN_POINT('',(-2.67972872331797,0.551973886059748,13.7435492065112));
#432297=CARTESIAN_POINT('Origin',(-2.62262909424378,0.514694818196436,13.7445212918693));
#432298=CARTESIAN_POINT('',(-2.67972872331797,0.551973886059748,12.5369868989719));
#432299=CARTESIAN_POINT('',(-2.67972872331797,0.551973886059748,12.5));
#432300=CARTESIAN_POINT('Ctrl Pts',(-2.67972872331797,0.551973886059748,
12.5369868989719));
#432301=CARTESIAN_POINT('Ctrl Pts',(-2.66397194574709,0.541686746546334,
12.5544431401645));
#432302=CARTESIAN_POINT('Ctrl Pts',(-2.64820389851011,0.531392249397325,
12.5718848856037));
#432303=CARTESIAN_POINT('Ctrl Pts',(-2.63242388933657,0.521089942649588,
12.5893111709658));
#432304=CARTESIAN_POINT('Origin',(-2.91290005437388,0.401048100265817,12.5));
#432305=CARTESIAN_POINT('',(-2.69924879928632,0.446852460011815,13.7435492065112));
#432306=CARTESIAN_POINT('',(-2.67898229736197,0.451197363787623,13.7902182540695));
#432307=CARTESIAN_POINT('Origin',(-2.62572543305949,0.462615019960319,13.7418732680442));
#432308=CARTESIAN_POINT('',(-2.64401005104369,0.458695009195004,13.8235269408515));
#432309=CARTESIAN_POINT('',(-2.67898229736197,0.451197363787623,13.7902182540695));
#432310=CARTESIAN_POINT('',(-2.64401005104369,0.458695009195004,12.5893111709658));
#432311=CARTESIAN_POINT('',(-2.64401005104369,0.458695009195004,12.5));
#432312=CARTESIAN_POINT('',(-2.69924879928632,0.446852460011815,12.5369868989719));
#432313=CARTESIAN_POINT('Ctrl Pts',(-2.64401005104369,0.458695009195004,
12.5893111709658));
#432314=CARTESIAN_POINT('Ctrl Pts',(-2.66243666584474,0.454744555953329,
12.5718848856037));
#432315=CARTESIAN_POINT('Ctrl Pts',(-2.68084931246654,0.450797097327846,
12.5544431401645));
#432316=CARTESIAN_POINT('Ctrl Pts',(-2.69924879928632,0.446852460011815,
12.5369868989719));
#432317=CARTESIAN_POINT('',(-2.69924879928632,0.446852460011815,12.5));
#432318=CARTESIAN_POINT('Origin',(-2.65121591465983,0.492306259611278,12.5));
#432319=CARTESIAN_POINT('',(-2.61723291503602,0.487134614926502,13.8587068136939));
#432320=CARTESIAN_POINT('Ctrl Pts',(-2.64401005104216,0.458695009188572,
13.8235269408542));
#432321=CARTESIAN_POINT('Ctrl Pts',(-2.64229668557668,0.459062334941593,
13.8262006681044));
#432322=CARTESIAN_POINT('Ctrl Pts',(-2.64057972648819,0.459608118342289,
13.8288634856214));
#432323=CARTESIAN_POINT('Ctrl Pts',(-2.63886090087308,0.460319137318725,
13.8314912288862));
#432324=CARTESIAN_POINT('Ctrl Pts',(-2.63708896895254,0.461052124545224,
13.8342001611531));
#432325=CARTESIAN_POINT('Ctrl Pts',(-2.63531289527057,0.461961070621593,
13.8368750301949));
#432326=CARTESIAN_POINT('Ctrl Pts',(-2.63353194277321,0.463076614130332,
13.8394886372969));
#432327=CARTESIAN_POINT('Ctrl Pts',(-2.63339439549185,0.463162770261442,
13.8396904925131));
#432328=CARTESIAN_POINT('Ctrl Pts',(-2.63325682745648,0.463250179229894,
13.8398919674349));
#432329=CARTESIAN_POINT('Ctrl Pts',(-2.63311924355486,0.463338865330674,
13.8400930404591));
#432330=CARTESIAN_POINT('Ctrl Pts',(-2.63097559380562,0.464720654445926,
13.8432258934518));
#432331=CARTESIAN_POINT('Ctrl Pts',(-2.62883842087517,0.466404480074774,
13.8462331177034));
#432332=CARTESIAN_POINT('Ctrl Pts',(-2.62683712799038,0.468411198488729,
13.8489036603661));
#432333=CARTESIAN_POINT('Ctrl Pts',(-2.62618228166826,0.469067820107131,
13.8497774930041));
#432334=CARTESIAN_POINT('Ctrl Pts',(-2.62554222827764,0.469758961651016,
13.85061494757));
#432335=CARTESIAN_POINT('Ctrl Pts',(-2.62492219736293,0.470485195353339,
13.8514076489583));
#432336=CARTESIAN_POINT('Ctrl Pts',(-2.62361074255648,0.472021284372325,
13.8530843267192));
#432337=CARTESIAN_POINT('Ctrl Pts',(-2.62226229521561,0.473867174909691,
13.8546805203176));
#432338=CARTESIAN_POINT('Ctrl Pts',(-2.62106529722913,0.475996218981072,
13.8559412814273));
#432339=CARTESIAN_POINT('Ctrl Pts',(-2.62090510007897,0.476281154124366,
13.8561100121513));
#432340=CARTESIAN_POINT('Ctrl Pts',(-2.62074758894407,0.476571088798741,
13.8562727473908));
#432341=CARTESIAN_POINT('Ctrl Pts',(-2.62059318056477,0.47686589182133,
13.8564289040185));
#432342=CARTESIAN_POINT('Ctrl Pts',(-2.61989294032619,0.478202820165509,
13.8571370725437));
#432343=CARTESIAN_POINT('Ctrl Pts',(-2.61924622003635,0.479664427228443,
13.8577210840553));
#432344=CARTESIAN_POINT('Ctrl Pts',(-2.61870499601779,0.481205775232603,
13.8581177131616));
#432345=CARTESIAN_POINT('Ctrl Pts',(-2.6185525687058,0.481639871882158,
13.8582294175695));
#432346=CARTESIAN_POINT('Ctrl Pts',(-2.61840835633688,0.48208020288325,
13.8583265086086));
#432347=CARTESIAN_POINT('Ctrl Pts',(-2.61827312910673,0.482525563282829,
13.8584082369006));
#432348=CARTESIAN_POINT('Ctrl Pts',(-2.61807884383963,0.483165426748914,
13.8585256585398));
#432349=CARTESIAN_POINT('Ctrl Pts',(-2.61790099965483,0.483823720844838,
13.8586122832068));
#432350=CARTESIAN_POINT('Ctrl Pts',(-2.61774497878506,0.484483550955413,
13.8586682984299));
#432351=CARTESIAN_POINT('Ctrl Pts',(-2.6176201775551,0.485011349637018,
13.8587131050557));
#432352=CARTESIAN_POINT('Ctrl Pts',(-2.61750773316542,0.485545906707866,
13.8587357943552));
#432353=CARTESIAN_POINT('Ctrl Pts',(-2.61740812785469,0.486087389937754,
13.8587355499465));
#432354=CARTESIAN_POINT('Ctrl Pts',(-2.61734375056764,0.486437363458876,
13.8587353919793));
#432355=CARTESIAN_POINT('Ctrl Pts',(-2.61728539474004,0.486786438712572,
13.8587257282814));
#432356=CARTESIAN_POINT('Ctrl Pts',(-2.61723291503602,0.487134614926502,
13.8587068136939));
#432357=CARTESIAN_POINT('Ctrl Pts',(-2.61723291503602,0.487134614926502,
13.8587068136939));
#432358=CARTESIAN_POINT('Ctrl Pts',(-2.61706031215051,0.488279747512706,
13.8586446046466));
#432359=CARTESIAN_POINT('Ctrl Pts',(-2.61695119376834,0.489415167789454,
13.858482427929));
#432360=CARTESIAN_POINT('Ctrl Pts',(-2.61690109098488,0.490540753901813,
13.8582284286032));
#432361=CARTESIAN_POINT('Ctrl Pts',(-2.61684969135724,0.491695474319623,
13.8579678548414));
#432362=CARTESIAN_POINT('Ctrl Pts',(-2.61686180652745,0.492842733674225,
13.857615680862));
#432363=CARTESIAN_POINT('Ctrl Pts',(-2.61692726973463,0.493937404435696,
13.8571944833187));
#432364=CARTESIAN_POINT('Ctrl Pts',(-2.6170906398632,0.496669267274696,
13.8561433417727));
#432365=CARTESIAN_POINT('Ctrl Pts',(-2.61758911828645,0.499201680998632,
13.8546163505474));
#432366=CARTESIAN_POINT('Ctrl Pts',(-2.61824353044091,0.501431425733235,
13.8528973491086));
#432367=CARTESIAN_POINT('Ctrl Pts',(-2.61836308188658,0.501838767199425,
13.8525833129072));
#432368=CARTESIAN_POINT('Ctrl Pts',(-2.6184877355625,0.502236105361634,
13.8522628768812));
#432369=CARTESIAN_POINT('Ctrl Pts',(-2.61861629108584,0.502622953433333,
13.851937733538));
#432370=CARTESIAN_POINT('Ctrl Pts',(-2.61940136183063,0.504985380934481,
13.8499521282529));
#432371=CARTESIAN_POINT('Ctrl Pts',(-2.6204138385287,0.507190088317489,
13.847639871647));
#432372=CARTESIAN_POINT('Ctrl Pts',(-2.62152749917535,0.509154732977702,
13.8452109780794));
#432373=CARTESIAN_POINT('Ctrl Pts',(-2.62202855815191,0.510038667276455,
13.8441181685877));
#432374=CARTESIAN_POINT('Ctrl Pts',(-2.62254963617414,0.510874554073736,
13.8430021611332));
#432375=CARTESIAN_POINT('Ctrl Pts',(-2.62307798757882,0.511657957505856,
13.8418824960098));
#432376=CARTESIAN_POINT('Ctrl Pts',(-2.62432306115589,0.513504067698561,
13.8392439765549));
#432377=CARTESIAN_POINT('Ctrl Pts',(-2.62566490940633,0.515149093362416,
13.8364981347964));
#432378=CARTESIAN_POINT('Ctrl Pts',(-2.62708056355634,0.516619015251649,
13.8336931113419));
#432379=CARTESIAN_POINT('Ctrl Pts',(-2.62845932079609,0.518050625823091,
13.8309611966328));
#432380=CARTESIAN_POINT('Ctrl Pts',(-2.6299098749629,0.519317184367395,
13.8281701127186));
#432381=CARTESIAN_POINT('Ctrl Pts',(-2.63142745582177,0.520407000643875,
13.8253580685121));
#432382=CARTESIAN_POINT('Ctrl Pts',(-2.63175646898981,0.520643273988785,
13.8247484142933));
#432383=CARTESIAN_POINT('Ctrl Pts',(-2.6320886380345,0.520871066873691,
13.8241378483365));
#432384=CARTESIAN_POINT('Ctrl Pts',(-2.63242388933657,0.521089942649588,
13.8235269408515));
#432385=CARTESIAN_POINT('',(-2.61744190074819,0.485910236786106,12.5969504640361));
#432386=CARTESIAN_POINT('Origin',(-2.65124840825318,0.492312492524074,12.584524458991));
#432387=CARTESIAN_POINT('Origin',(-2.65124840825318,0.492312492524074,12.584524458991));
#432388=CARTESIAN_POINT('Ctrl Pts',(-2.64401005104369,0.458695009195004,
12.5893111709658));
#432389=CARTESIAN_POINT('Ctrl Pts',(-2.63292791152546,0.461070891822232,
12.5770542771492));
#432390=CARTESIAN_POINT('Ctrl Pts',(-2.63331499706307,0.477431021395115,
12.5737548217797));
#432391=CARTESIAN_POINT('Ctrl Pts',(-2.66824297089342,0.453499751259175,
12.5663937883685));
#432392=CARTESIAN_POINT('Ctrl Pts',(-2.6571466945672,0.455878664654639,
12.5540940315303));
#432393=CARTESIAN_POINT('Ctrl Pts',(-2.65753818989281,0.472289414994709,
12.5508374392248));
#432394=CARTESIAN_POINT('Ctrl Pts',(-2.69245144002421,0.448309735274893,
12.5434499600945));
#432395=CARTESIAN_POINT('Ctrl Pts',(-2.68131908575214,0.450696383364917,
12.5311293540533));
#432396=CARTESIAN_POINT('Ctrl Pts',(-2.68173747116724,0.467151677899152,
12.5278936106989));
#432397=CARTESIAN_POINT('Ctrl Pts',(-2.71663737369418,0.443124550632948,
12.5204817579905));
#432398=CARTESIAN_POINT('Ctrl Pts',(-2.70544992187638,0.445523011000026,
12.5081597038247));
#432399=CARTESIAN_POINT('Ctrl Pts',(-2.70591469650934,0.462017495818755,
12.5049254088044));
#432400=CARTESIAN_POINT('Ctrl Pts',(-2.69924879928632,0.446852460011815,
12.5369868989719));
#432401=CARTESIAN_POINT('Ctrl Pts',(-2.70015960777715,0.446657193363936,
12.5342545179733));
#432402=CARTESIAN_POINT('Ctrl Pts',(-2.7010549917397,0.446592814229371,
12.5314872231885));
#432403=CARTESIAN_POINT('Ctrl Pts',(-2.70188852178364,0.446718706151211,
12.5287124745063));
#432404=CARTESIAN_POINT('Ctrl Pts',(-2.70264024055,0.446832241735042,12.5262100684184));
#432405=CARTESIAN_POINT('Ctrl Pts',(-2.70334074612475,0.447101389050586,
12.5237004536639));
#432406=CARTESIAN_POINT('Ctrl Pts',(-2.70397829100729,0.447592649769733,
12.5212220730815));
#432407=CARTESIAN_POINT('Ctrl Pts',(-2.7044663867669,0.447968752347681,
12.5193246583486));
#432408=CARTESIAN_POINT('Ctrl Pts',(-2.70492302594465,0.448480038260301,
12.517417831369));
#432409=CARTESIAN_POINT('Ctrl Pts',(-2.70528989456734,0.449204311770227,
12.5155812248348));
#432410=CARTESIAN_POINT('Ctrl Pts',(-2.70544618257253,0.449512856178445,
12.5147988205793));
#432411=CARTESIAN_POINT('Ctrl Pts',(-2.70558658474796,0.449860241736385,
12.5140295443047));
#432412=CARTESIAN_POINT('Ctrl Pts',(-2.70570870206013,0.450252759398287,
12.5132817086137));
#432413=CARTESIAN_POINT('Ctrl Pts',(-2.70589351009244,0.450846781780985,
12.5121499604604));
#432414=CARTESIAN_POINT('Ctrl Pts',(-2.70603360275183,0.451559121000489,
12.5110494206568));
#432415=CARTESIAN_POINT('Ctrl Pts',(-2.70609669465267,0.452408339185497,
12.5100666561695));
#432416=CARTESIAN_POINT('Ctrl Pts',(-2.70613292187684,0.452895958311753,
12.5095023550641));
#432417=CARTESIAN_POINT('Ctrl Pts',(-2.70614352934085,0.453434389196007,
12.5089719619137));
#432418=CARTESIAN_POINT('Ctrl Pts',(-2.70612193248006,0.454013665349975,
12.5085043804652));
#432419=CARTESIAN_POINT('Ctrl Pts',(-2.70609032828747,0.45486136054528,
12.5078201359221));
#432420=CARTESIAN_POINT('Ctrl Pts',(-2.70598763652439,0.455821064882285,
12.5072563000949));
#432421=CARTESIAN_POINT('Ctrl Pts',(-2.70581240023266,0.45682682381386,
12.5068768744332));
#432422=CARTESIAN_POINT('Ctrl Pts',(-2.70568604280301,0.457552045240207,
12.5066032824114));
#432423=CARTESIAN_POINT('Ctrl Pts',(-2.70551980580727,0.458313963662298,
12.5064197834844));
#432424=CARTESIAN_POINT('Ctrl Pts',(-2.70532549779722,0.459070582585212,
12.5063282718343));
#432425=CARTESIAN_POINT('Ctrl Pts',(-2.70504186825879,0.460175011969369,
12.5061946931565));
#432426=CARTESIAN_POINT('Ctrl Pts',(-2.70469339448344,0.461292019806346,
12.5062515701262));
#432427=CARTESIAN_POINT('Ctrl Pts',(-2.70431646617486,0.46235688818737,
12.5064436508398));
#432428=CARTESIAN_POINT('',(-2.63331499706307,0.477431021395115,12.5737548217797));
#432429=CARTESIAN_POINT('Origin',(-2.64862180375802,0.480206209461419,12.5893111709658));
#432430=CARTESIAN_POINT('Ctrl Pts',(-2.70431646617486,0.46235688818737,
12.5064436508398));
#432431=CARTESIAN_POINT('Ctrl Pts',(-2.69380650386284,0.464588721503536,
12.5164271754438));
#432432=CARTESIAN_POINT('Ctrl Pts',(-2.68329233200359,0.466821235139596,
12.5264061185523));
#432433=CARTESIAN_POINT('Ctrl Pts',(-2.67277380253701,0.469054453981689,
12.536380305637));
#432434=CARTESIAN_POINT('Ctrl Pts',(-2.65962777409142,0.471845524588721,
12.5488460165097));
#432435=CARTESIAN_POINT('Ctrl Pts',(-2.64647493520526,0.474637697523352,
12.5613043021964));
#432436=CARTESIAN_POINT('Ctrl Pts',(-2.63331499706307,0.477431021395115,
12.5737548217797));
#432437=CARTESIAN_POINT('Ctrl Pts',(-2.63242388933657,0.521089942649588,
12.5893111709658));
#432438=CARTESIAN_POINT('Ctrl Pts',(-2.62293347207068,0.514893926616768,
12.5770542771492));
#432439=CARTESIAN_POINT('Ctrl Pts',(-2.62916808382621,0.499763384950565,
12.5737548217797));
#432440=CARTESIAN_POINT('Ctrl Pts',(-2.62356941257079,0.515309113581068,
12.5928319619712));
#432441=CARTESIAN_POINT('Ctrl Pts',(-2.61897219921629,0.508417158434331,
12.5821634970842));
#432442=CARTESIAN_POINT('Ctrl Pts',(-2.62593745225667,0.497665472409182,
12.5773203894503));
#432443=CARTESIAN_POINT('Ctrl Pts',(-2.61464112153564,0.501136262120216,
12.5969440695591));
#432444=CARTESIAN_POINT('Ctrl Pts',(-2.61535703541883,0.497180758376851,
12.5878292599214));
#432445=CARTESIAN_POINT('Ctrl Pts',(-2.62275695826244,0.492612888411841,
12.5813877129824));
#432446=CARTESIAN_POINT('Ctrl Pts',(-2.62017418048675,0.471043729754444,
12.596957478804));
#432447=CARTESIAN_POINT('Ctrl Pts',(-2.61946363627608,0.474970015540476,
12.5878468778671));
#432448=CARTESIAN_POINT('Ctrl Pts',(-2.62474318353181,0.481843432646413,
12.5814011370086));
#432449=CARTESIAN_POINT('Ctrl Pts',(-2.63365549826659,0.460914905634202,
12.5928371701607));
#432450=CARTESIAN_POINT('Ctrl Pts',(-2.6268988684393,0.465698525506302,
12.5821692192952));
#432451=CARTESIAN_POINT('Ctrl Pts',(-2.62953446995646,0.478231578869737,
12.5773318885715));
#432452=CARTESIAN_POINT('Ctrl Pts',(-2.64401005104367,0.45869500919495,
12.5893111709658));
#432453=CARTESIAN_POINT('Ctrl Pts',(-2.63292791152545,0.461070891822178,
12.5770542771492));
#432454=CARTESIAN_POINT('Ctrl Pts',(-2.63331499706305,0.477431021395061,
12.5737548217797));
#432455=CARTESIAN_POINT('',(-2.62916808382621,0.499763384950565,12.5737548217797));
#432456=CARTESIAN_POINT('Origin',(-2.64445078554346,0.502668385505069,12.5893111709658));
#432457=CARTESIAN_POINT('Ctrl Pts',(-2.63331499706305,0.477431021395061,
12.5737548217797));
#432458=CARTESIAN_POINT('Ctrl Pts',(-2.63232877521056,0.477609027262011,
12.5746934679442));
#432459=CARTESIAN_POINT('Ctrl Pts',(-2.63126999273989,0.477986274022145,
12.5756680099006));
#432460=CARTESIAN_POINT('Ctrl Pts',(-2.63025799136356,0.478516704868041,
12.5765688348656));
#432461=CARTESIAN_POINT('Ctrl Pts',(-2.62999007520239,0.47865713056243,
12.5768073183026));
#432462=CARTESIAN_POINT('Ctrl Pts',(-2.629725377434,0.478808042528843,12.5770407398754));
#432463=CARTESIAN_POINT('Ctrl Pts',(-2.62946584690868,0.478968089551087,
12.5772674179684));
#432464=CARTESIAN_POINT('Ctrl Pts',(-2.62840080381277,0.47962487925183,
12.5781976435658));
#432465=CARTESIAN_POINT('Ctrl Pts',(-2.62736820911834,0.48048241390408,
12.5790594849312));
#432466=CARTESIAN_POINT('Ctrl Pts',(-2.6264686363198,0.481519940532074,
12.5797571720116));
#432467=CARTESIAN_POINT('Ctrl Pts',(-2.62588253229579,0.482195926436344,
12.580211740231));
#432468=CARTESIAN_POINT('Ctrl Pts',(-2.62534044437038,0.482991336809329,
12.5806009430798));
#432469=CARTESIAN_POINT('Ctrl Pts',(-2.62489517322748,0.483860155705081,
12.5808812374708));
#432470=CARTESIAN_POINT('Ctrl Pts',(-2.62451253759856,0.484606759364201,
12.5811221033394));
#432471=CARTESIAN_POINT('Ctrl Pts',(-2.62419366442237,0.485422908646014,
12.581287365893));
#432472=CARTESIAN_POINT('Ctrl Pts',(-2.62396431767964,0.486265573084002,
12.581359338449));
#432473=CARTESIAN_POINT('Ctrl Pts',(-2.62393244321822,0.486382686040527,
12.5813693411482));
#432474=CARTESIAN_POINT('Ctrl Pts',(-2.62390223826965,0.486500315574401,
12.5813775999465));
#432475=CARTESIAN_POINT('Ctrl Pts',(-2.62387371091115,0.486618351795548,
12.5813841266931));
#432476=CARTESIAN_POINT('Ctrl Pts',(-2.62382531079715,0.48681861452091,
12.5813952001081));
#432477=CARTESIAN_POINT('Ctrl Pts',(-2.6237820073354,0.487021532204495,
12.5814007534795));
#432478=CARTESIAN_POINT('Ctrl Pts',(-2.62374401225294,0.487227057627631,
12.5814005856065));
#432479=CARTESIAN_POINT('Ctrl Pts',(-2.62357008562053,0.488167872659516,
12.5813998171494));
#432480=CARTESIAN_POINT('Ctrl Pts',(-2.62351907856417,0.48909826713547,
12.58127954464));
#432481=CARTESIAN_POINT('Ctrl Pts',(-2.6235617356765,0.490011339135859,
12.5810700125799));
#432482=CARTESIAN_POINT('Ctrl Pts',(-2.6236132606113,0.491114226150758,
12.5808169217085));
#432483=CARTESIAN_POINT('Ctrl Pts',(-2.62381816296463,0.492191158546528,
12.5804173076348));
#432484=CARTESIAN_POINT('Ctrl Pts',(-2.62413290203032,0.493152623412337,
12.5799304713245));
#432485=CARTESIAN_POINT('Ctrl Pts',(-2.62452296288574,0.49434418127374,
12.5793271277669));
#432486=CARTESIAN_POINT('Ctrl Pts',(-2.62507531595854,0.495442324657529,
12.5785808224116));
#432487=CARTESIAN_POINT('Ctrl Pts',(-2.62573834403119,0.496415016611789,
12.5777485681082));
#432488=CARTESIAN_POINT('Ctrl Pts',(-2.62672632849958,0.497864434189996,
12.576508418016));
#432489=CARTESIAN_POINT('Ctrl Pts',(-2.62794606111148,0.499026962411696,
12.5750928681475));
#432490=CARTESIAN_POINT('Ctrl Pts',(-2.62916808382621,0.499763384950565,
12.5737548217797));
#432491=CARTESIAN_POINT('Ctrl Pts',(-2.62916808382621,0.499763384950565,
12.5737548217797));
#432492=CARTESIAN_POINT('Ctrl Pts',(-2.62293347207068,0.514893926616768,
12.5770542771492));
#432493=CARTESIAN_POINT('Ctrl Pts',(-2.63242388933657,0.521089942649588,
12.5893111709658));
#432494=CARTESIAN_POINT('Ctrl Pts',(-2.64992750452856,0.513256398189767,
12.5508408821982));
#432495=CARTESIAN_POINT('Ctrl Pts',(-2.64367060449799,0.5284325942427,12.55409748406));
#432496=CARTESIAN_POINT('Ctrl Pts',(-2.65317312910571,0.534636514805103,
12.5663972313419));
#432497=CARTESIAN_POINT('Ctrl Pts',(-2.67066600309183,0.526737219423367,
12.52790050457));
#432498=CARTESIAN_POINT('Ctrl Pts',(-2.6643680203809,0.54194533209766,12.5311362602938));
#432499=CARTESIAN_POINT('Ctrl Pts',(-2.67390143630145,0.548169420695304,
12.5434568539655));
#432500=CARTESIAN_POINT('Ctrl Pts',(-2.69138519788797,0.540206807737659,
12.5049357605811));
#432501=CARTESIAN_POINT('Ctrl Pts',(-2.68502985996609,0.555434843227771,
12.5081700652078));
#432502=CARTESIAN_POINT('Ctrl Pts',(-2.69461045036723,0.56168973066488,
12.5204921097672));
#432503=CARTESIAN_POINT('Ctrl Pts',(-2.69002469347584,0.539322343100433,
12.5064436508395));
#432504=CARTESIAN_POINT('Ctrl Pts',(-2.68999175912047,0.540542082055627,
12.5062361689309));
#432505=CARTESIAN_POINT('Ctrl Pts',(-2.68990549770766,0.541809106360485,
12.5061871075061));
#432506=CARTESIAN_POINT('Ctrl Pts',(-2.68975320661061,0.543028870297842,
12.5063648335164));
#432507=CARTESIAN_POINT('Ctrl Pts',(-2.68968402660063,0.54358296231635,
12.5064455676329));
#432508=CARTESIAN_POINT('Ctrl Pts',(-2.68960003758825,0.544135003120524,
12.506574497099));
#432509=CARTESIAN_POINT('Ctrl Pts',(-2.68950380177739,0.5446611647812,12.5067492519495));
#432510=CARTESIAN_POINT('Ctrl Pts',(-2.68931041217985,0.545718507062495,
12.5071004286051));
#432511=CARTESIAN_POINT('Ctrl Pts',(-2.68905966175249,0.546710072287434,
12.5076537929613));
#432512=CARTESIAN_POINT('Ctrl Pts',(-2.68877954041675,0.547563757172874,
12.5083435010505));
#432513=CARTESIAN_POINT('Ctrl Pts',(-2.68876190510465,0.547617501738062,
12.5083869222964));
#432514=CARTESIAN_POINT('Ctrl Pts',(-2.68874414011912,0.54767070196071,
12.5084308732337));
#432515=CARTESIAN_POINT('Ctrl Pts',(-2.68872624710657,0.547723341111141,
12.5084753333615));
#432516=CARTESIAN_POINT('Ctrl Pts',(-2.68858272152925,0.548145576574968,
12.5088319622689));
#432517=CARTESIAN_POINT('Ctrl Pts',(-2.68842926613241,0.548540699037134,
12.509227847131));
#432518=CARTESIAN_POINT('Ctrl Pts',(-2.68827305406093,0.54889797314926,
12.5096423454524));
#432519=CARTESIAN_POINT('Ctrl Pts',(-2.68778355456546,0.550017512093765,
12.5109411997424));
#432520=CARTESIAN_POINT('Ctrl Pts',(-2.68724573827064,0.550838143388983,
12.5124831113042));
#432521=CARTESIAN_POINT('Ctrl Pts',(-2.68671124461061,0.551439171676893,
12.5140723025008));
#432522=CARTESIAN_POINT('Ctrl Pts',(-2.68666116196925,0.551495488685758,
12.5142212114565));
#432523=CARTESIAN_POINT('Ctrl Pts',(-2.68661111490232,0.551549906510581,
12.5143705582413));
#432524=CARTESIAN_POINT('Ctrl Pts',(-2.68656115105941,0.551602506571629,
12.5145201959299));
#432525=CARTESIAN_POINT('Ctrl Pts',(-2.68591929110873,0.552278232669096,
12.5164425148273));
#432526=CARTESIAN_POINT('Ctrl Pts',(-2.68527695902345,0.552684517386472,
12.5184635205941));
#432527=CARTESIAN_POINT('Ctrl Pts',(-2.68463688404735,0.55291153017412,
12.5205025929158));
#432528=CARTESIAN_POINT('Ctrl Pts',(-2.68426561519101,0.553043206588901,
12.5216853356836));
#432529=CARTESIAN_POINT('Ctrl Pts',(-2.68389593802785,0.553114785563373,
12.5228750347131));
#432530=CARTESIAN_POINT('Ctrl Pts',(-2.68353428572838,0.553143341873244,
12.5240609649613));
#432531=CARTESIAN_POINT('Ctrl Pts',(-2.68264662956129,0.553213431803828,
12.5269717671326));
#432532=CARTESIAN_POINT('Ctrl Pts',(-2.68178151709282,0.553015949133506,
12.5299036066169));
#432533=CARTESIAN_POINT('Ctrl Pts',(-2.68093349742623,0.552637379759122,
12.5328133004019));
#432534=CARTESIAN_POINT('Ctrl Pts',(-2.68052639860756,0.552455644415982,
12.5342101228451));
#432535=CARTESIAN_POINT('Ctrl Pts',(-2.68012396050527,0.552231924768891,
12.5356023438238));
#432536=CARTESIAN_POINT('Ctrl Pts',(-2.67972872331797,0.551973886059748,
12.5369868989719));
#432537=CARTESIAN_POINT('Origin',(-13.3497998213102,7.52447901476919,-1.24101070188029));
#432538=CARTESIAN_POINT('Ctrl Pts',(-2.69920792530587,0.446861182319613,
12.5369868989719));
#432539=CARTESIAN_POINT('Ctrl Pts',(-2.71421215066287,0.443674251959329,
12.5369868989719));
#432540=CARTESIAN_POINT('Ctrl Pts',(-2.71641003076791,0.428493585744408,
12.5369868989719));
#432541=CARTESIAN_POINT('Ctrl Pts',(-2.70427992653162,0.445783810450665,
12.5218025310015));
#432542=CARTESIAN_POINT('Ctrl Pts',(-2.71468600954219,0.440182980147849,
12.5216901060417));
#432543=CARTESIAN_POINT('Ctrl Pts',(-2.71640334722253,0.428539863809084,
12.5161920673678));
#432544=CARTESIAN_POINT('Ctrl Pts',(-2.70873673120405,0.449842500301691,
12.5042015548895));
#432545=CARTESIAN_POINT('Ctrl Pts',(-2.71373584230073,0.44579450903935,
12.4980677368514));
#432546=CARTESIAN_POINT('Ctrl Pts',(-2.7148315199549,0.439087030362391,
12.4907278922777));
#432547=CARTESIAN_POINT('Ctrl Pts',(-2.70429675115723,0.462353517522103,
12.506463626192));
#432548=CARTESIAN_POINT('Ctrl Pts',(-2.71074591258632,0.463456130417869,
12.4999376786891));
#432549=CARTESIAN_POINT('Ctrl Pts',(-2.71066714545653,0.463442663604545,
12.4906970594712));
#432550=CARTESIAN_POINT('Origin',(-2.69463704657199,0.425341259745399,12.5369868989719));
#432551=CARTESIAN_POINT('Origin',(-2.69463704657199,0.425341259745399,14.));
#432552=CARTESIAN_POINT('Origin',(-2.69463704657199,0.4253412597454,13.7435492065112));
#432553=CARTESIAN_POINT('Ctrl Pts',(-2.67503881381097,0.452042773314378,
13.793642941384));
#432554=CARTESIAN_POINT('Ctrl Pts',(-2.68561657471053,0.449802864084712,
13.8071662555867));
#432555=CARTESIAN_POINT('Ctrl Pts',(-2.68457645852668,0.432804701185187,
13.8103758687955));
#432556=CARTESIAN_POINT('Ctrl Pts',(-2.69129064578038,0.448558571417166,
13.7804579775006));
#432557=CARTESIAN_POINT('Ctrl Pts',(-2.70434054585607,0.44578480507073,
13.7901904343351));
#432558=CARTESIAN_POINT('Ctrl Pts',(-2.70593540090513,0.43010959019064,
13.7927914348262));
#432559=CARTESIAN_POINT('Ctrl Pts',(-2.70085871087808,0.446507290597821,
13.7597120340895));
#432560=CARTESIAN_POINT('Ctrl Pts',(-2.71595992897568,0.443291656610529,
13.7635825532445));
#432561=CARTESIAN_POINT('Ctrl Pts',(-2.71852754465409,0.428494925016269,
13.7651073818884));
#432562=CARTESIAN_POINT('Ctrl Pts',(-2.69898506464799,0.446908978350449,
13.7381884353898));
#432563=CARTESIAN_POINT('Ctrl Pts',(-2.71373299779985,0.44376949139001,
13.7368803041982));
#432564=CARTESIAN_POINT('Ctrl Pts',(-2.71606156587467,0.428810634219766,
13.7363986145813));
#432565=CARTESIAN_POINT('Origin',(-2.67437054464763,0.429686163521208,13.7902182540695));
#432566=CARTESIAN_POINT('Ctrl Pts',(-2.64400620214131,0.458695833579019,
13.8235227101244));
#432567=CARTESIAN_POINT('Ctrl Pts',(-2.65524875977548,0.456290093326659,
13.8358800583119));
#432568=CARTESIAN_POINT('Ctrl Pts',(-2.65474553983446,0.439725890395412,
13.8390832900376));
#432569=CARTESIAN_POINT('Ctrl Pts',(-2.6556687725148,0.456195513283816,
13.8124254819053));
#432570=CARTESIAN_POINT('Ctrl Pts',(-2.66693316297831,0.453785100845986,
13.8247886449158));
#432571=CARTESIAN_POINT('Ctrl Pts',(-2.66641227077076,0.437200485914952,
13.8279860620657));
#432572=CARTESIAN_POINT('Ctrl Pts',(-2.66732611610358,0.453696313550856,
13.8013225099954));
#432573=CARTESIAN_POINT('Ctrl Pts',(-2.67860702483252,0.451282368215402,
13.8136962257787));
#432574=CARTESIAN_POINT('Ctrl Pts',(-2.67807365792967,0.434676515493284,
13.8168830918626));
#432575=CARTESIAN_POINT('Ctrl Pts',(-2.67897843627399,0.45119819078075,
13.7902140179785));
#432576=CARTESIAN_POINT('Ctrl Pts',(-2.69027089604951,0.448781777371834,
13.802602731458));
#432577=CARTESIAN_POINT('Ctrl Pts',(-2.68972991167053,0.43215392458132,
13.8057746032558));
#432578=CARTESIAN_POINT('Origin',(-2.63939829832935,0.437183808928588,13.8235269408515));
#432579=CARTESIAN_POINT('Ctrl Pts',(-2.63242388933657,0.521089942649588,
13.8235269408515));
#432580=CARTESIAN_POINT('Ctrl Pts',(-2.6423108072789,0.52754482238454,13.8362179249168));
#432581=CARTESIAN_POINT('Ctrl Pts',(-2.63541047324264,0.54316687072159,
13.8391868794938));
#432582=CARTESIAN_POINT('Ctrl Pts',(-2.62337778977126,0.515184008656295,
13.8400110824519));
#432583=CARTESIAN_POINT('Ctrl Pts',(-2.62943449763647,0.523223794268897,
13.8494522556836));
#432584=CARTESIAN_POINT('Ctrl Pts',(-2.62058457010541,0.533353289326912,
13.85569149686));
#432585=CARTESIAN_POINT('Ctrl Pts',(-2.61457773780764,0.501474274469136,
13.8586819406588));
#432586=CARTESIAN_POINT('Ctrl Pts',(-2.61379653394518,0.505757470023888,
13.868010383617));
#432587=CARTESIAN_POINT('Ctrl Pts',(-2.6060991751906,0.510515992378134,
13.8744918421245));
#432588=CARTESIAN_POINT('Ctrl Pts',(-2.62023852895725,0.470700471624714,
13.8587686893867));
#432589=CARTESIAN_POINT('Ctrl Pts',(-2.62101272471808,0.466455386367178,
13.8680909899357));
#432590=CARTESIAN_POINT('Ctrl Pts',(-2.6155252605559,0.459287113313332,
13.8745789365162));
#432591=CARTESIAN_POINT('Ctrl Pts',(-2.63342956069134,0.460963344032332,
13.8400379222776));
#432592=CARTESIAN_POINT('Ctrl Pts',(-2.64196284407893,0.455629179755203,
13.8494748685453));
#432593=CARTESIAN_POINT('Ctrl Pts',(-2.63734258833735,0.443003240497187,
13.8557104837033));
#432594=CARTESIAN_POINT('Ctrl Pts',(-2.64401005104216,0.458695009188572,
13.8235269408542));
#432595=CARTESIAN_POINT('Ctrl Pts',(-2.65555519189024,0.456219864427462,
13.8362179249195));
#432596=CARTESIAN_POINT('Ctrl Pts',(-2.65472321565694,0.439161997632241,
13.8391868794965));
#432597=CARTESIAN_POINT('Origin',(-2.62039699312969,0.539511499794106,13.8235269408515));
#432598=CARTESIAN_POINT('Ctrl Pts',(-2.66236978713557,0.540640744926744,
13.7902140241683));
#432599=CARTESIAN_POINT('Ctrl Pts',(-2.67204194591,0.546950098303653,13.8026027327198));
#432600=CARTESIAN_POINT('Ctrl Pts',(-2.66556758396333,0.562275259629291,
13.8057746032556));
#432601=CARTESIAN_POINT('Ctrl Pts',(-2.65239108398142,0.53412594130855,
13.8013225161808));
#432602=CARTESIAN_POINT('Ctrl Pts',(-2.66205334779722,0.540428844277751,
13.8136962270464));
#432603=CARTESIAN_POINT('Ctrl Pts',(-2.65559399359612,0.555736206840193,
13.8168830918628));
#432604=CARTESIAN_POINT('Ctrl Pts',(-2.64240807891856,0.527608329099887,
13.8124254880875));
#432605=CARTESIAN_POINT('Ctrl Pts',(-2.65205619396754,0.533902004579433,
13.8247886461867));
#432606=CARTESIAN_POINT('Ctrl Pts',(-2.64561610727078,0.549194023593803,
13.8279860620656));
#432607=CARTESIAN_POINT('Ctrl Pts',(-2.63242059778891,0.521087794598028,
13.8235227163066));
#432608=CARTESIAN_POINT('Ctrl Pts',(-2.64205001280595,0.527369271308659,
13.8358800595848));
#432609=CARTESIAN_POINT('Ctrl Pts',(-2.6356337482334,0.542648583457214,
13.8390832900376));
#432610=CARTESIAN_POINT('Origin',(-2.6503461928975,0.559064456922601,13.7902182540695));
#432611=CARTESIAN_POINT('Ctrl Pts',(-2.67950274280156,0.551826382928712,
13.7382347919292));
#432612=CARTESIAN_POINT('Ctrl Pts',(-2.69215163179234,0.560055810371279,
13.7369371795942));
#432613=CARTESIAN_POINT('Ctrl Pts',(-2.68894413082543,0.574863096232227,
13.7364597369711));
#432614=CARTESIAN_POINT('Ctrl Pts',(-2.68108662734283,0.552860454369261,
13.7595490285574));
#432615=CARTESIAN_POINT('Ctrl Pts',(-2.69403675967933,0.561287071655363,
13.7633824266926));
#432616=CARTESIAN_POINT('Ctrl Pts',(-2.69110574879531,0.576028266841136,
13.7648920890506));
#432617=CARTESIAN_POINT('Ctrl Pts',(-2.67300890295897,0.547586746666806,
13.780380659011));
#432618=CARTESIAN_POINT('Ctrl Pts',(-2.68421324823137,0.554870944153222,
13.7901039518744));
#432619=CARTESIAN_POINT('Ctrl Pts',(-2.68008734598676,0.570084831627961,
13.7926933640891));
#432620=CARTESIAN_POINT('Ctrl Pts',(-2.65896801476284,0.538419865504878,
13.7936647693663));
#432621=CARTESIAN_POINT('Ctrl Pts',(-2.66804058847989,0.54430728752929,
13.8072068914933));
#432622=CARTESIAN_POINT('Ctrl Pts',(-2.660950206824,0.559811182453508,13.8104111085397));
#432623=CARTESIAN_POINT('Origin',(-2.66770182711108,0.570395443204266,13.7435492065112));
#432624=CARTESIAN_POINT('Origin',(-2.66770182711109,0.570395443204266,14.));
#432625=CARTESIAN_POINT('Origin',(-2.66770182711109,0.570395443204266,12.5369868989719));
#432626=CARTESIAN_POINT('Ctrl Pts',(-2.69000666893073,0.539318729353612,
12.506462012331));
#432627=CARTESIAN_POINT('Ctrl Pts',(-2.69641771158035,0.540604077607787,
12.4999388158272));
#432628=CARTESIAN_POINT('Ctrl Pts',(-2.69634186053824,0.540588870252309,
12.4907030323752));
#432629=CARTESIAN_POINT('Ctrl Pts',(-2.68965717673216,0.552589239455252,
12.5042014951932));
#432630=CARTESIAN_POINT('Ctrl Pts',(-2.69286920995931,0.558159153248441,
12.4980716682128));
#432631=CARTESIAN_POINT('Ctrl Pts',(-2.69148635757615,0.564808460318541,
12.4907355092743));
#432632=CARTESIAN_POINT('Ctrl Pts',(-2.68404205200784,0.554779233878853,
12.5218047446509));
#432633=CARTESIAN_POINT('Ctrl Pts',(-2.69173908484124,0.563738840817663,
12.5216906929433));
#432634=CARTESIAN_POINT('Ctrl Pts',(-2.68916697438798,0.575217298995718,
12.5161988840776));
#432635=CARTESIAN_POINT('Ctrl Pts',(-2.67969653749964,0.551952912936035,
12.5369868989719));
#432636=CARTESIAN_POINT('Ctrl Pts',(-2.69254753580896,0.560310985319929,
12.5369868989719));
#432637=CARTESIAN_POINT('Ctrl Pts',(-2.68915699292679,0.575261227809088,
12.5369868989719));
#432638=CARTESIAN_POINT('Origin',(-5.06527468391093E-31,-4.21128796913923E-31,
12.5));
#432639=CARTESIAN_POINT('Origin',(-2.66613838389344,0.304789073640317,12.5));
#432640=CARTESIAN_POINT('',(-2.66613838389344,0.304789073640317,12.5893111709658));
#432641=CARTESIAN_POINT('',(-2.66613838389344,0.304789073640317,13.8235269408515));
#432642=CARTESIAN_POINT('',(-2.66613838389344,0.304789073640317,12.5));
#432643=CARTESIAN_POINT('',(-2.69758167769643,0.32183583210109,13.7902182540695));
#432644=CARTESIAN_POINT('',(-2.66613838389344,0.304789073640317,13.8235269408515));
#432645=CARTESIAN_POINT('',(-2.71580314304261,0.331714470150389,13.7435492065112));
#432646=CARTESIAN_POINT('Origin',(-2.65585491815991,0.299213595166166,13.7445212918688));
#432647=CARTESIAN_POINT('',(-2.71580314304261,0.331714470150389,12.5369868989719));
#432648=CARTESIAN_POINT('',(-2.71580314304261,0.331714470150389,12.5));
#432649=CARTESIAN_POINT('Ctrl Pts',(-2.71580314304261,0.331714470150389,
12.5369868989719));
#432650=CARTESIAN_POINT('Ctrl Pts',(-2.69926029747777,0.32274588389589,
12.5544431401645));
#432651=CARTESIAN_POINT('Ctrl Pts',(-2.6827056200301,0.313770883070132,
12.5718848856037));
#432652=CARTESIAN_POINT('Ctrl Pts',(-2.66613838389344,0.304789073640317,
12.5893111709658));
#432653=CARTESIAN_POINT('Origin',(-2.93589676306087,0.162285249320105,12.5));
#432654=CARTESIAN_POINT('',(-2.72668989544586,0.225351759568759,13.7435492065112));
#432655=CARTESIAN_POINT('',(-2.70684497862863,0.231334114087542,13.7902182540695));
#432656=CARTESIAN_POINT('Origin',(-2.65469596712568,0.247054707803714,13.7418732680452));
#432657=CARTESIAN_POINT('',(-2.67260022728041,0.241657374439776,13.8235269408515));
#432658=CARTESIAN_POINT('',(-2.70684497862863,0.231334114087542,13.7902182540695));
#432659=CARTESIAN_POINT('',(-2.67260022728041,0.241657374439776,12.5893111709658));
#432660=CARTESIAN_POINT('',(-2.67260022728041,0.241657374439776,12.5));
#432661=CARTESIAN_POINT('',(-2.72668989544586,0.225351759568759,12.5369868989719));
#432662=CARTESIAN_POINT('Ctrl Pts',(-2.67260022728041,0.241657374439776,
12.5893111709658));
#432663=CARTESIAN_POINT('Ctrl Pts',(-2.69064353042739,0.236218125834742,
12.5718848856037));
#432664=CARTESIAN_POINT('Ctrl Pts',(-2.70867315596209,0.230783000417846,
12.5544431401645));
#432665=CARTESIAN_POINT('Ctrl Pts',(-2.72668989544586,0.225351759568759,
12.5369868989719));
#432666=CARTESIAN_POINT('',(-2.72668989544586,0.225351759568759,12.5));
#432667=CARTESIAN_POINT('Origin',(-2.68252174292037,0.274569441412333,12.5));
#432668=CARTESIAN_POINT('',(-2.64823028187141,0.272184934900437,13.8587068136939));
#432669=CARTESIAN_POINT('Ctrl Pts',(-2.67260022727837,0.241657374433491,
13.8235269408542));
#432670=CARTESIAN_POINT('Ctrl Pts',(-2.67092250335409,0.242163133131915,
13.8262006681044));
#432671=CARTESIAN_POINT('Ctrl Pts',(-2.6692557437193,0.242847048588549,
13.8288634856214));
#432672=CARTESIAN_POINT('Ctrl Pts',(-2.66760059200199,0.243695801952421,
13.8314912288862));
#432673=CARTESIAN_POINT('Ctrl Pts',(-2.66589430130243,0.244570779125726,
13.834200161153));
#432674=CARTESIAN_POINT('Ctrl Pts',(-2.66419822490259,0.245621467252351,
13.8368750301949));
#432675=CARTESIAN_POINT('Ctrl Pts',(-2.66251412552991,0.246878463044179,
13.8394886372968));
#432676=CARTESIAN_POINT('Ctrl Pts',(-2.66238405845029,0.246975543878232,
13.839690492513));
#432677=CARTESIAN_POINT('Ctrl Pts',(-2.6622540728036,0.24707387507256,13.8398919674349));
#432678=CARTESIAN_POINT('Ctrl Pts',(-2.66212417544159,0.24717348044291,
13.8400930404591));
#432679=CARTESIAN_POINT('Ctrl Pts',(-2.66010028715085,0.248725399124106,
13.8432258934518));
#432680=CARTESIAN_POINT('Ctrl Pts',(-2.65810747290765,0.250577821396457,
13.8462331177034));
#432681=CARTESIAN_POINT('Ctrl Pts',(-2.65627640534004,0.252740986569638,
13.8489036603661));
#432682=CARTESIAN_POINT('Ctrl Pts',(-2.65567725872272,0.253448799388322,
13.8497774930041));
#432683=CARTESIAN_POINT('Ctrl Pts',(-2.65509566950902,0.254189811509037,
13.85061494757));
#432684=CARTESIAN_POINT('Ctrl Pts',(-2.6545368964848,0.254964167004262,
13.8514076489583));
#432685=CARTESIAN_POINT('Ctrl Pts',(-2.65335501095143,0.256602040555441,
13.8530843267192));
#432686=CARTESIAN_POINT('Ctrl Pts',(-2.65216150767304,0.258551700020984,
13.8546805203176));
#432687=CARTESIAN_POINT('Ctrl Pts',(-2.65114202945552,0.260771226322149,
13.8559412814273));
#432688=CARTESIAN_POINT('Ctrl Pts',(-2.65100559020755,0.261068270922185,
13.8561100121513));
#432689=CARTESIAN_POINT('Ctrl Pts',(-2.65087223554554,0.261370079482595,
13.8562727473908));
#432690=CARTESIAN_POINT('Ctrl Pts',(-2.65074237013054,0.261676487288807,
13.8564289040185));
#432691=CARTESIAN_POINT('Ctrl Pts',(-2.65015343195509,0.263066043194364,
13.8571370725437));
#432692=CARTESIAN_POINT('Ctrl Pts',(-2.64962799811819,0.264575500587848,
13.8577210840553));
#432693=CARTESIAN_POINT('Ctrl Pts',(-2.64921420914942,0.266155834665666,
13.8581177131616));
#432694=CARTESIAN_POINT('Ctrl Pts',(-2.64909767193363,0.266600911135426,
13.8582294175695));
#432695=CARTESIAN_POINT('Ctrl Pts',(-2.64898983048389,0.267051531618308,
13.8583265086086));
#432696=CARTESIAN_POINT('Ctrl Pts',(-2.64889135421829,0.267506432392544,
13.8584082369006));
#432697=CARTESIAN_POINT('Ctrl Pts',(-2.64874987023207,0.268160002818657,
13.8585256585398));
#432698=CARTESIAN_POINT('Ctrl Pts',(-2.64862627488924,0.268830602447368,
13.8586122832068));
#432699=CARTESIAN_POINT('Ctrl Pts',(-2.64852455544563,0.269500954176995,
13.8586682984299));
#432700=CARTESIAN_POINT('Ctrl Pts',(-2.64844318997386,0.270037169110867,
13.8587131050557));
#432701=CARTESIAN_POINT('Ctrl Pts',(-2.64837469109747,0.270579112748801,
13.8587357943552));
#432702=CARTESIAN_POINT('Ctrl Pts',(-2.64831955312531,0.271126912995427,
13.8587355499465));
#432703=CARTESIAN_POINT('Ctrl Pts',(-2.64828391613936,0.271480969354972,
13.8587353919793));
#432704=CARTESIAN_POINT('Ctrl Pts',(-2.64825420735979,0.271833639631159,
13.8587257282814));
#432705=CARTESIAN_POINT('Ctrl Pts',(-2.64823028187141,0.272184934900437,
13.8587068136939));
#432706=CARTESIAN_POINT('Ctrl Pts',(-2.64823028187141,0.272184934900437,
13.8587068136939));
#432707=CARTESIAN_POINT('Ctrl Pts',(-2.64815159224441,0.273340325890064,
13.8586446046466));
#432708=CARTESIAN_POINT('Ctrl Pts',(-2.64813538423794,0.274480862310758,
13.858482427929));
#432709=CARTESIAN_POINT('Ctrl Pts',(-2.64817719388495,0.275606786970262,
13.8582284286032));
#432710=CARTESIAN_POINT('Ctrl Pts',(-2.64822008571928,0.276761854697963,
13.8579678548414));
#432711=CARTESIAN_POINT('Ctrl Pts',(-2.64832567286529,0.277904309142861,
13.857615680862));
#432712=CARTESIAN_POINT('Ctrl Pts',(-2.64848014407854,0.278990001618561,
13.8571944833187));
#432713=CARTESIAN_POINT('Ctrl Pts',(-2.64886564278924,0.281699458227203,
13.8561433417727));
#432714=CARTESIAN_POINT('Ctrl Pts',(-2.64956887779495,0.284182814934247,
13.8546163505474));
#432715=CARTESIAN_POINT('Ctrl Pts',(-2.65040285734276,0.286351799711337,
13.8528973491086));
#432716=CARTESIAN_POINT('Ctrl Pts',(-2.65055521310192,0.286748041229711,
13.8525833129072));
#432717=CARTESIAN_POINT('Ctrl Pts',(-2.65071183875195,0.28713389685014,
13.8522628768811));
#432718=CARTESIAN_POINT('Ctrl Pts',(-2.65087149822655,0.287508979248182,
13.851937733538));
#432719=CARTESIAN_POINT('Ctrl Pts',(-2.65184651648625,0.289799555412767,
13.8499521282529));
#432720=CARTESIAN_POINT('Ctrl Pts',(-2.65303532837086,0.291914400563566,
13.847639871647));
#432721=CARTESIAN_POINT('Ctrl Pts',(-2.65430542018226,0.293781734349322,
13.8452109780794));
#432722=CARTESIAN_POINT('Ctrl Pts',(-2.6548768607778,0.294621886471421,
13.8441181685877));
#432723=CARTESIAN_POINT('Ctrl Pts',(-2.65546433748986,0.295412519228075,
13.8430021611332));
#432724=CARTESIAN_POINT('Ctrl Pts',(-2.65605478550131,0.296150250405443,
13.8418824960098));
#432725=CARTESIAN_POINT('Ctrl Pts',(-2.65744619131792,0.297888732763546,
13.8392439765549));
#432726=CARTESIAN_POINT('Ctrl Pts',(-2.65891765954228,0.299418911650689,
13.8364981347964));
#432727=CARTESIAN_POINT('Ctrl Pts',(-2.66044841549995,0.300768553540579,
13.8336931113419));
#432728=CARTESIAN_POINT('Ctrl Pts',(-2.66193927459073,0.302083019031147,
13.8309611966328));
#432729=CARTESIAN_POINT('Ctrl Pts',(-2.66348823843773,0.303227129575497,
13.8281701127186));
#432730=CARTESIAN_POINT('Ctrl Pts',(-2.66508959981538,0.304189622649689,
13.8253580685121));
#432731=CARTESIAN_POINT('Ctrl Pts',(-2.6654367766903,0.304398292186929,
13.8247484142933));
#432732=CARTESIAN_POINT('Ctrl Pts',(-2.66578640770474,0.304598252248951,
13.8241378483365));
#432733=CARTESIAN_POINT('Ctrl Pts',(-2.66613838389344,0.304789073640317,
13.8235269408515));
#432734=CARTESIAN_POINT('',(-2.64833877401582,0.270947596501946,12.5969504640361));
#432735=CARTESIAN_POINT('Origin',(-2.68255463643422,0.274573005056113,12.584524458991));
#432736=CARTESIAN_POINT('Origin',(-2.68255463643422,0.274573005056113,12.584524458991));
#432737=CARTESIAN_POINT('Ctrl Pts',(-2.67260022728041,0.241657374439776,
12.5893111709658));
#432738=CARTESIAN_POINT('Ctrl Pts',(-2.66174861915796,0.244928648765858,
12.5770542771492));
#432739=CARTESIAN_POINT('Ctrl Pts',(-2.6634679191406,0.261202790292361,
12.5737548217797));
#432740=CARTESIAN_POINT('Ctrl Pts',(-2.69632905233628,0.234504195360933,
12.5663937883685));
#432741=CARTESIAN_POINT('Ctrl Pts',(-2.68546360148064,0.237779642651723,
12.5540940315304));
#432742=CARTESIAN_POINT('Ctrl Pts',(-2.68719142264049,0.2541038770703,12.5508374392248));
#432743=CARTESIAN_POINT('Ctrl Pts',(-2.72003393529857,0.227358233752083,
12.5434499600945));
#432744=CARTESIAN_POINT('Ctrl Pts',(-2.70913315699288,0.230644330688506,
12.5311293540533));
#432745=CARTESIAN_POINT('Ctrl Pts',(-2.71089140953306,0.247010769292089,
12.5278936106989));
#432746=CARTESIAN_POINT('Ctrl Pts',(-2.74371675158423,0.22021892425893,
12.5204817579905));
#432747=CARTESIAN_POINT('Ctrl Pts',(-2.73276202187558,0.223521285129382,
12.5081597038247));
#432748=CARTESIAN_POINT('Ctrl Pts',(-2.73456970364935,0.239923002463233,
12.5049254088044));
#432749=CARTESIAN_POINT('Ctrl Pts',(-2.72668989544586,0.225351759568759,
12.5369868989719));
#432750=CARTESIAN_POINT('Ctrl Pts',(-2.727581757252,0.225082903307011,12.5342545179733));
#432751=CARTESIAN_POINT('Ctrl Pts',(-2.72846891440114,0.224945756283421,
12.5314872231885));
#432752=CARTESIAN_POINT('Ctrl Pts',(-2.72930993230297,0.22500328887358,
12.5287124745063));
#432753=CARTESIAN_POINT('Ctrl Pts',(-2.73006840399125,0.225055174619049,
12.5262100684184));
#432754=CARTESIAN_POINT('Ctrl Pts',(-2.73078851669635,0.225266328661584,
12.5237004536639));
#432755=CARTESIAN_POINT('Ctrl Pts',(-2.73146398251014,0.225703988924608,
12.5212220730815));
#432756=CARTESIAN_POINT('Ctrl Pts',(-2.73198111002305,0.226039055716585,
12.5193246583486));
#432757=CARTESIAN_POINT('Ctrl Pts',(-2.73247790432002,0.226511420035291,
12.517417831369));
#432758=CARTESIAN_POINT('Ctrl Pts',(-2.73290258723252,0.227203380386272,
12.5155812248347));
#432759=CARTESIAN_POINT('Ctrl Pts',(-2.73308350443592,0.227498159215093,
12.5147988205793));
#432760=CARTESIAN_POINT('Ctrl Pts',(-2.73325175458264,0.227832944795516,
12.5140295443047));
#432761=CARTESIAN_POINT('Ctrl Pts',(-2.73340545939293,0.228214202692653,
12.5132817086137));
#432762=CARTESIAN_POINT('Ctrl Pts',(-2.73363807083058,0.228791184944568,
12.5121499604604));
#432763=CARTESIAN_POINT('Ctrl Pts',(-2.73383575960262,0.229489735061785,
12.5110494206568));
#432764=CARTESIAN_POINT('Ctrl Pts',(-2.7339678607362,0.230330984967703,
12.5100666561695));
#432765=CARTESIAN_POINT('Ctrl Pts',(-2.7340437129029,0.230814028726455,
12.5095023550641));
#432766=CARTESIAN_POINT('Ctrl Pts',(-2.73409817218707,0.231349803419567,
12.5089719619137));
#432767=CARTESIAN_POINT('Ctrl Pts',(-2.73412386357233,0.23192891242457,
12.5085043804652));
#432768=CARTESIAN_POINT('Ctrl Pts',(-2.73416145956812,0.232776363019137,
12.5078201359221));
#432769=CARTESIAN_POINT('Ctrl Pts',(-2.73413733431634,0.233741244351165,
12.5072563000949));
#432770=CARTESIAN_POINT('Ctrl Pts',(-2.73404465979884,0.234757940087455,
12.5068768744332));
#432771=CARTESIAN_POINT('Ctrl Pts',(-2.73397783509199,0.235491047702893,
12.5066032824114));
#432772=CARTESIAN_POINT('Ctrl Pts',(-2.73387425466085,0.236263980762711,
12.5064197834844));
#432773=CARTESIAN_POINT('Ctrl Pts',(-2.733742264661,0.237033920005263,12.5063282718343));
#432774=CARTESIAN_POINT('Ctrl Pts',(-2.73354960012429,0.238157792932223,
12.5061946931565));
#432775=CARTESIAN_POINT('Ctrl Pts',(-2.73329333237519,0.239299487865532,
12.5062515701262));
#432776=CARTESIAN_POINT('Ctrl Pts',(-2.73300445492327,0.240391536141246,
12.5064436508398));
#432777=CARTESIAN_POINT('',(-2.6634679191406,0.261202790292361,12.5737548217797));
#432778=CARTESIAN_POINT('Origin',(-2.67894999728999,0.262721097302213,12.5893111709658));
#432779=CARTESIAN_POINT('Ctrl Pts',(-2.73300445492327,0.240391536141246,
12.5064436508398));
#432780=CARTESIAN_POINT('Ctrl Pts',(-2.72271137877843,0.243472602714325,
12.5164271754438));
#432781=CARTESIAN_POINT('Ctrl Pts',(-2.71241416254567,0.246554690460763,
12.5264061185523));
#432782=CARTESIAN_POINT('Ctrl Pts',(-2.70211266068599,0.249637836252174,
12.536380305637));
#432783=CARTESIAN_POINT('Ctrl Pts',(-2.68923787273109,0.253491143162093,
12.5488460165097));
#432784=CARTESIAN_POINT('Ctrl Pts',(-2.67635638684673,0.257346103845855,
12.5613043021964));
#432785=CARTESIAN_POINT('Ctrl Pts',(-2.6634679191406,0.261202790292361,
12.5737548217797));
#432786=CARTESIAN_POINT('Ctrl Pts',(-2.66613838389344,0.304789073640317,
12.5893111709658));
#432787=CARTESIAN_POINT('Ctrl Pts',(-2.65617451238041,0.299387231451617,
12.5770542771492));
#432788=CARTESIAN_POINT('Ctrl Pts',(-2.66115509936876,0.283798856677239,
12.5737548217797));
#432789=CARTESIAN_POINT('Ctrl Pts',(-2.65684217843296,0.299749201861002,
12.5928319619712));
#432790=CARTESIAN_POINT('Ctrl Pts',(-2.65169850360042,0.293254894693306,
12.5821634970842));
#432791=CARTESIAN_POINT('Ctrl Pts',(-2.65776421811106,0.281971251231409,
12.5773203894503));
#432792=CARTESIAN_POINT('Ctrl Pts',(-2.64678837658131,0.286351247999782,
12.5969440695591));
#432793=CARTESIAN_POINT('Ctrl Pts',(-2.64717949804393,0.282350552241116,
12.5878292599214));
#432794=CARTESIAN_POINT('Ctrl Pts',(-2.65418247444654,0.277194719077306,
12.5813877129824));
#432795=CARTESIAN_POINT('Ctrl Pts',(-2.64985020398195,0.25590785038207,
12.596957478804));
#432796=CARTESIAN_POINT('Ctrl Pts',(-2.64946205278996,0.259878987725584,
12.5878468778671));
#432797=CARTESIAN_POINT('Ctrl Pts',(-2.65528428009154,0.266299201988851,
12.5814011370086));
#432798=CARTESIAN_POINT('Ctrl Pts',(-2.6624610705918,0.244713876535013,
12.5928371701607));
#432799=CARTESIAN_POINT('Ctrl Pts',(-2.65611683232142,0.250032307363024,
12.5821692192952));
#432800=CARTESIAN_POINT('Ctrl Pts',(-2.65976522429226,0.262308832033917,
12.5773318885715));
#432801=CARTESIAN_POINT('Ctrl Pts',(-2.67260022728039,0.241657374439724,
12.5893111709658));
#432802=CARTESIAN_POINT('Ctrl Pts',(-2.66174861915794,0.244928648765806,
12.5770542771492));
#432803=CARTESIAN_POINT('Ctrl Pts',(-2.66346791914058,0.261202790292308,
12.5737548217797));
#432804=CARTESIAN_POINT('',(-2.66115509936876,0.283798856677239,12.5737548217797));
#432805=CARTESIAN_POINT('Origin',(-2.67662373367068,0.285448509014408,12.5893111709658));
#432806=CARTESIAN_POINT('Ctrl Pts',(-2.66346791914058,0.261202790292308,
12.5737548217797));
#432807=CARTESIAN_POINT('Ctrl Pts',(-2.66249948799061,0.261460590096039,
12.5746934679442));
#432808=CARTESIAN_POINT('Ctrl Pts',(-2.6614749776444,0.261922882199321,
12.5756680099006));
#432809=CARTESIAN_POINT('Ctrl Pts',(-2.66050957865738,0.262534035587474,
12.5765688348656));
#432810=CARTESIAN_POINT('Ctrl Pts',(-2.66025399996289,0.262695831681293,
12.5768073183026));
#432811=CARTESIAN_POINT('Ctrl Pts',(-2.66000248368076,0.26286781682604,
12.5770407398754));
#432812=CARTESIAN_POINT('Ctrl Pts',(-2.65975686203997,0.263048485452194,
12.5772674179684));
#432813=CARTESIAN_POINT('Ctrl Pts',(-2.65874889724505,0.263789900639083,
12.5781976435658));
#432814=CARTESIAN_POINT('Ctrl Pts',(-2.65778963545941,0.264728747969256,
12.5790594849312));
#432815=CARTESIAN_POINT('Ctrl Pts',(-2.65697762396725,0.265836145847293,
12.5797571720116));
#432816=CARTESIAN_POINT('Ctrl Pts',(-2.65644856928278,0.266557655383312,
12.580211740231));
#432817=CARTESIAN_POINT('Ctrl Pts',(-2.65597311843985,0.267394604292317,
12.5806009430798));
#432818=CARTESIAN_POINT('Ctrl Pts',(-2.65560014570566,0.268296825996709,
12.5808812374708));
#432819=CARTESIAN_POINT('Ctrl Pts',(-2.65527963839458,0.269072133749717,
12.5811221033394));
#432820=CARTESIAN_POINT('Ctrl Pts',(-2.65502834998581,0.269911558486257,
12.581287365893));
#432821=CARTESIAN_POINT('Ctrl Pts',(-2.65486845135005,0.270770112916528,
12.581359338449));
#432822=CARTESIAN_POINT('Ctrl Pts',(-2.65484622874146,0.270889434253864,
12.5813693411482));
#432823=CARTESIAN_POINT('Ctrl Pts',(-2.65482571219639,0.271009134368885,
12.5813775999465));
#432824=CARTESIAN_POINT('Ctrl Pts',(-2.65480690080815,0.271129103078795,
12.5813841266931));
#432825=CARTESIAN_POINT('Ctrl Pts',(-2.6547749850128,0.271332644505073,
12.5813952001081));
#432826=CARTESIAN_POINT('Ctrl Pts',(-2.65474836531475,0.271538416630948,
12.5814007534795));
#432827=CARTESIAN_POINT('Ctrl Pts',(-2.65472724888778,0.271746355137143,
12.5814005856065));
#432828=CARTESIAN_POINT('Ctrl Pts',(-2.6546305861411,0.272698216319819,
12.5813998171494));
#432829=CARTESIAN_POINT('Ctrl Pts',(-2.65465558459366,0.273629672533526,
12.58127954464));
#432830=CARTESIAN_POINT('Ctrl Pts',(-2.65477252361255,0.274536229411493,
12.5810700125799));
#432831=CARTESIAN_POINT('Ctrl Pts',(-2.65491377263279,0.275631246900311,
12.5808169217085));
#432832=CARTESIAN_POINT('Ctrl Pts',(-2.65520577317846,0.276687894448358,
12.5804173076348));
#432833=CARTESIAN_POINT('Ctrl Pts',(-2.65559783328823,0.277620505963392,
12.5799304713245));
#432834=CARTESIAN_POINT('Ctrl Pts',(-2.65608371927592,0.278776305433444,
12.5793271277669));
#432835=CARTESIAN_POINT('Ctrl Pts',(-2.65672374331989,0.279825772932485,
12.5785808224116));
#432836=CARTESIAN_POINT('Ctrl Pts',(-2.65746384864562,0.280741185391335,
12.5777485681082));
#432837=CARTESIAN_POINT('Ctrl Pts',(-2.65856668666556,0.282105250245944,
12.576508418016));
#432838=CARTESIAN_POINT('Ctrl Pts',(-2.65987711756026,0.283164490719574,
12.5750928681475));
#432839=CARTESIAN_POINT('Ctrl Pts',(-2.66115509936876,0.283798856677239,
12.5737548217797));
#432840=CARTESIAN_POINT('Ctrl Pts',(-2.66115509936876,0.283798856677239,
12.5737548217797));
#432841=CARTESIAN_POINT('Ctrl Pts',(-2.65617451238041,0.299387231451617,
12.5770542771492));
#432842=CARTESIAN_POINT('Ctrl Pts',(-2.66613838389344,0.304789073640317,
12.5893111709658));
#432843=CARTESIAN_POINT('Ctrl Pts',(-2.68294525065326,0.295554887519686,
12.5508408821982));
#432844=CARTESIAN_POINT('Ctrl Pts',(-2.67794617080864,0.311190581470929,
12.55409748406));
#432845=CARTESIAN_POINT('Ctrl Pts',(-2.68792275366984,0.316599315026769,
12.5663972313419));
#432846=CARTESIAN_POINT('Ctrl Pts',(-2.70471355565376,0.30730047227298,
12.52790050457));
#432847=CARTESIAN_POINT('Ctrl Pts',(-2.69967613132898,0.322971325265517,
12.5311362602938));
#432848=CARTESIAN_POINT('Ctrl Pts',(-2.70968514659679,0.328397641820345,
12.5434568539655));
#432849=CARTESIAN_POINT('Ctrl Pts',(-2.72646170553159,0.319036434919816,
12.5049357605811));
#432850=CARTESIAN_POINT('Ctrl Pts',(-2.721368740735,0.334731819418772,12.5081700652078));
#432851=CARTESIAN_POINT('Ctrl Pts',(-2.73142728390559,0.34018498717437,
12.5204921097672));
#432852=CARTESIAN_POINT('Ctrl Pts',(-2.72503363600676,0.318265807005603,
12.5064436508395));
#432853=CARTESIAN_POINT('Ctrl Pts',(-2.72510023128608,0.319484171835756,
12.5062361689309));
#432854=CARTESIAN_POINT('Ctrl Pts',(-2.72511753114434,0.320754011327717,
12.5061871075061));
#432855=CARTESIAN_POINT('Ctrl Pts',(-2.72506516886799,0.321982129739407,
12.5063648335164));
#432856=CARTESIAN_POINT('Ctrl Pts',(-2.72504138269223,0.322540016875481,
12.5064455676329));
#432857=CARTESIAN_POINT('Ctrl Pts',(-2.72500266959679,0.323097066693645,
12.506574497099));
#432858=CARTESIAN_POINT('Ctrl Pts',(-2.72494964106265,0.323629321706796,
12.5067492519495));
#432859=CARTESIAN_POINT('Ctrl Pts',(-2.72484307816486,0.324698908816405,
12.5071004286051));
#432860=CARTESIAN_POINT('Ctrl Pts',(-2.72467398385993,0.325707613177533,
12.5076537929613));
#432861=CARTESIAN_POINT('Ctrl Pts',(-2.72446437784822,0.326581289986317,
12.5083435010505));
#432862=CARTESIAN_POINT('Ctrl Pts',(-2.72445118189717,0.32663629316256,
12.5083869222964));
#432863=CARTESIAN_POINT('Ctrl Pts',(-2.72443781233519,0.326690764377107,
12.5084308732337));
#432864=CARTESIAN_POINT('Ctrl Pts',(-2.72442426943959,0.326744686821748,
12.5084753333615));
#432865=CARTESIAN_POINT('Ctrl Pts',(-2.72431563754193,0.32717721599888,
12.5088319622689));
#432866=CARTESIAN_POINT('Ctrl Pts',(-2.72419489890408,0.3275835317631,12.509227847131));
#432867=CARTESIAN_POINT('Ctrl Pts',(-2.72406832777229,0.327952349809118,
12.5096423454524));
#432868=CARTESIAN_POINT('Ctrl Pts',(-2.72367170986328,0.329108062333313,
12.5109411997424));
#432869=CARTESIAN_POINT('Ctrl Pts',(-2.72320257217674,0.329969800066465,
12.5124831113042));
#432870=CARTESIAN_POINT('Ctrl Pts',(-2.72271884638541,0.330612394677618,
12.5140723025008));
#432871=CARTESIAN_POINT('Ctrl Pts',(-2.72267352074896,0.330672606496496,
12.5142212114565));
#432872=CARTESIAN_POINT('Ctrl Pts',(-2.72262807576743,0.330730922551065,
12.5143705582413));
#432873=CARTESIAN_POINT('Ctrl Pts',(-2.72258256556837,0.330787420106788,
12.5145201959299));
#432874=CARTESIAN_POINT('Ctrl Pts',(-2.72199791930382,0.331513215326123,
12.5164425148273));
#432875=CARTESIAN_POINT('Ctrl Pts',(-2.72139084050179,0.331970504192687,
12.518463520594));
#432876=CARTESIAN_POINT('Ctrl Pts',(-2.72077139897204,0.33224893366673,
12.5205025929157));
#432877=CARTESIAN_POINT('Ctrl Pts',(-2.72041209833242,0.332410433797589,
12.5216853356836));
#432878=CARTESIAN_POINT('Ctrl Pts',(-2.72004948559046,0.332511906719643,
12.5228750347131));
#432879=CARTESIAN_POINT('Ctrl Pts',(-2.71969136426353,0.332569846030572,
12.5240609649613));
#432880=CARTESIAN_POINT('Ctrl Pts',(-2.71881237467914,0.33271205496091,
12.5269717671326));
#432881=CARTESIAN_POINT('Ctrl Pts',(-2.71793404413007,0.332585744095375,
12.5299036066169));
#432882=CARTESIAN_POINT('Ctrl Pts',(-2.71705798926049,0.332277555854814,
12.5328133004019));
#432883=CARTESIAN_POINT('Ctrl Pts',(-2.71663743191193,0.332129607554079,
12.5342101228451));
#432884=CARTESIAN_POINT('Ctrl Pts',(-2.71621809766108,0.331939434757048,
12.5356023438238));
#432885=CARTESIAN_POINT('Ctrl Pts',(-2.71580314304261,0.331714470150389,
12.5369868989719));
#432886=CARTESIAN_POINT('Origin',(-13.9183178550687,6.41110437652535,-1.24054849490876));
#432887=CARTESIAN_POINT('Ctrl Pts',(-2.72664986841926,0.225363784462659,
12.5369868989719));
#432888=CARTESIAN_POINT('Ctrl Pts',(-2.74134440404376,0.220964474691219,
12.5369868989719));
#432889=CARTESIAN_POINT('Ctrl Pts',(-2.74229760565712,0.205655173258131,
12.5369868989719));
#432890=CARTESIAN_POINT('Ctrl Pts',(-2.73161717717023,0.223876582273657,
12.5218025310015));
#432891=CARTESIAN_POINT('Ctrl Pts',(-2.74153211513278,0.217446195900894,
12.5216901060417));
#432892=CARTESIAN_POINT('Ctrl Pts',(-2.74229471644259,0.205701842107343,
12.5161920673678));
#432893=CARTESIAN_POINT('Ctrl Pts',(-2.73638997309462,0.227558496213283,
12.5042015548895));
#432894=CARTESIAN_POINT('Ctrl Pts',(-2.74104250119392,0.223116500344086,
12.4980677368514));
#432895=CARTESIAN_POINT('Ctrl Pts',(-2.74158781128973,0.216342032348497,
12.4907278922777));
#432896=CARTESIAN_POINT('Ctrl Pts',(-2.73298453076523,0.240389783648551,
12.506463626192));
#432897=CARTESIAN_POINT('Ctrl Pts',(-2.73950210632884,0.240963061163302,
12.4999376786891));
#432898=CARTESIAN_POINT('Ctrl Pts',(-2.73942250361987,0.240956059412004,
12.4906970594712));
#432899=CARTESIAN_POINT('Origin',(-2.72034012543628,0.204288036706323,12.5369868989719));
#432900=CARTESIAN_POINT('Origin',(-2.72034012543628,0.204288036706323,14.));
#432901=CARTESIAN_POINT('Origin',(-2.72034012543628,0.204288036706323,13.7435492065112));
#432902=CARTESIAN_POINT('Ctrl Pts',(-2.70298352541866,0.23249814110276,
13.793642941384));
#432903=CARTESIAN_POINT('Ctrl Pts',(-2.71334351629492,0.229403499273819,
13.8071662555867));
#432904=CARTESIAN_POINT('Ctrl Pts',(-2.71092135293231,0.212546675484043,
13.8103758687955));
#432905=CARTESIAN_POINT('Ctrl Pts',(-2.71889728595751,0.227700857419778,
13.7804579775006));
#432906=CARTESIAN_POINT('Ctrl Pts',(-2.73167767585962,0.223872632546517,
13.7901904343352));
#432907=CARTESIAN_POINT('Ctrl Pts',(-2.73198954862573,0.208119580158416,
13.7927914348263));
#432908=CARTESIAN_POINT('Ctrl Pts',(-2.72826631567795,0.2248765159371,13.7597120340895));
#432909=CARTESIAN_POINT('Ctrl Pts',(-2.74305518169568,0.220440692238788,
13.7635825532444));
#432910=CARTESIAN_POINT('Ctrl Pts',(-2.74440818285361,0.205483911033912,
13.7651073818884));
#432911=CARTESIAN_POINT('Ctrl Pts',(-2.72643164513206,0.2254295866687,13.7381884353898));
#432912=CARTESIAN_POINT('Ctrl Pts',(-2.74087460842012,0.22109845262713,
13.7368803041982));
#432913=CARTESIAN_POINT('Ctrl Pts',(-2.74197614264614,0.205999569904626,
13.7363986145813));
#432914=CARTESIAN_POINT('Origin',(-2.70049520861906,0.210270391225106,13.7902182540695));
#432915=CARTESIAN_POINT('Ctrl Pts',(-2.67259645837988,0.241658509801999,
13.8235227101244));
#432916=CARTESIAN_POINT('Ctrl Pts',(-2.68360551716661,0.238344401633875,
13.8358800583119));
#432917=CARTESIAN_POINT('Ctrl Pts',(-2.68175383533497,0.221876331818285,
13.8390832900376));
#432918=CARTESIAN_POINT('Ctrl Pts',(-2.68401642319661,0.238215901360868,
13.8124254819053));
#432919=CARTESIAN_POINT('Ctrl Pts',(-2.69504686133929,0.234895356975299,
13.8247886449157));
#432920=CARTESIAN_POINT('Ctrl Pts',(-2.69317590227665,0.21840838353296,
13.8279860620657));
#432921=CARTESIAN_POINT('Ctrl Pts',(-2.69543126995668,0.23477483578484,
13.8013225099955));
#432922=CARTESIAN_POINT('Ctrl Pts',(-2.70647788343758,0.231449423865085,
13.8136962257787));
#432923=CARTESIAN_POINT('Ctrl Pts',(-2.70459276011104,0.214942300102144,
13.8168830918626));
#432924=CARTESIAN_POINT('Ctrl Pts',(-2.70684119779572,0.231335253043433,
13.7902140179785));
#432925=CARTESIAN_POINT('Ctrl Pts',(-2.71789912271719,0.228006439745012,
13.802602731458));
#432926=CARTESIAN_POINT('Ctrl Pts',(-2.71600461405122,0.211478010012094,
13.8057746032558));
#432927=CARTESIAN_POINT('Origin',(-2.66625045727084,0.22059365157734,13.8235269408515));
#432928=CARTESIAN_POINT('Ctrl Pts',(-2.66613838389344,0.304789073640317,
13.8235269408515));
#432929=CARTESIAN_POINT('Ctrl Pts',(-2.67651853655451,0.310416599697473,
13.8362179249168));
#432930=CARTESIAN_POINT('Ctrl Pts',(-2.670914504778,0.326549108240942,13.8391868794938));
#432931=CARTESIAN_POINT('Ctrl Pts',(-2.65664099602971,0.299640132249645,
13.8400110824519));
#432932=CARTESIAN_POINT('Ctrl Pts',(-2.66333286786432,0.307159488220104,
13.8494522556836));
#432933=CARTESIAN_POINT('Ctrl Pts',(-2.65533803562189,0.317976629471443,
13.85569149686));
#432934=CARTESIAN_POINT('Ctrl Pts',(-2.64675275490183,0.286693302002753,
13.8586819406588));
#432935=CARTESIAN_POINT('Ctrl Pts',(-2.64632327063174,0.291025920944768,
13.868010383617));
#432936=CARTESIAN_POINT('Ctrl Pts',(-2.63903938795127,0.296396015905721,
13.8744918421245));
#432937=CARTESIAN_POINT('Ctrl Pts',(-2.64988635961401,0.255560489417721,
13.8587686893867));
#432938=CARTESIAN_POINT('Ctrl Pts',(-2.65031196544437,0.251266425189394,
13.8680909899357));
#432939=CARTESIAN_POINT('Ctrl Pts',(-2.64425847956561,0.244569283245145,
13.8745789365163));
#432940=CARTESIAN_POINT('Ctrl Pts',(-2.66223983298432,0.244780569768255,
13.8400379222776));
#432941=CARTESIAN_POINT('Ctrl Pts',(-2.67030993866681,0.238768612667464,
13.8494748685453));
#432942=CARTESIAN_POINT('Ctrl Pts',(-2.66467592518206,0.226561278916095,
13.8557104837033));
#432943=CARTESIAN_POINT('Ctrl Pts',(-2.67260022727837,0.241657374433491,
13.8235269408542));
#432944=CARTESIAN_POINT('Ctrl Pts',(-2.68390520534653,0.238249429353411,
13.8362179249195));
#432945=CARTESIAN_POINT('Ctrl Pts',(-2.68168562294419,0.221316134989481,
13.8391868794965));
#432946=CARTESIAN_POINT('Origin',(-2.6556530341162,0.324129638266227,13.8235269408515));
#432947=CARTESIAN_POINT('Ctrl Pts',(-2.69757821107425,0.321833953560952,
13.7902140241682));
#432948=CARTESIAN_POINT('Ctrl Pts',(-2.70773245741165,0.327333942352926,
13.8026027327198));
#432949=CARTESIAN_POINT('Ctrl Pts',(-2.70252878129016,0.343135831072191,
13.8057746032556));
#432950=CARTESIAN_POINT('Ctrl Pts',(-2.68710169425629,0.316154184359189,
13.8013225161808));
#432951=CARTESIAN_POINT('Ctrl Pts',(-2.69724555279159,0.321648550737635,
13.8136962270464));
#432952=CARTESIAN_POINT('Ctrl Pts',(-2.69205538371422,0.337431476647038,
13.8168830918628));
#432953=CARTESIAN_POINT('Ctrl Pts',(-2.67662066091767,0.310471966557803,
13.8124254880875));
#432954=CARTESIAN_POINT('Ctrl Pts',(-2.68674966563899,0.315958289406157,
13.8247886461867));
#432955=CARTESIAN_POINT('Ctrl Pts',(-2.68157744931327,0.331724352341398,
13.8279860620656));
#432956=CARTESIAN_POINT('Ctrl Pts',(-2.66613492821198,0.304787201027912,
13.8235227163065));
#432957=CARTESIAN_POINT('Ctrl Pts',(-2.67624430081123,0.310262889923955,
13.8358800595848));
#432958=CARTESIAN_POINT('Ctrl Pts',(-2.67109479161606,0.326014346550151,
13.8390832900376));
#432959=CARTESIAN_POINT('Origin',(-2.6870963279192,0.341176396726999,13.7902182540695));
#432960=CARTESIAN_POINT('Ctrl Pts',(-2.7155658915832,0.331585877333848,
13.7382347919292));
#432961=CARTESIAN_POINT('Ctrl Pts',(-2.72884346717415,0.338756920156188,
13.7369371795943));
#432962=CARTESIAN_POINT('Ctrl Pts',(-2.72685357016392,0.353776377100719,
13.7364597369712));
#432963=CARTESIAN_POINT('Ctrl Pts',(-2.71722879230157,0.332487406692799,
13.7595490285573));
#432964=CARTESIAN_POINT('Ctrl Pts',(-2.73082268167875,0.339830429096406,
13.7633824266926));
#432965=CARTESIAN_POINT('Ctrl Pts',(-2.72910296774987,0.354761478768508,
13.7648920890506));
#432966=CARTESIAN_POINT('Ctrl Pts',(-2.7087480897428,0.327889656344912,
13.7803806590111));
#432967=CARTESIAN_POINT('Ctrl Pts',(-2.72050888319893,0.334236358109327,
13.7901039518744));
#432968=CARTESIAN_POINT('Ctrl Pts',(-2.71763678262167,0.349735921964489,
13.7926933640892));
#432969=CARTESIAN_POINT('Ctrl Pts',(-2.69400673552795,0.319897739961045,
13.7936647693663));
#432970=CARTESIAN_POINT('Ctrl Pts',(-2.70352900055552,0.325026073090752,
13.8072068914933));
#432971=CARTESIAN_POINT('Ctrl Pts',(-2.69772592292715,0.341056312012424,
13.8104111085397));
#432972=CARTESIAN_POINT('Origin',(-2.70531779326537,0.351055034776299,13.7435492065112));
#432973=CARTESIAN_POINT('Origin',(-2.70531779326537,0.351055034776299,14.));
#432974=CARTESIAN_POINT('Origin',(-2.70531779326537,0.351055034776299,12.5369868989719));
#432975=CARTESIAN_POINT('Ctrl Pts',(-2.72501537688291,0.318263674450985,
12.506462012331));
#432976=CARTESIAN_POINT('Ctrl Pts',(-2.7315098551323,0.319022186321717,
12.4999388158272));
#432977=CARTESIAN_POINT('Ctrl Pts',(-2.73143301693763,0.319013212131559,
12.4907030323752));
#432978=CARTESIAN_POINT('Ctrl Pts',(-2.72574871736152,0.33151851488371,
12.5042014951932));
#432979=CARTESIAN_POINT('Ctrl Pts',(-2.72940406249579,0.336808084721183,
12.4980716682127));
#432980=CARTESIAN_POINT('Ctrl Pts',(-2.7285677916952,0.343547982077514,
12.4907355092743));
#432981=CARTESIAN_POINT('Ctrl Pts',(-2.7203307813779,0.334158907074822,
12.5218047446509));
#432982=CARTESIAN_POINT('Ctrl Pts',(-2.72873249411198,0.342461322028952,
12.5216906929434));
#432983=CARTESIAN_POINT('Ctrl Pts',(-2.72710454304638,0.354111237464613,
12.5161988840776));
#432984=CARTESIAN_POINT('Ctrl Pts',(-2.71576935481563,0.331696190256002,
12.5369868989719));
#432985=CARTESIAN_POINT('Ctrl Pts',(-2.72925885298006,0.33897897617847,
12.5369868989719));
#432986=CARTESIAN_POINT('Ctrl Pts',(-2.72709817540379,0.354155833690222,
12.5369868989719));
#432987=CARTESIAN_POINT('Origin',(-5.12508596464071E-31,-4.62728456409025E-31,
12.5));
#432988=CARTESIAN_POINT('Origin',(-2.68211016738736,0.0864598836326287,
12.5));
#432989=CARTESIAN_POINT('',(-2.68211016738736,0.0864598836326287,12.5893111709658));
#432990=CARTESIAN_POINT('',(-2.68211016738736,0.0864598836326287,13.8235269408515));
#432991=CARTESIAN_POINT('',(-2.68211016738736,0.0864598836326287,12.5));
#432992=CARTESIAN_POINT('',(-2.71483830529306,0.10088700006064,13.7902182540695));
#432993=CARTESIAN_POINT('',(-2.68211016738736,0.0864598836326287,13.8235269408515));
#432994=CARTESIAN_POINT('',(-2.73380434092628,0.109247549171216,13.7435492065112));
#432995=CARTESIAN_POINT('Origin',(-2.67140646578605,0.0817411550293193,
13.7445212918704));
#432996=CARTESIAN_POINT('',(-2.73380434092628,0.109247549171216,12.5369868989719));
#432997=CARTESIAN_POINT('',(-2.73380434092628,0.109247549171216,12.5));
#432998=CARTESIAN_POINT('Ctrl Pts',(-2.73380434092628,0.109247549171216,
12.5369868989719));
#432999=CARTESIAN_POINT('Ctrl Pts',(-2.71658551727533,0.101657200637442,
12.5544431401645));
#433000=CARTESIAN_POINT('Ctrl Pts',(-2.69935437826406,0.0940614232846584,
12.5718848856037));
#433001=CARTESIAN_POINT('Ctrl Pts',(-2.68211016738736,0.0864598836326287,
12.5893111709658));
#433002=CARTESIAN_POINT('Origin',(-2.93935556317855,-0.0775575831846505,
12.5));
#433003=CARTESIAN_POINT('',(-2.73598532022336,0.00235138034619718,13.7435492065112));
#433004=CARTESIAN_POINT('',(-2.71669405316051,0.00993137402565123,13.7902182540695));
#433005=CARTESIAN_POINT('Origin',(-2.66599993752196,0.0298502873284301,
13.7418732680452));
#433006=CARTESIAN_POINT('',(-2.68340468995259,0.0230115497283134,13.8235269408515));
#433007=CARTESIAN_POINT('',(-2.71669405316051,0.00993137402565123,13.7902182540695));
#433008=CARTESIAN_POINT('',(-2.68340468995259,0.0230115497283134,12.5893111709658));
#433009=CARTESIAN_POINT('',(-2.68340468995259,0.0230115497283134,12.5));
#433010=CARTESIAN_POINT('',(-2.73598532022336,0.00235138034619718,12.5369868989719));
#433011=CARTESIAN_POINT('Ctrl Pts',(-2.68340468995259,0.0230115497283134,
12.5893111709658));
#433012=CARTESIAN_POINT('Ctrl Pts',(-2.70094460623998,0.0161197030619724,
12.5718848856037));
#433013=CARTESIAN_POINT('Ctrl Pts',(-2.71847122650434,0.00923308071658,
12.5544431401645));
#433014=CARTESIAN_POINT('Ctrl Pts',(-2.73598532022336,0.00235138034619718,
12.5369868989719));
#433015=CARTESIAN_POINT('',(-2.73598532022336,0.00235138034619717,12.5));
#433016=CARTESIAN_POINT('Origin',(-2.69597583156671,0.0550054088815593,
12.5));
#433017=CARTESIAN_POINT('',(-2.66160411310814,0.0554239090400246,13.8587068136939));
#433018=CARTESIAN_POINT('Ctrl Pts',(-2.68340468995004,0.0230115497222156,
13.8235269408542));
#433019=CARTESIAN_POINT('Ctrl Pts',(-2.68177377254287,0.0236523756253514,
13.8262006681044));
#433020=CARTESIAN_POINT('Ctrl Pts',(-2.68016830437213,0.0244698717934027,
13.8288634856214));
#433021=CARTESIAN_POINT('Ctrl Pts',(-2.67858784131422,0.0254507112311175,
13.8314912288862));
#433022=CARTESIAN_POINT('Ctrl Pts',(-2.67695854691872,0.0264618555225051,
13.8342001611531));
#433023=CARTESIAN_POINT('Ctrl Pts',(-2.67535375490961,0.0276472935432582,
13.8368750301949));
#433024=CARTESIAN_POINT('Ctrl Pts',(-2.67377771606508,0.0290373765185761,
13.8394886372969));
#433025=CARTESIAN_POINT('Ctrl Pts',(-2.67365599476218,0.0291447359986302,
13.8396904925131));
#433026=CARTESIAN_POINT('Ctrl Pts',(-2.67353445653721,0.029253335040948,
13.8398919674349));
#433027=CARTESIAN_POINT('Ctrl Pts',(-2.67341311016033,0.0293631968235529,
13.8400930404591));
#433028=CARTESIAN_POINT('Ctrl Pts',(-2.67152245197074,0.0310749173079189,
13.8432258934518));
#433029=CARTESIAN_POINT('Ctrl Pts',(-2.66968725826479,0.0330836086591771,
13.8462331177034));
#433030=CARTESIAN_POINT('Ctrl Pts',(-2.66803860146692,0.0353888250842538,
13.8489036603661));
#433031=CARTESIAN_POINT('Ctrl Pts',(-2.66749914177628,0.0361431187256927,
13.849777493004));
#433032=CARTESIAN_POINT('Ctrl Pts',(-2.66697988711977,0.0369290701098329,
13.85061494757));
#433033=CARTESIAN_POINT('Ctrl Pts',(-2.66648609052831,0.0377463941898977,
13.8514076489583));
#433034=CARTESIAN_POINT('Ctrl Pts',(-2.66544163952125,0.0394751524950208,
13.8530843267192));
#433035=CARTESIAN_POINT('Ctrl Pts',(-2.66441102287276,0.0415156062266747,
13.8546805203176));
#433036=CARTESIAN_POINT('Ctrl Pts',(-2.66357584888352,0.04381084417629,
13.8559412814274));
#433037=CARTESIAN_POINT('Ctrl Pts',(-2.66346407551843,0.0441180214502598,
13.8561100121513));
#433038=CARTESIAN_POINT('Ctrl Pts',(-2.66335576478259,0.0444296954105265,
13.8562727473908));
#433039=CARTESIAN_POINT('Ctrl Pts',(-2.66325130656481,0.044745668906959,
13.8564289040185));
#433040=CARTESIAN_POINT('Ctrl Pts',(-2.66277758973886,0.0461786051086078,
13.8571370725437));
#433041=CARTESIAN_POINT('Ctrl Pts',(-2.66237693903039,0.0477258676427366,
13.8577210840554));
#433042=CARTESIAN_POINT('Ctrl Pts',(-2.66209333880873,0.0493346709316656,
13.8581177131616));
#433043=CARTESIAN_POINT('Ctrl Pts',(-2.66201346722509,0.0497877653111516,
13.8582294175695));
#433044=CARTESIAN_POINT('Ctrl Pts',(-2.66194271436159,0.0502456764708526,
13.8583265086086));
#433045=CARTESIAN_POINT('Ctrl Pts',(-2.66188164440383,0.0507070903301426,
13.8584082369006));
#433046=CARTESIAN_POINT('Ctrl Pts',(-2.66179390325108,0.0513700183129284,
13.8585256585398));
#433047=CARTESIAN_POINT('Ctrl Pts',(-2.66172537925685,0.0520484607445389,
13.8586122832068));
#433048=CARTESIAN_POINT('Ctrl Pts',(-2.6616786381655,0.052724873013058,
13.8586682984299));
#433049=CARTESIAN_POINT('Ctrl Pts',(-2.66164124992571,0.0532659357772812,
13.8587131050557));
#433050=CARTESIAN_POINT('Ctrl Pts',(-2.66161715241133,0.0538116594368054,
13.8587357943552));
#433051=CARTESIAN_POINT('Ctrl Pts',(-2.66160684871186,0.054362131179908,
13.8587355499465));
#433052=CARTESIAN_POINT('Ctrl Pts',(-2.66160018918524,0.0547179141912392,
13.8587353919793));
#433053=CARTESIAN_POINT('Ctrl Pts',(-2.66159932516072,0.0550718325274348,
13.8587257282814));
#433054=CARTESIAN_POINT('Ctrl Pts',(-2.66160411310814,0.0554239090400246,
13.8587068136939));
#433055=CARTESIAN_POINT('Ctrl Pts',(-2.66160411310814,0.0554239090400246,
13.8587068136939));
#433056=CARTESIAN_POINT('Ctrl Pts',(-2.66161986040616,0.0565818694966455,
13.8586446046466));
#433057=CARTESIAN_POINT('Ctrl Pts',(-2.661696670637,0.0577199319795604,
13.858482427929));
#433058=CARTESIAN_POINT('Ctrl Pts',(-2.66183011447819,0.0588387023433441,
13.8582284286032));
#433059=CARTESIAN_POINT('Ctrl Pts',(-2.66196701233641,0.0599864305957805,
13.8579678548414));
#433060=CARTESIAN_POINT('Ctrl Pts',(-2.6621653687932,0.0611164772851363,
13.857615680862));
#433061=CARTESIAN_POINT('Ctrl Pts',(-2.66240782003208,0.0621859663707654,
13.8571944833187));
#433062=CARTESIAN_POINT('Ctrl Pts',(-2.66301288189458,0.0648549857623171,
13.8561433417727));
#433063=CARTESIAN_POINT('Ctrl Pts',(-2.6639161935698,0.0672727591232808,
13.8546163505475));
#433064=CARTESIAN_POINT('Ctrl Pts',(-2.66492419051466,0.0693665497070066,
13.8528973491086));
#433065=CARTESIAN_POINT('Ctrl Pts',(-2.66510833668488,0.069749054355661,
13.8525833129072));
#433066=CARTESIAN_POINT('Ctrl Pts',(-2.66529589199116,0.0701208596288435,
13.8522628768812));
#433067=CARTESIAN_POINT('Ctrl Pts',(-2.66548559290958,0.0704816802417791,
13.851937733538));
#433068=CARTESIAN_POINT('Ctrl Pts',(-2.66664407009854,0.0726851616633413,
13.8499521282529));
#433069=CARTESIAN_POINT('Ctrl Pts',(-2.66800130582272,0.0746960706363772,
13.847639871647));
#433070=CARTESIAN_POINT('Ctrl Pts',(-2.66941937654741,0.0764536667494184,
13.8452109780794));
#433071=CARTESIAN_POINT('Ctrl Pts',(-2.67005739591905,0.0772444456211071,
13.8441181685877));
#433072=CARTESIAN_POINT('Ctrl Pts',(-2.67070736176037,0.0779845628065856,
13.8430021611332));
#433073=CARTESIAN_POINT('Ctrl Pts',(-2.67135597704449,0.0786717122499349,
13.8418824960098));
#433074=CARTESIAN_POINT('Ctrl Pts',(-2.67288445552449,0.0802909974601713,
13.8392439765549));
#433075=CARTESIAN_POINT('Ctrl Pts',(-2.67447575134451,0.0816961464825684,
13.8364981347964));
#433076=CARTESIAN_POINT('Ctrl Pts',(-2.6761114221815,0.0829165267290124,
13.8336931113419));
#433077=CARTESIAN_POINT('Ctrl Pts',(-2.67770446170203,0.0841050995877381,
13.8309611966328));
#433078=CARTESIAN_POINT('Ctrl Pts',(-2.67934152713037,0.0851191482652251,
13.8281701127186));
#433079=CARTESIAN_POINT('Ctrl Pts',(-2.68101601223104,0.0859479129045207,
13.8253580685121));
#433080=CARTESIAN_POINT('Ctrl Pts',(-2.68137904240803,0.08612758997275,
13.8247484142933));
#433081=CARTESIAN_POINT('Ctrl Pts',(-2.68174380865551,0.0862983865106671,
13.8241378483365));
#433082=CARTESIAN_POINT('Ctrl Pts',(-2.68211016738736,0.0864598836326288,
13.8235269408515));
#433083=CARTESIAN_POINT('',(-2.66161138968753,0.0541818446662489,12.5969504640361));
#433084=CARTESIAN_POINT('Origin',(-2.69600890610016,0.0550062795408617,
12.584524458991));
#433085=CARTESIAN_POINT('Origin',(-2.69600890610016,0.0550062795408617,
12.584524458991));
#433086=CARTESIAN_POINT('Ctrl Pts',(-2.68340468995259,0.0230115497283134,
12.5893111709658));
#433087=CARTESIAN_POINT('Ctrl Pts',(-2.67285582888757,0.0271564459623303,
12.5770542771492));
#433088=CARTESIAN_POINT('Ctrl Pts',(-2.67589590165752,0.0432362977156396,
12.5737548217797));
#433089=CARTESIAN_POINT('Ctrl Pts',(-2.70647150879878,0.0139480527330364,
12.5663937883685));
#433090=CARTESIAN_POINT('Ctrl Pts',(-2.69590919119647,0.0180982363578279,
12.5540940315304));
#433091=CARTESIAN_POINT('Ctrl Pts',(-2.69896183982587,0.0342273197682056,
12.5508374392248));
#433092=CARTESIAN_POINT('Ctrl Pts',(-2.72951505350752,0.00489370069512543,
12.5434499600945));
#433093=CARTESIAN_POINT('Ctrl Pts',(-2.71891839404936,0.00905737804472826,
12.5311293540533));
#433094=CARTESIAN_POINT('Ctrl Pts',(-2.72200481283406,0.0252260447692931,
12.5278936106989));
#433095=CARTESIAN_POINT('Ctrl Pts',(-2.75253714717388,-0.00415222272246555,
12.5204817579905));
#433096=CARTESIAN_POINT('Ctrl Pts',(-2.74188804149321,3.20619846197456E-5,
12.5081597038247));
#433097=CARTESIAN_POINT('Ctrl Pts',(-2.74502660058381,0.0162318611108275,
12.5049254088044));
#433098=CARTESIAN_POINT('Ctrl Pts',(-2.73598532022336,0.00235138034619827,
12.5369868989719));
#433099=CARTESIAN_POINT('Ctrl Pts',(-2.73685230015164,0.00201072366463625,
12.5342545179733));
#433100=CARTESIAN_POINT('Ctrl Pts',(-2.73772532660293,0.00180172144282968,
12.5314872231885));
#433101=CARTESIAN_POINT('Ctrl Pts',(-2.73856823552727,0.0017905118314122,
12.5287124745063));
#433102=CARTESIAN_POINT('Ctrl Pts',(-2.73932841263351,0.00178040244744051,
12.5262100684184));
#433103=CARTESIAN_POINT('Ctrl Pts',(-2.74006334023772,0.00193215802165255,
12.5237004536639));
#433104=CARTESIAN_POINT('Ctrl Pts',(-2.74077223186921,0.00231330527171363,
12.5212220730815));
#433105=CARTESIAN_POINT('Ctrl Pts',(-2.74131494973713,0.00260510646350231,
12.5193246583486));
#433106=CARTESIAN_POINT('Ctrl Pts',(-2.74184859306926,0.00303540568168749,
12.517417831369));
#433107=CARTESIAN_POINT('Ctrl Pts',(-2.74232826407684,0.00369044799174734,
12.5155812248348));
#433108=CARTESIAN_POINT('Ctrl Pts',(-2.74253260650432,0.00396949953670413,
12.5147988205794));
#433109=CARTESIAN_POINT('Ctrl Pts',(-2.74272758494536,0.00428945719681405,
12.5140295443047));
#433110=CARTESIAN_POINT('Ctrl Pts',(-2.74291185437362,0.00465691812078847,
12.5132817086137));
#433111=CARTESIAN_POINT('Ctrl Pts',(-2.74319072122587,0.00521302052023,
12.5121499604604));
#433112=CARTESIAN_POINT('Ctrl Pts',(-2.74344469052441,0.00589313279938605,
12.5110494206568));
#433113=CARTESIAN_POINT('Ctrl Pts',(-2.74364492177948,0.00672081604688685,
12.5100666561695));
#433114=CARTESIAN_POINT('Ctrl Pts',(-2.74375989410505,0.00719606986161615,
12.5095023550641));
#433115=CARTESIAN_POINT('Ctrl Pts',(-2.74385784279182,0.00772562287140146,
12.5089719619137));
#433116=CARTESIAN_POINT('Ctrl Pts',(-2.74393065145121,0.00830071085255689,
12.5085043804652));
#433117=CARTESIAN_POINT('Ctrl Pts',(-2.74403719744023,0.00914227720249921,
12.5078201359221));
#433118=CARTESIAN_POINT('Ctrl Pts',(-2.74409179924932,0.0101059144034801,
12.5072563000949));
#433119=CARTESIAN_POINT('Ctrl Pts',(-2.74408230323968,0.0111267810021032,
12.5068768744332));
#433120=CARTESIAN_POINT('Ctrl Pts',(-2.74407545596303,0.0118628960964068,
12.5066032824114));
#433121=CARTESIAN_POINT('Ctrl Pts',(-2.74403522140716,0.0126417000519628,
12.5064197834844));
#433122=CARTESIAN_POINT('Ctrl Pts',(-2.74396642778918,0.0134198357955237,
12.5063282718343));
#433123=CARTESIAN_POINT('Ctrl Pts',(-2.7438660104049,0.0145556730763847,
12.5061946931565));
#433124=CARTESIAN_POINT('Ctrl Pts',(-2.74370365410164,0.0157144573146118,
12.5062515701262));
#433125=CARTESIAN_POINT('Ctrl Pts',(-2.74350474993816,0.0168264180839142,
12.5064436508398));
#433126=CARTESIAN_POINT('',(-2.67589590165752,0.0432362977156397,12.5737548217797));
#433127=CARTESIAN_POINT('Origin',(-2.69145022058562,0.0434876195863907,
12.5893111709658));
#433128=CARTESIAN_POINT('Ctrl Pts',(-2.74350474993816,0.0168264180839145,
12.5064436508398));
#433129=CARTESIAN_POINT('Ctrl Pts',(-2.733497058684,0.0207362139242025,
12.5164271754438));
#433130=CARTESIAN_POINT('Ctrl Pts',(-2.72348532435284,0.0246473649955796,
12.5264061185523));
#433131=CARTESIAN_POINT('Ctrl Pts',(-2.71346940489532,0.0285599199097525,
12.536380305637));
#433132=CARTESIAN_POINT('Ctrl Pts',(-2.70095153702076,0.033449820000828,
12.5488460165097));
#433133=CARTESIAN_POINT('Ctrl Pts',(-2.68842712830146,0.0383419143063837,
12.5613043021964));
#433134=CARTESIAN_POINT('Ctrl Pts',(-2.67589590165752,0.0432362977156394,
12.5737548217797));
#433135=CARTESIAN_POINT('Ctrl Pts',(-2.68211016738736,0.0864598836326288,
12.5893111709658));
#433136=CARTESIAN_POINT('Ctrl Pts',(-2.6717391495482,0.0818881636565727,
12.5770542771492));
#433137=CARTESIAN_POINT('Ctrl Pts',(-2.67543256678469,0.0659456938362415,
12.5737548217797));
#433138=CARTESIAN_POINT('Ctrl Pts',(-2.67243409794577,0.0821945086576885,
12.5928319619712));
#433139=CARTESIAN_POINT('Ctrl Pts',(-2.66677819194253,0.0761410680117523,
12.5821634970842));
#433140=CARTESIAN_POINT('Ctrl Pts',(-2.67190400159415,0.0644005578986747,
12.5773203894503));
#433141=CARTESIAN_POINT('Ctrl Pts',(-2.66132169167018,0.06966061356854,
12.5969440695591));
#433142=CARTESIAN_POINT('Ctrl Pts',(-2.66138541786341,0.0656413497647797,
12.5878292599214));
#433143=CARTESIAN_POINT('Ctrl Pts',(-2.66794484417248,0.0599318646212225,
12.5813877129824));
#433144=CARTESIAN_POINT('Ctrl Pts',(-2.66189191156417,0.0390689464872274,
12.596957478804));
#433145=CARTESIAN_POINT('Ctrl Pts',(-2.66182873647298,0.0430585081243937,
12.5878468778671));
#433146=CARTESIAN_POINT('Ctrl Pts',(-2.66815489785834,0.0489827940783303,
12.5814011370086));
#433147=CARTESIAN_POINT('Ctrl Pts',(-2.67354840376738,0.0268843169624308,
12.5928371701607));
#433148=CARTESIAN_POINT('Ctrl Pts',(-2.66765877691286,0.0327021654666717,
12.5821692192952));
#433149=CARTESIAN_POINT('Ctrl Pts',(-2.67229567989076,0.0446404631988242,
12.5773318885715));
#433150=CARTESIAN_POINT('Ctrl Pts',(-2.68340468995256,0.0230115497282627,
12.5893111709658));
#433151=CARTESIAN_POINT('Ctrl Pts',(-2.67285582888755,0.0271564459622794,
12.5770542771492));
#433152=CARTESIAN_POINT('Ctrl Pts',(-2.6758959016575,0.0432362977155884,
12.5737548217797));
#433153=CARTESIAN_POINT('',(-2.67543256678469,0.0659456938362415,12.5737548217797));
#433154=CARTESIAN_POINT('Origin',(-2.69098419246214,0.0663290197919444,
12.5893111709658));
#433155=CARTESIAN_POINT('Ctrl Pts',(-2.6758959016575,0.0432362977155884,
12.5737548217797));
#433156=CARTESIAN_POINT('Ctrl Pts',(-2.67495170595959,0.0435721758409372,
12.5746934679442));
#433157=CARTESIAN_POINT('Ctrl Pts',(-2.67396828568517,0.044116436809687,
12.5756680099006));
#433158=CARTESIAN_POINT('Ctrl Pts',(-2.67305591365844,0.0448042456151264,
12.5765688348656));
#433159=CARTESIAN_POINT('Ctrl Pts',(-2.67281437326466,0.0449863353820681,
12.5768073183026));
#433160=CARTESIAN_POINT('Ctrl Pts',(-2.67257771226814,0.0451782491723921,
12.5770407398754));
#433161=CARTESIAN_POINT('Ctrl Pts',(-2.67234763408338,0.0453783370825612,
12.5772674179684));
#433162=CARTESIAN_POINT('Ctrl Pts',(-2.67140345542886,0.0461994437598534,
12.5781976435658));
#433163=CARTESIAN_POINT('Ctrl Pts',(-2.67052391028091,0.0472133558938664,
12.5790594849312));
#433164=CARTESIAN_POINT('Ctrl Pts',(-2.66980486389765,0.0483832554717753,
12.5797571720116));
#433165=CARTESIAN_POINT('Ctrl Pts',(-2.66933637932435,0.0491454871126227,
12.580211740231));
#433166=CARTESIAN_POINT('Ctrl Pts',(-2.66893072961081,0.0500184048007455,
12.5806009430798));
#433167=CARTESIAN_POINT('Ctrl Pts',(-2.66863253735736,0.0509480251771897,
12.5808812374708));
#433168=CARTESIAN_POINT('Ctrl Pts',(-2.66837629128739,0.0517468774789039,
12.5811221033394));
#433169=CARTESIAN_POINT('Ctrl Pts',(-2.66819425992894,0.0526039914370422,
12.581287365893));
#433170=CARTESIAN_POINT('Ctrl Pts',(-2.6681048734992,0.0534727223215106,
12.581359338449));
#433171=CARTESIAN_POINT('Ctrl Pts',(-2.66809245063123,0.0535934579758461,
12.5813693411482));
#433172=CARTESIAN_POINT('Ctrl Pts',(-2.66808175902388,0.0537144320875003,
12.5813775999465));
#433173=CARTESIAN_POINT('Ctrl Pts',(-2.66807278879257,0.0538355349142049,
12.5813841266931));
#433174=CARTESIAN_POINT('Ctrl Pts',(-2.66805756971023,0.0540410005067911,
12.5813952001081));
#433175=CARTESIAN_POINT('Ctrl Pts',(-2.66804781092558,0.0542482576954088,
12.5814007534795));
#433176=CARTESIAN_POINT('Ctrl Pts',(-2.66804371368044,0.0544572254882118,
12.5814005856065));
#433177=CARTESIAN_POINT('Ctrl Pts',(-2.66802495809412,0.0554137983425526,
12.5813998171494));
#433178=CARTESIAN_POINT('Ctrl Pts',(-2.66812579569502,0.0563401176065905,
12.58127954464));
#433179=CARTESIAN_POINT('Ctrl Pts',(-2.66831623841059,0.0572341263756829,
12.5810700125799));
#433180=CARTESIAN_POINT('Ctrl Pts',(-2.66854627152736,0.0583139871776976,
12.5808169217085));
#433181=CARTESIAN_POINT('Ctrl Pts',(-2.66892342704989,0.0593433180629238,
12.5804173076348));
#433182=CARTESIAN_POINT('Ctrl Pts',(-2.66939019910842,0.0602408698514211,
12.5799304713245));
#433183=CARTESIAN_POINT('Ctrl Pts',(-2.66996867673729,0.0613532192753413,
12.5793271277669));
#433184=CARTESIAN_POINT('Ctrl Pts',(-2.670692112498,0.0623470268565772,
12.5785808224116));
#433185=CARTESIAN_POINT('Ctrl Pts',(-2.67150436979799,0.0631990679011367,
12.5777485681082));
#433186=CARTESIAN_POINT('Ctrl Pts',(-2.67271472216441,0.0644687024055957,
12.576508418016));
#433187=CARTESIAN_POINT('Ctrl Pts',(-2.67410713064052,0.0654176060605656,
12.5750928681475));
#433188=CARTESIAN_POINT('Ctrl Pts',(-2.67543256678469,0.0659456938362415,
12.5737548217797));
#433189=CARTESIAN_POINT('Ctrl Pts',(-2.67543256678469,0.0659456938362415,
12.5737548217797));
#433190=CARTESIAN_POINT('Ctrl Pts',(-2.6717391495482,0.0818881636565725,
12.5770542771492));
#433191=CARTESIAN_POINT('Ctrl Pts',(-2.68211016738736,0.0864598836326287,
12.5893111709658));
#433192=CARTESIAN_POINT('Ctrl Pts',(-2.69810843878968,0.0758865078362841,
12.5508408821982));
#433193=CARTESIAN_POINT('Ctrl Pts',(-2.69440044718258,0.0918776467222681,
12.55409748406));
#433194=CARTESIAN_POINT('Ctrl Pts',(-2.70478469578434,0.0964551990421396,
12.5663972313419));
#433195=CARTESIAN_POINT('Ctrl Pts',(-2.72076168574913,0.0858186911806309,
12.52790050457));
#433196=CARTESIAN_POINT('Ctrl Pts',(-2.71701834303816,0.101847997550193,
12.5311362602938));
#433197=CARTESIAN_POINT('Ctrl Pts',(-2.7274363493081,0.106440430820861,
12.5434568539655));
#433198=CARTESIAN_POINT('Ctrl Pts',(-2.74339406035942,0.0957429272648899,
12.5049357605811));
#433199=CARTESIAN_POINT('Ctrl Pts',(-2.73959736152855,0.111801210578403,
12.5081700652078));
#433200=CARTESIAN_POINT('Ctrl Pts',(-2.75006691952333,0.116416368720788,
12.5204921097672));
#433201=CARTESIAN_POINT('Ctrl Pts',(-2.74190792928895,0.0950912644753132,
12.5064436508395));
#433202=CARTESIAN_POINT('Ctrl Pts',(-2.74207361102238,0.0963001471634963,
12.5062361689309));
#433203=CARTESIAN_POINT('Ctrl Pts',(-2.742194357024,0.0975643512702508,
12.5061871075061));
#433204=CARTESIAN_POINT('Ctrl Pts',(-2.74224227203065,0.0987926512308685,
12.5063648335164));
#433205=CARTESIAN_POINT('Ctrl Pts',(-2.74226403798219,0.099350620837665,
12.5064455676329));
#433206=CARTESIAN_POINT('Ctrl Pts',(-2.74227085843297,0.0999089725951846,
12.506574497099));
#433207=CARTESIAN_POINT('Ctrl Pts',(-2.74226139007168,0.100443778891512,
12.5067492519495));
#433208=CARTESIAN_POINT('Ctrl Pts',(-2.74224236303213,0.101518492903706,
12.5071004286051));
#433209=CARTESIAN_POINT('Ctrl Pts',(-2.74215605014434,0.102537623639935,
12.5076537929613));
#433210=CARTESIAN_POINT('Ctrl Pts',(-2.74201835435008,0.103425478197055,
12.5083435010505));
#433211=CARTESIAN_POINT('Ctrl Pts',(-2.74200968557695,0.10348137394728,
12.5083869222964));
#433212=CARTESIAN_POINT('Ctrl Pts',(-2.74200080041076,0.103536753656767,
12.5084308732337));
#433213=CARTESIAN_POINT('Ctrl Pts',(-2.74199169775787,0.103591600550636,
12.5084753333615));
#433214=CARTESIAN_POINT('Ctrl Pts',(-2.74191868246723,0.10403154503076,
12.5088319622689));
#433215=CARTESIAN_POINT('Ctrl Pts',(-2.74183146408406,0.104446350132662,
12.509227847131));
#433216=CARTESIAN_POINT('Ctrl Pts',(-2.74173537620196,0.104824257689328,
12.5096423454524));
#433217=CARTESIAN_POINT('Ctrl Pts',(-2.74143427930616,0.106008452717044,
12.5109411997424));
#433218=CARTESIAN_POINT('Ctrl Pts',(-2.74103694226181,0.106905562165694,
12.5124831113042));
#433219=CARTESIAN_POINT('Ctrl Pts',(-2.74060720345451,0.107585446738974,
12.5140723025008));
#433220=CARTESIAN_POINT('Ctrl Pts',(-2.74056693645759,0.107649152668145,
12.5142212114565));
#433221=CARTESIAN_POINT('Ctrl Pts',(-2.74052639599032,0.107710978868737,
12.5143705582413));
#433222=CARTESIAN_POINT('Ctrl Pts',(-2.74048564229798,0.107770997937223,
12.5145201959299));
#433223=CARTESIAN_POINT('Ctrl Pts',(-2.73996210044397,0.108542032230993,
12.5164425148273));
#433224=CARTESIAN_POINT('Ctrl Pts',(-2.73939431493446,0.109047282064788,
12.5184635205941));
#433225=CARTESIAN_POINT('Ctrl Pts',(-2.73879962913225,0.109375275323014,
12.5205025929157));
#433226=CARTESIAN_POINT('Ctrl Pts',(-2.73845468779583,0.109565524413223,
12.5216853356836));
#433227=CARTESIAN_POINT('Ctrl Pts',(-2.73810155260303,0.109696215997301,
12.5228750347131));
#433228=CARTESIAN_POINT('Ctrl Pts',(-2.73774934548699,0.109783152732733,
12.5240609649613));
#433229=CARTESIAN_POINT('Ctrl Pts',(-2.73688487201596,0.109996534285856,
12.5269717671326));
#433230=CARTESIAN_POINT('Ctrl Pts',(-2.73599916853119,0.109942235803077,
12.5299036066169));
#433231=CARTESIAN_POINT('Ctrl Pts',(-2.73510090845922,0.10970647963823,
12.5328133004019));
#433232=CARTESIAN_POINT('Ctrl Pts',(-2.73466969132056,0.109593302951431,
12.5342101228451));
#433233=CARTESIAN_POINT('Ctrl Pts',(-2.7342362515214,0.109437942573048,
12.5356023438238));
#433234=CARTESIAN_POINT('Ctrl Pts',(-2.73380434092628,0.109247549171216,
12.5369868989719));
#433235=CARTESIAN_POINT('Origin',(-14.394554771405,5.25529295237477,-1.24053018555564));
#433236=CARTESIAN_POINT('Ctrl Pts',(-2.73594640652385,0.00236662780252761,
12.5369868989719));
#433237=CARTESIAN_POINT('Ctrl Pts',(-2.75023346270574,-0.00321578469936245,
12.5369868989719));
#433238=CARTESIAN_POINT('Ctrl Pts',(-2.74993564242795,-0.0185518404754673,
12.5369868989719));
#433239=CARTESIAN_POINT('Ctrl Pts',(-2.74077596617979,0.000479492378690292,
12.5218025310016));
#433240=CARTESIAN_POINT('Ctrl Pts',(-2.75013377681806,-0.00673765690360874,
12.5216901060418));
#433241=CARTESIAN_POINT('Ctrl Pts',(-2.7499365667715,-0.0185050914151908,
12.5161920673678));
#433242=CARTESIAN_POINT('Ctrl Pts',(-2.74583299118687,0.0037601278770949,
12.5042015548894));
#433243=CARTESIAN_POINT('Ctrl Pts',(-2.75010797448188,-0.00104631184936697,
12.4980677368513));
#433244=CARTESIAN_POINT('Ctrl Pts',(-2.75009928807058,-0.00784268619677183,
12.4907278922777));
#433245=CARTESIAN_POINT('Ctrl Pts',(-2.74348474923167,0.0168262954263408,
12.506463626192));
#433246=CARTESIAN_POINT('Ctrl Pts',(-2.75002736553977,0.0168664224927999,
12.4999376786891));
#433247=CARTESIAN_POINT('Ctrl Pts',(-2.74994745699453,0.0168659323990281,
12.4906970594712));
#433248=CARTESIAN_POINT('Origin',(-2.72793978959033,-0.0181246895118802,
12.5369868989719));
#433249=CARTESIAN_POINT('Origin',(-2.72793978959033,-0.0181246895118802,
14.));
#433250=CARTESIAN_POINT('Origin',(-2.72793978959033,-0.0181246895118801,
13.7435492065112));
#433251=CARTESIAN_POINT('Ctrl Pts',(-2.71294032762559,0.0114062721215966,
13.793642941384));
#433252=CARTESIAN_POINT('Ctrl Pts',(-2.72301360444854,0.00747749202417046,
13.8071662555867));
#433253=CARTESIAN_POINT('Ctrl Pts',(-2.71922551300471,-0.00912581327471074,
13.8103758687955));
#433254=CARTESIAN_POINT('Ctrl Pts',(-2.72841011328307,0.00532783178425798,
13.7804579775006));
#433255=CARTESIAN_POINT('Ctrl Pts',(-2.74083594162536,0.000470624589080533,
13.7901904343351));
#433256=CARTESIAN_POINT('Ctrl Pts',(-2.73986275664679,-0.0152554313424525,
13.7927914348263));
#433257=CARTESIAN_POINT('Ctrl Pts',(-2.73751775827926,0.00174922516482727,
13.7597120340895));
#433258=CARTESIAN_POINT('Ctrl Pts',(-2.7518958547537,-0.00387726856962336,
13.7635825532445));
#433259=CARTESIAN_POINT('Ctrl Pts',(-2.75202523739173,-0.0188945644739232,
13.7651073818884));
#433260=CARTESIAN_POINT('Ctrl Pts',(-2.73573427284735,0.00244999828093495,
13.7381884353898));
#433261=CARTESIAN_POINT('Ctrl Pts',(-2.74977615073385,-0.00304395985931783,
13.7368803041982));
#433262=CARTESIAN_POINT('Ctrl Pts',(-2.74964332058253,-0.0181823875606896,
13.7363986145813));
#433263=CARTESIAN_POINT('Origin',(-2.70864852252747,-0.0105446958324261,
13.7902182540695));
#433264=CARTESIAN_POINT('Ctrl Pts',(-2.68340102613533,0.0230129885130929,
13.8235227101244));
#433265=CARTESIAN_POINT('Ctrl Pts',(-2.69410332260474,0.0188125672722698,
13.8358800583119));
#433266=CARTESIAN_POINT('Ctrl Pts',(-2.69091550151957,0.00255022285992592,
13.8390832900376));
#433267=CARTESIAN_POINT('Ctrl Pts',(-2.69450238741364,0.0186510019172073,
13.8124254819052));
#433268=CARTESIAN_POINT('Ctrl Pts',(-2.70522546748948,0.0144424232589427,
13.8247886449157));
#433269=CARTESIAN_POINT('Ctrl Pts',(-2.70201689249565,-0.00183719060661301,
13.8279860620657));
#433270=CARTESIAN_POINT('Ctrl Pts',(-2.70559877342302,0.0142909702218092,
13.8013225099955));
#433271=CARTESIAN_POINT('Ctrl Pts',(-2.71633757826577,0.0100762217854295,
13.8136962257787));
#433272=CARTESIAN_POINT('Ctrl Pts',(-2.71311324370024,-0.00622232083317992,
13.8168830918626));
#433273=CARTESIAN_POINT('Ctrl Pts',(-2.71669037774349,0.00993281736474199,
13.7902140179785));
#433274=CARTESIAN_POINT('Ctrl Pts',(-2.72744017914498,0.00571375688009667,
13.802602731458));
#433275=CARTESIAN_POINT('Ctrl Pts',(-2.72420475383462,-0.0106052558223468,
13.8057746032558));
#433276=CARTESIAN_POINT('Origin',(-2.67535915931955,0.00253547987023609,
13.8235269408515));
#433277=CARTESIAN_POINT('Ctrl Pts',(-2.68211016738736,0.0864598836326288,
13.8235269408515));
#433278=CARTESIAN_POINT('Ctrl Pts',(-2.69291447656381,0.0912226057545551,
13.8362179249168));
#433279=CARTESIAN_POINT('Ctrl Pts',(-2.68864404095394,0.107758215321761,
13.8391868794938));
#433280=CARTESIAN_POINT('Ctrl Pts',(-2.67222469477449,0.0821022002000186,
13.8400110824519));
#433281=CARTESIAN_POINT('Ctrl Pts',(-2.67950719727548,0.0890510864549605,
13.8494522556836));
#433282=CARTESIAN_POINT('Ctrl Pts',(-2.67242066461126,0.100483887609305,
13.85569149686));
#433283=CARTESIAN_POINT('Ctrl Pts',(-2.66131406909561,0.0700044329126074,
13.8586819406588));
#433284=CARTESIAN_POINT('Ctrl Pts',(-2.66123916256485,0.0743576423776596,
13.868010383617));
#433285=CARTESIAN_POINT('Ctrl Pts',(-2.65441722899596,0.0803035728493568,
13.8744918421245));
#433286=CARTESIAN_POINT('Ctrl Pts',(-2.661899633748,0.0387197943181669,
13.8587686893867));
#433287=CARTESIAN_POINT('Ctrl Pts',(-2.66197381731131,0.0344053274080189,
13.8680909899357));
#433288=CARTESIAN_POINT('Ctrl Pts',(-2.65539459466576,0.0282238849480537,
13.8745789365163));
#433289=CARTESIAN_POINT('Ctrl Pts',(-2.67333333842744,0.02696882119832,
13.8400379222776));
#433290=CARTESIAN_POINT('Ctrl Pts',(-2.68088656118302,0.0203190798565372,
13.8494748685453));
#433291=CARTESIAN_POINT('Ctrl Pts',(-2.67427628338526,0.00861158940378663,
13.8557104837033));
#433292=CARTESIAN_POINT('Ctrl Pts',(-2.68340468995004,0.0230115497222156,
13.8235269408542));
#433293=CARTESIAN_POINT('Ctrl Pts',(-2.69439427247443,0.0186934836354026,
13.8362179249195));
#433294=CARTESIAN_POINT('Ctrl Pts',(-2.69080185485773,0.00199744998295956,
13.8391868794965));
#433295=CARTESIAN_POINT('Origin',(-2.67323614231258,0.106590747473313,13.8235269408515));
#433296=CARTESIAN_POINT('Ctrl Pts',(-2.7148346970873,0.100885410333076,
13.7902140241682));
#433297=CARTESIAN_POINT('Ctrl Pts',(-2.72540345615365,0.105539433022133,
13.8026027327198));
#433298=CARTESIAN_POINT('Ctrl Pts',(-2.72150509546337,0.121712890172733,
13.8057746032556));
#433299=CARTESIAN_POINT('Ctrl Pts',(-2.70393008609646,0.0960784734746837,
13.8013225161808));
#433300=CARTESIAN_POINT('Ctrl Pts',(-2.71448803364637,0.10072773916065,
13.8136962270464));
#433301=CARTESIAN_POINT('Ctrl Pts',(-2.71060158941156,0.116881195649068,
13.8168830918628));
#433302=CARTESIAN_POINT('Ctrl Pts',(-2.69302077402973,0.0912694643025583,
13.8124254880875));
#433303=CARTESIAN_POINT('Ctrl Pts',(-2.70356326156808,0.0959119239463373,
13.8247886461868));
#433304=CARTESIAN_POINT('Ctrl Pts',(-2.69969333585972,0.112047110254848,
13.8279860620656));
#433305=CARTESIAN_POINT('Ctrl Pts',(-2.68210657056909,0.0864582989213033,
13.8235227163065));
#433306=CARTESIAN_POINT('Ctrl Pts',(-2.69262862454384,0.0910917601965746,
13.8358800595847));
#433307=CARTESIAN_POINT('Ctrl Pts',(-2.68878013986014,0.107210537955378,
13.8390832900376));
#433308=CARTESIAN_POINT('Origin',(-2.70596428021828,0.121017863901323,13.7902182540695));
#433309=CARTESIAN_POINT('Ctrl Pts',(-2.73355739739318,0.109138722433136,
13.7382347919292));
#433310=CARTESIAN_POINT('Ctrl Pts',(-2.74737529950942,0.115203658528389,
13.7369371795942));
#433311=CARTESIAN_POINT('Ctrl Pts',(-2.74661624889214,0.130335334548605,
13.7364597369711));
#433312=CARTESIAN_POINT('Ctrl Pts',(-2.73528824795873,0.109901710181357,
13.7595490285574));
#433313=CARTESIAN_POINT('Ctrl Pts',(-2.74943542928561,0.116112271099933,
13.7633824266926));
#433314=CARTESIAN_POINT('Ctrl Pts',(-2.74893845672435,0.131133811586217,
13.7648920890506));
#433315=CARTESIAN_POINT('Ctrl Pts',(-2.72646100490131,0.10601051445799,
13.780380659011));
#433316=CARTESIAN_POINT('Ctrl Pts',(-2.73869998040111,0.111377484247306,
13.7901039518744));
#433317=CARTESIAN_POINT('Ctrl Pts',(-2.73710079484676,0.127059577442688,
13.7926933640892));
#433318=CARTESIAN_POINT('Ctrl Pts',(-2.71111728594794,0.0992467477371861,
13.7936647693663));
#433319=CARTESIAN_POINT('Ctrl Pts',(-2.72102587318337,0.103581863761312,
13.8072068914933));
#433320=CARTESIAN_POINT('Ctrl Pts',(-2.71654871810667,0.120031768085242,
13.8104111085397));
#433321=CARTESIAN_POINT('Origin',(-2.7249303158515,0.1293784130119,13.7435492065112));
#433322=CARTESIAN_POINT('Origin',(-2.7249303158515,0.1293784130119,14.));
#433323=CARTESIAN_POINT('Origin',(-2.7249303158515,0.1293784130119,12.5369868989719));
#433324=CARTESIAN_POINT('Ctrl Pts',(-2.74188955709783,0.0950906273046976,
12.506462012331));
#433325=CARTESIAN_POINT('Ctrl Pts',(-2.74842425126575,0.0953172550206331,
12.4999388158272));
#433326=CARTESIAN_POINT('Ctrl Pts',(-2.74834693726402,0.0953145737175499,
12.4907030323752));
#433327=CARTESIAN_POINT('Ctrl Pts',(-2.74370084999371,0.108241589292313,
12.5042014951932));
#433328=CARTESIAN_POINT('Ctrl Pts',(-2.74777518131633,0.113215613959498,
12.4980716682127));
#433329=CARTESIAN_POINT('Ctrl Pts',(-2.74749105734251,0.120001248697188,
12.4907355092743));
#433330=CARTESIAN_POINT('Ctrl Pts',(-2.73851615822091,0.111314807876567,
12.5218047446509));
#433331=CARTESIAN_POINT('Ctrl Pts',(-2.74756663884357,0.11890477964432,
12.5216906929434));
#433332=CARTESIAN_POINT('Ctrl Pts',(-2.74689368091139,0.130648624072426,
12.5161988840776));
#433333=CARTESIAN_POINT('Ctrl Pts',(-2.73376917514574,0.10923208415584,
12.5369868989719));
#433334=CARTESIAN_POINT('Ctrl Pts',(-2.7478074027806,0.115391117878143,
12.5369868989719));
#433335=CARTESIAN_POINT('Ctrl Pts',(-2.746890969463,0.130693590929748,12.5369868989719));
#433336=CARTESIAN_POINT('Origin',(-5.15079064385546E-31,-5.04677213932918E-31,
12.5));
#433337=CARTESIAN_POINT('Origin',(-2.68023295023435,-0.132444682635759,
12.5));
#433338=CARTESIAN_POINT('',(-2.68023295023435,-0.132444682635759,12.5893111709658));
#433339=CARTESIAN_POINT('',(-2.68023295023435,-0.132444682635759,13.8235269408515));
#433340=CARTESIAN_POINT('',(-2.68023295023435,-0.132444682635759,12.5));
#433341=CARTESIAN_POINT('',(-2.71402813188475,-0.120733218320032,13.7902182540695));
#433342=CARTESIAN_POINT('',(-2.68023295023435,-0.132444682635759,13.8235269408515));
#433343=CARTESIAN_POINT('',(-2.73361252196705,-0.113946396223116,13.7435492065112));
#433344=CARTESIAN_POINT('Origin',(-2.66918024413258,-0.136275259008993,
13.7445212918717));
#433345=CARTESIAN_POINT('',(-2.73361252196705,-0.113946396223116,12.5369868989719));
#433346=CARTESIAN_POINT('',(-2.73361252196705,-0.113946396223116,12.5));
#433347=CARTESIAN_POINT('Ctrl Pts',(-2.73361252196705,-0.113946396223116,
12.5369868989719));
#433348=CARTESIAN_POINT('Ctrl Pts',(-2.71583230866048,-0.120107994518991,
12.5544431401645));
#433349=CARTESIAN_POINT('Ctrl Pts',(-2.69803937847279,-0.126273999753732,
12.5718848856037));
#433350=CARTESIAN_POINT('Ctrl Pts',(-2.68023295023435,-0.132444682635759,
12.5893111709658));
#433351=CARTESIAN_POINT('Origin',(-2.92325343698282,-0.316884282769413,
12.5));
#433352=CARTESIAN_POINT('',(-2.72707321410059,-0.220664646924619,13.7435492065112));
#433353=CARTESIAN_POINT('',(-2.70846397699157,-0.211537457691819,13.7902182540695));
#433354=CARTESIAN_POINT('Origin',(-2.65956211819432,-0.187552781884673,
13.7418732680455));
#433355=CARTESIAN_POINT('',(-2.67635153714374,-0.195787413049954,13.8235269408515));
#433356=CARTESIAN_POINT('',(-2.70846397699157,-0.211537457691819,13.7902182540695));
#433357=CARTESIAN_POINT('',(-2.67635153714374,-0.195787413049954,12.5893111709658));
#433358=CARTESIAN_POINT('',(-2.67635153714374,-0.195787413049954,12.5));
#433359=CARTESIAN_POINT('',(-2.72707321410059,-0.220664646924619,12.5369868989719));
#433360=CARTESIAN_POINT('Ctrl Pts',(-2.67635153714374,-0.195787413049954,
12.5893111709658));
#433361=CARTESIAN_POINT('Ctrl Pts',(-2.69327134132254,-0.204085993675111,
12.5718848856037));
#433362=CARTESIAN_POINT('Ctrl Pts',(-2.71017831955037,-0.212378283613504,
12.5544431401645));
#433363=CARTESIAN_POINT('Ctrl Pts',(-2.72707321410059,-0.220664646924619,
12.5369868989719));
#433364=CARTESIAN_POINT('',(-2.72707321410059,-0.220664646924619,12.5));
#433365=CARTESIAN_POINT('Origin',(-2.69148864585867,-0.164924675570068,
12.5));
#433366=CARTESIAN_POINT('',(-2.65726540810591,-0.161705953790234,13.8587068136939));
#433367=CARTESIAN_POINT('Ctrl Pts',(-2.6763515371407,-0.195787413055823,
13.8235269408542));
#433368=CARTESIAN_POINT('Ctrl Pts',(-2.67477827973691,-0.195015784538633,
13.8262006681044));
#433369=CARTESIAN_POINT('Ctrl Pts',(-2.67324478715602,-0.194070147961288,
13.8288634856214));
#433370=CARTESIAN_POINT('Ctrl Pts',(-2.6717495304784,-0.192963749774365,
13.8314912288862));
#433371=CARTESIAN_POINT('Ctrl Pts',(-2.67020807507234,-0.191823167363328,
13.8342001611531));
#433372=CARTESIAN_POINT('Ctrl Pts',(-2.66870524708003,-0.190510868342892,
13.8368750301949));
#433373=CARTESIAN_POINT('Ctrl Pts',(-2.66724775704212,-0.18899694895694,
13.8394886372969));
#433374=CARTESIAN_POINT('Ctrl Pts',(-2.66713519155111,-0.188880025290508,
13.8396904925131));
#433375=CARTESIAN_POINT('Ctrl Pts',(-2.6670229095647,-0.188761881108905,
13.8398919674349));
#433376=CARTESIAN_POINT('Ctrl Pts',(-2.66691092171307,-0.188642494026079,
13.8400930404591));
#433377=CARTESIAN_POINT('Ctrl Pts',(-2.66516607564295,-0.186782362955953,
13.8432258934518));
#433378=CARTESIAN_POINT('Ctrl Pts',(-2.66350071538557,-0.184630770035319,
13.8462331177034));
#433379=CARTESIAN_POINT('Ctrl Pts',(-2.66204544089643,-0.182198843193322,
13.8489036603661));
#433380=CARTESIAN_POINT('Ctrl Pts',(-2.66156925814769,-0.181403088428862,
13.849777493004));
#433381=CARTESIAN_POINT('Ctrl Pts',(-2.66111579360245,-0.180577428158085,
13.85061494757));
#433382=CARTESIAN_POINT('Ctrl Pts',(-2.66069025957861,-0.179722574650084,
13.8514076489583));
#433383=CARTESIAN_POINT('Ctrl Pts',(-2.65979019374699,-0.177914436192341,
13.8530843267192));
#433384=CARTESIAN_POINT('Ctrl Pts',(-2.65892932231216,-0.175796767077549,
13.8546805203176));
#433385=CARTESIAN_POINT('Ctrl Pts',(-2.65828401049632,-0.173441091909396,
13.8559412814273));
#433386=CARTESIAN_POINT('Ctrl Pts',(-2.6581976468474,-0.173125826175534,
13.8561100121513));
#433387=CARTESIAN_POINT('Ctrl Pts',(-2.65811510082779,-0.172806360954155,
13.8562727473908));
#433388=CARTESIAN_POINT('Ctrl Pts',(-2.65803674495943,-0.17248292451895,
13.8564289040185));
#433389=CARTESIAN_POINT('Ctrl Pts',(-2.6576814019903,-0.171016143975212,
13.8571370725437));
#433390=CARTESIAN_POINT('Ctrl Pts',(-2.65740820067463,-0.169441373077321,
13.8577210840554));
#433391=CARTESIAN_POINT('Ctrl Pts',(-2.65725667651276,-0.167814806897733,
13.8581177131616));
#433392=CARTESIAN_POINT('Ctrl Pts',(-2.65721400209347,-0.167356709876862,
13.8582294175695));
#433393=CARTESIAN_POINT('Ctrl Pts',(-2.65718080866484,-0.166894555363562,
13.8583265086086));
#433394=CARTESIAN_POINT('Ctrl Pts',(-2.65715755142542,-0.166429699052326,
13.8584082369006));
#433395=CARTESIAN_POINT('Ctrl Pts',(-2.65712413700904,-0.165761825189217,
13.8585256585398));
#433396=CARTESIAN_POINT('Ctrl Pts',(-2.65711114037927,-0.165080054877154,
13.8586122832068));
#433397=CARTESIAN_POINT('Ctrl Pts',(-2.65711968869444,-0.16440208348179,
13.8586682984299));
#433398=CARTESIAN_POINT('Ctrl Pts',(-2.6571265264992,-0.163859773570642,
13.8587131050557));
#433399=CARTESIAN_POINT('Ctrl Pts',(-2.65714699071182,-0.163313901590444,
13.8587357943552));
#433400=CARTESIAN_POINT('Ctrl Pts',(-2.65718158985444,-0.162764421649494,
13.8587355499465));
#433401=CARTESIAN_POINT('Ctrl Pts',(-2.65720395210521,-0.162409279663444,
13.8587353919793));
#433402=CARTESIAN_POINT('Ctrl Pts',(-2.65723193858569,-0.162056468535203,
13.8587257282814));
#433403=CARTESIAN_POINT('Ctrl Pts',(-2.65726540810591,-0.161705953790234,
13.8587068136939));
#433404=CARTESIAN_POINT('Ctrl Pts',(-2.65726540810591,-0.161705953790234,
13.8587068136939));
#433405=CARTESIAN_POINT('Ctrl Pts',(-2.65737548753329,-0.160553129902586,
13.8586446046466));
#433406=CARTESIAN_POINT('Ctrl Pts',(-2.65754480484203,-0.159425114975678,
13.858482427929));
#433407=CARTESIAN_POINT('Ctrl Pts',(-2.65776899483064,-0.158320944139967,
13.8582284286032));
#433408=CARTESIAN_POINT('Ctrl Pts',(-2.65799898768009,-0.157188193304953,
13.8579678548414));
#433409=CARTESIAN_POINT('Ctrl Pts',(-2.65828879341816,-0.156078074645413,
13.857615680862));
#433410=CARTESIAN_POINT('Ctrl Pts',(-2.65861761120967,-0.155031906223266,
13.8571944833187));
#433411=CARTESIAN_POINT('Ctrl Pts',(-2.65943820963712,-0.152421085932469,
13.8561433417727));
#433412=CARTESIAN_POINT('Ctrl Pts',(-2.66053558659169,-0.150084985800373,
13.8546163505474));
#433413=CARTESIAN_POINT('Ctrl Pts',(-2.66171089288025,-0.148080323240879,
13.8528973491086));
#433414=CARTESIAN_POINT('Ctrl Pts',(-2.66192560399914,-0.147714100967296,
13.8525833129072));
#433415=CARTESIAN_POINT('Ctrl Pts',(-2.66214284081204,-0.147358820344133,
13.8522628768812));
#433416=CARTESIAN_POINT('Ctrl Pts',(-2.66236132074595,-0.147014662717974,
13.851937733538));
#433417=CARTESIAN_POINT('Ctrl Pts',(-2.66369554738961,-0.144912939844747,
13.8499521282529));
#433418=CARTESIAN_POINT('Ctrl Pts',(-2.66521217477356,-0.143019349316914,
13.847639871647));
#433419=CARTESIAN_POINT('Ctrl Pts',(-2.66676878738483,-0.141383187388737,
13.8452109780794));
#433420=CARTESIAN_POINT('Ctrl Pts',(-2.66746913961893,-0.140647044270379,
13.8441181685877));
#433421=CARTESIAN_POINT('Ctrl Pts',(-2.66817726917405,-0.139962368013835,
13.8430021611332));
#433422=CARTESIAN_POINT('Ctrl Pts',(-2.66887973530314,-0.139330373170678,
13.8418824960098));
#433423=CARTESIAN_POINT('Ctrl Pts',(-2.67053511467444,-0.13784106118422,
13.8392439765549));
#433424=CARTESIAN_POINT('Ctrl Pts',(-2.67223564827898,-0.136570293061481,
13.8364981347964));
#433425=CARTESIAN_POINT('Ctrl Pts',(-2.67396534887573,-0.135487295887676,
13.8336931113419));
#433426=CARTESIAN_POINT('Ctrl Pts',(-2.67564996741083,-0.134432525417069,
13.8309611966328));
#433427=CARTESIAN_POINT('Ctrl Pts',(-2.67736424002019,-0.133555286933089,
13.8281701127186));
#433428=CARTESIAN_POINT('Ctrl Pts',(-2.6791007054218,-0.132865766020628,
13.8253580685121));
#433429=CARTESIAN_POINT('Ctrl Pts',(-2.67947717299492,-0.132716277142651,
13.8247484142933));
#433430=CARTESIAN_POINT('Ctrl Pts',(-2.67985464701624,-0.132575780751616,
13.8241378483365));
#433431=CARTESIAN_POINT('Ctrl Pts',(-2.68023295023436,-0.132444682635759,
13.8235269408515));
#433432=CARTESIAN_POINT('',(-2.65717142069583,-0.162944478406341,12.5969504640361));
#433433=CARTESIAN_POINT('Origin',(-2.69152168130615,-0.164926503689338,
12.584524458991));
#433434=CARTESIAN_POINT('Origin',(-2.69152168130615,-0.164926503689338,
12.584524458991));
#433435=CARTESIAN_POINT('Ctrl Pts',(-2.67635153714374,-0.195787413049954,
12.5893111709658));
#433436=CARTESIAN_POINT('Ctrl Pts',(-2.66617562406611,-0.190796478508579,
12.5770542771492));
#433437=CARTESIAN_POINT('Ctrl Pts',(-2.67051623844065,-0.175017925288893,
12.5737548217797));
#433438=CARTESIAN_POINT('Ctrl Pts',(-2.69860284390658,-0.206700911884528,
12.5663937883685));
#433439=CARTESIAN_POINT('Ctrl Pts',(-2.68841395003863,-0.201703610713006,
12.5540940315304));
#433440=CARTESIAN_POINT('Ctrl Pts',(-2.69277111126456,-0.185877014699834,
12.5508374392248));
#433441=CARTESIAN_POINT('Ctrl Pts',(-2.72083169937371,-0.217603399132581,
12.5434499600945));
#433442=CARTESIAN_POINT('Ctrl Pts',(-2.71060967778341,-0.212589849955346,
12.5311293540533));
#433443=CARTESIAN_POINT('Ctrl Pts',(-2.71500372320481,-0.196726554919452,
12.5278936106989));
#433444=CARTESIAN_POINT('Ctrl Pts',(-2.74303986218576,-0.228495737346712,
12.5204817579905));
#433445=CARTESIAN_POINT('Ctrl Pts',(-2.73276724857437,-0.223457374527361,
12.5081597038247));
#433446=CARTESIAN_POINT('Ctrl Pts',(-2.73721579838891,-0.207567300599202,
12.5049254088044));
#433447=CARTESIAN_POINT('Ctrl Pts',(-2.72707321410058,-0.220664646924618,
12.5369868989719));
#433448=CARTESIAN_POINT('Ctrl Pts',(-2.72790954254262,-0.221074837011971,
12.5342545179733));
#433449=CARTESIAN_POINT('Ctrl Pts',(-2.72876262844905,-0.221354303556684,
12.5314872231885));
#433450=CARTESIAN_POINT('Ctrl Pts',(-2.72960181897609,-0.221434180771564,
12.5287124745063));
#433451=CARTESIAN_POINT('Ctrl Pts',(-2.73035864264708,-0.221506218008694,
12.5262100684184));
#433452=CARTESIAN_POINT('Ctrl Pts',(-2.73110349432844,-0.221414870811116,
12.5237004536639));
#433453=CARTESIAN_POINT('Ctrl Pts',(-2.73184109422079,-0.221092773046081,
12.5212220730815));
#433454=CARTESIAN_POINT('Ctrl Pts',(-2.73240579074586,-0.22084617934327,
12.5193246583486));
#433455=CARTESIAN_POINT('Ctrl Pts',(-2.7329727318048,-0.220460808795907,
12.517417831369));
#433456=CARTESIAN_POINT('Ctrl Pts',(-2.73350419877607,-0.219847043725262,
12.5155812248348));
#433457=CARTESIAN_POINT('Ctrl Pts',(-2.73373060656248,-0.219585576506165,
12.5147988205793));
#433458=CARTESIAN_POINT('Ctrl Pts',(-2.73395101574848,-0.219282576031812,
12.5140295443047));
#433459=CARTESIAN_POINT('Ctrl Pts',(-2.73416462351205,-0.218931357472827,
12.5132817086137));
#433460=CARTESIAN_POINT('Ctrl Pts',(-2.73448788996602,-0.218399835695578,
12.5121499604604));
#433461=CARTESIAN_POINT('Ctrl Pts',(-2.73479644966733,-0.217742687289853,
12.511049420657));
#433462=CARTESIAN_POINT('Ctrl Pts',(-2.73506347853791,-0.216934078796233,
12.5100666561697));
#433463=CARTESIAN_POINT('Ctrl Pts',(-2.73521680590049,-0.216469777661257,
12.5095023550643));
#433464=CARTESIAN_POINT('Ctrl Pts',(-2.73535759215747,-0.215949970422336,
12.5089719619137));
#433465=CARTESIAN_POINT('Ctrl Pts',(-2.73547703356137,-0.21538273058066,
12.5085043804652));
#433466=CARTESIAN_POINT('Ctrl Pts',(-2.73565182049765,-0.214552648960552,
12.5078201359221));
#433467=CARTESIAN_POINT('Ctrl Pts',(-2.73578478600157,-0.213596668737202,
12.5072563000949));
#433468=CARTESIAN_POINT('Ctrl Pts',(-2.73585853169418,-0.212578424975029,
12.5068768744332));
#433469=CARTESIAN_POINT('Ctrl Pts',(-2.73591170741522,-0.211844201126362,
12.5066032824114));
#433470=CARTESIAN_POINT('Ctrl Pts',(-2.73593508648895,-0.211064709086899,
12.5064197834844));
#433471=CARTESIAN_POINT('Ctrl Pts',(-2.73592994706302,-0.210283555207319,
12.5063282718343));
#433472=CARTESIAN_POINT('Ctrl Pts',(-2.73592244509229,-0.209143312382261,
12.5061946931565));
#433473=CARTESIAN_POINT('Ctrl Pts',(-2.73585508068928,-0.207975150357036,
12.5062515701262));
#433474=CARTESIAN_POINT('Ctrl Pts',(-2.73574747348863,-0.206850677009604,
12.5064436508398));
#433475=CARTESIAN_POINT('',(-2.67051623844065,-0.175017925288893,12.5737548217797));
#433476=CARTESIAN_POINT('Origin',(-2.68603928672129,-0.176035261062827,
12.5893111709658));
#433477=CARTESIAN_POINT('Ctrl Pts',(-2.73574747348863,-0.206850677009604,
12.5064436508398));
#433478=CARTESIAN_POINT('Ctrl Pts',(-2.72609176665931,-0.202138170948357,
12.5164271754438));
#433479=CARTESIAN_POINT('Ctrl Pts',(-2.7164321406699,-0.197423984617126,
12.5264061185523));
#433480=CARTESIAN_POINT('Ctrl Pts',(-2.706768457906,-0.192708057987618,
12.536380305637));
#433481=CARTESIAN_POINT('Ctrl Pts',(-2.69469081445718,-0.186814106193713,
12.5488460165097));
#433482=CARTESIAN_POINT('Ctrl Pts',(-2.6826068307766,-0.180917434346827,
12.5613043021964));
#433483=CARTESIAN_POINT('Ctrl Pts',(-2.67051623844065,-0.175017925288894,
12.5737548217797));
#433484=CARTESIAN_POINT('Ctrl Pts',(-2.68023295023435,-0.132444682635759,
12.5893111709658));
#433485=CARTESIAN_POINT('Ctrl Pts',(-2.66952380348168,-0.136155856357012,
12.5770542771492));
#433486=CARTESIAN_POINT('Ctrl Pts',(-2.67190547188397,-0.152346326716963,
12.5737548217797));
#433487=CARTESIAN_POINT('Ctrl Pts',(-2.67024140945735,-0.135907175439603,
12.5928319619712));
#433488=CARTESIAN_POINT('Ctrl Pts',(-2.66411091140471,-0.141479464915032,
12.5821634970842));
#433489=CARTESIAN_POINT('Ctrl Pts',(-2.66826270477977,-0.153598710521533,
12.5773203894503));
#433490=CARTESIAN_POINT('Ctrl Pts',(-2.65814434998816,-0.147493600752807,
12.5969440695591));
#433491=CARTESIAN_POINT('Ctrl Pts',(-2.6578802568247,-0.15150468506418,
12.5878292599214));
#433492=CARTESIAN_POINT('Ctrl Pts',(-2.66395248114037,-0.157729826505854,
12.5813877129824));
#433493=CARTESIAN_POINT('Ctrl Pts',(-2.65621916765618,-0.178029954800566,
12.596957478804));
#433494=CARTESIAN_POINT('Ctrl Pts',(-2.65648138908561,-0.174048518744211,
12.5878468778671));
#433495=CARTESIAN_POINT('Ctrl Pts',(-2.66326938499446,-0.168659586245191,
12.5814011370086));
#433496=CARTESIAN_POINT('Ctrl Pts',(-2.66684371342032,-0.191124153303934,
12.5928371701607));
#433497=CARTESIAN_POINT('Ctrl Pts',(-2.66144789247666,-0.18484560394538,
12.5821692192952));
#433498=CARTESIAN_POINT('Ctrl Pts',(-2.66704244863735,-0.173324980553701,
12.5773318885715));
#433499=CARTESIAN_POINT('Ctrl Pts',(-2.67635153714371,-0.195787413050002,
12.5893111709658));
#433500=CARTESIAN_POINT('Ctrl Pts',(-2.66617562406608,-0.190796478508627,
12.5770542771492));
#433501=CARTESIAN_POINT('Ctrl Pts',(-2.67051623844063,-0.175017925288943,
12.5737548217797));
#433502=CARTESIAN_POINT('',(-2.67190547188397,-0.152346326716963,12.5737548217797));
#433503=CARTESIAN_POINT('Origin',(-2.68743659543392,-0.153231878113717,
12.5893111709658));
#433504=CARTESIAN_POINT('Ctrl Pts',(-2.67051623844063,-0.175017925288943,
12.5737548217797));
#433505=CARTESIAN_POINT('Ctrl Pts',(-2.66960256166138,-0.174606204055485,
12.5746934679442));
#433506=CARTESIAN_POINT('Ctrl Pts',(-2.66866677595842,-0.17398359618822,
12.5756680099006));
#433507=CARTESIAN_POINT('Ctrl Pts',(-2.6678135025773,-0.173223709219617,
12.5765688348656));
#433508=CARTESIAN_POINT('Ctrl Pts',(-2.6675876078957,-0.173022537556906,
12.5768073183026));
#433509=CARTESIAN_POINT('Ctrl Pts',(-2.66736737712466,-0.172811972275615,
12.5770407398754));
#433510=CARTESIAN_POINT('Ctrl Pts',(-2.66715437352828,-0.172593796633459,
12.5772674179684));
#433511=CARTESIAN_POINT('Ctrl Pts',(-2.66628026436733,-0.171698462795228,
12.5781976435658));
#433512=CARTESIAN_POINT('Ctrl Pts',(-2.66548628908493,-0.170616233275343,
12.5790594849312));
#433513=CARTESIAN_POINT('Ctrl Pts',(-2.66486499294561,-0.169391617486232,
12.5797571720116));
#433514=CARTESIAN_POINT('Ctrl Pts',(-2.66446019617102,-0.168593736266367,
12.580211740231));
#433515=CARTESIAN_POINT('Ctrl Pts',(-2.6641270471188,-0.16769065892232,
12.5806009430798));
#433516=CARTESIAN_POINT('Ctrl Pts',(-2.66390561976632,-0.166739826344052,
12.5808812374708));
#433517=CARTESIAN_POINT('Ctrl Pts',(-2.66371534021279,-0.165922745723894,
12.5811221033394));
#433518=CARTESIAN_POINT('Ctrl Pts',(-2.66360377729331,-0.165053646496132,
12.581287365893));
#433519=CARTESIAN_POINT('Ctrl Pts',(-2.66358549792153,-0.164180520418168,
12.581359338449));
#433520=CARTESIAN_POINT('Ctrl Pts',(-2.66358295746631,-0.164059173922696,
12.5813693411482));
#433521=CARTESIAN_POINT('Ctrl Pts',(-2.66358216194757,-0.163937730877166,
12.5813775999465));
#433522=CARTESIAN_POINT('Ctrl Pts',(-2.66358309256861,-0.163816299853001,
12.5813841266931));
#433523=CARTESIAN_POINT('Ctrl Pts',(-2.66358467147975,-0.163610277433727,
12.5813952001081));
#433524=CARTESIAN_POINT('Ctrl Pts',(-2.66359183855161,-0.163402914444762,
12.5814007534795));
#433525=CARTESIAN_POINT('Ctrl Pts',(-2.66360478775479,-0.163194308011535,
12.5814005856065));
#433526=CARTESIAN_POINT('Ctrl Pts',(-2.66366406414415,-0.162239389320051,
12.5813998171494));
#433527=CARTESIAN_POINT('Ctrl Pts',(-2.6638400698358,-0.161324371507552,
12.58127954464));
#433528=CARTESIAN_POINT('Ctrl Pts',(-2.6641027488832,-0.160448860328191,
12.5810700125799));
#433529=CARTESIAN_POINT('Ctrl Pts',(-2.66442003526405,-0.159391342508453,
12.5808169217085));
#433530=CARTESIAN_POINT('Ctrl Pts',(-2.66487983585568,-0.158396178313262,
12.5804173076348));
#433531=CARTESIAN_POINT('Ctrl Pts',(-2.66541821357192,-0.157539659310368,
12.5799304713245));
#433532=CARTESIAN_POINT('Ctrl Pts',(-2.6660854331688,-0.156478162434471,
12.5793271277669));
#433533=CARTESIAN_POINT('Ctrl Pts',(-2.66688746630062,-0.155546628396526,
12.5785808224116));
#433534=CARTESIAN_POINT('Ctrl Pts',(-2.66776647013655,-0.154763628958832,
12.5777485681082));
#433535=CARTESIAN_POINT('Ctrl Pts',(-2.66907628215414,-0.153596874012674,
12.576508418016));
#433536=CARTESIAN_POINT('Ctrl Pts',(-2.67054140196298,-0.15276462197363,
12.5750928681475));
#433537=CARTESIAN_POINT('Ctrl Pts',(-2.67190547188397,-0.152346326716963,
12.5737548217797));
#433538=CARTESIAN_POINT('Ctrl Pts',(-2.67190547188397,-0.152346326716963,
12.5737548217797));
#433539=CARTESIAN_POINT('Ctrl Pts',(-2.66952380348168,-0.136155856357012,
12.5770542771492));
#433540=CARTESIAN_POINT('Ctrl Pts',(-2.68023295023435,-0.132444682635759,
12.5893111709658));
#433541=CARTESIAN_POINT('Ctrl Pts',(-2.69531616042252,-0.144286884036376,
12.5508408821982));
#433542=CARTESIAN_POINT('Ctrl Pts',(-2.69292393312528,-0.12804671860655,
12.55409748406));
#433543=CARTESIAN_POINT('Ctrl Pts',(-2.70364674200648,-0.124330810378115,
12.5663972313419));
#433544=CARTESIAN_POINT('Ctrl Pts',(-2.71870359571991,-0.136234199142437,
12.52790050457));
#433545=CARTESIAN_POINT('Ctrl Pts',(-2.71627924595099,-0.119953111785028,
12.5311362602938));
#433546=CARTESIAN_POINT('Ctrl Pts',(-2.72703691311007,-0.116225123684305,
12.5434568539655));
#433547=CARTESIAN_POINT('Ctrl Pts',(-2.74206958034371,-0.128187733774514,
12.5049357605811));
#433548=CARTESIAN_POINT('Ctrl Pts',(-2.73959441388288,-0.111873416872463,
12.5081700652078));
#433549=CARTESIAN_POINT('Ctrl Pts',(-2.75040531352075,-0.108126981459283,
12.5204921097672));
#433550=CARTESIAN_POINT('Ctrl Pts',(-2.74053527768469,-0.128716094731106,
12.5064436508395));
#433551=CARTESIAN_POINT('Ctrl Pts',(-2.74079894328763,-0.127524739099731,
12.5062361689309));
#433552=CARTESIAN_POINT('Ctrl Pts',(-2.74102233188788,-0.126274583447935,
12.5061871075061));
#433553=CARTESIAN_POINT('Ctrl Pts',(-2.74117020531107,-0.125054276071972,
12.5063648335164));
#433554=CARTESIAN_POINT('Ctrl Pts',(-2.74123737854109,-0.124499937190128,
12.5064455676329));
#433555=CARTESIAN_POINT('Ctrl Pts',(-2.74128968714911,-0.123943999232077,
12.506574497099));
#433556=CARTESIAN_POINT('Ctrl Pts',(-2.74132384197106,-0.123410200700237,
12.5067492519495));
#433557=CARTESIAN_POINT('Ctrl Pts',(-2.74139247741156,-0.122337511830006,
12.5071004286051));
#433558=CARTESIAN_POINT('Ctrl Pts',(-2.74138952033895,-0.121314736865664,
12.5076537929612));
#433559=CARTESIAN_POINT('Ctrl Pts',(-2.74132465110495,-0.120418613085864,
12.5083435010503));
#433560=CARTESIAN_POINT('Ctrl Pts',(-2.741320567199,-0.120362196738561,
12.5083869222963));
#433561=CARTESIAN_POINT('Ctrl Pts',(-2.74131622555791,-0.120306277076869,
12.5084308732336));
#433562=CARTESIAN_POINT('Ctrl Pts',(-2.74131162372435,-0.120250870730712,
12.5084753333615));
#433563=CARTESIAN_POINT('Ctrl Pts',(-2.74127471094544,-0.119806438705525,
12.508831962269));
#433564=CARTESIAN_POINT('Ctrl Pts',(-2.74122159324092,-0.119385904725475,
12.509227847131));
#433565=CARTESIAN_POINT('Ctrl Pts',(-2.74115662805751,-0.119001422570601,
12.5096423454524));
#433566=CARTESIAN_POINT('Ctrl Pts',(-2.74095305592508,-0.117796625661898,
12.5109411997424));
#433567=CARTESIAN_POINT('Ctrl Pts',(-2.74063016373539,-0.116870114613123,
12.5124831113042));
#433568=CARTESIAN_POINT('Ctrl Pts',(-2.74025727175298,-0.11615746459738,
12.5140723025008));
#433569=CARTESIAN_POINT('Ctrl Pts',(-2.74022233136581,-0.116090688510361,
12.5142212114565));
#433570=CARTESIAN_POINT('Ctrl Pts',(-2.74018696520292,-0.116025763606908,
12.5143705582413));
#433571=CARTESIAN_POINT('Ctrl Pts',(-2.7401512392264,-0.115962622442655,
12.5145201959299));
#433572=CARTESIAN_POINT('Ctrl Pts',(-2.73969228586759,-0.115151480180464,
12.5164425148273));
#433573=CARTESIAN_POINT('Ctrl Pts',(-2.73916757216949,-0.114601631733722,
12.5184635205941));
#433574=CARTESIAN_POINT('Ctrl Pts',(-2.73860159963072,-0.114226257432332,
12.5205025929158));
#433575=CARTESIAN_POINT('Ctrl Pts',(-2.73827331312518,-0.114008525459078,
12.5216853356836));
#433576=CARTESIAN_POINT('Ctrl Pts',(-2.73793200553798,-0.113849484943904,
12.5228750347131));
#433577=CARTESIAN_POINT('Ctrl Pts',(-2.73758805651309,-0.113734129333599,
12.5240609649613));
#433578=CARTESIAN_POINT('Ctrl Pts',(-2.73674385208373,-0.11345099517672,
12.5269717671327));
#433579=CARTESIAN_POINT('Ctrl Pts',(-2.7358566698738,-0.113432919929299,
12.5299036066169));
#433580=CARTESIAN_POINT('Ctrl Pts',(-2.73494218237204,-0.113594675100055,
12.5328133004019));
#433581=CARTESIAN_POINT('Ctrl Pts',(-2.73450317512218,-0.113672327000739,
12.5342101228452));
#433582=CARTESIAN_POINT('Ctrl Pts',(-2.73405851424506,-0.113791841062789,
12.5356023438238));
#433583=CARTESIAN_POINT('Ctrl Pts',(-2.73361252196705,-0.113946396223116,
12.5369868989719));
#433584=CARTESIAN_POINT('Origin',(-14.7751638741716,4.06456903460374,-1.24070212061166));
#433585=CARTESIAN_POINT('Ctrl Pts',(-2.72703567269247,-0.220646278375188,
12.5369868989719));
#433586=CARTESIAN_POINT('Ctrl Pts',(-2.74082017142999,-0.227374643573386,
12.5369868989719));
#433587=CARTESIAN_POINT('Ctrl Pts',(-2.73927331120585,-0.242635394771541,
12.5369868989719));
#433588=CARTESIAN_POINT('Ctrl Pts',(-2.73169534333072,-0.222920788458994,
12.5218025310016));
#433589=CARTESIAN_POINT('Ctrl Pts',(-2.74043375195878,-0.230876671713106,
12.5216901060418));
#433590=CARTESIAN_POINT('Ctrl Pts',(-2.73927804295614,-0.242588876607485,
12.5161920673677));
#433591=CARTESIAN_POINT('Ctrl Pts',(-2.73700294375324,-0.220063263489773,
12.5042015548895));
#433592=CARTESIAN_POINT('Ctrl Pts',(-2.74087193293557,-0.225202161010103,
12.4980677368512));
#433593=CARTESIAN_POINT('Ctrl Pts',(-2.74030930782376,-0.231975212959352,
12.4907278922778));
#433594=CARTESIAN_POINT('Ctrl Pts',(-2.73572752933513,-0.206849169015788,
12.506463626192));
#433595=CARTESIAN_POINT('Ctrl Pts',(-2.74225164635562,-0.207342459436628,
12.4999376786891));
#433596=CARTESIAN_POINT('Ctrl Pts',(-2.74217196375227,-0.207336434611381,
12.4906970594712));
#433597=CARTESIAN_POINT('Origin',(-2.71738546452303,-0.240416798911745,
12.5369868989719));
#433598=CARTESIAN_POINT('Origin',(-2.71738546452303,-0.240416798911746,
14.));
#433599=CARTESIAN_POINT('Origin',(-2.71738546452303,-0.240416798911745,
13.7435492065112));
#433600=CARTESIAN_POINT('Ctrl Pts',(-2.70484295955581,-0.209761503718633,
13.793642941384));
#433601=CARTESIAN_POINT('Ctrl Pts',(-2.71456248633017,-0.214498276701194,
13.8071662555867));
#433602=CARTESIAN_POINT('Ctrl Pts',(-2.70943367592869,-0.230737571251773,
13.8103758687955));
#433603=CARTESIAN_POINT('Ctrl Pts',(-2.71976582146069,-0.217080649692748,
13.7804579775006));
#433604=CARTESIAN_POINT('Ctrl Pts',(-2.73175439640573,-0.222934515297326,
13.7901904343352));
#433605=CARTESIAN_POINT('Ctrl Pts',(-2.72950263006789,-0.238528920464716,
13.7927914348262));
#433606=CARTESIAN_POINT('Ctrl Pts',(-2.72855147185785,-0.221389706412309,
13.7597120340895));
#433607=CARTESIAN_POINT('Ctrl Pts',(-2.74242311492923,-0.228169426795429,
13.7635825532445));
#433608=CARTESIAN_POINT('Ctrl Pts',(-2.74132801802721,-0.243147299772559,
13.7651073818884));
#433609=CARTESIAN_POINT('Ctrl Pts',(-2.7268310403412,-0.220545894441165,
13.7381884353898));
#433610=CARTESIAN_POINT('Ctrl Pts',(-2.74037838644556,-0.227166115295103,
13.7368803041982));
#433611=CARTESIAN_POINT('Ctrl Pts',(-2.73901207587965,-0.242243344236675,
13.7363986145813));
#433612=CARTESIAN_POINT('Origin',(-2.69877622741401,-0.231289609678946,
13.7902182540695));
#433613=CARTESIAN_POINT('Ctrl Pts',(-2.67634800279185,-0.195785680417494,
13.8235227101244));
#433614=CARTESIAN_POINT('Ctrl Pts',(-2.68667231492669,-0.200844461620682,
13.8358800583119));
#433615=CARTESIAN_POINT('Ctrl Pts',(-2.68216956901137,-0.216792857410809,
13.8390832900376));
#433616=CARTESIAN_POINT('Ctrl Pts',(-2.68705688280404,-0.201038016867016,
13.8124254819053));
#433617=CARTESIAN_POINT('Ctrl Pts',(-2.69740124448431,-0.206106622401379,
13.8247886449158));
#433618=CARTESIAN_POINT('Ctrl Pts',(-2.69287640609648,-0.222070538545803,
13.8279860620657));
#433619=CARTESIAN_POINT('Ctrl Pts',(-2.6977609634446,-0.2062879993902,13.8013225099955));
#433620=CARTESIAN_POINT('Ctrl Pts',(-2.70812049467478,-0.211364035887708,
13.8136962257787));
#433621=CARTESIAN_POINT('Ctrl Pts',(-2.70357840628482,-0.227345533249965,
13.8168830918626));
#433622=CARTESIAN_POINT('Ctrl Pts',(-2.70846043144973,-0.211535719574715,
13.7902140179785));
#433623=CARTESIAN_POINT('Ctrl Pts',(-2.71883057117651,-0.216616950094158,
13.802602731458));
#433624=CARTESIAN_POINT('Ctrl Pts',(-2.71427576044339,-0.232617945429034,
13.8057746032558));
#433625=CARTESIAN_POINT('Origin',(-2.66666378756618,-0.21553956503708,13.8235269408515));
#433626=CARTESIAN_POINT('Ctrl Pts',(-2.68023295023436,-0.132444682635759,
13.8235269408515));
#433627=CARTESIAN_POINT('Ctrl Pts',(-2.69138951503121,-0.128578459578989,
13.8362179249168));
#433628=CARTESIAN_POINT('Ctrl Pts',(-2.68848109463237,-0.111749790741529,
13.8391868794938));
#433629=CARTESIAN_POINT('Ctrl Pts',(-2.67002517906158,-0.135982108446035,
13.8400110824519));
#433630=CARTESIAN_POINT('Ctrl Pts',(-2.67784984837637,-0.12964993559815,
13.8494522556836));
#433631=CARTESIAN_POINT('Ctrl Pts',(-2.67171877499601,-0.11767755794622,
13.85569149686));
#433632=CARTESIAN_POINT('Ctrl Pts',(-2.65816477724548,-0.147150304128653,
13.8586819406588));
#433633=CARTESIAN_POINT('Ctrl Pts',(-2.65844494694465,-0.142805474031326,
13.868010383617));
#433634=CARTESIAN_POINT('Ctrl Pts',(-2.65213036132971,-0.136323277235162,
13.8744918421245));
#433635=CARTESIAN_POINT('Ctrl Pts',(-2.65619840500193,-0.178378574624259,
13.8587686893867));
#433636=CARTESIAN_POINT('Ctrl Pts',(-2.65592067261882,-0.18268473215078,
13.8680909899357));
#433637=CARTESIAN_POINT('Ctrl Pts',(-2.64885949684767,-0.188309338646756,
13.8745789365163));
#433638=CARTESIAN_POINT('Ctrl Pts',(-2.66663625157229,-0.191022400427148,
13.8400379222776));
#433639=CARTESIAN_POINT('Ctrl Pts',(-2.6736223259497,-0.198265673078453,
13.8494748685453));
#433640=CARTESIAN_POINT('Ctrl Pts',(-2.66607977414707,-0.209395408815177,
13.8557104837033));
#433641=CARTESIAN_POINT('Ctrl Pts',(-2.6763515371407,-0.195787413055823,
13.8235269408542));
#433642=CARTESIAN_POINT('Ctrl Pts',(-2.68695259026277,-0.200986864131993,
13.8362179249195));
#433643=CARTESIAN_POINT('Ctrl Pts',(-2.68201124437825,-0.217334527723647,
13.8391868794965));
#433644=CARTESIAN_POINT('Origin',(-2.67302930503479,-0.111657487157801,
13.8235269408515));
#433645=CARTESIAN_POINT('Ctrl Pts',(-2.71402440610745,-0.120734508655639,
13.7902140241683));
#433646=CARTESIAN_POINT('Ctrl Pts',(-2.72493734455485,-0.116957423822622,
13.8026027327198));
#433647=CARTESIAN_POINT('Ctrl Pts',(-2.722370242243,-0.100520029929612,
13.8057746032556));
#433648=CARTESIAN_POINT('Ctrl Pts',(-2.70276426933073,-0.124636623798955,
13.8013225161808));
#433649=CARTESIAN_POINT('Ctrl Pts',(-2.71366604449621,-0.120863398901542,
13.8136962270464));
#433650=CARTESIAN_POINT('Ctrl Pts',(-2.71110918874919,-0.104446910421896,
13.8168830918628));
#433651=CARTESIAN_POINT('Ctrl Pts',(-2.69149927820773,-0.128540421179234,
13.8124254880875));
#433652=CARTESIAN_POINT('Ctrl Pts',(-2.70238509004795,-0.124772719542996,
13.8247886461868));
#433653=CARTESIAN_POINT('Ctrl Pts',(-2.69984320867404,-0.108375786864016,
13.8279860620656));
#433654=CARTESIAN_POINT('Ctrl Pts',(-2.68022923621552,-0.132445968900005,
13.8235227163065));
#433655=CARTESIAN_POINT('Ctrl Pts',(-2.69109394903256,-0.128685570165813,
13.8358800595847));
#433656=CARTESIAN_POINT('Ctrl Pts',(-2.68857209989094,-0.112306739080995,
13.8390832900376));
#433657=CARTESIAN_POINT('Origin',(-2.70682448668518,-0.0999460228420741,
13.7902182540695));
#433658=CARTESIAN_POINT('Ctrl Pts',(-2.73335752972873,-0.114034732658743,
13.7382347919292));
#433659=CARTESIAN_POINT('Ctrl Pts',(-2.74762380251145,-0.109116264439644,
13.7369371795942));
#433660=CARTESIAN_POINT('Ctrl Pts',(-2.74810064964376,-0.0939730681511174,
13.7364597369712));
#433661=CARTESIAN_POINT('Ctrl Pts',(-2.73514481161654,-0.113415364078833,
13.7595490285574));
#433662=CARTESIAN_POINT('Ctrl Pts',(-2.74975113773552,-0.108378594903541,
13.7633824266926));
#433663=CARTESIAN_POINT('Ctrl Pts',(-2.75048021381224,-0.0933665294766319,
13.7648920890506));
#433664=CARTESIAN_POINT('Ctrl Pts',(-2.72602977190662,-0.11657410991213,
13.7803806590111));
#433665=CARTESIAN_POINT('Ctrl Pts',(-2.73866548108742,-0.112222588396372,
13.7901039518744));
#433666=CARTESIAN_POINT('Ctrl Pts',(-2.73834985287197,-0.096462327603629,
13.7926933640891));
#433667=CARTESIAN_POINT('Ctrl Pts',(-2.71018579813282,-0.122064715218304,
13.7936647693663));
#433668=CARTESIAN_POINT('Ctrl Pts',(-2.72041476756285,-0.118551665781653,
13.8072068914933));
#433669=CARTESIAN_POINT('Ctrl Pts',(-2.71729332976618,-0.101791567454706,
13.8104111085397));
#433670=CARTESIAN_POINT('Origin',(-2.72640887676748,-0.0931592007451578,
13.7435492065112));
#433671=CARTESIAN_POINT('Origin',(-2.72640887676748,-0.0931592007451578,
14.));
#433672=CARTESIAN_POINT('Origin',(-2.72640887676748,-0.093159200745158,
12.5369868989719));
#433673=CARTESIAN_POINT('Ctrl Pts',(-2.7405169146902,-0.128715232277453,
12.506462012331));
#433674=CARTESIAN_POINT('Ctrl Pts',(-2.74704833746511,-0.129021996886374,
12.4999388158272));
#433675=CARTESIAN_POINT('Ctrl Pts',(-2.74697106216825,-0.129018367458753,
12.4907030323752));
#433676=CARTESIAN_POINT('Ctrl Pts',(-2.74339410614793,-0.115755666217203,
12.5042014951932));
#433677=CARTESIAN_POINT('Ctrl Pts',(-2.7478603096561,-0.111130288033808,
12.4980716682127));
#433678=CARTESIAN_POINT('Ctrl Pts',(-2.74813022330732,-0.104344073194392,
12.4907355092743));
#433679=CARTESIAN_POINT('Ctrl Pts',(-2.73847716185432,-0.112270073002454,
12.5218047446509));
#433680=CARTESIAN_POINT('Ctrl Pts',(-2.74811618091026,-0.105443054430946,
12.5216906929434));
#433681=CARTESIAN_POINT('Ctrl Pts',(-2.74840269453549,-0.0936834343574711,
12.5161988840776));
#433682=CARTESIAN_POINT('Ctrl Pts',(-2.73357621265543,-0.113958943442349,
12.5369868989719));
#433683=CARTESIAN_POINT('Ctrl Pts',(-2.74806974767195,-0.108964649273456,
12.5369868989719));
#433684=CARTESIAN_POINT('Ctrl Pts',(-2.74840365732554,-0.0936383961154349,
12.5369868989719));
#433685=CARTESIAN_POINT('Origin',(-5.14221766115599E-31,-5.4669590742534E-31,
12.5));
#433686=CARTESIAN_POINT('Origin',(-2.66051922500485,-0.35046785139304,12.5));
#433687=CARTESIAN_POINT('',(-2.66051922500485,-0.35046785139304,12.5893111709658));
#433688=CARTESIAN_POINT('',(-2.66051922500485,-0.35046785139304,13.8235269408515));
#433689=CARTESIAN_POINT('',(-2.66051922500485,-0.35046785139304,12.5));
#433690=CARTESIAN_POINT('',(-2.69515654904186,-0.341549977052361,13.7902182540695));
#433691=CARTESIAN_POINT('',(-2.66051922500485,-0.35046785139304,13.8235269408515));
#433692=CARTESIAN_POINT('',(-2.71522896268844,-0.336382047150414,13.7435492065112));
#433693=CARTESIAN_POINT('Origin',(-2.64919106833208,-0.35338478368455,13.7445212918706));
#433694=CARTESIAN_POINT('',(-2.71522896268844,-0.336382047150414,12.5369868989719));
#433695=CARTESIAN_POINT('',(-2.71522896268844,-0.336382047150414,12.5));
#433696=CARTESIAN_POINT('Ctrl Pts',(-2.71522896268844,-0.336382047150414,
12.5369868989719));
#433697=CARTESIAN_POINT('Ctrl Pts',(-2.69700568411229,-0.341073890788324,
12.5544431401645));
#433698=CARTESIAN_POINT('Ctrl Pts',(-2.67876937176296,-0.345769090157505,
12.5718848856037));
#433699=CARTESIAN_POINT('Ctrl Pts',(-2.66051922500485,-0.35046785139304,
12.5893111709658));
#433700=CARTESIAN_POINT('Origin',(-2.88769754146683,-0.554102169734571,
12.5));
#433701=CARTESIAN_POINT('',(-2.70001288567338,-0.442212187377255,13.7435492065112));
#433702=CARTESIAN_POINT('',(-2.68220951992085,-0.431598542529574,13.7902182540695));
#433703=CARTESIAN_POINT('Origin',(-2.63542535176389,-0.403707718276761,
13.7418732680449));
#433704=CARTESIAN_POINT('',(-2.65148770642212,-0.413283442897022,13.8235269408515));
#433705=CARTESIAN_POINT('',(-2.68220951992085,-0.431598542529574,13.7902182540695));
#433706=CARTESIAN_POINT('',(-2.65148770642212,-0.413283442897022,12.5893111709658));
#433707=CARTESIAN_POINT('',(-2.65148770642212,-0.413283442897022,12.5));
#433708=CARTESIAN_POINT('',(-2.70001288567338,-0.442212187377255,12.5369868989719));
#433709=CARTESIAN_POINT('Ctrl Pts',(-2.65148770642212,-0.413283442897022,
12.5893111709658));
#433710=CARTESIAN_POINT('Ctrl Pts',(-2.66767479998709,-0.422933531796104,
12.5718848856037));
#433711=CARTESIAN_POINT('Ctrl Pts',(-2.68384962302775,-0.43257630550609,
12.5544431401645));
#433712=CARTESIAN_POINT('Ctrl Pts',(-2.70001288567338,-0.442212187377255,
12.5369868989719));
#433713=CARTESIAN_POINT('',(-2.70001288567338,-0.442212187377255,12.5));
#433714=CARTESIAN_POINT('Origin',(-2.66909004727681,-0.383757213516432,
12.5));
#433715=CARTESIAN_POINT('',(-2.63524304023065,-0.377759690177983,13.8587068136939));
#433716=CARTESIAN_POINT('Ctrl Pts',(-2.65148770641861,-0.413283442902624,
13.8235269408542));
#433717=CARTESIAN_POINT('Ctrl Pts',(-2.64998257878664,-0.412386146831852,
13.8262006681044));
#433718=CARTESIAN_POINT('Ctrl Pts',(-2.64853126693574,-0.411318662900615,
13.8288634856214));
#433719=CARTESIAN_POINT('Ctrl Pts',(-2.64713116732489,-0.410094068861876,
13.8314912288862));
#433720=CARTESIAN_POINT('Ctrl Pts',(-2.64568780903969,-0.408831638718954,
13.8342001611531));
#433721=CARTESIAN_POINT('Ctrl Pts',(-2.64429694613649,-0.407401211832304,
13.8368750301949));
#433722=CARTESIAN_POINT('Ctrl Pts',(-2.64296770426095,-0.405773530919453,
13.8394886372969));
#433723=CARTESIAN_POINT('Ctrl Pts',(-2.64286504368661,-0.405647821174351,
13.8396904925131));
#433724=CARTESIAN_POINT('Ctrl Pts',(-2.64276276515684,-0.405520918083497,
13.8398919674349));
#433725=CARTESIAN_POINT('Ctrl Pts',(-2.64266088109114,-0.405392800201788,
13.8400930404591));
#433726=CARTESIAN_POINT('Ctrl Pts',(-2.64107345880321,-0.403396637411273,
13.8432258934518));
#433727=CARTESIAN_POINT('Ctrl Pts',(-2.63958901469215,-0.401116461417161,
13.8462331177034));
#433728=CARTESIAN_POINT('Ctrl Pts',(-2.63833680712334,-0.398574008230136,
13.8489036603661));
#433729=CARTESIAN_POINT('Ctrl Pts',(-2.63792707023415,-0.397742087959324,
13.849777493004));
#433730=CARTESIAN_POINT('Ctrl Pts',(-2.6375424135319,-0.396882213434789,
13.85061494757));
#433731=CARTESIAN_POINT('Ctrl Pts',(-2.63718797393439,-0.395995519407907,
13.8514076489583));
#433732=CARTESIAN_POINT('Ctrl Pts',(-2.63643828306783,-0.394120033660651,
13.8530843267192));
#433733=CARTESIAN_POINT('Ctrl Pts',(-2.63575288580402,-0.391939241901277,
13.8546805203176));
#433734=CARTESIAN_POINT('Ctrl Pts',(-2.63530173060524,-0.389538806144157,
13.8559412814273));
#433735=CARTESIAN_POINT('Ctrl Pts',(-2.63524135140833,-0.389217549991856,
13.8561100121513));
#433736=CARTESIAN_POINT('Ctrl Pts',(-2.6351851194351,-0.388892419497718,
13.8562727473908));
#433737=CARTESIAN_POINT('Ctrl Pts',(-2.63513338736153,-0.388563672539864,
13.8564289040185));
#433738=CARTESIAN_POINT('Ctrl Pts',(-2.63489878299806,-0.387072808836557,
13.8571370725437));
#433739=CARTESIAN_POINT('Ctrl Pts',(-2.63475484918487,-0.385481009415416,
13.8577210840554));
#433740=CARTESIAN_POINT('Ctrl Pts',(-2.63473640945108,-0.383847504874734,
13.8581177131616));
#433741=CARTESIAN_POINT('Ctrl Pts',(-2.63473121618737,-0.383387453772568,
13.8582294175695));
#433742=CARTESIAN_POINT('Ctrl Pts',(-2.63473580309041,-0.382924131467699,
13.8583265086086));
#433743=CARTESIAN_POINT('Ctrl Pts',(-2.63475051334241,-0.382458926246567,
13.8584082369006));
#433744=CARTESIAN_POINT('Ctrl Pts',(-2.63477164802983,-0.381790551093503,
13.8585256585398));
#433745=CARTESIAN_POINT('Ctrl Pts',(-2.63481426525496,-0.381109989969931,
13.8586122832068));
#433746=CARTESIAN_POINT('Ctrl Pts',(-2.63487804608901,-0.380434971235501,
13.8586682984299));
#433747=CARTESIAN_POINT('Ctrl Pts',(-2.63492906443386,-0.379895023160412,
13.8587131050557));
#433748=CARTESIAN_POINT('Ctrl Pts',(-2.63499395418751,-0.379352635547506,
13.8587357943552));
#433749=CARTESIAN_POINT('Ctrl Pts',(-2.63507322592065,-0.378807804107057,
13.8587355499465));
#433750=CARTESIAN_POINT('Ctrl Pts',(-2.63512446113171,-0.378455666557732,
13.8587353919793));
#433751=CARTESIAN_POINT('Ctrl Pts',(-2.63518111187177,-0.378106310537414,
13.8587257282814));
#433752=CARTESIAN_POINT('Ctrl Pts',(-2.63524304023065,-0.377759690177983,
13.8587068136939));
#433753=CARTESIAN_POINT('Ctrl Pts',(-2.63524304023065,-0.377759690177983,
13.8587068136939));
#433754=CARTESIAN_POINT('Ctrl Pts',(-2.63544671922696,-0.376619674711952,
13.8586446046466));
#433755=CARTESIAN_POINT('Ctrl Pts',(-2.63570741683485,-0.375509214094161,
13.858482427929));
#433756=CARTESIAN_POINT('Ctrl Pts',(-2.6360208610235,-0.374426990861144,
13.8582284286032));
#433757=CARTESIAN_POINT('Ctrl Pts',(-2.63634241829973,-0.373316755713468,
13.8579678548414));
#433758=CARTESIAN_POINT('Ctrl Pts',(-2.63672174470969,-0.372233952740267,
13.857615680862));
#433759=CARTESIAN_POINT('Ctrl Pts',(-2.63713474082569,-0.371218067059845,
13.8571944833187));
#433760=CARTESIAN_POINT('Ctrl Pts',(-2.63816541487094,-0.368682820448085,
13.8561433417727));
#433761=CARTESIAN_POINT('Ctrl Pts',(-2.63944955424229,-0.366443939905809,
13.8546163505474));
#433762=CARTESIAN_POINT('Ctrl Pts',(-2.64078434840511,-0.364541746069135,
13.8528973491086));
#433763=CARTESIAN_POINT('Ctrl Pts',(-2.6410281956056,-0.364194243319431,
13.8525833129072));
#433764=CARTESIAN_POINT('Ctrl Pts',(-2.64127366824998,-0.363857851680216,
13.8522628768812));
#433765=CARTESIAN_POINT('Ctrl Pts',(-2.64151947325147,-0.363532647353053,
13.851937733538));
#433766=CARTESIAN_POINT('Ctrl Pts',(-2.64302057029165,-0.361546669647119,
13.8499521282529));
#433767=CARTESIAN_POINT('Ctrl Pts',(-2.64468649643034,-0.35978299909703,
13.847639871647));
#433768=CARTESIAN_POINT('Ctrl Pts',(-2.6463712919281,-0.3582791597414,13.8452109780794));
#433769=CARTESIAN_POINT('Ctrl Pts',(-2.64712931629607,-0.357602551287374,
13.8441181685877));
#433770=CARTESIAN_POINT('Ctrl Pts',(-2.64789089707965,-0.356977872367289,
13.8430021611332));
#433771=CARTESIAN_POINT('Ctrl Pts',(-2.64864253925751,-0.356405237945735,
13.8418824960098));
#433772=CARTESIAN_POINT('Ctrl Pts',(-2.65041380324351,-0.355055810308606,
13.8392439765549));
#433773=CARTESIAN_POINT('Ctrl Pts',(-2.652212257862,-0.353927879837718,
13.8364981347964));
#433774=CARTESIAN_POINT('Ctrl Pts',(-2.65402447734643,-0.35298947290406,
13.8336931113419));
#433775=CARTESIAN_POINT('Ctrl Pts',(-2.65578946403768,-0.352075524145027,
13.8309611966328));
#433776=CARTESIAN_POINT('Ctrl Pts',(-2.65756953562669,-0.351340933731929,
13.8281701127186));
#433777=CARTESIAN_POINT('Ctrl Pts',(-2.65935642543848,-0.350795245194212,
13.8253580685121));
#433778=CARTESIAN_POINT('Ctrl Pts',(-2.65974382507816,-0.350676939330308,
13.8247484142933));
#433779=CARTESIAN_POINT('Ctrl Pts',(-2.66013149484599,-0.35056767806646,
13.8241378483365));
#433780=CARTESIAN_POINT('Ctrl Pts',(-2.66051922500485,-0.35046785139304,
13.8235269408515));
#433781=CARTESIAN_POINT('',(-2.63504841430183,-0.378986432859003,12.5969504640361));
#433782=CARTESIAN_POINT('Origin',(-2.66912282379287,-0.383761728248441,
12.584524458991));
#433783=CARTESIAN_POINT('Origin',(-2.66912282379287,-0.383761728248441,
12.584524458991));
#433784=CARTESIAN_POINT('Ctrl Pts',(-2.65148770642212,-0.413283442897022,
12.5893111709658));
#433785=CARTESIAN_POINT('Ctrl Pts',(-2.6417524603545,-0.407479683894216,
12.5770542771492));
#433786=CARTESIAN_POINT('Ctrl Pts',(-2.64736473026113,-0.392107432876553,
12.5737548217797));
#433787=CARTESIAN_POINT('Ctrl Pts',(-2.67277542232632,-0.425974316036751,
12.5663937883685));
#433788=CARTESIAN_POINT('Ctrl Pts',(-2.66302775760034,-0.420163153533316,
12.5540940315304));
#433789=CARTESIAN_POINT('Ctrl Pts',(-2.66866043523377,-0.404744368302604,
12.5508374392248));
#433790=CARTESIAN_POINT('Ctrl Pts',(-2.69404165918613,-0.438652384241057,
12.5434499600945));
#433791=CARTESIAN_POINT('Ctrl Pts',(-2.68426230133086,-0.432822327578891,
12.5311293540533));
#433792=CARTESIAN_POINT('Ctrl Pts',(-2.68993473174172,-0.417369971842775,
12.5278936106989));
#433793=CARTESIAN_POINT('Ctrl Pts',(-2.71528809948451,-0.451318650538058,
12.5204817579905));
#433794=CARTESIAN_POINT('Ctrl Pts',(-2.70546034049114,-0.445459739079734,
12.5081597038247));
#433795=CARTESIAN_POINT('Ctrl Pts',(-2.71118927666454,-0.429985136169938,
12.5049254088044));
#433796=CARTESIAN_POINT('Ctrl Pts',(-2.70001288567338,-0.442212187377255,
12.5369868989719));
#433797=CARTESIAN_POINT('Ctrl Pts',(-2.70081299700138,-0.442689181123054,
12.5342545179733));
#433798=CARTESIAN_POINT('Ctrl Pts',(-2.701640465217,-0.443037252186933,
12.5314872231885));
#433799=CARTESIAN_POINT('Ctrl Pts',(-2.70247035267223,-0.443185265435587,
12.5287124745063));
#433800=CARTESIAN_POINT('Ctrl Pts',(-2.70321878637129,-0.443318751129947,
12.5262100684184));
#433801=CARTESIAN_POINT('Ctrl Pts',(-2.70396860526476,-0.443288420209528,
12.5237004536639));
#433802=CARTESIAN_POINT('Ctrl Pts',(-2.70473000481237,-0.443027515437006,
12.5212220730815));
#433803=CARTESIAN_POINT('Ctrl Pts',(-2.70531292203238,-0.442827770263577,
12.5193246583486));
#433804=CARTESIAN_POINT('Ctrl Pts',(-2.70590938791894,-0.442489892964446,
12.517417831369));
#433805=CARTESIAN_POINT('Ctrl Pts',(-2.70648911402888,-0.441921489638494,
12.5155812248347));
#433806=CARTESIAN_POINT('Ctrl Pts',(-2.70673608046776,-0.441679346766459,
12.5147988205793));
#433807=CARTESIAN_POINT('Ctrl Pts',(-2.70698045361195,-0.441395319896029,
12.5140295443047));
#433808=CARTESIAN_POINT('Ctrl Pts',(-2.70722197818642,-0.441062681003598,
12.5132817086137));
#433809=CARTESIAN_POINT('Ctrl Pts',(-2.70758749295719,-0.440559277038272,
12.5121499604604));
#433810=CARTESIAN_POINT('Ctrl Pts',(-2.70794858964725,-0.439929465719476,
12.5110494206568));
#433811=CARTESIAN_POINT('Ctrl Pts',(-2.7082806391003,-0.439145313135833,
12.5100666561695));
#433812=CARTESIAN_POINT('Ctrl Pts',(-2.70847130113159,-0.438695054528048,
12.5095023550641));
#433813=CARTESIAN_POINT('Ctrl Pts',(-2.70865398804955,-0.438188452292117,
12.5089719619137));
#433814=CARTESIAN_POINT('Ctrl Pts',(-2.70881926733513,-0.437632835477477,
12.5085043804652));
#433815=CARTESIAN_POINT('Ctrl Pts',(-2.70906113204043,-0.436819762643432,
12.5078201359221));
#433816=CARTESIAN_POINT('Ctrl Pts',(-2.7092715763757,-0.435877801288408,
12.5072563000949));
#433817=CARTESIAN_POINT('Ctrl Pts',(-2.70942807300513,-0.434868956606923,
12.5068768744332));
#433818=CARTESIAN_POINT('Ctrl Pts',(-2.70954091784821,-0.434141510142467,
12.5066032824114));
#433819=CARTESIAN_POINT('Ctrl Pts',(-2.70962775496767,-0.433366517410012,
12.5064197834844));
#433820=CARTESIAN_POINT('Ctrl Pts',(-2.70968630393582,-0.4325875438446,
12.5063282718343));
#433821=CARTESIAN_POINT('Ctrl Pts',(-2.70977176730302,-0.43145048360322,
12.5061946931565));
#433822=CARTESIAN_POINT('Ctrl Pts',(-2.70979984309925,-0.430280717716541,
12.5062515701262));
#433823=CARTESIAN_POINT('Ctrl Pts',(-2.7097842489696,-0.429151214975581,
12.5064436508398));
#433824=CARTESIAN_POINT('',(-2.64736473026113,-0.392107432876553,12.5737548217797));
#433825=CARTESIAN_POINT('Origin',(-2.66275320456912,-0.394386656093445,
12.5893111709658));
#433826=CARTESIAN_POINT('Ctrl Pts',(-2.7097842489696,-0.42915121497558,
12.5064436508398));
#433827=CARTESIAN_POINT('Ctrl Pts',(-2.70054478370098,-0.423667359643695,
12.5164271754438));
#433828=CARTESIAN_POINT('Ctrl Pts',(-2.69130154927055,-0.418181510184859,
12.5264061185523));
#433829=CARTESIAN_POINT('Ctrl Pts',(-2.68205441341468,-0.412693595553663,
12.536380305637));
#433830=CARTESIAN_POINT('Ctrl Pts',(-2.67049736911609,-0.405834815333688,
12.5488460165097));
#433831=CARTESIAN_POINT('Ctrl Pts',(-2.6589342273919,-0.398972807323734,
12.5613043021964));
#433832=CARTESIAN_POINT('Ctrl Pts',(-2.64736473026113,-0.392107432876553,
12.5737548217797));
#433833=CARTESIAN_POINT('Ctrl Pts',(-2.66051922500485,-0.35046785139304,
12.5893111709658));
#433834=CARTESIAN_POINT('Ctrl Pts',(-2.64954321694341,-0.353293781610674,
12.5770542771492));
#433835=CARTESIAN_POINT('Ctrl Pts',(-2.65059728690124,-0.36962450760124,
12.5737548217797));
#433836=CARTESIAN_POINT('Ctrl Pts',(-2.6502787049478,-0.353104419707449,
12.5928319619712));
#433837=CARTESIAN_POINT('Ctrl Pts',(-2.64371441229884,-0.358158475345272,
12.5821634970843));
#433838=CARTESIAN_POINT('Ctrl Pts',(-2.64686455989743,-0.37057580486522,
12.5773203894503));
#433839=CARTESIAN_POINT('Ctrl Pts',(-2.63727749621991,-0.363666269495877,
12.5969440695591));
#433840=CARTESIAN_POINT('Ctrl Pts',(-2.6366873411962,-0.367642481210552,
12.5878292599214));
#433841=CARTESIAN_POINT('Ctrl Pts',(-2.64223195386749,-0.374341851661124,
12.5813877129824));
#433842=CARTESIAN_POINT('Ctrl Pts',(-2.63286972343275,-0.393944096112038,
12.596957478804));
#433843=CARTESIAN_POINT('Ctrl Pts',(-2.63345559634244,-0.389997281436558,
12.5878468778671));
#433844=CARTESIAN_POINT('Ctrl Pts',(-2.64066025378196,-0.385179564849123,
12.5814011370086));
#433845=CARTESIAN_POINT('Ctrl Pts',(-2.64239161815869,-0.407860723863328,
12.5928371701607));
#433846=CARTESIAN_POINT('Ctrl Pts',(-2.63752551142403,-0.401163256360554,
12.5821692192952));
#433847=CARTESIAN_POINT('Ctrl Pts',(-2.64404048991929,-0.390136975157249,
12.5773318885715));
#433848=CARTESIAN_POINT('Ctrl Pts',(-2.65148770642209,-0.413283442897068,
12.5893111709658));
#433849=CARTESIAN_POINT('Ctrl Pts',(-2.64175246035447,-0.407479683894262,
12.5770542771492));
#433850=CARTESIAN_POINT('Ctrl Pts',(-2.6473647302611,-0.3921074328766,12.5737548217797));
#433851=CARTESIAN_POINT('',(-2.65059728690124,-0.36962450760124,12.5737548217797));
#433852=CARTESIAN_POINT('Origin',(-2.6660045512589,-0.371773043152011,12.5893111709658));
#433853=CARTESIAN_POINT('Ctrl Pts',(-2.6473647302611,-0.3921074328766,12.5737548217797));
#433854=CARTESIAN_POINT('Ctrl Pts',(-2.64648765276873,-0.391622608471913,
12.5746934679442));
#433855=CARTESIAN_POINT('Ctrl Pts',(-2.6456057291367,-0.390925797058764,
12.5756680099006));
#433856=CARTESIAN_POINT('Ctrl Pts',(-2.64481723279475,-0.390098888849399,
12.5765688348656));
#433857=CARTESIAN_POINT('Ctrl Pts',(-2.64460848711716,-0.389879974055145,
12.5768073183026));
#433858=CARTESIAN_POINT('Ctrl Pts',(-2.64440615217106,-0.389652158560094,
12.5770407398754));
#433859=CARTESIAN_POINT('Ctrl Pts',(-2.64421164066685,-0.389417347108852,
12.5772674179684));
#433860=CARTESIAN_POINT('Ctrl Pts',(-2.64341341805172,-0.388453744408658,
12.5781976435658));
#433861=CARTESIAN_POINT('Ctrl Pts',(-2.64271029640937,-0.3873103995618,
12.5790594849312));
#433862=CARTESIAN_POINT('Ctrl Pts',(-2.64219088513729,-0.386039217177518,
12.5797571720115));
#433863=CARTESIAN_POINT('Ctrl Pts',(-2.64185247001716,-0.385210996146513,
12.580211740231));
#433864=CARTESIAN_POINT('Ctrl Pts',(-2.64159403867823,-0.384283768977268,
12.5806009430798));
#433865=CARTESIAN_POINT('Ctrl Pts',(-2.64145084978923,-0.383318051831108,
12.5808812374708));
#433866=CARTESIAN_POINT('Ctrl Pts',(-2.64132780303116,-0.38248818042923,
12.5811221033394));
#433867=CARTESIAN_POINT('Ctrl Pts',(-2.64128745098348,-0.381612879643817,
12.581287365893));
#433868=CARTESIAN_POINT('Ctrl Pts',(-2.64134040031586,-0.380741168882355,
12.581359338449));
#433869=CARTESIAN_POINT('Ctrl Pts',(-2.6413477591797,-0.380620019086649,
12.5813693411482));
#433870=CARTESIAN_POINT('Ctrl Pts',(-2.64135686504362,-0.380498915290669,
12.5813775999465));
#433871=CARTESIAN_POINT('Ctrl Pts',(-2.64136769032387,-0.380377964172472,
12.5813841266931));
#433872=CARTESIAN_POINT('Ctrl Pts',(-2.64138605672111,-0.380172755971718,
12.5813952001081));
#433873=CARTESIAN_POINT('Ctrl Pts',(-2.64141010195379,-0.379966667148885,
12.5814007534795));
#433874=CARTESIAN_POINT('Ctrl Pts',(-2.64144001143049,-0.37975981031663,
12.5814005856065));
#433875=CARTESIAN_POINT('Ctrl Pts',(-2.64157692532093,-0.378812900614344,
12.5813998171494));
#433876=CARTESIAN_POINT('Ctrl Pts',(-2.6418269278145,-0.377915273545959,
12.58127954464));
#433877=CARTESIAN_POINT('Ctrl Pts',(-2.642160095108,-0.37706408633878,12.5810700125799));
#433878=CARTESIAN_POINT('Ctrl Pts',(-2.64256252326442,-0.37603594910793,
12.5808169217085));
#433879=CARTESIAN_POINT('Ctrl Pts',(-2.64310190902808,-0.375081574256301,
12.5804173076348));
#433880=CARTESIAN_POINT('Ctrl Pts',(-2.64370830958714,-0.37427178803166,
12.5799304713245));
#433881=CARTESIAN_POINT('Ctrl Pts',(-2.6444598309157,-0.37326820779036,
12.5793271277669));
#433882=CARTESIAN_POINT('Ctrl Pts',(-2.64533512402048,-0.372405146501036,
12.5785808224116));
#433883=CARTESIAN_POINT('Ctrl Pts',(-2.64627502476683,-0.37169639940228,
12.5777485681082));
#433884=CARTESIAN_POINT('Ctrl Pts',(-2.64767557985272,-0.37064028857609,
12.576508418016));
#433885=CARTESIAN_POINT('Ctrl Pts',(-2.6492036608637,-0.36993022665298,
12.5750928681475));
#433886=CARTESIAN_POINT('Ctrl Pts',(-2.65059728690124,-0.36962450760124,
12.5737548217797));
#433887=CARTESIAN_POINT('Ctrl Pts',(-2.65059728690124,-0.36962450760124,
12.5737548217797));
#433888=CARTESIAN_POINT('Ctrl Pts',(-2.64954321694341,-0.353293781610674,
12.5770542771492));
#433889=CARTESIAN_POINT('Ctrl Pts',(-2.66051922500485,-0.350467851393039,
12.5893111709658));
#433890=CARTESIAN_POINT('Ctrl Pts',(-2.6745869977036,-0.363500070501432,
12.5508408821982));
#433891=CARTESIAN_POINT('Ctrl Pts',(-2.67352645459423,-0.347118954149279,
12.55409748406));
#433892=CARTESIAN_POINT('Ctrl Pts',(-2.68451646523087,-0.34428941876845,
12.5663972313419));
#433893=CARTESIAN_POINT('Ctrl Pts',(-2.6985529818157,-0.357380473347283,
12.52790050457));
#433894=CARTESIAN_POINT('Ctrl Pts',(-2.69746375863649,-0.340955952952226,
12.5311362602938));
#433895=CARTESIAN_POINT('Ctrl Pts',(-2.70848949618474,-0.338117219167138,
12.5434568539655));
#433896=CARTESIAN_POINT('Ctrl Pts',(-2.72249707968045,-0.351265326595135,
12.5049357605811));
#433897=CARTESIAN_POINT('Ctrl Pts',(-2.72135991741408,-0.334803545191858,
12.5081700652078));
#433898=CARTESIAN_POINT('Ctrl Pts',(-2.73244021394163,-0.331950764417438,
12.5204921097672));
#433899=CARTESIAN_POINT('Ctrl Pts',(-2.72092481596393,-0.35166686956375,
12.5064436508395));
#433900=CARTESIAN_POINT('Ctrl Pts',(-2.72128471078529,-0.35050096926435,
12.5062361689309));
#433901=CARTESIAN_POINT('Ctrl Pts',(-2.72160925536991,-0.349273181647114,
12.5061871075061));
#433902=CARTESIAN_POINT('Ctrl Pts',(-2.7218561031364,-0.348068987800056,
12.5063648335164));
#433903=CARTESIAN_POINT('Ctrl Pts',(-2.72196823661814,-0.347521968676965,
12.5064455676329));
#433904=CARTESIAN_POINT('Ctrl Pts',(-2.72206568527824,-0.34697214419377,
12.506574497099));
#433905=CARTESIAN_POINT('Ctrl Pts',(-2.72214323598872,-0.346442905767576,
12.5067492519495));
#433906=CARTESIAN_POINT('Ctrl Pts',(-2.72229907715176,-0.345379380606543,
12.5071004286051));
#433907=CARTESIAN_POINT('Ctrl Pts',(-2.72237949557313,-0.344359767812568,
12.5076537929613));
#433908=CARTESIAN_POINT('Ctrl Pts',(-2.7223878845934,-0.343461338365866,
12.5083435010505));
#433909=CARTESIAN_POINT('Ctrl Pts',(-2.72238841273236,-0.34340477686315,
12.5083869222964));
#433910=CARTESIAN_POINT('Ctrl Pts',(-2.72238864350928,-0.343348689385558,
12.5084308732337));
#433911=CARTESIAN_POINT('Ctrl Pts',(-2.72238857311952,-0.343293092307382,
12.5084753333615));
#433912=CARTESIAN_POINT('Ctrl Pts',(-2.7223880085008,-0.342847130358932,
12.5088319622689));
#433913=CARTESIAN_POINT('Ctrl Pts',(-2.72236934496448,-0.342423666084951,
12.509227847131));
#433914=CARTESIAN_POINT('Ctrl Pts',(-2.72233593481234,-0.342035167997174,
12.5096423454524));
#433915=CARTESIAN_POINT('Ctrl Pts',(-2.72223124218224,-0.340817786932132,
12.5109411997424));
#433916=CARTESIAN_POINT('Ctrl Pts',(-2.72198494364145,-0.339868040061396,
12.5124831113042));
#433917=CARTESIAN_POINT('Ctrl Pts',(-2.72167138001856,-0.339127367171464,
12.5140723025008));
#433918=CARTESIAN_POINT('Ctrl Pts',(-2.72164199876366,-0.339057965310441,
12.5142212114565));
#433919=CARTESIAN_POINT('Ctrl Pts',(-2.72161204226112,-0.338990373768649,
12.5143705582413));
#433920=CARTESIAN_POINT('Ctrl Pts',(-2.7215815817509,-0.338924530702661,
12.5145201959299));
#433921=CARTESIAN_POINT('Ctrl Pts',(-2.72119027114618,-0.338078678489976,
12.5164425148273));
#433922=CARTESIAN_POINT('Ctrl Pts',(-2.72071212114258,-0.337487890580984,
12.518463520594));
#433923=CARTESIAN_POINT('Ctrl Pts',(-2.72017862832111,-0.337067633290473,
12.5205025929157));
#433924=CARTESIAN_POINT('Ctrl Pts',(-2.71986918133898,-0.336823867404533,
12.5216853356836));
#433925=CARTESIAN_POINT('Ctrl Pts',(-2.71954197270307,-0.336637536346651,
12.5228750347131));
#433926=CARTESIAN_POINT('Ctrl Pts',(-2.71920857069333,-0.336494529534027,
12.5240609649613));
#433927=CARTESIAN_POINT('Ctrl Pts',(-2.71839025334684,-0.336143526984493,
12.5269717671327));
#433928=CARTESIAN_POINT('Ctrl Pts',(-2.717507496463,-0.33605319829466,12.5299036066169));
#433929=CARTESIAN_POINT('Ctrl Pts',(-2.71658286729487,-0.336139876017347,
12.5328133004019));
#433930=CARTESIAN_POINT('Ctrl Pts',(-2.71613899145463,-0.336181486371329,
12.5342101228451));
#433931=CARTESIAN_POINT('Ctrl Pts',(-2.71568606864433,-0.336264358770682,
12.5356023438238));
#433932=CARTESIAN_POINT('Ctrl Pts',(-2.71522896268844,-0.336382047150414,
12.5369868989719));
#433933=CARTESIAN_POINT('Origin',(-15.0568630004311,2.84661798304233,-1.24021445932235));
#433934=CARTESIAN_POINT('Ctrl Pts',(-2.69997696638848,-0.442190819974361,
12.5369868989719));
#433935=CARTESIAN_POINT('Ctrl Pts',(-2.71316717411687,-0.450020361708556,
12.5369868989719));
#433936=CARTESIAN_POINT('Ctrl Pts',(-2.71038156804597,-0.46510425054743,
12.5369868989719));
#433937=CARTESIAN_POINT('Ctrl Pts',(-2.70443573866972,-0.444837568228778,
12.5218025310016));
#433938=CARTESIAN_POINT('Ctrl Pts',(-2.71249659261995,-0.453479240364314,
12.5216901060418));
#433939=CARTESIAN_POINT('Ctrl Pts',(-2.71039007571397,-0.465058272850304,
12.5161920673678));
#433940=CARTESIAN_POINT('Ctrl Pts',(-2.70995859330271,-0.442422170145969,
12.5042015548894));
#433941=CARTESIAN_POINT('Ctrl Pts',(-2.71339584088752,-0.447859326945022,
12.4980677368514));
#433942=CARTESIAN_POINT('Ctrl Pts',(-2.71228302125259,-0.454563982952899,
12.4907278922777));
#433943=CARTESIAN_POINT('Ctrl Pts',(-2.70976449409411,-0.429148086365825,
12.506463626192));
#433944=CARTESIAN_POINT('Ctrl Pts',(-2.71622669490464,-0.430171511507603,
12.4999376786891));
#433945=CARTESIAN_POINT('Ctrl Pts',(-2.71614776851777,-0.430159011857555,
12.4906970594712));
#433946=CARTESIAN_POINT('Origin',(-2.68874738752638,-0.461108974180832,
12.5369868989719));
#433947=CARTESIAN_POINT('Origin',(-2.68874738752638,-0.461108974180832,
14.));
#433948=CARTESIAN_POINT('Origin',(-2.68874738752638,-0.461108974180832,
13.7435492065112));
#433949=CARTESIAN_POINT('Ctrl Pts',(-2.67874530785786,-0.429533351359827,
13.793642941384));
#433950=CARTESIAN_POINT('Ctrl Pts',(-2.68804640273655,-0.435046594784841,
13.8071662555867));
#433951=CARTESIAN_POINT('Ctrl Pts',(-2.68161100476447,-0.450813808761179,
13.8103758687955));
#433952=CARTESIAN_POINT('Ctrl Pts',(-2.6930219368263,-0.438044495261849,
13.7804579775006));
#433953=CARTESIAN_POINT('Ctrl Pts',(-2.70449347638579,-0.444856062766058,
13.7901904343352));
#433954=CARTESIAN_POINT('Ctrl Pts',(-2.70097811382212,-0.460215038975772,
13.7927914348262));
#433955=CARTESIAN_POINT('Ctrl Pts',(-2.70142712557053,-0.443055326020003,
13.7597120340895));
#433956=CARTESIAN_POINT('Ctrl Pts',(-2.71470000174282,-0.450943155131201,
13.7635825532445));
#433957=CARTESIAN_POINT('Ctrl Pts',(-2.71238771299,-0.465781929907696,13.7651073818884));
#433958=CARTESIAN_POINT('Ctrl Pts',(-2.69978119715705,-0.442074090623276,
13.7381884353898));
#433959=CARTESIAN_POINT('Ctrl Pts',(-2.7127438561261,-0.449776517713384,
13.7368803041982));
#433960=CARTESIAN_POINT('Ctrl Pts',(-2.71015315771698,-0.464692211424101,
13.7363986145813));
#433961=CARTESIAN_POINT('Origin',(-2.67094402177385,-0.450495329333152,
13.7902182540695));
#433962=CARTESIAN_POINT('Ctrl Pts',(-2.65148432505612,-0.41328142794726,
13.8235227101244));
#433963=CARTESIAN_POINT('Ctrl Pts',(-2.66136194626255,-0.419164903758537,
13.8358800583119));
#433964=CARTESIAN_POINT('Ctrl Pts',(-2.65557424054822,-0.434693216983779,
13.8390832900376));
#433965=CARTESIAN_POINT('Ctrl Pts',(-2.66172945797254,-0.419389160817917,
13.8124254819052));
#433966=CARTESIAN_POINT('Ctrl Pts',(-2.671626261237,-0.425284062494811,
13.8247886449158));
#433967=CARTESIAN_POINT('Ctrl Pts',(-2.66581527150809,-0.440826043690033,
13.8279860620657));
#433968=CARTESIAN_POINT('Ctrl Pts',(-2.67196999935371,-0.4254941564014,
13.8013225099955));
#433969=CARTESIAN_POINT('Ctrl Pts',(-2.68188131600011,-0.43139770077468,
13.8136962257787));
#433970=CARTESIAN_POINT('Ctrl Pts',(-2.67605170063459,-0.446955798652356,
13.8168830918626));
#433971=CARTESIAN_POINT('Ctrl Pts',(-2.68220612784919,-0.431596521201332,
13.7902140179785));
#433972=CARTESIAN_POINT('Ctrl Pts',(-2.69212759433233,-0.437506107004801,
13.802602731458));
#433973=CARTESIAN_POINT('Ctrl Pts',(-2.6862837096904,-0.45308260098815,
13.8057746032558));
#433974=CARTESIAN_POINT('Origin',(-2.64022220827511,-0.432180229700599,
13.8235269408515));
#433975=CARTESIAN_POINT('Ctrl Pts',(-2.66051922500485,-0.35046785139304,
13.8235269408515));
#433976=CARTESIAN_POINT('Ctrl Pts',(-2.67195380032408,-0.347523856477988,
13.8362179249168));
#433977=CARTESIAN_POINT('Ctrl Pts',(-2.67042675019419,-0.330514120384856,
13.8391868794938));
#433978=CARTESIAN_POINT('Ctrl Pts',(-2.65005708630518,-0.353161478595842,
13.8400110824519));
#433979=CARTESIAN_POINT('Ctrl Pts',(-2.65837185055042,-0.347488158720583,
13.8494522556836));
#433980=CARTESIAN_POINT('Ctrl Pts',(-2.65323703773573,-0.335055878769023,
13.85569149686));
#433981=CARTESIAN_POINT('Ctrl Pts',(-2.63732583736909,-0.363325780174028,
13.8586819406588));
#433982=CARTESIAN_POINT('Ctrl Pts',(-2.63795921881506,-0.359018243571877,
13.868010383617));
#433983=CARTESIAN_POINT('Ctrl Pts',(-2.63219400367951,-0.352042918401439,
13.8744918421245));
#433984=CARTESIAN_POINT('Ctrl Pts',(-2.63282061411247,-0.394289863582954,
13.8587686893867));
#433985=CARTESIAN_POINT('Ctrl Pts',(-2.63219281404613,-0.398559054957974,
13.8680909899357));
#433986=CARTESIAN_POINT('Ctrl Pts',(-2.62469667610912,-0.403589394661724,
13.8745789365163));
#433987=CARTESIAN_POINT('Ctrl Pts',(-2.64219314042693,-0.407742399494244,
13.8400379222776));
#433988=CARTESIAN_POINT('Ctrl Pts',(-2.64856557525381,-0.41553100067065,
13.8494748685453));
#433989=CARTESIAN_POINT('Ctrl Pts',(-2.64014094388412,-0.426008915136298,
13.8557104837033));
#433990=CARTESIAN_POINT('Ctrl Pts',(-2.65148770641861,-0.413283442902624,
13.8235269408542));
#433991=CARTESIAN_POINT('Ctrl Pts',(-2.66162968187889,-0.419329677479087,
13.8362179249195));
#433992=CARTESIAN_POINT('Ctrl Pts',(-2.65537229156814,-0.43522018000592,
13.8391868794965));
#433993=CARTESIAN_POINT('Origin',(-2.65503389875079,-0.329162659634068,
13.8235269408515));
#433994=CARTESIAN_POINT('Ctrl Pts',(-2.69515273048745,-0.341550959409045,
13.7902140241682));
#433995=CARTESIAN_POINT('Ctrl Pts',(-2.70633722451106,-0.338675948308463,
13.8026027327198));
#433996=CARTESIAN_POINT('Ctrl Pts',(-2.70511846421998,-0.322084005817412,
13.8057746032556));
#433997=CARTESIAN_POINT('Ctrl Pts',(-2.68361200227733,-0.344522284904809,
13.8013225161808));
#433998=CARTESIAN_POINT('Ctrl Pts',(-2.69478505554331,-0.341650210985101,
13.8136962270464));
#433999=CARTESIAN_POINT('Ctrl Pts',(-2.69357480373718,-0.325079939536543,
13.8168830918628));
#434000=CARTESIAN_POINT('Ctrl Pts',(-2.67206629875538,-0.347494891365753,
13.8124254880875));
#434001=CARTESIAN_POINT('Ctrl Pts',(-2.68322299161573,-0.344627021169827,
13.8247886461867));
#434002=CARTESIAN_POINT('Ctrl Pts',(-2.68202607037744,-0.328077461002025,
13.8279860620656));
#434003=CARTESIAN_POINT('Ctrl Pts',(-2.66051541850163,-0.350468830650333,
13.8235227163065));
#434004=CARTESIAN_POINT('Ctrl Pts',(-2.67165048728972,-0.347606519290379,
13.8358800595847));
#434005=CARTESIAN_POINT('Ctrl Pts',(-2.67047205618014,-0.33107663329809,
13.8390832900376));
#434006=CARTESIAN_POINT('Origin',(-2.6896712227878,-0.32024478529339,13.7902182540695));
#434007=CARTESIAN_POINT('Ctrl Pts',(-2.7149676186762,-0.33644930541918,
13.7382347919292));
#434008=CARTESIAN_POINT('Ctrl Pts',(-2.72958732243381,-0.332710036670744,
13.7369371795943));
#434009=CARTESIAN_POINT('Ctrl Pts',(-2.7312968939767,-0.317656095586762,
13.7364597369711));
#434010=CARTESIAN_POINT('Ctrl Pts',(-2.71679943782014,-0.335977677803303,
13.7595490285573));
#434011=CARTESIAN_POINT('Ctrl Pts',(-2.73176770604075,-0.332148219239129,
13.7633824266926));
#434012=CARTESIAN_POINT('Ctrl Pts',(-2.73371797887451,-0.317245531690206,
13.7648920890506));
#434013=CARTESIAN_POINT('Ctrl Pts',(-2.70745726054319,-0.338382952814148,
13.7803806590111));
#434014=CARTESIAN_POINT('Ctrl Pts',(-2.72040561484516,-0.3350758382297,
13.7901039518744));
#434015=CARTESIAN_POINT('Ctrl Pts',(-2.72137564442225,-0.319342291774907,
13.7926933640892));
#434016=CARTESIAN_POINT('Ctrl Pts',(-2.6912184709803,-0.342563857633278,
13.7936647693663));
#434017=CARTESIAN_POINT('Ctrl Pts',(-2.70169975050101,-0.33989625354848,
13.8072068914933));
#434018=CARTESIAN_POINT('Ctrl Pts',(-2.69995480263794,-0.322937496907673,
13.8104111085397));
#434019=CARTESIAN_POINT('Origin',(-2.70974363643439,-0.315076855391442,
13.7435492065112));
#434020=CARTESIAN_POINT('Origin',(-2.70974363643439,-0.315076855391442,
14.));
#434021=CARTESIAN_POINT('Origin',(-2.70974363643439,-0.315076855391443,
12.5369868989719));
#434022=CARTESIAN_POINT('Ctrl Pts',(-2.72090658436879,-0.351664513225318,
12.506462012331));
#434023=CARTESIAN_POINT('Ctrl Pts',(-2.72739127020971,-0.352502628691232,
12.4999388158272));
#434024=CARTESIAN_POINT('Ctrl Pts',(-2.72731454787207,-0.352492712686149,
12.4907030323752));
#434025=CARTESIAN_POINT('Ctrl Pts',(-2.72483052715391,-0.338982586866375,
12.5042014951932));
#434026=CARTESIAN_POINT('Ctrl Pts',(-2.72965888100028,-0.33473663629545,
12.4980716682128));
#434027=CARTESIAN_POINT('Ctrl Pts',(-2.73048103604559,-0.327995002494423,
12.4907355092744));
#434028=CARTESIAN_POINT('Ctrl Pts',(-2.72021405179254,-0.335107815068892,
12.5218047446509));
#434029=CARTESIAN_POINT('Ctrl Pts',(-2.73037746320019,-0.329089182375839,
12.5216906929433));
#434030=CARTESIAN_POINT('Ctrl Pts',(-2.73162154168198,-0.317392044988393,
12.5161988840775));
#434031=CARTESIAN_POINT('Ctrl Pts',(-2.71519175147824,-0.336391593073828,
12.5369868989719));
#434032=CARTESIAN_POINT('Ctrl Pts',(-2.73004414179213,-0.33259527466203,
12.5369868989719));
#434033=CARTESIAN_POINT('Ctrl Pts',(-2.73162617230327,-0.317347235083714,
12.5369868989719));
#434034=CARTESIAN_POINT('Origin',(-5.09942406832773E-31,-5.88504909413694E-31,
12.5));
#434035=CARTESIAN_POINT('Origin',(-2.6231001832877,-0.566158714422425,12.5));
#434036=CARTESIAN_POINT('',(-2.6231001832877,-0.566158714422425,12.5893111709658));
#434037=CARTESIAN_POINT('',(-2.6231001832877,-0.566158714422425,13.8235269408515));
#434038=CARTESIAN_POINT('',(-2.6231001832877,-0.566158714422425,12.5));
#434039=CARTESIAN_POINT('',(-2.65834914403464,-0.560093777039188,13.7902182540695));
#434040=CARTESIAN_POINT('',(-2.6231001832877,-0.566158714422425,13.8235269408515));
#434041=CARTESIAN_POINT('',(-2.6787760026444,-0.556579131053058,13.7435492065112));
#434042=CARTESIAN_POINT('Origin',(-2.61157196305983,-0.568142590928179,
13.7445212918702));
#434043=CARTESIAN_POINT('',(-2.6787760026444,-0.556579131053058,12.5369868989719));
#434044=CARTESIAN_POINT('',(-2.6787760026444,-0.556579131053058,12.5));
#434045=CARTESIAN_POINT('Ctrl Pts',(-2.6787760026444,-0.556579131053058,
12.5369868989719));
#434046=CARTESIAN_POINT('Ctrl Pts',(-2.66023093171095,-0.559769996587692,
12.5544431401645));
#434047=CARTESIAN_POINT('Ctrl Pts',(-2.64167259684988,-0.562963144314164,
12.5718848856037));
#434048=CARTESIAN_POINT('Ctrl Pts',(-2.6231001832877,-0.566158714422425,
12.5893111709658));
#434049=CARTESIAN_POINT('Origin',(-2.83292449524894,-0.787632598180569,
12.5));
#434050=CARTESIAN_POINT('',(-2.65498441696279,-0.660816878682771,13.7435492065112));
#434051=CARTESIAN_POINT('',(-2.63810540102849,-0.648787410275543,13.7902182540695));
#434052=CARTESIAN_POINT('Origin',(-2.59375026443174,-0.617176046410157,
13.7418732680438));
#434053=CARTESIAN_POINT('',(-2.60897866247894,-0.62802913961858,13.8235269408515));
#434054=CARTESIAN_POINT('',(-2.63810540102849,-0.648787410275543,13.7902182540695));
#434055=CARTESIAN_POINT('',(-2.60897866247894,-0.62802913961858,12.5893111709658));
#434056=CARTESIAN_POINT('',(-2.60897866247894,-0.62802913961858,12.5));
#434057=CARTESIAN_POINT('',(-2.65498441696279,-0.660816878682771,12.5369868989719));
#434058=CARTESIAN_POINT('Ctrl Pts',(-2.60897866247894,-0.62802913961858,
12.5893111709658));
#434059=CARTESIAN_POINT('Ctrl Pts',(-2.62432532299308,-0.638966517042117,
12.5718848856037));
#434060=CARTESIAN_POINT('Ctrl Pts',(-2.6396603500679,-0.6498956034556,12.5544431401645));
#434061=CARTESIAN_POINT('Ctrl Pts',(-2.65498441696279,-0.660816878682771,
12.5369868989719));
#434062=CARTESIAN_POINT('',(-2.65498441696279,-0.660816878682771,12.5));
#434063=CARTESIAN_POINT('Origin',(-2.62892909479919,-0.600035910522329,
12.5));
#434064=CARTESIAN_POINT('',(-2.59568356470713,-0.591299498153624,13.8587068136939));
#434065=CARTESIAN_POINT('Ctrl Pts',(-2.60897866247499,-0.628029139623877,
13.8235269408542));
#434066=CARTESIAN_POINT('Ctrl Pts',(-2.60755168099091,-0.62701214735683,
13.8262006681044));
#434067=CARTESIAN_POINT('Ctrl Pts',(-2.60619220811089,-0.625829920001143,
13.8288634856214));
#434068=CARTESIAN_POINT('Ctrl Pts',(-2.60489658299874,-0.624495279581872,
13.8314912288862));
#434069=CARTESIAN_POINT('Ctrl Pts',(-2.60356092714564,-0.62311940297138,
13.8342001611531));
#434070=CARTESIAN_POINT('Ctrl Pts',(-2.60229128529472,-0.621580367473445,
13.8368750301949));
#434071=CARTESIAN_POINT('Ctrl Pts',(-2.60109913746691,-0.619849756981623,
13.8394886372968));
#434072=CARTESIAN_POINT('Ctrl Pts',(-2.60100706499842,-0.619716097735462,
13.8396904925131));
#434073=CARTESIAN_POINT('Ctrl Pts',(-2.60091547057203,-0.619581280254489,
13.8398919674349));
#434074=CARTESIAN_POINT('Ctrl Pts',(-2.6008243683139,-0.619445284177259,
13.8400930404591));
#434075=CARTESIAN_POINT('Ctrl Pts',(-2.59940493384158,-0.61732637380038,
13.8432258934518));
#434076=CARTESIAN_POINT('Ctrl Pts',(-2.59811128460748,-0.614932788927828,
13.8462331177034));
#434077=CARTESIAN_POINT('Ctrl Pts',(-2.59707047719378,-0.612296729002257,
13.8489036603661));
#434078=CARTESIAN_POINT('Ctrl Pts',(-2.59672991289554,-0.611434179517238,
13.8497774930041));
#434079=CARTESIAN_POINT('Ctrl Pts',(-2.59641662386316,-0.610545813062039,
13.85061494757));
#434080=CARTESIAN_POINT('Ctrl Pts',(-2.59613563742903,-0.609633179318732,
13.8514076489583));
#434081=CARTESIAN_POINT('Ctrl Pts',(-2.59554131059654,-0.607702827330148,
13.8530843267192));
#434082=CARTESIAN_POINT('Ctrl Pts',(-2.59503594870946,-0.605473425735505,
13.8546805203176));
#434083=CARTESIAN_POINT('Ctrl Pts',(-2.59478195249114,-0.603044203893294,
13.8559412814273));
#434084=CARTESIAN_POINT('Ctrl Pts',(-2.59474795955984,-0.602719095229282,
13.8561100121513));
#434085=CARTESIAN_POINT('Ctrl Pts',(-2.59471841584751,-0.602390463152217,
13.8562727473908));
#434086=CARTESIAN_POINT('Ctrl Pts',(-2.59469365183714,-0.602058593428518,
13.8564289040185));
#434087=CARTESIAN_POINT('Ctrl Pts',(-2.59458134733266,-0.60055356801762,
13.8571370725437));
#434088=CARTESIAN_POINT('Ctrl Pts',(-2.59456763887773,-0.598955333235754,
13.8577210840553));
#434089=CARTESIAN_POINT('Ctrl Pts',(-2.59468240628542,-0.597325761037194,
13.8581177131616));
#434090=CARTESIAN_POINT('Ctrl Pts',(-2.5947147287376,-0.596866817417908,
13.8582294175695));
#434091=CARTESIAN_POINT('Ctrl Pts',(-2.59475706544722,-0.596405410654961,
13.8583265086086));
#434092=CARTESIAN_POINT('Ctrl Pts',(-2.59480964529635,-0.59594295238792,
13.8584082369006));
#434093=CARTESIAN_POINT('Ctrl Pts',(-2.5948851884397,-0.59527852387127,
13.8585256585398));
#434094=CARTESIAN_POINT('Ctrl Pts',(-2.59498313590912,-0.594603700958181,
13.8586122832068));
#434095=CARTESIAN_POINT('Ctrl Pts',(-2.59510172481113,-0.593936127022992,
13.8586682984299));
#434096=CARTESIAN_POINT('Ctrl Pts',(-2.5951965841774,-0.593402134049317,
13.8587131050557));
#434097=CARTESIAN_POINT('Ctrl Pts',(-2.59530546764148,-0.592866840303779,
13.8587357943552));
#434098=CARTESIAN_POINT('Ctrl Pts',(-2.59542888442484,-0.592330283127177,
13.8587355499465));
#434099=CARTESIAN_POINT('Ctrl Pts',(-2.5955086516343,-0.591983493431892,
13.8587353919793));
#434100=CARTESIAN_POINT('Ctrl Pts',(-2.59559358963261,-0.591639917426194,
13.8587257282814));
#434101=CARTESIAN_POINT('Ctrl Pts',(-2.59568356470713,-0.591299498153624,
13.8587068136939));
#434102=CARTESIAN_POINT('Ctrl Pts',(-2.59568356470713,-0.591299498153624,
13.8587068136939));
#434103=CARTESIAN_POINT('Ctrl Pts',(-2.59597948782226,-0.590179877724025,
13.8586446046466));
#434104=CARTESIAN_POINT('Ctrl Pts',(-2.59632983082974,-0.589094361347527,
13.858482427929));
#434105=CARTESIAN_POINT('Ctrl Pts',(-2.59673044329909,-0.588041287734245,
13.8582284286032));
#434106=CARTESIAN_POINT('Ctrl Pts',(-2.59714142509146,-0.58696095670564,
13.8579678548414));
#434107=CARTESIAN_POINT('Ctrl Pts',(-2.59760774781866,-0.585912675293914,
13.857615680862));
#434108=CARTESIAN_POINT('Ctrl Pts',(-2.59810217383812,-0.584933832906813,
13.8571944833187));
#434109=CARTESIAN_POINT('Ctrl Pts',(-2.59933606453546,-0.582491031621999,
13.8561433417727));
#434110=CARTESIAN_POINT('Ctrl Pts',(-2.60079842058794,-0.580364270050159,
13.8546163505474));
#434111=CARTESIAN_POINT('Ctrl Pts',(-2.6022838197901,-0.578577203722447,
13.8528973491086));
#434112=CARTESIAN_POINT('Ctrl Pts',(-2.6025551803093,-0.578250733070091,
13.8525833129072));
#434113=CARTESIAN_POINT('Ctrl Pts',(-2.6028272552052,-0.577935469045686,
13.8522628768812));
#434114=CARTESIAN_POINT('Ctrl Pts',(-2.60309874948253,-0.577631382198665,
13.851937733538));
#434115=CARTESIAN_POINT('Ctrl Pts',(-2.60475672736609,-0.575774366013995,
13.8499521282529));
#434116=CARTESIAN_POINT('Ctrl Pts',(-2.60656086579594,-0.574152352378175,
13.847639871647));
#434117=CARTESIAN_POINT('Ctrl Pts',(-2.60836263214411,-0.572790843397887,
13.8452109780794));
#434118=CARTESIAN_POINT('Ctrl Pts',(-2.60917328411886,-0.572178272325822,
13.8441181685877));
#434119=CARTESIAN_POINT('Ctrl Pts',(-2.60998324793643,-0.571617747877346,
13.8430021611332));
#434120=CARTESIAN_POINT('Ctrl Pts',(-2.61077906410839,-0.571108284664993,
13.8418824960098));
#434121=CARTESIAN_POINT('Ctrl Pts',(-2.6126544252395,-0.569907721595472,
13.8392439765549));
#434122=CARTESIAN_POINT('Ctrl Pts',(-2.61453883245319,-0.568930134967618,
13.8364981347964));
#434123=CARTESIAN_POINT('Ctrl Pts',(-2.61642151080363,-0.568142563217421,
13.8336931113419));
#434124=CARTESIAN_POINT('Ctrl Pts',(-2.61825511995583,-0.567375518348159,
13.8309611966327));
#434125=CARTESIAN_POINT('Ctrl Pts',(-2.62008914444175,-0.566788464583941,
13.8281701127185));
#434126=CARTESIAN_POINT('Ctrl Pts',(-2.62191456720686,-0.566390239888157,
13.825358068512));
#434127=CARTESIAN_POINT('Ctrl Pts',(-2.62231032083238,-0.566303904344336,
13.8247484142932));
#434128=CARTESIAN_POINT('Ctrl Pts',(-2.62270560646835,-0.566226605323364,
13.8241378483365));
#434129=CARTESIAN_POINT('Ctrl Pts',(-2.6231001832877,-0.566158714422425,
13.8235269408515));
#434130=CARTESIAN_POINT('',(-2.59538959546303,-0.592506295129496,12.5969504640361));
#434131=CARTESIAN_POINT('Origin',(-2.62896139426152,-0.60004308182228,12.584524458991));
#434132=CARTESIAN_POINT('Origin',(-2.62896139426152,-0.60004308182228,12.584524458991));
#434133=CARTESIAN_POINT('Ctrl Pts',(-2.60897866247894,-0.62802913961858,
12.5893111709658));
#434134=CARTESIAN_POINT('Ctrl Pts',(-2.59974886987771,-0.621451179212954,
12.5770542771492));
#434135=CARTESIAN_POINT('Ctrl Pts',(-2.60659544658616,-0.606587530191593,
12.5737548217797));
#434136=CARTESIAN_POINT('Ctrl Pts',(-2.62916112128738,-0.642412931396569,
12.5663937883685));
#434137=CARTESIAN_POINT('Ctrl Pts',(-2.61991955480387,-0.635826579888902,
12.5540940315304));
#434138=CARTESIAN_POINT('Ctrl Pts',(-2.62679026430446,-0.620918214912444,
12.5508374392248));
#434139=CARTESIAN_POINT('Ctrl Pts',(-2.64932321624227,-0.656782210104961,
12.5434499600945));
#434140=CARTESIAN_POINT('Ctrl Pts',(-2.64005160213515,-0.650174444023033,
12.5311293540533));
#434141=CARTESIAN_POINT('Ctrl Pts',(-2.64696466844689,-0.635235860464691,
12.5278936106989));
#434142=CARTESIAN_POINT('Ctrl Pts',(-2.66946654247219,-0.67113811257241,
12.5204817579905));
#434143=CARTESIAN_POINT('Ctrl Pts',(-2.66014904021147,-0.664497642564215,
12.5081597038247));
#434144=CARTESIAN_POINT('Ctrl Pts',(-2.66712023761871,-0.649541491602016,
12.5049254088044));
#434145=CARTESIAN_POINT('Ctrl Pts',(-2.65498441696279,-0.660816878682772,
12.5369868989719));
#434146=CARTESIAN_POINT('Ctrl Pts',(-2.65574298656787,-0.661357501772333,
12.5342545179733));
#434147=CARTESIAN_POINT('Ctrl Pts',(-2.65653933042822,-0.661771860999872,
12.5314872231885));
#434148=CARTESIAN_POINT('Ctrl Pts',(-2.65735439204755,-0.661987025278552,
12.5287124745063));
#434149=CARTESIAN_POINT('Ctrl Pts',(-2.65808945507192,-0.662181071104868,
12.5262100684184));
#434150=CARTESIAN_POINT('Ctrl Pts',(-2.65883925125646,-0.662211958308881,
12.5237004536639));
#434151=CARTESIAN_POINT('Ctrl Pts',(-2.65961938347097,-0.662013982807086,
12.5212220730815));
#434152=CARTESIAN_POINT('Ctrl Pts',(-2.660216642168,-0.661862415434214,
12.5193246583486));
#434153=CARTESIAN_POINT('Ctrl Pts',(-2.66083866350011,-0.661574279900998,
12.517417831369));
#434154=CARTESIAN_POINT('Ctrl Pts',(-2.6614627907671,-0.661055020950102,
12.5155812248347));
#434155=CARTESIAN_POINT('Ctrl Pts',(-2.66172867233754,-0.66083381384599,
12.5147988205793));
#434156=CARTESIAN_POINT('Ctrl Pts',(-2.66199538317697,-0.66057065073144,
12.5140295443047));
#434157=CARTESIAN_POINT('Ctrl Pts',(-2.66226321725615,-0.660258805162506,
12.5132817086137));
#434158=CARTESIAN_POINT('Ctrl Pts',(-2.66266854790322,-0.659786869079438,
12.5121499604604));
#434159=CARTESIAN_POINT('Ctrl Pts',(-2.6630797785432,-0.659188586138715,
12.511049420657));
#434160=CARTESIAN_POINT('Ctrl Pts',(-2.66347463884435,-0.658434107871132,
12.5100666561697));
#434161=CARTESIAN_POINT('Ctrl Pts',(-2.66370136671998,-0.658000888187295,
12.5095023550643));
#434162=CARTESIAN_POINT('Ctrl Pts',(-2.66392473854761,-0.657510862307966,
12.5089719619137));
#434163=CARTESIAN_POINT('Ctrl Pts',(-2.66413475580849,-0.656970566058595,
12.5085043804652));
#434164=CARTESIAN_POINT('Ctrl Pts',(-2.66444208871311,-0.656179912876177,
12.5078201359221));
#434165=CARTESIAN_POINT('Ctrl Pts',(-2.66472861140739,-0.655258238986815,
12.5072563000949));
#434166=CARTESIAN_POINT('Ctrl Pts',(-2.6649668175144,-0.654265507080926,
12.5068768744332));
#434167=CARTESIAN_POINT('Ctrl Pts',(-2.66513858051571,-0.653549679036882,
12.5066032824114));
#434168=CARTESIAN_POINT('Ctrl Pts',(-2.6652882977942,-0.652784343060205,
12.5064197834844));
#434169=CARTESIAN_POINT('Ctrl Pts',(-2.66541014552271,-0.652012733749517,
12.5063282718343));
#434170=CARTESIAN_POINT('Ctrl Pts',(-2.66558800548322,-0.650886423040119,
12.5061946931565));
#434171=CARTESIAN_POINT('Ctrl Pts',(-2.66571133463889,-0.649722837890964,
12.5062515701262));
#434172=CARTESIAN_POINT('Ctrl Pts',(-2.66578785735661,-0.648595822410862,
12.5064436508398));
#434173=CARTESIAN_POINT('',(-2.60659544658616,-0.606587530191593,12.5737548217797));
#434174=CARTESIAN_POINT('Origin',(-2.6217469391639,-0.610113472996979,12.5893111709658));
#434175=CARTESIAN_POINT('Ctrl Pts',(-2.66578785735661,-0.648595822410862,
12.5064436508398));
#434176=CARTESIAN_POINT('Ctrl Pts',(-2.65702612076564,-0.642377111960802,
12.5164271754438));
#434177=CARTESIAN_POINT('Ctrl Pts',(-2.6482607900943,-0.636156106797407,
12.5264061185523));
#434178=CARTESIAN_POINT('Ctrl Pts',(-2.63949173930992,-0.629932725330953,
12.536380305637));
#434179=CARTESIAN_POINT('Ctrl Pts',(-2.62853220438458,-0.622154760735652,
12.5488460165097));
#434180=CARTESIAN_POINT('Ctrl Pts',(-2.61756685541717,-0.614373082093783,
12.5613043021964));
#434181=CARTESIAN_POINT('Ctrl Pts',(-2.60659544658616,-0.606587530191593,
12.5737548217797));
#434182=CARTESIAN_POINT('Ctrl Pts',(-2.6231001832877,-0.566158714422425,
12.5893111709658));
#434183=CARTESIAN_POINT('Ctrl Pts',(-2.61193035744024,-0.568080595037089,
12.5770542771492));
#434184=CARTESIAN_POINT('Ctrl Pts',(-2.61164981429194,-0.584442898371182,
12.5737548217797));
#434185=CARTESIAN_POINT('Ctrl Pts',(-2.61267883292203,-0.567951812320271,
12.5928319619712));
#434186=CARTESIAN_POINT('Ctrl Pts',(-2.6057244299613,-0.572454000214079,
12.5821634970843));
#434187=CARTESIAN_POINT('Ctrl Pts',(-2.60785196807089,-0.585086778368237,
12.5773203894503));
#434188=CARTESIAN_POINT('Ctrl Pts',(-2.59885999583447,-0.577418799216162,
12.5969440695591));
#434189=CARTESIAN_POINT('Ctrl Pts',(-2.59794770633483,-0.581333677301208,
12.5878292599214));
#434190=CARTESIAN_POINT('Ctrl Pts',(-2.60292780887921,-0.588462693555647,
12.5813877129824));
#434191=CARTESIAN_POINT('Ctrl Pts',(-2.5919989655928,-0.607236604460083,
12.596957478804));
#434192=CARTESIAN_POINT('Ctrl Pts',(-2.59290459109521,-0.603350676565965,
12.5878468778671));
#434193=CARTESIAN_POINT('Ctrl Pts',(-2.60047796425882,-0.599136236999139,
12.5814011370086));
#434194=CARTESIAN_POINT('Ctrl Pts',(-2.60035484264215,-0.621883048597696,
12.5928371701607));
#434195=CARTESIAN_POINT('Ctrl Pts',(-2.59605083325396,-0.614811233491929,
12.5821692192952));
#434196=CARTESIAN_POINT('Ctrl Pts',(-2.60344287797678,-0.604352672559195,
12.5773318885715));
#434197=CARTESIAN_POINT('Ctrl Pts',(-2.6089786624789,-0.628029139618622,
12.5893111709658));
#434198=CARTESIAN_POINT('Ctrl Pts',(-2.59974886987767,-0.621451179212996,
12.5770542771492));
#434199=CARTESIAN_POINT('Ctrl Pts',(-2.60659544658613,-0.606587530191637,
12.5737548217797));
#434200=CARTESIAN_POINT('',(-2.61164981429194,-0.584442898371182,12.5737548217797));
#434201=CARTESIAN_POINT('Origin',(-2.62683068665505,-0.587840119926364,
12.5893111709658));
#434202=CARTESIAN_POINT('Ctrl Pts',(-2.60659544658613,-0.606587530191637,
12.5737548217797));
#434203=CARTESIAN_POINT('Ctrl Pts',(-2.60576080518662,-0.60603282904214,
12.5746934679442));
#434204=CARTESIAN_POINT('Ctrl Pts',(-2.60493861268177,-0.605266451248091,
12.5756680099006));
#434205=CARTESIAN_POINT('Ctrl Pts',(-2.60422014069206,-0.60437802473566,
12.5765688348656));
#434206=CARTESIAN_POINT('Ctrl Pts',(-2.60402993318653,-0.604142823651705,
12.5768073183026));
#434207=CARTESIAN_POINT('Ctrl Pts',(-2.60384684057106,-0.603899274017432,
12.5770407398754));
#434208=CARTESIAN_POINT('Ctrl Pts',(-2.603672115601,-0.603649389388578,
12.5772674179684));
#434209=CARTESIAN_POINT('Ctrl Pts',(-2.60295509157148,-0.602623930443406,
12.5781976435658));
#434210=CARTESIAN_POINT('Ctrl Pts',(-2.60234750272771,-0.601427079040893,
12.5790594849312));
#434211=CARTESIAN_POINT('Ctrl Pts',(-2.60193343291919,-0.600117789570475,
12.5797571720116));
#434212=CARTESIAN_POINT('Ctrl Pts',(-2.60166365155031,-0.599264740402644,
12.580211740231));
#434213=CARTESIAN_POINT('Ctrl Pts',(-2.60148165774259,-0.598319533952032,
12.5806009430798));
#434214=CARTESIAN_POINT('Ctrl Pts',(-2.6014176602155,-0.597345358926255,
12.5808812374708));
#434215=CARTESIAN_POINT('Ctrl Pts',(-2.60136266510878,-0.596508219399915,
12.5811221033394));
#434216=CARTESIAN_POINT('Ctrl Pts',(-2.60139379246911,-0.595632542039162,
12.581287365893));
#434217=CARTESIAN_POINT('Ctrl Pts',(-2.60151761813658,-0.594768047685495,
12.581359338449));
#434218=CARTESIAN_POINT('Ctrl Pts',(-2.60153482734746,-0.594647900821458,
12.5813693411482));
#434219=CARTESIAN_POINT('Ctrl Pts',(-2.60155377399602,-0.594527942200814,
12.5813775999465));
#434220=CARTESIAN_POINT('Ctrl Pts',(-2.60157442189503,-0.594408275898322,
12.5813841266931));
#434221=CARTESIAN_POINT('Ctrl Pts',(-2.60160945355302,-0.594205247542808,
12.5813952001081));
#434222=CARTESIAN_POINT('Ctrl Pts',(-2.60165021692947,-0.59400180437322,
12.5814007534795));
#434223=CARTESIAN_POINT('Ctrl Pts',(-2.60169688763704,-0.593798073740026,
12.5814005856065));
#434224=CARTESIAN_POINT('Ctrl Pts',(-2.60191052788922,-0.592865474554778,
12.5813998171494));
#434225=CARTESIAN_POINT('Ctrl Pts',(-2.60223286345935,-0.59199121179055,
12.58127954464));
#434226=CARTESIAN_POINT('Ctrl Pts',(-2.60263430182559,-0.591170013065979,
12.5810700125799));
#434227=CARTESIAN_POINT('Ctrl Pts',(-2.60311919366459,-0.590178098507659,
12.5808169217085));
#434228=CARTESIAN_POINT('Ctrl Pts',(-2.60373457507701,-0.58927086420677,
12.5804173076348));
#434229=CARTESIAN_POINT('Ctrl Pts',(-2.60440496298324,-0.588513199754099,
12.5799304713245));
#434230=CARTESIAN_POINT('Ctrl Pts',(-2.60523578479302,-0.587574214808325,
12.5793271277669));
#434231=CARTESIAN_POINT('Ctrl Pts',(-2.60617851293955,-0.586785369798107,
12.5785808224116));
#434232=CARTESIAN_POINT('Ctrl Pts',(-2.60717305571194,-0.586155591633295,
12.5777485681082));
#434233=CARTESIAN_POINT('Ctrl Pts',(-2.60865503340311,-0.585217153170376,
12.576508418016));
#434234=CARTESIAN_POINT('Ctrl Pts',(-2.61023590648921,-0.584634006708146,
12.5750928681475));
#434235=CARTESIAN_POINT('Ctrl Pts',(-2.61164981429194,-0.584442898371182,
12.5737548217797));
#434236=CARTESIAN_POINT('Ctrl Pts',(-2.61164981429194,-0.584442898371182,
12.5737548217797));
#434237=CARTESIAN_POINT('Ctrl Pts',(-2.61193035744024,-0.568080595037088,
12.5770542771492));
#434238=CARTESIAN_POINT('Ctrl Pts',(-2.6231001832877,-0.566158714422425,
12.5893111709658));
#434239=CARTESIAN_POINT('Ctrl Pts',(-2.63605889979076,-0.580294223970602,
12.5508408821982));
#434240=CARTESIAN_POINT('Ctrl Pts',(-2.63633709860868,-0.563881170322734,
12.55409748406));
#434241=CARTESIAN_POINT('Ctrl Pts',(-2.64752117429318,-0.56195683788064,
12.5663972313419));
#434242=CARTESIAN_POINT('Ctrl Pts',(-2.66044394304741,-0.57614843946563,
12.52790050457));
#434243=CARTESIAN_POINT('Ctrl Pts',(-2.66069709505851,-0.559689788506306,
12.5311362602938));
#434244=CARTESIAN_POINT('Ctrl Pts',(-2.6719175285316,-0.557759200341832,
12.5434568539655));
#434245=CARTESIAN_POINT('Ctrl Pts',(-2.68480681013232,-0.572005306621965,
12.5049357605811));
#434246=CARTESIAN_POINT('Ctrl Pts',(-2.68501521968767,-0.555505611156697,
12.5081700652078));
#434247=CARTESIAN_POINT('Ctrl Pts',(-2.69629117555962,-0.553565469806416,
12.5204921097672));
#434248=CARTESIAN_POINT('Ctrl Pts',(-2.68320704851393,-0.572277359400397,
12.5064436508395));
#434249=CARTESIAN_POINT('Ctrl Pts',(-2.68366077751305,-0.571144673307105,
12.5062361689309));
#434250=CARTESIAN_POINT('Ctrl Pts',(-2.68408431829136,-0.56994742444845,
12.5061871075062));
#434251=CARTESIAN_POINT('Ctrl Pts',(-2.68442849767,-0.568767357841671,12.5063648335164));
#434252=CARTESIAN_POINT('Ctrl Pts',(-2.68458484517365,-0.568231298799345,
12.5064455676329));
#434253=CARTESIAN_POINT('Ctrl Pts',(-2.68472678538106,-0.567691246782228,
12.506574497099));
#434254=CARTESIAN_POINT('Ctrl Pts',(-2.6848472158929,-0.567170090456088,
12.5067492519495));
#434255=CARTESIAN_POINT('Ctrl Pts',(-2.68508922568121,-0.566122806588952,
12.5071004286051));
#434256=CARTESIAN_POINT('Ctrl Pts',(-2.68525248442525,-0.565113141320434,
12.5076537929612));
#434257=CARTESIAN_POINT('Ctrl Pts',(-2.68533407587227,-0.564218385106703,
12.5083435010503));
#434258=CARTESIAN_POINT('Ctrl Pts',(-2.68533921254146,-0.564162054855853,
12.5083869222963));
#434259=CARTESIAN_POINT('Ctrl Pts',(-2.68534401420061,-0.56410617281508,
12.5084308732336));
#434260=CARTESIAN_POINT('Ctrl Pts',(-2.68534847572309,-0.564050754994082,
12.5084753333615));
#434261=CARTESIAN_POINT('Ctrl Pts',(-2.685384263022,-0.563606230925559,
12.508831962269));
#434262=CARTESIAN_POINT('Ctrl Pts',(-2.68540017785663,-0.563182654442561,
12.509227847131));
#434263=CARTESIAN_POINT('Ctrl Pts',(-2.68539854507481,-0.562792725812558,
12.5096423454524));
#434264=CARTESIAN_POINT('Ctrl Pts',(-2.68539342865921,-0.561570862061311,
12.5109411997424));
#434265=CARTESIAN_POINT('Ctrl Pts',(-2.68522536284349,-0.560604199777341,
12.5124831113042));
#434266=CARTESIAN_POINT('Ctrl Pts',(-2.68497321429429,-0.559840433069102,
12.5140723025008));
#434267=CARTESIAN_POINT('Ctrl Pts',(-2.68494958769906,-0.559768867292009,
12.5142212114565));
#434268=CARTESIAN_POINT('Ctrl Pts',(-2.68492524021245,-0.559699058922436,
12.5143705582413));
#434269=CARTESIAN_POINT('Ctrl Pts',(-2.6849002478782,-0.559630952129454,
12.5145201959299));
#434270=CARTESIAN_POINT('Ctrl Pts',(-2.68457918413508,-0.558756018973192,
12.5164425148273));
#434271=CARTESIAN_POINT('Ctrl Pts',(-2.68415077983536,-0.558128223198006,
12.5184635205941));
#434272=CARTESIAN_POINT('Ctrl Pts',(-2.6836533170379,-0.557665879661304,
12.5205025929158));
#434273=CARTESIAN_POINT('Ctrl Pts',(-2.68336476889779,-0.557397702084433,
12.5216853356836));
#434274=CARTESIAN_POINT('Ctrl Pts',(-2.68305383673265,-0.557185320486293,
12.5228750347131));
#434275=CARTESIAN_POINT('Ctrl Pts',(-2.68273320047344,-0.557015614158095,
12.5240609649613));
#434276=CARTESIAN_POINT('Ctrl Pts',(-2.68194621597675,-0.556599079079963,
12.5269717671327));
#434277=CARTESIAN_POINT('Ctrl Pts',(-2.68107375902041,-0.556437098070245,
12.5299036066169));
#434278=CARTESIAN_POINT('Ctrl Pts',(-2.68014514144049,-0.55644812151892,
12.5328133004019));
#434279=CARTESIAN_POINT('Ctrl Pts',(-2.67969935093035,-0.55645341341616,
12.5342101228451));
#434280=CARTESIAN_POINT('Ctrl Pts',(-2.67924118031344,-0.55649909265067,
12.5356023438238));
#434281=CARTESIAN_POINT('Ctrl Pts',(-2.67877600264439,-0.556579131053058,
12.5369868989719));
#434282=CARTESIAN_POINT('Origin',(-15.2392792397904,1.6099572959598,-1.24075170958192));
#434283=CARTESIAN_POINT('Ctrl Pts',(-2.65495035883805,-0.660792654622976,
12.5369868989719));
#434284=CARTESIAN_POINT('Ctrl Pts',(-2.66745849690108,-0.669671268584721,
12.5369868989719));
#434285=CARTESIAN_POINT('Ctrl Pts',(-2.66345268273223,-0.684477914272724,
12.5369868989719));
#434286=CARTESIAN_POINT('Ctrl Pts',(-2.65917856036841,-0.663794027375063,
12.5218025310016));
#434287=CARTESIAN_POINT('Ctrl Pts',(-2.66650821598767,-0.673063979489715,
12.5216901060418));
#434288=CARTESIAN_POINT('Ctrl Pts',(-2.66346490970081,-0.684432783016522,
12.5161920673677));
#434289=CARTESIAN_POINT('Ctrl Pts',(-2.66487991552539,-0.661836830254383,
12.5042015548895));
#434290=CARTESIAN_POINT('Ctrl Pts',(-2.66786254719726,-0.667536062950742,
12.4980677368513));
#434291=CARTESIAN_POINT('Ctrl Pts',(-2.66620693867018,-0.67412770463767,
12.4907278922778));
#434292=CARTESIAN_POINT('Ctrl Pts',(-2.66576842322458,-0.648591094005551,
12.506463626192));
#434293=CARTESIAN_POINT('Ctrl Pts',(-2.67212570294493,-0.650137843142798,
12.4999376786891));
#434294=CARTESIAN_POINT('Ctrl Pts',(-2.67204805801663,-0.650118951851058,
12.4906970594712));
#434295=CARTESIAN_POINT('Origin',(-2.64221614027783,-0.678732545304372,
12.5369868989719));
#434296=CARTESIAN_POINT('Origin',(-2.64221614027783,-0.678732545304372,
14.));
#434297=CARTESIAN_POINT('Origin',(-2.64221614027783,-0.678732545304372,
13.7435492065112));
#434298=CARTESIAN_POINT('Ctrl Pts',(-2.63482104809799,-0.646446725415739,
13.793642941384));
#434299=CARTESIAN_POINT('Ctrl Pts',(-2.64364181382917,-0.652699749557833,
13.8071662555867));
#434300=CARTESIAN_POINT('Ctrl Pts',(-2.63594265479821,-0.66788995475232,
13.8103758687955));
#434301=CARTESIAN_POINT('Ctrl Pts',(-2.64835643551964,-0.656093226987222,
13.7804579775006));
#434302=CARTESIAN_POINT('Ctrl Pts',(-2.65923459849045,-0.663817166533145,
13.7901904343351));
#434303=CARTESIAN_POINT('Ctrl Pts',(-2.65447903385889,-0.678838502332587,
13.7927914348263));
#434304=CARTESIAN_POINT('Ctrl Pts',(-2.65632522746666,-0.66177248553203,
13.7597120340895));
#434305=CARTESIAN_POINT('Ctrl Pts',(-2.66891100793882,-0.670715931169972,
13.7635825532445));
#434306=CARTESIAN_POINT('Ctrl Pts',(-2.66539691523532,-0.685316858147909,
13.7651073818884));
#434307=CARTESIAN_POINT('Ctrl Pts',(-2.65476475553836,-0.660660356669375,
13.7381884353898));
#434308=CARTESIAN_POINT('Ctrl Pts',(-2.66705646301534,-0.669393731614178,
13.7368803041982));
#434309=CARTESIAN_POINT('Ctrl Pts',(-2.66325861743349,-0.684048628613317,
13.7363986145813));
#434310=CARTESIAN_POINT('Origin',(-2.62533712434353,-0.666703076897143,
13.7902182540695));
#434311=CARTESIAN_POINT('Ctrl Pts',(-2.60897545660127,-0.628026855760681,
13.8235227101244));
#434312=CARTESIAN_POINT('Ctrl Pts',(-2.61834065293983,-0.634695872619238,
13.8358800583119));
#434313=CARTESIAN_POINT('Ctrl Pts',(-2.61130650365314,-0.649700764917055,
13.8390832900376));
#434314=CARTESIAN_POINT('Ctrl Pts',(-2.61868866275269,-0.634949339097926,
13.8124254819052));
#434315=CARTESIAN_POINT('Ctrl Pts',(-2.62807204600843,-0.641631307319277,
13.8247886449157));
#434316=CARTESIAN_POINT('Ctrl Pts',(-2.62101357611637,-0.656647924244691,
13.8279860620657));
#434317=CARTESIAN_POINT('Ctrl Pts',(-2.62839751576113,-0.641868720003337,
13.8013225099955));
#434318=CARTESIAN_POINT('Ctrl Pts',(-2.63779465964678,-0.648560485138564,
13.8136962257787));
#434319=CARTESIAN_POINT('Ctrl Pts',(-2.6307163124341,-0.663591646957212,
13.8168830918626));
#434320=CARTESIAN_POINT('Ctrl Pts',(-2.63810218500068,-0.648785119187777,
13.7902140179785));
#434321=CARTESIAN_POINT('Ctrl Pts',(-2.64750895251766,-0.655483732956772,
13.802602731458));
#434322=CARTESIAN_POINT('Ctrl Pts',(-2.64041488405503,-0.670532066591058,
13.8057746032558));
#434323=CARTESIAN_POINT('Origin',(-2.59621038579398,-0.64594480624018,13.8235269408515));
#434324=CARTESIAN_POINT('Ctrl Pts',(-2.6231001832877,-0.566158714422425,
13.8235269408515));
#434325=CARTESIAN_POINT('Ctrl Pts',(-2.63473667391714,-0.564156539449527,
13.8362179249168));
#434326=CARTESIAN_POINT('Ctrl Pts',(-2.63460115632286,-0.547078933088014,
13.8391868794938));
#434327=CARTESIAN_POINT('Ctrl Pts',(-2.61245330086808,-0.567990617373133,
13.8400110824519));
#434328=CARTESIAN_POINT('Ctrl Pts',(-2.62120282665965,-0.563013905478216,
13.8494522556837));
#434329=CARTESIAN_POINT('Ctrl Pts',(-2.61709844574261,-0.550204457998946,
13.85569149686));
#434330=CARTESIAN_POINT('Ctrl Pts',(-2.59893592917315,-0.57708338309688,
13.8586819406588));
#434331=CARTESIAN_POINT('Ctrl Pts',(-2.59991830731691,-0.572841805935299,
13.868010383617));
#434332=CARTESIAN_POINT('Ctrl Pts',(-2.59474082921627,-0.565419772028747,
13.8744918421245));
#434333=CARTESIAN_POINT('Ctrl Pts',(-2.5919218364209,-0.607577218552753,
13.8587686893867));
#434334=CARTESIAN_POINT('Ctrl Pts',(-2.59094814657719,-0.611781033012038,
13.8680909899357));
#434335=CARTESIAN_POINT('Ctrl Pts',(-2.58306693203553,-0.616183629842783,
13.8745789365163));
#434336=CARTESIAN_POINT('Ctrl Pts',(-2.60016666986321,-0.621748940165471,
13.8400379222776));
#434337=CARTESIAN_POINT('Ctrl Pts',(-2.60588305763718,-0.630031038011176,
13.8494748685453));
#434338=CARTESIAN_POINT('Ctrl Pts',(-2.59663241123223,-0.639787402413708,
13.8557104837033));
#434339=CARTESIAN_POINT('Ctrl Pts',(-2.60897866247499,-0.628029139623877,
13.8235269408542));
#434340=CARTESIAN_POINT('Ctrl Pts',(-2.61859406710009,-0.634881921007085,
13.8362179249195));
#434341=CARTESIAN_POINT('Ctrl Pts',(-2.61106227426324,-0.65020951379653,
13.8391868794965));
#434342=CARTESIAN_POINT('Origin',(-2.61936967992036,-0.544477308918487,
13.8235269408515));
#434343=CARTESIAN_POINT('Ctrl Pts',(-2.65834525811495,-0.560094444879529,
13.7902140241682));
#434344=CARTESIAN_POINT('Ctrl Pts',(-2.66972687675236,-0.558140640235927,
13.8026027327198));
#434345=CARTESIAN_POINT('Ctrl Pts',(-2.66986456913071,-0.541504565786618,
13.8057746032556));
#434346=CARTESIAN_POINT('Ctrl Pts',(-2.64660074011354,-0.562115207046805,
13.8013225161807));
#434347=CARTESIAN_POINT('Ctrl Pts',(-2.65797071665401,-0.560163397282895,
13.8136962270464));
#434348=CARTESIAN_POINT('Ctrl Pts',(-2.65811512281489,-0.543549615287982,
13.8168830918628));
#434349=CARTESIAN_POINT('Ctrl Pts',(-2.63485115894477,-0.564136840382844,
13.8124254880876));
#434350=CARTESIAN_POINT('Ctrl Pts',(-2.64620448687496,-0.562187886830223,
13.8247886461868));
#434351=CARTESIAN_POINT('Ctrl Pts',(-2.64636049108562,-0.545595833766026,
13.8279860620656));
#434352=CARTESIAN_POINT('Ctrl Pts',(-2.62309630963174,-0.566159380155974,
13.8235227163065));
#434353=CARTESIAN_POINT('Ctrl Pts',(-2.63442763234527,-0.564214204380124,
13.8358800595847));
#434354=CARTESIAN_POINT('Ctrl Pts',(-2.63460046153234,-0.547643267144387,
13.8390832900376));
#434355=CARTESIAN_POINT('Origin',(-2.65461864066729,-0.538412371535249,
13.7902182540695));
#434356=CARTESIAN_POINT('Ctrl Pts',(-2.67851004605948,-0.556624863562287,
13.7382347919292));
#434357=CARTESIAN_POINT('Ctrl Pts',(-2.69338588907555,-0.554089678501094,
13.7369371795943));
#434358=CARTESIAN_POINT('Ctrl Pts',(-2.69631680811249,-0.539225174115846,
13.7364597369711));
#434359=CARTESIAN_POINT('Ctrl Pts',(-2.68037421200545,-0.5563041155144,
13.7595490285573));
#434360=CARTESIAN_POINT('Ctrl Pts',(-2.69560481097229,-0.553707451976304,
13.7633824266925));
#434361=CARTESIAN_POINT('Ctrl Pts',(-2.69876330181909,-0.5390133172322,
13.7648920890506));
#434362=CARTESIAN_POINT('Ctrl Pts',(-2.6708670678098,-0.557939912994462,
13.7803806590111));
#434363=CARTESIAN_POINT('Ctrl Pts',(-2.68404189807138,-0.55569921364324,
13.7901039518745));
#434364=CARTESIAN_POINT('Ctrl Pts',(-2.68629113005427,-0.540097085682201,
13.7926933640892));
#434365=CARTESIAN_POINT('Ctrl Pts',(-2.65434152892321,-0.56078329409476,
13.7936647693663));
#434366=CARTESIAN_POINT('Ctrl Pts',(-2.6650053673487,-0.558978887826884,
13.8072068914932));
#434367=CARTESIAN_POINT('Ctrl Pts',(-2.66464852175933,-0.541934330599655,
13.8104111085397));
#434368=CARTESIAN_POINT('Origin',(-2.67504549927705,-0.53489772554912,13.7435492065112));
#434369=CARTESIAN_POINT('Origin',(-2.67504549927705,-0.53489772554912,14.));
#434370=CARTESIAN_POINT('Origin',(-2.67504549927705,-0.53489772554912,12.5369868989719));
#434371=CARTESIAN_POINT('Ctrl Pts',(-2.68318906964636,-0.572273524858225,
12.506462012331));
#434372=CARTESIAN_POINT('Ctrl Pts',(-2.68958386403895,-0.573637413660991,
12.4999388158272));
#434373=CARTESIAN_POINT('Ctrl Pts',(-2.68950820523503,-0.573621277067824,
12.4907030323752));
#434374=CARTESIAN_POINT('Ctrl Pts',(-2.68813365056713,-0.559953634328176,
12.5042014951932));
#434375=CARTESIAN_POINT('Ctrl Pts',(-2.69329202285334,-0.55611536747025,
12.4980716682127));
#434376=CARTESIAN_POINT('Ctrl Pts',(-2.69466094798664,-0.549463179168228,
12.4907355092744));
#434377=CARTESIAN_POINT('Ctrl Pts',(-2.68384836601972,-0.55571546991498,
12.5218047446509));
#434378=CARTESIAN_POINT('Ctrl Pts',(-2.69446853395318,-0.550545276107923,
12.5216906929434));
#434379=CARTESIAN_POINT('Ctrl Pts',(-2.6966618981544,-0.538988463925912,
12.5161988840775));
#434380=CARTESIAN_POINT('Ctrl Pts',(-2.67873813717001,-0.55658561215412,
12.5369868989719));
#434381=CARTESIAN_POINT('Ctrl Pts',(-2.69385054257426,-0.554012533372128,
12.5369868989719));
#434382=CARTESIAN_POINT('Ctrl Pts',(-2.69667016579091,-0.538944180561122,
12.5369868989719));
#434383=CARTESIAN_POINT('Origin',(-5.02269464967049E-31,-6.29825987887749E-31,
12.5));
#434384=CARTESIAN_POINT('Origin',(-2.56822484263185,-0.778081884616942,
12.5));
#434385=CARTESIAN_POINT('',(-2.56822484263185,-0.778081884616942,12.5893111709658));
#434386=CARTESIAN_POINT('',(-2.56822484263185,-0.778081884616942,13.8235269408515));
#434387=CARTESIAN_POINT('',(-2.56822484263185,-0.778081884616942,12.5));
#434388=CARTESIAN_POINT('',(-2.6038508640706,-0.774910245348786,13.7902182540695));
#434389=CARTESIAN_POINT('',(-2.56822484263185,-0.778081884616942,13.8235269408515));
#434390=CARTESIAN_POINT('',(-2.62449623026968,-0.773072272667636,13.7435492065112));
#434391=CARTESIAN_POINT('Origin',(-2.55657327724839,-0.779119502966356,
13.7445212918686));
#434392=CARTESIAN_POINT('',(-2.62449623026968,-0.773072272667636,12.5369868989719));
#434393=CARTESIAN_POINT('',(-2.62449623026968,-0.773072272667636,12.5));
#434394=CARTESIAN_POINT('Ctrl Pts',(-2.62449623026968,-0.773072272667636,
12.5369868989719));
#434395=CARTESIAN_POINT('Ctrl Pts',(-2.60575278136628,-0.774740925415317,
12.5544431401645));
#434396=CARTESIAN_POINT('Ctrl Pts',(-2.58699592665006,-0.776410771627792,
12.5718848856037));
#434397=CARTESIAN_POINT('Ctrl Pts',(-2.56822484263185,-0.778081884616942,
12.5893111709658));
#434398=CARTESIAN_POINT('Origin',(-2.75929880391481,-1.01592146163591,12.5));
#434399=CARTESIAN_POINT('',(-2.5922874649989,-0.875023942687764,13.7435492065112));
#434400=CARTESIAN_POINT('',(-2.57644512594903,-0.861658704848515,13.7902182540695));
#434401=CARTESIAN_POINT('Origin',(-2.5348141970342,-0.826537169785806,13.7418732680453));
#434402=CARTESIAN_POINT('',(-2.54910729598814,-0.83859540603349,13.8235269408515));
#434403=CARTESIAN_POINT('',(-2.57644512594903,-0.861658704848515,13.7902182540695));
#434404=CARTESIAN_POINT('',(-2.54910729598814,-0.83859540603349,12.5893111709658));
#434405=CARTESIAN_POINT('',(-2.54910729598814,-0.83859540603349,12.5));
#434406=CARTESIAN_POINT('',(-2.5922874649989,-0.875023942687764,12.5369868989719));
#434407=CARTESIAN_POINT('Ctrl Pts',(-2.54910729598814,-0.83859540603349,
12.5893111709658));
#434408=CARTESIAN_POINT('Ctrl Pts',(-2.56351139395776,-0.850747285539268,
12.5718848856037));
#434409=CARTESIAN_POINT('Ctrl Pts',(-2.57790457299165,-0.86288995338934,
12.5544431401645));
#434410=CARTESIAN_POINT('Ctrl Pts',(-2.5922874649989,-0.875023942687764,
12.5369868989719));
#434411=CARTESIAN_POINT('',(-2.5922874649989,-0.875023942687764,12.5));
#434412=CARTESIAN_POINT('Origin',(-2.57127305293844,-0.812321467542656,
12.5));
#434413=CARTESIAN_POINT('',(-2.53885024331821,-0.800904305526286,13.8587068136939));
#434414=CARTESIAN_POINT('Ctrl Pts',(-2.54910729598377,-0.838595406038448,
13.8235269408542));
#434415=CARTESIAN_POINT('Ctrl Pts',(-2.54776795697393,-0.837465485490875,
13.8262006681044));
#434416=CARTESIAN_POINT('Ctrl Pts',(-2.54650937013253,-0.83617638223874,
13.8288634856214));
#434417=CARTESIAN_POINT('Ctrl Pts',(-2.54532684169042,-0.834740577250732,
13.8314912288862));
#434418=CARTESIAN_POINT('Ctrl Pts',(-2.54410777683876,-0.833260410404508,
13.834200161153));
#434419=CARTESIAN_POINT('Ctrl Pts',(-2.54296780529715,-0.831623008322601,
13.8368750301949));
#434420=CARTESIAN_POINT('Ctrl Pts',(-2.54192068506418,-0.829800985179098,
13.8394886372968));
#434421=CARTESIAN_POINT('Ctrl Pts',(-2.54183981342862,-0.829660265912108,
13.839690492513));
#434422=CARTESIAN_POINT('Ctrl Pts',(-2.54175951265142,-0.829518431229104,
13.8398919674349));
#434423=CARTESIAN_POINT('Ctrl Pts',(-2.54167979847135,-0.829375461987807,
13.8400930404591));
#434424=CARTESIAN_POINT('Ctrl Pts',(-2.54043779791686,-0.82714790502353,
13.8432258934518));
#434425=CARTESIAN_POINT('Ctrl Pts',(-2.53934355258194,-0.824656840184953,
13.8462331177034));
#434426=CARTESIAN_POINT('Ctrl Pts',(-2.53852107172497,-0.821944716064727,
13.8489036603661));
#434427=CARTESIAN_POINT('Ctrl Pts',(-2.53825194641688,-0.821057277490011,
13.849777493004));
#434428=CARTESIAN_POINT('Ctrl Pts',(-2.53801210994121,-0.820146331036332,
13.85061494757));
#434429=CARTESIAN_POINT('Ctrl Pts',(-2.53780644658882,-0.819213831003585,
13.8514076489583));
#434430=CARTESIAN_POINT('Ctrl Pts',(-2.53737143893741,-0.817241458947682,
13.8530843267192));
#434431=CARTESIAN_POINT('Ctrl Pts',(-2.53704947552703,-0.814978283817573,
13.8546805203176));
#434432=CARTESIAN_POINT('Ctrl Pts',(-2.53699432859212,-0.812536441960855,
13.8559412814274));
#434433=CARTESIAN_POINT('Ctrl Pts',(-2.53698694814377,-0.812209644329637,
13.8561100121513));
#434434=CARTESIAN_POINT('Ctrl Pts',(-2.53698428930086,-0.811879697661884,
13.8562727473908));
#434435=CARTESIAN_POINT('Ctrl Pts',(-2.53698665815411,-0.811546913710582,
13.8564289040185));
#434436=CARTESIAN_POINT('Ctrl Pts',(-2.53699740087656,-0.810037742287886,
13.8571370725437));
#434437=CARTESIAN_POINT('Ctrl Pts',(-2.53711400900739,-0.808443708134074,
13.8577210840553));
#434438=CARTESIAN_POINT('Ctrl Pts',(-2.53736121979839,-0.806828912811752,
13.8581177131616));
#434439=CARTESIAN_POINT('Ctrl Pts',(-2.53743084286587,-0.806374130869416,
13.8582294175695));
#434440=CARTESIAN_POINT('Ctrl Pts',(-2.53751064763825,-0.805917710234276,
13.8583265086086));
#434441=CARTESIAN_POINT('Ctrl Pts',(-2.53760074717429,-0.805461076504797,
13.8584082369006));
#434442=CARTESIAN_POINT('Ctrl Pts',(-2.53773019604643,-0.804805016286717,
13.8585256585398));
#434443=CARTESIAN_POINT('Ctrl Pts',(-2.53788282193589,-0.80414042241926,
13.8586122832068));
#434444=CARTESIAN_POINT('Ctrl Pts',(-2.53805542971628,-0.803484735877709,
13.8586682984299));
#434445=CARTESIAN_POINT('Ctrl Pts',(-2.53819349883054,-0.802960251640585,
13.8587131050557));
#434446=CARTESIAN_POINT('Ctrl Pts',(-2.53834565140356,-0.802435614053973,
13.8587357943552));
#434447=CARTESIAN_POINT('Ctrl Pts',(-2.5385123919188,-0.801910901840702,
13.8587355499465));
#434448=CARTESIAN_POINT('Ctrl Pts',(-2.53862016028908,-0.801571767827555,
13.8587353919793));
#434449=CARTESIAN_POINT('Ctrl Pts',(-2.53873282029729,-0.801236258278003,
13.8587257282814));
#434450=CARTESIAN_POINT('Ctrl Pts',(-2.53885024331821,-0.800904305526286,
13.8587068136939));
#434451=CARTESIAN_POINT('Ctrl Pts',(-2.53885024331821,-0.800904305526286,
13.8587068136939));
#434452=CARTESIAN_POINT('Ctrl Pts',(-2.53923644123263,-0.799812531022465,
13.8586446046466));
#434453=CARTESIAN_POINT('Ctrl Pts',(-2.53967409816476,-0.798759182819753,
13.858482427929));
#434454=CARTESIAN_POINT('Ctrl Pts',(-2.54015921290488,-0.797742266857458,
13.8582284286032));
#434455=CARTESIAN_POINT('Ctrl Pts',(-2.54065688419738,-0.796699029372676,
13.8579678548414));
#434456=CARTESIAN_POINT('Ctrl Pts',(-2.541207099941,-0.795692245662266,
13.857615680862));
#434457=CARTESIAN_POINT('Ctrl Pts',(-2.54177966554035,-0.794756960603073,
13.8571944833187));
#434458=CARTESIAN_POINT('Ctrl Pts',(-2.54320856155074,-0.792422861084746,
13.8561433417727));
#434459=CARTESIAN_POINT('Ctrl Pts',(-2.54483940254608,-0.790422371730728,
13.8546163505474));
#434460=CARTESIAN_POINT('Ctrl Pts',(-2.54646552170094,-0.788762325543555,
13.8528973491086));
#434461=CARTESIAN_POINT('Ctrl Pts',(-2.54676258967939,-0.788459059596855,
13.8525833129072));
#434462=CARTESIAN_POINT('Ctrl Pts',(-2.54705945621328,-0.788167021217311,
13.8522628768812));
#434463=CARTESIAN_POINT('Ctrl Pts',(-2.54735483301685,-0.787886075498211,
13.851937733538));
#434464=CARTESIAN_POINT('Ctrl Pts',(-2.54915865817453,-0.786170378971128,
13.8499521282529));
#434465=CARTESIAN_POINT('Ctrl Pts',(-2.55108900265194,-0.784700816482711,
13.847639871647));
#434466=CARTESIAN_POINT('Ctrl Pts',(-2.55299574939275,-0.783490698495397,
13.8452109780794));
#434467=CARTESIAN_POINT('Ctrl Pts',(-2.55385363421913,-0.782946241364709,
13.8441181685877));
#434468=CARTESIAN_POINT('Ctrl Pts',(-2.55470659089512,-0.782453601585564,
13.8430021611332));
#434469=CARTESIAN_POINT('Ctrl Pts',(-2.55554128503584,-0.782010699976034,
13.8418824960098));
#434470=CARTESIAN_POINT('Ctrl Pts',(-2.55750826309315,-0.780966991023276,
13.8392439765549));
#434471=CARTESIAN_POINT('Ctrl Pts',(-2.55946608248293,-0.78014625391618,
13.8364981347964));
#434472=CARTESIAN_POINT('Ctrl Pts',(-2.56140669078557,-0.779514758509505,
13.8336931113419));
#434473=CARTESIAN_POINT('Ctrl Pts',(-2.56329672003233,-0.778899722087069,
13.8309611966327));
#434474=CARTESIAN_POINT('Ctrl Pts',(-2.56517249228479,-0.778464111717678,
13.8281701127185));
#434475=CARTESIAN_POINT('Ctrl Pts',(-2.56702430011589,-0.778216000983472,
13.825358068512));
#434476=CARTESIAN_POINT('Ctrl Pts',(-2.56742577405218,-0.77816221030853,
13.8247484142932));
#434477=CARTESIAN_POINT('Ctrl Pts',(-2.56782604499562,-0.778117387942658,
13.8241378483365));
#434478=CARTESIAN_POINT('Ctrl Pts',(-2.56822484263185,-0.778081884616942,
13.8235269408515));
#434479=CARTESIAN_POINT('',(-2.53845888707557,-0.802083125762464,12.5969504640361));
#434480=CARTESIAN_POINT('Origin',(-2.57130466039945,-0.81233124768673,12.584524458991));
#434481=CARTESIAN_POINT('Origin',(-2.57130466039945,-0.81233124768673,12.584524458991));
#434482=CARTESIAN_POINT('Ctrl Pts',(-2.54910729598814,-0.83859540603349,
12.5893111709658));
#434483=CARTESIAN_POINT('Ctrl Pts',(-2.54044437960025,-0.831287019466255,
12.5770542771492));
#434484=CARTESIAN_POINT('Ctrl Pts',(-2.54847970027214,-0.817030887573105,
12.5737548217797));
#434485=CARTESIAN_POINT('Ctrl Pts',(-2.56805018676731,-0.854576394688601,
12.5663937883685));
#434486=CARTESIAN_POINT('Ctrl Pts',(-2.55937621962647,-0.847258685259328,
12.5540940315304));
#434487=CARTESIAN_POINT('Ctrl Pts',(-2.5674392375561,-0.83295995324631,
12.5508374392248));
#434488=CARTESIAN_POINT('Ctrl Pts',(-2.58697396440188,-0.870541258722054,
12.5434499600944));
#434489=CARTESIAN_POINT('Ctrl Pts',(-2.57827179510498,-0.863199756813581,
12.5311293540533));
#434490=CARTESIAN_POINT('Ctrl Pts',(-2.58637949200197,-0.848874359241767,
12.5278936106989));
#434491=CARTESIAN_POINT('Ctrl Pts',(-2.6058801260507,-0.886491261197587,
12.5204817579905));
#434492=CARTESIAN_POINT('Ctrl Pts',(-2.5971348869629,-0.879113423871825,
12.5081597038247));
#434493=CARTESIAN_POINT('Ctrl Pts',(-2.60530195343539,-0.864775255574287,
12.5049254088044));
#434494=CARTESIAN_POINT('Ctrl Pts',(-2.5922874649989,-0.875023942687763,
12.5369868989719));
#434495=CARTESIAN_POINT('Ctrl Pts',(-2.5929994447255,-0.875624597363629,
12.5342545179733));
#434496=CARTESIAN_POINT('Ctrl Pts',(-2.59375936469358,-0.876102487262538,
12.5314872231885));
#434497=CARTESIAN_POINT('Ctrl Pts',(-2.59455417637642,-0.87638337068847,
12.5287124745063));
#434498=CARTESIAN_POINT('Ctrl Pts',(-2.59527097700292,-0.876636685303784,
12.5262100684184));
#434499=CARTESIAN_POINT('Ctrl Pts',(-2.59601576070864,-0.876728585082981,
12.5237004536639));
#434500=CARTESIAN_POINT('Ctrl Pts',(-2.59680943393888,-0.876594856346212,
12.5212220730815));
#434501=CARTESIAN_POINT('Ctrl Pts',(-2.59741705945484,-0.876492475429756,
12.5193246583486));
#434502=CARTESIAN_POINT('Ctrl Pts',(-2.59806049678315,-0.876255999156885,
12.517417831369));
#434503=CARTESIAN_POINT('Ctrl Pts',(-2.59872487174322,-0.875789340163682,
12.5155812248347));
#434504=CARTESIAN_POINT('Ctrl Pts',(-2.59900789904724,-0.875590540924276,
12.5147988205793));
#434505=CARTESIAN_POINT('Ctrl Pts',(-2.59929517266528,-0.875349992872718,
12.5140295443047));
#434506=CARTESIAN_POINT('Ctrl Pts',(-2.59958753385755,-0.875061015908095,
12.5132817086137));
#434507=CARTESIAN_POINT('Ctrl Pts',(-2.60002998297234,-0.874623688364053,
12.5121499604604));
#434508=CARTESIAN_POINT('Ctrl Pts',(-2.60048861089017,-0.874060915274934,
12.5110494206568));
#434509=CARTESIAN_POINT('Ctrl Pts',(-2.6009436543093,-0.873341132251789,
12.5100666561695));
#434510=CARTESIAN_POINT('Ctrl Pts',(-2.60120493919269,-0.872927834497413,
12.5095023550641));
#434511=CARTESIAN_POINT('Ctrl Pts',(-2.60146750942728,-0.872457646016778,
12.5089719619137));
#434512=CARTESIAN_POINT('Ctrl Pts',(-2.60172086703324,-0.871936265915072,
12.5085043804652));
#434513=CARTESIAN_POINT('Ctrl Pts',(-2.60209162288741,-0.87117329405076,
12.5078201359221));
#434514=CARTESIAN_POINT('Ctrl Pts',(-2.60245231717916,-0.870278041215723,
12.5072563000953));
#434515=CARTESIAN_POINT('Ctrl Pts',(-2.60277064754136,-0.869308028552474,
12.5068768744336));
#434516=CARTESIAN_POINT('Ctrl Pts',(-2.60300018564644,-0.868608582646373,
12.5066032824118));
#434517=CARTESIAN_POINT('Ctrl Pts',(-2.60321178674052,-0.867857996609167,
12.5064197834844));
#434518=CARTESIAN_POINT('Ctrl Pts',(-2.60339612235286,-0.86709888648586,
12.5063282718343));
#434519=CARTESIAN_POINT('Ctrl Pts',(-2.603665195278,-0.865990820720387,
12.5061946931565));
#434520=CARTESIAN_POINT('Ctrl Pts',(-2.60388295705793,-0.864841159775945,
12.5062515701262));
#434521=CARTESIAN_POINT('Ctrl Pts',(-2.60405108737695,-0.863724131658777,
12.5064436508398));
#434522=CARTESIAN_POINT('',(-2.54847970027214,-0.817030887573105,12.5737548217797));
#434523=CARTESIAN_POINT('Origin',(-2.56329338043633,-0.821780085399356,
12.5893111709658));
#434524=CARTESIAN_POINT('Ctrl Pts',(-2.60405108737695,-0.863724131658777,
12.5064436508398));
#434525=CARTESIAN_POINT('Ctrl Pts',(-2.59582538737506,-0.856811950582574,
12.5164271754438));
#434526=CARTESIAN_POINT('Ctrl Pts',(-2.58759629229226,-0.849897189477589,
12.5264061185523));
#434527=CARTESIAN_POINT('Ctrl Pts',(-2.57936368316554,-0.842979756752747,
12.536380305637));
#434528=CARTESIAN_POINT('Ctrl Pts',(-2.56907459151018,-0.834334368853223,
12.5488460165097));
#434529=CARTESIAN_POINT('Ctrl Pts',(-2.55878000788777,-0.82568480536692,
12.5613043021964));
#434530=CARTESIAN_POINT('Ctrl Pts',(-2.54847970027214,-0.817030887573105,
12.5737548217797));
#434531=CARTESIAN_POINT('Ctrl Pts',(-2.56822484263185,-0.778081884616942,
12.5893111709658));
#434532=CARTESIAN_POINT('Ctrl Pts',(-2.55693553234648,-0.779086925830232,
12.5770542771492));
#434533=CARTESIAN_POINT('Ctrl Pts',(-2.55532224306043,-0.795371918078755,
12.5737548217797));
#434534=CARTESIAN_POINT('Ctrl Pts',(-2.55769201432484,-0.779019579327555,
12.5928319619712));
#434535=CARTESIAN_POINT('Ctrl Pts',(-2.55039378145664,-0.782939938159727,
12.5821634970842));
#434536=CARTESIAN_POINT('Ctrl Pts',(-2.55148455166212,-0.795704095893736,
12.5773203894503));
#434537=CARTESIAN_POINT('Ctrl Pts',(-2.54314751095848,-0.787328702095061,
12.5969440695591));
#434538=CARTESIAN_POINT('Ctrl Pts',(-2.541919158119,-0.79115619368273,12.5878292599214));
#434539=CARTESIAN_POINT('Ctrl Pts',(-2.5463016087757,-0.798667413314068,
12.5813877129824));
#434540=CARTESIAN_POINT('Ctrl Pts',(-2.53387888228656,-0.816488053392434,
12.596957478804));
#434541=CARTESIAN_POINT('Ctrl Pts',(-2.53509823359339,-0.812688872488681,
12.5878468778671));
#434542=CARTESIAN_POINT('Ctrl Pts',(-2.54298992293219,-0.809105756342446,
12.5814011370086));
#434543=CARTESIAN_POINT('Ctrl Pts',(-2.54101313467616,-0.831766844247121,
12.5928371701607));
#434544=CARTESIAN_POINT('Ctrl Pts',(-2.53729986510681,-0.824367743301106,
12.5821692192951));
#434545=CARTESIAN_POINT('Ctrl Pts',(-2.54551978321918,-0.81454650263643,
12.5773318885715));
#434546=CARTESIAN_POINT('Ctrl Pts',(-2.5491072959881,-0.83859540603353,
12.5893111709658));
#434547=CARTESIAN_POINT('Ctrl Pts',(-2.54044437960021,-0.831287019466295,
12.5770542771492));
#434548=CARTESIAN_POINT('Ctrl Pts',(-2.5484797002721,-0.817030887573146,
12.5737548217797));
#434549=CARTESIAN_POINT('',(-2.55532224306043,-0.795371918078755,12.5737548217797));
#434550=CARTESIAN_POINT('Origin',(-2.57017569722807,-0.799995217689399,
12.5893111709658));
#434551=CARTESIAN_POINT('Ctrl Pts',(-2.5484797002721,-0.817030887573146,
12.5737548217797));
#434552=CARTESIAN_POINT('Ctrl Pts',(-2.54769304936628,-0.816410001123474,
12.5746934679442));
#434553=CARTESIAN_POINT('Ctrl Pts',(-2.54693605954408,-0.815579157066309,
12.5756680099006));
#434554=CARTESIAN_POINT('Ctrl Pts',(-2.54629239321916,-0.814635124582682,
12.5765688348656));
#434555=CARTESIAN_POINT('Ctrl Pts',(-2.54612198968525,-0.814385202433427,
12.5768073183026));
#434556=CARTESIAN_POINT('Ctrl Pts',(-2.54595935785156,-0.814127539442557,
12.5770407398754));
#434557=CARTESIAN_POINT('Ctrl Pts',(-2.54580558218149,-0.813864244577062,
12.5772674179684));
#434558=CARTESIAN_POINT('Ctrl Pts',(-2.5451745284142,-0.812783753647002,
12.5781976435658));
#434559=CARTESIAN_POINT('Ctrl Pts',(-2.54466651577252,-0.811541360537451,
12.5790594849312));
#434560=CARTESIAN_POINT('Ctrl Pts',(-2.54436054299381,-0.810202677086306,
12.5797571720116));
#434561=CARTESIAN_POINT('Ctrl Pts',(-2.54416119072669,-0.809330476683118,
12.580211740231));
#434562=CARTESIAN_POINT('Ctrl Pts',(-2.54405684558894,-0.808373581144119,
12.5806009430798));
#434563=CARTESIAN_POINT('Ctrl Pts',(-2.54407246531675,-0.807397431212796,
12.5808812374708));
#434564=CARTESIAN_POINT('Ctrl Pts',(-2.54408588784472,-0.80655859458742,
12.5811221033394));
#434565=CARTESIAN_POINT('Ctrl Pts',(-2.54418828746562,-0.805688368139684,
12.581287365893));
#434566=CARTESIAN_POINT('Ctrl Pts',(-2.5443821654288,-0.804836843261101,
12.581359338449));
#434567=CARTESIAN_POINT('Ctrl Pts',(-2.54440911046226,-0.804718498886295,
12.5813693411482));
#434568=CARTESIAN_POINT('Ctrl Pts',(-2.54443777180863,-0.804600483745816,
12.5813775999465));
#434569=CARTESIAN_POINT('Ctrl Pts',(-2.54446810491804,-0.804482898618531,
12.5813841266931));
#434570=CARTESIAN_POINT('Ctrl Pts',(-2.54451956870687,-0.804283401228465,
12.5813952001081));
#434571=CARTESIAN_POINT('Ctrl Pts',(-2.54457677895355,-0.804083957592851,
12.5814007534795));
#434572=CARTESIAN_POINT('Ctrl Pts',(-2.54463990030613,-0.803884708952469,
12.5814005856065));
#434573=CARTESIAN_POINT('Ctrl Pts',(-2.54492884517943,-0.802972626577968,
12.5813998171494));
#434574=CARTESIAN_POINT('Ctrl Pts',(-2.54532136873609,-0.802127546192349,
12.58127954464));
#434575=CARTESIAN_POINT('Ctrl Pts',(-2.54578840666897,-0.801341800892411,
12.5810700125799));
#434576=CARTESIAN_POINT('Ctrl Pts',(-2.54635253531537,-0.800392710034351,
12.5808169217085));
#434577=CARTESIAN_POINT('Ctrl Pts',(-2.54703981711477,-0.799538653778791,
12.5804173076348));
#434578=CARTESIAN_POINT('Ctrl Pts',(-2.54776973104725,-0.798838153230019,
12.5799304713245));
#434579=CARTESIAN_POINT('Ctrl Pts',(-2.54867432435619,-0.797970012369661,
12.5793271277669));
#434580=CARTESIAN_POINT('Ctrl Pts',(-2.54967821384419,-0.797260633271943,
12.5785808224116));
#434581=CARTESIAN_POINT('Ctrl Pts',(-2.55072078012457,-0.796714015110856,
12.5777485681082));
#434582=CARTESIAN_POINT('Ctrl Pts',(-2.55227431810398,-0.795899494164346,
12.576508418016));
#434583=CARTESIAN_POINT('Ctrl Pts',(-2.55389746281564,-0.79544714390649,
12.5750928681475));
#434584=CARTESIAN_POINT('Ctrl Pts',(-2.55532224306043,-0.795371918078755,
12.5737548217797));
#434585=CARTESIAN_POINT('Ctrl Pts',(-2.55532224306043,-0.795371918078755,
12.5737548217797));
#434586=CARTESIAN_POINT('Ctrl Pts',(-2.55693553234648,-0.779086925830232,
12.5770542771492));
#434587=CARTESIAN_POINT('Ctrl Pts',(-2.56822484263185,-0.778081884616942,
12.5893111709658));
#434588=CARTESIAN_POINT('Ctrl Pts',(-2.57998826481891,-0.793226615121052,
12.5508408821982));
#434589=CARTESIAN_POINT('Ctrl Pts',(-2.58160335419684,-0.77689085034156,
12.55409748406));
#434590=CARTESIAN_POINT('Ctrl Pts',(-2.59290706675081,-0.775884526953087,
12.5663972313419));
#434591=CARTESIAN_POINT('Ctrl Pts',(-2.60463008878051,-0.791082232777121,
12.52790050457));
#434592=CARTESIAN_POINT('Ctrl Pts',(-2.60622393129696,-0.774698980860186,
12.5311362602937));
#434593=CARTESIAN_POINT('Ctrl Pts',(-2.61756439056145,-0.77368938606204,
12.5434568539655));
#434594=CARTESIAN_POINT('Ctrl Pts',(-2.6292495942247,-0.788938685707459,
12.5049357605811));
#434595=CARTESIAN_POINT('Ctrl Pts',(-2.63080218867057,-0.772510878931263,
12.5081700652078));
#434596=CARTESIAN_POINT('Ctrl Pts',(-2.642198764261,-0.771496288325706,
12.5204921097672));
#434597=CARTESIAN_POINT('Ctrl Pts',(-2.62763298085407,-0.789079437829352,
12.5064436508395));
#434598=CARTESIAN_POINT('Ctrl Pts',(-2.62817752453933,-0.787987503781238,
12.5062361689309));
#434599=CARTESIAN_POINT('Ctrl Pts',(-2.62869724291733,-0.786828761174787,
12.5061871075061));
#434600=CARTESIAN_POINT('Ctrl Pts',(-2.62913646345114,-0.785680674956858,
12.5063648335164));
#434601=CARTESIAN_POINT('Ctrl Pts',(-2.62933598450984,-0.78515914337978,
12.5064455676329));
#434602=CARTESIAN_POINT('Ctrl Pts',(-2.62952147167592,-0.784632457785811,
12.506574497099));
#434603=CARTESIAN_POINT('Ctrl Pts',(-2.62968398054393,-0.784122851769093,
12.5067492519495));
#434604=CARTESIAN_POINT('Ctrl Pts',(-2.63001054842234,-0.783098778696979,
12.5071004286051));
#434605=CARTESIAN_POINT('Ctrl Pts',(-2.63025556102904,-0.782105780109526,
12.5076537929613));
#434606=CARTESIAN_POINT('Ctrl Pts',(-2.63040981192518,-0.781220651583605,
12.5083435010505));
#434607=CARTESIAN_POINT('Ctrl Pts',(-2.6304195229409,-0.781164927453336,
12.5083869222964));
#434608=CARTESIAN_POINT('Ctrl Pts',(-2.63042886352802,-0.781109622735334,
12.5084308732337));
#434609=CARTESIAN_POINT('Ctrl Pts',(-2.63043782727202,-0.781054752968155,
12.5084753333615));
#434610=CARTESIAN_POINT('Ctrl Pts',(-2.63050972832999,-0.780614625013893,
12.5088319622689));
#434611=CARTESIAN_POINT('Ctrl Pts',(-2.63056011562499,-0.780193755153452,
12.509227847131));
#434612=CARTESIAN_POINT('Ctrl Pts',(-2.63059027107938,-0.779804990891921,
12.5096423454524));
#434613=CARTESIAN_POINT('Ctrl Pts',(-2.63068476492719,-0.778586775756137,
12.5109411997424));
#434614=CARTESIAN_POINT('Ctrl Pts',(-2.6305960502868,-0.777609631036941,
12.5124831113042));
#434615=CARTESIAN_POINT('Ctrl Pts',(-2.63040699481828,-0.776827853251822,
12.5140723025008));
#434616=CARTESIAN_POINT('Ctrl Pts',(-2.63038928011381,-0.776754599817102,
12.5142212114565));
#434617=CARTESIAN_POINT('Ctrl Pts',(-2.63037070367165,-0.776683039182932,
12.5143705582413));
#434618=CARTESIAN_POINT('Ctrl Pts',(-2.63035134583323,-0.776613121902429,
12.5145201959299));
#434619=CARTESIAN_POINT('Ctrl Pts',(-2.63010266557795,-0.775714930338395,
12.5164425148273));
#434620=CARTESIAN_POINT('Ctrl Pts',(-2.62972685794205,-0.775054304574326,
12.518463520594));
#434621=CARTESIAN_POINT('Ctrl Pts',(-2.62926873570144,-0.774552951611391,
12.5205025929157));
#434622=CARTESIAN_POINT('Ctrl Pts',(-2.62900300664362,-0.774262147021112,
12.5216853356836));
#434623=CARTESIAN_POINT('Ctrl Pts',(-2.62871042015151,-0.774025128247206,
12.5228750347131));
#434624=CARTESIAN_POINT('Ctrl Pts',(-2.62840468342422,-0.773829851771047,
12.5240609649613));
#434625=CARTESIAN_POINT('Ctrl Pts',(-2.62765426902932,-0.773350556136539,
12.5269717671326));
#434626=CARTESIAN_POINT('Ctrl Pts',(-2.62679791805758,-0.773118000763833,
12.5299036066169));
#434627=CARTESIAN_POINT('Ctrl Pts',(-2.62587149186265,-0.773053296579262,
12.5328133004019));
#434628=CARTESIAN_POINT('Ctrl Pts',(-2.6254267533449,-0.773022234803056,
12.5342101228451));
#434629=CARTESIAN_POINT('Ctrl Pts',(-2.62496638397125,-0.773030416884956,
12.5356023438238));
#434630=CARTESIAN_POINT('Ctrl Pts',(-2.62449623026968,-0.773072272667636,
12.5369868989719));
#434631=CARTESIAN_POINT('Origin',(-15.3184123001101,0.362331832531667,-1.23925115604868));
#434632=CARTESIAN_POINT('Ctrl Pts',(-2.59225549468539,-0.874997023178067,
12.5369868989719));
#434633=CARTESIAN_POINT('Ctrl Pts',(-2.60399832348813,-0.884865623656304,
12.5369868989719));
#434634=CARTESIAN_POINT('Ctrl Pts',(-2.59879895925366,-0.899296490409444,
12.5369868989719));
#434635=CARTESIAN_POINT('Ctrl Pts',(-2.5962249874813,-0.87833304678732,
12.5218025310016));
#434636=CARTESIAN_POINT('Ctrl Pts',(-2.60277466712086,-0.88816958887924,
12.5216901060418));
#434637=CARTESIAN_POINT('Ctrl Pts',(-2.59881482415437,-0.899252505935221,
12.5161920673678));
#434638=CARTESIAN_POINT('Ctrl Pts',(-2.6020669015845,-0.876847075452772,
12.5042015548895));
#434639=CARTESIAN_POINT('Ctrl Pts',(-2.60457506842166,-0.882770456593155,
12.4980677368514));
#434640=CARTESIAN_POINT('Ctrl Pts',(-2.6023876888041,-0.889205217671326,
12.4907278922777));
#434641=CARTESIAN_POINT('Ctrl Pts',(-2.60403210331923,-0.863717834924639,
12.5064636261921));
#434642=CARTESIAN_POINT('Ctrl Pts',(-2.61024215530184,-0.865777614697072,
12.4999376786892));
#434643=CARTESIAN_POINT('Ctrl Pts',(-2.61016630854628,-0.865752457482069,
12.4906970594712));
#434644=CARTESIAN_POINT('Origin',(-2.57810138055071,-0.891839263321898,
12.5369868989719));
#434645=CARTESIAN_POINT('Origin',(-2.57810138055071,-0.891839263321898,
14.));
#434646=CARTESIAN_POINT('Origin',(-2.57810138055071,-0.891839263321898,
13.7435492065112));
#434647=CARTESIAN_POINT('Ctrl Pts',(-2.5733624889779,-0.859058103170204,
13.793642941384));
#434648=CARTESIAN_POINT('Ctrl Pts',(-2.58164422482094,-0.866009295185383,
13.8071662555867));
#434649=CARTESIAN_POINT('Ctrl Pts',(-2.57273254136418,-0.880521403288669,
13.8103758687955));
#434650=CARTESIAN_POINT('Ctrl Pts',(-2.58606655908268,-0.869775766534773,
13.7804579775006));
#434651=CARTESIAN_POINT('Ctrl Pts',(-2.59627895308506,-0.878360676579107,
13.7901904343351));
#434652=CARTESIAN_POINT('Ctrl Pts',(-2.59031483388354,-0.892944407456857,
13.7927914348262));
#434653=CARTESIAN_POINT('Ctrl Pts',(-2.59354592323677,-0.876085658337585,
13.7597120340895));
#434654=CARTESIAN_POINT('Ctrl Pts',(-2.60536085171629,-0.88602520334712,
13.7635825532445));
#434655=CARTESIAN_POINT('Ctrl Pts',(-2.60066834076928,-0.900291115766461,
13.7651073818884));
#434656=CARTESIAN_POINT('Ctrl Pts',(-2.59208129247692,-0.874850037043129,
13.7381884353898));
#434657=CARTESIAN_POINT('Ctrl Pts',(-2.60362024917657,-0.884556240673273,
13.7368803041982));
#434658=CARTESIAN_POINT('Ctrl Pts',(-2.59864053045773,-0.898852815039194,
13.7363986145813));
#434659=CARTESIAN_POINT('Origin',(-2.56225904150083,-0.878474025482649,
13.7902182540695));
#434660=CARTESIAN_POINT('Ctrl Pts',(-2.54910428693338,-0.838592868466142,
13.8235227101244));
#434661=CARTESIAN_POINT('Ctrl Pts',(-2.5578947345676,-0.846003045165089,
13.8358800583119));
#434662=CARTESIAN_POINT('Ctrl Pts',(-2.54966095281149,-0.860384661452888,
13.8390832900376));
#434663=CARTESIAN_POINT('Ctrl Pts',(-2.55822092653545,-0.846284034285507,
13.8124254819053));
#434664=CARTESIAN_POINT('Ctrl Pts',(-2.5670284449151,-0.853708601655244,
13.8247886449158));
#434665=CARTESIAN_POINT('Ctrl Pts',(-2.55876946781238,-0.868099921202787,
13.8279860620657));
#434666=CARTESIAN_POINT('Ctrl Pts',(-2.56733348035622,-0.853971753174535,
13.8013225099954));
#434667=CARTESIAN_POINT('Ctrl Pts',(-2.57615391503897,-0.861407206478814,
13.8136962257787));
#434668=CARTESIAN_POINT('Ctrl Pts',(-2.567873941212,-0.875811402336499,
13.8168830918626));
#434669=CARTESIAN_POINT('Ctrl Pts',(-2.57644210736721,-0.861656159248027,
13.7902140179785));
#434670=CARTESIAN_POINT('Ctrl Pts',(-2.58527157543221,-0.869099222813102,
13.802602731458));
#434671=CARTESIAN_POINT('Ctrl Pts',(-2.57697453300406,-0.883519251920806,
13.8057746032558));
#434672=CARTESIAN_POINT('Origin',(-2.53492121153995,-0.855410726667624,
13.8235269408515));
#434673=CARTESIAN_POINT('Ctrl Pts',(-2.56822484263185,-0.778081884616942,
13.8235269408515));
#434674=CARTESIAN_POINT('Ctrl Pts',(-2.57998580964624,-0.777034853730306,
13.8362179249168));
#434675=CARTESIAN_POINT('Ctrl Pts',(-2.5812427264348,-0.760003025753138,
13.8391868794938));
#434676=CARTESIAN_POINT('Ctrl Pts',(-2.55746406973814,-0.77903987230367,
13.8400110824519));
#434677=CARTESIAN_POINT('Ctrl Pts',(-2.56659013042535,-0.774792887585658,
13.8494522556837));
#434678=CARTESIAN_POINT('Ctrl Pts',(-2.56354349538393,-0.761691517338244,
13.85569149686));
#434679=CARTESIAN_POINT('Ctrl Pts',(-2.54325053116281,-0.787000591317278,
13.8586819406588));
#434680=CARTESIAN_POINT('Ctrl Pts',(-2.54457536843989,-0.78285320059247,
13.868010383617));
#434681=CARTESIAN_POINT('Ctrl Pts',(-2.54002008263671,-0.775033850360904,
13.8744918421245));
#434682=CARTESIAN_POINT('Ctrl Pts',(-2.53377424654496,-0.816821247376267,
13.8587686893867));
#434683=CARTESIAN_POINT('Ctrl Pts',(-2.53246114666913,-0.820931709228164,
13.8680909899357));
#434684=CARTESIAN_POINT('Ctrl Pts',(-2.52424730370528,-0.824677264630375,
13.8745789365163));
#434685=CARTESIAN_POINT('Ctrl Pts',(-2.54083651910886,-0.831617844221254,
13.8400379222776));
#434686=CARTESIAN_POINT('Ctrl Pts',(-2.54585881821242,-0.840338322741523,
13.8494748685452));
#434687=CARTESIAN_POINT('Ctrl Pts',(-2.53584371829778,-0.849308210085531,
13.8557104837033));
#434688=CARTESIAN_POINT('Ctrl Pts',(-2.54910729598377,-0.838595406038448,
13.8235269408542));
#434689=CARTESIAN_POINT('Ctrl Pts',(-2.55813214084235,-0.846209130098926,
13.8362179249195));
#434690=CARTESIAN_POINT('Ctrl Pts',(-2.54937606831806,-0.860871810549845,
13.8391868794965));
#434691=CARTESIAN_POINT('Origin',(-2.56627398803563,-0.756168551544486,
13.8235269408515));
#434692=CARTESIAN_POINT('Ctrl Pts',(-2.60384693664582,-0.774910594228413,
13.7902140241682));
#434693=CARTESIAN_POINT('Ctrl Pts',(-2.6153499371028,-0.77389099828931,
13.8026027327198));
#434694=CARTESIAN_POINT('Ctrl Pts',(-2.61684316583052,-0.757321502212479,
13.8057746032556));
#434695=CARTESIAN_POINT('Ctrl Pts',(-2.59197678668273,-0.775967345228378,
13.8013225161808));
#434696=CARTESIAN_POINT('Ctrl Pts',(-2.60346802117969,-0.774948788592186,
13.8136962270464));
#434697=CARTESIAN_POINT('Ctrl Pts',(-2.60496612430837,-0.758402058029048,
13.8168830918628));
#434698=CARTESIAN_POINT('Ctrl Pts',(-2.58010151939116,-0.777024551803223,
13.8124254880875));
#434699=CARTESIAN_POINT('Ctrl Pts',(-2.59157592786698,-0.776007484858214,
13.8247886461867));
#434700=CARTESIAN_POINT('Ctrl Pts',(-2.59308381934438,-0.759483356273309,
13.8279860620656));
#434701=CARTESIAN_POINT('Ctrl Pts',(-2.56822092760171,-0.778082232396394,
13.8235227163065));
#434702=CARTESIAN_POINT('Ctrl Pts',(-2.57967309615752,-0.777067137028476,
13.8358800595847));
#434703=CARTESIAN_POINT('Ctrl Pts',(-2.58119603549152,-0.760565425402617,
13.8390832900376));
#434704=CARTESIAN_POINT('Origin',(-2.60190000947438,-0.75299691227633,13.7902182540695));
#434705=CARTESIAN_POINT('Ctrl Pts',(-2.6242274310093,-0.773096175075023,
13.7382347919292));
#434706=CARTESIAN_POINT('Ctrl Pts',(-2.63926041700291,-0.771781944939381,
13.7369371795943));
#434707=CARTESIAN_POINT('Ctrl Pts',(-2.64339317875125,-0.757205798077073,
13.7364597369711));
#434708=CARTESIAN_POINT('Ctrl Pts',(-2.62611153804043,-0.772928441120475,
13.7595490285574));
#434709=CARTESIAN_POINT('Ctrl Pts',(-2.64150311063024,-0.771581852975879,
13.7633824266925));
#434710=CARTESIAN_POINT('Ctrl Pts',(-2.64584880025467,-0.757194058078969,
13.7648920890506));
#434711=CARTESIAN_POINT('Ctrl Pts',(-2.61650269540219,-0.773783875107399,
13.7803806590111));
#434712=CARTESIAN_POINT('Ctrl Pts',(-2.62981632530171,-0.772624502473894,
13.7901039518744));
#434713=CARTESIAN_POINT('Ctrl Pts',(-2.63332979142262,-0.757257622594016,
13.7926933640892));
#434714=CARTESIAN_POINT('Ctrl Pts',(-2.59980038192665,-0.775270810256772,
13.7936647693663));
#434715=CARTESIAN_POINT('Ctrl Pts',(-2.61057581317161,-0.774341609831827,
13.8072068914933));
#434716=CARTESIAN_POINT('Ctrl Pts',(-2.61160944460447,-0.757324680734365,
13.8104111085397));
#434717=CARTESIAN_POINT('Origin',(-2.62254537567346,-0.75115893959518,13.7435492065112));
#434718=CARTESIAN_POINT('Origin',(-2.62254537567346,-0.75115893959518,14.));
#434719=CARTESIAN_POINT('Origin',(-2.62254537567346,-0.75115893959518,12.5369868989719));
#434720=CARTESIAN_POINT('Ctrl Pts',(-2.62761537436049,-0.78907415060169,
12.506462012331));
#434721=CARTESIAN_POINT('Ctrl Pts',(-2.63387772100312,-0.790954736286347,
12.4999388158272));
#434722=CARTESIAN_POINT('Ctrl Pts',(-2.63380362922977,-0.790932486491461,
12.4907030323752));
#434723=CARTESIAN_POINT('Ctrl Pts',(-2.6335476880466,-0.777198282739337,
12.5042014951932));
#434724=CARTESIAN_POINT('Ctrl Pts',(-2.63900175065624,-0.773793242627058,
12.4980716682127));
#434725=CARTESIAN_POINT('Ctrl Pts',(-2.6409083359066,-0.767274769039712,
12.4907355092743));
#434726=CARTESIAN_POINT('Ctrl Pts',(-2.62962211217494,-0.772624929995355,
12.5218047446509));
#434727=CARTESIAN_POINT('Ctrl Pts',(-2.64062836116866,-0.768337581861103,
12.5216906929434));
#434728=CARTESIAN_POINT('Ctrl Pts',(-2.64375641461251,-0.756998003562851,
12.5161988840776));
#434729=CARTESIAN_POINT('Ctrl Pts',(-2.62445796251965,-0.77307564581568,
12.5369868989719));
#434730=CARTESIAN_POINT('Ctrl Pts',(-2.63972981244962,-0.771742930078233,
12.5369868989719));
#434731=CARTESIAN_POINT('Ctrl Pts',(-2.64376826424447,-0.756954541436434,
12.5369868989719));
#434732=CARTESIAN_POINT('Origin',(-4.91254002680598E-31,-6.70384157887756E-31,
12.5));
#434733=CARTESIAN_POINT('Origin',(-2.49625838937555,-0.984827048243808,
12.5));
#434734=CARTESIAN_POINT('',(-2.49625838937555,-0.984827048243808,12.5893111709658));
#434735=CARTESIAN_POINT('',(-2.49625838937555,-0.984827048243808,13.8235269408515));
#434736=CARTESIAN_POINT('',(-2.49625838937555,-0.984827048243808,12.5));
#434737=CARTESIAN_POINT('',(-2.53202438621132,-0.98456981382678,13.7902182540695));
#434738=CARTESIAN_POINT('',(-2.49625838937555,-0.984827048243808,13.8235269408515));
#434739=CARTESIAN_POINT('',(-2.55275086849392,-0.984420745855558,13.7435492065112));
#434740=CARTESIAN_POINT('Origin',(-2.48456101808811,-0.984911503257141,
13.7445212918691));
#434741=CARTESIAN_POINT('',(-2.55275086849392,-0.984420745855558,12.5369868989719));
#434742=CARTESIAN_POINT('',(-2.55275086849392,-0.984420745855558,12.5));
#434743=CARTESIAN_POINT('Ctrl Pts',(-2.55275086849392,-0.984420745855558,
12.5369868989719));
#434744=CARTESIAN_POINT('Ctrl Pts',(-2.53393377618057,-0.984556081207558,
12.5544431401645));
#434745=CARTESIAN_POINT('Ctrl Pts',(-2.51510322538267,-0.984691513354999,
12.5718848856037));
#434746=CARTESIAN_POINT('Ctrl Pts',(-2.49625838937555,-0.984827048243808,
12.5893111709658));
#434747=CARTESIAN_POINT('Origin',(-2.66731043429289,-1.2374495353793,12.5));
#434748=CARTESIAN_POINT('',(-2.51233926765277,-1.08340786672296,13.7435492065112));
#434749=CARTESIAN_POINT('',(-2.4976390336399,-1.0687958029044,13.7902182540695));
#434750=CARTESIAN_POINT('Origin',(-2.45900935936426,-1.03039782466055,13.7418732680442));
#434751=CARTESIAN_POINT('',(-2.47227204101564,-1.04358095837975,13.8235269408515));
#434752=CARTESIAN_POINT('',(-2.4976390336399,-1.0687958029044,13.7902182540695));
#434753=CARTESIAN_POINT('',(-2.47227204101564,-1.04358095837975,12.5893111709658));
#434754=CARTESIAN_POINT('',(-2.47227204101564,-1.04358095837975,12.5));
#434755=CARTESIAN_POINT('',(-2.51233926765277,-1.08340786672296,12.5369868989719));
#434756=CARTESIAN_POINT('Ctrl Pts',(-2.47227204101564,-1.04358095837975,
12.5893111709658));
#434757=CARTESIAN_POINT('Ctrl Pts',(-2.48563771954525,-1.05686647121458,
12.5718848856037));
#434758=CARTESIAN_POINT('Ctrl Pts',(-2.49899326630645,-1.0701419130501,
12.5544431401645));
#434759=CARTESIAN_POINT('Ctrl Pts',(-2.51233926765277,-1.08340786672296,
12.5369868989719));
#434760=CARTESIAN_POINT('',(-2.51233926765277,-1.08340786672296,12.5));
#434761=CARTESIAN_POINT('Origin',(-2.49650561314058,-1.01920115922009,12.5));
#434762=CARTESIAN_POINT('',(-2.4651212924408,-1.00517922688567,13.8587068136939));
#434763=CARTESIAN_POINT('Ctrl Pts',(-2.47227204101088,-1.04358095838433,
13.8235269408542));
#434764=CARTESIAN_POINT('Ctrl Pts',(-2.4710292575554,-1.04234562899105,
13.8262006681044));
#434765=CARTESIAN_POINT('Ctrl Pts',(-2.46987993244038,-1.04095822861191,
13.8288634856214));
#434766=CARTESIAN_POINT('Ctrl Pts',(-2.4688183702,-1.03943081410046,13.8314912288862));
#434767=CARTESIAN_POINT('Ctrl Pts',(-2.46772400902523,-1.03785620728465,
13.8342001611531));
#434768=CARTESIAN_POINT('Ctrl Pts',(-2.46672129411546,-1.03613133525948,
13.8368750301949));
#434769=CARTESIAN_POINT('Ctrl Pts',(-2.46582616988972,-1.0342300247277,
13.8394886372969));
#434770=CARTESIAN_POINT('Ctrl Pts',(-2.4657570372745,-1.03408318190339,
13.8396904925131));
#434771=CARTESIAN_POINT('Ctrl Pts',(-2.4656885645349,-1.03393527390479,
13.8398919674349));
#434772=CARTESIAN_POINT('Ctrl Pts',(-2.46562076891762,-1.03378628293615,
13.8400930404591));
#434773=CARTESIAN_POINT('Ctrl Pts',(-2.46456446758973,-1.03146490340854,
13.8432258934518));
#434774=CARTESIAN_POINT('Ctrl Pts',(-2.46367690817616,-1.02889293622944,
13.8462331177034));
#434775=CARTESIAN_POINT('Ctrl Pts',(-2.46307822735032,-1.02612279665311,
13.8489036603661));
#434776=CARTESIAN_POINT('Ctrl Pts',(-2.46288233201691,-1.02521637474599,
13.849777493004));
#434777=CARTESIAN_POINT('Ctrl Pts',(-2.46271754417012,-1.02428891049219,
13.85061494757));
#434778=CARTESIAN_POINT('Ctrl Pts',(-2.46258857255514,-1.02334274980388,
13.8514076489583));
#434779=CARTESIAN_POINT('Ctrl Pts',(-2.46231577898897,-1.0213414834913,
13.8530843267192));
#434780=CARTESIAN_POINT('Ctrl Pts',(-2.46217935666868,-1.01905959588286,
13.8546805203176));
#434781=CARTESIAN_POINT('Ctrl Pts',(-2.46232342601092,-1.01662138406636,
13.8559412814273));
#434782=CARTESIAN_POINT('Ctrl Pts',(-2.46234270716119,-1.01629507225221,
13.8561100121513));
#434783=CARTESIAN_POINT('Ctrl Pts',(-2.46236695088185,-1.01596600673437,
13.8562727473908));
#434784=CARTESIAN_POINT('Ctrl Pts',(-2.46239643683439,-1.01563452317772,
13.8564289040185));
#434785=CARTESIAN_POINT('Ctrl Pts',(-2.46253015529273,-1.01413124903004,
13.8571370725437));
#434786=CARTESIAN_POINT('Ctrl Pts',(-2.46277630400145,-1.01255202353858,
13.8577210840554));
#434787=CARTESIAN_POINT('Ctrl Pts',(-2.46315431302874,-1.01096275128894,
13.8581177131616));
#434788=CARTESIAN_POINT('Ctrl Pts',(-2.46326077338149,-1.01051515752235,
13.8582294175695));
#434789=CARTESIAN_POINT('Ctrl Pts',(-2.46337751512905,-1.01006676041904,
13.8583265086086));
#434790=CARTESIAN_POINT('Ctrl Pts',(-2.46350453475444,-1.00961899004926,
13.8584082369006));
#434791=CARTESIAN_POINT('Ctrl Pts',(-2.46368702789447,-1.00897566410226,
13.8585256585398));
#434792=CARTESIAN_POINT('Ctrl Pts',(-2.46389331650387,-1.00832572204297,
13.8586122832068));
#434793=CARTESIAN_POINT('Ctrl Pts',(-2.46411879448634,-1.00768628638081,
13.8586682984299));
#434794=CARTESIAN_POINT('Ctrl Pts',(-2.46429915452141,-1.0071748012363,
13.8587131050557));
#434795=CARTESIAN_POINT('Ctrl Pts',(-2.46449356365311,-1.00666431118519,
13.8587357943552));
#434796=CARTESIAN_POINT('Ctrl Pts',(-2.46470251826961,-1.00615493580846,
13.8587355499465));
#434797=CARTESIAN_POINT('Ctrl Pts',(-2.46483757061997,-1.00582571435839,
13.8587353919793));
#434798=CARTESIAN_POINT('Ctrl Pts',(-2.46497720290432,-1.00550050402571,
13.8587257282814));
#434799=CARTESIAN_POINT('Ctrl Pts',(-2.4651212924408,-1.00517922688567,
13.8587068136939));
#434800=CARTESIAN_POINT('Ctrl Pts',(-2.4651212924408,-1.00517922688567,
13.8587068136939));
#434801=CARTESIAN_POINT('Ctrl Pts',(-2.46559519507111,-1.00412256388679,
13.8586446046466));
#434802=CARTESIAN_POINT('Ctrl Pts',(-2.46611725339322,-1.00310839371633,
13.858482427929));
#434803=CARTESIAN_POINT('Ctrl Pts',(-2.46668364204556,-1.00213440281294,
13.8582284286032));
#434804=CARTESIAN_POINT('Ctrl Pts',(-2.46726469091784,-1.00113520144532,
13.8579678548414));
#434805=CARTESIAN_POINT('Ctrl Pts',(-2.46789513808288,-1.00017661541572,
13.857615680862));
#434806=CARTESIAN_POINT('Ctrl Pts',(-2.46854203293253,-0.999291111852187,
13.8571944833187));
#434807=CARTESIAN_POINT('Ctrl Pts',(-2.47015642518878,-0.997081247147531,
13.8561433417727));
#434808=CARTESIAN_POINT('Ctrl Pts',(-2.47194489814923,-0.99522034293792,
13.8546163505474));
#434809=CARTESIAN_POINT('Ctrl Pts',(-2.47370091570212,-0.993698364224767,
13.8528973491086));
#434810=CARTESIAN_POINT('Ctrl Pts',(-2.47402171420141,-0.993420321168572,
13.8525833129072));
#434811=CARTESIAN_POINT('Ctrl Pts',(-2.47434139677549,-0.993153451901128,
13.8522628768812));
#434812=CARTESIAN_POINT('Ctrl Pts',(-2.47465869042139,-0.992897516957365,
13.851937733538));
#434813=CARTESIAN_POINT('Ctrl Pts',(-2.47659635869437,-0.991334557765187,
13.8499521282529));
#434814=CARTESIAN_POINT('Ctrl Pts',(-2.47864006309533,-0.990027226120073,
13.847639871647));
#434815=CARTESIAN_POINT('Ctrl Pts',(-2.48063910114381,-0.988976552261284,
13.8452109780794));
#434816=CARTESIAN_POINT('Ctrl Pts',(-2.48153850973985,-0.988503832344347,
13.8441181685877));
#434817=CARTESIAN_POINT('Ctrl Pts',(-2.48242878298831,-0.988082355670984,
13.8430021611332));
#434818=CARTESIAN_POINT('Ctrl Pts',(-2.48329680034602,-0.987708963101414,
13.8418824960098));
#434819=CARTESIAN_POINT('Ctrl Pts',(-2.48534230541506,-0.986829053976304,
13.8392439765549));
#434820=CARTESIAN_POINT('Ctrl Pts',(-2.4873605080159,-0.986170628260006,
13.8364981347964));
#434821=CARTESIAN_POINT('Ctrl Pts',(-2.48934613184266,-0.985699411694597,
13.8336931113419));
#434822=CARTESIAN_POINT('Ctrl Pts',(-2.49128000335114,-0.985240476684907,
13.8309611966328));
#434823=CARTESIAN_POINT('Ctrl Pts',(-2.49318504041528,-0.984959208625481,
13.8281701127186));
#434824=CARTESIAN_POINT('Ctrl Pts',(-2.49505090983676,-0.984862862988851,
13.8253580685121));
#434825=CARTESIAN_POINT('Ctrl Pts',(-2.49545543234105,-0.98484197515085,
13.8247484142933));
#434826=CARTESIAN_POINT('Ctrl Pts',(-2.4958580248549,-0.984829927725528,
13.8241378483365));
#434827=CARTESIAN_POINT('Ctrl Pts',(-2.49625838937555,-0.984827048243808,
13.8235269408515));
#434828=CARTESIAN_POINT('',(-2.46463515361085,-1.0063222255279,12.5969504640361));
#434829=CARTESIAN_POINT('Origin',(-2.49653631825785,-1.01921348312305,12.584524458991));
#434830=CARTESIAN_POINT('Origin',(-2.49653631825785,-1.01921348312305,12.584524458991));
#434831=CARTESIAN_POINT('Ctrl Pts',(-2.47227204101564,-1.04358095837975,
12.5893111709658));
#434832=CARTESIAN_POINT('Ctrl Pts',(-2.46423365112037,-1.03559078175771,
12.5770542771492));
#434833=CARTESIAN_POINT('Ctrl Pts',(-2.47340424202235,-1.02203703919843,
12.5737548217797));
#434834=CARTESIAN_POINT('Ctrl Pts',(-2.48984930195276,-1.06105279306917,
12.5663937883685));
#434835=CARTESIAN_POINT('Ctrl Pts',(-2.48180065797481,-1.0530524238672,
12.5540940315304));
#434836=CARTESIAN_POINT('Ctrl Pts',(-2.49100232627946,-1.03945848052007,
12.5508374392248));
#434837=CARTESIAN_POINT('Ctrl Pts',(-2.50740882764907,-1.07850699889156,
12.5434499600945));
#434838=CARTESIAN_POINT('Ctrl Pts',(-2.49933401466334,-1.07048061764037,
12.5311293540533));
#434839=CARTESIAN_POINT('Ctrl Pts',(-2.50858238676034,-1.0568637392125,
12.5278936106989));
#434840=CARTESIAN_POINT('Ctrl Pts',(-2.52495200733029,-1.09594495674026,
12.5204817579905));
#434841=CARTESIAN_POINT('Ctrl Pts',(-2.51683722953868,-1.08787885038707,
12.5081597038247));
#434842=CARTESIAN_POINT('Ctrl Pts',(-2.52614581459653,-1.07425408289858,
12.5049254088044));
#434843=CARTESIAN_POINT('Ctrl Pts',(-2.51233926765277,-1.08340786672296,
12.5369868989719));
#434844=CARTESIAN_POINT('Ctrl Pts',(-2.51299991939328,-1.08406455572736,
12.5342545179733));
#434845=CARTESIAN_POINT('Ctrl Pts',(-2.51371835832708,-1.0846027960192,
12.5314872231885));
#434846=CARTESIAN_POINT('Ctrl Pts',(-2.5144876307328,-1.08494752935953,
12.5287124745062));
#434847=CARTESIAN_POINT('Ctrl Pts',(-2.51518139877155,-1.08525842699687,
12.5262100684184));
#434848=CARTESIAN_POINT('Ctrl Pts',(-2.51591621358577,-1.08541072777338,
12.5237004536639));
#434849=CARTESIAN_POINT('Ctrl Pts',(-2.51671814606732,-1.08534213574432,
12.5212220730815));
#434850=CARTESIAN_POINT('Ctrl Pts',(-2.51733209475465,-1.08528962261239,
12.5193246583486));
#434851=CARTESIAN_POINT('Ctrl Pts',(-2.51799266610991,-1.08510637931045,
12.517417831369));
#434852=CARTESIAN_POINT('Ctrl Pts',(-2.5186928674573,-1.08469542581355,
12.5155812248348));
#434853=CARTESIAN_POINT('Ctrl Pts',(-2.51899115699489,-1.08452035741499,
12.5147988205793));
#434854=CARTESIAN_POINT('Ctrl Pts',(-2.519297081633,-1.08430402523402,12.5140295443047));
#434855=CARTESIAN_POINT('Ctrl Pts',(-2.51961202432288,-1.08403983996772,
12.5132817086137));
#434856=CARTESIAN_POINT('Ctrl Pts',(-2.52008864747953,-1.08364003130536,
12.5121499604604));
#434857=CARTESIAN_POINT('Ctrl Pts',(-2.5205916205821,-1.08311651323026,
12.5110494206568));
#434858=CARTESIAN_POINT('Ctrl Pts',(-2.52110381888031,-1.08243621548882,
12.5100666561695));
#434859=CARTESIAN_POINT('Ctrl Pts',(-2.52139792196366,-1.08204559009228,
12.5095023550641));
#434860=CARTESIAN_POINT('Ctrl Pts',(-2.52169794324365,-1.0815983680367,
12.5089719619137));
#434861=CARTESIAN_POINT('Ctrl Pts',(-2.52199295514162,-1.08109937378121,
12.5085043804652));
#434862=CARTESIAN_POINT('Ctrl Pts',(-2.5224246666263,-1.08036916068688,
12.5078201359221));
#434863=CARTESIAN_POINT('Ctrl Pts',(-2.52285713215508,-1.0795062866642,
12.5072563000949));
#434864=CARTESIAN_POINT('Ctrl Pts',(-2.52325346833651,-1.07856544851782,
12.5068768744332));
#434865=CARTESIAN_POINT('Ctrl Pts',(-2.5235392540072,-1.07788703944677,
12.5066032824114));
#434866=CARTESIAN_POINT('Ctrl Pts',(-2.52381133074579,-1.07715619837718,
12.5064197834844));
#434867=CARTESIAN_POINT('Ctrl Pts',(-2.52405692751887,-1.07641463919388,
12.5063282718343));
#434868=CARTESIAN_POINT('Ctrl Pts',(-2.52441542277272,-1.07533219236719,
12.5061946931565));
#434869=CARTESIAN_POINT('Ctrl Pts',(-2.5247261680082,-1.07420410643136,
12.5062515701262));
#434870=CARTESIAN_POINT('Ctrl Pts',(-2.52498478704898,-1.07310449931496,
12.5064436508398));
#434871=CARTESIAN_POINT('',(-2.47340424202235,-1.02203703919843,12.5737548217797));
#434872=CARTESIAN_POINT('Origin',(-2.4877815271756,-1.02797788691757,12.5893111709658));
#434873=CARTESIAN_POINT('Ctrl Pts',(-2.52498478704898,-1.07310449931495,
12.5064436508398));
#434874=CARTESIAN_POINT('Ctrl Pts',(-2.51734986431254,-1.06554484703725,
12.5164271754438));
#434875=CARTESIAN_POINT('Ctrl Pts',(-2.50971176808834,-1.05798234658497,
12.5264061185523));
#434876=CARTESIAN_POINT('Ctrl Pts',(-2.50207038727473,-1.05041689697523,
12.536380305637));
#434877=CARTESIAN_POINT('Ctrl Pts',(-2.49252021109674,-1.04096161940157,
12.5488460165097));
#434878=CARTESIAN_POINT('Ctrl Pts',(-2.48296490157486,-1.03150173248874,
12.5613043021964));
#434879=CARTESIAN_POINT('Ctrl Pts',(-2.47340424202235,-1.02203703919843,
12.5737548217797));
#434880=CARTESIAN_POINT('Ctrl Pts',(-2.49625838937555,-0.984827048243808,
12.5893111709658));
#434881=CARTESIAN_POINT('Ctrl Pts',(-2.48492472314963,-0.984908561672269,
12.5770542771492));
#434882=CARTESIAN_POINT('Ctrl Pts',(-2.48198942389984,-1.00100786889864,
12.5737548217797));
#434883=CARTESIAN_POINT('Ctrl Pts',(-2.48568417736179,-0.984903099563596,
12.5928319619712));
#434884=CARTESIAN_POINT('Ctrl Pts',(-2.47809068312174,-0.988215539992912,
12.5821634970843));
#434885=CARTESIAN_POINT('Ctrl Pts',(-2.47813742652736,-1.001026133943,12.5773203894503));
#434886=CARTESIAN_POINT('Ctrl Pts',(-2.47051079898685,-0.991999062361609,
12.5969440695591));
#434887=CARTESIAN_POINT('Ctrl Pts',(-2.46897455729303,-0.995713696126876,
12.5878292599214));
#434888=CARTESIAN_POINT('Ctrl Pts',(-2.47273019157598,-1.00355713320773,
12.5813877129824));
#434889=CARTESIAN_POINT('Ctrl Pts',(-2.4588962530793,-1.02030590904051,
12.596957478804));
#434890=CARTESIAN_POINT('Ctrl Pts',(-2.46042121560877,-1.01661875804921,
12.5878468778671));
#434891=CARTESIAN_POINT('Ctrl Pts',(-2.46857870323226,-1.01369081037035,
12.5814011370086));
#434892=CARTESIAN_POINT('Ctrl Pts',(-2.46476140353657,-1.03611536877996,
12.5928371701607));
#434893=CARTESIAN_POINT('Ctrl Pts',(-2.46166358498239,-1.02843822178975,
12.5821692192951));
#434894=CARTESIAN_POINT('Ctrl Pts',(-2.47065667428546,-1.01931966012934,
12.5773318885715));
#434895=CARTESIAN_POINT('Ctrl Pts',(-2.4722720410156,-1.04358095837979,
12.5893111709658));
#434896=CARTESIAN_POINT('Ctrl Pts',(-2.46423365112033,-1.03559078175775,
12.5770542771492));
#434897=CARTESIAN_POINT('Ctrl Pts',(-2.47340424202231,-1.02203703919846,
12.5737548217797));
#434898=CARTESIAN_POINT('',(-2.48198942389984,-1.00100786889864,12.5737548217797));
#434899=CARTESIAN_POINT('Origin',(-2.49641661258517,-1.00682647926863,12.5893111709658));
#434900=CARTESIAN_POINT('Ctrl Pts',(-2.47340424202231,-1.02203703919846,
12.5737548217797));
#434901=CARTESIAN_POINT('Ctrl Pts',(-2.47267081664216,-1.0213540993455,
12.5746934679442));
#434902=CARTESIAN_POINT('Ctrl Pts',(-2.47198406714499,-1.02046431815534,
12.5756680099006));
#434903=CARTESIAN_POINT('Ctrl Pts',(-2.47141948997805,-1.01947096208094,
12.5765688348656));
#434904=CARTESIAN_POINT('Ctrl Pts',(-2.47127002442318,-1.01920798205705,
12.5768073183026));
#434905=CARTESIAN_POINT('Ctrl Pts',(-2.47112893565927,-1.01893792041428,
12.5770407398754));
#434906=CARTESIAN_POINT('Ctrl Pts',(-2.4709971326409,-1.01866296749603,
12.5772674179684));
#434907=CARTESIAN_POINT('Ctrl Pts',(-2.47045624869456,-1.01753463506996,
12.5781976435658));
#434908=CARTESIAN_POINT('Ctrl Pts',(-2.47005119299528,-1.01625496817453,
12.5790594849312));
#434909=CARTESIAN_POINT('Ctrl Pts',(-2.46985535344476,-1.01489579946016,
12.5797571720116));
#434910=CARTESIAN_POINT('Ctrl Pts',(-2.46972775693583,-1.0140102521714,
12.580211740231));
#434911=CARTESIAN_POINT('Ctrl Pts',(-2.46970175486773,-1.01304803552594,
12.5806009430798));
#434912=CARTESIAN_POINT('Ctrl Pts',(-2.46979688790372,-1.01207640680581,
12.5808812374708));
#434913=CARTESIAN_POINT('Ctrl Pts',(-2.46987863874168,-1.01124145540075,
12.5811221033394));
#434914=CARTESIAN_POINT('Ctrl Pts',(-2.47005162917057,-1.01038247107947,
12.581287365893));
#434915=CARTESIAN_POINT('Ctrl Pts',(-2.4703142692036,-1.00954958243355,
12.581359338449));
#434916=CARTESIAN_POINT('Ctrl Pts',(-2.47035077074488,-1.00943382811026,
12.5813693411482));
#434917=CARTESIAN_POINT('Ctrl Pts',(-2.47038895605253,-1.00931854182123,
12.5813775999465));
#434918=CARTESIAN_POINT('Ctrl Pts',(-2.47042877251051,-1.00920382037877,
12.5813841266931));
#434919=CARTESIAN_POINT('Ctrl Pts',(-2.47049632594716,-1.00900918157637,
12.5813952001081));
#434920=CARTESIAN_POINT('Ctrl Pts',(-2.47056960233931,-1.00881506473922,
12.5814007534795));
#434921=CARTESIAN_POINT('Ctrl Pts',(-2.47064875427473,-1.00862162405847,
12.5814005856065));
#434922=CARTESIAN_POINT('Ctrl Pts',(-2.47101108088868,-1.00773612825244,
12.5813998171494));
#434923=CARTESIAN_POINT('Ctrl Pts',(-2.47147118025235,-1.00692585411597,
12.58127954464));
#434924=CARTESIAN_POINT('Ctrl Pts',(-2.47200070969148,-1.00618079124599,
12.5810700125799));
#434925=CARTESIAN_POINT('Ctrl Pts',(-2.47264032096221,-1.00528084013127,
12.5808169217085));
#434926=CARTESIAN_POINT('Ctrl Pts',(-2.47339492940163,-1.00448564552451,
12.5804173076348));
#434927=CARTESIAN_POINT('Ctrl Pts',(-2.47417951190356,-1.00384697059521,
12.5799304713245));
#434928=CARTESIAN_POINT('Ctrl Pts',(-2.47515185679244,-1.00305545115446,
12.5793271277669));
#434929=CARTESIAN_POINT('Ctrl Pts',(-2.476210226903,-1.0024302587701,12.5785808224116));
#434930=CARTESIAN_POINT('Ctrl Pts',(-2.47729387858476,-1.00197043826641,
12.5777485681082));
#434931=CARTESIAN_POINT('Ctrl Pts',(-2.4789086383135,-1.00128525533883,
12.576508418016));
#434932=CARTESIAN_POINT('Ctrl Pts',(-2.48056325289046,-1.00096671160168,
12.5750928681475));
#434933=CARTESIAN_POINT('Ctrl Pts',(-2.48198942389984,-1.00100786889864,
12.5737548217797));
#434934=CARTESIAN_POINT('Ctrl Pts',(-2.48198942389984,-1.00100786889864,
12.5737548217797));
#434935=CARTESIAN_POINT('Ctrl Pts',(-2.48492472314963,-0.984908561672269,
12.5770542771492));
#434936=CARTESIAN_POINT('Ctrl Pts',(-2.49625838937555,-0.984827048243808,
12.5893111709658));
#434937=CARTESIAN_POINT('Ctrl Pts',(-2.5067482336128,-1.00088021402104,
12.5508408821982));
#434938=CARTESIAN_POINT('Ctrl Pts',(-2.50968946539744,-0.984730449929319,
12.5540974840599));
#434939=CARTESIAN_POINT('Ctrl Pts',(-2.52103759047877,-0.984648832510594,
12.5663972313419));
#434940=CARTESIAN_POINT('Ctrl Pts',(-2.53148285100647,-1.00075150434887,
12.52790050457));
#434941=CARTESIAN_POINT('Ctrl Pts',(-2.53440677726936,-0.984552679312757,
12.5311362602938));
#434942=CARTESIAN_POINT('Ctrl Pts',(-2.54579179343984,-0.98447079656777,
12.5434568539655));
#434943=CARTESIAN_POINT('Ctrl Pts',(-2.55619515606317,-1.00062180800529,
12.5049357605811));
#434944=CARTESIAN_POINT('Ctrl Pts',(-2.55908160313967,-0.984375214261865,
12.5081700652078));
#434945=CARTESIAN_POINT('Ctrl Pts',(-2.57052295611833,-0.984292926334116,
12.5204921097672));
#434946=CARTESIAN_POINT('Ctrl Pts',(-2.55457244923555,-1.0006303227885,
12.5064436508395));
#434947=CARTESIAN_POINT('Ctrl Pts',(-2.55520418375856,-0.999586407426494,
12.5062361689309));
#434948=CARTESIAN_POINT('Ctrl Pts',(-2.5558166210962,-0.998473882313115,
12.5061871075061));
#434949=CARTESIAN_POINT('Ctrl Pts',(-2.55634795984499,-0.997365416808395,
12.5063648335164));
#434950=CARTESIAN_POINT('Ctrl Pts',(-2.55658932667902,-0.996861883403164,
12.5064455676329));
#434951=CARTESIAN_POINT('Ctrl Pts',(-2.55681712641728,-0.996352069238074,
12.506574497099));
#434952=CARTESIAN_POINT('Ctrl Pts',(-2.55702063217175,-0.995857404874738,
12.5067492519495));
#434953=CARTESIAN_POINT('Ctrl Pts',(-2.5574295848849,-0.994863357635075,
12.5071004286051));
#434954=CARTESIAN_POINT('Ctrl Pts',(-2.5577547208358,-0.993893633970525,
12.5076537929613));
#434955=CARTESIAN_POINT('Ctrl Pts',(-2.5579806046668,-0.993024023516777,
12.5083435010505));
#434956=CARTESIAN_POINT('Ctrl Pts',(-2.55799482540385,-0.992969276341902,
12.5083869222964));
#434957=CARTESIAN_POINT('Ctrl Pts',(-2.55800864275887,-0.992914916990364,
12.5084308732337));
#434958=CARTESIAN_POINT('Ctrl Pts',(-2.55802204907216,-0.992860960426174,
12.5084753333615));
#434959=CARTESIAN_POINT('Ctrl Pts',(-2.55812958539951,-0.992428157565093,
12.5088319622689));
#434960=CARTESIAN_POINT('Ctrl Pts',(-2.55821410983573,-0.992012795146706,
12.509227847131));
#434961=CARTESIAN_POINT('Ctrl Pts',(-2.55827585284676,-0.991627782415668,
12.5096423454524));
#434962=CARTESIAN_POINT('Ctrl Pts',(-2.55846932811701,-0.990421322916091,
12.5109411997424));
#434963=CARTESIAN_POINT('Ctrl Pts',(-2.55846055503325,-0.989440198498566,
12.5124831113042));
#434964=CARTESIAN_POINT('Ctrl Pts',(-2.55833585077837,-0.988645612238747,
12.5140723025007));
#434965=CARTESIAN_POINT('Ctrl Pts',(-2.5583241658531,-0.988571158635915,
12.5142212114565));
#434966=CARTESIAN_POINT('Ctrl Pts',(-2.55831148407854,-0.988498321961358,
12.5143705582413));
#434967=CARTESIAN_POINT('Ctrl Pts',(-2.55829788955917,-0.988427059481295,
12.5145201959299));
#434968=CARTESIAN_POINT('Ctrl Pts',(-2.5581232477178,-0.98751158682615,
12.5164425148273));
#434969=CARTESIAN_POINT('Ctrl Pts',(-2.55780253768352,-0.986822527428655,
12.5184635205941));
#434970=CARTESIAN_POINT('Ctrl Pts',(-2.55738680472768,-0.986285501460735,
12.5205025929158));
#434971=CARTESIAN_POINT('Ctrl Pts',(-2.55714566313518,-0.985974005113623,
12.5216853356836));
#434972=CARTESIAN_POINT('Ctrl Pts',(-2.55687336943095,-0.985713926484789,
12.5228750347131));
#434973=CARTESIAN_POINT('Ctrl Pts',(-2.55658456686307,-0.985494379393402,
12.5240609649613));
#434974=CARTESIAN_POINT('Ctrl Pts',(-2.55587571645393,-0.984955512835885,
12.5269717671327));
#434975=CARTESIAN_POINT('Ctrl Pts',(-2.55504117034121,-0.984653930717825,
12.5299036066169));
#434976=CARTESIAN_POINT('Ctrl Pts',(-2.55412310074475,-0.984513929495684,
12.5328133004019));
#434977=CARTESIAN_POINT('Ctrl Pts',(-2.55368237388086,-0.98444672075703,
12.5342101228452));
#434978=CARTESIAN_POINT('Ctrl Pts',(-2.55322286943268,-0.984417351235913,
12.5356023438238));
#434979=CARTESIAN_POINT('Ctrl Pts',(-2.55275086849392,-0.984420745855558,
12.5369868989719));
#434980=CARTESIAN_POINT('Origin',(-15.2975147215125,-0.887461820663325,
-1.23983318115551));
#434981=CARTESIAN_POINT('Ctrl Pts',(-2.51230959790793,-1.0833784309085,
12.5369868989719));
#434982=CARTESIAN_POINT('Ctrl Pts',(-2.52320897086175,-1.09417134399527,
12.5369868989719));
#434983=CARTESIAN_POINT('Ctrl Pts',(-2.5168506574729,-1.10813039677596,
12.5369868989719));
#434984=CARTESIAN_POINT('Ctrl Pts',(-2.51599396564969,-1.08702690468825,
12.5218025310016));
#434985=CARTESIAN_POINT('Ctrl Pts',(-2.52172008227195,-1.09736457619265,
12.5216901060418));
#434986=CARTESIAN_POINT('Ctrl Pts',(-2.51687005472745,-1.10808785179314,
12.5161920673678));
#434987=CARTESIAN_POINT('Ctrl Pts',(-2.52193756172439,-1.08602204803375,
12.5042015548895));
#434988=CARTESIAN_POINT('Ctrl Pts',(-2.52395457229035,-1.09213015849392,
12.4980677368514));
#434989=CARTESIAN_POINT('Ctrl Pts',(-2.52124997823278,-1.09836521668991,
12.4907278922776));
#434990=CARTESIAN_POINT('Ctrl Pts',(-2.52496637940152,-1.07309667615577,
12.506463626192));
#434991=CARTESIAN_POINT('Ctrl Pts',(-2.53098787677485,-1.07565577906879,
12.4999376786891));
#434992=CARTESIAN_POINT('Ctrl Pts',(-2.53091433293968,-1.07562452334764,
12.4906970594712));
#434993=CARTESIAN_POINT('Origin',(-2.49682978149281,-1.09901093818514,12.5369868989719));
#434994=CARTESIAN_POINT('Origin',(-2.49682978149281,-1.09901093818514,14.));
#434995=CARTESIAN_POINT('Origin',(-2.49682978149281,-1.09901093818514,13.7435492065112));
#434996=CARTESIAN_POINT('Ctrl Pts',(-2.49477862706859,-1.06595259098269,
13.793642941384));
#434997=CARTESIAN_POINT('Ctrl Pts',(-2.50246621943784,-1.07355569183496,
13.8071662555867));
#434998=CARTESIAN_POINT('Ctrl Pts',(-2.49240131733838,-1.08729312716194,
13.8103758687955));
#434999=CARTESIAN_POINT('Ctrl Pts',(-2.50656683636598,-1.07767009185895,
13.7804579775007));
#435000=CARTESIAN_POINT('Ctrl Pts',(-2.51604549960272,-1.08705884124179,
13.7901904343352));
#435001=CARTESIAN_POINT('Ctrl Pts',(-2.50891251606055,-1.10110791487494,
13.7927914348263));
#435002=CARTESIAN_POINT('Ctrl Pts',(-2.51350699879274,-1.0845686256309,
13.7597120340894));
#435003=CARTESIAN_POINT('Ctrl Pts',(-2.52447244887986,-1.0954381239799,
13.7635825532444));
#435004=CARTESIAN_POINT('Ctrl Pts',(-2.51863274757549,-1.10927408454719,
13.7651073818884));
#435005=CARTESIAN_POINT('Ctrl Pts',(-2.51214795607736,-1.08321773476046,
13.7381884353898));
#435006=CARTESIAN_POINT('Ctrl Pts',(-2.52285737214662,-1.0938321738922,
13.7368803041982));
#435007=CARTESIAN_POINT('Ctrl Pts',(-2.51672891949728,-1.10767528428125,
13.7363986145813));
#435008=CARTESIAN_POINT('Origin',(-2.48212954747994,-1.08439887436658,13.7902182540695));
#435009=CARTESIAN_POINT('Ctrl Pts',(-2.47226924880857,-1.04357818399006,
13.8235227101244));
#435010=CARTESIAN_POINT('Ctrl Pts',(-2.48042644875974,-1.05168020702606,
13.8358800583119));
#435011=CARTESIAN_POINT('Ctrl Pts',(-2.47104782899332,-1.06534284002023,
13.8390832900376));
#435012=CARTESIAN_POINT('Ctrl Pts',(-2.48072865212883,-1.05198684885194,
13.8124254819053));
#435013=CARTESIAN_POINT('Ctrl Pts',(-2.48890169305066,-1.06010460609919,
13.8247886449158));
#435014=CARTESIAN_POINT('Ctrl Pts',(-2.47949717086737,-1.07377485641168,
13.8279860620657));
#435015=CARTESIAN_POINT('Ctrl Pts',(-2.48918426421976,-1.06039174522379,
13.8013225099955));
#435016=CARTESIAN_POINT('Ctrl Pts',(-2.49736929116205,-1.06852140498214,
13.8136962257787));
#435017=CARTESIAN_POINT('Ctrl Pts',(-2.48794279258049,-1.08220277733194,
13.8168830918626));
#435018=CARTESIAN_POINT('Ctrl Pts',(-2.49763623259224,-1.06879301973175,
13.7902140179785));
#435019=CARTESIAN_POINT('Ctrl Pts',(-2.50582964255204,-1.07693100073291,
13.802602731458));
#435020=CARTESIAN_POINT('Ctrl Pts',(-2.49638484160682,-1.09062676239944,
13.8057746032558));
#435021=CARTESIAN_POINT('Origin',(-2.45676255485568,-1.05918402984193,13.8235269408515));
#435022=CARTESIAN_POINT('Ctrl Pts',(-2.49625838937555,-0.984827048243808,
13.8235269408515));
#435023=CARTESIAN_POINT('Ctrl Pts',(-2.50806556547983,-0.984742129261236,
13.8362179249168));
#435024=CARTESIAN_POINT('Ctrl Pts',(-2.51070655207738,-0.967869423673549,
13.8391868794938));
#435025=CARTESIAN_POINT('Ctrl Pts',(-2.48545533717591,-0.984904745416557,
13.8400110824519));
#435026=CARTESIAN_POINT('Ctrl Pts',(-2.49489720033065,-0.981415750858121,
13.8494522556837));
#435027=CARTESIAN_POINT('Ctrl Pts',(-2.49292858601838,-0.968109645299923,
13.85569149686));
#435028=CARTESIAN_POINT('Ctrl Pts',(-2.47064022047438,-0.991680440448419,
13.8586819406588));
#435029=CARTESIAN_POINT('Ctrl Pts',(-2.47229870031127,-0.987654836361377,
13.868010383617));
#435030=CARTESIAN_POINT('Ctrl Pts',(-2.46839592148099,-0.979490206290489,
13.8744918421245));
#435031=CARTESIAN_POINT('Ctrl Pts',(-2.45876480710159,-1.02062946556451,
13.8587686893867));
#435032=CARTESIAN_POINT('Ctrl Pts',(-2.45712103565668,-1.02461922036359,
13.8680909899357));
#435033=CARTESIAN_POINT('Ctrl Pts',(-2.44862922604038,-1.02768280828403,
13.8745789365163));
#435034=CARTESIAN_POINT('Ctrl Pts',(-2.46459752052836,-1.03595246873103,
13.8400379222776));
#435035=CARTESIAN_POINT('Ctrl Pts',(-2.46889230838958,-1.0450532945801,
13.8494748685453));
#435036=CARTESIAN_POINT('Ctrl Pts',(-2.4581794038028,-1.05317701174524,
13.8557104837033));
#435037=CARTESIAN_POINT('Ctrl Pts',(-2.47227204101088,-1.04358095838433,
13.8235269408542));
#435038=CARTESIAN_POINT('Ctrl Pts',(-2.4806462672494,-1.05190495704464,
13.8362179249195));
#435039=CARTESIAN_POINT('Ctrl Pts',(-2.47072418525568,-1.0658051474378,
13.8391868794965));
#435040=CARTESIAN_POINT('Origin',(-2.49610016616593,-0.962827617218985,
13.8235269408515));
#435041=CARTESIAN_POINT('Ctrl Pts',(-2.53202044341779,-0.984569841423958,
13.7902140241683));
#435042=CARTESIAN_POINT('Ctrl Pts',(-2.54356827512419,-0.984491239432124,
13.8026027327198));
#435043=CARTESIAN_POINT('Ctrl Pts',(-2.54640710301046,-0.968098588990368,
13.8057746032556));
#435044=CARTESIAN_POINT('Ctrl Pts',(-2.52010365538259,-0.98465554875306,
13.8013225161808));
#435045=CARTESIAN_POINT('Ctrl Pts',(-2.53163967556639,-0.984577023570956,
13.8136962270464));
#435046=CARTESIAN_POINT('Ctrl Pts',(-2.53448150603375,-0.96820746020147,
13.8168830918628));
#435047=CARTESIAN_POINT('Ctrl Pts',(-2.50818172991283,-0.984741293031374,
13.8124254880875));
#435048=CARTESIAN_POINT('Ctrl Pts',(-2.51970085863903,-0.984662881106717,
13.8247886461868));
#435049=CARTESIAN_POINT('Ctrl Pts',(-2.52255060261411,-0.968316642350521,
13.8279860620656));
#435050=CARTESIAN_POINT('Ctrl Pts',(-2.49625445902509,-0.98482707575475,
13.8235227163065));
#435051=CARTESIAN_POINT('Ctrl Pts',(-2.50775126113095,-0.984748816086976,
13.8358800595847));
#435052=CARTESIAN_POINT('Ctrl Pts',(-2.51061417570187,-0.968426146239254,
13.8390832900376));
#435053=CARTESIAN_POINT('Origin',(-2.5318661630017,-0.962570382801957,13.7902182540695));
#435054=CARTESIAN_POINT('Ctrl Pts',(-2.55248101537279,-0.984422659094525,
13.7382347919292));
#435055=CARTESIAN_POINT('Ctrl Pts',(-2.56757110230241,-0.984338129869166,
13.7369371795943));
#435056=CARTESIAN_POINT('Ctrl Pts',(-2.5728782039146,-0.970147342382266,
13.7364597369711));
#435057=CARTESIAN_POINT('Ctrl Pts',(-2.55437252506769,-0.984409055475106,
13.7595490285574));
#435058=CARTESIAN_POINT('Ctrl Pts',(-2.56982264290434,-0.984321504045932,
13.7633824266926));
#435059=CARTESIAN_POINT('Ctrl Pts',(-2.57532661145888,-0.970335797397424,
13.7648920890506));
#435060=CARTESIAN_POINT('Ctrl Pts',(-2.5447259292492,-0.984478433196848,
13.7803806590111));
#435061=CARTESIAN_POINT('Ctrl Pts',(-2.55808975877626,-0.984408102714666,
13.7901039518744));
#435062=CARTESIAN_POINT('Ctrl Pts',(-2.56284407749788,-0.969378734966195,
13.7926933640892));
#435063=CARTESIAN_POINT('Ctrl Pts',(-2.52795799232525,-0.984599027087206,
13.7936647693663));
#435064=CARTESIAN_POINT('Ctrl Pts',(-2.53877330767256,-0.984551216180718,
13.8072068914933));
#435065=CARTESIAN_POINT('Ctrl Pts',(-2.541190537481,-0.967675160068563,
13.8104111085397));
#435066=CARTESIAN_POINT('Origin',(-2.5525926452843,-0.962421314830735,13.7435492065112));
#435067=CARTESIAN_POINT('Origin',(-2.5525926452843,-0.962421314830735,14.));
#435068=CARTESIAN_POINT('Origin',(-2.5525926452843,-0.962421314830735,12.5369868989719));
#435069=CARTESIAN_POINT('Ctrl Pts',(-2.55455533228426,-1.00062361806097,
12.506462012331));
#435070=CARTESIAN_POINT('Ctrl Pts',(-2.56064355629324,-1.00300838564006,
12.4999388158272));
#435071=CARTESIAN_POINT('Ctrl Pts',(-2.560571524619,-1.00298017071217,12.4907030323752));
#435072=CARTESIAN_POINT('Ctrl Pts',(-2.56143590016693,-0.989270804807574,
12.5042014951932));
#435073=CARTESIAN_POINT('Ctrl Pts',(-2.56714935721315,-0.986321651421119,
12.4980716682127));
#435074=CARTESIAN_POINT('Ctrl Pts',(-2.56958091457031,-0.979980271914656,
12.4907355092743));
#435075=CARTESIAN_POINT('Ctrl Pts',(-2.55789615703068,-0.984392698640763,
12.5218047446509));
#435076=CARTESIAN_POINT('Ctrl Pts',(-2.56921524231361,-0.981016727773746,
12.5216906929434));
#435077=CARTESIAN_POINT('Ctrl Pts',(-2.57325716832047,-0.969969846381957,
12.5161988840776));
#435078=CARTESIAN_POINT('Ctrl Pts',(-2.55271245313378,-0.984420988602842,
12.5369868989719));
#435079=CARTESIAN_POINT('Ctrl Pts',(-2.56804211594788,-0.984337504913307,
12.5369868989719));
#435080=CARTESIAN_POINT('Ctrl Pts',(-2.57327252109055,-0.969927494727188,
12.5369868989719));
#435081=CARTESIAN_POINT('Origin',(-4.76969326057513E-31,-7.09909511483994E-31,
12.5));
#435082=CARTESIAN_POINT('Origin',(-2.40767974839161,-1.18501835034964,12.5));
#435083=CARTESIAN_POINT('',(-2.40767974839161,-1.18501835034964,12.5893111709658));
#435084=CARTESIAN_POINT('',(-2.40767974839161,-1.18501835034964,13.8235269408515));
#435085=CARTESIAN_POINT('',(-2.40767974839161,-1.18501835034964,12.5));
#435086=CARTESIAN_POINT('',(-2.44334770381643,-1.18767723263634,13.7902182540695));
#435087=CARTESIAN_POINT('',(-2.40767974839161,-1.18501835034964,13.8235269408515));
#435088=CARTESIAN_POINT('',(-2.46401737086258,-1.1892180613978,13.7435492065112));
#435089=CARTESIAN_POINT('Origin',(-2.39601441527465,-1.18414907999287,13.7445212918693));
#435090=CARTESIAN_POINT('',(-2.46401737086258,-1.1892180613978,12.5369868989719));
#435091=CARTESIAN_POINT('',(-2.46401737086258,-1.1892180613978,12.5));
#435092=CARTESIAN_POINT('Ctrl Pts',(-2.46401737086258,-1.1892180613978,
12.5369868989719));
#435093=CARTESIAN_POINT('Ctrl Pts',(-2.44525185978402,-1.18781917871968,
12.5544431401645));
#435094=CARTESIAN_POINT('Ctrl Pts',(-2.42647292711318,-1.18641929552349,
12.5718848856037));
#435095=CARTESIAN_POINT('Ctrl Pts',(-2.40767974839161,-1.18501835034964,
12.5893111709658));
#435096=CARTESIAN_POINT('Origin',(-2.55757155380599,-1.45074258662954,12.5));
#435097=CARTESIAN_POINT('',(-2.41567186698722,-1.28458189015483,13.7435492065112));
#435098=CARTESIAN_POINT('',(-2.40221156564333,-1.26882024123085,13.7902182540695));
#435099=CARTESIAN_POINT('Origin',(-2.36684022012061,-1.22740135202068,13.7418732680454));
#435100=CARTESIAN_POINT('',(-2.37898422350636,-1.24162165162673,13.8235269408515));
#435101=CARTESIAN_POINT('',(-2.40221156564333,-1.26882024123085,13.7902182540695));
#435102=CARTESIAN_POINT('',(-2.37898422350636,-1.24162165162673,12.5893111709658));
#435103=CARTESIAN_POINT('',(-2.37898422350636,-1.24162165162673,12.5));
#435104=CARTESIAN_POINT('',(-2.41567186698722,-1.28458189015483,12.5369868989719));
#435105=CARTESIAN_POINT('Ctrl Pts',(-2.37898422350636,-1.24162165162673,
12.5893111709658));
#435106=CARTESIAN_POINT('Ctrl Pts',(-2.39122253621053,-1.25595238489465,
12.5718848856037));
#435107=CARTESIAN_POINT('Ctrl Pts',(-2.40345157173885,-1.27027225484049,
12.5544431401645));
#435108=CARTESIAN_POINT('Ctrl Pts',(-2.41567186698722,-1.28458189015483,
12.5369868989719));
#435109=CARTESIAN_POINT('',(-2.41567186698722,-1.28458189015483,12.5));
#435110=CARTESIAN_POINT('Origin',(-2.40512434038171,-1.21929823533928,12.5));
#435111=CARTESIAN_POINT('',(-2.37498736607852,-1.20276484633319,13.8587068136939));
#435112=CARTESIAN_POINT('Ctrl Pts',(-2.37898422350124,-1.24162165163091,
13.8235269408542));
#435113=CARTESIAN_POINT('Ctrl Pts',(-2.37784626611898,-1.24028913430522,
13.8262006681044));
#435114=CARTESIAN_POINT('Ctrl Pts',(-2.37681385129937,-1.2388126697197,
13.8288634856214));
#435115=CARTESIAN_POINT('Ctrl Pts',(-2.37588031978227,-1.23720381037638,
13.8314912288862));
#435116=CARTESIAN_POINT('Ctrl Pts',(-2.37491794507746,-1.23554524233957,
13.834200161153));
#435117=CARTESIAN_POINT('Ctrl Pts',(-2.37405915970181,-1.23374437910986,
13.8368750301949));
#435118=CARTESIAN_POINT('Ctrl Pts',(-2.37332198838734,-1.23177643409771,
13.8394886372968));
#435119=CARTESIAN_POINT('Ctrl Pts',(-2.37326505485859,-1.23162444493085,
13.8396904925131));
#435120=CARTESIAN_POINT('Ctrl Pts',(-2.37320886583138,-1.23147144791995,
13.8398919674349));
#435121=CARTESIAN_POINT('Ctrl Pts',(-2.37315343994553,-1.23131742673428,
13.8400930404591));
#435122=CARTESIAN_POINT('Ctrl Pts',(-2.37228986735531,-1.22891767304111,
13.8432258934518));
#435123=CARTESIAN_POINT('Ctrl Pts',(-2.37161490042454,-1.22628191953871,
13.8462331177034));
#435124=CARTESIAN_POINT('Ctrl Pts',(-2.37124400375196,-1.22347219932811,
13.8489036603661));
#435125=CARTESIAN_POINT('Ctrl Pts',(-2.37112264204435,-1.22255282617684,
13.8497774930041));
#435126=CARTESIAN_POINT('Ctrl Pts',(-2.37103399946237,-1.22161501624451,
13.85061494757));
#435127=CARTESIAN_POINT('Ctrl Pts',(-2.37098257786962,-1.22066149144389,
13.8514076489583));
#435128=CARTESIAN_POINT('Ctrl Pts',(-2.37087381378487,-1.21864464897173,
13.8530843267192));
#435129=CARTESIAN_POINT('Ctrl Pts',(-2.3709238404227,-1.21635923447046,
13.8546805203176));
#435130=CARTESIAN_POINT('Ctrl Pts',(-2.37126616728438,-1.21394087859148,
13.8559412814274));
#435131=CARTESIAN_POINT('Ctrl Pts',(-2.3713119817204,-1.21361722414575,
13.8561100121513));
#435132=CARTESIAN_POINT('Ctrl Pts',(-2.37136296666668,-1.21329122965459,
13.8562727473908));
#435133=CARTESIAN_POINT('Ctrl Pts',(-2.37141937349435,-1.21296325246101,
13.8564289040185));
#435134=CARTESIAN_POINT('Ctrl Pts',(-2.37167517781431,-1.21147587962978,
13.8571370725437));
#435135=CARTESIAN_POINT('Ctrl Pts',(-2.37204922902188,-1.20992197228575,
13.8577210840554));
#435136=CARTESIAN_POINT('Ctrl Pts',(-2.37255552069773,-1.2083687994534,
13.8581177131616));
#435137=CARTESIAN_POINT('Ctrl Pts',(-2.37269810985969,-1.20793137252523,
13.8582294175695));
#435138=CARTESIAN_POINT('Ctrl Pts',(-2.37285101168534,-1.2074939829625,
13.8583265086086));
#435139=CARTESIAN_POINT('Ctrl Pts',(-2.37301410610544,-1.20705805579035,
13.8584082369006));
#435140=CARTESIAN_POINT('Ctrl Pts',(-2.37324842905163,-1.20643174534246,
13.8585256585398));
#435141=CARTESIAN_POINT('Ctrl Pts',(-2.37350700756429,-1.20580078034851,
13.8586122832068));
#435142=CARTESIAN_POINT('Ctrl Pts',(-2.37378385523008,-1.20518185090458,
13.8586682984299));
#435143=CARTESIAN_POINT('Ctrl Pts',(-2.37400530591969,-1.20468676870193,
13.8587131050557));
#435144=CARTESIAN_POINT('Ctrl Pts',(-2.37424067784936,-1.2041938234134,
13.8587357943552));
#435145=CARTESIAN_POINT('Ctrl Pts',(-2.37449045600862,-1.2037031746823,
13.8587355499465));
#435146=CARTESIAN_POINT('Ctrl Pts',(-2.37465189358794,-1.20338605670978,
13.8587353919793));
#435147=CARTESIAN_POINT('Ctrl Pts',(-2.37481756891859,-1.20307330981514,
13.8587257282814));
#435148=CARTESIAN_POINT('Ctrl Pts',(-2.37498736607852,-1.20276484633319,
13.8587068136939));
#435149=CARTESIAN_POINT('Ctrl Pts',(-2.37498736607852,-1.20276484633319,
13.8587068136939));
#435150=CARTESIAN_POINT('Ctrl Pts',(-2.37554581968092,-1.20175032675711,
13.8586446046466));
#435151=CARTESIAN_POINT('Ctrl Pts',(-2.37614880518103,-1.20078208375401,
13.858482427929));
#435152=CARTESIAN_POINT('Ctrl Pts',(-2.37679269852259,-1.19985749965825,
13.8582284286032));
#435153=CARTESIAN_POINT('Ctrl Pts',(-2.37745325819027,-1.19890898392803,
13.8579678548414));
#435154=CARTESIAN_POINT('Ctrl Pts',(-2.37815974125487,-1.1980049748111,
13.857615680862));
#435155=CARTESIAN_POINT('Ctrl Pts',(-2.37887666037631,-1.19717514562335,
13.8571944833187));
#435156=CARTESIAN_POINT('Ctrl Pts',(-2.38066580536432,-1.19510422201738,
13.8561433417727));
#435157=CARTESIAN_POINT('Ctrl Pts',(-2.38260000829739,-1.19339528696266,
13.8546163505475));
#435158=CARTESIAN_POINT('Ctrl Pts',(-2.38447423824122,-1.19202150424076,
13.8528973491086));
#435159=CARTESIAN_POINT('Ctrl Pts',(-2.38481663240028,-1.19177053440573,
13.8525833129073));
#435160=CARTESIAN_POINT('Ctrl Pts',(-2.38515700357976,-1.19153061022133,
13.8522628768812));
#435161=CARTESIAN_POINT('Ctrl Pts',(-2.38549410253113,-1.19130138925773,
13.851937733538));
#435162=CARTESIAN_POINT('Ctrl Pts',(-2.38755271905675,-1.18990156863601,
13.8499521282529));
#435163=CARTESIAN_POINT('Ctrl Pts',(-2.38969618286566,-1.1887651679106,
13.847639871647));
#435164=CARTESIAN_POINT('Ctrl Pts',(-2.39177420895342,-1.18788093024152,
13.8452109780794));
#435165=CARTESIAN_POINT('Ctrl Pts',(-2.3927091559033,-1.18748309341139,
13.8441181685877));
#435166=CARTESIAN_POINT('Ctrl Pts',(-2.39363082110264,-1.18713558470153,
13.8430021611332));
#435167=CARTESIAN_POINT('Ctrl Pts',(-2.39452638516502,-1.18683418603786,
13.8418824960098));
#435168=CARTESIAN_POINT('Ctrl Pts',(-2.39663680474706,-1.18612393239045,
13.8392439765549));
#435169=CARTESIAN_POINT('Ctrl Pts',(-2.39870195975365,-1.18563219977946,
13.8364981347964));
#435170=CARTESIAN_POINT('Ctrl Pts',(-2.40071938510556,-1.18532439792381,
13.8336931113419));
#435171=CARTESIAN_POINT('Ctrl Pts',(-2.40268422927996,-1.18502461846363,
13.8309611966328));
#435172=CARTESIAN_POINT('Ctrl Pts',(-2.40460585344843,-1.1848995645067,
13.8281701127186));
#435173=CARTESIAN_POINT('Ctrl Pts',(-2.40647336740714,-1.18495562513197,
13.8253580685121));
#435174=CARTESIAN_POINT('Ctrl Pts',(-2.40687824644888,-1.18496777913603,
13.8247484142933));
#435175=CARTESIAN_POINT('Ctrl Pts',(-2.40728048134637,-1.18498858682488,
13.8241378483365));
#435176=CARTESIAN_POINT('Ctrl Pts',(-2.40767974839161,-1.18501835034964,
13.8235269408515));
#435177=CARTESIAN_POINT('',(-2.37440967983503,-1.20386441691394,12.5969504640361));
#435178=CARTESIAN_POINT('Origin',(-2.40515393881772,-1.21931302098757,12.584524458991));
#435179=CARTESIAN_POINT('Origin',(-2.40515393881772,-1.21931302098757,12.584524458991));
#435180=CARTESIAN_POINT('Ctrl Pts',(-2.37898422350636,-1.24162165162673,
12.5893111709658));
#435181=CARTESIAN_POINT('Ctrl Pts',(-2.37162385426222,-1.23300285825703,
12.5770542771492));
#435182=CARTESIAN_POINT('Ctrl Pts',(-2.38186868662488,-1.22024170295212,
12.5737548217797));
#435183=CARTESIAN_POINT('Ctrl Pts',(-2.39507888082995,-1.26046806017326,
12.5663937883685));
#435184=CARTESIAN_POINT('Ctrl Pts',(-2.38770912241267,-1.25183827233565,
12.5540940315304));
#435185=CARTESIAN_POINT('Ctrl Pts',(-2.39798820550788,-1.23903958310452,
12.5508374392248));
#435186=CARTESIAN_POINT('Ctrl Pts',(-2.41115729884161,-1.27929545292459,
12.5434499600945));
#435187=CARTESIAN_POINT('Ctrl Pts',(-2.40376357871525,-1.27063760657353,
12.5311293540533));
#435188=CARTESIAN_POINT('Ctrl Pts',(-2.41409107962181,-1.25781986536901,
12.5278936106989));
#435189=CARTESIAN_POINT('Ctrl Pts',(-2.42722074958886,-1.29810531941401,
12.5204817579905));
#435190=CARTESIAN_POINT('Ctrl Pts',(-2.41979043560079,-1.28940462264037,
12.5081597038247));
#435191=CARTESIAN_POINT('Ctrl Pts',(-2.43017859214625,-1.27658392654064,
12.5049254088044));
#435192=CARTESIAN_POINT('Ctrl Pts',(-2.41567186698722,-1.28458189015483,
12.5369868989719));
#435193=CARTESIAN_POINT('Ctrl Pts',(-2.4162767942133,-1.28529024333077,
12.5342545179733));
#435194=CARTESIAN_POINT('Ctrl Pts',(-2.41694897102025,-1.28588525211521,
12.5314872231885));
#435195=CARTESIAN_POINT('Ctrl Pts',(-2.41768758476792,-1.28629154122643,
12.5287124745063));
#435196=CARTESIAN_POINT('Ctrl Pts',(-2.41835370330707,-1.28665795291332,
12.5262100684184));
#435197=CARTESIAN_POINT('Ctrl Pts',(-2.41907365915844,-1.28686964115061,
12.5237004536639));
#435198=CARTESIAN_POINT('Ctrl Pts',(-2.41987851416296,-1.28686664229789,
12.5212220730815));
#435199=CARTESIAN_POINT('Ctrl Pts',(-2.42049470029444,-1.28686434641671,
12.5193246583486));
#435200=CARTESIAN_POINT('Ctrl Pts',(-2.42116800968327,-1.28673555553964,
12.517417831369));
#435201=CARTESIAN_POINT('Ctrl Pts',(-2.42189937769354,-1.28638304236677,
12.5155812248347));
#435202=CARTESIAN_POINT('Ctrl Pts',(-2.42221094439704,-1.28623286986036,
12.5147988205793));
#435203=CARTESIAN_POINT('Ctrl Pts',(-2.42253348417723,-1.28604219320495,
12.5140295443047));
#435204=CARTESIAN_POINT('Ctrl Pts',(-2.42286891247307,-1.28580455774634,
12.5132817086137));
#435205=CARTESIAN_POINT('Ctrl Pts',(-2.42337653782311,-1.28544492862634,
12.5121499604604));
#435206=CARTESIAN_POINT('Ctrl Pts',(-2.42392050890739,-1.28496414949169,
12.5110494206568));
#435207=CARTESIAN_POINT('Ctrl Pts',(-2.42448645348953,-1.28432786430119,
12.5100666561695));
#435208=CARTESIAN_POINT('Ctrl Pts',(-2.42481141756533,-1.28396251081004,
12.5095023550641));
#435209=CARTESIAN_POINT('Ctrl Pts',(-2.42514689329859,-1.28354123136856,
12.5089719619137));
#435210=CARTESIAN_POINT('Ctrl Pts',(-2.42548159623306,-1.28306794368374,
12.5085043804652));
#435211=CARTESIAN_POINT('Ctrl Pts',(-2.42597139037954,-1.28237534880706,
12.5078201359221));
#435212=CARTESIAN_POINT('Ctrl Pts',(-2.42647274915835,-1.28155059588188,
12.5072563000949));
#435213=CARTESIAN_POINT('Ctrl Pts',(-2.42694445360708,-1.28064519337502,
12.5068768744332));
#435214=CARTESIAN_POINT('Ctrl Pts',(-2.42728458498685,-1.27999233583945,
12.5066032824114));
#435215=CARTESIAN_POINT('Ctrl Pts',(-2.42761532674451,-1.27928610336327,
12.5064197834844));
#435216=CARTESIAN_POINT('Ctrl Pts',(-2.42792055027233,-1.27856703007399,
12.5063282718343));
#435217=CARTESIAN_POINT('Ctrl Pts',(-2.42836608212811,-1.27751740569111,
12.5061946931565));
#435218=CARTESIAN_POINT('Ctrl Pts',(-2.42876774286086,-1.27641840198969,
12.5062515701262));
#435219=CARTESIAN_POINT('Ctrl Pts',(-2.42911512955636,-1.27534353357797,
12.5064436508398));
#435220=CARTESIAN_POINT('',(-2.38186868662489,-1.22024170295212,12.5737548217797));
#435221=CARTESIAN_POINT('Origin',(-2.39571389830658,-1.22733466520276,12.5893111709658));
#435222=CARTESIAN_POINT('Ctrl Pts',(-2.42911512955636,-1.27534353357797,
12.5064436508398));
#435223=CARTESIAN_POINT('Ctrl Pts',(-2.42212179323652,-1.2671867183374,
12.5164271754438));
#435224=CARTESIAN_POINT('Ctrl Pts',(-2.41512552614109,-1.25902680573062,
12.5264061185523));
#435225=CARTESIAN_POINT('Ctrl Pts',(-2.40812622576917,-1.25086368605492,
12.536380305637));
#435226=CARTESIAN_POINT('Ctrl Pts',(-2.39937851991535,-1.24066144211936,
12.5488460165097));
#435227=CARTESIAN_POINT('Ctrl Pts',(-2.39062607350234,-1.23045418576666,
12.5613043021964));
#435228=CARTESIAN_POINT('Ctrl Pts',(-2.38186868662488,-1.22024170295212,
12.5737548217797));
#435229=CARTESIAN_POINT('Ctrl Pts',(-2.40767974839161,-1.18501835034964,
12.5893111709658));
#435230=CARTESIAN_POINT('Ctrl Pts',(-2.39637714990393,-1.18417579353485,
12.5770542771492));
#435231=CARTESIAN_POINT('Ctrl Pts',(-2.39213937462263,-1.19998227750568,
12.5737548217797));
#435232=CARTESIAN_POINT('Ctrl Pts',(-2.39713452230741,-1.18423225216962,
12.5928319619712));
#435233=CARTESIAN_POINT('Ctrl Pts',(-2.38929630014685,-1.18691473045154,
12.5821634970843));
#435234=CARTESIAN_POINT('Ctrl Pts',(-2.38829870568296,-1.19968650822855,
12.5773203894503));
#435235=CARTESIAN_POINT('Ctrl Pts',(-2.38143324525357,-1.19006783253646,
12.5969440695591));
#435236=CARTESIAN_POINT('Ctrl Pts',(-2.3795993381404,-1.19364488820449,
12.5878292599214));
#435237=CARTESIAN_POINT('Ctrl Pts',(-2.38270316292309,-1.20176834595517,
12.5813877129824));
#435238=CARTESIAN_POINT('Ctrl Pts',(-2.36755007499711,-1.21733379720254,
12.596957478804));
#435239=CARTESIAN_POINT('Ctrl Pts',(-2.3693705003752,-1.21378321350521,
12.5878468778671));
#435240=CARTESIAN_POINT('Ctrl Pts',(-2.37773949954914,-1.21152991930245,
12.5814011370086));
#435241=CARTESIAN_POINT('Ctrl Pts',(-2.37210709191346,-1.23356871648057,
12.5928371701607));
#435242=CARTESIAN_POINT('Ctrl Pts',(-2.36964533984581,-1.22566461359273,
12.5821692192951));
#435243=CARTESIAN_POINT('Ctrl Pts',(-2.37935175281402,-1.21730941345999,
12.5773318885715));
#435244=CARTESIAN_POINT('Ctrl Pts',(-2.37898422350631,-1.24162165162676,
12.5893111709658));
#435245=CARTESIAN_POINT('Ctrl Pts',(-2.37162385426218,-1.23300285825706,
12.5770542771492));
#435246=CARTESIAN_POINT('Ctrl Pts',(-2.38186868662484,-1.22024170295216,
12.5737548217797));
#435247=CARTESIAN_POINT('',(-2.39213937462263,-1.19998227750568,12.5737548217797));
#435248=CARTESIAN_POINT('Origin',(-2.40604428726527,-1.20695747674301,12.5893111709658));
#435249=CARTESIAN_POINT('Ctrl Pts',(-2.38186868662484,-1.22024170295216,
12.5737548217797));
#435250=CARTESIAN_POINT('Ctrl Pts',(-2.38119336759526,-1.21950125454794,
12.5746934679442));
#435251=CARTESIAN_POINT('Ctrl Pts',(-2.38058142862772,-1.2185584575718,
12.5756680099006));
#435252=CARTESIAN_POINT('Ctrl Pts',(-2.38009969778665,-1.2175223885274,
12.5765688348656));
#435253=CARTESIAN_POINT('Ctrl Pts',(-2.37997216487942,-1.21724810071756,
12.5768073183026));
#435254=CARTESIAN_POINT('Ctrl Pts',(-2.37985355810775,-1.21696743763857,
12.5770407398754));
#435255=CARTESIAN_POINT('Ctrl Pts',(-2.37974460486843,-1.21668265643388,
12.5772674179684));
#435256=CARTESIAN_POINT('Ctrl Pts',(-2.37929749023645,-1.21551399137792,
12.5781976435658));
#435257=CARTESIAN_POINT('Ctrl Pts',(-2.37899808705842,-1.21420556666868,
12.5790594849312));
#435258=CARTESIAN_POINT('Ctrl Pts',(-2.37891368401597,-1.21283495773463,
12.5797571720116));
#435259=CARTESIAN_POINT('Ctrl Pts',(-2.37885869239895,-1.21194195673139,
12.580211740231));
#435260=CARTESIAN_POINT('Ctrl Pts',(-2.37891120643998,-1.21098082237251,
12.5806009430798));
#435261=CARTESIAN_POINT('Ctrl Pts',(-2.37908521968949,-1.21002018089239,
12.5808812374708));
#435262=CARTESIAN_POINT('Ctrl Pts',(-2.37923475479911,-1.20919467117148,
12.5811221033394));
#435263=CARTESIAN_POINT('Ctrl Pts',(-2.37947718481323,-1.20835264537558,
12.581287365893));
#435264=CARTESIAN_POINT('Ctrl Pts',(-2.37980683909001,-1.20754393569884,
12.581359338449));
#435265=CARTESIAN_POINT('Ctrl Pts',(-2.37985265422739,-1.20743154175299,
12.5813693411482));
#435266=CARTESIAN_POINT('Ctrl Pts',(-2.3799001093794,-1.20731975152665,
12.5813775999465));
#435267=CARTESIAN_POINT('Ctrl Pts',(-2.37994914421397,-1.2072086572213,
12.5813841266931));
#435268=CARTESIAN_POINT('Ctrl Pts',(-2.38003233774148,-1.20702017229568,
12.5813952001081));
#435269=CARTESIAN_POINT('Ctrl Pts',(-2.38012119263679,-1.20683267407251,
12.5814007534795));
#435270=CARTESIAN_POINT('Ctrl Pts',(-2.38021584841197,-1.20664632866722,
12.5814005856065));
#435271=CARTESIAN_POINT('Ctrl Pts',(-2.38064914554274,-1.20579331225815,
12.5813998171494));
#435272=CARTESIAN_POINT('Ctrl Pts',(-2.38117375882807,-1.20502323661152,
12.58127954464));
#435273=CARTESIAN_POINT('Ctrl Pts',(-2.38176225584241,-1.20432381444198,
12.5810700125799));
#435274=CARTESIAN_POINT('Ctrl Pts',(-2.38247309322999,-1.20347899209677,
12.5808169217085));
#435275=CARTESIAN_POINT('Ctrl Pts',(-2.38329000651475,-1.20274795102772,
12.5804173076348));
#435276=CARTESIAN_POINT('Ctrl Pts',(-2.38412403631904,-1.20217535199418,
12.5799304713245));
#435277=CARTESIAN_POINT('Ctrl Pts',(-2.38515766199304,-1.20146572140433,
12.5793271277669));
#435278=CARTESIAN_POINT('Ctrl Pts',(-2.3862634694477,-1.20092887628549,
12.5785808224116));
#435279=CARTESIAN_POINT('Ctrl Pts',(-2.3873809950077,-1.2005589134688,12.5777485681082));
#435280=CARTESIAN_POINT('Ctrl Pts',(-2.38904623052617,-1.20000762833946,
12.576508418016));
#435281=CARTESIAN_POINT('Ctrl Pts',(-2.39072130378142,-1.19982501097904,
12.5750928681475));
#435282=CARTESIAN_POINT('Ctrl Pts',(-2.39213937462263,-1.19998227750568,
12.5737548217797));
#435283=CARTESIAN_POINT('Ctrl Pts',(-2.39213937462263,-1.19998227750568,
12.5737548217797));
#435284=CARTESIAN_POINT('Ctrl Pts',(-2.39637714990393,-1.18417579353485,
12.5770542771492));
#435285=CARTESIAN_POINT('Ctrl Pts',(-2.40767974839161,-1.18501835034964,
12.5893111709658));
#435286=CARTESIAN_POINT('Ctrl Pts',(-2.41682620649634,-1.20187312023033,
12.5508408821982));
#435287=CARTESIAN_POINT('Ctrl Pts',(-2.42107400727543,-1.18601683084187,
12.55409748406));
#435288=CARTESIAN_POINT('Ctrl Pts',(-2.43239102498403,-1.18686046254337,
12.5663972313419));
#435289=CARTESIAN_POINT('Ctrl Pts',(-2.44148901252426,-1.20376093977156,
12.52790050457));
#435290=CARTESIAN_POINT('Ctrl Pts',(-2.44572356428675,-1.18785434212425,
12.5311362602938));
#435291=CARTESIAN_POINT('Ctrl Pts',(-2.45707737195896,-1.18870071634859,
12.5434568539655));
#435292=CARTESIAN_POINT('Ctrl Pts',(-2.46612966088055,-1.20564595726182,
12.5049357605811));
#435293=CARTESIAN_POINT('Ctrl Pts',(-2.47033075175862,-1.18968869495203,
12.5081700652078));
#435294=CARTESIAN_POINT('Ctrl Pts',(-2.48174074180913,-1.19053925731467,
12.5204921097672));
#435295=CARTESIAN_POINT('Ctrl Pts',(-2.46451165944216,-1.20552217804186,
12.5064436508395));
#435296=CARTESIAN_POINT('Ctrl Pts',(-2.46522638071389,-1.20453322845048,
12.5062361689309));
#435297=CARTESIAN_POINT('Ctrl Pts',(-2.46592746134174,-1.20347432450124,
12.5061871075061));
#435298=CARTESIAN_POINT('Ctrl Pts',(-2.4665473823338,-1.20241285636478,
12.5063648335164));
#435299=CARTESIAN_POINT('Ctrl Pts',(-2.4668289886867,-1.20193067206313,
12.5064455676329));
#435300=CARTESIAN_POINT('Ctrl Pts',(-2.46709758502746,-1.20144112205608,
12.506574497099));
#435301=CARTESIAN_POINT('Ctrl Pts',(-2.46734073337117,-1.20096469125585,
12.5067492519495));
#435302=CARTESIAN_POINT('Ctrl Pts',(-2.46782934940616,-1.20000728506915,
12.5071004286051));
#435303=CARTESIAN_POINT('Ctrl Pts',(-2.46823244497511,-1.1990672896786,
12.5076537929612));
#435304=CARTESIAN_POINT('Ctrl Pts',(-2.46852845852134,-1.19821898441121,
12.5083435010503));
#435305=CARTESIAN_POINT('Ctrl Pts',(-2.4685470943431,-1.19816557852503,
12.5083869222963));
#435306=CARTESIAN_POINT('Ctrl Pts',(-2.46856529651385,-1.19811252629235,
12.5084308732336));
#435307=CARTESIAN_POINT('Ctrl Pts',(-2.46858305617966,-1.19805984200306,
12.5084753333616));
#435308=CARTESIAN_POINT('Ctrl Pts',(-2.46872551213987,-1.1976372444668,
12.508831962269));
#435309=CARTESIAN_POINT('Ctrl Pts',(-2.46884361122113,-1.19723015365885,
12.509227847131));
#435310=CARTESIAN_POINT('Ctrl Pts',(-2.46893653089925,-1.1968514546545,
12.5096423454524));
#435311=CARTESIAN_POINT('Ctrl Pts',(-2.46922770004594,-1.19566477958005,
12.5109411997424));
#435312=CARTESIAN_POINT('Ctrl Pts',(-2.46929892690224,-1.19468620468532,
12.5124831113042));
#435313=CARTESIAN_POINT('Ctrl Pts',(-2.46923940374723,-1.19388409779126,
12.5140723025007));
#435314=CARTESIAN_POINT('Ctrl Pts',(-2.46923382636241,-1.19380893949676,
12.5142212114565));
#435315=CARTESIAN_POINT('Ctrl Pts',(-2.46922712365056,-1.19373531149787,
12.5143705582413));
#435316=CARTESIAN_POINT('Ctrl Pts',(-2.46921938291953,-1.1936631780583,
12.5145201959299));
#435317=CARTESIAN_POINT('Ctrl Pts',(-2.4691199417047,-1.19273651663152,
12.5164425148273));
#435318=CARTESIAN_POINT('Ctrl Pts',(-2.46885646354442,-1.19202360917721,
12.5184635205941));
#435319=CARTESIAN_POINT('Ctrl Pts',(-2.4684858865076,-1.19145448402352,
12.5205025929158));
#435320=CARTESIAN_POINT('Ctrl Pts',(-2.46827093713793,-1.19112436887637,
12.5216853356836));
#435321=CARTESIAN_POINT('Ctrl Pts',(-2.46802074829123,-1.19084296117297,
12.5228750347131));
#435322=CARTESIAN_POINT('Ctrl Pts',(-2.4677508018162,-1.19060060451602,
12.5240609649613));
#435323=CARTESIAN_POINT('Ctrl Pts',(-2.46708823267535,-1.19000575310353,
12.5269717671327));
#435324=CARTESIAN_POINT('Ctrl Pts',(-2.46628104518835,-1.18963715121935,
12.5299036066169));
#435325=CARTESIAN_POINT('Ctrl Pts',(-2.46537744179204,-1.18942278464467,
12.532813300402));
#435326=CARTESIAN_POINT('Ctrl Pts',(-2.46494365954657,-1.18931987620664,
12.5342101228452));
#435327=CARTESIAN_POINT('Ctrl Pts',(-2.46448807795016,-1.18925315053182,
12.5356023438239));
#435328=CARTESIAN_POINT('Ctrl Pts',(-2.46401737086258,-1.1892180613978,
12.5369868989719));
#435329=CARTESIAN_POINT('Origin',(-15.1745209143218,-2.13141609154649,-1.24009674915699));
#435330=CARTESIAN_POINT('Ctrl Pts',(-2.41564469525815,-1.28455013392597,
12.5369868989719));
#435331=CARTESIAN_POINT('Ctrl Pts',(-2.42562807883452,-1.29619553456537,
12.5369868989719));
#435332=CARTESIAN_POINT('Ctrl Pts',(-2.41815312981779,-1.30958987818059,
12.5369868989719));
#435333=CARTESIAN_POINT('Ctrl Pts',(-2.41901941908637,-1.28848677788516,
12.5218025310015));
#435334=CARTESIAN_POINT('Ctrl Pts',(-2.42388386633006,-1.29925678330379,
12.5216901060418));
#435335=CARTESIAN_POINT('Ctrl Pts',(-2.41817593034064,-1.30954905581901,
12.5161920673677));
#435336=CARTESIAN_POINT('Ctrl Pts',(-2.42502514348139,-1.287969723066,12.5042015548895));
#435337=CARTESIAN_POINT('Ctrl Pts',(-2.42653757490369,-1.29422191437866,
12.4980677368513));
#435338=CARTESIAN_POINT('Ctrl Pts',(-2.42333376503328,-1.30021577640893,
12.4907278922778));
#435339=CARTESIAN_POINT('Ctrl Pts',(-2.42909742081894,-1.27533423605555,
12.506463626192));
#435340=CARTESIAN_POINT('Ctrl Pts',(-2.43489029151153,-1.27837563170151,
12.4999376786891));
#435341=CARTESIAN_POINT('Ctrl Pts',(-2.43481954001884,-1.27833848547588,
12.4906970594712));
#435342=CARTESIAN_POINT('Origin',(-2.39894219218699,-1.2988688765788,12.5369868989719));
#435343=CARTESIAN_POINT('Origin',(-2.39894219218699,-1.2988688765788,14.));
#435344=CARTESIAN_POINT('Origin',(-2.39894219218699,-1.2988688765788,13.7435492065112));
#435345=CARTESIAN_POINT('Ctrl Pts',(-2.39959242500563,-1.26575334017198,
13.793642941384));
#435346=CARTESIAN_POINT('Ctrl Pts',(-2.40663471424226,-1.27395775247959,
13.8071662555867));
#435347=CARTESIAN_POINT('Ctrl Pts',(-2.39548357376296,-1.28682909466469,
13.8103758687955));
#435348=CARTESIAN_POINT('Ctrl Pts',(-2.41038632490764,-1.2783927005248,
13.7804579775006));
#435349=CARTESIAN_POINT('Ctrl Pts',(-2.41906817843885,-1.288522808668,13.7901904343352));
#435350=CARTESIAN_POINT('Ctrl Pts',(-2.41081379938462,-1.30194373078957,
13.7927914348263));
#435351=CARTESIAN_POINT('Ctrl Pts',(-2.41674109997117,-1.28583396766183,
13.7597120340895));
#435352=CARTESIAN_POINT('Ctrl Pts',(-2.42678409840478,-1.2975610846321,
13.7635825532444));
#435353=CARTESIAN_POINT('Ctrl Pts',(-2.41983606899175,-1.31087501731256,
13.7651073818884));
#435354=CARTESIAN_POINT('Ctrl Pts',(-2.41549668950532,-1.2843767971713,
13.7381884353898));
#435355=CARTESIAN_POINT('Ctrl Pts',(-2.42530529554721,-1.29582883446347,
13.7368803041982));
#435356=CARTESIAN_POINT('Ctrl Pts',(-2.41806889280862,-1.30912635725999,
13.7363986145813));
#435357=CARTESIAN_POINT('Origin',(-2.38548189084311,-1.28310722765482,13.7902182540695));
#435358=CARTESIAN_POINT('Ctrl Pts',(-2.37898166672864,-1.24161865887779,
13.8235227101244));
#435359=CARTESIAN_POINT('Ctrl Pts',(-2.38645133417696,-1.25035861062428,
13.8358800583119));
#435360=CARTESIAN_POINT('Ctrl Pts',(-2.3759902895674,-1.26321133775643,
13.8390832900376));
#435361=CARTESIAN_POINT('Ctrl Pts',(-2.38672753783373,-1.25068886450489,
13.8124254819052));
#435362=CARTESIAN_POINT('Ctrl Pts',(-2.3942117110589,-1.25944578929451,
13.8247886449157));
#435363=CARTESIAN_POINT('Ctrl Pts',(-2.38372422933846,-1.27230399711153,
13.8279860620657));
#435364=CARTESIAN_POINT('Ctrl Pts',(-2.3944699374914,-1.25975500516089,
13.8013225099955));
#435365=CARTESIAN_POINT('Ctrl Pts',(-2.40196508668937,-1.26852476982893,
13.8136962257787));
#435366=CARTESIAN_POINT('Ctrl Pts',(-2.39145479514605,-1.28139227139512,
13.8168830918626));
#435367=CARTESIAN_POINT('Ctrl Pts',(-2.40220900077034,-1.26881723900759,
13.7902140179785));
#435368=CARTESIAN_POINT('Ctrl Pts',(-2.40971182683348,-1.27759598052393,
13.802602731458));
#435369=CARTESIAN_POINT('Ctrl Pts',(-2.3991821209632,-1.29047633171505,
13.8057746032558));
#435370=CARTESIAN_POINT('Origin',(-2.36225454870613,-1.2559086380507,13.8235269408515));
#435371=CARTESIAN_POINT('Ctrl Pts',(-2.40767974839161,-1.18501835034964,
13.8235269408515));
#435372=CARTESIAN_POINT('Ctrl Pts',(-2.41945455877684,-1.18589610839295,
13.8362179249168));
#435373=CARTESIAN_POINT('Ctrl Pts',(-2.42346203985331,-1.16929481026663,
13.8391868794938));
#435374=CARTESIAN_POINT('Ctrl Pts',(-2.39690630941608,-1.18421523994654,
13.8400110824519));
#435375=CARTESIAN_POINT('Ctrl Pts',(-2.4066011409968,-1.18150745423075,
13.8494522556836));
#435376=CARTESIAN_POINT('Ctrl Pts',(-2.40572364821714,-1.16808516329897,
13.85569149686));
#435377=CARTESIAN_POINT('Ctrl Pts',(-2.38158820674563,-1.18976081986413,
13.8586819406588));
#435378=CARTESIAN_POINT('Ctrl Pts',(-2.38356929223266,-1.18588379214588,
13.868010383617));
#435379=CARTESIAN_POINT('Ctrl Pts',(-2.38034499272449,-1.17742821650172,
13.8744918421245));
#435380=CARTESIAN_POINT('Ctrl Pts',(-2.36739269353459,-1.21764556305143,
13.8587686893867));
#435381=CARTESIAN_POINT('Ctrl Pts',(-2.36542918954836,-1.22148805963776,
13.8680909899357));
#435382=CARTESIAN_POINT('Ctrl Pts',(-2.35671592487156,-1.22384929240428,
13.8745789365163));
#435383=CARTESIAN_POINT('Ctrl Pts',(-2.3719570320787,-1.23339300048152,
13.8400379222776));
#435384=CARTESIAN_POINT('Ctrl Pts',(-2.37549572759296,-1.24281360916491,
13.8494748685453));
#435385=CARTESIAN_POINT('Ctrl Pts',(-2.36415631094658,-1.25003709415377,
13.8557104837033));
#435386=CARTESIAN_POINT('Ctrl Pts',(-2.37898422350124,-1.24162165163091,
13.8235269408542));
#435387=CARTESIAN_POINT('Ctrl Pts',(-2.38665210202572,-1.25060053005331,
13.8362179249195));
#435388=CARTESIAN_POINT('Ctrl Pts',(-2.37563004038121,-1.26364572691502,
13.8391868794965));
#435389=CARTESIAN_POINT('Origin',(-2.40931520951794,-1.16307922395627,13.8235269408515));
#435390=CARTESIAN_POINT('Ctrl Pts',(-2.44334377189279,-1.18767693876742,
13.7902140241683));
#435391=CARTESIAN_POINT('Ctrl Pts',(-2.45485958593386,-1.18853985380613,
13.8026027327198));
#435392=CARTESIAN_POINT('Ctrl Pts',(-2.45902512104747,-1.17243313938355,
13.8057746032556));
#435393=CARTESIAN_POINT('Ctrl Pts',(-2.43145965004371,-1.18679103205752,
13.8013225161808));
#435394=CARTESIAN_POINT('Ctrl Pts',(-2.44296368560333,-1.18765306090166,
13.8136962270464));
#435395=CARTESIAN_POINT('Ctrl Pts',(-2.44713033149648,-1.17156960146924,
13.8168830918628));
#435396=CARTESIAN_POINT('Ctrl Pts',(-2.41957040484278,-1.18590474342528,
13.8124254880875));
#435397=CARTESIAN_POINT('Ctrl Pts',(-2.4310575959182,-1.1867655083394,13.8247886461867));
#435398=CARTESIAN_POINT('Ctrl Pts',(-2.435230227815,-1.17070594093389,13.8279860620656));
#435399=CARTESIAN_POINT('Ctrl Pts',(-2.40767582887667,-1.18501805740899,
13.8235227163066));
#435400=CARTESIAN_POINT('Ctrl Pts',(-2.41914075521139,-1.18587715424653,
13.8358800595848));
#435401=CARTESIAN_POINT('Ctrl Pts',(-2.42332459279511,-1.16984215085174,
13.8390832900376));
#435402=CARTESIAN_POINT('Origin',(-2.44498316494276,-1.16573810624297,13.7902182540695));
#435403=CARTESIAN_POINT('Ctrl Pts',(-2.46374825970872,-1.18919797273606,
13.7382347919292));
#435404=CARTESIAN_POINT('Ctrl Pts',(-2.47879502553553,-1.19034370694901,
13.7369371795942));
#435405=CARTESIAN_POINT('Ctrl Pts',(-2.48524114912593,-1.17663271618693,
13.7364597369712));
#435406=CARTESIAN_POINT('Ctrl Pts',(-2.46563458438239,-1.18933858998161,
13.7595490285574));
#435407=CARTESIAN_POINT('Ctrl Pts',(-2.48104042948073,-1.1905106579082,
13.7633824266926));
#435408=CARTESIAN_POINT('Ctrl Pts',(-2.4876660489628,-1.17702011207837,
13.7648920890506));
#435409=CARTESIAN_POINT('Ctrl Pts',(-2.45601443188735,-1.18862144974088,
13.780380659011));
#435410=CARTESIAN_POINT('Ctrl Pts',(-2.46933952696129,-1.18964062944777,
13.7901039518744));
#435411=CARTESIAN_POINT('Ctrl Pts',(-2.47530305907691,-1.17504879179339,
13.7926933640892));
#435412=CARTESIAN_POINT('Ctrl Pts',(-2.43929245936862,-1.18737489983978,
13.7936647693663));
#435413=CARTESIAN_POINT('Ctrl Pts',(-2.45007568467906,-1.18820879662543,
13.8072068914933));
#435414=CARTESIAN_POINT('Ctrl Pts',(-2.45386042659752,-1.17158592086766,
13.8104111085397));
#435415=CARTESIAN_POINT('Origin',(-2.46565283198891,-1.16727893500443,13.7435492065112));
#435416=CARTESIAN_POINT('Origin',(-2.46565283198891,-1.16727893500443,14.));
#435417=CARTESIAN_POINT('Origin',(-2.46565283198891,-1.16727893500443,12.5369868989719));
#435418=CARTESIAN_POINT('Ctrl Pts',(-2.46449514594364,-1.20551410043333,
12.506462012331));
#435419=CARTESIAN_POINT('Ctrl Pts',(-2.47036873119268,-1.20838717967208,
12.4999388158272));
#435420=CARTESIAN_POINT('Ctrl Pts',(-2.47029923897645,-1.20835318737687,
12.4907030323752));
#435421=CARTESIAN_POINT('Ctrl Pts',(-2.47227817897883,-1.19475989288802,
12.5042014951932));
#435422=CARTESIAN_POINT('Ctrl Pts',(-2.47821300834767,-1.19228625235656,
12.4980716682127));
#435423=CARTESIAN_POINT('Ctrl Pts',(-2.48115335619857,-1.18616416776537,
12.4907355092744));
#435424=CARTESIAN_POINT('Ctrl Pts',(-2.46914782498458,-1.18960949629008,
12.5218047446509));
#435425=CARTESIAN_POINT('Ctrl Pts',(-2.4807044199116,-1.18716736921946,
12.5216906929434));
#435426=CARTESIAN_POINT('Ctrl Pts',(-2.48563332013081,-1.17648669990714,
12.5161988840775));
#435427=CARTESIAN_POINT('Ctrl Pts',(-2.46397906354022,-1.18921517212888,
12.5369868989719));
#435428=CARTESIAN_POINT('Ctrl Pts',(-2.47926452286165,-1.19038147605744,
12.5369868989719));
#435429=CARTESIAN_POINT('Ctrl Pts',(-2.48565207386886,-1.1764457405673,
12.5369868989719));
#435430=CARTESIAN_POINT('Origin',(-4.59510497263915E-31,-7.48139013969503E-31,
12.5));
#435431=CARTESIAN_POINT('Origin',(-2.30307839592131,-1.37732355084816,12.5));
#435432=CARTESIAN_POINT('',(-2.30307839592131,-1.37732355084816,12.5893111709658));
#435433=CARTESIAN_POINT('',(-2.30307839592131,-1.37732355084816,13.8235269408515));
#435434=CARTESIAN_POINT('',(-2.30307839592131,-1.37732355084816,12.5));
#435435=CARTESIAN_POINT('',(-2.33841094557663,-1.38288085541566,13.7902182540695));
#435436=CARTESIAN_POINT('',(-2.30307839592131,-1.37732355084816,13.8235269408515));
#435437=CARTESIAN_POINT('',(-2.35888624416239,-1.38610132694861,13.7435492065112));
#435438=CARTESIAN_POINT('Origin',(-2.29152273184205,-1.3755063399721,13.7445212918693));
#435439=CARTESIAN_POINT('',(-2.35888624416239,-1.38610132694861,12.5369868989719));
#435440=CARTESIAN_POINT('',(-2.35888624416239,-1.38610132694861,12.5));
#435441=CARTESIAN_POINT('Ctrl Pts',(-2.35888624416239,-1.38610132694861,
12.5369868989719));
#435442=CARTESIAN_POINT('Ctrl Pts',(-2.34029719569876,-1.3831775355738,
12.5544431401645));
#435443=CARTESIAN_POINT('Ctrl Pts',(-2.32169485185361,-1.38025165302568,
12.5718848856037));
#435444=CARTESIAN_POINT('Ctrl Pts',(-2.30307839592131,-1.37732355084816,
12.5893111709658));
#435445=CARTESIAN_POINT('Origin',(-2.43081245659811,-1.65438118532145,12.5));
#435446=CARTESIAN_POINT('',(-2.30292856860467,-1.47720723304881,13.7435492065112));
#435447=CARTESIAN_POINT('',(-2.29079777601442,-1.46040089019251,13.7902182540695));
#435448=CARTESIAN_POINT('Origin',(-2.2589201497101,-1.41623672588671,13.7418732680448));
#435449=CARTESIAN_POINT('',(-2.26986465849441,-1.43139955763529,13.8235269408515));
#435450=CARTESIAN_POINT('',(-2.29079777601442,-1.46040089019251,13.7902182540695));
#435451=CARTESIAN_POINT('',(-2.26986465849441,-1.43139955763529,12.5893111709658));
#435452=CARTESIAN_POINT('',(-2.26986465849441,-1.43139955763529,12.5));
#435453=CARTESIAN_POINT('',(-2.30292856860467,-1.47720723304881,12.5369868989719));
#435454=CARTESIAN_POINT('Ctrl Pts',(-2.26986465849441,-1.43139955763529,
12.5893111709658));
#435455=CARTESIAN_POINT('Ctrl Pts',(-2.28089416142127,-1.4466801426708,
12.5718848856037));
#435456=CARTESIAN_POINT('Ctrl Pts',(-2.29191530350293,-1.46194914435509,
12.5544431401645));
#435457=CARTESIAN_POINT('Ctrl Pts',(-2.30292856860467,-1.47720723304881,
12.5369868989719));
#435458=CARTESIAN_POINT('',(-2.30292856860467,-1.47720723304881,12.5));
#435459=CARTESIAN_POINT('Origin',(-2.29773736195518,-1.41128108287233,12.5));
#435460=CARTESIAN_POINT('',(-2.26904829064012,-1.39234626417087,13.8587068136939));
#435461=CARTESIAN_POINT('Ctrl Pts',(-2.26986465848896,-1.43139955763904,
13.8235269408542));
#435462=CARTESIAN_POINT('Ctrl Pts',(-2.26883910009855,-1.42997872006389,
13.8262006681044));
#435463=CARTESIAN_POINT('Ctrl Pts',(-2.26793046612463,-1.42842301690021,
13.8288634856214));
#435464=CARTESIAN_POINT('Ctrl Pts',(-2.26713117782905,-1.42674341941851,
13.8314912288862));
#435465=CARTESIAN_POINT('Ctrl Pts',(-2.26630719403907,-1.42501192765731,
13.8342001611531));
#435466=CARTESIAN_POINT('Ctrl Pts',(-2.26559805327254,-1.42314705767076,
13.8368750301949));
#435467=CARTESIAN_POINT('Ctrl Pts',(-2.2650237406228,-1.42112557452759,
13.8394886372969));
#435468=CARTESIAN_POINT('Ctrl Pts',(-2.26497938506377,-1.42096945048101,
13.8396904925131));
#435469=CARTESIAN_POINT('Ctrl Pts',(-2.26493585367766,-1.4208123826277,
13.8398919674349));
#435470=CARTESIAN_POINT('Ctrl Pts',(-2.26489316637337,-1.42065435621056,
13.8400930404591));
#435471=CARTESIAN_POINT('Ctrl Pts',(-2.26422806945392,-1.41819219831672,
13.8432258934518));
#435472=CARTESIAN_POINT('Ctrl Pts',(-2.26377018679952,-1.41551019899573,
13.8462331177034));
#435473=CARTESIAN_POINT('Ctrl Pts',(-2.26362954253635,-1.4126795963753,
13.8489036603661));
#435474=CARTESIAN_POINT('Ctrl Pts',(-2.26358352209669,-1.41175339025651,
13.8497774930041));
#435475=CARTESIAN_POINT('Ctrl Pts',(-2.26357161468127,-1.41081147561601,
13.85061494757));
#435476=CARTESIAN_POINT('Ctrl Pts',(-2.26359808531297,-1.40985693225332,
13.8514076489583));
#435477=CARTESIAN_POINT('Ctrl Pts',(-2.26365407451668,-1.40783793537547,
13.8530843267192));
#435478=CARTESIAN_POINT('Ctrl Pts',(-2.2638902171936,-1.40556420303781,
13.8546805203176));
#435479=CARTESIAN_POINT('Ctrl Pts',(-2.26442852344596,-1.40318179685575,
13.8559412814274));
#435480=CARTESIAN_POINT('Ctrl Pts',(-2.26450056628021,-1.40286295364535,
13.8561100121513));
#435481=CARTESIAN_POINT('Ctrl Pts',(-2.26457795315569,-1.40254219962042,
13.8562727473908));
#435482=CARTESIAN_POINT('Ctrl Pts',(-2.26466090548036,-1.40221991142402,
13.8564289040185));
#435483=CARTESIAN_POINT('Ctrl Pts',(-2.26503709332639,-1.40075833813004,
13.8571370725437));
#435484=CARTESIAN_POINT('Ctrl Pts',(-2.26553655778373,-1.39924008993045,
13.8577210840553));
#435485=CARTESIAN_POINT('Ctrl Pts',(-2.26616776282059,-1.39773335262434,
13.8581177131616));
#435486=CARTESIAN_POINT('Ctrl Pts',(-2.26634553188439,-1.39730900353862,
13.8582294175695));
#435487=CARTESIAN_POINT('Ctrl Pts',(-2.26653357625172,-1.39688553227183,
13.8583265086086));
#435488=CARTESIAN_POINT('Ctrl Pts',(-2.26673166010008,-1.39646434932072,
13.8584082369006));
#435489=CARTESIAN_POINT('Ctrl Pts',(-2.26701625347188,-1.39585922236464,
13.8585256585398));
#435490=CARTESIAN_POINT('Ctrl Pts',(-2.26732540109047,-1.39525143340397,
13.8586122832068));
#435491=CARTESIAN_POINT('Ctrl Pts',(-2.26765177606403,-1.39465712905159,
13.8586682984299));
#435492=CARTESIAN_POINT('Ctrl Pts',(-2.26791284369037,-1.39418174448118,
13.8587131050557));
#435493=CARTESIAN_POINT('Ctrl Pts',(-2.26818761205666,-1.39370962442479,
13.8587357943552));
#435494=CARTESIAN_POINT('Ctrl Pts',(-2.26847655152625,-1.39324096752567,
13.8587355499465));
#435495=CARTESIAN_POINT('Ctrl Pts',(-2.26866329999401,-1.39293806339859,
13.8587353919793));
#435496=CARTESIAN_POINT('Ctrl Pts',(-2.2688539158289,-1.39263986122106,
13.8587257282814));
#435497=CARTESIAN_POINT('Ctrl Pts',(-2.26904829064012,-1.39234626417087,
13.8587068136939));
#435498=CARTESIAN_POINT('Ctrl Pts',(-2.26904829064012,-1.39234626417087,
13.8587068136939));
#435499=CARTESIAN_POINT('Ctrl Pts',(-2.26968757879808,-1.39138063947788,
13.8586446046467));
#435500=CARTESIAN_POINT('Ctrl Pts',(-2.27036747870724,-1.39046476713949,
13.858482427929));
#435501=CARTESIAN_POINT('Ctrl Pts',(-2.27108459173413,-1.38959574280588,
13.8582284286032));
#435502=CARTESIAN_POINT('Ctrl Pts',(-2.27182026628162,-1.38870422492876,
13.8579678548414));
#435503=CARTESIAN_POINT('Ctrl Pts',(-2.27259808371754,-1.38786080875602,
13.857615680862));
#435504=CARTESIAN_POINT('Ctrl Pts',(-2.2733802561323,-1.38709217632039,
13.8571944833187));
#435505=CARTESIAN_POINT('Ctrl Pts',(-2.27533224738737,-1.38517397546801,
13.8561433417727));
#435506=CARTESIAN_POINT('Ctrl Pts',(-2.2773993084917,-1.38362838224901,
13.8546163505474));
#435507=CARTESIAN_POINT('Ctrl Pts',(-2.27937927813542,-1.38241193781571,
13.8528973491086));
#435508=CARTESIAN_POINT('Ctrl Pts',(-2.2797409893776,-1.3821897113647,13.8525833129072));
#435509=CARTESIAN_POINT('Ctrl Pts',(-2.28009978404843,-1.38197832891922,
13.8522628768812));
#435510=CARTESIAN_POINT('Ctrl Pts',(-2.28045444496735,-1.38177734736348,
13.851937733538));
#435511=CARTESIAN_POINT('Ctrl Pts',(-2.28262030999228,-1.38054998088751,
13.8499521282529));
#435512=CARTESIAN_POINT('Ctrl Pts',(-2.28484926881114,-1.37959207364114,
13.847639871647));
#435513=CARTESIAN_POINT('Ctrl Pts',(-2.2869924540174,-1.37888015661756,
13.8452109780794));
#435514=CARTESIAN_POINT('Ctrl Pts',(-2.28795671740343,-1.3785598504127,
13.8441181685877));
#435515=CARTESIAN_POINT('Ctrl Pts',(-2.28890364102382,-1.37828862227948,
13.8430021611332));
#435516=CARTESIAN_POINT('Ctrl Pts',(-2.2898207919598,-1.3780612232801,13.8418824960098));
#435517=CARTESIAN_POINT('Ctrl Pts',(-2.29198208156072,-1.37752535173122,
13.8392439765549));
#435518=CARTESIAN_POINT('Ctrl Pts',(-2.29408044570721,-1.37720358462492,
13.8364981347964));
#435519=CARTESIAN_POINT('Ctrl Pts',(-2.29611624695142,-1.3770612458496,
13.8336931113419));
#435520=CARTESIAN_POINT('Ctrl Pts',(-2.29809898807794,-1.37692261692179,
13.8309611966328));
#435521=CARTESIAN_POINT('Ctrl Pts',(-2.30002441125895,-1.3769546092808,
13.8281701127186));
#435522=CARTESIAN_POINT('Ctrl Pts',(-2.30188114175763,-1.37716270309375,
13.8253580685121));
#435523=CARTESIAN_POINT('Ctrl Pts',(-2.30228368293359,-1.37720781805697,
13.8247484142933));
#435524=CARTESIAN_POINT('Ctrl Pts',(-2.30268288340781,-1.37726134238827,
13.8241378483365));
#435525=CARTESIAN_POINT('Ctrl Pts',(-2.30307839592131,-1.37732355084816,
13.8235269408515));
#435526=CARTESIAN_POINT('',(-2.26838290138995,-1.39339508922901,12.5969504640361));
#435527=CARTESIAN_POINT('Origin',(-2.29776565673724,-1.41129823186991,12.584524458991));
#435528=CARTESIAN_POINT('Origin',(-2.29776565673724,-1.41129823186991,12.584524458991));
#435529=CARTESIAN_POINT('Ctrl Pts',(-2.26986465849441,-1.43139955763529,
12.5893111709658));
#435530=CARTESIAN_POINT('Ctrl Pts',(-2.26323129194435,-1.42220950416579,
12.5770542771492));
#435531=CARTESIAN_POINT('Ctrl Pts',(-2.2744821880986,-1.41032585949838,
12.5737548217797));
#435532=CARTESIAN_POINT('Ctrl Pts',(-2.28436960491541,-1.45149512029947,
12.5663937883685));
#435533=CARTESIAN_POINT('Ctrl Pts',(-2.27772777658511,-1.44229334364049,
12.5540940315304));
#435534=CARTESIAN_POINT('Ctrl Pts',(-2.28901586886885,-1.43037508169057,
12.5508374392248));
#435535=CARTESIAN_POINT('Ctrl Pts',(-2.29885991602329,-1.47157040678728,
12.5434499600945));
#435536=CARTESIAN_POINT('Ctrl Pts',(-2.29219649274381,-1.46233871187557,
12.5311293540533));
#435537=CARTESIAN_POINT('Ctrl Pts',(-2.30353439464537,-1.45040540784716,
12.5278936106989));
#435538=CARTESIAN_POINT('Ctrl Pts',(-2.31333673822216,-1.49162700535937,
12.5204817579905));
#435539=CARTESIAN_POINT('Ctrl Pts',(-2.3066403355513,-1.48234961986679,
12.5081597038247));
#435540=CARTESIAN_POINT('Ctrl Pts',(-2.31803893211648,-1.47041831477309,
12.5049254088044));
#435541=CARTESIAN_POINT('Ctrl Pts',(-2.30292856860467,-1.47720723304881,
12.5369868989719));
#435542=CARTESIAN_POINT('Ctrl Pts',(-2.30347374562544,-1.4779625364228,
12.5342545179733));
#435543=CARTESIAN_POINT('Ctrl Pts',(-2.30409518707979,-1.47861035401455,
12.5314872231885));
#435544=CARTESIAN_POINT('Ctrl Pts',(-2.30479822681678,-1.47907549510966,
12.5287124745062));
#435545=CARTESIAN_POINT('Ctrl Pts',(-2.30543226294736,-1.47949498243676,
12.5262100684184));
#435546=CARTESIAN_POINT('Ctrl Pts',(-2.30613256864847,-1.47976464938453,
12.5237004536639));
#435547=CARTESIAN_POINT('Ctrl Pts',(-2.30693498999869,-1.47982726366503,
12.5212220730815));
#435548=CARTESIAN_POINT('Ctrl Pts',(-2.30754931295728,-1.47987520031331,
12.5193246583486));
#435549=CARTESIAN_POINT('Ctrl Pts',(-2.30823087961677,-1.47980171894315,
12.517417831369));
#435550=CARTESIAN_POINT('Ctrl Pts',(-2.30898854715649,-1.47950999201131,
12.5155812248348));
#435551=CARTESIAN_POINT('Ctrl Pts',(-2.30931131760089,-1.4793857147703,
12.5147988205793));
#435552=CARTESIAN_POINT('Ctrl Pts',(-2.30964832607415,-1.47922196256213,
12.5140295443047));
#435553=CARTESIAN_POINT('Ctrl Pts',(-2.31000200775598,-1.47901245833598,
12.5132817086137));
#435554=CARTESIAN_POINT('Ctrl Pts',(-2.31053725713645,-1.4786954020308,
12.5121499604604));
#435555=CARTESIAN_POINT('Ctrl Pts',(-2.31111860616464,-1.47826056134241,
12.5110494206568));
#435556=CARTESIAN_POINT('Ctrl Pts',(-2.31173453076288,-1.47767252307581,
12.5100666561695));
#435557=CARTESIAN_POINT('Ctrl Pts',(-2.31208819324883,-1.47733487285726,
12.5095023550641));
#435558=CARTESIAN_POINT('Ctrl Pts',(-2.31245689089972,-1.47694233957501,
12.5089719619137));
#435559=CARTESIAN_POINT('Ctrl Pts',(-2.3128290574779,-1.4764979081123,12.5085043804652));
#435560=CARTESIAN_POINT('Ctrl Pts',(-2.31337367478695,-1.4758475405579,
12.5078201359221));
#435561=CARTESIAN_POINT('Ctrl Pts',(-2.31394059035579,-1.47506639732494,
12.5072563000949));
#435562=CARTESIAN_POINT('Ctrl Pts',(-2.31448452395654,-1.47420245576189,
12.5068768744332));
#435563=CARTESIAN_POINT('Ctrl Pts',(-2.31487673752719,-1.47357949442099,
12.5066032824114));
#435564=CARTESIAN_POINT('Ctrl Pts',(-2.31526394327209,-1.47290257039882,
12.5064197834844));
#435565=CARTESIAN_POINT('Ctrl Pts',(-2.31562676234242,-1.47221076831766,
12.5063282718343));
#435566=CARTESIAN_POINT('Ctrl Pts',(-2.31615636585915,-1.47120095145569,
12.5061946931565));
#435567=CARTESIAN_POINT('Ctrl Pts',(-2.31664626910326,-1.47013834367698,
12.5062515701262));
#435568=CARTESIAN_POINT('Ctrl Pts',(-2.31708011165234,-1.4690953670419,
12.5064436508398));
#435569=CARTESIAN_POINT('',(-2.2744821880986,-1.41032585949838,12.5737548217797));
#435570=CARTESIAN_POINT('Origin',(-2.2877031887093,-1.41852373378699,12.5893111709658));
#435571=CARTESIAN_POINT('Ctrl Pts',(-2.31708011165234,-1.4690953670419,
12.5064436508398));
#435572=CARTESIAN_POINT('Ctrl Pts',(-2.31077490124847,-1.46039567109812,
12.5164271754438));
#435573=CARTESIAN_POINT('Ctrl Pts',(-2.30446702228504,-1.45169264920894,
12.5264061185523));
#435574=CARTESIAN_POINT('Ctrl Pts',(-2.29815638154398,-1.4429861836819,
12.536380305637));
#435575=CARTESIAN_POINT('Ctrl Pts',(-2.29026936055351,-1.43210486763459,
12.5488460165097));
#435576=CARTESIAN_POINT('Ctrl Pts',(-2.2823780233362,-1.42121816944895,
12.5613043021964));
#435577=CARTESIAN_POINT('Ctrl Pts',(-2.2744821880986,-1.41032585949838,
12.5737548217797));
#435578=CARTESIAN_POINT('Ctrl Pts',(-2.30307839592131,-1.37732355084815,
12.5893111709658));
#435579=CARTESIAN_POINT('Ctrl Pts',(-2.29188208210002,-1.37556253086672,
12.5770542771492));
#435580=CARTESIAN_POINT('Ctrl Pts',(-2.28637003248251,-1.39097100203906,
12.5737548217797));
#435581=CARTESIAN_POINT('Ctrl Pts',(-2.29263233250645,-1.37568053452202,
12.5928319619712));
#435582=CARTESIAN_POINT('Ctrl Pts',(-2.28460154450062,-1.37771519920616,
12.5821634970842));
#435583=CARTESIAN_POINT('Ctrl Pts',(-2.28256625099379,-1.39036316673619,
12.5773203894503));
#435584=CARTESIAN_POINT('Ctrl Pts',(-2.27650764618195,-1.38021689763316,
12.5969440695591));
#435585=CARTESIAN_POINT('Ctrl Pts',(-2.2743882779987,-1.38363257048866,
12.5878292599214));
#435586=CARTESIAN_POINT('Ctrl Pts',(-2.27681963783929,-1.3919819886381,
12.5813877129824));
#435587=CARTESIAN_POINT('Ctrl Pts',(-2.26044824178409,-1.40626052979013,
12.596957478804));
#435588=CARTESIAN_POINT('Ctrl Pts',(-2.26255201538024,-1.40287014193547,
12.5878468778671));
#435589=CARTESIAN_POINT('Ctrl Pts',(-2.27107683179591,-1.40130649650995,
12.5814011370086));
#435590=CARTESIAN_POINT('Ctrl Pts',(-2.26366679896377,-1.42281286789751,
12.5928371701607));
#435591=CARTESIAN_POINT('Ctrl Pts',(-2.26185749593652,-1.4147344096127,
12.5821692192952));
#435592=CARTESIAN_POINT('Ctrl Pts',(-2.27221263799302,-1.40719817348598,
12.5773318885715));
#435593=CARTESIAN_POINT('Ctrl Pts',(-2.26986465849436,-1.43139955763532,
12.5893111709658));
#435594=CARTESIAN_POINT('Ctrl Pts',(-2.2632312919443,-1.42220950416582,
12.5770542771492));
#435595=CARTESIAN_POINT('Ctrl Pts',(-2.27448218809855,-1.41032585949842,
12.5737548217797));
#435596=CARTESIAN_POINT('',(-2.28637003248251,-1.39097100203906,12.5737548217797));
#435597=CARTESIAN_POINT('Origin',(-2.29966013418298,-1.39905637134363,12.5893111709658));
#435598=CARTESIAN_POINT('Ctrl Pts',(-2.27448218809855,-1.41032585949842,
12.5737548217797));
#435599=CARTESIAN_POINT('Ctrl Pts',(-2.27386946955627,-1.40953283010492,
12.5746934679442));
#435600=CARTESIAN_POINT('Ctrl Pts',(-2.27333641347121,-1.40854329150111,
12.5756680099006));
#435601=CARTESIAN_POINT('Ctrl Pts',(-2.27294073479529,-1.40747140435528,
12.5765688348656));
#435602=CARTESIAN_POINT('Ctrl Pts',(-2.27283598324615,-1.4071876340996,
12.5768073183026));
#435603=CARTESIAN_POINT('Ctrl Pts',(-2.27274064777522,-1.40689823735086,
12.5770407398754));
#435604=CARTESIAN_POINT('Ctrl Pts',(-2.27265526938078,-1.40660552303166,
12.5772674179684));
#435605=CARTESIAN_POINT('Ctrl Pts',(-2.27230489953727,-1.40540430261896,
12.5781976435658));
#435606=CARTESIAN_POINT('Ctrl Pts',(-2.27211314135924,-1.40407582744646,
12.5790594849312));
#435607=CARTESIAN_POINT('Ctrl Pts',(-2.27214073651319,-1.40270289946905,
12.5797571720116));
#435608=CARTESIAN_POINT('Ctrl Pts',(-2.27215871574822,-1.40180838752568,
12.580211740231));
#435609=CARTESIAN_POINT('Ctrl Pts',(-2.2722893964261,-1.40085473164395,
12.5806009430798));
#435610=CARTESIAN_POINT('Ctrl Pts',(-2.27254113185966,-1.39991147031441,
12.5808812374708));
#435611=CARTESIAN_POINT('Ctrl Pts',(-2.27275745610945,-1.39910089590865,
12.5811221033394));
#435612=CARTESIAN_POINT('Ctrl Pts',(-2.27306771237705,-1.39828143218088,
12.581287365893));
#435613=CARTESIAN_POINT('Ctrl Pts',(-2.27346218710277,-1.3975022833028,
12.581359338449));
#435614=CARTESIAN_POINT('Ctrl Pts',(-2.27351701094406,-1.39739399769756,
12.5813693411482));
#435615=CARTESIAN_POINT('Ctrl Pts',(-2.27357342013422,-1.39728644747941,
12.5813775999465));
#435616=CARTESIAN_POINT('Ctrl Pts',(-2.27363134702667,-1.39717971962542,
12.5813841266931));
#435617=CARTESIAN_POINT('Ctrl Pts',(-2.27372962700582,-1.39699864291267,
12.5813952001081));
#435618=CARTESIAN_POINT('Ctrl Pts',(-2.27383346908963,-1.39681901107323,
12.5814007534795));
#435619=CARTESIAN_POINT('Ctrl Pts',(-2.27394299878601,-1.39664100104132,
12.5814005856065));
#435620=CARTESIAN_POINT('Ctrl Pts',(-2.27444438291267,-1.39582614071267,
12.5813998171494));
#435621=CARTESIAN_POINT('Ctrl Pts',(-2.27503001890481,-1.39510138828226,
12.58127954464));
#435622=CARTESIAN_POINT('Ctrl Pts',(-2.27567356714382,-1.3944522613523,
12.5810700125799));
#435623=CARTESIAN_POINT('Ctrl Pts',(-2.27645090014271,-1.39366818992993,
12.5808169217085));
#435624=CARTESIAN_POINT('Ctrl Pts',(-2.27732468184969,-1.39300616735629,
12.5804173076348));
#435625=CARTESIAN_POINT('Ctrl Pts',(-2.27820260862559,-1.39250345477061,
12.5799304713245));
#435626=CARTESIAN_POINT('Ctrl Pts',(-2.27929063647639,-1.39188043550615,
12.5793271277669));
#435627=CARTESIAN_POINT('Ctrl Pts',(-2.28043652230898,-1.39143551026852,
12.5785808224116));
#435628=CARTESIAN_POINT('Ctrl Pts',(-2.281580484799,-1.39115786718032,12.5777485681082));
#435629=CARTESIAN_POINT('Ctrl Pts',(-2.28328511423958,-1.39074414856083,
12.576508418016));
#435630=CARTESIAN_POINT('Ctrl Pts',(-2.28496949883696,-1.39069867286553,
12.5750928681475));
#435631=CARTESIAN_POINT('Ctrl Pts',(-2.28637003248251,-1.39097100203906,
12.5737548217797));
#435632=CARTESIAN_POINT('Ctrl Pts',(-2.28637003248251,-1.39097100203906,
12.5737548217797));
#435633=CARTESIAN_POINT('Ctrl Pts',(-2.29188208210002,-1.37556253086672,
12.5770542771492));
#435634=CARTESIAN_POINT('Ctrl Pts',(-2.30307839592131,-1.37732355084816,
12.5893111709658));
#435635=CARTESIAN_POINT('Ctrl Pts',(-2.3108205997239,-1.39486775911961,
12.5508408821982));
#435636=CARTESIAN_POINT('Ctrl Pts',(-2.31634670108406,-1.37941046542419,
12.55409748406));
#435637=CARTESIAN_POINT('Ctrl Pts',(-2.32755729853427,-1.3811737320161,
12.5663972313419));
#435638=CARTESIAN_POINT('Ctrl Pts',(-2.33524746748103,-1.39875954474662,
12.52790050457));
#435639=CARTESIAN_POINT('Ctrl Pts',(-2.34076446449977,-1.38325103027111,
12.5311362602938));
#435640=CARTESIAN_POINT('Ctrl Pts',(-2.35201150595693,-1.38502002898392,
12.5434568539655));
#435641=CARTESIAN_POINT('Ctrl Pts',(-2.35965247968752,-1.40264673159036,
12.5049357605811));
#435642=CARTESIAN_POINT('Ctrl Pts',(-2.36514025680051,-1.38708499366211,
12.5081700652078));
#435643=CARTESIAN_POINT('Ctrl Pts',(-2.37644295232159,-1.38886274596296,
12.5204921097672));
#435644=CARTESIAN_POINT('Ctrl Pts',(-2.35804995117097,-1.40239148209752,
12.5064436508395));
#435645=CARTESIAN_POINT('Ctrl Pts',(-2.3588429028393,-1.40146407957311,
12.5062361689309));
#435646=CARTESIAN_POINT('Ctrl Pts',(-2.35962796118144,-1.4004658436191,
12.5061871075061));
#435647=CARTESIAN_POINT('Ctrl Pts',(-2.36033233894485,-1.39945843674622,
12.5063648335164));
#435648=CARTESIAN_POINT('Ctrl Pts',(-2.36065231077281,-1.39900081040512,
12.5064455676329));
#435649=CARTESIAN_POINT('Ctrl Pts',(-2.36095991625174,-1.39853478243063,
12.506574497099));
#435650=CARTESIAN_POINT('Ctrl Pts',(-2.36124108907258,-1.39807975576188,
12.5067492519495));
#435651=CARTESIAN_POINT('Ctrl Pts',(-2.36180611677043,-1.39716536200812,
12.5071004286051));
#435652=CARTESIAN_POINT('Ctrl Pts',(-2.36228448942298,-1.39626135040563,
12.5076537929613));
#435653=CARTESIAN_POINT('Ctrl Pts',(-2.36264866276314,-1.39543999565603,
12.5083435010505));
#435654=CARTESIAN_POINT('Ctrl Pts',(-2.36267158965122,-1.39538828646611,
12.5083869222964));
#435655=CARTESIAN_POINT('Ctrl Pts',(-2.36269405550518,-1.39533689440635,
12.5084308732337));
#435656=CARTESIAN_POINT('Ctrl Pts',(-2.3627160503358,-1.39528583299742,
12.5084753333615));
#435657=CARTESIAN_POINT('Ctrl Pts',(-2.36289247790797,-1.39487625310285,
12.5088319622689));
#435658=CARTESIAN_POINT('Ctrl Pts',(-2.36304336570438,-1.39448014302746,
12.509227847131));
#435659=CARTESIAN_POINT('Ctrl Pts',(-2.36316684368446,-1.39411027792921,
12.5096423454524));
#435660=CARTESIAN_POINT('Ctrl Pts',(-2.36355376902495,-1.39295128440671,
12.5109411997424));
#435661=CARTESIAN_POINT('Ctrl Pts',(-2.36370452181833,-1.39198177128923,
12.5124831113042));
#435662=CARTESIAN_POINT('Ctrl Pts',(-2.36371057587997,-1.39117748164997,
12.5140723025008));
#435663=CARTESIAN_POINT('Ctrl Pts',(-2.36371114315218,-1.39110211882986,
12.5142212114565));
#435664=CARTESIAN_POINT('Ctrl Pts',(-2.36371046410849,-1.39102818948882,
12.5143705582413));
#435665=CARTESIAN_POINT('Ctrl Pts',(-2.36370862867909,-1.39095566512588,
12.5145201959299));
#435666=CARTESIAN_POINT('Ctrl Pts',(-2.36368504985568,-1.39002398170639,
12.5164425148273));
#435667=CARTESIAN_POINT('Ctrl Pts',(-2.36348055697308,-1.38929197047674,
12.5184635205941));
#435668=CARTESIAN_POINT('Ctrl Pts',(-2.3631576019843,-1.38869453357128,
12.5205025929158));
#435669=CARTESIAN_POINT('Ctrl Pts',(-2.36297027529006,-1.38834799648593,
12.5216853356836));
#435670=CARTESIAN_POINT('Ctrl Pts',(-2.3627438562664,-1.3880471324298,12.5228750347131));
#435671=CARTESIAN_POINT('Ctrl Pts',(-2.36249456233346,-1.38778357905086,
12.5240609649613));
#435672=CARTESIAN_POINT('Ctrl Pts',(-2.36188268374922,-1.3871367014214,
12.5269717671326));
#435673=CARTESIAN_POINT('Ctrl Pts',(-2.3611082265875,-1.38670353275584,
12.5299036066169));
#435674=CARTESIAN_POINT('Ctrl Pts',(-2.36022510272288,-1.38641622740281,
12.5328133004019));
#435675=CARTESIAN_POINT('Ctrl Pts',(-2.35980115184509,-1.38627830410407,
12.5342101228451));
#435676=CARTESIAN_POINT('Ctrl Pts',(-2.35935252492081,-1.38617466632391,
12.5356023438238));
#435677=CARTESIAN_POINT('Ctrl Pts',(-2.35888624416239,-1.38610132694861,
12.5369868989719));
#435678=CARTESIAN_POINT('Origin',(-14.9503750405813,-3.36120017670074,-1.24017999715448));
#435679=CARTESIAN_POINT('Ctrl Pts',(-2.30290407571476,-1.47717336773802,
12.5369868989719));
#435680=CARTESIAN_POINT('Ctrl Pts',(-2.3119050321431,-1.48959375771016,
12.5369868989719));
#435681=CARTESIAN_POINT('Ctrl Pts',(-2.30336319205093,-1.50233425501304,
12.5369868989719));
#435682=CARTESIAN_POINT('Ctrl Pts',(-2.30594669739915,-1.48137198416061,
12.5218025310015));
#435683=CARTESIAN_POINT('Ctrl Pts',(-2.30991710317046,-1.49250265088438,
12.5216901060417));
#435684=CARTESIAN_POINT('Ctrl Pts',(-2.30338924410837,-1.50229542693877,
12.5161920673678));
#435685=CARTESIAN_POINT('Ctrl Pts',(-2.31197458300952,-1.48134617209131,
12.5042015548895));
#435686=CARTESIAN_POINT('Ctrl Pts',(-2.31297237030655,-1.48770083695479,
12.4980677368514));
#435687=CARTESIAN_POINT('Ctrl Pts',(-2.30929066544941,-1.49341361465647,
12.4907278922777));
#435688=CARTESIAN_POINT('Ctrl Pts',(-2.31706321967367,-1.46908465702972,
12.506463626192));
#435689=CARTESIAN_POINT('Ctrl Pts',(-2.32258891308682,-1.4725881054224,
12.4999376786891));
#435690=CARTESIAN_POINT('Ctrl Pts',(-2.32252142477613,-1.47254531589429,
12.4906970594712));
#435691=CARTESIAN_POINT('Origin',(-2.28509003838978,-1.4900830568971,12.5369868989719));
#435692=CARTESIAN_POINT('Origin',(-2.28509003838978,-1.49008305689711,14.));
#435693=CARTESIAN_POINT('Origin',(-2.28509003838978,-1.49008305689711,13.7435492065112));
#435694=CARTESIAN_POINT('Ctrl Pts',(-2.28843733125914,-1.45713070971702,
13.793642941384));
#435695=CARTESIAN_POINT('Ctrl Pts',(-2.29478745209017,-1.46588183446972,
13.8071662555867));
#435696=CARTESIAN_POINT('Ctrl Pts',(-2.2826242822311,-1.47780142685429,
13.8103758687955));
#435697=CARTESIAN_POINT('Ctrl Pts',(-2.29816509014281,-1.47060781668864,
13.7804579775006));
#435698=CARTESIAN_POINT('Ctrl Pts',(-2.30599235766558,-1.48141186939382,
13.7901904343351));
#435699=CARTESIAN_POINT('Ctrl Pts',(-2.29667151463007,-1.49411532598138,
13.7927914348262));
#435700=CARTESIAN_POINT('Ctrl Pts',(-2.30389218786353,-1.47854229678566,
13.7597120340895));
#435701=CARTESIAN_POINT('Ctrl Pts',(-2.31294590014608,-1.49104899034863,
13.7635825532445));
#435702=CARTESIAN_POINT('Ctrl Pts',(-2.30493578061372,-1.50375229311687,
13.7651073818885));
#435703=CARTESIAN_POINT('Ctrl Pts',(-2.30277069099354,-1.47698854390422,
13.7381884353898));
#435704=CARTESIAN_POINT('Ctrl Pts',(-2.31161321235313,-1.4892019679381,
13.7368803041982));
#435705=CARTESIAN_POINT('Ctrl Pts',(-2.3033170165916,-1.50186541032181,
13.7363986145813));
#435706=CARTESIAN_POINT('Origin',(-2.27295924579953,-1.47327671404081,13.7902182540695));
#435707=CARTESIAN_POINT('Ctrl Pts',(-2.26986235416098,-1.43139636644336,
13.8235227101244));
#435708=CARTESIAN_POINT('Ctrl Pts',(-2.27659477970197,-1.44071608396346,
13.8358800583119));
#435709=CARTESIAN_POINT('Ctrl Pts',(-2.26512092677521,-1.45267337245507,
13.8390832900376));
#435710=CARTESIAN_POINT('Ctrl Pts',(-2.27684314555667,-1.44106775211369,
13.8124254819052));
#435711=CARTESIAN_POINT('Ctrl Pts',(-2.28358864514716,-1.45040556855599,
13.8247886449157));
#435712=CARTESIAN_POINT('Ctrl Pts',(-2.27208799635011,-1.46236616462598,
13.8279860620657));
#435713=CARTESIAN_POINT('Ctrl Pts',(-2.28382080838877,-1.45073480338359,
13.8013225099955));
#435714=CARTESIAN_POINT('Ctrl Pts',(-2.29057620086112,-1.46008631162437,
13.8136962257787));
#435715=CARTESIAN_POINT('Ctrl Pts',(-2.27905206061218,-1.47205431130703,
13.8168830918626));
#435716=CARTESIAN_POINT('Ctrl Pts',(-2.2907954643849,-1.46039768889795,
13.7902140179785));
#435717=CARTESIAN_POINT('Ctrl Pts',(-2.29755777648181,-1.46975876985307,
13.802602731458));
#435718=CARTESIAN_POINT('Ctrl Pts',(-2.28601323914175,-1.4817379939567,
13.8057746032558));
#435719=CARTESIAN_POINT('Origin',(-2.25202612827951,-1.44427538148359,13.8235269408515));
#435720=CARTESIAN_POINT('Ctrl Pts',(-2.30307839592131,-1.37732355084816,
13.8235269408515));
#435721=CARTESIAN_POINT('Ctrl Pts',(-2.31474248116712,-1.37915814458239,
13.8362179249168));
#435722=CARTESIAN_POINT('Ctrl Pts',(-2.32008978759712,-1.36293873281744,
13.8391868794938));
#435723=CARTESIAN_POINT('Ctrl Pts',(-2.2924062656288,-1.37564497743644,
13.8400110824519));
#435724=CARTESIAN_POINT('Ctrl Pts',(-2.3022895481309,-1.3737364204305,13.8494522556836));
#435725=CARTESIAN_POINT('Ctrl Pts',(-2.30250901645348,-1.36028726725673,
13.85569149686));
#435726=CARTESIAN_POINT('Ctrl Pts',(-2.27668711643539,-1.37992353732036,
13.8586819406588));
#435727=CARTESIAN_POINT('Ctrl Pts',(-2.27897762377551,-1.37622088695071,
13.868010383617));
#435728=CARTESIAN_POINT('Ctrl Pts',(-2.27645326077068,-1.36753063619411,
13.8744918421245));
#435729=CARTESIAN_POINT('Ctrl Pts',(-2.26026597218442,-1.40655843021363,
13.8587686893867));
#435730=CARTESIAN_POINT('Ctrl Pts',(-2.25799580245194,-1.41022809740638,
13.8680909899357));
#435731=CARTESIAN_POINT('Ctrl Pts',(-2.24911906805347,-1.4118712614045,
13.8745789365163));
#435732=CARTESIAN_POINT('Ctrl Pts',(-2.26353156092593,-1.42262550530934,
13.8400379222776));
#435733=CARTESIAN_POINT('Ctrl Pts',(-2.26629061465845,-1.43230320423053,
13.8494748685453));
#435734=CARTESIAN_POINT('Ctrl Pts',(-2.25440014789936,-1.43857838594228,
13.8557104837033));
#435735=CARTESIAN_POINT('Ctrl Pts',(-2.26986465848896,-1.43139955763904,
13.8235269408542));
#435736=CARTESIAN_POINT('Ctrl Pts',(-2.27677516083295,-1.44097356286906,
13.8362179249195));
#435737=CARTESIAN_POINT('Ctrl Pts',(-2.26472646953937,-1.45307695256651,
13.8391868794965));
#435738=CARTESIAN_POINT('Origin',(-2.30649665765963,-1.35559073035269,13.8235269408515));
#435739=CARTESIAN_POINT('Ctrl Pts',(-2.33840705068917,-1.38288024203628,
13.7902140241682));
#435740=CARTESIAN_POINT('Ctrl Pts',(-2.34981421122245,-1.38467893154836,
13.8026027327198));
#435741=CARTESIAN_POINT('Ctrl Pts',(-2.35527873261449,-1.36896534067199,
13.8057746032556));
#435742=CARTESIAN_POINT('Ctrl Pts',(-2.3266346818964,-1.38102861685037,
13.8013225161808));
#435743=CARTESIAN_POINT('Ctrl Pts',(-2.33803017537325,-1.38282546306104,
13.8136962270464));
#435744=CARTESIAN_POINT('Ctrl Pts',(-2.3434939083512,-1.3671351403346,13.8168830918628));
#435745=CARTESIAN_POINT('Ctrl Pts',(-2.31485723792953,-1.3791761934122,
13.8124254880875));
#435746=CARTESIAN_POINT('Ctrl Pts',(-2.32623604599283,-1.38097040691662,
13.8247886461868));
#435747=CARTESIAN_POINT('Ctrl Pts',(-2.33170379763449,-1.36530438463322,
13.8279860620656));
#435748=CARTESIAN_POINT('Ctrl Pts',(-2.3030745133256,-1.37732293940539,
13.8235227163065));
#435749=CARTESIAN_POINT('Ctrl Pts',(-2.31443126669601,-1.37911367560055,
13.8358800595847));
#435750=CARTESIAN_POINT('Ctrl Pts',(-2.31990818454371,-1.36347304896067,
13.8390832900376));
#435751=CARTESIAN_POINT('Origin',(-2.34182920731495,-1.36114803492019,13.7902182540695));
#435752=CARTESIAN_POINT('Ctrl Pts',(-2.35861966586612,-1.38605937007289,
13.7382347919292));
#435753=CARTESIAN_POINT('Ctrl Pts',(-2.3735229768461,-1.38842774305202,
13.7369371795942));
#435754=CARTESIAN_POINT('Ctrl Pts',(-2.38106522452574,-1.37528779339612,
13.7364597369711));
#435755=CARTESIAN_POINT('Ctrl Pts',(-2.36048825233909,-1.38635327239884,
13.7595490285574));
#435756=CARTESIAN_POINT('Ctrl Pts',(-2.37574730134179,-1.38877715976248,
13.7633824266926));
#435757=CARTESIAN_POINT('Ctrl Pts',(-2.38345047934689,-1.37587155210806,
13.7648920890506));
#435758=CARTESIAN_POINT('Ctrl Pts',(-2.35095856369513,-1.38485438664562,
13.780380659011));
#435759=CARTESIAN_POINT('Ctrl Pts',(-2.36415624800675,-1.38695629406881,
13.7901039518744));
#435760=CARTESIAN_POINT('Ctrl Pts',(-2.37128930719404,-1.37289909278063,
13.7926933640891));
#435761=CARTESIAN_POINT('Ctrl Pts',(-2.33439383754983,-1.38224898853699,
13.7936647693663));
#435762=CARTESIAN_POINT('Ctrl Pts',(-2.34507321223805,-1.38395904356925,
13.8072068914933));
#435763=CARTESIAN_POINT('Ctrl Pts',(-2.3502002794335,-1.36769997066146,
13.8104111085397));
#435764=CARTESIAN_POINT('Origin',(-2.36230450590072,-1.36436850645314,13.7435492065112));
#435765=CARTESIAN_POINT('Origin',(-2.36230450590072,-1.36436850645314,14.));
#435766=CARTESIAN_POINT('Origin',(-2.36230450590072,-1.36436850645314,12.5369868989719));
#435767=CARTESIAN_POINT('Ctrl Pts',(-2.35803415101985,-1.40238208536313,
12.506462012331));
#435768=CARTESIAN_POINT('Ctrl Pts',(-2.36365400976818,-1.40572435639323,
12.4999388158272));
#435769=CARTESIAN_POINT('Ctrl Pts',(-2.3635875194692,-1.40568481294382,
12.4907030323752));
#435770=CARTESIAN_POINT('Ctrl Pts',(-2.3666678544068,-1.3922980510028,12.5042014951932));
#435771=CARTESIAN_POINT('Ctrl Pts',(-2.37278456078797,-1.39031638499599,
12.4980716682127));
#435772=CARTESIAN_POINT('Ctrl Pts',(-2.3762141316028,-1.38445433678294,
12.4907355092744));
#435773=CARTESIAN_POINT('Ctrl Pts',(-2.36396772154394,-1.38690963901333,
12.5218047446509));
#435774=CARTESIAN_POINT('Ctrl Pts',(-2.37568491888256,-1.38541760769181,
12.5216906929434));
#435775=CARTESIAN_POINT('Ctrl Pts',(-2.38146799229632,-1.37517422855108,
12.5161988840775));
#435776=CARTESIAN_POINT('Ctrl Pts',(-2.35884829980673,-1.3860953248911,
12.5369868989719));
#435777=CARTESIAN_POINT('Ctrl Pts',(-2.37398783342561,-1.38850365487752,
12.5369868989719));
#435778=CARTESIAN_POINT('Ctrl Pts',(-2.38149002219928,-1.37513493410383,
12.5369868989719));
#435779=CARTESIAN_POINT('Origin',(-4.38993701924921E-31,-7.84818254312667E-31,
12.5));
#435780=CARTESIAN_POINT('Origin',(-2.18315043670734,-1.56046289035817,12.5));
#435781=CARTESIAN_POINT('',(-2.18315043670734,-1.56046289035817,12.5893111709658));
#435782=CARTESIAN_POINT('',(-2.18315043670734,-1.56046289035817,13.8235269408515));
#435783=CARTESIAN_POINT('',(-2.18315043670734,-1.56046289035817,12.5));
#435784=CARTESIAN_POINT('',(-2.21791244830466,-1.56888163426146,13.7902182540695));
#435785=CARTESIAN_POINT('',(-2.18315043670734,-1.56046289035817,13.8235269408515));
#435786=CARTESIAN_POINT('',(-2.23805711869615,-1.5737603168592,13.7435492065112));
#435787=CARTESIAN_POINT('Origin',(-2.17178134270818,-1.55770983220249,13.7445212918709));
#435788=CARTESIAN_POINT('',(-2.23805711869615,-1.5737603168592,12.5369868989719));
#435789=CARTESIAN_POINT('',(-2.23805711869615,-1.5737603168592,12.5));
#435790=CARTESIAN_POINT('Ctrl Pts',(-2.23805711869615,-1.5737603168592,
12.5369868989719));
#435791=CARTESIAN_POINT('Ctrl Pts',(-2.21976823989799,-1.5693310741369,
12.5544431401645));
#435792=CARTESIAN_POINT('Ctrl Pts',(-2.20146628040763,-1.56489866350248,
12.5718848856037));
#435793=CARTESIAN_POINT('Ctrl Pts',(-2.18315043670734,-1.56046289035817,
12.5893111709658));
#435794=CARTESIAN_POINT('Origin',(-2.2878767035474,-1.84701015017872,12.5));
#435795=CARTESIAN_POINT('',(-2.17485966055452,-1.66000200552889,13.7435492065112));
#435796=CARTESIAN_POINT('',(-2.16413910514116,-1.64226281217913,13.7902182540695));
#435797=CARTESIAN_POINT('Origin',(-2.13596733839878,-1.59564727800405,13.7418732680442));
#435798=CARTESIAN_POINT('',(-2.14563951868149,-1.61165173575209,13.8235269408515));
#435799=CARTESIAN_POINT('',(-2.16413910514116,-1.64226281217913,13.7902182540695));
#435800=CARTESIAN_POINT('',(-2.14563951868149,-1.61165173575209,12.5893111709658));
#435801=CARTESIAN_POINT('',(-2.14563951868149,-1.61165173575209,12.5));
#435802=CARTESIAN_POINT('',(-2.17485966055452,-1.66000200552889,12.5369868989719));
#435803=CARTESIAN_POINT('Ctrl Pts',(-2.14563951868149,-1.61165173575209,
12.5893111709658));
#435804=CARTESIAN_POINT('Ctrl Pts',(-2.15538681230881,-1.6277804827829,
12.5718848856037));
#435805=CARTESIAN_POINT('Ctrl Pts',(-2.1651267170616,-1.64389700351864,
12.5544431401645));
#435806=CARTESIAN_POINT('Ctrl Pts',(-2.17485966055452,-1.66000200552889,
12.5369868989719));
#435807=CARTESIAN_POINT('',(-2.17485966055452,-1.66000200552889,12.5));
#435808=CARTESIAN_POINT('Origin',(-2.17505932048481,-1.59387208764385,12.5));
#435809=CARTESIAN_POINT('',(-2.14800907319443,-1.57266184734094,13.8587068136939));
#435810=CARTESIAN_POINT('Ctrl Pts',(-2.14563951867576,-1.61165173575538,
13.8235269408542));
#435811=CARTESIAN_POINT('Ctrl Pts',(-2.14473318419907,-1.61015203337041,
13.8262006681044));
#435812=CARTESIAN_POINT('Ctrl Pts',(-2.14395437788002,-1.60852744457645,
13.8288634856214));
#435813=CARTESIAN_POINT('Ctrl Pts',(-2.14329465193769,-1.60678828640047,
13.8314912288862));
#435814=CARTESIAN_POINT('Ctrl Pts',(-2.14261454253872,-1.6049953937069,
13.8342001611531));
#435815=CARTESIAN_POINT('Ctrl Pts',(-2.1420597655961,-1.60307892736555,
13.836875030195));
#435816=CARTESIAN_POINT('Ctrl Pts',(-2.14165213356702,-1.60101735872816,
13.8394886372969));
#435817=CARTESIAN_POINT('Ctrl Pts',(-2.14162065115665,-1.60085813878165,
13.8396904925131));
#435818=CARTESIAN_POINT('Ctrl Pts',(-2.14159006710582,-1.60069804534658,
13.8398919674349));
#435819=CARTESIAN_POINT('Ctrl Pts',(-2.14156040246006,-1.60053706533774,
13.8400930404591));
#435820=CARTESIAN_POINT('Ctrl Pts',(-2.14109820732166,-1.59802888849779,
13.8432258934518));
#435821=CARTESIAN_POINT('Ctrl Pts',(-2.14086045607714,-1.59531849162118,
13.8462331177034));
#435822=CARTESIAN_POINT('Ctrl Pts',(-2.14095100018776,-1.59248584378433,
13.8489036603661));
#435823=CARTESIAN_POINT('Ctrl Pts',(-2.14098062727446,-1.59155896844693,
13.8497774930041));
#435824=CARTESIAN_POINT('Ctrl Pts',(-2.1410455342675,-1.59061921738479,
13.85061494757));
#435825=CARTESIAN_POINT('Ctrl Pts',(-2.14114972096597,-1.58967000778862,
13.8514076489583));
#435826=CARTESIAN_POINT('Ctrl Pts',(-2.14137009085921,-1.58766229259623,
13.8530843267192));
#435827=CARTESIAN_POINT('Ctrl Pts',(-2.14179077808467,-1.58541537373579,
13.8546805203176));
#435828=CARTESIAN_POINT('Ctrl Pts',(-2.14252148138838,-1.58308477177075,
13.8559412814273));
#435829=CARTESIAN_POINT('Ctrl Pts',(-2.14261927318769,-1.58277286164461,
13.8561100121513));
#435830=CARTESIAN_POINT('Ctrl Pts',(-2.14272254699551,-1.58245948265099,
13.8562727473908));
#435831=CARTESIAN_POINT('Ctrl Pts',(-2.14283149278315,-1.5821450282265,
13.8564289040185));
#435832=CARTESIAN_POINT('Ctrl Pts',(-2.1433255606872,-1.58071898099889,
13.8571370725437));
#435833=CARTESIAN_POINT('Ctrl Pts',(-2.14394711454076,-1.579246495635,13.8577210840554));
#435834=CARTESIAN_POINT('Ctrl Pts',(-2.14469903237326,-1.5777962209433,
13.8581177131616));
#435835=CARTESIAN_POINT('Ctrl Pts',(-2.14491079831511,-1.57738777367319,
13.8582294175695));
#435836=CARTESIAN_POINT('Ctrl Pts',(-2.14513273381987,-1.57698103883377,
13.8583265086086));
#435837=CARTESIAN_POINT('Ctrl Pts',(-2.14536448888114,-1.57657740300675,
13.8584082369006));
#435838=CARTESIAN_POINT('Ctrl Pts',(-2.14569745875663,-1.57599748656254,
13.8585256585398));
#435839=CARTESIAN_POINT('Ctrl Pts',(-2.14605511815475,-1.5754169183704,
13.8586122832068));
#435840=CARTESIAN_POINT('Ctrl Pts',(-2.14642884846448,-1.57485119410699,
13.8586682984299));
#435841=CARTESIAN_POINT('Ctrl Pts',(-2.14672779566557,-1.5743986707747,
13.8587131050557));
#435842=CARTESIAN_POINT('Ctrl Pts',(-2.14704013193033,-1.57395051783153,
13.8587357943552));
#435843=CARTESIAN_POINT('Ctrl Pts',(-2.14736630986575,-1.57350697159873,
13.8587355499465));
#435844=CARTESIAN_POINT('Ctrl Pts',(-2.14757712644181,-1.57322029709392,
13.8587353919793));
#435845=CARTESIAN_POINT('Ctrl Pts',(-2.14779141426411,-1.57293862411962,
13.8587257282814));
#435846=CARTESIAN_POINT('Ctrl Pts',(-2.14800907319443,-1.57266184734094,
13.8587068136939));
#435847=CARTESIAN_POINT('Ctrl Pts',(-2.14800907319443,-1.57266184734094,
13.8587068136939));
#435848=CARTESIAN_POINT('Ctrl Pts',(-2.14872494155066,-1.57175154360425,
13.8586446046466));
#435849=CARTESIAN_POINT('Ctrl Pts',(-2.14947723124705,-1.57089413691004,
13.858482427929));
#435850=CARTESIAN_POINT('Ctrl Pts',(-2.15026279169027,-1.5700864555523,
13.8582284286032));
#435851=CARTESIAN_POINT('Ctrl Pts',(-2.15106868532482,-1.56925786843266,
13.8579678548414));
#435852=CARTESIAN_POINT('Ctrl Pts',(-2.15191266088537,-1.56848065799959,
13.857615680862));
#435853=CARTESIAN_POINT('Ctrl Pts',(-2.15275488136508,-1.56777833743812,
13.8571944833187));
#435854=CARTESIAN_POINT('Ctrl Pts',(-2.15485672870745,-1.56602562464953,
13.8561433417727));
#435855=CARTESIAN_POINT('Ctrl Pts',(-2.15704289203238,-1.56465365893415,
13.8546163505475));
#435856=CARTESIAN_POINT('Ctrl Pts',(-2.15911542500467,-1.56360264802645,
13.8528973491086));
#435857=CARTESIAN_POINT('Ctrl Pts',(-2.15949404620135,-1.56341064383982,
13.8525833129073));
#435858=CARTESIAN_POINT('Ctrl Pts',(-2.15986887664421,-1.56322920984854,
13.8522628768812));
#435859=CARTESIAN_POINT('Ctrl Pts',(-2.16023873932082,-1.56305780519975,
13.851937733538));
#435860=CARTESIAN_POINT('Ctrl Pts',(-2.16249743937065,-1.56201106079091,
13.8499521282529));
#435861=CARTESIAN_POINT('Ctrl Pts',(-2.16479705984628,-1.56123802173827,
13.847639871647));
#435862=CARTESIAN_POINT('Ctrl Pts',(-2.16699114162711,-1.56070316305052,
13.8452109780794));
#435863=CARTESIAN_POINT('Ctrl Pts',(-2.16797830443553,-1.56046251905589,
13.8441181685877));
#435864=CARTESIAN_POINT('Ctrl Pts',(-2.16894418485651,-1.56026937647777,
13.8430021611332));
#435865=CARTESIAN_POINT('Ctrl Pts',(-2.16987681917792,-1.5601174904455,
13.8418824960098));
#435866=CARTESIAN_POINT('Ctrl Pts',(-2.17207459577202,-1.5597595671319,
13.8392439765549));
#435867=CARTESIAN_POINT('Ctrl Pts',(-2.17419220479122,-1.5596099068373,
13.8364981347964));
#435868=CARTESIAN_POINT('Ctrl Pts',(-2.17623283400634,-1.55963397838338,
13.8336931113419));
#435869=CARTESIAN_POINT('Ctrl Pts',(-2.17822027726992,-1.55965742254057,
13.8309611966328));
#435870=CARTESIAN_POINT('Ctrl Pts',(-2.18013668608987,-1.55984624831165,
13.8281701127185));
#435871=CARTESIAN_POINT('Ctrl Pts',(-2.18197027689338,-1.56020499048229,
13.825358068512));
#435872=CARTESIAN_POINT('Ctrl Pts',(-2.18236780135844,-1.56028276617205,
13.8247484142932));
#435873=CARTESIAN_POINT('Ctrl Pts',(-2.18276131079612,-1.5603686509502,
13.8241378483365));
#435874=CARTESIAN_POINT('Ctrl Pts',(-2.18315043670734,-1.56046289035817,
13.8235269408515));
#435875=CARTESIAN_POINT('',(-2.14726040899293,-1.57365294711932,12.5969504640361));
#435876=CARTESIAN_POINT('Origin',(-2.17508612331582,-1.59389148586697,12.584524458991));
#435877=CARTESIAN_POINT('Origin',(-2.17508612331582,-1.59389148586697,12.584524458991));
#435878=CARTESIAN_POINT('Ctrl Pts',(-2.14563951868149,-1.61165173575209,
12.5893111709658));
#435879=CARTESIAN_POINT('Ctrl Pts',(-2.13977729878546,-1.60195158047238,
12.5770542771492));
#435880=CARTESIAN_POINT('Ctrl Pts',(-2.15195938587367,-1.59102453013707,
12.5737548217797));
#435881=CARTESIAN_POINT('Ctrl Pts',(-2.15845822617462,-1.63286271987995,
12.5663937883685));
#435882=CARTESIAN_POINT('Ctrl Pts',(-2.15258852820297,-1.62315019070507,
12.5540940315304));
#435883=CARTESIAN_POINT('Ctrl Pts',(-2.16481050928352,-1.61219167010326,
12.5508374392248));
#435884=CARTESIAN_POINT('Ctrl Pts',(-2.17126399974902,-1.65405230238483,
12.5434499600945));
#435885=CARTESIAN_POINT('Ctrl Pts',(-2.1653752172991,-1.64430819431878,
12.5311293540533));
#435886=CARTESIAN_POINT('Ctrl Pts',(-2.17764806832898,-1.63333874163613,
12.5278936106989));
#435887=CARTESIAN_POINT('Ctrl Pts',(-2.18405785253628,-1.67522215968519,
12.5204817579905));
#435888=CARTESIAN_POINT('Ctrl Pts',(-2.17813992463758,-1.66542982494346,
12.5081597038247));
#435889=CARTESIAN_POINT('Ctrl Pts',(-2.19047310544298,-1.65446731172267,
12.5049254088044));
#435890=CARTESIAN_POINT('Ctrl Pts',(-2.17485966055452,-1.66000200552889,
12.5369868989719));
#435891=CARTESIAN_POINT('Ctrl Pts',(-2.17534145930686,-1.66079923268157,
12.5342545179733));
#435892=CARTESIAN_POINT('Ctrl Pts',(-2.17590802981826,-1.66149554796143,
12.5314872231885));
#435893=CARTESIAN_POINT('Ctrl Pts',(-2.1765708169311,-1.66201644560318,
12.5287124745063));
#435894=CARTESIAN_POINT('Ctrl Pts',(-2.17716855124728,-1.66248621695156,
12.5262100684184));
#435895=CARTESIAN_POINT('Ctrl Pts',(-2.17784454637923,-1.66281206802078,
12.5237004536639));
#435896=CARTESIAN_POINT('Ctrl Pts',(-2.17863919409348,-1.66293987874678,
12.5212220730815));
#435897=CARTESIAN_POINT('Ctrl Pts',(-2.17924756566123,-1.66303772891404,
12.5193246583486));
#435898=CARTESIAN_POINT('Ctrl Pts',(-2.17993285387773,-1.66302004605718,
12.517417831369));
#435899=CARTESIAN_POINT('Ctrl Pts',(-2.18071177879441,-1.66279104676097,
12.5155812248348));
#435900=CARTESIAN_POINT('Ctrl Pts',(-2.18104360499566,-1.66269349182991,
12.5147988205793));
#435901=CARTESIAN_POINT('Ctrl Pts',(-2.18139283942619,-1.6625577538129,
12.5140295443047));
#435902=CARTESIAN_POINT('Ctrl Pts',(-2.18176242080078,-1.66237777503528,
12.5132817086137));
#435903=CARTESIAN_POINT('Ctrl Pts',(-2.18232173221537,-1.66210540150232,
12.5121499604604));
#435904=CARTESIAN_POINT('Ctrl Pts',(-2.18293659040559,-1.66171939305322,
12.5110494206568));
#435905=CARTESIAN_POINT('Ctrl Pts',(-2.18359839614335,-1.66118351500816,
12.5100666561695));
#435906=CARTESIAN_POINT('Ctrl Pts',(-2.18397840347396,-1.66087581506871,
12.5095023550641));
#435907=CARTESIAN_POINT('Ctrl Pts',(-2.18437786942042,-1.66051464018997,
12.5089719619137));
#435908=CARTESIAN_POINT('Ctrl Pts',(-2.18478502293511,-1.66010202256744,
12.5085043804652));
#435909=CARTESIAN_POINT('Ctrl Pts',(-2.1853808390684,-1.6594982104241,12.5078201359221));
#435910=CARTESIAN_POINT('Ctrl Pts',(-2.18600953869774,-1.65876587526262,
12.5072563000949));
#435911=CARTESIAN_POINT('Ctrl Pts',(-2.18662208166213,-1.65794914403194,
12.5068768744332));
#435912=CARTESIAN_POINT('Ctrl Pts',(-2.18706376730705,-1.65736022459066,
12.5066032824114));
#435913=CARTESIAN_POINT('Ctrl Pts',(-2.18750486024884,-1.65671711384018,
12.5064197834844));
#435914=CARTESIAN_POINT('Ctrl Pts',(-2.18792286036064,-1.65605718679586,
12.5063282718343));
#435915=CARTESIAN_POINT('Ctrl Pts',(-2.18853301111429,-1.65509389761941,
12.5061946931565));
#435916=CARTESIAN_POINT('Ctrl Pts',(-2.18910789664451,-1.65407475724285,
12.5062515701262));
#435917=CARTESIAN_POINT('Ctrl Pts',(-2.18962530789657,-1.65307061322183,
12.5064436508398));
#435918=CARTESIAN_POINT('',(-2.15195938587367,-1.59102453013707,12.5737548217797));
#435919=CARTESIAN_POINT('Origin',(-2.16446819183562,-1.60027276096282,12.5893111709658));
#435920=CARTESIAN_POINT('Ctrl Pts',(-2.18962530789657,-1.65307061322183,
12.5064436508398));
#435921=CARTESIAN_POINT('Ctrl Pts',(-2.18405018354364,-1.643885931616,12.5164271754438));
#435922=CARTESIAN_POINT('Ctrl Pts',(-2.17847267060597,-1.6346977176192,
12.5264061185523));
#435923=CARTESIAN_POINT('Ctrl Pts',(-2.17289268576872,-1.62550584633245,
12.536380305637));
#435924=CARTESIAN_POINT('Ctrl Pts',(-2.16591883646502,-1.61401787153639,
12.5488460165097));
#435925=CARTESIAN_POINT('Ctrl Pts',(-2.15894112399064,-1.60252418069806,
12.5613043021964));
#435926=CARTESIAN_POINT('Ctrl Pts',(-2.15195938587367,-1.59102453013707,
12.5737548217797));
#435927=CARTESIAN_POINT('Ctrl Pts',(-2.18315043670734,-1.56046289035817,
12.5893111709658));
#435928=CARTESIAN_POINT('Ctrl Pts',(-2.17213491717367,-1.5577951265075,
12.5770542771492));
#435929=CARTESIAN_POINT('Ctrl Pts',(-2.16538527500074,-1.57270304404793,
12.5737548217797));
#435930=CARTESIAN_POINT('Ctrl Pts',(-2.17287305279036,-1.55797388988848,
12.5928319619712));
#435931=CARTESIAN_POINT('Ctrl Pts',(-2.16470314250846,-1.55934720061706,
12.5821634970842));
#435932=CARTESIAN_POINT('Ctrl Pts',(-2.16164369450117,-1.57178718776297,
12.5773203894503));
#435933=CARTESIAN_POINT('Ctrl Pts',(-2.15643226432231,-1.56118084699587,
12.5969440695591));
#435934=CARTESIAN_POINT('Ctrl Pts',(-2.15404153911457,-1.56441240629952,
12.5878292599214));
#435935=CARTESIAN_POINT('Ctrl Pts',(-2.15578425371447,-1.5729322208475,
12.5813877129824));
#435936=CARTESIAN_POINT('Ctrl Pts',(-2.1383034984697,-1.58582883056862,
12.596957478804));
#435937=CARTESIAN_POINT('Ctrl Pts',(-2.14067662001774,-1.58262120102843,
12.5878468778671));
#435938=CARTESIAN_POINT('Ctrl Pts',(-2.14930052242839,-1.58175761018249,
12.5814011370086));
#435939=CARTESIAN_POINT('Ctrl Pts',(-2.14016217694572,-1.60258843442619,
12.5928371701607));
#435940=CARTESIAN_POINT('Ctrl Pts',(-2.13901736357199,-1.59438938155143,
12.5821692192952));
#435941=CARTESIAN_POINT('Ctrl Pts',(-2.14995232295486,-1.58772226183877,
12.5773318885715));
#435942=CARTESIAN_POINT('Ctrl Pts',(-2.14563951868144,-1.61165173575211,
12.5893111709658));
#435943=CARTESIAN_POINT('Ctrl Pts',(-2.13977729878542,-1.60195158047241,
12.5770542771492));
#435944=CARTESIAN_POINT('Ctrl Pts',(-2.15195938587362,-1.5910245301371,
12.5737548217797));
#435945=CARTESIAN_POINT('',(-2.16538527500074,-1.57270304404793,12.5737548217797));
#435946=CARTESIAN_POINT('Origin',(-2.17797212232493,-1.581844776621,12.5893111709658));
#435947=CARTESIAN_POINT('Ctrl Pts',(-2.15195938587362,-1.5910245301371,
12.5737548217797));
#435948=CARTESIAN_POINT('Ctrl Pts',(-2.15141334535943,-1.59018419723408,
12.5746934679442));
#435949=CARTESIAN_POINT('Ctrl Pts',(-2.15096271955715,-1.58915450221877,
12.5756680099006));
#435950=CARTESIAN_POINT('Ctrl Pts',(-2.15065572622269,-1.58805393020359,
12.5765688348656));
#435951=CARTESIAN_POINT('Ctrl Pts',(-2.15057445313592,-1.58776256594631,
12.5768073183026));
#435952=CARTESIAN_POINT('Ctrl Pts',(-2.15050302340756,-1.58746636141546,
12.5770407398754));
#435953=CARTESIAN_POINT('Ctrl Pts',(-2.15044178803712,-1.58716766194725,
12.5772674179684));
#435954=CARTESIAN_POINT('Ctrl Pts',(-2.15019049463559,-1.58594188010145,
12.5781976435658));
#435955=CARTESIAN_POINT('Ctrl Pts',(-2.15010765757659,-1.5846021952488,
12.5790594849312));
#435956=CARTESIAN_POINT('Ctrl Pts',(-2.15024706728575,-1.5832360848372,
12.5797571720116));
#435957=CARTESIAN_POINT('Ctrl Pts',(-2.15033789772399,-1.58234601478309,
12.580211740231));
#435958=CARTESIAN_POINT('Ctrl Pts',(-2.15054587538036,-1.58140618380107,
12.5806009430798));
#435959=CARTESIAN_POINT('Ctrl Pts',(-2.1508736577402,-1.58048657987062,
12.5808812374708));
#435960=CARTESIAN_POINT('Ctrl Pts',(-2.15115533152798,-1.57969633501893,
12.5811221033394));
#435961=CARTESIAN_POINT('Ctrl Pts',(-2.15153134934478,-1.57890488675521,
12.581287365893));
#435962=CARTESIAN_POINT('Ctrl Pts',(-2.15198801935523,-1.57816048378301,
12.581359338449));
#435963=CARTESIAN_POINT('Ctrl Pts',(-2.1520514870568,-1.57805702714121,
12.5813693411482));
#435964=CARTESIAN_POINT('Ctrl Pts',(-2.15211647489126,-1.57795443266022,
12.5813775999465));
#435965=CARTESIAN_POINT('Ctrl Pts',(-2.15218290834766,-1.57785278151387,
12.5813841266931));
#435966=CARTESIAN_POINT('Ctrl Pts',(-2.15229562074141,-1.57768031804963,
12.5813952001081));
#435967=CARTESIAN_POINT('Ctrl Pts',(-2.1524137589618,-1.57750974801417,
12.5814007534795));
#435968=CARTESIAN_POINT('Ctrl Pts',(-2.15253743367731,-1.57734125798304,
12.5814005856065));
#435969=CARTESIAN_POINT('Ctrl Pts',(-2.15310356817123,-1.57656997649586,
12.5813998171494));
#435970=CARTESIAN_POINT('Ctrl Pts',(-2.15374632955927,-1.5758953703895,
12.58127954464));
#435971=CARTESIAN_POINT('Ctrl Pts',(-2.15444064631559,-1.57530085853175,
12.5810700125799));
#435972=CARTESIAN_POINT('Ctrl Pts',(-2.15527930190294,-1.57458275589817,
12.5808169217085));
#435973=CARTESIAN_POINT('Ctrl Pts',(-2.15620413715905,-1.57399415747095,
12.5804173076348));
#435974=CARTESIAN_POINT('Ctrl Pts',(-2.15712011844871,-1.57356467680243,
12.5799304713245));
#435975=CARTESIAN_POINT('Ctrl Pts',(-2.15825530783048,-1.57303241495377,
12.5793271277669));
#435976=CARTESIAN_POINT('Ctrl Pts',(-2.15943364635984,-1.57268237050142,
12.5785808224116));
#435977=CARTESIAN_POINT('Ctrl Pts',(-2.16059643289824,-1.57249889481065,
12.5777485681082));
#435978=CARTESIAN_POINT('Ctrl Pts',(-2.16232911223324,-1.57222549593015,
12.576508418016));
#435979=CARTESIAN_POINT('Ctrl Pts',(-2.16401159887118,-1.57231746453322,
12.5750928681475));
#435980=CARTESIAN_POINT('Ctrl Pts',(-2.16538527500074,-1.57270304404793,
12.5737548217797));
#435981=CARTESIAN_POINT('Ctrl Pts',(-2.16538527500074,-1.57270304404793,
12.5737548217797));
#435982=CARTESIAN_POINT('Ctrl Pts',(-2.17213491717367,-1.5577951265075,
12.5770542771492));
#435983=CARTESIAN_POINT('Ctrl Pts',(-2.18315043670734,-1.56046289035817,
12.5893111709658));
#435984=CARTESIAN_POINT('Ctrl Pts',(-2.18943686311886,-1.57857978320892,
12.5508408821982));
#435985=CARTESIAN_POINT('Ctrl Pts',(-2.19620448976733,-1.56362435094581,
12.55409748406));
#435986=CARTESIAN_POINT('Ctrl Pts',(-2.2072340622827,-1.5662955181799,12.5663972313419));
#435987=CARTESIAN_POINT('Ctrl Pts',(-2.21346523583044,-1.58444963573048,
12.52790050457));
#435988=CARTESIAN_POINT('Ctrl Pts',(-2.22022796340049,-1.56944241103187,
12.5311362602938));
#435989=CARTESIAN_POINT('Ctrl Pts',(-2.23129339143735,-1.57212226183859,
12.5434568539655));
#435990=CARTESIAN_POINT('Ctrl Pts',(-2.23747220055742,-1.59031312334059,
12.5049357605811));
#435991=CARTESIAN_POINT('Ctrl Pts',(-2.24421014365406,-1.57525047059229,
12.5081700652078));
#435992=CARTESIAN_POINT('Ctrl Pts',(-2.25533032707183,-1.57794358218308,
12.5204921097672));
#435993=CARTESIAN_POINT('Ctrl Pts',(-2.23589580952561,-1.58992810221813,
12.5064436508395));
#435994=CARTESIAN_POINT('Ctrl Pts',(-2.236761714628,-1.58906841847149,12.5062361689309));
#435995=CARTESIAN_POINT('Ctrl Pts',(-2.23762552625068,-1.58813749360828,
12.5061871075061));
#435996=CARTESIAN_POINT('Ctrl Pts',(-2.23840967326764,-1.5871908521255,
12.5063648335164));
#435997=CARTESIAN_POINT('Ctrl Pts',(-2.23876588121094,-1.58676082917275,
12.5064455676329));
#435998=CARTESIAN_POINT('Ctrl Pts',(-2.23911044876432,-1.58632142457011,
12.506574497099));
#435999=CARTESIAN_POINT('Ctrl Pts',(-2.23942777490356,-1.58589083016024,
12.5067492519495));
#436000=CARTESIAN_POINT('Ctrl Pts',(-2.24006545409804,-1.58502553397919,
12.5071004286051));
#436001=CARTESIAN_POINT('Ctrl Pts',(-2.24061592034305,-1.58416352221299,
12.5076537929612));
#436002=CARTESIAN_POINT('Ctrl Pts',(-2.24104582996362,-1.58337458396168,
12.5083435010503));
#436003=CARTESIAN_POINT('Ctrl Pts',(-2.24107289534344,-1.58332491558395,
12.5083869222963));
#436004=CARTESIAN_POINT('Ctrl Pts',(-2.24109947537414,-1.58327552570261,
12.5084308732336));
#436005=CARTESIAN_POINT('Ctrl Pts',(-2.24112555899769,-1.5832264269791,
12.5084753333615));
#436006=CARTESIAN_POINT('Ctrl Pts',(-2.24133478408543,-1.58283259041285,
12.508831962269));
#436007=CARTESIAN_POINT('Ctrl Pts',(-2.24151745646358,-1.58245009711726,
12.509227847131));
#436008=CARTESIAN_POINT('Ctrl Pts',(-2.24167067102003,-1.5820915273163,
12.5096423454524));
#436009=CARTESIAN_POINT('Ctrl Pts',(-2.24215077763003,-1.58096792825642,
12.5109411997424));
#436010=CARTESIAN_POINT('Ctrl Pts',(-2.24238005312552,-1.58001392886605,
12.5124831113042));
#436011=CARTESIAN_POINT('Ctrl Pts',(-2.24245164411503,-1.57921280889644,
12.5140723025008));
#436012=CARTESIAN_POINT('Ctrl Pts',(-2.24245835226916,-1.57913774307785,
12.5142212114565));
#436013=CARTESIAN_POINT('Ctrl Pts',(-2.24246370141256,-1.57906400438223,
12.5143705582413));
#436014=CARTESIAN_POINT('Ctrl Pts',(-2.24246778349925,-1.57899157173358,
12.5145201959299));
#436015=CARTESIAN_POINT('Ctrl Pts',(-2.24252022398046,-1.5780610665208,
12.5164425148273));
#436016=CARTESIAN_POINT('Ctrl Pts',(-2.24237607724193,-1.57731482292979,
12.5184635205941));
#436017=CARTESIAN_POINT('Ctrl Pts',(-2.24210289351335,-1.57669305011659,
12.5205025929158));
#436018=CARTESIAN_POINT('Ctrl Pts',(-2.24194443612279,-1.57633239724016,
12.5216853356836));
#436019=CARTESIAN_POINT('Ctrl Pts',(-2.24174329370341,-1.57601407903197,
12.5228750347131));
#436020=CARTESIAN_POINT('Ctrl Pts',(-2.24151631132257,-1.57573108283529,
12.5240609649613));
#436021=CARTESIAN_POINT('Ctrl Pts',(-2.24095919524596,-1.57503648385276,
12.5269717671326));
#436022=CARTESIAN_POINT('Ctrl Pts',(-2.24022262229414,-1.57454163107181,
12.5299036066169));
#436023=CARTESIAN_POINT('Ctrl Pts',(-2.23936585500481,-1.57418329891015,
12.5328133004019));
#436024=CARTESIAN_POINT('Ctrl Pts',(-2.23895455681786,-1.5740112786075,
12.5342101228451));
#436025=CARTESIAN_POINT('Ctrl Pts',(-2.23851587010387,-1.57387141841433,
12.5356023438238));
#436026=CARTESIAN_POINT('Ctrl Pts',(-2.23805711869614,-1.5737603168592,
12.5369868989719));
#436027=CARTESIAN_POINT('Origin',(-14.6270958531998,-4.56871522885748,-1.24066348164869));
#436028=CARTESIAN_POINT('Ctrl Pts',(-2.17483800949988,-1.65996625650419,
12.5369868989719));
#436029=CARTESIAN_POINT('Ctrl Pts',(-2.18279663890026,-1.67307898016302,
12.5369868989719));
#436030=CARTESIAN_POINT('Ctrl Pts',(-2.17324475226915,-1.68508084524608,
12.5369868989719));
#436031=CARTESIAN_POINT('Ctrl Pts',(-2.17752828089512,-1.66439890429058,
12.5218025310016));
#436032=CARTESIAN_POINT('Ctrl Pts',(-2.18057822279872,-1.67581615956887,
12.5216901060418));
#436033=CARTESIAN_POINT('Ctrl Pts',(-2.17327388248902,-1.68504426985358,
12.5161920673678));
#436034=CARTESIAN_POINT('Ctrl Pts',(-2.18353821313673,-1.66486450674627,
12.5042015548894));
#436035=CARTESIAN_POINT('Ctrl Pts',(-2.18401471619858,-1.67127935591431,
12.4980677368513));
#436036=CARTESIAN_POINT('Ctrl Pts',(-2.17987961749313,-1.67667303169434,
12.4907278922777));
#436037=CARTESIAN_POINT('Ctrl Pts',(-2.18960934508998,-1.65305856199325,
12.506463626192));
#436038=CARTESIAN_POINT('Ctrl Pts',(-2.19483108864571,-1.65700074826163,
12.4999376786891));
#436039=CARTESIAN_POINT('Ctrl Pts',(-2.19476731264059,-1.6569526001883,
12.4906970594712));
#436040=CARTESIAN_POINT('Origin',(-2.15603098740039,-1.67138098031816,12.5369868989719));
#436041=CARTESIAN_POINT('Origin',(-2.15603098740039,-1.67138098031816,14.));
#436042=CARTESIAN_POINT('Origin',(-2.15603098740039,-1.67138098031816,13.7435492065112));
#436043=CARTESIAN_POINT('Ctrl Pts',(-2.16205306463871,-1.63881111479855,
13.793642941384));
#436044=CARTESIAN_POINT('Ctrl Pts',(-2.1676687580577,-1.64805071470493,
13.8071662555867));
#436045=CARTESIAN_POINT('Ctrl Pts',(-2.15457450270751,-1.65893923436826,
13.8103758687955));
#436046=CARTESIAN_POINT('Ctrl Pts',(-2.17064994587363,-1.65303628046563,
13.7804579775006));
#436047=CARTESIAN_POINT('Ctrl Pts',(-2.177570538214,-1.66444237854459,13.7901904343351));
#436048=CARTESIAN_POINT('Ctrl Pts',(-2.16724525986977,-1.67634383019045,
13.7927914348262));
#436049=CARTESIAN_POINT('Ctrl Pts',(-2.17571125336112,-1.66141117086671,
13.7597120340895));
#436050=CARTESIAN_POINT('Ctrl Pts',(-2.18371542853105,-1.67461421104018,
13.7635825532445));
#436051=CARTESIAN_POINT('Ctrl Pts',(-2.17469652490333,-1.68662234551219,
13.7651073818884));
#436052=CARTESIAN_POINT('Ctrl Pts',(-2.17472013346362,-1.65977117556342,
13.7381884353898));
#436053=CARTESIAN_POINT('Ctrl Pts',(-2.18253772462018,-1.67266470801713,
13.7368803041982));
#436054=CARTESIAN_POINT('Ctrl Pts',(-2.17323694564973,-1.68460979686827,
13.7363986145813));
#436055=CARTESIAN_POINT('Origin',(-2.14531043198703,-1.65364178696841,13.7902182540695));
#436056=CARTESIAN_POINT('Ctrl Pts',(-2.1456374821273,-1.61164836735401,
13.8235227101244));
#436057=CARTESIAN_POINT('Ctrl Pts',(-2.15158786257978,-1.62148582946527,
13.8358800583119));
#436058=CARTESIAN_POINT('Ctrl Pts',(-2.13917755793398,-1.63246810553425,
13.8390832900376));
#436059=CARTESIAN_POINT('Ctrl Pts',(-2.1518067377986,-1.62185657159162,
13.8124254819052));
#436060=CARTESIAN_POINT('Ctrl Pts',(-2.15776867356756,-1.63171313805881,
13.8247886449157));
#436061=CARTESIAN_POINT('Ctrl Pts',(-2.1453313926142,-1.64269652658828,
13.8279860620657));
#436062=CARTESIAN_POINT('Ctrl Pts',(-2.15797322861023,-1.63206020084418,
13.8013225099955));
#436063=CARTESIAN_POINT('Ctrl Pts',(-2.1639439083346,-1.64193121991324,
13.8136962257787));
#436064=CARTESIAN_POINT('Ctrl Pts',(-2.15148261063204,-1.65292007264905,
13.8168830918626));
#436065=CARTESIAN_POINT('Ctrl Pts',(-2.16413706213862,-1.64225943311734,
13.7902140179785));
#436066=CARTESIAN_POINT('Ctrl Pts',(-2.17011385819802,-1.65214055706196,
13.802602731458));
#436067=CARTESIAN_POINT('Ctrl Pts',(-2.15763131637945,-1.66313893431814,
13.8057746032558));
#436068=CARTESIAN_POINT('Origin',(-2.12681084552735,-1.62303071054136,13.8235269408515));
#436069=CARTESIAN_POINT('Ctrl Pts',(-2.18315043670734,-1.56046289035817,
13.8235269408515));
#436070=CARTESIAN_POINT('Ctrl Pts',(-2.19462617425083,-1.56324211086471,
13.8362179249168));
#436071=CARTESIAN_POINT('Ctrl Pts',(-2.20127772059233,-1.54751252297043,
13.8391868794938));
#436072=CARTESIAN_POINT('Ctrl Pts',(-2.17265063636421,-1.55792002456695,
13.8400110824519));
#436073=CARTESIAN_POINT('Ctrl Pts',(-2.18265659817329,-1.55682339740282,
13.8494522556837));
#436074=CARTESIAN_POINT('Ctrl Pts',(-2.18397156707257,-1.54343688388251,
13.85569149686));
#436075=CARTESIAN_POINT('Ctrl Pts',(-2.15663504899221,-1.56090309130709,
13.8586819406588));
#436076=CARTESIAN_POINT('Ctrl Pts',(-2.15921973523695,-1.55739945881335,
13.868010383617));
#436077=CARTESIAN_POINT('Ctrl Pts',(-2.1574121079548,-1.54853236512931,
13.8744918421245));
#436078=CARTESIAN_POINT('Ctrl Pts',(-2.138097553707,-1.58611088308855,13.8587686893867));
#436079=CARTESIAN_POINT('Ctrl Pts',(-2.1355358258333,-1.58958329985802,
13.8680909899357));
#436080=CARTESIAN_POINT('Ctrl Pts',(-2.12655469491602,-1.59049746010243,
13.8745789365162));
#436081=CARTESIAN_POINT('Ctrl Pts',(-2.14004266069163,-1.60239067211602,
13.8400379222776));
#436082=CARTESIAN_POINT('Ctrl Pts',(-2.142003711595,-1.6122610577854,13.8494748685453));
#436083=CARTESIAN_POINT('Ctrl Pts',(-2.12964132381769,-1.61754617592111,
13.8557104837033));
#436084=CARTESIAN_POINT('Ctrl Pts',(-2.14563951867576,-1.61165173575538,
13.8235269408542));
#436085=CARTESIAN_POINT('Ctrl Pts',(-2.15174665658629,-1.6217571543678,
13.8362179249195));
#436086=CARTESIAN_POINT('Ctrl Pts',(-2.13875151769632,-1.63283819083947,
13.8391868794965));
#436087=CARTESIAN_POINT('Origin',(-2.18832875108976,-1.53908100409533,13.8235269408515));
#436088=CARTESIAN_POINT('Ctrl Pts',(-2.21790861637325,-1.56888070545357,
13.7902140241682));
#436089=CARTESIAN_POINT('Ctrl Pts',(-2.22913121062742,-1.57160319945704,
13.8026027327198));
#436090=CARTESIAN_POINT('Ctrl Pts',(-2.2358583528096,-1.55638730348163,
13.8057746032556));
#436091=CARTESIAN_POINT('Ctrl Pts',(-2.20632634380879,-1.56607568405177,
13.8013225161808));
#436092=CARTESIAN_POINT('Ctrl Pts',(-2.21753746007388,-1.56879538991384,
13.8136962270464));
#436093=CARTESIAN_POINT('Ctrl Pts',(-2.22426191989512,-1.55360262040246,
13.8168830918628));
#436094=CARTESIAN_POINT('Ctrl Pts',(-2.19473907802239,-1.56326945338002,
13.8124254880875));
#436095=CARTESIAN_POINT('Ctrl Pts',(-2.20593377898326,-1.56598517527985,
13.8247886461868));
#436096=CARTESIAN_POINT('Ctrl Pts',(-2.21266026338476,-1.55081695291219,
13.8279860620656));
#436097=CARTESIAN_POINT('Ctrl Pts',(-2.18314661686892,-1.56046196448233,
13.8235227163065));
#436098=CARTESIAN_POINT('Ctrl Pts',(-2.19431961995507,-1.56317242298117,
13.8358800595847));
#436099=CARTESIAN_POINT('Ctrl Pts',(-2.20105317008208,-1.54803025888599,
13.8390832900376));
#436100=CARTESIAN_POINT('Origin',(-2.22309076268708,-1.54749974799863,13.7902182540695));
#436101=CARTESIAN_POINT('Ctrl Pts',(-2.23779484729206,-1.57369677098558,
13.7382347919292));
#436102=CARTESIAN_POINT('Ctrl Pts',(-2.25245552434945,-1.57727202159944,
13.7369371795943));
#436103=CARTESIAN_POINT('Ctrl Pts',(-2.26104370370444,-1.56479055724679,
13.7364597369711));
#436104=CARTESIAN_POINT('Ctrl Pts',(-2.23963326042968,-1.57414200252046,
13.7595490285573));
#436105=CARTESIAN_POINT('Ctrl Pts',(-2.25464396688323,-1.57780157875066,
13.7633824266926));
#436106=CARTESIAN_POINT('Ctrl Pts',(-2.26337344003257,-1.5655667939613,
13.7648920890506));
#436107=CARTESIAN_POINT('Ctrl Pts',(-2.2302574541424,-1.57187134609213,
13.7803806590111));
#436108=CARTESIAN_POINT('Ctrl Pts',(-2.24323989928002,-1.57504199338444,
13.7901039518744));
#436109=CARTESIAN_POINT('Ctrl Pts',(-2.25149501620699,-1.56161297681778,
13.7926933640892));
#436110=CARTESIAN_POINT('Ctrl Pts',(-2.21396020989002,-1.56792443827051,
13.7936647693663));
#436111=CARTESIAN_POINT('Ctrl Pts',(-2.22446466447944,-1.57049927141529,
13.8072068914933));
#436112=CARTESIAN_POINT('Ctrl Pts',(-2.2308999371656,-1.55471220280514,
13.8104111085397));
#436113=CARTESIAN_POINT('Origin',(-2.24323543307856,-1.55237843059637,13.7435492065112));
#436114=CARTESIAN_POINT('Origin',(-2.24323543307856,-1.55237843059637,14.));
#436115=CARTESIAN_POINT('Origin',(-2.24323543307856,-1.55237843059637,12.5369868989719));
#436116=CARTESIAN_POINT('Ctrl Pts',(-2.23588082786927,-1.5899174488916,
12.506462012331));
#436117=CARTESIAN_POINT('Ctrl Pts',(-2.24120956088414,-1.59370666945078,
12.4999388158272));
#436118=CARTESIAN_POINT('Ctrl Pts',(-2.24114651498437,-1.5936618380023,
12.4907030323752));
#436119=CARTESIAN_POINT('Ctrl Pts',(-2.24530774573641,-1.58057069530115,
12.5042014951932));
#436120=CARTESIAN_POINT('Ctrl Pts',(-2.25156562345814,-1.57909419147928,
12.4980716682127));
#436121=CARTESIAN_POINT('Ctrl Pts',(-2.25546159400896,-1.57353119060809,
12.4907355092743));
#436122=CARTESIAN_POINT('Ctrl Pts',(-2.24305580294359,-1.57498012691293,
12.5218047446509));
#436123=CARTESIAN_POINT('Ctrl Pts',(-2.25485562667871,-1.57444812056282,
12.5216906929434));
#436124=CARTESIAN_POINT('Ctrl Pts',(-2.26145438788765,-1.56471019959181,
12.5161988840776));
#436125=CARTESIAN_POINT('Ctrl Pts',(-2.23801978982061,-1.57375124195579,
12.5369868989719));
#436126=CARTESIAN_POINT('Ctrl Pts',(-2.25291264663855,-1.57738557096137,
12.5369868989719));
#436127=CARTESIAN_POINT('Ctrl Pts',(-2.26147954735017,-1.56467283153519,
12.5369868989719));
#436128=CARTESIAN_POINT('Origin',(-4.15555475928479E-31,-8.1970313822065E-31,
12.5));
#436129=CARTESIAN_POINT('Origin',(-2.04869397153156,-1.7332176067911,12.5));
#436130=CARTESIAN_POINT('',(-2.04869397153156,-1.7332176067911,12.5893111709658));
#436131=CARTESIAN_POINT('',(-2.04869397153156,-1.7332176067911,13.8235269408515));
#436132=CARTESIAN_POINT('',(-2.04869397153156,-1.7332176067911,12.5));
#436133=CARTESIAN_POINT('',(-2.08265410961903,-1.74444176467851,13.7902182540695));
#436134=CARTESIAN_POINT('',(-2.04869397153156,-1.7332176067911,13.8235269408515));
#436135=CARTESIAN_POINT('',(-2.10233409235841,-1.75094619151327,13.7435492065112));
#436136=CARTESIAN_POINT('Origin',(-2.0375871070498,-1.72954702250194,13.74452129187));
#436137=CARTESIAN_POINT('',(-2.10233409235841,-1.75094619151327,12.5369868989719));
#436138=CARTESIAN_POINT('',(-2.10233409235841,-1.75094619151327,12.5));
#436139=CARTESIAN_POINT('Ctrl Pts',(-2.10233409235841,-1.75094619151327,
12.5369868989719));
#436140=CARTESIAN_POINT('Ctrl Pts',(-2.08446709269668,-1.74504097332302,
12.5544431401645));
#436141=CARTESIAN_POINT('Ctrl Pts',(-2.06658731408192,-1.73913153156377,
12.5718848856037));
#436142=CARTESIAN_POINT('Ctrl Pts',(-2.04869397153156,-1.7332176067911,
12.5893111709658));
#436143=CARTESIAN_POINT('Origin',(-2.12971550850767,-2.02734756722178,12.5));
#436144=CARTESIAN_POINT('',(-2.03231742028997,-1.83174973854323,13.7435492065112));
#436145=CARTESIAN_POINT('',(-2.02307844558101,-1.81319574610499,13.7902182540695));
#436146=CARTESIAN_POINT('Origin',(-1.99880001686223,-1.76443906075294,13.7418732680451));
#436147=CARTESIAN_POINT('',(-2.00713550187734,-1.78117863747128,13.8235269408515));
#436148=CARTESIAN_POINT('',(-2.02307844558101,-1.81319574610499,13.7902182540695));
#436149=CARTESIAN_POINT('',(-2.00713550187734,-1.78117863747128,12.5893111709658));
#436150=CARTESIAN_POINT('',(-2.00713550187734,-1.78117863747128,12.5));
#436151=CARTESIAN_POINT('',(-2.03231742028997,-1.83174973854323,12.5369868989719));
#436152=CARTESIAN_POINT('Ctrl Pts',(-2.00713550187734,-1.78117863747128,
12.5893111709658));
#436153=CARTESIAN_POINT('Ctrl Pts',(-2.01553571957422,-1.79804821234696,
12.5718848856037));
#436154=CARTESIAN_POINT('Ctrl Pts',(-2.02392956953899,-1.81490499934768,
12.5544431401645));
#436155=CARTESIAN_POINT('Ctrl Pts',(-2.03231742028997,-1.83174973854323,
12.5369868989719));
#436156=CARTESIAN_POINT('',(-2.03231742028997,-1.83174973854323,12.5));
#436157=CARTESIAN_POINT('Origin',(-2.03790661809615,-1.76585613664249,12.5));
#436158=CARTESIAN_POINT('',(-2.01267520976314,-1.74251162538801,13.8587068136939));
#436159=CARTESIAN_POINT('Ctrl Pts',(-2.00713550187136,-1.78117863747409,
13.8235269408542));
#436160=CARTESIAN_POINT('Ctrl Pts',(-2.00635442281481,-1.77961005055124,
13.8262006681044));
#436161=CARTESIAN_POINT('Ctrl Pts',(-2.0057106269782,-1.7779273874974,13.8288634856214));
#436162=CARTESIAN_POINT('Ctrl Pts',(-2.00519485375642,-1.7761402424379,
13.8314912288862));
#436163=CARTESIAN_POINT('Ctrl Pts',(-2.0046631447643,-1.77429788021702,
13.834200161153));
#436164=CARTESIAN_POINT('Ctrl Pts',(-2.00426642359461,-1.77234257128823,
13.8368750301949));
#436165=CARTESIAN_POINT('Ctrl Pts',(-2.0040281849101,-1.77025463655578,
13.8394886372968));
#436166=CARTESIAN_POINT('Ctrl Pts',(-2.00400978515861,-1.77009338029176,
13.839690492513));
#436167=CARTESIAN_POINT('Ctrl Pts',(-2.00399235197489,-1.76993132667031,
13.8398919674349));
#436168=CARTESIAN_POINT('Ctrl Pts',(-2.00397590740097,-1.76976846436512,
13.8400930404591));
#436169=CARTESIAN_POINT('Ctrl Pts',(-2.00371968987599,-1.7672309600821,
13.8432258934518));
#436170=CARTESIAN_POINT('Ctrl Pts',(-2.00370365223667,-1.76451020289391,
13.8462331177034));
#436171=CARTESIAN_POINT('Ctrl Pts',(-2.00402478216495,-1.76169436064464,
13.8489036603661));
#436172=CARTESIAN_POINT('Ctrl Pts',(-2.00412985961466,-1.76077298429107,
13.8497774930041));
#436173=CARTESIAN_POINT('Ctrl Pts',(-2.00427114907082,-1.75984165069557,
13.85061494757));
#436174=CARTESIAN_POINT('Ctrl Pts',(-2.00445235849077,-1.75890409169918,
13.8514076489583));
#436175=CARTESIAN_POINT('Ctrl Pts',(-2.00483564254826,-1.75692101920558,
13.8530843267192));
#436176=CARTESIAN_POINT('Ctrl Pts',(-2.00543807471819,-1.75471586669665,
13.8546805203176));
#436177=CARTESIAN_POINT('Ctrl Pts',(-2.00635631236334,-1.75245257872016,
13.8559412814273));
#436178=CARTESIAN_POINT('Ctrl Pts',(-2.00647920233942,-1.75214967738872,
13.8561100121513));
#436179=CARTESIAN_POINT('Ctrl Pts',(-2.00660767580941,-1.75184575891194,
13.8562727473908));
#436180=CARTESIAN_POINT('Ctrl Pts',(-2.00674189004378,-1.7515412309017,
13.8564289040185));
#436181=CARTESIAN_POINT('Ctrl Pts',(-2.00735055006546,-1.75016019984948,
13.8571370725437));
#436182=CARTESIAN_POINT('Ctrl Pts',(-2.00809005697689,-1.74874327646846,
13.8577210840554));
#436183=CARTESIAN_POINT('Ctrl Pts',(-2.00895768371589,-1.74735911572998,
13.8581177131616));
#436184=CARTESIAN_POINT('Ctrl Pts',(-2.00920203726839,-1.74696928842465,
13.8582294175695));
#436185=CARTESIAN_POINT('Ctrl Pts',(-2.00945638696643,-1.74658199676585,
13.8583265086086));
#436186=CARTESIAN_POINT('Ctrl Pts',(-2.00972027094894,-1.74619859419274,
13.8584082369006));
#436187=CARTESIAN_POINT('Ctrl Pts',(-2.01009940146851,-1.74564774750865,
13.8585256585398));
#436188=CARTESIAN_POINT('Ctrl Pts',(-2.01050319248188,-1.74509826367057,
13.8586122832068));
#436189=CARTESIAN_POINT('Ctrl Pts',(-2.01092179101424,-1.74456488429777,
13.8586682984299));
#436190=CARTESIAN_POINT('Ctrl Pts',(-2.01125662834578,-1.74413823367172,
13.8587131050557));
#436191=CARTESIAN_POINT('Ctrl Pts',(-2.0116044539627,-1.74371703022565,
13.8587357943552));
#436192=CARTESIAN_POINT('Ctrl Pts',(-2.01196569970361,-1.74330154638619,
13.8587355499465));
#436193=CARTESIAN_POINT('Ctrl Pts',(-2.01219918143841,-1.74303300927519,
13.8587353919793));
#436194=CARTESIAN_POINT('Ctrl Pts',(-2.01243571519801,-1.74276973999133,
13.8587257282814));
#436195=CARTESIAN_POINT('Ctrl Pts',(-2.01267520976314,-1.74251162538801,
13.8587068136939));
#436196=CARTESIAN_POINT('Ctrl Pts',(-2.01267520976314,-1.74251162538801,
13.8587068136939));
#436197=CARTESIAN_POINT('Ctrl Pts',(-2.01346289433184,-1.74166270052876,
13.8586446046466));
#436198=CARTESIAN_POINT('Ctrl Pts',(-2.01428256745166,-1.74086946537878,
13.858482427929));
#436199=CARTESIAN_POINT('Ctrl Pts',(-2.0151313475361,-1.74012850198304,
13.8582284286032));
#436200=CARTESIAN_POINT('Ctrl Pts',(-2.01600209716854,-1.73936835973146,
13.8579678548414));
#436201=CARTESIAN_POINT('Ctrl Pts',(-2.0169066143356,-1.73866252724527,
13.857615680862));
#436202=CARTESIAN_POINT('Ctrl Pts',(-2.01780327804193,-1.73803119238542,
13.8571944833187));
#436203=CARTESIAN_POINT('Ctrl Pts',(-2.02004099402433,-1.73645563167503,
13.8561433417727));
#436204=CARTESIAN_POINT('Ctrl Pts',(-2.02233171101368,-1.73526642366871,
13.8546163505474));
#436205=CARTESIAN_POINT('Ctrl Pts',(-2.02448301494958,-1.7343878405908,
13.8528973491086));
#436206=CARTESIAN_POINT('Ctrl Pts',(-2.02487602643913,-1.73422733642475,
13.8525833129072));
#436207=CARTESIAN_POINT('Ctrl Pts',(-2.02526439821924,-1.73407705830097,
13.8522628768812));
#436208=CARTESIAN_POINT('Ctrl Pts',(-2.0256470012784,-1.73393637122879,
13.851937733538));
#436209=CARTESIAN_POINT('Ctrl Pts',(-2.02798350507697,-1.73307721479843,
13.8499521282529));
#436210=CARTESIAN_POINT('Ctrl Pts',(-2.0303384836145,-1.73249418838686,
13.847639871647));
#436211=CARTESIAN_POINT('Ctrl Pts',(-2.03256886071764,-1.73213994743128,
13.8452109780794));
#436212=CARTESIAN_POINT('Ctrl Pts',(-2.03357235354285,-1.73198056709294,
13.8441181685877));
#436213=CARTESIAN_POINT('Ctrl Pts',(-2.03455076298957,-1.73186679540193,
13.8430021611332));
#436214=CARTESIAN_POINT('Ctrl Pts',(-2.03549267416889,-1.73179143311325,
13.8418824960098));
#436215=CARTESIAN_POINT('Ctrl Pts',(-2.03771231191553,-1.73161383995553,
13.8392439765549));
#436216=CARTESIAN_POINT('Ctrl Pts',(-2.03983507346879,-1.7316372824372,
13.8364981347964));
#436217=CARTESIAN_POINT('Ctrl Pts',(-2.04186695060406,-1.7318276041125,
13.8336931113419));
#436218=CARTESIAN_POINT('Ctrl Pts',(-2.04384586989768,-1.7320129653377,
13.8309611966328));
#436219=CARTESIAN_POINT('Ctrl Pts',(-2.04574051097205,-1.7323573679165,
13.8281701127185));
#436220=CARTESIAN_POINT('Ctrl Pts',(-2.04753875983612,-1.73286437107488,
13.8253580685121));
#436221=CARTESIAN_POINT('Ctrl Pts',(-2.04792862213057,-1.73297428990679,
13.8247484142932));
#436222=CARTESIAN_POINT('Ctrl Pts',(-2.04831382179132,-1.73309196358275,
13.8241378483365));
#436223=CARTESIAN_POINT('Ctrl Pts',(-2.04869397153156,-1.7332176067911,
13.8235269408515));
#436224=CARTESIAN_POINT('',(-2.01184825284715,-1.74343840428094,12.5969504640361));
#436225=CARTESIAN_POINT('Origin',(-2.03793175060768,-1.76587765499918,12.584524458991));
#436226=CARTESIAN_POINT('Origin',(-2.03793175060768,-1.76587765499918,12.584524458991));
#436227=CARTESIAN_POINT('Ctrl Pts',(-2.00713550187734,-1.78117863747128,
12.5893111709658));
#436228=CARTESIAN_POINT('Ctrl Pts',(-2.00208344074157,-1.77103293331434,
12.5770542771492));
#436229=CARTESIAN_POINT('Ctrl Pts',(-2.01511564898405,-1.76113519502827,
12.5737548217797));
#436230=CARTESIAN_POINT('Ctrl Pts',(-2.01818266405917,-1.803363887463,12.5663937883685));
#436231=CARTESIAN_POINT('Ctrl Pts',(-2.01312415831784,-1.79320524105137,
12.5540940315304));
#436232=CARTESIAN_POINT('Ctrl Pts',(-2.02619869292755,-1.78327938894427,
12.5508374392248));
#436233=CARTESIAN_POINT('Ctrl Pts',(-2.02921867978978,-1.82552675280944,
12.5434499600945));
#436234=CARTESIAN_POINT('Ctrl Pts',(-2.02414372704488,-1.81533507702074,
12.5311293540533));
#436235=CARTESIAN_POINT('Ctrl Pts',(-2.03726985340451,-1.80540247558145,
12.5278936106989));
#436236=CARTESIAN_POINT('Ctrl Pts',(-2.04024442218595,-1.84766898693051,
12.5204817579905));
#436237=CARTESIAN_POINT('Ctrl Pts',(-2.03514435189319,-1.83742686931171,
12.5081597038247));
#436238=CARTESIAN_POINT('Ctrl Pts',(-2.04833004165538,-1.82750610168062,
12.5049254088044));
#436239=CARTESIAN_POINT('Ctrl Pts',(-2.03231742028997,-1.83174973854323,
12.5369868989719));
#436240=CARTESIAN_POINT('Ctrl Pts',(-2.03273263448266,-1.83258358405944,
12.5342545179733));
#436241=CARTESIAN_POINT('Ctrl Pts',(-2.03324056361785,-1.83332376316411,
12.5314872231885));
#436242=CARTESIAN_POINT('Ctrl Pts',(-2.03385868736767,-1.83389695086464,
12.5287124745063));
#436243=CARTESIAN_POINT('Ctrl Pts',(-2.03441614204618,-1.83441387998348,
12.5262100684184));
#436244=CARTESIAN_POINT('Ctrl Pts',(-2.0350633279729,-1.83479374668903,
12.5237004536639));
#436245=CARTESIAN_POINT('Ctrl Pts',(-2.03584491380172,-1.83498590330125,
12.5212220730815));
#436246=CARTESIAN_POINT('Ctrl Pts',(-2.03644328536625,-1.83513301581077,
12.5193246583486));
#436247=CARTESIAN_POINT('Ctrl Pts',(-2.03712773465973,-1.83517124914371,
12.517417831369));
#436248=CARTESIAN_POINT('Ctrl Pts',(-2.03792273333658,-1.83500650143566,
12.5155812248347));
#436249=CARTESIAN_POINT('Ctrl Pts',(-2.03826140704605,-1.8349363180265,
12.5147988205793));
#436250=CARTESIAN_POINT('Ctrl Pts',(-2.03862054333634,-1.83482949751477,
12.5140295443047));
#436251=CARTESIAN_POINT('Ctrl Pts',(-2.03900356490061,-1.83468024191474,
12.5132817086137));
#436252=CARTESIAN_POINT('Ctrl Pts',(-2.03958321622414,-1.83445436375493,
12.5121499604604));
#436253=CARTESIAN_POINT('Ctrl Pts',(-2.04022749179658,-1.83411975636767,
12.5110494206568));
#436254=CARTESIAN_POINT('Ctrl Pts',(-2.04093077446586,-1.83363960472413,
12.5100666561695));
#436255=CARTESIAN_POINT('Ctrl Pts',(-2.04133459775504,-1.8333639027561,
12.5095023550641));
#436256=CARTESIAN_POINT('Ctrl Pts',(-2.04176217361714,-1.83303648984005,
12.5089719619137));
#436257=CARTESIAN_POINT('Ctrl Pts',(-2.04220160452889,-1.83265843195989,
12.5085043804652));
#436258=CARTESIAN_POINT('Ctrl Pts',(-2.04284465442835,-1.83210519349779,
12.5078201359221));
#436259=CARTESIAN_POINT('Ctrl Pts',(-2.04353095422585,-1.83142653997754,
12.5072563000949));
#436260=CARTESIAN_POINT('Ctrl Pts',(-2.04420803018151,-1.83066245429082,
12.5068768744332));
#436261=CARTESIAN_POINT('Ctrl Pts',(-2.04469624855562,-1.83011149591086,
12.5066032824114));
#436262=CARTESIAN_POINT('Ctrl Pts',(-2.04518829329354,-1.82950647822802,
12.5064197834844));
#436263=CARTESIAN_POINT('Ctrl Pts',(-2.04565869272502,-1.82888281792614,
12.5063282718343));
#436264=CARTESIAN_POINT('Ctrl Pts',(-2.046345330263,-1.82797246696574,12.5061946931565));
#436265=CARTESIAN_POINT('Ctrl Pts',(-2.04700137231097,-1.82700357620241,
12.5062515701262));
#436266=CARTESIAN_POINT('Ctrl Pts',(-2.0475989089795,-1.82604494720823,
12.5064436508398));
#436267=CARTESIAN_POINT('',(-2.01511564898405,-1.76113519502827,12.5737548217797));
#436268=CARTESIAN_POINT('Origin',(-2.02682901625738,-1.77137223694085,12.5893111709658));
#436269=CARTESIAN_POINT('Ctrl Pts',(-2.0475989089795,-1.82604494720823,
12.5064436508398));
#436270=CARTESIAN_POINT('Ctrl Pts',(-2.04279097221024,-1.81643640248107,
12.5164271754438));
#436271=CARTESIAN_POINT('Ctrl Pts',(-2.03798094272672,-1.80682414242484,
12.5264061185523));
#436272=CARTESIAN_POINT('Ctrl Pts',(-2.03316874767174,-1.79720803576523,
12.536380305637));
#436273=CARTESIAN_POINT('Ctrl Pts',(-2.02715447987134,-1.7851898527973,
12.5488460165097));
#436274=CARTESIAN_POINT('Ctrl Pts',(-2.02113682766512,-1.77316565792249,
12.5613043021964));
#436275=CARTESIAN_POINT('Ctrl Pts',(-2.01511564898405,-1.76113519502827,
12.5737548217797));
#436276=CARTESIAN_POINT('Ctrl Pts',(-2.04869397153156,-1.7332176067911,
12.5893111709658));
#436277=CARTESIAN_POINT('Ctrl Pts',(-2.03793255275056,-1.72966085259949,
12.5770542771492));
#436278=CARTESIAN_POINT('Ctrl Pts',(-2.02999023577725,-1.7439690067764,
12.5737548217797));
#436279=CARTESIAN_POINT('Ctrl Pts',(-2.03865366140676,-1.72989918606534,
12.5928319619712));
#436280=CARTESIAN_POINT('Ctrl Pts',(-2.03039899825379,-1.73060200368204,
12.5821634970843));
#436281=CARTESIAN_POINT('Ctrl Pts',(-2.02633575586776,-1.74275122438183,
12.5773203894503));
#436282=CARTESIAN_POINT('Ctrl Pts',(-2.02200618152989,-1.73175539539853,
12.5969440695591));
#436283=CARTESIAN_POINT('Ctrl Pts',(-2.01936000917948,-1.73478133565634,
12.5878292599214));
#436284=CARTESIAN_POINT('Ctrl Pts',(-2.02040248106055,-1.74341484864271,
12.5813877129824));
#436285=CARTESIAN_POINT('Ctrl Pts',(-2.00192869816824,-1.75484370212301,
12.596957478804));
#436286=CARTESIAN_POINT('Ctrl Pts',(-2.0045553749358,-1.75184017714266,
12.5878468778671));
#436287=CARTESIAN_POINT('Ctrl Pts',(-2.01322097269373,-1.75168238793089,
12.5814011370086));
#436288=CARTESIAN_POINT('Ctrl Pts',(-2.002415128742,-1.77169903933225,12.5928371701607));
#436289=CARTESIAN_POINT('Ctrl Pts',(-2.00194242356592,-1.76343395521167,
12.5821692192952));
#436290=CARTESIAN_POINT('Ctrl Pts',(-2.01338442992461,-1.75768032049477,
12.5773318885715));
#436291=CARTESIAN_POINT('Ctrl Pts',(-2.00713550187729,-1.7811786374713,
12.5893111709658));
#436292=CARTESIAN_POINT('Ctrl Pts',(-2.00208344074152,-1.77103293331436,
12.5770542771492));
#436293=CARTESIAN_POINT('Ctrl Pts',(-2.015115648984,-1.76113519502829,12.5737548217797));
#436294=CARTESIAN_POINT('',(-2.02999023577725,-1.7439690067764,12.5737548217797));
#436295=CARTESIAN_POINT('Origin',(-2.0417900653329,-1.75410626589599,12.5893111709658));
#436296=CARTESIAN_POINT('Ctrl Pts',(-2.015115648984,-1.76113519502829,12.5737548217797));
#436297=CARTESIAN_POINT('Ctrl Pts',(-2.01463992030744,-1.76025315089259,
12.5746934679442));
#436298=CARTESIAN_POINT('Ctrl Pts',(-2.01427472362832,-1.75919015191621,
12.5756680099006));
#436299=CARTESIAN_POINT('Ctrl Pts',(-2.01405845862531,-1.75806821915688,
12.5765688348656));
#436300=CARTESIAN_POINT('Ctrl Pts',(-2.01400120485989,-1.75777119987905,
12.5768073183026));
#436301=CARTESIAN_POINT('Ctrl Pts',(-2.01395415622715,-1.75747015875835,
12.5770407398754));
#436302=CARTESIAN_POINT('Ctrl Pts',(-2.013917471392,-1.75716746193681,12.5772674179684));
#436303=CARTESIAN_POINT('Ctrl Pts',(-2.01376692674856,-1.75592527603386,
12.5781976435658));
#436304=CARTESIAN_POINT('Ctrl Pts',(-2.01379356207557,-1.75458329688271,
12.5790594849312));
#436305=CARTESIAN_POINT('Ctrl Pts',(-2.01404385859131,-1.75323309527633,
12.5797571720116));
#436306=CARTESIAN_POINT('Ctrl Pts',(-2.01420693577118,-1.75235339038084,
12.580211740231));
#436307=CARTESIAN_POINT('Ctrl Pts',(-2.01449082634906,-1.75143363871864,
12.5806009430798));
#436308=CARTESIAN_POINT('Ctrl Pts',(-2.01489247429766,-1.75054381199972,
12.5808812374708));
#436309=CARTESIAN_POINT('Ctrl Pts',(-2.01523762313082,-1.74977915565123,
12.5811221033394));
#436310=CARTESIAN_POINT('Ctrl Pts',(-2.01567690016029,-1.74902098980917,
12.581287365893));
#436311=CARTESIAN_POINT('Ctrl Pts',(-2.01619272639188,-1.74831628662182,
12.581359338449));
#436312=CARTESIAN_POINT('Ctrl Pts',(-2.01626441558667,-1.74821834743035,
12.5813693411482));
#436313=CARTESIAN_POINT('Ctrl Pts',(-2.01633754958212,-1.74812139143585,
12.5813775999465));
#436314=CARTESIAN_POINT('Ctrl Pts',(-2.01641204749879,-1.74802549346873,
12.5813841266931));
#436315=CARTESIAN_POINT('Ctrl Pts',(-2.01653844222476,-1.7478627909689,
12.5813952001081));
#436316=CARTESIAN_POINT('Ctrl Pts',(-2.01667009039135,-1.74770241785286,
12.5814007534795));
#436317=CARTESIAN_POINT('Ctrl Pts',(-2.01680708709116,-1.74754456909587,
12.5814005856065));
#436318=CARTESIAN_POINT('Ctrl Pts',(-2.0174342044207,-1.7468219992012,12.5813998171494));
#436319=CARTESIAN_POINT('Ctrl Pts',(-2.01812981373364,-1.74620202881124,
12.58127954464));
#436320=CARTESIAN_POINT('Ctrl Pts',(-2.01887027844383,-1.74566608840401,
12.5810700125799));
#436321=CARTESIAN_POINT('Ctrl Pts',(-2.01976467550507,-1.74501873341378,
12.5808169217085));
#436322=CARTESIAN_POINT('Ctrl Pts',(-2.02073440968425,-1.74450747615839,
12.5804173076348));
#436323=CARTESIAN_POINT('Ctrl Pts',(-2.02168234978333,-1.74415408553003,
12.5799304713245));
#436324=CARTESIAN_POINT('Ctrl Pts',(-2.02285714619801,-1.74371612321196,
12.5793271277669));
#436325=CARTESIAN_POINT('Ctrl Pts',(-2.02406009577564,-1.74346328903295,
12.5785808224116));
#436326=CARTESIAN_POINT('Ctrl Pts',(-2.02523396820987,-1.74337520174007,
12.5777485681082));
#436327=CARTESIAN_POINT('Ctrl Pts',(-2.02698316674419,-1.74324394202301,
12.576508418016));
#436328=CARTESIAN_POINT('Ctrl Pts',(-2.02865255875168,-1.74347274288858,
12.5750928681475));
#436329=CARTESIAN_POINT('Ctrl Pts',(-2.02999023577725,-1.7439690067764,
12.5737548217797));
#436330=CARTESIAN_POINT('Ctrl Pts',(-2.02999023577725,-1.7439690067764,
12.5737548217797));
#436331=CARTESIAN_POINT('Ctrl Pts',(-2.03793255275056,-1.72966085259949,
12.5770542771492));
#436332=CARTESIAN_POINT('Ctrl Pts',(-2.04869397153156,-1.7332176067911,
12.5893111709658));
#436333=CARTESIAN_POINT('Ctrl Pts',(-2.05348278542143,-1.7517866192883,
12.5508408821982));
#436334=CARTESIAN_POINT('Ctrl Pts',(-2.06144689991941,-1.73743257439174,
12.55409748406));
#436335=CARTESIAN_POINT('Ctrl Pts',(-2.07222204751465,-1.74099386609078,
12.5663972313419));
#436336=CARTESIAN_POINT('Ctrl Pts',(-2.07695275823144,-1.75959547580437,
12.52790050457));
#436337=CARTESIAN_POINT('Ctrl Pts',(-2.08491621151662,-1.74518941148699,
12.5311362602938));
#436338=CARTESIAN_POINT('Ctrl Pts',(-2.09572638753523,-1.74876228042263,
12.5434568539655));
#436339=CARTESIAN_POINT('Ctrl Pts',(-2.10040191308955,-1.76739624363818,
12.5049357605811));
#436340=CARTESIAN_POINT('Ctrl Pts',(-2.10834518227021,-1.7529329155387,
12.5081700652078));
#436341=CARTESIAN_POINT('Ctrl Pts',(-2.11920885059873,-1.75652346420613,
12.5204921097672));
#436342=CARTESIAN_POINT('Ctrl Pts',(-2.09886215016469,-1.76688401313815,
12.5064436508395));
#436343=CARTESIAN_POINT('Ctrl Pts',(-2.09979524624555,-1.76609776922277,
12.5062361689309));
#436344=CARTESIAN_POINT('Ctrl Pts',(-2.10073206262496,-1.76524035060173,
12.5061871075061));
#436345=CARTESIAN_POINT('Ctrl Pts',(-2.10159076052644,-1.76436077425194,
12.5063648335164));
#436346=CARTESIAN_POINT('Ctrl Pts',(-2.10198083407998,-1.76396121641935,
12.5064455676329));
#436347=CARTESIAN_POINT('Ctrl Pts',(-2.1023600706676,-1.76355135935368,
12.506574497099));
#436348=CARTESIAN_POINT('Ctrl Pts',(-2.10271143837214,-1.76314806273744,
12.5067492519495));
#436349=CARTESIAN_POINT('Ctrl Pts',(-2.10341752541355,-1.76233762253225,
12.5071004286051));
#436350=CARTESIAN_POINT('Ctrl Pts',(-2.10403642198906,-1.76152334714826,
12.5076537929613));
#436351=CARTESIAN_POINT('Ctrl Pts',(-2.10452920691249,-1.760772075649,12.5083435010505));
#436352=CARTESIAN_POINT('Ctrl Pts',(-2.10456023066832,-1.7607247786185,
12.5083869222964));
#436353=CARTESIAN_POINT('Ctrl Pts',(-2.10459074798995,-1.76067771959725,
12.5084308732337));
#436354=CARTESIAN_POINT('Ctrl Pts',(-2.10462074682411,-1.76063091030325,
12.5084753333615));
#436355=CARTESIAN_POINT('Ctrl Pts',(-2.10486137706898,-1.76025543798268,
12.5088319622689));
#436356=CARTESIAN_POINT('Ctrl Pts',(-2.10507461837437,-1.75988910689663,
12.509227847131));
#436357=CARTESIAN_POINT('Ctrl Pts',(-2.1052565498896,-1.75954421861582,
12.5096423454524));
#436358=CARTESIAN_POINT('Ctrl Pts',(-2.10582664273882,-1.75846349138493,
12.5109411997424));
#436359=CARTESIAN_POINT('Ctrl Pts',(-2.10613291514583,-1.75753135443021,
12.5124831113042));
#436360=CARTESIAN_POINT('Ctrl Pts',(-2.10626956663698,-1.75673873545148,
12.5140723025008));
#436361=CARTESIAN_POINT('Ctrl Pts',(-2.10628237103138,-1.75666446618504,
12.5142212114565));
#436362=CARTESIAN_POINT('Ctrl Pts',(-2.10629371276419,-1.75659140885369,
12.5143705582413));
#436363=CARTESIAN_POINT('Ctrl Pts',(-2.10630368520137,-1.75651954994667,
12.5145201959299));
#436364=CARTESIAN_POINT('Ctrl Pts',(-2.10643179600443,-1.75559641529929,
12.5164425148273));
#436365=CARTESIAN_POINT('Ctrl Pts',(-2.10634895468274,-1.75484090547488,
12.518463520594));
#436366=CARTESIAN_POINT('Ctrl Pts',(-2.10612736020703,-1.75419893454944,
12.5205025929157));
#436367=CARTESIAN_POINT('Ctrl Pts',(-2.10599882662793,-1.75382656596732,
12.5216853356836));
#436368=CARTESIAN_POINT('Ctrl Pts',(-2.10582429938244,-1.75349291196221,
12.5228750347131));
#436369=CARTESIAN_POINT('Ctrl Pts',(-2.10562113908398,-1.75319235624078,
12.5240609649613));
#436370=CARTESIAN_POINT('Ctrl Pts',(-2.10512249303057,-1.75245465834681,
12.5269717671327));
#436371=CARTESIAN_POINT('Ctrl Pts',(-2.10442870606012,-1.75190141461407,
12.5299036066169));
#436372=CARTESIAN_POINT('Ctrl Pts',(-2.10360399699103,-1.7514744402852,
12.5328133004019));
#436373=CARTESIAN_POINT('Ctrl Pts',(-2.1032080886165,-1.75126946774538,
12.5342101228452));
#436374=CARTESIAN_POINT('Ctrl Pts',(-2.1027822615005,-1.7510943158857,12.5356023438238));
#436375=CARTESIAN_POINT('Ctrl Pts',(-2.10233409235841,-1.75094619151327,
12.5369868989719));
#436376=CARTESIAN_POINT('Origin',(-14.20522036749,-5.7454903392375,-1.23974147293322));
#436377=CARTESIAN_POINT('Ctrl Pts',(-2.03229875515483,-1.83171234370852,
12.5369868989719));
#436378=CARTESIAN_POINT('Ctrl Pts',(-2.03916209416162,-1.84543013804155,
12.5369868989719));
#436379=CARTESIAN_POINT('Ctrl Pts',(-2.02866372722115,-1.85661350047279,
12.5369868989719));
#436380=CARTESIAN_POINT('Ctrl Pts',(-2.03461877294864,-1.83634952431904,
12.5218025310016));
#436381=CARTESIAN_POINT('Ctrl Pts',(-2.03672795412435,-1.84797738820165,
12.5216901060418));
#436382=CARTESIAN_POINT('Ctrl Pts',(-2.02869574174667,-1.85657942116523,
12.5161920673677));
#436383=CARTESIAN_POINT('Ctrl Pts',(-2.0405707567139,-1.83730344279213,
12.5042015548895));
#436384=CARTESIAN_POINT('Ctrl Pts',(-2.04052280449143,-1.84373578650199,
12.4980677368513));
#436385=CARTESIAN_POINT('Ctrl Pts',(-2.03596183033724,-1.84877446633788,
12.4907278922778));
#436386=CARTESIAN_POINT('Ctrl Pts',(-2.04758398157485,-1.82603163496219,
12.506463626192));
#436387=CARTESIAN_POINT('Ctrl Pts',(-2.05246702543131,-1.83038632450706,
12.4999376786891));
#436388=CARTESIAN_POINT('Ctrl Pts',(-2.05240738615054,-1.83033313830599,
12.4906970594712));
#436389=CARTESIAN_POINT('Origin',(-2.01262390590993,-1.84155613907365,12.5369868989719));
#436390=CARTESIAN_POINT('Origin',(-2.01262390590993,-1.84155613907365,14.));
#436391=CARTESIAN_POINT('Origin',(-2.01262390590993,-1.84155613907365,13.7435492065112));
#436392=CARTESIAN_POINT('Ctrl Pts',(-2.02128069158676,-1.8095855022959,
13.793642941384));
#436393=CARTESIAN_POINT('Ctrl Pts',(-2.02612458608051,-1.819252089343,13.8071662555867));
#436394=CARTESIAN_POINT('Ctrl Pts',(-2.01218638534816,-1.82903707498322,
13.8103758687955));
#436395=CARTESIAN_POINT('Ctrl Pts',(-2.02868948434669,-1.82446406052789,
13.7804579775006));
#436396=CARTESIAN_POINT('Ctrl Pts',(-2.03465734610451,-1.83639629827982,
13.7901904343351));
#436397=CARTESIAN_POINT('Ctrl Pts',(-2.02339634547535,-1.84741654278687,
13.7927914348262));
#436398=CARTESIAN_POINT('Ctrl Pts',(-2.03305131943469,-1.8332236277192,
13.7597120340895));
#436399=CARTESIAN_POINT('Ctrl Pts',(-2.03995269102682,-1.84703515044914,
13.7635825532445));
#436400=CARTESIAN_POINT('Ctrl Pts',(-2.02998502261937,-1.85826820447123,
13.7651073818884));
#436401=CARTESIAN_POINT('Ctrl Pts',(-2.03219717224905,-1.8315083038922,
13.7381884353898));
#436402=CARTESIAN_POINT('Ctrl Pts',(-2.03893780842326,-1.84499614043455,
13.7368803041982));
#436403=CARTESIAN_POINT('Ctrl Pts',(-2.02869434139341,-1.85614338315763,
13.7363986145813));
#436404=CARTESIAN_POINT('Origin',(-2.00338493120097,-1.82300214663542,13.7902182540695));
#436405=CARTESIAN_POINT('Ctrl Pts',(-2.00713374665534,-1.7811751142832,
13.8235227101244));
#436406=CARTESIAN_POINT('Ctrl Pts',(-2.01226248321911,-1.79146485429833,
13.8358800583119));
#436407=CARTESIAN_POINT('Ctrl Pts',(-1.99899831538416,-1.80139903270938,
13.8390832900376));
#436408=CARTESIAN_POINT('Ctrl Pts',(-2.01245041122361,-1.79185220317311,
13.8124254819052));
#436409=CARTESIAN_POINT('Ctrl Pts',(-2.01758910747214,-1.80216192584157,
13.8247886449157));
#436410=CARTESIAN_POINT('Ctrl Pts',(-2.0042979624152,-1.81209501419199,
13.8279860620657));
#436411=CARTESIAN_POINT('Ctrl Pts',(-2.0177646930358,-1.80252450693912,
13.8013225099955));
#436412=CARTESIAN_POINT('Ctrl Pts',(-2.02291092612378,-1.81284934683313,
13.8136962257787));
#436413=CARTESIAN_POINT('Ctrl Pts',(-2.00959539884781,-1.82278592362019,
13.8168830918626));
#436414=CARTESIAN_POINT('Ctrl Pts',(-2.0230766848013,-1.81319221176308,
13.7902140179785));
#436415=CARTESIAN_POINT('Ctrl Pts',(-2.02822819023148,-1.82352762144762,
13.802602731458));
#436416=CARTESIAN_POINT('Ctrl Pts',(-2.01489071319075,-1.8334719594703,
13.8057746032558));
#436417=CARTESIAN_POINT('Origin',(-1.9874419874973,-1.7909850380017,13.8235269408515));
#436418=CARTESIAN_POINT('Ctrl Pts',(-2.04869397153156,-1.7332176067911,
13.8235269408515));
#436419=CARTESIAN_POINT('Ctrl Pts',(-2.05990499223275,-1.73692295881603,
13.8362179249168));
#436420=CARTESIAN_POINT('Ctrl Pts',(-2.06781651354226,-1.72178787260463,
13.8391868794938));
#436421=CARTESIAN_POINT('Ctrl Pts',(-2.03843637557668,-1.72982737097268,
13.8400110824519));
#436422=CARTESIAN_POINT('Ctrl Pts',(-2.04849842866773,-1.72954997152324,
13.8494522556837));
#436423=CARTESIAN_POINT('Ctrl Pts',(-2.05090014724273,-1.71631518269521,
13.85569149686));
#436424=CARTESIAN_POINT('Ctrl Pts',(-2.02223093111772,-1.73149509275204,
13.8586819406588));
#436425=CARTESIAN_POINT('Ctrl Pts',(-2.02509259560658,-1.7282137942304,
13.868010383617));
#436426=CARTESIAN_POINT('Ctrl Pts',(-2.02401373350842,-1.71922886666443,
13.8744918421245));
#436427=CARTESIAN_POINT('Ctrl Pts',(-2.00170044877093,-1.7551080297264,
13.8587686893867));
#436428=CARTESIAN_POINT('Ctrl Pts',(-1.99886421063234,-1.7583600877119,
13.8680909899357));
#436429=CARTESIAN_POINT('Ctrl Pts',(-1.98983845114073,-1.75853916061699,
13.8745789365163));
#436430=CARTESIAN_POINT('Ctrl Pts',(-2.00231212963259,-1.77149219337558,
13.8400379222776));
#436431=CARTESIAN_POINT('Ctrl Pts',(-2.00346212723657,-1.78148958000506,
13.8494748685453));
#436432=CARTESIAN_POINT('Ctrl Pts',(-1.99071008809211,-1.7857494629755,
13.8557104837033));
#436433=CARTESIAN_POINT('Ctrl Pts',(-2.00713550187136,-1.78117863747409,
13.8235269408542));
#436434=CARTESIAN_POINT('Ctrl Pts',(-2.01239863335326,-1.79174821957533,
13.8362179249195));
#436435=CARTESIAN_POINT('Ctrl Pts',(-1.99854352737215,-1.80173316035175,
13.8391868794965));
#436436=CARTESIAN_POINT('Origin',(-2.05559787773022,-1.71232894768622,13.8235269408515));
#436437=CARTESIAN_POINT('Ctrl Pts',(-2.08265036614452,-1.74444052662317,
13.7902140241682));
#436438=CARTESIAN_POINT('Ctrl Pts',(-2.09361370960642,-1.74806870736962,
13.8026027327198));
#436439=CARTESIAN_POINT('Ctrl Pts',(-2.10155870455742,-1.73345176557244,
13.8057746032556));
#436440=CARTESIAN_POINT('Ctrl Pts',(-2.07133526792135,-1.74070077596011,
13.8013225161808));
#436441=CARTESIAN_POINT('Ctrl Pts',(-2.08228739884563,-1.7443252422798,
13.8136962270464));
#436442=CARTESIAN_POINT('Ctrl Pts',(-2.09022783533951,-1.72973113135793,
13.8168830918628));
#436443=CARTESIAN_POINT('Ctrl Pts',(-2.06001529165748,-1.73695941305689,
13.8124254880875));
#436444=CARTESIAN_POINT('Ctrl Pts',(-2.07095138662803,-1.74057857067098,
13.8247886461868));
#436445=CARTESIAN_POINT('Ctrl Pts',(-2.07889184014546,-1.72600909023632,
13.8279860620656));
#436446=CARTESIAN_POINT('Ctrl Pts',(-2.04869023987082,-1.73321637264375,
13.8235227163065));
#436447=CARTESIAN_POINT('Ctrl Pts',(-2.05960513818058,-1.73682851579214,
13.8358800595847));
#436448=CARTESIAN_POINT('Ctrl Pts',(-2.06755050992176,-1.72228558284544,
13.8390832900376));
#436449=CARTESIAN_POINT('Origin',(-2.08955801581769,-1.72355310557363,13.7902182540695));
#436450=CARTESIAN_POINT('Ctrl Pts',(-2.1020778732194,-1.75086147952906,
13.7382347919292));
#436451=CARTESIAN_POINT('Ctrl Pts',(-2.11639835196728,-1.75561981507471,
13.7369371795943));
#436452=CARTESIAN_POINT('Ctrl Pts',(-2.12597531008095,-1.74387989811122,
13.7364597369711));
#436453=CARTESIAN_POINT('Ctrl Pts',(-2.10387387868557,-1.75145507733044,
13.7595490285574));
#436454=CARTESIAN_POINT('Ctrl Pts',(-2.11853634881506,-1.75632598855121,
13.7633824266926));
#436455=CARTESIAN_POINT('Ctrl Pts',(-2.12823402390517,-1.74484344710107,
13.7648920890506));
#436456=CARTESIAN_POINT('Ctrl Pts',(-2.09471434919886,-1.7484277610709,
13.7803806590111));
#436457=CARTESIAN_POINT('Ctrl Pts',(-2.10739515913211,-1.75264604809777,
13.7901039518744));
#436458=CARTESIAN_POINT('Ctrl Pts',(-2.11671739735761,-1.73993458414225,
13.7926933640892));
#436459=CARTESIAN_POINT('Ctrl Pts',(-2.07879304231111,-1.74316560955667,
13.7936647693663));
#436460=CARTESIAN_POINT('Ctrl Pts',(-2.08905267138956,-1.74658808572421,
13.8072068914933));
#436461=CARTESIAN_POINT('Ctrl Pts',(-2.09675332388845,-1.73137808174858,
13.8104111085397));
#436462=CARTESIAN_POINT('Origin',(-2.10923799855707,-1.73005753240838,13.7435492065112));
#436463=CARTESIAN_POINT('Origin',(-2.10923799855707,-1.73005753240838,14.));
#436464=CARTESIAN_POINT('Origin',(-2.10923799855707,-1.73005753240838,12.5369868989719));
#436465=CARTESIAN_POINT('Ctrl Pts',(-2.09884808670359,-1.76687217411561,
12.506462012331));
#436466=CARTESIAN_POINT('Ctrl Pts',(-2.10385023214597,-1.77108312756622,
12.4999388158272));
#436467=CARTESIAN_POINT('Ctrl Pts',(-2.10379105020547,-1.77103330646457,
12.4907030323752));
#436468=CARTESIAN_POINT('Ctrl Pts',(-2.10900548446784,-1.7583249023981,
12.5042014951932));
#436469=CARTESIAN_POINT('Ctrl Pts',(-2.11536288838638,-1.75736338665051,
12.4980716682127));
#436470=CARTESIAN_POINT('Ctrl Pts',(-2.11969933163196,-1.7521364539741,
12.4907355092744));
#436471=CARTESIAN_POINT('Ctrl Pts',(-2.10721671805287,-1.75256938192137,
12.5218047446509));
#436472=CARTESIAN_POINT('Ctrl Pts',(-2.11902064230432,-1.75300094095711,
12.5216906929434));
#436473=CARTESIAN_POINT('Ctrl Pts',(-2.12639117764129,-1.74383328241327,
12.5161988840775));
#436474=CARTESIAN_POINT('Ctrl Pts',(-2.10229762738049,-1.75093410415595,
12.5369868989719));
#436475=CARTESIAN_POINT('Ctrl Pts',(-2.11684469789254,-1.75577024632078,
12.5369868989719));
#436476=CARTESIAN_POINT('Ctrl Pts',(-2.12641929923131,-1.74379808942553,
12.5369868989719));
#436477=CARTESIAN_POINT('Origin',(-3.8935179680156E-31,-8.52561512546645E-31,
12.5));
#436478=CARTESIAN_POINT('Origin',(-1.90060378598595,-1.89443804601162,12.5));
#436479=CARTESIAN_POINT('',(-1.90060378598595,-1.89443804601162,12.5893111709658));
#436480=CARTESIAN_POINT('',(-1.90060378598595,-1.89443804601162,13.8235269408515));
#436481=CARTESIAN_POINT('',(-1.90060378598595,-1.89443804601162,12.5));
#436482=CARTESIAN_POINT('',(-1.93353605144762,-1.90839292296425,13.7902182540695));
#436483=CARTESIAN_POINT('',(-1.90060378598595,-1.89443804601162,13.8235269408515));
#436484=CARTESIAN_POINT('',(-1.95262037949673,-1.9164798081486,13.7435492065112));
#436485=CARTESIAN_POINT('Origin',(-1.88983306537385,-1.88987436272198,13.7445212918695));
#436486=CARTESIAN_POINT('',(-1.95262037949673,-1.9164798081486,12.5369868989719));
#436487=CARTESIAN_POINT('',(-1.95262037949673,-1.9164798081486,12.5));
#436488=CARTESIAN_POINT('Ctrl Pts',(-1.95262037949673,-1.9164798081486,
12.5369868989719));
#436489=CARTESIAN_POINT('Ctrl Pts',(-1.93529416090633,-1.90913791274317,
12.5544431401645));
#436490=CARTESIAN_POINT('Ctrl Pts',(-1.9179555501439,-1.90179076621901,
12.5718848856037));
#436491=CARTESIAN_POINT('Ctrl Pts',(-1.90060378598595,-1.89443804601162,
12.5893111709658));
#436492=CARTESIAN_POINT('Origin',(-1.95738140813714,-2.19419332069378,12.5));
#436493=CARTESIAN_POINT('',(-1.87625044290217,-1.99130747926499,13.7435492065112));
#436494=CARTESIAN_POINT('',(-1.86855453274996,-1.97206216149676,13.7902182540695));
#436495=CARTESIAN_POINT('Origin',(-1.84833101098961,-1.92148879265888,13.7418732680436));
#436496=CARTESIAN_POINT('',(-1.85527432946225,-1.93885208923188,13.8235269408515));
#436497=CARTESIAN_POINT('',(-1.86855453274996,-1.97206216149676,13.7902182540695));
#436498=CARTESIAN_POINT('',(-1.85527432946225,-1.93885208923188,12.5893111709658));
#436499=CARTESIAN_POINT('',(-1.85527432946225,-1.93885208923188,12.5));
#436500=CARTESIAN_POINT('',(-1.87625044290217,-1.99130747926499,12.5369868989719));
#436501=CARTESIAN_POINT('Ctrl Pts',(-1.85527432946225,-1.93885208923188,
12.5893111709658));
#436502=CARTESIAN_POINT('Ctrl Pts',(-1.86227156916585,-1.95635022771492,
12.5718848856037));
#436503=CARTESIAN_POINT('Ctrl Pts',(-1.86926350465598,-1.97383510184432,
12.5544431401645));
#436504=CARTESIAN_POINT('Ctrl Pts',(-1.87625044290217,-1.99130747926499,
12.5369868989719));
#436505=CARTESIAN_POINT('',(-1.87625044290217,-1.99130747926499,12.5));
#436506=CARTESIAN_POINT('Origin',(-1.88719198339499,-1.92608870439752,12.5));
#436507=CARTESIAN_POINT('',(-1.86394732487897,-1.90076527606225,13.8587068136939));
#436508=CARTESIAN_POINT('Ctrl Pts',(-1.85527432945606,-1.9388520892342,
13.8235269408542));
#436509=CARTESIAN_POINT('Ctrl Pts',(-1.8546237037719,-1.93722505646064,
13.8262006681044));
#436510=CARTESIAN_POINT('Ctrl Pts',(-1.85411920277279,-1.9354955169919,
13.8288634856214));
#436511=CARTESIAN_POINT('Ctrl Pts',(-1.85375081465725,-1.93367227820437,
13.8314912288862));
#436512=CARTESIAN_POINT('Ctrl Pts',(-1.8533710445076,-1.93179270707279,
13.8342001611531));
#436513=CARTESIAN_POINT('Ctrl Pts',(-1.85313501922478,-1.92981156781484,
13.8368750301949));
#436514=CARTESIAN_POINT('Ctrl Pts',(-1.85306775932398,-1.92771116184849,
13.8394886372969));
#436515=CARTESIAN_POINT('Ctrl Pts',(-1.85306256467869,-1.92754894240083,
13.8396904925131));
#436516=CARTESIAN_POINT('Ctrl Pts',(-1.85305839837702,-1.92738600703313,
13.8398919674349));
#436517=CARTESIAN_POINT('Ctrl Pts',(-1.85305528331088,-1.9272223462534,
13.8400930404591));
#436518=CARTESIAN_POINT('Ctrl Pts',(-1.85300674848469,-1.92467240119966,
13.8432258934518));
#436519=CARTESIAN_POINT('Ctrl Pts',(-1.8532125311784,-1.92195938989007,
13.8462331177034));
#436520=CARTESIAN_POINT('Ctrl Pts',(-1.85376210985766,-1.91917909219397,
13.8489036603661));
#436521=CARTESIAN_POINT('Ctrl Pts',(-1.85394193839728,-1.91826934643186,
13.8497774930041));
#436522=CARTESIAN_POINT('Ctrl Pts',(-1.85415867005854,-1.91735262817441,
13.85061494757));
#436523=CARTESIAN_POINT('Ctrl Pts',(-1.85441569628117,-1.91643295907823,
13.8514076489583));
#436524=CARTESIAN_POINT('Ctrl Pts',(-1.85495934381076,-1.91448772630367,
13.8530843267192));
#436525=CARTESIAN_POINT('Ctrl Pts',(-1.85573951183846,-1.91233901507234,
13.8546805203176));
#436526=CARTESIAN_POINT('Ctrl Pts',(-1.85683917310503,-1.91015810289246,
13.8559412814273));
#436527=CARTESIAN_POINT('Ctrl Pts',(-1.85698634344535,-1.90986622611413,
13.8561100121513));
#436528=CARTESIAN_POINT('Ctrl Pts',(-1.85713916160777,-1.90957379068151,
13.8562727473908));
#436529=CARTESIAN_POINT('Ctrl Pts',(-1.85729775111527,-1.9092812156692,
13.8564289040185));
#436530=CARTESIAN_POINT('Ctrl Pts',(-1.85801695272257,-1.90795439132617,
13.8571370725437));
#436531=CARTESIAN_POINT('Ctrl Pts',(-1.85886949139538,-1.90660245931935,
13.8577210840553));
#436532=CARTESIAN_POINT('Ctrl Pts',(-1.85984705312809,-1.90529362389541,
13.8581177131616));
#436533=CARTESIAN_POINT('Ctrl Pts',(-1.86012236815867,-1.90492501079129,
13.8582294175695));
#436534=CARTESIAN_POINT('Ctrl Pts',(-1.8604074393947,-1.90455973967519,
13.8583265086086));
#436535=CARTESIAN_POINT('Ctrl Pts',(-1.86070169619407,-1.90419912183687,
13.8584082369006));
#436536=CARTESIAN_POINT('Ctrl Pts',(-1.86112446430668,-1.9036810107067,
13.8585256585398));
#436537=CARTESIAN_POINT('Ctrl Pts',(-1.86157169977273,-1.90316626794696,
13.8586122832068));
#436538=CARTESIAN_POINT('Ctrl Pts',(-1.86203238082353,-1.90266878301648,
13.8586682984299));
#436539=CARTESIAN_POINT('Ctrl Pts',(-1.86240087999833,-1.9022708443862,
13.8587131050557));
#436540=CARTESIAN_POINT('Ctrl Pts',(-1.86278188024532,-1.90187939347669,
13.8587357943552));
#436541=CARTESIAN_POINT('Ctrl Pts',(-1.8631757897609,-1.90149473700695,
13.8587355499465));
#436542=CARTESIAN_POINT('Ctrl Pts',(-1.86343038287205,-1.90124612435993,
13.8587353919793));
#436543=CARTESIAN_POINT('Ctrl Pts',(-1.86368758847582,-1.90100301078014,
13.8587257282814));
#436544=CARTESIAN_POINT('Ctrl Pts',(-1.86394732487897,-1.90076527606225,
13.8587068136939));
#436545=CARTESIAN_POINT('Ctrl Pts',(-1.86394732487897,-1.90076527606225,
13.8587068136939));
#436546=CARTESIAN_POINT('Ctrl Pts',(-1.86480158374928,-1.89998337953533,
13.8586446046466));
#436547=CARTESIAN_POINT('Ctrl Pts',(-1.86568318550313,-1.89925959477865,
13.858482427929));
#436548=CARTESIAN_POINT('Ctrl Pts',(-1.86658953673735,-1.89859028033409,
13.8582284286032));
#436549=CARTESIAN_POINT('Ctrl Pts',(-1.86751934767254,-1.89790364157183,
13.8579678548414));
#436550=CARTESIAN_POINT('Ctrl Pts',(-1.86847838703359,-1.89727388423125,
13.857615680862));
#436551=CARTESIAN_POINT('Ctrl Pts',(-1.86942352681752,-1.89671773650235,
13.8571944833187));
#436552=CARTESIAN_POINT('Ctrl Pts',(-1.87178221980925,-1.89532981296677,
13.8561433417727));
#436553=CARTESIAN_POINT('Ctrl Pts',(-1.87416224611936,-1.89433127665259,
13.8546163505475));
#436554=CARTESIAN_POINT('Ctrl Pts',(-1.87637800444609,-1.89363096822991,
13.8528973491086));
#436555=CARTESIAN_POINT('Ctrl Pts',(-1.87678279080193,-1.89350303221316,
13.8525833129073));
#436556=CARTESIAN_POINT('Ctrl Pts',(-1.87718211936919,-1.89338491003298,
13.8522628768812));
#436557=CARTESIAN_POINT('Ctrl Pts',(-1.87757491665071,-1.89327587678666,
13.851937733538));
#436558=CARTESIAN_POINT('Ctrl Pts',(-1.87997367515072,-1.89261002587908,
13.8499521282529));
#436559=CARTESIAN_POINT('Ctrl Pts',(-1.88236833975653,-1.89222089205316,
13.847639871647));
#436560=CARTESIAN_POINT('Ctrl Pts',(-1.88462016939034,-1.89204962624485,
13.8452109780794));
#436561=CARTESIAN_POINT('Ctrl Pts',(-1.88563331415315,-1.89197257021266,
13.8441181685877));
#436562=CARTESIAN_POINT('Ctrl Pts',(-1.88661774147218,-1.89193892654058,
13.8430021611332));
#436563=CARTESIAN_POINT('Ctrl Pts',(-1.88756266124592,-1.89194058951909,
13.8418824960098));
#436564=CARTESIAN_POINT('Ctrl Pts',(-1.8897893888221,-1.89194450837042,
13.8392439765549));
#436565=CARTESIAN_POINT('Ctrl Pts',(-1.89190317628152,-1.89214089762252,
13.8364981347964));
#436566=CARTESIAN_POINT('Ctrl Pts',(-1.89391277952983,-1.89249620286769,
13.833693111342));
#436567=CARTESIAN_POINT('Ctrl Pts',(-1.89587000547208,-1.89284224761252,
13.8309611966328));
#436568=CARTESIAN_POINT('Ctrl Pts',(-1.89773027027713,-1.89333993505671,
13.8281701127186));
#436569=CARTESIAN_POINT('Ctrl Pts',(-1.89948121015224,-1.89399182518045,
13.8253580685121));
#436570=CARTESIAN_POINT('Ctrl Pts',(-1.89986081580685,-1.89413315566282,
13.8247484142933));
#436571=CARTESIAN_POINT('Ctrl Pts',(-1.9002351422505,-1.89428183513771,
13.8241378483365));
#436572=CARTESIAN_POINT('Ctrl Pts',(-1.90060378598595,-1.89443804601162,
13.8235269408515));
#436573=CARTESIAN_POINT('',(-1.86304757851021,-1.90162156650924,12.5969504640361));
#436574=CARTESIAN_POINT('Origin',(-1.88721527833432,-1.92611219968666,12.584524458991));
#436575=CARTESIAN_POINT('Origin',(-1.88721527833432,-1.92611219968666,12.584524458991));
#436576=CARTESIAN_POINT('Ctrl Pts',(-1.85527432946225,-1.93885208923188,
12.5893111709658));
#436577=CARTESIAN_POINT('Ctrl Pts',(-1.85106604772005,-1.92832835418495,
12.5770542771492));
#436578=CARTESIAN_POINT('Ctrl Pts',(-1.86486164992112,-1.9195257957634,
12.5737548217797));
#436579=CARTESIAN_POINT('Ctrl Pts',(-1.8644764292911,-1.96186396590907,
12.5663937883685));
#436580=CARTESIAN_POINT('Ctrl Pts',(-1.86026277930111,-1.95132680637659,
12.5540940315304));
#436581=CARTESIAN_POINT('Ctrl Pts',(-1.87410285856934,-1.94249967767227,
12.5508374392248));
#436582=CARTESIAN_POINT('Ctrl Pts',(-1.87366924431403,-1.98485262388478,
12.5434499600944));
#436583=CARTESIAN_POINT('Ctrl Pts',(-1.86944189424743,-1.97428120429418,
12.5311293540532));
#436584=CARTESIAN_POINT('Ctrl Pts',(-1.88333394373153,-1.9654515539222,
12.5278936106989));
#436585=CARTESIAN_POINT('Ctrl Pts',(-1.88285350182261,-2.00781988191172,
12.5204817579905));
#436586=CARTESIAN_POINT('Ctrl Pts',(-1.87860522926214,-1.99719614101879,
12.5081597038247));
#436587=CARTESIAN_POINT('Ctrl Pts',(-1.89255567939123,-1.98838314004918,
12.5049254088044));
#436588=CARTESIAN_POINT('Ctrl Pts',(-1.87625044290217,-1.99130747926499,
12.5369868989719));
#436589=CARTESIAN_POINT('Ctrl Pts',(-1.87659630935327,-1.99217239404041,
12.5342545179733));
#436590=CARTESIAN_POINT('Ctrl Pts',(-1.87704221692763,-1.99295151120007,
12.5314872231885));
#436591=CARTESIAN_POINT('Ctrl Pts',(-1.87761156380286,-1.9935731744898,
12.5287124745063));
#436592=CARTESIAN_POINT('Ctrl Pts',(-1.87812502907479,-1.99413382130109,
12.5262100684184));
#436593=CARTESIAN_POINT('Ctrl Pts',(-1.87873909888072,-1.99456517569273,
12.5237004536639));
#436594=CARTESIAN_POINT('Ctrl Pts',(-1.87950242149938,-1.9948203994206,
12.5212220730815));
#436595=CARTESIAN_POINT('Ctrl Pts',(-1.88008681099664,-1.99501579526291,
12.5193246583486));
#436596=CARTESIAN_POINT('Ctrl Pts',(-1.88076586646999,-1.99510969034912,
12.517417831369));
#436597=CARTESIAN_POINT('Ctrl Pts',(-1.88157164832197,-1.99501029059805,
12.5155812248347));
#436598=CARTESIAN_POINT('Ctrl Pts',(-1.88191491572201,-1.99496794576981,
12.5147988205793));
#436599=CARTESIAN_POINT('Ctrl Pts',(-1.8822815638793,-1.99489075363624,
12.5140295443047));
#436600=CARTESIAN_POINT('Ctrl Pts',(-1.88267547668793,-1.99477321448519,
12.5132817086137));
#436601=CARTESIAN_POINT('Ctrl Pts',(-1.88327161043647,-1.99459533488041,
12.5121499604604));
#436602=CARTESIAN_POINT('Ctrl Pts',(-1.8839410158435,-1.99431435531195,
12.5110494206568));
#436603=CARTESIAN_POINT('Ctrl Pts',(-1.88468109521418,-1.99389312539989,
12.5100666561695));
#436604=CARTESIAN_POINT('Ctrl Pts',(-1.88510604708456,-1.9936512561544,
12.5095023550641));
#436605=CARTESIAN_POINT('Ctrl Pts',(-1.88555888741544,-1.99335978408002,
12.5089719619137));
#436606=CARTESIAN_POINT('Ctrl Pts',(-1.88602767138404,-1.99301880185507,
12.5085043804652));
#436607=CARTESIAN_POINT('Ctrl Pts',(-1.88671367565868,-1.9925198187849,
12.5078201359221));
#436608=CARTESIAN_POINT('Ctrl Pts',(-1.88745300841245,-1.99189936323301,
12.5072563000949));
#436609=CARTESIAN_POINT('Ctrl Pts',(-1.88819011153062,-1.99119300795444,
12.5068768744332));
#436610=CARTESIAN_POINT('Ctrl Pts',(-1.88872161362118,-1.99068367717293,
12.5066032824114));
#436611=CARTESIAN_POINT('Ctrl Pts',(-1.88926133567869,-1.99012077885057,
12.5064197834844));
#436612=CARTESIAN_POINT('Ctrl Pts',(-1.88978100399925,-1.98953753564754,
12.5063282718343));
#436613=CARTESIAN_POINT('Ctrl Pts',(-1.89053955886202,-1.98868618113864,
12.5061946931565));
#436614=CARTESIAN_POINT('Ctrl Pts',(-1.89127239157615,-1.9877739877967,
12.5062515701262));
#436615=CARTESIAN_POINT('Ctrl Pts',(-1.89194607715322,-1.98686725334717,
12.5064436508398));
#436616=CARTESIAN_POINT('',(-1.86486164992112,-1.9195257957634,12.5737548217797));
#436617=CARTESIAN_POINT('Origin',(-1.8757016279792,-1.93068352293789,12.5893111709658));
#436618=CARTESIAN_POINT('Ctrl Pts',(-1.89194607715322,-1.98686725334717,
12.5064436508398));
#436619=CARTESIAN_POINT('Ctrl Pts',(-1.88793732399357,-1.97689878877853,
12.5164271754438));
#436620=CARTESIAN_POINT('Ctrl Pts',(-1.88392678791681,-1.96692645066764,
12.5264061185523));
#436621=CARTESIAN_POINT('Ctrl Pts',(-1.87991440700823,-1.95695010223845,
12.536380305637));
#436622=CARTESIAN_POINT('Ctrl Pts',(-1.87489974467104,-1.94448169012345,
12.5488460165097));
#436623=CARTESIAN_POINT('Ctrl Pts',(-1.8698821992156,-1.93200701024519,
12.5613043021964));
#436624=CARTESIAN_POINT('Ctrl Pts',(-1.86486164992112,-1.9195257957634,
12.5737548217797));
#436625=CARTESIAN_POINT('Ctrl Pts',(-1.90060378598595,-1.89443804601162,
12.5893111709658));
#436626=CARTESIAN_POINT('Ctrl Pts',(-1.8901680834241,-1.89001597109137,
12.5770542771492));
#436627=CARTESIAN_POINT('Ctrl Pts',(-1.88108594645948,-1.90362914349941,
12.5737548217797));
#436628=CARTESIAN_POINT('Ctrl Pts',(-1.89086736626069,-1.89031228857221,
12.5928319619712));
#436629=CARTESIAN_POINT('Ctrl Pts',(-1.882582883658,-1.89033993594174,12.5821634970842));
#436630=CARTESIAN_POINT('Ctrl Pts',(-1.87754288710091,-1.90211753913613,
12.5773203894503));
#436631=CARTESIAN_POINT('Ctrl Pts',(-1.87412398120692,-1.89080539736434,
12.5969440695591));
#436632=CARTESIAN_POINT('Ctrl Pts',(-1.87123997155424,-1.89360558144314,
12.5878292599214));
#436633=CARTESIAN_POINT('Ctrl Pts',(-1.87157526323811,-1.90229533826341,
12.5813877129824));
#436634=CARTESIAN_POINT('Ctrl Pts',(-1.85223139267545,-1.91218037836861,
12.596957478804));
#436635=CARTESIAN_POINT('Ctrl Pts',(-1.85509414456203,-1.90940094591129,
12.5878468778671));
#436636=CARTESIAN_POINT('Ctrl Pts',(-1.86374376954388,-1.90995000839486,
12.5814011370086));
#436637=CARTESIAN_POINT('Ctrl Pts',(-1.85134233823174,-1.92901927944131,
12.5928371701607));
#436638=CARTESIAN_POINT('Ctrl Pts',(-1.85154488702826,-1.92074316684609,
12.5821692192952));
#436639=CARTESIAN_POINT('Ctrl Pts',(-1.86341779569826,-1.91594130661471,
12.5773318885715));
#436640=CARTESIAN_POINT('Ctrl Pts',(-1.8552743294622,-1.9388520892319,12.5893111709658));
#436641=CARTESIAN_POINT('Ctrl Pts',(-1.85106604772,-1.92832835418497,12.5770542771492));
#436642=CARTESIAN_POINT('Ctrl Pts',(-1.86486164992107,-1.91952579576342,
12.5737548217797));
#436643=CARTESIAN_POINT('',(-1.88108594645948,-1.90362914349941,12.5737548217797));
#436644=CARTESIAN_POINT('Origin',(-1.89202023232773,-1.9146944673786,12.5893111709658));
#436645=CARTESIAN_POINT('Ctrl Pts',(-1.86486164992107,-1.91952579576342,
12.5737548217797));
#436646=CARTESIAN_POINT('Ctrl Pts',(-1.864459398978,-1.91860791025323,12.5746934679442));
#436647=CARTESIAN_POINT('Ctrl Pts',(-1.86418206174568,-1.91751868139859,
12.5756680099006));
#436648=CARTESIAN_POINT('Ctrl Pts',(-1.86405796428202,-1.91638285417251,
12.5765688348656));
#436649=CARTESIAN_POINT('Ctrl Pts',(-1.86402511085232,-1.91608215648843,
12.5768073183026));
#436650=CARTESIAN_POINT('Ctrl Pts',(-1.86400275641609,-1.91577828215687,
12.5770407398754));
#436651=CARTESIAN_POINT('Ctrl Pts',(-1.86399086624776,-1.9154736023794,
12.5772674179684));
#436652=CARTESIAN_POINT('Ctrl Pts',(-1.86394207221219,-1.91422327896154,
12.5781976435658));
#436653=CARTESIAN_POINT('Ctrl Pts',(-1.86407800267149,-1.91288793616173,
12.5790594849312));
#436654=CARTESIAN_POINT('Ctrl Pts',(-1.8644375203118,-1.91156262872948,
12.5797571720116));
#436655=CARTESIAN_POINT('Ctrl Pts',(-1.86467175898157,-1.91069914328356,
12.580211740231));
#436656=CARTESIAN_POINT('Ctrl Pts',(-1.86502967323599,-1.90980559173675,
12.5806009430798));
#436657=CARTESIAN_POINT('Ctrl Pts',(-1.86550251387252,-1.90895146387936,
12.5808812374708));
#436658=CARTESIAN_POINT('Ctrl Pts',(-1.86590884084254,-1.9082174846959,
12.5811221033394));
#436659=CARTESIAN_POINT('Ctrl Pts',(-1.86640845376854,-1.90749764674408,
12.581287365893));
#436660=CARTESIAN_POINT('Ctrl Pts',(-1.86698000348281,-1.90683733302502,
12.581359338449));
#436661=CARTESIAN_POINT('Ctrl Pts',(-1.86705943709104,-1.90674556305303,
12.5813693411482));
#436662=CARTESIAN_POINT('Ctrl Pts',(-1.8671402305528,-1.90665489077119,
12.5813775999465));
#436663=CARTESIAN_POINT('Ctrl Pts',(-1.86722229715839,-1.90656538416846,
12.5813841266931));
#436664=CARTESIAN_POINT('Ctrl Pts',(-1.86736153308052,-1.90641352539133,
12.5813952001081));
#436665=CARTESIAN_POINT('Ctrl Pts',(-1.86750581509648,-1.90626441645135,
12.5814007534795));
#436666=CARTESIAN_POINT('Ctrl Pts',(-1.86765522209018,-1.90611825942592,
12.5814005856065));
#436667=CARTESIAN_POINT('Ctrl Pts',(-1.86833914889296,-1.9054492097072,
12.5813998171494));
#436668=CARTESIAN_POINT('Ctrl Pts',(-1.8690829769656,-1.9048880008343,12.58127954464));
#436669=CARTESIAN_POINT('Ctrl Pts',(-1.86986466195916,-1.90441419847258,
12.5810700125799));
#436670=CARTESIAN_POINT('Ctrl Pts',(-1.87080884842942,-1.90384189916634,
12.5808169217085));
#436671=CARTESIAN_POINT('Ctrl Pts',(-1.87181702811071,-1.90341138541547,
12.5804173076348));
#436672=CARTESIAN_POINT('Ctrl Pts',(-1.87279061863424,-1.90313643658359,
12.5799304713245));
#436673=CARTESIAN_POINT('Ctrl Pts',(-1.87399720400554,-1.90279568836309,
12.5793271277669));
#436674=CARTESIAN_POINT('Ctrl Pts',(-1.87521675920047,-1.90264174702716,
12.5785808224116));
#436675=CARTESIAN_POINT('Ctrl Pts',(-1.87639390560314,-1.90264963433858,
12.5777485681082));
#436676=CARTESIAN_POINT('Ctrl Pts',(-1.87814798270914,-1.9026613872967,
12.576508418016));
#436677=CARTESIAN_POINT('Ctrl Pts',(-1.87979317055781,-1.90302549779276,
12.5750928681475));
#436678=CARTESIAN_POINT('Ctrl Pts',(-1.88108594645948,-1.90362914349941,
12.5737548217797));
#436679=CARTESIAN_POINT('Ctrl Pts',(-1.88108594645948,-1.90362914349941,
12.5737548217797));
#436680=CARTESIAN_POINT('Ctrl Pts',(-1.8901680834241,-1.89001597109137,
12.5770542771492));
#436681=CARTESIAN_POINT('Ctrl Pts',(-1.90060378598595,-1.89443804601162,
12.5893111709658));
#436682=CARTESIAN_POINT('Ctrl Pts',(-1.90386311858782,-1.91333560444078,
12.5508408821982));
#436683=CARTESIAN_POINT('Ctrl Pts',(-1.91297072106733,-1.89967847071131,
12.55409748406));
#436684=CARTESIAN_POINT('Ctrl Pts',(-1.92341973691294,-1.9041061870666,
12.5663972313419));
#436685=CARTESIAN_POINT('Ctrl Pts',(-1.92661850269949,-1.92303149829958,
12.52790050457));
#436686=CARTESIAN_POINT('Ctrl Pts',(-1.93572968623204,-1.90932246434462,
12.5311362602938));
#436687=CARTESIAN_POINT('Ctrl Pts',(-1.94621267029458,-1.91376457455593,
12.5434568539655));
#436688=CARTESIAN_POINT('Ctrl Pts',(-1.94935379743199,-1.93271763353421,
12.5049357605811));
#436689=CARTESIAN_POINT('Ctrl Pts',(-1.95844953155081,-1.91894988114578,
12.5081700652078));
#436690=CARTESIAN_POINT('Ctrl Pts',(-1.96898438886974,-1.92341397238087,
12.5204921097672));
#436691=CARTESIAN_POINT('Ctrl Pts',(-1.94786090948231,-1.93208160246608,
12.5064436508395));
#436692=CARTESIAN_POINT('Ctrl Pts',(-1.94885498694117,-1.9313740307055,
12.5062361689309));
#436693=CARTESIAN_POINT('Ctrl Pts',(-1.94985857371886,-1.93059582430609,
12.5061871075061));
#436694=CARTESIAN_POINT('Ctrl Pts',(-1.95078610801201,-1.92978916652478,
12.5063648335164));
#436695=CARTESIAN_POINT('Ctrl Pts',(-1.95120745130064,-1.92942273280379,
12.5064455676329));
#436696=CARTESIAN_POINT('Ctrl Pts',(-1.95161883316559,-1.92904515080624,
12.506574497099));
#436697=CARTESIAN_POINT('Ctrl Pts',(-1.95200190414132,-1.92867183585609,
12.5067492519495));
#436698=CARTESIAN_POINT('Ctrl Pts',(-1.95277170013684,-1.92792164497268,
12.5071004286051));
#436699=CARTESIAN_POINT('Ctrl Pts',(-1.9534549083882,-1.92716052483932,
12.5076537929613));
#436700=CARTESIAN_POINT('Ctrl Pts',(-1.95400728921211,-1.92645191968004,
12.5083435010505));
#436701=CARTESIAN_POINT('Ctrl Pts',(-1.95404206488602,-1.92640730875062,
12.5083869222964));
#436702=CARTESIAN_POINT('Ctrl Pts',(-1.95407631641088,-1.92636289375941,
12.5084308732337));
#436703=CARTESIAN_POINT('Ctrl Pts',(-1.95411003081841,-1.92631868540296,
12.5084753333615));
#436704=CARTESIAN_POINT('Ctrl Pts',(-1.95438046486583,-1.92596407603442,
12.5088319622689));
#436705=CARTESIAN_POINT('Ctrl Pts',(-1.95462285601273,-1.92561634503086,
12.509227847131));
#436706=CARTESIAN_POINT('Ctrl Pts',(-1.95483229376253,-1.92528743344482,
12.5096423454524));
#436707=CARTESIAN_POINT('Ctrl Pts',(-1.95548857897713,-1.92425677010434,
12.5109411997424));
#436708=CARTESIAN_POINT('Ctrl Pts',(-1.95586981010331,-1.92335269880289,
12.5124831113042));
#436709=CARTESIAN_POINT('Ctrl Pts',(-1.95607061270299,-1.92257385556357,
12.5140723025008));
#436710=CARTESIAN_POINT('Ctrl Pts',(-1.95608942812651,-1.922500877099,12.5142212114565));
#436711=CARTESIAN_POINT('Ctrl Pts',(-1.95610668697138,-1.92242898731641,
12.5143705582413));
#436712=CARTESIAN_POINT('Ctrl Pts',(-1.95612248339413,-1.92235818036019,
12.5145201959299));
#436713=CARTESIAN_POINT('Ctrl Pts',(-1.95632541196278,-1.92144855958696,
12.5164425148273));
#436714=CARTESIAN_POINT('Ctrl Pts',(-1.95630442735326,-1.92068881132239,
12.5184635205941));
#436715=CARTESIAN_POINT('Ctrl Pts',(-1.95613589680507,-1.92003091449528,
12.5205025929157));
#436716=CARTESIAN_POINT('Ctrl Pts',(-1.95603814240719,-1.91964930825897,
12.5216853356836));
#436717=CARTESIAN_POINT('Ctrl Pts',(-1.95589139178563,-1.91930253886929,
12.5228750347131));
#436718=CARTESIAN_POINT('Ctrl Pts',(-1.95571340556782,-1.91898642377186,
12.5240609649613));
#436719=CARTESIAN_POINT('Ctrl Pts',(-1.95527654794483,-1.91821053622422,
12.5269717671327));
#436720=CARTESIAN_POINT('Ctrl Pts',(-1.95463016399357,-1.91760258328547,
12.5299036066169));
#436721=CARTESIAN_POINT('Ctrl Pts',(-1.95384300144752,-1.9171098082331,
12.5328133004019));
#436722=CARTESIAN_POINT('Ctrl Pts',(-1.95346511759031,-1.91687324751453,
12.5342101228451));
#436723=CARTESIAN_POINT('Ctrl Pts',(-1.95305498388151,-1.91666396959508,
12.5356023438238));
#436724=CARTESIAN_POINT('Ctrl Pts',(-1.95262037949673,-1.9164798081486,
12.5369868989719));
#436725=CARTESIAN_POINT('Origin',(-13.6892547326121,-6.88406632582468,-1.23928728697254));
#436726=CARTESIAN_POINT('Ctrl Pts',(-1.87623488789991,-1.99126868747673,
12.5369868989719));
#436727=CARTESIAN_POINT('Ctrl Pts',(-1.8819572621244,-2.00550026282593,
12.5369868989719));
#436728=CARTESIAN_POINT('Ctrl Pts',(-1.87058227977446,-2.01579069917351,
12.5369868989719));
#436729=CARTESIAN_POINT('Ctrl Pts',(-1.87816921275666,-1.99607954123951,
12.5218025310015));
#436730=CARTESIAN_POINT('Ctrl Pts',(-1.87932359695175,-2.00784063221076,
12.5216901060418));
#436731=CARTESIAN_POINT('Ctrl Pts',(-1.87061696555422,-2.01575934274308,
12.5161920673677));
#436732=CARTESIAN_POINT('Ctrl Pts',(-1.88402363857561,-1.99751542755993,
12.5042015548895));
#436733=CARTESIAN_POINT('Ctrl Pts',(-1.88345155018289,-2.00392245962545,
12.4980677368512));
#436734=CARTESIAN_POINT('Ctrl Pts',(-1.87849505311052,-2.00857261193425,
12.4907278922778));
#436735=CARTESIAN_POINT('Ctrl Pts',(-1.89193228448991,-1.98685276867447,
12.506463626192));
#436736=CARTESIAN_POINT('Ctrl Pts',(-1.89644413279589,-1.99159098175539,
12.4999376786891));
#436737=CARTESIAN_POINT('Ctrl Pts',(-1.89638902712905,-1.99153311137196,
12.4906970594712));
#436738=CARTESIAN_POINT('Origin',(-1.85582314438521,-1.99947604555898,12.5369868989719));
#436739=CARTESIAN_POINT('Origin',(-1.85582314438521,-1.99947604555898,14.));
#436740=CARTESIAN_POINT('Origin',(-1.85582314438521,-1.99947604555898,13.7435492065112));
#436741=CARTESIAN_POINT('Ctrl Pts',(-1.86705702902013,-1.96831739683604,
13.793642941384));
#436742=CARTESIAN_POINT('Ctrl Pts',(-1.87109688927,-1.97834664148194,13.8071662555867));
#436743=CARTESIAN_POINT('Ctrl Pts',(-1.85640749958171,-1.98696297563403,
13.8103758687955));
#436744=CARTESIAN_POINT('Ctrl Pts',(-1.87322842901165,-1.98375033328277,
13.7804579775005));
#436745=CARTESIAN_POINT('Ctrl Pts',(-1.87820384505148,-1.99612930363412,
13.7901904343351));
#436746=CARTESIAN_POINT('Ctrl Pts',(-1.86608206223867,-2.00619500309334,
13.7927914348262));
#436747=CARTESIAN_POINT('Ctrl Pts',(-1.87686176440724,-1.99283628378975,
13.7597120340895));
#436748=CARTESIAN_POINT('Ctrl Pts',(-1.88261440493231,-2.00716437567116,
13.7635825532445));
#436749=CARTESIAN_POINT('Ctrl Pts',(-1.87176430493386,-2.01754759512214,
13.7651073818885));
#436750=CARTESIAN_POINT('Ctrl Pts',(-1.87615027414212,-1.9910570466362,
13.7381884353898));
#436751=CARTESIAN_POINT('Ctrl Pts',(-1.88176909751235,-2.00504942794033,
13.7368803041982));
#436752=CARTESIAN_POINT('Ctrl Pts',(-1.87065111100612,-2.01532464147419,
13.7363986145813));
#436753=CARTESIAN_POINT('Origin',(-1.84812723423301,-1.98023072779075,13.7902182540695));
#436754=CARTESIAN_POINT('Ctrl Pts',(-1.85527286725314,-1.93884843470003,
13.8235227101244));
#436755=CARTESIAN_POINT('Ctrl Pts',(-1.85954582903258,-1.94952197609691,
13.8358800583119));
#436756=CARTESIAN_POINT('Ctrl Pts',(-1.84551606885696,-1.95834194653175,
13.8390832900376));
#436757=CARTESIAN_POINT('Ctrl Pts',(-1.85970155919287,-1.94992335397727,
13.8124254819052));
#436758=CARTESIAN_POINT('Ctrl Pts',(-1.86398281874529,-1.96061762334364,
13.8247886449157));
#436759=CARTESIAN_POINT('Ctrl Pts',(-1.84992625996221,-1.96943430845088,
13.8279860620657));
#436760=CARTESIAN_POINT('Ctrl Pts',(-1.86412826633697,-1.96099330983601,
13.8013225099955));
#436761=CARTESIAN_POINT('Ctrl Pts',(-1.86841580545634,-1.97170326044898,
13.8136962257787));
#436762=CARTESIAN_POINT('Ctrl Pts',(-1.85433466124413,-1.98052143500817,
13.8168830918626));
#436763=CARTESIAN_POINT('Ctrl Pts',(-1.86855306591077,-1.97205849539518,
13.7902140179785));
#436764=CARTESIAN_POINT('Ctrl Pts',(-1.87284499829307,-1.98277941037341,
13.802602731458));
#436765=CARTESIAN_POINT('Ctrl Pts',(-1.85874134473934,-1.99160353123376,
13.8057746032558));
#436766=CARTESIAN_POINT('Origin',(-1.8348470309453,-1.94702065552588,13.8235269408515));
#436767=CARTESIAN_POINT('Ctrl Pts',(-1.90060378598595,-1.89443804601162,
13.8235269408515));
#436768=CARTESIAN_POINT('Ctrl Pts',(-1.91147548235175,-1.89904487104853,
13.8362179249168));
#436769=CARTESIAN_POINT('Ctrl Pts',(-1.92059432876028,-1.88460500802166,
13.8391868794938));
#436770=CARTESIAN_POINT('Ctrl Pts',(-1.89065665702799,-1.89022300162599,
13.8400110824519));
#436771=CARTESIAN_POINT('Ctrl Pts',(-1.90070784009783,-1.89076667593883,
13.8494522556837));
#436772=CARTESIAN_POINT('Ctrl Pts',(-1.9041803253077,-1.87777168713915,
13.85569149686));
#436773=CARTESIAN_POINT('Ctrl Pts',(-1.87436920004126,-1.89056428003132,
13.8586819406588));
#436774=CARTESIAN_POINT('Ctrl Pts',(-1.87748879886921,-1.88752715198205,
13.868010383617));
#436775=CARTESIAN_POINT('Ctrl Pts',(-1.87714588160431,-1.87848418374469,
13.8744918421245));
#436776=CARTESIAN_POINT('Ctrl Pts',(-1.85198235760561,-1.91242522199886,
13.8587686893867));
#436777=CARTESIAN_POINT('Ctrl Pts',(-1.848890483899,-1.91543527929105,13.8680909899357));
#436778=CARTESIAN_POINT('Ctrl Pts',(-1.83988016077333,-1.91487807315619,
13.8745789365163));
#436779=CARTESIAN_POINT('Ctrl Pts',(-1.8512565417091,-1.92880472636389,
13.8400379222776));
#436780=CARTESIAN_POINT('Ctrl Pts',(-1.85158783296944,-1.93886258299485,
13.8494748685453));
#436781=CARTESIAN_POINT('Ctrl Pts',(-1.83853100517432,-1.9420688819817,
13.8557104837033));
#436782=CARTESIAN_POINT('Ctrl Pts',(-1.85527432945606,-1.9388520892342,
13.8235269408542));
#436783=CARTESIAN_POINT('Ctrl Pts',(-1.85965842923767,-1.94981549599923,
13.8362179249195));
#436784=CARTESIAN_POINT('Ctrl Pts',(-1.8450355596098,-1.95863789294693,
13.8391868794965));
#436785=CARTESIAN_POINT('Origin',(-1.90918733964416,-1.87418162464464,13.8235269408515));
#436786=CARTESIAN_POINT('Ctrl Pts',(-1.93353242134223,-1.90839138390051,
13.7902140241683));
#436787=CARTESIAN_POINT('Ctrl Pts',(-1.94416355476995,-1.91290110644569,
13.8026027327198));
#436788=CARTESIAN_POINT('Ctrl Pts',(-1.95327352985919,-1.89898039216277,
13.8057746032556));
#436789=CARTESIAN_POINT('Ctrl Pts',(-1.92255979757213,-1.90374179139983,
13.8013225161808));
#436790=CARTESIAN_POINT('Ctrl Pts',(-1.9331800585313,-1.90824689795181,
13.8136962270464));
#436791=CARTESIAN_POINT('Ctrl Pts',(-1.94228362940304,-1.89434856701977,
13.8168830918628));
#436792=CARTESIAN_POINT('Ctrl Pts',(-1.91158244340521,-1.89909019441801,
13.8124254880875));
#436793=CARTESIAN_POINT('Ctrl Pts',(-1.92218715447773,-1.90358870284954,
13.8247886461868));
#436794=CARTESIAN_POINT('Ctrl Pts',(-1.931288734703,-1.88971492183638,13.8279860620656));
#436795=CARTESIAN_POINT('Ctrl Pts',(-1.90060016733647,-1.8944365118058,
13.8235227163065));
#436796=CARTESIAN_POINT('Ctrl Pts',(-1.91118432402242,-1.89892630138706,
13.8358800595847));
#436797=CARTESIAN_POINT('Ctrl Pts',(-1.92028864223974,-1.88507938040817,
13.8390832900376));
#436798=CARTESIAN_POINT('Origin',(-1.94211960510584,-1.88813650159727,13.7902182540695));
#436799=CARTESIAN_POINT('Ctrl Pts',(-1.95237191771892,-1.91637449379808,
13.7382347919292));
#436800=CARTESIAN_POINT('Ctrl Pts',(-1.96625689773392,-1.92228424833753,
13.7369371795942));
#436801=CARTESIAN_POINT('Ctrl Pts',(-1.97675890153011,-1.91136400597366,
13.7364597369712));
#436802=CARTESIAN_POINT('Ctrl Pts',(-1.95411356339353,-1.91711250757053,
13.7595490285574));
#436803=CARTESIAN_POINT('Ctrl Pts',(-1.96833022087941,-1.92316233867132,
13.7633824266926));
#436804=CARTESIAN_POINT('Ctrl Pts',(-1.97893156148258,-1.91250845497929,
13.7648920890506));
#436805=CARTESIAN_POINT('Ctrl Pts',(-1.94523126586499,-1.91334867777003,
13.780380659011));
#436806=CARTESIAN_POINT('Ctrl Pts',(-1.95752605189593,-1.91858653252729,
13.7901039518744));
#436807=CARTESIAN_POINT('Ctrl Pts',(-1.96785337346261,-1.90667721387824,
13.7926933640891));
#436808=CARTESIAN_POINT('Ctrl Pts',(-1.92979185001233,-1.90680630131331,
13.7936647693663));
#436809=CARTESIAN_POINT('Ctrl Pts',(-1.93973837744101,-1.91105364448938,
13.8072068914933));
#436810=CARTESIAN_POINT('Ctrl Pts',(-1.94865316318078,-1.89652192521527,
13.8104111085397));
#436811=CARTESIAN_POINT('Origin',(-1.96120393315495,-1.89622338678162,13.7435492065112));
#436812=CARTESIAN_POINT('Origin',(-1.96120393315495,-1.89622338678162,14.));
#436813=CARTESIAN_POINT('Origin',(-1.96120393315495,-1.89622338678162,12.5369868989719));
#436814=CARTESIAN_POINT('Ctrl Pts',(-1.94784785780646,-1.93206865653427,
12.506462012331));
#436815=CARTESIAN_POINT('Ctrl Pts',(-1.95249012722371,-1.93667331967586,
12.4999388158272));
#436816=CARTESIAN_POINT('Ctrl Pts',(-1.95243520308855,-1.93661884047225,
12.4907030323752));
#436817=CARTESIAN_POINT('Ctrl Pts',(-1.95866813966155,-1.92437774737275,
12.5042014951932));
#436818=CARTESIAN_POINT('Ctrl Pts',(-1.96508276230269,-1.92393761842813,
12.4980716682127));
#436819=CARTESIAN_POINT('Ctrl Pts',(-1.96983081992872,-1.9190815383211,
12.4907355092743));
#436820=CARTESIAN_POINT('Ctrl Pts',(-1.95735445356975,-1.9184955768467,
12.5218047446509));
#436821=CARTESIAN_POINT('Ctrl Pts',(-1.96908392516923,-1.91988782931414,
12.5216906929434));
#436822=CARTESIAN_POINT('Ctrl Pts',(-1.97717718493758,-1.91135144245249,
12.5161988840776));
#436823=CARTESIAN_POINT('Ctrl Pts',(-1.95258502108486,-1.91646478877674,
12.5369868989719));
#436824=CARTESIAN_POINT('Ctrl Pts',(-1.96668949693684,-1.92247056037261,
12.5369868989719));
#436825=CARTESIAN_POINT('Ctrl Pts',(-1.97720808151055,-1.91131865873717,
12.5369868989719));
#436826=CARTESIAN_POINT('Origin',(-3.60557045705452E-31,-8.83174710230764E-31,
12.5));
#436827=CARTESIAN_POINT('Origin',(-1.73986539582215,-2.04305131259621,12.5));
#436828=CARTESIAN_POINT('',(-1.73986539582215,-2.04305131259621,12.5893111709658));
#436829=CARTESIAN_POINT('',(-1.73986539582215,-2.04305131259621,13.8235269408515));
#436830=CARTESIAN_POINT('',(-1.73986539582215,-2.04305131259621,12.5));
#436831=CARTESIAN_POINT('',(-1.77155062986483,-2.05964404121034,13.7902182540695));
#436832=CARTESIAN_POINT('',(-1.73986539582215,-2.04305131259621,13.8235269408515));
#436833=CARTESIAN_POINT('',(-1.7899123001692,-2.06925956785762,13.7435492065112));
#436834=CARTESIAN_POINT('Origin',(-1.72950249645161,-2.03762490086689,13.7445212918703));
#436835=CARTESIAN_POINT('',(-1.7899123001692,-2.06925956785762,12.5369868989719));
#436836=CARTESIAN_POINT('',(-1.7899123001692,-2.06925956785762,12.5));
#436837=CARTESIAN_POINT('Ctrl Pts',(-1.7899123001692,-2.06925956785762,
12.5369868989719));
#436838=CARTESIAN_POINT('Ctrl Pts',(-1.77324216577622,-2.0605298543396,
12.5544431401645));
#436839=CARTESIAN_POINT('Ctrl Pts',(-1.75656010846005,-2.05179389709846,
12.5718848856037));
#436840=CARTESIAN_POINT('Ctrl Pts',(-1.73986539582215,-2.04305131259621,
12.5893111709658));
#436841=CARTESIAN_POINT('Origin',(-1.77202125744066,-2.34643707963298,12.5));
#436842=CARTESIAN_POINT('',(-1.70769732837638,-2.13761339725486,13.7435492065112));
#436843=CARTESIAN_POINT('',(-1.70159569779326,-2.11780482857113,13.7902182540695));
#436844=CARTESIAN_POINT('Origin',(-1.68556166719576,-2.06575133368299,13.7418732680461));
#436845=CARTESIAN_POINT('',(-1.6910666124833,-2.08362280022673,13.8235269408515));
#436846=CARTESIAN_POINT('',(-1.70159569779326,-2.11780482857113,13.7902182540695));
#436847=CARTESIAN_POINT('',(-1.6910666124833,-2.08362280022673,12.5893111709658));
#436848=CARTESIAN_POINT('',(-1.6910666124833,-2.08362280022673,12.5));
#436849=CARTESIAN_POINT('',(-1.70769732837638,-2.13761339725486,12.5369868989719));
#436850=CARTESIAN_POINT('Ctrl Pts',(-1.6910666124833,-2.08362280022673,
12.5893111709658));
#436851=CARTESIAN_POINT('Ctrl Pts',(-1.69661430871786,-2.10163305509251,
12.5718848856037));
#436852=CARTESIAN_POINT('Ctrl Pts',(-1.70215779955624,-2.11962965739805,
12.5544431401645));
#436853=CARTESIAN_POINT('Ctrl Pts',(-1.70769732837638,-2.13761339725486,
12.5369868989719));
#436854=CARTESIAN_POINT('',(-1.70769732837638,-2.13761339725486,12.5));
#436855=CARTESIAN_POINT('Origin',(-1.72391839740909,-2.07350346960706,12.5));
#436856=CARTESIAN_POINT('',(-1.70281517807711,-2.04636964742875,13.8587068136939));
#436857=CARTESIAN_POINT('Ctrl Pts',(-1.69106661247695,-2.08362280022854,
13.8235269408542));
#436858=CARTESIAN_POINT('Ctrl Pts',(-1.69055076997176,-2.08194814923894,
13.8262006681044));
#436859=CARTESIAN_POINT('Ctrl Pts',(-1.69018892118107,-2.08018324315511,
13.8288634856214));
#436860=CARTESIAN_POINT('Ctrl Pts',(-1.6899703697339,-2.07833604399288,
13.8314912288862));
#436861=CARTESIAN_POINT('Ctrl Pts',(-1.68974506573441,-2.07643177218637,
13.8342001611531));
#436862=CARTESIAN_POINT('Ctrl Pts',(-1.68967130704777,-2.07443798675416,
13.8368750301949));
#436863=CARTESIAN_POINT('Ctrl Pts',(-1.68977547353421,-2.07233908740906,
13.8394886372969));
#436864=CARTESIAN_POINT('Ctrl Pts',(-1.68978351856463,-2.07217698432142,
13.8396904925131));
#436865=CARTESIAN_POINT('Ctrl Pts',(-1.68979264687108,-2.07201425151545,
13.8398919674349));
#436866=CARTESIAN_POINT('Ctrl Pts',(-1.68980288204296,-2.07185088139667,
13.8400930404591));
#436867=CARTESIAN_POINT('Ctrl Pts',(-1.68996235290682,-2.06930546503583,
13.8432258934518));
#436868=CARTESIAN_POINT('Ctrl Pts',(-1.6903885864837,-2.06661825424749,
13.8462331177034));
#436869=CARTESIAN_POINT('Ctrl Pts',(-1.69116295655849,-2.06389200352702,
13.8489036603661));
#436870=CARTESIAN_POINT('Ctrl Pts',(-1.69141633945876,-2.06299994256431,
13.8497774930041));
#436871=CARTESIAN_POINT('Ctrl Pts',(-1.69170707101167,-2.06210394025367,
13.85061494757));
#436872=CARTESIAN_POINT('Ctrl Pts',(-1.69203820356988,-2.0612082813038,
13.8514076489583));
#436873=CARTESIAN_POINT('Ctrl Pts',(-1.69273859668696,-2.05931383345145,
13.8530843267192));
#436874=CARTESIAN_POINT('Ctrl Pts',(-1.69369130868293,-2.05723586281645,
13.8546805203176));
#436875=CARTESIAN_POINT('Ctrl Pts',(-1.69496507550662,-2.05515184004389,
13.8559412814274));
#436876=CARTESIAN_POINT('Ctrl Pts',(-1.69513554681686,-2.05487293021049,
13.8561100121513));
#436877=CARTESIAN_POINT('Ctrl Pts',(-1.69531169269203,-2.05459392393159,
13.8562727473908));
#436878=CARTESIAN_POINT('Ctrl Pts',(-1.69549360208566,-2.05431524895565,
13.8564289040185));
#436879=CARTESIAN_POINT('Ctrl Pts',(-1.69631855911052,-2.05305146111891,
13.8571370725437));
#436880=CARTESIAN_POINT('Ctrl Pts',(-1.69727845604051,-2.05177351737073,
13.8577210840554));
#436881=CARTESIAN_POINT('Ctrl Pts',(-1.69835944725488,-2.05054871734515,
13.8581177131616));
#436882=CARTESIAN_POINT('Ctrl Pts',(-1.69866389158743,-2.05020377150161,
13.8582294175695));
#436883=CARTESIAN_POINT('Ctrl Pts',(-1.69897778725942,-2.04986295174723,
13.8583265086086));
#436884=CARTESIAN_POINT('Ctrl Pts',(-1.69930045864519,-2.04952751849591,
13.8584082369006));
#436885=CARTESIAN_POINT('Ctrl Pts',(-1.6997640508988,-2.04904559086375,
13.8585256585398));
#436886=CARTESIAN_POINT('Ctrl Pts',(-1.70025175453929,-2.0485690147105,
13.8586122832068));
#436887=CARTESIAN_POINT('Ctrl Pts',(-1.70075145235216,-2.04811073490248,
13.8586682984299));
#436888=CARTESIAN_POINT('Ctrl Pts',(-1.70115116106901,-2.04774415648388,
13.8587131050557));
#436889=CARTESIAN_POINT('Ctrl Pts',(-1.70156280045229,-2.04738506315215,
13.8587357943552));
#436890=CARTESIAN_POINT('Ctrl Pts',(-1.70198675233971,-2.04703379387748,
13.8587355499465));
#436891=CARTESIAN_POINT('Ctrl Pts',(-1.70226076255196,-2.04680676017067,
13.8587353919793));
#436892=CARTESIAN_POINT('Ctrl Pts',(-1.70253692833895,-2.0465854201758,
13.8587257282814));
#436893=CARTESIAN_POINT('Ctrl Pts',(-1.70281517807711,-2.04636964742875,
13.8587068136939));
#436894=CARTESIAN_POINT('Ctrl Pts',(-1.70281517807711,-2.04636964742875,
13.8587068136939));
#436895=CARTESIAN_POINT('Ctrl Pts',(-1.70373032629727,-2.04565998262645,
13.8586446046466));
#436896=CARTESIAN_POINT('Ctrl Pts',(-1.70466798977104,-2.04501046493111,
13.858482427929));
#436897=CARTESIAN_POINT('Ctrl Pts',(-1.7056258805372,-2.04441725361486,
13.8582284286032));
#436898=CARTESIAN_POINT('Ctrl Pts',(-1.70660856503678,-2.0438086878096,
13.8579678548414));
#436899=CARTESIAN_POINT('Ctrl Pts',(-1.70761574434311,-2.04325919654583,
13.857615680862));
#436900=CARTESIAN_POINT('Ctrl Pts',(-1.7086030704553,-2.04278193701926,
13.8571944833187));
#436901=CARTESIAN_POINT('Ctrl Pts',(-1.71106704374375,-2.04159088706059,
13.8561433417727));
#436902=CARTESIAN_POINT('Ctrl Pts',(-1.71352054069227,-2.04078966753298,
13.8546163505474));
#436903=CARTESIAN_POINT('Ctrl Pts',(-1.71578600790379,-2.04027229420252,
13.8528973491085));
#436904=CARTESIAN_POINT('Ctrl Pts',(-1.71619987533943,-2.04017777772819,
13.8525833129072));
#436905=CARTESIAN_POINT('Ctrl Pts',(-1.71660750322806,-2.04009259757524,
13.8522628768811));
#436906=CARTESIAN_POINT('Ctrl Pts',(-1.71700788073077,-2.04001594375306,
13.851937733538));
#436907=CARTESIAN_POINT('Ctrl Pts',(-1.71945293059018,-2.03954782949618,
13.8499521282529));
#436908=CARTESIAN_POINT('Ctrl Pts',(-1.72187134516643,-2.03935517787733,
13.847639871647));
#436909=CARTESIAN_POINT('Ctrl Pts',(-1.72412964177623,-2.03936802696199,
13.8452109780794));
#436910=CARTESIAN_POINT('Ctrl Pts',(-1.72514569616539,-2.03937380803114,
13.8441181685877));
#436911=CARTESIAN_POINT('Ctrl Pts',(-1.72612959015532,-2.03942051627108,
13.8430021611332));
#436912=CARTESIAN_POINT('Ctrl Pts',(-1.72707123023827,-2.03949919344993,
13.8418824960098));
#436913=CARTESIAN_POINT('Ctrl Pts',(-1.72929022913938,-2.039684598231,13.8392439765549));
#436914=CARTESIAN_POINT('Ctrl Pts',(-1.73138097559818,-2.04005262731545,
13.8364981347964));
#436915=CARTESIAN_POINT('Ctrl Pts',(-1.7333549313815,-2.04057055163272,
13.8336931113419));
#436916=CARTESIAN_POINT('Ctrl Pts',(-1.73527743895667,-2.0410749770265,
13.8309611966327));
#436917=CARTESIAN_POINT('Ctrl Pts',(-1.73709094773704,-2.04172263730824,
13.8281701127185));
#436918=CARTESIAN_POINT('Ctrl Pts',(-1.73878292640722,-2.04251507617613,
13.825358068512));
#436919=CARTESIAN_POINT('Ctrl Pts',(-1.73914974920895,-2.04268687777791,
13.8247484142932));
#436920=CARTESIAN_POINT('Ctrl Pts',(-1.73951071135475,-2.04286557361434,
13.8241378483365));
#436921=CARTESIAN_POINT('Ctrl Pts',(-1.73986539582215,-2.04305131259621,
13.8235269408515));
#436922=CARTESIAN_POINT('',(-1.7018486299195,-2.04714975095789,12.5969504640361));
#436923=CARTESIAN_POINT('Origin',(-1.72393969975224,-2.07352878547137,12.584524458991));
#436924=CARTESIAN_POINT('Origin',(-1.72393969975224,-2.07352878547137,12.584524458991));
#436925=CARTESIAN_POINT('Ctrl Pts',(-1.6910666124833,-2.08362280022673,
12.5893111709658));
#436926=CARTESIAN_POINT('Ctrl Pts',(-1.68773011555536,-2.07279106801025,
12.5770542771492));
#436927=CARTESIAN_POINT('Ctrl Pts',(-1.70219730425849,-2.0651422690272,
12.5737548217797));
#436928=CARTESIAN_POINT('Ctrl Pts',(-1.69836241150306,-2.10730816334679,
12.5663937883685));
#436929=CARTESIAN_POINT('Ctrl Pts',(-1.69502165840993,-2.09646261375159,
12.5540940315304));
#436930=CARTESIAN_POINT('Ctrl Pts',(-1.70953517889259,-2.08879295153526,
12.5508374392248));
#436931=CARTESIAN_POINT('Ctrl Pts',(-1.70565084915105,-2.13096962822584,
12.5434499600945));
#436932=CARTESIAN_POINT('Ctrl Pts',(-1.70229923407987,-2.12008881588674,
12.5311293540533));
#436933=CARTESIAN_POINT('Ctrl Pts',(-1.71686475739119,-2.11242087644829,
12.5278936106989));
#436934=CARTESIAN_POINT('Ctrl Pts',(-1.7129325020536,-2.15460906684579,
12.5204817579905));
#436935=CARTESIAN_POINT('Ctrl Pts',(-1.70956429877839,-2.14367440192156,
12.5081597038247));
#436936=CARTESIAN_POINT('Ctrl Pts',(-1.72418667133044,-2.13602781668084,
12.5049254088044));
#436937=CARTESIAN_POINT('Ctrl Pts',(-1.70769732837638,-2.13761339725486,
12.5369868989719));
#436938=CARTESIAN_POINT('Ctrl Pts',(-1.70797154540172,-2.13850362542434,
12.5342545179733));
#436939=CARTESIAN_POINT('Ctrl Pts',(-1.70835246397393,-2.13931649574285,
12.5314872231885));
#436940=CARTESIAN_POINT('Ctrl Pts',(-1.70886924506505,-2.13998249755516,
12.5287124745063));
#436941=CARTESIAN_POINT('Ctrl Pts',(-1.70933530390373,-2.14058313104687,
12.5262100684184));
#436942=CARTESIAN_POINT('Ctrl Pts',(-1.70991217105562,-2.14106310253228,
12.5237004536639));
#436943=CARTESIAN_POINT('Ctrl Pts',(-1.71065215067803,-2.14137969490402,
12.5212220730815));
#436944=CARTESIAN_POINT('Ctrl Pts',(-1.7112186690923,-2.14162207375199,
12.5193246583487));
#436945=CARTESIAN_POINT('Ctrl Pts',(-1.71188781174333,-2.14177100573518,
12.5174178313692));
#436946=CARTESIAN_POINT('Ctrl Pts',(-1.7126990144251,-2.14173761543006,
12.515581224835));
#436947=CARTESIAN_POINT('Ctrl Pts',(-1.71304459112783,-2.1417233909806,
12.5147988205795));
#436948=CARTESIAN_POINT('Ctrl Pts',(-1.71341631116917,-2.1416763409261,
12.5140295443048));
#436949=CARTESIAN_POINT('Ctrl Pts',(-1.71381849379747,-2.14159130042768,
12.5132817086137));
#436950=CARTESIAN_POINT('Ctrl Pts',(-1.71442714279929,-2.14146260313735,
12.5121499604604));
#436951=CARTESIAN_POINT('Ctrl Pts',(-1.71511722325838,-2.14123712126033,
12.5110494206568));
#436952=CARTESIAN_POINT('Ctrl Pts',(-1.71588917422434,-2.14087761629533,
12.5100666561695));
#436953=CARTESIAN_POINT('Ctrl Pts',(-1.71633242669134,-2.1406711893723,
12.5095023550641));
#436954=CARTESIAN_POINT('Ctrl Pts',(-1.71680751791336,-2.14041759783811,
12.5089719619137));
#436955=CARTESIAN_POINT('Ctrl Pts',(-1.71730253525883,-2.1401159604488,
12.5085043804652));
#436956=CARTESIAN_POINT('Ctrl Pts',(-1.71802692866339,-2.13967455342057,
12.5078201359221));
#436957=CARTESIAN_POINT('Ctrl Pts',(-1.7188143742359,-2.13911642486643,
12.5072563000949));
#436958=CARTESIAN_POINT('Ctrl Pts',(-1.71960659921693,-2.13847250067384,
12.5068768744332));
#436959=CARTESIAN_POINT('Ctrl Pts',(-1.72017784796522,-2.1380081870031,
12.5066032824114));
#436960=CARTESIAN_POINT('Ctrl Pts',(-1.72076165558107,-2.1374911540367,
12.5064197834844));
#436961=CARTESIAN_POINT('Ctrl Pts',(-1.72132713448378,-2.1369522093198,
12.5063282718343));
#436962=CARTESIAN_POINT('Ctrl Pts',(-1.72215255861389,-2.13616551688619,
12.5061946931565));
#436963=CARTESIAN_POINT('Ctrl Pts',(-1.72295730511337,-2.13531609146183,
12.5062515701262));
#436964=CARTESIAN_POINT('Ctrl Pts',(-1.7237026563326,-2.1344672857251,12.5064436508398));
#436965=CARTESIAN_POINT('',(-1.70219730425849,-2.0651422690272,12.5737548217797));
#436966=CARTESIAN_POINT('Origin',(-1.7120917548358,-2.07714642863014,12.5893111709658));
#436967=CARTESIAN_POINT('Ctrl Pts',(-1.7237026563326,-2.13446728572511,
12.5064436508398));
#436968=CARTESIAN_POINT('Ctrl Pts',(-1.72051976437344,-2.12420523980202,
12.5164271754438));
#436969=CARTESIAN_POINT('Ctrl Pts',(-1.71733541115934,-2.11393918790128,
12.5264061185523));
#436970=CARTESIAN_POINT('Ctrl Pts',(-1.71414954613012,-2.10366898865532,
12.536380305637));
#436971=CARTESIAN_POINT('Ctrl Pts',(-1.71016786100664,-2.09083332261872,
12.5488460165097));
#436972=CARTESIAN_POINT('Ctrl Pts',(-1.70618381323914,-2.07799117467343,
12.5613043021964));
#436973=CARTESIAN_POINT('Ctrl Pts',(-1.70219730425849,-2.0651422690272,
12.5737548217797));
#436974=CARTESIAN_POINT('Ctrl Pts',(-1.73986539582215,-2.0430513125962,
12.5893111709658));
#436975=CARTESIAN_POINT('Ctrl Pts',(-1.72982485735823,-2.03779334512633,
12.5770542771492));
#436976=CARTESIAN_POINT('Ctrl Pts',(-1.71966334052536,-2.05062094234913,
12.5737548217797));
#436977=CARTESIAN_POINT('Ctrl Pts',(-1.7304976607633,-2.0381456746782,12.5928319619712));
#436978=CARTESIAN_POINT('Ctrl Pts',(-1.72223849057577,-2.03749796781189,
12.5821634970843));
#436979=CARTESIAN_POINT('Ctrl Pts',(-1.71625528019318,-2.04882557549479,
12.5773203894503));
#436980=CARTESIAN_POINT('Ctrl Pts',(-1.71376979499771,-2.03727240137162,
12.5969440695591));
#436981=CARTESIAN_POINT('Ctrl Pts',(-1.71066714065118,-2.03982819450837,
12.5878292599214));
#436982=CARTESIAN_POINT('Ctrl Pts',(-1.71029302082701,-2.0485163662646,
12.5813877129824));
#436983=CARTESIAN_POINT('Ctrl Pts',(-1.69020779286108,-2.05679180968373,
12.596957478804));
#436984=CARTESIAN_POINT('Ctrl Pts',(-1.69328756872517,-2.05425496641387,
12.5878468778671));
#436985=CARTESIAN_POINT('Ctrl Pts',(-1.70186365910379,-2.05550722667254,
12.5814011370086));
#436986=CARTESIAN_POINT('Ctrl Pts',(-1.68794916991053,-2.07350221451147,
12.5928371701607));
#436987=CARTESIAN_POINT('Ctrl Pts',(-1.68882562475084,-2.06527014960546,
12.5821692192951));
#436988=CARTESIAN_POINT('Ctrl Pts',(-1.70105042348384,-2.0614520194472,
12.5773318885715));
#436989=CARTESIAN_POINT('Ctrl Pts',(-1.69106661248325,-2.08362280022674,
12.5893111709658));
#436990=CARTESIAN_POINT('Ctrl Pts',(-1.68773011555531,-2.07279106801026,
12.5770542771492));
#436991=CARTESIAN_POINT('Ctrl Pts',(-1.70219730425843,-2.06514226902721,
12.5737548217797));
#436992=CARTESIAN_POINT('',(-1.71966334052536,-2.05062094234913,12.5737548217797));
#436993=CARTESIAN_POINT('Origin',(-1.72965931683779,-2.06254069308315,12.5893111709658));
#436994=CARTESIAN_POINT('Ctrl Pts',(-1.70219730425843,-2.06514226902721,
12.5737548217797));
#436995=CARTESIAN_POINT('Ctrl Pts',(-1.7018712079625,-2.06419465051916,
12.5746934679442));
#436996=CARTESIAN_POINT('Ctrl Pts',(-1.70168357581051,-2.06308644042457,
12.5756680099006));
#436997=CARTESIAN_POINT('Ctrl Pts',(-1.70165247173435,-2.06194427747454,
12.5765688348656));
#436998=CARTESIAN_POINT('Ctrl Pts',(-1.70164423727452,-2.06164190247768,
12.5768073183026));
#436999=CARTESIAN_POINT('Ctrl Pts',(-1.70164672579989,-2.06133721716881,
12.5770407398754));
#437000=CARTESIAN_POINT('Ctrl Pts',(-1.70165970942549,-2.06103258202906,
12.5772674179684));
#437001=CARTESIAN_POINT('Ctrl Pts',(-1.70171299071403,-2.05978244179235,
12.5781976435658));
#437002=CARTESIAN_POINT('Ctrl Pts',(-1.70195731171084,-2.0584626218299,
12.5790594849312));
#437003=CARTESIAN_POINT('Ctrl Pts',(-1.70242365794515,-2.05717102827408,
12.5797571720116));
#437004=CARTESIAN_POINT('Ctrl Pts',(-1.70272749928512,-2.0563295086309,
12.580211740231));
#437005=CARTESIAN_POINT('Ctrl Pts',(-1.70315705535578,-2.0554681036376,
12.5806009430798));
#437006=CARTESIAN_POINT('Ctrl Pts',(-1.70369794200381,-2.05465535872171,
12.5808812374708));
#437007=CARTESIAN_POINT('Ctrl Pts',(-1.70416274307174,-2.05395694121364,
12.5811221033394));
#437008=CARTESIAN_POINT('Ctrl Pts',(-1.70471936705266,-2.05328022155487,
12.581287365893));
#437009=CARTESIAN_POINT('Ctrl Pts',(-1.70534283668056,-2.05266869158297,
12.581359338449));
#437010=CARTESIAN_POINT('Ctrl Pts',(-1.70542948608469,-2.05258370154449,
12.5813693411482));
#437011=CARTESIAN_POINT('Ctrl Pts',(-1.70551740134559,-2.05249991638436,
12.5813775999465));
#437012=CARTESIAN_POINT('Ctrl Pts',(-1.70560649050039,-2.05241739679769,
12.5813841266931));
#437013=CARTESIAN_POINT('Ctrl Pts',(-1.7057576410266,-2.05227739233838,
12.5813952001081));
#437014=CARTESIAN_POINT('Ctrl Pts',(-1.70591359671892,-2.05214053986984,
12.5814007534795));
#437015=CARTESIAN_POINT('Ctrl Pts',(-1.7060744197276,-2.05200704722687,
12.5814005856065));
#437016=CARTESIAN_POINT('Ctrl Pts',(-1.70681060458359,-2.05139597009959,
12.5813998171494));
#437017=CARTESIAN_POINT('Ctrl Pts',(-1.70759770136284,-2.0508972574962,
12.58127954464));
#437018=CARTESIAN_POINT('Ctrl Pts',(-1.70841540465512,-2.05048874625654,
12.5810700125799));
#437019=CARTESIAN_POINT('Ctrl Pts',(-1.70940309712921,-2.04999531119176,
12.5808169217085));
#437020=CARTESIAN_POINT('Ctrl Pts',(-1.71044301304317,-2.04964840594338,
12.5804173076348));
#437021=CARTESIAN_POINT('Ctrl Pts',(-1.71143577490685,-2.04945372864711,
12.5799304713245));
#437022=CARTESIAN_POINT('Ctrl Pts',(-1.71266611960818,-2.04921246214735,
12.5793271277669));
#437023=CARTESIAN_POINT('Ctrl Pts',(-1.71389416448181,-2.0491584381087,
12.5785808224116));
#437024=CARTESIAN_POINT('Ctrl Pts',(-1.71506675113783,-2.04926224753565,
12.5777485681082));
#437025=CARTESIAN_POINT('Ctrl Pts',(-1.71681403372176,-2.04941693495497,
12.576508418016));
#437026=CARTESIAN_POINT('Ctrl Pts',(-1.71842406895792,-2.04991393198624,
12.5750928681475));
#437027=CARTESIAN_POINT('Ctrl Pts',(-1.71966334052536,-2.05062094234913,
12.5737548217797));
#437028=CARTESIAN_POINT('Ctrl Pts',(-1.71966334052536,-2.05062094234913,
12.5737548217797));
#437029=CARTESIAN_POINT('Ctrl Pts',(-1.72982485735823,-2.03779334512633,
12.5770542771492));
#437030=CARTESIAN_POINT('Ctrl Pts',(-1.73986539582215,-2.0430513125962,
12.5893111709658));
#437031=CARTESIAN_POINT('Ctrl Pts',(-1.74157355681532,-2.06215165682384,
12.5508408821982));
#437032=CARTESIAN_POINT('Ctrl Pts',(-1.75176403768451,-2.04928232023313,
12.55409748406));
#437033=CARTESIAN_POINT('Ctrl Pts',(-1.76181738530398,-2.05454699552289,
12.5663972313419));
#437034=CARTESIAN_POINT('Ctrl Pts',(-1.76346291890175,-2.07367006345149,
12.52790050457));
#437035=CARTESIAN_POINT('Ctrl Pts',(-1.77366119925847,-2.06074929121809,
12.5311362602938));
#437036=CARTESIAN_POINT('Ctrl Pts',(-1.78374722883563,-2.06603108119449,
12.5434568539655));
#437037=CARTESIAN_POINT('Ctrl Pts',(-1.78533305387325,-2.08517710645503,
12.5049357605811));
#437038=CARTESIAN_POINT('Ctrl Pts',(-1.79552072232037,-2.07219655189828,
12.5081700652078));
#437039=CARTESIAN_POINT('Ctrl Pts',(-1.80565666089238,-2.07750447791038,
12.5204921097672));
#437040=CARTESIAN_POINT('Ctrl Pts',(-1.78389697582175,-2.08442150750062,
12.5064436508395));
#437041=CARTESIAN_POINT('Ctrl Pts',(-1.78494541923713,-2.08379731666816,
12.5062361689309));
#437042=CARTESIAN_POINT('Ctrl Pts',(-1.78600909770868,-2.08310350132558,
12.5061871075061));
#437043=CARTESIAN_POINT('Ctrl Pts',(-1.7869992958058,-2.08237513028719,
12.5063648335164));
#437044=CARTESIAN_POINT('Ctrl Pts',(-1.78744910485947,-2.08204425923376,
12.5064455676329));
#437045=CARTESIAN_POINT('Ctrl Pts',(-1.78788989432329,-2.08170146505024,
12.506574497099));
#437046=CARTESIAN_POINT('Ctrl Pts',(-1.78830211929608,-2.08136061611557,
12.5067492519495));
#437047=CARTESIAN_POINT('Ctrl Pts',(-1.78913050138035,-2.08067566695052,
12.5071004286051));
#437048=CARTESIAN_POINT('Ctrl Pts',(-1.78987347466938,-2.0799727671967,
12.5076537929613));
#437049=CARTESIAN_POINT('Ctrl Pts',(-1.7904817753905,-2.07931154402785,
12.5083435010505));
#437050=CARTESIAN_POINT('Ctrl Pts',(-1.79052007155613,-2.07926991607787,
12.5083869222964));
#437051=CARTESIAN_POINT('Ctrl Pts',(-1.79055782934599,-2.07922844069112,
12.5084308732337));
#437052=CARTESIAN_POINT('Ctrl Pts',(-1.79059503496308,-2.07918712747152,
12.5084753333615));
#437053=CARTESIAN_POINT('Ctrl Pts',(-1.79089347311909,-2.07885574092186,
12.5088319622689));
#437054=CARTESIAN_POINT('Ctrl Pts',(-1.7911634010344,-2.07852892409326,
12.509227847131));
#437055=CARTESIAN_POINT('Ctrl Pts',(-1.79139895124509,-2.07821817805432,
12.5096423454524));
#437056=CARTESIAN_POINT('Ctrl Pts',(-1.79213706135524,-2.07724443749871,
12.5109411997424));
#437057=CARTESIAN_POINT('Ctrl Pts',(-1.79259071417036,-2.0763744482959,
12.5124831113042));
#437058=CARTESIAN_POINT('Ctrl Pts',(-1.79285433157038,-2.07561456386924,
12.5140723025008));
#437059=CARTESIAN_POINT('Ctrl Pts',(-1.7928790328095,-2.07554336186619,
12.5142212114565));
#437060=CARTESIAN_POINT('Ctrl Pts',(-1.79290209391165,-2.075473118047,12.5143705582413));
#437061=CARTESIAN_POINT('Ctrl Pts',(-1.79292360919738,-2.07540383425019,
12.5145201959299));
#437062=CARTESIAN_POINT('Ctrl Pts',(-1.79320000507549,-2.07451378072728,
12.5164425148273));
#437063=CARTESIAN_POINT('Ctrl Pts',(-1.79324101682725,-2.0737548500219,
12.518463520594));
#437064=CARTESIAN_POINT('Ctrl Pts',(-1.79312667174958,-2.07308540548798,
12.5205025929157));
#437065=CARTESIAN_POINT('Ctrl Pts',(-1.79306034707231,-2.072697101124,12.5216853356836));
#437066=CARTESIAN_POINT('Ctrl Pts',(-1.79294234967585,-2.07233952404283,
12.5228750347131));
#437067=CARTESIAN_POINT('Ctrl Pts',(-1.79279072200761,-2.07200995326322,
12.5240609649613));
#437068=CARTESIAN_POINT('Ctrl Pts',(-1.79241856003044,-2.07120103946552,
12.5269717671327));
#437069=CARTESIAN_POINT('Ctrl Pts',(-1.79182388067692,-2.07054242314726,
12.5299036066169));
#437070=CARTESIAN_POINT('Ctrl Pts',(-1.79107950309077,-2.06998712670806,
12.532813300402));
#437071=CARTESIAN_POINT('Ctrl Pts',(-1.79072215850561,-2.06972055208331,
12.5342101228452));
#437072=CARTESIAN_POINT('Ctrl Pts',(-1.79033044757617,-2.06947854081411,
12.5356023438239));
#437073=CARTESIAN_POINT('Ctrl Pts',(-1.7899123001692,-2.06925956785762,
12.5369868989719));
#437074=CARTESIAN_POINT('Origin',(-13.0832437096424,-7.97730267717418,-1.24008275899548));
#437075=CARTESIAN_POINT('Ctrl Pts',(-1.70768498702298,-2.13757346666599,
12.5369868989719));
#437076=CARTESIAN_POINT('Ctrl Pts',(-1.71222831500884,-2.15222411424545,
12.5369868989719));
#437077=CARTESIAN_POINT('Ctrl Pts',(-1.70005241588022,-2.16155314335328,
12.5369868989719));
#437078=CARTESIAN_POINT('Ctrl Pts',(-1.70922074632988,-2.14252597814296,
12.5218025310015));
#437079=CARTESIAN_POINT('Ctrl Pts',(-1.70941265130796,-2.15434202808292,
12.5216901060417));
#437080=CARTESIAN_POINT('Ctrl Pts',(-1.70008954208609,-2.16152471847184,
12.5161920673678));
#437081=CARTESIAN_POINT('Ctrl Pts',(-1.71493865396465,-2.14443427672418,
12.5042015548895));
#437082=CARTESIAN_POINT('Ctrl Pts',(-1.71384623655552,-2.15077335940398,
12.4980677368514));
#437083=CARTESIAN_POINT('Ctrl Pts',(-1.70852720123522,-2.15500403818936,
12.4907278922777));
#437084=CARTESIAN_POINT('Ctrl Pts',(-1.72369009019854,-2.13445172501886,
12.506463626192));
#437085=CARTESIAN_POINT('Ctrl Pts',(-1.72780071734796,-2.13954192960951,
12.4999376786891));
#437086=CARTESIAN_POINT('Ctrl Pts',(-1.72775051201418,-2.13947976016159,
12.4906970594712));
#437087=CARTESIAN_POINT('Origin',(-1.68667218602388,-2.14408976885145,12.5369868989719));
#437088=CARTESIAN_POINT('Origin',(-1.68667218602388,-2.14408976885145,14.));
#437089=CARTESIAN_POINT('Origin',(-1.68667218602388,-2.14408976885145,13.7435492065112));
#437090=CARTESIAN_POINT('Ctrl Pts',(-1.7004084099681,-2.11395046384977,
13.793642941384));
#437091=CARTESIAN_POINT('Ctrl Pts',(-1.70361735137066,-2.12427562312607,
13.8071662555867));
#437092=CARTESIAN_POINT('Ctrl Pts',(-1.68827452819122,-2.13166596550781,
13.8103758687955));
#437093=CARTESIAN_POINT('Ctrl Pts',(-1.70530134754244,-2.12983507486535,
13.7804579775006));
#437094=CARTESIAN_POINT('Ctrl Pts',(-1.70925120729145,-2.1425783978108,
13.7901904343351));
#437095=CARTESIAN_POINT('Ctrl Pts',(-1.69634931075966,-2.15162256665308,
13.7927914348263));
#437096=CARTESIAN_POINT('Ctrl Pts',(-1.70818200399808,-2.13918694318659,
13.7597120340895));
#437097=CARTESIAN_POINT('Ctrl Pts',(-1.71274763058253,-2.15393625313195,
13.7635825532445));
#437098=CARTESIAN_POINT('Ctrl Pts',(-1.70108730461836,-2.16340053939947,
13.7651073818884));
#437099=CARTESIAN_POINT('Ctrl Pts',(-1.70761790550376,-2.1373556332361,
13.7381884353898));
#437100=CARTESIAN_POINT('Ctrl Pts',(-1.71207752372754,-2.15175944231302,
13.7368803041982));
#437101=CARTESIAN_POINT('Ctrl Pts',(-1.7001590061108,-2.16109424680689,
13.7363986145813));
#437102=CARTESIAN_POINT('Origin',(-1.68057055544076,-2.12428120016772,13.7902182540695));
#437103=CARTESIAN_POINT('Ctrl Pts',(-1.69106545301784,-2.08361903867141,
13.8235227101244));
#437104=CARTESIAN_POINT('Ctrl Pts',(-1.69445420415729,-2.09460535079307,
13.8358800583119));
#437105=CARTESIAN_POINT('Ctrl Pts',(-1.67975221738023,-2.10225241780362,
13.8390832900376));
#437106=CARTESIAN_POINT('Ctrl Pts',(-1.69457670011487,-2.09501808657546,
13.8124254819053));
#437107=CARTESIAN_POINT('Ctrl Pts',(-1.69797203189519,-2.10602573404153,
13.8247886449158));
#437108=CARTESIAN_POINT('Ctrl Pts',(-1.6832436034655,-2.11366734232083,
13.8279860620657));
#437109=CARTESIAN_POINT('Ctrl Pts',(-1.69808637358516,-2.10641202579702,
13.8013225099955));
#437110=CARTESIAN_POINT('Ctrl Pts',(-1.70148668587057,-2.11743581417462,
13.8136962257787));
#437111=CARTESIAN_POINT('Ctrl Pts',(-1.68673363241358,-2.12507690300919,
13.8168830918626));
#437112=CARTESIAN_POINT('Ctrl Pts',(-1.70159453465617,-2.11780105510718,
13.7902140179785));
#437113=CARTESIAN_POINT('Ctrl Pts',(-1.70499833188868,-2.12883612945875,
13.802602731458));
#437114=CARTESIAN_POINT('Ctrl Pts',(-1.69022235930942,-2.13648131008831,
13.8057746032558));
#437115=CARTESIAN_POINT('Origin',(-1.6700414701308,-2.09009917182332,13.8235269408515));
#437116=CARTESIAN_POINT('Ctrl Pts',(-1.73986539582215,-2.04305131259621,
13.8235269408515));
#437117=CARTESIAN_POINT('Ctrl Pts',(-1.75032541850696,-2.04852895298456,
13.8362179249168));
#437118=CARTESIAN_POINT('Ctrl Pts',(-1.76059090559615,-2.03488040804824,
13.8391868794938));
#437119=CARTESIAN_POINT('Ctrl Pts',(-1.73029493036326,-2.03803951006836,
13.8400110824519));
#437120=CARTESIAN_POINT('Ctrl Pts',(-1.74026835444688,-2.03940064008055,
13.8494522556837));
#437121=CARTESIAN_POINT('Ctrl Pts',(-1.74478849747539,-2.0267319308157,
13.85569149686));
#437122=CARTESIAN_POINT('Ctrl Pts',(-1.71403385118767,-2.03705207394814,
13.8586819406588));
#437123=CARTESIAN_POINT('Ctrl Pts',(-1.71739062393921,-2.03427932795733,
13.868010383617));
#437124=CARTESIAN_POINT('Ctrl Pts',(-1.71778593356539,-2.02523849851021,
13.8744918421245));
#437125=CARTESIAN_POINT('Ctrl Pts',(-1.68993962940601,-2.05701553994687,
13.8587686893867));
#437126=CARTESIAN_POINT('Ctrl Pts',(-1.68661269604077,-2.05976356511108,
13.8680909899357));
#437127=CARTESIAN_POINT('Ctrl Pts',(-1.67767777149484,-2.05847378805118,
13.8745789365163));
#437128=CARTESIAN_POINT('Ctrl Pts',(-1.68788114693638,-2.07328138212866,
13.8400379222776));
#437129=CARTESIAN_POINT('Ctrl Pts',(-1.68739152716436,-2.08333277538466,
13.8494748685453));
#437130=CARTESIAN_POINT('Ctrl Pts',(-1.67411680175335,-2.08546415299714,
13.8557104837033));
#437131=CARTESIAN_POINT('Ctrl Pts',(-1.69106661247695,-2.08362280022854,
13.8235269408542));
#437132=CARTESIAN_POINT('Ctrl Pts',(-1.69454250509754,-2.09490707199417,
13.8362179249195));
#437133=CARTESIAN_POINT('Ctrl Pts',(-1.67924918460769,-2.10250821351705,
13.8391868794965));
#437134=CARTESIAN_POINT('Origin',(-1.75007147480651,-2.02356193210926,13.8235269408515));
#437135=CARTESIAN_POINT('Ctrl Pts',(-1.77154713728628,-2.05964221138041,
13.7902140241682));
#437136=CARTESIAN_POINT('Ctrl Pts',(-1.78177531224088,-2.06500346426484,
13.8026027327198));
#437137=CARTESIAN_POINT('Ctrl Pts',(-1.7919896420872,-2.05187161755297,
13.8057746032556));
#437138=CARTESIAN_POINT('Ctrl Pts',(-1.76099000897013,-2.05411371931309,
13.8013225161808));
#437139=CARTESIAN_POINT('Ctrl Pts',(-1.7712077238797,-2.05946948535651,
13.8136962270464));
#437140=CARTESIAN_POINT('Ctrl Pts',(-1.78141384636714,-2.0463594255136,
13.8168830918628));
#437141=CARTESIAN_POINT('Ctrl Pts',(-1.75042832938096,-2.0485828438631,
13.8124254880875));
#437142=CARTESIAN_POINT('Ctrl Pts',(-1.76063108395295,-2.05393076628067,
13.8247886461867));
#437143=CARTESIAN_POINT('Ctrl Pts',(-1.77083322137131,-2.04084501241263,
13.8279860620656));
#437144=CARTESIAN_POINT('Ctrl Pts',(-1.73986191426544,-2.0430494885418,
13.8235227163065));
#437145=CARTESIAN_POINT('Ctrl Pts',(-1.75004489351111,-2.04838704574704,
13.8358800595847));
#437146=CARTESIAN_POINT('Ctrl Pts',(-1.76024757046894,-2.03532828571048,
13.8390832900376));
#437147=CARTESIAN_POINT('Origin',(-1.78175670884918,-2.04015466072339,13.7902182540695));
#437148=CARTESIAN_POINT('Ctrl Pts',(-1.78967324922472,-2.06913435199042,
13.7382347919292));
#437149=CARTESIAN_POINT('Ctrl Pts',(-1.80303032825568,-2.07615619708222,
13.7369371795943));
#437150=CARTESIAN_POINT('Ctrl Pts',(-1.81438748863182,-2.06612830172923,
13.7364597369711));
#437151=CARTESIAN_POINT('Ctrl Pts',(-1.7913489447432,-2.07001187037406,
13.7595490285574));
#437152=CARTESIAN_POINT('Ctrl Pts',(-1.8050251800755,-2.07720036072702,
13.7633824266926));
#437153=CARTESIAN_POINT('Ctrl Pts',(-1.81645963601905,-2.0674460346313,
13.7648920890506));
#437154=CARTESIAN_POINT('Ctrl Pts',(-1.7828029893974,-2.06553657469893,
13.7803806590111));
#437155=CARTESIAN_POINT('Ctrl Pts',(-1.79462993175343,-2.07175914012728,
13.7901039518744));
#437156=CARTESIAN_POINT('Ctrl Pts',(-1.80589361004016,-2.06073122133546,
13.7926933640892));
#437157=CARTESIAN_POINT('Ctrl Pts',(-1.76794821134497,-2.05775751173561,
13.7936647693663));
#437158=CARTESIAN_POINT('Ctrl Pts',(-1.7775154446249,-2.06280145655211,
13.8072068914932));
#437159=CARTESIAN_POINT('Ctrl Pts',(-1.78758503717726,-2.04904472817376,
13.8104111085397));
#437160=CARTESIAN_POINT('Origin',(-1.80011837915356,-2.04977018737067,13.7435492065112));
#437161=CARTESIAN_POINT('Origin',(-1.80011837915356,-2.04977018737067,14.));
#437162=CARTESIAN_POINT('Origin',(-1.80011837915356,-2.04977018737067,12.5369868989719));
#437163=CARTESIAN_POINT('Ctrl Pts',(-1.7838850227879,-2.08440754081258,
12.506462012331));
#437164=CARTESIAN_POINT('Ctrl Pts',(-1.78813652264298,-2.08937527037166,
12.4999388158272));
#437165=CARTESIAN_POINT('Ctrl Pts',(-1.7880862218242,-2.0893164956162,12.4907030323752));
#437166=CARTESIAN_POINT('Ctrl Pts',(-1.79529618154332,-2.07762417593863,
12.5042014951932));
#437167=CARTESIAN_POINT('Ctrl Pts',(-1.80172533465173,-2.07770836278244,
12.4980716682127));
#437168=CARTESIAN_POINT('Ctrl Pts',(-1.80685340911806,-2.07325545165674,
12.4907355092743));
#437169=CARTESIAN_POINT('Ctrl Pts',(-1.79446631813886,-2.0716545002376,
12.5218047446509));
#437170=CARTESIAN_POINT('Ctrl Pts',(-1.80604327938808,-2.07399818092629,
12.5216906929434));
#437171=CARTESIAN_POINT('Ctrl Pts',(-1.8148054042794,-2.06614987399298,
12.5161988840776));
#437172=CARTESIAN_POINT('Ctrl Pts',(-1.78987828362776,-2.06924171642266,
12.5369868989719));
#437173=CARTESIAN_POINT('Ctrl Pts',(-1.80344630185995,-2.07637715003048,
12.5369868989719));
#437174=CARTESIAN_POINT('Ctrl Pts',(-1.8148388702237,-2.06611971772031,
12.5369868989719));
#437175=CARTESIAN_POINT('Origin',(-3.293628469579E-31,-9.1133900549324E-31,
12.5));
#437176=CARTESIAN_POINT('Origin',(-1.56754848850674,-2.1780684097752,12.5));
#437177=CARTESIAN_POINT('',(-1.56754848850674,-2.1780684097752,12.5893111709658));
#437178=CARTESIAN_POINT('',(-1.56754848850674,-2.1780684097752,13.8235269408515));
#437179=CARTESIAN_POINT('',(-1.56754848850674,-2.1780684097752,12.5));
#437180=CARTESIAN_POINT('',(-1.59777583112556,-2.19718856817951,13.7902182540695));
#437181=CARTESIAN_POINT('',(-1.56754848850674,-2.1780684097752,13.8235269408515));
#437182=CARTESIAN_POINT('',(-1.61529264979877,-2.20826874654634,13.7435492065112));
#437183=CARTESIAN_POINT('Origin',(-1.55766237376227,-2.17181538148075,13.7445212918706));
#437184=CARTESIAN_POINT('',(-1.61529264979877,-2.20826874654634,12.5369868989719));
#437185=CARTESIAN_POINT('',(-1.61529264979877,-2.20826874654634,12.5));
#437186=CARTESIAN_POINT('Ctrl Pts',(-1.61529264979877,-2.20826874654634,
12.5369868989719));
#437187=CARTESIAN_POINT('Ctrl Pts',(-1.59938953659722,-2.1982093097189,
12.5544431401645));
#437188=CARTESIAN_POINT('Ctrl Pts',(-1.58347504906643,-2.18814267811487,
12.5718848856037));
#437189=CARTESIAN_POINT('Ctrl Pts',(-1.56754848850674,-2.1780684097752,
12.5893111709658));
#437190=CARTESIAN_POINT('Origin',(-1.57486859763885,-2.48306568694209,12.5));
#437191=CARTESIAN_POINT('',(-1.52777976988047,-2.26969385076738,13.7435492065112));
#437192=CARTESIAN_POINT('',(-1.52331302421127,-2.24945385392455,13.7902182540695));
#437193=CARTESIAN_POINT('Origin',(-1.51157518860124,-2.19626664039524,13.7418732680442));
#437194=CARTESIAN_POINT('',(-1.51560512620464,-2.21452734525963,13.8235269408515));
#437195=CARTESIAN_POINT('',(-1.52331302421127,-2.24945385392455,13.7902182540695));
#437196=CARTESIAN_POINT('',(-1.51560512620464,-2.21452734525963,12.5893111709658));
#437197=CARTESIAN_POINT('',(-1.51560512620464,-2.21452734525963,12.5));
#437198=CARTESIAN_POINT('',(-1.52777976988047,-2.26969385076738,12.5369868989719));
#437199=CARTESIAN_POINT('Ctrl Pts',(-1.51560512620464,-2.21452734525963,
12.5893111709658));
#437200=CARTESIAN_POINT('Ctrl Pts',(-1.51966635996702,-2.2329298612335,
12.5718848856037));
#437201=CARTESIAN_POINT('Ctrl Pts',(-1.52372451513673,-2.25131842729607,
12.5544431401645));
#437202=CARTESIAN_POINT('Ctrl Pts',(-1.52777976988047,-2.26969385076738,
12.5369868989719));
#437203=CARTESIAN_POINT('',(-1.52777976988047,-2.26969385076738,12.5));
#437204=CARTESIAN_POINT('Origin',(-1.54917241891494,-2.20711941133036,12.5));
#437205=CARTESIAN_POINT('',(-1.53035107720997,-2.17835576641872,13.8587068136939));
#437206=CARTESIAN_POINT('Ctrl Pts',(-1.51560512619815,-2.21452734526091,
13.8235269408542));
#437207=CARTESIAN_POINT('Ctrl Pts',(-1.5152274997187,-2.21281622058131,
13.8262006681044));
#437208=CARTESIAN_POINT('Ctrl Pts',(-1.51501071118043,-2.2110276930412,
13.8288634856214));
#437209=CARTESIAN_POINT('Ctrl Pts',(-1.51494345082546,-2.20916882630991,
13.8314912288862));
#437210=CARTESIAN_POINT('Ctrl Pts',(-1.51487411233706,-2.20725252644317,
13.8342001611531));
#437211=CARTESIAN_POINT('Ctrl Pts',(-1.51496311109849,-2.2052593631498,
13.836875030195));
#437212=CARTESIAN_POINT('Ctrl Pts',(-1.5152380107614,-2.2031759382548,13.8394886372969));
#437213=CARTESIAN_POINT('Ctrl Pts',(-1.51525924192918,-2.20301503029649,
13.8396904925131));
#437214=CARTESIAN_POINT('Ctrl Pts',(-1.51528160409637,-2.20285358301223,
13.8398919674349));
#437215=CARTESIAN_POINT('Ctrl Pts',(-1.5153051213929,-2.20269159075557,
13.8400930404591));
#437216=CARTESIAN_POINT('Ctrl Pts',(-1.51567153669451,-2.20016764241355,
13.8432258934518));
#437217=CARTESIAN_POINT('Ctrl Pts',(-1.51631538464042,-2.19752411509091,
13.8462331177034));
#437218=CARTESIAN_POINT('Ctrl Pts',(-1.51730939280566,-2.19487005409481,
13.8489036603661));
#437219=CARTESIAN_POINT('Ctrl Pts',(-1.51763464384518,-2.19400161445002,
13.8497774930041));
#437220=CARTESIAN_POINT('Ctrl Pts',(-1.51799744051924,-2.19313229083374,
13.85061494757));
#437221=CARTESIAN_POINT('Ctrl Pts',(-1.51840047578048,-2.19226660249271,
13.8514076489583));
#437222=CARTESIAN_POINT('Ctrl Pts',(-1.51925295348439,-2.19043554680052,
13.8530843267192));
#437223=CARTESIAN_POINT('Ctrl Pts',(-1.52037186930745,-2.18844214531363,
13.8546805203176));
#437224=CARTESIAN_POINT('Ctrl Pts',(-1.52181126498018,-2.18646888077616,
13.8559412814273));
#437225=CARTESIAN_POINT('Ctrl Pts',(-1.52200390280191,-2.18620479398656,
13.8561100121513));
#437226=CARTESIAN_POINT('Ctrl Pts',(-1.52220220416813,-2.18594107360209,
13.8562727473908));
#437227=CARTESIAN_POINT('Ctrl Pts',(-1.52240622287091,-2.18567815319846,
13.8564289040185));
#437228=CARTESIAN_POINT('Ctrl Pts',(-1.52333144536046,-2.18448581216754,
13.8571370725437));
#437229=CARTESIAN_POINT('Ctrl Pts',(-1.52439231259193,-2.18329036118281,
13.8577210840553));
#437230=CARTESIAN_POINT('Ctrl Pts',(-1.52556953946978,-2.18215774739768,
13.8581177131616));
#437231=CARTESIAN_POINT('Ctrl Pts',(-1.5259010870775,-2.18183876437241,
13.8582294175695));
#437232=CARTESIAN_POINT('Ctrl Pts',(-1.52624171826153,-2.18152466407897,
13.8583265086086));
#437233=CARTESIAN_POINT('Ctrl Pts',(-1.52659065690888,-2.1812166476676,
13.8584082369006));
#437234=CARTESIAN_POINT('Ctrl Pts',(-1.52709198817353,-2.18077411068233,
13.8585256585398));
#437235=CARTESIAN_POINT('Ctrl Pts',(-1.52761691440119,-2.18033887267123,
13.8586122832068));
#437236=CARTESIAN_POINT('Ctrl Pts',(-1.52815230356963,-2.17992284776219,
13.8586682984299));
#437237=CARTESIAN_POINT('Ctrl Pts',(-1.52858056183296,-2.17959006907418,
13.8587131050557));
#437238=CARTESIAN_POINT('Ctrl Pts',(-1.52902010096034,-2.17926572302709,
13.8587357943552));
#437239=CARTESIAN_POINT('Ctrl Pts',(-1.52947127388974,-2.17895017858655,
13.8587355499465));
#437240=CARTESIAN_POINT('Ctrl Pts',(-1.52976287771037,-2.17874623469178,
13.8587353919793));
#437241=CARTESIAN_POINT('Ctrl Pts',(-1.53005616584286,-2.17854814126293,
13.8587257282814));
#437242=CARTESIAN_POINT('Ctrl Pts',(-1.53035107720997,-2.17835576641872,
13.8587068136939));
#437243=CARTESIAN_POINT('Ctrl Pts',(-1.53035107720997,-2.17835576641872,
13.8587068136939));
#437244=CARTESIAN_POINT('Ctrl Pts',(-1.53132102461955,-2.17772305604325,
13.8586446046466));
#437245=CARTESIAN_POINT('Ctrl Pts',(-1.53230850981748,-2.17715212784241,
13.858482427929));
#437246=CARTESIAN_POINT('Ctrl Pts',(-1.53331156551055,-2.17663896737792,
13.8582284286032));
#437247=CARTESIAN_POINT('Ctrl Pts',(-1.53434058397129,-2.17611252443469,
13.8579678548414));
#437248=CARTESIAN_POINT('Ctrl Pts',(-1.53538920061079,-2.17564695602143,
13.857615680862));
#437249=CARTESIAN_POINT('Ctrl Pts',(-1.53641214255887,-2.1752517607806,
13.8571944833187));
#437250=CARTESIAN_POINT('Ctrl Pts',(-1.53896499880822,-2.17426551063984,
13.8561433417727));
#437251=CARTESIAN_POINT('Ctrl Pts',(-1.54147563877766,-2.17366693988258,
13.8546163505474));
#437252=CARTESIAN_POINT('Ctrl Pts',(-1.54377573856338,-2.1733359446785,
13.8528973491086));
#437253=CARTESIAN_POINT('Ctrl Pts',(-1.54419593285942,-2.1732754767381,
13.8525833129072));
#437254=CARTESIAN_POINT('Ctrl Pts',(-1.54460914737315,-2.17322380547224,
13.8522628768812));
#437255=CARTESIAN_POINT('Ctrl Pts',(-1.54501444065091,-2.17318004119271,
13.851937733538));
#437256=CARTESIAN_POINT('Ctrl Pts',(-1.54748951046632,-2.17291277880968,
13.8499521282529));
#437257=CARTESIAN_POINT('Ctrl Pts',(-1.54991558086299,-2.17291789146262,
13.847639871647));
#437258=CARTESIAN_POINT('Ctrl Pts',(-1.55216531585744,-2.17311476993172,
13.8452109780794));
#437259=CARTESIAN_POINT('Ctrl Pts',(-1.55317751819863,-2.17320334963015,
13.8441181685877));
#437260=CARTESIAN_POINT('Ctrl Pts',(-1.55415433120731,-2.17333009894648,
13.8430021611332));
#437261=CARTESIAN_POINT('Ctrl Pts',(-1.55508642514008,-2.17348526674203,
13.8418824960098));
#437262=CARTESIAN_POINT('Ctrl Pts',(-1.55728292829453,-2.1738509236146,
13.8392439765549));
#437263=CARTESIAN_POINT('Ctrl Pts',(-1.55933672017995,-2.17438814335857,
13.8364981347964));
#437264=CARTESIAN_POINT('Ctrl Pts',(-1.5612618921482,-2.17506524004704,
13.8336931113419));
#437265=CARTESIAN_POINT('Ctrl Pts',(-1.56313688738556,-2.17572468922201,
13.8309611966328));
#437266=CARTESIAN_POINT('Ctrl Pts',(-1.56489157153951,-2.17651801226898,
13.8281701127186));
#437267=CARTESIAN_POINT('Ctrl Pts',(-1.56651332916587,-2.17744572633109,
13.8253580685121));
#437268=CARTESIAN_POINT('Ctrl Pts',(-1.56686492796953,-2.17764685574097,
13.8247484142933));
#437269=CARTESIAN_POINT('Ctrl Pts',(-1.56721012367397,-2.17785437874765,
13.8241378483365));
#437270=CARTESIAN_POINT('Ctrl Pts',(-1.56754848850674,-2.1780684097752,
13.8235269408515));
#437271=CARTESIAN_POINT('',(-1.52932415948195,-2.17905449156983,12.5969504640361));
#437272=CARTESIAN_POINT('Origin',(-1.54919158689835,-2.20714637929695,12.584524458991));
#437273=CARTESIAN_POINT('Origin',(-1.54919158689835,-2.20714637929695,12.584524458991));
#437274=CARTESIAN_POINT('Ctrl Pts',(-1.51560512620464,-2.21452734525963,
12.5893111709658));
#437275=CARTESIAN_POINT('Ctrl Pts',(-1.51316261792752,-2.20345969926439,
12.5770542771492));
#437276=CARTESIAN_POINT('Ctrl Pts',(-1.5282051163788,-2.1970155612151,12.5737548217797));
#437277=CARTESIAN_POINT('Ctrl Pts',(-1.52094607207655,-2.23872857263882,
12.5663937883685));
#437278=CARTESIAN_POINT('Ctrl Pts',(-1.51850044804093,-2.22764680832408,
12.5540940315304));
#437279=CARTESIAN_POINT('Ctrl Pts',(-1.53359082465374,-2.22118565293236,
12.5508374392248));
#437280=CARTESIAN_POINT('Ctrl Pts',(-1.52628162899956,-2.26290538127628,
12.5434499600945));
#437281=CARTESIAN_POINT('Ctrl Pts',(-1.52382805336934,-2.25178758619933,
12.5311293540532));
#437282=CARTESIAN_POINT('Ctrl Pts',(-1.53897011935321,-2.24533238656652,
12.5278936106989));
#437283=CARTESIAN_POINT('Ctrl Pts',(-1.5316122190974,-2.28705968392546,
12.5204817579905));
#437284=CARTESIAN_POINT('Ctrl Pts',(-1.52914649994453,-2.27588686336092,
12.5081597038247));
#437285=CARTESIAN_POINT('Ctrl Pts',(-1.54434348544273,-2.26945758061226,
12.5049254088044));
#437286=CARTESIAN_POINT('Ctrl Pts',(-1.52777976988047,-2.26969385076738,
12.5369868989719));
#437287=CARTESIAN_POINT('Ctrl Pts',(-1.527980512611,-2.27060346800934,12.5342545179733));
#437288=CARTESIAN_POINT('Ctrl Pts',(-1.52829390723081,-2.27144468196882,
12.5314872231885));
#437289=CARTESIAN_POINT('Ctrl Pts',(-1.52875468344491,-2.27215059017153,
12.5287124745063));
#437290=CARTESIAN_POINT('Ctrl Pts',(-1.52917023430568,-2.27278721322688,
12.5262100684184));
#437291=CARTESIAN_POINT('Ctrl Pts',(-1.52970605984781,-2.27331260767502,
12.5237004536639));
#437292=CARTESIAN_POINT('Ctrl Pts',(-1.53041777203167,-2.27368846182062,
12.5212220730815));
#437293=CARTESIAN_POINT('Ctrl Pts',(-1.53096264927644,-2.27397621068306,
12.5193246583486));
#437294=CARTESIAN_POINT('Ctrl Pts',(-1.53161742607129,-2.27417918844543,
12.517417831369));
#437295=CARTESIAN_POINT('Ctrl Pts',(-1.53242865116297,-2.27421202979317,
12.5155812248347));
#437296=CARTESIAN_POINT('Ctrl Pts',(-1.53277423741238,-2.27422602038384,
12.5147988205793));
#437297=CARTESIAN_POINT('Ctrl Pts',(-1.53314855560214,-2.27420942551876,
12.5140295443047));
#437298=CARTESIAN_POINT('Ctrl Pts',(-1.53355633159097,-2.27415744960347,
12.5132817086137));
#437299=CARTESIAN_POINT('Ctrl Pts',(-1.53417344538737,-2.27407879108683,
12.5121499604604));
#437300=CARTESIAN_POINT('Ctrl Pts',(-1.53487960852689,-2.27391030744599,
12.5110494206568));
#437301=CARTESIAN_POINT('Ctrl Pts',(-1.53567829388182,-2.27361491987427,
12.5100666561695));
#437302=CARTESIAN_POINT('Ctrl Pts',(-1.53613689717341,-2.27344530901081,
12.5095023550641));
#437303=CARTESIAN_POINT('Ctrl Pts',(-1.53663107763282,-2.27323128562668,
12.5089719619137));
#437304=CARTESIAN_POINT('Ctrl Pts',(-1.5371490340964,-2.27297100042007,
12.5085043804652));
#437305=CARTESIAN_POINT('Ctrl Pts',(-1.53790699591229,-2.27259010692472,
12.5078201359221));
#437306=CARTESIAN_POINT('Ctrl Pts',(-1.53873731398321,-2.27209801962174,
12.5072563000949));
#437307=CARTESIAN_POINT('Ctrl Pts',(-1.53957938870058,-2.27152081172439,
12.5068768744332));
#437308=CARTESIAN_POINT('Ctrl Pts',(-1.54018658254042,-2.27110460509528,
12.5066032824114));
#437309=CARTESIAN_POINT('Ctrl Pts',(-1.54081059057126,-2.27063687825392,
12.5064197834844));
#437310=CARTESIAN_POINT('Ctrl Pts',(-1.54141811688731,-2.27014581861132,
12.5063282718343));
#437311=CARTESIAN_POINT('Ctrl Pts',(-1.54230491722335,-2.26942902356136,
12.5061946931565));
#437312=CARTESIAN_POINT('Ctrl Pts',(-1.54317622205301,-2.26864801884064,
12.5062515701262));
#437313=CARTESIAN_POINT('Ctrl Pts',(-1.54398827872502,-2.26786279047885,
12.5064436508398));
#437314=CARTESIAN_POINT('',(-1.5282051163788,-2.19701556121511,12.5737548217797));
#437315=CARTESIAN_POINT('Origin',(-1.53708819353923,-2.20978626754489,12.5893111709658));
#437316=CARTESIAN_POINT('Ctrl Pts',(-1.54398827872502,-2.26786279047885,
12.5064436508398));
#437317=CARTESIAN_POINT('Ctrl Pts',(-1.54165242958721,-2.25737545542381,
12.5164271754438));
#437318=CARTESIAN_POINT('Ctrl Pts',(-1.53931545058102,-2.24688400861484,
12.5264061185523));
#437319=CARTESIAN_POINT('Ctrl Pts',(-1.53697730283729,-2.23638830503363,
12.536380305637));
#437320=CARTESIAN_POINT('Ctrl Pts',(-1.53405509238508,-2.22327080431518,
12.5488460165097));
#437321=CARTESIAN_POINT('Ctrl Pts',(-1.53113105548609,-2.21014665067863,
12.5613043021964));
#437322=CARTESIAN_POINT('Ctrl Pts',(-1.5282051163788,-2.19701556121511,
12.5737548217797));
#437323=CARTESIAN_POINT('Ctrl Pts',(-1.56754848850674,-2.1780684097752,
12.5893111709658));
#437324=CARTESIAN_POINT('Ctrl Pts',(-1.55796993226765,-2.17200954066172,
12.5770542771492));
#437325=CARTESIAN_POINT('Ctrl Pts',(-1.54679665878452,-2.18396619715615,
12.5737548217797));
#437326=CARTESIAN_POINT('Ctrl Pts',(-1.55861177884555,-2.17241553758958,
12.5928319619712));
#437327=CARTESIAN_POINT('Ctrl Pts',(-1.5504328844881,-2.17109678686975,
12.5821634970842));
#437328=CARTESIAN_POINT('Ctrl Pts',(-1.54354627755795,-2.18189901568095,
12.5773203894503));
#437329=CARTESIAN_POINT('Ctrl Pts',(-1.54201075355491,-2.17018169367406,
12.5969440695591));
#437330=CARTESIAN_POINT('Ctrl Pts',(-1.53871010216729,-2.1724760874871,
12.5878292599214));
#437331=CARTESIAN_POINT('Ctrl Pts',(-1.53762906054079,-2.18110485582971,
12.5813877129824));
#437332=CARTESIAN_POINT('Ctrl Pts',(-1.51693613904987,-2.18771563085215,
12.596957478804));
#437333=CARTESIAN_POINT('Ctrl Pts',(-1.52021244349124,-2.18543825904317,
12.5878468778671));
#437334=CARTESIAN_POINT('Ctrl Pts',(-1.5286579268001,-2.18738538349153,
12.5814011370086));
#437335=CARTESIAN_POINT('Ctrl Pts',(-1.51332297835558,-2.20418633444784,
12.5928371701607));
#437336=CARTESIAN_POINT('Ctrl Pts',(-1.51486750657731,-2.1960531002648,
12.5821692192951));
#437337=CARTESIAN_POINT('Ctrl Pts',(-1.52736284135469,-2.1932441092059,
12.5773318885715));
#437338=CARTESIAN_POINT('Ctrl Pts',(-1.51560512620458,-2.21452734525964,
12.5893111709658));
#437339=CARTESIAN_POINT('Ctrl Pts',(-1.51316261792746,-2.2034596992644,
12.5770542771492));
#437340=CARTESIAN_POINT('Ctrl Pts',(-1.52820511637874,-2.19701556121512,
12.5737548217797));
#437341=CARTESIAN_POINT('',(-1.54679665878452,-2.18396619715615,12.5737548217797));
#437342=CARTESIAN_POINT('Origin',(-1.55578780396799,-2.1966610507705,12.5893111709658));
#437343=CARTESIAN_POINT('Ctrl Pts',(-1.52820511637874,-2.19701556121512,
12.5737548217797));
#437344=CARTESIAN_POINT('Ctrl Pts',(-1.527957344847,-2.19604451595402,12.5746934679442));
#437345=CARTESIAN_POINT('Ctrl Pts',(-1.52786066643634,-2.19492469957481,
12.5756680099006));
#437346=CARTESIAN_POINT('Ctrl Pts',(-1.52792276274019,-2.1937838018068,
12.5765688348656));
#437347=CARTESIAN_POINT('Ctrl Pts',(-1.5279392020492,-2.19348176175288,
12.5768073183026));
#437348=CARTESIAN_POINT('Ctrl Pts',(-1.52796651697544,-2.19317829309718,
12.5770407398754));
#437349=CARTESIAN_POINT('Ctrl Pts',(-1.52800428799108,-2.19287572989175,
12.5772674179684));
#437350=CARTESIAN_POINT('Ctrl Pts',(-1.52815929002556,-2.19163409231321,
12.5781976435658));
#437351=CARTESIAN_POINT('Ctrl Pts',(-1.52851037564396,-2.19033857837221,
12.5790594849312));
#437352=CARTESIAN_POINT('Ctrl Pts',(-1.52908044701501,-2.18908929403484,
12.5797571720116));
#437353=CARTESIAN_POINT('Ctrl Pts',(-1.52945186901119,-2.18827534036879,
12.580211740231));
#437354=CARTESIAN_POINT('Ctrl Pts',(-1.52995020827331,-2.18745181443711,
12.5806009430798));
#437355=CARTESIAN_POINT('Ctrl Pts',(-1.53055554142144,-2.18668586114604,
12.5808812374708));
#437356=CARTESIAN_POINT('Ctrl Pts',(-1.53107572341285,-2.18602765316665,
12.5811221033394));
#437357=CARTESIAN_POINT('Ctrl Pts',(-1.53168565420794,-2.18539855525862,
12.581287365893));
#437358=CARTESIAN_POINT('Ctrl Pts',(-1.53235689466196,-2.18483987866494,
12.581359338449));
#437359=CARTESIAN_POINT('Ctrl Pts',(-1.53245018322449,-2.18476223415464,
12.5813693411482));
#437360=CARTESIAN_POINT('Ctrl Pts',(-1.532544635223,-2.18468589369265,12.5813775999465));
#437361=CARTESIAN_POINT('Ctrl Pts',(-1.53264015405337,-2.18461091027627,
12.5813841266931));
#437362=CARTESIAN_POINT('Ctrl Pts',(-1.53280221330185,-2.18448369184134,
12.5813952001081));
#437363=CARTESIAN_POINT('Ctrl Pts',(-1.53296880481113,-2.18436000657486,
12.5814007534795));
#437364=CARTESIAN_POINT('Ctrl Pts',(-1.5331399735842,-2.18424006668586,
12.5814005856065));
#437365=CARTESIAN_POINT('Ctrl Pts',(-1.53392351730465,-2.18369102876748,
12.5813998171494));
#437366=CARTESIAN_POINT('Ctrl Pts',(-1.5347486447913,-2.18325813128369,
12.58127954464));
#437367=CARTESIAN_POINT('Ctrl Pts',(-1.53559692470179,-2.18291762974099,
12.5810700125799));
#437368=CARTESIAN_POINT('Ctrl Pts',(-1.53662155024926,-2.18250634264661,
12.5808169217085));
#437369=CARTESIAN_POINT('Ctrl Pts',(-1.53768628192706,-2.18224535449793,
12.5804173076348));
#437370=CARTESIAN_POINT('Ctrl Pts',(-1.53869160846448,-2.18213224428254,
12.5799304713245));
#437371=CARTESIAN_POINT('Ctrl Pts',(-1.53993752475485,-2.18199206509227,
12.5793271277669));
#437372=CARTESIAN_POINT('Ctrl Pts',(-1.54116588687115,-2.18203831787197,
12.5785808224116));
#437373=CARTESIAN_POINT('Ctrl Pts',(-1.54232611040979,-2.18223735857984,
12.5777485681082));
#437374=CARTESIAN_POINT('Ctrl Pts',(-1.54405497059434,-2.18253395104111,
12.576508418016));
#437375=CARTESIAN_POINT('Ctrl Pts',(-1.54561913869913,-2.18316052717434,
12.5750928681475));
#437376=CARTESIAN_POINT('Ctrl Pts',(-1.54679665878452,-2.18396619715615,
12.5737548217797));
#437377=CARTESIAN_POINT('Ctrl Pts',(-1.54679665878452,-2.18396619715615,
12.5737548217797));
#437378=CARTESIAN_POINT('Ctrl Pts',(-1.55796993226765,-2.17200954066172,
12.5770542771492));
#437379=CARTESIAN_POINT('Ctrl Pts',(-1.56754848850674,-2.1780684097752,
12.5893111709658));
#437380=CARTESIAN_POINT('Ctrl Pts',(-1.56769411036162,-2.19724443016183,
12.5508408821982));
#437381=CARTESIAN_POINT('Ctrl Pts',(-1.57889965365159,-2.18524853402163,
12.55409748406));
#437382=CARTESIAN_POINT('Ctrl Pts',(-1.58849042967524,-2.19131513270037,
12.5663972313419));
#437383=CARTESIAN_POINT('Ctrl Pts',(-1.58857178032965,-2.21050869646258,
12.52790050457));
#437384=CARTESIAN_POINT('Ctrl Pts',(-1.59978928963743,-2.19846217155821,
12.5311362602938));
#437385=CARTESIAN_POINT('Ctrl Pts',(-1.60941124386633,-2.20454849185883,
12.5434568539655));
#437386=CARTESIAN_POINT('Ctrl Pts',(-1.60943121340021,-2.22376006976241,
12.5049357605811));
#437387=CARTESIAN_POINT('Ctrl Pts',(-1.62064301892296,-2.21165309648626,
12.5081700652078));
#437388=CARTESIAN_POINT('Ctrl Pts',(-1.63031258574915,-2.21776953390351,
12.5204921097672));
#437389=CARTESIAN_POINT('Ctrl Pts',(-1.60806150210938,-2.22288993130809,
12.5064436508395));
#437390=CARTESIAN_POINT('Ctrl Pts',(-1.60915733426334,-2.22235327529076,
12.5062361689309));
#437391=CARTESIAN_POINT('Ctrl Pts',(-1.610274025824,-2.22174846823163,12.5061871075061));
#437392=CARTESIAN_POINT('Ctrl Pts',(-1.61132029812014,-2.22110323112525,
12.5063648335164));
#437393=CARTESIAN_POINT('Ctrl Pts',(-1.6117955795338,-2.22081012463166,
12.5064455676329));
#437394=CARTESIAN_POINT('Ctrl Pts',(-1.61226284321535,-2.2205043995009,
12.506574497099));
#437395=CARTESIAN_POINT('Ctrl Pts',(-1.61270147889601,-2.22019828487513,
12.5067492519495));
#437396=CARTESIAN_POINT('Ctrl Pts',(-1.61358293432294,-2.21958313565211,
12.5071004286051));
#437397=CARTESIAN_POINT('Ctrl Pts',(-1.61438072828498,-2.21894313395972,
12.5076537929613));
#437398=CARTESIAN_POINT('Ctrl Pts',(-1.6150409007624,-2.21833369311237,
12.5083435010505));
#437399=CARTESIAN_POINT('Ctrl Pts',(-1.61508246256507,-2.21829532516899,
12.5083869222964));
#437400=CARTESIAN_POINT('Ctrl Pts',(-1.61512347534805,-2.21825706539857,
12.5084308732337));
#437401=CARTESIAN_POINT('Ctrl Pts',(-1.61516392457745,-2.2182189222485,
12.5084753333615));
#437402=CARTESIAN_POINT('Ctrl Pts',(-1.61548838078535,-2.21791296384052,
12.5088319622689));
#437403=CARTESIAN_POINT('Ctrl Pts',(-1.61578404914335,-2.21760923609894,
12.509227847131));
#437404=CARTESIAN_POINT('Ctrl Pts',(-1.61604414426715,-2.21731872357072,
12.5096423454524));
#437405=CARTESIAN_POINT('Ctrl Pts',(-1.61685916727184,-2.21640838588275,
12.5109411997424));
#437406=CARTESIAN_POINT('Ctrl Pts',(-1.61738222279126,-2.21557826841318,
12.5124831113042));
#437407=CARTESIAN_POINT('Ctrl Pts',(-1.61770690066132,-2.21484239970466,
12.5140723025008));
#437408=CARTESIAN_POINT('Ctrl Pts',(-1.61773732333336,-2.2147734480007,
12.5142212114565));
#437409=CARTESIAN_POINT('Ctrl Pts',(-1.61776603322498,-2.21470531760595,
12.5143705582413));
#437410=CARTESIAN_POINT('Ctrl Pts',(-1.61779312419301,-2.21463801804078,
12.5145201959299));
#437411=CARTESIAN_POINT('Ctrl Pts',(-1.6181411480116,-2.21377345492755,
12.5164425148273));
#437412=CARTESIAN_POINT('Ctrl Pts',(-1.61824388319819,-2.21302039233999,
12.518463520594));
#437413=CARTESIAN_POINT('Ctrl Pts',(-1.61818448453867,-2.21234385514217,
12.5205025929157));
#437414=CARTESIAN_POINT('Ctrl Pts',(-1.61815003096181,-2.211951436752,12.5216853356836));
#437415=CARTESIAN_POINT('Ctrl Pts',(-1.61806157204364,-2.21158543159583,
12.5228750347131));
#437416=CARTESIAN_POINT('Ctrl Pts',(-1.61793731198208,-2.21124459837319,
12.5240609649613));
#437417=CARTESIAN_POINT('Ctrl Pts',(-1.6176323223273,-2.2104080415133,12.5269717671327));
#437418=CARTESIAN_POINT('Ctrl Pts',(-1.6170933050645,-2.20970314479846,
12.5299036066169));
#437419=CARTESIAN_POINT('Ctrl Pts',(-1.61639666614827,-2.20908902237862,
12.532813300402));
#437420=CARTESIAN_POINT('Ctrl Pts',(-1.61606223890442,-2.20879420785782,
12.5342101228452));
#437421=CARTESIAN_POINT('Ctrl Pts',(-1.61569155752594,-2.20852107378394,
12.5356023438238));
#437422=CARTESIAN_POINT('Ctrl Pts',(-1.61529264979877,-2.20826874654634,
12.5369868989719));
#437423=CARTESIAN_POINT('Origin',(-12.389845183083,-9.01739099410739,-1.24054046559061));
#437424=CARTESIAN_POINT('Ctrl Pts',(-1.52777072430559,-2.26965304710934,
12.5369868989719));
#437425=CARTESIAN_POINT('Ctrl Pts',(-1.53110477095469,-2.28462526927665,
12.5369868989719));
#437426=CARTESIAN_POINT('Ctrl Pts',(-1.5182089836472,-2.29293080799521,
12.5369868989719));
#437427=CARTESIAN_POINT('Ctrl Pts',(-1.52889769783785,-2.27471425815371,
12.5218025310016));
#437428=CARTESIAN_POINT('Ctrl Pts',(-1.52812584650303,-2.28650663319956,
12.5216901060418));
#437429=CARTESIAN_POINT('Ctrl Pts',(-1.51824830321041,-2.29290550382566,
12.5161920673678));
#437430=CARTESIAN_POINT('Ctrl Pts',(-1.53444103555654,-2.27708226958361,
12.5042015548894));
#437431=CARTESIAN_POINT('Ctrl Pts',(-1.5328355589886,-2.28331121732834,
12.4980677368513));
#437432=CARTESIAN_POINT('Ctrl Pts',(-1.52718938272283,-2.28709426812096,
12.4907278922777));
#437433=CARTESIAN_POINT('Ctrl Pts',(-1.54397702274574,-2.26784625729298,
12.506463626192));
#437434=CARTESIAN_POINT('Ctrl Pts',(-1.54765907319314,-2.27325457892166,
12.4999376786891));
#437435=CARTESIAN_POINT('Ctrl Pts',(-1.54761410230062,-2.27318852413666,
12.4906970594712));
#437436=CARTESIAN_POINT('Origin',(-1.50629670254587,-2.27443492848211,12.5369868989719));
#437437=CARTESIAN_POINT('Origin',(-1.50629670254587,-2.27443492848211,14.));
#437438=CARTESIAN_POINT('Origin',(-1.50629670254587,-2.27443492848211,13.7435492065112));
#437439=CARTESIAN_POINT('Ctrl Pts',(-1.52244385349537,-2.24551553930385,
13.793642941384));
#437440=CARTESIAN_POINT('Ctrl Pts',(-1.52480052107501,-2.25606790097908,
13.8071662555867));
#437441=CARTESIAN_POINT('Ctrl Pts',(-1.50890636836131,-2.26218307008128,
13.8103758687955));
#437442=CARTESIAN_POINT('Ctrl Pts',(-1.52602576696028,-2.26174611542281,
13.7804579775006));
#437443=CARTESIAN_POINT('Ctrl Pts',(-1.52892378475354,-2.27476898625067,
13.7901904343352));
#437444=CARTESIAN_POINT('Ctrl Pts',(-1.5153276344955,-2.28273143702447,
13.7927914348263));
#437445=CARTESIAN_POINT('Ctrl Pts',(-1.5281345741825,-2.27130166641751,
13.7597120340895));
#437446=CARTESIAN_POINT('Ctrl Pts',(-1.53148280333467,-2.28637404020259,
13.7635825532445));
#437447=CARTESIAN_POINT('Ctrl Pts',(-1.51908984895029,-2.29485641002304,
13.7651073818884));
#437448=CARTESIAN_POINT('Ctrl Pts',(-1.5277216214414,-2.26943047073569,
13.7381884353898));
#437449=CARTESIAN_POINT('Ctrl Pts',(-1.53099235649522,-2.28414985261245,
13.7368803041982));
#437450=CARTESIAN_POINT('Ctrl Pts',(-1.5183526235363,-2.29248212648255,
13.7363986145813));
#437451=CARTESIAN_POINT('Origin',(-1.50182995687668,-2.25419493163929,13.7902182540695));
#437452=CARTESIAN_POINT('Ctrl Pts',(-1.51560427719888,-2.21452350171337,
13.8235227101244));
#437453=CARTESIAN_POINT('Ctrl Pts',(-1.51808626611861,-2.22574947246525,
13.8358800583119));
#437454=CARTESIAN_POINT('Ctrl Pts',(-1.50280989203645,-2.23217274608225,
13.8390832900376));
#437455=CARTESIAN_POINT('Ctrl Pts',(-1.51817471268307,-2.22617081946112,
13.8124254819053));
#437456=CARTESIAN_POINT('Ctrl Pts',(-1.5206615213185,-2.2374185909491,13.8247886449158));
#437457=CARTESIAN_POINT('Ctrl Pts',(-1.5053592385034,-2.2438342687582,13.8279860620657));
#437458=CARTESIAN_POINT('Ctrl Pts',(-1.52074399618169,-2.2378129172599,
13.8013225099955));
#437459=CARTESIAN_POINT('Ctrl Pts',(-1.52323445311582,-2.24907718190935,
13.8136962257787));
#437460=CARTESIAN_POINT('Ctrl Pts',(-1.50790766955075,-2.25549033483369,
13.8168830918626));
#437461=CARTESIAN_POINT('Ctrl Pts',(-1.52331217251677,-2.24944999821001,
13.7902140179785));
#437462=CARTESIAN_POINT('Ctrl Pts',(-1.5258051828905,-2.26072579533578,
13.802602731458));
#437463=CARTESIAN_POINT('Ctrl Pts',(-1.51045522294536,-2.26714115831884,
13.8057746032558));
#437464=CARTESIAN_POINT('Origin',(-1.49412205887004,-2.21926842297437,13.8235269408515));
#437465=CARTESIAN_POINT('Ctrl Pts',(-1.56754848850674,-2.1780684097752,
13.8235269408515));
#437466=CARTESIAN_POINT('Ctrl Pts',(-1.57752722778538,-2.18438041272197,
13.8362179249168));
#437467=CARTESIAN_POINT('Ctrl Pts',(-1.58887104043234,-2.1716140146909,
13.8391868794938));
#437468=CARTESIAN_POINT('Ctrl Pts',(-1.55841837641544,-2.17229320182404,
13.8400110824519));
#437469=CARTESIAN_POINT('Ctrl Pts',(-1.56824767002107,-2.17446272943999,
13.8494522556837));
#437470=CARTESIAN_POINT('Ctrl Pts',(-1.57378539006221,-2.1622046078799,
13.85569149686));
#437471=CARTESIAN_POINT('Ctrl Pts',(-1.54229188985012,-2.16998362240276,
13.8586819406588));
#437472=CARTESIAN_POINT('Ctrl Pts',(-1.5458634977564,-2.16749371063752,
13.868010383617));
#437473=CARTESIAN_POINT('Ctrl Pts',(-1.54699440355332,-2.15851518520896,
13.8744918421245));
#437474=CARTESIAN_POINT('Ctrl Pts',(-1.51665063179312,-2.1879167588602,
13.8587686893867));
#437475=CARTESIAN_POINT('Ctrl Pts',(-1.5131107789619,-2.19038446424236,
13.8680909899357));
#437476=CARTESIAN_POINT('Ctrl Pts',(-1.50431071344441,-2.18837069951095,
13.8745789365163));
#437477=CARTESIAN_POINT('Ctrl Pts',(-1.51327318161156,-2.20396069236267,
13.8400379222776));
#437478=CARTESIAN_POINT('Ctrl Pts',(-1.51196590914601,-2.21393873187997,
13.8494748685453));
#437479=CARTESIAN_POINT('Ctrl Pts',(-1.49856162722656,-2.21498100415174,
13.8557104837033));
#437480=CARTESIAN_POINT('Ctrl Pts',(-1.51560512619815,-2.21452734526091,
13.8235269408542));
#437481=CARTESIAN_POINT('Ctrl Pts',(-1.51814968016583,-2.22605738706032,
13.8362179249195));
#437482=CARTESIAN_POINT('Ctrl Pts',(-1.50228768333862,-2.23238668881565,
13.8391868794965));
#437483=CARTESIAN_POINT('Origin',(-1.57930917304549,-2.1594757687799,13.8235269408515));
#437484=CARTESIAN_POINT('Ctrl Pts',(-1.59777249931641,-2.19718645976062,
13.7902140241682));
#437485=CARTESIAN_POINT('Ctrl Pts',(-1.60752964898108,-2.20336356473089,
13.8026027327198));
#437486=CARTESIAN_POINT('Ctrl Pts',(-1.6187803589046,-2.19110797586335,
13.8057746032556));
#437487=CARTESIAN_POINT('Ctrl Pts',(-1.58770112240133,-2.19081585932922,
13.8013225161808));
#437488=CARTESIAN_POINT('Ctrl Pts',(-1.59744829405439,-2.19698664312471,
13.8136962270464));
#437489=CARTESIAN_POINT('Ctrl Pts',(-1.60868904809625,-2.18475209965617,
13.8168830918628));
#437490=CARTESIAN_POINT('Ctrl Pts',(-1.57762540362503,-2.18444251247466,
13.8124254880875));
#437491=CARTESIAN_POINT('Ctrl Pts',(-1.58735830404812,-2.19060425933693,
13.8247886461867));
#437492=CARTESIAN_POINT('Ctrl Pts',(-1.59859310511831,-2.178393616147,13.8279860620656));
#437493=CARTESIAN_POINT('Ctrl Pts',(-1.56754516721199,-2.17806630801099,
13.8235227163065));
#437494=CARTESIAN_POINT('Ctrl Pts',(-1.57725920297056,-2.18421611227764,
13.8358800595847));
#437495=CARTESIAN_POINT('Ctrl Pts',(-1.58849234153707,-2.17203241707693,
13.8390832900376));
#437496=CARTESIAN_POINT('Origin',(-1.60953651566431,-2.17859592718422,13.7902182540695));
#437497=CARTESIAN_POINT('Ctrl Pts',(-1.61506460053222,-2.20812446245339,
13.7382347919292));
#437498=CARTESIAN_POINT('Ctrl Pts',(-1.62780488942199,-2.21621166887702,
13.7369371795943));
#437499=CARTESIAN_POINT('Ctrl Pts',(-1.63994162634958,-2.20714285452394,
13.7364597369711));
#437500=CARTESIAN_POINT('Ctrl Pts',(-1.61666319441731,-2.20913564570813,
13.7595490285573));
#437501=CARTESIAN_POINT('Ctrl Pts',(-1.62970799450626,-2.21741495709601,
13.7633824266926));
#437502=CARTESIAN_POINT('Ctrl Pts',(-1.64189947137254,-2.20862510202744,
13.7648920890506));
#437503=CARTESIAN_POINT('Ctrl Pts',(-1.60851045317711,-2.20397866651274,
13.7803806590111));
#437504=CARTESIAN_POINT('Ctrl Pts',(-1.61979084550826,-2.21114453246598,
13.7901039518744));
#437505=CARTESIAN_POINT('Ctrl Pts',(-1.63191592259437,-2.20107140251142,
13.7926933640892));
#437506=CARTESIAN_POINT('Ctrl Pts',(-1.59433916902201,-2.19501468542339,
13.7936647693663));
#437507=CARTESIAN_POINT('Ctrl Pts',(-1.60346343979419,-2.20082166525979,
13.8072068914933));
#437508=CARTESIAN_POINT('Ctrl Pts',(-1.61462082768211,-2.18793147653482,
13.8104111085397));
#437509=CARTESIAN_POINT('Origin',(-1.62705333433752,-2.18967610555104,13.7435492065112));
#437510=CARTESIAN_POINT('Origin',(-1.62705333433752,-2.18967610555104,14.));
#437511=CARTESIAN_POINT('Origin',(-1.62705333433752,-2.18967610555104,12.5369868989719));
#437512=CARTESIAN_POINT('Ctrl Pts',(-1.608050727263,-2.22287503680982,12.506462012331));
#437513=CARTESIAN_POINT('Ctrl Pts',(-1.61188316452582,-2.22817277336579,
12.4999388158272));
#437514=CARTESIAN_POINT('Ctrl Pts',(-1.61183782176707,-2.22811009419478,
12.4907030323752));
#437515=CARTESIAN_POINT('Ctrl Pts',(-1.61997682353992,-2.2170443583975,
12.5042014951932));
#437516=CARTESIAN_POINT('Ctrl Pts',(-1.62637772216243,-2.21765230078023,
12.4980716682127));
#437517=CARTESIAN_POINT('Ctrl Pts',(-1.63185168697956,-2.21363219202466,
12.4907355092744));
#437518=CARTESIAN_POINT('Ctrl Pts',(-1.6196363054269,-2.21102690472837,
12.5218047446509));
#437519=CARTESIAN_POINT('Ctrl Pts',(-1.63098371355879,-2.21430641682998,
12.5216906929434));
#437520=CARTESIAN_POINT('Ctrl Pts',(-1.64035639307753,-2.2071984190128,
12.5161988840775));
#437521=CARTESIAN_POINT('Ctrl Pts',(-1.61526020150225,-2.20824818184664,
12.5369868989719));
#437522=CARTESIAN_POINT('Ctrl Pts',(-1.62820146919188,-2.21646579233303,
12.5369868989719));
#437523=CARTESIAN_POINT('Ctrl Pts',(-1.64039220568286,-2.20717109086776,
12.5369868989719));
#437524=CARTESIAN_POINT('Origin',(-2.95976792804887E-31,-9.36866969595883E-31,
12.5));
#437525=CARTESIAN_POINT('Origin',(-1.38479980462761,-2.29859082104314,12.5));
#437526=CARTESIAN_POINT('',(-1.38479980462761,-2.29859082104314,12.5893111709658));
#437527=CARTESIAN_POINT('',(-1.38479980462761,-2.29859082104314,13.8235269408515));
#437528=CARTESIAN_POINT('',(-1.38479980462761,-2.29859082104314,12.5));
#437529=CARTESIAN_POINT('',(-1.41336809784461,-2.32011116773805,13.7902182540695));
#437530=CARTESIAN_POINT('',(-1.38479980462761,-2.29859082104314,13.8235269408515));
#437531=CARTESIAN_POINT('',(-1.42992349334847,-2.33258226106549,13.7435492065112));
#437532=CARTESIAN_POINT('Origin',(-1.37545626496778,-2.29155278905242,13.7445212918694));
#437533=CARTESIAN_POINT('',(-1.42992349334847,-2.33258226106549,12.5369868989719));
#437534=CARTESIAN_POINT('',(-1.42992349334847,-2.33258226106549,12.5));
#437535=CARTESIAN_POINT('Ctrl Pts',(-1.42992349334847,-2.33258226106549,
12.5369868989719));
#437536=CARTESIAN_POINT('Ctrl Pts',(-1.41489323393287,-2.32126004482102,
12.5544431401645));
#437537=CARTESIAN_POINT('Ctrl Pts',(-1.39985222447626,-2.30992973062657,
12.5718848856037));
#437538=CARTESIAN_POINT('Ctrl Pts',(-1.38479980462761,-2.29859082104314,
12.5893111709658));
#437539=CARTESIAN_POINT('Origin',(-1.36723544715477,-2.6031699017816,12.5));
#437540=CARTESIAN_POINT('',(-1.33769508908193,-2.38666986617617,13.7435492065112));
#437541=CARTESIAN_POINT('',(-1.33489295378212,-2.36613313501387,13.7902182540695));
#437542=CARTESIAN_POINT('Origin',(-1.3275294265206,-2.31216615498027,13.7418732680447));
#437543=CARTESIAN_POINT('',(-1.33005753786832,-2.33069457618112,13.8235269408515));
#437544=CARTESIAN_POINT('',(-1.33489295378212,-2.36613313501387,13.7902182540695));
#437545=CARTESIAN_POINT('',(-1.33005753786832,-2.33069457618112,12.5893111709658));
#437546=CARTESIAN_POINT('',(-1.33005753786832,-2.33069457618112,12.5));
#437547=CARTESIAN_POINT('',(-1.33769508908193,-2.38666986617617,12.5369868989719));
#437548=CARTESIAN_POINT('Ctrl Pts',(-1.33005753786832,-2.33069457618112,
12.5893111709658));
#437549=CARTESIAN_POINT('Ctrl Pts',(-1.33260528231789,-2.34936688755548,
12.5718848856037));
#437550=CARTESIAN_POINT('Ctrl Pts',(-1.33515109546584,-2.36802504450183,
12.5544431401645));
#437551=CARTESIAN_POINT('Ctrl Pts',(-1.33769508908193,-2.38666986617617,
12.5369868989719));
#437552=CARTESIAN_POINT('',(-1.33769508908193,-2.38666986617617,12.5));
#437553=CARTESIAN_POINT('Origin',(-1.36411695356838,-2.32604733752032,12.5));
#437554=CARTESIAN_POINT('',(-1.34770274241472,-2.29584528718626,13.8587068136939));
#437555=CARTESIAN_POINT('Ctrl Pts',(-1.33005753786175,-2.33069457618187,
13.8235269408542));
#437556=CARTESIAN_POINT('Ctrl Pts',(-1.32982064044995,-2.3289583650647,
13.8262006681044));
#437557=CARTESIAN_POINT('Ctrl Pts',(-1.32975035485606,-2.327158118424,13.8288634856214));
#437558=CARTESIAN_POINT('Ctrl Pts',(-1.32983483319984,-2.32529995457508,
13.8314912288862));
#437559=CARTESIAN_POINT('Ctrl Pts',(-1.32992192165874,-2.32338437930756,
13.8342001611531));
#437560=CARTESIAN_POINT('Ctrl Pts',(-1.33017308559617,-2.32140510232591,
13.8368750301949));
#437561=CARTESIAN_POINT('Ctrl Pts',(-1.33061688902365,-2.31935101672995,
13.8394886372969));
#437562=CARTESIAN_POINT('Ctrl Pts',(-1.33065116503887,-2.31919237471686,
13.8396904925131));
#437563=CARTESIAN_POINT('Ctrl Pts',(-1.33068661225026,-2.31903328735934,
13.8398919674349));
#437564=CARTESIAN_POINT('Ctrl Pts',(-1.3307232551677,-2.31887375099653,
13.8400930404591));
#437565=CARTESIAN_POINT('Ctrl Pts',(-1.3312941764737,-2.31638806713311,
13.8432258934518));
#437566=CARTESIAN_POINT('Ctrl Pts',(-1.33215135408679,-2.31380581551435,
13.8462331177034));
#437567=CARTESIAN_POINT('Ctrl Pts',(-1.33335838538214,-2.31124160658065,
13.8489036603661));
#437568=CARTESIAN_POINT('Ctrl Pts',(-1.33375334006891,-2.31040256757635,
13.8497774930041));
#437569=CARTESIAN_POINT('Ctrl Pts',(-1.33418578751209,-2.30956570785966,
13.85061494757));
#437570=CARTESIAN_POINT('Ctrl Pts',(-1.3346580433432,-2.30873575114057,
13.8514076489583));
#437571=CARTESIAN_POINT('Ctrl Pts',(-1.33565693253548,-2.30698027298202,
13.8530843267192));
#437572=CARTESIAN_POINT('Ctrl Pts',(-1.33693460598547,-2.30508470640123,
13.8546805203176));
#437573=CARTESIAN_POINT('Ctrl Pts',(-1.33853005156653,-2.30323533184876,
13.8559412814273));
#437574=CARTESIAN_POINT('Ctrl Pts',(-1.33874357392681,-2.30298782555699,
13.8561100121513));
#437575=CARTESIAN_POINT('Ctrl Pts',(-1.33896271112119,-2.30274114608263,
13.8562727473908));
#437576=CARTESIAN_POINT('Ctrl Pts',(-1.3391874814223,-2.30249572994325,
13.8564289040185));
#437577=CARTESIAN_POINT('Ctrl Pts',(-1.34020681217352,-2.30138277055099,
13.8571370725437));
#437578=CARTESIAN_POINT('Ctrl Pts',(-1.34136158981007,-2.30027776785877,
13.8577210840553));
#437579=CARTESIAN_POINT('Ctrl Pts',(-1.34262721810076,-2.29924487767196,
13.8581177131616));
#437580=CARTESIAN_POINT('Ctrl Pts',(-1.34298366258902,-2.29895398024436,
13.8582294175695));
#437581=CARTESIAN_POINT('Ctrl Pts',(-1.34334876244077,-2.2986686896975,
13.8583265086086));
#437582=CARTESIAN_POINT('Ctrl Pts',(-1.34372164622057,-2.29839013992448,
13.8584082369006));
#437583=CARTESIAN_POINT('Ctrl Pts',(-1.3442573802194,-2.29798993859672,
13.8585256585398));
#437584=CARTESIAN_POINT('Ctrl Pts',(-1.3448160357368,-2.29759893516493,
13.8586122832068));
#437585=CARTESIAN_POINT('Ctrl Pts',(-1.34538355333422,-2.29722793373199,
13.8586682984299));
#437586=CARTESIAN_POINT('Ctrl Pts',(-1.34583751115595,-2.29693116936183,
13.8587131050557));
#437587=CARTESIAN_POINT('Ctrl Pts',(-1.34630202496706,-2.29664372906882,
13.8587357943552));
#437588=CARTESIAN_POINT('Ctrl Pts',(-1.34677741645704,-2.29636600935861,
13.8587355499465));
#437589=CARTESIAN_POINT('Ctrl Pts',(-1.34708467331092,-2.29618651248872,
13.8587353919793));
#437590=CARTESIAN_POINT('Ctrl Pts',(-1.34739313200497,-2.29601298390489,
13.8587257282814));
#437591=CARTESIAN_POINT('Ctrl Pts',(-1.34770274241472,-2.29584528718626,
13.8587068136939));
#437592=CARTESIAN_POINT('Ctrl Pts',(-1.34770274241472,-2.29584528718626,
13.8587068136939));
#437593=CARTESIAN_POINT('Ctrl Pts',(-1.34872103417355,-2.29529374182091,
13.8586446046466));
#437594=CARTESIAN_POINT('Ctrl Pts',(-1.34975176954439,-2.29480520254764,
13.858482427929));
#437595=CARTESIAN_POINT('Ctrl Pts',(-1.35079331499402,-2.29437550793324,
13.8582284286032));
#437596=CARTESIAN_POINT('Ctrl Pts',(-1.35186181946785,-2.29393469124296,
13.8579678548414));
#437597=CARTESIAN_POINT('Ctrl Pts',(-1.3529448950698,-2.29355614396119,
13.857615680862));
#437598=CARTESIAN_POINT('Ctrl Pts',(-1.35399664534387,-2.29324564296522,
13.8571944833187));
#437599=CARTESIAN_POINT('Ctrl Pts',(-1.356621395717,-2.29247075597434,13.8561433417727));
#437600=CARTESIAN_POINT('Ctrl Pts',(-1.35917247081262,-2.29207881737704,
13.8546163505475));
#437601=CARTESIAN_POINT('Ctrl Pts',(-1.36149189638798,-2.29193640301783,
13.8528973491086));
#437602=CARTESIAN_POINT('Ctrl Pts',(-1.36191562122068,-2.29191038601552,
13.8525833129073));
#437603=CARTESIAN_POINT('Ctrl Pts',(-1.36233167248507,-2.2918925675005,
13.8522628768812));
#437604=CARTESIAN_POINT('Ctrl Pts',(-1.36273918437797,-2.2918819840077,
13.851937733538));
#437605=CARTESIAN_POINT('Ctrl Pts',(-1.36522780296811,-2.29181735208559,
13.8499521282529));
#437606=CARTESIAN_POINT('Ctrl Pts',(-1.367645384087,-2.29202019498647,13.847639871647));
#437607=CARTESIAN_POINT('Ctrl Pts',(-1.36987158585087,-2.29239979264626,
13.8452109780794));
#437608=CARTESIAN_POINT('Ctrl Pts',(-1.37087320010452,-2.29257058149069,
13.8441181685877));
#437609=CARTESIAN_POINT('Ctrl Pts',(-1.37183643160253,-2.29277652838762,
13.8430021611332));
#437610=CARTESIAN_POINT('Ctrl Pts',(-1.37275277645379,-2.29300715418379,
13.8418824960098));
#437611=CARTESIAN_POINT('Ctrl Pts',(-1.37491216649548,-2.29355062976171,
13.8392439765549));
#437612=CARTESIAN_POINT('Ctrl Pts',(-1.37691533616139,-2.29425346505643,
13.8364981347964));
#437613=CARTESIAN_POINT('Ctrl Pts',(-1.37877891261276,-2.29508522814937,
13.8336931113419));
#437614=CARTESIAN_POINT('Ctrl Pts',(-1.38059391772835,-2.29589531258005,
13.8309611966328));
#437615=CARTESIAN_POINT('Ctrl Pts',(-1.38227810012235,-2.29682901895827,
13.8281701127186));
#437616=CARTESIAN_POINT('Ctrl Pts',(-1.38381884417546,-2.29788583443058,
13.8253580685121));
#437617=CARTESIAN_POINT('Ctrl Pts',(-1.384152879149,-2.29811495316553,13.8247484142933));
#437618=CARTESIAN_POINT('Ctrl Pts',(-1.38448001119162,-2.29834992231107,
13.8241378483365));
#437619=CARTESIAN_POINT('Ctrl Pts',(-1.38479980462761,-2.29859082104314,
13.8235269408515));
#437620=CARTESIAN_POINT('',(-1.34662228908371,-2.29645798405909,12.5969504640361));
#437621=CARTESIAN_POINT('Origin',(-1.36413385963227,-2.32607577812183,12.584524458991));
#437622=CARTESIAN_POINT('Origin',(-1.36413385963227,-2.32607577812183,12.584524458991));
#437623=CARTESIAN_POINT('Ctrl Pts',(-1.33005753786832,-2.33069457618112,
12.5893111709658));
#437624=CARTESIAN_POINT('Ctrl Pts',(-1.32852527273163,-2.31946466976519,
12.5770542771492));
#437625=CARTESIAN_POINT('Ctrl Pts',(-1.3440429755857,-2.31426807732518,
12.5737548217797));
#437626=CARTESIAN_POINT('Ctrl Pts',(-1.3334080874788,-2.35525061264415,
12.5663937883685));
#437627=CARTESIAN_POINT('Ctrl Pts',(-1.33187386772512,-2.344006380923,12.5540940315304));
#437628=CARTESIAN_POINT('Ctrl Pts',(-1.34744067650152,-2.33879673027902,
12.5508374392248));
#437629=CARTESIAN_POINT('Ctrl Pts',(-1.33675525642581,-2.37978187236747,
12.5434499600945));
#437630=CARTESIAN_POINT('Ctrl Pts',(-1.33521604837739,-2.3685010816448,
12.5311293540533));
#437631=CARTESIAN_POINT('Ctrl Pts',(-1.35083388908308,-2.36330158010592,
12.5278936106989));
#437632=CARTESIAN_POINT('Ctrl Pts',(-1.34009930952133,-2.4042902961469,
12.5204817579905));
#437633=CARTESIAN_POINT('Ctrl Pts',(-1.33855248344495,-2.39295367321952,
12.5081597038247));
#437634=CARTESIAN_POINT('Ctrl Pts',(-1.35422294845813,-2.38778447877886,
12.5049254088044));
#437635=CARTESIAN_POINT('Ctrl Pts',(-1.33769508908193,-2.38666986617616,
12.5369868989719));
#437636=CARTESIAN_POINT('Ctrl Pts',(-1.33782102160788,-2.38759281913793,
12.5342545179733));
#437637=CARTESIAN_POINT('Ctrl Pts',(-1.33806480668581,-2.38845677859828,
12.5314872231885));
#437638=CARTESIAN_POINT('Ctrl Pts',(-1.33846651163321,-2.38919789548877,
12.5287124745063));
#437639=CARTESIAN_POINT('Ctrl Pts',(-1.33882878909364,-2.38986627148637,
12.5262100684185));
#437640=CARTESIAN_POINT('Ctrl Pts',(-1.33932000719543,-2.39043359248387,
12.5237004536639));
#437641=CARTESIAN_POINT('Ctrl Pts',(-1.33999871561359,-2.39086620715601,
12.5212220730815));
#437642=CARTESIAN_POINT('Ctrl Pts',(-1.34051832562065,-2.39119741111168,
12.5193246583486));
#437643=CARTESIAN_POINT('Ctrl Pts',(-1.34115437912775,-2.39145308386972,
12.5174178313691));
#437644=CARTESIAN_POINT('Ctrl Pts',(-1.34196022806013,-2.39155193831661,
12.5155812248348));
#437645=CARTESIAN_POINT('Ctrl Pts',(-1.34230352403678,-2.39159405084233,
12.5147988205794));
#437646=CARTESIAN_POINT('Ctrl Pts',(-1.34267794934921,-2.39160802160276,
12.5140295443047));
#437647=CARTESIAN_POINT('Ctrl Pts',(-1.34308860501669,-2.39158945616174,
12.5132817086137));
#437648=CARTESIAN_POINT('Ctrl Pts',(-1.34371007681718,-2.39156135987824,
12.5121499604604));
#437649=CARTESIAN_POINT('Ctrl Pts',(-1.34442762323797,-2.39145099570438,
12.5110494206568));
#437650=CARTESIAN_POINT('Ctrl Pts',(-1.34524772786261,-2.3912216912815,
12.5100666561695));
#437651=CARTESIAN_POINT('Ctrl Pts',(-1.34571863004954,-2.39109002520993,
12.5095023550641));
#437652=CARTESIAN_POINT('Ctrl Pts',(-1.34622861105696,-2.39091699426612,
12.5089719619137));
#437653=CARTESIAN_POINT('Ctrl Pts',(-1.34676605972385,-2.39069979339732,
12.5085043804652));
#437654=CARTESIAN_POINT('Ctrl Pts',(-1.34755254584023,-2.39038194821823,
12.5078201359221));
#437655=CARTESIAN_POINT('Ctrl Pts',(-1.34842021077976,-2.38995917692624,
12.5072563000949));
#437656=CARTESIAN_POINT('Ctrl Pts',(-1.34930653136514,-2.38945252654746,
12.5068768744332));
#437657=CARTESIAN_POINT('Ctrl Pts',(-1.34994562952171,-2.38908719674643,
12.5066032824114));
#437658=CARTESIAN_POINT('Ctrl Pts',(-1.35060568529704,-2.38867188867508,
12.5064197834844));
#437659=CARTESIAN_POINT('Ctrl Pts',(-1.35125121603904,-2.38823198202769,
12.5063282718343));
#437660=CARTESIAN_POINT('Ctrl Pts',(-1.35219349107109,-2.38758985451416,
12.5061946931565));
#437661=CARTESIAN_POINT('Ctrl Pts',(-1.35312555584104,-2.38688246795464,
12.5062515701262));
#437662=CARTESIAN_POINT('Ctrl Pts',(-1.35399891386266,-2.38616604253298,
12.5064436508398));
#437663=CARTESIAN_POINT('',(-1.3440429755857,-2.31426807732518,12.5737548217797));
#437664=CARTESIAN_POINT('Origin',(-1.35185556391636,-2.32772034343821,12.5893111709658));
#437665=CARTESIAN_POINT('Ctrl Pts',(-1.35399891386266,-2.38616604253298,
12.5064436508398));
#437666=CARTESIAN_POINT('Ctrl Pts',(-1.3525256522368,-2.3755232098305,12.5164271754438));
#437667=CARTESIAN_POINT('Ctrl Pts',(-1.35105159964824,-2.36487618696084,
12.5264061185523));
#437668=CARTESIAN_POINT('Ctrl Pts',(-1.34957672917747,-2.35422482622005,
12.536380305637));
#437669=CARTESIAN_POINT('Ctrl Pts',(-1.34773344022497,-2.34091278562278,
12.5488460165097));
#437670=CARTESIAN_POINT('Ctrl Pts',(-1.34588887317763,-2.32759396537209,
12.5613043021964));
#437671=CARTESIAN_POINT('Ctrl Pts',(-1.3440429755857,-2.31426807732518,
12.5737548217797));
#437672=CARTESIAN_POINT('Ctrl Pts',(-1.38479980462761,-2.29859082104314,
12.5893111709658));
#437673=CARTESIAN_POINT('Ctrl Pts',(-1.37574697432478,-2.29177137106034,
12.5770542771492));
#437674=CARTESIAN_POINT('Ctrl Pts',(-1.36363630048295,-2.30277751725016,
12.5737548217797));
#437675=CARTESIAN_POINT('Ctrl Pts',(-1.37635359269243,-2.29222833352163,
12.5928319619712));
#437676=CARTESIAN_POINT('Ctrl Pts',(-1.3683094033576,-2.29024731501676,
12.5821634970842));
#437677=CARTESIAN_POINT('Ctrl Pts',(-1.36056522911279,-2.30045227790575,
12.5773203894503));
#437678=CARTESIAN_POINT('Ctrl Pts',(-1.35998988496106,-2.28864878485988,
12.5969440695591));
#437679=CARTESIAN_POINT('Ctrl Pts',(-1.35651320182277,-2.29066651053694,
12.5878292599214));
#437680=CARTESIAN_POINT('Ctrl Pts',(-1.35473243254761,-2.29917845243625,
12.5813877129824));
#437681=CARTESIAN_POINT('Ctrl Pts',(-1.33356952551014,-2.30408056544493,
12.596957478804));
#437682=CARTESIAN_POINT('Ctrl Pts',(-1.33702055526328,-2.30207782063047,
12.5878468778671));
#437683=CARTESIAN_POINT('Ctrl Pts',(-1.34527922820436,-2.30470685147657,
12.5814011370086));
#437684=CARTESIAN_POINT('Ctrl Pts',(-1.32862587206039,-2.32020195799361,
12.5928371701607));
#437685=CARTESIAN_POINT('Ctrl Pts',(-1.33082819508306,-2.31222167986515,
12.5821692192951));
#437686=CARTESIAN_POINT('Ctrl Pts',(-1.34351091151346,-2.31044052127765,
12.5773318885715));
#437687=CARTESIAN_POINT('Ctrl Pts',(-1.33005753786826,-2.33069457618113,
12.5893111709658));
#437688=CARTESIAN_POINT('Ctrl Pts',(-1.32852527273157,-2.31946466976519,
12.5770542771492));
#437689=CARTESIAN_POINT('Ctrl Pts',(-1.34404297558565,-2.31426807732519,
12.5737548217797));
#437690=CARTESIAN_POINT('',(-1.36363630048295,-2.30277751725016,12.5737548217797));
#437691=CARTESIAN_POINT('Origin',(-1.3715627799497,-2.31616299158853,12.5893111709658));
#437692=CARTESIAN_POINT('Ctrl Pts',(-1.34404297558565,-2.31426807732519,
12.5737548217797));
#437693=CARTESIAN_POINT('Ctrl Pts',(-1.34387517769676,-2.31328006745706,
12.5746934679442));
#437694=CARTESIAN_POINT('Ctrl Pts',(-1.34387009640631,-2.31215609698649,
12.5756680099006));
#437695=CARTESIAN_POINT('Ctrl Pts',(-1.3440249798495,-2.31102405688693,
12.5765688348656));
#437696=CARTESIAN_POINT('Ctrl Pts',(-1.34406598352647,-2.31072436180267,
12.5768073183026));
#437697=CARTESIAN_POINT('Ctrl Pts',(-1.34411794307724,-2.31042412933394,
12.5770407398754));
#437698=CARTESIAN_POINT('Ctrl Pts',(-1.34418025012305,-2.31012565157104,
12.5772674179684));
#437699=CARTESIAN_POINT('Ctrl Pts',(-1.3444359413905,-2.30890077954389,
12.5781976435658));
#437700=CARTESIAN_POINT('Ctrl Pts',(-1.34489145521362,-2.30763819305588,
12.5790594849312));
#437701=CARTESIAN_POINT('Ctrl Pts',(-1.3455614579905,-2.30643953171811,
12.5797571720116));
#437702=CARTESIAN_POINT('Ctrl Pts',(-1.34599798889079,-2.30565856075654,
12.580211740231));
#437703=CARTESIAN_POINT('Ctrl Pts',(-1.3465617949788,-2.30487839431568,
12.5806009430798));
#437704=CARTESIAN_POINT('Ctrl Pts',(-1.34722754623479,-2.30416432994221,
12.5808812374708));
#437705=CARTESIAN_POINT('Ctrl Pts',(-1.34779964742438,-2.30355071175701,
12.5811221033394));
#437706=CARTESIAN_POINT('Ctrl Pts',(-1.34845882604483,-2.30297342214248,
12.581287365893));
#437707=CARTESIAN_POINT('Ctrl Pts',(-1.34917337033051,-2.30247131682757,
12.581359338449));
#437708=CARTESIAN_POINT('Ctrl Pts',(-1.34927267723144,-2.30240153455688,
12.5813693411482));
#437709=CARTESIAN_POINT('Ctrl Pts',(-1.34937303740507,-2.30233314682621,
12.5813775999465));
#437710=CARTESIAN_POINT('Ctrl Pts',(-1.34947435024895,-2.3022661985824,
12.5813841266931));
#437711=CARTESIAN_POINT('Ctrl Pts',(-1.34964623974214,-2.30215261278955,
12.5813952001081));
#437712=CARTESIAN_POINT('Ctrl Pts',(-1.34982235842937,-2.30204291783015,
12.5814007534795));
#437713=CARTESIAN_POINT('Ctrl Pts',(-1.35000273386689,-2.3019373288753,
12.5814005856065));
#437714=CARTESIAN_POINT('Ctrl Pts',(-1.35082842209762,-2.30145398392258,
12.5813998171494));
#437715=CARTESIAN_POINT('Ctrl Pts',(-1.35168608920437,-2.30108978241973,
12.58127954464));
#437716=CARTESIAN_POINT('Ctrl Pts',(-1.35255930057023,-2.30081955655557,
12.5810700125799));
#437717=CARTESIAN_POINT('Ctrl Pts',(-1.35361404047712,-2.30049315447935,
12.5808169217085));
#437718=CARTESIAN_POINT('Ctrl Pts',(-1.35469650230511,-2.30031982026343,
12.5804173076348));
#437719=CARTESIAN_POINT('Ctrl Pts',(-1.35570770323402,-2.30028902985874,
12.5799304713245));
#437720=CARTESIAN_POINT('Ctrl Pts',(-1.35696089974608,-2.30025087084736,
12.5793271277669));
#437721=CARTESIAN_POINT('Ctrl Pts',(-1.35818140455784,-2.30039709264079,
12.5785808224116));
#437722=CARTESIAN_POINT('Ctrl Pts',(-1.35932154388287,-2.30069004004651,
12.5777485681082));
#437723=CARTESIAN_POINT('Ctrl Pts',(-1.36102047638875,-2.30112656377583,
12.576508418016));
#437724=CARTESIAN_POINT('Ctrl Pts',(-1.3625283680815,-2.30187854925022,
12.5750928681475));
#437725=CARTESIAN_POINT('Ctrl Pts',(-1.36363630048295,-2.30277751725016,
12.5737548217797));
#437726=CARTESIAN_POINT('Ctrl Pts',(-1.36363630048295,-2.30277751725016,
12.5737548217797));
#437727=CARTESIAN_POINT('Ctrl Pts',(-1.37574697432478,-2.29177137106034,
12.5770542771492));
#437728=CARTESIAN_POINT('Ctrl Pts',(-1.38479980462761,-2.29859082104314,
12.5893111709658));
#437729=CARTESIAN_POINT('Ctrl Pts',(-1.38338191825478,-2.31771490433691,
12.5508408821982));
#437730=CARTESIAN_POINT('Ctrl Pts',(-1.39552795292374,-2.30667227935687,
12.55409748406));
#437731=CARTESIAN_POINT('Ctrl Pts',(-1.40459233231949,-2.31350042921128,
12.5663972313419));
#437732=CARTESIAN_POINT('Ctrl Pts',(-1.40310895865535,-2.33263675880696,
12.52790050457));
#437733=CARTESIAN_POINT('Ctrl Pts',(-1.41527104624047,-2.3215446488673,
12.5311362602938));
#437734=CARTESIAN_POINT('Ctrl Pts',(-1.42436489260328,-2.32839499603476,
12.5434568539655));
#437735=CARTESIAN_POINT('Ctrl Pts',(-1.42281887373945,-2.3475442767001,
12.5049357605811));
#437736=CARTESIAN_POINT('Ctrl Pts',(-1.4349802036219,-2.3363914546142,12.5081700652078));
#437737=CARTESIAN_POINT('Ctrl Pts',(-1.44411904933042,-2.34327569955473,
12.5204921097672));
#437738=CARTESIAN_POINT('Ctrl Pts',(-1.42152464441194,-2.34656538937372,
12.5064436508395));
#437739=CARTESIAN_POINT('Ctrl Pts',(-1.42266057272229,-2.34611983952878,
12.5062361689309));
#437740=CARTESIAN_POINT('Ctrl Pts',(-1.42382284597399,-2.3456080656443,
12.5061871075061));
#437741=CARTESIAN_POINT('Ctrl Pts',(-1.42491822969963,-2.34505025641642,
12.5063648335164));
#437742=CARTESIAN_POINT('Ctrl Pts',(-1.42541582055389,-2.34479686505801,
12.5064455676329));
#437743=CARTESIAN_POINT('Ctrl Pts',(-1.42590644889045,-2.34453024353031,
12.506574497099));
#437744=CARTESIAN_POINT('Ctrl Pts',(-1.4263685762309,-2.34426090035578,
12.5067492519495));
#437745=CARTESIAN_POINT('Ctrl Pts',(-1.42729723905996,-2.34371964479143,
12.5071004286051));
#437746=CARTESIAN_POINT('Ctrl Pts',(-1.42814454450776,-2.3431468002662,
12.5076537929612));
#437747=CARTESIAN_POINT('Ctrl Pts',(-1.42885219540251,-2.3425931974687,
12.5083435010503));
#437748=CARTESIAN_POINT('Ctrl Pts',(-1.42889674625536,-2.34255834486418,
12.5083869222963));
#437749=CARTESIAN_POINT('Ctrl Pts',(-1.42894074109824,-2.3425235553225,
12.5084308732336));
#437750=CARTESIAN_POINT('Ctrl Pts',(-1.42898416475707,-2.34248883607826,
12.5084753333615));
#437751=CARTESIAN_POINT('Ctrl Pts',(-1.42933247981433,-2.34221034191469,
12.508831962269));
#437752=CARTESIAN_POINT('Ctrl Pts',(-1.42965192099085,-2.34193172451815,
12.509227847131));
#437753=CARTESIAN_POINT('Ctrl Pts',(-1.42993483013762,-2.3416633788136,
12.5096423454524));
#437754=CARTESIAN_POINT('Ctrl Pts',(-1.43082134219323,-2.34082250214037,
12.5109411997424));
#437755=CARTESIAN_POINT('Ctrl Pts',(-1.43141031956876,-2.34003778069885,
12.5124831113042));
#437756=CARTESIAN_POINT('Ctrl Pts',(-1.43179389723121,-2.33933082479333,
12.5140723025008));
#437757=CARTESIAN_POINT('Ctrl Pts',(-1.4318298388783,-2.33926458225068,
12.5142212114565));
#437758=CARTESIAN_POINT('Ctrl Pts',(-1.43186400649979,-2.33919901867689,
12.5143705582413));
#437759=CARTESIAN_POINT('Ctrl Pts',(-1.4318964928642,-2.33913415121086,
12.5145201959299));
#437760=CARTESIAN_POINT('Ctrl Pts',(-1.43231382858219,-2.33830083203218,
12.5164425148273));
#437761=CARTESIAN_POINT('Ctrl Pts',(-1.4324776035179,-2.3375586490697,12.5184635205941));
#437762=CARTESIAN_POINT('Ctrl Pts',(-1.43247354656481,-2.33687952145141,
12.5205025929157));
#437763=CARTESIAN_POINT('Ctrl Pts',(-1.43247119337121,-2.3364856005147,
12.5216853356836));
#437764=CARTESIAN_POINT('Ctrl Pts',(-1.43241286161085,-2.33611360298746,
12.5228750347131));
#437765=CARTESIAN_POINT('Ctrl Pts',(-1.43231679608618,-2.33576377551066,
12.5240609649613));
#437766=CARTESIAN_POINT('Ctrl Pts',(-1.43208100840961,-2.33490514273647,
12.5269717671326));
#437767=CARTESIAN_POINT('Ctrl Pts',(-1.4316012403085,-2.33415865659639,
12.5299036066169));
#437768=CARTESIAN_POINT('Ctrl Pts',(-1.43095697607925,-2.33348979507929,
12.5328133004019));
#437769=CARTESIAN_POINT('Ctrl Pts',(-1.43064769173483,-2.33316870260444,
12.5342101228451));
#437770=CARTESIAN_POINT('Ctrl Pts',(-1.43030050673073,-2.33286626338807,
12.5356023438238));
#437771=CARTESIAN_POINT('Ctrl Pts',(-1.42992349334847,-2.33258226106549,
12.5369868989719));
#437772=CARTESIAN_POINT('Origin',(-11.6129774570238,-9.99679300240355,-1.23967694121652));
#437773=CARTESIAN_POINT('Ctrl Pts',(-1.33768939948239,-2.38662846099065,
12.5369868989719));
#437774=CARTESIAN_POINT('Ctrl Pts',(-1.33979197726431,-2.40182262007747,
12.5369868989719));
#437775=CARTESIAN_POINT('Ctrl Pts',(-1.32626212111486,-2.40904939641688,
12.5369868989719));
#437776=CARTESIAN_POINT('Ctrl Pts',(-1.33840008741708,-2.39176469007801,
12.5218025310015));
#437777=CARTESIAN_POINT('Ctrl Pts',(-1.33666961631256,-2.40345491391935,
12.5216901060417));
#437778=CARTESIAN_POINT('Ctrl Pts',(-1.3263033723702,-2.40902738135429,
12.5161920673678));
#437779=CARTESIAN_POINT('Ctrl Pts',(-1.34373196522167,-2.39457665563101,
12.5042015548895));
#437780=CARTESIAN_POINT('Ctrl Pts',(-1.3416241136767,-2.40065401582123,
12.4980677368515));
#437781=CARTESIAN_POINT('Ctrl Pts',(-1.33568837083694,-2.4039642630422,
12.4907278922777));
#437782=CARTESIAN_POINT('Ctrl Pts',(-1.35398904294486,-2.38614864689313,
12.506463626192));
#437783=CARTESIAN_POINT('Ctrl Pts',(-1.35721801325199,-2.39183909407168,
12.4999376786891));
#437784=CARTESIAN_POINT('Ctrl Pts',(-1.35717857607461,-2.3917695935333,
12.4906970594712));
#437785=CARTESIAN_POINT('Origin',(-1.31589706303389,-2.38964409891908,12.5369868989719));
#437786=CARTESIAN_POINT('Origin',(-1.31589706303389,-2.38964409891908,14.));
#437787=CARTESIAN_POINT('Origin',(-1.31589706303389,-2.38964409891908,13.7435492065112));
#437788=CARTESIAN_POINT('Ctrl Pts',(-1.33434768436319,-2.36213707932785,
13.793642941384));
#437789=CARTESIAN_POINT('Ctrl Pts',(-1.33583639488598,-2.37284641917609,
13.8071662555867));
#437790=CARTESIAN_POINT('Ctrl Pts',(-1.31949668560198,-2.37764571955728,
13.8103758687955));
#437791=CARTESIAN_POINT('Ctrl Pts',(-1.33659473667552,-2.37860560874395,
13.7804579775006));
#437792=CARTESIAN_POINT('Ctrl Pts',(-1.33842162668272,-2.39182136239747,
13.7901904343352));
#437793=CARTESIAN_POINT('Ctrl Pts',(-1.32422170283523,-2.39864910630666,
13.7927914348262));
#437794=CARTESIAN_POINT('Ctrl Pts',(-1.3379176609002,-2.38830125179683,
13.7597120340895));
#437795=CARTESIAN_POINT('Ctrl Pts',(-1.34002621070749,-2.40359638526088,
13.7635825532444));
#437796=CARTESIAN_POINT('Ctrl Pts',(-1.32698310096964,-2.41104038986257,
13.7651073818884));
#437797=CARTESIAN_POINT('Ctrl Pts',(-1.33765860204468,-2.3864026228822,
13.7381884353898));
#437798=CARTESIAN_POINT('Ctrl Pts',(-1.33971868772639,-2.40133962250093,
13.7368803041982));
#437799=CARTESIAN_POINT('Ctrl Pts',(-1.32644185476272,-2.40861391583939,
13.7363986145813));
#437800=CARTESIAN_POINT('Origin',(-1.31309492773408,-2.36910736775679,13.7902182540695));
#437801=CARTESIAN_POINT('Ctrl Pts',(-1.33005700497226,-2.33069067622211,
13.8235227101244));
#437802=CARTESIAN_POINT('Ctrl Pts',(-1.33161571444549,-2.342081598621,13.8358800583119));
#437803=CARTESIAN_POINT('Ctrl Pts',(-1.31586661480734,-2.34723833301828,
13.8390832900376));
#437804=CARTESIAN_POINT('Ctrl Pts',(-1.33166952301955,-2.34250875283556,
13.8124254819052));
#437805=CARTESIAN_POINT('Ctrl Pts',(-1.33323125920889,-2.353921796282,13.8247886449158));
#437806=CARTESIAN_POINT('Ctrl Pts',(-1.31745695617586,-2.35906884834355,
13.8279860620657));
#437807=CARTESIAN_POINT('Ctrl Pts',(-1.33328131838873,-2.35432153297157,
13.8013225099955));
#437808=CARTESIAN_POINT('Ctrl Pts',(-1.33484534639161,-2.36575131207001,
13.8136962257787));
#437809=CARTESIAN_POINT('Ctrl Pts',(-1.31904682993433,-2.3708938506096,
13.8168830918626));
#437810=CARTESIAN_POINT('Ctrl Pts',(-1.33489241919809,-2.36612922270791,
13.7902140179785));
#437811=CARTESIAN_POINT('Ctrl Pts',(-1.3364580521403,-2.37757070403835,
13.802602731458));
#437812=CARTESIAN_POINT('Ctrl Pts',(-1.32063625628017,-2.38271355619271,
13.8057746032558));
#437813=CARTESIAN_POINT('Origin',(-1.30825951182028,-2.33366880892404,13.8235269408515));
#437814=CARTESIAN_POINT('Ctrl Pts',(-1.38479980462761,-2.29859082104314,
13.8235269408515));
#437815=CARTESIAN_POINT('Ctrl Pts',(-1.39423085363655,-2.30569518121011,
13.8362179249168));
#437816=CARTESIAN_POINT('Ctrl Pts',(-1.40657750063972,-2.29389588835687,
13.8391868794938));
#437817=CARTESIAN_POINT('Ctrl Pts',(-1.37617080529356,-2.29209064072475,
13.8400110824519));
#437818=CARTESIAN_POINT('Ctrl Pts',(-1.38579055609397,-2.29505412809609,
13.8494522556837));
#437819=CARTESIAN_POINT('Ctrl Pts',(-1.39230900053449,-2.2832881700173,
13.85569149686));
#437820=CARTESIAN_POINT('Ctrl Pts',(-1.36028623044585,-2.28847428787239,
13.8586819406588));
#437821=CARTESIAN_POINT('Ctrl Pts',(-1.36404890504555,-2.28628378028469,
13.868010383617));
#437822=CARTESIAN_POINT('Ctrl Pts',(-1.36590788102171,-2.27742730948009,
13.8744918421245));
#437823=CARTESIAN_POINT('Ctrl Pts',(-1.33326857445539,-2.30425775272418,
13.8587686893867));
#437824=CARTESIAN_POINT('Ctrl Pts',(-1.32953935929475,-2.30642871615213,
13.8680909899357));
#437825=CARTESIAN_POINT('Ctrl Pts',(-1.32093271578979,-2.30370436502123,
13.8745789365163));
#437826=CARTESIAN_POINT('Ctrl Pts',(-1.32859463293563,-2.31997300781692,
13.8400379222776));
#437827=CARTESIAN_POINT('Ctrl Pts',(-1.32647840745911,-2.3298112913888,
13.8494748685453));
#437828=CARTESIAN_POINT('Ctrl Pts',(-1.31303377231583,-2.32975752216985,
13.8557104837033));
#437829=CARTESIAN_POINT('Ctrl Pts',(-1.33005753786175,-2.33069457618187,
13.8235269408542));
#437830=CARTESIAN_POINT('Ctrl Pts',(-1.33165381958967,-2.34239365748921,
13.8362179249195));
#437831=CARTESIAN_POINT('Ctrl Pts',(-1.31532870539695,-2.34740899901807,
13.8391868794965));
#437832=CARTESIAN_POINT('Origin',(-1.39803682930552,-2.28101865049774,13.8235269408515));
#437833=CARTESIAN_POINT('Ctrl Pts',(-1.41336494897749,-2.32010879476138,
13.7902140241683));
#437834=CARTESIAN_POINT('Ctrl Pts',(-1.42258614113104,-2.32706064420306,
13.8026027327198));
#437835=CARTESIAN_POINT('Ctrl Pts',(-1.43479835951345,-2.31576287210172,
13.8057746032556));
#437836=CARTESIAN_POINT('Ctrl Pts',(-1.4038463468152,-2.3129384812607,13.8013225161808));
#437837=CARTESIAN_POINT('Ctrl Pts',(-1.41305810939257,-2.31988321726021,
13.8136962270464));
#437838=CARTESIAN_POINT('Ctrl Pts',(-1.42525868962529,-2.30860560903426,
13.8168830918628));
#437839=CARTESIAN_POINT('Ctrl Pts',(-1.39432364109784,-2.30576507657335,
13.8124254880875));
#437840=CARTESIAN_POINT('Ctrl Pts',(-1.40352191652556,-2.31269964247155,
13.8247886461867));
#437841=CARTESIAN_POINT('Ctrl Pts',(-1.41571461550004,-2.30144536977557,
13.8279860620656));
#437842=CARTESIAN_POINT('Ctrl Pts',(-1.3847966656975,-2.29858845555602,
13.8235227163066));
#437843=CARTESIAN_POINT('Ctrl Pts',(-1.39397711266371,-2.30550958095132,
13.8358800595847));
#437844=CARTESIAN_POINT('Ctrl Pts',(-1.40616595815507,-2.29428203106785,
13.8390832900376));
#437845=CARTESIAN_POINT('Origin',(-1.42660512252251,-2.30253899719266,13.7902182540695));
#437846=CARTESIAN_POINT('Ctrl Pts',(-1.42970796339007,-2.33241986893362,
13.7382347919292));
#437847=CARTESIAN_POINT('Ctrl Pts',(-1.44174667761807,-2.34151861766462,
13.7369371795942));
#437848=CARTESIAN_POINT('Ctrl Pts',(-1.45458222311529,-2.33346923577475,
13.7364597369711));
#437849=CARTESIAN_POINT('Ctrl Pts',(-1.43121881726327,-2.33355798780178,
13.7595490285574));
#437850=CARTESIAN_POINT('Ctrl Pts',(-1.44354537111657,-2.34287302277328,
13.7633824266926));
#437851=CARTESIAN_POINT('Ctrl Pts',(-1.45641273663841,-2.33510613376707,
13.7648920890506));
#437852=CARTESIAN_POINT('Ctrl Pts',(-1.42351354527644,-2.32775364393176,
13.780380659011));
#437853=CARTESIAN_POINT('Ctrl Pts',(-1.43417231843284,-2.3358151227542,
13.7901039518744));
#437854=CARTESIAN_POINT('Ctrl Pts',(-1.4470781039309,-2.32676381665488,
13.7926933640892));
#437855=CARTESIAN_POINT('Ctrl Pts',(-1.41012006257667,-2.31766439853161,
13.7936647693663));
#437856=CARTESIAN_POINT('Ctrl Pts',(-1.41874065032452,-2.3241957688952,
13.8072068914933));
#437857=CARTESIAN_POINT('Ctrl Pts',(-1.43091158297241,-2.31225790190283,
13.8104111085397));
#437858=CARTESIAN_POINT('Origin',(-1.44316051802638,-2.31501009052009,13.7435492065112));
#437859=CARTESIAN_POINT('Origin',(-1.44316051802638,-2.31501009052009,14.));
#437860=CARTESIAN_POINT('Origin',(-1.44316051802638,-2.31501009052009,12.5369868989719));
#437861=CARTESIAN_POINT('Ctrl Pts',(-1.42151511945786,-2.34654966618566,
12.506462012331));
#437862=CARTESIAN_POINT('Ctrl Pts',(-1.42490298989075,-2.3521421541758,
12.4999388158272));
#437863=CARTESIAN_POINT('Ctrl Pts',(-1.42486290694061,-2.35207598770878,
12.4907030323752));
#437864=CARTESIAN_POINT('Ctrl Pts',(-1.43387678705323,-2.34171047643781,
12.5042014951932));
#437865=CARTESIAN_POINT('Ctrl Pts',(-1.44020683426554,-2.3428381286032,
12.4980716682127));
#437866=CARTESIAN_POINT('Ctrl Pts',(-1.44599026110078,-2.33927757537827,
12.4907355092744));
#437867=CARTESIAN_POINT('Ctrl Pts',(-1.4340278803235,-2.33568528996193,
12.5218047446509));
#437868=CARTESIAN_POINT('Ctrl Pts',(-1.44507022020915,-2.3398788088645,
12.5216906929434));
#437869=CARTESIAN_POINT('Ctrl Pts',(-1.4549910807195,-2.33355842271618,
12.5161988840775));
#437870=CARTESIAN_POINT('Ctrl Pts',(-1.42989282923491,-2.33255911995573,
12.5369868989719));
#437871=CARTESIAN_POINT('Ctrl Pts',(-1.44212122438067,-2.3418042204787,
12.5369868989719));
#437872=CARTESIAN_POINT('Ctrl Pts',(-1.45502900165886,-2.3335341045631,
12.5369868989719));
#437873=CARTESIAN_POINT('Origin',(-2.60621061928491E-31,-9.59588718149408E-31,
12.5));
#437874=CARTESIAN_POINT('Origin',(-1.19283550652458,-2.40381648963782,12.5));
#437875=CARTESIAN_POINT('',(-1.19283550652458,-2.40381648963782,12.5893111709658));
#437876=CARTESIAN_POINT('',(-1.19283550652458,-2.40381648963782,13.8235269408515));
#437877=CARTESIAN_POINT('',(-1.19283550652458,-2.40381648963782,12.5));
#437878=CARTESIAN_POINT('',(-1.21955463306182,-2.42759381026669,13.7902182540695));
#437879=CARTESIAN_POINT('',(-1.19283550652458,-2.40381648963782,13.8235269408515));
#437880=CARTESIAN_POINT('',(-1.2350384319707,-2.44137282548623,13.7435492065112));
#437881=CARTESIAN_POINT('Origin',(-1.18409672167107,-2.39604029089782,13.7445212918711));
#437882=CARTESIAN_POINT('',(-1.2350384319707,-2.44137282548623,12.5369868989719));
#437883=CARTESIAN_POINT('',(-1.2350384319707,-2.44137282548623,12.5));
#437884=CARTESIAN_POINT('Ctrl Pts',(-1.2350384319707,-2.44137282548623,
12.5369868989719));
#437885=CARTESIAN_POINT('Ctrl Pts',(-1.22098105023765,-2.42886317730581,
12.5544431401645));
#437886=CARTESIAN_POINT('Ctrl Pts',(-1.20691361429157,-2.41634458189252,
12.5718848856037));
#437887=CARTESIAN_POINT('Ctrl Pts',(-1.19283550652458,-2.40381648963782,
12.5893111709658));
#437888=CARTESIAN_POINT('Origin',(-1.15050357034785,-2.70595045041756,12.5));
#437889=CARTESIAN_POINT('',(-1.1387082681697,-2.48776298739836,13.7435492065112));
#437890=CARTESIAN_POINT('',(-1.13758939098738,-2.46706619047416,13.7902182540695));
#437891=CARTESIAN_POINT('Origin',(-1.13464917513303,-2.41267858528178,13.7418732680441));
#437892=CARTESIAN_POINT('',(-1.13565863606154,-2.43135141923567,13.8235269408515));
#437893=CARTESIAN_POINT('',(-1.13758939098738,-2.46706619047416,13.7902182540695));
#437894=CARTESIAN_POINT('',(-1.13565863606154,-2.43135141923567,12.5893111709658));
#437895=CARTESIAN_POINT('',(-1.13565863606154,-2.43135141923567,12.5));
#437896=CARTESIAN_POINT('',(-1.1387082681697,-2.48776298739836,12.5369868989719));
#437897=CARTESIAN_POINT('Ctrl Pts',(-1.13565863606154,-2.43135141923567,
12.5893111709658));
#437898=CARTESIAN_POINT('Ctrl Pts',(-1.13667593637934,-2.45016926485903,
12.5718848856037));
#437899=CARTESIAN_POINT('Ctrl Pts',(-1.13769246553904,-2.46897284573306,
12.5544431401645));
#437900=CARTESIAN_POINT('Ctrl Pts',(-1.1387082681697,-2.48776298739836,
12.5369868989719));
#437901=CARTESIAN_POINT('',(-1.1387082681697,-2.48776298739836,12.5));
#437902=CARTESIAN_POINT('Origin',(-1.16998351495927,-2.42949580244988,12.5));
#437903=CARTESIAN_POINT('',(-1.15608566822344,-2.39805633635573,13.8587068136939));
#437904=CARTESIAN_POINT('Ctrl Pts',(-1.13565863605493,-2.43135141923588,
13.8235269408542));
#437905=CARTESIAN_POINT('Ctrl Pts',(-1.13556404422397,-2.42960167587965,
13.8262006681044));
#437906=CARTESIAN_POINT('Ctrl Pts',(-1.13564072931349,-2.42780169048275,
13.8288634856214));
#437907=CARTESIAN_POINT('Ctrl Pts',(-1.13587638416659,-2.42595659529002,
13.8314912288862));
#437908=CARTESIAN_POINT('Ctrl Pts',(-1.13611932001346,-2.42405449245906,
13.8342001611531));
#437909=CARTESIAN_POINT('Ctrl Pts',(-1.13653097767233,-2.42210227355088,
13.8368750301949));
#437910=CARTESIAN_POINT('Ctrl Pts',(-1.13714073142578,-2.4200911968547,
13.8394886372969));
#437911=CARTESIAN_POINT('Ctrl Pts',(-1.13718782418721,-2.41993587652327,
13.8396904925131));
#437912=CARTESIAN_POINT('Ctrl Pts',(-1.13723612054746,-2.41978020779261,
13.8398919674349));
#437913=CARTESIAN_POINT('Ctrl Pts',(-1.13728564523326,-2.41962418901184,
13.8400930404591));
#437914=CARTESIAN_POINT('Ctrl Pts',(-1.13805727315653,-2.41719331144304,
13.8432258934518));
#437915=CARTESIAN_POINT('Ctrl Pts',(-1.13912207606121,-2.41468951998664,
13.8462331177034));
#437916=CARTESIAN_POINT('Ctrl Pts',(-1.14053409789255,-2.41223222750274,
13.8489036603661));
#437917=CARTESIAN_POINT('Ctrl Pts',(-1.14099612786829,-2.41142817280506,
13.849777493004));
#437918=CARTESIAN_POINT('Ctrl Pts',(-1.14149534821422,-2.41062934615131,
13.85061494757));
#437919=CARTESIAN_POINT('Ctrl Pts',(-1.14203368183056,-2.40984064427917,
13.8514076489583));
#437920=CARTESIAN_POINT('Ctrl Pts',(-1.14317233506844,-2.40817242607178,
13.8530843267192));
#437921=CARTESIAN_POINT('Ctrl Pts',(-1.14460026343935,-2.40638730907992,
13.8546805203176));
#437922=CARTESIAN_POINT('Ctrl Pts',(-1.14634114150165,-2.40467413179495,
13.8559412814273));
#437923=CARTESIAN_POINT('Ctrl Pts',(-1.1465741274444,-2.40444485311456,
13.8561100121513));
#437924=CARTESIAN_POINT('Ctrl Pts',(-1.14681264214506,-2.40421685616153,
13.8562727473908));
#437925=CARTESIAN_POINT('Ctrl Pts',(-1.14705666823522,-2.40399057749032,
13.8564289040185));
#437926=CARTESIAN_POINT('Ctrl Pts',(-1.14816332377013,-2.40296440629786,
13.8571370725437));
#437927=CARTESIAN_POINT('Ctrl Pts',(-1.14940432695712,-2.40195720550874,
13.8577210840553));
#437928=CARTESIAN_POINT('Ctrl Pts',(-1.15074993411319,-2.40103091263404,
13.8581177131616));
#437929=CARTESIAN_POINT('Ctrl Pts',(-1.15112890340273,-2.40077003667849,
13.8582294175695));
#437930=CARTESIAN_POINT('Ctrl Pts',(-1.15151604224291,-2.40051545443973,
13.8583265086086));
#437931=CARTESIAN_POINT('Ctrl Pts',(-1.15191038967512,-2.40026822500784,
13.8584082369006));
#437932=CARTESIAN_POINT('Ctrl Pts',(-1.15247696118677,-2.3999130226114,
13.8585256585398));
#437933=CARTESIAN_POINT('Ctrl Pts',(-1.15306562823362,-2.39956885582225,
13.8586122832068));
#437934=CARTESIAN_POINT('Ctrl Pts',(-1.15366149752404,-2.39924534681874,
13.8586682984299));
#437935=CARTESIAN_POINT('Ctrl Pts',(-1.15413813388975,-2.39898657168434,
13.8587131050557));
#437936=CARTESIAN_POINT('Ctrl Pts',(-1.15462453112183,-2.39873795001314,
13.8587357943552));
#437937=CARTESIAN_POINT('Ctrl Pts',(-1.15512097752044,-2.39849990321211,
13.8587355499465));
#437938=CARTESIAN_POINT('Ctrl Pts',(-1.15544184266373,-2.39834604788929,
13.8587353919793));
#437939=CARTESIAN_POINT('Ctrl Pts',(-1.15576341917743,-2.39819823895467,
13.8587257282814));
#437940=CARTESIAN_POINT('Ctrl Pts',(-1.15608566822344,-2.39805633635573,
13.8587068136939));
#437941=CARTESIAN_POINT('Ctrl Pts',(-1.15608566822344,-2.39805633635573,
13.8587068136939));
#437942=CARTESIAN_POINT('Ctrl Pts',(-1.15714552776804,-2.39758962644377,
13.8586446046466));
#437943=CARTESIAN_POINT('Ctrl Pts',(-1.15821265393815,-2.39718672724622,
13.858482427929));
#437944=CARTESIAN_POINT('Ctrl Pts',(-1.15928575783141,-2.39684335802857,
13.8582284286032));
#437945=CARTESIAN_POINT('Ctrl Pts',(-1.16038663759735,-2.3964911011536,
13.8579678548414));
#437946=CARTESIAN_POINT('Ctrl Pts',(-1.16149696447231,-2.39620209417302,
13.857615680862));
#437947=CARTESIAN_POINT('Ctrl Pts',(-1.16257052384783,-2.39597835375481,
13.8571944833187));
#437948=CARTESIAN_POINT('Ctrl Pts',(-1.16524970106408,-2.39541998665887,
13.8561433417727));
#437949=CARTESIAN_POINT('Ctrl Pts',(-1.16782423430203,-2.39523728850824,
13.8546163505475));
#437950=CARTESIAN_POINT('Ctrl Pts',(-1.17014755027251,-2.39528440273794,
13.8528973491086));
#437951=CARTESIAN_POINT('Ctrl Pts',(-1.170571985823,-2.3952930098126,13.8525833129073));
#437952=CARTESIAN_POINT('Ctrl Pts',(-1.17098810508553,-2.3953091626277,
13.8522628768812));
#437953=CARTESIAN_POINT('Ctrl Pts',(-1.17139512366914,-2.39533183035303,
13.851937733538));
#437954=CARTESIAN_POINT('Ctrl Pts',(-1.17388072968787,-2.3954702590066,
13.8499521282529));
#437955=CARTESIAN_POINT('Ctrl Pts',(-1.1762737329255,-2.39586948226938,
13.847639871647));
#437956=CARTESIAN_POINT('Ctrl Pts',(-1.17846158645337,-2.39642927296008,
13.8452109780794));
#437957=CARTESIAN_POINT('Ctrl Pts',(-1.17944594704187,-2.39668113437892,
13.8441181685877));
#437958=CARTESIAN_POINT('Ctrl Pts',(-1.18038918688252,-2.39696490831384,
13.8430021611332));
#437959=CARTESIAN_POINT('Ctrl Pts',(-1.18128368452846,-2.39726945733401,
13.8418824960098));
#437960=CARTESIAN_POINT('Ctrl Pts',(-1.18339159107294,-2.39798713487697,
13.8392439765549));
#437961=CARTESIAN_POINT('Ctrl Pts',(-1.18533080775571,-2.39885090846952,
13.8364981347964));
#437962=CARTESIAN_POINT('Ctrl Pts',(-1.18712038689639,-2.39983180272077,
13.8336931113419));
#437963=CARTESIAN_POINT('Ctrl Pts',(-1.18886332333062,-2.40078713142894,
13.8309611966328));
#437964=CARTESIAN_POINT('Ctrl Pts',(-1.19046579600871,-2.40185500747651,
13.8281701127186));
#437965=CARTESIAN_POINT('Ctrl Pts',(-1.1919152730911,-2.40303389142641,
13.8253580685121));
#437966=CARTESIAN_POINT('Ctrl Pts',(-1.19222952128689,-2.40328947473904,
13.8247484142933));
#437967=CARTESIAN_POINT('Ctrl Pts',(-1.19253641265792,-2.40355032634256,
13.8241378483365));
#437968=CARTESIAN_POINT('Ctrl Pts',(-1.19283550652458,-2.40381648963782,
13.8235269408515));
#437969=CARTESIAN_POINT('',(-1.15495886952874,-2.39857892755329,12.5969504640361));
#437970=CARTESIAN_POINT('Origin',(-1.16999804659657,-2.42952552641878,12.584524458991));
#437971=CARTESIAN_POINT('Origin',(-1.16999804659657,-2.42952552641878,12.584524458991));
#437972=CARTESIAN_POINT('Ctrl Pts',(-1.13565863606154,-2.43135141923567,
12.5893111709658));
#437973=CARTESIAN_POINT('Ctrl Pts',(-1.13504681103694,-2.42003398557344,
12.5770542771492));
#437974=CARTESIAN_POINT('Ctrl Pts',(-1.15093645054157,-2.41611952120801,
12.5737548217797));
#437975=CARTESIAN_POINT('Ctrl Pts',(-1.13699649205574,-2.45609884841133,
12.5663937883685));
#437976=CARTESIAN_POINT('Ctrl Pts',(-1.13638388656337,-2.44476697779074,
12.5540940315304));
#437977=CARTESIAN_POINT('Ctrl Pts',(-1.15232353295924,-2.44084350125998,
12.5508374392248));
#437978=CARTESIAN_POINT('Ctrl Pts',(-1.13833299816964,-2.48082130773439,
12.5434499600945));
#437979=CARTESIAN_POINT('Ctrl Pts',(-1.13771840087868,-2.46945259316697,
12.5311293540533));
#437980=CARTESIAN_POINT('Ctrl Pts',(-1.15370808215303,-2.46554339154704,
12.5278936106989));
#437981=CARTESIAN_POINT('Ctrl Pts',(-1.13966826014122,-2.50552075312746,
12.5204817579905));
#437982=CARTESIAN_POINT('Ctrl Pts',(-1.13905062101366,-2.4940957711924,
12.5081597038247));
#437983=CARTESIAN_POINT('Ctrl Pts',(-1.1550902811826,-2.49022106519589,
12.5049254088044));
#437984=CARTESIAN_POINT('Ctrl Pts',(-1.1387082681697,-2.48776298739836,
12.5369868989719));
#437985=CARTESIAN_POINT('Ctrl Pts',(-1.1387585524309,-2.48869313398025,
12.5342545179733));
#437986=CARTESIAN_POINT('Ctrl Pts',(-1.13893110561746,-2.48957408943381,
12.5314872231885));
#437987=CARTESIAN_POINT('Ctrl Pts',(-1.13927106601802,-2.49034548300144,
12.5287124745063));
#437988=CARTESIAN_POINT('Ctrl Pts',(-1.13957765918138,-2.49104116400929,
12.5262100684184));
#437989=CARTESIAN_POINT('Ctrl Pts',(-1.14002100086742,-2.49164663612851,
12.5237004536639));
#437990=CARTESIAN_POINT('Ctrl Pts',(-1.14066218882733,-2.49213313234792,
12.5212220730815));
#437991=CARTESIAN_POINT('Ctrl Pts',(-1.14115307367782,-2.49250558728916,
12.5193246583486));
#437992=CARTESIAN_POINT('Ctrl Pts',(-1.14176617106602,-2.49281225358285,
12.517417831369));
#437993=CARTESIAN_POINT('Ctrl Pts',(-1.14256128104741,-2.49297646326884,
12.5155812248347));
#437994=CARTESIAN_POINT('Ctrl Pts',(-1.14290000217322,-2.49304641747771,
12.5147988205793));
#437995=CARTESIAN_POINT('Ctrl Pts',(-1.14327204286964,-2.49309086089055,
12.5140295443047));
#437996=CARTESIAN_POINT('Ctrl Pts',(-1.14368284537006,-2.49310582947374,
12.5132817086137));
#437997=CARTESIAN_POINT('Ctrl Pts',(-1.14430453938234,-2.4931284823995,
12.5121499604604));
#437998=CARTESIAN_POINT('Ctrl Pts',(-1.14502869393135,-2.493076972148,12.5110494206568));
#437999=CARTESIAN_POINT('Ctrl Pts',(-1.14586476016472,-2.49291527685706,
12.5100666561695));
#438000=CARTESIAN_POINT('Ctrl Pts',(-1.14634482747063,-2.49282243179336,
12.5095023550641));
#438001=CARTESIAN_POINT('Ctrl Pts',(-1.14686721518658,-2.49269154478228,
12.5089719619137));
#438002=CARTESIAN_POINT('Ctrl Pts',(-1.14742057942457,-2.49251887368723,
12.5085043804652));
#438003=CARTESIAN_POINT('Ctrl Pts',(-1.14823035590611,-2.49226619203162,
12.5078201359221));
#438004=CARTESIAN_POINT('Ctrl Pts',(-1.14912959354634,-2.49191555022426,
12.5072563000953));
#438005=CARTESIAN_POINT('Ctrl Pts',(-1.15005426168245,-2.4914828290387,
12.5068768744336));
#438006=CARTESIAN_POINT('Ctrl Pts',(-1.15072101106295,-2.49117080727528,
12.5066032824118));
#438007=CARTESIAN_POINT('Ctrl Pts',(-1.15141272202142,-2.49081068178022,
12.5064197834844));
#438008=CARTESIAN_POINT('Ctrl Pts',(-1.15209196128879,-2.4904248556342,
12.5063282718343));
#438009=CARTESIAN_POINT('Ctrl Pts',(-1.15308344033198,-2.48986166890977,
12.5061946931565));
#438010=CARTESIAN_POINT('Ctrl Pts',(-1.15407006230495,-2.48923260805229,
12.5062515701262));
#438011=CARTESIAN_POINT('Ctrl Pts',(-1.15499890962263,-2.48858975326374,
12.5064436508398));
#438012=CARTESIAN_POINT('',(-1.15093645054157,-2.41611952120801,12.5737548217797));
#438013=CARTESIAN_POINT('Origin',(-1.15762655855609,-2.43016382449276,12.5893111709658));
#438014=CARTESIAN_POINT('Ctrl Pts',(-1.15499890962263,-2.48858975326374,
12.5064436508398));
#438015=CARTESIAN_POINT('Ctrl Pts',(-1.15439803982179,-2.47786224920951,
12.5164271754438));
#438016=CARTESIAN_POINT('Ctrl Pts',(-1.15379672322763,-2.46713050445973,
12.5264061185523));
#438017=CARTESIAN_POINT('Ctrl Pts',(-1.15319494504947,-2.45639436960773,
12.536380305637));
#438018=CARTESIAN_POINT('Ctrl Pts',(-1.15244284438053,-2.44297637856549,
12.5488460165097));
#438019=CARTESIAN_POINT('Ctrl Pts',(-1.1516900224742,-2.42955152625198,
12.5613043021964));
#438020=CARTESIAN_POINT('Ctrl Pts',(-1.15093645054157,-2.41611952120801,
12.5737548217797));
#438021=CARTESIAN_POINT('Ctrl Pts',(-1.19283550652457,-2.40381648963782,
12.5893111709658));
#438022=CARTESIAN_POINT('Ctrl Pts',(-1.18436864725005,-2.39628184110022,
12.5770542771492));
#438023=CARTESIAN_POINT('Ctrl Pts',(-1.17140116758582,-2.40626423289842,
12.5737548217797));
#438024=CARTESIAN_POINT('Ctrl Pts',(-1.1849360004623,-2.39678672808515,
12.5928319619712));
#438025=CARTESIAN_POINT('Ctrl Pts',(-1.1770800489029,-2.39415662514653,
12.5821634970842));
#438026=CARTESIAN_POINT('Ctrl Pts',(-1.16852984354534,-2.40369640976901,
12.5773203894503));
#438027=CARTESIAN_POINT('Ctrl Pts',(-1.16891850806534,-2.39188529598292,
12.5969440695591));
#438028=CARTESIAN_POINT('Ctrl Pts',(-1.16528892992905,-2.39361292589252,
12.5878292599214));
#438029=CARTESIAN_POINT('Ctrl Pts',(-1.16282028373094,-2.40195139577956,
12.5813877129824));
#438030=CARTESIAN_POINT('Ctrl Pts',(-1.14132822680162,-2.40511222402121,
12.596957478804));
#438031=CARTESIAN_POINT('Ctrl Pts',(-1.14493101583289,-2.40339743413758,
12.5878468778671));
#438032=CARTESIAN_POINT('Ctrl Pts',(-1.15294791830037,-2.4066908756149,
12.5814011370086));
#438033=CARTESIAN_POINT('Ctrl Pts',(-1.13508697979447,-2.42077702031531,
12.5928371701607));
#438034=CARTESIAN_POINT('Ctrl Pts',(-1.13793244152173,-2.41300280567571,
12.5821692192951));
#438035=CARTESIAN_POINT('Ctrl Pts',(-1.1507181382198,-2.41226133287615,
12.5773318885715));
#438036=CARTESIAN_POINT('Ctrl Pts',(-1.13565863606148,-2.43135141923566,
12.5893111709658));
#438037=CARTESIAN_POINT('Ctrl Pts',(-1.13504681103689,-2.42003398557343,
12.5770542771492));
#438038=CARTESIAN_POINT('Ctrl Pts',(-1.15093645054151,-2.41611952120801,
12.5737548217797));
#438039=CARTESIAN_POINT('',(-1.17140116758582,-2.40626423289842,12.5737548217797));
#438040=CARTESIAN_POINT('Origin',(-1.17821023192278,-2.42025124983754,12.5893111709658));
#438041=CARTESIAN_POINT('Ctrl Pts',(-1.15093645054151,-2.41611952120801,
12.5737548217797));
#438042=CARTESIAN_POINT('Ctrl Pts',(-1.15084974296275,-2.41512112177552,
12.5746934679442));
#438043=CARTESIAN_POINT('Ctrl Pts',(-1.15093629260766,-2.41400047705163,
12.5756680099006));
#438044=CARTESIAN_POINT('Ctrl Pts',(-1.15118293246642,-2.4128848281606,
12.5765688348656));
#438045=CARTESIAN_POINT('Ctrl Pts',(-1.15124822763864,-2.41258947246734,
12.5768073183026));
#438046=CARTESIAN_POINT('Ctrl Pts',(-1.15132448603172,-2.41229447418314,
12.5770407398754));
#438047=CARTESIAN_POINT('Ctrl Pts',(-1.15141091446458,-2.41200206818303,
12.5772674179684));
#438048=CARTESIAN_POINT('Ctrl Pts',(-1.1517655933818,-2.41080211302853,
12.5781976435658));
#438049=CARTESIAN_POINT('Ctrl Pts',(-1.15232250404031,-2.40958085629827,
12.5790594849312));
#438050=CARTESIAN_POINT('Ctrl Pts',(-1.15308797946507,-2.40844079485354,
12.5797571720116));
#438051=CARTESIAN_POINT('Ctrl Pts',(-1.15358671422835,-2.40769800382934,
12.580211740231));
#438052=CARTESIAN_POINT('Ctrl Pts',(-1.15421223510576,-2.40696638875824,
12.5806009430798));
#438053=CARTESIAN_POINT('Ctrl Pts',(-1.15493397400486,-2.40630896528297,
12.5808812374708));
#438054=CARTESIAN_POINT('Ctrl Pts',(-1.15555418715358,-2.40574402041974,
12.5811221033394));
#438055=CARTESIAN_POINT('Ctrl Pts',(-1.15625822687442,-2.40522238086587,
12.581287365893));
#438056=CARTESIAN_POINT('Ctrl Pts',(-1.15701131981742,-2.40478018825776,
12.581359338449));
#438057=CARTESIAN_POINT('Ctrl Pts',(-1.15711598418572,-2.40471873261616,
12.5813693411482));
#438058=CARTESIAN_POINT('Ctrl Pts',(-1.15722158465408,-2.40465875272587,
12.5813775999465));
#438059=CARTESIAN_POINT('Ctrl Pts',(-1.15732801729123,-2.40460028518414,
12.5813841266931));
#438060=CARTESIAN_POINT('Ctrl Pts',(-1.1575085931329,-2.40450108792808,
12.5813952001081));
#438061=CARTESIAN_POINT('Ctrl Pts',(-1.15769306695728,-2.40440611327763,
12.5814007534795));
#438062=CARTESIAN_POINT('Ctrl Pts',(-1.15788144869047,-2.40431557793399,
12.5814005856065));
#438063=CARTESIAN_POINT('Ctrl Pts',(-1.15874378661253,-2.40390114252785,
12.5813998171494));
#438064=CARTESIAN_POINT('Ctrl Pts',(-1.1596282857063,-2.40360806070685,
12.58127954464));
#438065=CARTESIAN_POINT('Ctrl Pts',(-1.16052061744996,-2.40340990882978,
12.5810700125799));
#438066=CARTESIAN_POINT('Ctrl Pts',(-1.16159845259619,-2.40317056392368,
12.5808169217085));
#438067=CARTESIAN_POINT('Ctrl Pts',(-1.1626914409695,-2.40308603715113,
12.5804173076348));
#438068=CARTESIAN_POINT('Ctrl Pts',(-1.16370178691457,-2.40313777146221,
12.5799304713245));
#438069=CARTESIAN_POINT('Ctrl Pts',(-1.1649539238323,-2.40320188657163,
12.5793271277669));
#438070=CARTESIAN_POINT('Ctrl Pts',(-1.16615844908136,-2.40344710429688,
12.5785808224116));
#438071=CARTESIAN_POINT('Ctrl Pts',(-1.16727091675368,-2.40383200888381,
12.5777485681082));
#438072=CARTESIAN_POINT('Ctrl Pts',(-1.16892861546537,-2.40440555888777,
12.576508418016));
#438073=CARTESIAN_POINT('Ctrl Pts',(-1.17037019597565,-2.40527794936408,
12.5750928681475));
#438074=CARTESIAN_POINT('Ctrl Pts',(-1.17140116758582,-2.40626423289842,
12.5737548217797));
#438075=CARTESIAN_POINT('Ctrl Pts',(-1.17140116758582,-2.40626423289842,
12.5737548217797));
#438076=CARTESIAN_POINT('Ctrl Pts',(-1.18436864725005,-2.39628184110022,
12.5770542771492));
#438077=CARTESIAN_POINT('Ctrl Pts',(-1.19283550652458,-2.40381648963782,
12.5893111709658));
#438078=CARTESIAN_POINT('Ctrl Pts',(-1.1898635477239,-2.42276136821965,
12.5508408821982));
#438079=CARTESIAN_POINT('Ctrl Pts',(-1.20286924391508,-2.4127455012471,
12.55409748406));
#438080=CARTESIAN_POINT('Ctrl Pts',(-1.21134690473358,-2.42028976206649,
12.5663972313419));
#438081=CARTESIAN_POINT('Ctrl Pts',(-1.20830867835785,-2.43924150837951,
12.52790050457));
#438082=CARTESIAN_POINT('Ctrl Pts',(-1.22133440753403,-2.4291776295661,
12.5311362602938));
#438083=CARTESIAN_POINT('Ctrl Pts',(-1.22983962798362,-2.4367464156702,
12.5434568539655));
#438084=CARTESIAN_POINT('Ctrl Pts',(-1.22673790922254,-2.45570596379389,
12.5049357605811));
#438085=CARTESIAN_POINT('Ctrl Pts',(-1.23976783182079,-2.44558151308914,
12.5081700652078));
#438086=CARTESIAN_POINT('Ctrl Pts',(-1.24831513890126,-2.45318775203869,
12.5204921097672));
#438087=CARTESIAN_POINT('Ctrl Pts',(-1.225527774741,-2.45462484192911,12.5064436508395));
#438088=CARTESIAN_POINT('Ctrl Pts',(-1.22669623979225,-2.45427336331726,
12.5062361689309));
#438089=CARTESIAN_POINT('Ctrl Pts',(-1.22789635999824,-2.45385802837819,
12.5061871075061));
#438090=CARTESIAN_POINT('Ctrl Pts',(-1.22903356555542,-2.45339135915718,
12.5063648335164));
#438091=CARTESIAN_POINT('Ctrl Pts',(-1.22955015446524,-2.45317936921165,
12.5064455676329));
#438092=CARTESIAN_POINT('Ctrl Pts',(-1.2300608824062,-2.4529536256093,12.506574497099));
#438093=CARTESIAN_POINT('Ctrl Pts',(-1.23054342602523,-2.45272284632038,
12.5067492519495));
#438094=CARTESIAN_POINT('Ctrl Pts',(-1.23151311615859,-2.45225908638114,
12.5071004286051));
#438095=CARTESIAN_POINT('Ctrl Pts',(-1.23240429441423,-2.4517572112088,
12.5076537929612));
#438096=CARTESIAN_POINT('Ctrl Pts',(-1.2331547144264,-2.45126313059638,
12.5083435010503));
#438097=CARTESIAN_POINT('Ctrl Pts',(-1.23320195785079,-2.45123202526912,
12.5083869222963));
#438098=CARTESIAN_POINT('Ctrl Pts',(-1.23324864197509,-2.45120093747488,
12.5084308732336));
#438099=CARTESIAN_POINT('Ctrl Pts',(-1.233294751086,-2.45116987318738,12.5084753333615));
#438100=CARTESIAN_POINT('Ctrl Pts',(-1.23366460701339,-2.45092069660093,
12.508831962269));
#438101=CARTESIAN_POINT('Ctrl Pts',(-1.23400569518013,-2.45066904370223,
12.509227847131));
#438102=CARTESIAN_POINT('Ctrl Pts',(-1.23430953563616,-2.45042465061774,
12.5096423454524));
#438103=CARTESIAN_POINT('Ctrl Pts',(-1.23526163715123,-2.44965883085478,
12.5109411997424));
#438104=CARTESIAN_POINT('Ctrl Pts',(-1.23591261683561,-2.44892472763303,
12.5124831113042));
#438105=CARTESIAN_POINT('Ctrl Pts',(-1.23635254164439,-2.44825138920541,
12.5140723025008));
#438106=CARTESIAN_POINT('Ctrl Pts',(-1.23639376308081,-2.44818829665726,
12.5142212114565));
#438107=CARTESIAN_POINT('Ctrl Pts',(-1.23643316105228,-2.4481257362192,
12.5143705582413));
#438108=CARTESIAN_POINT('Ctrl Pts',(-1.23647082662168,-2.4480637325346,
12.5145201959299));
#438109=CARTESIAN_POINT('Ctrl Pts',(-1.23695469693871,-2.44726720289212,
12.5164425148273));
#438110=CARTESIAN_POINT('Ctrl Pts',(-1.23717842172837,-2.44654083865989,
12.5184635205941));
#438111=CARTESIAN_POINT('Ctrl Pts',(-1.23722973348005,-2.44586364010339,
12.5205025929158));
#438112=CARTESIAN_POINT('Ctrl Pts',(-1.23725949632984,-2.44547083809898,
12.5216853356836));
#438113=CARTESIAN_POINT('Ctrl Pts',(-1.23723167991553,-2.44509532378282,
12.5228750347131));
#438114=CARTESIAN_POINT('Ctrl Pts',(-1.23716444822797,-2.44473883009601,
12.5240609649613));
#438115=CARTESIAN_POINT('Ctrl Pts',(-1.23699943165769,-2.44386383546695,
12.5269717671326));
#438116=CARTESIAN_POINT('Ctrl Pts',(-1.23658210549582,-2.44308072764374,
12.5299036066169));
#438117=CARTESIAN_POINT('Ctrl Pts',(-1.2359945034257,-2.44236157819242,
12.5328133004019));
#438118=CARTESIAN_POINT('Ctrl Pts',(-1.23571242021699,-2.44201634458096,
12.5342101228451));
#438119=CARTESIAN_POINT('Ctrl Pts',(-1.2353910420462,-2.44168661290519,
12.5356023438238));
#438120=CARTESIAN_POINT('Ctrl Pts',(-1.2350384319707,-2.44137282548623,
12.5369868989719));
#438121=CARTESIAN_POINT('Origin',(-10.7595719109441,-10.9101544928126,-1.23977369531144));
#438122=CARTESIAN_POINT('Ctrl Pts',(-1.13870597240883,-2.48772125622983,
12.5369868989719));
#438123=CARTESIAN_POINT('Ctrl Pts',(-1.1395630890155,-2.50303623761445,
12.5369868989719));
#438124=CARTESIAN_POINT('Ctrl Pts',(-1.12548920298435,-2.50913615857057,
12.5369868989719));
#438125=CARTESIAN_POINT('Ctrl Pts',(-1.13899564523504,-2.49289832260301,
12.5218025310015));
#438126=CARTESIAN_POINT('Ctrl Pts',(-1.13631807036062,-2.50440859872906,
12.5216901060418));
#438127=CARTESIAN_POINT('Ctrl Pts',(-1.12553211141151,-2.50911757912156,
12.5161920673677));
#438128=CARTESIAN_POINT('Ctrl Pts',(-1.14408058035852,-2.49613552911253,
12.5042015548896));
#438129=CARTESIAN_POINT('Ctrl Pts',(-1.14148438124073,-2.50202085791889,
12.4980677368514));
#438130=CARTESIAN_POINT('Ctrl Pts',(-1.13529857321621,-2.50483627241908,
12.4907278922778));
#438131=CARTESIAN_POINT('Ctrl Pts',(-1.15499048945561,-2.48857161093493,
12.5064636261921));
#438132=CARTESIAN_POINT('Ctrl Pts',(-1.15774489135786,-2.49450631467633,
12.4999376786892));
#438133=CARTESIAN_POINT('Ctrl Pts',(-1.15771125034352,-2.49443383089918,
12.4906970594712));
#438134=CARTESIAN_POINT('Origin',(-1.11674034567515,-2.48895058214127,12.5369868989719));
#438135=CARTESIAN_POINT('Origin',(-1.11674034567515,-2.48895058214127,14.));
#438136=CARTESIAN_POINT('Origin',(-1.11674034567515,-2.48895058214127,13.7435492065112));
#438137=CARTESIAN_POINT('Ctrl Pts',(-1.13737165154344,-2.46303898681411,
13.793642941384));
#438138=CARTESIAN_POINT('Ctrl Pts',(-1.1379824978865,-2.47383403594557,
13.8071662555867));
#438139=CARTESIAN_POINT('Ctrl Pts',(-1.1213059701016,-2.47728552905356,
13.8103758687955));
#438140=CARTESIAN_POINT('Ctrl Pts',(-1.13826888894079,-2.4796358741812,
13.7804579775006));
#438141=CARTESIAN_POINT('Ctrl Pts',(-1.13901249351036,-2.4929565620003,
13.7901904343351));
#438142=CARTESIAN_POINT('Ctrl Pts',(-1.12430329422377,-2.49860416153562,
13.7927914348263));
#438143=CARTESIAN_POINT('Ctrl Pts',(-1.13879712632548,-2.48940708638739,
13.7597120340895));
#438144=CARTESIAN_POINT('Ctrl Pts',(-1.13965196473683,-2.50482319294067,
13.7635825532445));
#438145=CARTESIAN_POINT('Ctrl Pts',(-1.12604549938884,-2.51117929370123,
13.7651073818884));
#438146=CARTESIAN_POINT('Ctrl Pts',(-1.13869368534948,-2.48749365930215,
13.7381884353898));
#438147=CARTESIAN_POINT('Ctrl Pts',(-1.13952941212877,-2.50254887339484,
13.7368803041982));
#438148=CARTESIAN_POINT('Ctrl Pts',(-1.12570383429319,-2.50871677697964,
13.7363986145813));
#438149=CARTESIAN_POINT('Origin',(-1.11562146849283,-2.46825378521706,13.7902182540695));
#438150=CARTESIAN_POINT('Ctrl Pts',(-1.13565842282151,-2.43134748881746,
13.8235227101244));
#438151=CARTESIAN_POINT('Ctrl Pts',(-1.13628347989388,-2.44282755815418,
13.8358800583119));
#438152=CARTESIAN_POINT('Ctrl Pts',(-1.1201664623594,-2.44668343611514,
13.8390832900376));
#438153=CARTESIAN_POINT('Ctrl Pts',(-1.13630229239036,-2.44325767694664,
13.8124254819053));
#438154=CARTESIAN_POINT('Ctrl Pts',(-1.13692856303695,-2.45476004043042,
13.8247886449157));
#438155=CARTESIAN_POINT('Ctrl Pts',(-1.12078721517006,-2.45860421396217,
13.8279860620657));
#438156=CARTESIAN_POINT('Ctrl Pts',(-1.13694587339782,-2.45516252731703,
13.8013225099955));
#438157=CARTESIAN_POINT('Ctrl Pts',(-1.1375730641211,-2.46668175757036,
13.8136962257787));
#438158=CARTESIAN_POINT('Ctrl Pts',(-1.1214079512921,-2.47051945897964,
13.8168830918626));
#438159=CARTESIAN_POINT('Ctrl Pts',(-1.13758917707139,-2.46706224761251,
13.7902140179785));
#438160=CARTESIAN_POINT('Ctrl Pts',(-1.13821701355319,-2.4785932719771,
13.802602731458));
#438161=CARTESIAN_POINT('Ctrl Pts',(-1.12202867321908,-2.48242938847018,
13.8057746032558));
#438162=CARTESIAN_POINT('Origin',(-1.11369071356699,-2.43253901397857,13.8235269408515));
#438163=CARTESIAN_POINT('Ctrl Pts',(-1.19283550652458,-2.40381648963782,
13.8235269408515));
#438164=CARTESIAN_POINT('Ctrl Pts',(-1.20165610318867,-2.41166592868022,
13.8362179249168));
#438165=CARTESIAN_POINT('Ctrl Pts',(-1.2149234196493,-2.40091226335202,
13.8391868794938));
#438166=CARTESIAN_POINT('Ctrl Pts',(-1.18476504451463,-2.39663459457976,
13.8400110824519));
#438167=CARTESIAN_POINT('Ctrl Pts',(-1.19411123465536,-2.40037232018696,
13.8494522556836));
#438168=CARTESIAN_POINT('Ctrl Pts',(-1.20156702432301,-2.38917682609929,
13.85569149686));
#438169=CARTESIAN_POINT('Ctrl Pts',(-1.16922809060941,-2.39173553452791,
13.8586819406588));
#438170=CARTESIAN_POINT('Ctrl Pts',(-1.17315679192385,-2.38985900858434,
13.868010383617));
#438171=CARTESIAN_POINT('Ctrl Pts',(-1.17573146690084,-2.3811835307557,
13.8744918421245));
#438172=CARTESIAN_POINT('Ctrl Pts',(-1.14101383472849,-2.40526429141955,
13.8587686893867));
#438173=CARTESIAN_POINT('Ctrl Pts',(-1.13712007455004,-2.40712406548985,
13.8680909899357));
#438174=CARTESIAN_POINT('Ctrl Pts',(-1.12876412885016,-2.40370725806675,
13.8745789365163));
#438175=CARTESIAN_POINT('Ctrl Pts',(-1.13507450618019,-2.42054628567277,
13.8400379222776));
#438176=CARTESIAN_POINT('Ctrl Pts',(-1.1321634108241,-2.43017934114523,
13.8494748685453));
#438177=CARTESIAN_POINT('Ctrl Pts',(-1.11876789428566,-2.42902988826086,
13.8557104837033));
#438178=CARTESIAN_POINT('Ctrl Pts',(-1.13565863605493,-2.43135141923588,
13.8235269408542));
#438179=CARTESIAN_POINT('Ctrl Pts',(-1.13629602255157,-2.44314168459525,
13.8362179249195));
#438180=CARTESIAN_POINT('Ctrl Pts',(-1.11961643193484,-2.44680968962724,
13.8391868794965));
#438181=CARTESIAN_POINT('Origin',(-1.20746078112637,-2.38738172943811,13.8235269408515));
#438182=CARTESIAN_POINT('Ctrl Pts',(-1.21955168809193,-2.427591188524,13.7902140241682));
#438183=CARTESIAN_POINT('Ctrl Pts',(-1.22817555722196,-2.43527151902604,
13.8026027327198));
#438184=CARTESIAN_POINT('Ctrl Pts',(-1.2412680137648,-2.42500674850023,
13.8057746032556));
#438185=CARTESIAN_POINT('Ctrl Pts',(-1.21064920540935,-2.41966887920736,
13.8013225161808));
#438186=CARTESIAN_POINT('Ctrl Pts',(-1.21926425615093,-2.42734135133865,
13.8136962270464));
#438187=CARTESIAN_POINT('Ctrl Pts',(-1.23234346972602,-2.41709572897734,
13.8168830918628));
#438188=CARTESIAN_POINT('Ctrl Pts',(-1.20174288478636,-2.4117431545119,
13.8124254880875));
#438189=CARTESIAN_POINT('Ctrl Pts',(-1.21034532221329,-2.41940439105412,
13.8247886461868));
#438190=CARTESIAN_POINT('Ctrl Pts',(-1.22341477869207,-2.40918138418004,
13.8279860620656));
#438191=CARTESIAN_POINT('Ctrl Pts',(-1.19283257084815,-2.40381387616973,
13.8235227163065));
#438192=CARTESIAN_POINT('Ctrl Pts',(-1.2014183346621,-2.41146026374608,
13.8358800595848));
#438193=CARTESIAN_POINT('Ctrl Pts',(-1.21448177232259,-2.40126357667191,
13.8390832900376));
#438194=CARTESIAN_POINT('Origin',(-1.23417990766361,-2.41115905006698,13.7902182540695));
#438195=CARTESIAN_POINT('Ctrl Pts',(-1.23483685563678,-2.44119340600829,
13.7382347919292));
#438196=CARTESIAN_POINT('Ctrl Pts',(-1.24609387954608,-2.45124314637504,
13.7369371795942));
#438197=CARTESIAN_POINT('Ctrl Pts',(-1.25954281517536,-2.44426676425679,
13.7364597369711));
#438198=CARTESIAN_POINT('Ctrl Pts',(-1.23624991501483,-2.44245088649656,
13.7595490285574));
#438199=CARTESIAN_POINT('Ctrl Pts',(-1.2477761914503,-2.4527396550308,13.7633824266926));
#438200=CARTESIAN_POINT('Ctrl Pts',(-1.26123381543314,-2.44604741945186,
13.7648920890506));
#438201=CARTESIAN_POINT('Ctrl Pts',(-1.22904338959518,-2.43603780490276,
13.780380659011));
#438202=CARTESIAN_POINT('Ctrl Pts',(-1.23900961120005,-2.44494124878293,
13.7901039518743));
#438203=CARTESIAN_POINT('Ctrl Pts',(-1.25261021923682,-2.43697200148753,
13.7926933640892));
#438204=CARTESIAN_POINT('Ctrl Pts',(-1.21651683976832,-2.42489043745532,
13.7936647693663));
#438205=CARTESIAN_POINT('Ctrl Pts',(-1.22457637590267,-2.4321027331539,
13.8072068914933));
#438206=CARTESIAN_POINT('Ctrl Pts',(-1.23767985776185,-2.42119663242936,
13.8104111085397));
#438207=CARTESIAN_POINT('Origin',(-1.24966370657249,-2.42493806528651,13.7435492065112));
#438208=CARTESIAN_POINT('Origin',(-1.24966370657249,-2.42493806528651,14.));
#438209=CARTESIAN_POINT('Origin',(-1.24966370657249,-2.42493806528651,12.5369868989719));
#438210=CARTESIAN_POINT('Ctrl Pts',(-1.22551956306621,-2.45460839468648,
12.506462012331));
#438211=CARTESIAN_POINT('Ctrl Pts',(-1.22844032095039,-2.46045841702592,
12.4999388158272));
#438212=CARTESIAN_POINT('Ctrl Pts',(-1.22840576455428,-2.46038920358981,
12.4907030323752));
#438213=CARTESIAN_POINT('Ctrl Pts',(-1.23823453712172,-2.45079289761245,
12.5042014951932));
#438214=CARTESIAN_POINT('Ctrl Pts',(-1.24445160750402,-2.45243275522135,
12.4980716682127));
#438215=CARTESIAN_POINT('Ctrl Pts',(-1.25050600860596,-2.44935545242138,
12.4907355092743));
#438216=CARTESIAN_POINT('Ctrl Pts',(-1.23887623627451,-2.44480007495175,
12.5218047446509));
#438217=CARTESIAN_POINT('Ctrl Pts',(-1.24954002296379,-2.44987969347884,
12.5216906929434));
#438218=CARTESIAN_POINT('Ctrl Pts',(-1.25994304277591,-2.44438898012643,
12.5161988840776));
#438219=CARTESIAN_POINT('Ctrl Pts',(-1.23500975610474,-2.44134726196669,
12.5369868989719));
#438220=CARTESIAN_POINT('Ctrl Pts',(-1.24644390075447,-2.45155832790758,
12.5369868989719));
#438221=CARTESIAN_POINT('Ctrl Pts',(-1.25998281969171,-2.44436783379859,
12.5369868989719));
#438222=CARTESIAN_POINT('Origin',(-2.2353094088441E-31,-9.79353041666015E-31,
12.5));
#438223=CARTESIAN_POINT('Origin',(-0.992933084929622,-2.49304515609577,
12.5));
#438224=CARTESIAN_POINT('',(-0.992933084929622,-2.49304515609577,12.5893111709658));
#438225=CARTESIAN_POINT('',(-0.992933084929622,-2.49304515609577,13.8235269408515));
#438226=CARTESIAN_POINT('',(-0.992933084929622,-2.49304515609577,12.5));
#438227=CARTESIAN_POINT('',(-1.01762523340836,-2.51892121651279,13.7902182540695));
#438228=CARTESIAN_POINT('',(-0.992933084929622,-2.49304515609577,13.8235269408515));
#438229=CARTESIAN_POINT('',(-1.03193439359516,-2.53391645655153,13.7435492065112));
#438230=CARTESIAN_POINT('Origin',(-0.984857210047735,-2.48458253992091,
13.7445212918699));
#438231=CARTESIAN_POINT('',(-1.03193439359516,-2.53391645655153,12.5369868989719));
#438232=CARTESIAN_POINT('',(-1.03193439359516,-2.53391645655153,12.5));
#438233=CARTESIAN_POINT('Ctrl Pts',(-1.03193439359516,-2.53391645655153,
12.5369868989719));
#438234=CARTESIAN_POINT('Ctrl Pts',(-1.01894343910079,-2.52030262607984,
12.5544431401645));
#438235=CARTESIAN_POINT('Ctrl Pts',(-1.00594319313049,-2.50667905863477,
12.5718848856037));
#438236=CARTESIAN_POINT('Ctrl Pts',(-0.992933084929622,-2.49304515609577,
12.5893111709658));
#438237=CARTESIAN_POINT('Origin',(-0.926115282099995,-2.79072334525639,
12.5));
#438238=CARTESIAN_POINT('',(-0.932143531606444,-2.57230045639142,13.7435492065112));
#438239=CARTESIAN_POINT('',(-0.932715358484657,-2.55158132747411,13.7902182540695));
#438240=CARTESIAN_POINT('Origin',(-0.934218020689041,-2.4971350376651,13.7418732680449));
#438241=CARTESIAN_POINT('',(-0.93370211340225,-2.51582801973994,13.8235269408515));
#438242=CARTESIAN_POINT('',(-0.932715358484657,-2.55158132747411,13.7902182540695));
#438243=CARTESIAN_POINT('',(-0.93370211340225,-2.51582801973994,12.5893111709658));
#438244=CARTESIAN_POINT('',(-0.93370211340225,-2.51582801973994,12.5));
#438245=CARTESIAN_POINT('',(-0.932143531606444,-2.57230045639142,12.5369868989719));
#438246=CARTESIAN_POINT('Ctrl Pts',(-0.93370211340225,-2.51582801973994,
12.5893111709658));
#438247=CARTESIAN_POINT('Ctrl Pts',(-0.933182199622504,-2.53466616995441,
12.5718848856037));
#438248=CARTESIAN_POINT('Ctrl Pts',(-0.932662679960124,-2.55349004002779,
12.5544431401645));
#438249=CARTESIAN_POINT('Ctrl Pts',(-0.932143531606444,-2.57230045639142,
12.5369868989719));
#438250=CARTESIAN_POINT('',(-0.932143531606444,-2.57230045639142,12.5));
#438251=CARTESIAN_POINT('Origin',(-0.968064029091806,-2.51677637365273,
12.5));
#438252=CARTESIAN_POINT('',(-0.956775034650937,-2.48430871625815,13.8587068136939));
#438253=CARTESIAN_POINT('Ctrl Pts',(-0.933702113395648,-2.51582801973962,
13.8235269408542));
#438254=CARTESIAN_POINT('Ctrl Pts',(-0.93375045663856,-2.5140763883977,
13.8262006681044));
#438255=CARTESIAN_POINT('Ctrl Pts',(-0.933973602084865,-2.51228864285042,
13.8288634856214));
#438256=CARTESIAN_POINT('Ctrl Pts',(-0.934358865203114,-2.51046889511799,
13.8314912288862));
#438257=CARTESIAN_POINT('Ctrl Pts',(-0.934756031739981,-2.50859292290412,
13.834200161153));
#438258=CARTESIAN_POINT('Ctrl Pts',(-0.935325443606471,-2.50668075376416,
13.8368750301949));
#438259=CARTESIAN_POINT('Ctrl Pts',(-0.93609708987527,-2.50472606935137,
13.8394886372968));
#438260=CARTESIAN_POINT('Ctrl Pts',(-0.936156685988365,-2.50457510433276,
13.839690492513));
#438261=CARTESIAN_POINT('Ctrl Pts',(-0.936217510093172,-2.50442389017867,
13.8398919674349));
#438262=CARTESIAN_POINT('Ctrl Pts',(-0.936279586968705,-2.50427242725917,
13.8400930404591));
#438263=CARTESIAN_POINT('Ctrl Pts',(-0.937246786452742,-2.50191253307414,
13.8432258934518));
#438264=CARTESIAN_POINT('Ctrl Pts',(-0.938512128561357,-2.49950386409913,
13.8462331177034));
#438265=CARTESIAN_POINT('Ctrl Pts',(-0.940119744156371,-2.49716984094109,
13.8489036603661));
#438266=CARTESIAN_POINT('Ctrl Pts',(-0.940645774687823,-2.49640612140139,
13.8497774930041));
#438267=CARTESIAN_POINT('Ctrl Pts',(-0.941208445707454,-2.49565064387015,
13.85061494757));
#438268=CARTESIAN_POINT('Ctrl Pts',(-0.941809274587624,-2.49490844552581,
13.8514076489583));
#438269=CARTESIAN_POINT('Ctrl Pts',(-0.94308011432168,-2.49333858898651,
13.8530843267192));
#438270=CARTESIAN_POINT('Ctrl Pts',(-0.944648794985787,-2.49167580124265,
13.8546805203176));
#438271=CARTESIAN_POINT('Ctrl Pts',(-0.946523520273043,-2.49011022213736,
13.8559412814273));
#438272=CARTESIAN_POINT('Ctrl Pts',(-0.946774419315257,-2.48990069688014,
13.8561100121513));
#438273=CARTESIAN_POINT('Ctrl Pts',(-0.947030724246209,-2.48969289973054,
13.8562727473908));
#438274=CARTESIAN_POINT('Ctrl Pts',(-0.94729238217205,-2.48948726437471,
13.8564289040185));
#438275=CARTESIAN_POINT('Ctrl Pts',(-0.948478997880653,-2.48855471038203,
13.8571370725437));
#438276=CARTESIAN_POINT('Ctrl Pts',(-0.94979796794662,-2.48765201425111,
13.8577210840554));
#438277=CARTESIAN_POINT('Ctrl Pts',(-0.951214599174453,-2.48683848301476,
13.8581177131616));
#438278=CARTESIAN_POINT('Ctrl Pts',(-0.951613571287177,-2.48660936461771,
13.8582294175695));
#438279=CARTESIAN_POINT('Ctrl Pts',(-0.952020172770695,-2.48638718488984,
13.8583265086086));
#438280=CARTESIAN_POINT('Ctrl Pts',(-0.952433359538227,-2.48617292107015,
13.8584082369006));
#438281=CARTESIAN_POINT('Ctrl Pts',(-0.953026998122757,-2.48586508141838,
13.8585256585398));
#438282=CARTESIAN_POINT('Ctrl Pts',(-0.953641759216969,-2.48557004164507,
13.8586122832068));
#438283=CARTESIAN_POINT('Ctrl Pts',(-0.954262014788582,-2.48529617797002,
13.8586682984299));
#438284=CARTESIAN_POINT('Ctrl Pts',(-0.954758157761914,-2.48507711417722,
13.8587131050557));
#438285=CARTESIAN_POINT('Ctrl Pts',(-0.95526320152162,-2.48486896566403,
13.8587357943552));
#438286=CARTESIAN_POINT('Ctrl Pts',(-0.955777399059998,-2.48467217593436,
13.8587355499465));
#438287=CARTESIAN_POINT('Ctrl Pts',(-0.956109737188121,-2.48454498604038,
13.8587353919793));
#438288=CARTESIAN_POINT('Ctrl Pts',(-0.956442291482867,-2.48442388039903,
13.8587257282814));
#438289=CARTESIAN_POINT('Ctrl Pts',(-0.956775034650937,-2.48430871625814,
13.8587068136939));
#438290=CARTESIAN_POINT('Ctrl Pts',(-0.956775034650937,-2.48430871625814,
13.8587068136939));
#438291=CARTESIAN_POINT('Ctrl Pts',(-0.957869408790883,-2.48392994767706,
13.8586446046466));
#438292=CARTESIAN_POINT('Ctrl Pts',(-0.958965824211619,-2.48361536978293,
13.858482427929));
#438293=CARTESIAN_POINT('Ctrl Pts',(-0.960063345219124,-2.48336061102754,
13.8582284286032));
#438294=CARTESIAN_POINT('Ctrl Pts',(-0.961189274103965,-2.48309925817926,
13.8579678548414));
#438295=CARTESIAN_POINT('Ctrl Pts',(-0.962319463209768,-2.48290171479365,
13.857615680862));
#438296=CARTESIAN_POINT('Ctrl Pts',(-0.96340768732622,-2.48276622390876,
13.8571944833187));
#438297=CARTESIAN_POINT('Ctrl Pts',(-0.966123461903261,-2.48242809254866,
13.8561433417727));
#438298=CARTESIAN_POINT('Ctrl Pts',(-0.96870432018962,-2.48245585067075,
13.8546163505474));
#438299=CARTESIAN_POINT('Ctrl Pts',(-0.971016065270771,-2.48269217995195,
13.8528973491086));
#438300=CARTESIAN_POINT('Ctrl Pts',(-0.971438386990478,-2.48273535382492,
13.8525833129072));
#438301=CARTESIAN_POINT('Ctrl Pts',(-0.971851805046089,-2.48278537047581,
13.8522628768812));
#438302=CARTESIAN_POINT('Ctrl Pts',(-0.972255621678871,-2.48284113856929,
13.851937733538));
#438303=CARTESIAN_POINT('Ctrl Pts',(-0.974721673828254,-2.48318170657871,
13.8499521282529));
#438304=CARTESIAN_POINT('Ctrl Pts',(-0.977074174142894,-2.48377465343844,
13.847639871647));
#438305=CARTESIAN_POINT('Ctrl Pts',(-0.979209119630498,-2.48451091184536,
13.8452109780794));
#438306=CARTESIAN_POINT('Ctrl Pts',(-0.980169675796545,-2.48484216974243,
13.8441181685877));
#438307=CARTESIAN_POINT('Ctrl Pts',(-0.981086646874305,-2.48520188224661,
13.8430021611332));
#438308=CARTESIAN_POINT('Ctrl Pts',(-0.981953344580685,-2.48557832776729,
13.8418824960098));
#438309=CARTESIAN_POINT('Ctrl Pts',(-0.983995739857683,-2.48646543124966,
13.8392439765549));
#438310=CARTESIAN_POINT('Ctrl Pts',(-0.985858098390244,-2.48748439486929,
13.8364981347964));
#438311=CARTESIAN_POINT('Ctrl Pts',(-0.987561770866305,-2.48860789258945,
13.8336931113419));
#438312=CARTESIAN_POINT('Ctrl Pts',(-0.989221039664782,-2.48970210802017,
13.8309611966328));
#438313=CARTESIAN_POINT('Ctrl Pts',(-0.990731138435674,-2.49089704719818,
13.8281701127186));
#438314=CARTESIAN_POINT('Ctrl Pts',(-0.9920797025165,-2.49219015434749,
13.8253580685121));
#438315=CARTESIAN_POINT('Ctrl Pts',(-0.992372072664643,-2.49247050137303,
13.8247484142933));
#438316=CARTESIAN_POINT('Ctrl Pts',(-0.992656681052636,-2.49275549951013,
13.8241378483365));
#438317=CARTESIAN_POINT('Ctrl Pts',(-0.992933084929622,-2.49304515609577,
13.8235269408515));
#438318=CARTESIAN_POINT('',(-0.955609389251859,-2.4847377240223,12.5969504640361));
#438319=CARTESIAN_POINT('Origin',(-0.968076089596869,-2.51680718318092,
12.584524458991));
#438320=CARTESIAN_POINT('Origin',(-0.968076089596869,-2.51680718318092,
12.584524458991));
#438321=CARTESIAN_POINT('Ctrl Pts',(-0.93370211340225,-2.51582801973994,
12.5893111709658));
#438322=CARTESIAN_POINT('Ctrl Pts',(-0.934014800084356,-2.50449837448519,
12.5770542771492));
#438323=CARTESIAN_POINT('Ctrl Pts',(-0.950170633310224,-2.50189208830887,
12.5737548217797));
#438324=CARTESIAN_POINT('Ctrl Pts',(-0.933018372569254,-2.54060215157013,
12.5663937883685));
#438325=CARTESIAN_POINT('Ctrl Pts',(-0.933331458126653,-2.52925805377942,
12.5540940315304));
#438326=CARTESIAN_POINT('Ctrl Pts',(-0.949537866425113,-2.52664686145088,
12.5508374392248));
#438327=CARTESIAN_POINT('Ctrl Pts',(-0.932335321622376,-2.565351286605,
12.5434499600945));
#438328=CARTESIAN_POINT('Ctrl Pts',(-0.932649425132359,-2.55397030511269,
12.5311293540533));
#438329=CARTESIAN_POINT('Ctrl Pts',(-0.948904538284701,-2.55137741850342,
12.5278936106989));
#438330=CARTESIAN_POINT('Ctrl Pts',(-0.931652906521892,-2.59007738287778,
12.5204817579905));
#438331=CARTESIAN_POINT('Ctrl Pts',(-0.931968564629642,-2.57864007330484,
12.5081597038247));
#438332=CARTESIAN_POINT('Ctrl Pts',(-0.948270678662287,-2.5760856412816,
12.5049254088044));
#438333=CARTESIAN_POINT('Ctrl Pts',(-0.932143531606444,-2.57230045639142,
12.5369868989719));
#438334=CARTESIAN_POINT('Ctrl Pts',(-0.932117832969429,-2.5732316066214,
12.5342545179733));
#438335=CARTESIAN_POINT('Ctrl Pts',(-0.932218005951635,-2.57412369545498,
12.5314872231885));
#438336=CARTESIAN_POINT('Ctrl Pts',(-0.932493959424984,-2.57492023220284,
12.5287124745063));
#438337=CARTESIAN_POINT('Ctrl Pts',(-0.932742827964356,-2.5756385885786,
12.5262100684184));
#438338=CARTESIAN_POINT('Ctrl Pts',(-0.933135342868856,-2.57627818250249,
12.5237004536639));
#438339=CARTESIAN_POINT('Ctrl Pts',(-0.933734743370431,-2.57681532271708,
12.5212220730815));
#438340=CARTESIAN_POINT('Ctrl Pts',(-0.934193636306667,-2.5772265500177,
12.5193246583486));
#438341=CARTESIAN_POINT('Ctrl Pts',(-0.934779697513991,-2.57758216903345,
12.517417831369));
#438342=CARTESIAN_POINT('Ctrl Pts',(-0.935558777218661,-2.57781064117019,
12.5155812248348));
#438343=CARTESIAN_POINT('Ctrl Pts',(-0.935890669360424,-2.57790797152848,
12.5147988205793));
#438344=CARTESIAN_POINT('Ctrl Pts',(-0.93625784957137,-2.57798259183014,
12.5140295443047));
#438345=CARTESIAN_POINT('Ctrl Pts',(-0.936666065081868,-2.5780309948241,
12.5132817086137));
#438346=CARTESIAN_POINT('Ctrl Pts',(-0.937283844034861,-2.57810424620765,
12.5121499604604));
#438347=CARTESIAN_POINT('Ctrl Pts',(-0.938009787583041,-2.57811193267073,
12.5110494206568));
#438348=CARTESIAN_POINT('Ctrl Pts',(-0.938856251542312,-2.57801892256721,
12.5100666561695));
#438349=CARTESIAN_POINT('Ctrl Pts',(-0.939342289198491,-2.57796551637995,
12.5095023550641));
#438350=CARTESIAN_POINT('Ctrl Pts',(-0.939873607218879,-2.57787764433308,
12.5089719619137));
#438351=CARTESIAN_POINT('Ctrl Pts',(-0.940439204480263,-2.57775065210944,
12.5085043804652));
#438352=CARTESIAN_POINT('Ctrl Pts',(-0.941266882398073,-2.57756481553203,
12.5078201359221));
#438353=CARTESIAN_POINT('Ctrl Pts',(-0.9421917084627,-2.57728863667177,
12.5072563000949));
#438354=CARTESIAN_POINT('Ctrl Pts',(-0.943148570635696,-2.57693272436758,
12.5068768744332));
#438355=CARTESIAN_POINT('Ctrl Pts',(-0.943838534133043,-2.57667608709517,
12.5066032824114));
#438356=CARTESIAN_POINT('Ctrl Pts',(-0.944557297050483,-2.57637354075296,
12.5064197834844));
#438357=CARTESIAN_POINT('Ctrl Pts',(-0.945265724617955,-2.57604436271765,
12.5063282718343));
#438358=CARTESIAN_POINT('Ctrl Pts',(-0.946299809542831,-2.57556386469705,
12.5061946931565));
#438359=CARTESIAN_POINT('Ctrl Pts',(-0.947334422912381,-2.57501731583782,
12.5062515701262));
#438360=CARTESIAN_POINT('Ctrl Pts',(-0.948312578200474,-2.57445230977494,
12.5064436508398));
#438361=CARTESIAN_POINT('',(-0.950170633310224,-2.50189208830887,12.5737548217797));
#438362=CARTESIAN_POINT('Origin',(-0.955693739443566,-2.51643496624412,
12.5893111709658));
#438363=CARTESIAN_POINT('Ctrl Pts',(-0.948312578200474,-2.57445230977494,
12.5064436508398));
#438364=CARTESIAN_POINT('Ctrl Pts',(-0.948588098914043,-2.56371152413852,
12.5164271754438));
#438365=CARTESIAN_POINT('Ctrl Pts',(-0.948863519977009,-2.55296647549931,
12.5264061185523));
#438366=CARTESIAN_POINT('Ctrl Pts',(-0.949138838825944,-2.5422170137422,
12.536380305637));
#438367=CARTESIAN_POINT('Ctrl Pts',(-0.949482931546433,-2.52878236677158,
12.5488460165097));
#438368=CARTESIAN_POINT('Ctrl Pts',(-0.949826864686682,-2.51534082257244,
12.5613043021964));
#438369=CARTESIAN_POINT('Ctrl Pts',(-0.950170633310223,-2.50189208830887,
12.5737548217797));
#438370=CARTESIAN_POINT('Ctrl Pts',(-0.992933084929621,-2.49304515609577,
12.5893111709658));
#438371=CARTESIAN_POINT('Ctrl Pts',(-0.985108542234949,-2.48484545084625,
12.5770542771492));
#438372=CARTESIAN_POINT('Ctrl Pts',(-0.971370553186003,-2.49373765708239,
12.5737548217797));
#438373=CARTESIAN_POINT('Ctrl Pts',(-0.985632854649774,-2.48539490241525,
12.5928319619712));
#438374=CARTESIAN_POINT('Ctrl Pts',(-0.978017420927295,-2.482133217944,
12.5821634970843));
#438375=CARTESIAN_POINT('Ctrl Pts',(-0.96871808466295,-2.49094433860724,
12.5773203894503));
#438376=CARTESIAN_POINT('Ctrl Pts',(-0.970068171356415,-2.47920420509449,
12.5969440695591));
#438377=CARTESIAN_POINT('Ctrl Pts',(-0.966309852465797,-2.48063024214462,
12.5878292599214));
#438378=CARTESIAN_POINT('Ctrl Pts',(-0.963169757777886,-2.48873974887805,
12.5813877129824));
#438379=CARTESIAN_POINT('Ctrl Pts',(-0.941491577049632,-2.49013825756221,
12.596957478804));
#438380=CARTESIAN_POINT('Ctrl Pts',(-0.945222149392466,-2.48872283425317,
12.5878468778671));
#438381=CARTESIAN_POINT('Ctrl Pts',(-0.952943930223114,-2.49265876905205,
12.5814011370086));
#438382=CARTESIAN_POINT('Ctrl Pts',(-0.933994270954195,-2.50524221096691,
12.5928371701607));
#438383=CARTESIAN_POINT('Ctrl Pts',(-0.937463935307683,-2.49772579593194,
12.5821692192952));
#438384=CARTESIAN_POINT('Ctrl Pts',(-0.950267525571416,-2.49802894329946,
12.5773318885715));
#438385=CARTESIAN_POINT('Ctrl Pts',(-0.933702113402194,-2.51582801973994,
12.5893111709658));
#438386=CARTESIAN_POINT('Ctrl Pts',(-0.934014800084301,-2.50449837448519,
12.5770542771492));
#438387=CARTESIAN_POINT('Ctrl Pts',(-0.950170633310168,-2.50189208830886,
12.5737548217797));
#438388=CARTESIAN_POINT('',(-0.971370553186003,-2.49373765708239,12.5737548217797));
#438389=CARTESIAN_POINT('Origin',(-0.977016889193419,-2.50823313533222,
12.5893111709658));
#438390=CARTESIAN_POINT('Ctrl Pts',(-0.950170633310168,-2.50189208830886,
12.5737548217797));
#438391=CARTESIAN_POINT('Ctrl Pts',(-0.950165593066157,-2.50088994349549,
12.5746934679442));
#438392=CARTESIAN_POINT('Ctrl Pts',(-0.950343197672823,-2.49978008222401,
12.5756680099006));
#438393=CARTESIAN_POINT('Ctrl Pts',(-0.950679952599606,-2.49868824900081,
12.5765688348656));
#438394=CARTESIAN_POINT('Ctrl Pts',(-0.95076910473847,-2.49839919824197,
12.5768073183026));
#438395=CARTESIAN_POINT('Ctrl Pts',(-0.95086915448683,-2.49811139730721,
12.5770407398754));
#438396=CARTESIAN_POINT('Ctrl Pts',(-0.95097912913978,-2.4978270089836,
12.5772674179684));
#438397=CARTESIAN_POINT('Ctrl Pts',(-0.951430435377096,-2.49665995620531,
12.5781976435658));
#438398=CARTESIAN_POINT('Ctrl Pts',(-0.95208503672244,-2.49548815649485,
12.5790594849312));
#438399=CARTESIAN_POINT('Ctrl Pts',(-0.952940890682436,-2.49441428186397,
12.5797571720116));
#438400=CARTESIAN_POINT('Ctrl Pts',(-0.953498510311139,-2.49371461392887,
12.580211740231));
#438401=CARTESIAN_POINT('Ctrl Pts',(-0.954181583239703,-2.49303641900513,
12.5806009430798));
#438402=CARTESIAN_POINT('Ctrl Pts',(-0.954954506728614,-2.49244001147281,
12.5808812374708));
#438403=CARTESIAN_POINT('Ctrl Pts',(-0.955618704420289,-2.4919274995464,
12.5811221033394));
#438404=CARTESIAN_POINT('Ctrl Pts',(-0.956362919973353,-2.49146498147834,
12.581287365893));
#438405=CARTESIAN_POINT('Ctrl Pts',(-0.957149549864385,-2.49108564429589,
12.581359338449));
#438406=CARTESIAN_POINT('Ctrl Pts',(-0.95725887517595,-2.49103292426054,
12.5813693411482));
#438407=CARTESIAN_POINT('Ctrl Pts',(-0.957369013185351,-2.49098175136691,
12.5813775999465));
#438408=CARTESIAN_POINT('Ctrl Pts',(-0.957479857324108,-2.4909321536191,
12.5813841266931));
#438409=CARTESIAN_POINT('Ctrl Pts',(-0.957667917811834,-2.49084800504121,
12.5813952001081));
#438410=CARTESIAN_POINT('Ctrl Pts',(-0.957859519130497,-2.49076838274033,
12.5814007534795));
#438411=CARTESIAN_POINT('Ctrl Pts',(-0.958054653510005,-2.49069350350569,
12.5814005856065));
#438412=CARTESIAN_POINT('Ctrl Pts',(-0.958947902406796,-2.49035073564537,
12.5813998171494));
#438413=CARTESIAN_POINT('Ctrl Pts',(-0.95985334729205,-2.49013072391739,
12.58127954464));
#438414=CARTESIAN_POINT('Ctrl Pts',(-0.960758861092978,-2.49000596469546,
12.5810700125799));
#438415=CARTESIAN_POINT('Ctrl Pts',(-0.961852618663497,-2.48985526976033,
12.5808169217085));
#438416=CARTESIAN_POINT('Ctrl Pts',(-0.962948859924826,-2.48986011294288,
12.5804173076348));
#438417=CARTESIAN_POINT('Ctrl Pts',(-0.963951627200476,-2.48999402768643,
12.5799304713245));
#438418=CARTESIAN_POINT('Ctrl Pts',(-0.965194371759275,-2.49015999024118,
12.5793271277669));
#438419=CARTESIAN_POINT('Ctrl Pts',(-0.966374901528837,-2.49050257201474,
12.5785808224116));
#438420=CARTESIAN_POINT('Ctrl Pts',(-0.967452294259638,-2.49097687230634,
12.5777485681082));
#438421=CARTESIAN_POINT('Ctrl Pts',(-0.969057727465717,-2.49168363170431,
12.576508418016));
#438422=CARTESIAN_POINT('Ctrl Pts',(-0.970423403313072,-2.49267062156785,
12.5750928681475));
#438423=CARTESIAN_POINT('Ctrl Pts',(-0.971370553186003,-2.49373765708239,
12.5737548217797));
#438424=CARTESIAN_POINT('Ctrl Pts',(-0.971370553186003,-2.49373765708239,
12.5737548217797));
#438425=CARTESIAN_POINT('Ctrl Pts',(-0.985108542234949,-2.48484545084625,
12.5770542771492));
#438426=CARTESIAN_POINT('Ctrl Pts',(-0.992933084929622,-2.49304515609577,
12.5893111709658));
#438427=CARTESIAN_POINT('Ctrl Pts',(-0.988426831596606,-2.51168475492439,
12.5508408821982));
#438428=CARTESIAN_POINT('Ctrl Pts',(-1.00220563854764,-2.50276229990149,
12.55409748406));
#438429=CARTESIAN_POINT('Ctrl Pts',(-1.01004016335483,-2.51097246587486,
12.5663972313419));
#438430=CARTESIAN_POINT('Ctrl Pts',(-1.0054673031628,-2.52961350816027,
12.52790050457));
#438431=CARTESIAN_POINT('Ctrl Pts',(-1.01926998985148,-2.52064483392629,
12.5311362602938));
#438432=CARTESIAN_POINT('Ctrl Pts',(-1.02712998354897,-2.52888168994422,
12.5434568539655));
#438433=CARTESIAN_POINT('Ctrl Pts',(-1.02249320631727,-2.5475253328616,
12.5049357605811));
#438434=CARTESIAN_POINT('Ctrl Pts',(-1.03630500964622,-2.53849663008702,
12.5081700652078));
#438435=CARTESIAN_POINT('Ctrl Pts',(-1.04420389718021,-2.54677424478032,
12.5204921097672));
#438436=CARTESIAN_POINT('Ctrl Pts',(-1.02137521992701,-2.54634917114605,
12.5064436508395));
#438437=CARTESIAN_POINT('Ctrl Pts',(-1.02256844577703,-2.54609410279946,
12.5062361689309));
#438438=CARTESIAN_POINT('Ctrl Pts',(-1.02379842633536,-2.5457779707913,
12.5061871075061));
#438439=CARTESIAN_POINT('Ctrl Pts',(-1.02496988580871,-2.54540554718385,
12.5063648335164));
#438440=CARTESIAN_POINT('Ctrl Pts',(-1.02550203496013,-2.5452363694093,
12.5064455676329));
#438441=CARTESIAN_POINT('Ctrl Pts',(-1.02602946369528,-2.54505300601871,
12.506574497099));
#438442=CARTESIAN_POINT('Ctrl Pts',(-1.02652921234473,-2.54486232641351,
12.5067492519495));
#438443=CARTESIAN_POINT('Ctrl Pts',(-1.02753347665467,-2.54447914834519,
12.5071004286051));
#438444=CARTESIAN_POINT('Ctrl Pts',(-1.028462597074,-2.54405158242217,12.5076537929613));
#438445=CARTESIAN_POINT('Ctrl Pts',(-1.02925079228227,-2.54362031201972,
12.5083435010505));
#438446=CARTESIAN_POINT('Ctrl Pts',(-1.02930041388091,-2.5435931609706,
12.5083869222964));
#438447=CARTESIAN_POINT('Ctrl Pts',(-1.02934947661137,-2.54356598180801,
12.5084308732337));
#438448=CARTESIAN_POINT('Ctrl Pts',(-1.02939796432575,-2.54353877920501,
12.5084753333615));
#438449=CARTESIAN_POINT('Ctrl Pts',(-1.02978689979309,-2.54332057842475,
12.5088319622689));
#438450=CARTESIAN_POINT('Ctrl Pts',(-1.03014736506458,-2.5430975647324,
12.509227847131));
#438451=CARTESIAN_POINT('Ctrl Pts',(-1.03047011482179,-2.54287875066362,
12.5096423454524));
#438452=CARTESIAN_POINT('Ctrl Pts',(-1.03148146971781,-2.54219308421511,
12.5109411997424));
#438453=CARTESIAN_POINT('Ctrl Pts',(-1.03219011954864,-2.54151448454895,
12.5124831113042));
#438454=CARTESIAN_POINT('Ctrl Pts',(-1.03268346387674,-2.54087924455539,
12.5140723025008));
#438455=CARTESIAN_POINT('Ctrl Pts',(-1.03272969078062,-2.54081972187223,
12.5142212114565));
#438456=CARTESIAN_POINT('Ctrl Pts',(-1.03277405691508,-2.54076058089929,
12.5143705582413));
#438457=CARTESIAN_POINT('Ctrl Pts',(-1.03281665103131,-2.54070185362042,
12.5145201959299));
#438458=CARTESIAN_POINT('Ctrl Pts',(-1.03336383587027,-2.53994741428748,
12.5164425148273));
#438459=CARTESIAN_POINT('Ctrl Pts',(-1.0336460216623,-2.53924170261964,
12.518463520594));
#438460=CARTESIAN_POINT('Ctrl Pts',(-1.03375236064752,-2.53857093976959,
12.5205025929157));
#438461=CARTESIAN_POINT('Ctrl Pts',(-1.03381404147384,-2.53818187073,12.5216853356836));
#438462=CARTESIAN_POINT('Ctrl Pts',(-1.03381692551923,-2.53780533861075,
12.5228750347131));
#438463=CARTESIAN_POINT('Ctrl Pts',(-1.03377897508456,-2.53744455112058,
12.5240609649613));
#438464=CARTESIAN_POINT('Ctrl Pts',(-1.03368582777863,-2.53655901758155,
12.5269717671327));
#438465=CARTESIAN_POINT('Ctrl Pts',(-1.03333372079274,-2.53574449952855,
12.5299036066169));
#438466=CARTESIAN_POINT('Ctrl Pts',(-1.03280669127657,-2.53497984796395,
12.532813300402));
#438467=CARTESIAN_POINT('Ctrl Pts',(-1.0325536864208,-2.53461277068862,
12.5342101228452));
#438468=CARTESIAN_POINT('Ctrl Pts',(-1.03226025380202,-2.53425794086336,
12.5356023438238));
#438469=CARTESIAN_POINT('Ctrl Pts',(-1.03193439359517,-2.53391645655153,
12.5369868989719));
#438470=CARTESIAN_POINT('Origin',(-9.8341648617864,-11.7505157552943,-1.23926451155288));
#438471=CARTESIAN_POINT('Ctrl Pts',(-0.932144644962174,-2.57225867695425,
12.5369868989719));
#438472=CARTESIAN_POINT('Ctrl Pts',(-0.931750596423733,-2.58759256196211,
12.5369868989719));
#438473=CARTESIAN_POINT('Ctrl Pts',(-0.917226339900628,-2.5925250335673,
12.5369868989719));
#438474=CARTESIAN_POINT('Ctrl Pts',(-0.93201137495496,-2.57744212809063,
12.5218025310015));
#438475=CARTESIAN_POINT('Ctrl Pts',(-0.928404515129539,-2.58869585751265,
12.5216901060417));
#438476=CARTESIAN_POINT('Ctrl Pts',(-0.917270619951127,-2.59251001337502,
12.5161920673678));
#438477=CARTESIAN_POINT('Ctrl Pts',(-0.936815527993009,-2.58108303248129,
12.5042015548895));
#438478=CARTESIAN_POINT('Ctrl Pts',(-0.93374825857915,-2.58673716401142,
12.4980677368514));
#438479=CARTESIAN_POINT('Ctrl Pts',(-0.927353550901787,-2.58903900967191,
12.4907278922777));
#438480=CARTESIAN_POINT('Ctrl Pts',(-0.948305664819111,-2.57443354149153,
12.506463626192));
#438481=CARTESIAN_POINT('Ctrl Pts',(-0.950567168226204,-2.58057300732139,
12.4999376786891));
#438482=CARTESIAN_POINT('Ctrl Pts',(-0.95053954725031,-2.58049802267305,
12.4906970594712));
#438483=CARTESIAN_POINT('Origin',(-0.910151905565128,-2.57169350988724,
12.5369868989719));
#438484=CARTESIAN_POINT('Origin',(-0.910151905565129,-2.57169350988724,
14.));
#438485=CARTESIAN_POINT('Origin',(-0.910151905565129,-2.57169350988724,
13.7435492065112));
#438486=CARTESIAN_POINT('Ctrl Pts',(-0.932826598035787,-2.54754977621595,
13.793642941384));
#438487=CARTESIAN_POINT('Ctrl Pts',(-0.932555515117465,-2.55835869535974,
13.8071662555867));
#438488=CARTESIAN_POINT('Ctrl Pts',(-0.915653148372656,-2.56043941207733,
13.8103758687955));
#438489=CARTESIAN_POINT('Ctrl Pts',(-0.932368049551305,-2.56416457198688,
13.7804579775006));
#438490=CARTESIAN_POINT('Ctrl Pts',(-0.93202342011753,-2.57750154699185,
13.7901904343352));
#438491=CARTESIAN_POINT('Ctrl Pts',(-0.916902832686253,-2.58193141831023,
13.7927914348263));
#438492=CARTESIAN_POINT('Ctrl Pts',(-0.932098084763358,-2.57394632754132,
13.7597120340895));
#438493=CARTESIAN_POINT('Ctrl Pts',(-0.931693522970168,-2.58938081553827,
13.7635825532445));
#438494=CARTESIAN_POINT('Ctrl Pts',(-0.917614250794026,-2.59460671365573,
13.7651073818884));
#438495=CARTESIAN_POINT('Ctrl Pts',(-0.932150950049518,-2.572030835827,
13.7381884353898));
#438496=CARTESIAN_POINT('Ctrl Pts',(-0.931756756302547,-2.58710407442778,
13.7368803041982));
#438497=CARTESIAN_POINT('Ctrl Pts',(-0.917474440534505,-2.59212454187823,
13.7363986145813));
#438498=CARTESIAN_POINT('Origin',(-0.910723732443341,-2.55097438096993,
13.7902182540695));
#438499=CARTESIAN_POINT('Ctrl Pts',(-0.933702221237335,-2.51582408501885,
13.8235227101244));
#438500=CARTESIAN_POINT('Ctrl Pts',(-0.93338946625715,-2.52731690332603,
13.8358800583119));
#438501=CARTESIAN_POINT('Ctrl Pts',(-0.917011786918914,-2.52984626461901,
13.8390832900376));
#438502=CARTESIAN_POINT('Ctrl Pts',(-0.933373157481985,-2.52774712432683,
13.8124254819052));
#438503=CARTESIAN_POINT('Ctrl Pts',(-0.933059794858003,-2.53926226151667,
13.8247886449157));
#438504=CARTESIAN_POINT('Ctrl Pts',(-0.916658820164166,-2.541777974178,
13.8279860620657));
#438505=CARTESIAN_POINT('Ctrl Pts',(-0.933044241202318,-2.53966482011645,
13.8013225099955));
#438506=CARTESIAN_POINT('Ctrl Pts',(-0.932730420795263,-2.5511968429479,
13.8136962257787));
#438507=CARTESIAN_POINT('Ctrl Pts',(-0.916306287753314,-2.5537041679572,
13.8168830918626));
#438508=CARTESIAN_POINT('Ctrl Pts',(-0.932715466660279,-2.55157738029588,
13.7902140179785));
#438509=CARTESIAN_POINT('Ctrl Pts',(-0.932401328533452,-2.56312121062995,
13.802602731458));
#438510=CARTESIAN_POINT('Ctrl Pts',(-0.915954174459412,-2.5656250627394,
13.8057746032558));
#438511=CARTESIAN_POINT('Origin',(-0.911710487360935,-2.51522107323576,
13.8235269408515));
#438512=CARTESIAN_POINT('Ctrl Pts',(-0.992933084929622,-2.49304515609577,
13.8235269408515));
#438513=CARTESIAN_POINT('Ctrl Pts',(-1.00108452963338,-2.50158743729183,
13.8362179249168));
#438514=CARTESIAN_POINT('Ctrl Pts',(-1.01518422374936,-2.4919509633572,
13.8391868794938));
#438515=CARTESIAN_POINT('Ctrl Pts',(-0.985474867836949,-2.48522934062473,
13.8400110824519));
#438516=CARTESIAN_POINT('Ctrl Pts',(-0.99448529996465,-2.48971643052063,
13.8494522556837));
#438517=CARTESIAN_POINT('Ctrl Pts',(-1.00282881780928,-2.47916590459,13.85569149686));
#438518=CARTESIAN_POINT('Ctrl Pts',(-0.970388930739011,-2.47908017580974,
13.8586819406588));
#438519=CARTESIAN_POINT('Ctrl Pts',(-0.974457513909136,-2.47753011948085,
13.868010383617));
#438520=CARTESIAN_POINT('Ctrl Pts',(-0.977730753849783,-2.46909336850175,
13.8744918421245));
#438521=CARTESIAN_POINT('Ctrl Pts',(-0.941165836185502,-2.4902641930962,
13.8587686893867));
#438522=CARTESIAN_POINT('Ctrl Pts',(-0.937133443320806,-2.49180040131925,
13.8680909899357));
#438523=CARTESIAN_POINT('Ctrl Pts',(-0.929083802866002,-2.48771387589363,
13.8745789365163));
#438524=CARTESIAN_POINT('Ctrl Pts',(-0.934000645860243,-2.50501122735948,
13.8400379222776));
#438525=CARTESIAN_POINT('Ctrl Pts',(-0.93031405348387,-2.51437494833773,
13.8494748685453));
#438526=CARTESIAN_POINT('Ctrl Pts',(-0.917056800502737,-2.51213746120722,
13.8557104837033));
#438527=CARTESIAN_POINT('Ctrl Pts',(-0.933702113395648,-2.51582801973962,
13.8235269408542));
#438528=CARTESIAN_POINT('Ctrl Pts',(-0.933376362959024,-2.52763100688032,
13.8362179249195));
#438529=CARTESIAN_POINT('Ctrl Pts',(-0.916453295841902,-2.52992726544712,
13.8391868794965));
#438530=CARTESIAN_POINT('Origin',(-1.00884928066582,-2.47785717685932,13.8235269408515));
#438531=CARTESIAN_POINT('Ctrl Pts',(-1.01762251193398,-2.51891836345134,
13.7902140241682));
#438532=CARTESIAN_POINT('Ctrl Pts',(-1.02559166761428,-2.52727606368141,
13.8026027327198));
#438533=CARTESIAN_POINT('Ctrl Pts',(-1.03947723417935,-2.51811260508543,
13.8057746032556));
#438534=CARTESIAN_POINT('Ctrl Pts',(-1.00939539328456,-2.51029677998016,
13.8013225161808));
#438535=CARTESIAN_POINT('Ctrl Pts',(-1.01735640044902,-2.51864592920702,
13.8136962270464));
#438536=CARTESIAN_POINT('Ctrl Pts',(-1.0312272073581,-2.50950047563681,
13.8168830918628));
#438537=CARTESIAN_POINT('Ctrl Pts',(-1.00116472785025,-2.50167147966678,
13.8124254880875));
#438538=CARTESIAN_POINT('Ctrl Pts',(-1.00911407947467,-2.51000840258784,
13.8247886461867));
#438539=CARTESIAN_POINT('Ctrl Pts',(-1.02297331838114,-2.50088469395972,
13.8279860620656));
#438540=CARTESIAN_POINT('Ctrl Pts',(-0.99293037204333,-2.49304231203889,
13.8235227163065));
#438541=CARTESIAN_POINT('Ctrl Pts',(-1.00086431586339,-2.50136307634855,
13.8358800595848));
#438542=CARTESIAN_POINT('Ctrl Pts',(-1.01471541067069,-2.49226510935382,
13.8390832900376));
#438543=CARTESIAN_POINT('Origin',(-1.03354142914456,-2.50373323727634,13.7902182540695));
#438544=CARTESIAN_POINT('Ctrl Pts',(-1.03174811234297,-2.53372120373454,
13.7382347919292));
#438545=CARTESIAN_POINT('Ctrl Pts',(-1.04214853229672,-2.54465505637297,
13.7369371795943));
#438546=CARTESIAN_POINT('Ctrl Pts',(-1.05612135761036,-2.53879810069833,
13.7364597369711));
#438547=CARTESIAN_POINT('Ctrl Pts',(-1.03305397354885,-2.53508967751775,
13.7595490285573));
#438548=CARTESIAN_POINT('Ctrl Pts',(-1.04370326709854,-2.54628370955771,
13.7633824266925));
#438549=CARTESIAN_POINT('Ctrl Pts',(-1.05766159127508,-2.54071066312963,
13.7648920890506));
#438550=CARTESIAN_POINT('Ctrl Pts',(-1.02639415293407,-2.52811053620009,
13.7803806590111));
#438551=CARTESIAN_POINT('Ctrl Pts',(-1.03560149942692,-2.53779669418791,
13.7901039518745));
#438552=CARTESIAN_POINT('Ctrl Pts',(-1.04980642019989,-2.53096253972233,
13.7926933640892));
#438553=CARTESIAN_POINT('Ctrl Pts',(-1.01481789810246,-2.51597923059652,
13.7936647693663));
#438554=CARTESIAN_POINT('Ctrl Pts',(-1.02226274774007,-2.52382445499216,
13.8072068914932));
#438555=CARTESIAN_POINT('Ctrl Pts',(-1.03621157730066,-2.51402269883642,
13.8104111085397));
#438556=CARTESIAN_POINT('Origin',(-1.04785058933137,-2.51872847731507,13.7435492065112));
#438557=CARTESIAN_POINT('Origin',(-1.04785058933137,-2.51872847731508,14.));
#438558=CARTESIAN_POINT('Origin',(-1.04785058933137,-2.51872847731508,12.5369868989719));
#438559=CARTESIAN_POINT('Ctrl Pts',(-1.02136837617885,-2.54633210930254,
12.506462012331));
#438560=CARTESIAN_POINT('Ctrl Pts',(-1.0238025843525,-2.55240073505779,
12.4999388158272));
#438561=CARTESIAN_POINT('Ctrl Pts',(-1.02377378447754,-2.55232893525659,
12.4907030323752));
#438562=CARTESIAN_POINT('Ctrl Pts',(-1.03435204063999,-2.54356569640584,
12.5042014951932));
#438563=CARTESIAN_POINT('Ctrl Pts',(-1.04041476061465,-2.54570684647648,
12.4980716682127));
#438564=CARTESIAN_POINT('Ctrl Pts',(-1.04669984494285,-2.54313327304381,
12.4907355092743));
#438565=CARTESIAN_POINT('Ctrl Pts',(-1.03548007527325,-2.53764511880636,
12.5218047446509));
#438566=CARTESIAN_POINT('Ctrl Pts',(-1.04569434302523,-2.54357703293483,
12.5216906929434));
#438567=CARTESIAN_POINT('Ctrl Pts',(-1.05651029175862,-2.53895253216972,
12.5161988840776));
#438568=CARTESIAN_POINT('Ctrl Pts',(-1.03190789680994,-2.53388864074319,
12.5369868989719));
#438569=CARTESIAN_POINT('Ctrl Pts',(-1.04247169861751,-2.5449977191429,
12.5369868989719));
#438570=CARTESIAN_POINT('Ctrl Pts',(-1.05655165994204,-2.53893469839246,
12.5369868989719));
#438571=CARTESIAN_POINT('Origin',(-1.84953258308752E-31,-9.96028411833586E-31,
12.5));
#438572=CARTESIAN_POINT('Origin',(-0.786422857476889,-2.5656830183634,12.5));
#438573=CARTESIAN_POINT('',(-0.786422857476889,-2.5656830183634,12.5893111709658));
#438574=CARTESIAN_POINT('',(-0.786422857476889,-2.5656830183634,13.8235269408515));
#438575=CARTESIAN_POINT('',(-0.786422857476889,-2.5656830183634,12.5));
#438576=CARTESIAN_POINT('',(-0.808923705722909,-2.59348561765575,13.7902182540695));
#438577=CARTESIAN_POINT('',(-0.786422857476889,-2.5656830183634,13.8235269408515));
#438578=CARTESIAN_POINT('',(-0.821963002087443,-2.60959729166526,13.7435492065112));
#438579=CARTESIAN_POINT('Origin',(-0.779063636183257,-2.55659030206942,
13.7445212918697));
#438580=CARTESIAN_POINT('',(-0.821963002087443,-2.60959729166526,12.5369868989719));
#438581=CARTESIAN_POINT('',(-0.821963002087443,-2.60959729166526,12.5));
#438582=CARTESIAN_POINT('Ctrl Pts',(-0.821963002087443,-2.60959729166526,
12.5369868989719));
#438583=CARTESIAN_POINT('Ctrl Pts',(-0.810124927490551,-2.59496987669798,
12.5544431401645));
#438584=CARTESIAN_POINT('Ctrl Pts',(-0.79827838598807,-2.58033199981474,
12.5718848856037));
#438585=CARTESIAN_POINT('Ctrl Pts',(-0.786422857476889,-2.5656830183634,
12.5893111709658));
#438586=CARTESIAN_POINT('Origin',(-0.695563849448027,-2.85692443666948,
12.5));
#438587=CARTESIAN_POINT('',(-0.719375533633202,-2.6397196902469,13.7435492065112));
#438588=CARTESIAN_POINT('',(-0.72163425915842,-2.61911611172101,13.7902182540695));
#438589=CARTESIAN_POINT('Origin',(-0.727569799452577,-2.56497346836795,
13.7418732680442));
#438590=CARTESIAN_POINT('',(-0.725531957228276,-2.58356219985526,13.8235269408515));
#438591=CARTESIAN_POINT('',(-0.72163425915842,-2.61911611172101,13.7902182540695));
#438592=CARTESIAN_POINT('',(-0.725531957228276,-2.58356219985526,12.5893111709658));
#438593=CARTESIAN_POINT('',(-0.725531957228276,-2.58356219985526,12.5));
#438594=CARTESIAN_POINT('',(-0.719375533633202,-2.6397196902469,12.5369868989719));
#438595=CARTESIAN_POINT('Ctrl Pts',(-0.725531957228276,-2.58356219985526,
12.5893111709658));
#438596=CARTESIAN_POINT('Ctrl Pts',(-0.723478289291409,-2.60229528987923,
12.5718848856037));
#438597=CARTESIAN_POINT('Ctrl Pts',(-0.721426178124584,-2.62101417940233,
12.5544431401645));
#438598=CARTESIAN_POINT('Ctrl Pts',(-0.719375533633202,-2.6397196902469,
12.5369868989719));
#438599=CARTESIAN_POINT('',(-0.719375533633202,-2.6397196902469,12.5));
#438600=CARTESIAN_POINT('Origin',(-0.759702236830053,-2.58730821332779,
12.5));
#438601=CARTESIAN_POINT('',(-0.75109722107967,-2.55402843153593,13.8587068136939));
#438602=CARTESIAN_POINT('Ctrl Pts',(-0.725531957221722,-2.5835621998544,
13.8235269408542));
#438603=CARTESIAN_POINT('Ctrl Pts',(-0.7257229138222,-2.58182033734436,
13.8262006681044));
#438604=CARTESIAN_POINT('Ctrl Pts',(-0.726091034629165,-2.58005672879837,
13.8288634856214));
#438605=CARTESIAN_POINT('Ctrl Pts',(-0.726623342150079,-2.57827443864714,
13.8314912288862));
#438606=CARTESIAN_POINT('Ctrl Pts',(-0.727172096299167,-2.57643708133592,
13.8342001611531));
#438607=CARTESIAN_POINT('Ctrl Pts',(-0.727895473031266,-2.57457768713431,
13.8368750301949));
#438608=CARTESIAN_POINT('Ctrl Pts',(-0.728823876636812,-2.57269240310717,
13.8394886372969));
#438609=CARTESIAN_POINT('Ctrl Pts',(-0.728895579499261,-2.57254679804869,
13.8396904925131));
#438610=CARTESIAN_POINT('Ctrl Pts',(-0.728968526574237,-2.57240104477644,
13.8398919674349));
#438611=CARTESIAN_POINT('Ctrl Pts',(-0.729042742528137,-2.57225514567896,
13.8400930404591));
#438612=CARTESIAN_POINT('Ctrl Pts',(-0.730199077019948,-2.56998193958415,
13.8432258934518));
#438613=CARTESIAN_POINT('Ctrl Pts',(-0.731656537689533,-2.56768442238517,
13.8462331177034));
#438614=CARTESIAN_POINT('Ctrl Pts',(-0.733449048631665,-2.56548920109201,
13.8489036603661));
#438615=CARTESIAN_POINT('Ctrl Pts',(-0.734035579072432,-2.56477089913782,
13.849777493004));
#438616=CARTESIAN_POINT('Ctrl Pts',(-0.734657956282971,-2.56406379830743,
13.85061494757));
#438617=CARTESIAN_POINT('Ctrl Pts',(-0.735317282009905,-2.56337304269841,
13.8514076489583));
#438618=CARTESIAN_POINT('Ctrl Pts',(-0.736711851011371,-2.56191199496346,
13.8530843267192));
#438619=CARTESIAN_POINT('Ctrl Pts',(-0.738410844657664,-2.56038260204569,
13.8546805203176));
#438620=CARTESIAN_POINT('Ctrl Pts',(-0.740406941182383,-2.55897503979074,
13.8559412814273));
#438621=CARTESIAN_POINT('Ctrl Pts',(-0.740674083632336,-2.55878666231271,
13.8561100121513));
#438622=CARTESIAN_POINT('Ctrl Pts',(-0.740946473126565,-2.55860044782226,
13.8562727473908));
#438623=CARTESIAN_POINT('Ctrl Pts',(-0.741224021597772,-2.55841682425119,
13.8564289040185));
#438624=CARTESIAN_POINT('Ctrl Pts',(-0.742482700748308,-2.55758409345124,
13.8571370725437));
#438625=CARTESIAN_POINT('Ctrl Pts',(-0.743870860165083,-2.55679190927231,
13.8577210840554));
#438626=CARTESIAN_POINT('Ctrl Pts',(-0.74534908801759,-2.55609655359047,
13.8581177131616));
#438627=CARTESIAN_POINT('Ctrl Pts',(-0.74576540785991,-2.55590071749705,
13.8582294175695));
#438628=CARTESIAN_POINT('Ctrl Pts',(-0.746188766120969,-2.55571241884951,
13.8583265086086));
#438629=CARTESIAN_POINT('Ctrl Pts',(-0.746618042534046,-2.55553254653241,
13.8584082369006));
#438630=CARTESIAN_POINT('Ctrl Pts',(-0.747234797624621,-2.55527411824739,
13.8585256585398));
#438631=CARTESIAN_POINT('Ctrl Pts',(-0.747871561632547,-2.55503016893092,
13.8586122832068));
#438632=CARTESIAN_POINT('Ctrl Pts',(-0.748512075786855,-2.55480777310193,
13.8586682984299));
#438633=CARTESIAN_POINT('Ctrl Pts',(-0.749024423618175,-2.55462987848412,
13.8587131050557));
#438634=CARTESIAN_POINT('Ctrl Pts',(-0.749544752922616,-2.55446358832294,
13.8587357943552));
#438635=CARTESIAN_POINT('Ctrl Pts',(-0.750073279700978,-2.55430936526782,
13.8587355499465));
#438636=CARTESIAN_POINT('Ctrl Pts',(-0.750414879158553,-2.55420968723043,
13.8587353919793));
#438637=CARTESIAN_POINT('Ctrl Pts',(-0.750756198140403,-2.55411609082041,
13.8587257282814));
#438638=CARTESIAN_POINT('Ctrl Pts',(-0.75109722107967,-2.55402843153593,
13.8587068136939));
#438639=CARTESIAN_POINT('Ctrl Pts',(-0.75109722107967,-2.55402843153593,
13.8587068136939));
#438640=CARTESIAN_POINT('Ctrl Pts',(-0.752218826935593,-2.55374012492815,
13.8586446046466));
#438641=CARTESIAN_POINT('Ctrl Pts',(-0.753337235143209,-2.55351596180143,
13.858482427929));
#438642=CARTESIAN_POINT('Ctrl Pts',(-0.754451869443705,-2.55335150888579,
13.8582284286032));
#438643=CARTESIAN_POINT('Ctrl Pts',(-0.755595354576482,-2.55318279932427,
13.8579678548414));
#438644=CARTESIAN_POINT('Ctrl Pts',(-0.756737884691099,-2.55307803415227,
13.857615680862));
#438645=CARTESIAN_POINT('Ctrl Pts',(-0.75783353159653,-2.5530316944702,
13.8571944833187));
#438646=CARTESIAN_POINT('Ctrl Pts',(-0.760567830502609,-2.55291604905436,
13.8561433417727));
#438647=CARTESIAN_POINT('Ctrl Pts',(-0.763137838651283,-2.55315407872345,
13.8546163505474));
#438648=CARTESIAN_POINT('Ctrl Pts',(-0.76542262856099,-2.55357805032377,
13.8528973491086));
#438649=CARTESIAN_POINT('Ctrl Pts',(-0.765840025968559,-2.55365550368003,
13.8525833129072));
#438650=CARTESIAN_POINT('Ctrl Pts',(-0.766247991588314,-2.55373905131416,
13.8522628768812));
#438651=CARTESIAN_POINT('Ctrl Pts',(-0.766645918937218,-2.55382754864833,
13.851937733538));
#438652=CARTESIAN_POINT('Ctrl Pts',(-0.769076006047064,-2.55436798958969,
13.8499521282529));
#438653=CARTESIAN_POINT('Ctrl Pts',(-0.771372347937259,-2.55515071408284,
13.847639871647));
#438654=CARTESIAN_POINT('Ctrl Pts',(-0.773440177674622,-2.55605854052776,
13.8452109780794));
#438655=CARTESIAN_POINT('Ctrl Pts',(-0.774370537075405,-2.5564669904364,
13.8441181685877));
#438656=CARTESIAN_POINT('Ctrl Pts',(-0.775255137099046,-2.55690024768248,
13.8430021611332));
#438657=CARTESIAN_POINT('Ctrl Pts',(-0.776088267135618,-2.55734608452085,
13.8418824960098));
#438658=CARTESIAN_POINT('Ctrl Pts',(-0.778051559341545,-2.5583967104153,
13.8392439765549));
#438659=CARTESIAN_POINT('Ctrl Pts',(-0.779824666035133,-2.55956408302726,
13.8364981347964));
#438660=CARTESIAN_POINT('Ctrl Pts',(-0.781431094187344,-2.56082270752436,
13.8336931113419));
#438661=CARTESIAN_POINT('Ctrl Pts',(-0.782995653189977,-2.56204852785448,
13.8309611966328));
#438662=CARTESIAN_POINT('Ctrl Pts',(-0.784403328595506,-2.56336257803986,
13.8281701127185));
#438663=CARTESIAN_POINT('Ctrl Pts',(-0.785642005203312,-2.56476130297386,
13.825358068512));
#438664=CARTESIAN_POINT('Ctrl Pts',(-0.785910551628698,-2.56506454804909,
13.8247484142932));
#438665=CARTESIAN_POINT('Ctrl Pts',(-0.786170983011782,-2.56537179610419,
13.8241378483365));
#438666=CARTESIAN_POINT('Ctrl Pts',(-0.786422857476889,-2.5656830183634,
13.8235269408515));
#438667=CARTESIAN_POINT('',(-0.749900486153921,-2.55436100089082,12.5969504640361));
#438668=CARTESIAN_POINT('Origin',(-0.759711745942211,-2.58733990338295,
12.584524458991));
#438669=CARTESIAN_POINT('Origin',(-0.759711745942211,-2.58733990338295,
12.584524458991));
#438670=CARTESIAN_POINT('Ctrl Pts',(-0.725531957228276,-2.58356219985526,
12.5893111709658));
#438671=CARTESIAN_POINT('Ctrl Pts',(-0.726767074738799,-2.57229573992789,
12.5770542771492));
#438672=CARTESIAN_POINT('Ctrl Pts',(-0.743081587281321,-2.57101497634516,
12.5737548217797));
#438673=CARTESIAN_POINT('Ctrl Pts',(-0.722831169750517,-2.60819816658008,
12.5663937883685));
#438674=CARTESIAN_POINT('Ctrl Pts',(-0.724067862824956,-2.59691733471841,
12.5540940315304));
#438675=CARTESIAN_POINT('Ctrl Pts',(-0.740433182052644,-2.59563580364621,
12.5508374392248));
#438676=CARTESIAN_POINT('Ctrl Pts',(-0.720133107334208,-2.63280927591654,
12.5434499600945));
#438677=CARTESIAN_POINT('Ctrl Pts',(-0.72137382133825,-2.62149176605326,
12.5311293540533));
#438678=CARTESIAN_POINT('Ctrl Pts',(-0.737786191272279,-2.62023244968732,
12.5278936106989));
#438679=CARTESIAN_POINT('Ctrl Pts',(-0.717437556521574,-2.65739747497773,
12.5204817579905));
#438680=CARTESIAN_POINT('Ctrl Pts',(-0.718684411212006,-2.6460239511751,
12.5081597038247));
#438681=CARTESIAN_POINT('Ctrl Pts',(-0.735140491229121,-2.64480679244879,
12.5049254088044));
#438682=CARTESIAN_POINT('Ctrl Pts',(-0.719375533633203,-2.6397196902469,
12.5369868989719));
#438683=CARTESIAN_POINT('Ctrl Pts',(-0.719274023118167,-2.64064564747381,
12.5342545179733));
#438684=CARTESIAN_POINT('Ctrl Pts',(-0.719301149261355,-2.64154293298339,
12.5314872231885));
#438685=CARTESIAN_POINT('Ctrl Pts',(-0.719511259382647,-2.64235931209083,
12.5287124745063));
#438686=CARTESIAN_POINT('Ctrl Pts',(-0.719700747118965,-2.64309556329136,
12.5262100684184));
#438687=CARTESIAN_POINT('Ctrl Pts',(-0.720039823120004,-2.64376502262788,
12.5237004536639));
#438688=CARTESIAN_POINT('Ctrl Pts',(-0.720593447251803,-2.64434923225817,
12.5212220730815));
#438689=CARTESIAN_POINT('Ctrl Pts',(-0.721017294417001,-2.64479649526832,
12.5193246583486));
#438690=CARTESIAN_POINT('Ctrl Pts',(-0.721572419302811,-2.64519870042026,
12.517417831369));
#438691=CARTESIAN_POINT('Ctrl Pts',(-0.722330284083855,-2.64548991456336,
12.5155812248348));
#438692=CARTESIAN_POINT('Ctrl Pts',(-0.722653138554123,-2.64561397335361,
12.5147988205793));
#438693=CARTESIAN_POINT('Ctrl Pts',(-0.723013014755882,-2.6457182739583,
12.5140295443047));
#438694=CARTESIAN_POINT('Ctrl Pts',(-0.723415926669586,-2.64579978924908,
12.5132817086137));
#438695=CARTESIAN_POINT('Ctrl Pts',(-0.724025679346283,-2.64592315161454,
12.5121499604604));
#438696=CARTESIAN_POINT('Ctrl Pts',(-0.724748580859092,-2.64598998364006,
12.5110494206568));
#438697=CARTESIAN_POINT('Ctrl Pts',(-0.725599809466267,-2.64596627769085,
12.5100666561695));
#438698=CARTESIAN_POINT('Ctrl Pts',(-0.726088582972301,-2.64595266578941,
12.5095023550641));
#438699=CARTESIAN_POINT('Ctrl Pts',(-0.726625295463391,-2.64590839348071,
12.5089719619137));
#438700=CARTESIAN_POINT('Ctrl Pts',(-0.727199361791711,-2.64582792524076,
12.5085043804652));
#438701=CARTESIAN_POINT('Ctrl Pts',(-0.72803943308581,-2.64571017045333,
12.5078201359221));
#438702=CARTESIAN_POINT('Ctrl Pts',(-0.728983693009031,-2.64551029246537,
12.5072563000949));
#438703=CARTESIAN_POINT('Ctrl Pts',(-0.729966381459002,-2.64523355758019,
12.5068768744332));
#438704=CARTESIAN_POINT('Ctrl Pts',(-0.730674967479934,-2.64503401267748,
12.5066032824114));
#438705=CARTESIAN_POINT('Ctrl Pts',(-0.731415999108655,-2.64479105888369,
12.5064197834844));
#438706=CARTESIAN_POINT('Ctrl Pts',(-0.732148900507654,-2.64452071958462,
12.5063282718343));
#438707=CARTESIAN_POINT('Ctrl Pts',(-0.733218709649654,-2.64412610790289,
12.5061946931565));
#438708=CARTESIAN_POINT('Ctrl Pts',(-0.734294429234505,-2.64366570823441,
12.5062515701262));
#438709=CARTESIAN_POINT('Ctrl Pts',(-0.735315383030953,-2.64318231091932,
12.5064436508398));
#438710=CARTESIAN_POINT('',(-0.743081587281321,-2.57101497634516,12.5737548217797));
#438711=CARTESIAN_POINT('Origin',(-0.747400936173413,-2.58595964847768,
12.5893111709658));
#438712=CARTESIAN_POINT('Ctrl Pts',(-0.735315383030953,-2.64318231091932,
12.5064436508398));
#438713=CARTESIAN_POINT('Ctrl Pts',(-0.736465460714024,-2.63249972185702,
12.5164271754438));
#438714=CARTESIAN_POINT('Ctrl Pts',(-0.737615786552383,-2.62181287585427,
12.5264061185523));
#438715=CARTESIAN_POINT('Ctrl Pts',(-0.7387663702269,-2.61112162308651,
12.536380305637));
#438716=CARTESIAN_POINT('Ctrl Pts',(-0.740204366456533,-2.59775972554652,
12.5488460165097));
#438717=CARTESIAN_POINT('Ctrl Pts',(-0.741642765825077,-2.58439094072071,
12.5613043021964));
#438718=CARTESIAN_POINT('Ctrl Pts',(-0.743081587281321,-2.57101497634516,
12.5737548217797));
#438719=CARTESIAN_POINT('Ctrl Pts',(-0.786422857476888,-2.5656830183634,
12.5893111709658));
#438720=CARTESIAN_POINT('Ctrl Pts',(-0.779292702402738,-2.55687282408755,
12.5770542771492));
#438721=CARTESIAN_POINT('Ctrl Pts',(-0.764875628019588,-2.56461566859623,
12.5737548217797));
#438722=CARTESIAN_POINT('Ctrl Pts',(-0.779770484807521,-2.55746318373105,
12.5928319619712));
#438723=CARTESIAN_POINT('Ctrl Pts',(-0.77244624837694,-2.55359162369919,
12.5821634970842));
#438724=CARTESIAN_POINT('Ctrl Pts',(-0.762459666754359,-2.56161544384893,
12.5773203894503));
#438725=CARTESIAN_POINT('Ctrl Pts',(-0.764762191017099,-2.55002441926106,
12.5969440695591));
#438726=CARTESIAN_POINT('Ctrl Pts',(-0.760900142364282,-2.55113937341043,
12.5878292599214));
#438727=CARTESIAN_POINT('Ctrl Pts',(-0.757109495998643,-2.55896594956091,
12.5813877129824));
#438728=CARTESIAN_POINT('Ctrl Pts',(-0.735389456187558,-2.55859283184303,
12.596957478804));
#438729=CARTESIAN_POINT('Ctrl Pts',(-0.739222985498508,-2.55748619451717,
12.5878468778671));
#438730=CARTESIAN_POINT('Ctrl Pts',(-0.746598257514899,-2.56203842964092,
12.5814011370086));
#438731=CARTESIAN_POINT('Ctrl Pts',(-0.726685984338924,-2.57303542804039,
12.5928371701607));
#438732=CARTESIAN_POINT('Ctrl Pts',(-0.730756761274845,-2.565826833112,
12.5821692192952));
#438733=CARTESIAN_POINT('Ctrl Pts',(-0.743493039323462,-2.56717258325088,
12.5773318885715));
#438734=CARTESIAN_POINT('Ctrl Pts',(-0.725531957228221,-2.58356219985525,
12.5893111709658));
#438735=CARTESIAN_POINT('Ctrl Pts',(-0.726767074738745,-2.57229573992789,
12.5770542771492));
#438736=CARTESIAN_POINT('Ctrl Pts',(-0.743081587281266,-2.57101497634516,
12.5737548217797));
#438737=CARTESIAN_POINT('',(-0.764875628019588,-2.56461566859623,12.5737548217797));
#438738=CARTESIAN_POINT('Origin',(-0.769321660262914,-2.57952314314061,
12.5893111709658));
#438739=CARTESIAN_POINT('Ctrl Pts',(-0.743081587281266,-2.57101497634516,
12.5737548217797));
#438740=CARTESIAN_POINT('Ctrl Pts',(-0.743158247913999,-2.5700157552593,
12.5746934679442));
#438741=CARTESIAN_POINT('Ctrl Pts',(-0.743425725553061,-2.56892406338389,
12.5756680099006));
#438742=CARTESIAN_POINT('Ctrl Pts',(-0.743850354499381,-2.56786331179849,
12.5765688348656));
#438743=CARTESIAN_POINT('Ctrl Pts',(-0.74396277031212,-2.56758248955916,
12.5768073183026));
#438744=CARTESIAN_POINT('Ctrl Pts',(-0.744085945601193,-2.56730380124158,
12.5770407398754));
#438745=CARTESIAN_POINT('Ctrl Pts',(-0.744218734611065,-2.56702932315182,
12.5772674179684));
#438746=CARTESIAN_POINT('Ctrl Pts',(-0.744763664799926,-2.56590293929345,
12.5781976435658));
#438747=CARTESIAN_POINT('Ctrl Pts',(-0.745511600568155,-2.56478839473652,
12.5790594849312));
#438748=CARTESIAN_POINT('Ctrl Pts',(-0.746452137496484,-2.56378785337799,
12.5797571720116));
#438749=CARTESIAN_POINT('Ctrl Pts',(-0.747064931123984,-2.56313596470665,
12.580211740231));
#438750=CARTESIAN_POINT('Ctrl Pts',(-0.747801010366068,-2.56251570320559,
12.5806009430798));
#438751=CARTESIAN_POINT('Ctrl Pts',(-0.748619974766494,-2.56198428060995,
12.5808812374708));
#438752=CARTESIAN_POINT('Ctrl Pts',(-0.749323736875072,-2.56152761230268,
12.5811221033394));
#438753=CARTESIAN_POINT('Ctrl Pts',(-0.750103175628632,-2.56112729370187,
12.581287365893));
#438754=CARTESIAN_POINT('Ctrl Pts',(-0.750918107575558,-2.56081333637143,
12.581359338449));
#438755=CARTESIAN_POINT('Ctrl Pts',(-0.751031366288477,-2.56076970278548,
12.5813693411482));
#438756=CARTESIAN_POINT('Ctrl Pts',(-0.751145308888634,-2.56072767743566,
12.5813775999465));
#438757=CARTESIAN_POINT('Ctrl Pts',(-0.751259826879553,-2.5606872795466,
12.5813841266931));
#438758=CARTESIAN_POINT('Ctrl Pts',(-0.751454120501815,-2.56061873964178,
12.5813952001081));
#438759=CARTESIAN_POINT('Ctrl Pts',(-0.751651574239596,-2.56055499956375,
12.5814007534795));
#438760=CARTESIAN_POINT('Ctrl Pts',(-0.751852162678322,-2.56049627474705,
12.5814005856065));
#438761=CARTESIAN_POINT('Ctrl Pts',(-0.752770378125813,-2.56022745549613,
12.5813998171494));
#438762=CARTESIAN_POINT('Ctrl Pts',(-0.753690743216226,-2.56008197800291,
12.58127954464));
#438763=CARTESIAN_POINT('Ctrl Pts',(-0.754603413029476,-2.56003144168815,
12.5810700125799));
#438764=CARTESIAN_POINT('Ctrl Pts',(-0.755705814248104,-2.55997039957394,
12.5808169217085));
#438765=CARTESIAN_POINT('Ctrl Pts',(-0.756798013092731,-2.560064580481,
12.5804173076348));
#438766=CARTESIAN_POINT('Ctrl Pts',(-0.75778652844819,-2.56027978447649,
12.5799304713245));
#438767=CARTESIAN_POINT('Ctrl Pts',(-0.759011610388055,-2.56054649002315,
12.5793271277669));
#438768=CARTESIAN_POINT('Ctrl Pts',(-0.760160288447277,-2.56098415601984,
12.5785808224116));
#438769=CARTESIAN_POINT('Ctrl Pts',(-0.761195436365689,-2.56154469562594,
12.5777485681082));
#438770=CARTESIAN_POINT('Ctrl Pts',(-0.762737920173045,-2.56237996105073,
12.576508418016));
#438771=CARTESIAN_POINT('Ctrl Pts',(-0.764018603010034,-2.56347498204679,
12.5750928681475));
#438772=CARTESIAN_POINT('Ctrl Pts',(-0.764875628019588,-2.56461566859623,
12.5737548217797));
#438773=CARTESIAN_POINT('Ctrl Pts',(-0.764875628019588,-2.56461566859623,
12.5737548217797));
#438774=CARTESIAN_POINT('Ctrl Pts',(-0.779292702402738,-2.55687282408755,
12.5770542771492));
#438775=CARTESIAN_POINT('Ctrl Pts',(-0.786422857476888,-2.5656830183634,
12.5893111709658));
#438776=CARTESIAN_POINT('Ctrl Pts',(-0.780412297983975,-2.58389329398392,
12.5508408821982));
#438777=CARTESIAN_POINT('Ctrl Pts',(-0.794872520007951,-2.57612362837677,
12.55409748406));
#438778=CARTESIAN_POINT('Ctrl Pts',(-0.802011771333854,-2.58494506220412,
12.5663972313419));
#438779=CARTESIAN_POINT('Ctrl Pts',(-0.795934708955605,-2.60315134740109,
12.52790050457));
#438780=CARTESIAN_POINT('Ctrl Pts',(-0.810422498554156,-2.59533756279374,
12.5311362602938));
#438781=CARTESIAN_POINT('Ctrl Pts',(-0.817584958538338,-2.60418767380778,
12.5434568539655));
#438782=CARTESIAN_POINT('Ctrl Pts',(-0.811443979823457,-2.62239134115121,
12.5049357605811));
#438783=CARTESIAN_POINT('Ctrl Pts',(-0.825945748610739,-2.61451847083413,
12.5081700652078));
#438784=CARTESIAN_POINT('Ctrl Pts',(-0.833143650804941,-2.62341237511111,
12.5204921097672));
#438785=CARTESIAN_POINT('Ctrl Pts',(-0.810425581539454,-2.62112796674706,
12.5064436508395));
#438786=CARTESIAN_POINT('Ctrl Pts',(-0.811635627467077,-2.6209710061035,
12.5062361689309));
#438787=CARTESIAN_POINT('Ctrl Pts',(-0.812887283060052,-2.6207561808326,
12.5061871075061));
#438788=CARTESIAN_POINT('Ctrl Pts',(-0.814085200580072,-2.62048048125635,
12.5063648335164));
#438789=CARTESIAN_POINT('Ctrl Pts',(-0.814629368608283,-2.62035524150297,
12.5064455676329));
#438790=CARTESIAN_POINT('Ctrl Pts',(-0.815169988186426,-2.62021547857725,
12.506574497099));
#438791=CARTESIAN_POINT('Ctrl Pts',(-0.815683616121469,-2.62006616759708,
12.5067492519495));
#438792=CARTESIAN_POINT('Ctrl Pts',(-0.81671577139458,-2.61976612138657,
12.5071004286051));
#438793=CARTESIAN_POINT('Ctrl Pts',(-0.817676650834413,-2.6194157100936,
12.5076537929613));
#438794=CARTESIAN_POINT('Ctrl Pts',(-0.818497375929666,-2.61905011993456,
12.5083435010505));
#438795=CARTESIAN_POINT('Ctrl Pts',(-0.818549045479092,-2.61902710384927,
12.5083869222964));
#438796=CARTESIAN_POINT('Ctrl Pts',(-0.818600160311445,-2.61900401419111,
12.5084308732337));
#438797=CARTESIAN_POINT('Ctrl Pts',(-0.81865070395164,-2.61898085430138,
12.5084753333615));
#438798=CARTESIAN_POINT('Ctrl Pts',(-0.819056130657566,-2.61879508141751,
12.5088319622689));
#438799=CARTESIAN_POINT('Ctrl Pts',(-0.819433574196886,-2.61860219105085,
12.509227847131));
#438800=CARTESIAN_POINT('Ctrl Pts',(-0.819773085408875,-2.61841041216931,
12.5096423454524));
#438801=CARTESIAN_POINT('Ctrl Pts',(-0.820836963285881,-2.61780946203232,
12.5109411997424));
#438802=CARTESIAN_POINT('Ctrl Pts',(-0.821598567315469,-2.61719088189056,
12.5124831113042));
#438803=CARTESIAN_POINT('Ctrl Pts',(-0.822142048037762,-2.6165979677484,
12.5140723025008));
#438804=CARTESIAN_POINT('Ctrl Pts',(-0.822192972776699,-2.61654241104388,
12.5142212114565));
#438805=CARTESIAN_POINT('Ctrl Pts',(-0.822242011824836,-2.61648708310949,
12.5143705582413));
#438806=CARTESIAN_POINT('Ctrl Pts',(-0.822289251031082,-2.61643202305668,
12.5145201959299));
#438807=CARTESIAN_POINT('Ctrl Pts',(-0.822896108967137,-2.61572469470258,
12.5164425148273));
#438808=CARTESIAN_POINT('Ctrl Pts',(-0.823234877861664,-2.61504433199383,
12.5184635205941));
#438809=CARTESIAN_POINT('Ctrl Pts',(-0.823395536412026,-2.61438446866632,
12.5205025929158));
#438810=CARTESIAN_POINT('Ctrl Pts',(-0.823488724739145,-2.61400172178183,
12.5216853356836));
#438811=CARTESIAN_POINT('Ctrl Pts',(-0.823522290051381,-2.61362667761862,
12.5228750347131));
#438812=CARTESIAN_POINT('Ctrl Pts',(-0.823513873423488,-2.61326399730633,
12.5240609649613));
#438813=CARTESIAN_POINT('Ctrl Pts',(-0.823493215261862,-2.61237381793693,
12.5269717671326));
#438814=CARTESIAN_POINT('Ctrl Pts',(-0.823208670665855,-2.61153331013741,
12.5299036066169));
#438815=CARTESIAN_POINT('Ctrl Pts',(-0.822745720998118,-2.61072824508954,
12.5328133004019));
#438816=CARTESIAN_POINT('Ctrl Pts',(-0.822523478200853,-2.61034176698903,
12.5342101228451));
#438817=CARTESIAN_POINT('Ctrl Pts',(-0.822259943879739,-2.60996420034821,
12.5356023438238));
#438818=CARTESIAN_POINT('Ctrl Pts',(-0.821963002087443,-2.60959729166526,
12.5369868989719));
#438819=CARTESIAN_POINT('Origin',(-8.84453359361121,-12.5140605108539,-1.24074782725411));
#438820=CARTESIAN_POINT('Ctrl Pts',(-0.719380048696327,-2.63967814057616,
12.5369868989719));
#438821=CARTESIAN_POINT('Ctrl Pts',(-0.717737457340924,-2.65492888473259,
12.5369868989719));
#438822=CARTESIAN_POINT('Ctrl Pts',(-0.70285948685656,-2.65866108220216,
12.5369868989719));
#438823=CARTESIAN_POINT('Ctrl Pts',(-0.718824722745646,-2.6448334814637,
12.5218025310016));
#438824=CARTESIAN_POINT('Ctrl Pts',(-0.714312581026351,-2.65575577246924,
12.5216901060418));
#438825=CARTESIAN_POINT('Ctrl Pts',(-0.702904843853943,-2.65864972122353,
12.5161920673678));
#438826=CARTESIAN_POINT('Ctrl Pts',(-0.723316122852456,-2.64885385411758,
12.5042015548894));
#438827=CARTESIAN_POINT('Ctrl Pts',(-0.719798195314405,-2.65423916105906,
12.4980677368513));
#438828=CARTESIAN_POINT('Ctrl Pts',(-0.713237143708695,-2.65601211947674,
12.4907278922777));
#438829=CARTESIAN_POINT('Ctrl Pts',(-0.735310022442628,-2.64316304158105,
12.506463626192));
#438830=CARTESIAN_POINT('Ctrl Pts',(-0.737063577422545,-2.64946641236729,
12.4999376786891));
#438831=CARTESIAN_POINT('Ctrl Pts',(-0.737042160298133,-2.64938942585823,
12.4906970594712));
#438832=CARTESIAN_POINT('Origin',(-0.697506554688065,-2.63732224162448,
12.5369868989719));
#438833=CARTESIAN_POINT('Origin',(-0.697506554688065,-2.63732224162448,
14.));
#438834=CARTESIAN_POINT('Origin',(-0.697506554688065,-2.63732224162448,
13.7435492065112));
#438835=CARTESIAN_POINT('Ctrl Pts',(-0.722073737423757,-2.61510704217319,
13.793642941384));
#438836=CARTESIAN_POINT('Ctrl Pts',(-0.720922529256145,-2.62585789975576,
13.8071662555867));
#438837=CARTESIAN_POINT('Ctrl Pts',(-0.703906806013424,-2.62655399325649,
13.8103758687955));
#438838=CARTESIAN_POINT('Ctrl Pts',(-0.720262454621957,-2.6316291776234,
13.7804579775006));
#438839=CARTESIAN_POINT('Ctrl Pts',(-0.718831884636872,-2.64489368444598,
13.7901904343351));
#438840=CARTESIAN_POINT('Ctrl Pts',(-0.703400534075535,-2.64807634748468,
13.7927914348263));
#438841=CARTESIAN_POINT('Ctrl Pts',(-0.7191960842325,-2.6413563805567,13.7597120340895));
#438842=CARTESIAN_POINT('Ctrl Pts',(-0.717534814526755,-2.65670653602619,
13.7635825532445));
#438843=CARTESIAN_POINT('Ctrl Pts',(-0.703076430755867,-2.66076745401083,
13.7651073818884));
#438844=CARTESIAN_POINT('Ctrl Pts',(-0.719404903971055,-2.63945157149465,
13.7381884353898));
#438845=CARTESIAN_POINT('Ctrl Pts',(-0.717783412992171,-2.65444252468754,
13.7368803041982));
#438846=CARTESIAN_POINT('Ctrl Pts',(-0.703139405746687,-2.65828214562106,
13.7363986145813));
#438847=CARTESIAN_POINT('Origin',(-0.699765280213282,-2.61671866309859,
13.7902182540695));
#438848=CARTESIAN_POINT('Ctrl Pts',(-0.725532385420848,-2.58355828701616,
13.8235227101244));
#438849=CARTESIAN_POINT('Ctrl Pts',(-0.724283899720923,-2.59498737148417,
13.8358800583119));
#438850=CARTESIAN_POINT('Ctrl Pts',(-0.707754549332778,-2.59617338362709,
13.8390832900376));
#438851=CARTESIAN_POINT('Ctrl Pts',(-0.724232578206299,-2.5954148316435,
13.8124254819053));
#438852=CARTESIAN_POINT('Ctrl Pts',(-0.722981667688322,-2.60686611120135,
13.8247886449158));
#438853=CARTESIAN_POINT('Ctrl Pts',(-0.706430211948133,-2.60803662133952,
13.8279860620657));
#438854=CARTESIAN_POINT('Ctrl Pts',(-0.722933353523072,-2.60726606255325,
13.8013225099955));
#438855=CARTESIAN_POINT('Ctrl Pts',(-0.721680610408695,-2.61873413425349,
13.8136962257787));
#438856=CARTESIAN_POINT('Ctrl Pts',(-0.705106757049417,-2.61989439702853,
13.8168830918626));
#438857=CARTESIAN_POINT('Ctrl Pts',(-0.721634688705769,-2.61911218649399,
13.7902140179785));
#438858=CARTESIAN_POINT('Ctrl Pts',(-0.720380666507743,-2.63059200051128,
13.802602731458));
#438859=CARTESIAN_POINT('Ctrl Pts',(-0.703784151790519,-2.63174692551444,
13.8057746032558));
#438860=CARTESIAN_POINT('Origin',(-0.703662978283139,-2.58116475123284,
13.8235269408515));
#438861=CARTESIAN_POINT('Ctrl Pts',(-0.786422857476889,-2.5656830183634,
13.8235269408515));
#438862=CARTESIAN_POINT('Ctrl Pts',(-0.793850903700689,-2.57486129424115,
13.8362179249168));
#438863=CARTESIAN_POINT('Ctrl Pts',(-0.808689144333974,-2.56640614084421,
13.8391868794938));
#438864=CARTESIAN_POINT('Ctrl Pts',(-0.779626518505738,-2.55728529544185,
13.8400110824519));
#438865=CARTESIAN_POINT('Ctrl Pts',(-0.788241229681228,-2.56249188878345,
13.8494522556837));
#438866=CARTESIAN_POINT('Ctrl Pts',(-0.79741695096815,-2.55265654301925,
13.85569149686));
#438867=CARTESIAN_POINT('Ctrl Pts',(-0.765091992637448,-2.54992694754099,
13.8586819406588));
#438868=CARTESIAN_POINT('Ctrl Pts',(-0.769273381913537,-2.54871367619591,
13.868010383617));
#438869=CARTESIAN_POINT('Ctrl Pts',(-0.773223403946076,-2.54057179725215,
13.8744918421245));
#438870=CARTESIAN_POINT('Ctrl Pts',(-0.735054534284133,-2.55869179743246,
13.8587686893867));
#438871=CARTESIAN_POINT('Ctrl Pts',(-0.730910343642403,-2.55989421659599,
13.8680909899357));
#438872=CARTESIAN_POINT('Ctrl Pts',(-0.723220577461804,-2.55516516832033,
13.8745789365163));
#438873=CARTESIAN_POINT('Ctrl Pts',(-0.726711165341349,-2.57280573262591,
13.8400379222776));
#438874=CARTESIAN_POINT('Ctrl Pts',(-0.722273609608704,-2.5818378050917,
13.8494748685453));
#438875=CARTESIAN_POINT('Ctrl Pts',(-0.709242845016182,-2.57852717382274,
13.8557104837033));
#438876=CARTESIAN_POINT('Ctrl Pts',(-0.725531957221722,-2.5835621998544,
13.8235269408542));
#438877=CARTESIAN_POINT('Ctrl Pts',(-0.72424523766725,-2.59529936184436,
13.8362179249195));
#438878=CARTESIAN_POINT('Ctrl Pts',(-0.707191314269287,-2.59620859272407,
13.8391868794965));
#438879=CARTESIAN_POINT('Origin',(-0.803524054690863,-2.55184289358619,
13.8235269408515));
#438880=CARTESIAN_POINT('Ctrl Pts',(-0.808921225855,-2.59348255226219,13.7902140241682));
#438881=CARTESIAN_POINT('Ctrl Pts',(-0.816182634669319,-2.6024620031042,
13.8026027327198));
#438882=CARTESIAN_POINT('Ctrl Pts',(-0.830768905102112,-2.59446083774312,
13.8057746032556));
#438883=CARTESIAN_POINT('Ctrl Pts',(-0.801424221355978,-2.58421906985202,
13.8013225161807));
#438884=CARTESIAN_POINT('Ctrl Pts',(-0.80867820575412,-2.59318933396389,
13.8136962270464));
#438885=CARTESIAN_POINT('Ctrl Pts',(-0.823248298065677,-2.58520491066934,
13.8168830918628));
#438886=CARTESIAN_POINT('Ctrl Pts',(-0.793923984830844,-2.57495159387123,
13.8124254880875));
#438887=CARTESIAN_POINT('Ctrl Pts',(-0.801167349029216,-2.58390872232463,
13.8247886461868));
#438888=CARTESIAN_POINT('Ctrl Pts',(-0.815724139415132,-2.57594502871805,
13.8279860620656));
#438889=CARTESIAN_POINT('Ctrl Pts',(-0.78642038543453,-2.56567996264446,
13.8235227163065));
#438890=CARTESIAN_POINT('Ctrl Pts',(-0.793649710173589,-2.57461973037378,
13.8358800595847));
#438891=CARTESIAN_POINT('Ctrl Pts',(-0.808196285377042,-2.56668102892777,
13.8390832900376));
#438892=CARTESIAN_POINT('Origin',(-0.826024902936883,-2.57964549287854,
13.7902182540695));
#438893=CARTESIAN_POINT('Ctrl Pts',(-0.821793255587976,-2.60938750488452,
13.7382347919292));
#438894=CARTESIAN_POINT('Ctrl Pts',(-0.831267858507332,-2.62113270680929,
13.7369371795943));
#438895=CARTESIAN_POINT('Ctrl Pts',(-0.845671586658218,-2.61643415465193,
13.7364597369711));
#438896=CARTESIAN_POINT('Ctrl Pts',(-0.822983228330782,-2.61085786499539,
13.7595490285573));
#438897=CARTESIAN_POINT('Ctrl Pts',(-0.832684669703119,-2.62288266610469,
13.7633824266925));
#438898=CARTESIAN_POINT('Ctrl Pts',(-0.84705080372898,-2.61846589653202,
13.7648920890506));
#438899=CARTESIAN_POINT('Ctrl Pts',(-0.816914432528308,-2.60335910898789,
13.7803806590111));
#438900=CARTESIAN_POINT('Ctrl Pts',(-0.825301630537322,-2.61376352130003,
13.7901039518745));
#438901=CARTESIAN_POINT('Ctrl Pts',(-0.84001633264238,-2.60810993983472,
13.7926933640891));
#438902=CARTESIAN_POINT('Ctrl Pts',(-0.806365510757895,-2.59032459706546,
13.7936647693663));
#438903=CARTESIAN_POINT('Ctrl Pts',(-0.813146129652744,-2.59875054148418,
13.8072068914933));
#438904=CARTESIAN_POINT('Ctrl Pts',(-0.827847479755415,-2.59011835896727,
13.8104111085397));
#438905=CARTESIAN_POINT('Origin',(-0.839064199301418,-2.59575716688805,
13.7435492065112));
#438906=CARTESIAN_POINT('Origin',(-0.839064199301418,-2.59575716688805,
14.));
#438907=CARTESIAN_POINT('Origin',(-0.839064199301418,-2.59575716688805,
12.5369868989719));
#438908=CARTESIAN_POINT('Ctrl Pts',(-0.810420151261945,-2.62111040384641,
12.506462012331));
#438909=CARTESIAN_POINT('Ctrl Pts',(-0.812351610471273,-2.62735724731432,
12.4999388158272));
#438910=CARTESIAN_POINT('Ctrl Pts',(-0.812328758775875,-2.62728333896387,
12.4907030323752));
#438911=CARTESIAN_POINT('Ctrl Pts',(-0.823586101983871,-2.61941148514846,
12.5042014951932));
#438912=CARTESIAN_POINT('Ctrl Pts',(-0.829454125149732,-2.62203967868035,
12.4980716682127));
#438913=CARTESIAN_POINT('Ctrl Pts',(-0.83592806650496,-2.6199869613216,
12.4907355092743));
#438914=CARTESIAN_POINT('Ctrl Pts',(-0.825192965213259,-2.61360255307729,
12.5218047446509));
#438915=CARTESIAN_POINT('Ctrl Pts',(-0.834889739761238,-2.62034728689729,
12.5216906929434));
#438916=CARTESIAN_POINT('Ctrl Pts',(-0.846046639061602,-2.61661977400911,
12.5161988840776));
#438917=CARTESIAN_POINT('Ctrl Pts',(-0.821938860714689,-2.60956740867775,
12.5369868989719));
#438918=CARTESIAN_POINT('Ctrl Pts',(-0.831562019321965,-2.62150057045239,
12.5369868989719));
#438919=CARTESIAN_POINT('Ctrl Pts',(-0.846089323214206,-2.61660537146327,
12.5369868989719));
#438920=CARTESIAN_POINT('Origin',(-1.45144742314189E-31,-1.0095038568149E-30,
12.5));
#438921=CARTESIAN_POINT('Origin',(-0.574679115658286,-2.62124668345172,
12.5));
#438922=CARTESIAN_POINT('',(-0.574679115658286,-2.62124668345172,12.5893111709658));
#438923=CARTESIAN_POINT('',(-0.574679115658286,-2.62124668345172,13.8235269408515));
#438924=CARTESIAN_POINT('',(-0.574679115658286,-2.62124668345172,12.5));
#438925=CARTESIAN_POINT('',(-0.594838924238891,-2.65079079990822,13.7902182540695));
#438926=CARTESIAN_POINT('',(-0.574679115658286,-2.62124668345172,13.8235269408515));
#438927=CARTESIAN_POINT('',(-0.60652158241518,-2.66791168735621,13.7435492065112));
#438928=CARTESIAN_POINT('Origin',(-0.568085522355904,-2.61158437756436,
13.744521291869));
#438929=CARTESIAN_POINT('',(-0.60652158241518,-2.66791168735621,12.5369868989719));
#438930=CARTESIAN_POINT('',(-0.60652158241518,-2.66791168735621,12.5));
#438931=CARTESIAN_POINT('Ctrl Pts',(-0.60652158241518,-2.66791168735621,
12.5369868989719));
#438932=CARTESIAN_POINT('Ctrl Pts',(-0.595915168149065,-2.65236803092659,
12.5544431401645));
#438933=CARTESIAN_POINT('Ctrl Pts',(-0.585301167893566,-2.63681325726076,
12.5718848856037));
#438934=CARTESIAN_POINT('Ctrl Pts',(-0.574679115658286,-2.62124668345172,
12.5893111709658));
#438935=CARTESIAN_POINT('Origin',(-0.460383554137941,-2.90411316731588,
12.5));
#438936=CARTESIAN_POINT('',(-0.501820210172241,-2.68957202508688,13.7435492065112));
#438937=CARTESIAN_POINT('',(-0.505750802898757,-2.66922111036815,13.7902182540695));
#438938=CARTESIAN_POINT('Origin',(-0.516079721241096,-2.61574242383222,
13.7418732680445));
#438939=CARTESIAN_POINT('',(-0.512533505583296,-2.6341031997883,13.8235269408515));
#438940=CARTESIAN_POINT('',(-0.505750802898757,-2.66922111036815,13.7902182540695));
#438941=CARTESIAN_POINT('',(-0.512533505583296,-2.6341031997883,12.5893111709658));
#438942=CARTESIAN_POINT('',(-0.512533505583296,-2.6341031997883,12.5));
#438943=CARTESIAN_POINT('',(-0.501820210172241,-2.68957202508688,12.5369868989719));
#438944=CARTESIAN_POINT('Ctrl Pts',(-0.512533505583296,-2.6341031997883,
12.5893111709658));
#438945=CARTESIAN_POINT('Ctrl Pts',(-0.508959750310596,-2.65260656399841,
12.5718848856037));
#438946=CARTESIAN_POINT('Ctrl Pts',(-0.505388704100567,-2.67109590184985,
12.5544431401645));
#438947=CARTESIAN_POINT('Ctrl Pts',(-0.501820210172241,-2.68957202508688,
12.5369868989719));
#438948=CARTESIAN_POINT('',(-0.501820210172241,-2.68957202508688,12.5));
#438949=CARTESIAN_POINT('Origin',(-0.546284751524244,-2.64062194371897,
12.5));
#438950=CARTESIAN_POINT('',(-0.54042097942408,-2.60675150898696,13.8587068136939));
#438951=CARTESIAN_POINT('Ctrl Pts',(-0.512533505576834,-2.6341031997869,
13.8235269408542));
#438952=CARTESIAN_POINT('Ctrl Pts',(-0.512865804750207,-2.63238269791637,
13.8262006681044));
#438953=CARTESIAN_POINT('Ctrl Pts',(-0.513376451134595,-2.63065496289556,
13.8288634856214));
#438954=CARTESIAN_POINT('Ctrl Pts',(-0.514052260639445,-2.62892199117244,
13.8314912288862));
#438955=CARTESIAN_POINT('Ctrl Pts',(-0.514748950532427,-2.62713547607364,
13.834200161153));
#438956=CARTESIAN_POINT('Ctrl Pts',(-0.515621478177327,-2.62534123077201,
13.8368750301949));
#438957=CARTESIAN_POINT('Ctrl Pts',(-0.516700460746796,-2.62353789338469,
13.8394886372968));
#438958=CARTESIAN_POINT('Ctrl Pts',(-0.516783793187885,-2.62339861726397,
13.839690492513));
#438959=CARTESIAN_POINT('Ctrl Pts',(-0.516868377782284,-2.62325929483752,
13.8398919674349));
#438960=CARTESIAN_POINT('Ctrl Pts',(-0.516954238919628,-2.62311993049648,
13.8400930404591));
#438961=CARTESIAN_POINT('Ctrl Pts',(-0.518292013203951,-2.62094854030339,
13.8432258934518));
#438962=CARTESIAN_POINT('Ctrl Pts',(-0.519931893274218,-2.61877746447833,
13.8462331177034));
#438963=CARTESIAN_POINT('Ctrl Pts',(-0.521897370698895,-2.61673565388558,
13.8489036603661));
#438964=CARTESIAN_POINT('Ctrl Pts',(-0.522540497785662,-2.61606754969789,
13.849777493004));
#438965=CARTESIAN_POINT('Ctrl Pts',(-0.523218439369455,-2.61541353120771,
13.85061494757));
#438966=CARTESIAN_POINT('Ctrl Pts',(-0.52393187423922,-2.61477881519862,
13.8514076489583));
#438967=CARTESIAN_POINT('Ctrl Pts',(-0.525440891881487,-2.61343629929965,
13.8530843267192));
#438968=CARTESIAN_POINT('Ctrl Pts',(-0.527258891987578,-2.6120504790655,
13.8546805203176));
#438969=CARTESIAN_POINT('Ctrl Pts',(-0.529363076056738,-2.61081030075545,
13.8559412814274));
#438970=CARTESIAN_POINT('Ctrl Pts',(-0.529644684125489,-2.61064432467764,
13.8561100121513));
#438971=CARTESIAN_POINT('Ctrl Pts',(-0.52993134547584,-2.61048093207307,
13.8562727473908));
#438972=CARTESIAN_POINT('Ctrl Pts',(-0.530222937453116,-2.61032054227133,
13.8564289040185));
#438973=CARTESIAN_POINT('Ctrl Pts',(-0.531545303743502,-2.6095931763502,
13.8571370725437));
#438974=CARTESIAN_POINT('Ctrl Pts',(-0.532993414539191,-2.60891677597829,
13.8577210840553));
#438975=CARTESIAN_POINT('Ctrl Pts',(-0.534523401653899,-2.6083442233283,
13.8581177131616));
#438976=CARTESIAN_POINT('Ctrl Pts',(-0.534954298685957,-2.6081829727954,
13.8582294175695));
#438977=CARTESIAN_POINT('Ctrl Pts',(-0.535391596345183,-2.60802980832461,
13.8583265086086));
#438978=CARTESIAN_POINT('Ctrl Pts',(-0.535834105640109,-2.60788552453068,
13.8584082369006));
#438979=CARTESIAN_POINT('Ctrl Pts',(-0.536469872833358,-2.60767822741002,
13.8585256585398));
#438980=CARTESIAN_POINT('Ctrl Pts',(-0.537124402195584,-2.60748699199285,
13.8586122832068));
#438981=CARTESIAN_POINT('Ctrl Pts',(-0.537780912416568,-2.60731754401745,
13.8586682984299));
#438982=CARTESIAN_POINT('Ctrl Pts',(-0.538306055515589,-2.60718200243396,
13.8587131050557));
#438983=CARTESIAN_POINT('Ctrl Pts',(-0.538838207659092,-2.6070586772584,
13.8587357943552));
#438984=CARTESIAN_POINT('Ctrl Pts',(-0.53937754641893,-2.60694804720681,
13.8587355499465));
#438985=CARTESIAN_POINT('Ctrl Pts',(-0.539726133917808,-2.60687654436693,
13.8587353919793));
#438986=CARTESIAN_POINT('Ctrl Pts',(-0.540073946165131,-2.60681108005693,
13.8587257282814));
#438987=CARTESIAN_POINT('Ctrl Pts',(-0.54042097942408,-2.60675150898696,
13.8587068136939));
#438988=CARTESIAN_POINT('Ctrl Pts',(-0.54042097942408,-2.60675150898696,
13.8587068136939));
#438989=CARTESIAN_POINT('Ctrl Pts',(-0.541562352894183,-2.60655558298533,
13.8586446046466));
#438990=CARTESIAN_POINT('Ctrl Pts',(-0.542695311066701,-2.60642332639463,
13.858482427929));
#438991=CARTESIAN_POINT('Ctrl Pts',(-0.543819640952938,-2.60635027372574,
13.8582284286032));
#438992=CARTESIAN_POINT('Ctrl Pts',(-0.544973072628753,-2.60627533018529,
13.8579678548414));
#438993=CARTESIAN_POINT('Ctrl Pts',(-0.546120340402775,-2.60626404042183,
13.857615680862));
#438994=CARTESIAN_POINT('Ctrl Pts',(-0.547216118747798,-2.60630716032551,
13.8571944833187));
#438995=CARTESIAN_POINT('Ctrl Pts',(-0.549950745674822,-2.60641477045508,
13.8561433417727));
#438996=CARTESIAN_POINT('Ctrl Pts',(-0.552492800705602,-2.606861487623,
13.8546163505474));
#438997=CARTESIAN_POINT('Ctrl Pts',(-0.554735430543981,-2.60747028008139,
13.8528973491086));
#438998=CARTESIAN_POINT('Ctrl Pts',(-0.555145125928532,-2.60758149748164,
13.8525833129072));
#438999=CARTESIAN_POINT('Ctrl Pts',(-0.555544924168542,-2.60769802010329,
13.8522628768812));
#439000=CARTESIAN_POINT('Ctrl Pts',(-0.555934314092714,-2.607818657743,
13.851937733538));
#439001=CARTESIAN_POINT('Ctrl Pts',(-0.55831226433424,-2.60855537507098,
13.8499521282529));
#439002=CARTESIAN_POINT('Ctrl Pts',(-0.560537166023577,-2.6095226682952,
13.847639871647));
#439003=CARTESIAN_POINT('Ctrl Pts',(-0.562524118944962,-2.6105960213429,
13.8452109780794));
#439004=CARTESIAN_POINT('Ctrl Pts',(-0.563418090192172,-2.61107894509637,
13.8441181685877));
#439005=CARTESIAN_POINT('Ctrl Pts',(-0.564264432294491,-2.61158286382886,
13.8430021611332));
#439006=CARTESIAN_POINT('Ctrl Pts',(-0.565058450318323,-2.6120951250143,
13.8418824960098));
#439007=CARTESIAN_POINT('Ctrl Pts',(-0.566929574067454,-2.61330228157887,
13.8392439765549));
#439008=CARTESIAN_POINT('Ctrl Pts',(-0.568601629189551,-2.61461029451099,
13.8364981347964));
#439009=CARTESIAN_POINT('Ctrl Pts',(-0.570100122503587,-2.61599566984666,
13.8336931113419));
#439010=CARTESIAN_POINT('Ctrl Pts',(-0.571559559828334,-2.61734493744413,
13.8309611966328));
#439011=CARTESIAN_POINT('Ctrl Pts',(-0.572855444020918,-2.61876935384968,
13.8281701127186));
#439012=CARTESIAN_POINT('Ctrl Pts',(-0.573975989967246,-2.62026438828469,
13.8253580685121));
#439013=CARTESIAN_POINT('Ctrl Pts',(-0.574218925537742,-2.6205885133637,
13.8247484142933));
#439014=CARTESIAN_POINT('Ctrl Pts',(-0.574453446788048,-2.6209159666517,
13.8241378483365));
#439015=CARTESIAN_POINT('Ctrl Pts',(-0.574679115658286,-2.62124668345172,
13.8235269408515));
#439016=CARTESIAN_POINT('',(-0.539201119045522,-2.6069854267383,12.5969504640361));
#439017=CARTESIAN_POINT('Origin',(-0.546291645961924,-2.64065430340899,
12.584524458991));
#439018=CARTESIAN_POINT('Origin',(-0.546291645961924,-2.64065430340899,
12.584524458991));
#439019=CARTESIAN_POINT('Ctrl Pts',(-0.512533505583295,-2.6341031997883,
12.5893111709658));
#439020=CARTESIAN_POINT('Ctrl Pts',(-0.514682834418984,-2.6229749016203,
12.5770542771492));
#439021=CARTESIAN_POINT('Ctrl Pts',(-0.531047455888894,-2.6230281839015,
12.5737548217797));
#439022=CARTESIAN_POINT('Ctrl Pts',(-0.507833644755842,-2.65843705311383,
12.5663937883685));
#439023=CARTESIAN_POINT('Ctrl Pts',(-0.50998571535895,-2.64729455925604,
12.5540940315304));
#439024=CARTESIAN_POINT('Ctrl Pts',(-0.526401037016491,-2.64735121781805,
12.5508374392248));
#439025=CARTESIAN_POINT('Ctrl Pts',(-0.503138526030348,-2.68274635387966,
12.5434499600944));
#439026=CARTESIAN_POINT('Ctrl Pts',(-0.505297593781433,-2.67156763180639,
12.5311293540532));
#439027=CARTESIAN_POINT('Ctrl Pts',(-0.521757998883145,-2.67165026622646,
12.5278936106989));
#439028=CARTESIAN_POINT('Ctrl Pts',(-0.498447777951471,-2.70703302532143,
12.5204817579905));
#439029=CARTESIAN_POINT('Ctrl Pts',(-0.500617531612337,-2.69579897621351,
12.5081597038247));
#439030=CARTESIAN_POINT('Ctrl Pts',(-0.517118065116471,-2.69592719077464,
12.5049254088044));
#439031=CARTESIAN_POINT('Ctrl Pts',(-0.501820210172241,-2.68957202508688,
12.5369868989719));
#439032=CARTESIAN_POINT('Ctrl Pts',(-0.501643563314908,-2.69048662721815,
12.5342545179733));
#439033=CARTESIAN_POINT('Ctrl Pts',(-0.501597462099068,-2.69138313811672,
12.5314872231885));
#439034=CARTESIAN_POINT('Ctrl Pts',(-0.501740330620115,-2.69221392671548,
12.5287124745063));
#439035=CARTESIAN_POINT('Ctrl Pts',(-0.501869176543756,-2.69296317311051,
12.5262100684184));
#439036=CARTESIAN_POINT('Ctrl Pts',(-0.502152557146489,-2.69365804271822,
12.5237004536639));
#439037=CARTESIAN_POINT('Ctrl Pts',(-0.502656720631253,-2.69428543394549,
12.5212220730815));
#439038=CARTESIAN_POINT('Ctrl Pts',(-0.50304270139246,-2.69476575620364,
12.5193246583486));
#439039=CARTESIAN_POINT('Ctrl Pts',(-0.503563195692237,-2.69521187088284,
12.517417831369));
#439040=CARTESIAN_POINT('Ctrl Pts',(-0.504294802084582,-2.69556388905023,
12.5155812248347));
#439041=CARTESIAN_POINT('Ctrl Pts',(-0.504606470340122,-2.69571385068165,
12.5147988205793));
#439042=CARTESIAN_POINT('Ctrl Pts',(-0.504956647615943,-2.69584713748605,
12.5140295443047));
#439043=CARTESIAN_POINT('Ctrl Pts',(-0.50535157462054,-2.69596122260285,
12.5132817086137));
#439044=CARTESIAN_POINT('Ctrl Pts',(-0.505949243217482,-2.69613387499403,
12.5121499604604));
#439045=CARTESIAN_POINT('Ctrl Pts',(-0.506664291904626,-2.69625940782588,
12.5110494206568));
#439046=CARTESIAN_POINT('Ctrl Pts',(-0.507514620373767,-2.69630516379017,
12.5100666561695));
#439047=CARTESIAN_POINT('Ctrl Pts',(-0.508002877022615,-2.6963314367595,
12.5095023550641));
#439048=CARTESIAN_POINT('Ctrl Pts',(-0.508541412251363,-2.69633105881386,
12.5089719619137));
#439049=CARTESIAN_POINT('Ctrl Pts',(-0.509120127329921,-2.69629765006048,
12.5085043804652));
#439050=CARTESIAN_POINT('Ctrl Pts',(-0.509967001464448,-2.6962487607017,
12.5078201359221));
#439051=CARTESIAN_POINT('Ctrl Pts',(-0.510924411352231,-2.69612651374109,
12.5072563000949));
#439052=CARTESIAN_POINT('Ctrl Pts',(-0.511926386449674,-2.69593079789991,
12.5068768744332));
#439053=CARTESIAN_POINT('Ctrl Pts',(-0.512648879471132,-2.6957896733053,
12.5066032824114));
#439054=CARTESIAN_POINT('Ctrl Pts',(-0.513407248367904,-2.69560792887737,
12.5064197834844));
#439055=CARTESIAN_POINT('Ctrl Pts',(-0.514159746260541,-2.69539822737795,
12.5063282718343));
#439056=CARTESIAN_POINT('Ctrl Pts',(-0.515258160216331,-2.69509212811074,
12.5061946931565));
#439057=CARTESIAN_POINT('Ctrl Pts',(-0.516367827280128,-2.69472094151683,
12.5062515701262));
#439058=CARTESIAN_POINT('Ctrl Pts',(-0.517424785305864,-2.69432236987892,
12.5064436508398));
#439059=CARTESIAN_POINT('',(-0.531047455888895,-2.6230281839015,12.5737548217797));
#439060=CARTESIAN_POINT('Origin',(-0.534134302985502,-2.63827519590392,
12.5893111709658));
#439061=CARTESIAN_POINT('Ctrl Pts',(-0.517424785305864,-2.69432236987892,
12.5064436508398));
#439062=CARTESIAN_POINT('Ctrl Pts',(-0.519441766381226,-2.68376906825844,
12.5164271754438));
#439063=CARTESIAN_POINT('Ctrl Pts',(-0.521459341766315,-2.67321154408909,
12.5264061185523));
#439064=CARTESIAN_POINT('Ctrl Pts',(-0.52347753332189,-2.66264964883392,
12.536380305637));
#439065=CARTESIAN_POINT('Ctrl Pts',(-0.525999863433005,-2.64944942194814,
12.5488460165097));
#439066=CARTESIAN_POINT('Ctrl Pts',(-0.52852315671935,-2.63624236355297,
12.5613043021964));
#439067=CARTESIAN_POINT('Ctrl Pts',(-0.531047455888894,-2.6230281839015,
12.5737548217797));
#439068=CARTESIAN_POINT('Ctrl Pts',(-0.574679115658286,-2.62124668345172,
12.5893111709658));
#439069=CARTESIAN_POINT('Ctrl Pts',(-0.568290798210283,-2.61188463053886,
12.5770542771492));
#439070=CARTESIAN_POINT('Ctrl Pts',(-0.553290581744299,-2.61842658596736,
12.5737548217797));
#439071=CARTESIAN_POINT('Ctrl Pts',(-0.56871887104195,-2.61251196951086,
12.5928319619712));
#439072=CARTESIAN_POINT('Ctrl Pts',(-0.561734573488288,-2.60805629851163,
12.5821634970843));
#439073=CARTESIAN_POINT('Ctrl Pts',(-0.551127205560511,-2.6152394209486,
12.5773203894503));
#439074=CARTESIAN_POINT('Ctrl Pts',(-0.554366844473443,-2.60387464164186,
12.5969440695591));
#439075=CARTESIAN_POINT('Ctrl Pts',(-0.550426767355019,-2.60467109305456,
12.5878292599214));
#439076=CARTESIAN_POINT('Ctrl Pts',(-0.546010795437804,-2.61216265404911,
12.5813877129824));
#439077=CARTESIAN_POINT('Ctrl Pts',(-0.524393439825277,-2.61002039296604,
12.596957478804));
#439078=CARTESIAN_POINT('Ctrl Pts',(-0.528304414599265,-2.60922990611218,
12.5878468778671));
#439079=CARTESIAN_POINT('Ctrl Pts',(-0.535284096582965,-2.6143681471871,
12.5814011370086));
#439080=CARTESIAN_POINT('Ctrl Pts',(-0.514541722392628,-2.62370551886122,
12.5928371701607));
#439081=CARTESIAN_POINT('Ctrl Pts',(-0.51918652156212,-2.61685271604931,
12.5821692192951));
#439082=CARTESIAN_POINT('Ctrl Pts',(-0.531770729566533,-2.61923211321443,
12.5773318885715));
#439083=CARTESIAN_POINT('Ctrl Pts',(-0.512533505583241,-2.63410319978828,
12.5893111709658));
#439084=CARTESIAN_POINT('Ctrl Pts',(-0.514682834418931,-2.62297490162029,
12.5770542771492));
#439085=CARTESIAN_POINT('Ctrl Pts',(-0.53104745588884,-2.62302818390148,
12.5737548217797));
#439086=CARTESIAN_POINT('',(-0.553290581744299,-2.61842658596736,12.5737548217797));
#439087=CARTESIAN_POINT('Origin',(-0.556506722612499,-2.63364685002276,
12.5893111709658));
#439088=CARTESIAN_POINT('Ctrl Pts',(-0.53104745588884,-2.62302818390148,
12.5737548217797));
#439089=CARTESIAN_POINT('Ctrl Pts',(-0.531205307234454,-2.62203853619462,
12.5746934679442));
#439090=CARTESIAN_POINT('Ctrl Pts',(-0.531560877886354,-2.6209722787446,
12.5756680099006));
#439091=CARTESIAN_POINT('Ctrl Pts',(-0.532070555016628,-2.61994966792378,
12.5765688348656));
#439092=CARTESIAN_POINT('Ctrl Pts',(-0.532205486394558,-2.61967894302964,
12.5768073183026));
#439093=CARTESIAN_POINT('Ctrl Pts',(-0.532350967513118,-2.619411221954,
12.5770407398754));
#439094=CARTESIAN_POINT('Ctrl Pts',(-0.532505687190963,-2.6191484807045,
12.5772674179684));
#439095=CARTESIAN_POINT('Ctrl Pts',(-0.533140614910869,-2.61807026166477,
12.5781976435658));
#439096=CARTESIAN_POINT('Ctrl Pts',(-0.533976907712846,-2.61702038937152,
12.5790594849312));
#439097=CARTESIAN_POINT('Ctrl Pts',(-0.534995868491428,-2.616099839723,
12.5797571720115));
#439098=CARTESIAN_POINT('Ctrl Pts',(-0.535659758077238,-2.61550006852697,
12.580211740231));
#439099=CARTESIAN_POINT('Ctrl Pts',(-0.53644394514693,-2.61494186818654,
12.5806009430798));
#439100=CARTESIAN_POINT('Ctrl Pts',(-0.537303500385903,-2.61447896705728,
12.5808812374708));
#439101=CARTESIAN_POINT('Ctrl Pts',(-0.538042143490665,-2.61408118142139,
12.5811221033394));
#439102=CARTESIAN_POINT('Ctrl Pts',(-0.538851618408412,-2.61374572634208,
12.581287365893));
#439103=CARTESIAN_POINT('Ctrl Pts',(-0.539689429173579,-2.61349923819789,
12.581359338449));
#439104=CARTESIAN_POINT('Ctrl Pts',(-0.539805867569806,-2.61346498143563,
12.5813693411482));
#439105=CARTESIAN_POINT('Ctrl Pts',(-0.539922856491515,-2.61343238330141,
12.5813775999465));
#439106=CARTESIAN_POINT('Ctrl Pts',(-0.540040286236262,-2.61340145411238,
12.5813841266931));
#439107=CARTESIAN_POINT('Ctrl Pts',(-0.540239520001061,-2.61334897900239,
12.5813952001081));
#439108=CARTESIAN_POINT('Ctrl Pts',(-0.540441512135912,-2.61330154532691,
12.5814007534795));
#439109=CARTESIAN_POINT('Ctrl Pts',(-0.540646219750891,-2.61325936573213,
12.5814005856065));
#439110=CARTESIAN_POINT('Ctrl Pts',(-0.541583291176775,-2.61306628403835,
12.5813998171494));
#439111=CARTESIAN_POINT('Ctrl Pts',(-0.542512451594518,-2.61299630890861,
12.58127954464));
#439112=CARTESIAN_POINT('Ctrl Pts',(-0.543426203753064,-2.61302033181186,
12.5810700125799));
#439113=CARTESIAN_POINT('Ctrl Pts',(-0.544529912321574,-2.61304934874376,
12.5808169217085));
#439114=CARTESIAN_POINT('Ctrl Pts',(-0.545610800346387,-2.61323224061694,
12.5804173076348));
#439115=CARTESIAN_POINT('Ctrl Pts',(-0.546578485375059,-2.61352730171729,
12.5799304713245));
#439116=CARTESIAN_POINT('Ctrl Pts',(-0.547777751977805,-2.61389297537445,
12.5793271277669));
#439117=CARTESIAN_POINT('Ctrl Pts',(-0.548886934063721,-2.61442281299927,
12.5785808224116));
#439118=CARTESIAN_POINT('Ctrl Pts',(-0.549872948431136,-2.61506586162127,
12.5777485681082));
#439119=CARTESIAN_POINT('Ctrl Pts',(-0.551342217864523,-2.61602407451928,
12.576508418016));
#439120=CARTESIAN_POINT('Ctrl Pts',(-0.552529384958163,-2.6172198394638,
12.5750928681475));
#439121=CARTESIAN_POINT('Ctrl Pts',(-0.553290581744299,-2.61842658596736,
12.5737548217797));
#439122=CARTESIAN_POINT('Ctrl Pts',(-0.553290581744299,-2.61842658596736,
12.5737548217797));
#439123=CARTESIAN_POINT('Ctrl Pts',(-0.568290798210284,-2.61188463053886,
12.5770542771492));
#439124=CARTESIAN_POINT('Ctrl Pts',(-0.574679115658286,-2.62124668345172,
12.5893111709658));
#439125=CARTESIAN_POINT('Ctrl Pts',(-0.567204249287228,-2.63890644948437,
12.5508408821982));
#439126=CARTESIAN_POINT('Ctrl Pts',(-0.582249655992346,-2.63234127913569,
12.55409748406));
#439127=CARTESIAN_POINT('Ctrl Pts',(-0.588646123297284,-2.64171527563033,
12.5663972313419));
#439128=CARTESIAN_POINT('Ctrl Pts',(-0.581105300580312,-2.6593656439147,
12.52790050457));
#439129=CARTESIAN_POINT('Ctrl Pts',(-0.596181779239276,-2.65275874838143,
12.5311362602938));
#439130=CARTESIAN_POINT('Ctrl Pts',(-0.602599040520637,-2.66216321836284,
12.5434568539655));
#439131=CARTESIAN_POINT('Ctrl Pts',(-0.594994727522753,-2.67980576772958,
12.5049357605811));
#439132=CARTESIAN_POINT('Ctrl Pts',(-0.610089954889711,-2.67314112252303,
12.5081700652078));
#439133=CARTESIAN_POINT('Ctrl Pts',(-0.616538970892595,-2.68259212891811,
12.5204921097672));
#439134=CARTESIAN_POINT('Ctrl Pts',(-0.594082694617563,-2.67846358818504,
12.5064436508395));
#439135=CARTESIAN_POINT('Ctrl Pts',(-0.595301507966785,-2.67840577979169,
12.5062361689309));
#439136=CARTESIAN_POINT('Ctrl Pts',(-0.596566509032947,-2.67829369088479,
12.5061871075061));
#439137=CARTESIAN_POINT('Ctrl Pts',(-0.597782912656175,-2.67811655007494,
12.5063648335164));
#439138=CARTESIAN_POINT('Ctrl Pts',(-0.598335478212733,-2.67803608179261,
12.5064455676329));
#439139=CARTESIAN_POINT('Ctrl Pts',(-0.598885690899769,-2.67794084943099,
12.506574497099));
#439140=CARTESIAN_POINT('Ctrl Pts',(-0.599409780011249,-2.67783390071578,
12.5067492519495));
#439141=CARTESIAN_POINT('Ctrl Pts',(-0.600462957424485,-2.67761898312111,
12.5071004286051));
#439142=CARTESIAN_POINT('Ctrl Pts',(-0.601449201390686,-2.67734805838752,
12.5076537929613));
#439143=CARTESIAN_POINT('Ctrl Pts',(-0.602296994582825,-2.67705058141408,
12.5083435010505));
#439144=CARTESIAN_POINT('Ctrl Pts',(-0.60235036823071,-2.67703185346087,
12.5083869222964));
#439145=CARTESIAN_POINT('Ctrl Pts',(-0.602403195004169,-2.67701300696501,
12.5084308732337));
#439146=CARTESIAN_POINT('Ctrl Pts',(-0.60245545821059,-2.6769940439138,
12.5084753333615));
#439147=CARTESIAN_POINT('Ctrl Pts',(-0.602874678107263,-2.67684193521421,
12.5088319622689));
#439148=CARTESIAN_POINT('Ctrl Pts',(-0.603266588089933,-2.6766804518268,
12.509227847131));
#439149=CARTESIAN_POINT('Ctrl Pts',(-0.603620601365606,-2.67651698438931,
12.5096423454524));
#439150=CARTESIAN_POINT('Ctrl Pts',(-0.604729922291853,-2.67600474978787,
12.5109411997424));
#439151=CARTESIAN_POINT('Ctrl Pts',(-0.605539412171032,-2.6754503057193,
12.5124831113042));
#439152=CARTESIAN_POINT('Ctrl Pts',(-0.606129412512988,-2.67490366317433,
12.5140723025008));
#439153=CARTESIAN_POINT('Ctrl Pts',(-0.606184696191238,-2.67485244216915,
12.5142212114565));
#439154=CARTESIAN_POINT('Ctrl Pts',(-0.60623808180628,-2.67480129547157,
12.5143705582413));
#439155=CARTESIAN_POINT('Ctrl Pts',(-0.606289651733421,-2.67475026906041,
12.5145201959299));
#439156=CARTESIAN_POINT('Ctrl Pts',(-0.606952144227129,-2.67409475883863,
12.5164425148273));
#439157=CARTESIAN_POINT('Ctrl Pts',(-0.607345241773047,-2.67344427279055,
12.518463520594));
#439158=CARTESIAN_POINT('Ctrl Pts',(-0.6075591507324,-2.67279970026717,
12.5205025929157));
#439159=CARTESIAN_POINT('Ctrl Pts',(-0.607683226407384,-2.67242582265514,
12.5216853356836));
#439160=CARTESIAN_POINT('Ctrl Pts',(-0.607747249614855,-2.672054762305,
12.5228750347131));
#439161=CARTESIAN_POINT('Ctrl Pts',(-0.607768422805009,-2.67169260274821,
12.5240609649613));
#439162=CARTESIAN_POINT('Ctrl Pts',(-0.607820391264341,-2.67080370154528,
12.5269717671327));
#439163=CARTESIAN_POINT('Ctrl Pts',(-0.607605302655558,-2.66994279743996,
12.5299036066169));
#439164=CARTESIAN_POINT('Ctrl Pts',(-0.607209513689908,-2.66910267648389,
12.5328133004019));
#439165=CARTESIAN_POINT('Ctrl Pts',(-0.607019511940296,-2.6686993695062,
12.5342101228452));
#439166=CARTESIAN_POINT('Ctrl Pts',(-0.606787629694283,-2.66830157869353,
12.5356023438238));
#439167=CARTESIAN_POINT('Ctrl Pts',(-0.60652158241518,-2.66791168735621,
12.5369868989719));
#439168=CARTESIAN_POINT('Origin',(-7.79562337705996,-13.1941084893106,-1.24176179718076));
#439169=CARTESIAN_POINT('Ctrl Pts',(-0.50182809689576,-2.6895309816888,
12.5369868989719));
#439170=CARTESIAN_POINT('Ctrl Pts',(-0.49894789389784,-2.7045970938076,
12.5369868989719));
#439171=CARTESIAN_POINT('Ctrl Pts',(-0.483815219891114,-2.70710417998317,
12.5369868989719));
#439172=CARTESIAN_POINT('Ctrl Pts',(-0.500854410604185,-2.69462390438445,
12.5218025310016));
#439173=CARTESIAN_POINT('Ctrl Pts',(-0.495467014549673,-2.70514207092888,
12.5216901060418));
#439174=CARTESIAN_POINT('Ctrl Pts',(-0.483861351992054,-2.70709655382362,
12.5161920673678));
#439175=CARTESIAN_POINT('Ctrl Pts',(-0.505003168253044,-2.69899699038481,
12.5042015548894));
#439176=CARTESIAN_POINT('Ctrl Pts',(-0.501057993818192,-2.70407763440851,
12.4980677368513));
#439177=CARTESIAN_POINT('Ctrl Pts',(-0.494374261000064,-2.70530990683761,
12.4907278922777));
#439178=CARTESIAN_POINT('Ctrl Pts',(-0.51742101318441,-2.69430272772006,
12.506463626192));
#439179=CARTESIAN_POINT('Ctrl Pts',(-0.518654950118071,-2.70072805557008,
12.4999376786891));
#439180=CARTESIAN_POINT('Ctrl Pts',(-0.51863987937257,-2.70064957953281,
12.4906970594712));
#439181=CARTESIAN_POINT('Origin',(-0.480219412770034,-2.68540002897125,
12.5369868989719));
#439182=CARTESIAN_POINT('Origin',(-0.480219412770034,-2.68540002897125,
14.));
#439183=CARTESIAN_POINT('Origin',(-0.480219412770035,-2.68540002897125,
13.7435492065112));
#439184=CARTESIAN_POINT('Ctrl Pts',(-0.506515595222954,-2.66526120222706,
13.793642941384));
#439185=CARTESIAN_POINT('Ctrl Pts',(-0.504491922906485,-2.67588245306495,
13.8071662555867));
#439186=CARTESIAN_POINT('Ctrl Pts',(-0.487476079996624,-2.67518929096144,
13.8103758687955));
#439187=CARTESIAN_POINT('Ctrl Pts',(-0.50336363189204,-2.68158072527108,
13.7804579775006));
#439188=CARTESIAN_POINT('Ctrl Pts',(-0.500856641562832,-2.69468449080693,
13.7901904343351));
#439189=CARTESIAN_POINT('Ctrl Pts',(-0.485217220963456,-2.69659876546848,
13.7927914348262));
#439190=CARTESIAN_POINT('Ctrl Pts',(-0.50150795242008,-2.69118864265259,
13.7597120340895));
#439191=CARTESIAN_POINT('Ctrl Pts',(-0.498601030277574,-2.70635231284253,
13.7635825532445));
#439192=CARTESIAN_POINT('Ctrl Pts',(-0.4838597530705,-2.7092212259552,13.7651073818885));
#439193=CARTESIAN_POINT('Ctrl Pts',(-0.501871336950118,-2.68930719243286,
13.7381884353898));
#439194=CARTESIAN_POINT('Ctrl Pts',(-0.499033339494265,-2.70411609789771,
13.7368803041982));
#439195=CARTESIAN_POINT('Ctrl Pts',(-0.484125094223456,-2.70674932027047,
13.7363986145813));
#439196=CARTESIAN_POINT('Origin',(-0.48415000549655,-2.66504911425252,13.7902182540695));
#439197=CARTESIAN_POINT('Ctrl Pts',(-0.512534251283801,-2.63409933487053,
13.8235227101244));
#439198=CARTESIAN_POINT('Ctrl Pts',(-0.510358343330453,-2.64538862682787,
13.8358800583119));
#439199=CARTESIAN_POINT('Ctrl Pts',(-0.493787321992115,-2.64522339710559,
13.8390832900376));
#439200=CARTESIAN_POINT('Ctrl Pts',(-0.510272350612621,-2.64581048146887,
13.8124254819053));
#439201=CARTESIAN_POINT('Ctrl Pts',(-0.508092216803741,-2.65712169701854,
13.8247886449158));
#439202=CARTESIAN_POINT('Ctrl Pts',(-0.49150042722439,-2.65693921508178,
13.8279860620657));
#439203=CARTESIAN_POINT('Ctrl Pts',(-0.508011463651739,-2.65751637951236,
13.8013225099955));
#439204=CARTESIAN_POINT('Ctrl Pts',(-0.505828134628754,-2.66884418195635,
13.8136962257787));
#439205=CARTESIAN_POINT('Ctrl Pts',(-0.48921485721179,-2.66864966113977,
13.8168830918626));
#439206=CARTESIAN_POINT('Ctrl Pts',(-0.505751550959262,-2.6692172332141,
13.7902140179785));
#439207=CARTESIAN_POINT('Ctrl Pts',(-0.503565990000837,-2.68055663464635,
13.802602731458));
#439208=CARTESIAN_POINT('Ctrl Pts',(-0.486930561707674,-2.68035494670785,
13.8057746032558));
#439209=CARTESIAN_POINT('Origin',(-0.490932708181089,-2.62993120367267,
13.8235269408515));
#439210=CARTESIAN_POINT('Ctrl Pts',(-0.574679115658286,-2.62124668345172,
13.8235269408515));
#439211=CARTESIAN_POINT('Ctrl Pts',(-0.581334330980055,-2.6309998740995,
13.8362179249168));
#439212=CARTESIAN_POINT('Ctrl Pts',(-0.596812372087366,-2.6237823088911,
13.8391868794938));
#439213=CARTESIAN_POINT('Ctrl Pts',(-0.568589883323139,-2.61232293854011,
13.8400110824519));
#439214=CARTESIAN_POINT('Ctrl Pts',(-0.57675154406485,-2.61821438630772,
13.8494522556836));
#439215=CARTESIAN_POINT('Ctrl Pts',(-0.586698405882847,-2.6091596733134,
13.85569149686));
#439216=CARTESIAN_POINT('Ctrl Pts',(-0.554703493556176,-2.60380437614469,
13.8586819406588));
#439217=CARTESIAN_POINT('Ctrl Pts',(-0.558969862482477,-2.60293596390406,
13.868010383617));
#439218=CARTESIAN_POINT('Ctrl Pts',(-0.563570379861988,-2.59514313985668,
13.8744918421245));
#439219=CARTESIAN_POINT('Ctrl Pts',(-0.524051565732569,-2.61009173001124,
13.8587686893867));
#439220=CARTESIAN_POINT('Ctrl Pts',(-0.519823156218783,-2.6109523582141,
13.8680909899357));
#439221=CARTESIAN_POINT('Ctrl Pts',(-0.512544438437598,-2.60561225812444,
13.8745789365163));
#439222=CARTESIAN_POINT('Ctrl Pts',(-0.514585541916014,-2.62347864022474,
13.8400379222776));
#439223=CARTESIAN_POINT('Ctrl Pts',(-0.509426554028352,-2.63211895722606,
13.8494748685453));
#439224=CARTESIAN_POINT('Ctrl Pts',(-0.496708995412886,-2.62775721352352,
13.8557104837033));
#439225=CARTESIAN_POINT('Ctrl Pts',(-0.512533505576834,-2.6341031997869,
13.8235269408542));
#439226=CARTESIAN_POINT('Ctrl Pts',(-0.510294379810855,-2.64569642774958,
13.8362179249195));
#439227=CARTESIAN_POINT('Ctrl Pts',(-0.493223091178564,-2.64521258016071,
13.8391868794964));
#439228=CARTESIAN_POINT('Origin',(-0.592851508704073,-2.60884651688069,
13.8235269408515));
#439229=CARTESIAN_POINT('Ctrl Pts',(-0.594836702480581,-2.65078754258225,
13.7902140241683));
#439230=CARTESIAN_POINT('Ctrl Pts',(-0.601342040951324,-2.66032898727232,
13.8026027327198));
#439231=CARTESIAN_POINT('Ctrl Pts',(-0.61653194602864,-2.65354336158153,
13.8057746032556));
#439232=CARTESIAN_POINT('Ctrl Pts',(-0.588119703459966,-2.64094380818014,
13.8013225161808));
#439233=CARTESIAN_POINT('Ctrl Pts',(-0.594618391022464,-2.65047549154932,
13.8136962270464));
#439234=CARTESIAN_POINT('Ctrl Pts',(-0.609790807176059,-2.64370523355015,
13.8168830918628));
#439235=CARTESIAN_POINT('Ctrl Pts',(-0.581399808680621,-2.63109583005556,
13.8124254880875));
#439236=CARTESIAN_POINT('Ctrl Pts',(-0.587888982059299,-2.64061355582919,
13.8247886461868));
#439237=CARTESIAN_POINT('Ctrl Pts',(-0.603046450886306,-2.63386287431128,
13.8279860620656));
#439238=CARTESIAN_POINT('Ctrl Pts',(-0.574676900910916,-2.62124343640604,
13.8235227163066));
#439239=CARTESIAN_POINT('Ctrl Pts',(-0.581153496605596,-2.63074271487572,
13.8358800595847));
#439240=CARTESIAN_POINT('Ctrl Pts',(-0.596298747147209,-2.62401610972678,
13.8390832900376));
#439241=CARTESIAN_POINT('Origin',(-0.613011317284678,-2.63839063333718,
13.7902182540695));
#439242=CARTESIAN_POINT('Ctrl Pts',(-0.606369500303375,-2.66768876270811,
13.7382347919292));
#439243=CARTESIAN_POINT('Ctrl Pts',(-0.614855234269111,-2.68016715153825,
13.7369371795943));
#439244=CARTESIAN_POINT('Ctrl Pts',(-0.629594010822871,-2.67665827098757,
13.7364597369711));
#439245=CARTESIAN_POINT('Ctrl Pts',(-0.607435665510839,-2.66925122414269,
13.7595490285574));
#439246=CARTESIAN_POINT('Ctrl Pts',(-0.616124693214113,-2.68202677125392,
13.7633824266926));
#439247=CARTESIAN_POINT('Ctrl Pts',(-0.6308030328376,-2.67879567140946,
13.7648920890506));
#439248=CARTESIAN_POINT('Ctrl Pts',(-0.601998281355425,-2.66128275642936,
13.7803806590111));
#439249=CARTESIAN_POINT('Ctrl Pts',(-0.609509515461666,-2.67233618341856,
13.7901039518744));
#439250=CARTESIAN_POINT('Ctrl Pts',(-0.624636074984075,-2.66790079860536,
13.7926933640892));
#439251=CARTESIAN_POINT('Ctrl Pts',(-0.592546893980175,-2.64743178071439,
13.7936647693663));
#439252=CARTESIAN_POINT('Ctrl Pts',(-0.598618158232228,-2.65638237188629,
13.8072068914933));
#439253=CARTESIAN_POINT('Ctrl Pts',(-0.613974193817631,-2.64897720875863,
13.8104111085397));
#439254=CARTESIAN_POINT('Origin',(-0.624693975460967,-2.65551152078517,
13.7435492065112));
#439255=CARTESIAN_POINT('Origin',(-0.624693975460967,-2.65551152078517,
14.));
#439256=CARTESIAN_POINT('Origin',(-0.624693975460967,-2.65551152078517,
12.5369868989719));
#439257=CARTESIAN_POINT('Ctrl Pts',(-0.594078713948304,-2.67844564110547,
12.506462012331));
#439258=CARTESIAN_POINT('Ctrl Pts',(-0.595494570650946,-2.68482913057342,
12.4999388158272));
#439259=CARTESIAN_POINT('Ctrl Pts',(-0.595477819209372,-2.68475360552158,
12.4907030323752));
#439260=CARTESIAN_POINT('Ctrl Pts',(-0.607339333701184,-2.67782552262988,
12.5042014951932));
#439261=CARTESIAN_POINT('Ctrl Pts',(-0.612973609332226,-2.68092326942868,
12.4980716682127));
#439262=CARTESIAN_POINT('Ctrl Pts',(-0.619593324702907,-2.67940506863922,
12.4907355092743));
#439263=CARTESIAN_POINT('Ctrl Pts',(-0.609414332117057,-2.6721668935716,
12.5218047446509));
#439264=CARTESIAN_POINT('Ctrl Pts',(-0.618529083026261,-2.67967956199229,
12.5216906929434));
#439265=CARTESIAN_POINT('Ctrl Pts',(-0.629952685569496,-2.67687384296435,
12.5161988840776));
#439266=CARTESIAN_POINT('Ctrl Pts',(-0.606499957111761,-2.66787993605588,
12.5369868989719));
#439267=CARTESIAN_POINT('Ctrl Pts',(-0.615118431985925,-2.68055776798267,
12.5369868989719));
#439268=CARTESIAN_POINT('Ctrl Pts',(-0.629996401635299,-2.67686296749648,
12.5369868989719));
#439269=CARTESIAN_POINT('Origin',(-1.04370312006722E-31,-1.01968969974689E-30,
12.5));
#439270=CARTESIAN_POINT('Origin',(-0.359110979140358,-2.65936638433693,
12.5));
#439271=CARTESIAN_POINT('',(-0.359110979140358,-2.65936638433693,12.5893111709658));
#439272=CARTESIAN_POINT('',(-0.359110979140358,-2.65936638433693,13.8235269408515));
#439273=CARTESIAN_POINT('',(-0.359110979140358,-2.65936638433693,12.5));
#439274=CARTESIAN_POINT('',(-0.376795587855578,-2.69045540673699,13.7902182540695));
#439275=CARTESIAN_POINT('',(-0.359110979140358,-2.65936638433693,13.8235269408515));
#439276=CARTESIAN_POINT('',(-0.38704386168096,-2.70847157094225,13.7435492065112));
#439277=CARTESIAN_POINT('Origin',(-0.353326893110259,-2.64919878991666,
13.744521291872));
#439278=CARTESIAN_POINT('',(-0.38704386168096,-2.70847157094225,12.5369868989719));
#439279=CARTESIAN_POINT('',(-0.38704386168096,-2.70847157094225,12.5));
#439280=CARTESIAN_POINT('Ctrl Pts',(-0.38704386168096,-2.70847157094225,
12.5369868989719));
#439281=CARTESIAN_POINT('Ctrl Pts',(-0.377739691682629,-2.6921151135193,
12.5544431401645));
#439282=CARTESIAN_POINT('Ctrl Pts',(-0.368428867094625,-2.67574695752327,
12.5718848856037));
#439283=CARTESIAN_POINT('Ctrl Pts',(-0.359110979140358,-2.65936638433693,
12.5893111709658));
#439284=CARTESIAN_POINT('Origin',(-0.222139482233007,-2.93197550397874,
12.5));
#439285=CARTESIAN_POINT('',(-0.280925356007091,-2.72152570184806,13.7435492065112));
#439286=CARTESIAN_POINT('',(-0.286501658488811,-2.70156288291627,13.7902182540695));
#439287=CARTESIAN_POINT('Origin',(-0.301155217631046,-2.6491040450355,13.7418732680457));
#439288=CARTESIAN_POINT('',(-0.296124228020734,-2.66711467752318,13.8235269408515));
#439289=CARTESIAN_POINT('',(-0.286501658488811,-2.70156288291627,13.7902182540695));
#439290=CARTESIAN_POINT('',(-0.296124228020734,-2.66711467752318,12.5893111709658));
#439291=CARTESIAN_POINT('',(-0.296124228020734,-2.66711467752318,12.5));
#439292=CARTESIAN_POINT('',(-0.280925356007091,-2.72152570184806,12.5369868989719));
#439293=CARTESIAN_POINT('Ctrl Pts',(-0.296124228020734,-2.66711467752318,
12.5893111709658));
#439294=CARTESIAN_POINT('Ctrl Pts',(-0.291054168163914,-2.68526517908345,
12.5718848856037));
#439295=CARTESIAN_POINT('Ctrl Pts',(-0.285987951634028,-2.70340192177036,
12.5544431401645));
#439296=CARTESIAN_POINT('Ctrl Pts',(-0.280925356007091,-2.72152570184806,
12.5369868989719));
#439297=CARTESIAN_POINT('',(-0.280925356007091,-2.72152570184806,12.5));
#439298=CARTESIAN_POINT('Origin',(-0.32923183132768,-2.67636277074664,12.5));
#439299=CARTESIAN_POINT('',(-0.326148325313847,-2.64212708522933,13.8587068136939));
#439300=CARTESIAN_POINT('Ctrl Pts',(-0.296124228014408,-2.66711467752126,
13.8235269408542));
#439301=CARTESIAN_POINT('Ctrl Pts',(-0.296595658364503,-2.66542698594632,
13.8262006681044));
#439302=CARTESIAN_POINT('Ctrl Pts',(-0.297245432058879,-2.6637466222422,
13.8288634856214));
#439303=CARTESIAN_POINT('Ctrl Pts',(-0.298060246146911,-2.66207450158807,
13.8314912288862));
#439304=CARTESIAN_POINT('Ctrl Pts',(-0.298900235427497,-2.66035071766492,
13.8342001611531));
#439305=CARTESIAN_POINT('Ctrl Pts',(-0.299916107457681,-2.65863356166973,
13.8368750301949));
#439306=CARTESIAN_POINT('Ctrl Pts',(-0.301138488540095,-2.65692417183499,
13.8394886372968));
#439307=CARTESIAN_POINT('Ctrl Pts',(-0.301232895996174,-2.65679215151165,
13.8396904925131));
#439308=CARTESIAN_POINT('Ctrl Pts',(-0.301328555213474,-2.65666018709877,
13.8398919674349));
#439309=CARTESIAN_POINT('Ctrl Pts',(-0.301425490142556,-2.65652828496087,
13.8400930404591));
#439310=CARTESIAN_POINT('Ctrl Pts',(-0.302935801552247,-2.65447316091299,
13.8432258934518));
#439311=CARTESIAN_POINT('Ctrl Pts',(-0.304747187891887,-2.65244297461327,
13.8462331177034));
#439312=CARTESIAN_POINT('Ctrl Pts',(-0.306872551871129,-2.65056816263354,
13.8489036603661));
#439313=CARTESIAN_POINT('Ctrl Pts',(-0.307567995699242,-2.64995470233548,
13.8497774930041));
#439314=CARTESIAN_POINT('Ctrl Pts',(-0.308296990066901,-2.64935811857066,
13.85061494757));
#439315=CARTESIAN_POINT('Ctrl Pts',(-0.309059786288148,-2.64878366609183,
13.8514076489583));
#439316=CARTESIAN_POINT('Ctrl Pts',(-0.31067321030777,-2.64756861625064,
13.8530843267192));
#439317=CARTESIAN_POINT('Ctrl Pts',(-0.312598118382892,-2.64633559110513,
13.8546805203176));
#439318=CARTESIAN_POINT('Ctrl Pts',(-0.314796386998666,-2.64527104992204,
13.8559412814274));
#439319=CARTESIAN_POINT('Ctrl Pts',(-0.315090586630988,-2.64512857978785,
13.8561100121513));
#439320=CARTESIAN_POINT('Ctrl Pts',(-0.315389612153481,-2.64498909641999,
13.8562727473908));
#439321=CARTESIAN_POINT('Ctrl Pts',(-0.315693307140336,-2.64485300775523,
13.8564289040185));
#439322=CARTESIAN_POINT('Ctrl Pts',(-0.317070560441086,-2.64423584721311,
13.8571370725437));
#439323=CARTESIAN_POINT('Ctrl Pts',(-0.318568985677268,-2.6436797319811,
13.8577210840553));
#439324=CARTESIAN_POINT('Ctrl Pts',(-0.320140550242359,-2.64323379260637,
13.8581177131616));
#439325=CARTESIAN_POINT('Ctrl Pts',(-0.320583156915499,-2.64310820072968,
13.8582294175695));
#439326=CARTESIAN_POINT('Ctrl Pts',(-0.321031483829118,-2.64299118971994,
13.8583265086086));
#439327=CARTESIAN_POINT('Ctrl Pts',(-0.321484281179541,-2.64288345463402,
13.8584082369006));
#439328=CARTESIAN_POINT('Ctrl Pts',(-0.322134829549688,-2.64272866820585,
13.8585256585398));
#439329=CARTESIAN_POINT('Ctrl Pts',(-0.322802768481298,-2.64259141932814,
13.8586122832068));
#439330=CARTESIAN_POINT('Ctrl Pts',(-0.323470905801753,-2.64247604685465,
13.8586682984299));
#439331=CARTESIAN_POINT('Ctrl Pts',(-0.324005349427795,-2.64238376031236,
13.8587131050557));
#439332=CARTESIAN_POINT('Ctrl Pts',(-0.324545783025643,-2.6423042208311,
13.8587357943552));
#439333=CARTESIAN_POINT('Ctrl Pts',(-0.325092344556493,-2.64223792000778,
13.8587355499465));
#439334=CARTESIAN_POINT('Ctrl Pts',(-0.325445600304463,-2.64219506820499,
13.8587353919793));
#439335=CARTESIAN_POINT('Ctrl Pts',(-0.325797591184218,-2.64215817164918,
13.8587257282814));
#439336=CARTESIAN_POINT('Ctrl Pts',(-0.326148325313847,-2.64212708522933,
13.8587068136939));
#439337=CARTESIAN_POINT('Ctrl Pts',(-0.326148325313847,-2.64212708522933,
13.8587068136939));
#439338=CARTESIAN_POINT('Ctrl Pts',(-0.327301870745918,-2.64202484368912,
13.8586446046466));
#439339=CARTESIAN_POINT('Ctrl Pts',(-0.328441839233545,-2.64198537378024,
13.858482427929));
#439340=CARTESIAN_POINT('Ctrl Pts',(-0.329568382475551,-2.64200420751158,
13.8582284286032));
#439341=CARTESIAN_POINT('Ctrl Pts',(-0.330724084796904,-2.64202352872909,
13.8579678548414));
#439342=CARTESIAN_POINT('Ctrl Pts',(-0.331868455352584,-2.64210578950569,
13.857615680862));
#439343=CARTESIAN_POINT('Ctrl Pts',(-0.332957072913103,-2.64223808203927,
13.8571944833187));
#439344=CARTESIAN_POINT('Ctrl Pts',(-0.335673829370046,-2.64256823158661,
13.8561433417727));
#439345=CARTESIAN_POINT('Ctrl Pts',(-0.338171014326103,-2.64322066342429,
13.8546163505474));
#439346=CARTESIAN_POINT('Ctrl Pts',(-0.34035655976158,-2.64401022532738,
13.8528973491086));
#439347=CARTESIAN_POINT('Ctrl Pts',(-0.340755826667932,-2.64415446663818,
13.8525833129072));
#439348=CARTESIAN_POINT('Ctrl Pts',(-0.341144796936879,-2.64430318880852,
13.8522628768812));
#439349=CARTESIAN_POINT('Ctrl Pts',(-0.341523058110627,-2.64445516393018,
13.851937733538));
#439350=CARTESIAN_POINT('Ctrl Pts',(-0.34383304661731,-2.64538325491252,
13.8499521282529));
#439351=CARTESIAN_POINT('Ctrl Pts',(-0.34597170175213,-2.646528679691,13.847639871647));
#439352=CARTESIAN_POINT('Ctrl Pts',(-0.347864555013669,-2.64776041635405,
13.8452109780794));
#439353=CARTESIAN_POINT('Ctrl Pts',(-0.348716188876148,-2.64831460017443,
13.8441181685877));
#439354=CARTESIAN_POINT('Ctrl Pts',(-0.34951864079009,-2.6488858268973,
13.8430021611332));
#439355=CARTESIAN_POINT('Ctrl Pts',(-0.350268262742234,-2.64946110341616,
13.8418824960098));
#439356=CARTESIAN_POINT('Ctrl Pts',(-0.352034766014743,-2.65081675722306,
13.8392439765549));
#439357=CARTESIAN_POINT('Ctrl Pts',(-0.35359464231439,-2.65225670586511,
13.8364981347964));
#439358=CARTESIAN_POINT('Ctrl Pts',(-0.354975228564488,-2.65375961259506,
13.8336931113419));
#439359=CARTESIAN_POINT('Ctrl Pts',(-0.35631983189675,-2.65522334830663,
13.8309611966328));
#439360=CARTESIAN_POINT('Ctrl Pts',(-0.357495300980898,-2.6567486516762,
13.8281701127186));
#439361=CARTESIAN_POINT('Ctrl Pts',(-0.358490259217353,-2.65833004640473,
13.8253580685121));
#439362=CARTESIAN_POINT('Ctrl Pts',(-0.358705967236808,-2.65867289448857,
13.8247484142933));
#439363=CARTESIAN_POINT('Ctrl Pts',(-0.358913017654098,-2.65901837386185,
13.8241378483365));
#439364=CARTESIAN_POINT('Ctrl Pts',(-0.359110979140358,-2.65936638433693,
13.8235269408515));
#439365=CARTESIAN_POINT('',(-0.324913457451728,-2.64226079469317,12.5969504640361));
#439366=CARTESIAN_POINT('Origin',(-0.329236065209537,-2.67639558472314,
12.584524458991));
#439367=CARTESIAN_POINT('Origin',(-0.329236065209537,-2.67639558472314,
12.584524458991));
#439368=CARTESIAN_POINT('Ctrl Pts',(-0.296124228020734,-2.66711467752318,
12.5893111709658));
#439369=CARTESIAN_POINT('Ctrl Pts',(-0.2991734647528,-2.65619859810282,
12.5770542771492));
#439370=CARTESIAN_POINT('Ctrl Pts',(-0.31547929129419,-2.65758557166315,
12.5737548217797));
#439371=CARTESIAN_POINT('Ctrl Pts',(-0.289456570641965,-2.69098447967037,
12.5663937883685));
#439372=CARTESIAN_POINT('Ctrl Pts',(-0.292509697098965,-2.68005447527472,
12.5540940315304));
#439373=CARTESIAN_POINT('Ctrl Pts',(-0.308865779929059,-2.6814489464175,
12.5508374392248));
#439374=CARTESIAN_POINT('Ctrl Pts',(-0.282795640847762,-2.71483019747978,
12.5434499600945));
#439375=CARTESIAN_POINT('Ctrl Pts',(-0.285858694106043,-2.70386465574756,
12.5311293540533));
#439376=CARTESIAN_POINT('Ctrl Pts',(-0.302257593095427,-2.70528869103514,
12.5278936106989));
#439377=CARTESIAN_POINT('Ctrl Pts',(-0.276140911657195,-2.73865371751063,
12.5204817579905));
#439378=CARTESIAN_POINT('Ctrl Pts',(-0.279219124935868,-2.72763390384074,
12.5081597038247));
#439379=CARTESIAN_POINT('Ctrl Pts',(-0.295654303598946,-2.72910663844256,
12.5049254088044));
#439380=CARTESIAN_POINT('Ctrl Pts',(-0.280925356007091,-2.72152570184806,
12.5369868989719));
#439381=CARTESIAN_POINT('Ctrl Pts',(-0.280674748363148,-2.7224228623574,
12.5342545179733));
#439382=CARTESIAN_POINT('Ctrl Pts',(-0.280555726584263,-2.72331263251285,
12.5314872231885));
#439383=CARTESIAN_POINT('Ctrl Pts',(-0.28063040273863,-2.72415230184187,
12.5287124745062));
#439384=CARTESIAN_POINT('Ctrl Pts',(-0.280697749401231,-2.72490955732024,
12.5262100684184));
#439385=CARTESIAN_POINT('Ctrl Pts',(-0.280923548754504,-2.72562521295656,
12.5237004536639));
#439386=CARTESIAN_POINT('Ctrl Pts',(-0.281374896467423,-2.72629161059571,
12.5212220730815));
#439387=CARTESIAN_POINT('Ctrl Pts',(-0.281720442186355,-2.72680179563647,
12.5193246583486));
#439388=CARTESIAN_POINT('Ctrl Pts',(-0.282202842096404,-2.72728885102334,
12.517417831369));
#439389=CARTESIAN_POINT('Ctrl Pts',(-0.282903321380209,-2.7276993305922,
12.5155812248348));
#439390=CARTESIAN_POINT('Ctrl Pts',(-0.283201729320206,-2.72787419709488,
12.5147988205793));
#439391=CARTESIAN_POINT('Ctrl Pts',(-0.283539877298099,-2.7280355830973,
12.5140295443047));
#439392=CARTESIAN_POINT('Ctrl Pts',(-0.283924191219537,-2.72818147882248,
12.5132817086137));
#439393=CARTESIAN_POINT('Ctrl Pts',(-0.284505798350819,-2.72840227226621,
12.5121499604604));
#439394=CARTESIAN_POINT('Ctrl Pts',(-0.285208235681259,-2.72858567050411,
12.5110494206568));
#439395=CARTESIAN_POINT('Ctrl Pts',(-0.286052005216699,-2.7287005838835,
12.5100666561695));
#439396=CARTESIAN_POINT('Ctrl Pts',(-0.286536495740919,-2.72876656688133,
12.509502355064));
#439397=CARTESIAN_POINT('Ctrl Pts',(-0.287073269844165,-2.72881008581394,
12.5089719619137));
#439398=CARTESIAN_POINT('Ctrl Pts',(-0.287652782419591,-2.72882395887686,
12.5085043804652));
#439399=CARTESIAN_POINT('Ctrl Pts',(-0.288500823586905,-2.72884426029734,
12.5078201359221));
#439400=CARTESIAN_POINT('Ctrl Pts',(-0.289465012034477,-2.72880045789742,
12.5072563000949));
#439401=CARTESIAN_POINT('Ctrl Pts',(-0.290479605800433,-2.72868706355689,
12.5068768744332));
#439402=CARTESIAN_POINT('Ctrl Pts',(-0.291211197750561,-2.72860529843127,
12.5066032824114));
#439403=CARTESIAN_POINT('Ctrl Pts',(-0.2919818570955,-2.72848597284837,
12.5064197834844));
#439404=CARTESIAN_POINT('Ctrl Pts',(-0.292748943732452,-2.72833830467749,
12.5063282718343));
#439405=CARTESIAN_POINT('Ctrl Pts',(-0.293868652738381,-2.72812275486491,
12.5061946931565));
#439406=CARTESIAN_POINT('Ctrl Pts',(-0.295004882629896,-2.72784325153112,
12.5062515701262));
#439407=CARTESIAN_POINT('Ctrl Pts',(-0.296090811003642,-2.72753215799887,
12.5064436508398));
#439408=CARTESIAN_POINT('',(-0.31547929129419,-2.65758557166315,12.5737548217797));
#439409=CARTESIAN_POINT('Origin',(-0.31731309413718,-2.6730334571862,12.5893111709658));
#439410=CARTESIAN_POINT('Ctrl Pts',(-0.296090811003642,-2.72753215799887,
12.5064436508398));
#439411=CARTESIAN_POINT('Ctrl Pts',(-0.298961272795007,-2.71717837430133,
12.5164271754438));
#439412=CARTESIAN_POINT('Ctrl Pts',(-0.301832671095516,-2.70682043054686,
12.5264061185523));
#439413=CARTESIAN_POINT('Ctrl Pts',(-0.304705039800327,-2.69645818047462,
12.536380305637));
#439414=CARTESIAN_POINT('Ctrl Pts',(-0.308294918102195,-2.68350746957508,
12.5488460165097));
#439415=CARTESIAN_POINT('Ctrl Pts',(-0.311886313205838,-2.67055002840516,
12.5613043021964));
#439416=CARTESIAN_POINT('Ctrl Pts',(-0.31547929129419,-2.65758557166315,
12.5737548217797));
#439417=CARTESIAN_POINT('Ctrl Pts',(-0.359110979140358,-2.65936638433693,
12.5893111709658));
#439418=CARTESIAN_POINT('Ctrl Pts',(-0.353507012517122,-2.64951477570456,
12.5770542771492));
#439419=CARTESIAN_POINT('Ctrl Pts',(-0.338023477934023,-2.65481230641886,
12.5737548217797));
#439420=CARTESIAN_POINT('Ctrl Pts',(-0.353882527021608,-2.6501749191677,
12.5928319619712));
#439421=CARTESIAN_POINT('Ctrl Pts',(-0.347284647692764,-2.64516478895648,
12.5821634970842));
#439422=CARTESIAN_POINT('Ctrl Pts',(-0.336127083743247,-2.651459411186,
12.5773203894503));
#439423=CARTESIAN_POINT('Ctrl Pts',(-0.34028227804391,-2.64039650789161,
12.5969440695591));
#439424=CARTESIAN_POINT('Ctrl Pts',(-0.336290393023035,-2.6408691563149,
12.5878292599214));
#439425=CARTESIAN_POINT('Ctrl Pts',(-0.331278483118768,-2.64797584705111,
12.5813877129824));
#439426=CARTESIAN_POINT('Ctrl Pts',(-0.309907671639785,-2.64407869899691,
12.596957478804));
#439427=CARTESIAN_POINT('Ctrl Pts',(-0.313870064984958,-2.64360962317464,
12.5878468778671));
#439428=CARTESIAN_POINT('Ctrl Pts',(-0.320407708303931,-2.64929967605414,
12.5814011370086));
#439429=CARTESIAN_POINT('Ctrl Pts',(-0.298973270177215,-2.65691528233498,
12.5928371701607));
#439430=CARTESIAN_POINT('Ctrl Pts',(-0.304161181208116,-2.65046387591163,
12.5821692192952));
#439431=CARTESIAN_POINT('Ctrl Pts',(-0.316509573340324,-2.65386108560742,
12.5773318885715));
#439432=CARTESIAN_POINT('Ctrl Pts',(-0.296124228020682,-2.66711467752316,
12.5893111709658));
#439433=CARTESIAN_POINT('Ctrl Pts',(-0.299173464752748,-2.6561985981028,
12.5770542771492));
#439434=CARTESIAN_POINT('Ctrl Pts',(-0.315479291294137,-2.65758557166314,
12.5737548217797));
#439435=CARTESIAN_POINT('',(-0.338023477934023,-2.65481230641886,12.5737548217797));
#439436=CARTESIAN_POINT('Origin',(-0.339988324540244,-2.67024407163915,
12.5893111709658));
#439437=CARTESIAN_POINT('Ctrl Pts',(-0.315479291294137,-2.65758557166314,
12.5737548217797));
#439438=CARTESIAN_POINT('Ctrl Pts',(-0.315717282877971,-2.65661208327746,
12.5746934679442));
#439439=CARTESIAN_POINT('Ctrl Pts',(-0.316158580278691,-2.65557835602022,
12.5756680099006));
#439440=CARTESIAN_POINT('Ctrl Pts',(-0.316749913775715,-2.65460069127028,
12.5765688348656));
#439441=CARTESIAN_POINT('Ctrl Pts',(-0.316906462772773,-2.65434186535084,
12.5768073183026));
#439442=CARTESIAN_POINT('Ctrl Pts',(-0.317073281567976,-2.65408689315674,
12.5770407398754));
#439443=CARTESIAN_POINT('Ctrl Pts',(-0.317248902279859,-2.65383763724717,
12.5772674179684));
#439444=CARTESIAN_POINT('Ctrl Pts',(-0.31796960219159,-2.6528147583959,
12.5781976435658));
#439445=CARTESIAN_POINT('Ctrl Pts',(-0.318888686636697,-2.65183654509322,
12.5790594849312));
#439446=CARTESIAN_POINT('Ctrl Pts',(-0.319979290249667,-2.65100211326074,
12.5797571720116));
#439447=CARTESIAN_POINT('Ctrl Pts',(-0.320689857718127,-2.65045845091839,
12.580211740231));
#439448=CARTESIAN_POINT('Ctrl Pts',(-0.32151693397986,-2.64996602646976,
12.5806009430798));
#439449=CARTESIAN_POINT('Ctrl Pts',(-0.322411359859084,-2.64957472733751,
12.5808812374708));
#439450=CARTESIAN_POINT('Ctrl Pts',(-0.323179968412034,-2.64923847157078,
12.5811221033394));
#439451=CARTESIAN_POINT('Ctrl Pts',(-0.324014092571948,-2.64897011241116,
12.581287365893));
#439452=CARTESIAN_POINT('Ctrl Pts',(-0.324869206662944,-2.64879273379116,
12.581359338449));
#439453=CARTESIAN_POINT('Ctrl Pts',(-0.32498804986416,-2.64876808182571,
12.5813693411482));
#439454=CARTESIAN_POINT('Ctrl Pts',(-0.325107306565449,-2.64874512784228,
12.5813775999465));
#439455=CARTESIAN_POINT('Ctrl Pts',(-0.325226866588446,-2.64872387318194,
12.5813841266931));
#439456=CARTESIAN_POINT('Ctrl Pts',(-0.325429714627947,-2.64868781207998,
12.5813952001081));
#439457=CARTESIAN_POINT('Ctrl Pts',(-0.325634900935537,-2.64865700047033,
12.5814007534795));
#439458=CARTESIAN_POINT('Ctrl Pts',(-0.325842365431365,-2.6486316467957,
12.5814005856065));
#439459=CARTESIAN_POINT('Ctrl Pts',(-0.326792056779908,-2.64851558758589,
12.5813998171494));
#439460=CARTESIAN_POINT('Ctrl Pts',(-0.327723829115703,-2.64852158049257,
12.58127954464));
#439461=CARTESIAN_POINT('Ctrl Pts',(-0.328632582749688,-2.64862000274537,
12.5810700125799));
#439462=CARTESIAN_POINT('Ctrl Pts',(-0.329730253669656,-2.64873888562049,
12.5808169217085));
#439463=CARTESIAN_POINT('Ctrl Pts',(-0.330792637743183,-2.64900927134455,
12.5804173076348));
#439464=CARTESIAN_POINT('Ctrl Pts',(-0.331733052660859,-2.64938222596681,
12.5799304713245));
#439465=CARTESIAN_POINT('Ctrl Pts',(-0.33289852300511,-2.64984443423661,
12.5793271277669));
#439466=CARTESIAN_POINT('Ctrl Pts',(-0.33396082769394,-2.65046291750759,
12.5785808224116));
#439467=CARTESIAN_POINT('Ctrl Pts',(-0.334891146747424,-2.651184195763,
12.5777485681082));
#439468=CARTESIAN_POINT('Ctrl Pts',(-0.336277424061175,-2.6522589793855,
12.576508418016));
#439469=CARTESIAN_POINT('Ctrl Pts',(-0.337363175010326,-2.65354753066006,
12.5750928681475));
#439470=CARTESIAN_POINT('Ctrl Pts',(-0.338023477934023,-2.65481230641886,
12.5737548217797));
#439471=CARTESIAN_POINT('Ctrl Pts',(-0.338023477934023,-2.65481230641886,
12.5737548217797));
#439472=CARTESIAN_POINT('Ctrl Pts',(-0.353507012517122,-2.64951477570456,
12.5770542771492));
#439473=CARTESIAN_POINT('Ctrl Pts',(-0.359110979140358,-2.65936638433693,
12.5893111709658));
#439474=CARTESIAN_POINT('Ctrl Pts',(-0.350221549893586,-2.67635811795242,
12.5508408821982));
#439475=CARTESIAN_POINT('Ctrl Pts',(-0.365752016580534,-2.67104113298767,
12.55409748406));
#439476=CARTESIAN_POINT('Ctrl Pts',(-0.371363132429934,-2.68090530974955,
12.5663972313419));
#439477=CARTESIAN_POINT('Ctrl Pts',(-0.362408732305296,-2.69788230083249,
12.52790050457));
#439478=CARTESIAN_POINT('Ctrl Pts',(-0.377973568546624,-2.69252626217299,
12.5311362602938));
#439479=CARTESIAN_POINT('Ctrl Pts',(-0.383602925310125,-2.70242250592573,
12.5434568539655));
#439480=CARTESIAN_POINT('Ctrl Pts',(-0.374585883477606,-2.71938652906053,
12.5049357605811));
#439481=CARTESIAN_POINT('Ctrl Pts',(-0.39017411317665,-2.71397446107877,
12.5081700652078));
#439482=CARTESIAN_POINT('Ctrl Pts',(-0.395831325850728,-2.72391967470371,
12.5204921097672));
#439483=CARTESIAN_POINT('Ctrl Pts',(-0.373786285379738,-2.71797447635903,
12.5064436508395));
#439484=CARTESIAN_POINT('Ctrl Pts',(-0.37500575514881,-2.71801620492121,
12.5062361689309));
#439485=CARTESIAN_POINT('Ctrl Pts',(-0.376275683314774,-2.7180075983115,
12.5061871075061));
#439486=CARTESIAN_POINT('Ctrl Pts',(-0.37750247807579,-2.71793019511092,
12.5063648335164));
#439487=CARTESIAN_POINT('Ctrl Pts',(-0.378059763928082,-2.71789503380278,
12.5064455676329));
#439488=CARTESIAN_POINT('Ctrl Pts',(-0.378615908149357,-2.71784496576091,
12.506574497099));
#439489=CARTESIAN_POINT('Ctrl Pts',(-0.379146970710706,-2.71778109103672,
12.5067492519495));
#439490=CARTESIAN_POINT('Ctrl Pts',(-0.380214161542032,-2.71765273229903,
12.5071004286051));
#439491=CARTESIAN_POINT('Ctrl Pts',(-0.381219206743642,-2.71746309708426,
12.5076537929612));
#439492=CARTESIAN_POINT('Ctrl Pts',(-0.382088426108788,-2.71723571295662,
12.5083435010503));
#439493=CARTESIAN_POINT('Ctrl Pts',(-0.382143148662405,-2.71722139776691,
12.5083869222963));
#439494=CARTESIAN_POINT('Ctrl Pts',(-0.3821973358236,-2.71720691985364,
12.5084308732336));
#439495=CARTESIAN_POINT('Ctrl Pts',(-0.38225097079332,-2.71719227983691,
12.5084753333615));
#439496=CARTESIAN_POINT('Ctrl Pts',(-0.382681194041496,-2.71707484757989,
12.508831962269));
#439497=CARTESIAN_POINT('Ctrl Pts',(-0.383084962371223,-2.71694584581703,
12.509227847131));
#439498=CARTESIAN_POINT('Ctrl Pts',(-0.383451121810638,-2.71681177767242,
12.5096423454524));
#439499=CARTESIAN_POINT('Ctrl Pts',(-0.384598503438387,-2.71639166744329,
12.5109411997424));
#439500=CARTESIAN_POINT('Ctrl Pts',(-0.385450492145566,-2.71590504918171,
12.5124831113042));
#439501=CARTESIAN_POINT('Ctrl Pts',(-0.386083085752253,-2.71540831604987,
12.5140723025008));
#439502=CARTESIAN_POINT('Ctrl Pts',(-0.38614236046606,-2.71536177161137,
12.5142212114565));
#439503=CARTESIAN_POINT('Ctrl Pts',(-0.386199737375547,-2.71531514652344,
12.5143705582413));
#439504=CARTESIAN_POINT('Ctrl Pts',(-0.386255294834225,-2.71526849332626,
12.5145201959299));
#439505=CARTESIAN_POINT('Ctrl Pts',(-0.386969013107346,-2.7146691635492,
12.5164425148273));
#439506=CARTESIAN_POINT('Ctrl Pts',(-0.387413823305344,-2.71405288303911,
12.518463520594));
#439507=CARTESIAN_POINT('Ctrl Pts',(-0.387679559144856,-2.71342789084365,
12.5205025929157));
#439508=CARTESIAN_POINT('Ctrl Pts',(-0.387833696464559,-2.71306537059791,
12.5216853356836));
#439509=CARTESIAN_POINT('Ctrl Pts',(-0.387927751503383,-2.71270076340624,
12.5228750347131));
#439510=CARTESIAN_POINT('Ctrl Pts',(-0.387978373607497,-2.71234153471706,
12.5240609649613));
#439511=CARTESIAN_POINT('Ctrl Pts',(-0.388102622846261,-2.71145982717144,
12.5269717671326));
#439512=CARTESIAN_POINT('Ctrl Pts',(-0.38795842160391,-2.71058425593512,
12.5299036066169));
#439513=CARTESIAN_POINT('Ctrl Pts',(-0.387632427250619,-2.7097146699372,
12.5328133004019));
#439514=CARTESIAN_POINT('Ctrl Pts',(-0.387475930978956,-2.70929721802372,
12.5342101228451));
#439515=CARTESIAN_POINT('Ctrl Pts',(-0.387277243946127,-2.70888185027142,
12.5356023438238));
#439516=CARTESIAN_POINT('Ctrl Pts',(-0.38704386168096,-2.70847157094225,
12.5369868989719));
#439517=CARTESIAN_POINT('Origin',(-6.69284171101566,-13.7831702063622,-1.23871760707945));
#439518=CARTESIAN_POINT('Ctrl Pts',(-0.28093656190616,-2.72148543785968,
12.5369868989719));
#439519=CARTESIAN_POINT('Ctrl Pts',(-0.276837914541471,-2.73626665545045,
12.5369868989719));
#439520=CARTESIAN_POINT('Ctrl Pts',(-0.261551242461182,-2.73753194608714,
12.5369868989719));
#439521=CARTESIAN_POINT('Ctrl Pts',(-0.279550994995317,-2.72648204980315,
12.5218025310016));
#439522=CARTESIAN_POINT('Ctrl Pts',(-0.273324196837474,-2.73652609522353,
12.5216901060418));
#439523=CARTESIAN_POINT('Ctrl Pts',(-0.261597842664173,-2.7375281054975,
12.5161920673678));
#439524=CARTESIAN_POINT('Ctrl Pts',(-0.283329500888561,-2.73117874698419,
12.5042015548894));
#439525=CARTESIAN_POINT('Ctrl Pts',(-0.278983334041869,-2.7359209172424,
12.4980677368513));
#439526=CARTESIAN_POINT('Ctrl Pts',(-0.272221399150479,-2.73660430311319,
12.4907278922777));
#439527=CARTESIAN_POINT('Ctrl Pts',(-0.296088652451907,-2.72751227373476,
12.506463626192));
#439528=CARTESIAN_POINT('Ctrl Pts',(-0.296794759692605,-2.73401679915181,
12.4999376786891));
#439529=CARTESIAN_POINT('Ctrl Pts',(-0.296786135619339,-2.73393735583142,
12.4906970594712));
#439530=CARTESIAN_POINT('Origin',(-0.259736489890645,-2.71560692218504,
12.5369868989719));
#439531=CARTESIAN_POINT('Origin',(-0.259736489890645,-2.71560692218504,
14.));
#439532=CARTESIAN_POINT('Origin',(-0.259736489890645,-2.71560692218504,
13.7435492065112));
#439533=CARTESIAN_POINT('Ctrl Pts',(-0.287586675305132,-2.69767848871726,
13.793642941384));
#439534=CARTESIAN_POINT('Ctrl Pts',(-0.284704006045186,-2.70809945013853,
13.8071662555867));
#439535=CARTESIAN_POINT('Ctrl Pts',(-0.267801281095337,-2.70602164531021,
13.8103758687955));
#439536=CARTESIAN_POINT('Ctrl Pts',(-0.283115007241042,-2.71368679562173,
13.7804579775006));
#439537=CARTESIAN_POINT('Ctrl Pts',(-0.279548280174751,-2.72654261647316,
13.7901904343351));
#439538=CARTESIAN_POINT('Ctrl Pts',(-0.263804867301074,-2.72717576357554,
13.7927914348263));
#439539=CARTESIAN_POINT('Ctrl Pts',(-0.280482367927284,-2.72311148834653,
13.7597120340895));
#439540=CARTESIAN_POINT('Ctrl Pts',(-0.276349138435289,-2.73798776153368,
13.7635825532445));
#439541=CARTESIAN_POINT('Ctrl Pts',(-0.261423068559663,-2.7396455776309,
13.7651073818884));
#439542=CARTESIAN_POINT('Ctrl Pts',(-0.280997898984724,-2.72126591770987,
13.7381884353898));
#439543=CARTESIAN_POINT('Ctrl Pts',(-0.276962281456728,-2.7357942246241,
13.7368803041982));
#439544=CARTESIAN_POINT('Ctrl Pts',(-0.261889010073193,-2.73720352477568,
13.7363986145813));
#439545=CARTESIAN_POINT('Origin',(-0.265312792372365,-2.69564410325325,
13.7902182540695));
#439546=CARTESIAN_POINT('Ctrl Pts',(-0.296125286266661,-2.66711088624712,
13.8235227101244));
#439547=CARTESIAN_POINT('Ctrl Pts',(-0.293036436368329,-2.67818525731844,
13.8358800583119));
#439548=CARTESIAN_POINT('Ctrl Pts',(-0.276534021492768,-2.67666988530749,
13.8390832900376));
#439549=CARTESIAN_POINT('Ctrl Pts',(-0.29291634471462,-2.67859869906812,
13.8124254819052));
#439550=CARTESIAN_POINT('Ctrl Pts',(-0.289821496045629,-2.68969457633634,
13.8247886449158));
#439551=CARTESIAN_POINT('Ctrl Pts',(-0.273299788249322,-2.68816031671179,
13.8279860620657));
#439552=CARTESIAN_POINT('Ctrl Pts',(-0.2897088413058,-2.69008136342514,
13.8013225099955));
#439553=CARTESIAN_POINT('Ctrl Pts',(-0.286609456068655,-2.70119351195657,
13.8136962257787));
#439554=CARTESIAN_POINT('Ctrl Pts',(-0.270067313214188,-2.69964550205236,
13.8168830918626));
#439555=CARTESIAN_POINT('Ctrl Pts',(-0.286502720084255,-2.70155907963701,
13.7902140179785));
#439556=CARTESIAN_POINT('Ctrl Pts',(-0.283400164913025,-2.71268260663856,
13.802602731458));
#439557=CARTESIAN_POINT('Ctrl Pts',(-0.266836529074552,-2.71112564795836,
13.8057746032558));
#439558=CARTESIAN_POINT('Origin',(-0.274935361904289,-2.66119589786016,
13.8235269408515));
#439559=CARTESIAN_POINT('Ctrl Pts',(-0.359110979140358,-2.65936638433693,
13.8235269408515));
#439560=CARTESIAN_POINT('Ctrl Pts',(-0.364949074200162,-2.66962958388014,
13.8362179249168));
#439561=CARTESIAN_POINT('Ctrl Pts',(-0.38096391197163,-2.66369763856593,
13.8391868794938));
#439562=CARTESIAN_POINT('Ctrl Pts',(-0.353769376277788,-2.64997600348538,
13.8400110824519));
#439563=CARTESIAN_POINT('Ctrl Pts',(-0.361423672080065,-2.65651309906617,
13.8494522556836));
#439564=CARTESIAN_POINT('Ctrl Pts',(-0.372075479704802,-2.64829927646268,
13.85569149686));
#439565=CARTESIAN_POINT('Ctrl Pts',(-0.340623534244925,-2.64035391622262,
13.8586819406588));
#439566=CARTESIAN_POINT('Ctrl Pts',(-0.344946490840129,-2.63983614222662,
13.868010383617));
#439567=CARTESIAN_POINT('Ctrl Pts',(-0.350166887882488,-2.63244423303395,
13.8744918421245));
#439568=CARTESIAN_POINT('Ctrl Pts',(-0.309561120473473,-2.64412193276161,
13.8587686893867));
#439569=CARTESIAN_POINT('Ctrl Pts',(-0.305276631455309,-2.64463504266512,
13.8680909899357));
#439570=CARTESIAN_POINT('Ctrl Pts',(-0.298457400739466,-2.63871942824649,
13.8745789365163));
#439571=CARTESIAN_POINT('Ctrl Pts',(-0.299035436609865,-2.6566927303164,
13.8400379222776));
#439572=CARTESIAN_POINT('Ctrl Pts',(-0.293189348780438,-2.66488379196912,
13.8494748685453));
#439573=CARTESIAN_POINT('Ctrl Pts',(-0.280869629396328,-2.65949996251772,
13.8557104837033));
#439574=CARTESIAN_POINT('Ctrl Pts',(-0.296124228014408,-2.66711467752126,
13.8235269408542));
#439575=CARTESIAN_POINT('Ctrl Pts',(-0.292947597049464,-2.67848682043731,
13.8362179249195));
#439576=CARTESIAN_POINT('Ctrl Pts',(-0.275972549792128,-2.67661311430574,
13.8391868794965));
#439577=CARTESIAN_POINT('Origin',(-0.378233633740471,-2.64848869703472,
13.8235269408515));
#439578=CARTESIAN_POINT('Ctrl Pts',(-0.376793638992285,-2.69045197915557,
13.7902140241682));
#439579=CARTESIAN_POINT('Ctrl Pts',(-0.38249961516522,-2.70049192095354,
13.8026027327198));
#439580=CARTESIAN_POINT('Ctrl Pts',(-0.398192068574959,-2.69496699215246,
13.8057746032556));
#439581=CARTESIAN_POINT('Ctrl Pts',(-0.370901345970342,-2.68009350118988,
13.8013225161807));
#439582=CARTESIAN_POINT('Ctrl Pts',(-0.376601489003658,-2.69012317203617,
13.8136962270464));
#439583=CARTESIAN_POINT('Ctrl Pts',(-0.392275259073093,-2.68461213428235,
13.8168830918628));
#439584=CARTESIAN_POINT('Ctrl Pts',(-0.365006512727856,-2.66973055759115,
13.8124254880875));
#439585=CARTESIAN_POINT('Ctrl Pts',(-0.370698310908615,-2.67974554179035,
13.8247886461868));
#439586=CARTESIAN_POINT('Ctrl Pts',(-0.386355587722492,-2.67425279703273,
13.8279860620656));
#439587=CARTESIAN_POINT('Ctrl Pts',(-0.359109036426738,-2.65936296757305,
13.8235227163065));
#439588=CARTESIAN_POINT('Ctrl Pts',(-0.364789802401239,-2.66935854065216,
13.8358800595847));
#439589=CARTESIAN_POINT('Ctrl Pts',(-0.380432939137479,-2.66388879624773,
13.8390832900376));
#439590=CARTESIAN_POINT('Origin',(-0.395918242455691,-2.67957771943477,
13.7902182540695));
#439591=CARTESIAN_POINT('Ctrl Pts',(-0.386910456038192,-2.70823699195356,
13.7382347919292));
#439592=CARTESIAN_POINT('Ctrl Pts',(-0.394350849890824,-2.72136552607016,
13.7369371795943));
#439593=CARTESIAN_POINT('Ctrl Pts',(-0.409326590721183,-2.71906966814732,
13.7364597369711));
#439594=CARTESIAN_POINT('Ctrl Pts',(-0.387845718556795,-2.70988115678884,
13.7595490285573));
#439595=CARTESIAN_POINT('Ctrl Pts',(-0.395464508545196,-2.72332243074375,
13.7633824266926));
#439596=CARTESIAN_POINT('Ctrl Pts',(-0.410357371837858,-2.72129850306384,
13.7648920890506));
#439597=CARTESIAN_POINT('Ctrl Pts',(-0.383075930942875,-2.70149600620757,
13.7803806590111));
#439598=CARTESIAN_POINT('Ctrl Pts',(-0.389661215122637,-2.71312488914086,
13.7901039518744));
#439599=CARTESIAN_POINT('Ctrl Pts',(-0.405098967304464,-2.70993721773393,
13.7926933640892));
#439600=CARTESIAN_POINT('Ctrl Pts',(-0.374784975386382,-2.68692074265818,
13.7936647693663));
#439601=CARTESIAN_POINT('Ctrl Pts',(-0.380106481733742,-2.69633641587572,
13.8072068914933));
#439602=CARTESIAN_POINT('Ctrl Pts',(-0.396015010918582,-2.69020755227619,
13.8104111085397));
#439603=CARTESIAN_POINT('Origin',(-0.406166516281074,-2.69759388364003,
13.7435492065112));
#439604=CARTESIAN_POINT('Origin',(-0.406166516281074,-2.69759388364003,
14.));
#439605=CARTESIAN_POINT('Origin',(-0.406166516281074,-2.69759388364003,
12.5369868989719));
#439606=CARTESIAN_POINT('Ctrl Pts',(-0.373783780809424,-2.71795626453539,
12.506462012331));
#439607=CARTESIAN_POINT('Ctrl Pts',(-0.374674612712626,-2.72443391893418,
12.4999388158272));
#439608=CARTESIAN_POINT('Ctrl Pts',(-0.374664073002957,-2.72435727978771,
12.4907030323752));
#439609=CARTESIAN_POINT('Ctrl Pts',(-0.38705082235667,-2.71841907306833,
12.5042014951932));
#439610=CARTESIAN_POINT('Ctrl Pts',(-0.392413855278163,-2.72196575814019,
12.4980716682127));
#439611=CARTESIAN_POINT('Ctrl Pts',(-0.399135291550663,-2.72099217729576,
12.4907355092744));
#439612=CARTESIAN_POINT('Ctrl Pts',(-0.389580147186854,-2.71294840426563,
12.5218047446509));
#439613=CARTESIAN_POINT('Ctrl Pts',(-0.398052217293834,-2.72117901171824,
12.5216906929434));
#439614=CARTESIAN_POINT('Ctrl Pts',(-0.409666500889807,-2.71931375814775,
12.5161988840775));
#439615=CARTESIAN_POINT('Ctrl Pts',(-0.387024896359692,-2.70843816262876,
12.5369868989719));
#439616=CARTESIAN_POINT('Ctrl Pts',(-0.394581332972405,-2.72177629582793,
12.5369868989719));
#439617=CARTESIAN_POINT('Ctrl Pts',(-0.409710957945607,-2.71930648213231,
12.5369868989719));
#439618=CARTESIAN_POINT('Origin',(-6.29013144927391E-32,-1.0265181555254E-30,
12.5));
#439619=CARTESIAN_POINT('Origin',(-0.141153018305391,-2.67978844069895,
12.5));
#439620=CARTESIAN_POINT('',(-0.141153018305391,-2.67978844069895,12.5893111709658));
#439621=CARTESIAN_POINT('',(-0.141153018305391,-2.67978844069895,13.8235269408515));
#439622=CARTESIAN_POINT('',(-0.141153018305391,-2.67978844069895,12.5));
#439623=CARTESIAN_POINT('',(-0.156244739001983,-2.71221547672782,13.7902182540695));
#439624=CARTESIAN_POINT('',(-0.141153018305391,-2.67978844069895,13.8235269408515));
#439625=CARTESIAN_POINT('',(-0.164990427904997,-2.73100702309002,13.7435492065112));
#439626=CARTESIAN_POINT('Origin',(-0.136216931677467,-2.66918322139446,
13.7445212918691));
#439627=CARTESIAN_POINT('',(-0.164990427904997,-2.73100702309002,12.5369868989719));
#439628=CARTESIAN_POINT('',(-0.164990427904997,-2.73100702309002,12.5));
#439629=CARTESIAN_POINT('Ctrl Pts',(-0.164990427904997,-2.73100702309002,
12.5369868989719));
#439630=CARTESIAN_POINT('Ctrl Pts',(-0.157050419890708,-2.71394661419927,
12.5544431401645));
#439631=CARTESIAN_POINT('Ctrl Pts',(-0.149104732971654,-2.69687400325064,
12.5718848856037));
#439632=CARTESIAN_POINT('Ctrl Pts',(-0.141153018305391,-2.67978844069895,
12.5893111709658));
#439633=CARTESIAN_POINT('Origin',(0.017582891275753,-2.94032602740454,12.5));
#439634=CARTESIAN_POINT('',(-0.0581609899471342,-2.73536807408357,13.7435492065112));
#439635=CARTESIAN_POINT('',(-0.0653458928110684,-2.71592620020509,13.7902182540695));
#439636=CARTESIAN_POINT('Origin',(-0.0842265757358376,-2.66483631588591,
13.7418732680455));
#439637=CARTESIAN_POINT('',(-0.0777442925777539,-2.68237694712209,13.8235269408515));
#439638=CARTESIAN_POINT('',(-0.0653458928110684,-2.71592620020509,13.7902182540695));
#439639=CARTESIAN_POINT('',(-0.0777442925777539,-2.68237694712209,12.5893111709658));
#439640=CARTESIAN_POINT('',(-0.0777442925777539,-2.68237694712209,12.5));
#439641=CARTESIAN_POINT('',(-0.0581609899471342,-2.73536807408357,12.5369868989719));
#439642=CARTESIAN_POINT('Ctrl Pts',(-0.0777442925777539,-2.68237694712209,
12.5893111709658));
#439643=CARTESIAN_POINT('Ctrl Pts',(-0.0712116685486591,-2.70005379743926,
12.5718848856037));
#439644=CARTESIAN_POINT('Ctrl Pts',(-0.0646839965340555,-2.71771724793141,
12.5544431401645));
#439645=CARTESIAN_POINT('Ctrl Pts',(-0.0581609899471342,-2.73536807408357,
12.5369868989719));
#439646=CARTESIAN_POINT('',(-0.0581609899471342,-2.73536807408357,12.5));
#439647=CARTESIAN_POINT('Origin',(-0.10998792761306,-2.69429284510378,12.5));
#439648=CARTESIAN_POINT('',(-0.109705207909741,-2.65991974163977,13.8587068136939));
#439649=CARTESIAN_POINT('Ctrl Pts',(-0.0777442925716052,-2.68237694711966,
13.8235269408542));
#439650=CARTESIAN_POINT('Ctrl Pts',(-0.0783517168072231,-2.68073329714929,
13.8262006681044));
#439651=CARTESIAN_POINT('Ctrl Pts',(-0.0791362936748559,-2.67911148730507,
13.8288634856214));
#439652=CARTESIAN_POINT('Ctrl Pts',(-0.0800846898927516,-2.67751134540702,
13.8314912288862));
#439653=CARTESIAN_POINT('Ctrl Pts',(-0.0810623885708681,-2.67586176415711,
13.8342001611531));
#439654=CARTESIAN_POINT('Ctrl Pts',(-0.0822148445255834,-2.6742331248582,
13.8368750301949));
#439655=CARTESIAN_POINT('Ctrl Pts',(-0.0835724893765199,-2.67262905828337,
13.8394886372969));
#439656=CARTESIAN_POINT('Ctrl Pts',(-0.0836773435815423,-2.67250517233087,
13.8396904925131));
#439657=CARTESIAN_POINT('Ctrl Pts',(-0.0837834408254324,-2.67238144413296,
13.8398919674349));
#439658=CARTESIAN_POINT('Ctrl Pts',(-0.0838908044602892,-2.67225788198516,
13.8400930404591));
#439659=CARTESIAN_POINT('Ctrl Pts',(-0.0855636021221009,-2.67033270059394,
13.8432258934518));
#439660=CARTESIAN_POINT('Ctrl Pts',(-0.0875344402538826,-2.66845691437443,
13.8462331177034));
#439661=CARTESIAN_POINT('Ctrl Pts',(-0.0898055468410686,-2.66676157757213,
13.8489036603661));
#439662=CARTESIAN_POINT('Ctrl Pts',(-0.0905486793465914,-2.66620684364079,
13.8497774930041));
#439663=CARTESIAN_POINT('Ctrl Pts',(-0.0913238751608761,-2.66567166476784,
13.85061494757));
#439664=CARTESIAN_POINT('Ctrl Pts',(-0.0921309564506031,-2.66516129870573,
13.8514076489583));
#439665=CARTESIAN_POINT('Ctrl Pts',(-0.0938380497769036,-2.66408180087857,
13.8530843267192));
#439666=CARTESIAN_POINT('Ctrl Pts',(-0.0958570558753725,-2.66300977640063,
13.8546805203176));
#439667=CARTESIAN_POINT('Ctrl Pts',(-0.0981347799227737,-2.66212795669042,
13.8559412814273));
#439668=CARTESIAN_POINT('Ctrl Pts',(-0.0984396132686843,-2.6620099406151,
13.8561100121513));
#439669=CARTESIAN_POINT('Ctrl Pts',(-0.0987490129978316,-2.66189529472272,
13.8562727473908));
#439670=CARTESIAN_POINT('Ctrl Pts',(-0.0990627899542671,-2.66178441284256,
13.8564289040185));
#439671=CARTESIAN_POINT('Ctrl Pts',(-0.100485764871901,-2.66128156478103,
13.8571370725437));
#439672=CARTESIAN_POINT('Ctrl Pts',(-0.102024532775858,-2.66084943554403,
13.8577210840554));
#439673=CARTESIAN_POINT('Ctrl Pts',(-0.10362721628845,-2.66053307709753,
13.8581177131616));
#439674=CARTESIAN_POINT('Ctrl Pts',(-0.10407858712828,-2.66044397967027,
13.8582294175695));
#439675=CARTESIAN_POINT('Ctrl Pts',(-0.104534959754643,-2.66036390081054,
13.8583265086086));
#439676=CARTESIAN_POINT('Ctrl Pts',(-0.104995031868896,-2.66029343139185,
13.8584082369006));
#439677=CARTESIAN_POINT('Ctrl Pts',(-0.105656032123871,-2.66019218573432,
13.8585256585398));
#439678=CARTESIAN_POINT('Ctrl Pts',(-0.106332935601478,-2.66010983676469,
13.8586122832068));
#439679=CARTESIAN_POINT('Ctrl Pts',(-0.107008253677771,-2.66004930757789,
13.8586682984299));
#439680=CARTESIAN_POINT('Ctrl Pts',(-0.107548441196678,-2.66000089022851,
13.8587131050557));
#439681=CARTESIAN_POINT('Ctrl Pts',(-0.108093559752444,-2.65996566576368,
13.8587357943552));
#439682=CARTESIAN_POINT('Ctrl Pts',(-0.108643706777496,-2.65994413538968,
13.8587355499465));
#439683=CARTESIAN_POINT('Ctrl Pts',(-0.108999279915972,-2.65993021979565,
13.8587353919793));
#439684=CARTESIAN_POINT('Ctrl Pts',(-0.109353106987064,-2.6599221365345,
13.8587257282814));
#439685=CARTESIAN_POINT('Ctrl Pts',(-0.109705207909741,-2.65991974163977,
13.8587068136939));
#439686=CARTESIAN_POINT('Ctrl Pts',(-0.109705207909741,-2.65991974163977,
13.8587068136939));
#439687=CARTESIAN_POINT('Ctrl Pts',(-0.110863248649113,-2.65991186496157,
13.8586446046466));
#439688=CARTESIAN_POINT('Ctrl Pts',(-0.11200264114951,-2.65996544440026,
13.858482427929));
#439689=CARTESIAN_POINT('Ctrl Pts',(-0.113123900787746,-2.66007603919643,
13.8582284286032));
#439690=CARTESIAN_POINT('Ctrl Pts',(-0.114274182746367,-2.6601894965924,
13.8579678548414));
#439691=CARTESIAN_POINT('Ctrl Pts',(-0.115408040486462,-2.66036476047715,
13.857615680862));
#439692=CARTESIAN_POINT('Ctrl Pts',(-0.116482252692222,-2.66058534525566,
13.8571944833187));
#439693=CARTESIAN_POINT('Ctrl Pts',(-0.119163059113111,-2.66113583712999,
13.8561433417727));
#439694=CARTESIAN_POINT('Ctrl Pts',(-0.121598755640584,-2.66198964181121,
13.8546163505474));
#439695=CARTESIAN_POINT('Ctrl Pts',(-0.123712672228886,-2.66295471875481,
13.8528973491086));
#439696=CARTESIAN_POINT('Ctrl Pts',(-0.124098853601637,-2.66313102407402,
13.8525833129072));
#439697=CARTESIAN_POINT('Ctrl Pts',(-0.124474407366545,-2.66331095607156,
13.8522628768812));
#439698=CARTESIAN_POINT('Ctrl Pts',(-0.124839022524153,-2.6634932573058,
13.851937733538));
#439699=CARTESIAN_POINT('Ctrl Pts',(-0.127065676703604,-2.66460654565014,
13.8499521282529));
#439700=CARTESIAN_POINT('Ctrl Pts',(-0.12910385288684,-2.66592247936995,
13.847639871647));
#439701=CARTESIAN_POINT('Ctrl Pts',(-0.130890009862378,-2.66730440264407,
13.8452109780794));
#439702=CARTESIAN_POINT('Ctrl Pts',(-0.131693638857281,-2.66792615852948,
13.8441181685877));
#439703=CARTESIAN_POINT('Ctrl Pts',(-0.132446860397751,-2.66856089182315,
13.8430021611332));
#439704=CARTESIAN_POINT('Ctrl Pts',(-0.133147097667796,-2.66919535530509,
13.8418824960098));
#439705=CARTESIAN_POINT('Ctrl Pts',(-0.134797224675853,-2.67069048470191,
13.8392439765549));
#439706=CARTESIAN_POINT('Ctrl Pts',(-0.136234541433634,-2.67225278643325,
13.8364981347964));
#439707=CARTESIAN_POINT('Ctrl Pts',(-0.137488033046078,-2.67386322296115,
13.8336931113419));
#439708=CARTESIAN_POINT('Ctrl Pts',(-0.138708854272521,-2.67543168586716,
13.8309611966328));
#439709=CARTESIAN_POINT('Ctrl Pts',(-0.139756085695415,-2.67704772555847,
13.8281701127186));
#439710=CARTESIAN_POINT('Ctrl Pts',(-0.140618834939088,-2.67870495665951,
13.8253580685121));
#439711=CARTESIAN_POINT('Ctrl Pts',(-0.140805879906225,-2.67906424615075,
13.8247484142933));
#439712=CARTESIAN_POINT('Ctrl Pts',(-0.140984081604137,-2.6794254525011,
13.8241378483365));
#439713=CARTESIAN_POINT('Ctrl Pts',(-0.141153018305391,-2.67978844069895,
13.8235269408515));
#439714=CARTESIAN_POINT('',(-0.108463550405648,-2.65995235300169,12.5969504640361));
#439715=CARTESIAN_POINT('Origin',(-0.10998947276331,-2.69432589499518,12.584524458991));
#439716=CARTESIAN_POINT('Origin',(-0.10998947276331,-2.69432589499518,12.584524458991));
#439717=CARTESIAN_POINT('Ctrl Pts',(-0.0777442925777539,-2.68237694712209,
12.5893111709658));
#439718=CARTESIAN_POINT('Ctrl Pts',(-0.0816731450388344,-2.67174573115689,
12.5770542771492));
#439719=CARTESIAN_POINT('Ctrl Pts',(-0.0978116640663424,-2.67445716591615,
12.5737548217797));
#439720=CARTESIAN_POINT('Ctrl Pts',(-0.0691532108074482,-2.70562384849586,
12.5663937883685));
#439721=CARTESIAN_POINT('Ctrl Pts',(-0.0730870750654656,-2.69497907093825,
12.5540940315304));
#439722=CARTESIAN_POINT('Ctrl Pts',(-0.0892750720354502,-2.69770207468649,
12.5508374392248));
#439723=CARTESIAN_POINT('Ctrl Pts',(-0.0605707973333296,-2.72884729403113,
12.5434499600944));
#439724=CARTESIAN_POINT('Ctrl Pts',(-0.0645174519850021,-2.71816790651098,
12.5311293540532));
#439725=CARTESIAN_POINT('Ctrl Pts',(-0.08074571289465,-2.72092386594619,
12.5278936106989));
#439726=CARTESIAN_POINT('Ctrl Pts',(-0.0519963731558851,-2.75204912105586,
12.5204817579905));
#439727=CARTESIAN_POINT('Ctrl Pts',(-0.0559625610508614,-2.74131687786583,
12.5081597038247));
#439728=CARTESIAN_POINT('Ctrl Pts',(-0.0722230114704962,-2.74412433170255,
12.5049254088044));
#439729=CARTESIAN_POINT('Ctrl Pts',(-0.0581609899471349,-2.73536807408356,
12.5369868989719));
#439730=CARTESIAN_POINT('Ctrl Pts',(-0.0578380892691153,-2.73624182251581,
12.5342545179733));
#439731=CARTESIAN_POINT('Ctrl Pts',(-0.0576469389974919,-2.73711893065454,
12.5314872231885));
#439732=CARTESIAN_POINT('Ctrl Pts',(-0.0576529258276875,-2.73796189285297,
12.5287124745063));
#439733=CARTESIAN_POINT('Ctrl Pts',(-0.0576583250483176,-2.73872211800443,
12.5262100684184));
#439734=CARTESIAN_POINT('Ctrl Pts',(-0.0578250404946854,-2.73945379709917,
12.5237004536639));
#439735=CARTESIAN_POINT('Ctrl Pts',(-0.0582205687912007,-2.74015476638387,
12.5212220730815));
#439736=CARTESIAN_POINT('Ctrl Pts',(-0.0585233799181101,-2.74069141900998,
12.5193246583486));
#439737=CARTESIAN_POINT('Ctrl Pts',(-0.0589644751466254,-2.74121617383129,
12.517417831369));
#439738=CARTESIAN_POINT('Ctrl Pts',(-0.0596291657478373,-2.74168238312781,
12.5155812248347));
#439739=CARTESIAN_POINT('Ctrl Pts',(-0.0599123275166779,-2.74188099079401,
12.5147988205793));
#439740=CARTESIAN_POINT('Ctrl Pts',(-0.0602361958776334,-2.74206940199723,
12.5140295443047));
#439741=CARTESIAN_POINT('Ctrl Pts',(-0.060607339170164,-2.74224613741881,
12.5132817086137));
#439742=CARTESIAN_POINT('Ctrl Pts',(-0.0611690143362852,-2.74251360257115,
12.5121499604604));
#439743=CARTESIAN_POINT('Ctrl Pts',(-0.0618541657054794,-2.74275364573008,
12.5110494206568));
#439744=CARTESIAN_POINT('Ctrl Pts',(-0.0626857611601713,-2.742936951795,
12.5100666561695));
#439745=CARTESIAN_POINT('Ctrl Pts',(-0.0631632613552607,-2.74304220571536,
12.5095023550641));
#439746=CARTESIAN_POINT('Ctrl Pts',(-0.0636947021899745,-2.74312933191489,
12.5089719619137));
#439747=CARTESIAN_POINT('Ctrl Pts',(-0.0642711557016938,-2.74319039447116,
12.5085043804652));
#439748=CARTESIAN_POINT('Ctrl Pts',(-0.0651147203277434,-2.74327975156831,
12.5078201359221));
#439749=CARTESIAN_POINT('Ctrl Pts',(-0.0660792708199977,-2.74331468522683,
12.5072563000949));
#439750=CARTESIAN_POINT('Ctrl Pts',(-0.0670997313003516,-2.74328436700756,
12.5068768744332));
#439751=CARTESIAN_POINT('Ctrl Pts',(-0.0678355535554259,-2.74326250548436,
12.5066032824114));
#439752=CARTESIAN_POINT('Ctrl Pts',(-0.0686133747377393,-2.74320639283856,
12.5064197834844));
#439753=CARTESIAN_POINT('Ctrl Pts',(-0.0693899452839983,-2.74312174070353,
12.5063282718343));
#439754=CARTESIAN_POINT('Ctrl Pts',(-0.0705234978613715,-2.74299817479403,
12.5061946931565));
#439755=CARTESIAN_POINT('Ctrl Pts',(-0.0716787291581415,-2.74281221476893,
12.5062515701262));
#439756=CARTESIAN_POINT('Ctrl Pts',(-0.072786401205737,-2.74259066961847,
12.5064436508398));
#439757=CARTESIAN_POINT('',(-0.0978116640663425,-2.67445716591615,12.5737548217797));
#439758=CARTESIAN_POINT('Origin',(-0.0983802190003496,-2.69000312183037,
12.5893111709658));
#439759=CARTESIAN_POINT('Ctrl Pts',(-0.0727864012057365,-2.74259066961847,
12.5064436508398));
#439760=CARTESIAN_POINT('Ctrl Pts',(-0.0764912412634739,-2.73250530656612,
12.5164271754438));
#439761=CARTESIAN_POINT('Ctrl Pts',(-0.0801973537974575,-2.72241587363327,
12.5264061185523));
#439762=CARTESIAN_POINT('Ctrl Pts',(-0.0839047845116802,-2.71232222780853,
12.536380305637));
#439763=CARTESIAN_POINT('Ctrl Pts',(-0.0885383209564884,-2.69970721773956,
12.5488460165097));
#439764=CARTESIAN_POINT('Ctrl Pts',(-0.0931739177355619,-2.68708562342805,
12.5613043021964));
#439765=CARTESIAN_POINT('Ctrl Pts',(-0.0978116640663423,-2.67445716591615,
12.5737548217797));
#439766=CARTESIAN_POINT('Ctrl Pts',(-0.141153018305391,-2.67978844069895,
12.5893111709658));
#439767=CARTESIAN_POINT('Ctrl Pts',(-0.136370695980209,-2.66951283717712,
12.5770542771492));
#439768=CARTESIAN_POINT('Ctrl Pts',(-0.120506883648043,-2.67353068898434,
12.5737548217797));
#439769=CARTESIAN_POINT('Ctrl Pts',(-0.136691153170441,-2.67020139198557,
12.5928319619712));
#439770=CARTESIAN_POINT('Ctrl Pts',(-0.130523599864772,-2.6646701441523,
12.5821634970842));
#439771=CARTESIAN_POINT('Ctrl Pts',(-0.118890091640733,-2.67003437650195,
12.5773203894503));
#439772=CARTESIAN_POINT('Ctrl Pts',(-0.123933189196619,-2.65934697101611,
12.5969440695591));
#439773=CARTESIAN_POINT('Ctrl Pts',(-0.119916061609491,-2.6594926710527,
12.5878292599214));
#439774=CARTESIAN_POINT('Ctrl Pts',(-0.114341567151678,-2.66616719767624,
12.5813877129824));
#439775=CARTESIAN_POINT('Ctrl Pts',(-0.0933595190306978,-2.66054109752823,
12.596957478804));
#439776=CARTESIAN_POINT('Ctrl Pts',(-0.0973469618730906,-2.66039655435977,
12.5878468778671));
#439777=CARTESIAN_POINT('Ctrl Pts',(-0.103399059589684,-2.66660055268072,
12.5814011370086));
#439778=CARTESIAN_POINT('Ctrl Pts',(-0.0814152001758918,-2.67244371296496,
12.5928371701607));
#439779=CARTESIAN_POINT('Ctrl Pts',(-0.0871116983762444,-2.66643663597552,
12.5821692192952));
#439780=CARTESIAN_POINT('Ctrl Pts',(-0.099142098123944,-2.67082905033195,
12.5773318885715));
#439781=CARTESIAN_POINT('Ctrl Pts',(-0.0777442925777029,-2.68237694712207,
12.5893111709658));
#439782=CARTESIAN_POINT('Ctrl Pts',(-0.0816731450387836,-2.67174573115687,
12.5770542771492));
#439783=CARTESIAN_POINT('Ctrl Pts',(-0.0978116640662907,-2.67445716591612,
12.5737548217797));
#439784=CARTESIAN_POINT('',(-0.120506883648043,-2.67353068898434,12.5737548217797));
#439785=CARTESIAN_POINT('Origin',(-0.121207360262299,-2.68907125951804,
12.5893111709658));
#439786=CARTESIAN_POINT('Ctrl Pts',(-0.0978116640662907,-2.67445716591612,
12.5737548217797));
#439787=CARTESIAN_POINT('Ctrl Pts',(-0.09812821209362,-2.67350631525623,
12.5746934679442));
#439788=CARTESIAN_POINT('Ctrl Pts',(-0.0986522994817637,-2.67251199747613,
12.5756680099006));
#439789=CARTESIAN_POINT('Ctrl Pts',(-0.0993213541186758,-2.67158578499467,
12.5765688348656));
#439790=CARTESIAN_POINT('Ctrl Pts',(-0.0994984789271169,-2.67134058049372,
12.5768073183026));
#439791=CARTESIAN_POINT('Ctrl Pts',(-0.0996855252474055,-2.67110005397904,
12.5770407398754));
#439792=CARTESIAN_POINT('Ctrl Pts',(-0.0998808782664673,-2.67086594216634,
12.5772674179684));
#439793=CARTESIAN_POINT('Ctrl Pts',(-0.100682554231018,-2.66990521059353,
12.5781976435658));
#439794=CARTESIAN_POINT('Ctrl Pts',(-0.10167831396391,-2.66900516612956,
12.5790594849312));
#439795=CARTESIAN_POINT('Ctrl Pts',(-0.10283330262416,-2.66826240511929,
12.5797571720116));
#439796=CARTESIAN_POINT('Ctrl Pts',(-0.103585819266005,-2.6677784696138,
12.580211740231));
#439797=CARTESIAN_POINT('Ctrl Pts',(-0.104450280663714,-2.66735509806044,
12.5806009430798));
#439798=CARTESIAN_POINT('Ctrl Pts',(-0.105373624926531,-2.66703800495638,
12.5808812374708));
#439799=CARTESIAN_POINT('Ctrl Pts',(-0.106167083964563,-2.66676551678545,
12.5811221033394));
#439800=CARTESIAN_POINT('Ctrl Pts',(-0.107020306407977,-2.66656603943146,
12.581287365893));
#439801=CARTESIAN_POINT('Ctrl Pts',(-0.10788703318161,-2.66645895076109,
12.581359338449));
#439802=CARTESIAN_POINT('Ctrl Pts',(-0.108007490305921,-2.6664440676472,
12.5813693411482));
#439803=CARTESIAN_POINT('Ctrl Pts',(-0.108128221153119,-2.66643091056954,
12.5813775999465));
#439804=CARTESIAN_POINT('Ctrl Pts',(-0.108249115802138,-2.66641947188415,
12.5813841266931));
#439805=CARTESIAN_POINT('Ctrl Pts',(-0.108454228196106,-2.66640006477089,
12.5813952001081));
#439806=CARTESIAN_POINT('Ctrl Pts',(-0.108661243195412,-2.66638608027326,
12.5814007534795));
#439807=CARTESIAN_POINT('Ctrl Pts',(-0.1088700839301,-2.66637772124331,
12.5814005856065));
#439808=CARTESIAN_POINT('Ctrl Pts',(-0.109826075162065,-2.66633945687235,
12.5813998171494));
#439809=CARTESIAN_POINT('Ctrl Pts',(-0.110754258624749,-2.66642137793365,
12.58127954464));
#439810=CARTESIAN_POINT('Ctrl Pts',(-0.111651966128673,-2.66659354455215,
12.5810700125799));
#439811=CARTESIAN_POINT('Ctrl Pts',(-0.112736294581228,-2.66680150222457,
12.5808169217085));
#439812=CARTESIAN_POINT('Ctrl Pts',(-0.113773104712742,-2.66715758242712,
12.5804173076348));
#439813=CARTESIAN_POINT('Ctrl Pts',(-0.114679991213303,-2.66760594861982,
12.5799304713245));
#439814=CARTESIAN_POINT('Ctrl Pts',(-0.115803909286207,-2.66816161558249,
12.5793271277669));
#439815=CARTESIAN_POINT('Ctrl Pts',(-0.116812267115515,-2.6688646285955,
12.5785808224116));
#439816=CARTESIAN_POINT('Ctrl Pts',(-0.117680699735257,-2.66965933649654,
12.5777485681082));
#439817=CARTESIAN_POINT('Ctrl Pts',(-0.118974759482569,-2.67084353833583,
12.576508418016));
#439818=CARTESIAN_POINT('Ctrl Pts',(-0.119951868793801,-2.67221630084431,
12.5750928681475));
#439819=CARTESIAN_POINT('Ctrl Pts',(-0.120506883648043,-2.67353068898434,
12.5737548217797));
#439820=CARTESIAN_POINT('Ctrl Pts',(-0.120506883648043,-2.67353068898434,
12.5737548217797));
#439821=CARTESIAN_POINT('Ctrl Pts',(-0.13637069598021,-2.66951283717712,
12.5770542771492));
#439822=CARTESIAN_POINT('Ctrl Pts',(-0.141153018305391,-2.67978844069895,
12.5893111709658));
#439823=CARTESIAN_POINT('Ctrl Pts',(-0.13090818386789,-2.69599906471351,
12.5508408821982));
#439824=CARTESIAN_POINT('Ctrl Pts',(-0.146820357843191,-2.69196564879042,
12.55409748406));
#439825=CARTESIAN_POINT('Ctrl Pts',(-0.151608781186871,-2.70225436135064,
12.5663972313419));
#439826=CARTESIAN_POINT('Ctrl Pts',(-0.141300393710007,-2.7184449961575,
12.52790050457));
#439827=CARTESIAN_POINT('Ctrl Pts',(-0.157250006116537,-2.71437545792533,
12.5311362602938));
#439828=CARTESIAN_POINT('Ctrl Pts',(-0.162053995921704,-2.72469761758001,
12.5434568539655));
#439829=CARTESIAN_POINT('Ctrl Pts',(-0.151684232180235,-2.74087022170778,
12.5049357605811));
#439830=CARTESIAN_POINT('Ctrl Pts',(-0.167661727114596,-2.7367467473703,
12.5081700652078));
#439831=CARTESIAN_POINT('Ctrl Pts',(-0.172489488642897,-2.74711998446926,
12.5204921097672));
#439832=CARTESIAN_POINT('Ctrl Pts',(-0.151002390083106,-2.73939769282708,
12.5064436508395));
#439833=CARTESIAN_POINT('Ctrl Pts',(-0.152214400901913,-2.7395386806481,
12.5062361689309));
#439834=CARTESIAN_POINT('Ctrl Pts',(-0.153480805005259,-2.73963361361113,
12.5061871075061));
#439835=CARTESIAN_POINT('Ctrl Pts',(-0.154709826787334,-2.73965646312534,
12.5063648335164));
#439836=CARTESIAN_POINT('Ctrl Pts',(-0.15526812428996,-2.73966684278411,
12.5064455676329));
#439837=CARTESIAN_POINT('Ctrl Pts',(-0.15582649899744,-2.73966227225654,
12.506574497099));
#439838=CARTESIAN_POINT('Ctrl Pts',(-0.156361000874931,-2.73964189659912,
12.5067492519495));
#439839=CARTESIAN_POINT('Ctrl Pts',(-0.157435103145554,-2.73960095092461,
12.5071004286051));
#439840=CARTESIAN_POINT('Ctrl Pts',(-0.158452261172662,-2.73949386721969,
12.5076537929612));
#439841=CARTESIAN_POINT('Ctrl Pts',(-0.159337122199412,-2.73933808914168,
12.5083435010503));
#439842=CARTESIAN_POINT('Ctrl Pts',(-0.159392829489099,-2.73932828198072,
12.5083869222963));
#439843=CARTESIAN_POINT('Ctrl Pts',(-0.15944801643132,-2.73931826899819,
12.5084308732336));
#439844=CARTESIAN_POINT('Ctrl Pts',(-0.159502666232373,-2.73930804944287,
12.5084753333615));
#439845=CARTESIAN_POINT('Ctrl Pts',(-0.159941029767316,-2.73922607512072,
12.508831962269));
#439846=CARTESIAN_POINT('Ctrl Pts',(-0.160353969432502,-2.73913041346787,
12.509227847131));
#439847=CARTESIAN_POINT('Ctrl Pts',(-0.160729838305002,-2.73902663681752,
12.5096423454524));
#439848=CARTESIAN_POINT('Ctrl Pts',(-0.161907644998823,-2.73870144672494,
12.5109411997424));
#439849=CARTESIAN_POINT('Ctrl Pts',(-0.162796462689724,-2.7382858926346,
12.5124831113042));
#439850=CARTESIAN_POINT('Ctrl Pts',(-0.163467439755059,-2.73784237459294,
12.5140723025007));
#439851=CARTESIAN_POINT('Ctrl Pts',(-0.163530311040982,-2.73780081646667,
12.5142212114565));
#439852=CARTESIAN_POINT('Ctrl Pts',(-0.16359129741105,-2.73775902327066,
12.5143705582413));
#439853=CARTESIAN_POINT('Ctrl Pts',(-0.163650472675545,-2.7377170537568,
12.5145201959299));
#439854=CARTESIAN_POINT('Ctrl Pts',(-0.16441066705073,-2.73717789286522,
12.5164425148273));
#439855=CARTESIAN_POINT('Ctrl Pts',(-0.164904229762332,-2.73659991913824,
12.5184635205941));
#439856=CARTESIAN_POINT('Ctrl Pts',(-0.165220024053834,-2.73599866649064,
12.5205025929158));
#439857=CARTESIAN_POINT('Ctrl Pts',(-0.165403197259821,-2.73564991612361,
12.5216853356836));
#439858=CARTESIAN_POINT('Ctrl Pts',(-0.16552665820923,-2.73529418849112,
12.5228750347131));
#439859=CARTESIAN_POINT('Ctrl Pts',(-0.165606392345552,-2.73494028127722,
12.5240609649613));
#439860=CARTESIAN_POINT('Ctrl Pts',(-0.165802095505566,-2.73407163500715,
12.5269717671326));
#439861=CARTESIAN_POINT('Ctrl Pts',(-0.165729741265119,-2.73318722342193,
12.5299036066169));
#439862=CARTESIAN_POINT('Ctrl Pts',(-0.165475710962818,-2.73229395933351,
12.5328133004019));
#439863=CARTESIAN_POINT('Ctrl Pts',(-0.165353761625971,-2.73186514055786,
12.5342101228451));
#439864=CARTESIAN_POINT('Ctrl Pts',(-0.165189592035753,-2.73143496006979,
12.5356023438238));
#439865=CARTESIAN_POINT('Ctrl Pts',(-0.164990427904997,-2.73100702309002,
12.5369868989719));
#439866=CARTESIAN_POINT('Origin',(-5.54802939368013,-14.2847916318076,-1.24104469436926));
#439867=CARTESIAN_POINT('Ctrl Pts',(-0.0581754404483332,-2.73532885745512,
12.5369868989719));
#439868=CARTESIAN_POINT('Ctrl Pts',(-0.0528856245388476,-2.74972681395348,
12.5369868989719));
#439869=CARTESIAN_POINT('Ctrl Pts',(-0.0375466846655909,-2.74974188875088,
12.5369868989719));
#439870=CARTESIAN_POINT('Ctrl Pts',(-0.0563872136373922,-2.74019590701836,
12.5218025310015));
#439871=CARTESIAN_POINT('Ctrl Pts',(-0.049362451690614,-2.74969898984949,
12.5216901060417));
#439872=CARTESIAN_POINT('Ctrl Pts',(-0.0375934428539549,-2.74974185928964,
12.5161920673678));
#439873=CARTESIAN_POINT('Ctrl Pts',(-0.0597703224417318,-2.74518495963511,
12.5042015548895));
#439874=CARTESIAN_POINT('Ctrl Pts',(-0.0550520862064945,-2.74955709776713,
12.4980677368514));
#439875=CARTESIAN_POINT('Ctrl Pts',(-0.0482569488029278,-2.74968704925948,
12.4907278922777));
#439876=CARTESIAN_POINT('Ctrl Pts',(-0.0727858705885265,-2.74257067557562,
12.506463626192));
#439877=CARTESIAN_POINT('Ctrl Pts',(-0.0729594491090722,-2.74911111201621,
12.4999376786891));
#439878=CARTESIAN_POINT('Ctrl Pts',(-0.0729573290998271,-2.74903123009488,
12.4906970594712));
#439879=CARTESIAN_POINT('Origin',(-0.0375250635245384,-2.72774189937528,
12.5369868989719));
#439880=CARTESIAN_POINT('Origin',(-0.0375250635245384,-2.72774189937529,
14.));
#439881=CARTESIAN_POINT('Origin',(-0.0375250635245385,-2.72774189937529,
13.7435492065112));
#439882=CARTESIAN_POINT('Ctrl Pts',(-0.0667439135116158,-2.71214316995067,
13.793642941384));
#439883=CARTESIAN_POINT('Ctrl Pts',(-0.0630214309965092,-2.7222944921764,
13.8071662555867));
#439884=CARTESIAN_POINT('Ctrl Pts',(-0.0463443088524619,-2.71884587207157,
13.8103758687955));
#439885=CARTESIAN_POINT('Ctrl Pts',(-0.0609822989275359,-2.72773372807434,
13.7804579775006));
#439886=CARTESIAN_POINT('Ctrl Pts',(-0.056379571104308,-2.74025605087462,
13.7901904343351));
#439887=CARTESIAN_POINT('Ctrl Pts',(-0.0406369357715464,-2.73960385692835,
13.7927914348262));
#439888=CARTESIAN_POINT('Ctrl Pts',(-0.0575902195522705,-2.73691247636728,
13.7597120340895));
#439889=CARTESIAN_POINT('Ctrl Pts',(-0.0522581886711211,-2.75140235340799,
13.7635825532445));
#439890=CARTESIAN_POINT('Ctrl Pts',(-0.0372466566593459,-2.75183803999715,
13.7651073818885));
#439891=CARTESIAN_POINT('Ctrl Pts',(-0.0582544663629731,-2.7351150672818,
13.7381884353898));
#439892=CARTESIAN_POINT('Ctrl Pts',(-0.0530480851316511,-2.74926609215989,
13.7368803041982));
#439893=CARTESIAN_POINT('Ctrl Pts',(-0.0379100977695342,-2.7494420914303,
13.7363986145813));
#439894=CARTESIAN_POINT('Origin',(-0.0447099663884728,-2.70830002549681,
13.7902182540695));
#439895=CARTESIAN_POINT('Ctrl Pts',(-0.0777456563266526,-2.68237325471805,
13.8235227101244));
#439896=CARTESIAN_POINT('Ctrl Pts',(-0.0737644202697953,-2.69315900679101,
13.8358800583119));
#439897=CARTESIAN_POINT('Ctrl Pts',(-0.0574404327052881,-2.69030357704212,
13.8390832900376));
#439898=CARTESIAN_POINT('Ctrl Pts',(-0.0736110288703346,-2.69356128426274,
13.8124254819053));
#439899=CARTESIAN_POINT('Ctrl Pts',(-0.0696220610485445,-2.70436798201703,
13.8247886449158));
#439900=CARTESIAN_POINT('Ctrl Pts',(-0.0532803842747365,-2.70149215494931,
13.8279860620657));
#439901=CARTESIAN_POINT('Ctrl Pts',(-0.0694782544195676,-2.7047442996965,
13.8013225099954));
#439902=CARTESIAN_POINT('Ctrl Pts',(-0.0654834388656869,-2.71556684480029,
13.8136962257787));
#439903=CARTESIAN_POINT('Ctrl Pts',(-0.0491225158051164,-2.71267564755892,
13.8168830918626));
#439904=CARTESIAN_POINT('Ctrl Pts',(-0.0653472608767126,-2.7159224961108,
13.7902140179785));
#439905=CARTESIAN_POINT('Ctrl Pts',(-0.0613483584854679,-2.72675612344471,
13.802602731458));
#439906=CARTESIAN_POINT('Ctrl Pts',(-0.0449667433653669,-2.72385425532595,
13.8057746032558));
#439907=CARTESIAN_POINT('Origin',(-0.0571083661551582,-2.67475077241381,
13.8235269408515));
#439908=CARTESIAN_POINT('Ctrl Pts',(-0.141153018305391,-2.67978844069895,
13.8235269408515));
#439909=CARTESIAN_POINT('Ctrl Pts',(-0.146135141543826,-2.69049334923794,
13.8362179249168));
#439910=CARTESIAN_POINT('Ctrl Pts',(-0.162580199876342,-2.68588649993529,
13.8391868794938));
#439911=CARTESIAN_POINT('Ctrl Pts',(-0.136594592401137,-2.6699939153427,
13.8400110824519));
#439912=CARTESIAN_POINT('Ctrl Pts',(-0.143690585188303,-2.67713315544417,
13.8494522556837));
#439913=CARTESIAN_POINT('Ctrl Pts',(-0.154976452597479,-2.66981488486574,
13.85569149686));
#439914=CARTESIAN_POINT('Ctrl Pts',(-0.1242767815122,-2.65933233661583,
13.8586819406588));
#439915=CARTESIAN_POINT('Ctrl Pts',(-0.128627557213407,-2.65916864656495,
13.868010383617));
#439916=CARTESIAN_POINT('Ctrl Pts',(-0.134433093037599,-2.65222684416309,
13.8744918421245));
#439917=CARTESIAN_POINT('Ctrl Pts',(-0.0930105970316168,-2.66055594029887,
13.8587686893867));
#439918=CARTESIAN_POINT('Ctrl Pts',(-0.0886985410766003,-2.66071811724128,
13.8680909899357));
#439919=CARTESIAN_POINT('Ctrl Pts',(-0.0823841782814193,-2.65426635593163,
13.8745789365163));
#439920=CARTESIAN_POINT('Ctrl Pts',(-0.0814952998104526,-2.67222696861125,
13.8400379222776));
#439921=CARTESIAN_POINT('Ctrl Pts',(-0.0750010167891939,-2.6799142647515,
13.8494748685453));
#439922=CARTESIAN_POINT('Ctrl Pts',(-0.0631611223363676,-2.67354417804797,
13.8557104837033));
#439923=CARTESIAN_POINT('Ctrl Pts',(-0.0777442925716052,-2.68237694711966,
13.8235269408542));
#439924=CARTESIAN_POINT('Ctrl Pts',(-0.0736512963626614,-2.69345232525425,
13.8362179249195));
#439925=CARTESIAN_POINT('Ctrl Pts',(-0.0568854566190928,-2.69020122978514,
13.8391868794965));
#439926=CARTESIAN_POINT('Origin',(-0.161098676348483,-2.67050562187986,
13.8235269408515));
#439927=CARTESIAN_POINT('Ctrl Pts',(-0.156243076003075,-2.71221190170094,
13.7902140241682));
#439928=CARTESIAN_POINT('Ctrl Pts',(-0.161111717548197,-2.72268352645062,
13.8026027327198));
#439929=CARTESIAN_POINT('Ctrl Pts',(-0.177202288601978,-2.71845606202887,
13.8057746032556));
#439930=CARTESIAN_POINT('Ctrl Pts',(-0.151214701217703,-2.7014076141335,
13.8013225161808));
#439931=CARTESIAN_POINT('Ctrl Pts',(-0.156078366210402,-2.71186852665221,
13.8136962270464));
#439932=CARTESIAN_POINT('Ctrl Pts',(-0.172149183841851,-2.70765338419072,
13.8168830918628));
#439933=CARTESIAN_POINT('Ctrl Pts',(-0.146184158654719,-2.6905986687405,
13.8124254880875));
#439934=CARTESIAN_POINT('Ctrl Pts',(-0.15104070365975,-2.70104426329777,
13.8247886461868));
#439935=CARTESIAN_POINT('Ctrl Pts',(-0.167093591866573,-2.6968460086106,
13.8279860620656));
#439936=CARTESIAN_POINT('Ctrl Pts',(-0.141151360553966,-2.67978487695487,
13.8235227163065));
#439937=CARTESIAN_POINT('Ctrl Pts',(-0.145998492247995,-2.69021022575372,
13.8358800595847));
#439938=CARTESIAN_POINT('Ctrl Pts',(-0.162035412684806,-2.68603374234038,
13.8390832900376));
#439939=CARTESIAN_POINT('Origin',(-0.176190397045074,-2.70293265790873,
13.7902182540695));
#439940=CARTESIAN_POINT('Ctrl Pts',(-0.164876586523801,-2.73076235084519,
13.7382347919292));
#439941=CARTESIAN_POINT('Ctrl Pts',(-0.1712221256698,-2.7444536620198,13.7369371795942));
#439942=CARTESIAN_POINT('Ctrl Pts',(-0.186335169692392,-2.74338610528046,
13.7364597369711));
#439943=CARTESIAN_POINT('Ctrl Pts',(-0.165674722335759,-2.73247727743542,
13.7595490285574));
#439944=CARTESIAN_POINT('Ctrl Pts',(-0.172172572818978,-2.74649482877354,
13.7633824266926));
#439945=CARTESIAN_POINT('Ctrl Pts',(-0.187180850232742,-2.74569154216298,
13.7648920890506));
#439946=CARTESIAN_POINT('Ctrl Pts',(-0.161604273412965,-2.72373124577991,
13.780380659011));
#439947=CARTESIAN_POINT('Ctrl Pts',(-0.167219783686543,-2.73585819635999,
13.7901039518744));
#439948=CARTESIAN_POINT('Ctrl Pts',(-0.182865992834047,-2.73393945178664,
13.7926933640892));
#439949=CARTESIAN_POINT('Ctrl Pts',(-0.154528924616555,-2.70852869037029,
13.7936647693663));
#439950=CARTESIAN_POINT('Ctrl Pts',(-0.159065259312451,-2.71834678588172,
13.8072068914933));
#439951=CARTESIAN_POINT('Ctrl Pts',(-0.175420413459769,-2.71353500838634,
13.8104111085397));
#439952=CARTESIAN_POINT('Origin',(-0.184936085948089,-2.72172420427093,
13.7435492065112));
#439953=CARTESIAN_POINT('Origin',(-0.184936085948089,-2.72172420427093,
14.));
#439954=CARTESIAN_POINT('Origin',(-0.184936085948089,-2.72172420427093,
12.5369868989719));
#439955=CARTESIAN_POINT('Ctrl Pts',(-0.15100137827924,-2.73937933745604,
12.506462012331));
#439956=CARTESIAN_POINT('Ctrl Pts',(-0.151361257043662,-2.74590804906438,
12.4999388158272));
#439957=CARTESIAN_POINT('Ctrl Pts',(-0.151356999205927,-2.74583080584417,
12.4907030323752));
#439958=CARTESIAN_POINT('Ctrl Pts',(-0.164186551648245,-2.74092199308309,
12.5042014951932));
#439959=CARTESIAN_POINT('Ctrl Pts',(-0.169242651760944,-2.74489401382405,
12.4980716682127));
#439960=CARTESIAN_POINT('Ctrl Pts',(-0.176021078885824,-2.7444715319445,
12.4907355092743));
#439961=CARTESIAN_POINT('Ctrl Pts',(-0.167153370653351,-2.73567569093429,
12.5218047446509));
#439962=CARTESIAN_POINT('Ctrl Pts',(-0.174926379729319,-2.74456946408416,
12.5216906929434));
#439963=CARTESIAN_POINT('Ctrl Pts',(-0.186654053236909,-2.74365708892587,
12.5161988840776));
#439964=CARTESIAN_POINT('Ctrl Pts',(-0.164974248776966,-2.73097218009018,
12.5369868989719));
#439965=CARTESIAN_POINT('Ctrl Pts',(-0.171418360289289,-2.74488185148592,
12.5369868989719));
#439966=CARTESIAN_POINT('Ctrl Pts',(-0.186698955428321,-2.74365346078353,
12.5369868989719));
#439967=CARTESIAN_POINT('Origin',(-2.10137191087939E-32,-1.02994378190383E-30,
12.5));
#439968=CARTESIAN_POINT('Origin',(0.0777442925777901,-2.68237694712209,
12.5));
#439969=CARTESIAN_POINT('',(0.0777442925777901,-2.68237694712209,12.5893111709658));
#439970=CARTESIAN_POINT('',(0.0777442925777901,-2.68237694712209,13.8235269408515));
#439971=CARTESIAN_POINT('',(0.0777442925777901,-2.68237694712209,12.5));
#439972=CARTESIAN_POINT('',(0.0653458928111052,-2.71592620020509,13.7902182540695));
#439973=CARTESIAN_POINT('',(0.0777442925777901,-2.68237694712209,13.8235269408515));
#439974=CARTESIAN_POINT('',(0.0581609899471712,-2.73536807408357,13.7435492065112));
#439975=CARTESIAN_POINT('Origin',(0.081799530956857,-2.67140467892656,13.7445212918695));
#439976=CARTESIAN_POINT('',(0.0581609899471712,-2.73536807408357,12.5369868989719));
#439977=CARTESIAN_POINT('',(0.0581609899471712,-2.73536807408357,12.5));
#439978=CARTESIAN_POINT('Ctrl Pts',(0.0581609899471712,-2.73536807408357,
12.5369868989719));
#439979=CARTESIAN_POINT('Ctrl Pts',(0.0646839965340922,-2.71771724793141,
12.5544431401645));
#439980=CARTESIAN_POINT('Ctrl Pts',(0.0712116685486955,-2.70005379743926,
12.5718848856037));
#439981=CARTESIAN_POINT('Ctrl Pts',(0.0777442925777901,-2.68237694712209,
12.5893111709658));
#439982=CARTESIAN_POINT('Origin',(0.257188253544047,-2.9291091662376,12.5));
#439983=CARTESIAN_POINT('',(0.164990427905034,-2.73100702309001,13.7435492065112));
#439984=CARTESIAN_POINT('',(0.156244739002019,-2.71221547672782,13.7902182540695));
#439985=CARTESIAN_POINT('Origin',(0.133262580124126,-2.66283454072077,13.7418732680448));
#439986=CARTESIAN_POINT('',(0.141153018305427,-2.67978844069895,13.8235269408515));
#439987=CARTESIAN_POINT('',(0.156244739002019,-2.71221547672782,13.7902182540695));
#439988=CARTESIAN_POINT('',(0.141153018305427,-2.67978844069895,12.5893111709658));
#439989=CARTESIAN_POINT('',(0.141153018305427,-2.67978844069895,12.5));
#439990=CARTESIAN_POINT('',(0.164990427905034,-2.73100702309001,12.5369868989719));
#439991=CARTESIAN_POINT('Ctrl Pts',(0.141153018305427,-2.67978844069895,
12.5893111709658));
#439992=CARTESIAN_POINT('Ctrl Pts',(0.14910473297169,-2.69687400325064,
12.5718848856037));
#439993=CARTESIAN_POINT('Ctrl Pts',(0.157050419890744,-2.71394661419926,
12.5544431401645));
#439994=CARTESIAN_POINT('Ctrl Pts',(0.164990427905034,-2.73100702309001,
12.5369868989719));
#439995=CARTESIAN_POINT('',(0.164990427905034,-2.73100702309001,12.5));
#439996=CARTESIAN_POINT('Origin',(0.109987927613096,-2.69429284510378,12.5));
#439997=CARTESIAN_POINT('',(0.107467979553556,-2.66001107102548,13.8587068136939));
#439998=CARTESIAN_POINT('Ctrl Pts',(0.141153018311358,-2.67978844069603,
13.8235269408542));
#439999=CARTESIAN_POINT('Ctrl Pts',(0.140413642498288,-2.67819977054959,
13.8262006681044));
#440000=CARTESIAN_POINT('Ctrl Pts',(0.139499483687007,-2.67664730744221,
13.8288634856214));
#440001=CARTESIAN_POINT('Ctrl Pts',(0.138423816759605,-2.67512979298056,
13.8314912288862));
#440002=CARTESIAN_POINT('Ctrl Pts',(0.137314915107352,-2.67356539209496,
13.8342001611531));
#440003=CARTESIAN_POINT('Ctrl Pts',(0.136033544632342,-2.67203610781815,
13.8368750301949));
#440004=CARTESIAN_POINT('Ctrl Pts',(0.134549670915372,-2.67054803930163,
13.8394886372969));
#440005=CARTESIAN_POINT('Ctrl Pts',(0.134435067748838,-2.67043311216055,
13.8396904925131));
#440006=CARTESIAN_POINT('Ctrl Pts',(0.13431923853801,-2.67031844356835,
13.8398919674349));
#440007=CARTESIAN_POINT('Ctrl Pts',(0.134202160684652,-2.67020404369636,
13.8400930404591));
#440008=CARTESIAN_POINT('Ctrl Pts',(0.132378008963169,-2.66842161672634,
13.8432258934518));
#440009=CARTESIAN_POINT('Ctrl Pts',(0.13026083464185,-2.66671271363484,
13.8462331177034));
#440010=CARTESIAN_POINT('Ctrl Pts',(0.127859099286356,-2.66520813419667,
13.8489036603661));
#440011=CARTESIAN_POINT('Ctrl Pts',(0.127073223527637,-2.66471581829483,
13.849777493004));
#440012=CARTESIAN_POINT('Ctrl Pts',(0.12625698506697,-2.66424560584087,
13.85061494757));
#440013=CARTESIAN_POINT('Ctrl Pts',(0.125410989701583,-2.66380272259741,
13.8514076489583));
#440014=CARTESIAN_POINT('Ctrl Pts',(0.123621587492998,-2.66286596066418,
13.8530843267192));
#440015=CARTESIAN_POINT('Ctrl Pts',(0.121521919523597,-2.66196207099981,
13.8546805203176));
#440016=CARTESIAN_POINT('Ctrl Pts',(0.119179897922236,-2.66126884112717,
13.8559412814273));
#440017=CARTESIAN_POINT('Ctrl Pts',(0.118866459478416,-2.66117606448823,
13.8561100121513));
#440018=CARTESIAN_POINT('Ctrl Pts',(0.11854874454682,-2.66108701902086,
13.8562727473908));
#440019=CARTESIAN_POINT('Ctrl Pts',(0.118226973754739,-2.66100208182593,
13.8564289040185));
#440020=CARTESIAN_POINT('Ctrl Pts',(0.116767746883536,-2.66061689261589,
13.8571370725437));
#440021=CARTESIAN_POINT('Ctrl Pts',(0.115198876558341,-2.66031162512267,
13.8577210840553));
#440022=CARTESIAN_POINT('Ctrl Pts',(0.113575739692616,-2.66012695291767,
13.8581177131616));
#440023=CARTESIAN_POINT('Ctrl Pts',(0.11311860848455,-2.66007494286852,
13.8582294175695));
#440024=CARTESIAN_POINT('Ctrl Pts',(0.112657227229961,-2.66003232907039,
13.8583265086086));
#440025=CARTESIAN_POINT('Ctrl Pts',(0.112192942055877,-2.65999959428129,
13.8584082369006));
#440026=CARTESIAN_POINT('Ctrl Pts',(0.111525888763714,-2.65995256316754,
13.8585256585398));
#440027=CARTESIAN_POINT('Ctrl Pts',(0.110844525421073,-2.6599256621248,
13.8586122832068));
#440028=CARTESIAN_POINT('Ctrl Pts',(0.110166520719318,-2.65992037903644,
13.8586682984299));
#440029=CARTESIAN_POINT('Ctrl Pts',(0.10962418416636,-2.65991615308945,
13.8587131050557));
#440030=CARTESIAN_POINT('Ctrl Pts',(0.109078008326726,-2.65992547805404,
13.8587357943552));
#440031=CARTESIAN_POINT('Ctrl Pts',(0.108527936945158,-2.65994886141044,
13.8587355499465));
#440032=CARTESIAN_POINT('Ctrl Pts',(0.108172412696959,-2.65996397463117,
13.8587353919793));
#440033=CARTESIAN_POINT('Ctrl Pts',(0.107819104095523,-2.65998475845746,
13.8587257282814));
#440034=CARTESIAN_POINT('Ctrl Pts',(0.107467979553556,-2.66001107102548,
13.8587068136939));
#440035=CARTESIAN_POINT('Ctrl Pts',(0.107467979553556,-2.66001107102548,
13.8587068136939));
#440036=CARTESIAN_POINT('Ctrl Pts',(0.106313150076722,-2.66009761162726,
13.8586446046466));
#440037=CARTESIAN_POINT('Ctrl Pts',(0.105181916032446,-2.66024388385118,
13.858482427929));
#440038=CARTESIAN_POINT('Ctrl Pts',(0.104073401795672,-2.66044550372209,
13.8582284286032));
#440039=CARTESIAN_POINT('Ctrl Pts',(0.102936195136436,-2.66065234225626,
13.8579678548414));
#440040=CARTESIAN_POINT('Ctrl Pts',(0.101820395848112,-2.66091944289693,
13.857615680862));
#440041=CARTESIAN_POINT('Ctrl Pts',(0.100767737702107,-2.66122685196505,
13.8571944833187));
#440042=CARTESIAN_POINT('Ctrl Pts',(0.0981407216417111,-2.66199402273378,
13.8561433417727));
#440043=CARTESIAN_POINT('Ctrl Pts',(0.0957827227013604,-2.66304351832924,
13.8546163505474));
#440044=CARTESIAN_POINT('Ctrl Pts',(0.093754502726362,-2.66417768788552,
13.8528973491086));
#440045=CARTESIAN_POINT('Ctrl Pts',(0.0933839768605227,-2.66438488393034,
13.8525833129072));
#440046=CARTESIAN_POINT('Ctrl Pts',(0.0930243388479905,-2.66459482833731,
13.8522628768812));
#440047=CARTESIAN_POINT('Ctrl Pts',(0.0926757961602304,-2.6648062424995,
13.851937733538));
#440048=CARTESIAN_POINT('Ctrl Pts',(0.0905472943242078,-2.66609731945559,
13.8499521282529));
#440049=CARTESIAN_POINT('Ctrl Pts',(0.088623160818785,-2.66757500479494,
13.847639871647));
#440050=CARTESIAN_POINT('Ctrl Pts',(0.0869555867092282,-2.66909791820874,
13.8452109780794));
#440051=CARTESIAN_POINT('Ctrl Pts',(0.086205310600268,-2.66978310847635,
13.8441181685877));
#440052=CARTESIAN_POINT('Ctrl Pts',(0.0855063319983435,-2.67047712429546,
13.8430021611332));
#440053=CARTESIAN_POINT('Ctrl Pts',(0.0848601393738974,-2.67116655249071,
13.8418824960098));
#440054=CARTESIAN_POINT('Ctrl Pts',(0.0833373699532803,-2.67279120763798,
13.8392439765549));
#440055=CARTESIAN_POINT('Ctrl Pts',(0.0820321778432484,-2.67446546559834,
13.8364981347964));
#440056=CARTESIAN_POINT('Ctrl Pts',(0.0809141226483275,-2.67617271473482,
13.8336931113419));
#440057=CARTESIAN_POINT('Ctrl Pts',(0.079825207891543,-2.6778354669734,
13.8309611966328));
#440058=CARTESIAN_POINT('Ctrl Pts',(0.0789131832822403,-2.67953148850894,
13.8281701127186));
#440059=CARTESIAN_POINT('Ctrl Pts',(0.0781883844852199,-2.68125352738293,
13.8253580685121));
#440060=CARTESIAN_POINT('Ctrl Pts',(0.0780312473237982,-2.6816268672693,
13.8247484142933));
#440061=CARTESIAN_POINT('Ctrl Pts',(0.0778830802481646,-2.68200139682803,
13.8241378483365));
#440062=CARTESIAN_POINT('Ctrl Pts',(0.0777442925777901,-2.68237694712209,
13.8235269408515));
#440063=CARTESIAN_POINT('',(0.108708163673209,-2.65994236726223,12.5969504640361));
#440064=CARTESIAN_POINT('Origin',(0.109989081477175,-2.69432591096847,12.584524458991));
#440065=CARTESIAN_POINT('Origin',(0.109989081477175,-2.69432591096847,12.584524458991));
#440066=CARTESIAN_POINT('Ctrl Pts',(0.141153018305427,-2.67978844069895,
12.5893111709658));
#440067=CARTESIAN_POINT('Ctrl Pts',(0.136370695980246,-2.66951283717712,
12.5770542771492));
#440068=CARTESIAN_POINT('Ctrl Pts',(0.12050688364808,-2.67353068898434,
12.5737548217797));
#440069=CARTESIAN_POINT('Ctrl Pts',(0.151610352235496,-2.70225773700608,
12.5663937883685));
#440070=CARTESIAN_POINT('Ctrl Pts',(0.146821929394034,-2.69196902552492,
12.5540940315303));
#440071=CARTESIAN_POINT('Ctrl Pts',(0.130909746733166,-2.69600244073795,
12.5508374392248));
#440072=CARTESIAN_POINT('Ctrl Pts',(0.162057134843887,-2.72470436206883,
12.5434499600945));
#440073=CARTESIAN_POINT('Ctrl Pts',(0.157253143134597,-2.71438219832273,
12.5311293540533));
#440074=CARTESIAN_POINT('Ctrl Pts',(0.141303516703331,-2.71845174145023,
12.5278936106989));
#440075=CARTESIAN_POINT('Ctrl Pts',(0.172494192629982,-2.7471300917566,
12.5204817579905));
#440076=CARTESIAN_POINT('Ctrl Pts',(0.167666424444766,-2.73675684035417,
12.5081597038247));
#440077=CARTESIAN_POINT('Ctrl Pts',(0.151688912883333,-2.74088033028371,
12.5049254088044));
#440078=CARTESIAN_POINT('Ctrl Pts',(0.164990427905034,-2.73100702309001,
12.5369868989719));
#440079=CARTESIAN_POINT('Ctrl Pts',(0.165383472766402,-2.73185154479352,
12.5342545179733));
#440080=CARTESIAN_POINT('Ctrl Pts',(0.165645479457248,-2.73271015390558,
12.5314872231885));
#440081=CARTESIAN_POINT('Ctrl Pts',(0.165708221792586,-2.73355079919908,
12.5287124745063));
#440082=CARTESIAN_POINT('Ctrl Pts',(0.165764805944844,-2.73430893485067,
12.5262100684184));
#440083=CARTESIAN_POINT('Ctrl Pts',(0.165658283869168,-2.73505176820016,
12.5237004536639));
#440084=CARTESIAN_POINT('Ctrl Pts',(0.165321207164616,-2.73578264429546,
12.5212220730815));
#440085=CARTESIAN_POINT('Ctrl Pts',(0.16506314578782,-2.73634219317223,
12.5193246583486));
#440086=CARTESIAN_POINT('Ctrl Pts',(0.164666290656814,-2.73690115527121,
12.517417831369));
#440087=CARTESIAN_POINT('Ctrl Pts',(0.164041812144491,-2.73741999174944,
12.5155812248347));
#440088=CARTESIAN_POINT('Ctrl Pts',(0.163775780941654,-2.73764101887792,
12.5147988205793));
#440089=CARTESIAN_POINT('Ctrl Pts',(0.163468347488137,-2.73785520143648,
12.5140295443047));
#440090=CARTESIAN_POINT('Ctrl Pts',(0.163112844721882,-2.73806160040939,
12.5132817086137));
#440091=CARTESIAN_POINT('Ctrl Pts',(0.162574839376482,-2.73837395733388,
12.5121499604604));
#440092=CARTESIAN_POINT('Ctrl Pts',(0.161911533537851,-2.73866904796622,
12.5110494206568));
#440093=CARTESIAN_POINT('Ctrl Pts',(0.161097646294455,-2.73891952684504,
12.5100666561695));
#440094=CARTESIAN_POINT('Ctrl Pts',(0.160630314113512,-2.73906335124046,
12.5095023550641));
#440095=CARTESIAN_POINT('Ctrl Pts',(0.160107743198438,-2.73919350489643,
12.5089719619137));
#440096=CARTESIAN_POINT('Ctrl Pts',(0.159538184953438,-2.73930135058482,
12.5085043804652));
#440097=CARTESIAN_POINT('Ctrl Pts',(0.158704710652061,-2.7394591687019,
12.5078201359221));
#440098=CARTESIAN_POINT('Ctrl Pts',(0.157746217039477,-2.73957260594112,
12.5072563000949));
#440099=CARTESIAN_POINT('Ctrl Pts',(0.156726680840859,-2.73962556560587,
12.5068768744332));
#440100=CARTESIAN_POINT('Ctrl Pts',(0.155991525056544,-2.73966375316991,
12.5066032824114));
#440101=CARTESIAN_POINT('Ctrl Pts',(0.155211718308491,-2.73967122688161,
12.5064197834844));
#440102=CARTESIAN_POINT('Ctrl Pts',(0.154430831801786,-2.73965015412842,
12.5063282718343));
#440103=CARTESIAN_POINT('Ctrl Pts',(0.153290979258348,-2.73961939443274,
12.5061946931565));
#440104=CARTESIAN_POINT('Ctrl Pts',(0.152124434430004,-2.73952821524961,
12.5062515701262));
#440105=CARTESIAN_POINT('Ctrl Pts',(0.151002390083283,-2.73939769282737,
12.5064436508398));
#440106=CARTESIAN_POINT('',(0.120506883648079,-2.67353068898434,12.5737548217797));
#440107=CARTESIAN_POINT('Origin',(0.121207360262335,-2.68907125951804,12.5893111709658));
#440108=CARTESIAN_POINT('Ctrl Pts',(0.151002390083283,-2.73939769282737,
12.5064436508398));
#440109=CARTESIAN_POINT('Ctrl Pts',(0.146487826858497,-2.72964786684735,
12.5164271754438));
#440110=CARTESIAN_POINT('Ctrl Pts',(0.141971663658479,-2.71989408824766,
12.5264061185523));
#440111=CARTESIAN_POINT('Ctrl Pts',(0.137453843274561,-2.71013621821805,
12.536380305637));
#440112=CARTESIAN_POINT('Ctrl Pts',(0.131807484107369,-2.69794085979033,
12.5488460165097));
#440113=CARTESIAN_POINT('Ctrl Pts',(0.126158534784632,-2.68573910696496,
12.5613043021964));
#440114=CARTESIAN_POINT('Ctrl Pts',(0.12050688364808,-2.67353068898434,
12.5737548217797));
#440115=CARTESIAN_POINT('Ctrl Pts',(0.0777442925777903,-2.68237694712209,
12.5893111709658));
#440116=CARTESIAN_POINT('Ctrl Pts',(0.0816731450388711,-2.67174573115689,
12.5770542771492));
#440117=CARTESIAN_POINT('Ctrl Pts',(0.0978116640663786,-2.67445716591614,
12.5737548217797));
#440118=CARTESIAN_POINT('Ctrl Pts',(0.0814098777526247,-2.67245811509199,
12.5928319619712));
#440119=CARTESIAN_POINT('Ctrl Pts',(0.0871060609854467,-2.6664425591784,
12.5821634970842));
#440120=CARTESIAN_POINT('Ctrl Pts',(0.099138094406165,-2.67084070356696,
12.5773203894503));
#440121=CARTESIAN_POINT('Ctrl Pts',(0.0932406545772418,-2.66059991880985,
12.5969440695591));
#440122=CARTESIAN_POINT('Ctrl Pts',(0.0972562914093082,-2.66041770085005,
12.5878292599214));
#440123=CARTESIAN_POINT('Ctrl Pts',(0.103356273079777,-2.66661564548747,
12.5813877129824));
#440124=CARTESIAN_POINT('Ctrl Pts',(0.123809925774304,-2.65929803401389,
12.596957478804));
#440125=CARTESIAN_POINT('Ctrl Pts',(0.119823969208925,-2.65947898541016,
12.5878468778671));
#440126=CARTESIAN_POINT('Ctrl Pts',(0.114297692806488,-2.66615564258733,
12.5814011370086));
#440127=CARTESIAN_POINT('Ctrl Pts',(0.136684674550041,-2.67018747160734,
12.5928371701607));
#440128=CARTESIAN_POINT('Ctrl Pts',(0.130517498435897,-2.66466470015807,
12.5821692192952));
#440129=CARTESIAN_POINT('Ctrl Pts',(0.118885151398158,-2.67002308838229,
12.5773318885715));
#440130=CARTESIAN_POINT('Ctrl Pts',(0.141153018305476,-2.67978844069892,
12.5893111709658));
#440131=CARTESIAN_POINT('Ctrl Pts',(0.136370695980294,-2.6695128371771,
12.5770542771492));
#440132=CARTESIAN_POINT('Ctrl Pts',(0.120506883648129,-2.67353068898432,
12.5737548217797));
#440133=CARTESIAN_POINT('',(0.0978116640663786,-2.67445716591615,12.5737548217797));
#440134=CARTESIAN_POINT('Origin',(0.0983802190003859,-2.69000312183037,
12.5893111709658));
#440135=CARTESIAN_POINT('Ctrl Pts',(0.120506883648129,-2.67353068898432,
12.5737548217797));
#440136=CARTESIAN_POINT('Ctrl Pts',(0.120113885752202,-2.67260880380448,
12.5746934679442));
#440137=CARTESIAN_POINT('Ctrl Pts',(0.119510496091739,-2.67166051252229,
12.5756680099006));
#440138=CARTESIAN_POINT('Ctrl Pts',(0.118768172763169,-2.67079191610057,
12.5765688348656));
#440139=CARTESIAN_POINT('Ctrl Pts',(0.118571650879716,-2.67056196481359,
12.5768073183026));
#440140=CARTESIAN_POINT('Ctrl Pts',(0.118365621796738,-2.6703374846426,
12.5770407398754));
#440141=CARTESIAN_POINT('Ctrl Pts',(0.118151836512603,-2.67012007490227,
12.5772674179684));
#440142=CARTESIAN_POINT('Ctrl Pts',(0.117274519516509,-2.66922788411801,
12.5781976435658));
#440143=CARTESIAN_POINT('Ctrl Pts',(0.116208711112566,-2.66841199814016,
12.5790594849312));
#440144=CARTESIAN_POINT('Ctrl Pts',(0.114997023664009,-2.66776585090409,
12.5797571720116));
#440145=CARTESIAN_POINT('Ctrl Pts',(0.114207565722877,-2.6673448627464,
12.580211740231));
#440146=CARTESIAN_POINT('Ctrl Pts',(0.113311472037167,-2.66699336155614,
12.5806009430798));
#440147=CARTESIAN_POINT('Ctrl Pts',(0.112365354094484,-2.66675258468255,
12.5808812374708));
#440148=CARTESIAN_POINT('Ctrl Pts',(0.111552324910359,-2.66654567747125,
12.5811221033394));
#440149=CARTESIAN_POINT('Ctrl Pts',(0.110685682238033,-2.66641640941177,
12.581287365893));
#440150=CARTESIAN_POINT('Ctrl Pts',(0.109813110705442,-2.66638032334846,
12.581359338449));
#440151=CARTESIAN_POINT('Ctrl Pts',(0.109691841280325,-2.66637530813081,
12.5813693411482));
#440152=CARTESIAN_POINT('Ctrl Pts',(0.109570439731087,-2.6663720355171,
12.5813775999465));
#440153=CARTESIAN_POINT('Ctrl Pts',(0.109449014989987,-2.66637048892921,
12.5813841266931));
#440154=CARTESIAN_POINT('Ctrl Pts',(0.109243003230692,-2.66636786495581,
12.5813952001081));
#440155=CARTESIAN_POINT('Ctrl Pts',(0.109035537190336,-2.66637080063471,
12.5814007534795));
#440156=CARTESIAN_POINT('Ctrl Pts',(0.108826710017423,-2.6663794918774,
12.5814005856065));
#440157=CARTESIAN_POINT('Ctrl Pts',(0.107870780865955,-2.66641927698838,
12.5813998171494));
#440158=CARTESIAN_POINT('Ctrl Pts',(0.106952363184188,-2.66657658103314,
12.58127954464));
#440159=CARTESIAN_POINT('Ctrl Pts',(0.106071675905653,-2.66682134627691,
12.5810700125799));
#440160=CARTESIAN_POINT('Ctrl Pts',(0.105007905947459,-2.66711699482262,
12.5808169217085));
#440161=CARTESIAN_POINT('Ctrl Pts',(0.104003569558322,-2.66755639984867,
12.5804173076348));
#440162=CARTESIAN_POINT('Ctrl Pts',(0.103136246654913,-2.66807719380877,
12.5799304713245));
#440163=CARTESIAN_POINT('Ctrl Pts',(0.102061360342698,-2.66872262159235,
12.5793271277669));
#440164=CARTESIAN_POINT('Ctrl Pts',(0.101113659827898,-2.66950548591178,
12.5785808224116));
#440165=CARTESIAN_POINT('Ctrl Pts',(0.1003128929177,-2.67036833480848,12.5777485681082));
#440166=CARTESIAN_POINT('Ctrl Pts',(0.0991196624909412,-2.67165407419672,
12.576508418016));
#440167=CARTESIAN_POINT('Ctrl Pts',(0.0982576973188824,-2.67310191243109,
12.5750928681475));
#440168=CARTESIAN_POINT('Ctrl Pts',(0.0978116640663786,-2.67445716591614,
12.5737548217797));
#440169=CARTESIAN_POINT('Ctrl Pts',(0.0978116640663786,-2.67445716591614,
12.5737548217797));
#440170=CARTESIAN_POINT('Ctrl Pts',(0.0816731450388708,-2.67174573115689,
12.5770542771492));
#440171=CARTESIAN_POINT('Ctrl Pts',(0.0777442925777901,-2.68237694712209,
12.5893111709658));
#440172=CARTESIAN_POINT('Ctrl Pts',(0.0892763545231182,-2.69769858250746,
12.5508408821982));
#440173=CARTESIAN_POINT('Ctrl Pts',(0.0730883661518879,-2.69497557734355,
12.55409748406));
#440174=CARTESIAN_POINT('Ctrl Pts',(0.0691545014812997,-2.70562035601753,
12.5663972313419));
#440175=CARTESIAN_POINT('Ctrl Pts',(0.080748275692504,-2.72091688854494,
12.52790050457));
#440176=CARTESIAN_POINT('Ctrl Pts',(0.0645200291598312,-2.71816093284563,
12.5311362602938));
#440177=CARTESIAN_POINT('Ctrl Pts',(0.0605733760725459,-2.72884031613277,
12.5434568539655));
#440178=CARTESIAN_POINT('Ctrl Pts',(0.0722268526561591,-2.74411387524132,
12.5049357605811));
#440179=CARTESIAN_POINT('Ctrl Pts',(0.0559664200791695,-2.74130643558952,
12.5081700652078));
#440180=CARTESIAN_POINT('Ctrl Pts',(0.0520002376530914,-2.75203866398107,
12.5204921097672));
#440181=CARTESIAN_POINT('Ctrl Pts',(0.0727864012058899,-2.74259066961817,
12.5064436508395));
#440182=CARTESIAN_POINT('Ctrl Pts',(0.0715899150693781,-2.74282997844734,
12.5062361689309));
#440183=CARTESIAN_POINT('Ctrl Pts',(0.0703354627390177,-2.74302781921991,
12.5061871075061));
#440184=CARTESIAN_POINT('Ctrl Pts',(0.0691123928730676,-2.74315076938917,
12.5063648335164));
#440185=CARTESIAN_POINT('Ctrl Pts',(0.0685567990978748,-2.74320662093993,
12.5064455676329));
#440186=CARTESIAN_POINT('Ctrl Pts',(0.0679999097957444,-2.74324757834277,
12.506574497099));
#440187=CARTESIAN_POINT('Ctrl Pts',(0.0674655256239186,-2.74327083734875,
12.5067492519495));
#440188=CARTESIAN_POINT('Ctrl Pts',(0.0663916598874039,-2.74331757722413,
12.5071004286051));
#440189=CARTESIAN_POINT('Ctrl Pts',(0.0653691580536572,-2.74329375765344,
12.5076537929612));
#440190=CARTESIAN_POINT('Ctrl Pts',(0.0644745439694499,-2.74321062230247,
12.5083435010503));
#440191=CARTESIAN_POINT('Ctrl Pts',(0.0644182226665065,-2.7432053884353,
12.5083869222963));
#440192=CARTESIAN_POINT('Ctrl Pts',(0.0643624032032485,-2.74319990701827,
12.5084308732336));
#440193=CARTESIAN_POINT('Ctrl Pts',(0.064307102256264,-2.7431941759338,
12.5084753333615));
#440194=CARTESIAN_POINT('Ctrl Pts',(0.0638635156715535,-2.74314820507212,
12.508831962269));
#440195=CARTESIAN_POINT('Ctrl Pts',(0.0634441527162526,-2.74308652014177,
12.509227847131));
#440196=CARTESIAN_POINT('Ctrl Pts',(0.0630610757559996,-2.74301372560217,
12.5096423454524));
#440197=CARTESIAN_POINT('Ctrl Pts',(0.0618606821053256,-2.74278561973258,
12.5109411997424));
#440198=CARTESIAN_POINT('Ctrl Pts',(0.0609409503657873,-2.74244389525738,
12.5124831113042));
#440199=CARTESIAN_POINT('Ctrl Pts',(0.0602360550834692,-2.74205654384529,
12.5140723025008));
#440200=CARTESIAN_POINT('Ctrl Pts',(0.0601700056234664,-2.74202024859372,
12.5142212114565));
#440201=CARTESIAN_POINT('Ctrl Pts',(0.0601058156470521,-2.74198356541646,
12.5143705582413));
#440202=CARTESIAN_POINT('Ctrl Pts',(0.0600434163783638,-2.74194655888611,
12.5145201959299));
#440203=CARTESIAN_POINT('Ctrl Pts',(0.0592418048692627,-2.74147115490679,
12.5164425148273));
#440204=CARTESIAN_POINT('Ctrl Pts',(0.0587027742224739,-2.74093533428272,
12.5184635205941));
#440205=CARTESIAN_POINT('Ctrl Pts',(0.0583390230378892,-2.74036182242016,
12.5205025929157));
#440206=CARTESIAN_POINT('Ctrl Pts',(0.0581280329330801,-2.74002916280799,
12.5216853356836));
#440207=CARTESIAN_POINT('Ctrl Pts',(0.0579759876853332,-2.73968468204338,
12.5228750347131));
#440208=CARTESIAN_POINT('Ctrl Pts',(0.0578676721343238,-2.73933845149886,
12.5240609649613));
#440209=CARTESIAN_POINT('Ctrl Pts',(0.0576018174252999,-2.73848864720195,
12.5269717671327));
#440210=CARTESIAN_POINT('Ctrl Pts',(0.0576018431583101,-2.73760128088103,
12.5299036066169));
#440211=CARTESIAN_POINT('Ctrl Pts',(0.0577822188798732,-2.73669028322723,
12.5328133004019));
#440212=CARTESIAN_POINT('Ctrl Pts',(0.0578688097291865,-2.7362529513076,
12.5342101228452));
#440213=CARTESIAN_POINT('Ctrl Pts',(0.0579973693552569,-2.73581082086395,
12.5356023438238));
#440214=CARTESIAN_POINT('Ctrl Pts',(0.0581609899471714,-2.73536807408357,
12.5369868989719));
#440215=CARTESIAN_POINT('Origin',(-4.36479134863697,-14.6883069150384,-1.23969978058422));
#440216=CARTESIAN_POINT('Ctrl Pts',(0.164972828967398,-2.73096911480167,
12.5369868989719));
#440217=CARTESIAN_POINT('Ctrl Pts',(0.171418610569547,-2.74488799418265,
12.5369868989719));
#440218=CARTESIAN_POINT('Ctrl Pts',(0.186707740121687,-2.74365275282046,
12.5369868989719));
#440219=CARTESIAN_POINT('Ctrl Pts',(0.167151815324024,-2.73567421257279,
12.5218025310015));
#440220=CARTESIAN_POINT('Ctrl Pts',(0.174927792427972,-2.74457309136637,
12.5216901060418));
#440221=CARTESIAN_POINT('Ctrl Pts',(0.186661135115968,-2.74365653468369,
12.5161920673677));
#440222=CARTESIAN_POINT('Ctrl Pts',(0.164186617639527,-2.74092241930334,
12.5042015548895));
#440223=CARTESIAN_POINT('Ctrl Pts',(0.169245524179631,-2.74489542945129,
12.4980677368513));
#440224=CARTESIAN_POINT('Ctrl Pts',(0.17602864357708,-2.74447108175938,
12.4907278922778));
#440225=CARTESIAN_POINT('Ctrl Pts',(0.1510012892348,-2.73937772206282,12.506463626192));
#440226=CARTESIAN_POINT('Ctrl Pts',(0.15136139457082,-2.74591054400155,
12.4999376786891));
#440227=CARTESIAN_POINT('Ctrl Pts',(0.151356996407733,-2.74583075508029,
12.4906970594712));
#440228=CARTESIAN_POINT('Origin',(0.184936085948126,-2.72172420427093,12.5369868989719));
#440229=CARTESIAN_POINT('Origin',(0.184936085948126,-2.72172420427093,14.));
#440230=CARTESIAN_POINT('Origin',(0.184936085948126,-2.72172420427093,13.7435492065112));
#440231=CARTESIAN_POINT('Ctrl Pts',(0.154543018014346,-2.70855898586017,
13.793642941384));
#440232=CARTESIAN_POINT('Ctrl Pts',(0.159080541277636,-2.7183731135158,
13.8071662555867));
#440233=CARTESIAN_POINT('Ctrl Pts',(0.175421077119549,-2.71357662813231,
13.8103758687955));
#440234=CARTESIAN_POINT('Ctrl Pts',(0.16155623652397,-2.72362804261103,
13.7804579775005));
#440235=CARTESIAN_POINT('Ctrl Pts',(0.167164334709864,-2.73573353336799,
13.7901904343351));
#440236=CARTESIAN_POINT('Ctrl Pts',(0.182801427860942,-2.73380033861611,
13.7927914348263));
#440237=CARTESIAN_POINT('Ctrl Pts',(0.165685182232128,-2.73249976341654,
13.7597120340895));
#440238=CARTESIAN_POINT('Ctrl Pts',(0.172180530716661,-2.74650681656974,
13.7635825532445));
#440239=CARTESIAN_POINT('Ctrl Pts',(0.187177625595774,-2.74571747422855,
13.7651073818884));
#440240=CARTESIAN_POINT('Ctrl Pts',(0.164876640121115,-2.7307624773432,
13.7381884353898));
#440241=CARTESIAN_POINT('Ctrl Pts',(0.171219137447652,-2.74444204744936,
13.7368803041982));
#440242=CARTESIAN_POINT('Ctrl Pts',(0.186321099980056,-2.74338357459246,
13.7363986145813));
#440243=CARTESIAN_POINT('Origin',(0.176190397045111,-2.70293265790873,13.7902182540695));
#440244=CARTESIAN_POINT('Ctrl Pts',(0.141151358129088,-2.67978487173929,
13.8235227101244));
#440245=CARTESIAN_POINT('Ctrl Pts',(0.145998485875386,-2.69021022741335,
13.8358800583119));
#440246=CARTESIAN_POINT('Ctrl Pts',(0.162035412684842,-2.68603374234037,
13.8390832900376));
#440247=CARTESIAN_POINT('Ctrl Pts',(0.146184156226102,-2.69059866351688,
13.8124254819053));
#440248=CARTESIAN_POINT('Ctrl Pts',(0.151040697278011,-2.7010442649666,
13.8247886449157));
#440249=CARTESIAN_POINT('Ctrl Pts',(0.167093591866549,-2.69684600861049,
13.8279860620657));
#440250=CARTESIAN_POINT('Ctrl Pts',(0.151214698786735,-2.70140760890482,
13.8013225099955));
#440251=CARTESIAN_POINT('Ctrl Pts',(0.156078359818992,-2.71186852832885,
13.8136962257787));
#440252=CARTESIAN_POINT('Ctrl Pts',(0.172149183841997,-2.70765338419096,
13.8168830918626));
#440253=CARTESIAN_POINT('Ctrl Pts',(0.156243073570434,-2.71221189646866,
13.7902140179785));
#440254=CARTESIAN_POINT('Ctrl Pts',(0.16111171114607,-2.72268352813243,
13.802602731458));
#440255=CARTESIAN_POINT('Ctrl Pts',(0.177202288601925,-2.71845606202867,
13.8057746032558));
#440256=CARTESIAN_POINT('Origin',(0.161098676348519,-2.67050562187986,13.8235269408515));
#440257=CARTESIAN_POINT('Ctrl Pts',(0.0777442925777901,-2.68237694712209,
13.8235269408515));
#440258=CARTESIAN_POINT('Ctrl Pts',(0.0736512963688843,-2.69345232525672,
13.8362179249168));
#440259=CARTESIAN_POINT('Ctrl Pts',(0.0568854566252772,-2.69020122978765,
13.8391868794938));
#440260=CARTESIAN_POINT('Ctrl Pts',(0.0814892059514253,-2.6722434582114,
13.8400110824519));
#440261=CARTESIAN_POINT('Ctrl Pts',(0.0749987388406147,-2.67993733236846,
13.8494522556836));
#440262=CARTESIAN_POINT('Ctrl Pts',(0.0631539172325783,-2.67356331569846,
13.85569149686));
#440263=CARTESIAN_POINT('Ctrl Pts',(0.0928970126972653,-2.66061333906781,
13.8586819406588));
#440264=CARTESIAN_POINT('Ctrl Pts',(0.0885473715845184,-2.66080482229236,
13.868010383617));
#440265=CARTESIAN_POINT('Ctrl Pts',(0.0821953318615578,-2.65435932323096,
13.8744918421245));
#440266=CARTESIAN_POINT('Ctrl Pts',(0.124158896587816,-2.65928438701428,
13.8587686893867));
#440267=CARTESIAN_POINT('Ctrl Pts',(0.128469823458744,-2.65909455173477,
13.8680909899357));
#440268=CARTESIAN_POINT('Ctrl Pts',(0.134237297290658,-2.65214957894116,
13.8745789365163));
#440269=CARTESIAN_POINT('Ctrl Pts',(0.136587174763426,-2.66997797731641,
13.8400379222776));
#440270=CARTESIAN_POINT('Ctrl Pts',(0.143686434594472,-2.67711035025669,
13.8494748685453));
#440271=CARTESIAN_POINT('Ctrl Pts',(0.1549677115719,-2.66979639817705,13.8557104837033));
#440272=CARTESIAN_POINT('Ctrl Pts',(0.141153018311358,-2.67978844069603,
13.8235269408542));
#440273=CARTESIAN_POINT('Ctrl Pts',(0.146135141549828,-2.69049334923498,
13.8362179249195));
#440274=CARTESIAN_POINT('Ctrl Pts',(0.162580199882306,-2.68588649993228,
13.8391868794965));
#440275=CARTESIAN_POINT('Origin',(0.0571083661551944,-2.67475077241381,
13.8235269408515));
#440276=CARTESIAN_POINT('Ctrl Pts',(0.0653472588786357,-2.71592250152398,
13.7902140241683));
#440277=CARTESIAN_POINT('Ctrl Pts',(0.061348351967527,-2.72675612229032,
13.8026027327198));
#440278=CARTESIAN_POINT('Ctrl Pts',(0.0449667433653299,-2.72385425532615,
13.8057746032556));
#440279=CARTESIAN_POINT('Ctrl Pts',(0.0694782524228607,-2.70474430510597,
13.8013225161808));
#440280=CARTESIAN_POINT('Ctrl Pts',(0.0654834323588351,-2.71556684365019,
13.8136962270464));
#440281=CARTESIAN_POINT('Ctrl Pts',(0.0491225158052474,-2.71267564755867,
13.8168830918628));
#440282=CARTESIAN_POINT('Ctrl Pts',(0.0736110268755906,-2.69356128966689,
13.8124254880875));
#440283=CARTESIAN_POINT('Ctrl Pts',(0.0696220545519912,-2.70436798087383,
13.8247886461867));
#440284=CARTESIAN_POINT('Ctrl Pts',(0.0532803842747332,-2.70149215494944,
13.8279860620656));
#440285=CARTESIAN_POINT('Ctrl Pts',(0.0777456543349514,-2.68237326011396,
13.8235227163066));
#440286=CARTESIAN_POINT('Ctrl Pts',(0.0737644137830837,-2.69315900565633,
13.8358800595847));
#440287=CARTESIAN_POINT('Ctrl Pts',(0.0574404327053244,-2.69030357704212,
13.8390832900376));
#440288=CARTESIAN_POINT('Origin',(0.0447099663885099,-2.7083000254968,13.7902182540695));
#440289=CARTESIAN_POINT('Ctrl Pts',(0.0582545094711805,-2.73511493683604,
13.7382347919292));
#440290=CARTESIAN_POINT('Ctrl Pts',(0.0530460535478754,-2.74927791165169,
13.7369371795942));
#440291=CARTESIAN_POINT('Ctrl Pts',(0.0378962811475617,-2.74944576050981,
13.7364597369711));
#440292=CARTESIAN_POINT('Ctrl Pts',(0.0575988118280146,-2.73688921262768,
13.7595490285574));
#440293=CARTESIAN_POINT('Ctrl Pts',(0.0522651429729168,-2.75138975685757,
13.7633824266926));
#440294=CARTESIAN_POINT('Ctrl Pts',(0.0372413290480186,-2.75181245705624,
13.7648920890506));
#440295=CARTESIAN_POINT('Ctrl Pts',(0.0609428338936695,-2.72784050329564,
13.780380659011));
#440296=CARTESIAN_POINT('Ctrl Pts',(0.0563344678206781,-2.74038481866723,
13.7901039518743));
#440297=CARTESIAN_POINT('Ctrl Pts',(0.0405839246479046,-2.73974776985598,
13.7926933640892));
#440298=CARTESIAN_POINT('Ctrl Pts',(0.0667554906511187,-2.71211182652376,
13.7936647693663));
#440299=CARTESIAN_POINT('Ctrl Pts',(0.0630345161656322,-2.7222670065233,
13.8072068914933));
#440300=CARTESIAN_POINT('Ctrl Pts',(0.0463415779082944,-2.71880433671745,
13.8104111085397));
#440301=CARTESIAN_POINT('Origin',(0.0375250635245752,-2.72774189937528,
13.7435492065112));
#440302=CARTESIAN_POINT('Origin',(0.0375250635245752,-2.72774189937529,
14.));
#440303=CARTESIAN_POINT('Origin',(0.0375250635245754,-2.72774189937529,
12.5369868989719));
#440304=CARTESIAN_POINT('Ctrl Pts',(0.0727859135099193,-2.74257229285171,
12.506462012331));
#440305=CARTESIAN_POINT('Ctrl Pts',(0.0729593828180789,-2.749108614171,
12.4999388158272));
#440306=CARTESIAN_POINT('Ctrl Pts',(0.0729573304486722,-2.74903128091793,
12.4907030323752));
#440307=CARTESIAN_POINT('Ctrl Pts',(0.0597703534725135,-2.74518452945416,
12.5042014951932));
#440308=CARTESIAN_POINT('Ctrl Pts',(0.0550548336806712,-2.74955545272149,
12.4980716682127));
#440309=CARTESIAN_POINT('Ctrl Pts',(0.0482645250175523,-2.74968688135409,
12.4907355092743));
#440310=CARTESIAN_POINT('Ctrl Pts',(0.0563857839834866,-2.7401975072345,
12.5218047446509));
#440311=CARTESIAN_POINT('Ctrl Pts',(0.0493635640314674,-2.74969525948866,
12.5216906929434));
#440312=CARTESIAN_POINT('Ctrl Pts',(0.0376005463445374,-2.74974183444874,
12.5161988840776));
#440313=CARTESIAN_POINT('Ctrl Pts',(0.0581742752125333,-2.73533202827181,
12.5369868989719));
#440314=CARTESIAN_POINT('Ctrl Pts',(0.0528853732995049,-2.74972067129591,
12.5369868989719));
#440315=CARTESIAN_POINT('Ctrl Pts',(0.0375554978341709,-2.7497418783242,
12.5369868989719));
#440316=CARTESIAN_POINT('Origin',(2.10137191088009E-32,-1.02994378190383E-30,
12.5));
#440317=CARTESIAN_POINT('Origin',(0.29612422802077,-2.66711467752317,12.5));
#440318=CARTESIAN_POINT('',(0.29612422802077,-2.66711467752317,12.5893111709658));
#440319=CARTESIAN_POINT('',(0.29612422802077,-2.66711467752317,13.8235269408515));
#440320=CARTESIAN_POINT('',(0.29612422802077,-2.66711467752317,12.5));
#440321=CARTESIAN_POINT('',(0.286501658488847,-2.70156288291627,13.7902182540695));
#440322=CARTESIAN_POINT('',(0.29612422802077,-2.66711467752317,13.8235269408515));
#440323=CARTESIAN_POINT('',(0.280925356007127,-2.72152570184805,13.7435492065112));
#440324=CARTESIAN_POINT('Origin',(0.299271631209852,-2.65584837906756,13.7445212918687));
#440325=CARTESIAN_POINT('',(0.280925356007127,-2.72152570184805,12.5369868989719));
#440326=CARTESIAN_POINT('',(0.280925356007127,-2.72152570184805,12.5));
#440327=CARTESIAN_POINT('Ctrl Pts',(0.280925356007127,-2.72152570184805,
12.5369868989719));
#440328=CARTESIAN_POINT('Ctrl Pts',(0.285987951634065,-2.70340192177036,
12.5544431401645));
#440329=CARTESIAN_POINT('Ctrl Pts',(0.29105416816395,-2.68526517908345,
12.5718848856037));
#440330=CARTESIAN_POINT('Ctrl Pts',(0.29612422802077,-2.66711467752317,
12.5893111709658));
#440331=CARTESIAN_POINT('Origin',(0.495082070418079,-2.89839956683834,12.5));
#440332=CARTESIAN_POINT('',(0.387043861680997,-2.70847157094224,13.7435492065112));
#440333=CARTESIAN_POINT('',(0.376795587855615,-2.69045540673698,13.7902182540695));
#440334=CARTESIAN_POINT('Origin',(0.349864895500878,-2.64311204102572,13.7418732680451));
#440335=CARTESIAN_POINT('',(0.359110979140394,-2.65936638433693,13.8235269408515));
#440336=CARTESIAN_POINT('',(0.376795587855615,-2.69045540673698,13.7902182540695));
#440337=CARTESIAN_POINT('',(0.359110979140394,-2.65936638433693,12.5893111709658));
#440338=CARTESIAN_POINT('',(0.359110979140394,-2.65936638433693,12.5));
#440339=CARTESIAN_POINT('',(0.387043861680997,-2.70847157094224,12.5369868989719));
#440340=CARTESIAN_POINT('Ctrl Pts',(0.359110979140394,-2.65936638433693,
12.5893111709658));
#440341=CARTESIAN_POINT('Ctrl Pts',(0.368428867094661,-2.67574695752327,
12.5718848856037));
#440342=CARTESIAN_POINT('Ctrl Pts',(0.377739691682666,-2.69211511351929,
12.5544431401645));
#440343=CARTESIAN_POINT('Ctrl Pts',(0.387043861680997,-2.70847157094224,
12.5369868989719));
#440344=CARTESIAN_POINT('',(0.387043861680997,-2.70847157094224,12.5));
#440345=CARTESIAN_POINT('Origin',(0.329231831327716,-2.67636277074664,12.5));
#440346=CARTESIAN_POINT('',(0.32392598534368,-2.64240046560444,13.8587068136939));
#440347=CARTESIAN_POINT('Ctrl Pts',(0.359110979146066,-2.65936638433354,
13.8235269408542));
#440348=CARTESIAN_POINT('Ctrl Pts',(0.358244572179592,-2.65784326634875,
13.8262006681044));
#440349=CARTESIAN_POINT('Ctrl Pts',(0.35720691500073,-2.65637048136405,
13.8288634856214));
#440350=CARTESIAN_POINT('Ctrl Pts',(0.356011135749757,-2.65494569314718,
13.8314912288862));
#440351=CARTESIAN_POINT('Ctrl Pts',(0.354778410680912,-2.65347688345567,
13.834200161153));
#440352=CARTESIAN_POINT('Ctrl Pts',(0.353376652994714,-2.65205713133551,
13.8368750301949));
#440353=CARTESIAN_POINT('Ctrl Pts',(0.35177642534648,-2.65069496372777,
13.8394886372968));
#440354=CARTESIAN_POINT('Ctrl Pts',(0.351652835883593,-2.65058976021926,
13.8396904925131));
#440355=CARTESIAN_POINT('Ctrl Pts',(0.351528045530105,-2.65048491433332,
13.8398919674349));
#440356=CARTESIAN_POINT('Ctrl Pts',(0.351402032592036,-2.65038043804941,
13.8400930404591));
#440357=CARTESIAN_POINT('Ctrl Pts',(0.349438666239621,-2.64875262725799,
13.8432258934518));
#440358=CARTESIAN_POINT('Ctrl Pts',(0.34718924517456,-2.64722197976263,
13.8462331177034));
#440359=CARTESIAN_POINT('Ctrl Pts',(0.344672864203285,-2.64591817041652,
13.8489036603661));
#440360=CARTESIAN_POINT('Ctrl Pts',(0.343849475064886,-2.64549154882528,
13.8497774930041));
#440361=CARTESIAN_POINT('Ctrl Pts',(0.342997625890127,-2.6450894319766,
13.85061494757));
#440362=CARTESIAN_POINT('Ctrl Pts',(0.342118346408661,-2.64471697886672,
13.8514076489583));
#440363=CARTESIAN_POINT('Ctrl Pts',(0.340258543494292,-2.64392918682355,
13.8530843267192));
#440364=CARTESIAN_POINT('Ctrl Pts',(0.338092186597919,-2.64319944720935,
13.8546805203176));
#440365=CARTESIAN_POINT('Ctrl Pts',(0.335701453210003,-2.6426994205047,
13.8559412814273));
#440366=CARTESIAN_POINT('Ctrl Pts',(0.33538149554936,-2.64263250071536,
13.8561100121513));
#440367=CARTESIAN_POINT('Ctrl Pts',(0.335057579755724,-2.64256964825588,
13.8562727473908));
#440368=CARTESIAN_POINT('Ctrl Pts',(0.334729956459484,-2.64251122098918,
13.8564289040185));
#440369=CARTESIAN_POINT('Ctrl Pts',(0.333244188548769,-2.64224625400127,
13.8571370725437));
#440370=CARTESIAN_POINT('Ctrl Pts',(0.331655656375487,-2.64206987975664,
13.8577210840554));
#440371=CARTESIAN_POINT('Ctrl Pts',(0.330022867864652,-2.64201812275619,
13.8581177131616));
#440372=CARTESIAN_POINT('Ctrl Pts',(0.329563018421135,-2.64200354620344,
13.8582294175695));
#440373=CARTESIAN_POINT('Ctrl Pts',(0.329099698954464,-2.64199868105471,
13.8583265086086));
#440374=CARTESIAN_POINT('Ctrl Pts',(0.328634290461799,-2.64200389873983,
13.8584082369006));
#440375=CARTESIAN_POINT('Ctrl Pts',(0.327965623262051,-2.64201139515416,
13.8585256585398));
#440376=CARTESIAN_POINT('Ctrl Pts',(0.327284334415004,-2.64204012106032,
13.8586122832068));
#440377=CARTESIAN_POINT('Ctrl Pts',(0.326608155097216,-2.64209011922848,
13.8586682984299));
#440378=CARTESIAN_POINT('Ctrl Pts',(0.326067278670486,-2.64213011280685,
13.8587131050557));
#440379=CARTESIAN_POINT('Ctrl Pts',(0.325523680257086,-2.64218392514477,
13.8587357943552));
#440380=CARTESIAN_POINT('Ctrl Pts',(0.324977345153289,-2.6422520666192,
13.8587355499465));
#440381=CARTESIAN_POINT('Ctrl Pts',(0.324624235750512,-2.64229610807868,
13.8587353919793));
#440382=CARTESIAN_POINT('Ctrl Pts',(0.324273796829112,-2.64234562067947,
13.8587257282814));
#440383=CARTESIAN_POINT('Ctrl Pts',(0.32392598534368,-2.64240046560444,
13.8587068136939));
#440384=CARTESIAN_POINT('Ctrl Pts',(0.32392598534368,-2.64240046560444,
13.8587068136939));
#440385=CARTESIAN_POINT('Ctrl Pts',(0.322782052329091,-2.64258084757279,
13.8586446046466));
#440386=CARTESIAN_POINT('Ctrl Pts',(0.321666504916931,-2.64281883916442,
13.858482427929));
#440387=CARTESIAN_POINT('Ctrl Pts',(0.320578113061042,-2.64311014236309,
13.8582284286032));
#440388=CARTESIAN_POINT('Ctrl Pts',(0.319461549623881,-2.64340898555914,
13.8579678548414));
#440389=CARTESIAN_POINT('Ctrl Pts',(0.318371234247498,-2.64376614544504,
13.857615680862));
#440390=CARTESIAN_POINT('Ctrl Pts',(0.317347135427535,-2.64415833304615,
13.8571944833187));
#440391=CARTESIAN_POINT('Ctrl Pts',(0.314791392086088,-2.64513707731437,
13.8561433417727));
#440392=CARTESIAN_POINT('Ctrl Pts',(0.312526782826766,-2.64637527960405,
13.8546163505474));
#440393=CARTESIAN_POINT('Ctrl Pts',(0.310597756934373,-2.64767099406172,
13.8528973491086));
#440394=CARTESIAN_POINT('Ctrl Pts',(0.31024535236395,-2.64790770197666,
13.8525833129072));
#440395=CARTESIAN_POINT('Ctrl Pts',(0.30990402343543,-2.64814626164768,
13.8522628768812));
#440396=CARTESIAN_POINT('Ctrl Pts',(0.3095738727116,-2.64838538181145,13.851937733538));
#440397=CARTESIAN_POINT('Ctrl Pts',(0.307557688047539,-2.64984565547516,
13.8499521282529));
#440398=CARTESIAN_POINT('Ctrl Pts',(0.305760402010941,-2.65147525868192,
13.847639871647));
#440399=CARTESIAN_POINT('Ctrl Pts',(0.304222508197929,-2.65312902749791,
13.8452109780794));
#440400=CARTESIAN_POINT('Ctrl Pts',(0.303530577938638,-2.65387309231953,
13.8441181685877));
#440401=CARTESIAN_POINT('Ctrl Pts',(0.302890493862539,-2.6546217721033,
13.8430021611332));
#440402=CARTESIAN_POINT('Ctrl Pts',(0.302302646188998,-2.65536157698095,
13.8418824960098));
#440403=CARTESIAN_POINT('Ctrl Pts',(0.300917368135071,-2.65710494606673,
13.8392439765549));
#440404=CARTESIAN_POINT('Ctrl Pts',(0.299752986510935,-2.65888001834563,
13.8364981347964));
#440405=CARTESIAN_POINT('Ctrl Pts',(0.298777808206391,-2.66067271862935,
13.8336931113419));
#440406=CARTESIAN_POINT('Ctrl Pts',(0.297828046467313,-2.66241869485869,
13.8309611966328));
#440407=CARTESIAN_POINT('Ctrl Pts',(0.297057298044904,-2.66418341149497,
13.8281701127186));
#440408=CARTESIAN_POINT('Ctrl Pts',(0.296475273110949,-2.66595879825733,
13.8253580685121));
#440409=CARTESIAN_POINT('Ctrl Pts',(0.296349089477127,-2.66634370402347,
13.8247484142932));
#440410=CARTESIAN_POINT('Ctrl Pts',(0.296231943051216,-2.66672906435817,
13.8241378483365));
#440411=CARTESIAN_POINT('Ctrl Pts',(0.29612422802077,-2.66711467752317,
13.8235269408515));
#440412=CARTESIAN_POINT('',(0.325156442858397,-2.64223090392825,12.5969504640361));
#440413=CARTESIAN_POINT('Origin',(0.329235676527349,-2.67639563253677,12.584524458991));
#440414=CARTESIAN_POINT('Origin',(0.329235676527349,-2.67639563253677,12.584524458991));
#440415=CARTESIAN_POINT('Ctrl Pts',(0.359110979140394,-2.65936638433693,
12.5893111709658));
#440416=CARTESIAN_POINT('Ctrl Pts',(0.353507012517157,-2.64951477570456,
12.5770542771492));
#440417=CARTESIAN_POINT('Ctrl Pts',(0.338023477934059,-2.65481230641886,
12.5737548217797));
#440418=CARTESIAN_POINT('Ctrl Pts',(0.371364973398318,-2.6809085461178,
12.5663937883685));
#440419=CARTESIAN_POINT('Ctrl Pts',(0.365753858137378,-2.67104437039046,
12.5540940315304));
#440420=CARTESIAN_POINT('Ctrl Pts',(0.3502233827359,-2.6763613553554,12.5508374392248));
#440421=CARTESIAN_POINT('Ctrl Pts',(0.383606603526242,-2.70242897212149,
12.5434499600945));
#440422=CARTESIAN_POINT('Ctrl Pts',(0.377977244531486,-2.69253272444612,
12.5311293540533));
#440423=CARTESIAN_POINT('Ctrl Pts',(0.362412394711088,-2.69788876912786,
12.5278936106989));
#440424=CARTESIAN_POINT('Ctrl Pts',(0.395836838023433,-2.72392936494126,
12.5204817579905));
#440425=CARTESIAN_POINT('Ctrl Pts',(0.390179617548724,-2.71398413760305,
12.5081597038247));
#440426=CARTESIAN_POINT('Ctrl Pts',(0.374591372548831,-2.71939622248025,
12.5049254088044));
#440427=CARTESIAN_POINT('Ctrl Pts',(0.387043861680996,-2.70847157094224,
12.5369868989719));
#440428=CARTESIAN_POINT('Ctrl Pts',(0.387504435077004,-2.70928124576439,
12.5342545179733));
#440429=CARTESIAN_POINT('Ctrl Pts',(0.387835554575771,-2.7101156419478,
12.5314872231885));
#440430=CARTESIAN_POINT('Ctrl Pts',(0.387966608536756,-2.71094837598063,
12.5287124745063));
#440431=CARTESIAN_POINT('Ctrl Pts',(0.38808479950371,-2.71169937686467,
12.5262100684184));
#440432=CARTESIAN_POINT('Ctrl Pts',(0.388039179685566,-2.71244842103555,
12.5237004536639));
#440433=CARTESIAN_POINT('Ctrl Pts',(0.387762797762829,-2.71320434008162,
12.5212220730815));
#440434=CARTESIAN_POINT('Ctrl Pts',(0.387551203492031,-2.7137830615036,
12.5193246583486));
#440435=CARTESIAN_POINT('Ctrl Pts',(0.387201229463953,-2.7143725110797,
12.517417831369));
#440436=CARTESIAN_POINT('Ctrl Pts',(0.386621118841982,-2.71494052196848,
12.5155812248348));
#440437=CARTESIAN_POINT('Ctrl Pts',(0.386373988598914,-2.71518249766018,
12.5147988205793));
#440438=CARTESIAN_POINT('Ctrl Pts',(0.386085035971748,-2.71542102622447,
12.5140295443047));
#440439=CARTESIAN_POINT('Ctrl Pts',(0.385747539544028,-2.7156557151976,
12.5132817086137));
#440440=CARTESIAN_POINT('Ctrl Pts',(0.385236784356158,-2.71601088521044,
12.5121499604604));
#440441=CARTESIAN_POINT('Ctrl Pts',(0.384599738239009,-2.71635905953673,
12.5110494206568));
#440442=CARTESIAN_POINT('Ctrl Pts',(0.38380897549223,-2.71667504433384,
12.5100666561695));
#440443=CARTESIAN_POINT('Ctrl Pts',(0.383354921343995,-2.7168564820767,
12.5095023550641));
#440444=CARTESIAN_POINT('Ctrl Pts',(0.382844697971814,-2.717028797038,12.5089719619137));
#440445=CARTESIAN_POINT('Ctrl Pts',(0.382285825309685,-2.71718270816325,
12.5085043804652));
#440446=CARTESIAN_POINT('Ctrl Pts',(0.381467987966943,-2.71740793704672,
12.5078201359221));
#440447=CARTESIAN_POINT('Ctrl Pts',(0.380521929851842,-2.71759912296043,
12.5072563000953));
#440448=CARTESIAN_POINT('Ctrl Pts',(0.379510102780157,-2.71773500807132,
12.5068768744336));
#440449=CARTESIAN_POINT('Ctrl Pts',(0.378780505807059,-2.71783299059064,
12.5066032824118));
#440450=CARTESIAN_POINT('Ctrl Pts',(0.378003902977509,-2.71790400092369,
12.5064197834844));
#440451=CARTESIAN_POINT('Ctrl Pts',(0.377223897181221,-2.71794664778805,
12.5063282718343));
#440452=CARTESIAN_POINT('Ctrl Pts',(0.376085330202333,-2.71800889900688,
12.5061946931565));
#440453=CARTESIAN_POINT('Ctrl Pts',(0.374915235005781,-2.71801310744814,
12.5062515701262));
#440454=CARTESIAN_POINT('Ctrl Pts',(0.373786285379937,-2.7179744763593,
12.5064436508398));
#440455=CARTESIAN_POINT('',(0.338023477934059,-2.65481230641886,12.5737548217797));
#440456=CARTESIAN_POINT('Origin',(0.33998832454028,-2.67024407163914,12.5893111709658));
#440457=CARTESIAN_POINT('Ctrl Pts',(0.373786285379937,-2.7179744763593,
12.5064436508398));
#440458=CARTESIAN_POINT('Ctrl Pts',(0.368492042661514,-2.70862507093491,
12.5164271754438));
#440459=CARTESIAN_POINT('Ctrl Pts',(0.363195883116453,-2.6992718564557,
12.5264061185523));
#440460=CARTESIAN_POINT('Ctrl Pts',(0.357897738412111,-2.68991469923633,
12.536380305637));
#440461=CARTESIAN_POINT('Ctrl Pts',(0.351276132111214,-2.6782201505481,
12.5488460165097));
#440462=CARTESIAN_POINT('Ctrl Pts',(0.344651423070526,-2.66651943986077,
12.5613043021964));
#440463=CARTESIAN_POINT('Ctrl Pts',(0.338023477934059,-2.65481230641886,
12.5737548217797));
#440464=CARTESIAN_POINT('Ctrl Pts',(0.296124228020771,-2.66711467752317,
12.5893111709658));
#440465=CARTESIAN_POINT('Ctrl Pts',(0.299173464752837,-2.65619859810282,
12.5770542771492));
#440466=CARTESIAN_POINT('Ctrl Pts',(0.315479291294226,-2.65758557166315,
12.5737548217797));
#440467=CARTESIAN_POINT('Ctrl Pts',(0.298969139370926,-2.65693007036703,
12.5928319619712));
#440468=CARTESIAN_POINT('Ctrl Pts',(0.3041560453713,-2.65047023890524,12.5821634970842));
#440469=CARTESIAN_POINT('Ctrl Pts',(0.316506532791419,-2.65387302640742,
12.5773203894503));
#440470=CARTESIAN_POINT('Ctrl Pts',(0.309793997178513,-2.64414701311201,
12.5969440695591));
#440471=CARTESIAN_POINT('Ctrl Pts',(0.313781419854935,-2.64363808978626,
12.5878292599214));
#440472=CARTESIAN_POINT('Ctrl Pts',(0.32036629436647,-2.64931820613859,
12.5813877129824));
#440473=CARTESIAN_POINT('Ctrl Pts',(0.340155435950474,-2.64035778083647,
12.596957478804));
#440474=CARTESIAN_POINT('Ctrl Pts',(0.336197491545416,-2.6408630225958,
12.5878468778671));
#440475=CARTESIAN_POINT('Ctrl Pts',(0.331233812914824,-2.64796790657724,
12.5814011370086));
#440476=CARTESIAN_POINT('Ctrl Pts',(0.353874935318227,-2.65016157317609,
12.5928371701607));
#440477=CARTESIAN_POINT('Ctrl Pts',(0.347278122829823,-2.64515986039979,
12.5821692192952));
#440478=CARTESIAN_POINT('Ctrl Pts',(0.336121239852369,-2.65144856330225,
12.5773318885715));
#440479=CARTESIAN_POINT('Ctrl Pts',(0.35911097914044,-2.6593663843369,12.5893111709658));
#440480=CARTESIAN_POINT('Ctrl Pts',(0.353507012517204,-2.64951477570453,
12.5770542771492));
#440481=CARTESIAN_POINT('Ctrl Pts',(0.338023477934106,-2.65481230641883,
12.5737548217797));
#440482=CARTESIAN_POINT('',(0.315479291294226,-2.65758557166315,12.5737548217797));
#440483=CARTESIAN_POINT('Origin',(0.317313094137216,-2.67303345718619,12.5893111709658));
#440484=CARTESIAN_POINT('Ctrl Pts',(0.338023477934106,-2.65481230641883,
12.5737548217797));
#440485=CARTESIAN_POINT('Ctrl Pts',(0.337556645505732,-2.6539255217128,
12.5746934679442));
#440486=CARTESIAN_POINT('Ctrl Pts',(0.336877969031576,-2.65302956765055,
12.5756680099006));
#440487=CARTESIAN_POINT('Ctrl Pts',(0.336067317050609,-2.65222436765443,
12.5765688348656));
#440488=CARTESIAN_POINT('Ctrl Pts',(0.335852705912866,-2.65201119986932,
12.5768073183026));
#440489=CARTESIAN_POINT('Ctrl Pts',(0.335629065156764,-2.65180425992053,
12.5770407398754));
#440490=CARTESIAN_POINT('Ctrl Pts',(0.335398270313362,-2.65160499907852,
12.5772674179684));
#440491=CARTESIAN_POINT('Ctrl Pts',(0.334451150685588,-2.6507872864653,
12.5781976435658));
#440492=CARTESIAN_POINT('Ctrl Pts',(0.333322386389675,-2.65006098856013,
12.5790594849312));
#440493=CARTESIAN_POINT('Ctrl Pts',(0.332062063732868,-2.6495157551015,
12.5797571720116));
#440494=CARTESIAN_POINT('Ctrl Pts',(0.331240918204794,-2.64916051589835,
12.580211740231));
#440495=CARTESIAN_POINT('Ctrl Pts',(0.330319155586716,-2.64888322425361,
12.5806009430798));
#440496=CARTESIAN_POINT('Ctrl Pts',(0.329356560222978,-2.64872036594087,
12.5808812374708));
#440497=CARTESIAN_POINT('Ctrl Pts',(0.328529371467841,-2.64858041662254,
12.5811221033394));
#440498=CARTESIAN_POINT('Ctrl Pts',(0.327655075930601,-2.64852221811518,
12.581287365893));
#440499=CARTESIAN_POINT('Ctrl Pts',(0.326782466458639,-2.64855737480574,
12.581359338449));
#440500=CARTESIAN_POINT('Ctrl Pts',(0.326661191760731,-2.64856226085977,
12.5813693411482));
#440501=CARTESIAN_POINT('Ctrl Pts',(0.326539927416732,-2.6485688944887,
12.5813775999465));
#440502=CARTESIAN_POINT('Ctrl Pts',(0.326418780645168,-2.64857725029061,
12.5813841266931));
#440503=CARTESIAN_POINT('Ctrl Pts',(0.326213240494816,-2.64859142691917,
12.5813952001081));
#440504=CARTESIAN_POINT('Ctrl Pts',(0.326006704065679,-2.64861126323816,
12.5814007534795));
#440505=CARTESIAN_POINT('Ctrl Pts',(0.32579928016492,-2.6486369469147,12.5814005856065));
#440506=CARTESIAN_POINT('Ctrl Pts',(0.324849774644737,-2.64875451674426,
12.5813998171494));
#440507=CARTESIAN_POINT('Ctrl Pts',(0.32394723466203,-2.64898615694003,
12.58127954464));
#440508=CARTESIAN_POINT('Ctrl Pts',(0.323089428437419,-2.64930189193674,
12.5810700125799));
#440509=CARTESIAN_POINT('Ctrl Pts',(0.322053296187149,-2.64968326386346,
12.5808169217085));
#440510=CARTESIAN_POINT('Ctrl Pts',(0.321088117233356,-2.65020306954505,
12.5804173076348));
#440511=CARTESIAN_POINT('Ctrl Pts',(0.320266129817922,-2.65079282547467,
12.5799304713245));
#440512=CARTESIAN_POINT('Ctrl Pts',(0.31924742845746,-2.65152371886375,
12.5793271277669));
#440513=CARTESIAN_POINT('Ctrl Pts',(0.318366692047735,-2.65238122465672,
12.5785808224116));
#440514=CARTESIAN_POINT('Ctrl Pts',(0.317638919818751,-2.65330647243203,
12.5777485681082));
#440515=CARTESIAN_POINT('Ctrl Pts',(0.316554459464165,-2.65468519298571,
12.576508418016));
#440516=CARTESIAN_POINT('Ctrl Pts',(0.315813374667285,-2.65619847182142,
12.5750928681475));
#440517=CARTESIAN_POINT('Ctrl Pts',(0.315479291294226,-2.65758557166315,
12.5737548217797));
#440518=CARTESIAN_POINT('Ctrl Pts',(0.315479291294226,-2.65758557166315,
12.5737548217797));
#440519=CARTESIAN_POINT('Ctrl Pts',(0.299173464752836,-2.65619859810282,
12.5770542771492));
#440520=CARTESIAN_POINT('Ctrl Pts',(0.29612422802077,-2.66711467752317,
12.5893111709658));
#440521=CARTESIAN_POINT('Ctrl Pts',(0.308866773504334,-2.68144536132376,
12.5508408821982));
#440522=CARTESIAN_POINT('Ctrl Pts',(0.292510699128997,-2.6800508880691,
12.55409748406));
#440523=CARTESIAN_POINT('Ctrl Pts',(0.289457572351812,-2.69098089361103,
12.5663972313419));
#440524=CARTESIAN_POINT('Ctrl Pts',(0.302259578642799,-2.70528152795879,
12.52790050457));
#440525=CARTESIAN_POINT('Ctrl Pts',(0.285860694287199,-2.70385749522283,
12.5311362602938));
#440526=CARTESIAN_POINT('Ctrl Pts',(0.282797642242939,-2.71482303260862,
12.5434568539655));
#440527=CARTESIAN_POINT('Ctrl Pts',(0.295657279704717,-2.72909590368206,
12.5049357605811));
#440528=CARTESIAN_POINT('Ctrl Pts',(0.279222119981116,-2.72762318176361,
12.5081700652078));
#440529=CARTESIAN_POINT('Ctrl Pts',(0.276143910946933,-2.7386429802385,
12.5204921097672));
#440530=CARTESIAN_POINT('Ctrl Pts',(0.29609081100377,-2.72753215799855,
12.5064436508395));
#440531=CARTESIAN_POINT('Ctrl Pts',(0.294917811967386,-2.7278681952751,
12.5062361689309));
#440532=CARTESIAN_POINT('Ctrl Pts',(0.293683659583299,-2.72816762725951,
12.5061871075061));
#440533=CARTESIAN_POINT('Ctrl Pts',(0.29247468096164,-2.72838985987073,
12.5063648335164));
#440534=CARTESIAN_POINT('Ctrl Pts',(0.291925488298788,-2.72849081163062,
12.5064455676329));
#440535=CARTESIAN_POINT('Ctrl Pts',(0.291373790408432,-2.72857702439911,
12.506574497099));
#440536=CARTESIAN_POINT('Ctrl Pts',(0.290843080180768,-2.72864376328366,
12.5067492519495));
#440537=CARTESIAN_POINT('Ctrl Pts',(0.289776597377541,-2.72877787766278,
12.5071004286051));
#440538=CARTESIAN_POINT('Ctrl Pts',(0.288755556318065,-2.72883748074164,
12.5076537929613));
#440539=CARTESIAN_POINT('Ctrl Pts',(0.287857142685456,-2.72882754136973,
12.5083435010505));
#440540=CARTESIAN_POINT('Ctrl Pts',(0.28780058217834,-2.72882691562687,
12.5083869222964));
#440541=CARTESIAN_POINT('Ctrl Pts',(0.287744501663466,-2.72882600225326,
12.5084308732337));
#440542=CARTESIAN_POINT('Ctrl Pts',(0.287688917589329,-2.72882479777907,
12.5084753333615));
#440543=CARTESIAN_POINT('Ctrl Pts',(0.287243059950386,-2.72881513630635,
12.5088319622689));
#440544=CARTESIAN_POINT('Ctrl Pts',(0.286820064496226,-2.72878783860156,
12.509227847131));
#440545=CARTESIAN_POINT('Ctrl Pts',(0.286432328762188,-2.72874651060836,
12.5096423454524));
#440546=CARTESIAN_POINT('Ctrl Pts',(0.285217336576357,-2.72861700696867,
12.5109411997424));
#440547=CARTESIAN_POINT('Ctrl Pts',(0.284272811451165,-2.72835138622861,
12.5124831113042));
#440548=CARTESIAN_POINT('Ctrl Pts',(0.283538688913669,-2.72802277920583,
12.5140723025008));
#440549=CARTESIAN_POINT('Ctrl Pts',(0.283469900827844,-2.72799198836788,
12.5142212114565));
#440550=CARTESIAN_POINT('Ctrl Pts',(0.283402934418785,-2.72796065932985,
12.5143705582413));
#440551=CARTESIAN_POINT('Ctrl Pts',(0.28333772640274,-2.72792886205536,
12.5145201959299));
#440552=CARTESIAN_POINT('Ctrl Pts',(0.28250003235206,-2.72752037872336,
12.5164425148273));
#440553=CARTESIAN_POINT('Ctrl Pts',(0.281919120930104,-2.72703027700005,
12.518463520594));
#440554=CARTESIAN_POINT('Ctrl Pts',(0.281509833556556,-2.72648832254934,
12.5205025929157));
#440555=CARTESIAN_POINT('Ctrl Pts',(0.281272430657261,-2.72617396748687,
12.5216853356836));
#440556=CARTESIAN_POINT('Ctrl Pts',(0.281092812947214,-2.7258430260528,
12.5228750347131));
#440557=CARTESIAN_POINT('Ctrl Pts',(0.280956636803638,-2.72550677628481,
12.5240609649613));
#440558=CARTESIAN_POINT('Ctrl Pts',(0.280622399764832,-2.72468146926846,
12.5269717671326));
#440559=CARTESIAN_POINT('Ctrl Pts',(0.280550096819154,-2.72379705348828,
12.5299036066169));
#440560=CARTESIAN_POINT('Ctrl Pts',(0.280655617589308,-2.72287438480819,
12.5328133004019));
#440561=CARTESIAN_POINT('Ctrl Pts',(0.280706273703273,-2.72243145011636,
12.5342101228451));
#440562=CARTESIAN_POINT('Ctrl Pts',(0.280798367822096,-2.72198031202227,
12.5356023438238));
#440563=CARTESIAN_POINT('Ctrl Pts',(0.280925356007128,-2.72152570184805,
12.5369868989719));
#440564=CARTESIAN_POINT('Origin',(-3.15300310277255,-14.9950921493851,-1.23957475124779));
#440565=CARTESIAN_POINT('Ctrl Pts',(0.387023231424868,-2.70843522326725,
12.5369868989719));
#440566=CARTESIAN_POINT('Ctrl Pts',(0.394582083106558,-2.72178239768519,
12.5369868989719));
#440567=CARTESIAN_POINT('Ctrl Pts',(0.409719655703063,-2.71930506049086,
12.5369868989719));
#440568=CARTESIAN_POINT('Ctrl Pts',(0.389578476532465,-2.71294705759693,
12.5218025310015));
#440569=CARTESIAN_POINT('Ctrl Pts',(0.398053920948921,-2.72118251178293,
12.5216901060418));
#440570=CARTESIAN_POINT('Ctrl Pts',(0.409673514028607,-2.71931262851088,
12.5161920673677));
#440571=CARTESIAN_POINT('Ctrl Pts',(0.387050922869208,-2.71841949249145,
12.5042015548895));
#440572=CARTESIAN_POINT('Ctrl Pts',(0.392416833525845,-2.72196693492833,
12.4980677368514));
#440573=CARTESIAN_POINT('Ctrl Pts',(0.399142794376768,-2.72099111201602,
12.4907278922778));
#440574=CARTESIAN_POINT('Ctrl Pts',(0.373783560391716,-2.71795466177511,
12.5064636261921));
#440575=CARTESIAN_POINT('Ctrl Pts',(0.374674953142716,-2.72443639435991,
12.4999376786892));
#440576=CARTESIAN_POINT('Ctrl Pts',(0.374664066076346,-2.72435722942082,
12.4906970594712));
#440577=CARTESIAN_POINT('Origin',(0.40616651628111,-2.69759388364003,12.5369868989719));
#440578=CARTESIAN_POINT('Origin',(0.406166516281111,-2.69759388364003,14.));
#440579=CARTESIAN_POINT('Origin',(0.40616651628111,-2.69759388364003,13.7435492065112));
#440580=CARTESIAN_POINT('Ctrl Pts',(0.374801491253232,-2.68694978859957,
13.793642941384));
#440581=CARTESIAN_POINT('Ctrl Pts',(0.380123858796038,-2.69636141028476,
13.8071662555867));
#440582=CARTESIAN_POINT('Ctrl Pts',(0.396019064765778,-2.69024897944144,
13.8103758687955));
#440583=CARTESIAN_POINT('Ctrl Pts',(0.383019641876292,-2.70139706189109,
13.7804579775006));
#440584=CARTESIAN_POINT('Ctrl Pts',(0.389595789456672,-2.71300516056098,
13.7901904343351));
#440585=CARTESIAN_POINT('Ctrl Pts',(0.405023278151095,-2.7098038300957,
13.7927914348262));
#440586=CARTESIAN_POINT('Ctrl Pts',(0.387857976464934,-2.70990271537105,
13.7597120340895));
#440587=CARTESIAN_POINT('Ctrl Pts',(0.395473417080355,-2.72333373000905,
13.7635825532445));
#440588=CARTESIAN_POINT('Ctrl Pts',(0.4103562716347,-2.72132461168045,13.7651073818884));
#440589=CARTESIAN_POINT('Ctrl Pts',(0.386910519767921,-2.70823711366196,
13.7381884353898));
#440590=CARTESIAN_POINT('Ctrl Pts',(0.394346924916404,-2.72135419371408,
13.7368803041981));
#440591=CARTESIAN_POINT('Ctrl Pts',(0.409312361550093,-2.71906829269215,
13.7363986145813));
#440592=CARTESIAN_POINT('Origin',(0.395918242455728,-2.67957771943477,13.7902182540695));
#440593=CARTESIAN_POINT('Ctrl Pts',(0.359109033584807,-2.65936296257247,
13.8235227101244));
#440594=CARTESIAN_POINT('Ctrl Pts',(0.364789796185102,-2.66935854282569,
13.8358800583119));
#440595=CARTESIAN_POINT('Ctrl Pts',(0.380432939137515,-2.66388879624773,
13.8390832900376));
#440596=CARTESIAN_POINT('Ctrl Pts',(0.365006509881553,-2.66973055258288,
13.8124254819052));
#440597=CARTESIAN_POINT('Ctrl Pts',(0.370698304684128,-2.67974554397383,
13.8247886449158));
#440598=CARTESIAN_POINT('Ctrl Pts',(0.386355587722459,-2.67425279703263,
13.8279860620657));
#440599=CARTESIAN_POINT('Ctrl Pts',(0.370901343121275,-2.68009349617674,
13.8013225099955));
#440600=CARTESIAN_POINT('Ctrl Pts',(0.376601482770181,-2.6901231742282,
13.8136962257787));
#440601=CARTESIAN_POINT('Ctrl Pts',(0.392275259073256,-2.68461213428257,
13.8168830918626));
#440602=CARTESIAN_POINT('Ctrl Pts',(0.376793636141255,-2.69045197413897,
13.7902140179785));
#440603=CARTESIAN_POINT('Ctrl Pts',(0.382499608921472,-2.7004919231516,
13.802602731458));
#440604=CARTESIAN_POINT('Ctrl Pts',(0.39819206857489,-2.69496699215227,
13.8057746032558));
#440605=CARTESIAN_POINT('Origin',(0.378233633740507,-2.64848869703471,13.8235269408515));
#440606=CARTESIAN_POINT('Ctrl Pts',(0.29612422802077,-2.66711467752317,
13.8235269408515));
#440607=CARTESIAN_POINT('Ctrl Pts',(0.292947597055868,-2.67848682043926,
13.8362179249168));
#440608=CARTESIAN_POINT('Ctrl Pts',(0.275972549798502,-2.67661311430774,
13.8391868794938));
#440609=CARTESIAN_POINT('Ctrl Pts',(0.299030707083143,-2.65670966175486,
13.8400110824519));
#440610=CARTESIAN_POINT('Ctrl Pts',(0.293188958636471,-2.6649069685045,
13.8494522556837));
#440611=CARTESIAN_POINT('Ctrl Pts',(0.280864008163117,-2.6595196237721,
13.85569149686));
#440612=CARTESIAN_POINT('Ctrl Pts',(0.309452592614156,-2.6441883987186,
13.8586819406588));
#440613=CARTESIAN_POINT('Ctrl Pts',(0.305133032233838,-2.6447337809293,
13.868010383617));
#440614=CARTESIAN_POINT('Ctrl Pts',(0.298276760388452,-2.6388274789412,
13.8744918421245));
#440615=CARTESIAN_POINT('Ctrl Pts',(0.340502133235233,-2.64031573488514,
13.8587686893867));
#440616=CARTESIAN_POINT('Ctrl Pts',(0.344783242515,-2.63977515070619,13.8680909899357));
#440617=CARTESIAN_POINT('Ctrl Pts',(0.349965445796858,-2.63238318407672,
13.8745789365163));
#440618=CARTESIAN_POINT('Ctrl Pts',(0.353760684224538,-2.64996072309787,
13.8400379222776));
#440619=CARTESIAN_POINT('Ctrl Pts',(0.361417676462514,-2.65649070807303,
13.8494748685453));
#440620=CARTESIAN_POINT('Ctrl Pts',(0.372065260927524,-2.64828156376166,
13.8557104837033));
#440621=CARTESIAN_POINT('Ctrl Pts',(0.359110979146066,-2.65936638433354,
13.8235269408542));
#440622=CARTESIAN_POINT('Ctrl Pts',(0.364949074205902,-2.6696295838767,
13.8362179249195));
#440623=CARTESIAN_POINT('Ctrl Pts',(0.380963911977324,-2.66369763856245,
13.8391868794965));
#440624=CARTESIAN_POINT('Origin',(0.274935361904325,-2.66119589786016,13.8235269408515));
#440625=CARTESIAN_POINT('Ctrl Pts',(0.286502718534059,-2.70155908519502,
13.7902140241682));
#440626=CARTESIAN_POINT('Ctrl Pts',(0.28340015832271,-2.71268260601928,
13.8026027327198));
#440627=CARTESIAN_POINT('Ctrl Pts',(0.266836529074531,-2.71112564795856,
13.8057746032556));
#440628=CARTESIAN_POINT('Ctrl Pts',(0.289708839756668,-2.69008136897932,
13.8013225161808));
#440629=CARTESIAN_POINT('Ctrl Pts',(0.286609449489767,-2.70119351134068,
13.8136962270464));
#440630=CARTESIAN_POINT('Ctrl Pts',(0.270067313214294,-2.6996455020521,
13.8168830918628));
#440631=CARTESIAN_POINT('Ctrl Pts',(0.292916343166988,-2.67859870461692,
13.8124254880875));
#440632=CARTESIAN_POINT('Ctrl Pts',(0.289821489477539,-2.68969457572655,
13.8247886461868));
#440633=CARTESIAN_POINT('Ctrl Pts',(0.273299788249313,-2.6881603167119,
13.8279860620656));
#440634=CARTESIAN_POINT('Ctrl Pts',(0.29612528472141,-2.66711089178739,
13.8235227163065));
#440635=CARTESIAN_POINT('Ctrl Pts',(0.293036429810745,-2.67818525671626,
13.8358800595847));
#440636=CARTESIAN_POINT('Ctrl Pts',(0.276534021492804,-2.67666988530749,
13.8390832900376));
#440637=CARTESIAN_POINT('Origin',(0.265312792372402,-2.69564410325325,13.7902182540695));
#440638=CARTESIAN_POINT('Ctrl Pts',(0.280997931316952,-2.72126578418443,
13.7382347919292));
#440639=CARTESIAN_POINT('Ctrl Pts',(0.276961220031182,-2.73580617038043,
13.7369371795942));
#440640=CARTESIAN_POINT('Ctrl Pts',(0.261875538488943,-2.73720830782959,
13.7364597369712));
#440641=CARTESIAN_POINT('Ctrl Pts',(0.280489035402188,-2.72308760166488,
13.7595490285574));
#440642=CARTESIAN_POINT('Ctrl Pts',(0.276355042861444,-2.7379746400571,
13.7633824266926));
#440643=CARTESIAN_POINT('Ctrl Pts',(0.261415673428344,-2.73962051406489,
13.7648920890506));
#440644=CARTESIAN_POINT('Ctrl Pts',(0.283084376695607,-2.71379643232392,
13.780380659011));
#440645=CARTESIAN_POINT('Ctrl Pts',(0.27951382273908,-2.72667463213789,
13.7901039518744));
#440646=CARTESIAN_POINT('Ctrl Pts',(0.263763762807191,-2.72732351854348,
13.7926933640892));
#440647=CARTESIAN_POINT('Ctrl Pts',(0.287595659142386,-2.69764630593868,
13.7936647693663));
#440648=CARTESIAN_POINT('Ctrl Pts',(0.284714807338599,-2.70807098937891,
13.8072068914933));
#440649=CARTESIAN_POINT('Ctrl Pts',(0.267795173721219,-2.70598047075885,
13.8104111085397));
#440650=CARTESIAN_POINT('Origin',(0.259736489890682,-2.71560692218503,13.7435492065112));
#440651=CARTESIAN_POINT('Origin',(0.259736489890682,-2.71560692218504,14.));
#440652=CARTESIAN_POINT('Origin',(0.259736489890682,-2.71560692218504,12.5369868989719));
#440653=CARTESIAN_POINT('Ctrl Pts',(0.296088827053501,-2.72751388213103,
12.506462012331));
#440654=CARTESIAN_POINT('Ctrl Pts',(0.296794490024615,-2.7340143150213,
12.4999388158272));
#440655=CARTESIAN_POINT('Ctrl Pts',(0.296786141106247,-2.73393740637542,
12.4907030323752));
#440656=CARTESIAN_POINT('Ctrl Pts',(0.283329496752321,-2.73117831570525,
12.5042014951932));
#440657=CARTESIAN_POINT('Ctrl Pts',(0.278985938287572,-2.73591905372581,
12.4980716682127));
#440658=CARTESIAN_POINT('Ctrl Pts',(0.272228936470035,-2.73660351823466,
12.4907355092744));
#440659=CARTESIAN_POINT('Ctrl Pts',(0.279549700530896,-2.72648376122487,
12.5218047446509));
#440660=CARTESIAN_POINT('Ctrl Pts',(0.273325001417991,-2.7365222866091,
12.5216906929433));
#440661=CARTESIAN_POINT('Ctrl Pts',(0.2616049204937,-2.73752750173883,12.5161988840775));
#440662=CARTESIAN_POINT('Ctrl Pts',(0.280935658998568,-2.72148869310332,
12.5369868989719));
#440663=CARTESIAN_POINT('Ctrl Pts',(0.27683716345445,-2.7362605537104,12.5369868989719));
#440664=CARTESIAN_POINT('Ctrl Pts',(0.2615600254548,-2.7375312173401,12.5369868989719));
#440665=CARTESIAN_POINT('Origin',(6.2901314492746E-32,-1.0265181555254E-30,
12.5));
#440666=CARTESIAN_POINT('Origin',(0.512533505583331,-2.63410319978829,12.5));
#440667=CARTESIAN_POINT('',(0.512533505583331,-2.63410319978829,12.5893111709658));
#440668=CARTESIAN_POINT('',(0.512533505583331,-2.63410319978829,13.8235269408515));
#440669=CARTESIAN_POINT('',(0.512533505583331,-2.63410319978829,12.5));
#440670=CARTESIAN_POINT('',(0.505750802898792,-2.66922111036814,13.7902182540695));
#440671=CARTESIAN_POINT('',(0.512533505583331,-2.63410319978829,13.8235269408515));
#440672=CARTESIAN_POINT('',(0.501820210172278,-2.68957202508688,13.7435492065112));
#440673=CARTESIAN_POINT('Origin',(0.514752128131608,-2.62261784643754,13.7445212918704));
#440674=CARTESIAN_POINT('',(0.501820210172278,-2.68957202508688,12.5369868989719));
#440675=CARTESIAN_POINT('',(0.501820210172278,-2.68957202508688,12.5));
#440676=CARTESIAN_POINT('Ctrl Pts',(0.501820210172278,-2.68957202508688,
12.5369868989719));
#440677=CARTESIAN_POINT('Ctrl Pts',(0.505388704100603,-2.67109590184984,
12.5544431401645));
#440678=CARTESIAN_POINT('Ctrl Pts',(0.508959750310632,-2.6526065639984,
12.5718848856037));
#440679=CARTESIAN_POINT('Ctrl Pts',(0.512533505583331,-2.63410319978829,
12.5893111709658));
#440680=CARTESIAN_POINT('Origin',(0.729681197796271,-2.84840159652405,12.5));
#440681=CARTESIAN_POINT('',(0.606521582415215,-2.6679116873562,13.7435492065112));
#440682=CARTESIAN_POINT('',(0.594838924238927,-2.65079079990821,13.7902182540695));
#440683=CARTESIAN_POINT('Origin',(0.564138917721049,-2.60580006677933,13.7418732680446));
#440684=CARTESIAN_POINT('',(0.574679115658322,-2.62124668345171,13.8235269408515));
#440685=CARTESIAN_POINT('',(0.594838924238927,-2.65079079990821,13.7902182540695));
#440686=CARTESIAN_POINT('',(0.574679115658322,-2.62124668345171,12.5893111709658));
#440687=CARTESIAN_POINT('',(0.574679115658322,-2.62124668345171,12.5));
#440688=CARTESIAN_POINT('',(0.606521582415215,-2.6679116873562,12.5369868989719));
#440689=CARTESIAN_POINT('Ctrl Pts',(0.574679115658322,-2.62124668345171,
12.5893111709658));
#440690=CARTESIAN_POINT('Ctrl Pts',(0.585301167893602,-2.63681325726075,
12.5718848856037));
#440691=CARTESIAN_POINT('Ctrl Pts',(0.595915168149101,-2.65236803092658,
12.5544431401645));
#440692=CARTESIAN_POINT('Ctrl Pts',(0.606521582415215,-2.6679116873562,
12.5369868989719));
#440693=CARTESIAN_POINT('',(0.606521582415216,-2.6679116873562,12.5));
#440694=CARTESIAN_POINT('Origin',(0.546284751524279,-2.64062194371896,12.5));
#440695=CARTESIAN_POINT('',(0.538228317145139,-2.60720512105024,13.8587068136939));
#440696=CARTESIAN_POINT('Ctrl Pts',(0.574679115663699,-2.62124668344787,
13.8235269408542));
#440697=CARTESIAN_POINT('Ctrl Pts',(0.573691443339235,-2.61979925372363,
13.8262006681044));
#440698=CARTESIAN_POINT('Ctrl Pts',(0.572537193230111,-2.61841594800268,
13.8288634856214));
#440699=CARTESIAN_POINT('Ctrl Pts',(0.571229259369184,-2.61709336776109,
13.8314912288862));
#440700=CARTESIAN_POINT('Ctrl Pts',(0.569880914465689,-2.61572992394984,
13.8342001611531));
#440701=CARTESIAN_POINT('Ctrl Pts',(0.568368098034423,-2.61442915220244,
13.8368750301949));
#440702=CARTESIAN_POINT('Ctrl Pts',(0.566662165705898,-2.61320195050416,
13.8394886372969));
#440703=CARTESIAN_POINT('Ctrl Pts',(0.566530412414152,-2.61310717074023,
13.8396904925131));
#440704=CARTESIAN_POINT('Ctrl Pts',(0.56639749137723,-2.61301284529263,
13.8398919674349));
#440705=CARTESIAN_POINT('Ctrl Pts',(0.566263381949771,-2.61291898786924,
13.8400930404591));
#440706=CARTESIAN_POINT('Ctrl Pts',(0.56417386684557,-2.61145662606867,
13.8432258934518));
#440707=CARTESIAN_POINT('Ctrl Pts',(0.561807168562829,-2.61011442037599,
13.8462331177034));
#440708=CARTESIAN_POINT('Ctrl Pts',(0.559192888075967,-2.60902005775802,
13.8489036603661));
#440709=CARTESIAN_POINT('Ctrl Pts',(0.558337465076753,-2.60866196957368,
13.8497774930041));
#440710=CARTESIAN_POINT('Ctrl Pts',(0.557455674103611,-2.60833062435157,
13.85061494757));
#440711=CARTESIAN_POINT('Ctrl Pts',(0.556548961965943,-2.60803107998926,
13.8514076489583));
#440712=CARTESIAN_POINT('Ctrl Pts',(0.554631135027298,-2.60739750046221,
13.8530843267192));
#440713=CARTESIAN_POINT('Ctrl Pts',(0.552412505951619,-2.6068467671949,
13.8546805203176));
#440714=CARTESIAN_POINT('Ctrl Pts',(0.549988970713338,-2.60654327125346,
13.8559412814274));
#440715=CARTESIAN_POINT('Ctrl Pts',(0.549664623101367,-2.60650265365389,
13.8561100121513));
#440716=CARTESIAN_POINT('Ctrl Pts',(0.549336662051907,-2.60646641247506,
13.8562727473908));
#440717=CARTESIAN_POINT('Ctrl Pts',(0.549005366530546,-2.60643488396042,
13.8564289040185));
#440718=CARTESIAN_POINT('Ctrl Pts',(0.547502945120647,-2.60629190250622,
13.8571370725437));
#440719=CARTESIAN_POINT('Ctrl Pts',(0.545905322518818,-2.60624559525167,
13.8577210840553));
#440720=CARTESIAN_POINT('Ctrl Pts',(0.544273748301041,-2.60632709789007,
13.8581177131616));
#440721=CARTESIAN_POINT('Ctrl Pts',(0.543814240844234,-2.60635005183828,
13.8582294175695));
#440722=CARTESIAN_POINT('Ctrl Pts',(0.543352066480071,-2.60638296771572,
13.8583265086086));
#440723=CARTESIAN_POINT('Ctrl Pts',(0.542888631885539,-2.60642610315221,
13.8584082369006));
#440724=CARTESIAN_POINT('Ctrl Pts',(0.542222800648099,-2.60648807720723,
13.8585256585398));
#440725=CARTESIAN_POINT('Ctrl Pts',(0.541546120161518,-2.60657223889611,
13.8586122832068));
#440726=CARTESIAN_POINT('Ctrl Pts',(0.540876266089495,-2.60667718559124,
13.8586682984299));
#440727=CARTESIAN_POINT('Ctrl Pts',(0.540340449232375,-2.60676113254431,
13.8587131050557));
#440728=CARTESIAN_POINT('Ctrl Pts',(0.539803045802962,-2.60685907414333,
13.8587357943552));
#440729=CARTESIAN_POINT('Ctrl Pts',(0.539264082746913,-2.6069715202655,
13.8587355499465));
#440730=CARTESIAN_POINT('Ctrl Pts',(0.538915738074296,-2.6070441968751,
13.8587353919793));
#440731=CARTESIAN_POINT('Ctrl Pts',(0.53857050094606,-2.60712210875223,
13.8587257282814));
#440732=CARTESIAN_POINT('Ctrl Pts',(0.538228317145139,-2.60720512105024,
13.8587068136939));
#440733=CARTESIAN_POINT('Ctrl Pts',(0.538228317145139,-2.60720512105024,
13.8587068136939));
#440734=CARTESIAN_POINT('Ctrl Pts',(0.537102893278351,-2.6074781439729,
13.8586446046466));
#440735=CARTESIAN_POINT('Ctrl Pts',(0.536010456282359,-2.60780627113746,
13.858482427929));
#440736=CARTESIAN_POINT('Ctrl Pts',(0.534949429875656,-2.60818531908914,
13.8582284286032));
#440737=CARTESIAN_POINT('Ctrl Pts',(0.533860940206025,-2.6085741781949,
13.8579678548414));
#440738=CARTESIAN_POINT('Ctrl Pts',(0.532803364610523,-2.60901902048591,
13.857615680862));
#440739=CARTESIAN_POINT('Ctrl Pts',(0.531814640325284,-2.60949337667623,
13.8571944833187));
#440740=CARTESIAN_POINT('Ctrl Pts',(0.529347177753043,-2.61067718106234,
13.8561433417727));
#440741=CARTESIAN_POINT('Ctrl Pts',(0.527191028775726,-2.61209585001429,
13.8546163505474));
#440742=CARTESIAN_POINT('Ctrl Pts',(0.525374034314981,-2.61354448660743,
13.8528973491086));
#440743=CARTESIAN_POINT('Ctrl Pts',(0.525042096234256,-2.61380913114036,
13.8525833129072));
#440744=CARTESIAN_POINT('Ctrl Pts',(0.524721347877461,-2.61407471850016,
13.8522628768812));
#440745=CARTESIAN_POINT('Ctrl Pts',(0.524411786216164,-2.61433995336027,
13.851937733538));
#440746=CARTESIAN_POINT('Ctrl Pts',(0.522521336100362,-2.6159597058513,
13.8499521282529));
#440747=CARTESIAN_POINT('Ctrl Pts',(0.520862858174635,-2.617730382185,13.847639871647));
#440748=CARTESIAN_POINT('Ctrl Pts',(0.519464879087762,-2.61950400084454,
13.8452109780794));
#440749=CARTESIAN_POINT('Ctrl Pts',(0.518835899359852,-2.62030198859155,
13.8441181685877));
#440750=CARTESIAN_POINT('Ctrl Pts',(0.518258969463494,-2.62110034999956,
13.8430021611332));
#440751=CARTESIAN_POINT('Ctrl Pts',(0.517733378770134,-2.62188560828021,
13.8418824960098));
#440752=CARTESIAN_POINT('Ctrl Pts',(0.516494810879796,-2.62373608947086,
13.8392439765549));
#440753=CARTESIAN_POINT('Ctrl Pts',(0.515478988509157,-2.62560016325515,
13.8364981347964));
#440754=CARTESIAN_POINT('Ctrl Pts',(0.514653176745716,-2.62746638456149,
13.8336931113419));
#440755=CARTESIAN_POINT('Ctrl Pts',(0.51384888853202,-2.62928396559786,
13.8309611966328));
#440756=CARTESIAN_POINT('Ctrl Pts',(0.51322454550009,-2.63110563343681,
13.8281701127186));
#440757=CARTESIAN_POINT('Ctrl Pts',(0.512789167709108,-2.63292255318155,
13.8253580685121));
#440758=CARTESIAN_POINT('Ctrl Pts',(0.512694777334148,-2.63331646334309,
13.8247484142933));
#440759=CARTESIAN_POINT('Ctrl Pts',(0.512609431148093,-2.63371008994432,
13.8241378483365));
#440760=CARTESIAN_POINT('Ctrl Pts',(0.512533505583331,-2.63410319978829,
13.8235269408515));
#440761=CARTESIAN_POINT('',(0.539440859563399,-2.60693582986604,12.5969504640361));
#440762=CARTESIAN_POINT('Origin',(0.546291262470293,-2.6406543827447,12.584524458991));
#440763=CARTESIAN_POINT('Origin',(0.546291262470293,-2.6406543827447,12.584524458991));
#440764=CARTESIAN_POINT('Ctrl Pts',(0.574679115658322,-2.62124668345171,
12.5893111709658));
#440765=CARTESIAN_POINT('Ctrl Pts',(0.568290798210319,-2.61188463053885,
12.5770542771492));
#440766=CARTESIAN_POINT('Ctrl Pts',(0.553290581744335,-2.61842658596736,
12.5737548217797));
#440767=CARTESIAN_POINT('Ctrl Pts',(0.588648221934046,-2.64171835117381,
12.5663937883685));
#440768=CARTESIAN_POINT('Ctrl Pts',(0.58225175529996,-2.63234435566225,
12.5540940315304));
#440769=CARTESIAN_POINT('Ctrl Pts',(0.567206339909307,-2.63890952672148,
12.5508374392248));
#440770=CARTESIAN_POINT('Ctrl Pts',(0.602603233552784,-2.66216936323413,
12.5434499600945));
#440771=CARTESIAN_POINT('Ctrl Pts',(0.596185969727734,-2.65276488952507,
12.5311293540533));
#440772=CARTESIAN_POINT('Ctrl Pts',(0.581109478025895,-2.65937179216727,
12.5278936106989));
#440773=CARTESIAN_POINT('Ctrl Pts',(0.616545254568319,-2.68260133761895,
12.5204817579905));
#440774=CARTESIAN_POINT('Ctrl Pts',(0.610096229673003,-2.67315031819204,
12.5081597038247));
#440775=CARTESIAN_POINT('Ctrl Pts',(0.595000988433243,-2.67981498148497,
12.5049254088044));
#440776=CARTESIAN_POINT('Ctrl Pts',(0.606521582415215,-2.6679116873562,
12.5369868989719));
#440777=CARTESIAN_POINT('Ctrl Pts',(0.607046619305898,-2.66868112704464,
12.5342545179733));
#440778=CARTESIAN_POINT('Ctrl Pts',(0.60744464806695,-2.66948575753048,
12.5314872231885));
#440779=CARTESIAN_POINT('Ctrl Pts',(0.60764314151109,-2.67030503859505,
12.5287124745063));
#440780=CARTESIAN_POINT('Ctrl Pts',(0.607822152751352,-2.67104390692456,
12.5262100684184));
#440781=CARTESIAN_POINT('Ctrl Pts',(0.607837738783102,-2.67179417715144,
12.5237004536639));
#440782=CARTESIAN_POINT('Ctrl Pts',(0.60762389091828,-2.67257010863176,
12.5212220730815));
#440783=CARTESIAN_POINT('Ctrl Pts',(0.607460171878443,-2.67316415130336,
12.5193246583486));
#440784=CARTESIAN_POINT('Ctrl Pts',(0.60715940797271,-2.67378016566691,
12.517417831369));
#440785=CARTESIAN_POINT('Ctrl Pts',(0.606627525781574,-2.67439357094749,
12.5155812248348));
#440786=CARTESIAN_POINT('Ctrl Pts',(0.606400941109268,-2.67465488489409,
12.5147988205793));
#440787=CARTESIAN_POINT('Ctrl Pts',(0.606132392240512,-2.67491617209588,
12.5140295443047));
#440788=CARTESIAN_POINT('Ctrl Pts',(0.605815148134369,-2.67517758925284,
12.5132817086137));
#440789=CARTESIAN_POINT('Ctrl Pts',(0.605335042095536,-2.67557320875619,
12.5121499604604));
#440790=CARTESIAN_POINT('Ctrl Pts',(0.604728495136676,-2.67597214973372,
12.5110494206568));
#440791=CARTESIAN_POINT('Ctrl Pts',(0.603966119282129,-2.67635153762243,
12.5100666561695));
#440792=CARTESIAN_POINT('Ctrl Pts',(0.603528364822044,-2.67656938127448,
12.5095023550641));
#440793=CARTESIAN_POINT('Ctrl Pts',(0.603033884445084,-2.67678271081349,
12.5089719619137));
#440794=CARTESIAN_POINT('Ctrl Pts',(0.602489416571183,-2.67698166312245,
12.5085043804652));
#440795=CARTESIAN_POINT('Ctrl Pts',(0.601692658759658,-2.67727280391125,
12.5078201359221));
#440796=CARTESIAN_POINT('Ctrl Pts',(0.600765332000758,-2.67754046618894,
12.5072563000949));
#440797=CARTESIAN_POINT('Ctrl Pts',(0.599767947598214,-2.67775837245307,
12.5068768744332));
#440798=CARTESIAN_POINT('Ctrl Pts',(0.599048764783803,-2.67791549787022,
12.5066032824114));
#440799=CARTESIAN_POINT('Ctrl Pts',(0.598280534038465,-2.67804957226223,
12.5064197834844));
#440800=CARTESIAN_POINT('Ctrl Pts',(0.597506599762478,-2.67815565493628,
12.5063282718343));
#440801=CARTESIAN_POINT('Ctrl Pts',(0.596376895323534,-2.67831050279803,
12.5061946931565));
#440802=CARTESIAN_POINT('Ctrl Pts',(0.595211036549254,-2.67841007085721,
12.5062515701262));
#440803=CARTESIAN_POINT('Ctrl Pts',(0.594082694617785,-2.67846358818529,
12.5064436508398));
#440804=CARTESIAN_POINT('',(0.553290581744335,-2.61842658596736,12.5737548217797));
#440805=CARTESIAN_POINT('Origin',(0.556506722612535,-2.63364685002275,12.5893111709658));
#440806=CARTESIAN_POINT('Ctrl Pts',(0.594082694617785,-2.67846358818529,
12.5064436508398));
#440807=CARTESIAN_POINT('Ctrl Pts',(0.588044004717534,-2.66957682206708,
12.5164271754438));
#440808=CARTESIAN_POINT('Ctrl Pts',(0.582003093895394,-2.66068641580753,
12.5264061185523));
#440809=CARTESIAN_POINT('Ctrl Pts',(0.575959883149501,-2.65179224173588,
12.536380305637));
#440810=CARTESIAN_POINT('Ctrl Pts',(0.568407095412342,-2.64067632807919,
12.5488460165097));
#440811=CARTESIAN_POINT('Ctrl Pts',(0.560850712999367,-2.62955452582905,
12.5613043021964));
#440812=CARTESIAN_POINT('Ctrl Pts',(0.553290581744335,-2.61842658596736,
12.5737548217797));
#440813=CARTESIAN_POINT('Ctrl Pts',(0.512533505583331,-2.63410319978829,
12.5893111709658));
#440814=CARTESIAN_POINT('Ctrl Pts',(0.514682834419019,-2.6229749016203,
12.5770542771492));
#440815=CARTESIAN_POINT('Ctrl Pts',(0.53104745588893,-2.62302818390149,
12.5737548217797));
#440816=CARTESIAN_POINT('Ctrl Pts',(0.514538810693153,-2.62372059438638,
12.5928319619712));
#440817=CARTESIAN_POINT('Ctrl Pts',(0.5191819214574,-2.61685947648896,12.5821634970842));
#440818=CARTESIAN_POINT('Ctrl Pts',(0.531768672420854,-2.61924426211537,
12.5773203894503));
#440819=CARTESIAN_POINT('Ctrl Pts',(0.524285711840975,-2.61009774529545,
12.5969440695591));
#440820=CARTESIAN_POINT('Ctrl Pts',(0.528218384721718,-2.60926550340454,
12.5878292599214));
#440821=CARTESIAN_POINT('Ctrl Pts',(0.535244330820872,-2.61438999123459,
12.5813877129824));
#440822=CARTESIAN_POINT('Ctrl Pts',(0.554237267822093,-2.60384638225596,
12.596957478804));
#440823=CARTESIAN_POINT('Ctrl Pts',(0.550333675044355,-2.60467255207779,
12.5878468778671));
#440824=CARTESIAN_POINT('Ctrl Pts',(0.545965626647944,-2.61215838103284,
12.5814011370086));
#440825=CARTESIAN_POINT('Ctrl Pts',(0.568710216777123,-2.61249928672123,
12.5928371701607));
#440826=CARTESIAN_POINT('Ctrl Pts',(0.561727668613172,-2.60805191819121,
12.5821692192952));
#440827=CARTESIAN_POINT('Ctrl Pts',(0.551120496911469,-2.61522908549165,
12.5773318885715));
#440828=CARTESIAN_POINT('Ctrl Pts',(0.574679115658365,-2.62124668345168,
12.5893111709658));
#440829=CARTESIAN_POINT('Ctrl Pts',(0.568290798210363,-2.61188463053882,
12.5770542771492));
#440830=CARTESIAN_POINT('Ctrl Pts',(0.55329058174438,-2.61842658596732,
12.5737548217797));
#440831=CARTESIAN_POINT('',(0.53104745588893,-2.62302818390149,12.5737548217797));
#440832=CARTESIAN_POINT('Origin',(0.534134302985538,-2.63827519590392,12.5893111709658));
#440833=CARTESIAN_POINT('Ctrl Pts',(0.55329058174438,-2.61842658596732,
12.5737548217797));
#440834=CARTESIAN_POINT('Ctrl Pts',(0.552753021476352,-2.61758080314103,
12.5746934679442));
#440835=CARTESIAN_POINT('Ctrl Pts',(0.552003574668472,-2.61674314872517,
12.5756680099006));
#440836=CARTESIAN_POINT('Ctrl Pts',(0.551129988790303,-2.61600670362779,
12.5765688348656));
#440837=CARTESIAN_POINT('Ctrl Pts',(0.550898716599976,-2.61581173794098,
12.5768073183026));
#440838=CARTESIAN_POINT('Ctrl Pts',(0.550658952463078,-2.6156237153656,
12.5770407398754));
#440839=CARTESIAN_POINT('Ctrl Pts',(0.550412683962006,-2.61544392946994,
12.5772674179684));
#440840=CARTESIAN_POINT('Ctrl Pts',(0.549402064627409,-2.61470613677027,
12.5781976435658));
#440841=CARTESIAN_POINT('Ctrl Pts',(0.548217856179683,-2.61407426033052,
12.5790594849312));
#440842=CARTESIAN_POINT('Ctrl Pts',(0.546917285553968,-2.61363356908804,
12.5797571720116));
#440843=CARTESIAN_POINT('Ctrl Pts',(0.546069917026963,-2.61334644289771,
12.580211740231));
#440844=CARTESIAN_POINT('Ctrl Pts',(0.54512861965466,-2.61314520612865,
12.5806009430798));
#440845=CARTESIAN_POINT('Ctrl Pts',(0.544155952783195,-2.61306135017195,
12.5808812374708));
#440846=CARTESIAN_POINT('Ctrl Pts',(0.543320109261729,-2.61298929008622,
12.5811221033394));
#440847=CARTESIAN_POINT('Ctrl Pts',(0.542443979152123,-2.61300254843245,
12.581287365893));
#440848=CARTESIAN_POINT('Ctrl Pts',(0.54157713881285,-2.61310871391489,
12.581359338449));
#440849=CARTESIAN_POINT('Ctrl Pts',(0.541456665905261,-2.61312346872472,
12.5813693411482));
#440850=CARTESIAN_POINT('Ctrl Pts',(0.541336345760709,-2.6131399644506,
12.5813775999465));
#440851=CARTESIAN_POINT('Ctrl Pts',(0.541216283170465,-2.61315816703582,
12.5813841266931));
#440852=CARTESIAN_POINT('Ctrl Pts',(0.541012582464843,-2.61318904992321,
12.5813952001081));
#440853=CARTESIAN_POINT('Ctrl Pts',(0.540808350112785,-2.61322565487485,
12.5814007534795));
#440854=CARTESIAN_POINT('Ctrl Pts',(0.540603709856019,-2.61326816006462,
12.5814005856065));
#440855=CARTESIAN_POINT('Ctrl Pts',(0.5396669467697,-2.61346273220494,12.5813998171494));
#440856=CARTESIAN_POINT('Ctrl Pts',(0.538786290740728,-2.61376716702444,
12.58127954464));
#440857=CARTESIAN_POINT('Ctrl Pts',(0.537957074128939,-2.61415177060978,
12.5810700125799));
#440858=CARTESIAN_POINT('Ctrl Pts',(0.536955474875768,-2.61461632795025,
12.5808169217085));
#440859=CARTESIAN_POINT('Ctrl Pts',(0.536035876464012,-2.61521307506634,
12.5804173076348));
#440860=CARTESIAN_POINT('Ctrl Pts',(0.535264694727185,-2.61586786823707,
12.5799304713245));
#440861=CARTESIAN_POINT('Ctrl Pts',(0.534308957607955,-2.61667936325673,
12.5793271277669));
#440862=CARTESIAN_POINT('Ctrl Pts',(0.533501046458801,-2.61760580396366,
12.5785808224116));
#440863=CARTESIAN_POINT('Ctrl Pts',(0.532851112115142,-2.6185872932463,
12.5777485681082));
#440864=CARTESIAN_POINT('Ctrl Pts',(0.531882638737466,-2.62004981980761,
12.576508418016));
#440865=CARTESIAN_POINT('Ctrl Pts',(0.531267366112818,-2.62161846862367,
12.5750928681475));
#440866=CARTESIAN_POINT('Ctrl Pts',(0.53104745588893,-2.62302818390149,
12.5737548217797));
#440867=CARTESIAN_POINT('Ctrl Pts',(0.53104745588893,-2.62302818390149,
12.5737548217797));
#440868=CARTESIAN_POINT('Ctrl Pts',(0.514682834419019,-2.62297490162029,
12.5770542771492));
#440869=CARTESIAN_POINT('Ctrl Pts',(0.512533505583331,-2.63410319978829,
12.5893111709658));
#440870=CARTESIAN_POINT('Ctrl Pts',(0.526401735067308,-2.64734756366781,
12.5508408821982));
#440871=CARTESIAN_POINT('Ctrl Pts',(0.509986421664261,-2.64729090231181,
12.55409748406));
#440872=CARTESIAN_POINT('Ctrl Pts',(0.50783435083545,-2.65843339733818,
12.5663972313419));
#440873=CARTESIAN_POINT('Ctrl Pts',(0.521759393966551,-2.67164296514411,
12.52790050457));
#440874=CARTESIAN_POINT('Ctrl Pts',(0.505299003657782,-2.67156033207436,
12.5311362602938));
#440875=CARTESIAN_POINT('Ctrl Pts',(0.503139936762534,-2.68273904971673,
12.5434568539655));
#440876=CARTESIAN_POINT('Ctrl Pts',(0.517120156336858,-2.69591624915291,
12.5049357605811));
#440877=CARTESIAN_POINT('Ctrl Pts',(0.500619642742995,-2.69578804568921,
12.5081700652078));
#440878=CARTESIAN_POINT('Ctrl Pts',(0.49844989207396,-2.70702207930673,
12.5204921097672));
#440879=CARTESIAN_POINT('Ctrl Pts',(0.517424785305965,-2.69432236987859,
12.5064436508395));
#440880=CARTESIAN_POINT('Ctrl Pts',(0.516283079484765,-2.69475289932988,
12.5062361689309));
#440881=CARTESIAN_POINT('Ctrl Pts',(0.515077440127446,-2.69515192985568,
12.5061871075061));
#440882=CARTESIAN_POINT('Ctrl Pts',(0.513890598303338,-2.69547196598749,
12.5063648335164));
#440883=CARTESIAN_POINT('Ctrl Pts',(0.513351461539388,-2.6956173461392,
12.5064455676329));
#440884=CARTESIAN_POINT('Ctrl Pts',(0.512808626519243,-2.6957482405416,
12.506574497099));
#440885=CARTESIAN_POINT('Ctrl Pts',(0.512285122024746,-2.69585801516844,
12.5067492519495));
#440886=CARTESIAN_POINT('Ctrl Pts',(0.511233119422025,-2.69607861154224,
12.5071004286051));
#440887=CARTESIAN_POINT('Ctrl Pts',(0.5102203339967,-2.696221240622,12.5076537929613));
#440888=CARTESIAN_POINT('Ctrl Pts',(0.509324099610258,-2.69628456337405,
12.5083435010505));
#440889=CARTESIAN_POINT('Ctrl Pts',(0.509267676299709,-2.69628854991971,
12.5083869222964));
#440890=CARTESIAN_POINT('Ctrl Pts',(0.509211707939692,-2.69629221066786,
12.5084308732337));
#440891=CARTESIAN_POINT('Ctrl Pts',(0.509156210641147,-2.69629554081953,
12.5084753333615));
#440892=CARTESIAN_POINT('Ctrl Pts',(0.508711049056997,-2.69632225303127,
12.5088319622689));
#440893=CARTESIAN_POINT('Ctrl Pts',(0.508287236068956,-2.69632952421375,
12.509227847131));
#440894=CARTESIAN_POINT('Ctrl Pts',(0.507897421878471,-2.69631993779793,
12.5096423454524));
#440895=CARTESIAN_POINT('Ctrl Pts',(0.506675916730021,-2.6962898982135,
12.5109411997424));
#440896=CARTESIAN_POINT('Ctrl Pts',(0.505712883878049,-2.69610214887079,
12.5124831113042));
#440897=CARTESIAN_POINT('Ctrl Pts',(0.50495441954974,-2.69583447306283,
12.5140723025008));
#440898=CARTESIAN_POINT('Ctrl Pts',(0.504883350611455,-2.69580939154645,
12.5142212114565));
#440899=CARTESIAN_POINT('Ctrl Pts',(0.504814053420152,-2.69578362513724,
12.5143705582413));
#440900=CARTESIAN_POINT('Ctrl Pts',(0.504746470605339,-2.69575724872422,
12.5145201959299));
#440901=CARTESIAN_POINT('Ctrl Pts',(0.503878268728772,-2.69541840442872,
12.5164425148273));
#440902=CARTESIAN_POINT('Ctrl Pts',(0.503259342401318,-2.69497728315226,
12.5184635205941));
#440903=CARTESIAN_POINT('Ctrl Pts',(0.502807242578748,-2.69447049273086,
12.5205025929158));
#440904=CARTESIAN_POINT('Ctrl Pts',(0.502545006762095,-2.69417653419916,
12.5216853356836));
#440905=CARTESIAN_POINT('Ctrl Pts',(0.502339011915975,-2.69386133445627,
12.5228750347131));
#440906=CARTESIAN_POINT('Ctrl Pts',(0.502175881409603,-2.69353730315154,
12.5240609649613));
#440907=CARTESIAN_POINT('Ctrl Pts',(0.501775486333361,-2.69274198569777,
12.5269717671326));
#440908=CARTESIAN_POINT('Ctrl Pts',(0.501631335873172,-2.69186640609945,
12.5299036066169));
#440909=CARTESIAN_POINT('Ctrl Pts',(0.501661299468604,-2.6909382066009,
12.5328133004019));
#440910=CARTESIAN_POINT('Ctrl Pts',(0.50167568373914,-2.69049261679416,
12.5342101228451));
#440911=CARTESIAN_POINT('Ctrl Pts',(0.50173069947955,-2.69003547329922,
12.5356023438238));
#440912=CARTESIAN_POINT('Ctrl Pts',(0.501820210172278,-2.68957202508688,
12.5369868989719));
#440913=CARTESIAN_POINT('Origin',(-1.92036686075476,-15.2026802942216,-1.24010651594408));
#440914=CARTESIAN_POINT('Ctrl Pts',(0.606498058131685,-2.6678771421826,
12.5369868989719));
#440915=CARTESIAN_POINT('Ctrl Pts',(0.615119676982169,-2.68056378839359,
12.5369868989719));
#440916=CARTESIAN_POINT('Ctrl Pts',(0.63000495457471,-2.67686084163745,
12.5369868989719));
#440917=CARTESIAN_POINT('Ctrl Pts',(0.609412557255683,-2.6721656875577,
12.5218025310016));
#440918=CARTESIAN_POINT('Ctrl Pts',(0.618531066300393,-2.67968291154709,
12.5216901060418));
#440919=CARTESIAN_POINT('Ctrl Pts',(0.629959583296767,-2.67687214545033,
12.5161920673678));
#440920=CARTESIAN_POINT('Ctrl Pts',(0.607339468066221,-2.6778259324648,
12.5042015548894));
#440921=CARTESIAN_POINT('Ctrl Pts',(0.612976673589232,-2.6809241995463,
12.4980677368514));
#440922=CARTESIAN_POINT('Ctrl Pts',(0.619600715733787,-2.67940339535413,
12.4907278922777));
#440923=CARTESIAN_POINT('Ctrl Pts',(0.594078363624189,-2.6784440616444,
12.506463626192));
#440924=CARTESIAN_POINT('Ctrl Pts',(0.595495111718461,-2.68483157001417,
12.4999376786891));
#440925=CARTESIAN_POINT('Ctrl Pts',(0.59547780820044,-2.68475355588686,
12.4906970594712));
#440926=CARTESIAN_POINT('Origin',(0.624693975461002,-2.65551152078516,12.5369868989719));
#440927=CARTESIAN_POINT('Origin',(0.624693975461003,-2.65551152078516,14.));
#440928=CARTESIAN_POINT('Origin',(0.624693975461002,-2.65551152078516,13.7435492065112));
#440929=CARTESIAN_POINT('Ctrl Pts',(0.592565722405718,-2.64745938381134,
13.793642941384));
#440930=CARTESIAN_POINT('Ctrl Pts',(0.598637514750161,-2.65640586673658,
13.8071662555867));
#440931=CARTESIAN_POINT('Ctrl Pts',(0.613981610874529,-2.64901816765223,
13.8103758687955));
#440932=CARTESIAN_POINT('Ctrl Pts',(0.601934114705725,-2.66118872942342,
13.7804579775006));
#440933=CARTESIAN_POINT('Ctrl Pts',(0.609434548503473,-2.67222218602483,
13.7901904343351));
#440934=CARTESIAN_POINT('Ctrl Pts',(0.624549765349318,-2.66777402417215,
13.7927914348263));
#440935=CARTESIAN_POINT('Ctrl Pts',(0.60744963985642,-2.66927171185723,
13.7597120340895));
#440936=CARTESIAN_POINT('Ctrl Pts',(0.616134493101865,-2.68203730679351,
13.7635825532445));
#440937=CARTESIAN_POINT('Ctrl Pts',(0.630804064389904,-2.67882178282857,
13.7651073818884));
#440938=CARTESIAN_POINT('Ctrl Pts',(0.606369573741418,-2.66768887881698,
13.7381884353898));
#440939=CARTESIAN_POINT('Ctrl Pts',(0.614850398662509,-2.6801561768115,
13.7368803041982));
#440940=CARTESIAN_POINT('Ctrl Pts',(0.629579716885802,-2.67665805991866,
13.7363986145813));
#440941=CARTESIAN_POINT('Origin',(0.613011317284714,-2.63839063333717,13.7902182540695));
#440942=CARTESIAN_POINT('Ctrl Pts',(0.574676897670838,-2.62124343165373,
13.8235227101244));
#440943=CARTESIAN_POINT('Ctrl Pts',(0.581153490587285,-2.6307427175487,
13.8358800583119));
#440944=CARTESIAN_POINT('Ctrl Pts',(0.596298747147244,-2.62401610972677,
13.8390832900376));
#440945=CARTESIAN_POINT('Ctrl Pts',(0.581399805435583,-2.63109582529598,
13.8124254819053));
#440946=CARTESIAN_POINT('Ctrl Pts',(0.587888976033493,-2.6406135585128,
13.8247886449158));
#440947=CARTESIAN_POINT('Ctrl Pts',(0.603046450886266,-2.63386287431115,
13.8279860620657));
#440948=CARTESIAN_POINT('Ctrl Pts',(0.588119700211747,-2.64094380341589,
13.8013225099955));
#440949=CARTESIAN_POINT('Ctrl Pts',(0.594618384988356,-2.65047549424216,
13.8136962257787));
#440950=CARTESIAN_POINT('Ctrl Pts',(0.609790807176251,-2.64370523355036,
13.8168830918626));
#440951=CARTESIAN_POINT('Ctrl Pts',(0.594836699230128,-2.65078753781472,
13.7902140179785));
#440952=CARTESIAN_POINT('Ctrl Pts',(0.601342034907494,-2.66032898997199,
13.802602731458));
#440953=CARTESIAN_POINT('Ctrl Pts',(0.616531946028556,-2.65354336158135,
13.8057746032558));
#440954=CARTESIAN_POINT('Origin',(0.592851508704108,-2.60884651688068,13.8235269408515));
#440955=CARTESIAN_POINT('Ctrl Pts',(0.512533505583331,-2.63410319978829,
13.8235269408515));
#440956=CARTESIAN_POINT('Ctrl Pts',(0.510294379817396,-2.645696427751,13.8362179249168));
#440957=CARTESIAN_POINT('Ctrl Pts',(0.493223091185079,-2.64521258016219,
13.8391868794938));
#440958=CARTESIAN_POINT('Ctrl Pts',(0.51458220819582,-2.62349590082558,
13.8400110824519));
#440959=CARTESIAN_POINT('Ctrl Pts',(0.509428054285371,-2.63214208844374,
13.8494522556836));
#440960=CARTESIAN_POINT('Ctrl Pts',(0.496704995458622,-2.6277772675394,
13.85569149686));
#440961=CARTESIAN_POINT('Ctrl Pts',(0.523948816583283,-2.61016682083629,
13.8586819406588));
#440962=CARTESIAN_POINT('Ctrl Pts',(0.519688082897046,-2.61106247260452,
13.868010383617));
#440963=CARTESIAN_POINT('Ctrl Pts',(0.512373206287159,-2.60573467315496,
13.8744918421245));
#440964=CARTESIAN_POINT('Ctrl Pts',(0.554579384364869,-2.60377621716178,
13.8587686893867));
#440965=CARTESIAN_POINT('Ctrl Pts',(0.55880218597755,-2.6028884815819,13.8680909899357));
#440966=CARTESIAN_POINT('Ctrl Pts',(0.563364632001517,-2.5950987134349,
13.8745789365163));
#440967=CARTESIAN_POINT('Ctrl Pts',(0.568579974698556,-2.61230841747989,
13.8400379222776));
#440968=CARTESIAN_POINT('Ctrl Pts',(0.576743743323402,-2.61819255851727,
13.8494748685453));
#440969=CARTESIAN_POINT('Ctrl Pts',(0.586686777358123,-2.60914285247514,
13.8557104837033));
#440970=CARTESIAN_POINT('Ctrl Pts',(0.574679115663699,-2.62124668344787,
13.8235269408542));
#440971=CARTESIAN_POINT('Ctrl Pts',(0.581334330985496,-2.6309998740956,
13.8362179249195));
#440972=CARTESIAN_POINT('Ctrl Pts',(0.596812372092759,-2.62378230888716,
13.8391868794965));
#440973=CARTESIAN_POINT('Origin',(0.490932708181124,-2.62993120367266,13.8235269408515));
#440974=CARTESIAN_POINT('Ctrl Pts',(0.50575154986725,-2.66921723887999,
13.7902140241682));
#440975=CARTESIAN_POINT('Ctrl Pts',(0.503565983381956,-2.6805566345663,
13.8026027327198));
#440976=CARTESIAN_POINT('Ctrl Pts',(0.48693056170767,-2.68035494670805,
13.8057746032556));
#440977=CARTESIAN_POINT('Ctrl Pts',(0.508011462560479,-2.65751638517433,
13.8013225161808));
#440978=CARTESIAN_POINT('Ctrl Pts',(0.505828128021538,-2.66884418187874,
13.8136962270464));
#440979=CARTESIAN_POINT('Ctrl Pts',(0.489214857211879,-2.66864966113952,
13.8168830918628));
#440980=CARTESIAN_POINT('Ctrl Pts',(0.510272349522419,-2.64581048712535,
13.8124254880875));
#440981=CARTESIAN_POINT('Ctrl Pts',(0.50809221020777,-2.65712169694612,
13.8247886461867));
#440982=CARTESIAN_POINT('Ctrl Pts',(0.491500427224399,-2.6569392150819,
13.8279860620656));
#440983=CARTESIAN_POINT('Ctrl Pts',(0.512534250195273,-2.63409934051833,
13.8235227163065));
#440984=CARTESIAN_POINT('Ctrl Pts',(0.510358336745589,-2.64538862676221,
13.8358800595847));
#440985=CARTESIAN_POINT('Ctrl Pts',(0.493787321992151,-2.64522339710558,
13.8390832900376));
#440986=CARTESIAN_POINT('Origin',(0.484150005496586,-2.66504911425251,13.7902182540695));
#440987=CARTESIAN_POINT('Ctrl Pts',(0.501871358291202,-2.68930705671633,
13.7382347919292));
#440988=CARTESIAN_POINT('Ctrl Pts',(0.499033255290564,-2.70412809042155,
13.7369371795943));
#440989=CARTESIAN_POINT('Ctrl Pts',(0.484112057328093,-2.70675518546834,
13.7364597369712));
#440990=CARTESIAN_POINT('Ctrl Pts',(0.501512650723195,-2.69116429199084,
13.7595490285573));
#440991=CARTESIAN_POINT('Ctrl Pts',(0.498605845535065,-2.70633875376109,
13.7633824266926));
#440992=CARTESIAN_POINT('Ctrl Pts',(0.483850339632552,-2.70919684855801,
13.7648920890506));
#440993=CARTESIAN_POINT('Ctrl Pts',(0.503342039676267,-2.68169249383999,
13.7803806590111));
#440994=CARTESIAN_POINT('Ctrl Pts',(0.500833059283693,-2.69481887580129,
13.7901039518744));
#440995=CARTESIAN_POINT('Ctrl Pts',(0.485188296642965,-2.69674937919179,
13.7926933640892));
#440996=CARTESIAN_POINT('Ctrl Pts',(0.506521925972004,-2.66522839426788,
13.7936647693663));
#440997=CARTESIAN_POINT('Ctrl Pts',(0.504500368443352,-2.67585320660048,
13.8072068914933));
#440998=CARTESIAN_POINT('Ctrl Pts',(0.487466636836108,-2.6751487512227,
13.8104111085397));
#440999=CARTESIAN_POINT('Origin',(0.480219412770071,-2.68540002897125,13.7435492065112));
#441000=CARTESIAN_POINT('Origin',(0.480219412770071,-2.68540002897125,14.));
#441001=CARTESIAN_POINT('Origin',(0.480219412770071,-2.68540002897125,12.5369868989719));
#441002=CARTESIAN_POINT('Ctrl Pts',(0.517421318304256,-2.69430431653286,
12.506462012331));
#441003=CARTESIAN_POINT('Ctrl Pts',(0.518654478867682,-2.70072560168575,
12.4999388158272));
#441004=CARTESIAN_POINT('Ctrl Pts',(0.518639888961025,-2.7006496294614,
12.4907030323752));
#441005=CARTESIAN_POINT('Ctrl Pts',(0.505003128977343,-2.69899656087809,
12.5042014951932));
#441006=CARTESIAN_POINT('Ctrl Pts',(0.501060437504569,-2.70407556482246,
12.4980716682127));
#441007=CARTESIAN_POINT('Ctrl Pts',(0.494381709264913,-2.70530851020918,
12.4907355092743));
#441008=CARTESIAN_POINT('Ctrl Pts',(0.50085325994376,-2.69462571562236,
12.5218047446509));
#441009=CARTESIAN_POINT('Ctrl Pts',(0.495467506015631,-2.70513820940652,
12.5216906929434));
#441010=CARTESIAN_POINT('Ctrl Pts',(0.483868357058764,-2.70709537516508,
12.5161988840776));
#441011=CARTESIAN_POINT('Ctrl Pts',(0.5018274623251,-2.68953429969622,12.5369868989719));
#441012=CARTESIAN_POINT('Ctrl Pts',(0.498946647961556,-2.70459107359116,
12.5369868989719));
#441013=CARTESIAN_POINT('Ctrl Pts',(0.483823914260394,-2.70710273776546,
12.5369868989719));
#441014=CARTESIAN_POINT('Origin',(1.04370312006728E-31,-1.01968969974689E-30,
12.5));
#441015=CARTESIAN_POINT('Origin',(0.725531957228311,-2.58356219985525,12.5));
#441016=CARTESIAN_POINT('',(0.725531957228311,-2.58356219985525,12.5893111709658));
#441017=CARTESIAN_POINT('',(0.725531957228311,-2.58356219985525,13.8235269408515));
#441018=CARTESIAN_POINT('',(0.725531957228311,-2.58356219985525,12.5));
#441019=CARTESIAN_POINT('',(0.721634259158455,-2.619116111721,13.7902182540695));
#441020=CARTESIAN_POINT('',(0.725531957228311,-2.58356219985525,13.8235269408515));
#441021=CARTESIAN_POINT('',(0.719375533633238,-2.6397196902469,13.7435492065112));
#441022=CARTESIAN_POINT('Origin',(0.726807034570083,-2.57193422473676,13.7445212918707));
#441023=CARTESIAN_POINT('',(0.719375533633238,-2.6397196902469,12.5369868989719));
#441024=CARTESIAN_POINT('',(0.719375533633238,-2.6397196902469,12.5));
#441025=CARTESIAN_POINT('Ctrl Pts',(0.719375533633238,-2.6397196902469,
12.5369868989719));
#441026=CARTESIAN_POINT('Ctrl Pts',(0.72142617812462,-2.62101417940232,
12.5544431401645));
#441027=CARTESIAN_POINT('Ctrl Pts',(0.723478289291444,-2.60229528987922,
12.5718848856037));
#441028=CARTESIAN_POINT('Ctrl Pts',(0.725531957228311,-2.58356219985525,
12.5893111709658));
#441029=CARTESIAN_POINT('Origin',(0.959424417192052,-2.77944798353807,12.5));
#441030=CARTESIAN_POINT('',(0.821963002087478,-2.60959729166525,13.7435492065112));
#441031=CARTESIAN_POINT('',(0.808923705722944,-2.59348561765574,13.7902182540695));
#441032=CARTESIAN_POINT('Origin',(0.774658688519583,-2.55114692301479,13.741873268044));
#441033=CARTESIAN_POINT('',(0.786422857476923,-2.56568301836339,13.8235269408515));
#441034=CARTESIAN_POINT('',(0.808923705722944,-2.59348561765574,13.7902182540695));
#441035=CARTESIAN_POINT('',(0.786422857476923,-2.56568301836339,12.5893111709658));
#441036=CARTESIAN_POINT('',(0.786422857476923,-2.56568301836339,12.5));
#441037=CARTESIAN_POINT('',(0.821963002087478,-2.60959729166525,12.5369868989719));
#441038=CARTESIAN_POINT('Ctrl Pts',(0.786422857476923,-2.56568301836339,
12.5893111709658));
#441039=CARTESIAN_POINT('Ctrl Pts',(0.798278385988105,-2.58033199981473,
12.5718848856037));
#441040=CARTESIAN_POINT('Ctrl Pts',(0.810124927490586,-2.59496987669797,
12.5544431401645));
#441041=CARTESIAN_POINT('Ctrl Pts',(0.821963002087478,-2.60959729166525,
12.5369868989719));
#441042=CARTESIAN_POINT('',(0.821963002087478,-2.60959729166525,12.5));
#441043=CARTESIAN_POINT('Origin',(0.759702236830088,-2.58730821332778,12.5));
#441044=CARTESIAN_POINT('',(0.7489488282979,-2.55465925657388,13.8587068136939));
#441045=CARTESIAN_POINT('Ctrl Pts',(0.786422857481969,-2.56568301835912,
13.8235269408542));
#441046=CARTESIAN_POINT('Ctrl Pts',(0.78532049259588,-2.56432090930143,
13.8262006681044));
#441047=CARTESIAN_POINT('Ctrl Pts',(0.784057330900536,-2.56303628851558,
13.8288634856214));
#441048=CARTESIAN_POINT('Ctrl Pts',(0.782645946513711,-2.56182471780257,
13.8314912288862));
#441049=CARTESIAN_POINT('Ctrl Pts',(0.781190954788442,-2.56057571336518,
13.834200161153));
#441050=CARTESIAN_POINT('Ctrl Pts',(0.779577147155867,-2.55940257841192,
13.8368750301949));
#441051=CARTESIAN_POINT('Ctrl Pts',(0.777776862845244,-2.55831850944794,
13.8394886372968));
#441052=CARTESIAN_POINT('Ctrl Pts',(0.777637822521051,-2.55823478417226,
13.8396904925131));
#441053=CARTESIAN_POINT('Ctrl Pts',(0.777497655368256,-2.5581516068833,
13.8398919674349));
#441054=CARTESIAN_POINT('Ctrl Pts',(0.777356341927515,-2.55806899292609,
13.8400930404591));
#441055=CARTESIAN_POINT('Ctrl Pts',(0.775154583449799,-2.55678181189288,
13.8432258934518));
#441056=CARTESIAN_POINT('Ctrl Pts',(0.772686357935972,-2.55563698016031,
13.8462331177034));
#441057=CARTESIAN_POINT('Ctrl Pts',(0.769991575538835,-2.55475934707315,
13.8489036603661));
#441058=CARTESIAN_POINT('Ctrl Pts',(0.769109811377731,-2.5544721753135,
13.8497774930041));
#441059=CARTESIAN_POINT('Ctrl Pts',(0.768203946779649,-2.55421380676574,
13.85061494757));
#441060=CARTESIAN_POINT('Ctrl Pts',(0.767275836005458,-2.55398916456931,
13.8514076489583));
#441061=CARTESIAN_POINT('Ctrl Pts',(0.765312747864439,-2.5535140139256,
13.8530843267192));
#441062=CARTESIAN_POINT('Ctrl Pts',(0.763056611219965,-2.55314595204423,
13.8546805203176));
#441063=CARTESIAN_POINT('Ctrl Pts',(0.76061640235854,-2.55304100658142,
13.8559412814273));
#441064=CARTESIAN_POINT('Ctrl Pts',(0.760289823275029,-2.55302696147503,
13.8561100121513));
#441065=CARTESIAN_POINT('Ctrl Pts',(0.759959999496362,-2.5530175727559,
13.8562727473908));
#441066=CARTESIAN_POINT('Ctrl Pts',(0.759627236466857,-2.55301315281039,
13.8564289040185));
#441067=CARTESIAN_POINT('Ctrl Pts',(0.758118159924363,-2.55299310840789,
13.8571370725437));
#441068=CARTESIAN_POINT('Ctrl Pts',(0.756522078808802,-2.55307717631056,
13.8577210840554));
#441069=CARTESIAN_POINT('Ctrl Pts',(0.7549025767413,-2.5532913962012,13.8581177131616));
#441070=CARTESIAN_POINT('Ctrl Pts',(0.754446469217524,-2.55335172789563,
13.8582294175695));
#441071=CARTESIAN_POINT('Ctrl Pts',(0.753988515650023,-2.5534222057495,
13.8583265086086));
#441072=CARTESIAN_POINT('Ctrl Pts',(0.7535301390344,-2.55350297187816,13.8584082369006));
#441073=CARTESIAN_POINT('Ctrl Pts',(0.752871574756299,-2.55361901114674,
13.8585256585398));
#441074=CARTESIAN_POINT('Ctrl Pts',(0.752204005827178,-2.5537580485362,
13.8586122832068));
#441075=CARTESIAN_POINT('Ctrl Pts',(0.751544934769251,-2.55391724535535,
13.8586682984299));
#441076=CARTESIAN_POINT('Ctrl Pts',(0.751017743254522,-2.55404458702999,
13.8587131050557));
#441077=CARTESIAN_POINT('Ctrl Pts',(0.750490111140253,-2.55418600610493,
13.8587357943552));
#441078=CARTESIAN_POINT('Ctrl Pts',(0.749962106842168,-2.55434200856446,
13.8587355499465));
#441079=CARTESIAN_POINT('Ctrl Pts',(0.749620845076198,-2.55444283667331,
13.8587353919793));
#441080=CARTESIAN_POINT('Ctrl Pts',(0.749283107237414,-2.55454862933603,
13.8587257282814));
#441081=CARTESIAN_POINT('Ctrl Pts',(0.7489488282979,-2.55465925657388,13.8587068136939));
#441082=CARTESIAN_POINT('Ctrl Pts',(0.7489488282979,-2.55465925657388,13.8587068136939));
#441083=CARTESIAN_POINT('Ctrl Pts',(0.747849403088895,-2.55502310352839,
13.8586446046466));
#441084=CARTESIAN_POINT('Ctrl Pts',(0.74678734649688,-2.55543918263377,
13.858482427929));
#441085=CARTESIAN_POINT('Ctrl Pts',(0.745760746494891,-2.55590345283694,
13.8582284286032));
#441086=CARTESIAN_POINT('Ctrl Pts',(0.744707574311953,-2.55637974005923,
13.8579678548414));
#441087=CARTESIAN_POINT('Ctrl Pts',(0.743689776488433,-2.5569093044033,
13.857615680862));
#441088=CARTESIAN_POINT('Ctrl Pts',(0.742743006534908,-2.55746267242064,
13.8571944833187));
#441089=CARTESIAN_POINT('Ctrl Pts',(0.740380245288189,-2.55884365890176,
13.8561433417727));
#441090=CARTESIAN_POINT('Ctrl Pts',(0.738346905408584,-2.56043335350817,
13.8546163505474));
#441091=CARTESIAN_POINT('Ctrl Pts',(0.73665403417784,-2.56202527179926,
13.8528973491086));
#441092=CARTESIAN_POINT('Ctrl Pts',(0.736344771579975,-2.56231609178447,
13.8525833129072));
#441093=CARTESIAN_POINT('Ctrl Pts',(0.736046738322298,-2.562606939393,13.8522628768812));
#441094=CARTESIAN_POINT('Ctrl Pts',(0.735759825805316,-2.56289652385522,
13.851937733538));
#441095=CARTESIAN_POINT('Ctrl Pts',(0.734007690871391,-2.56466497598797,
13.8499521282529));
#441096=CARTESIAN_POINT('Ctrl Pts',(0.732499057953502,-2.56656494188974,
13.847639871647));
#441097=CARTESIAN_POINT('Ctrl Pts',(0.731250296912941,-2.56844660725329,
13.8452109780794));
#441098=CARTESIAN_POINT('Ctrl Pts',(0.730688453472725,-2.56929320744889,
13.8441181685877));
#441099=CARTESIAN_POINT('Ctrl Pts',(0.730178517129381,-2.57013593751768,
13.8430021611332));
#441100=CARTESIAN_POINT('Ctrl Pts',(0.72971868113555,-2.57096142343704,
13.8418824960098));
#441101=CARTESIAN_POINT('Ctrl Pts',(0.728635065873759,-2.57290670208555,
13.8392439765549));
#441102=CARTESIAN_POINT('Ctrl Pts',(0.727774562886895,-2.57484737227174,
13.8364981347964));
#441103=CARTESIAN_POINT('Ctrl Pts',(0.727103613305592,-2.57677469520582,
13.8336931113419));
#441104=CARTESIAN_POINT('Ctrl Pts',(0.72645015102264,-2.57865178534729,
13.8309611966328));
#441105=CARTESIAN_POINT('Ctrl Pts',(0.725976368281059,-2.58051828149001,
13.8281701127186));
#441106=CARTESIAN_POINT('Ctrl Pts',(0.725690535000416,-2.582364642916,13.8253580685121));
#441107=CARTESIAN_POINT('Ctrl Pts',(0.725628566036692,-2.58276493606581,
13.8247484142933));
#441108=CARTESIAN_POINT('Ctrl Pts',(0.725575588055282,-2.58316420941347,
13.8241378483365));
#441109=CARTESIAN_POINT('Ctrl Pts',(0.725531957228311,-2.58356219985525,
13.8235269408515));
#441110=CARTESIAN_POINT('',(0.75013538634949,-2.5542920279702,12.5969504640361));
#441111=CARTESIAN_POINT('Origin',(0.759711370193215,-2.5873400137128,12.584524458991));
#441112=CARTESIAN_POINT('Origin',(0.759711370193215,-2.5873400137128,12.584524458991));
#441113=CARTESIAN_POINT('Ctrl Pts',(0.786422857476923,-2.56568301836339,
12.5893111709658));
#441114=CARTESIAN_POINT('Ctrl Pts',(0.779292702402773,-2.55687282408754,
12.5770542771492));
#441115=CARTESIAN_POINT('Ctrl Pts',(0.764875628019623,-2.56461566859622,
12.5737548217797));
#441116=CARTESIAN_POINT('Ctrl Pts',(0.802014113672929,-2.5849479564556,
12.5663937883685));
#441117=CARTESIAN_POINT('Ctrl Pts',(0.794874863095769,-2.57612652355341,
12.5540940315304));
#441118=CARTESIAN_POINT('Ctrl Pts',(0.780414632473082,-2.58389619057666,
12.5508374392248));
#441119=CARTESIAN_POINT('Ctrl Pts',(0.817589638482575,-2.60419345646147,
12.5434499600945));
#441120=CARTESIAN_POINT('Ctrl Pts',(0.810427175659408,-2.5953433419395,
12.5311293540533));
#441121=CARTESIAN_POINT('Ctrl Pts',(0.795939373640742,-2.60315713469527,
12.5278936106989));
#441122=CARTESIAN_POINT('Ctrl Pts',(0.833150664166861,-2.62342104099285,
12.5204817579905));
#441123=CARTESIAN_POINT('Ctrl Pts',(0.825952752047599,-2.61452712445222,
12.5081597038247));
#441124=CARTESIAN_POINT('Ctrl Pts',(0.811450970907885,-2.62240001392627,
12.5049254088044));
#441125=CARTESIAN_POINT('Ctrl Pts',(0.821963002087479,-2.60959729166525,
12.5369868989719));
#441126=CARTESIAN_POINT('Ctrl Pts',(0.822549008438961,-2.61032137572581,
12.5342545179733));
#441127=CARTESIAN_POINT('Ctrl Pts',(0.823011297646569,-2.61109088583094,
12.5314872231885));
#441128=CARTESIAN_POINT('Ctrl Pts',(0.823275909632745,-2.61189126174693,
12.5287124745063));
#441129=CARTESIAN_POINT('Ctrl Pts',(0.823514549856045,-2.61261308047509,
12.5262100684184));
#441130=CARTESIAN_POINT('Ctrl Pts',(0.823591238015218,-2.6133595838334,
12.5237004536639));
#441131=CARTESIAN_POINT('Ctrl Pts',(0.823441347330567,-2.61415036405197,
12.5212220730815));
#441132=CARTESIAN_POINT('Ctrl Pts',(0.823326593044888,-2.61475577471723,
12.5193246583486));
#441133=CARTESIAN_POINT('Ctrl Pts',(0.823077040795667,-2.61539425439427,
12.517417831369));
#441134=CARTESIAN_POINT('Ctrl Pts',(0.822596926623588,-2.61604897195571,
12.5155812248348));
#441135=CARTESIAN_POINT('Ctrl Pts',(0.822392395405655,-2.61632788515601,
12.5147988205793));
#441136=CARTESIAN_POINT('Ctrl Pts',(0.822146037443724,-2.61661019217209,
12.5140295443047));
#441137=CARTESIAN_POINT('Ctrl Pts',(0.821851156866344,-2.61689659782483,
12.5132817086137));
#441138=CARTESIAN_POINT('Ctrl Pts',(0.821404895003024,-2.61733003403616,
12.5121499604604));
#441139=CARTESIAN_POINT('Ctrl Pts',(0.820832883672389,-2.61777708677856,
12.5110494206568));
#441140=CARTESIAN_POINT('Ctrl Pts',(0.820103968195602,-2.61821735299507,
12.5100666561695));
#441141=CARTESIAN_POINT('Ctrl Pts',(0.819685426607374,-2.61847015284274,
12.5095023550641));
#441142=CARTESIAN_POINT('Ctrl Pts',(0.819209979910961,-2.61872307728656,
12.5089719619137));
#441143=CARTESIAN_POINT('Ctrl Pts',(0.818683540169158,-2.61896574678444,
12.5085043804652));
#441144=CARTESIAN_POINT('Ctrl Pts',(0.817913164180629,-2.61932086198467,
12.5078201359221));
#441145=CARTESIAN_POINT('Ctrl Pts',(0.817010739985508,-2.61966321937794,
12.5072563000949));
#441146=CARTESIAN_POINT('Ctrl Pts',(0.816034435680754,-2.61996169666502,
12.5068768744332));
#441147=CARTESIAN_POINT('Ctrl Pts',(0.815330453068009,-2.62017691933625,
12.5066032824114));
#441148=CARTESIAN_POINT('Ctrl Pts',(0.814575706854735,-2.62037316554443,
12.5064197834844));
#441149=CARTESIAN_POINT('Ctrl Pts',(0.813812994503966,-2.62054197806549,
12.5063282718343));
#441150=CARTESIAN_POINT('Ctrl Pts',(0.812699670601618,-2.62078839208319,
12.5061946931565));
#441151=CARTESIAN_POINT('Ctrl Pts',(0.811545806847401,-2.62098265715127,
12.5062515701262));
#441152=CARTESIAN_POINT('Ctrl Pts',(0.810425581539696,-2.6211279667473,
12.5064436508398));
#441153=CARTESIAN_POINT('',(0.764875628019623,-2.56461566859622,12.5737548217797));
#441154=CARTESIAN_POINT('Origin',(0.769321660262949,-2.5795231431406,12.5893111709658));
#441155=CARTESIAN_POINT('Ctrl Pts',(0.810425581539697,-2.6211279667473,
12.5064436508398));
#441156=CARTESIAN_POINT('Ctrl Pts',(0.803682630942583,-2.61276297989757,
12.5164271754438));
#441157=CARTESIAN_POINT('Ctrl Pts',(0.796937170108206,-2.60439454604452,
12.5264061185523));
#441158=CARTESIAN_POINT('Ctrl Pts',(0.790189109891219,-2.5960225443816,
12.536380305637));
#441159=CARTESIAN_POINT('Ctrl Pts',(0.781755403274068,-2.58555924032784,
12.5488460165097));
#441160=CARTESIAN_POINT('Ctrl Pts',(0.773317633967052,-2.57509036027389,
12.5613043021964));
#441161=CARTESIAN_POINT('Ctrl Pts',(0.764875628019623,-2.56461566859622,
12.5737548217797));
#441162=CARTESIAN_POINT('Ctrl Pts',(0.725531957228311,-2.58356219985525,
12.5893111709658));
#441163=CARTESIAN_POINT('Ctrl Pts',(0.726767074738834,-2.57229573992789,
12.5770542771492));
#441164=CARTESIAN_POINT('Ctrl Pts',(0.743081587281356,-2.57101497634515,
12.5737548217797));
#441165=CARTESIAN_POINT('Ctrl Pts',(0.726684311123145,-2.57305069073351,
12.5928319619712));
#441166=CARTESIAN_POINT('Ctrl Pts',(0.730752727515209,-2.56583394600807,
12.5821634970842));
#441167=CARTESIAN_POINT('Ctrl Pts',(0.743491979270983,-2.56718485940383,
12.5773203894503));
#441168=CARTESIAN_POINT('Ctrl Pts',(0.735288391592189,-2.55867870761977,
12.5969440695591));
#441169=CARTESIAN_POINT('Ctrl Pts',(0.739140143388078,-2.55752868559616,
12.5878292599214));
#441170=CARTESIAN_POINT('Ctrl Pts',(0.746560404562759,-2.56206344228292,
12.5813877129824));
#441171=CARTESIAN_POINT('Ctrl Pts',(0.764630742119066,-2.55000681560595,
12.596957478804));
#441172=CARTESIAN_POINT('Ctrl Pts',(0.760807478734539,-2.55114841546642,
12.5878468778671));
#441173=CARTESIAN_POINT('Ctrl Pts',(0.757064129213709,-2.55896537243845,
12.5814011370086));
#441174=CARTESIAN_POINT('Ctrl Pts',(0.779760825573947,-2.55745124854529,
12.5928371701607));
#441175=CARTESIAN_POINT('Ctrl Pts',(0.772439009440422,-2.55358782076535,
12.5821692192951));
#441176=CARTESIAN_POINT('Ctrl Pts',(0.7624521379921,-2.56160568959954,12.5773318885715));
#441177=CARTESIAN_POINT('Ctrl Pts',(0.786422857476964,-2.56568301836335,
12.5893111709658));
#441178=CARTESIAN_POINT('Ctrl Pts',(0.779292702402813,-2.5568728240875,
12.5770542771492));
#441179=CARTESIAN_POINT('Ctrl Pts',(0.764875628019665,-2.56461566859618,
12.5737548217797));
#441180=CARTESIAN_POINT('',(0.743081587281356,-2.57101497634515,12.5737548217797));
#441181=CARTESIAN_POINT('Origin',(0.747400936173448,-2.58595964847767,12.5893111709658));
#441182=CARTESIAN_POINT('Ctrl Pts',(0.764875628019665,-2.56461566859618,
12.5737548217797));
#441183=CARTESIAN_POINT('Ctrl Pts',(0.764270917286879,-2.56381651619478,
12.5746934679442));
#441184=CARTESIAN_POINT('Ctrl Pts',(0.763455687590138,-2.56304273587727,
12.5756680099006));
#441185=CARTESIAN_POINT('Ctrl Pts',(0.762524981384661,-2.56237994659924,
12.5765688348656));
#441186=CARTESIAN_POINT('Ctrl Pts',(0.762278587220015,-2.56220448047521,
12.5768073183026));
#441187=CARTESIAN_POINT('Ctrl Pts',(0.762024295293087,-2.56203662653245,
12.5770407398754));
#441188=CARTESIAN_POINT('Ctrl Pts',(0.761764192010584,-2.5618775120286,
12.5772674179684));
#441189=CARTESIAN_POINT('Ctrl Pts',(0.760696798474097,-2.56122454913118,
12.5781976435658));
#441190=CARTESIAN_POINT('Ctrl Pts',(0.759465026586396,-2.56069129919031,
12.5790594849312));
#441191=CARTESIAN_POINT('Ctrl Pts',(0.758132863074708,-2.56035808289148,
12.5797571720116));
#441192=CARTESIAN_POINT('Ctrl Pts',(0.757264910646512,-2.5601409804914,
12.580211740231));
#441193=CARTESIAN_POINT('Ctrl Pts',(0.756310342698694,-2.56001713779551,
12.5806009430798));
#441194=CARTESIAN_POINT('Ctrl Pts',(0.755334077257052,-2.56001284224241,
12.5808812374708));
#441195=CARTESIAN_POINT('Ctrl Pts',(0.754495141369994,-2.56000915093727,
12.5811221033394));
#441196=CARTESIAN_POINT('Ctrl Pts',(0.753623007189356,-2.56009377790496,
12.581287365893));
#441197=CARTESIAN_POINT('Ctrl Pts',(0.752767704662216,-2.56027024566553,
12.581359338449));
#441198=CARTESIAN_POINT('Ctrl Pts',(0.752648835272265,-2.56029477104033,
12.5813693411482));
#441199=CARTESIAN_POINT('Ctrl Pts',(0.752530260037864,-2.56032101908682,
12.5813775999465));
#441200=CARTESIAN_POINT('Ctrl Pts',(0.752412080625663,-2.56034894732016,
12.5813841266931));
#441201=CARTESIAN_POINT('Ctrl Pts',(0.752211574959359,-2.56039633094586,
12.5813952001081));
#441202=CARTESIAN_POINT('Ctrl Pts',(0.752011005816987,-2.56044946093023,
12.5814007534795));
#441203=CARTESIAN_POINT('Ctrl Pts',(0.751810511051359,-2.5605085047682,
12.5814005856065));
#441204=CARTESIAN_POINT('Ctrl Pts',(0.750892724402688,-2.5607787843738,
12.5813998171494));
#441205=CARTESIAN_POINT('Ctrl Pts',(0.750039812948028,-2.56115398785352,
12.58127954464));
#441206=CARTESIAN_POINT('Ctrl Pts',(0.7492447042488,-2.56160490055409,12.5810700125799));
#441207=CARTESIAN_POINT('Ctrl Pts',(0.748284303470506,-2.56214955175587,
12.5808169217085));
#441208=CARTESIAN_POINT('Ctrl Pts',(0.747416405376494,-2.56281926905284,
12.5804173076348));
#441209=CARTESIAN_POINT('Ctrl Pts',(0.746701161405496,-2.56353474192417,
12.5799304713245));
#441210=CARTESIAN_POINT('Ctrl Pts',(0.745814748800342,-2.56442143820894,
12.5793271277669));
#441211=CARTESIAN_POINT('Ctrl Pts',(0.74508503942716,-2.56541064851979,
12.5785808224116));
#441212=CARTESIAN_POINT('Ctrl Pts',(0.744517268174651,-2.56644184766051,
12.5777485681082));
#441213=CARTESIAN_POINT('Ctrl Pts',(0.743671226804427,-2.56797844735649,
12.576508418016));
#441214=CARTESIAN_POINT('Ctrl Pts',(0.743185860889815,-2.56959202705384,
12.5750928681475));
#441215=CARTESIAN_POINT('Ctrl Pts',(0.743081587281356,-2.57101497634515,
12.5737548217797));
#441216=CARTESIAN_POINT('Ctrl Pts',(0.743081587281356,-2.57101497634515,
12.5737548217797));
#441217=CARTESIAN_POINT('Ctrl Pts',(0.726767074738834,-2.57229573992789,
12.5770542771492));
#441218=CARTESIAN_POINT('Ctrl Pts',(0.725531957228311,-2.58356219985525,
12.5893111709658));
#441219=CARTESIAN_POINT('Ctrl Pts',(0.740433579933582,-2.59563210475723,
12.5508408821982));
#441220=CARTESIAN_POINT('Ctrl Pts',(0.72406826870519,-2.59691363237191,
12.55409748406));
#441221=CARTESIAN_POINT('Ctrl Pts',(0.72283157550105,-2.60819446541667,
12.5663972313419));
#441222=CARTESIAN_POINT('Ctrl Pts',(0.737786986607698,-2.62022505918647,
12.52790050457));
#441223=CARTESIAN_POINT('Ctrl Pts',(0.721374631527474,-2.62148437569243,
12.5311362602938));
#441224=CARTESIAN_POINT('Ctrl Pts',(0.720133918015219,-2.63280188106977,
12.5434568539655));
#441225=CARTESIAN_POINT('Ctrl Pts',(0.735141683647397,-2.64479571678053,
12.5049357605811));
#441226=CARTESIAN_POINT('Ctrl Pts',(0.718685624378847,-2.64601288494447,
12.5081700652078));
#441227=CARTESIAN_POINT('Ctrl Pts',(0.717438771407679,-2.65738639306438,
12.5204921097672));
#441228=CARTESIAN_POINT('Ctrl Pts',(0.73531538303103,-2.64318231091899,
12.5064436508395));
#441229=CARTESIAN_POINT('Ctrl Pts',(0.734212568288885,-2.64370446744255,
12.5062361689309));
#441230=CARTESIAN_POINT('Ctrl Pts',(0.733043465289341,-2.64420044102743,
12.5061871075061));
#441231=CARTESIAN_POINT('Ctrl Pts',(0.731886658499308,-2.64461615089218,
12.5063648335164));
#441232=CARTESIAN_POINT('Ctrl Pts',(0.731361165500473,-2.64480499195479,
12.5064455676329));
#441233=CARTESIAN_POINT('Ctrl Pts',(0.730830805828037,-2.64497969691044,
12.506574497099));
#441234=CARTESIAN_POINT('Ctrl Pts',(0.730317990902744,-2.64513177674755,
12.5067492519495));
#441235=CARTESIAN_POINT('Ctrl Pts',(0.729287469404289,-2.64543738708354,
12.5071004286051));
#441236=CARTESIAN_POINT('Ctrl Pts',(0.72828967953303,-2.64566209299121,
12.5076537929613));
#441237=CARTESIAN_POINT('Ctrl Pts',(0.727401588684731,-2.64579825646475,
12.5083435010505));
#441238=CARTESIAN_POINT('Ctrl Pts',(0.727345678058567,-2.64580682876913,
12.5083869222964));
#441239=CARTESIAN_POINT('Ctrl Pts',(0.727290194313603,-2.64581503927738,
12.5084308732337));
#441240=CARTESIAN_POINT('Ctrl Pts',(0.727235153116011,-2.64582288189328,
12.5084753333615));
#441241=CARTESIAN_POINT('Ctrl Pts',(0.72679365006355,-2.64588579002413,
12.5088319622689));
#441242=CARTESIAN_POINT('Ctrl Pts',(0.726371839947139,-2.64592758170536,
12.509227847131));
#441243=CARTESIAN_POINT('Ctrl Pts',(0.725982541449329,-2.64594980066293,
12.5096423454524));
#441244=CARTESIAN_POINT('Ctrl Pts',(0.72476265225349,-2.64601942504223,
12.5109411997424));
#441245=CARTESIAN_POINT('Ctrl Pts',(0.72378752049948,-2.64591079653777,
12.5124831113042));
#441246=CARTESIAN_POINT('Ctrl Pts',(0.723009761835327,-2.64570583328299,
12.5140723025007));
#441247=CARTESIAN_POINT('Ctrl Pts',(0.722936884996639,-2.64568662800152,
12.5142212114565));
#441248=CARTESIAN_POINT('Ctrl Pts',(0.722865718184468,-2.64566659569232,
12.5143705582413));
#441249=CARTESIAN_POINT('Ctrl Pts',(0.722796210323367,-2.64564581567146,
12.5145201959299));
#441250=CARTESIAN_POINT('Ctrl Pts',(0.721903278361162,-2.64537886536533,
12.5164425148273));
#441251=CARTESIAN_POINT('Ctrl Pts',(0.721250455980803,-2.64498966012505,
12.5184635205941));
#441252=CARTESIAN_POINT('Ctrl Pts',(0.720758552358941,-2.6445214063396,
12.5205025929158));
#441253=CARTESIAN_POINT('Ctrl Pts',(0.720473228761024,-2.6442498005842,
12.5216853356836));
#441254=CARTESIAN_POINT('Ctrl Pts',(0.720242227640543,-2.64395244013477,
12.5228750347131));
#441255=CARTESIAN_POINT('Ctrl Pts',(0.720053228377979,-2.64364278366818,
12.5240609649613));
#441256=CARTESIAN_POINT('Ctrl Pts',(0.719589339827475,-2.64288274848343,
12.5269717671326));
#441257=CARTESIAN_POINT('Ctrl Pts',(0.719374301150302,-2.64202183190473,
12.5299036066169));
#441258=CARTESIAN_POINT('Ctrl Pts',(0.719328508168226,-2.64109427860225,
12.5328133004019));
#441259=CARTESIAN_POINT('Ctrl Pts',(0.719306524870384,-2.64064899900724,
12.5342101228451));
#441260=CARTESIAN_POINT('Ctrl Pts',(0.719324096111705,-2.64018889232598,
12.5356023438238));
#441261=CARTESIAN_POINT('Ctrl Pts',(0.719375533633238,-2.6397196902469,
12.5369868989719));
#441262=CARTESIAN_POINT('Origin',(-0.674793679548759,-15.3084091091921,
-1.23987515702209));
#441263=CARTESIAN_POINT('Ctrl Pts',(0.821936740326726,-2.60956477888538,
12.5369868989719));
#441264=CARTESIAN_POINT('Ctrl Pts',(0.831563750894994,-2.62150646935213,
12.5369868989719));
#441265=CARTESIAN_POINT('Ctrl Pts',(0.846097674417172,-2.61660255553389,
12.5369868989719));
#441266=CARTESIAN_POINT('Ctrl Pts',(0.825191097956303,-2.61360149574402,
12.5218025310016));
#441267=CARTESIAN_POINT('Ctrl Pts',(0.834891989456039,-2.62035046365142,
12.5216901060417));
#441268=CARTESIAN_POINT('Ctrl Pts',(0.846053375474105,-2.61661751991462,
12.5161920673677));
#441269=CARTESIAN_POINT('Ctrl Pts',(0.823586269307168,-2.61941188266763,
12.5042015548895));
#441270=CARTESIAN_POINT('Ctrl Pts',(0.829457255023867,-2.62204035593764,
12.4980677368514));
#441271=CARTESIAN_POINT('Ctrl Pts',(0.835935296554527,-2.61998469116661,
12.4907278922778));
#441272=CARTESIAN_POINT('Ctrl Pts',(0.81041967336277,-2.62110885819555,
12.506463626192));
#441273=CARTESIAN_POINT('Ctrl Pts',(0.812352348575499,-2.62735963453601,
12.4999376786891));
#441274=CARTESIAN_POINT('Ctrl Pts',(0.812328743757883,-2.62728329039163,
12.4906970594712));
#441275=CARTESIAN_POINT('Origin',(0.839064199301453,-2.59575716688804,12.5369868989719));
#441276=CARTESIAN_POINT('Origin',(0.839064199301453,-2.59575716688804,14.));
#441277=CARTESIAN_POINT('Origin',(0.839064199301453,-2.59575716688804,13.7435492065112));
#441278=CARTESIAN_POINT('Ctrl Pts',(0.806386526442056,-2.59035057362389,
13.793642941384));
#441279=CARTESIAN_POINT('Ctrl Pts',(0.813167336811863,-2.5987723804214,
13.8071662555867));
#441280=CARTESIAN_POINT('Ctrl Pts',(0.827858210662747,-2.59015857701453,
13.8103758687955));
#441281=CARTESIAN_POINT('Ctrl Pts',(0.816842815313936,-2.60327062502669,
13.7804579775006));
#441282=CARTESIAN_POINT('Ctrl Pts',(0.82521762117959,-2.61365601372629,
13.7901904343352));
#441283=CARTESIAN_POINT('Ctrl Pts',(0.839919976902593,-2.60799062226948,
13.7927914348262));
#441284=CARTESIAN_POINT('Ctrl Pts',(0.822998826116797,-2.61087714549983,
13.7597120340895));
#441285=CARTESIAN_POINT('Ctrl Pts',(0.832695295726823,-2.62289236780633,
13.7635825532445));
#441286=CARTESIAN_POINT('Ctrl Pts',(0.847053960171936,-2.61849183698646,
13.7651073818885));
#441287=CARTESIAN_POINT('Ctrl Pts',(0.821793338245602,-2.60938761462116,
13.7381884353898));
#441288=CARTESIAN_POINT('Ctrl Pts',(0.83126214444869,-2.62112216274687,
13.7368803041982));
#441289=CARTESIAN_POINT('Ctrl Pts',(0.845657323078979,-2.6164351093739,
13.7363986145813));
#441290=CARTESIAN_POINT('Origin',(0.826024902936919,-2.57964549287853,13.7902182540695));
#441291=CARTESIAN_POINT('Ctrl Pts',(0.786420381817885,-2.56567995817206,
13.8235227101244));
#441292=CARTESIAN_POINT('Ctrl Pts',(0.793649704393192,-2.5746197335284,
13.8358800583119));
#441293=CARTESIAN_POINT('Ctrl Pts',(0.808196285377077,-2.56668102892776,
13.8390832900376));
#441294=CARTESIAN_POINT('Ctrl Pts',(0.793923981208646,-2.57495158939197,
13.8124254819053));
#441295=CARTESIAN_POINT('Ctrl Pts',(0.801167343242206,-2.58390872549045,
13.8247886449158));
#441296=CARTESIAN_POINT('Ctrl Pts',(0.81572413941509,-2.57594502871794,
13.8279860620657));
#441297=CARTESIAN_POINT('Ctrl Pts',(0.801424217730241,-2.58421906536838,
13.8013225099954));
#441298=CARTESIAN_POINT('Ctrl Pts',(0.808678199959595,-2.59318933713958,
13.8136962257787));
#441299=CARTESIAN_POINT('Ctrl Pts',(0.823248298065882,-2.58520491066953,
13.8168830918626));
#441300=CARTESIAN_POINT('Ctrl Pts',(0.808921222226775,-2.59348254777547,
13.7902140179785));
#441301=CARTESIAN_POINT('Ctrl Pts',(0.816182628865665,-2.60246200628751,
13.802602731458));
#441302=CARTESIAN_POINT('Ctrl Pts',(0.830768905102013,-2.59446083774294,
13.8057746032558));
#441303=CARTESIAN_POINT('Origin',(0.803524054690898,-2.55184289358618,13.8235269408515));
#441304=CARTESIAN_POINT('Ctrl Pts',(0.725531957228311,-2.58356219985525,
13.8235269408515));
#441305=CARTESIAN_POINT('Ctrl Pts',(0.724245237673885,-2.59529936184524,
13.8362179249168));
#441306=CARTESIAN_POINT('Ctrl Pts',(0.707191314275894,-2.59620859272501,
13.8391868794938));
#441307=CARTESIAN_POINT('Ctrl Pts',(0.726709249613043,-2.57282320752265,
13.8400110824519));
#441308=CARTESIAN_POINT('Ctrl Pts',(0.722276990282717,-2.58186073705733,
13.8494522556837));
#441309=CARTESIAN_POINT('Ctrl Pts',(0.709240492959898,-2.57854748714394,
13.85569149686));
#441310=CARTESIAN_POINT('Ctrl Pts',(0.73495824762352,-2.55877501340853,
13.8586819406588));
#441311=CARTESIAN_POINT('Ctrl Pts',(0.730784695111075,-2.56001497431954,
13.868010383617));
#441312=CARTESIAN_POINT('Ctrl Pts',(0.723059893033655,-2.55530113303484,
13.8744918421245));
#441313=CARTESIAN_POINT('Ctrl Pts',(0.764966001190711,-2.54990899830604,
13.8587686893867));
#441314=CARTESIAN_POINT('Ctrl Pts',(0.769102393088287,-2.54868001905906,
13.8680909899357));
#441315=CARTESIAN_POINT('Ctrl Pts',(0.773014719528825,-2.54054428901632,
13.8745789365163));
#441316=CARTESIAN_POINT('Ctrl Pts',(0.779615459250033,-2.5572716303441,
13.8400379222776));
#441317=CARTESIAN_POINT('Ctrl Pts',(0.788231675728506,-2.56247076945594,
13.8494748685453));
#441318=CARTESIAN_POINT('Ctrl Pts',(0.797403990081898,-2.55264072598367,
13.8557104837033));
#441319=CARTESIAN_POINT('Ctrl Pts',(0.786422857481969,-2.56568301835912,
13.8235269408542));
#441320=CARTESIAN_POINT('Ctrl Pts',(0.793850903705796,-2.57486129423682,
13.8362179249195));
#441321=CARTESIAN_POINT('Ctrl Pts',(0.808689144339033,-2.56640614083984,
13.8391868794965));
#441322=CARTESIAN_POINT('Origin',(0.703662978283174,-2.58116475123283,13.8235269408515));
#441323=CARTESIAN_POINT('Ctrl Pts',(0.721634688079212,-2.61911219223003,
13.7902140241682));
#441324=CARTESIAN_POINT('Ctrl Pts',(0.72038065990436,-2.63059200097101,
13.8026027327198));
#441325=CARTESIAN_POINT('Ctrl Pts',(0.703784151790531,-2.63174692551464,
13.8057746032556));
#441326=CARTESIAN_POINT('Ctrl Pts',(0.722933352896948,-2.60726606828531,
13.8013225161808));
#441327=CARTESIAN_POINT('Ctrl Pts',(0.721680603817138,-2.61873413471468,
13.8136962270464));
#441328=CARTESIAN_POINT('Ctrl Pts',(0.705106757049487,-2.61989439702825,
13.8168830918628));
#441329=CARTESIAN_POINT('Ctrl Pts',(0.72423257758078,-2.59541483737002,
13.8124254880875));
#441330=CARTESIAN_POINT('Ctrl Pts',(0.722981661108411,-2.60686611166678,
13.8247886461868));
#441331=CARTESIAN_POINT('Ctrl Pts',(0.706430211948158,-2.60803662133964,
13.8279860620656));
#441332=CARTESIAN_POINT('Ctrl Pts',(0.725532384796289,-2.58355829273389,
13.8235227163065));
#441333=CARTESIAN_POINT('Ctrl Pts',(0.724283893152617,-2.59498737195546,
13.8358800595847));
#441334=CARTESIAN_POINT('Ctrl Pts',(0.707754549332814,-2.59617338362708,
13.8390832900376));
#441335=CARTESIAN_POINT('Origin',(0.699765280213318,-2.61671866309858,13.7902182540695));
#441336=CARTESIAN_POINT('Ctrl Pts',(0.719404914178971,-2.63945143449022,
13.7382347919292));
#441337=CARTESIAN_POINT('Ctrl Pts',(0.717784306570684,-2.65445448417065,
13.7369371795943));
#441338=CARTESIAN_POINT('Ctrl Pts',(0.703126890298583,-2.65828905393098,
13.7364597369711));
#441339=CARTESIAN_POINT('Ctrl Pts',(0.719198782097412,-2.6413317279644,
13.7595490285574));
#441340=CARTESIAN_POINT('Ctrl Pts',(0.71753850857087,-2.65669262957323,
13.7633824266926));
#441341=CARTESIAN_POINT('Ctrl Pts',(0.703065061656196,-2.66074392500999,
13.7648920890506));
#441342=CARTESIAN_POINT('Ctrl Pts',(0.720250044428475,-2.63174233425766,
13.780380659011));
#441343=CARTESIAN_POINT('Ctrl Pts',(0.718819334450415,-2.64502954446009,
13.7901039518744));
#441344=CARTESIAN_POINT('Ctrl Pts',(0.703383982415013,-2.64822881765391,
13.7926933640892));
#441345=CARTESIAN_POINT('Ctrl Pts',(0.722077372954516,-2.61507382736496,
13.7936647693663));
#441346=CARTESIAN_POINT('Ctrl Pts',(0.720928562832835,-2.62582806221682,
13.8072068914933));
#441347=CARTESIAN_POINT('Ctrl Pts',(0.70389408990918,-2.62651435811564,
13.8104111085397));
#441348=CARTESIAN_POINT('Origin',(0.6975065546881,-2.63732224162447,13.7435492065112));
#441349=CARTESIAN_POINT('Origin',(0.697506554688101,-2.63732224162448,14.));
#441350=CARTESIAN_POINT('Origin',(0.697506554688101,-2.63732224162448,12.5369868989719));
#441351=CARTESIAN_POINT('Ctrl Pts',(0.735310456050207,-2.6431646002371,
12.506462012331));
#441352=CARTESIAN_POINT('Ctrl Pts',(0.737062907725849,-2.64946400505934,
12.4999388158272));
#441353=CARTESIAN_POINT('Ctrl Pts',(0.737042173924327,-2.64938947483913,
12.4907030323752));
#441354=CARTESIAN_POINT('Ctrl Pts',(0.723316048698657,-2.64885342924135,
12.5042014951932));
#441355=CARTESIAN_POINT('Ctrl Pts',(0.719800462179154,-2.65423689917626,
12.4980716682127));
#441356=CARTESIAN_POINT('Ctrl Pts',(0.713244453351888,-2.65601012039275,
12.4907355092743));
#441357=CARTESIAN_POINT('Ctrl Pts',(0.718823723546654,-2.64483538046438,
12.5218047446509));
#441358=CARTESIAN_POINT('Ctrl Pts',(0.714312756107054,-2.65575188373671,
12.5216906929434));
#441359=CARTESIAN_POINT('Ctrl Pts',(0.702911729540246,-2.65864797550892,
12.5161988840776));
#441360=CARTESIAN_POINT('Ctrl Pts',(0.719379686685556,-2.63968149926658,
12.5369868989719));
#441361=CARTESIAN_POINT('Ctrl Pts',(0.717735724846863,-2.65492298610329,
12.5369868989719));
#441362=CARTESIAN_POINT('Ctrl Pts',(0.702868034741916,-2.6586589361115,
12.5369868989719));
#441363=CARTESIAN_POINT('Origin',(1.45144742314195E-31,-1.0095038568149E-30,
12.5));
#441364=CARTESIAN_POINT('Origin',(0.933702113402283,-2.51582801973993,12.5));
#441365=CARTESIAN_POINT('',(0.933702113402283,-2.51582801973993,12.5893111709658));
#441366=CARTESIAN_POINT('',(0.933702113402283,-2.51582801973993,13.8235269408515));
#441367=CARTESIAN_POINT('',(0.933702113402283,-2.51582801973993,12.5));
#441368=CARTESIAN_POINT('',(0.93271535848469,-2.5515813274741,13.7902182540695));
#441369=CARTESIAN_POINT('',(0.933702113402283,-2.51582801973993,13.8235269408515));
#441370=CARTESIAN_POINT('',(0.932143531606478,-2.57230045639141,13.7435492065112));
#441371=CARTESIAN_POINT('Origin',(0.934025160108408,-2.50413480510781,13.7445212918703));
#441372=CARTESIAN_POINT('',(0.932143531606478,-2.57230045639141,12.5369868989719));
#441373=CARTESIAN_POINT('',(0.932143531606478,-2.57230045639141,12.5));
#441374=CARTESIAN_POINT('Ctrl Pts',(0.932143531606478,-2.57230045639141,
12.5369868989719));
#441375=CARTESIAN_POINT('Ctrl Pts',(0.932662679960157,-2.55349004002777,
12.5544431401645));
#441376=CARTESIAN_POINT('Ctrl Pts',(0.933182199622538,-2.5346661699544,
12.5718848856037));
#441377=CARTESIAN_POINT('Ctrl Pts',(0.933702113402283,-2.51582801973993,
12.5893111709658));
#441378=CARTESIAN_POINT('Origin',(1.18278282538531,-2.69199760279828,12.5));
#441379=CARTESIAN_POINT('',(1.0319343935952,-2.53391645655151,13.7435492065112));
#441380=CARTESIAN_POINT('',(1.01762523340839,-2.51892121651278,13.7902182540695));
#441381=CARTESIAN_POINT('Origin',(0.980023233558798,-2.47951631739082,13.7418732680453));
#441382=CARTESIAN_POINT('',(0.992933084929655,-2.49304515609576,13.8235269408515));
#441383=CARTESIAN_POINT('',(1.01762523340839,-2.51892121651278,13.7902182540695));
#441384=CARTESIAN_POINT('',(0.992933084929655,-2.49304515609576,12.5893111709658));
#441385=CARTESIAN_POINT('',(0.992933084929655,-2.49304515609576,12.5));
#441386=CARTESIAN_POINT('',(1.0319343935952,-2.53391645655151,12.5369868989719));
#441387=CARTESIAN_POINT('Ctrl Pts',(0.992933084929655,-2.49304515609576,
12.5893111709658));
#441388=CARTESIAN_POINT('Ctrl Pts',(1.00594319313052,-2.50667905863476,
12.5718848856037));
#441389=CARTESIAN_POINT('Ctrl Pts',(1.01894343910083,-2.52030262607983,
12.5544431401645));
#441390=CARTESIAN_POINT('Ctrl Pts',(1.0319343935952,-2.53391645655151,12.5369868989719));
#441391=CARTESIAN_POINT('',(1.0319343935952,-2.53391645655151,12.5));
#441392=CARTESIAN_POINT('Origin',(0.968064029091839,-2.51677637365271,12.5));
#441393=CARTESIAN_POINT('',(0.954685208566533,-2.48511255623394,13.8587068136939));
#441394=CARTESIAN_POINT('Ctrl Pts',(0.992933084934336,-2.49304515609109,
13.8235269408542));
#441395=CARTESIAN_POINT('Ctrl Pts',(0.991723363543063,-2.491777432311,13.8262006681044));
#441396=CARTESIAN_POINT('Ctrl Pts',(0.990359696394175,-2.49060004539963,
13.8288634856214));
#441397=CARTESIAN_POINT('Ctrl Pts',(0.988854254011685,-2.48950754701841,
13.8314912288862));
#441398=CARTESIAN_POINT('Ctrl Pts',(0.987302298194516,-2.48838129387334,
13.834200161153));
#441399=CARTESIAN_POINT('Ctrl Pts',(0.985598238984165,-2.48734360273377,
13.8368750301949));
#441400=CARTESIAN_POINT('Ctrl Pts',(0.983715583286505,-2.48640988080418,
13.8394886372968));
#441401=CARTESIAN_POINT('Ctrl Pts',(0.983570181220282,-2.48633776719466,
13.839690492513));
#441402=CARTESIAN_POINT('Ctrl Pts',(0.983423700740891,-2.48626629159546,
13.8398919674349));
#441403=CARTESIAN_POINT('Ctrl Pts',(0.983276123704499,-2.48619547088669,
13.8400930404591));
#441404=CARTESIAN_POINT('Ctrl Pts',(0.980976774192673,-2.48509203659824,
13.8432258934518));
#441405=CARTESIAN_POINT('Ctrl Pts',(0.978423447081325,-2.48415219749209,
13.8462331177034));
#441406=CARTESIAN_POINT('Ctrl Pts',(0.975666096106158,-2.48349713443913,
13.8489036603661));
#441407=CARTESIAN_POINT('Ctrl Pts',(0.974763858778177,-2.48328279018485,
13.8497774930041));
#441408=CARTESIAN_POINT('Ctrl Pts',(0.973839948934597,-2.4830991177115,
13.85061494757));
#441409=CARTESIAN_POINT('Ctrl Pts',(0.972896615947958,-2.4829508726377,
13.8514076489583));
#441410=CARTESIAN_POINT('Ctrl Pts',(0.970901330632243,-2.48263731292648,
13.8530843267192));
#441411=CARTESIAN_POINT('Ctrl Pts',(0.968622700636087,-2.48245437182213,
13.8546805203176));
#441412=CARTESIAN_POINT('Ctrl Pts',(0.966182057338866,-2.48254867523269,
13.8559412814273));
#441413=CARTESIAN_POINT('Ctrl Pts',(0.965855420113751,-2.48256129608735,
13.8561100121513));
#441414=CARTESIAN_POINT('Ctrl Pts',(0.965525928528726,-2.48257882230831,
13.8562727473908));
#441415=CARTESIAN_POINT('Ctrl Pts',(0.965193912474154,-2.48260154034592,
13.8564289040185));
#441416=CARTESIAN_POINT('Ctrl Pts',(0.963688223454477,-2.48270456638732,
13.8571370725437));
#441417=CARTESIAN_POINT('Ctrl Pts',(0.962104305481676,-2.48291844998919,
13.8577210840554));
#441418=CARTESIAN_POINT('Ctrl Pts',(0.96050765308351,-2.48326396153404,
13.8581177131616));
#441419=CARTESIAN_POINT('Ctrl Pts',(0.960057980813083,-2.48336126947722,
13.8582294175695));
#441420=CARTESIAN_POINT('Ctrl Pts',(0.959607295647674,-2.48346884028903,
13.8583265086086));
#441421=CARTESIAN_POINT('Ctrl Pts',(0.95915702743171,-2.48358669962459,
13.8584082369006));
#441422=CARTESIAN_POINT('Ctrl Pts',(0.958510112749561,-2.48375603188456,
13.8585256585398));
#441423=CARTESIAN_POINT('Ctrl Pts',(0.957856097938983,-2.4839490197037,
13.8586122832068));
#441424=CARTESIAN_POINT('Ctrl Pts',(0.957212195904303,-2.48416140721831,
13.8586682984299));
#441425=CARTESIAN_POINT('Ctrl Pts',(0.956697138104515,-2.48433129617669,
13.8587131050557));
#441426=CARTESIAN_POINT('Ctrl Pts',(0.956182788610058,-2.48451525160693,
13.8587357943552));
#441427=CARTESIAN_POINT('Ctrl Pts',(0.955669256851426,-2.4847137722332,
13.8587355499465));
#441428=CARTESIAN_POINT('Ctrl Pts',(0.955337349032966,-2.48484208084679,
13.8587353919793));
#441429=CARTESIAN_POINT('Ctrl Pts',(0.955009358073341,-2.48497505026233,
13.8587257282814));
#441430=CARTESIAN_POINT('Ctrl Pts',(0.954685208566533,-2.48511255623394,
13.8587068136939));
#441431=CARTESIAN_POINT('Ctrl Pts',(0.954685208566533,-2.48511255623394,
13.8587068136939));
#441432=CARTESIAN_POINT('Ctrl Pts',(0.953619098508562,-2.48556480587889,
13.8586446046467));
#441433=CARTESIAN_POINT('Ctrl Pts',(0.952594490131804,-2.48606606798737,
13.8584824279291));
#441434=CARTESIAN_POINT('Ctrl Pts',(0.951609148388065,-2.4866124708005,
13.8582284286032));
#441435=CARTESIAN_POINT('Ctrl Pts',(0.950598302378936,-2.48717301652643,
13.8579678548414));
#441436=CARTESIAN_POINT('Ctrl Pts',(0.949627055603989,-2.48778377876022,
13.857615680862));
#441437=CARTESIAN_POINT('Ctrl Pts',(0.948728540580012,-2.48841247603173,
13.8571944833187));
#441438=CARTESIAN_POINT('Ctrl Pts',(0.94648620444509,-2.48998145437067,
13.8561433417727));
#441439=CARTESIAN_POINT('Ctrl Pts',(0.944589205204621,-2.49173159547621,
13.8546163505474));
#441440=CARTESIAN_POINT('Ctrl Pts',(0.943031722982616,-2.49345620151167,
13.8528973491086));
#441441=CARTESIAN_POINT('Ctrl Pts',(0.942747193959171,-2.49377126159015,
13.8525833129072));
#441442=CARTESIAN_POINT('Ctrl Pts',(0.942473859162767,-2.49408543390456,
13.8522628768812));
#441443=CARTESIAN_POINT('Ctrl Pts',(0.94221150514556,-2.49439744083207,
13.851937733538));
#441444=CARTESIAN_POINT('Ctrl Pts',(0.940609345562412,-2.49630282384938,
13.8499521282529));
#441445=CARTESIAN_POINT('Ctrl Pts',(0.939260597355519,-2.49831943535962,
13.847639871647));
#441446=CARTESIAN_POINT('Ctrl Pts',(0.938169364659963,-2.50029662525464,
13.8452109780794));
#441447=CARTESIAN_POINT('Ctrl Pts',(0.937678396482841,-2.5011862039142,
13.8441181685877));
#441448=CARTESIAN_POINT('Ctrl Pts',(0.937238847234745,-2.50206769441421,
13.8430021611332));
#441449=CARTESIAN_POINT('Ctrl Pts',(0.936847826073116,-2.50292791449968,
13.8418824960098));
#441450=CARTESIAN_POINT('Ctrl Pts',(0.935926374720656,-2.50495504509759,
13.8392439765549));
#441451=CARTESIAN_POINT('Ctrl Pts',(0.935226917622972,-2.50695939684577,
13.8364981347964));
#441452=CARTESIAN_POINT('Ctrl Pts',(0.934715295282572,-2.50893499539145,
13.8336931113419));
#441453=CARTESIAN_POINT('Ctrl Pts',(0.934217007614046,-2.51085910291283,
13.8309611966328));
#441454=CARTESIAN_POINT('Ctrl Pts',(0.933896938108789,-2.51275800613543,
13.8281701127186));
#441455=CARTESIAN_POINT('Ctrl Pts',(0.933762551511809,-2.51462152201201,
13.8253580685121));
#441456=CARTESIAN_POINT('Ctrl Pts',(0.933733416352549,-2.51502553426522,
13.8247484142933));
#441457=CARTESIAN_POINT('Ctrl Pts',(0.933713159135509,-2.51542779726107,
13.8241378483365));
#441458=CARTESIAN_POINT('Ctrl Pts',(0.933702113402283,-2.51582801973993,
13.8235269408515));
#441459=CARTESIAN_POINT('',(0.955837885903104,-2.48464983405672,12.5969504640361));
#441460=CARTESIAN_POINT('Origin',(0.968075724091053,-2.5168073237707,12.584524458991));
#441461=CARTESIAN_POINT('Origin',(0.968075724091053,-2.5168073237707,12.584524458991));
#441462=CARTESIAN_POINT('Ctrl Pts',(0.992933084929655,-2.49304515609576,
12.5893111709658));
#441463=CARTESIAN_POINT('Ctrl Pts',(0.985108542234981,-2.48484545084624,
12.5770542771492));
#441464=CARTESIAN_POINT('Ctrl Pts',(0.971370553186036,-2.49373765708238,
12.5737548217797));
#441465=CARTESIAN_POINT('Ctrl Pts',(1.01004273380832,-2.51097515957357,
12.5663937883685));
#441466=CARTESIAN_POINT('Ctrl Pts',(1.00220820982281,-2.50276499446125,
12.5540940315304));
#441467=CARTESIAN_POINT('Ctrl Pts',(0.988429394417114,-2.51168745159643,
12.5508374392248));
#441468=CARTESIAN_POINT('Ctrl Pts',(1.02713511926105,-2.52888707189772,
12.5434499600945));
#441469=CARTESIAN_POINT('Ctrl Pts',(1.01927512244805,-2.52065021261488,
12.5311293540533));
#441470=CARTESIAN_POINT('Ctrl Pts',(1.0054724240448,-2.52961889598253,12.5278936106989));
#441471=CARTESIAN_POINT('Ctrl Pts',(1.04421159355556,-2.54678231017295,
12.5204817579905));
#441472=CARTESIAN_POINT('Ctrl Pts',(1.03631269512993,-2.53850468406579,
12.5081597038247));
#441473=CARTESIAN_POINT('Ctrl Pts',(1.02250088105112,-2.54753340694043,
12.5049254088044));
#441474=CARTESIAN_POINT('Ctrl Pts',(1.0319343935952,-2.53391645655151,12.5369868989719));
#441475=CARTESIAN_POINT('Ctrl Pts',(1.03257746963189,-2.53459036632423,
12.5342545179733));
#441476=CARTESIAN_POINT('Ctrl Pts',(1.03310094282764,-2.53531963508585,
12.5314872231885));
#441477=CARTESIAN_POINT('Ctrl Pts',(1.03342991240674,-2.5360957794836,12.5287124745063));
#441478=CARTESIAN_POINT('Ctrl Pts',(1.03372659350178,-2.53679574502586,
12.5262100684184));
#441479=CARTESIAN_POINT('Ctrl Pts',(1.03386387344133,-2.53753351365892,
12.5237004536639));
#441480=CARTESIAN_POINT('Ctrl Pts',(1.03377893743462,-2.53833388010387,
12.5212220730815));
#441481=CARTESIAN_POINT('Ctrl Pts',(1.03371391157394,-2.53894662985469,
12.5193246583486));
#441482=CARTESIAN_POINT('Ctrl Pts',(1.03351723171028,-2.53960332586833,
12.517417831369));
#441483=CARTESIAN_POINT('Ctrl Pts',(1.03309208063785,-2.54029499867328,
12.5155812248347));
#441484=CARTESIAN_POINT('Ctrl Pts',(1.03291096399581,-2.54058965500595,
12.5147988205793));
#441485=CARTESIAN_POINT('Ctrl Pts',(1.03268843641229,-2.54089110312969,
12.5140295443047));
#441486=CARTESIAN_POINT('Ctrl Pts',(1.03241788174527,-2.54120059129584,
12.5132817086137));
#441487=CARTESIAN_POINT('Ctrl Pts',(1.03200843385653,-2.54166895976869,
12.5121499604604));
#441488=CARTESIAN_POINT('Ctrl Pts',(1.03147476479515,-2.54216114921371,
12.5110494206568));
#441489=CARTESIAN_POINT('Ctrl Pts',(1.03078416050836,-2.54265936385898,
12.5100666561695));
#441490=CARTESIAN_POINT('Ctrl Pts',(1.03038761711721,-2.54294543756101,
12.5095023550641));
#441491=CARTESIAN_POINT('Ctrl Pts',(1.02993436812066,-2.54323627373919,
12.5089719619137));
#441492=CARTESIAN_POINT('Ctrl Pts',(1.02942945988058,-2.54352104550052,
12.5085043804652));
#441493=CARTESIAN_POINT('Ctrl Pts',(1.02869059244015,-2.5439377718791,12.5078201359221));
#441494=CARTESIAN_POINT('Ctrl Pts',(1.02781907629294,-2.544352546056,12.5072563000949));
#441495=CARTESIAN_POINT('Ctrl Pts',(1.02687034923004,-2.54472960804893,
12.5068768744332));
#441496=CARTESIAN_POINT('Ctrl Pts',(1.0261862517071,-2.54500149570287,12.5066032824114));
#441497=CARTESIAN_POINT('Ctrl Pts',(1.02545001273742,-2.54525860774108,
12.5064197834844));
#441498=CARTESIAN_POINT('Ctrl Pts',(1.02470359803672,-2.54548902668966,
12.5063282718343));
#441499=CARTESIAN_POINT('Ctrl Pts',(1.02361406365786,-2.54582536701869,
12.5061946931565));
#441500=CARTESIAN_POINT('Ctrl Pts',(1.02247987369661,-2.5461130362937,12.5062515701262));
#441501=CARTESIAN_POINT('Ctrl Pts',(1.02137521992727,-2.54634917114627,
12.5064436508398));
#441502=CARTESIAN_POINT('',(0.971370553186036,-2.49373765708238,12.5737548217797));
#441503=CARTESIAN_POINT('Origin',(0.977016889193453,-2.50823313533221,12.5893111709658));
#441504=CARTESIAN_POINT('Ctrl Pts',(1.02137521992727,-2.54634917114627,
12.5064436508398));
#441505=CARTESIAN_POINT('Ctrl Pts',(1.01397288185703,-2.53856163117237,
12.5164271754438));
#441506=CARTESIAN_POINT('Ctrl Pts',(1.00656776093935,-2.53077086027243,
12.5264061185523));
#441507=CARTESIAN_POINT('Ctrl Pts',(0.999159758478661,-2.52297674530802,
12.536380305637));
#441508=CARTESIAN_POINT('Ctrl Pts',(0.989901257907586,-2.51323568241935,
12.5488460165097));
#441509=CARTESIAN_POINT('Ctrl Pts',(0.980638253669115,-2.50348939323112,
12.5613043021964));
#441510=CARTESIAN_POINT('Ctrl Pts',(0.971370553186036,-2.49373765708238,
12.5737548217797));
#441511=CARTESIAN_POINT('Ctrl Pts',(0.933702113402283,-2.51582801973993,
12.5893111709658));
#441512=CARTESIAN_POINT('Ctrl Pts',(0.93401480008439,-2.50449837448518,
12.5770542771492));
#441513=CARTESIAN_POINT('Ctrl Pts',(0.950170633310257,-2.50189208830885,
12.5737548217797));
#441514=CARTESIAN_POINT('Ctrl Pts',(0.933993847357083,-2.5052575592573,
12.5928319619712));
#441515=CARTESIAN_POINT('Ctrl Pts',(0.93746049473711,-2.49773321394931,
12.5821634970842));
#441516=CARTESIAN_POINT('Ctrl Pts',(0.950267469666604,-2.49804126500864,
12.5773203894503));
#441517=CARTESIAN_POINT('Ctrl Pts',(0.941397848411402,-2.49023208529715,
12.5969440695591));
#441518=CARTESIAN_POINT('Ctrl Pts',(0.94514304634973,-2.48877193634766,
12.5878292599214));
#441519=CARTESIAN_POINT('Ctrl Pts',(0.952908241986078,-2.49268678383356,
12.5813877129824));
#441520=CARTESIAN_POINT('Ctrl Pts',(0.969935724982431,-2.4791973743196,
12.596957478804));
#441521=CARTESIAN_POINT('Ctrl Pts',(0.966218234178142,-2.48064680705999,
12.5878468778671));
#441522=CARTESIAN_POINT('Ctrl Pts',(0.963124494906348,-2.48874287149005,
12.5814011370086));
#441523=CARTESIAN_POINT('Ctrl Pts',(0.985622254728059,-2.48538379426003,
12.5928371701607));
#441524=CARTESIAN_POINT('Ctrl Pts',(0.97800989610333,-2.48213001770463,
12.5821692192951));
#441525=CARTESIAN_POINT('Ctrl Pts',(0.968709785890143,-2.49093523047833,
12.5773318885715));
#441526=CARTESIAN_POINT('Ctrl Pts',(0.992933084929691,-2.49304515609571,
12.5893111709658));
#441527=CARTESIAN_POINT('Ctrl Pts',(0.985108542235019,-2.4848454508462,
12.5770542771492));
#441528=CARTESIAN_POINT('Ctrl Pts',(0.971370553186075,-2.49373765708234,
12.5737548217797));
#441529=CARTESIAN_POINT('',(0.950170633310257,-2.50189208830885,12.5737548217797));
#441530=CARTESIAN_POINT('Origin',(0.955693739443599,-2.51643496624411,12.5893111709658));
#441531=CARTESIAN_POINT('Ctrl Pts',(0.971370553186075,-2.49373765708234,
12.5737548217797));
#441532=CARTESIAN_POINT('Ctrl Pts',(0.970702716238683,-2.49299045333321,
12.5746934679442));
#441533=CARTESIAN_POINT('Ctrl Pts',(0.9698271288722,-2.49228569649437,12.5756680099006));
#441534=CARTESIAN_POINT('Ctrl Pts',(0.968845496035647,-2.491700973789,12.5765688348656));
#441535=CARTESIAN_POINT('Ctrl Pts',(0.968585619609202,-2.49154617492584,
12.5768073183026));
#441536=CARTESIAN_POINT('Ctrl Pts',(0.968318492163072,-2.49139960665602,
12.5770407398754));
#441537=CARTESIAN_POINT('Ctrl Pts',(0.968046285043574,-2.49126222242476,
12.5772674179684));
#441538=CARTESIAN_POINT('Ctrl Pts',(0.966929220633075,-2.49069843468993,
12.5781976435658));
#441539=CARTESIAN_POINT('Ctrl Pts',(0.965658082544084,-2.49026735993831,
12.5790594849312));
#441540=CARTESIAN_POINT('Ctrl Pts',(0.964303191474802,-2.49004383608263,
12.5797571720116));
#441541=CARTESIAN_POINT('Ctrl Pts',(0.963420431225624,-2.48989820225346,
12.580211740231));
#441542=CARTESIAN_POINT('Ctrl Pts',(0.962458945194491,-2.48985257778344,
12.5806009430798));
#441543=CARTESIAN_POINT('Ctrl Pts',(0.961485578068116,-2.48992787122014,
12.5808812374708));
#441544=CARTESIAN_POINT('Ctrl Pts',(0.960649132795379,-2.48999257326061,
12.5811221033394));
#441545=CARTESIAN_POINT('Ctrl Pts',(0.959786798452788,-2.49014800567127,
12.581287365893));
#441546=CARTESIAN_POINT('Ctrl Pts',(0.958948725634985,-2.49039360134612,
12.581359338449));
#441547=CARTESIAN_POINT('Ctrl Pts',(0.958832250818849,-2.49042773407357,
12.5813693411482));
#441548=CARTESIAN_POINT('Ctrl Pts',(0.958716209593221,-2.49046355976426,
12.5813775999465));
#441549=CARTESIAN_POINT('Ctrl Pts',(0.958600699823552,-2.49050102778792,
12.5813841266931));
#441550=CARTESIAN_POINT('Ctrl Pts',(0.958404723528695,-2.49056459682172,
12.5813952001081));
#441551=CARTESIAN_POINT('Ctrl Pts',(0.95820915235056,-2.49063389826755,
12.5814007534795));
#441552=CARTESIAN_POINT('Ctrl Pts',(0.958014137335656,-2.49070908782672,
12.5814005856065));
#441553=CARTESIAN_POINT('Ctrl Pts',(0.957121434843356,-2.49105327623141,
12.5813998171494));
#441554=CARTESIAN_POINT('Ctrl Pts',(0.956301943948017,-2.4914967514541,
12.58127954464));
#441555=CARTESIAN_POINT('Ctrl Pts',(0.955546234478559,-2.49201097252028,
12.5810700125799));
#441556=CARTESIAN_POINT('Ctrl Pts',(0.954633423483868,-2.49263209301946,
12.5808169217085));
#441557=CARTESIAN_POINT('Ctrl Pts',(0.953823001426223,-2.49337032363922,
12.5804173076348));
#441558=CARTESIAN_POINT('Ctrl Pts',(0.953168455051674,-2.49414171485722,
12.5799304713245));
#441559=CARTESIAN_POINT('Ctrl Pts',(0.952357265890236,-2.49509771158963,
12.5793271277669));
#441560=CARTESIAN_POINT('Ctrl Pts',(0.95171061438851,-2.49614310847298,
12.5785808224116));
#441561=CARTESIAN_POINT('Ctrl Pts',(0.95122878465116,-2.49721715501164,
12.5777485681082));
#441562=CARTESIAN_POINT('Ctrl Pts',(0.95051080555412,-2.49881760202482,
12.576508418016));
#441563=CARTESIAN_POINT('Ctrl Pts',(0.950158576379626,-2.5004653744968,
12.5750928681475));
#441564=CARTESIAN_POINT('Ctrl Pts',(0.950170633310256,-2.50189208830885,
12.5737548217797));
#441565=CARTESIAN_POINT('Ctrl Pts',(0.950170633310257,-2.50189208830885,
12.5737548217797));
#441566=CARTESIAN_POINT('Ctrl Pts',(0.934014800084389,-2.50449837448518,
12.5770542771492));
#441567=CARTESIAN_POINT('Ctrl Pts',(0.933702113402283,-2.51582801973993,
12.5893111709658));
#441568=CARTESIAN_POINT('Ctrl Pts',(0.949537961488343,-2.52664314243865,
12.5508408821982));
#441569=CARTESIAN_POINT('Ctrl Pts',(0.933331560880742,-2.52925433066919,
12.55409748406));
#441570=CARTESIAN_POINT('Ctrl Pts',(0.933018475290506,-2.54059842964961,
12.5663972313419));
#441571=CARTESIAN_POINT('Ctrl Pts',(0.948904728579262,-2.55136998776663,
12.52790050457));
#441572=CARTESIAN_POINT('Ctrl Pts',(0.932649630242801,-2.55396287330473,
12.5311362602938));
#441573=CARTESIAN_POINT('Ctrl Pts',(0.932335526857248,-2.565343850286,12.5434568539655));
#441574=CARTESIAN_POINT('Ctrl Pts',(0.948270964343104,-2.57607450527355,
12.5049357605811));
#441575=CARTESIAN_POINT('Ctrl Pts',(0.931968871759239,-2.57862894501183,
12.5081700652078));
#441576=CARTESIAN_POINT('Ctrl Pts',(0.931653214086745,-2.59006623881408,
12.5204921097672));
#441577=CARTESIAN_POINT('Ctrl Pts',(0.948312578200522,-2.57445230977461,
12.5064436508395));
#441578=CARTESIAN_POINT('Ctrl Pts',(0.947255993587591,-2.57506261850493,
12.5062361689309));
#441579=CARTESIAN_POINT('Ctrl Pts',(0.946131207133394,-2.5756522345265,
12.5061871075061));
#441580=CARTESIAN_POINT('Ctrl Pts',(0.945012133735765,-2.57616085164362,
12.5063648335164));
#441581=CARTESIAN_POINT('Ctrl Pts',(0.944503781571251,-2.57639189691103,
12.5064455676329));
#441582=CARTESIAN_POINT('Ctrl Pts',(0.94398942670264,-2.57660924978727,
12.506574497099));
#441583=CARTESIAN_POINT('Ctrl Pts',(0.943490714045272,-2.57680262276842,
12.5067492519495));
#441584=CARTESIAN_POINT('Ctrl Pts',(0.942488531601621,-2.57719121328025,
12.5071004286051));
#441585=CARTESIAN_POINT('Ctrl Pts',(0.941512377411389,-2.57749650063508,
12.5076537929613));
#441586=CARTESIAN_POINT('Ctrl Pts',(0.940638340199299,-2.57770459868467,
12.5083435010505));
#441587=CARTESIAN_POINT('Ctrl Pts',(0.94058331433352,-2.57771769970049,
12.5083869222964));
#441588=CARTESIAN_POINT('Ctrl Pts',(0.940528684438786,-2.57773040532925,
12.5084308732337));
#441589=CARTESIAN_POINT('Ctrl Pts',(0.940474465632242,-2.57774270821808,
12.5084753333615));
#441590=CARTESIAN_POINT('Ctrl Pts',(0.940039559241441,-2.5778413936248,
12.5088319622689));
#441591=CARTESIAN_POINT('Ctrl Pts',(0.939622559073392,-2.57791742768805,
12.509227847131));
#441592=CARTESIAN_POINT('Ctrl Pts',(0.939236366985531,-2.57797130415551,
12.5096423454524));
#441593=CARTESIAN_POINT('Ctrl Pts',(0.938026211903631,-2.57814012915979,
12.5109411997424));
#441594=CARTESIAN_POINT('Ctrl Pts',(0.937045470588517,-2.57811134439835,
12.5124831113042));
#441595=CARTESIAN_POINT('Ctrl Pts',(0.936253593444106,-2.57797045769338,
12.5140723025008));
#441596=CARTESIAN_POINT('Ctrl Pts',(0.936179393688356,-2.57795725645481,
12.5142212114565));
#441597=CARTESIAN_POINT('Ctrl Pts',(0.936106830858711,-2.57794309155734,
12.5143705582413));
#441598=CARTESIAN_POINT('Ctrl Pts',(0.936035860514673,-2.57792804621625,
12.5145201959299));
#441599=CARTESIAN_POINT('Ctrl Pts',(0.935124140781716,-2.57773476640973,
12.5164425148273));
#441600=CARTESIAN_POINT('Ctrl Pts',(0.934441766773685,-2.57740006730229,
12.5184635205941));
#441601=CARTESIAN_POINT('Ctrl Pts',(0.933913332889976,-2.57697346630447,
12.5205025929158));
#441602=CARTESIAN_POINT('Ctrl Pts',(0.933606820292262,-2.57672602081686,
12.5216853356836));
#441603=CARTESIAN_POINT('Ctrl Pts',(0.933352350171766,-2.57644847854563,
12.5228750347131));
#441604=CARTESIAN_POINT('Ctrl Pts',(0.933138739911918,-2.57615525762987,
12.5240609649613));
#441605=CARTESIAN_POINT('Ctrl Pts',(0.93261444498892,-2.5754355626229,12.5269717671326));
#441606=CARTESIAN_POINT('Ctrl Pts',(0.932329949141683,-2.5745950383216,
12.5299036066169));
#441607=CARTESIAN_POINT('Ctrl Pts',(0.932208704326839,-2.57367430392938,
12.5328133004019));
#441608=CARTESIAN_POINT('Ctrl Pts',(0.93215049975584,-2.57323229780835,
12.5342101228451));
#441609=CARTESIAN_POINT('Ctrl Pts',(0.932130509564359,-2.57277228987482,
12.5356023438238));
#441610=CARTESIAN_POINT('Ctrl Pts',(0.932143531606478,-2.57230045639141,
12.5369868989719));
#441611=CARTESIAN_POINT('Origin',(0.575248376757179,-15.3118151806691,-1.23916491245692));
#441612=CARTESIAN_POINT('Ctrl Pts',(1.0319055691249,-2.53388619253255,12.5369868989719));
#441613=CARTESIAN_POINT('Ctrl Pts',(1.04247390524396,-2.54500345727526,
12.5369868989719));
#441614=CARTESIAN_POINT('Ctrl Pts',(1.05655975383268,-2.53893121113229,
12.5369868989719));
#441615=CARTESIAN_POINT('Ctrl Pts',(1.03547812804696,-2.53764421719005,
12.5218025310015));
#441616=CARTESIAN_POINT('Ctrl Pts',(1.04569684416929,-2.54358001574756,
12.5216901060418));
#441617=CARTESIAN_POINT('Ctrl Pts',(1.05651682202664,-2.53894973649539,
12.5161920673677));
#441618=CARTESIAN_POINT('Ctrl Pts',(1.03435223980804,-2.54356607896389,
12.5042015548895));
#441619=CARTESIAN_POINT('Ctrl Pts',(1.04041793527717,-2.54570726636648,
12.4980677368513));
#441620=CARTESIAN_POINT('Ctrl Pts',(1.04670686589631,-2.54313042112641,
12.4907278922778));
#441621=CARTESIAN_POINT('Ctrl Pts',(1.02136777388495,-2.54633060774792,
12.506463626192));
#441622=CARTESIAN_POINT('Ctrl Pts',(1.02380351458147,-2.55240305417384,
12.4999376786891));
#441623=CARTESIAN_POINT('Ctrl Pts',(1.02377376555043,-2.55232888807008,
12.4906970594712));
#441624=CARTESIAN_POINT('Origin',(1.0478505893314,-2.51872847731506,12.5369868989719));
#441625=CARTESIAN_POINT('Origin',(1.0478505893314,-2.51872847731506,14.));
#441626=CARTESIAN_POINT('Origin',(1.0478505893314,-2.51872847731506,13.7435492065112));
#441627=CARTESIAN_POINT('Ctrl Pts',(1.01484096118934,-2.51600340774675,
13.793642941384));
#441628=CARTESIAN_POINT('Ctrl Pts',(1.02228566441025,-2.52384449268177,
13.8071662555867));
#441629=CARTESIAN_POINT('Ctrl Pts',(1.036225550646,-2.51406190839289,13.8103758687955));
#441630=CARTESIAN_POINT('Ctrl Pts',(1.02631556175581,-2.52802818412982,
13.7804579775006));
#441631=CARTESIAN_POINT('Ctrl Pts',(1.03550900673808,-2.53769639187931,
13.7901904343352));
#441632=CARTESIAN_POINT('Ctrl Pts',(1.04970065958661,-2.53085147306375,
13.7927914348263));
#441633=CARTESIAN_POINT('Ctrl Pts',(1.03307109097461,-2.53510762250353,
13.7597120340895));
#441634=CARTESIAN_POINT('Ctrl Pts',(1.04371464854379,-2.54629251285811,
13.7635825532445));
#441635=CARTESIAN_POINT('Ctrl Pts',(1.05766685160311,-2.54073625998993,
13.7651073818884));
#441636=CARTESIAN_POINT('Ctrl Pts',(1.03174820367012,-2.53372130636869,
13.7381884353898));
#441637=CARTESIAN_POINT('Ctrl Pts',(1.04214197781216,-2.54464501314388,
13.7368803041982));
#441638=CARTESIAN_POINT('Ctrl Pts',(1.0561072193107,-2.53880021485767,13.7363986145813));
#441639=CARTESIAN_POINT('Origin',(1.03354142914459,-2.50373323727633,13.7902182540695));
#441640=CARTESIAN_POINT('Ctrl Pts',(0.992930368074177,-2.49304230787617,
13.8235227101244));
#441641=CARTESIAN_POINT('Ctrl Pts',(1.00086431035936,-2.50136307996383,
13.8358800583119));
#441642=CARTESIAN_POINT('Ctrl Pts',(1.01471541067073,-2.4922651093538,13.8390832900376));
#441643=CARTESIAN_POINT('Ctrl Pts',(1.001164723875,-2.50167147549767,13.8124254819053));
#441644=CARTESIAN_POINT('Ctrl Pts',(1.00911407396496,-2.51000840621482,
13.8247886449158));
#441645=CARTESIAN_POINT('Ctrl Pts',(1.0229733183811,-2.50088469395962,13.8279860620657));
#441646=CARTESIAN_POINT('Ctrl Pts',(1.00939538930543,-2.51029677580698,
13.8013225099955));
#441647=CARTESIAN_POINT('Ctrl Pts',(1.01735639493263,-2.51864593284445,
13.8136962257787));
#441648=CARTESIAN_POINT('Ctrl Pts',(1.0312272073583,-2.50950047563698,13.8168830918626));
#441649=CARTESIAN_POINT('Ctrl Pts',(1.01762250795212,-2.51891835927529,
13.7902140179785));
#441650=CARTESIAN_POINT('Ctrl Pts',(1.02559166208941,-2.52727606732718,
13.802602731458));
#441651=CARTESIAN_POINT('Ctrl Pts',(1.03947723417924,-2.51811260508526,
13.8057746032558));
#441652=CARTESIAN_POINT('Origin',(1.00884928066586,-2.47785717685931,13.8235269408515));
#441653=CARTESIAN_POINT('Ctrl Pts',(0.933702113402283,-2.51582801973993,
13.8235269408515));
#441654=CARTESIAN_POINT('Ctrl Pts',(0.933376362965707,-2.52763100688066,
13.8362179249168));
#441655=CARTESIAN_POINT('Ctrl Pts',(0.916453295848555,-2.52992726544752,
13.8391868794938));
#441656=CARTESIAN_POINT('Ctrl Pts',(0.934000160872677,-2.50502880025961,
13.8400110824519));
#441657=CARTESIAN_POINT('Ctrl Pts',(0.930319292077029,-2.51439752844278,
13.8494522556836));
#441658=CARTESIAN_POINT('Ctrl Pts',(0.917056111996971,-2.51215789865194,
13.85569149686));
#441659=CARTESIAN_POINT('Ctrl Pts',(0.941076652785396,-2.49035498043469,
13.8586819406588));
#441660=CARTESIAN_POINT('Ctrl Pts',(0.937018055750126,-2.49193099875321,
13.868010383617));
#441661=CARTESIAN_POINT('Ctrl Pts',(0.928934735488491,-2.48786248546938,
13.8744918421245));
#441662=CARTESIAN_POINT('Ctrl Pts',(0.970261895489138,-2.47907255577194,
13.8587686893867));
#441663=CARTESIAN_POINT('Ctrl Pts',(0.974284350665984,-2.47751051151197,
13.8680909899357));
#441664=CARTESIAN_POINT('Ctrl Pts',(0.977520521636126,-2.46908296151464,
13.8745789365163));
#441665=CARTESIAN_POINT('Ctrl Pts',(0.985462731547706,-2.48521662242851,
13.8400379222776));
#441666=CARTESIAN_POINT('Ctrl Pts',(0.994474056380701,-2.48969616020182,
13.8494748685452));
#441667=CARTESIAN_POINT('Ctrl Pts',(1.00281461081408,-2.47915119661686,
13.8557104837033));
#441668=CARTESIAN_POINT('Ctrl Pts',(0.992933084934336,-2.49304515609109,
13.8235269408542));
#441669=CARTESIAN_POINT('Ctrl Pts',(1.00108452963812,-2.50158743728711,
13.8362179249195));
#441670=CARTESIAN_POINT('Ctrl Pts',(1.01518422375405,-2.49195096335243,
13.8391868794965));
#441671=CARTESIAN_POINT('Origin',(0.911710487360968,-2.51522107323575,13.8235269408515));
#441672=CARTESIAN_POINT('Ctrl Pts',(0.932715466503348,-2.5515773860639,
13.7902140241683));
#441673=CARTESIAN_POINT('Ctrl Pts',(0.932401321989514,-2.56312121162638,
13.8026027327198));
#441674=CARTESIAN_POINT('Ctrl Pts',(0.915954174459439,-2.5656250627396,
13.8057746032556));
#441675=CARTESIAN_POINT('Ctrl Pts',(0.933044241045491,-2.53966482588052,
13.8013225161808));
#441676=CARTESIAN_POINT('Ctrl Pts',(0.932730414263208,-2.55119684394483,
13.8136962270464));
#441677=CARTESIAN_POINT('Ctrl Pts',(0.916306287753358,-2.55370416795692,
13.8168830918628));
#441678=CARTESIAN_POINT('Ctrl Pts',(0.933373157325311,-2.52774713008525,
13.8124254880875));
#441679=CARTESIAN_POINT('Ctrl Pts',(0.933059788337923,-2.53926226251689,
13.8247886461867));
#441680=CARTESIAN_POINT('Ctrl Pts',(0.916658820164197,-2.54177797417812,
13.8279860620656));
#441681=CARTESIAN_POINT('Ctrl Pts',(0.933702221080902,-2.51582409076846,
13.8235227163066));
#441682=CARTESIAN_POINT('Ctrl Pts',(0.933389459749114,-2.52731690433112,
13.8358800595847));
#441683=CARTESIAN_POINT('Ctrl Pts',(0.917011786918948,-2.529846264619,13.8390832900376));
#441684=CARTESIAN_POINT('Origin',(0.910723732443375,-2.55097438096992,13.7902182540695));
#441685=CARTESIAN_POINT('Ctrl Pts',(0.932150949056334,-2.57203069844641,
13.7382347919292));
#441686=CARTESIAN_POINT('Ctrl Pts',(0.931758621716637,-2.58711592128174,
13.7369371795942));
#441687=CARTESIAN_POINT('Ctrl Pts',(0.917462529821921,-2.59213244732652,
13.7364597369711));
#441688=CARTESIAN_POINT('Ctrl Pts',(0.932098764236209,-2.57392153707748,
13.7595490285574));
#441689=CARTESIAN_POINT('Ctrl Pts',(0.931696071217628,-2.58936665425904,
13.7633824266926));
#441690=CARTESIAN_POINT('Ctrl Pts',(0.917601001692082,-2.59458418963287,
13.7648920890506));
#441691=CARTESIAN_POINT('Ctrl Pts',(0.932364903967904,-2.56427836364779,
13.7803806590111));
#441692=CARTESIAN_POINT('Ctrl Pts',(0.932021985543206,-2.57763797789961,
13.7901039518744));
#441693=CARTESIAN_POINT('Ctrl Pts',(0.916898763834281,-2.58208473026154,
13.7926933640892));
#441694=CARTESIAN_POINT('Ctrl Pts',(0.932827514154394,-2.54751637559775,
13.7936647693663));
#441695=CARTESIAN_POINT('Ctrl Pts',(0.932559096581482,-2.55832846531025,
13.8072068914933));
#441696=CARTESIAN_POINT('Ctrl Pts',(0.915637243948269,-2.56040094529968,
13.8104111085397));
#441697=CARTESIAN_POINT('Origin',(0.910151905565162,-2.57169350988723,13.7435492065112));
#441698=CARTESIAN_POINT('Origin',(0.910151905565162,-2.57169350988723,14.));
#441699=CARTESIAN_POINT('Origin',(0.910151905565162,-2.57169350988723,12.5369868989719));
#441700=CARTESIAN_POINT('Ctrl Pts',(0.948306224028831,-2.57443505961824,
12.506462012331));
#441701=CARTESIAN_POINT('Ctrl Pts',(0.950566304539922,-2.58057066261006,
12.4999388158272));
#441702=CARTESIAN_POINT('Ctrl Pts',(0.950539564823561,-2.58049807038031,
12.4907030323752));
#441703=CARTESIAN_POINT('Ctrl Pts',(0.936815419454617,-2.58108261506304,
12.5042014951932));
#441704=CARTESIAN_POINT('Ctrl Pts',(0.933750333536626,-2.58673472488428,
12.4980716682127));
#441705=CARTESIAN_POINT('Ctrl Pts',(0.927360673278842,-2.58903642143593,
12.4907355092744));
#441706=CARTESIAN_POINT('Ctrl Pts',(0.932010533866908,-2.57744410221653,
12.5218047446509));
#441707=CARTESIAN_POINT('Ctrl Pts',(0.928404372659909,-2.5886919674489,
12.5216906929434));
#441708=CARTESIAN_POINT('Ctrl Pts',(0.917277340433921,-2.59250771222178,
12.5161988840775));
#441709=CARTESIAN_POINT('Ctrl Pts',(0.932144557920413,-2.57226205397613,
12.5369868989719));
#441710=CARTESIAN_POINT('Ctrl Pts',(0.931748388901365,-2.58758682417437,
12.5369868989719));
#441711=CARTESIAN_POINT('Ctrl Pts',(0.917234684417284,-2.59252219788557,
12.5369868989719));
#441712=CARTESIAN_POINT('Origin',(1.84953258308758E-31,-9.96028411833584E-31,
12.5));
#441713=CARTESIAN_POINT('Origin',(1.13565863606157,-2.43135141923565,12.5));
#441714=CARTESIAN_POINT('',(1.13565863606157,-2.43135141923565,12.5893111709658));
#441715=CARTESIAN_POINT('',(1.13565863606157,-2.43135141923565,13.8235269408515));
#441716=CARTESIAN_POINT('',(1.13565863606157,-2.43135141923565,12.5));
#441717=CARTESIAN_POINT('',(1.13758939098741,-2.46706619047414,13.7902182540695));
#441718=CARTESIAN_POINT('',(1.13565863606157,-2.43135141923565,13.8235269408515));
#441719=CARTESIAN_POINT('',(1.13870826816973,-2.48776298739835,13.7435492065112));
#441720=CARTESIAN_POINT('Origin',(1.13502750230952,-2.41967078150723,13.7445212918712));
#441721=CARTESIAN_POINT('',(1.13870826816973,-2.48776298739835,12.5369868989719));
#441722=CARTESIAN_POINT('',(1.13870826816973,-2.48776298739835,12.5));
#441723=CARTESIAN_POINT('Ctrl Pts',(1.13870826816973,-2.48776298739835,
12.5369868989719));
#441724=CARTESIAN_POINT('Ctrl Pts',(1.13769246553907,-2.46897284573305,
12.5544431401645));
#441725=CARTESIAN_POINT('Ctrl Pts',(1.13667593637937,-2.45016926485901,
12.5718848856037));
#441726=CARTESIAN_POINT('Ctrl Pts',(1.13565863606157,-2.43135141923565,
12.5893111709658));
#441727=CARTESIAN_POINT('Origin',(1.39827000902105,-2.58663242216022,12.5));
#441728=CARTESIAN_POINT('',(1.23503843197073,-2.44137282548621,13.7435492065112));
#441729=CARTESIAN_POINT('',(1.21955463306185,-2.42759381026668,13.7902182540695));
#441730=CARTESIAN_POINT('Origin',(1.17886588566605,-2.39138493976081,13.7418732680438));
#441731=CARTESIAN_POINT('',(1.19283550652461,-2.40381648963781,13.8235269408515));
#441732=CARTESIAN_POINT('',(1.21955463306185,-2.42759381026668,13.7902182540695));
#441733=CARTESIAN_POINT('',(1.19283550652461,-2.40381648963781,12.5893111709658));
#441734=CARTESIAN_POINT('',(1.19283550652461,-2.40381648963781,12.5));
#441735=CARTESIAN_POINT('',(1.23503843197073,-2.44137282548621,12.5369868989719));
#441736=CARTESIAN_POINT('Ctrl Pts',(1.19283550652461,-2.40381648963781,
12.5893111709658));
#441737=CARTESIAN_POINT('Ctrl Pts',(1.2069136142916,-2.4163445818925,12.5718848856037));
#441738=CARTESIAN_POINT('Ctrl Pts',(1.22098105023769,-2.42886317730579,
12.5544431401645));
#441739=CARTESIAN_POINT('Ctrl Pts',(1.23503843197073,-2.44137282548621,
12.5369868989719));
#441740=CARTESIAN_POINT('',(1.23503843197073,-2.44137282548621,12.5));
#441741=CARTESIAN_POINT('Origin',(1.16998351495931,-2.42949580244986,12.5));
#441742=CARTESIAN_POINT('',(1.15406831628268,-2.39902784184759,13.8587068136939));
#441743=CARTESIAN_POINT('Ctrl Pts',(1.19283550652889,-2.40381648963277,
13.8235269408542));
#441744=CARTESIAN_POINT('Ctrl Pts',(1.1915264791287,-2.40265158762287,13.8262006681044));
#441745=CARTESIAN_POINT('Ctrl Pts',(1.19007138150615,-2.40158926990163,
13.8288634856214));
#441746=CARTESIAN_POINT('Ctrl Pts',(1.18848189959866,-2.40062311424865,
13.8314912288862));
#441747=CARTESIAN_POINT('Ctrl Pts',(1.18684330769949,-2.39962710742477,
13.8342001611531));
#441748=CARTESIAN_POINT('Ctrl Pts',(1.18506033714425,-2.39873176576222,
13.8368750301949));
#441749=CARTESIAN_POINT('Ctrl Pts',(1.1831078388226,-2.3979546046324,13.8394886372969));
#441750=CARTESIAN_POINT('Ctrl Pts',(1.18295704264112,-2.39789458259322,
13.8396904925131));
#441751=CARTESIAN_POINT('Ctrl Pts',(1.18280522363857,-2.39783528434211,
13.8398919674349));
#441752=CARTESIAN_POINT('Ctrl Pts',(1.18265236510737,-2.39777672818192,
13.8400930404591));
#441753=CARTESIAN_POINT('Ctrl Pts',(1.18027072635307,-2.39686438381137,
13.8432258934518));
#441754=CARTESIAN_POINT('Ctrl Pts',(1.17764928961486,-2.39613579180582,
13.8462331177034));
#441755=CARTESIAN_POINT('Ctrl Pts',(1.17484771977747,-2.3957076581236,13.8489036603661));
#441756=CARTESIAN_POINT('Ctrl Pts',(1.17393101352317,-2.39556756780034,
13.8497774930041));
#441757=CARTESIAN_POINT('Ctrl Pts',(1.17299520690167,-2.39545981371141,
13.85061494757));
#441758=CARTESIAN_POINT('Ctrl Pts',(1.17204292942797,-2.39538895230675,
13.8514076489583));
#441759=CARTESIAN_POINT('Ctrl Pts',(1.17002872523211,-2.39523907021616,
13.8530843267192));
#441760=CARTESIAN_POINT('Ctrl Pts',(1.16774276579092,-2.39524246733169,
13.8546805203176));
#441761=CARTESIAN_POINT('Ctrl Pts',(1.16531793013634,-2.39553539204199,
13.8559412814274));
#441762=CARTESIAN_POINT('Ctrl Pts',(1.16499340848649,-2.395574594868,13.8561100121513));
#441763=CARTESIAN_POINT('Ctrl Pts',(1.16466644180727,-2.39561891939493,
13.8562727473908));
#441764=CARTESIAN_POINT('Ctrl Pts',(1.16433738223972,-2.39566862423088,
13.8564289040185));
#441765=CARTESIAN_POINT('Ctrl Pts',(1.16284510085487,-2.39589403509486,
13.8571370725437));
#441766=CARTESIAN_POINT('Ctrl Pts',(1.16128388673762,-2.39623631103585,
13.8577210840553));
#441767=CARTESIAN_POINT('Ctrl Pts',(1.15972070946708,-2.39671081491259,
13.8581177131616));
#441768=CARTESIAN_POINT('Ctrl Pts',(1.15928046494476,-2.3968444515362,13.8582294175695));
#441769=CARTESIAN_POINT('Ctrl Pts',(1.15884004741686,-2.39698839943994,
13.8583265086086));
#441770=CARTESIAN_POINT('Ctrl Pts',(1.15840088406123,-2.39714256764798,
13.8584082369006));
#441771=CARTESIAN_POINT('Ctrl Pts',(1.15776992408551,-2.39736406602108,
13.8585256585398));
#441772=CARTESIAN_POINT('Ctrl Pts',(1.15713381575414,-2.39760971996782,
13.8586122832068));
#441773=CARTESIAN_POINT('Ctrl Pts',(1.15650936780451,-2.39787388477401,
13.8586682984299));
#441774=CARTESIAN_POINT('Ctrl Pts',(1.15600987134434,-2.39808519043314,
13.8587131050557));
#441775=CARTESIAN_POINT('Ctrl Pts',(1.15551222738072,-2.39831045802565,
13.8587357943552));
#441776=CARTESIAN_POINT('Ctrl Pts',(1.15501658563067,-2.39855017569664,
13.8587355499465));
#441777=CARTESIAN_POINT('Ctrl Pts',(1.15469624055099,-2.39870511094251,
13.8587353919793));
#441778=CARTESIAN_POINT('Ctrl Pts',(1.15438017919576,-2.39886437222156,
13.8587257282814));
#441779=CARTESIAN_POINT('Ctrl Pts',(1.15406831628268,-2.39902784184759,
13.8587068136939));
#441780=CARTESIAN_POINT('Ctrl Pts',(1.15406831628268,-2.39902784184759,
13.8587068136939));
#441781=CARTESIAN_POINT('Ctrl Pts',(1.1530426161628,-2.39956548453605,13.8586446046466));
#441782=CARTESIAN_POINT('Ctrl Pts',(1.15206227460148,-2.40014859383079,
13.858482427929));
#441783=CARTESIAN_POINT('Ctrl Pts',(1.15112474840317,-2.40077349303306,
13.8582284286032));
#441784=CARTESIAN_POINT('Ctrl Pts',(1.15016295558127,-2.4014145669233,13.8579678548414));
#441785=CARTESIAN_POINT('Ctrl Pts',(1.14924472334194,-2.40210246252492,
13.857615680862));
#441786=CARTESIAN_POINT('Ctrl Pts',(1.14840044271675,-2.40280230517398,
13.8571944833187));
#441787=CARTESIAN_POINT('Ctrl Pts',(1.14629345407065,-2.40454883407875,
13.8561433417727));
#441788=CARTESIAN_POINT('Ctrl Pts',(1.14454541968629,-2.40644777478311,
13.8546163505474));
#441789=CARTESIAN_POINT('Ctrl Pts',(1.14313369126025,-2.40829359159431,
13.8528973491086));
#441790=CARTESIAN_POINT('Ctrl Pts',(1.14287578930493,-2.40863079509322,
13.8525833129072));
#441791=CARTESIAN_POINT('Ctrl Pts',(1.14262897196776,-2.40896620134861,
13.8522628768812));
#441792=CARTESIAN_POINT('Ctrl Pts',(1.14239292237302,-2.40929855438679,
13.851937733538));
#441793=CARTESIAN_POINT('Ctrl Pts',(1.14095140024834,-2.41132818827904,
13.8499521282529));
#441794=CARTESIAN_POINT('Ctrl Pts',(1.13977151244923,-2.41344802518087,
13.847639871647));
#441795=CARTESIAN_POINT('Ctrl Pts',(1.13884507007223,-2.41550758173481,
13.8452109780794));
#441796=CARTESIAN_POINT('Ctrl Pts',(1.13842824447041,-2.41643421885913,
13.8441181685877));
#441797=CARTESIAN_POINT('Ctrl Pts',(1.13806200744529,-2.41734860361652,
13.8430021611332));
#441798=CARTESIAN_POINT('Ctrl Pts',(1.13774240329718,-2.41823783324536,
13.8418824960098));
#441799=CARTESIAN_POINT('Ctrl Pts',(1.13698924796077,-2.42033332557299,
13.8392439765549));
#441800=CARTESIAN_POINT('Ctrl Pts',(1.13645549152385,-2.42238802025298,
13.8364981347964));
#441801=CARTESIAN_POINT('Ctrl Pts',(1.13610660118662,-2.42439874712789,
13.8336931113419));
#441802=CARTESIAN_POINT('Ctrl Pts',(1.13576680415474,-2.42635706741108,
13.8309611966328));
#441803=CARTESIAN_POINT('Ctrl Pts',(1.13560257789555,-2.42827574082591,
13.8281701127186));
#441804=CARTESIAN_POINT('Ctrl Pts',(1.13562053230287,-2.43014400976238,
13.8253580685121));
#441805=CARTESIAN_POINT('Ctrl Pts',(1.13562442483775,-2.43054905248411,
13.8247484142933));
#441806=CARTESIAN_POINT('Ctrl Pts',(1.13563702319352,-2.43095162813426,
13.8241378483365));
#441807=CARTESIAN_POINT('Ctrl Pts',(1.13565863606157,-2.43135141923565,
13.8235269408515));
#441808=CARTESIAN_POINT('',(1.15517944202808,-2.39847270543601,12.5969504640361));
#441809=CARTESIAN_POINT('Origin',(1.16999769376632,-2.42952569633287,12.584524458991));
#441810=CARTESIAN_POINT('Origin',(1.16999769376632,-2.42952569633287,12.584524458991));
#441811=CARTESIAN_POINT('Ctrl Pts',(1.19283550652461,-2.40381648963781,
12.5893111709658));
#441812=CARTESIAN_POINT('Ctrl Pts',(1.18436864725009,-2.3962818411002,12.5770542771492));
#441813=CARTESIAN_POINT('Ctrl Pts',(1.17140116758586,-2.4062642328984,12.5737548217797));
#441814=CARTESIAN_POINT('Ctrl Pts',(1.21134968619555,-2.42029223728633,
12.5663937883685));
#441815=CARTESIAN_POINT('Ctrl Pts',(1.20287202626619,-2.41274797725812,
12.5540940315304));
#441816=CARTESIAN_POINT('Ctrl Pts',(1.18986632182064,-2.42276384702507,
12.5508374392248));
#441817=CARTESIAN_POINT('Ctrl Pts',(1.22984518528617,-2.43675136110744,
12.5434499600944));
#441818=CARTESIAN_POINT('Ctrl Pts',(1.22133996146542,-2.42918257200328,
12.5311293540533));
#441819=CARTESIAN_POINT('Ctrl Pts',(1.20831422135804,-2.43924646087483,
12.5278936106989));
#441820=CARTESIAN_POINT('Ctrl Pts',(1.24832346707192,-2.45319516326835,
12.5204817579905));
#441821=CARTESIAN_POINT('Ctrl Pts',(1.23977614820573,-2.44558891383069,
12.5081597038247));
#441822=CARTESIAN_POINT('Ctrl Pts',(1.22674621653173,-2.45571338544483,
12.5049254088044));
#441823=CARTESIAN_POINT('Ctrl Pts',(1.23503843197073,-2.44137282548621,
12.5369868989719));
#441824=CARTESIAN_POINT('Ctrl Pts',(1.23573429812772,-2.44199207621274,
12.5342545179733));
#441825=CARTESIAN_POINT('Ctrl Pts',(1.23631547168388,-2.44267625046758,
12.5314872231885));
#441826=CARTESIAN_POINT('Ctrl Pts',(1.23670660961763,-2.44342299823417,
12.5287124745062));
#441827=CARTESIAN_POINT('Ctrl Pts',(1.23705935722064,-2.44409645243533,
12.5262100684184));
#441828=CARTESIAN_POINT('Ctrl Pts',(1.23725631536522,-2.4448205766146,12.5237004536639));
#441829=CARTESIAN_POINT('Ctrl Pts',(1.23723689927158,-2.44562520297928,
12.5212220730815));
#441830=CARTESIAN_POINT('Ctrl Pts',(1.23722203457226,-2.44624121406717,
12.5193246583486));
#441831=CARTESIAN_POINT('Ctrl Pts',(1.2370795359662,-2.44691175621377,12.517417831369));
#441832=CARTESIAN_POINT('Ctrl Pts',(1.23671217730368,-2.44763578129384,
12.5155812248348));
#441833=CARTESIAN_POINT('Ctrl Pts',(1.23655568053889,-2.4479442198696,12.5147988205793));
#441834=CARTESIAN_POINT('Ctrl Pts',(1.23635846421814,-2.44826280301348,
12.5140295443047));
#441835=CARTESIAN_POINT('Ctrl Pts',(1.23611403595814,-2.44859331410036,
12.5132817086137));
#441836=CARTESIAN_POINT('Ctrl Pts',(1.23574412685214,-2.44909349791982,
12.5121499604604));
#441837=CARTESIAN_POINT('Ctrl Pts',(1.23525235153957,-2.4496275486279,12.5110494206568));
#441838=CARTESIAN_POINT('Ctrl Pts',(1.23460465430036,-2.45018039616567,
12.5100666561695));
#441839=CARTESIAN_POINT('Ctrl Pts',(1.23423274803712,-2.45049783994877,
12.5095023550641));
#441840=CARTESIAN_POINT('Ctrl Pts',(1.2338047130377,-2.45082465239455,12.5089719619137));
#441841=CARTESIAN_POINT('Ctrl Pts',(1.23332469638038,-2.45114963131024,
12.5085043804652));
#441842=CARTESIAN_POINT('Ctrl Pts',(1.23262225452895,-2.45162519562188,
12.5078201359221));
#441843=CARTESIAN_POINT('Ctrl Pts',(1.23178744622585,-2.45210962632866,
12.5072563000949));
#441844=CARTESIAN_POINT('Ctrl Pts',(1.23087261002689,-2.4525627637421,12.5068768744332));
#441845=CARTESIAN_POINT('Ctrl Pts',(1.2302129501499,-2.45288950701127,12.5066032824114));
#441846=CARTESIAN_POINT('Ctrl Pts',(1.22950011797268,-2.45320577384133,
12.5064197834844));
#441847=CARTESIAN_POINT('Ctrl Pts',(1.22877496818874,-2.45349626581735,
12.5063282718343));
#441848=CARTESIAN_POINT('Ctrl Pts',(1.22771647400488,-2.4539202941683,12.5061946931565));
#441849=CARTESIAN_POINT('Ctrl Pts',(1.22660950568368,-2.45429945325867,
12.5062515701262));
#441850=CARTESIAN_POINT('Ctrl Pts',(1.22552777474128,-2.45462484192931,
12.5064436508398));
#441851=CARTESIAN_POINT('',(1.17140116758586,-2.4062642328984,12.5737548217797));
#441852=CARTESIAN_POINT('Origin',(1.17821023192281,-2.42025124983752,12.5893111709658));
#441853=CARTESIAN_POINT('Ctrl Pts',(1.22552777474128,-2.4546248419293,12.5064436508398));
#441854=CARTESIAN_POINT('Ctrl Pts',(1.21751531053644,-2.44746657362494,
12.5164271754438));
#441855=CARTESIAN_POINT('Ctrl Pts',(1.20949980939339,-2.44030531197305,
12.5264061185523));
#441856=CARTESIAN_POINT('Ctrl Pts',(1.20148116372314,-2.4331409522563,12.536380305637));
#441857=CARTESIAN_POINT('Ctrl Pts',(1.19145948299191,-2.42418695569907,
12.5488460165097));
#441858=CARTESIAN_POINT('Ctrl Pts',(1.18143288758693,-2.41522811732307,
12.5613043021964));
#441859=CARTESIAN_POINT('Ctrl Pts',(1.17140116758586,-2.4062642328984,12.5737548217797));
#441860=CARTESIAN_POINT('Ctrl Pts',(1.13565863606157,-2.43135141923565,
12.5893111709658));
#441861=CARTESIAN_POINT('Ctrl Pts',(1.13504681103698,-2.42003398557342,
12.5770542771492));
#441862=CARTESIAN_POINT('Ctrl Pts',(1.1509364505416,-2.416119521208,12.5737548217797));
#441863=CARTESIAN_POINT('Ctrl Pts',(1.135087808635,-2.42079235206263,12.5928319619712));
#441864=CARTESIAN_POINT('Ctrl Pts',(1.13792961703663,-2.41301047944868,
12.5821634970843));
#441865=CARTESIAN_POINT('Ctrl Pts',(1.15071908683469,-2.41227361814261,
12.5773203894503));
#441866=CARTESIAN_POINT('Ctrl Pts',(1.14124245786915,-2.40521337930624,
12.5969440695591));
#441867=CARTESIAN_POINT('Ctrl Pts',(1.14485617827555,-2.40345282048125,
12.5878292599214));
#441868=CARTESIAN_POINT('Ctrl Pts',(1.15291463227777,-2.40672170610216,
12.5813877129824));
#441869=CARTESIAN_POINT('Ctrl Pts',(1.16878594562417,-2.39188928354591,
12.596957478804));
#441870=CARTESIAN_POINT('Ctrl Pts',(1.16519896668808,-2.39363690343048,
12.5878468778671));
#441871=CARTESIAN_POINT('Ctrl Pts',(1.16277542598974,-2.40195819734556,
12.5814011370086));
#441872=CARTESIAN_POINT('Ctrl Pts',(1.18492453039319,-2.39677652088344,
12.5928371701607));
#441873=CARTESIAN_POINT('Ctrl Pts',(1.17707228826797,-2.39415404889869,
12.5821692192952));
#441874=CARTESIAN_POINT('Ctrl Pts',(1.16852082998896,-2.40368800837367,
12.5773318885715));
#441875=CARTESIAN_POINT('Ctrl Pts',(1.19283550652464,-2.40381648963776,
12.5893111709658));
#441876=CARTESIAN_POINT('Ctrl Pts',(1.18436864725012,-2.39628184110016,
12.5770542771492));
#441877=CARTESIAN_POINT('Ctrl Pts',(1.17140116758589,-2.40626423289836,
12.5737548217797));
#441878=CARTESIAN_POINT('',(1.1509364505416,-2.416119521208,12.5737548217797));
#441879=CARTESIAN_POINT('Origin',(1.15762655855612,-2.43016382449275,12.5893111709658));
#441880=CARTESIAN_POINT('Ctrl Pts',(1.17140116758589,-2.40626423289836,
12.5737548217797));
#441881=CARTESIAN_POINT('Ctrl Pts',(1.1706746487686,-2.40557395031917,12.5746934679442));
#441882=CARTESIAN_POINT('Ctrl Pts',(1.16974453062184,-2.40494290699951,
12.5756680099006));
#441883=CARTESIAN_POINT('Ctrl Pts',(1.16871850375878,-2.40444014209991,
12.5765688348656));
#441884=CARTESIAN_POINT('Ctrl Pts',(1.16844687450528,-2.40430704065853,
12.5768073183026));
#441885=CARTESIAN_POINT('Ctrl Pts',(1.16816868922902,-2.40418273344928,
12.5770407398754));
#441886=CARTESIAN_POINT('Ctrl Pts',(1.167886189766,-2.40406799376,12.5772674179684));
#441887=CARTESIAN_POINT('Ctrl Pts',(1.16672688836083,-2.40359713310213,
12.5781976435658));
#441888=CARTESIAN_POINT('Ctrl Pts',(1.16542484328481,-2.40327110227111,
12.5790594849312));
#441889=CARTESIAN_POINT('Ctrl Pts',(1.16405624123446,-2.40315875837296,
12.5797571720116));
#441890=CARTESIAN_POINT('Ctrl Pts',(1.16316454778811,-2.4030855622838,12.580211740231));
#441891=CARTESIAN_POINT('Ctrl Pts',(1.16220254220457,-2.40311845966298,
12.5806009430798));
#441892=CARTESIAN_POINT('Ctrl Pts',(1.16123855099109,-2.40327284102408,
12.5808812374708));
#441893=CARTESIAN_POINT('Ctrl Pts',(1.16041016273796,-2.40340550582875,
12.5811221033394));
#441894=CARTESIAN_POINT('Ctrl Pts',(1.15956336692619,-2.40363070930533,
12.581287365893));
#441895=CARTESIAN_POINT('Ctrl Pts',(1.15874810105404,-2.40394379849578,
12.581359338449));
#441896=CARTESIAN_POINT('Ctrl Pts',(1.15863479593241,-2.4039873114282,12.5813693411482));
#441897=CARTESIAN_POINT('Ctrl Pts',(1.15852206095077,-2.40403247634902,
12.5813775999465));
#441898=CARTESIAN_POINT('Ctrl Pts',(1.1584099895221,-2.40407923481949,12.5813841266931));
#441899=CARTESIAN_POINT('Ctrl Pts',(1.1582198467886,-2.40415856621996,12.5813952001081));
#441900=CARTESIAN_POINT('Ctrl Pts',(1.15803057506862,-2.40424357793756,
12.5814007534795));
#441901=CARTESIAN_POINT('Ctrl Pts',(1.15784233759719,-2.40433441284383,
12.5814005856065));
#441902=CARTESIAN_POINT('Ctrl Pts',(1.15698066004906,-2.40475021953056,
12.5813998171494));
#441903=CARTESIAN_POINT('Ctrl Pts',(1.15620004328975,-2.40525901524178,
12.58127954464));
#441904=CARTESIAN_POINT('Ctrl Pts',(1.1554887621719,-2.40583312261721,12.5810700125799));
#441905=CARTESIAN_POINT('Ctrl Pts',(1.15462961556737,-2.40652657895936,
12.5808169217085));
#441906=CARTESIAN_POINT('Ctrl Pts',(1.15388206277118,-2.40732841009892,
12.5804173076348));
#441907=CARTESIAN_POINT('Ctrl Pts',(1.15329256989121,-2.40815058618232,
12.5799304713245));
#441908=CARTESIAN_POINT('Ctrl Pts',(1.15256200250352,-2.40916952136183,
12.5793271277669));
#441909=CARTESIAN_POINT('Ctrl Pts',(1.1520027122323,-2.4102641478739,12.5785808224116));
#441910=CARTESIAN_POINT('Ctrl Pts',(1.15161003050752,-2.41137389420799,
12.5777485681082));
#441911=CARTESIAN_POINT('Ctrl Pts',(1.15102489171609,-2.41302753782757,
12.576508418016));
#441912=CARTESIAN_POINT('Ctrl Pts',(1.15080814330876,-2.41469853742023,
12.5750928681475));
#441913=CARTESIAN_POINT('Ctrl Pts',(1.1509364505416,-2.416119521208,12.5737548217797));
#441914=CARTESIAN_POINT('Ctrl Pts',(1.1509364505416,-2.416119521208,12.5737548217797));
#441915=CARTESIAN_POINT('Ctrl Pts',(1.13504681103698,-2.42003398557342,
12.5770542771492));
#441916=CARTESIAN_POINT('Ctrl Pts',(1.13565863606157,-2.43135141923565,
12.5893111709658));
#441917=CARTESIAN_POINT('Ctrl Pts',(1.15232332457213,-2.44083978687392,
12.5508408821982));
#441918=CARTESIAN_POINT('Ctrl Pts',(1.13638368550749,-2.44476325869343,
12.55409748406));
#441919=CARTESIAN_POINT('Ctrl Pts',(1.13699629106412,-2.45609513050247,
12.5663972313419));
#441920=CARTESIAN_POINT('Ctrl Pts',(1.15370766614038,-2.46553597002463,
12.52790050457));
#441921=CARTESIAN_POINT('Ctrl Pts',(1.13771799954522,-2.46944516936941,
12.5311362602938));
#441922=CARTESIAN_POINT('Ctrl Pts',(1.13833259659258,-2.48081387943054,
12.5434568539655));
#441923=CARTESIAN_POINT('Ctrl Pts',(1.1550896582248,-2.49020994295635,12.5049357605811));
#441924=CARTESIAN_POINT('Ctrl Pts',(1.13905002006211,-2.49408465489395,
12.5081700652078));
#441925=CARTESIAN_POINT('Ctrl Pts',(1.13966765833803,-2.50550962107533,
12.5204921097672));
#441926=CARTESIAN_POINT('Ctrl Pts',(1.15499890962265,-2.48858975326341,
12.5064436508395));
#441927=CARTESIAN_POINT('Ctrl Pts',(1.15399558653521,-2.48928415269658,
12.5062361689309));
#441928=CARTESIAN_POINT('Ctrl Pts',(1.15292260189464,-2.4899634873575,12.5061871075061));
#441929=CARTESIAN_POINT('Ctrl Pts',(1.15184870913824,-2.49056162696401,
12.5063648335164));
#441930=CARTESIAN_POINT('Ctrl Pts',(1.15136088080783,-2.49083333886806,
12.5064455676329));
#441931=CARTESIAN_POINT('Ctrl Pts',(1.15086595368983,-2.49109189321737,
12.506574497099));
#441932=CARTESIAN_POINT('Ctrl Pts',(1.15038466215084,-2.49132527247727,
12.5067492519495));
#441933=CARTESIAN_POINT('Ctrl Pts',(1.1494174881209,-2.49179425715915,12.5071004286051));
#441934=CARTESIAN_POINT('Ctrl Pts',(1.14846946575685,-2.49217809432416,
12.5076537929612));
#441935=CARTESIAN_POINT('Ctrl Pts',(1.14761529875447,-2.4924567420916,12.5083435010503));
#441936=CARTESIAN_POINT('Ctrl Pts',(1.14756152383705,-2.49247428463379,
12.5083869222963));
#441937=CARTESIAN_POINT('Ctrl Pts',(1.1475081113454,-2.49249140082923,12.5084308732336));
#441938=CARTESIAN_POINT('Ctrl Pts',(1.14745507574704,-2.49250808211731,
12.5084753333615));
#441939=CARTESIAN_POINT('Ctrl Pts',(1.14702966024818,-2.4926418880648,12.508831962269));
#441940=CARTESIAN_POINT('Ctrl Pts',(1.14662024509582,-2.4927516585159,12.509227847131));
#441941=CARTESIAN_POINT('Ctrl Pts',(1.14623972946254,-2.49283683395425,
12.5096423454524));
#441942=CARTESIAN_POINT('Ctrl Pts',(1.14504736187699,-2.49310373608097,
12.5109411997424));
#441943=CARTESIAN_POINT('Ctrl Pts',(1.14406753767241,-2.49315498662039,
12.5124831113042));
#441944=CARTESIAN_POINT('Ctrl Pts',(1.14326681185949,-2.493079114043,12.5140723025008));
#441945=CARTESIAN_POINT('Ctrl Pts',(1.14319178297381,-2.4930720046994,12.5142212114565));
#441946=CARTESIAN_POINT('Ctrl Pts',(1.14311830702035,-2.49306380147871,
12.5143705582413));
#441947=CARTESIAN_POINT('Ctrl Pts',(1.1430463464893,-2.49305459094164,12.5145201959299));
#441948=CARTESIAN_POINT('Ctrl Pts',(1.14212190632999,-2.49293626787997,
12.5164425148273));
#441949=CARTESIAN_POINT('Ctrl Pts',(1.14141452178073,-2.4926583022727,12.518463520594));
#441950=CARTESIAN_POINT('Ctrl Pts',(1.14085307427549,-2.49227619302178,
12.5205025929157));
#441951=CARTESIAN_POINT('Ctrl Pts',(1.14052741246874,-2.49205455451085,
12.5216853356836));
#441952=CARTESIAN_POINT('Ctrl Pts',(1.1402511668049,-2.49179867741584,12.5228750347131));
#441953=CARTESIAN_POINT('Ctrl Pts',(1.1400143670888,-2.49152384338772,12.5240609649613));
#441954=CARTESIAN_POINT('Ctrl Pts',(1.13943315488952,-2.49084927801005,
12.5269717671327));
#441955=CARTESIAN_POINT('Ctrl Pts',(1.13908109514514,-2.4900347395367,12.5299036066169));
#441956=CARTESIAN_POINT('Ctrl Pts',(1.13888520536176,-2.4891269513902,12.5328133004019));
#441957=CARTESIAN_POINT('Ctrl Pts',(1.13879116685943,-2.48869116022097,
12.5342101228452));
#441958=CARTESIAN_POINT('Ctrl Pts',(1.13873374826657,-2.48823431231207,
12.5356023438238));
#441959=CARTESIAN_POINT('Ctrl Pts',(1.13870826816973,-2.48776298739835,
12.5369868989719));
#441960=CARTESIAN_POINT('Origin',(1.8214655920365,-15.2154335410399,-1.24073622122997));
#441961=CARTESIAN_POINT('Ctrl Pts',(1.23500723661298,-2.4413450116302,12.5369868989719));
#441962=CARTESIAN_POINT('Ctrl Pts',(1.24644656774961,-2.45156386708624,
12.5369868989719));
#441963=CARTESIAN_POINT('Ctrl Pts',(1.25999060240651,-2.44436369841476,
12.5369868989719));
#441964=CARTESIAN_POINT('Ctrl Pts',(1.23887422203735,-2.44479933505252,
12.5218025310015));
#441965=CARTESIAN_POINT('Ctrl Pts',(1.24954275891247,-2.44988246250011,
12.5216901060418));
#441966=CARTESIAN_POINT('Ctrl Pts',(1.2599493234416,-2.444385661477,12.5161920673677));
#441967=CARTESIAN_POINT('Ctrl Pts',(1.23823476680908,-2.45079326266352,
12.5042015548895));
#441968=CARTESIAN_POINT('Ctrl Pts',(1.24445480582807,-2.45243291494978,
12.4980677368513));
#441969=CARTESIAN_POINT('Ctrl Pts',(1.25051277374003,-2.4493520377206,12.4907278922778));
#441970=CARTESIAN_POINT('Ctrl Pts',(1.22551884038576,-2.45460694722071,
12.506463626192));
#441971=CARTESIAN_POINT('Ctrl Pts',(1.22844143711359,-2.46046065260301,
12.4999376786891));
#441972=CARTESIAN_POINT('Ctrl Pts',(1.22840574184401,-2.46038915810304,
12.4906970594712));
#441973=CARTESIAN_POINT('Origin',(1.24966370657253,-2.4249380652865,12.5369868989719));
#441974=CARTESIAN_POINT('Origin',(1.24966370657253,-2.4249380652865,14.));
#441975=CARTESIAN_POINT('Origin',(1.24966370657253,-2.4249380652865,13.7435492065112));
#441976=CARTESIAN_POINT('Ctrl Pts',(1.21654179677687,-2.42491265430238,
13.793642941384));
#441977=CARTESIAN_POINT('Ctrl Pts',(1.22460084957725,-2.43212083624836,
13.8071662555867));
#441978=CARTESIAN_POINT('Ctrl Pts',(1.23769698055489,-2.42123457256189,
13.8103758687955));
#441979=CARTESIAN_POINT('Ctrl Pts',(1.22895834746436,-2.43596213276286,
13.7804579775006));
#441980=CARTESIAN_POINT('Ctrl Pts',(1.23890925070369,-2.44484881923482,
13.7901904343351));
#441981=CARTESIAN_POINT('Ctrl Pts',(1.25249575756948,-2.43686992486593,
13.7927914348262));
#441982=CARTESIAN_POINT('Ctrl Pts',(1.2362684381667,-2.44246737654277,13.7597120340895));
#441983=CARTESIAN_POINT('Ctrl Pts',(1.24778825257543,-2.45274750134554,
13.7635825532445));
#441984=CARTESIAN_POINT('Ctrl Pts',(1.26124114463959,-2.44607250237516,
13.7651073818884));
#441985=CARTESIAN_POINT('Ctrl Pts',(1.23483695502569,-2.44119350085692,
13.7381884353898));
#441986=CARTESIAN_POINT('Ctrl Pts',(1.24608652825463,-2.45123367081529,
13.7368803041982));
#441987=CARTESIAN_POINT('Ctrl Pts',(1.25952889624334,-2.4442700237841,13.7363986145813));
#441988=CARTESIAN_POINT('Origin',(1.23417990766365,-2.41115905006696,13.7902182540695));
#441989=CARTESIAN_POINT('Ctrl Pts',(1.1928325665529,-2.40381387234437,13.8235227101244));
#441990=CARTESIAN_POINT('Ctrl Pts',(1.20141832947106,-2.41146026779797,
13.8358800583119));
#441991=CARTESIAN_POINT('Ctrl Pts',(1.21448177232262,-2.40126357667189,
13.8390832900376));
#441992=CARTESIAN_POINT('Ctrl Pts',(1.20174288048452,-2.41174315068067,
13.8124254819052));
#441993=CARTESIAN_POINT('Ctrl Pts',(1.21034531701755,-2.41940439511813,
13.8247886449158));
#441994=CARTESIAN_POINT('Ctrl Pts',(1.22341477869201,-2.40918138417994,
13.8279860620657));
#441995=CARTESIAN_POINT('Ctrl Pts',(1.21064920110331,-2.4196688753724,13.8013225099955));
#441996=CARTESIAN_POINT('Ctrl Pts',(1.21926425094939,-2.42734135541361,
13.8136962257787));
#441997=CARTESIAN_POINT('Ctrl Pts',(1.23234346972625,-2.4170957289775,13.8168830918626));
#441998=CARTESIAN_POINT('Ctrl Pts',(1.21955168378293,-2.42759118468639,
13.7902140179785));
#441999=CARTESIAN_POINT('Ctrl Pts',(1.22817555201263,-2.43527152311001,
13.802602731458));
#442000=CARTESIAN_POINT('Ctrl Pts',(1.24126801376467,-2.42500674850007,
13.8057746032558));
#442001=CARTESIAN_POINT('Origin',(1.2074607811264,-2.38738172943809,13.8235269408515));
#442002=CARTESIAN_POINT('Ctrl Pts',(1.13565863606157,-2.43135141923565,
13.8235269408515));
#442003=CARTESIAN_POINT('Ctrl Pts',(1.13629602255825,-2.44314168459504,
13.8362179249168));
#442004=CARTESIAN_POINT('Ctrl Pts',(1.11961643194152,-2.44680968962709,
13.8391868794938));
#442005=CARTESIAN_POINT('Ctrl Pts',(1.13507545516088,-2.4205638396315,13.8400110824519));
#442006=CARTESIAN_POINT('Ctrl Pts',(1.13217047247447,-2.43020141912292,
13.8494522556837));
#442007=CARTESIAN_POINT('Ctrl Pts',(1.11876887391233,-2.42905031382129,
13.85569149686));
#442008=CARTESIAN_POINT('Ctrl Pts',(1.14093234808971,-2.40536204594572,
13.8586819406588));
#442009=CARTESIAN_POINT('Ctrl Pts',(1.13701571582525,-2.40726363352982,
13.868010383617));
#442010=CARTESIAN_POINT('Ctrl Pts',(1.1286276705421,-2.40386752353154,13.8744918421245));
#442011=CARTESIAN_POINT('Ctrl Pts',(1.16910085695503,-2.39173829439737,
13.8587686893867));
#442012=CARTESIAN_POINT('Ctrl Pts',(1.17298260663561,-2.38985358027126,
13.8680909899357));
#442013=CARTESIAN_POINT('Ctrl Pts',(1.17552108595147,-2.3811902942741,13.8745789365162));
#442014=CARTESIAN_POINT('Ctrl Pts',(1.18475191195684,-2.39662290792254,
13.8400379222776));
#442015=CARTESIAN_POINT('Ctrl Pts',(1.19409837626435,-2.40035303377248,
13.8494748685453));
#442016=CARTESIAN_POINT('Ctrl Pts',(1.20155166576407,-2.3891633250677,13.8557104837033));
#442017=CARTESIAN_POINT('Ctrl Pts',(1.19283550652889,-2.40381648963277,
13.8235269408542));
#442018=CARTESIAN_POINT('Ctrl Pts',(1.20165610319301,-2.41166592867512,
13.8362179249195));
#442019=CARTESIAN_POINT('Ctrl Pts',(1.21492341965357,-2.40091226334689,
13.8391868794965));
#442020=CARTESIAN_POINT('Origin',(1.11369071356702,-2.43253901397856,13.8235269408515));
#442021=CARTESIAN_POINT('Ctrl Pts',(1.13758917738513,-2.46706225337413,
13.7902140241682));
#442022=CARTESIAN_POINT('Ctrl Pts',(1.13821700711224,-2.4785932735036,13.8026027327198));
#442023=CARTESIAN_POINT('Ctrl Pts',(1.12202867321912,-2.48242938847038,
13.8057746032556));
#442024=CARTESIAN_POINT('Ctrl Pts',(1.13694587371134,-2.45516253307467,
13.8013225161808));
#442025=CARTESIAN_POINT('Ctrl Pts',(1.13757305769207,-2.4666817590964,13.8136962270464));
#442026=CARTESIAN_POINT('Ctrl Pts',(1.12140795129213,-2.47051945897936,
13.8168830918628));
#442027=CARTESIAN_POINT('Ctrl Pts',(1.13630229270357,-2.44325768269871,
13.8124254880875));
#442028=CARTESIAN_POINT('Ctrl Pts',(1.1369285566201,-2.45476004195875,13.8247886461867));
#442029=CARTESIAN_POINT('Ctrl Pts',(1.1207872151701,-2.45860421396228,13.8279860620656));
#442030=CARTESIAN_POINT('Ctrl Pts',(1.13565842313425,-2.43134749456069,
13.8235227163065));
#442031=CARTESIAN_POINT('Ctrl Pts',(1.13628347348943,-2.44282755968639,
13.8358800595847));
#442032=CARTESIAN_POINT('Ctrl Pts',(1.12016646235943,-2.44668343611513,
13.8390832900376));
#442033=CARTESIAN_POINT('Origin',(1.11562146849286,-2.46825378521705,13.7902182540695));
#442034=CARTESIAN_POINT('Ctrl Pts',(1.13869367316181,-2.48749352245962,
13.7382347919292));
#442035=CARTESIAN_POINT('Ctrl Pts',(1.13953223696443,-2.50256052878079,
13.7369371795943));
#442036=CARTESIAN_POINT('Ctrl Pts',(1.12569260757996,-2.50872562695685,
13.7364597369712));
#442037=CARTESIAN_POINT('Ctrl Pts',(1.13879578288449,-2.48938232302847,
13.7595490285574));
#442038=CARTESIAN_POINT('Ctrl Pts',(1.13965335022948,-2.50480887107615,
13.7633824266925));
#442039=CARTESIAN_POINT('Ctrl Pts',(1.12603045845521,-2.51115792455001,
13.7648920890506));
#442040=CARTESIAN_POINT('Ctrl Pts',(1.13827502890081,-2.47974954360394,
13.7803806590111));
#442041=CARTESIAN_POINT('Ctrl Pts',(1.139022184095,-2.49309265587658,13.7901039518745));
#442042=CARTESIAN_POINT('Ctrl Pts',(1.12431173525789,-2.49875729500326,
13.7926933640892));
#442043=CARTESIAN_POINT('Ctrl Pts',(1.13736984215328,-2.46300562266155,
13.7936647693663));
#442044=CARTESIAN_POINT('Ctrl Pts',(1.13798360340382,-2.47380361456152,
13.8072068914932));
#442045=CARTESIAN_POINT('Ctrl Pts',(1.12128698319839,-2.47724848662918,
13.8104111085397));
#442046=CARTESIAN_POINT('Origin',(1.11674034567518,-2.48895058214125,13.7435492065112));
#442047=CARTESIAN_POINT('Origin',(1.11674034567518,-2.48895058214125,14.));
#442048=CARTESIAN_POINT('Origin',(1.11674034567518,-2.48895058214125,12.5369868989719));
#442049=CARTESIAN_POINT('Ctrl Pts',(1.15499117054605,-2.48857307842948,
12.506462012331));
#442050=CARTESIAN_POINT('Ctrl Pts',(1.15774383942968,-2.49450404816529,
12.4999388158272));
#442051=CARTESIAN_POINT('Ctrl Pts',(1.15771127174688,-2.49443387701532,
12.4907030323752));
#442052=CARTESIAN_POINT('Ctrl Pts',(1.1440804381578,-2.49613512193016,12.5042014951932));
#442053=CARTESIAN_POINT('Ctrl Pts',(1.14148625048243,-2.50201825777945,
12.4980716682127));
#442054=CARTESIAN_POINT('Ctrl Pts',(1.13530546092887,-2.50483311225539,
12.4907355092743));
#442055=CARTESIAN_POINT('Ctrl Pts',(1.1389949678552,-2.49290035871678,12.5218047446509));
#442056=CARTESIAN_POINT('Ctrl Pts',(1.13631761128863,-2.50440473322178,
12.5216906929434));
#442057=CARTESIAN_POINT('Ctrl Pts',(1.12553862196712,-2.50911473784347,
12.5161988840776));
#442058=CARTESIAN_POINT('Ctrl Pts',(1.13870616091534,-2.4877246291098,12.5369868989719));
#442059=CARTESIAN_POINT('Ctrl Pts',(1.13956042115541,-2.50303069885232,
12.5369868989719));
#442060=CARTESIAN_POINT('Ctrl Pts',(1.12549728860093,-2.50913265216876,
12.5369868989719));
#442061=CARTESIAN_POINT('Origin',(2.23530940884416E-31,-9.79353041666012E-31,
12.5));
#442062=CARTESIAN_POINT('Origin',(1.33005753786835,-2.3306945761811,12.5));
#442063=CARTESIAN_POINT('',(1.33005753786835,-2.3306945761811,12.5893111709658));
#442064=CARTESIAN_POINT('',(1.33005753786835,-2.3306945761811,13.8235269408515));
#442065=CARTESIAN_POINT('',(1.33005753786835,-2.3306945761811,12.5));
#442066=CARTESIAN_POINT('',(1.33489295378215,-2.36613313501385,13.7902182540695));
#442067=CARTESIAN_POINT('',(1.33005753786835,-2.3306945761811,13.8235269408515));
#442068=CARTESIAN_POINT('',(1.33769508908196,-2.38666986617615,13.7435492065112));
#442069=CARTESIAN_POINT('Origin',(1.32847642374838,-2.31910424806525,13.7445212918691));
#442070=CARTESIAN_POINT('',(1.33769508908196,-2.38666986617615,12.5369868989719));
#442071=CARTESIAN_POINT('',(1.33769508908196,-2.38666986617615,12.5));
#442072=CARTESIAN_POINT('Ctrl Pts',(1.33769508908196,-2.38666986617615,
12.5369868989719));
#442073=CARTESIAN_POINT('Ctrl Pts',(1.33515109546587,-2.36802504450181,
12.5544431401645));
#442074=CARTESIAN_POINT('Ctrl Pts',(1.33260528231792,-2.34936688755546,
12.5718848856037));
#442075=CARTESIAN_POINT('Ctrl Pts',(1.33005753786835,-2.3306945761811,12.5893111709658));
#442076=CARTESIAN_POINT('Origin',(1.60445193644508,-2.46405362951698,12.5));
#442077=CARTESIAN_POINT('',(1.4299234933485,-2.33258226106547,13.7435492065112));
#442078=CARTESIAN_POINT('',(1.41336809784464,-2.32011116773803,13.7902182540695));
#442079=CARTESIAN_POINT('Origin',(1.36986337980535,-2.28733928990974,13.7418732680433));
#442080=CARTESIAN_POINT('',(1.38479980462764,-2.29859082104312,13.8235269408515));
#442081=CARTESIAN_POINT('',(1.41336809784464,-2.32011116773803,13.7902182540695));
#442082=CARTESIAN_POINT('',(1.38479980462764,-2.29859082104312,12.5893111709658));
#442083=CARTESIAN_POINT('',(1.38479980462764,-2.29859082104312,12.5));
#442084=CARTESIAN_POINT('',(1.4299234933485,-2.33258226106547,12.5369868989719));
#442085=CARTESIAN_POINT('Ctrl Pts',(1.38479980462764,-2.29859082104312,
12.5893111709658));
#442086=CARTESIAN_POINT('Ctrl Pts',(1.39985222447629,-2.30992973062655,
12.5718848856037));
#442087=CARTESIAN_POINT('Ctrl Pts',(1.4148932339329,-2.321260044821,12.5544431401645));
#442088=CARTESIAN_POINT('Ctrl Pts',(1.4299234933485,-2.33258226106547,12.5369868989719));
#442089=CARTESIAN_POINT('',(1.4299234933485,-2.33258226106547,12.5));
#442090=CARTESIAN_POINT('Origin',(1.36411695356841,-2.3260473375203,12.5));
#442091=CARTESIAN_POINT('',(1.34577128976252,-2.29697799298522,13.8587068136939));
#442092=CARTESIAN_POINT('Ctrl Pts',(1.3847998046315,-2.29859082103775,13.8235269408542));
#442093=CARTESIAN_POINT('Ctrl Pts',(1.38340018258377,-2.29753649302872,
13.8262006681044));
#442094=CARTESIAN_POINT('Ctrl Pts',(1.38186333792216,-2.29659631404677,
13.8288634856214));
#442095=CARTESIAN_POINT('Ctrl Pts',(1.38020039422952,-2.29576293072852,
13.8314912288862));
#442096=CARTESIAN_POINT('Ctrl Pts',(1.3784860708071,-2.2949037984869,13.8342001611531));
#442097=CARTESIAN_POINT('Ctrl Pts',(1.37663605428186,-2.29415676465242,
13.8368750301949));
#442098=CARTESIAN_POINT('Ctrl Pts',(1.37462670689041,-2.29354133620147,
13.8394886372969));
#442099=CARTESIAN_POINT('Ctrl Pts',(1.37447152011737,-2.29349380516939,
13.8396904925131));
#442100=CARTESIAN_POINT('Ctrl Pts',(1.37431537292207,-2.29344707888645,
13.8398919674349));
#442101=CARTESIAN_POINT('Ctrl Pts',(1.37415825014436,-2.29340117695641,
13.8400930404591));
#442102=CARTESIAN_POINT('Ctrl Pts',(1.37171017156055,-2.29268599400502,
13.8432258934518));
#442103=CARTESIAN_POINT('Ctrl Pts',(1.36903807042446,-2.29217349775966,
13.8462331177034));
#442104=CARTESIAN_POINT('Ctrl Pts',(1.3662109257099,-2.29197514260721,13.8489036603661));
#442105=CARTESIAN_POINT('Ctrl Pts',(1.36528585105815,-2.29191023849295,
13.8497774930041));
#442106=CARTESIAN_POINT('Ctrl Pts',(1.3643443752974,-2.29187911987411,13.85061494757));
#442107=CARTESIAN_POINT('Ctrl Pts',(1.36338949058611,-2.29188611370955,
13.8514076489583));
#442108=CARTESIAN_POINT('Ctrl Pts',(1.36136977170674,-2.29190090668017,
13.8530843267192));
#442109=CARTESIAN_POINT('Ctrl Pts',(1.35909169550347,-2.29209061940835,
13.8546805203176));
#442110=CARTESIAN_POINT('Ctrl Pts',(1.35669880437277,-2.29258021605276,
13.8559412814274));
#442111=CARTESIAN_POINT('Ctrl Pts',(1.35637855793619,-2.29264573996178,
13.8561100121513));
#442112=CARTESIAN_POINT('Ctrl Pts',(1.35605629207205,-2.29271656782227,
13.8562727473908));
#442113=CARTESIAN_POINT('Ctrl Pts',(1.35573237882863,-2.29279292867908,
13.8564289040185));
#442114=CARTESIAN_POINT('Ctrl Pts',(1.35426343596501,-2.29313922429353,
13.8571370725437));
#442115=CARTESIAN_POINT('Ctrl Pts',(1.35273531532566,-2.29360761478373,
13.8577210840554));
#442116=CARTESIAN_POINT('Ctrl Pts',(1.35121601586956,-2.29420795324734,
13.8581177131616));
#442117=CARTESIAN_POINT('Ctrl Pts',(1.35078812885002,-2.29437702922171,
13.8582294175695));
#442118=CARTESIAN_POINT('Ctrl Pts',(1.35036090986562,-2.29455639626784,
13.8583265086086));
#442119=CARTESIAN_POINT('Ctrl Pts',(1.34993577393002,-2.29474584738435,
13.8584082369006));
#442120=CARTESIAN_POINT('Ctrl Pts',(1.34932496759527,-2.29501803783546,
13.8585256585398));
#442121=CARTESIAN_POINT('Ctrl Pts',(1.34871099893909,-2.29531472312331,
13.8586122832068));
#442122=CARTESIAN_POINT('Ctrl Pts',(1.34811016067259,-2.29562890724788,
13.8586682984299));
#442123=CARTESIAN_POINT('Ctrl Pts',(1.34762954961857,-2.29588022340347,
13.8587131050557));
#442124=CARTESIAN_POINT('Ctrl Pts',(1.34715192292426,-2.29614530403958,
13.8587357943552));
#442125=CARTESIAN_POINT('Ctrl Pts',(1.34667746959686,-2.29642462347374,
13.8587355499465));
#442126=CARTESIAN_POINT('Ctrl Pts',(1.34637081909986,-2.29660515428332,
13.8587353919793));
#442127=CARTESIAN_POINT('Ctrl Pts',(1.34606879068543,-2.29678964756824,
13.8587257282814));
#442128=CARTESIAN_POINT('Ctrl Pts',(1.34577128976252,-2.29697799298522,
13.8587068136939));
#442129=CARTESIAN_POINT('Ctrl Pts',(1.34577128976252,-2.29697799298522,
13.8587068136939));
#442130=CARTESIAN_POINT('Ctrl Pts',(1.34479282544556,-2.29759745079387,
13.8586446046466));
#442131=CARTESIAN_POINT('Ctrl Pts',(1.3438632747108,-2.2982585267788,13.858482427929));
#442132=CARTESIAN_POINT('Ctrl Pts',(1.34297980313987,-2.29895776376923,
13.8582284286032));
#442133=CARTESIAN_POINT('Ctrl Pts',(1.34207346407774,-2.29967509958282,
13.8579678548414));
#442134=CARTESIAN_POINT('Ctrl Pts',(1.34121435705807,-2.30043555072053,
13.857615680862));
#442135=CARTESIAN_POINT('Ctrl Pts',(1.34042992937994,-2.30120188140978,
13.8571944833187));
#442136=CARTESIAN_POINT('Ctrl Pts',(1.33847230988447,-2.30311433801868,
13.8561433417727));
#442137=CARTESIAN_POINT('Ctrl Pts',(1.33688487323664,-2.30514944118479,
13.8546163505474));
#442138=CARTESIAN_POINT('Ctrl Pts',(1.33562829342631,-2.30710418516538,
13.8528973491086));
#442139=CARTESIAN_POINT('Ctrl Pts',(1.33539873483407,-2.30746128805108,
13.8525833129072));
#442140=CARTESIAN_POINT('Ctrl Pts',(1.33518007748481,-2.30781569617413,
13.8522628768812));
#442141=CARTESIAN_POINT('Ctrl Pts',(1.33497190318365,-2.30816618356834,
13.851937733538));
#442142=CARTESIAN_POINT('Ctrl Pts',(1.33370061160934,-2.31030656145685,
13.8499521282529));
#442143=CARTESIAN_POINT('Ctrl Pts',(1.33269743617666,-2.31251551658544,
13.847639871647));
#442144=CARTESIAN_POINT('Ctrl Pts',(1.33194194943937,-2.31464373378926,
13.8452109780794));
#442145=CARTESIAN_POINT('Ctrl Pts',(1.33160204031847,-2.31560126276115,
13.8441181685877));
#442146=CARTESIAN_POINT('Ctrl Pts',(1.3313115527633,-2.31654245669621,13.8430021611332));
#442147=CARTESIAN_POINT('Ctrl Pts',(1.33106549254158,-2.31745477819194,
13.8418824960098));
#442148=CARTESIAN_POINT('Ctrl Pts',(1.33048564534573,-2.31960468709359,
13.8392439765549));
#442149=CARTESIAN_POINT('Ctrl Pts',(1.33012114163059,-2.3216960510513,13.8364981347964));
#442150=CARTESIAN_POINT('Ctrl Pts',(1.32993730510416,-2.32372852519983,
13.8336931113419));
#442151=CARTESIAN_POINT('Ctrl Pts',(1.32975826000211,-2.32570802594645,
13.8309611966328));
#442152=CARTESIAN_POINT('Ctrl Pts',(1.32975096988766,-2.3276337010985,13.8281701127186));
#442153=CARTESIAN_POINT('Ctrl Pts',(1.32992114581565,-2.32949429007333,
13.8253580685121));
#442154=CARTESIAN_POINT('Ctrl Pts',(1.3299580401405,-2.32989766777108,13.8247484142933));
#442155=CARTESIAN_POINT('Ctrl Pts',(1.33000341022909,-2.33029787700102,
13.8241378483365));
#442156=CARTESIAN_POINT('Ctrl Pts',(1.33005753786835,-2.3306945761811,13.8235269408515));
#442157=CARTESIAN_POINT('',(1.34683346955762,-2.29633413668072,12.5969504640361));
#442158=CARTESIAN_POINT('Origin',(1.3641335218256,-2.32607597622948,12.584524458991));
#442159=CARTESIAN_POINT('Origin',(1.3641335218256,-2.32607597622948,12.584524458991));
#442160=CARTESIAN_POINT('Ctrl Pts',(1.38479980462764,-2.29859082104312,
12.5893111709658));
#442161=CARTESIAN_POINT('Ctrl Pts',(1.37574697432481,-2.29177137106032,
12.5770542771492));
#442162=CARTESIAN_POINT('Ctrl Pts',(1.36363630048298,-2.30277751725014,
12.5737548217797));
#442163=CARTESIAN_POINT('Ctrl Pts',(1.40459530627978,-2.31350266948006,
12.5663937883685));
#442164=CARTESIAN_POINT('Ctrl Pts',(1.39553092783467,-2.30667452034175,
12.5540940315304));
#442165=CARTESIAN_POINT('Ctrl Pts',(1.38338488516658,-2.31771714877968,
12.5508374392248));
#442166=CARTESIAN_POINT('Ctrl Pts',(1.42437083451345,-2.32839947204475,
12.5434499600945));
#442167=CARTESIAN_POINT('Ctrl Pts',(1.41527698454607,-2.321549122162,12.5311293540533));
#442168=CARTESIAN_POINT('Ctrl Pts',(1.40311488688602,-2.3326412430173,12.5278936106989));
#442169=CARTESIAN_POINT('Ctrl Pts',(1.4441279538738,-2.34328240730091,12.5204817579905));
#442170=CARTESIAN_POINT('Ctrl Pts',(1.43498909556389,-2.33639815286782,
12.5081597038247));
#442171=CARTESIAN_POINT('Ctrl Pts',(1.42282775834021,-2.34755099653329,
12.5049254088044));
#442172=CARTESIAN_POINT('Ctrl Pts',(1.4299234933485,-2.33258226106547,12.5369868989719));
#442173=CARTESIAN_POINT('Ctrl Pts',(1.4306675187513,-2.33314273173438,12.5342545179733));
#442174=CARTESIAN_POINT('Ctrl Pts',(1.43130252505372,-2.33377725841565,
12.5314872231885));
#442175=CARTESIAN_POINT('Ctrl Pts',(1.43175322838372,-2.3344896400679,12.5287124745063));
#442176=CARTESIAN_POINT('Ctrl Pts',(1.43215969501762,-2.33513210120137,
12.5262100684184));
#442177=CARTESIAN_POINT('Ctrl Pts',(1.43241502064328,-2.33583776199992,
12.5237004536639));
#442178=CARTESIAN_POINT('Ctrl Pts',(1.43246125367359,-2.33664129362863,
12.5212220730815));
#442179=CARTESIAN_POINT('Ctrl Pts',(1.43249664905777,-2.33725646660144,
12.5193246583486));
#442180=CARTESIAN_POINT('Ctrl Pts',(1.43240928001402,-2.33793639253365,
12.517417831369));
#442181=CARTESIAN_POINT('Ctrl Pts',(1.43210215847269,-2.33868795162138,
12.5155812248348));
#442182=CARTESIAN_POINT('Ctrl Pts',(1.4319713230453,-2.3390081198324,12.5147988205793));
#442183=CARTESIAN_POINT('Ctrl Pts',(1.4318007304294,-2.33934171787815,12.5140295443047));
#442184=CARTESIAN_POINT('Ctrl Pts',(1.43158405520617,-2.339691052389,12.5132817086137));
#442185=CARTESIAN_POINT('Ctrl Pts',(1.43125614656697,-2.34021972291427,
12.5121499604604));
#442186=CARTESIAN_POINT('Ctrl Pts',(1.43080953768677,-2.34079208086607,
12.5110494206568));
#442187=CARTESIAN_POINT('Ctrl Pts',(1.43020905781341,-2.34139588218719,
12.5100666561695));
#442188=CARTESIAN_POINT('Ctrl Pts',(1.42986426365291,-2.34174258351535,
12.5095023550641));
#442189=CARTESIAN_POINT('Ctrl Pts',(1.42946429115295,-2.34210319734582,
12.5089719619137));
#442190=CARTESIAN_POINT('Ctrl Pts',(1.42901236051004,-2.34246622073481,
12.5085043804652));
#442191=CARTESIAN_POINT('Ctrl Pts',(1.42835101888226,-2.34299745817747,
12.5078201359221));
#442192=CARTESIAN_POINT('Ctrl Pts',(1.42755847393475,-2.34354832160772,
12.5072563000949));
#442193=CARTESIAN_POINT('Ctrl Pts',(1.42668361668369,-2.34407451888694,
12.5068768744332));
#442194=CARTESIAN_POINT('Ctrl Pts',(1.4260527843803,-2.34445394334879,12.5066032824114));
#442195=CARTESIAN_POINT('Ctrl Pts',(1.42536810277607,-2.34482726026711,
12.5064197834844));
#442196=CARTESIAN_POINT('Ctrl Pts',(1.42466904366106,-2.3451758920944,12.5063282718343));
#442197=CARTESIAN_POINT('Ctrl Pts',(1.42364863377637,-2.34568478662856,
12.5061946931565));
#442198=CARTESIAN_POINT('Ctrl Pts',(1.42257625378674,-2.34615291229311,
12.5062515701262));
#442199=CARTESIAN_POINT('Ctrl Pts',(1.42152464441223,-2.34656538937389,
12.5064436508398));
#442200=CARTESIAN_POINT('',(1.36363630048298,-2.30277751725014,12.5737548217797));
#442201=CARTESIAN_POINT('Origin',(1.37156277994973,-2.31616299158851,12.5893111709658));
#442202=CARTESIAN_POINT('Ctrl Pts',(1.42152464441223,-2.34656538937389,
12.5064436508398));
#442203=CARTESIAN_POINT('Ctrl Pts',(1.41295537570013,-2.34008402983357,
12.5164271754438));
#442204=CARTESIAN_POINT('Ctrl Pts',(1.40438283616937,-2.33359993444451,
12.5264061185523));
#442205=CARTESIAN_POINT('Ctrl Pts',(1.39580691005351,-2.32711300760729,
12.536380305637));
#442206=CARTESIAN_POINT('Ctrl Pts',(1.38508874179391,-2.3190056647513,12.5488460165097));
#442207=CARTESIAN_POINT('Ctrl Pts',(1.37436528056057,-2.31089389677882,
12.5613043021964));
#442208=CARTESIAN_POINT('Ctrl Pts',(1.36363630048298,-2.30277751725014,
12.5737548217797));
#442209=CARTESIAN_POINT('Ctrl Pts',(1.33005753786835,-2.3306945761811,12.5893111709658));
#442210=CARTESIAN_POINT('Ctrl Pts',(1.32852527273166,-2.31946466976517,
12.5770542771492));
#442211=CARTESIAN_POINT('Ctrl Pts',(1.34404297558573,-2.31426807732516,
12.5737548217797));
#442212=CARTESIAN_POINT('Ctrl Pts',(1.32862794782275,-2.32021717116761,
12.5928319619712));
#442213=CARTESIAN_POINT('Ctrl Pts',(1.33082600547995,-2.31222955832602,
12.5821634970842));
#442214=CARTESIAN_POINT('Ctrl Pts',(1.34351285833518,-2.31045268834498,
12.5773203894503));
#442215=CARTESIAN_POINT('Ctrl Pts',(1.33349228706153,-2.30418837510834,
12.5969440695591));
#442216=CARTESIAN_POINT('Ctrl Pts',(1.33695048122292,-2.30213912263633,
12.5878292599214));
#442217=CARTESIAN_POINT('Ctrl Pts',(1.34524856590918,-2.30474029249778,
12.5813877129824));
#442218=CARTESIAN_POINT('Ctrl Pts',(1.35985808863388,-2.28866356422419,
12.596957478804));
#442219=CARTESIAN_POINT('Ctrl Pts',(1.356425492319,-2.29069774113094,12.5878468778671));
#442220=CARTESIAN_POINT('Ctrl Pts',(1.35468827845761,-2.29918888769294,
12.5814011370086));
#442221=CARTESIAN_POINT('Ctrl Pts',(1.37634132880733,-2.29221909520066,
12.5928371701607));
#442222=CARTESIAN_POINT('Ctrl Pts',(1.36830145855742,-2.29024537990497,
12.5821692192952));
#442223=CARTESIAN_POINT('Ctrl Pts',(1.36055556075656,-2.30044463915389,
12.5773318885715));
#442224=CARTESIAN_POINT('Ctrl Pts',(1.38479980462767,-2.29859082104307,
12.5893111709658));
#442225=CARTESIAN_POINT('Ctrl Pts',(1.37574697432484,-2.29177137106028,
12.5770542771492));
#442226=CARTESIAN_POINT('Ctrl Pts',(1.36363630048301,-2.3027775172501,12.5737548217797));
#442227=CARTESIAN_POINT('',(1.34404297558573,-2.31426807732516,12.5737548217797));
#442228=CARTESIAN_POINT('Origin',(1.35185556391639,-2.32772034343819,12.5893111709658));
#442229=CARTESIAN_POINT('Ctrl Pts',(1.36363630048301,-2.3027775172501,12.5737548217797));
#442230=CARTESIAN_POINT('Ctrl Pts',(1.36285593465867,-2.30214874955753,
12.5746934679442));
#442231=CARTESIAN_POINT('Ctrl Pts',(1.36187747551444,-2.30159561924621,
12.5756680099006));
#442232=CARTESIAN_POINT('Ctrl Pts',(1.36081388266436,-2.30117815796984,
12.5765688348656));
#442233=CARTESIAN_POINT('Ctrl Pts',(1.36053230823167,-2.30106763971838,
12.5768073183026));
#442234=CARTESIAN_POINT('Ctrl Pts',(1.36024491640241,-2.30096642081367,
12.5770407398754));
#442235=CARTESIAN_POINT('Ctrl Pts',(1.35995400458318,-2.30087508924008,
12.5772674179684));
#442236=CARTESIAN_POINT('Ctrl Pts',(1.35876018114294,-2.30050028915916,
12.5781976435658));
#442237=CARTESIAN_POINT('Ctrl Pts',(1.35743589397504,-2.30028147193012,
12.5790594849312));
#442238=CARTESIAN_POINT('Ctrl Pts',(1.35606268876446,-2.30028105561961,
12.5797571720116));
#442239=CARTESIAN_POINT('Ctrl Pts',(1.35516799619371,-2.30028078437835,
12.580211740231));
#442240=CARTESIAN_POINT('Ctrl Pts',(1.3542118730462,-2.3003919846801,12.5806009430798));
#442241=CARTESIAN_POINT('Ctrl Pts',(1.35326367294809,-2.30062442658311,
12.5808812374708));
#442242=CARTESIAN_POINT('Ctrl Pts',(1.35244885450172,-2.3008241712896,12.5811221033394));
#442243=CARTESIAN_POINT('Ctrl Pts',(1.35162323250718,-2.30111764714012,
12.581287365893));
#442244=CARTESIAN_POINT('Ctrl Pts',(1.35083619904058,-2.30149614628925,
12.581359338449));
#442245=CARTESIAN_POINT('Ctrl Pts',(1.35072681764034,-2.30154874985527,
12.5813693411482));
#442246=CARTESIAN_POINT('Ctrl Pts',(1.35061813913538,-2.30160295344113,
12.5813775999465));
#442247=CARTESIAN_POINT('Ctrl Pts',(1.35051025186457,-2.3016586911885,12.5813841266931));
#442248=CARTESIAN_POINT('Ctrl Pts',(1.35032720806094,-2.30175325701826,
12.5813952001081));
#442249=CARTESIAN_POINT('Ctrl Pts',(1.3501454953712,-2.30185341326867,12.5814007534795));
#442250=CARTESIAN_POINT('Ctrl Pts',(1.34996528813256,-2.30195928903071,
12.5814005856065));
#442251=CARTESIAN_POINT('Ctrl Pts',(1.34914036985051,-2.30244394687459,
12.5813998171494));
#442252=CARTESIAN_POINT('Ctrl Pts',(1.34840382210296,-2.30301467712284,
12.58127954464));
#442253=CARTESIAN_POINT('Ctrl Pts',(1.34774170279521,-2.30364485021765,
12.5810700125799));
#442254=CARTESIAN_POINT('Ctrl Pts',(1.34694193805975,-2.30440602756523,
12.5808169217085));
#442255=CARTESIAN_POINT('Ctrl Pts',(1.34626222936553,-2.30526612317064,
12.5804173076348));
#442256=CARTESIAN_POINT('Ctrl Pts',(1.345741712958,-2.30613361267326,12.5799304713245));
#442257=CARTESIAN_POINT('Ctrl Pts',(1.34509662914949,-2.30720870545437,
12.5793271277669));
#442258=CARTESIAN_POINT('Ctrl Pts',(1.34462842209326,-2.30834527703632,
12.5785808224116));
#442259=CARTESIAN_POINT('Ctrl Pts',(1.34432750161313,-2.30948333798708,
12.5777485681082));
#442260=CARTESIAN_POINT('Ctrl Pts',(1.34387909712944,-2.31117917348759,
12.576508418016));
#442261=CARTESIAN_POINT('Ctrl Pts',(1.34379927191416,-2.31286227997435,
12.5750928681475));
#442262=CARTESIAN_POINT('Ctrl Pts',(1.34404297558573,-2.31426807732516,
12.5737548217797));
#442263=CARTESIAN_POINT('Ctrl Pts',(1.34404297558573,-2.31426807732516,
12.5737548217797));
#442264=CARTESIAN_POINT('Ctrl Pts',(1.32852527273166,-2.31946466976517,
12.5770542771492));
#442265=CARTESIAN_POINT('Ctrl Pts',(1.33005753786835,-2.3306945761811,12.5893111709658));
#442266=CARTESIAN_POINT('Ctrl Pts',(1.34744016605087,-2.33879304523776,
12.5508408821982));
#442267=CARTESIAN_POINT('Ctrl Pts',(1.33187336419732,-2.3440026905886,12.55409748406));
#442268=CARTESIAN_POINT('Ctrl Pts',(1.33340758411188,-2.35524692348901,
12.5663972313419));
#442269=CARTESIAN_POINT('Ctrl Pts',(1.35083286953169,-2.36329421718692,
12.52790050457));
#442270=CARTESIAN_POINT('Ctrl Pts',(1.33521504327091,-2.36849371526164,
12.5311362602938));
#442271=CARTESIAN_POINT('Ctrl Pts',(1.33675425070924,-2.37977450151295,
12.5434568539655));
#442272=CARTESIAN_POINT('Ctrl Pts',(1.3542214210074,-2.3877734443245,12.5049357605811));
#442273=CARTESIAN_POINT('Ctrl Pts',(1.3385509784115,-2.39294264289276,12.5081700652078));
#442274=CARTESIAN_POINT('Ctrl Pts',(1.34009780235499,-2.4042792501883,12.5204921097672));
#442275=CARTESIAN_POINT('Ctrl Pts',(1.35399891386265,-2.38616604253264,
12.5064436508395));
#442276=CARTESIAN_POINT('Ctrl Pts',(1.3530555292503,-2.38693991155501,12.5062361689309));
#442277=CARTESIAN_POINT('Ctrl Pts',(1.35204148695911,-2.3877044439952,12.5061871075061));
#442278=CARTESIAN_POINT('Ctrl Pts',(1.35101992142306,-2.38838812557069,
12.5063648335164));
#442279=CARTESIAN_POINT('Ctrl Pts',(1.3505558633438,-2.3886986959135,12.5064455676329));
#442280=CARTESIAN_POINT('Ctrl Pts',(1.35008365763473,-2.38899673109934,
12.506574497099));
#442281=CARTESIAN_POINT('Ctrl Pts',(1.3496229901299,-2.38926856353753,12.5067492519495));
#442282=CARTESIAN_POINT('Ctrl Pts',(1.34869726089708,-2.38981482137387,
12.5071004286051));
#442283=CARTESIAN_POINT('Ctrl Pts',(1.34778367929148,-2.39027465397608,
12.5076537929613));
#442284=CARTESIAN_POINT('Ctrl Pts',(1.34695506683916,-2.39062199710647,
12.5083435010505));
#442285=CARTESIAN_POINT('Ctrl Pts',(1.34690290073347,-2.39064386443225,
12.5083869222964));
#442286=CARTESIAN_POINT('Ctrl Pts',(1.3468510610964,-2.39066527728885,12.5084308732337));
#442287=CARTESIAN_POINT('Ctrl Pts',(1.34679956164954,-2.39068622596491,
12.5084753333615));
#442288=CARTESIAN_POINT('Ctrl Pts',(1.34638646811256,-2.39085426199668,
12.5088319622689));
#442289=CARTESIAN_POINT('Ctrl Pts',(1.34598736256616,-2.39099703833141,
12.509227847131));
#442290=CARTESIAN_POINT('Ctrl Pts',(1.34561505565621,-2.39111294591216,
12.5096423454524));
#442291=CARTESIAN_POINT('Ctrl Pts',(1.34444841057657,-2.3914761489717,12.5109411997424));
#442292=CARTESIAN_POINT('Ctrl Pts',(1.34347602405095,-2.39160709374809,
12.5124831113042));
#442293=CARTESIAN_POINT('Ctrl Pts',(1.34267177826769,-2.39159674021777,
12.5140723025007));
#442294=CARTESIAN_POINT('Ctrl Pts',(1.34259641955694,-2.39159577008064,
12.5142212114565));
#442295=CARTESIAN_POINT('Ctrl Pts',(1.34252251945001,-2.39159358312782,
12.5143705582413));
#442296=CARTESIAN_POINT('Ctrl Pts',(1.34245004761741,-2.39159026868938,
12.5145201959299));
#442297=CARTESIAN_POINT('Ctrl Pts',(1.34151903902849,-2.391547689793,12.5164425148273));
#442298=CARTESIAN_POINT('Ctrl Pts',(1.34079135146546,-2.39132830750116,
12.5184635205941));
#442299=CARTESIAN_POINT('Ctrl Pts',(1.34020062667919,-2.39099323287115,
12.5205025929158));
#442300=CARTESIAN_POINT('Ctrl Pts',(1.33985798288901,-2.39079887630463,
12.5216853356836));
#442301=CARTESIAN_POINT('Ctrl Pts',(1.33956180005114,-2.39056636720568,
12.5228750347131));
#442302=CARTESIAN_POINT('Ctrl Pts',(1.33930338674184,-2.39031174904033,
12.5240609649613));
#442303=CARTESIAN_POINT('Ctrl Pts',(1.33866912513756,-2.38968680241326,
12.5269717671326));
#442304=CARTESIAN_POINT('Ctrl Pts',(1.33825184439555,-2.38890367038702,
12.5299036066169));
#442305=CARTESIAN_POINT('Ctrl Pts',(1.33798261325784,-2.38801486966659,
12.5328133004019));
#442306=CARTESIAN_POINT('Ctrl Pts',(1.33785336663488,-2.38758819356747,
12.5342101228451));
#442307=CARTESIAN_POINT('Ctrl Pts',(1.33775890175191,-2.38713754593067,
12.5356023438238));
#442308=CARTESIAN_POINT('Ctrl Pts',(1.33769508908196,-2.38666986617615,
12.5369868989719));
#442309=CARTESIAN_POINT('Origin',(3.05553750638695,-15.0158462982873,-1.24020005376493));
#442310=CARTESIAN_POINT('Ctrl Pts',(1.42989013470326,-2.33255708246902,
12.5369868989719));
#442311=CARTESIAN_POINT('Ctrl Pts',(1.4421243339961,-2.34180952384133,12.5369868989719));
#442312=CARTESIAN_POINT('Ctrl Pts',(1.45503642140515,-2.33352934857591,
12.5369868989719));
#442313=CARTESIAN_POINT('Ctrl Pts',(1.43402581247992,-2.33568471670369,
12.5218025310015));
#442314=CARTESIAN_POINT('Ctrl Pts',(1.44507317275512,-2.33988134566683,
12.5216901060417));
#442315=CARTESIAN_POINT('Ctrl Pts',(1.45499706998605,-2.33355460317673,
12.5161920673678));
#442316=CARTESIAN_POINT('Ctrl Pts',(1.43387704573138,-2.34171082155254,
12.5042015548895));
#442317=CARTESIAN_POINT('Ctrl Pts',(1.44021003496673,-2.34283802710698,
12.4980677368514));
#442318=CARTESIAN_POINT('Ctrl Pts',(1.44599672539461,-2.33927362061841,
12.4907278922777));
#442319=CARTESIAN_POINT('Ctrl Pts',(1.42151428120016,-2.34654828244138,
12.506463626192));
#442320=CARTESIAN_POINT('Ctrl Pts',(1.42490428456029,-2.35214429133653,
12.4999376786891));
#442321=CARTESIAN_POINT('Ctrl Pts',(1.42486288059831,-2.35207594422447,
12.4906970594712));
#442322=CARTESIAN_POINT('Origin',(1.44316051802641,-2.31501009052007,12.5369868989719));
#442323=CARTESIAN_POINT('Origin',(1.44316051802641,-2.31501009052007,14.));
#442324=CARTESIAN_POINT('Origin',(1.44316051802641,-2.31501009052007,13.7435492065112));
#442325=CARTESIAN_POINT('Ctrl Pts',(1.41014674742212,-2.31768450722606,
13.793642941384));
#442326=CARTESIAN_POINT('Ctrl Pts',(1.41876651813523,-2.32421181692144,
13.8071662555867));
#442327=CARTESIAN_POINT('Ctrl Pts',(1.4309317412638,-2.3122943201261,13.8103758687955));
#442328=CARTESIAN_POINT('Ctrl Pts',(1.42342261813437,-2.32768515530782,
13.7804579775006));
#442329=CARTESIAN_POINT('Ctrl Pts',(1.4340647580115,-2.33573118106993,13.7901904343351));
#442330=CARTESIAN_POINT('Ctrl Pts',(1.44695570293302,-2.3266714093733,13.7927914348263));
#442331=CARTESIAN_POINT('Ctrl Pts',(1.43123862287275,-2.33357291316989,
13.7597120340895));
#442332=CARTESIAN_POINT('Ctrl Pts',(1.44355803165682,-2.34287985988636,
13.7635825532445));
#442333=CARTESIAN_POINT('Ctrl Pts',(1.45642208594866,-2.33513053583062,
13.7651073818884));
#442334=CARTESIAN_POINT('Ctrl Pts',(1.42970807017931,-2.33241995536553,
13.7381884353898));
#442335=CARTESIAN_POINT('Ctrl Pts',(1.44173857844135,-2.34150977283253,
13.7368803041982));
#442336=CARTESIAN_POINT('Ctrl Pts',(1.45456861617911,-2.33347361897843,
13.7363986145813));
#442337=CARTESIAN_POINT('Origin',(1.42660512252255,-2.30253899719264,13.7902182540695));
#442338=CARTESIAN_POINT('Ctrl Pts',(1.38479666110474,-2.29858845209351,
13.8235227101244));
#442339=CARTESIAN_POINT('Ctrl Pts',(1.3939771078202,-2.30550958541284,13.8358800583119));
#442340=CARTESIAN_POINT('Ctrl Pts',(1.4061659581551,-2.29428203106783,13.8390832900376));
#442341=CARTESIAN_POINT('Ctrl Pts',(1.39432363649803,-2.30576507310551,
13.8124254819053));
#442342=CARTESIAN_POINT('Ctrl Pts',(1.40352191167836,-2.31269964694552,
13.8247886449157));
#442343=CARTESIAN_POINT('Ctrl Pts',(1.41571461549997,-2.30144536977546,
13.8279860620657));
#442344=CARTESIAN_POINT('Ctrl Pts',(1.40384634221089,-2.31293847778947,
13.8013225099955));
#442345=CARTESIAN_POINT('Ctrl Pts',(1.41305810454048,-2.31988322174559,
13.8136962257787));
#442346=CARTESIAN_POINT('Ctrl Pts',(1.42525868962555,-2.3086056090344,13.8168830918626));
#442347=CARTESIAN_POINT('Ctrl Pts',(1.41336494437003,-2.32010879128777,
13.7902140179785));
#442348=CARTESIAN_POINT('Ctrl Pts',(1.42258613627193,-2.32706064869805,
13.802602731458));
#442349=CARTESIAN_POINT('Ctrl Pts',(1.43479835951331,-2.31576287210157,
13.8057746032558));
#442350=CARTESIAN_POINT('Origin',(1.39803682930555,-2.28101865049772,13.8235269408515));
#442351=CARTESIAN_POINT('Ctrl Pts',(1.33005753786835,-2.3306945761811,13.8235269408515));
#442352=CARTESIAN_POINT('Ctrl Pts',(1.33165381959632,-2.34239365748845,
13.8362179249168));
#442353=CARTESIAN_POINT('Ctrl Pts',(1.3153287054036,-2.34740899901737,13.8391868794938));
#442354=CARTESIAN_POINT('Ctrl Pts',(1.32859700956926,-2.31999042601557,
13.8400110824519));
#442355=CARTESIAN_POINT('Ctrl Pts',(1.32648724517256,-2.32983272031377,
13.8494522556837));
#442356=CARTESIAN_POINT('Ctrl Pts',(1.31303641355566,-2.32977779991724,
13.85569149686));
#442357=CARTESIAN_POINT('Ctrl Pts',(1.33319532685806,-2.30436182389777,
13.8586819406588));
#442358=CARTESIAN_POINT('Ctrl Pts',(1.32944672390595,-2.30657632599586,
13.868010383617));
#442359=CARTESIAN_POINT('Ctrl Pts',(1.32080977465871,-2.30387521983483,
13.8744918421245));
#442360=CARTESIAN_POINT('Ctrl Pts',(1.36015964510595,-2.28848740928262,
13.8587686893867));
#442361=CARTESIAN_POINT('Ctrl Pts',(1.36387485688658,-2.28629256775191,
13.8680909899357));
#442362=CARTESIAN_POINT('Ctrl Pts',(1.36569875138713,-2.2774511984939,13.8745789365163));
#442363=CARTESIAN_POINT('Ctrl Pts',(1.37615676386221,-2.29208006337928,
13.8400379222776));
#442364=CARTESIAN_POINT('Ctrl Pts',(1.38577616846632,-2.2950359539338,13.8494748685453));
#442365=CARTESIAN_POINT('Ctrl Pts',(1.39229259262045,-2.28327596577443,
13.8557104837033));
#442366=CARTESIAN_POINT('Ctrl Pts',(1.3847998046315,-2.29859082103775,13.8235269408542));
#442367=CARTESIAN_POINT('Ctrl Pts',(1.39423085364046,-2.30569518120467,
13.8362179249195));
#442368=CARTESIAN_POINT('Ctrl Pts',(1.40657750064357,-2.29389588835141,
13.8391868794965));
#442369=CARTESIAN_POINT('Origin',(1.30825951182031,-2.33366880892402,13.8235269408515));
#442370=CARTESIAN_POINT('Ctrl Pts',(1.33489241998041,-2.36612922842478,
13.7902140241682));
#442371=CARTESIAN_POINT('Ctrl Pts',(1.33645804584523,-2.37757070608477,
13.8026027327198));
#442372=CARTESIAN_POINT('Ctrl Pts',(1.32063625628023,-2.3827135561929,13.8057746032556));
#442373=CARTESIAN_POINT('Ctrl Pts',(1.33328131917051,-2.3543215386845,13.8013225161808));
#442374=CARTESIAN_POINT('Ctrl Pts',(1.33484534010834,-2.36575131411499,
13.8136962270464));
#442375=CARTESIAN_POINT('Ctrl Pts',(1.31904682993434,-2.37089385060931,
13.8168830918628));
#442376=CARTESIAN_POINT('Ctrl Pts',(1.33166952380057,-2.34250875854296,
13.8124254880875));
#442377=CARTESIAN_POINT('Ctrl Pts',(1.33323125293798,-2.35392179832831,
13.8247886461868));
#442378=CARTESIAN_POINT('Ctrl Pts',(1.3174569561759,-2.35906884834368,13.8279860620656));
#442379=CARTESIAN_POINT('Ctrl Pts',(1.33005700575208,-2.33069068192072,
13.8235227163065));
#442380=CARTESIAN_POINT('Ctrl Pts',(1.33161570818725,-2.34208160067013,
13.8358800595847));
#442381=CARTESIAN_POINT('Ctrl Pts',(1.31586661480737,-2.34723833301827,
13.8390832900376));
#442382=CARTESIAN_POINT('Origin',(1.31309492773411,-2.36910736775677,13.7902182540695));
#442383=CARTESIAN_POINT('Ctrl Pts',(1.33765857874362,-2.38640248748842,
13.7382347919292));
#442384=CARTESIAN_POINT('Ctrl Pts',(1.33972245318481,-2.40135100885424,
13.7369371795943));
#442385=CARTESIAN_POINT('Ctrl Pts',(1.32643138676074,-2.40862365145039,
13.7364597369712));
#442386=CARTESIAN_POINT('Ctrl Pts',(1.33791430348575,-2.38827668033879,
13.7595490285574));
#442387=CARTESIAN_POINT('Ctrl Pts',(1.34002642422511,-2.40358199812056,
13.7633824266926));
#442388=CARTESIAN_POINT('Ctrl Pts',(1.32696636829928,-2.41102031779116,
13.7648920890506));
#442389=CARTESIAN_POINT('Ctrl Pts',(1.33661012131854,-2.37871839947734,
13.7803806590111));
#442390=CARTESIAN_POINT('Ctrl Pts',(1.33844237793711,-2.39195621356006,
13.7901039518744));
#442391=CARTESIAN_POINT('Ctrl Pts',(1.32424259758171,-2.39880104221269,
13.7926933640892));
#442392=CARTESIAN_POINT('Ctrl Pts',(1.33434316150546,-2.36210397367384,
13.7936647693663));
#442393=CARTESIAN_POINT('Ctrl Pts',(1.33583501709958,-2.37281600890674,
13.8072068914933));
#442394=CARTESIAN_POINT('Ctrl Pts',(1.31947474257465,-2.37761034799738,
13.8104111085397));
#442395=CARTESIAN_POINT('Origin',(1.31589706303392,-2.38964409891906,13.7435492065112));
#442396=CARTESIAN_POINT('Origin',(1.31589706303392,-2.38964409891906,14.));
#442397=CARTESIAN_POINT('Origin',(1.31589706303392,-2.38964409891906,12.5369868989719));
#442398=CARTESIAN_POINT('Ctrl Pts',(1.35398984138342,-2.38615005398945,
12.506462012331));
#442399=CARTESIAN_POINT('Ctrl Pts',(1.35721678008233,-2.39183692084418,
12.4999388158272));
#442400=CARTESIAN_POINT('Ctrl Pts',(1.35717860116565,-2.39176963775142,
12.4907030323752));
#442401=CARTESIAN_POINT('Ctrl Pts',(1.34373179030501,-2.39457626139414,
12.5042014951932));
#442402=CARTESIAN_POINT('Ctrl Pts',(1.3416257647632,-2.400651271973,12.4980716682127));
#442403=CARTESIAN_POINT('Ctrl Pts',(1.33569497804863,-2.40396055198117,
12.4907355092744));
#442404=CARTESIAN_POINT('Ctrl Pts',(1.33839957825335,-2.39176677462936,
12.5218047446509));
#442405=CARTESIAN_POINT('Ctrl Pts',(1.33666884369345,-2.4034510986928,12.5216906929434));
#442406=CARTESIAN_POINT('Ctrl Pts',(1.32630962967192,-2.4090240188596,12.5161988840775));
#442407=CARTESIAN_POINT('Ctrl Pts',(1.33768986228266,-2.38663180728245,
12.5369868989719));
#442408=CARTESIAN_POINT('Ctrl Pts',(1.33978886682089,-2.40181731720043,
12.5369868989719));
#442409=CARTESIAN_POINT('Ctrl Pts',(1.32626989402292,-2.40904524262952,
12.5369868989719));
#442410=CARTESIAN_POINT('Origin',(2.60621061928497E-31,-9.59588718149404E-31,
12.5));
#442411=CARTESIAN_POINT('Origin',(1.51560512620467,-2.21452734525961,12.5));
#442412=CARTESIAN_POINT('',(1.51560512620467,-2.21452734525961,12.5893111709658));
#442413=CARTESIAN_POINT('',(1.51560512620467,-2.21452734525961,13.8235269408515));
#442414=CARTESIAN_POINT('',(1.51560512620467,-2.21452734525961,12.5));
#442415=CARTESIAN_POINT('',(1.5233130242113,-2.24945385392453,13.7902182540695));
#442416=CARTESIAN_POINT('',(1.51560512620467,-2.21452734525961,13.8235269408515));
#442417=CARTESIAN_POINT('',(1.5277797698805,-2.26969385076736,13.7435492065112));
#442418=CARTESIAN_POINT('Origin',(1.51308455377141,-2.20310445848677,13.7445212918701));
#442419=CARTESIAN_POINT('',(1.5277797698805,-2.26969385076736,12.5369868989719));
#442420=CARTESIAN_POINT('',(1.5277797698805,-2.26969385076736,12.5));
#442421=CARTESIAN_POINT('Ctrl Pts',(1.5277797698805,-2.26969385076736,12.5369868989719));
#442422=CARTESIAN_POINT('Ctrl Pts',(1.52372451513676,-2.25131842729605,
12.5544431401645));
#442423=CARTESIAN_POINT('Ctrl Pts',(1.51966635996705,-2.23292986123348,
12.5718848856037));
#442424=CARTESIAN_POINT('Ctrl Pts',(1.51560512620467,-2.21452734525961,
12.5893111709658));
#442425=CARTESIAN_POINT('Origin',(1.79995650094799,-2.32507696650954,12.5));
#442426=CARTESIAN_POINT('',(1.6152926497988,-2.20826874654631,13.7435492065112));
#442427=CARTESIAN_POINT('',(1.59777583112559,-2.19718856817949,13.7902182540695));
#442428=CARTESIAN_POINT('Origin',(1.55174465916705,-2.16807177447116,13.7418732680445));
#442429=CARTESIAN_POINT('',(1.56754848850677,-2.17806840977518,13.8235269408515));
#442430=CARTESIAN_POINT('',(1.59777583112559,-2.19718856817949,13.7902182540695));
#442431=CARTESIAN_POINT('',(1.56754848850677,-2.17806840977518,12.5893111709658));
#442432=CARTESIAN_POINT('',(1.56754848850677,-2.17806840977518,12.5));
#442433=CARTESIAN_POINT('',(1.6152926497988,-2.20826874654631,12.5369868989719));
#442434=CARTESIAN_POINT('Ctrl Pts',(1.56754848850677,-2.17806840977518,
12.5893111709658));
#442435=CARTESIAN_POINT('Ctrl Pts',(1.58347504906646,-2.18814267811485,
12.5718848856037));
#442436=CARTESIAN_POINT('Ctrl Pts',(1.59938953659725,-2.19820930971887,
12.5544431401645));
#442437=CARTESIAN_POINT('Ctrl Pts',(1.6152926497988,-2.20826874654631,12.5369868989719));
#442438=CARTESIAN_POINT('',(1.6152926497988,-2.20826874654631,12.5));
#442439=CARTESIAN_POINT('Origin',(1.54917241891497,-2.20711941133033,12.5));
#442440=CARTESIAN_POINT('',(1.52851837734599,-2.17964213455397,13.8587068136939));
#442441=CARTESIAN_POINT('Ctrl Pts',(1.56754848851018,-2.17806840976952,
13.8235269408542));
#442442=CARTESIAN_POINT('Ctrl Pts',(1.56606758606871,-2.17713167214031,
13.8262006681044));
#442443=CARTESIAN_POINT('Ctrl Pts',(1.56445922181571,-2.17631988863365,
13.8288634856214));
#442444=CARTESIAN_POINT('Ctrl Pts',(1.56273388295384,-2.17562482367861,
13.8314912288862));
#442445=CARTESIAN_POINT('Ctrl Pts',(1.5609552365477,-2.17490828340259,13.8342001611531));
#442446=CARTESIAN_POINT('Ctrl Pts',(1.5590504856072,-2.17431452878308,13.8368750301949));
#442447=CARTESIAN_POINT('Ctrl Pts',(1.55699766102132,-2.17386492858581,
13.8394886372969));
#442448=CARTESIAN_POINT('Ctrl Pts',(1.5568391163991,-2.173830204872,13.8396904925131));
#442449=CARTESIAN_POINT('Ctrl Pts',(1.55667968014485,-2.17379636151293,
13.8398919674349));
#442450=CARTESIAN_POINT('Ctrl Pts',(1.55651933874679,-2.17376341928281,
13.8400930404591));
#442451=CARTESIAN_POINT('Ctrl Pts',(1.55402111189254,-2.17325015717513,
13.8432258934518));
#442452=CARTESIAN_POINT('Ctrl Pts',(1.55131612875077,-2.17295716726792,
13.8462331177034));
#442453=CARTESIAN_POINT('Ctrl Pts',(1.54848222334066,-2.17298991066604,
13.8489036603661));
#442454=CARTESIAN_POINT('Ctrl Pts',(1.54755493651065,-2.17300062468696,
13.8497774930041));
#442455=CARTESIAN_POINT('Ctrl Pts',(1.54661405697649,-2.17304634862749,
13.85061494757));
#442456=CARTESIAN_POINT('Ctrl Pts',(1.54566291962783,-2.17313115116021,
13.8514076489583));
#442457=CARTESIAN_POINT('Ctrl Pts',(1.54365112696084,-2.17331052074727,
13.8530843267192));
#442458=CARTESIAN_POINT('Ctrl Pts',(1.54139609421675,-2.17368528658119,
13.8546805203176));
#442459=CARTESIAN_POINT('Ctrl Pts',(1.53905107190559,-2.17436829697483,
13.8559412814274));
#442460=CARTESIAN_POINT('Ctrl Pts',(1.5387372318695,-2.17445970591605,13.8561100121513));
#442461=CARTESIAN_POINT('Ctrl Pts',(1.53842181144662,-2.17455656576237,
13.8562727473908));
#442462=CARTESIAN_POINT('Ctrl Pts',(1.53810520011653,-2.17465907447112,
13.8564289040185));
#442463=CARTESIAN_POINT('Ctrl Pts',(1.53666937134654,-2.17512395029587,
13.8571370725437));
#442464=CARTESIAN_POINT('Ctrl Pts',(1.53518451357584,-2.17571533827384,
13.8577210840553));
#442465=CARTESIAN_POINT('Ctrl Pts',(1.5337192026214,-2.17643751617089,13.8581177131616));
#442466=CARTESIAN_POINT('Ctrl Pts',(1.53330652062216,-2.17664090632331,
13.8582294175695));
#442467=CARTESIAN_POINT('Ctrl Pts',(1.5328953432531,-2.17685449885373,13.8583265086086));
#442468=CARTESIAN_POINT('Ctrl Pts',(1.53248706394703,-2.1770779721128,13.8584082369006));
#442469=CARTESIAN_POINT('Ctrl Pts',(1.53190047606862,-2.17739904325937,
13.8585256585398));
#442470=CARTESIAN_POINT('Ctrl Pts',(1.53131273294775,-2.17774478549668,
13.8586122832068));
#442471=CARTESIAN_POINT('Ctrl Pts',(1.53073950284391,-2.17810689809613,
13.8586682984299));
#442472=CARTESIAN_POINT('Ctrl Pts',(1.53028097558332,-2.17839655228062,
13.8587131050557));
#442473=CARTESIAN_POINT('Ctrl Pts',(1.52982654468516,-2.17869968189244,
13.8587357943552));
#442474=CARTESIAN_POINT('Ctrl Pts',(1.52937643718902,-2.17901674426501,
13.8587355499465));
#442475=CARTESIAN_POINT('Ctrl Pts',(1.52908552198329,-2.17922166923547,
13.8587353919793));
#442476=CARTESIAN_POINT('Ctrl Pts',(1.52879953645905,-2.17943016675381,
13.8587257282814));
#442477=CARTESIAN_POINT('Ctrl Pts',(1.52851837734599,-2.17964213455397,
13.8587068136939));
#442478=CARTESIAN_POINT('Ctrl Pts',(1.52851837734599,-2.17964213455397,
13.8587068136939));
#442479=CARTESIAN_POINT('Ctrl Pts',(1.52759366035041,-2.18033928509337,
13.8586446046466));
#442480=CARTESIAN_POINT('Ctrl Pts',(1.52672108644886,-2.18107392841697,
13.858482427929));
#442481=CARTESIAN_POINT('Ctrl Pts',(1.52589754886275,-2.18184284988884,
13.8582284286032));
#442482=CARTESIAN_POINT('Ctrl Pts',(1.5250526950973,-2.1826316738743,13.8579678548414));
#442483=CARTESIAN_POINT('Ctrl Pts',(1.52425843051278,-2.18345961987124,
13.857615680862));
#442484=CARTESIAN_POINT('Ctrl Pts',(1.52353907601848,-2.18428733879638,
13.8571944833187));
#442485=CARTESIAN_POINT('Ctrl Pts',(1.5217438533084,-2.18635299602621,13.8561433417727));
#442486=CARTESIAN_POINT('Ctrl Pts',(1.52032757852607,-2.18851071837825,
13.8546163505475));
#442487=CARTESIAN_POINT('Ctrl Pts',(1.51923450966278,-2.19056138102956,
13.8528973491086));
#442488=CARTESIAN_POINT('Ctrl Pts',(1.51903482210818,-2.19093600684125,
13.8525833129073));
#442489=CARTESIAN_POINT('Ctrl Pts',(1.5188457798754,-2.1913070583044,13.8522628768812));
#442490=CARTESIAN_POINT('Ctrl Pts',(1.51866686623345,-2.19167334761887,
13.851937733538));
#442491=CARTESIAN_POINT('Ctrl Pts',(1.51757426544519,-2.19391022564192,
13.8499521282529));
#442492=CARTESIAN_POINT('Ctrl Pts',(1.51675447834592,-2.19619359876534,
13.847639871647));
#442493=CARTESIAN_POINT('Ctrl Pts',(1.51617497488795,-2.19837631368465,
13.8452109780794));
#442494=CARTESIAN_POINT('Ctrl Pts',(1.51591424428709,-2.19935836230681,
13.8441181685877));
#442495=CARTESIAN_POINT('Ctrl Pts',(1.51570143934861,-2.20032010192919,
13.8430021611332));
#442496=CARTESIAN_POINT('Ctrl Pts',(1.51553056054347,-2.20124944394279,
13.8418824960098));
#442497=CARTESIAN_POINT('Ctrl Pts',(1.51512788027559,-2.20343946212943,
13.8392439765549));
#442498=CARTESIAN_POINT('Ctrl Pts',(1.51493505499432,-2.20555357768276,
13.8364981347964));
#442499=CARTESIAN_POINT('Ctrl Pts',(1.51491749568044,-2.20759427332479,
13.8336931113419));
#442500=CARTESIAN_POINT('Ctrl Pts',(1.51490039402384,-2.20958178128397,
13.8309611966328));
#442501=CARTESIAN_POINT('Ctrl Pts',(1.51505008856863,-2.21150164312281,
13.8281701127186));
#442502=CARTESIAN_POINT('Ctrl Pts',(1.51537135352457,-2.21334217022334,
13.8253580685121));
#442503=CARTESIAN_POINT('Ctrl Pts',(1.51544100411374,-2.2137411984851,13.8247484142933));
#442504=CARTESIAN_POINT('Ctrl Pts',(1.51551884400471,-2.21413637796842,
13.8241378483365));
#442505=CARTESIAN_POINT('Ctrl Pts',(1.51560512620467,-2.21452734525961,
13.8235269408515));
#442506=CARTESIAN_POINT('',(1.52952454255909,-2.17891384311432,12.5969504640361));
#442507=CARTESIAN_POINT('Origin',(1.54919126636332,-2.2071466042798,12.584524458991));
#442508=CARTESIAN_POINT('Origin',(1.54919126636332,-2.2071466042798,12.584524458991));
#442509=CARTESIAN_POINT('Ctrl Pts',(1.56754848850677,-2.17806840977518,
12.5893111709658));
#442510=CARTESIAN_POINT('Ctrl Pts',(1.55796993226768,-2.17200954066169,
12.5770542771492));
#442511=CARTESIAN_POINT('Ctrl Pts',(1.54679665878455,-2.18396619715613,
12.5737548217797));
#442512=CARTESIAN_POINT('Ctrl Pts',(1.58849357634264,-2.19131712310947,
12.5663937883685));
#442513=CARTESIAN_POINT('Ctrl Pts',(1.57890280132482,-2.18525052506698,
12.5540940315304));
#442514=CARTESIAN_POINT('Ctrl Pts',(1.56769725034417,-2.19724642530556,
12.5508374392248));
#442515=CARTESIAN_POINT('Ctrl Pts',(1.60941753084162,-2.2045524686544,12.5434499600945));
#442516=CARTESIAN_POINT('Ctrl Pts',(1.5997955727989,-2.1984661459413,12.5311293540533));
#442517=CARTESIAN_POINT('Ctrl Pts',(1.58857805433939,-2.21051268254624,
12.5278936106989));
#442518=CARTESIAN_POINT('Ctrl Pts',(1.63032200740699,-2.21777549352727,
12.5204817579905));
#442519=CARTESIAN_POINT('Ctrl Pts',(1.62065242724761,-2.21165904767617,
12.5081597038247));
#442520=CARTESIAN_POINT('Ctrl Pts',(1.60944061616698,-2.22376604305847,
12.5049254088044));
#442521=CARTESIAN_POINT('Ctrl Pts',(1.6152926497988,-2.20826874654631,12.5369868989719));
#442522=CARTESIAN_POINT('Ctrl Pts',(1.61607988308113,-2.20876670731779,
12.5342545179733));
#442523=CARTESIAN_POINT('Ctrl Pts',(1.61676449626765,-2.20934736375511,
12.5314872231885));
#442524=CARTESIAN_POINT('Ctrl Pts',(1.61727176563758,-2.21002063851066,
12.5287124745063));
#442525=CARTESIAN_POINT('Ctrl Pts',(1.61772924633399,-2.21062783110359,
12.5262100684184));
#442526=CARTESIAN_POINT('Ctrl Pts',(1.6180412402908,-2.21131033246523,12.5237004536639));
#442527=CARTESIAN_POINT('Ctrl Pts',(1.61815281477188,-2.21210742198755,
12.5212220730815));
#442528=CARTESIAN_POINT('Ctrl Pts',(1.61823823468911,-2.21271766297064,
12.5193246583486));
#442529=CARTESIAN_POINT('Ctrl Pts',(1.61820657663425,-2.21340244789356,
12.517417831369));
#442530=CARTESIAN_POINT('Ctrl Pts',(1.61796173605729,-2.21417653948722,
12.5155812248347));
#442531=CARTESIAN_POINT('Ctrl Pts',(1.61785743265549,-2.21450630666688,
12.5147988205793));
#442532=CARTESIAN_POINT('Ctrl Pts',(1.61771459901015,-2.21485269957456,
12.5140295443047));
#442533=CARTESIAN_POINT('Ctrl Pts',(1.61752711876154,-2.21521853274585,
12.5132817086137));
#442534=CARTESIAN_POINT('Ctrl Pts',(1.61724339276703,-2.21577217176181,
12.5121499604604));
#442535=CARTESIAN_POINT('Ctrl Pts',(1.61684492242763,-2.21637902800959,
12.5110494206568));
#442536=CARTESIAN_POINT('Ctrl Pts',(1.6162956560146,-2.21702976491589,12.5100666561695));
#442537=CARTESIAN_POINT('Ctrl Pts',(1.61598026850509,-2.21740341654897,
12.5095023550641));
#442538=CARTESIAN_POINT('Ctrl Pts',(1.61561102025558,-2.21779543193857,
12.5089719619137));
#442539=CARTESIAN_POINT('Ctrl Pts',(1.61519018315096,-2.2181940839401,12.5085043804652));
#442540=CARTESIAN_POINT('Ctrl Pts',(1.61457434286623,-2.21877745921626,
12.5078201359221));
#442541=CARTESIAN_POINT('Ctrl Pts',(1.61382933553101,-2.21939108946418,
12.5072563000953));
#442542=CARTESIAN_POINT('Ctrl Pts',(1.61300027925851,-2.21998684485305,
12.5068768744336));
#442543=CARTESIAN_POINT('Ctrl Pts',(1.6124024726136,-2.22041642550037,12.5066032824118));
#442544=CARTESIAN_POINT('Ctrl Pts',(1.61175049802467,-2.2208443081451,12.5064197834844));
#442545=CARTESIAN_POINT('Ctrl Pts',(1.61108218170166,-2.22124875973636,
12.5063282718343));
#442546=CARTESIAN_POINT('Ctrl Pts',(1.61010664677556,-2.22183913384456,
12.5061946931565));
#442547=CARTESIAN_POINT('Ctrl Pts',(1.60907599162941,-2.22239311078423,
12.5062515701262));
#442548=CARTESIAN_POINT('Ctrl Pts',(1.60806150210968,-2.22288993130823,
12.5064436508398));
#442549=CARTESIAN_POINT('',(1.54679665878455,-2.18396619715613,12.5737548217797));
#442550=CARTESIAN_POINT('Origin',(1.55578780396802,-2.19666105077048,12.5893111709658));
#442551=CARTESIAN_POINT('Ctrl Pts',(1.60806150210968,-2.22288993130823,
12.5064436508398));
#442552=CARTESIAN_POINT('Ctrl Pts',(1.59899245595975,-2.21712861291036,
12.5164271754438));
#442553=CARTESIAN_POINT('Ctrl Pts',(1.58991992687748,-2.21136483436914,
12.5264061185523));
#442554=CARTESIAN_POINT('Ctrl Pts',(1.58084379168938,-2.2055985098393,12.536380305637));
#442555=CARTESIAN_POINT('Ctrl Pts',(1.56950046354282,-2.19839177371363,
12.5488460165097));
#442556=CARTESIAN_POINT('Ctrl Pts',(1.55815149934638,-2.19118105862217,
12.5613043021964));
#442557=CARTESIAN_POINT('Ctrl Pts',(1.54679665878455,-2.18396619715613,
12.5737548217797));
#442558=CARTESIAN_POINT('Ctrl Pts',(1.51560512620467,-2.21452734525961,
12.5893111709658));
#442559=CARTESIAN_POINT('Ctrl Pts',(1.51316261792755,-2.20345969926437,
12.5770542771492));
#442560=CARTESIAN_POINT('Ctrl Pts',(1.52820511637882,-2.19701556121508,
12.5737548217797));
#442561=CARTESIAN_POINT('Ctrl Pts',(1.51332628722593,-2.20420132780736,
12.5928319619712));
#442562=CARTESIAN_POINT('Ctrl Pts',(1.51486596642762,-2.19606113098374,
12.5821634970843));
#442563=CARTESIAN_POINT('Ctrl Pts',(1.52736577342746,-2.19325607710428,
12.5773203894503));
#442564=CARTESIAN_POINT('Ctrl Pts',(1.51686794509426,-2.1878293774384,12.5969440695591));
#442565=CARTESIAN_POINT('Ctrl Pts',(1.52014759929905,-2.18550506875648,
12.5878292599214));
#442566=CARTESIAN_POINT('Ctrl Pts',(1.52863009228486,-2.18742121250222,
12.5813877129824));
#442567=CARTESIAN_POINT('Ctrl Pts',(1.54188060042453,-2.17020716648546,
12.596957478804));
#442568=CARTESIAN_POINT('Ctrl Pts',(1.538625230093,-2.1725143633027,12.5878468778671));
#442569=CARTESIAN_POINT('Ctrl Pts',(1.53758590394018,-2.18111885533219,
12.5814011370086));
#442570=CARTESIAN_POINT('Ctrl Pts',(1.55859880275859,-2.17240732962884,
12.5928371701607));
#442571=CARTESIAN_POINT('Ctrl Pts',(1.55042480839402,-2.17109550577187,
12.5821692192952));
#442572=CARTESIAN_POINT('Ctrl Pts',(1.54353601874319,-2.18189219040719,
12.5773318885715));
#442573=CARTESIAN_POINT('Ctrl Pts',(1.56754848850679,-2.17806840977513,
12.5893111709658));
#442574=CARTESIAN_POINT('Ctrl Pts',(1.55796993226771,-2.17200954066164,
12.5770542771492));
#442575=CARTESIAN_POINT('Ctrl Pts',(1.54679665878457,-2.18396619715608,
12.5737548217797));
#442576=CARTESIAN_POINT('',(1.52820511637882,-2.19701556121508,12.5737548217797));
#442577=CARTESIAN_POINT('Origin',(1.53708819353926,-2.20978626754487,12.5893111709658));
#442578=CARTESIAN_POINT('Ctrl Pts',(1.54679665878457,-2.18396619715608,
12.5737548217797));
#442579=CARTESIAN_POINT('Ctrl Pts',(1.545967639159,-2.18340312869539,12.5746934679442));
#442580=CARTESIAN_POINT('Ctrl Pts',(1.54494735050147,-2.18293159238338,
12.5756680099006));
#442581=CARTESIAN_POINT('Ctrl Pts',(1.54385326969933,-2.18260221286617,
12.5765688348656));
#442582=CARTESIAN_POINT('Ctrl Pts',(1.54356362391883,-2.18251501328534,
12.5768073183026));
#442583=CARTESIAN_POINT('Ctrl Pts',(1.54326893808177,-2.18243755628029,
12.5770407398754));
#442584=CARTESIAN_POINT('Ctrl Pts',(1.54297154987649,-2.18237024061894,
12.5772674179684));
#442585=CARTESIAN_POINT('Ctrl Pts',(1.54175114909918,-2.18209399534766,
12.5781976435658));
#442586=CARTESIAN_POINT('Ctrl Pts',(1.54041343275203,-2.18198384791316,
12.5790594849312));
#442587=CARTESIAN_POINT('Ctrl Pts',(1.53904476283533,-2.18209536196077,
12.5797571720116));
#442588=CARTESIAN_POINT('Ctrl Pts',(1.53815302517162,-2.18216801737248,
12.580211740231));
#442589=CARTESIAN_POINT('Ctrl Pts',(1.53720914730193,-2.18235678057714,
12.5806009430798));
#442590=CARTESIAN_POINT('Ctrl Pts',(1.53628304843442,-2.18266573615955,
12.5808812374708));
#442591=CARTESIAN_POINT('Ctrl Pts',(1.53548722227712,-2.18293123149979,
12.5811221033394));
#442592=CARTESIAN_POINT('Ctrl Pts',(1.53468826847797,-2.18329102669088,
12.581287365893));
#442593=CARTESIAN_POINT('Ctrl Pts',(1.53393470499476,-2.18373241694931,
12.581359338449));
#442594=CARTESIAN_POINT('Ctrl Pts',(1.53382997523109,-2.18379376108087,
12.5813693411482));
#442595=CARTESIAN_POINT('Ctrl Pts',(1.53372607644035,-2.18385664261584,
12.5813775999465));
#442596=CARTESIAN_POINT('Ctrl Pts',(1.53362309129939,-2.1839209887146,12.5813841266931));
#442597=CARTESIAN_POINT('Ctrl Pts',(1.53344836455195,-2.18403015965366,
12.5813952001081));
#442598=CARTESIAN_POINT('Ctrl Pts',(1.53327542016041,-2.18414479391356,
12.5814007534795));
#442599=CARTESIAN_POINT('Ctrl Pts',(1.53310444240399,-2.18426500594565,
12.5814005856065));
#442600=CARTESIAN_POINT('Ctrl Pts',(1.5323217730831,-2.18481528962869,12.5813998171494));
#442601=CARTESIAN_POINT('Ctrl Pts',(1.53163419595105,-2.18544415629832,
12.58127954464));
#442602=CARTESIAN_POINT('Ctrl Pts',(1.53102564474814,-2.18612620141454,
12.5810700125799));
#442603=CARTESIAN_POINT('Ctrl Pts',(1.53029058418412,-2.18695003425788,
12.5808169217085));
#442604=CARTESIAN_POINT('Ctrl Pts',(1.52968324294109,-2.18786267053481,
12.5804173076348));
#442605=CARTESIAN_POINT('Ctrl Pts',(1.52923516695681,-2.18876970045712,
12.5799304713245));
#442606=CARTESIAN_POINT('Ctrl Pts',(1.52867985965379,-2.18989379627475,
12.5793271277669));
#442607=CARTESIAN_POINT('Ctrl Pts',(1.52830585165326,-2.19106474923022,
12.5785808224116));
#442608=CARTESIAN_POINT('Ctrl Pts',(1.52809869499393,-2.19222355118979,
12.5777485681082));
#442609=CARTESIAN_POINT('Ctrl Pts',(1.52779000887583,-2.19395029306578,
12.576508418016));
#442610=CARTESIAN_POINT('Ctrl Pts',(1.52784763807624,-2.19563430565066,
12.5750928681475));
#442611=CARTESIAN_POINT('Ctrl Pts',(1.52820511637882,-2.19701556121508,
12.5737548217797));
#442612=CARTESIAN_POINT('Ctrl Pts',(1.52820511637882,-2.19701556121508,
12.5737548217797));
#442613=CARTESIAN_POINT('Ctrl Pts',(1.51316261792755,-2.20345969926437,
12.5770542771492));
#442614=CARTESIAN_POINT('Ctrl Pts',(1.51560512620467,-2.21452734525961,
12.5893111709658));
#442615=CARTESIAN_POINT('Ctrl Pts',(1.53359001553651,-2.22118202175923,
12.5508408821982));
#442616=CARTESIAN_POINT('Ctrl Pts',(1.51849964539203,-2.22764317131114,
12.55409748406));
#442617=CARTESIAN_POINT('Ctrl Pts',(1.52094526968415,-2.23872493678811,
12.5663972313419));
#442618=CARTESIAN_POINT('Ctrl Pts',(1.538968503048,-2.24532513124994,12.52790050457));
#442619=CARTESIAN_POINT('Ctrl Pts',(1.52382645117862,-2.25178032625288,
12.5311362602938));
#442620=CARTESIAN_POINT('Ctrl Pts',(1.52628002583636,-2.26289811692294,
12.5434568539655));
#442621=CARTESIAN_POINT('Ctrl Pts',(1.54434106366399,-2.26944670737555,
12.5049357605811));
#442622=CARTESIAN_POINT('Ctrl Pts',(1.52914410084493,-2.27587599241087,
12.5081700652078));
#442623=CARTESIAN_POINT('Ctrl Pts',(1.53160981659786,-2.28704879756943,
12.5204921097672));
#442624=CARTESIAN_POINT('Ctrl Pts',(1.54398827872498,-2.26786279047851,
12.5064436508395));
#442625=CARTESIAN_POINT('Ctrl Pts',(1.54311111065669,-2.26871097911941,
12.5062361689309));
#442626=CARTESIAN_POINT('Ctrl Pts',(1.54216275899901,-2.26955562150162,
12.5061871075061));
#442627=CARTESIAN_POINT('Ctrl Pts',(1.5412003190334,-2.270320295258,12.5063648335164));
#442628=CARTESIAN_POINT('Ctrl Pts',(1.54076311943526,-2.27066765724518,
12.5064455676329));
#442629=CARTESIAN_POINT('Ctrl Pts',(1.5403167775862,-2.27100318989256,12.506574497099));
#442630=CARTESIAN_POINT('Ctrl Pts',(1.53987979978177,-2.271311666509,12.5067492519495));
#442631=CARTESIAN_POINT('Ctrl Pts',(1.53900167592157,-2.27193156224391,
12.5071004286051));
#442632=CARTESIAN_POINT('Ctrl Pts',(1.53812861480944,-2.27246433017317,
12.5076537929612));
#442633=CARTESIAN_POINT('Ctrl Pts',(1.53733107118647,-2.27287805715525,
12.5083435010503));
#442634=CARTESIAN_POINT('Ctrl Pts',(1.53728086104917,-2.27290410374127,
12.5083869222963));
#442635=CARTESIAN_POINT('Ctrl Pts',(1.53723093925072,-2.27292967076007,
12.5084308732336));
#442636=CARTESIAN_POINT('Ctrl Pts',(1.53718131867551,-2.2729547474142,12.5084753333615));
#442637=CARTESIAN_POINT('Ctrl Pts',(1.53678329616976,-2.27315589527817,
12.508831962269));
#442638=CARTESIAN_POINT('Ctrl Pts',(1.53639715621091,-2.27333072734357,
12.509227847131));
#442639=CARTESIAN_POINT('Ctrl Pts',(1.53603553566535,-2.27347659572089,
12.5096423454524));
#442640=CARTESIAN_POINT('Ctrl Pts',(1.53490237692214,-2.27393368265681,
12.5109411997424));
#442641=CARTESIAN_POINT('Ctrl Pts',(1.53394389914738,-2.27414345025429,
12.5124831113042));
#442642=CARTESIAN_POINT('Ctrl Pts',(1.53314148551678,-2.27419868467208,
12.5140723025007));
#442643=CARTESIAN_POINT('Ctrl Pts',(1.53306629848073,-2.27420386019752,
12.5142212114565));
#442644=CARTESIAN_POINT('Ctrl Pts',(1.53299246601335,-2.27420770406637,
12.5143705582413));
#442645=CARTESIAN_POINT('Ctrl Pts',(1.5329199651673,-2.27421030778361,12.5145201959299));
#442646=CARTESIAN_POINT('Ctrl Pts',(1.53198858385732,-2.27424375640805,
12.5164425148273));
#442647=CARTESIAN_POINT('Ctrl Pts',(1.53124543592119,-2.2740844173846,12.5184635205941));
#442648=CARTESIAN_POINT('Ctrl Pts',(1.53062936502989,-2.27379860724189,
12.5205025929157));
#442649=CARTESIAN_POINT('Ctrl Pts',(1.53027201949417,-2.27363282603066,
12.5216853356836));
#442650=CARTESIAN_POINT('Ctrl Pts',(1.52995787053018,-2.27342523223747,
12.5228750347131));
#442651=CARTESIAN_POINT('Ctrl Pts',(1.52967956332561,-2.27319252437676,
12.5240609649613));
#442652=CARTESIAN_POINT('Ctrl Pts',(1.52899647322267,-2.27262135541698,
12.5269717671326));
#442653=CARTESIAN_POINT('Ctrl Pts',(1.52851674841753,-2.27187484145228,
12.5299036066169));
#442654=CARTESIAN_POINT('Ctrl Pts',(1.52817596761428,-2.27101094298007,
12.5328133004019));
#442655=CARTESIAN_POINT('Ctrl Pts',(1.52801237298565,-2.2705962214101,12.5342101228451));
#442656=CARTESIAN_POINT('Ctrl Pts',(1.52788149046078,-2.27015477303107,
12.5356023438238));
#442657=CARTESIAN_POINT('Ctrl Pts',(1.5277797698805,-2.26969385076736,12.5369868989719));
#442658=CARTESIAN_POINT('Origin',(4.26941344976037,-14.7173397586424,-1.24076534767543));
#442659=CARTESIAN_POINT('Ctrl Pts',(1.61525734986217,-2.20824637076874,
12.5369868989719));
#442660=CARTESIAN_POINT('Ctrl Pts',(1.62820500073349,-2.21647082458671,
12.5369868989719));
#442661=CARTESIAN_POINT('Ctrl Pts',(1.64039921308345,-2.20716574592753,
12.5369868989719));
#442662=CARTESIAN_POINT('Ctrl Pts',(1.61963419773785,-2.21102650192599,
12.5218025310016));
#442663=CARTESIAN_POINT('Ctrl Pts',(1.63098686305326,-2.21430870453147,
12.5216901060418));
#442664=CARTESIAN_POINT('Ctrl Pts',(1.64036205108736,-2.20719412400173,
12.5161920673678));
#442665=CARTESIAN_POINT('Ctrl Pts',(1.61997710948733,-2.21704468127927,
12.5042015548895));
#442666=CARTESIAN_POINT('Ctrl Pts',(1.62638090394062,-2.21765193873491,
12.4980677368514));
#442667=CARTESIAN_POINT('Ctrl Pts',(1.63185780741435,-2.21362772352397,
12.4907278922777));
#442668=CARTESIAN_POINT('Ctrl Pts',(1.60804977900648,-2.22287372599554,
12.5064636261921));
#442669=CARTESIAN_POINT('Ctrl Pts',(1.6118846290859,-2.22817479788771,12.4999376786892));
#442670=CARTESIAN_POINT('Ctrl Pts',(1.61183779196805,-2.2281100530023,12.4906970594712));
#442671=CARTESIAN_POINT('Origin',(1.62705333433755,-2.18967610555101,12.5369868989719));
#442672=CARTESIAN_POINT('Origin',(1.62705333433755,-2.18967610555102,14.));
#442673=CARTESIAN_POINT('Origin',(1.62705333433755,-2.18967610555102,13.7435492065112));
#442674=CARTESIAN_POINT('Ctrl Pts',(1.59436740412112,-2.19503255214519,
13.793642941384));
#442675=CARTESIAN_POINT('Ctrl Pts',(1.60349052959503,-2.20083555142084,
13.8071662555867));
#442676=CARTESIAN_POINT('Ctrl Pts',(1.61464388732173,-2.18796613049156,
13.8103758687955));
#442677=CARTESIAN_POINT('Ctrl Pts',(1.6084142461289,-2.20391781718522,13.7804579775006));
#442678=CARTESIAN_POINT('Ctrl Pts',(1.61967680095876,-2.21106963726357,
13.7901904343351));
#442679=CARTESIAN_POINT('Ctrl Pts',(1.6317863968244,-2.20098927952511,13.7927914348262));
#442680=CARTESIAN_POINT('Ctrl Pts',(1.61668415068134,-2.20914890707229,
13.7597120340895));
#442681=CARTESIAN_POINT('Ctrl Pts',(1.62972117020784,-2.21742073950764,
13.7635825532445));
#442682=CARTESIAN_POINT('Ctrl Pts',(1.64191077856844,-2.20864866083957,
13.7651073818884));
#442683=CARTESIAN_POINT('Ctrl Pts',(1.61506471401112,-2.20812453989338,
13.7381884353898));
#442684=CARTESIAN_POINT('Ctrl Pts',(1.62779609625867,-2.21620351363346,
13.7368803041982));
#442685=CARTESIAN_POINT('Ctrl Pts',(1.63992842196115,-2.2071483322345,13.7363986145813));
#442686=CARTESIAN_POINT('Origin',(1.60953651566434,-2.1785959271842,13.7902182540695));
#442687=CARTESIAN_POINT('Ctrl Pts',(1.56754516235229,-2.17806630493435,
13.8235227101244));
#442688=CARTESIAN_POINT('Ctrl Pts',(1.57725919850684,-2.1842161171191,13.8358800583119));
#442689=CARTESIAN_POINT('Ctrl Pts',(1.5884923415371,-2.17203241707691,13.8390832900376));
#442690=CARTESIAN_POINT('Ctrl Pts',(1.57762539875787,-2.1844425093933,13.8124254819052));
#442691=CARTESIAN_POINT('Ctrl Pts',(1.58735829958171,-2.19060426419111,
13.8247886449158));
#442692=CARTESIAN_POINT('Ctrl Pts',(1.59859310511821,-2.17839361614691,
13.8279860620657));
#442693=CARTESIAN_POINT('Ctrl Pts',(1.58770111752941,-2.19081585624484,
13.8013225099955));
#442694=CARTESIAN_POINT('Ctrl Pts',(1.59744828958404,-2.19698664799067,
13.8136962257787));
#442695=CARTESIAN_POINT('Ctrl Pts',(1.60868904809652,-2.1847520996563,13.8168830918626));
#442696=CARTESIAN_POINT('Ctrl Pts',(1.59777249444115,-2.19718645667412,
13.7902140179785));
#442697=CARTESIAN_POINT('Ctrl Pts',(1.60752964450452,-2.20336356960699,
13.802602731458));
#442698=CARTESIAN_POINT('Ctrl Pts',(1.61878035890445,-2.19110797586321,
13.8057746032558));
#442699=CARTESIAN_POINT('Origin',(1.57930917304552,-2.15947576877988,13.8235269408515));
#442700=CARTESIAN_POINT('Ctrl Pts',(1.51560512620467,-2.21452734525961,
13.8235269408515));
#442701=CARTESIAN_POINT('Ctrl Pts',(1.51814968017239,-2.22605738705903,
13.8362179249168));
#442702=CARTESIAN_POINT('Ctrl Pts',(1.50228768334518,-2.23238668881442,
13.8391868794938));
#442703=CARTESIAN_POINT('Ctrl Pts',(1.51327697008203,-2.20397785888597,
13.8400110824519));
#442704=CARTESIAN_POINT('Ctrl Pts',(1.51197646410904,-2.21395936914624,
13.8494522556837));
#442705=CARTESIAN_POINT('Ctrl Pts',(1.49856591250255,-2.21500099914103,
13.85569149686));
#442706=CARTESIAN_POINT('Ctrl Pts',(1.51658611068793,-2.18802645410473,
13.8586819406588));
#442707=CARTESIAN_POINT('Ctrl Pts',(1.51303048338233,-2.1905391335707,13.868010383617));
#442708=CARTESIAN_POINT('Ctrl Pts',(1.50420210764325,-2.18855100666276,
13.8744918421245));
#442709=CARTESIAN_POINT('Ctrl Pts',(1.54216679522923,-2.17000701803294,
13.8587686893867));
#442710=CARTESIAN_POINT('Ctrl Pts',(1.54569074498848,-2.1675166554059,13.8680909899357));
#442711=CARTESIAN_POINT('Ctrl Pts',(1.54678791695674,-2.15855604074073,
13.8745789365163));
#442712=CARTESIAN_POINT('Ctrl Pts',(1.55840351955395,-2.17228380418083,
13.8400379222776));
#442713=CARTESIAN_POINT('Ctrl Pts',(1.56823184890414,-2.17444578847591,
13.8494748685453));
#442714=CARTESIAN_POINT('Ctrl Pts',(1.57376804198508,-2.16219378164295,
13.8557104837033));
#442715=CARTESIAN_POINT('Ctrl Pts',(1.56754848851018,-2.17806840976952,
13.8235269408542));
#442716=CARTESIAN_POINT('Ctrl Pts',(1.57752722778883,-2.18438041271623,
13.8362179249195));
#442717=CARTESIAN_POINT('Ctrl Pts',(1.58887104043573,-2.17161401468514,
13.8391868794965));
#442718=CARTESIAN_POINT('Origin',(1.49412205887007,-2.21926842297435,13.8235269408515));
#442719=CARTESIAN_POINT('Ctrl Pts',(1.52331217376247,-2.24945000384412,
13.7902140241683));
#442720=CARTESIAN_POINT('Ctrl Pts',(1.52580517678315,-2.2607257978885,13.8026027327198));
#442721=CARTESIAN_POINT('Ctrl Pts',(1.51045522294544,-2.26714115831902,
13.8057746032556));
#442722=CARTESIAN_POINT('Ctrl Pts',(1.52074399742653,-2.23781292289012,
13.8013225161808));
#442723=CARTESIAN_POINT('Ctrl Pts',(1.52323444702014,-2.24907718445967,
13.8136962270464));
#442724=CARTESIAN_POINT('Ctrl Pts',(1.50790766955073,-2.25549033483342,
13.8168830918628));
#442725=CARTESIAN_POINT('Ctrl Pts',(1.51817471392669,-2.22617082508583,
13.8124254880875));
#442726=CARTESIAN_POINT('Ctrl Pts',(1.5206615152352,-2.23741859349969,13.8247886461867));
#442727=CARTESIAN_POINT('Ctrl Pts',(1.50535923850348,-2.24383426875828,
13.8279860620656));
#442728=CARTESIAN_POINT('Ctrl Pts',(1.5156042784406,-2.21452350732949,13.8235227163065));
#442729=CARTESIAN_POINT('Ctrl Pts',(1.51808626004819,-2.22574947501768,
13.8358800595847));
#442730=CARTESIAN_POINT('Ctrl Pts',(1.50280989203648,-2.23217274608223,
13.8390832900376));
#442731=CARTESIAN_POINT('Origin',(1.50182995687671,-2.25419493163927,13.7902182540695));
#442732=CARTESIAN_POINT('Ctrl Pts',(1.52772158718203,-2.26943033769167,
13.7382347919292));
#442733=CARTESIAN_POINT('Ctrl Pts',(1.53099703751788,-2.28416089415877,
13.7369371795943));
#442734=CARTESIAN_POINT('Ctrl Pts',(1.51834298390841,-2.29249268293844,
13.7364597369712));
#442735=CARTESIAN_POINT('Ctrl Pts',(1.52812922513764,-2.27127745037945,
13.7595490285574));
#442736=CARTESIAN_POINT('Ctrl Pts',(1.53148184345635,-2.2863596835307,13.7633824266925));
#442737=CARTESIAN_POINT('Ctrl Pts',(1.51907153589636,-2.29483776860776,
13.7648920890506));
#442738=CARTESIAN_POINT('Ctrl Pts',(1.52605029390404,-2.2618572768631,13.7803806590111));
#442739=CARTESIAN_POINT('Ctrl Pts',(1.52895545858147,-2.27490169728723,
13.7901039518745));
#442740=CARTESIAN_POINT('Ctrl Pts',(1.51536084390328,-2.28288116426049,
13.7926933640892));
#442741=CARTESIAN_POINT('Ctrl Pts',(1.52243664726894,-2.24548291246107,
13.7936647693663));
#442742=CARTESIAN_POINT('Ctrl Pts',(1.5247966691538,-2.25603770419978,13.8072068914932));
#442743=CARTESIAN_POINT('Ctrl Pts',(1.50888161523708,-2.26214960477777,
13.8104111085397));
#442744=CARTESIAN_POINT('Origin',(1.5062967025459,-2.27443492848209,13.7435492065112));
#442745=CARTESIAN_POINT('Origin',(1.5062967025459,-2.27443492848209,14.));
#442746=CARTESIAN_POINT('Origin',(1.5062967025459,-2.27443492848209,12.5369868989719));
#442747=CARTESIAN_POINT('Ctrl Pts',(1.54397793321899,-2.26784759462715,
12.506462012331));
#442748=CARTESIAN_POINT('Ctrl Pts',(1.54765766698853,-2.27325251344016,
12.4999388158272));
#442749=CARTESIAN_POINT('Ctrl Pts',(1.54761413091236,-2.27318856616249,
12.4907030323752));
#442750=CARTESIAN_POINT('Ctrl Pts',(1.53444082908789,-2.27708189091582,
12.5042014951932));
#442751=CARTESIAN_POINT('Ctrl Pts',(1.53283698093214,-2.28330834803118,
12.4980716682127));
#442752=CARTESIAN_POINT('Ctrl Pts',(1.52719566546365,-2.28709003085908,
12.4907355092743));
#442753=CARTESIAN_POINT('Ctrl Pts',(1.52889736027862,-2.27471637727053,
12.5218047446509));
#442754=CARTESIAN_POINT('Ctrl Pts',(1.52812476547835,-2.2865028936435,12.5216906929434));
#442755=CARTESIAN_POINT('Ctrl Pts',(1.51825426561694,-2.29290164249121,
12.5161988840776));
#442756=CARTESIAN_POINT('Ctrl Pts',(1.52777145831979,-2.26965634454415,
12.5369868989719));
#442757=CARTESIAN_POINT('Ctrl Pts',(1.53110123862728,-2.28462023757452,
12.5369868989719));
#442758=CARTESIAN_POINT('Ctrl Pts',(1.51821639211932,-2.29292603446506,
12.5369868989719));
#442759=CARTESIAN_POINT('Origin',(2.95976792804893E-31,-9.36866969595879E-31,
12.5));
#442760=CARTESIAN_POINT('Origin',(1.69106661248333,-2.08362280022671,12.5));
#442761=CARTESIAN_POINT('',(1.69106661248333,-2.08362280022671,12.5893111709658));
#442762=CARTESIAN_POINT('',(1.69106661248333,-2.08362280022671,13.8235269408515));
#442763=CARTESIAN_POINT('',(1.69106661248333,-2.08362280022671,12.5));
#442764=CARTESIAN_POINT('',(1.70159569779329,-2.1178048285711,13.7902182540695));
#442765=CARTESIAN_POINT('',(1.69106661248333,-2.08362280022671,13.8235269408515));
#442766=CARTESIAN_POINT('',(1.70769732837641,-2.13761339725484,13.7435492065112));
#442767=CARTESIAN_POINT('Origin',(1.68762335573118,-2.0724433722242,13.7445212918716));
#442768=CARTESIAN_POINT('',(1.70769732837641,-2.13761339725484,12.5369868989719));
#442769=CARTESIAN_POINT('',(1.70769732837641,-2.13761339725484,12.5));
#442770=CARTESIAN_POINT('Ctrl Pts',(1.70769732837641,-2.13761339725484,
12.5369868989719));
#442771=CARTESIAN_POINT('Ctrl Pts',(1.70215779955627,-2.11962965739802,
12.5544431401645));
#442772=CARTESIAN_POINT('Ctrl Pts',(1.69661430871789,-2.10163305509249,
12.5718848856037));
#442773=CARTESIAN_POINT('Ctrl Pts',(1.69106661248333,-2.08362280022671,
12.5893111709658));
#442774=CARTESIAN_POINT('Origin',(1.98348265190902,-2.17062729990068,12.5));
#442775=CARTESIAN_POINT('',(1.78991230016922,-2.06925956785759,13.7435492065112));
#442776=CARTESIAN_POINT('',(1.77155062986485,-2.05964404121031,13.7902182540695));
#442777=CARTESIAN_POINT('Origin',(1.72329933383918,-2.03437609907816,13.7418732680444));
#442778=CARTESIAN_POINT('',(1.73986539582218,-2.04305131259618,13.8235269408515));
#442779=CARTESIAN_POINT('',(1.77155062986485,-2.05964404121031,13.7902182540695));
#442780=CARTESIAN_POINT('',(1.73986539582218,-2.04305131259618,12.5893111709658));
#442781=CARTESIAN_POINT('',(1.73986539582218,-2.04305131259618,12.5));
#442782=CARTESIAN_POINT('',(1.78991230016922,-2.06925956785759,12.5369868989719));
#442783=CARTESIAN_POINT('Ctrl Pts',(1.73986539582218,-2.04305131259618,
12.5893111709658));
#442784=CARTESIAN_POINT('Ctrl Pts',(1.75656010846008,-2.05179389709843,
12.5718848856037));
#442785=CARTESIAN_POINT('Ctrl Pts',(1.77324216577624,-2.06052985433958,
12.5544431401645));
#442786=CARTESIAN_POINT('Ctrl Pts',(1.78991230016922,-2.06925956785759,
12.5369868989719));
#442787=CARTESIAN_POINT('',(1.78991230016922,-2.06925956785759,12.5));
#442788=CARTESIAN_POINT('Origin',(1.72391839740911,-2.07350346960704,12.5));
#442789=CARTESIAN_POINT('',(1.70109342731553,-2.04780111733327,13.8587068136939));
#442790=CARTESIAN_POINT('Ctrl Pts',(1.73986539582511,-2.04305131259026,
13.8235269408542));
#442791=CARTESIAN_POINT('Ctrl Pts',(1.73831306815132,-2.04223839917525,
13.8262006681044));
#442792=CARTESIAN_POINT('Ctrl Pts',(1.73664388770567,-2.04156041342918,
13.8288634856214));
#442793=CARTESIAN_POINT('Ctrl Pts',(1.73486763552003,-2.04100829237994,
13.8314912288862));
#442794=CARTESIAN_POINT('Ctrl Pts',(1.73303650272855,-2.04043911252683,
13.8342001611531));
#442795=CARTESIAN_POINT('Ctrl Pts',(1.73108969317603,-2.04000258846134,
13.8368750301949));
#442796=CARTESIAN_POINT('Ctrl Pts',(1.72900705260465,-2.03972180853287,
13.8394886372969));
#442797=CARTESIAN_POINT('Ctrl Pts',(1.72884620522155,-2.03970012321792,
13.8396904925131));
#442798=CARTESIAN_POINT('Ctrl Pts',(1.72868454093034,-2.03967938800469,
13.8398919674349));
#442799=CARTESIAN_POINT('Ctrl Pts',(1.72852204795747,-2.03965962469961,
13.8400930404591));
#442800=CARTESIAN_POINT('Ctrl Pts',(1.72599029812032,-2.03935169911028,
13.8432258934518));
#442801=CARTESIAN_POINT('Ctrl Pts',(1.72327043418938,-2.0392801653407,13.8462331177034));
#442802=CARTESIAN_POINT('Ctrl Pts',(1.72044862725666,-2.03954378938749,
13.8489036603661));
#442803=CARTESIAN_POINT('Ctrl Pts',(1.71952529918926,-2.03963005024354,
13.8497774930041));
#442804=CARTESIAN_POINT('Ctrl Pts',(1.71859127727977,-2.03975231245817,
13.85061494757));
#442805=CARTESIAN_POINT('Ctrl Pts',(1.71765021695585,-2.0399143593413,13.8514076489583));
#442806=CARTESIAN_POINT('Ctrl Pts',(1.71565973864956,-2.04025711186978,
13.8530843267192));
#442807=CARTESIAN_POINT('Ctrl Pts',(1.71344275623555,-2.04081443680464,
13.8546805203176));
#442808=CARTESIAN_POINT('Ctrl Pts',(1.71116120848055,-2.04168631562601,
13.8559412814273));
#442809=CARTESIAN_POINT('Ctrl Pts',(1.71085586339857,-2.04180300128801,
13.8561100121513));
#442810=CARTESIAN_POINT('Ctrl Pts',(1.71054938748777,-2.04192524853389,
13.8562727473908));
#442811=CARTESIAN_POINT('Ctrl Pts',(1.71024218506715,-2.04205322291605,
13.8564289040185));
#442812=CARTESIAN_POINT('Ctrl Pts',(1.70884902559436,-2.04263358527919,
13.8571370725437));
#442813=CARTESIAN_POINT('Ctrl Pts',(1.70741731217578,-2.0433440351555,13.8577210840554));
#442814=CARTESIAN_POINT('Ctrl Pts',(1.70601574112564,-2.04418324651125,
13.8581177131616));
#442815=CARTESIAN_POINT('Ctrl Pts',(1.70562101047732,-2.04441959731381,
13.8582294175695));
#442816=CARTESIAN_POINT('Ctrl Pts',(1.70522861104116,-2.04466599390546,
13.8583265086086));
#442817=CARTESIAN_POINT('Ctrl Pts',(1.70483990539604,-2.04492200212943,
13.8584082369006));
#442818=CARTESIAN_POINT('Ctrl Pts',(1.70428143961953,-2.04528981729594,
13.8585256585398));
#442819=CARTESIAN_POINT('Ctrl Pts',(1.70372383336746,-2.04568231562517,
13.8586122832068));
#442820=CARTESIAN_POINT('Ctrl Pts',(1.70318202617805,-2.04608994689989,
13.8586682984299));
#442821=CARTESIAN_POINT('Ctrl Pts',(1.70274863413415,-2.04641601151248,
13.8587131050557));
#442822=CARTESIAN_POINT('Ctrl Pts',(1.70232042319479,-2.04675517282245,
13.8587357943552));
#442823=CARTESIAN_POINT('Ctrl Pts',(1.70189765692105,-2.04710786813566,
13.8587355499465));
#442824=CARTESIAN_POINT('Ctrl Pts',(1.70162441299911,-2.04733582352524,
13.8587353919793));
#442825=CARTESIAN_POINT('Ctrl Pts',(1.70135637355137,-2.04756693776055,
13.8587257282814));
#442826=CARTESIAN_POINT('Ctrl Pts',(1.70109342731553,-2.04780111733327,
13.8587068136939));
#442827=CARTESIAN_POINT('Ctrl Pts',(1.70109342731553,-2.04780111733327,
13.8587068136939));
#442828=CARTESIAN_POINT('Ctrl Pts',(1.70022861148054,-2.04857132118149,
13.8586446046466));
#442829=CARTESIAN_POINT('Ctrl Pts',(1.6994188212477,-2.04937464291353,13.858482427929));
#442830=CARTESIAN_POINT('Ctrl Pts',(1.69866069815332,-2.05020813182118,
13.8582284286032));
#442831=CARTESIAN_POINT('Ctrl Pts',(1.69788295204698,-2.05106319448503,
13.8579678548414));
#442832=CARTESIAN_POINT('Ctrl Pts',(1.69715881559737,-2.0519531254972,13.857615680862));
#442833=CARTESIAN_POINT('Ctrl Pts',(1.69650932147237,-2.05283672432534,
13.8571944833187));
#442834=CARTESIAN_POINT('Ctrl Pts',(1.69488844245862,-2.05504183556806,
13.8561433417727));
#442835=CARTESIAN_POINT('Ctrl Pts',(1.6936527546168,-2.05730781781979,13.8546163505474));
#442836=CARTESIAN_POINT('Ctrl Pts',(1.69273047089348,-2.05944075232021,
13.8528973491086));
#442837=CARTESIAN_POINT('Ctrl Pts',(1.69256198326426,-2.05983040798492,
13.8525833129072));
#442838=CARTESIAN_POINT('Ctrl Pts',(1.69240381419284,-2.06021563350189,
13.8522628768812));
#442839=CARTESIAN_POINT('Ctrl Pts',(1.69225535185086,-2.06059528714164,
13.851937733538));
#442840=CARTESIAN_POINT('Ctrl Pts',(1.69134871292664,-2.06291377924506,
13.8499521282529));
#442841=CARTESIAN_POINT('Ctrl Pts',(1.69071776970868,-2.06525637489189,
13.847639871647));
#442842=CARTESIAN_POINT('Ctrl Pts',(1.69031810602992,-2.06747906191905,
13.8452109780794));
#442843=CARTESIAN_POINT('Ctrl Pts',(1.69013828906821,-2.06847909481989,
13.8441181685877));
#442844=CARTESIAN_POINT('Ctrl Pts',(1.6900045829282,-2.0694549799111,13.8430021611332));
#442845=CARTESIAN_POINT('Ctrl Pts',(1.68991002270988,-2.07039515782479,
13.8418824960098));
#442846=CARTESIAN_POINT('Ctrl Pts',(1.68968718914072,-2.07261071108671,
13.8392439765549));
#442847=CARTESIAN_POINT('Ctrl Pts',(1.68966732551376,-2.07473350914547,
13.8364981347964));
#442848=CARTESIAN_POINT('Ctrl Pts',(1.68981616026676,-2.07676884578819,
13.8336931113419));
#442849=CARTESIAN_POINT('Ctrl Pts',(1.68996111586431,-2.07875113442236,
13.8309611966328));
#442850=CARTESIAN_POINT('Ctrl Pts',(1.69026679887585,-2.08065240658422,
13.8281701127186));
#442851=CARTESIAN_POINT('Ctrl Pts',(1.69073701489446,-2.08246062340627,
13.8253580685121));
#442852=CARTESIAN_POINT('Ctrl Pts',(1.69083895823477,-2.08285264676478,
13.8247484142932));
#442853=CARTESIAN_POINT('Ctrl Pts',(1.69094874991648,-2.08324016664723,
13.8241378483365));
#442854=CARTESIAN_POINT('Ctrl Pts',(1.69106661248333,-2.08362280022671,
13.8235269408515));
#442855=CARTESIAN_POINT('',(1.70203688208365,-2.04699323741746,12.5969504640361));
#442856=CARTESIAN_POINT('Origin',(1.72393939862195,-2.07352903583219,12.584524458991));
#442857=CARTESIAN_POINT('Origin',(1.72393939862195,-2.07352903583219,12.584524458991));
#442858=CARTESIAN_POINT('Ctrl Pts',(1.73986539582218,-2.04305131259618,
12.5893111709658));
#442859=CARTESIAN_POINT('Ctrl Pts',(1.72982485735825,-2.03779334512631,
12.5770542771492));
#442860=CARTESIAN_POINT('Ctrl Pts',(1.71966334052538,-2.0506209423491,12.5737548217797));
#442861=CARTESIAN_POINT('Ctrl Pts',(1.76182068373786,-2.05454872282643,
12.5663937883685));
#442862=CARTESIAN_POINT('Ctrl Pts',(1.75176733717272,-2.04928404808883,
12.5540940315303));
#442863=CARTESIAN_POINT('Ctrl Pts',(1.74157684897256,-2.06215338939119,
12.5508374392248));
#442864=CARTESIAN_POINT('Ctrl Pts',(1.78375381903733,-2.06603453231078,
12.5434499600945));
#442865=CARTESIAN_POINT('Ctrl Pts',(1.77366778546239,-2.06075274024082,
12.5311293540533));
#442866=CARTESIAN_POINT('Ctrl Pts',(1.76346949693809,-2.07367352488174,
12.5278936106989));
#442867=CARTESIAN_POINT('Ctrl Pts',(1.80566653696509,-2.0775096497514,12.5204817579905));
#442868=CARTESIAN_POINT('Ctrl Pts',(1.79553058441682,-2.07220171642029,
12.5081597038247));
#442869=CARTESIAN_POINT('Ctrl Pts',(1.78534291223217,-2.08518229346266,
12.5049254088044));
#442870=CARTESIAN_POINT('Ctrl Pts',(1.78991230016922,-2.06925956785759,
12.5369868989719));
#442871=CARTESIAN_POINT('Ctrl Pts',(1.79073750242346,-2.06969170488486,
12.5342545179733));
#442872=CARTESIAN_POINT('Ctrl Pts',(1.79146716650627,-2.07021462690545,
12.5314872231885));
#442873=CARTESIAN_POINT('Ctrl Pts',(1.79202762612217,-2.07084431423188,
12.5287124745063));
#442874=CARTESIAN_POINT('Ctrl Pts',(1.79253307642253,-2.07141219751775,
12.5262100684184));
#442875=CARTESIAN_POINT('Ctrl Pts',(1.7928996624422,-2.07206699750852,12.5237004536639));
#442876=CARTESIAN_POINT('Ctrl Pts',(1.79307583586429,-2.0728523404252,12.5212220730815));
#442877=CARTESIAN_POINT('Ctrl Pts',(1.79321071185911,-2.07345358836549,
12.5193246583486));
#442878=CARTESIAN_POINT('Ctrl Pts',(1.79323497547226,-2.07413867514844,
12.5174178313691));
#442879=CARTESIAN_POINT('Ctrl Pts',(1.79305404523333,-2.07493014779619,
12.5155812248348));
#442880=CARTESIAN_POINT('Ctrl Pts',(1.79297696797904,-2.07526731939831,
12.5147988205794));
#442881=CARTESIAN_POINT('Ctrl Pts',(1.7928628438386,-2.07562420198027,12.5140295443047));
#442882=CARTESIAN_POINT('Ctrl Pts',(1.79270580621475,-2.07600409925261,
12.5132817086137));
#442883=CARTESIAN_POINT('Ctrl Pts',(1.79246815101462,-2.07657902238295,
12.5121499604604));
#442884=CARTESIAN_POINT('Ctrl Pts',(1.79212047097037,-2.07721633839851,
12.5110494206568));
#442885=CARTESIAN_POINT('Ctrl Pts',(1.79162607329503,-2.07790968034323,
12.5100666561695));
#442886=CARTESIAN_POINT('Ctrl Pts',(1.79134219128834,-2.07830779569127,
12.5095023550641));
#442887=CARTESIAN_POINT('Ctrl Pts',(1.79100612457548,-2.07872860384227,
12.5089719619137));
#442888=CARTESIAN_POINT('Ctrl Pts',(1.79061918161063,-2.07916023149304,
12.5085043804652));
#442889=CARTESIAN_POINT('Ctrl Pts',(1.79005294098444,-2.07979186233648,
12.5078201359221));
#442890=CARTESIAN_POINT('Ctrl Pts',(1.78936042916077,-2.08046417579513,
12.5072563000949));
#442891=CARTESIAN_POINT('Ctrl Pts',(1.78858269109955,-2.08112552463992,
12.5068768744332));
#442892=CARTESIAN_POINT('Ctrl Pts',(1.78802188841774,-2.08160240268443,
12.5066032824114));
#442893=CARTESIAN_POINT('Ctrl Pts',(1.78740695962903,-2.08208200356589,
12.5064197834844));
#442894=CARTESIAN_POINT('Ctrl Pts',(1.78677383363288,-2.08253958336252,
12.5063282718343));
#442895=CARTESIAN_POINT('Ctrl Pts',(1.78584966568937,-2.08320750820248,
12.5061946931565));
#442896=CARTESIAN_POINT('Ctrl Pts',(1.78486759422664,-2.08384364979212,
12.5062515701262));
#442897=CARTESIAN_POINT('Ctrl Pts',(1.78389697582206,-2.08442150750074,
12.5064436508398));
#442898=CARTESIAN_POINT('',(1.71966334052538,-2.05062094234911,12.5737548217797));
#442899=CARTESIAN_POINT('Origin',(1.72965931683782,-2.06254069308313,12.5893111709658));
#442900=CARTESIAN_POINT('Ctrl Pts',(1.78389697582206,-2.08442150750074,
12.5064436508398));
#442901=CARTESIAN_POINT('Ctrl Pts',(1.77438850524016,-2.0794185708687,12.5164271754438));
#442902=CARTESIAN_POINT('Ctrl Pts',(1.76487636279056,-2.07441346617056,
12.5264061185523));
#442903=CARTESIAN_POINT('Ctrl Pts',(1.75536041871244,-2.06940611788646,
12.536380305637));
#442904=CARTESIAN_POINT('Ctrl Pts',(1.7434674186562,-2.06314794813101,12.5488460165097));
#442905=CARTESIAN_POINT('Ctrl Pts',(1.73156847698094,-2.05688627203981,
12.5613043021964));
#442906=CARTESIAN_POINT('Ctrl Pts',(1.71966334052538,-2.0506209423491,12.5737548217797));
#442907=CARTESIAN_POINT('Ctrl Pts',(1.69106661248333,-2.08362280022671,
12.5893111709658));
#442908=CARTESIAN_POINT('Ctrl Pts',(1.68773011555539,-2.07279106801023,
12.5770542771492));
#442909=CARTESIAN_POINT('Ctrl Pts',(1.70219730425851,-2.06514226902717,
12.5737548217797));
#442910=CARTESIAN_POINT('Ctrl Pts',(1.68795368986888,-2.07351688827816,
12.5928319619712));
#442911=CARTESIAN_POINT('Ctrl Pts',(1.68882474430402,-2.06527827913933,
12.5821634970842));
#442912=CARTESIAN_POINT('Ctrl Pts',(1.7010543212952,-2.06146370853223,12.5773203894503));
#442913=CARTESIAN_POINT('Ctrl Pts',(1.69014909721797,-2.05691073622806,
12.5969440695591));
#442914=CARTESIAN_POINT('Ctrl Pts',(1.69322838590855,-2.05432683922702,
12.5878292599214));
#442915=CARTESIAN_POINT('Ctrl Pts',(1.70183883760259,-2.05554520523655,
12.5813877129824));
#442916=CARTESIAN_POINT('Ctrl Pts',(1.71364215121175,-2.03730839811275,
12.596957478804));
#442917=CARTESIAN_POINT('Ctrl Pts',(1.71058567081602,-2.03987326082631,
12.5878468778671));
#442918=CARTESIAN_POINT('Ctrl Pts',(1.71025114891585,-2.04853383684849,
12.5814011370086));
#442919=CARTESIAN_POINT('Ctrl Pts',(1.7304840588282,-2.03813855170033,12.5928371701607));
#442920=CARTESIAN_POINT('Ctrl Pts',(1.72223033693283,-2.0374973492534,12.5821692192951));
#442921=CARTESIAN_POINT('Ctrl Pts',(1.7162444991906,-2.0488196091202,12.5773318885715));
#442922=CARTESIAN_POINT('Ctrl Pts',(1.7398653958222,-2.04305131259613,12.5893111709658));
#442923=CARTESIAN_POINT('Ctrl Pts',(1.72982485735828,-2.03779334512626,
12.5770542771492));
#442924=CARTESIAN_POINT('Ctrl Pts',(1.71966334052541,-2.05062094234906,
12.5737548217797));
#442925=CARTESIAN_POINT('',(1.70219730425851,-2.06514226902717,12.5737548217797));
#442926=CARTESIAN_POINT('Origin',(1.71209175483583,-2.07714642863012,12.5893111709658));
#442927=CARTESIAN_POINT('Ctrl Pts',(1.71966334052541,-2.05062094234906,
12.5737548217797));
#442928=CARTESIAN_POINT('Ctrl Pts',(1.71879118408743,-2.05012732024794,
12.5746934679442));
#442929=CARTESIAN_POINT('Ctrl Pts',(1.71773585576928,-2.04974051593159,
12.5756680099006));
#442930=CARTESIAN_POINT('Ctrl Pts',(1.71661856794228,-2.04950141013988,
12.5765688348656));
#442931=CARTESIAN_POINT('Ctrl Pts',(1.71632277835887,-2.04943810952852,
12.5768073183026));
#442932=CARTESIAN_POINT('Ctrl Pts',(1.71602275959963,-2.04938492988671,
12.5770407398754));
#442933=CARTESIAN_POINT('Ctrl Pts',(1.71572087407775,-2.04934207811222,
12.5772674179684));
#442934=CARTESIAN_POINT('Ctrl Pts',(1.71448201752921,-2.04916622601729,
12.5781976435658));
#442935=CARTESIAN_POINT('Ctrl Pts',(1.71313977428438,-2.04916548139034,
12.5790594849312));
#442936=CARTESIAN_POINT('Ctrl Pts',(1.71178474793405,-2.04938818368848,
12.5797571720116));
#442937=CARTESIAN_POINT('Ctrl Pts',(1.71090189954441,-2.04953328224338,
12.580211740231));
#442938=CARTESIAN_POINT('Ctrl Pts',(1.70997654830403,-2.04979835216295,
12.5806009430798));
#442939=CARTESIAN_POINT('Ctrl Pts',(1.70907871370227,-2.05018176537634,
12.5808812374708));
#442940=CARTESIAN_POINT('Ctrl Pts',(1.70830717592583,-2.05051124452265,
12.5811221033394));
#442941=CARTESIAN_POINT('Ctrl Pts',(1.70754020722779,-2.05093496467668,
12.581287365893));
#442942=CARTESIAN_POINT('Ctrl Pts',(1.70682512856864,-2.05143630866505,
12.581359338449));
#442943=CARTESIAN_POINT('Ctrl Pts',(1.70672574740083,-2.05150598512708,
12.5813693411482));
#442944=CARTESIAN_POINT('Ctrl Pts',(1.70662731975361,-2.05157712614493,
12.5813775999465));
#442945=CARTESIAN_POINT('Ctrl Pts',(1.70652992209161,-2.05164965238241,
12.5813841266931));
#442946=CARTESIAN_POINT('Ctrl Pts',(1.70636467517804,-2.05177270191617,
12.5813952001081));
#442947=CARTESIAN_POINT('Ctrl Pts',(1.70620165000108,-2.05190105131348,
12.5814007534795));
#442948=CARTESIAN_POINT('Ctrl Pts',(1.70604103955566,-2.05203479962438,
12.5814005856065));
#442949=CARTESIAN_POINT('Ctrl Pts',(1.70530582773112,-2.05264704709946,
12.5813998171494));
#442950=CARTESIAN_POINT('Ctrl Pts',(1.70467179692695,-2.05332986518653,
12.58127954464));
#442951=CARTESIAN_POINT('Ctrl Pts',(1.70412086363673,-2.05405924342645,
12.5810700125799));
#442952=CARTESIAN_POINT('Ctrl Pts',(1.70345539895092,-2.0549402492939,12.5808169217085));
#442953=CARTESIAN_POINT('Ctrl Pts',(1.70292446691484,-2.05589935279849,
12.5804173076348));
#442954=CARTESIAN_POINT('Ctrl Pts',(1.70255181322556,-2.05683988700601,
12.5799304713245));
#442955=CARTESIAN_POINT('Ctrl Pts',(1.70208997790651,-2.05800550518796,
12.5793271277669));
#442956=CARTESIAN_POINT('Ctrl Pts',(1.70181265792322,-2.05920304701824,
12.5785808224116));
#442957=CARTESIAN_POINT('Ctrl Pts',(1.70170064367809,-2.06037487835076,
12.5777485681082));
#442958=CARTESIAN_POINT('Ctrl Pts',(1.70153373018076,-2.06212103541993,
12.576508418016));
#442959=CARTESIAN_POINT('Ctrl Pts',(1.70172843028403,-2.06379474727702,
12.5750928681475));
#442960=CARTESIAN_POINT('Ctrl Pts',(1.70219730425851,-2.06514226902717,
12.5737548217797));
#442961=CARTESIAN_POINT('Ctrl Pts',(1.70219730425851,-2.06514226902717,
12.5737548217797));
#442962=CARTESIAN_POINT('Ctrl Pts',(1.68773011555539,-2.07279106801023,
12.5770542771492));
#442963=CARTESIAN_POINT('Ctrl Pts',(1.69106661248333,-2.08362280022671,
12.5893111709658));
#442964=CARTESIAN_POINT('Ctrl Pts',(1.70953407649328,-2.08878939839514,
12.5508408821982));
#442965=CARTESIAN_POINT('Ctrl Pts',(1.69502056198147,-2.09645905426385,
12.55409748406));
#442966=CARTESIAN_POINT('Ctrl Pts',(1.69836131542497,-2.10730460499651,
12.5663972313419));
#442967=CARTESIAN_POINT('Ctrl Pts',(1.71686255508848,-2.11241377701704,
12.52790050457));
#442968=CARTESIAN_POINT('Ctrl Pts',(1.7022970454674,-2.12008171069044,12.5311362602938));
#442969=CARTESIAN_POINT('Ctrl Pts',(1.70564865921001,-2.13096251871672,
12.5434568539655));
#442970=CARTESIAN_POINT('Ctrl Pts',(1.72418337134024,-2.13601717702138,
12.5049357605811));
#442971=CARTESIAN_POINT('Ctrl Pts',(1.70956102157824,-2.14366376269259,
12.5081700652078));
#442972=CARTESIAN_POINT('Ctrl Pts',(1.71292922020911,-2.15459841253922,
12.5204921097672));
#442973=CARTESIAN_POINT('Ctrl Pts',(1.72370265633254,-2.13446728572477,
12.5064436508395));
#442974=CARTESIAN_POINT('Ctrl Pts',(1.72289754221706,-2.13538414942873,
12.5062361689309));
#442975=CARTESIAN_POINT('Ctrl Pts',(1.72202119231672,-2.13630328079726,
12.5061871075061));
#442976=CARTESIAN_POINT('Ctrl Pts',(1.72112428280073,-2.13714385795685,
12.5063648335164));
#442977=CARTESIAN_POINT('Ctrl Pts',(1.72071685117489,-2.13752569995169,
12.5064455676329));
#442978=CARTESIAN_POINT('Ctrl Pts',(1.72029934351721,-2.13789649714619,
12.506574497099));
#442979=CARTESIAN_POINT('Ctrl Pts',(1.71988896342837,-2.13823956507991,
12.5067492519495));
#442980=CARTESIAN_POINT('Ctrl Pts',(1.71906428871011,-2.13892897340961,
12.5071004286051));
#442981=CARTESIAN_POINT('Ctrl Pts',(1.71823755816902,-2.13953113118327,
12.5076537929612));
#442982=CARTESIAN_POINT('Ctrl Pts',(1.71747639089655,-2.14000848873226,
12.5083435010503));
#442983=CARTESIAN_POINT('Ctrl Pts',(1.71742847086791,-2.14003854124273,
12.5083869222963));
#442984=CARTESIAN_POINT('Ctrl Pts',(1.7173807991295,-2.14006809227941,12.5084308732336));
#442985=CARTESIAN_POINT('Ctrl Pts',(1.71733338764277,-2.14009713003058,
12.5084753333615));
#442986=CARTESIAN_POINT('Ctrl Pts',(1.71695308494236,-2.14033005112091,
12.508831962269));
#442987=CARTESIAN_POINT('Ctrl Pts',(1.71658248026876,-2.14053577543842,
12.509227847131));
#442988=CARTESIAN_POINT('Ctrl Pts',(1.71623395261267,-2.14071063388234,
12.5096423454524));
#442989=CARTESIAN_POINT('Ctrl Pts',(1.71514182119035,-2.14125856285648,
12.5109411997424));
#442990=CARTESIAN_POINT('Ctrl Pts',(1.7142036306779,-2.14154575730631,12.5124831113042));
#442991=CARTESIAN_POINT('Ctrl Pts',(1.71340838913029,-2.14166621209627,
12.5140723025008));
#442992=CARTESIAN_POINT('Ctrl Pts',(1.71333387412627,-2.14167749884202,
12.5142212114565));
#442993=CARTESIAN_POINT('Ctrl Pts',(1.71326060064133,-2.14168734795223,
12.5143705582413));
#442994=CARTESIAN_POINT('Ctrl Pts',(1.71318855326299,-2.14169585249783,
12.5145201959299));
#442995=CARTESIAN_POINT('Ctrl Pts',(1.71226299742089,-2.14180510604802,
12.5164425148273));
#442996=CARTESIAN_POINT('Ctrl Pts',(1.71150933463858,-2.14170687066787,
12.5184635205941));
#442997=CARTESIAN_POINT('Ctrl Pts',(1.71087201749238,-2.14147222703179,
12.5205025929158));
#442998=CARTESIAN_POINT('Ctrl Pts',(1.7105023482867,-2.14133612442246,12.5216853356836));
#442999=CARTESIAN_POINT('Ctrl Pts',(1.71017232380612,-2.14115482743748,
12.5228750347131));
#443000=CARTESIAN_POINT('Ctrl Pts',(1.70987597479482,-2.14094557851382,
12.5240609649613));
#443001=CARTESIAN_POINT('Ctrl Pts',(1.70914860204515,-2.14043198825653,
12.5269717671326));
#443002=CARTESIAN_POINT('Ctrl Pts',(1.7086096256663,-2.13972706028063,12.5299036066169));
#443003=CARTESIAN_POINT('Ctrl Pts',(1.70819956303754,-2.13889381315844,
12.5328133004019));
#443004=CARTESIAN_POINT('Ctrl Pts',(1.7080027090985,-2.13849380602126,12.5342101228451));
#443005=CARTESIAN_POINT('Ctrl Pts',(1.70783627993333,-2.13806449466612,
12.5356023438238));
#443006=CARTESIAN_POINT('Ctrl Pts',(1.70769732837641,-2.13761339725483,
12.5369868989719));
#443007=CARTESIAN_POINT('Origin',(5.45451214630952,-14.3194087425353,-1.23967887089177));
#443008=CARTESIAN_POINT('Ctrl Pts',(1.7898752938568,-2.06924014380621,12.5369868989719));
#443009=CARTESIAN_POINT('Ctrl Pts',(1.80345023182615,-2.07638187768624,
12.5369868989719));
#443010=CARTESIAN_POINT('Ctrl Pts',(1.8148454186455,-2.06611381939672,12.5369868989719));
#443011=CARTESIAN_POINT('Ctrl Pts',(1.79446418463105,-2.0716542705718,12.5218025310015));
#443012=CARTESIAN_POINT('Ctrl Pts',(1.80604660487188,-2.07400020430251,
12.5216901060418));
#443013=CARTESIAN_POINT('Ctrl Pts',(1.81481069337939,-2.06614513209288,
12.5161920673677));
#443014=CARTESIAN_POINT('Ctrl Pts',(1.79529649285718,-2.07762447443862,
12.5042015548895));
#443015=CARTESIAN_POINT('Ctrl Pts',(1.80172847633282,-2.07770774259735,
12.4980677368513));
#443016=CARTESIAN_POINT('Ctrl Pts',(1.80685914496331,-2.07325049915236,
12.4907278922778));
#443017=CARTESIAN_POINT('Ctrl Pts',(1.78388397084315,-2.08440631165171,
12.506463626192));
#443018=CARTESIAN_POINT('Ctrl Pts',(1.78813814734719,-2.0893771687819,12.4999376786891));
#443019=CARTESIAN_POINT('Ctrl Pts',(1.78808618876676,-2.08931645698968,
12.4906970594712));
#443020=CARTESIAN_POINT('Origin',(1.80011837915358,-2.04977018737064,12.5369868989719));
#443021=CARTESIAN_POINT('Origin',(1.80011837915358,-2.04977018737064,14.));
#443022=CARTESIAN_POINT('Origin',(1.80011837915358,-2.04977018737064,13.7435492065112));
#443023=CARTESIAN_POINT('Ctrl Pts',(1.7679778087978,-2.05777301758466,13.793642941384));
#443024=CARTESIAN_POINT('Ctrl Pts',(1.77754357613767,-2.06281308843785,
13.8071662555867));
#443025=CARTESIAN_POINT('Ctrl Pts',(1.78761084470702,-2.04907738724762,
13.8103758687955));
#443026=CARTESIAN_POINT('Ctrl Pts',(1.78270214268511,-2.0654837696101,13.7804579775006));
#443027=CARTESIAN_POINT('Ctrl Pts',(1.79451016202354,-2.07169378982202,
13.7901904343352));
#443028=CARTESIAN_POINT('Ctrl Pts',(1.80575782147073,-2.06065992915931,
13.7927914348262));
#443029=CARTESIAN_POINT('Ctrl Pts',(1.79137091220124,-2.07002337948204,
13.7597120340895));
#443030=CARTESIAN_POINT('Ctrl Pts',(1.80503878325616,-2.07720504995615,
13.7635825532445));
#443031=CARTESIAN_POINT('Ctrl Pts',(1.81647282585308,-2.067468593412,13.7651073818884));
#443032=CARTESIAN_POINT('Ctrl Pts',(1.78967336863811,-2.06913441992315,
13.7381884353898));
#443033=CARTESIAN_POINT('Ctrl Pts',(1.80302089962284,-2.07614878569902,
13.7368803041982));
#443034=CARTESIAN_POINT('Ctrl Pts',(1.81437477466417,-2.06613483749339,
13.7363986145813));
#443035=CARTESIAN_POINT('Origin',(1.78175670884921,-2.04015466072337,13.7902182540695));
#443036=CARTESIAN_POINT('Ctrl Pts',(1.73986190917114,-2.04304948587151,
13.8235227101244));
#443037=CARTESIAN_POINT('Ctrl Pts',(1.75004488945686,-2.04838705093622,
13.8358800583119));
#443038=CARTESIAN_POINT('Ctrl Pts',(1.76024757046897,-2.03532828571046,
13.8390832900376));
#443039=CARTESIAN_POINT('Ctrl Pts',(1.75042832427883,-2.04858284118871,
13.8124254819052));
#443040=CARTESIAN_POINT('Ctrl Pts',(1.76063107989705,-2.05393077148275,
13.8247886449158));
#443041=CARTESIAN_POINT('Ctrl Pts',(1.77083322137122,-2.04084501241255,
13.8279860620657));
#443042=CARTESIAN_POINT('Ctrl Pts',(1.76099000386301,-2.05411371663608,
13.8013225099955));
#443043=CARTESIAN_POINT('Ctrl Pts',(1.77120771982084,-2.05946949057065,
13.8136962257787));
#443044=CARTESIAN_POINT('Ctrl Pts',(1.78141384636739,-2.0463594255137,13.8168830918626));
#443045=CARTESIAN_POINT('Ctrl Pts',(1.77154713217567,-2.05964220870156,
13.7902140179785));
#443046=CARTESIAN_POINT('Ctrl Pts',(1.78177530817666,-2.06500346948959,
13.802602731458));
#443047=CARTESIAN_POINT('Ctrl Pts',(1.79198964208704,-2.05187161755285,
13.8057746032558));
#443048=CARTESIAN_POINT('Origin',(1.75007147480654,-2.02356193210923,13.8235269408515));
#443049=CARTESIAN_POINT('Ctrl Pts',(1.69106661248333,-2.08362280022671,
13.8235269408515));
#443050=CARTESIAN_POINT('Ctrl Pts',(1.69454250510398,-2.09490707199234,
13.8362179249168));
#443051=CARTESIAN_POINT('Ctrl Pts',(1.67924918461413,-2.10250821351529,
13.8391868794938));
#443052=CARTESIAN_POINT('Ctrl Pts',(1.68788632203204,-2.07329818273625,
13.8400110824519));
#443053=CARTESIAN_POINT('Ctrl Pts',(1.68740372913541,-2.08335248365463,
13.8494522556836));
#443054=CARTESIAN_POINT('Ctrl Pts',(1.67412270254772,-2.08548373216496,
13.85569149686));
#443055=CARTESIAN_POINT('Ctrl Pts',(1.68988426417026,-2.05713012925857,
13.8586819406588));
#443056=CARTESIAN_POINT('Ctrl Pts',(1.68654527462426,-2.05992426462513,
13.868010383617));
#443057=CARTESIAN_POINT('Ctrl Pts',(1.67758422377729,-2.05866234762686,
13.8744918421245));
#443058=CARTESIAN_POINT('Ctrl Pts',(1.71391107976988,-2.03708558810421,
13.8587686893867));
#443059=CARTESIAN_POINT('Ctrl Pts',(1.7172203162035,-2.03431627733324,13.8680909899357));
#443060=CARTESIAN_POINT('Ctrl Pts',(1.71758346414105,-2.02529604867311,
13.8745789365163));
#443061=CARTESIAN_POINT('Ctrl Pts',(1.73027935694154,-2.03803135466715,
13.8400379222776));
#443062=CARTESIAN_POINT('Ctrl Pts',(1.74025120512754,-2.03938504505403,
13.8494748685453));
#443063=CARTESIAN_POINT('Ctrl Pts',(1.74477032468373,-2.02672255463149,
13.8557104837033));
#443064=CARTESIAN_POINT('Ctrl Pts',(1.73986539582511,-2.04305131259026,
13.8235269408542));
#443065=CARTESIAN_POINT('Ctrl Pts',(1.75032541850993,-2.04852895297857,
13.8362179249195));
#443066=CARTESIAN_POINT('Ctrl Pts',(1.76059090559906,-2.03488040804223,
13.8391868794965));
#443067=CARTESIAN_POINT('Origin',(1.67004147013083,-2.0900991718233,13.8235269408515));
#443068=CARTESIAN_POINT('Ctrl Pts',(1.70159453635695,-2.11780106062099,
13.7902140241683));
#443069=CARTESIAN_POINT('Ctrl Pts',(1.70499832600973,-2.12883613250079,
13.8026027327198));
#443070=CARTESIAN_POINT('Ctrl Pts',(1.69022235930951,-2.1364813100885,13.8057746032556));
#443071=CARTESIAN_POINT('Ctrl Pts',(1.69808637528478,-2.10641203130704,
13.8013225161808));
#443072=CARTESIAN_POINT('Ctrl Pts',(1.70148668000303,-2.11743581721336,
13.8136962270464));
#443073=CARTESIAN_POINT('Ctrl Pts',(1.68673363241353,-2.12507690300892,
13.8168830918628));
#443074=CARTESIAN_POINT('Ctrl Pts',(1.69457670181281,-2.09501809208009,
13.8124254880875));
#443075=CARTESIAN_POINT('Ctrl Pts',(1.69797202604004,-2.10602573707947,
13.8247886461867));
#443076=CARTESIAN_POINT('Ctrl Pts',(1.68324360346558,-2.11366734232092,
13.8279860620656));
#443077=CARTESIAN_POINT('Ctrl Pts',(1.69106545471319,-2.08361904416762,
13.8235227163066));
#443078=CARTESIAN_POINT('Ctrl Pts',(1.69445419831512,-2.0946053538318,13.8358800595847));
#443079=CARTESIAN_POINT('Ctrl Pts',(1.67975221738026,-2.1022524178036,13.8390832900376));
#443080=CARTESIAN_POINT('Origin',(1.68057055544079,-2.12428120016769,13.7902182540695));
#443081=CARTESIAN_POINT('Ctrl Pts',(1.70761786051406,-2.13735550342723,
13.7382347919292));
#443082=CARTESIAN_POINT('Ctrl Pts',(1.71208308916302,-2.15177006557272,
13.7369371795942));
#443083=CARTESIAN_POINT('Ctrl Pts',(1.70015025900713,-2.16110555385622,
13.7364597369711));
#443084=CARTESIAN_POINT('Ctrl Pts',(1.70817469891981,-2.1391632437222,13.7595490285574));
#443085=CARTESIAN_POINT('Ctrl Pts',(1.71274550369607,-2.15392202246967,
13.7633824266926));
#443086=CARTESIAN_POINT('Ctrl Pts',(1.70106753305121,-2.16338345269585,
13.7648920890506));
#443087=CARTESIAN_POINT('Ctrl Pts',(1.70533485356418,-2.1299438672515,13.780380659011));
#443088=CARTESIAN_POINT('Ctrl Pts',(1.70929359290887,-2.14270808555131,
13.7901039518744));
#443089=CARTESIAN_POINT('Ctrl Pts',(1.69639461382563,-2.15176908880903,
13.7926933640892));
#443090=CARTESIAN_POINT('Ctrl Pts',(1.7003985683292,-2.11391853294447,13.7936647693663));
#443091=CARTESIAN_POINT('Ctrl Pts',(1.70361105094856,-2.1242458407914,13.8072068914933));
#443092=CARTESIAN_POINT('Ctrl Pts',(1.68824712969806,-2.13163462916677,
13.8104111085397));
#443093=CARTESIAN_POINT('Origin',(1.68667218602391,-2.14408976885142,13.7435492065112));
#443094=CARTESIAN_POINT('Origin',(1.68667218602391,-2.14408976885142,14.));
#443095=CARTESIAN_POINT('Origin',(1.68667218602391,-2.14408976885142,12.5369868989719));
#443096=CARTESIAN_POINT('Ctrl Pts',(1.72369110664741,-2.13445298369114,
12.506462012331));
#443097=CARTESIAN_POINT('Ctrl Pts',(1.72779914746646,-2.13953998561947,
12.4999388158272));
#443098=CARTESIAN_POINT('Ctrl Pts',(1.72775054395621,-2.13947979971546,
12.4907030323752));
#443099=CARTESIAN_POINT('Ctrl Pts',(1.71493841731808,-2.14443391614551,
12.5042014951932));
#443100=CARTESIAN_POINT('Ctrl Pts',(1.71384741989327,-2.15077038375256,
12.4980716682127));
#443101=CARTESIAN_POINT('Ctrl Pts',(1.70853311769454,-2.15499930292493,
12.4907355092743));
#443102=CARTESIAN_POINT('Ctrl Pts',(1.70922058262154,-2.14252811772274,
12.5218047446509));
#443103=CARTESIAN_POINT('Ctrl Pts',(1.70941126907183,-2.15433838908345,
12.5216906929434));
#443104=CARTESIAN_POINT('Ctrl Pts',(1.70009516991862,-2.16152038399417,
12.5161988840776));
#443105=CARTESIAN_POINT('Ctrl Pts',(1.70768598736634,-2.13757669329985,
12.5369868989719));
#443106=CARTESIAN_POINT('Ctrl Pts',(1.71222438430453,-2.15221938720337,
12.5369868989719));
#443107=CARTESIAN_POINT('Ctrl Pts',(1.70005941061424,-2.16154778184741,
12.5369868989719));
#443108=CARTESIAN_POINT('Origin',(3.29362846957905E-31,-9.11339005493236E-31,
12.5));
#443109=CARTESIAN_POINT('Origin',(1.85527432946228,-1.93885208923186,12.5));
#443110=CARTESIAN_POINT('',(1.85527432946228,-1.93885208923186,12.5893111709658));
#443111=CARTESIAN_POINT('',(1.85527432946228,-1.93885208923186,13.8235269408515));
#443112=CARTESIAN_POINT('',(1.85527432946228,-1.93885208923186,12.5));
#443113=CARTESIAN_POINT('',(1.86855453274999,-1.97206216149674,13.7902182540695));
#443114=CARTESIAN_POINT('',(1.85527432946228,-1.93885208923186,13.8235269408515));
#443115=CARTESIAN_POINT('',(1.87625044290219,-1.99130747926497,13.7435492065112));
#443116=CARTESIAN_POINT('Origin',(1.85093130269374,-1.92799051723916,13.7445212918696));
#443117=CARTESIAN_POINT('',(1.87625044290219,-1.99130747926497,12.5369868989719));
#443118=CARTESIAN_POINT('',(1.87625044290219,-1.99130747926497,12.5));
#443119=CARTESIAN_POINT('Ctrl Pts',(1.87625044290219,-1.99130747926497,
12.5369868989719));
#443120=CARTESIAN_POINT('Ctrl Pts',(1.869263504656,-1.97383510184429,12.5544431401645));
#443121=CARTESIAN_POINT('Ctrl Pts',(1.86227156916588,-1.9563502277149,12.5718848856037));
#443122=CARTESIAN_POINT('Ctrl Pts',(1.85527432946228,-1.93885208923186,
12.5893111709658));
#443123=CARTESIAN_POINT('Origin',(2.15380905307319,-2.00173246673928,12.5));
#443124=CARTESIAN_POINT('',(1.95262037949676,-1.91647980814857,13.7435492065112));
#443125=CARTESIAN_POINT('',(1.93353605144765,-1.90839292296423,13.7902182540695));
#443126=CARTESIAN_POINT('Origin',(1.88338573577249,-1.88714198639574,13.7418732680459));
#443127=CARTESIAN_POINT('',(1.90060378598597,-1.89443804601159,13.8235269408515));
#443128=CARTESIAN_POINT('',(1.93353605144765,-1.90839292296423,13.7902182540695));
#443129=CARTESIAN_POINT('',(1.90060378598597,-1.89443804601159,12.5893111709658));
#443130=CARTESIAN_POINT('',(1.90060378598597,-1.89443804601159,12.5));
#443131=CARTESIAN_POINT('',(1.95262037949676,-1.91647980814857,12.5369868989719));
#443132=CARTESIAN_POINT('Ctrl Pts',(1.90060378598597,-1.89443804601159,
12.5893111709658));
#443133=CARTESIAN_POINT('Ctrl Pts',(1.91795555014392,-1.90179076621899,
12.5718848856037));
#443134=CARTESIAN_POINT('Ctrl Pts',(1.93529416090636,-1.90913791274315,
12.5544431401645));
#443135=CARTESIAN_POINT('Ctrl Pts',(1.95262037949676,-1.91647980814857,
12.5369868989719));
#443136=CARTESIAN_POINT('',(1.95262037949676,-1.91647980814857,12.5));
#443137=CARTESIAN_POINT('Origin',(1.88719198339501,-1.9260887043975,12.5));
#443138=CARTESIAN_POINT('',(1.86234798118716,-1.90233232153995,13.8587068136939));
#443139=CARTESIAN_POINT('Ctrl Pts',(1.90060378598842,-1.89443804600545,
13.8235269408542));
#443140=CARTESIAN_POINT('Ctrl Pts',(1.89899036356686,-1.89375436660929,
13.8262006681044));
#443141=CARTESIAN_POINT('Ctrl Pts',(1.89727147504902,-1.8932146905071,13.8288634856214));
#443142=CARTESIAN_POINT('Ctrl Pts',(1.89545613020484,-1.89280918763816,
13.8314912288862));
#443143=CARTESIAN_POINT('Ctrl Pts',(1.89358469691463,-1.89239115600596,
13.8342001611531));
#443144=CARTESIAN_POINT('Ctrl Pts',(1.89160878444647,-1.89211476749012,
13.8368750301949));
#443145=CARTESIAN_POINT('Ctrl Pts',(1.88951018751899,-1.89200467637456,
13.8394886372969));
#443146=CARTESIAN_POINT('Ctrl Pts',(1.88934810778779,-1.89199617377066,
13.8396904925131));
#443147=CARTESIAN_POINT('Ctrl Pts',(1.8891852913088,-1.8919886846927,13.8398919674349));
#443148=CARTESIAN_POINT('Ctrl Pts',(1.88902172812506,-1.89198223183418,
13.8400930404591));
#443149=CARTESIAN_POINT('Ctrl Pts',(1.88647330368247,-1.89188169195719,
13.8432258934518));
#443150=CARTESIAN_POINT('Ctrl Pts',(1.88375665920809,-1.89203209037069,
13.8462331177034));
#443151=CARTESIAN_POINT('Ctrl Pts',(1.88096572941233,-1.8925248406916,13.8489036603661));
#443152=CARTESIAN_POINT('Ctrl Pts',(1.88005250470348,-1.89268607433102,
13.849777493004));
#443153=CARTESIAN_POINT('Ctrl Pts',(1.87913155618036,-1.89288406118488,
13.85061494757));
#443154=CARTESIAN_POINT('Ctrl Pts',(1.87820683548238,-1.89312227402315,
13.8514076489583));
#443155=CARTESIAN_POINT('Ctrl Pts',(1.87625091784147,-1.89362612853153,
13.8530843267192));
#443156=CARTESIAN_POINT('Ctrl Pts',(1.87408673940969,-1.89436230366186,
13.8546805203176));
#443157=CARTESIAN_POINT('Ctrl Pts',(1.87188384953468,-1.89541724870127,
13.8559412814273));
#443158=CARTESIAN_POINT('Ctrl Pts',(1.871589031428,-1.89555843456022,13.8561100121513));
#443159=CARTESIAN_POINT('Ctrl Pts',(1.87129353957594,-1.89570525567038,
13.8562727473908));
#443160=CARTESIAN_POINT('Ctrl Pts',(1.87099779044625,-1.89585784407755,
13.8564289040185));
#443161=CARTESIAN_POINT('Ctrl Pts',(1.86965657151709,-1.89654983076329,
13.8571370725437));
#443162=CARTESIAN_POINT('Ctrl Pts',(1.86828753026721,-1.89737461461124,
13.8577210840554));
#443163=CARTESIAN_POINT('Ctrl Pts',(1.86695902634548,-1.89832527461257,
13.8581177131616));
#443164=CARTESIAN_POINT('Ctrl Pts',(1.8665848739154,-1.89859301318967,13.8582294175695));
#443165=CARTESIAN_POINT('Ctrl Pts',(1.86621386376566,-1.89887057411389,
13.8583265086086));
#443166=CARTESIAN_POINT('Ctrl Pts',(1.86584731855342,-1.89915741361026,
13.8584082369006));
#443167=CARTESIAN_POINT('Ctrl Pts',(1.86532069137642,-1.89956952504748,
13.8585256585398));
#443168=CARTESIAN_POINT('Ctrl Pts',(1.86479693277076,-1.900006167457,13.8586122832068));
#443169=CARTESIAN_POINT('Ctrl Pts',(1.86429015413323,-1.90045660468811,
13.8586682984299));
#443170=CARTESIAN_POINT('Ctrl Pts',(1.86388478145856,-1.90081690982259,
13.8587131050557));
#443171=CARTESIAN_POINT('Ctrl Pts',(1.86348564015117,-1.90118984576816,
13.8587357943552));
#443172=CARTESIAN_POINT('Ctrl Pts',(1.86309302853961,-1.90157582689289,
13.8587355499465));
#443173=CARTESIAN_POINT('Ctrl Pts',(1.86283927429476,-1.90182529569603,
13.8587353919793));
#443174=CARTESIAN_POINT('Ctrl Pts',(1.86259096468191,-1.90207748862114,
13.8587257282814));
#443175=CARTESIAN_POINT('Ctrl Pts',(1.86234798118716,-1.90233232153995,
13.8587068136939));
#443176=CARTESIAN_POINT('Ctrl Pts',(1.86234798118716,-1.90233232153995,
13.8587068136939));
#443177=CARTESIAN_POINT('Ctrl Pts',(1.86154882171938,-1.90317045311751,
13.8586446046466));
#443178=CARTESIAN_POINT('Ctrl Pts',(1.86080720417558,-1.90403710728445,
13.858482427929));
#443179=CARTESIAN_POINT('Ctrl Pts',(1.86011954075697,-1.90492961689678,
13.8582284286032));
#443180=CARTESIAN_POINT('Ctrl Pts',(1.85941407808175,-1.90584522793806,
13.8579678548414));
#443181=CARTESIAN_POINT('Ctrl Pts',(1.85876488877565,-1.9067912216214,13.857615680862));
#443182=CARTESIAN_POINT('Ctrl Pts',(1.8581895772962,-1.90772482014813,13.8571944833187));
#443183=CARTESIAN_POINT('Ctrl Pts',(1.85675382866118,-1.91005471075223,
13.8561433417727));
#443184=CARTESIAN_POINT('Ctrl Pts',(1.85570695105859,-1.91241387316563,
13.8546163505474));
#443185=CARTESIAN_POINT('Ctrl Pts',(1.85496159012127,-1.91461488518797,
13.8528973491086));
#443186=CARTESIAN_POINT('Ctrl Pts',(1.85482542367479,-1.91501697761155,
13.8525833129072));
#443187=CARTESIAN_POINT('Ctrl Pts',(1.8546991803538,-1.91541381357007,13.8522628768812));
#443188=CARTESIAN_POINT('Ctrl Pts',(1.85458215730419,-1.91580430500278,
13.851937733538));
#443189=CARTESIAN_POINT('Ctrl Pts',(1.85386751377646,-1.91818898200413,
13.8499521282529));
#443190=CARTESIAN_POINT('Ctrl Pts',(1.85342961326282,-1.92057521058686,
13.847639871647));
#443191=CARTESIAN_POINT('Ctrl Pts',(1.85321244905911,-1.92282307810641,
13.8452109780794));
#443192=CARTESIAN_POINT('Ctrl Pts',(1.85311474238879,-1.92383444023199,
13.8441181685877));
#443193=CARTESIAN_POINT('Ctrl Pts',(1.85306102483953,-1.92481797643773,
13.8430021611332));
#443194=CARTESIAN_POINT('Ctrl Pts',(1.85304341249069,-1.92576273352262,
13.8418824960098));
#443195=CARTESIAN_POINT('Ctrl Pts',(1.85300190854089,-1.92798907771841,
13.8392439765549));
#443196=CARTESIAN_POINT('Ctrl Pts',(1.85315513875739,-1.93010643141176,
13.8364981347964));
#443197=CARTESIAN_POINT('Ctrl Pts',(1.85346937710656,-1.93212286422562,
13.8336931113419));
#443198=CARTESIAN_POINT('Ctrl Pts',(1.85377542530267,-1.934086741731,13.8309611966328));
#443199=CARTESIAN_POINT('Ctrl Pts',(1.85423506251094,-1.93595677156332,
13.8281701127185));
#443200=CARTESIAN_POINT('Ctrl Pts',(1.85485110038221,-1.93772064472228,
13.825358068512));
#443201=CARTESIAN_POINT('Ctrl Pts',(1.85498465805755,-1.93810305432676,
13.8247484142932));
#443202=CARTESIAN_POINT('Ctrl Pts',(1.85512567088447,-1.93848033572744,
13.8241378483365));
#443203=CARTESIAN_POINT('Ctrl Pts',(1.85527432946228,-1.93885208923186,
13.8235269408515));
#443204=CARTESIAN_POINT('',(1.86322244697428,-1.90145022945566,12.5969504640361));
#443205=CARTESIAN_POINT('Origin',(1.88721499861276,-1.92611247375935,12.584524458991));
#443206=CARTESIAN_POINT('Origin',(1.88721499861276,-1.92611247375935,12.584524458991));
#443207=CARTESIAN_POINT('Ctrl Pts',(1.90060378598597,-1.89443804601159,
12.5893111709658));
#443208=CARTESIAN_POINT('Ctrl Pts',(1.89016808342412,-1.89001597109135,
12.5770542771492));
#443209=CARTESIAN_POINT('Ctrl Pts',(1.8810859464595,-1.90362914349938,12.5737548217797));
#443210=CARTESIAN_POINT('Ctrl Pts',(1.92342316516287,-1.90410763976972,
12.5663937883685));
#443211=CARTESIAN_POINT('Ctrl Pts',(1.91297415041314,-1.89967992387878,
12.5540940315304));
#443212=CARTESIAN_POINT('Ctrl Pts',(1.90386654101103,-1.91333706290175,
12.5508374392248));
#443213=CARTESIAN_POINT('Ctrl Pts',(1.94621951986594,-1.91376747702629,
12.5434499600945));
#443214=CARTESIAN_POINT('Ctrl Pts',(1.9357365316482,-1.90932536505424,12.5311293540533));
#443215=CARTESIAN_POINT('Ctrl Pts',(1.92662534098664,-1.92303441204117,
12.5278936106989));
#443216=CARTESIAN_POINT('Ctrl Pts',(1.96899465363369,-1.9234183220214,12.5204817579905));
#443217=CARTESIAN_POINT('Ctrl Pts',(1.95845978178843,-1.91895422463086,
12.5081597038247));
#443218=CARTESIAN_POINT('Ctrl Pts',(1.94936404577731,-1.93272199973472,
12.5049254088044));
#443219=CARTESIAN_POINT('Ctrl Pts',(1.95262037949676,-1.91647980814857,
12.5369868989719));
#443220=CARTESIAN_POINT('Ctrl Pts',(1.95347805913806,-1.916843245631,12.5342545179733));
#443221=CARTESIAN_POINT('Ctrl Pts',(1.95424791832307,-1.91730495327509,
12.5314872231885));
#443222=CARTESIAN_POINT('Ctrl Pts',(1.95485783841868,-1.91788686270714,
12.5287124745063));
#443223=CARTESIAN_POINT('Ctrl Pts',(1.95540789463462,-1.91841165751637,
12.5262100684184));
#443224=CARTESIAN_POINT('Ctrl Pts',(1.95582663314767,-1.91903439855037,
12.5237004536639));
#443225=CARTESIAN_POINT('Ctrl Pts',(1.9560662331057,-1.91980276853386,12.5212220730815));
#443226=CARTESIAN_POINT('Ctrl Pts',(1.95624966760063,-1.92039102222554,
12.5193246583486));
#443227=CARTESIAN_POINT('Ctrl Pts',(1.95632969141146,-1.92107185172901,
12.517417831369));
#443228=CARTESIAN_POINT('Ctrl Pts',(1.95621387557143,-1.92187543831097,
12.5155812248347));
#443229=CARTESIAN_POINT('Ctrl Pts',(1.95616453740107,-1.92221777051417,
12.5147988205793));
#443230=CARTESIAN_POINT('Ctrl Pts',(1.95607988224286,-1.92258276777569,
12.5140295443047));
#443231=CARTESIAN_POINT('Ctrl Pts',(1.95595433230324,-1.9229742009954,12.5132817086137));
#443232=CARTESIAN_POINT('Ctrl Pts',(1.95576432945362,-1.92356658222155,
12.5121499604604));
#443233=CARTESIAN_POINT('Ctrl Pts',(1.95546975345786,-1.92423011677195,
12.5110494206568));
#443234=CARTESIAN_POINT('Ctrl Pts',(1.95503351465517,-1.92496144967886,
12.5100666561695));
#443235=CARTESIAN_POINT('Ctrl Pts',(1.95478302733923,-1.92538137934989,
12.5095023550641));
#443236=CARTESIAN_POINT('Ctrl Pts',(1.95448237863155,-1.92582817985345,
12.5089719619137));
#443237=CARTESIAN_POINT('Ctrl Pts',(1.95413190484807,-1.92628991074266,
12.5085043804652));
#443238=CARTESIAN_POINT('Ctrl Pts',(1.95361903211837,-1.92696559375433,
12.5078201359222));
#443239=CARTESIAN_POINT('Ctrl Pts',(1.95298362435897,-1.92769211628802,
12.5072563000949));
#443240=CARTESIAN_POINT('Ctrl Pts',(1.9522623802275,-1.92841465742125,12.5068768744332));
#443241=CARTESIAN_POINT('Ctrl Pts',(1.9517423135581,-1.92893565931821,12.5066032824114));
#443242=CARTESIAN_POINT('Ctrl Pts',(1.95116852281845,-1.9294637867723,12.5064197834844));
#443243=CARTESIAN_POINT('Ctrl Pts',(1.95057480049822,-1.92997144965625,
12.5063282718343));
#443244=CARTESIAN_POINT('Ctrl Pts',(1.94970814972246,-1.93071248029835,
12.5061946931565));
#443245=CARTESIAN_POINT('Ctrl Pts',(1.94878119746672,-1.93142655312066,
12.5062515701262));
#443246=CARTESIAN_POINT('Ctrl Pts',(1.94786090948263,-1.93208160246618,
12.5064436508398));
#443247=CARTESIAN_POINT('',(1.8810859464595,-1.90362914349938,12.5737548217797));
#443248=CARTESIAN_POINT('Origin',(1.89202023232776,-1.91469446737857,12.5893111709658));
#443249=CARTESIAN_POINT('Ctrl Pts',(1.94786090948263,-1.93208160246617,
12.5064436508398));
#443250=CARTESIAN_POINT('Ctrl Pts',(1.93797629177169,-1.92787034131781,
12.5164271754438));
#443251=CARTESIAN_POINT('Ctrl Pts',(1.92808783769337,-1.92365721860872,
12.5264061185523));
#443252=CARTESIAN_POINT('Ctrl Pts',(1.91819541176305,-1.91944216964704,
12.536380305637));
#443253=CARTESIAN_POINT('Ctrl Pts',(1.90583188575032,-1.91417421334899,
12.5488460165097));
#443254=CARTESIAN_POINT('Ctrl Pts',(1.89346215208989,-1.90890324667937,
12.5613043021964));
#443255=CARTESIAN_POINT('Ctrl Pts',(1.8810859464595,-1.90362914349938,12.5737548217797));
#443256=CARTESIAN_POINT('Ctrl Pts',(1.85527432946227,-1.93885208923186,
12.5893111709658));
#443257=CARTESIAN_POINT('Ctrl Pts',(1.85106604772008,-1.92832835418493,
12.5770542771492));
#443258=CARTESIAN_POINT('Ctrl Pts',(1.86486164992115,-1.91952579576338,
12.5737548217797));
#443259=CARTESIAN_POINT('Ctrl Pts',(1.85134803919851,-1.92903353596369,
12.5928319619712));
#443260=CARTESIAN_POINT('Ctrl Pts',(1.85154467214355,-1.92075134109419,
12.5821634970842));
#443261=CARTESIAN_POINT('Ctrl Pts',(1.86342263330893,-1.91595263909747,
12.5773203894503));
#443262=CARTESIAN_POINT('Ctrl Pts',(1.85218258595468,-1.9123036934345,12.5969440695591));
#443263=CARTESIAN_POINT('Ctrl Pts',(1.85504101697285,-1.90947740352257,
12.5878292599214));
#443264=CARTESIAN_POINT('Ctrl Pts',(1.86372212623972,-1.90998988377111,
12.5813877129824));
#443265=CARTESIAN_POINT('Ctrl Pts',(1.87399969621371,-1.89085167848282,
12.596957478804));
#443266=CARTESIAN_POINT('Ctrl Pts',(1.87116244612653,-1.89365713835452,
12.5878468778671));
#443267=CARTESIAN_POINT('Ctrl Pts',(1.87153495466706,-1.90231616366485,
12.5814011370086));
#443268=CARTESIAN_POINT('Ctrl Pts',(1.89085322899608,-1.89030629797944,
12.5928371701607));
#443269=CARTESIAN_POINT('Ctrl Pts',(1.88257470672739,-1.89033998403904,
12.5821692192952));
#443270=CARTESIAN_POINT('Ctrl Pts',(1.87753165565631,-1.90211247136596,
12.5773318885715));
#443271=CARTESIAN_POINT('Ctrl Pts',(1.90060378598599,-1.89443804601154,
12.5893111709658));
#443272=CARTESIAN_POINT('Ctrl Pts',(1.89016808342414,-1.8900159710913,12.5770542771492));
#443273=CARTESIAN_POINT('Ctrl Pts',(1.88108594645952,-1.90362914349933,
12.5737548217797));
#443274=CARTESIAN_POINT('',(1.86486164992115,-1.91952579576338,12.5737548217797));
#443275=CARTESIAN_POINT('Origin',(1.87570162797923,-1.93068352293787,12.5893111709658));
#443276=CARTESIAN_POINT('Ctrl Pts',(1.88108594645952,-1.90362914349933,
12.5737548217797));
#443277=CARTESIAN_POINT('Ctrl Pts',(1.88017645726634,-1.90320825273144,
12.5746934679442));
#443278=CARTESIAN_POINT('Ctrl Pts',(1.87909311232341,-1.90290875452966,
12.5756680099006));
#443279=CARTESIAN_POINT('Ctrl Pts',(1.87796005283771,-1.90276151367305,
12.5765688348656));
#443280=CARTESIAN_POINT('Ctrl Pts',(1.87766008788226,-1.90272253328627,
12.5768073183026));
#443281=CARTESIAN_POINT('Ctrl Pts',(1.87735673277619,-1.90269398490945,
12.5770407398754));
#443282=CARTESIAN_POINT('Ctrl Pts',(1.87705235893604,-1.9026758821933,12.5772674179684));
#443283=CARTESIAN_POINT('Ctrl Pts',(1.8758032910022,-1.9026015935414,12.5781976435658));
#443284=CARTESIAN_POINT('Ctrl Pts',(1.87446545326703,-1.90271025667737,
12.5790594849312));
#443285=CARTESIAN_POINT('Ctrl Pts',(1.87313308795987,-1.90304266517898,
12.5797571720116));
#443286=CARTESIAN_POINT('Ctrl Pts',(1.87226500405466,-1.90325924127013,
12.580211740231));
#443287=CARTESIAN_POINT('Ctrl Pts',(1.87136433750344,-1.90359885390805,
12.5806009430798));
#443288=CARTESIAN_POINT('Ctrl Pts',(1.87050074210857,-1.90405417320073,
12.5808812374708));
#443289=CARTESIAN_POINT('Ctrl Pts',(1.8697586271696,-1.90444544352375,12.5811221033394));
#443290=CARTESIAN_POINT('Ctrl Pts',(1.86902874762281,-1.904930268853,12.581287365893));
#443291=CARTESIAN_POINT('Ctrl Pts',(1.86835691251821,-1.9054882302098,12.581359338449));
#443292=CARTESIAN_POINT('Ctrl Pts',(1.86826354131154,-1.90556577531693,
12.5813693411482));
#443293=CARTESIAN_POINT('Ctrl Pts',(1.86817123982759,-1.90564470238592,
12.5813775999465));
#443294=CARTESIAN_POINT('Ctrl Pts',(1.86808007780993,-1.90572492611198,
12.5813841266931));
#443295=CARTESIAN_POINT('Ctrl Pts',(1.86792541042117,-1.9058610353661,12.5813952001081));
#443296=CARTESIAN_POINT('Ctrl Pts',(1.86777338936446,-1.90600224575675,
12.5814007534795));
#443297=CARTESIAN_POINT('Ctrl Pts',(1.86762421506604,-1.90614864027351,
12.5814005856065));
#443298=CARTESIAN_POINT('Ctrl Pts',(1.86694135345125,-1.9068187771347,12.5813998171494));
#443299=CARTESIAN_POINT('Ctrl Pts',(1.86636508834534,-1.90755100259751,
12.58127954464));
#443300=CARTESIAN_POINT('Ctrl Pts',(1.86587543933797,-1.90832286006927,
12.5810700125799));
#443301=CARTESIAN_POINT('Ctrl Pts',(1.86528399908806,-1.90925517601214,
12.5808169217085));
#443302=CARTESIAN_POINT('Ctrl Pts',(1.86483300952404,-1.91025436406882,
12.5804173076348));
#443303=CARTESIAN_POINT('Ctrl Pts',(1.86453825807857,-1.91122214346158,
12.5799304713245));
#443304=CARTESIAN_POINT('Ctrl Pts',(1.86417296818135,-1.91242152701115,
12.5793271277669));
#443305=CARTESIAN_POINT('Ctrl Pts',(1.86399418173403,-1.91363768827293,
12.5785808224116));
#443306=CARTESIAN_POINT('Ctrl Pts',(1.86397805533941,-1.91481475063423,
12.5777485681082));
#443307=CARTESIAN_POINT('Ctrl Pts',(1.86395402524464,-1.91656870250939,
12.576508418016));
#443308=CARTESIAN_POINT('Ctrl Pts',(1.86428450055372,-1.91822097536242,
12.5750928681475));
#443309=CARTESIAN_POINT('Ctrl Pts',(1.86486164992115,-1.91952579576338,
12.5737548217797));
#443310=CARTESIAN_POINT('Ctrl Pts',(1.86486164992115,-1.91952579576338,
12.5737548217797));
#443311=CARTESIAN_POINT('Ctrl Pts',(1.85106604772008,-1.92832835418493,
12.5770542771492));
#443312=CARTESIAN_POINT('Ctrl Pts',(1.85527432946227,-1.93885208923186,
12.5893111709658));
#443313=CARTESIAN_POINT('Ctrl Pts',(1.87410147022428,-1.94249622621072,
12.5508408821982));
#443314=CARTESIAN_POINT('Ctrl Pts',(1.86026139638963,-1.95132334810186,
12.55409748406));
#443315=CARTESIAN_POINT('Ctrl Pts',(1.86447504682153,-1.96186050873944,
12.5663972313419));
#443316=CARTESIAN_POINT('Ctrl Pts',(1.88333117008723,-1.96544465762183,
12.52790050457));
#443317=CARTESIAN_POINT('Ctrl Pts',(1.86943913377784,-1.97427430113219,
12.5311362602938));
#443318=CARTESIAN_POINT('Ctrl Pts',(1.87366648216885,-1.9848457165325,12.5434568539655));
#443319=CARTESIAN_POINT('Ctrl Pts',(1.89255152315046,-1.98837280477215,
12.5049357605811));
#443320=CARTESIAN_POINT('Ctrl Pts',(1.87860109577067,-1.99718580431321,
12.5081700652078));
#443321=CARTESIAN_POINT('Ctrl Pts',(1.88284936247329,-2.00780953055728,
12.5204921097672));
#443322=CARTESIAN_POINT('Ctrl Pts',(1.89194607715313,-1.98686725334684,
12.5064436508395));
#443323=CARTESIAN_POINT('Ctrl Pts',(1.89121837489207,-1.98784669053719,
12.5062361689309));
#443324=CARTESIAN_POINT('Ctrl Pts',(1.89041985871306,-1.98883419422443,
12.5061871075062));
#443325=CARTESIAN_POINT('Ctrl Pts',(1.88959444843154,-1.98974508088492,
12.5063648335164));
#443326=CARTESIAN_POINT('Ctrl Pts',(1.88921949616825,-1.99015886179194,
12.5064455676329));
#443327=CARTESIAN_POINT('Ctrl Pts',(1.88883360114652,-1.99056245593942,
12.506574497099));
#443328=CARTESIAN_POINT('Ctrl Pts',(1.88845254978506,-1.99093783212991,
12.5067492519495));
#443329=CARTESIAN_POINT('Ctrl Pts',(1.88768681228283,-1.99169216515579,
12.5071004286051));
#443330=CARTESIAN_POINT('Ctrl Pts',(1.88691191406805,-1.99235970551328,
12.5076537929613));
#443331=CARTESIAN_POINT('Ctrl Pts',(1.88619218858864,-1.99289751689347,
12.5083435010505));
#443332=CARTESIAN_POINT('Ctrl Pts',(1.88614687756862,-1.99293137533383,
12.5083869222964));
#443333=CARTESIAN_POINT('Ctrl Pts',(1.8861017731379,-1.99296471373106,12.5084308732337));
#443334=CARTESIAN_POINT('Ctrl Pts',(1.88605688625536,-1.99299751933776,
12.5084753333615));
#443335=CARTESIAN_POINT('Ctrl Pts',(1.885696834212,-1.99326066360302,12.5088319622689));
#443336=CARTESIAN_POINT('Ctrl Pts',(1.8853442311366,-1.99349591111127,12.509227847131));
#443337=CARTESIAN_POINT('Ctrl Pts',(1.88501111576401,-1.99369859596769,
12.5096423454524));
#443338=CARTESIAN_POINT('Ctrl Pts',(1.88396727961702,-1.99433372060314,
12.5109411997424));
#443339=CARTESIAN_POINT('Ctrl Pts',(1.88305561986995,-1.99469643067363,
12.5124831113042));
#443340=CARTESIAN_POINT('Ctrl Pts',(1.88227284260661,-1.99488130422901,
12.5140723025008));
#443341=CARTESIAN_POINT('Ctrl Pts',(1.88219949551968,-1.99489862708363,
12.5142212114565));
#443342=CARTESIAN_POINT('Ctrl Pts',(1.88212726864014,-1.994914415891,12.5143705582413));
#443343=CARTESIAN_POINT('Ctrl Pts',(1.88205615419293,-1.99492876466862,
12.5145201959299));
#443344=CARTESIAN_POINT('Ctrl Pts',(1.88114258324015,-1.99511309608021,
12.5164425148273));
#443345=CARTESIAN_POINT('Ctrl Pts',(1.88038342111312,-1.9950766180836,12.518463520594));
#443346=CARTESIAN_POINT('Ctrl Pts',(1.87972909895249,-1.99489470246884,
12.5205025929157));
#443347=CARTESIAN_POINT('Ctrl Pts',(1.87934956616441,-1.99478918420182,
12.5216853356836));
#443348=CARTESIAN_POINT('Ctrl Pts',(1.87900586242571,-1.99463539052657,
12.5228750347131));
#443349=CARTESIAN_POINT('Ctrl Pts',(1.87869344376144,-1.99445099305703,
12.5240609649613));
#443350=CARTESIAN_POINT('Ctrl Pts',(1.87792662891068,-1.99399839936065,
12.5269717671327));
#443351=CARTESIAN_POINT('Ctrl Pts',(1.877331987757,-1.99333974855292,12.5299036066169));
#443352=CARTESIAN_POINT('Ctrl Pts',(1.87685537220185,-1.99254269790286,
12.532813300402));
#443353=CARTESIAN_POINT('Ctrl Pts',(1.8766265689829,-1.99216006717997,12.5342101228452));
#443354=CARTESIAN_POINT('Ctrl Pts',(1.87642570073608,-1.99174574984497,
12.5356023438238));
#443355=CARTESIAN_POINT('Ctrl Pts',(1.87625044290219,-1.99130747926497,
12.5369868989719));
#443356=CARTESIAN_POINT('Origin',(6.6038514439667,-13.8279828798786,-1.24062368834839));
#443357=CARTESIAN_POINT('Ctrl Pts',(1.95258191307926,-1.91646346508713,
12.5369868989719));
#443358=CARTESIAN_POINT('Ctrl Pts',(1.96669379917423,-1.92247495196876,
12.5369868989719));
#443359=CARTESIAN_POINT('Ctrl Pts',(1.97721412737488,-1.9113122462826,12.5369868989719));
#443360=CARTESIAN_POINT('Ctrl Pts',(1.95735230844105,-1.91849552184576,
12.5218025310016));
#443361=CARTESIAN_POINT('Ctrl Pts',(1.96908740451166,-1.91988957489999,
12.5216901060418));
#443362=CARTESIAN_POINT('Ctrl Pts',(1.97718206992965,-1.91134628521992,
12.5161920673677));
#443363=CARTESIAN_POINT('Ctrl Pts',(1.95866847427007,-1.92437801950455,
12.5042015548895));
#443364=CARTESIAN_POINT('Ctrl Pts',(1.96508584297928,-1.92393674423044,
12.4980677368513));
#443365=CARTESIAN_POINT('Ctrl Pts',(1.96983613301335,-1.91907613477113,
12.4907278922778));
#443366=CARTESIAN_POINT('Ctrl Pts',(1.94784670917394,-1.93206751720659,
12.506463626192));
#443367=CARTESIAN_POINT('Ctrl Pts',(1.95249190125991,-1.93667507934082,
12.4999376786891));
#443368=CARTESIAN_POINT('Ctrl Pts',(1.95243516699269,-1.93661880466874,
12.4906970594712));
#443369=CARTESIAN_POINT('Origin',(1.96120393315497,-1.8962233867816,12.5369868989719));
#443370=CARTESIAN_POINT('Origin',(1.96120393315497,-1.8962233867816,14.));
#443371=CARTESIAN_POINT('Origin',(1.96120393315497,-1.8962233867816,13.7435492065112));
#443372=CARTESIAN_POINT('Ctrl Pts',(1.92982261285273,-1.90681934310076,
13.793642941384));
#443373=CARTESIAN_POINT('Ctrl Pts',(1.93976736345518,-1.9110629446915,13.8071662555867));
#443374=CARTESIAN_POINT('Ctrl Pts',(1.94868154685581,-1.89655237206551,
13.8103758687955));
#443375=CARTESIAN_POINT('Ctrl Pts',(1.94512645060691,-1.91330426832906,
13.7804579775006));
#443376=CARTESIAN_POINT('Ctrl Pts',(1.95740135403334,-1.91853116201464,
13.7901904343352));
#443377=CARTESIAN_POINT('Ctrl Pts',(1.96771222574423,-1.90661722694993,
13.7927914348263));
#443378=CARTESIAN_POINT('Ctrl Pts',(1.95413639585587,-1.91712218783116,
13.7597120340895));
#443379=CARTESIAN_POINT('Ctrl Pts',(1.9683441610124,-1.9231659035119,13.7635825532445));
#443380=CARTESIAN_POINT('Ctrl Pts',(1.97894654617859,-1.91252986360357,
13.7651073818884));
#443381=CARTESIAN_POINT('Ctrl Pts',(1.95237204227213,-1.91637455177148,
13.7381884353898));
#443382=CARTESIAN_POINT('Ctrl Pts',(1.96624689637753,-1.92227763013618,
13.7368803041982));
#443383=CARTESIAN_POINT('Ctrl Pts',(1.97674676259257,-1.91137155629702,
13.7363986145813));
#443384=CARTESIAN_POINT('Origin',(1.94211960510586,-1.88813650159725,13.7902182540695));
#443385=CARTESIAN_POINT('Ctrl Pts',(1.90060016204145,-1.89443650955962,
13.8235227101244));
#443386=CARTESIAN_POINT('Ctrl Pts',(1.91118432040462,-1.89892630688945,
13.8358800583119));
#443387=CARTESIAN_POINT('Ctrl Pts',(1.92028864223977,-1.88507938040814,
13.8390832900376));
#443388=CARTESIAN_POINT('Ctrl Pts',(1.91158243810205,-1.89909019216838,
13.8124254819053));
#443389=CARTESIAN_POINT('Ctrl Pts',(1.92218715085937,-1.90358870836491,
13.8247886449157));
#443390=CARTESIAN_POINT('Ctrl Pts',(1.93128873470291,-1.8897149218363,13.8279860620657));
#443391=CARTESIAN_POINT('Ctrl Pts',(1.92255979226383,-1.90374178914802,
13.8013225099955));
#443392=CARTESIAN_POINT('Ctrl Pts',(1.93318005491093,-1.90824690347943,
13.8136962257787));
#443393=CARTESIAN_POINT('Ctrl Pts',(1.94228362940331,-1.89434856701984,
13.8168830918626));
#443394=CARTESIAN_POINT('Ctrl Pts',(1.93353241603026,-1.90839138164714,
13.7902140179785));
#443395=CARTESIAN_POINT('Ctrl Pts',(1.94416355114511,-1.91290111198434,
13.802602731458));
#443396=CARTESIAN_POINT('Ctrl Pts',(1.95327352985902,-1.89898039216267,
13.8057746032558));
#443397=CARTESIAN_POINT('Origin',(1.90918733964419,-1.87418162464462,13.8235269408515));
#443398=CARTESIAN_POINT('Ctrl Pts',(1.85527432946228,-1.93885208923186,
13.8235269408515));
#443399=CARTESIAN_POINT('Ctrl Pts',(1.85965842924394,-1.94981549599689,
13.8362179249168));
#443400=CARTESIAN_POINT('Ctrl Pts',(1.84503555961608,-1.95863789294465,
13.8391868794938));
#443401=CARTESIAN_POINT('Ctrl Pts',(1.85126306899057,-1.92882104925058,
13.8400110824519));
#443402=CARTESIAN_POINT('Ctrl Pts',(1.85160160074639,-1.93888123111336,
13.8494522556837));
#443403=CARTESIAN_POINT('Ctrl Pts',(1.83853848221819,-1.94208791503196,
13.85569149686));
#443404=CARTESIAN_POINT('Ctrl Pts',(1.85193651668582,-1.91254394280478,
13.8586819406588));
#443405=CARTESIAN_POINT('Ctrl Pts',(1.84883638532394,-1.91560093956207,
13.868010383617));
#443406=CARTESIAN_POINT('Ctrl Pts',(1.83980229368401,-1.91507363032288,
13.8744918421245));
#443407=CARTESIAN_POINT('Ctrl Pts',(1.87424956885007,-1.89060768968211,
13.8587686893867));
#443408=CARTESIAN_POINT('Ctrl Pts',(1.8773220695356,-1.88757786007349,13.8680909899357));
#443409=CARTESIAN_POINT('Ctrl Pts',(1.87694877675283,-1.87855804555188,
13.8745789365163));
#443410=CARTESIAN_POINT('Ctrl Pts',(1.89064047068469,-1.89021614273967,
13.8400379222776));
#443411=CARTESIAN_POINT('Ctrl Pts',(1.90068947670203,-1.89075253063221,
13.8494748685453));
#443412=CARTESIAN_POINT('Ctrl Pts',(1.90416144873845,-1.87776382340465,
13.8557104837033));
#443413=CARTESIAN_POINT('Ctrl Pts',(1.90060378598842,-1.89443804600545,
13.8235269408542));
#443414=CARTESIAN_POINT('Ctrl Pts',(1.91147548235422,-1.89904487104231,
13.8362179249195));
#443415=CARTESIAN_POINT('Ctrl Pts',(1.92059432876269,-1.88460500801543,
13.8391868794965));
#443416=CARTESIAN_POINT('Origin',(1.83484703094532,-1.94702065552585,13.8235269408515));
#443417=CARTESIAN_POINT('Ctrl Pts',(1.86855306805532,-1.97205850075201,
13.7902140241682));
#443418=CARTESIAN_POINT('Ctrl Pts',(1.87284499268163,-1.98277941388451,
13.8026027327198));
#443419=CARTESIAN_POINT('Ctrl Pts',(1.85874134473945,-1.99160353123393,
13.8057746032556));
#443420=CARTESIAN_POINT('Ctrl Pts',(1.86412826848003,-1.96099331518913,
13.8013225161808));
#443421=CARTESIAN_POINT('Ctrl Pts',(1.86841579985604,-1.97170326395582,
13.8136962270464));
#443422=CARTESIAN_POINT('Ctrl Pts',(1.85433466124407,-1.9805214350079,13.8168830918628));
#443423=CARTESIAN_POINT('Ctrl Pts',(1.85970156133385,-1.94992335932521,
13.8124254880875));
#443424=CARTESIAN_POINT('Ctrl Pts',(1.86398281315726,-1.96061762684874,
13.8247886461867));
#443425=CARTESIAN_POINT('Ctrl Pts',(1.84992625996228,-1.96943430845097,
13.8279860620656));
#443426=CARTESIAN_POINT('Ctrl Pts',(1.85527286939083,-1.93884844003976,
13.8235227163065));
#443427=CARTESIAN_POINT('Ctrl Pts',(1.85954582345754,-1.94952197960172,
13.8358800595848));
#443428=CARTESIAN_POINT('Ctrl Pts',(1.84551606885698,-1.95834194653172,
13.8390832900376));
#443429=CARTESIAN_POINT('Origin',(1.84812723423304,-1.98023072779073,13.7902182540695));
#443430=CARTESIAN_POINT('Ctrl Pts',(1.87615021872148,-1.99105692092633,
13.7382347919292));
#443431=CARTESIAN_POINT('Ctrl Pts',(1.88177551032358,-2.00505956221734,
13.7369371795942));
#443432=CARTESIAN_POINT('Ctrl Pts',(1.87064331463721,-2.01533662387039,
13.7364597369711));
#443433=CARTESIAN_POINT('Ctrl Pts',(1.87685255190966,-1.99281325861511,
13.7595490285574));
#443434=CARTESIAN_POINT('Ctrl Pts',(1.88261112519184,-2.00715036572127,
13.7633824266926));
#443435=CARTESIAN_POINT('Ctrl Pts',(1.87174320642998,-2.01753217683941,
13.7648920890506));
#443436=CARTESIAN_POINT('Ctrl Pts',(1.87327069113429,-1.98385603261937,
13.7803806590111));
#443437=CARTESIAN_POINT('Ctrl Pts',(1.87825666038903,-1.99625510502802,
13.7901039518744));
#443438=CARTESIAN_POINT('Ctrl Pts',(1.86613915747838,-2.00633734508844,
13.7926933640892));
#443439=CARTESIAN_POINT('Ctrl Pts',(1.86704461746326,-1.96828637436314,
13.7936647693663));
#443440=CARTESIAN_POINT('Ctrl Pts',(1.87108818227528,-1.97831747178844,
13.8072068914933));
#443441=CARTESIAN_POINT('Ctrl Pts',(1.85637763805206,-1.98693397679362,
13.8104111085397));
#443442=CARTESIAN_POINT('Origin',(1.85582314438524,-1.99947604555896,13.7435492065112));
#443443=CARTESIAN_POINT('Origin',(1.85582314438524,-1.99947604555896,14.));
#443444=CARTESIAN_POINT('Origin',(1.85582314438524,-1.99947604555896,12.5369868989719));
#443445=CARTESIAN_POINT('Ctrl Pts',(1.8919334001501,-1.9868539403086,12.506462012331));
#443446=CARTESIAN_POINT('Ctrl Pts',(1.8964424096848,-1.99158917219372,12.4999388158272));
#443447=CARTESIAN_POINT('Ctrl Pts',(1.8963890621888,-1.99153314819065,12.4907030323752));
#443448=CARTESIAN_POINT('Ctrl Pts',(1.88402337332597,-1.99751508746996,
12.5042014951932));
#443449=CARTESIAN_POINT('Ctrl Pts',(1.88345248703998,-2.00391939742223,
12.4980716682127));
#443450=CARTESIAN_POINT('Ctrl Pts',(1.87850056391531,-2.00856741017965,
12.4907355092743));
#443451=CARTESIAN_POINT('Ctrl Pts',(1.87816922398865,-1.99608168704376,
12.5218047446509));
#443452=CARTESIAN_POINT('Ctrl Pts',(1.87932192270261,-2.00783711798486,
12.5216906929434));
#443453=CARTESIAN_POINT('Ctrl Pts',(1.87062222136042,-2.01575456396743,
12.5161988840776));
#443454=CARTESIAN_POINT('Ctrl Pts',(1.87623614791533,-1.99127182183696,
12.5369868989719));
#443455=CARTESIAN_POINT('Ctrl Pts',(1.88195295920137,-2.00549587190157,
12.5369868989719));
#443456=CARTESIAN_POINT('Ctrl Pts',(1.87058881422157,-2.01578478537184,
12.5369868989719));
#443457=CARTESIAN_POINT('Origin',(3.60557045705457E-31,-8.83174710230759E-31,
12.5));
#443458=CARTESIAN_POINT('Origin',(2.00713550187736,-1.78117863747125,12.5));
#443459=CARTESIAN_POINT('',(2.00713550187736,-1.78117863747125,12.5893111709658));
#443460=CARTESIAN_POINT('',(2.00713550187736,-1.78117863747125,13.8235269408515));
#443461=CARTESIAN_POINT('',(2.00713550187736,-1.78117863747125,12.5));
#443462=CARTESIAN_POINT('',(2.02307844558103,-1.81319574610497,13.7902182540695));
#443463=CARTESIAN_POINT('',(2.00713550187736,-1.78117863747125,13.8235269408515));
#443464=CARTESIAN_POINT('',(2.03231742029,-1.8317497385432,13.7435492065112));
#443465=CARTESIAN_POINT('Origin',(2.00192160722038,-1.77070720346282,13.7445212918691));
#443466=CARTESIAN_POINT('',(2.03231742029,-1.8317497385432,12.5369868989719));
#443467=CARTESIAN_POINT('',(2.03231742029,-1.8317497385432,12.5));
#443468=CARTESIAN_POINT('Ctrl Pts',(2.03231742029,-1.8317497385432,12.5369868989719));
#443469=CARTESIAN_POINT('Ctrl Pts',(2.02392956953902,-1.81490499934765,
12.5544431401645));
#443470=CARTESIAN_POINT('Ctrl Pts',(2.01553571957424,-1.79804821234693,
12.5718848856037));
#443471=CARTESIAN_POINT('Ctrl Pts',(2.00713550187736,-1.78117863747125,
12.5893111709658));
#443472=CARTESIAN_POINT('Origin',(2.30980221034265,-1.81951643427433,12.5));
#443473=CARTESIAN_POINT('',(2.10233409235843,-1.75094619151324,13.7435492065112));
#443474=CARTESIAN_POINT('',(2.08265410961905,-1.74444176467848,13.7902182540695));
#443475=CARTESIAN_POINT('Origin',(2.03093851636564,-1.72734925514798,13.741873268045));
#443476=CARTESIAN_POINT('',(2.04869397153158,-1.73321760679108,13.8235269408515));
#443477=CARTESIAN_POINT('',(2.08265410961905,-1.74444176467848,13.7902182540695));
#443478=CARTESIAN_POINT('',(2.04869397153158,-1.73321760679108,12.5893111709658));
#443479=CARTESIAN_POINT('',(2.04869397153158,-1.73321760679108,12.5));
#443480=CARTESIAN_POINT('',(2.10233409235843,-1.75094619151324,12.5369868989719));
#443481=CARTESIAN_POINT('Ctrl Pts',(2.04869397153158,-1.73321760679108,
12.5893111709658));
#443482=CARTESIAN_POINT('Ctrl Pts',(2.06658731408194,-1.73913153156374,
12.5718848856037));
#443483=CARTESIAN_POINT('Ctrl Pts',(2.0844670926967,-1.74504097332299,12.5544431401645));
#443484=CARTESIAN_POINT('Ctrl Pts',(2.10233409235843,-1.75094619151324,
12.5369868989719));
#443485=CARTESIAN_POINT('',(2.10233409235843,-1.75094619151324,12.5));
#443486=CARTESIAN_POINT('Origin',(2.03790661809618,-1.76585613664246,12.5));
#443487=CARTESIAN_POINT('',(2.01120891650976,-1.74420381800956,13.8587068136939));
#443488=CARTESIAN_POINT('Ctrl Pts',(2.04869397153352,-1.73321760678476,
13.8235269408542));
#443489=CARTESIAN_POINT('Ctrl Pts',(2.04703019142421,-1.73266771118102,
13.8262006681044));
#443490=CARTESIAN_POINT('Ctrl Pts',(2.04527303375369,-1.73226993617813,
13.8288634856214));
#443491=CARTESIAN_POINT('Ctrl Pts',(2.0434306770714,-1.73201375004417,13.8314912288862));
#443492=CARTESIAN_POINT('Ctrl Pts',(2.04153139736224,-1.73174964856444,
13.8342001611531));
#443493=CARTESIAN_POINT('Ctrl Pts',(2.03953953134991,-1.73163523491821,
13.8368750301949));
#443494=CARTESIAN_POINT('Ctrl Pts',(2.03743894388263,-1.73169656525377,
13.8394886372968));
#443495=CARTESIAN_POINT('Ctrl Pts',(2.03727671041721,-1.73170130194435,
13.8396904925131));
#443496=CARTESIAN_POINT('Ctrl Pts',(2.03711382526724,-1.73170710884023,
13.8398919674349));
#443497=CARTESIAN_POINT('Ctrl Pts',(2.03695028035863,-1.73171400937099,
13.8400930404591));
#443498=CARTESIAN_POINT('Ctrl Pts',(2.0344021406548,-1.73182152428264,13.8432258934518));
#443499=CARTESIAN_POINT('Ctrl Pts',(2.03170679445772,-1.73219285400258,
13.8462331177034));
#443500=CARTESIAN_POINT('Ctrl Pts',(2.02896531497625,-1.73291145142553,
13.8489036603661));
#443501=CARTESIAN_POINT('Ctrl Pts',(2.02806827098571,-1.73314658486506,
13.8497774930041));
#443502=CARTESIAN_POINT('Ctrl Pts',(2.02716652460944,-1.73341897878829,
13.85061494757));
#443503=CARTESIAN_POINT('Ctrl Pts',(2.02626429740108,-1.73373177231457,
13.8514076489583));
#443504=CARTESIAN_POINT('Ctrl Pts',(2.02435595673476,-1.73439337573422,
13.8530843267192));
#443505=CARTESIAN_POINT('Ctrl Pts',(2.02225898453563,-1.73530350193597,
13.8546805203176));
#443506=CARTESIAN_POINT('Ctrl Pts',(2.02014941240931,-1.73653449270823,
13.8559412814273));
#443507=CARTESIAN_POINT('Ctrl Pts',(2.01986708324376,-1.73669923919554,
13.8561100121513));
#443508=CARTESIAN_POINT('Ctrl Pts',(2.01958454189996,-1.73686965709972,
13.8562727473908));
#443509=CARTESIAN_POINT('Ctrl Pts',(2.01930221422283,-1.73704584408123,
13.8564289040185));
#443510=CARTESIAN_POINT('Ctrl Pts',(2.01802186142799,-1.73784485003235,
13.8571370725437));
#443511=CARTESIAN_POINT('Ctrl Pts',(2.01672460309047,-1.73877847905152,
13.8577210840554));
#443512=CARTESIAN_POINT('Ctrl Pts',(2.01547800727154,-1.73983426121297,
13.8581177131616));
#443513=CARTESIAN_POINT('Ctrl Pts',(2.01512692298241,-1.74013160580855,
13.8582294175695));
#443514=CARTESIAN_POINT('Ctrl Pts',(2.01477977113041,-1.74043848394319,
13.8583265086086));
#443515=CARTESIAN_POINT('Ctrl Pts',(2.01443782564897,-1.74075424584243,
13.8584082369006));
#443516=CARTESIAN_POINT('Ctrl Pts',(2.01394654168844,-1.74120791101673,
13.8585256585398));
#443517=CARTESIAN_POINT('Ctrl Pts',(2.01346011625631,-1.74168579172336,
13.8586122832068));
#443518=CARTESIAN_POINT('Ctrl Pts',(2.01299173869888,-1.7421760373254,13.8586682984299));
#443519=CARTESIAN_POINT('Ctrl Pts',(2.01261708308171,-1.74256818521055,
13.8587131050557));
#443520=CARTESIAN_POINT('Ctrl Pts',(2.01224966762582,-1.74297241396452,
13.8587357943552));
#443521=CARTESIAN_POINT('Ctrl Pts',(2.01188982344196,-1.74338911226008,
13.8587355499465));
#443522=CARTESIAN_POINT('Ctrl Pts',(2.01165724756682,-1.74365843430307,
13.8587353919793));
#443523=CARTESIAN_POINT('Ctrl Pts',(2.01143032024835,-1.74393002761568,
13.8587257282814));
#443524=CARTESIAN_POINT('Ctrl Pts',(2.01120891650976,-1.74420381800956,
13.8587068136939));
#443525=CARTESIAN_POINT('Ctrl Pts',(2.01120891650976,-1.74420381800956,
13.8587068136939));
#443526=CARTESIAN_POINT('Ctrl Pts',(2.0104807316836,-1.74510429968908,13.8586446046466));
#443527=CARTESIAN_POINT('Ctrl Pts',(2.00981222217124,-1.74602851885042,
13.858482427929));
#443528=CARTESIAN_POINT('Ctrl Pts',(2.009199594715,-1.74697410966319,13.8582284286032));
#443529=CARTESIAN_POINT('Ctrl Pts',(2.00857111020862,-1.74794417584149,
13.8579678548414));
#443530=CARTESIAN_POINT('Ctrl Pts',(2.00800118829375,-1.74893993676411,
13.857615680862));
#443531=CARTESIAN_POINT('Ctrl Pts',(2.00750388806282,-1.74991732204527,
13.8571944833187));
#443532=CARTESIAN_POINT('Ctrl Pts',(2.00626282447684,-1.75235648697316,
13.8561433417727));
#443533=CARTESIAN_POINT('Ctrl Pts',(2.00541172391119,-1.75479312971158,
13.8546163505475));
#443534=CARTESIAN_POINT('Ctrl Pts',(2.00484824601392,-1.75704757188396,
13.8528973491086));
#443535=CARTESIAN_POINT('Ctrl Pts',(2.00474530691543,-1.75745942520767,
13.8525833129073));
#443536=CARTESIAN_POINT('Ctrl Pts',(2.00465182947333,-1.75786523072994,
13.8522628768812));
#443537=CARTESIAN_POINT('Ctrl Pts',(2.00456702448517,-1.75826396129958,
13.851937733538));
#443538=CARTESIAN_POINT('Ctrl Pts',(2.00404913218869,-1.76069895356687,
13.8499521282529));
#443539=CARTESIAN_POINT('Ctrl Pts',(2.00380718853504,-1.76311293512796,
13.847639871647));
#443540=CARTESIAN_POINT('Ctrl Pts',(2.00377396899834,-1.76537102395243,
13.8452109780794));
#443541=CARTESIAN_POINT('Ctrl Pts',(2.00375902284116,-1.76638698485467,
13.8441181685877));
#443542=CARTESIAN_POINT('Ctrl Pts',(2.00378565136409,-1.76737162690378,
13.8430021611332));
#443543=CARTESIAN_POINT('Ctrl Pts',(2.003845104092,-1.76831467595735,13.8418824960098));
#443544=CARTESIAN_POINT('Ctrl Pts',(2.0039852059635,-1.77053699513369,13.8392439765549));
#443545=CARTESIAN_POINT('Ctrl Pts',(2.00431051030166,-1.77263481382212,
13.8364981347964));
#443546=CARTESIAN_POINT('Ctrl Pts',(2.00478806104262,-1.77461892377942,
13.8336931113419));
#443547=CARTESIAN_POINT('Ctrl Pts',(2.00525316513704,-1.77655132087521,
13.8309611966328));
#443548=CARTESIAN_POINT('Ctrl Pts',(2.00586369773226,-1.77837766363799,
13.8281701127186));
#443549=CARTESIAN_POINT('Ctrl Pts',(2.00662145782579,-1.78008545484899,
13.8253580685121));
#443550=CARTESIAN_POINT('Ctrl Pts',(2.00678574103186,-1.78045570582664,
13.8247484142933));
#443551=CARTESIAN_POINT('Ctrl Pts',(2.00695703658691,-1.78082023800011,
13.8241378483365));
#443552=CARTESIAN_POINT('Ctrl Pts',(2.00713550187736,-1.78117863747125,
13.8235269408515));
#443553=CARTESIAN_POINT('',(2.01200857389031,-1.7432533839341,12.5969504640361));
#443554=CARTESIAN_POINT('Origin',(2.03793149415634,-1.76587795095981,12.584524458991));
#443555=CARTESIAN_POINT('Origin',(2.03793149415634,-1.76587795095981,12.584524458991));
#443556=CARTESIAN_POINT('Ctrl Pts',(2.04869397153158,-1.73321760679108,
12.5893111709658));
#443557=CARTESIAN_POINT('Ctrl Pts',(2.03793255275058,-1.72966085259946,
12.5770542771492));
#443558=CARTESIAN_POINT('Ctrl Pts',(2.02999023577727,-1.74396900677638,
12.5737548217797));
#443559=CARTESIAN_POINT('Ctrl Pts',(2.07222558276616,-1.74099503452596,
12.5663937883685));
#443560=CARTESIAN_POINT('Ctrl Pts',(2.06145043630097,-1.73743374320043,
12.5540940315304));
#443561=CARTESIAN_POINT('Ctrl Pts',(2.0534863153349,-1.7517877939371,12.5508374392248));
#443562=CARTESIAN_POINT('Ctrl Pts',(2.09573345089345,-1.74876461493159,
12.5434499600945));
#443563=CARTESIAN_POINT('Ctrl Pts',(2.08492327059005,-1.74519174457971,
12.5311293540533));
#443564=CARTESIAN_POINT('Ctrl Pts',(2.07695981126174,-1.75959782246685,
12.5278936106989));
#443565=CARTESIAN_POINT('Ctrl Pts',(2.11921943574361,-1.75652696270004,
12.5204817579905));
#443566=CARTESIAN_POINT('Ctrl Pts',(2.10835575243537,-1.75293640908167,
12.5081597038247));
#443567=CARTESIAN_POINT('Ctrl Pts',(2.10041248322022,-1.76739975997523,
12.5049254088044));
#443568=CARTESIAN_POINT('Ctrl Pts',(2.10233409235843,-1.75094619151324,
12.5369868989719));
#443569=CARTESIAN_POINT('Ctrl Pts',(2.10321854167028,-1.75123851083435,
12.5342545179733));
#443570=CARTESIAN_POINT('Ctrl Pts',(2.10402347267165,-1.75163593151374,
12.5314872231885));
#443571=CARTESIAN_POINT('Ctrl Pts',(2.10467879432935,-1.75216619054014,
12.5287124745063));
#443572=CARTESIAN_POINT('Ctrl Pts',(2.10526979592752,-1.75264440444987,
12.5262100684184));
#443573=CARTESIAN_POINT('Ctrl Pts',(2.10573790029822,-1.75323094228825,
12.5237004536639));
#443574=CARTESIAN_POINT('Ctrl Pts',(2.10603933229401,-1.75397722596309,
12.5212220730815));
#443575=CARTESIAN_POINT('Ctrl Pts',(2.10627010456274,-1.75454857067487,
12.5193246583486));
#443576=CARTESIAN_POINT('Ctrl Pts',(2.10640535602598,-1.75522061209085,
12.517417831369));
#443577=CARTESIAN_POINT('Ctrl Pts',(2.10635542532018,-1.75603096487088,
12.5155812248348));
#443578=CARTESIAN_POINT('Ctrl Pts',(2.10633415457113,-1.75637617951085,
12.5147988205793));
#443579=CARTESIAN_POINT('Ctrl Pts',(2.10627953176126,-1.75674686245539,
12.5140295443047));
#443580=CARTESIAN_POINT('Ctrl Pts',(2.10618630501999,-1.75714722669898,
12.5132817086137));
#443581=CARTESIAN_POINT('Ctrl Pts',(2.10604521895852,-1.75775312382161,
12.5121499604604));
#443582=CARTESIAN_POINT('Ctrl Pts',(2.1058057073659,-1.7584384611939,12.5110494206568));
#443583=CARTESIAN_POINT('Ctrl Pts',(2.10543053053311,-1.75920291816315,
12.5100666561695));
#443584=CARTESIAN_POINT('Ctrl Pts',(2.10521510485967,-1.75964186759451,
12.5095023550641));
#443585=CARTESIAN_POINT('Ctrl Pts',(2.10495187492468,-1.76011168706704,
12.5089719619137));
#443586=CARTESIAN_POINT('Ctrl Pts',(2.10464020266777,-1.76060044845179,
12.5085043804652));
#443587=CARTESIAN_POINT('Ctrl Pts',(2.10418411091795,-1.76131568707273,
12.5078201359221));
#443588=CARTESIAN_POINT('Ctrl Pts',(2.10361003575668,-1.76209158379383,
12.5072563000949));
#443589=CARTESIAN_POINT('Ctrl Pts',(2.10295008531567,-1.76287050882346,
12.5068768744332));
#443590=CARTESIAN_POINT('Ctrl Pts',(2.10247421561655,-1.76343216739121,
12.5066032824114));
#443591=CARTESIAN_POINT('Ctrl Pts',(2.10194538140866,-1.76400530681686,
12.5064197834844));
#443592=CARTESIAN_POINT('Ctrl Pts',(2.10139501388842,-1.76455967437539,
12.5063282718343));
#443593=CARTESIAN_POINT('Ctrl Pts',(2.10059164769835,-1.76536887938298,
12.5061946931565));
#443594=CARTESIAN_POINT('Ctrl Pts',(2.09972598336392,-1.76615613140112,
12.5062515701262));
#443595=CARTESIAN_POINT('Ctrl Pts',(2.09886215016502,-1.76688401313822,
12.5064436508398));
#443596=CARTESIAN_POINT('',(2.02999023577727,-1.74396900677638,12.5737548217797));
#443597=CARTESIAN_POINT('Origin',(2.04179006533292,-1.75410626589596,12.5893111709658));
#443598=CARTESIAN_POINT('Ctrl Pts',(2.09886215016502,-1.76688401313822,
12.5064436508398));
#443599=CARTESIAN_POINT('Ctrl Pts',(2.08866716582506,-1.76349245272168,
12.5164271754438));
#443600=CARTESIAN_POINT('Ctrl Pts',(2.07846820614843,-1.76009934963816,
12.5264061185523));
#443601=CARTESIAN_POINT('Ctrl Pts',(2.06826513082835,-1.75670465045431,
12.536380305637));
#443602=CARTESIAN_POINT('Ctrl Pts',(2.05551335608489,-1.75246196499368,
12.5488460165097));
#443603=CARTESIAN_POINT('Ctrl Pts',(2.04275514897594,-1.74821678515915,
12.5613043021964));
#443604=CARTESIAN_POINT('Ctrl Pts',(2.02999023577727,-1.74396900677638,
12.5737548217797));
#443605=CARTESIAN_POINT('Ctrl Pts',(2.00713550187736,-1.78117863747125,
12.5893111709658));
#443606=CARTESIAN_POINT('Ctrl Pts',(2.00208344074159,-1.77103293331431,
12.5770542771492));
#443607=CARTESIAN_POINT('Ctrl Pts',(2.01511564898407,-1.76113519502824,
12.5737548217797));
#443608=CARTESIAN_POINT('Ctrl Pts',(2.0024219727782,-1.7717127837355,12.5928319619712));
#443609=CARTESIAN_POINT('Ctrl Pts',(2.00194287567332,-1.76344211977573,
12.5821634970843));
#443610=CARTESIAN_POINT('Ctrl Pts',(2.01339017514108,-1.75769122095944,
12.5773203894503));
#443611=CARTESIAN_POINT('Ctrl Pts',(2.00189010517047,-1.75497058506903,
12.5969440695591));
#443612=CARTESIAN_POINT('Ctrl Pts',(2.00450865612942,-1.75192071073927,
12.5878292599214));
#443613=CARTESIAN_POINT('Ctrl Pts',(2.01320265161924,-1.75172389475533,
12.5813877129824));
#443614=CARTESIAN_POINT('Ctrl Pts',(2.02188608242554,-1.73181165290116,
12.596957478804));
#443615=CARTESIAN_POINT('Ctrl Pts',(2.01928694407814,-1.73483904005842,
12.5878468778671));
#443616=CARTESIAN_POINT('Ctrl Pts',(2.02036400407649,-1.74343889027209,
12.5814011370086));
#443617=CARTESIAN_POINT('Ctrl Pts',(2.03863908289381,-1.72989436772409,
12.5928371701607));
#443618=CARTESIAN_POINT('Ctrl Pts',(2.03039085245162,-1.73060271811505,
12.5821692192952));
#443619=CARTESIAN_POINT('Ctrl Pts',(2.02632414872455,-1.74274708894124,
12.5773318885715));
#443620=CARTESIAN_POINT('Ctrl Pts',(2.0486939715316,-1.73321760679102,12.5893111709658));
#443621=CARTESIAN_POINT('Ctrl Pts',(2.0379325527506,-1.72966085259941,12.5770542771492));
#443622=CARTESIAN_POINT('Ctrl Pts',(2.02999023577729,-1.74396900677632,
12.5737548217797));
#443623=CARTESIAN_POINT('',(2.01511564898407,-1.76113519502824,12.5737548217797));
#443624=CARTESIAN_POINT('Origin',(2.0268290162574,-1.77137223694082,12.5893111709658));
#443625=CARTESIAN_POINT('Ctrl Pts',(2.02999023577729,-1.74396900677632,
12.5737548217797));
#443626=CARTESIAN_POINT('Ctrl Pts',(2.02904946632942,-1.74362364830027,
12.5746934679442));
#443627=CARTESIAN_POINT('Ctrl Pts',(2.02794531424358,-1.74341344932419,
12.5756680099006));
#443628=CARTESIAN_POINT('Ctrl Pts',(2.02680402342312,-1.74335905326627,
12.5765688348656));
#443629=CARTESIAN_POINT('Ctrl Pts',(2.0265018793129,-1.74334465251212,12.5768073183026));
#443630=CARTESIAN_POINT('Ctrl Pts',(2.02619720663819,-1.74334092538503,
12.5770407398754));
#443631=CARTESIAN_POINT('Ctrl Pts',(2.02589237003745,-1.74334769219781,
12.5772674179684));
#443632=CARTESIAN_POINT('Ctrl Pts',(2.02464140305933,-1.74337546136766,
12.5781976435658));
#443633=CARTESIAN_POINT('Ctrl Pts',(2.02331687392322,-1.74359280913131,
12.5790594849312));
#443634=CARTESIAN_POINT('Ctrl Pts',(2.02201603633051,-1.74403271171266,
12.5797571720116));
#443635=CARTESIAN_POINT('Ctrl Pts',(2.02116849386492,-1.74431932406191,
12.580211740231));
#443636=CARTESIAN_POINT('Ctrl Pts',(2.02029850579014,-1.74473121935209,
12.5806009430798));
#443637=CARTESIAN_POINT('Ctrl Pts',(2.01947489668704,-1.7452554146493,12.5808812374708));
#443638=CARTESIAN_POINT('Ctrl Pts',(2.018767143238,-1.74570587230958,12.5811221033394));
#443639=CARTESIAN_POINT('Ctrl Pts',(2.01807921007043,-1.74624857638148,
12.581287365893));
#443640=CARTESIAN_POINT('Ctrl Pts',(2.01745508947216,-1.74685944196594,
12.581359338449));
#443641=CARTESIAN_POINT('Ctrl Pts',(2.0173683495966,-1.74694433966828,12.5813693411482));
#443642=CARTESIAN_POINT('Ctrl Pts',(2.01728278852707,-1.74703052754178,
12.5813775999465));
#443643=CARTESIAN_POINT('Ctrl Pts',(2.01719846882195,-1.74711791488075,
12.5813841266931));
#443644=CARTESIAN_POINT('Ctrl Pts',(2.01705541024395,-1.7472661780706,12.5813952001081));
#443645=CARTESIAN_POINT('Ctrl Pts',(2.01691540498254,-1.74741930972274,
12.5814007534795));
#443646=CARTESIAN_POINT('Ctrl Pts',(2.01677865956146,-1.74757737621402,
12.5814005856065));
#443647=CARTESIAN_POINT('Ctrl Pts',(2.0161526924878,-1.74830094281106,12.5813998171494));
#443648=CARTESIAN_POINT('Ctrl Pts',(2.01563802802936,-1.74907770280997,
12.58127954464));
#443649=CARTESIAN_POINT('Ctrl Pts',(2.01521292183819,-1.74988690292945,
12.5810700125799));
#443650=CARTESIAN_POINT('Ctrl Pts',(2.01469944196147,-1.75086432453896,
12.5808169217085));
#443651=CARTESIAN_POINT('Ctrl Pts',(2.01433139613065,-1.75189694771605,
12.5804173076348));
#443652=CARTESIAN_POINT('Ctrl Pts',(2.01411650845123,-1.75288553188186,
12.5799304713245));
#443653=CARTESIAN_POINT('Ctrl Pts',(2.01385019491983,-1.75411069909943,
12.5793271277669));
#443654=CARTESIAN_POINT('Ctrl Pts',(2.01377113180279,-1.75533738644016,
12.5785808224116));
#443655=CARTESIAN_POINT('Ctrl Pts',(2.01385100057718,-1.75651184667443,
12.5777485681082));
#443656=CARTESIAN_POINT('Ctrl Pts',(2.01397001380129,-1.75826192109522,
12.576508418016));
#443657=CARTESIAN_POINT('Ctrl Pts',(2.01443406505751,-1.75988175934096,
12.5750928681475));
#443658=CARTESIAN_POINT('Ctrl Pts',(2.01511564898407,-1.76113519502824,
12.5737548217797));
#443659=CARTESIAN_POINT('Ctrl Pts',(2.01511564898407,-1.76113519502824,
12.5737548217797));
#443660=CARTESIAN_POINT('Ctrl Pts',(2.00208344074159,-1.77103293331431,
12.5770542771492));
#443661=CARTESIAN_POINT('Ctrl Pts',(2.00713550187736,-1.78117863747125,
12.5893111709658));
#443662=CARTESIAN_POINT('Ctrl Pts',(2.02619702787589,-1.78327606213019,
12.5508408821982));
#443663=CARTESIAN_POINT('Ctrl Pts',(2.01312249812634,-1.79320190700391,
12.55409748406));
#443664=CARTESIAN_POINT('Ctrl Pts',(2.01818100439823,-1.80336055448091,
12.5663972313419));
#443665=CARTESIAN_POINT('Ctrl Pts',(2.03726652687681,-1.80539582830571,
12.52790050457));
#443666=CARTESIAN_POINT('Ctrl Pts',(2.02414041308868,-1.81532842183225,
12.5311362602938));
#443667=CARTESIAN_POINT('Ctrl Pts',(2.02921536382205,-1.82552009358126,
12.5434568539655));
#443668=CARTESIAN_POINT('Ctrl Pts',(2.04832505682313,-1.82749613956558,
12.5049357605811));
#443669=CARTESIAN_POINT('Ctrl Pts',(2.03513938961812,-1.8374169039186,12.5081700652078));
#443670=CARTESIAN_POINT('Ctrl Pts',(2.04023945287848,-1.84765900741473,
12.5204921097672));
#443671=CARTESIAN_POINT('Ctrl Pts',(2.04759890897939,-1.82604494720791,
12.5064436508395));
#443672=CARTESIAN_POINT('Ctrl Pts',(2.04695346131124,-1.82708043989174,
12.5062361689309));
#443673=CARTESIAN_POINT('Ctrl Pts',(2.04623809284699,-1.82812974422357,
12.5061871075061));
#443674=CARTESIAN_POINT('Ctrl Pts',(2.04548967476918,-1.82910487858453,
12.5063648335164));
#443675=CARTESIAN_POINT('Ctrl Pts',(2.04514969711389,-1.82954784476006,
12.5064455676329));
#443676=CARTESIAN_POINT('Ctrl Pts',(2.04479798279581,-1.82998155000805,
12.506574497099));
#443677=CARTESIAN_POINT('Ctrl Pts',(2.04444879599567,-1.8303867363887,12.5067492519495));
#443678=CARTESIAN_POINT('Ctrl Pts',(2.04374709156639,-1.83120097414877,
12.5071004286051));
#443679=CARTESIAN_POINT('Ctrl Pts',(2.04302918249784,-1.83192945471904,
12.5076537929612));
#443680=CARTESIAN_POINT('Ctrl Pts',(2.04235568846594,-1.83252414088437,
12.5083435010503));
#443681=CARTESIAN_POINT('Ctrl Pts',(2.04231328799173,-1.83256157993241,
12.5083869222963));
#443682=CARTESIAN_POINT('Ctrl Pts',(2.04227105103109,-1.83259848382877,
12.5084308732336));
#443683=CARTESIAN_POINT('Ctrl Pts',(2.04222898746737,-1.83263483897522,
12.5084753333615));
#443684=CARTESIAN_POINT('Ctrl Pts',(2.04189158216802,-1.83292645523374,
12.508831962269));
#443685=CARTESIAN_POINT('Ctrl Pts',(2.04155932720612,-1.83318966039935,
12.509227847131));
#443686=CARTESIAN_POINT('Ctrl Pts',(2.04124384094489,-1.83341882283399,
12.5096423454524));
#443687=CARTESIAN_POINT('Ctrl Pts',(2.04025524663057,-1.8341369164811,12.5109411997424));
#443688=CARTESIAN_POINT('Ctrl Pts',(2.03937618459408,-1.83457272839657,
12.5124831113042));
#443689=CARTESIAN_POINT('Ctrl Pts',(2.03861108086855,-1.83482079041435,
12.5140723025008));
#443690=CARTESIAN_POINT('Ctrl Pts',(2.03853938981148,-1.83484403409711,
12.5142212114565));
#443691=CARTESIAN_POINT('Ctrl Pts',(2.0384686901953,-1.83486565752973,12.5143705582413));
#443692=CARTESIAN_POINT('Ctrl Pts',(2.03839898193412,-1.83488575505061,
12.5145201959299));
#443693=CARTESIAN_POINT('Ctrl Pts',(2.03750347553461,-1.83514393762847,
12.5164425148273));
#443694=CARTESIAN_POINT('Ctrl Pts',(2.03674386616156,-1.83516945977046,
12.5184635205941));
#443695=CARTESIAN_POINT('Ctrl Pts',(2.03607689339251,-1.83504148279542,
12.5205025929158));
#443696=CARTESIAN_POINT('Ctrl Pts',(2.03569002275014,-1.83496725107737,
12.5216853356836));
#443697=CARTESIAN_POINT('Ctrl Pts',(2.03533492704499,-1.83484198418337,
12.5228750347131));
#443698=CARTESIAN_POINT('Ctrl Pts',(2.03500851782243,-1.8346836653027,12.5240609649613));
#443699=CARTESIAN_POINT('Ctrl Pts',(2.0342073638969,-1.83429508010361,12.5269717671326));
#443700=CARTESIAN_POINT('Ctrl Pts',(2.03356101520716,-1.83368708967651,
12.5299036066169));
#443701=CARTESIAN_POINT('Ctrl Pts',(2.03302101852352,-1.83293153973917,
12.5328133004019));
#443702=CARTESIAN_POINT('Ctrl Pts',(2.03276178867231,-1.83256883177489,
12.5342101228451));
#443703=CARTESIAN_POINT('Ctrl Pts',(2.03252781808887,-1.83217226567353,
12.5356023438238));
#443704=CARTESIAN_POINT('Ctrl Pts',(2.03231742029,-1.8317497385432,12.5369868989719));
#443705=CARTESIAN_POINT('Origin',(7.70874349513571,-13.2432058369479,-1.24003354080236));
#443706=CARTESIAN_POINT('Ctrl Pts',(2.10229442182352,-1.75093303820211,
12.5369868989719));
#443707=CARTESIAN_POINT('Ctrl Pts',(2.11684934377043,-1.75577427263197,
12.5369868989719));
#443708=CARTESIAN_POINT('Ctrl Pts',(2.12642480230394,-1.7437912055138,12.5369868989719));
#443709=CARTESIAN_POINT('Ctrl Pts',(2.10721457557878,-1.75256950195134,
12.5218025310016));
#443710=CARTESIAN_POINT('Ctrl Pts',(2.119024252351,-1.75300239713597,12.5216901060418));
#443711=CARTESIAN_POINT('Ctrl Pts',(2.12639562601662,-1.74382774416875,
12.5161920673678));
#443712=CARTESIAN_POINT('Ctrl Pts',(2.10900584014426,-1.75832514635071,
12.5042015548894));
#443713=CARTESIAN_POINT('Ctrl Pts',(2.11536588755699,-1.75736226425788,
12.4980677368513));
#443714=CARTESIAN_POINT('Ctrl Pts',(2.11970418659824,-1.75213063533829,
12.4907278922777));
#443715=CARTESIAN_POINT('Ctrl Pts',(2.09884684902727,-1.76687113220315,
12.506463626192));
#443716=CARTESIAN_POINT('Ctrl Pts',(2.10385214370824,-1.77108473677562,
12.4999376786891));
#443717=CARTESIAN_POINT('Ctrl Pts',(2.1037910113114,-1.77103327372235,12.4906970594712));
#443718=CARTESIAN_POINT('Origin',(2.10923799855709,-1.73005753240835,12.5369868989719));
#443719=CARTESIAN_POINT('Origin',(2.10923799855709,-1.73005753240835,14.));
#443720=CARTESIAN_POINT('Origin',(2.10923799855709,-1.73005753240835,13.7435492065112));
#443721=CARTESIAN_POINT('Ctrl Pts',(2.07882476581745,-1.74317610049156,
13.793642941384));
#443722=CARTESIAN_POINT('Ctrl Pts',(2.08908231900796,-1.74659499235143,
13.8071662555867));
#443723=CARTESIAN_POINT('Ctrl Pts',(2.09678409482011,-1.73140611375641,
13.8103758687955));
#443724=CARTESIAN_POINT('Ctrl Pts',(2.09460626292319,-1.74839204281527,
13.7804579775006));
#443725=CARTESIAN_POINT('Ctrl Pts',(2.10726636298059,-1.75260102585943,
13.7901904343352));
#443726=CARTESIAN_POINT('Ctrl Pts',(2.11657182980508,-1.73988630166491,
13.7927914348262));
#443727=CARTESIAN_POINT('Ctrl Pts',(2.10389742420584,-1.75146286432314,
13.7597120340895));
#443728=CARTESIAN_POINT('Ctrl Pts',(2.11855053313096,-1.75632840527981,
13.7635825532445));
#443729=CARTESIAN_POINT('Ctrl Pts',(2.12825070374247,-1.74486356309809,
13.7651073818884));
#443730=CARTESIAN_POINT('Ctrl Pts',(2.10207800208354,-1.75086152715731,
13.7381884353898));
#443731=CARTESIAN_POINT('Ctrl Pts',(2.11638784444474,-1.75561403409828,
13.7368803041982));
#443732=CARTESIAN_POINT('Ctrl Pts',(2.12596382695618,-1.7438884127476,13.7363986145813));
#443733=CARTESIAN_POINT('Origin',(2.08955801581772,-1.7235531055736,13.7902182540695));
#443734=CARTESIAN_POINT('Ctrl Pts',(2.04869023441034,-1.73321637083664,
13.8235227101244));
#443735=CARTESIAN_POINT('Ctrl Pts',(2.05960513502331,-1.7368285215711,13.8358800583119));
#443736=CARTESIAN_POINT('Ctrl Pts',(2.06755050992179,-1.72228558284541,
13.8390832900376));
#443737=CARTESIAN_POINT('Ctrl Pts',(2.06001528618862,-1.73695941124701,
13.8124254819052));
#443738=CARTESIAN_POINT('Ctrl Pts',(2.07095138347126,-1.74057857646292,
13.8247886449157));
#443739=CARTESIAN_POINT('Ctrl Pts',(2.07889184014536,-1.72600909023626,
13.8279860620657));
#443740=CARTESIAN_POINT('Ctrl Pts',(2.07133526244714,-1.74070077414845,
13.8013225099955));
#443741=CARTESIAN_POINT('Ctrl Pts',(2.08228739568786,-1.74432524808412,
13.8136962257787));
#443742=CARTESIAN_POINT('Ctrl Pts',(2.09022783533978,-1.72973113135799,
13.8168830918626));
#443743=CARTESIAN_POINT('Ctrl Pts',(2.08265036066656,-1.74444052481026,
13.7902140179785));
#443744=CARTESIAN_POINT('Ctrl Pts',(2.09361370644511,-1.74806871318529,
13.802602731458));
#443745=CARTESIAN_POINT('Ctrl Pts',(2.10155870455724,-1.73345176557235,
13.8057746032558));
#443746=CARTESIAN_POINT('Origin',(2.05559787773024,-1.71232894768619,13.8235269408515));
#443747=CARTESIAN_POINT('Ctrl Pts',(2.00713550187736,-1.78117863747125,
13.8235269408515));
#443748=CARTESIAN_POINT('Ctrl Pts',(2.01239863335932,-1.79174821957248,
13.8362179249168));
#443749=CARTESIAN_POINT('Ctrl Pts',(1.99854352737823,-1.80173316034896,
13.8391868794938));
#443750=CARTESIAN_POINT('Ctrl Pts',(2.00231996566185,-1.77150792991513,
13.8400110824519));
#443751=CARTESIAN_POINT('Ctrl Pts',(2.0034773691972,-1.78150704387178,13.8494522556837));
#443752=CARTESIAN_POINT('Ctrl Pts',(1.99071909162703,-1.78576782324635,
13.85569149686));
#443753=CARTESIAN_POINT('Ctrl Pts',(2.00166443723085,-1.75523009195916,
13.8586819406588));
#443754=CARTESIAN_POINT('Ctrl Pts',(1.99882379491583,-1.75852960629814,
13.868010383617));
#443755=CARTESIAN_POINT('Ctrl Pts',(1.98977678287228,-1.758740413974,13.8744918421245));
#443756=CARTESIAN_POINT('Ctrl Pts',(2.02211523627899,-1.73154810901348,
13.8587686893867));
#443757=CARTESIAN_POINT('Ctrl Pts',(2.02493055423129,-1.72827792358337,
13.8680909899357));
#443758=CARTESIAN_POINT('Ctrl Pts',(2.02382330493006,-1.71931854857778,
13.8745789365162));
#443759=CARTESIAN_POINT('Ctrl Pts',(2.03841968402915,-1.72982185424597,
13.8400379222776));
#443760=CARTESIAN_POINT('Ctrl Pts',(2.04847897340077,-1.72953737007122,
13.8494748685453));
#443761=CARTESIAN_POINT('Ctrl Pts',(2.05088069251635,-1.71630888374227,
13.8557104837033));
#443762=CARTESIAN_POINT('Ctrl Pts',(2.04869397153352,-1.73321760678476,
13.8235269408542));
#443763=CARTESIAN_POINT('Ctrl Pts',(2.0599049922347,-1.73692295880962,13.8362179249195));
#443764=CARTESIAN_POINT('Ctrl Pts',(2.06781651354415,-1.72178787259823,
13.8391868794965));
#443765=CARTESIAN_POINT('Origin',(1.98744198749732,-1.79098503800168,13.8235269408515));
#443766=CARTESIAN_POINT('Ctrl Pts',(2.02307668737534,-1.81319221692728,
13.7902140241682));
#443767=CARTESIAN_POINT('Ctrl Pts',(2.02822818492491,-1.82352762540441,
13.8026027327198));
#443768=CARTESIAN_POINT('Ctrl Pts',(2.01489071319087,-1.83347195947046,
13.8057746032556));
#443769=CARTESIAN_POINT('Ctrl Pts',(2.01776469560807,-1.80252451209978,
13.8013225161808));
#443770=CARTESIAN_POINT('Ctrl Pts',(2.02291092082792,-1.8128493507848,13.8136962270464));
#443771=CARTESIAN_POINT('Ctrl Pts',(2.00959539884771,-1.82278592361994,
13.8168830918628));
#443772=CARTESIAN_POINT('Ctrl Pts',(2.01245041379337,-1.79185220832873,
13.8124254880875));
#443773=CARTESIAN_POINT('Ctrl Pts',(2.01758910218842,-1.80216192979049,
13.8247886461868));
#443774=CARTESIAN_POINT('Ctrl Pts',(2.00429796241527,-1.81209501419208,
13.8279860620656));
#443775=CARTESIAN_POINT('Ctrl Pts',(2.00713374922116,-1.78117511943091,
13.8235227163065));
#443776=CARTESIAN_POINT('Ctrl Pts',(2.0122624779483,-1.79146485824588,13.8358800595847));
#443777=CARTESIAN_POINT('Ctrl Pts',(1.99899831538418,-1.80139903270935,
13.8390832900376));
#443778=CARTESIAN_POINT('Origin',(2.00338493120099,-1.82300214663539,13.7902182540695));
#443779=CARTESIAN_POINT('Ctrl Pts',(2.03219710676631,-1.83150818311793,
13.7382347919292));
#443780=CARTESIAN_POINT('Ctrl Pts',(2.03894502593405,-1.84500571828694,
13.7369371795943));
#443781=CARTESIAN_POINT('Ctrl Pts',(2.02868754764281,-1.85615596115984,
13.7364597369712));
#443782=CARTESIAN_POINT('Ctrl Pts',(2.03304026082543,-1.83320143006296,
13.7595490285574));
#443783=CARTESIAN_POINT('Ctrl Pts',(2.0399482802584,-1.84702145444543,13.7633824266925));
#443784=CARTESIAN_POINT('Ctrl Pts',(2.02996273758586,-1.85825455721548,
13.7648920890506));
#443785=CARTESIAN_POINT('Ctrl Pts',(2.02874022132283,-1.82456596340339,
13.7803806590111));
#443786=CARTESIAN_POINT('Ctrl Pts',(2.03472023968487,-1.83651737613972,
13.7901039518745));
#443787=CARTESIAN_POINT('Ctrl Pts',(2.02346485292937,-1.84755375735866,
13.7926933640892));
#443788=CARTESIAN_POINT('Ctrl Pts',(2.02126579270878,-1.80955559470482,
13.7936647693663));
#443789=CARTESIAN_POINT('Ctrl Pts',(2.02611353045677,-1.81922372641012,
13.8072068914932));
#443790=CARTESIAN_POINT('Ctrl Pts',(2.01215425950561,-1.82901060662593,
13.8104111085397));
#443791=CARTESIAN_POINT('Origin',(2.01262390590996,-1.84155613907362,13.7435492065112));
#443792=CARTESIAN_POINT('Origin',(2.01262390590996,-1.84155613907362,14.));
#443793=CARTESIAN_POINT('Origin',(2.01262390590996,-1.84155613907362,12.5369868989719));
#443794=CARTESIAN_POINT('Ctrl Pts',(2.04758518902183,-1.82603271176115,
12.506462012331));
#443795=CARTESIAN_POINT('Ctrl Pts',(2.05246516055766,-1.83038466141612,
12.4999388158272));
#443796=CARTESIAN_POINT('Ctrl Pts',(2.0524074240947,-1.83033317214447,12.4907030323752));
#443797=CARTESIAN_POINT('Ctrl Pts',(2.04057046462635,-1.83730312545407,
12.5042014951932));
#443798=CARTESIAN_POINT('Ctrl Pts',(2.04052348863317,-1.84373265812542,
12.4980716682127));
#443799=CARTESIAN_POINT('Ctrl Pts',(2.03596689881399,-1.84876883270994,
12.4907355092744));
#443800=CARTESIAN_POINT('Ctrl Pts',(2.03461895904624,-1.83635166206782,
12.5218047446509));
#443801=CARTESIAN_POINT('Ctrl Pts',(2.03672599900411,-1.8479740221359,12.5216906929434));
#443802=CARTESIAN_POINT('Ctrl Pts',(2.02870059055002,-1.85657422989357,
12.5161988840775));
#443803=CARTESIAN_POINT('Ctrl Pts',(2.03230026645711,-1.83171536493648,
12.5369868989719));
#443804=CARTESIAN_POINT('Ctrl Pts',(2.03915744765511,-1.8454261124558,12.5369868989719));
#443805=CARTESIAN_POINT('Ctrl Pts',(2.02866975789569,-1.85660707373071,
12.5369868989719));
#443806=CARTESIAN_POINT('Origin',(3.89351796801565E-31,-8.5256151254664E-31,
12.5));
#443807=CARTESIAN_POINT('Origin',(2.14563951868151,-1.61165173575206,12.5));
#443808=CARTESIAN_POINT('',(2.14563951868151,-1.61165173575206,12.5893111709658));
#443809=CARTESIAN_POINT('',(2.14563951868151,-1.61165173575206,13.8235269408515));
#443810=CARTESIAN_POINT('',(2.14563951868151,-1.61165173575206,12.5));
#443811=CARTESIAN_POINT('',(2.16413910514119,-1.64226281217911,13.7902182540695));
#443812=CARTESIAN_POINT('',(2.14563951868151,-1.61165173575206,13.8235269408515));
#443813=CARTESIAN_POINT('',(2.17485966055454,-1.66000200552886,13.7435492065112));
#443814=CARTESIAN_POINT('Origin',(2.13958945374545,-1.60164012539495,13.7445212918695));
#443815=CARTESIAN_POINT('',(2.17485966055454,-1.66000200552886,12.5369868989719));
#443816=CARTESIAN_POINT('',(2.17485966055454,-1.66000200552886,12.5));
#443817=CARTESIAN_POINT('Ctrl Pts',(2.17485966055454,-1.66000200552886,
12.5369868989719));
#443818=CARTESIAN_POINT('Ctrl Pts',(2.16512671706162,-1.64389700351861,
12.5544431401645));
#443819=CARTESIAN_POINT('Ctrl Pts',(2.15538681230883,-1.62778048278287,
12.5718848856037));
#443820=CARTESIAN_POINT('Ctrl Pts',(2.14563951868151,-1.61165173575206,
12.5893111709658));
#443821=CARTESIAN_POINT('Origin',(2.45042401499281,-1.62519182013837,12.5));
#443822=CARTESIAN_POINT('',(2.23805711869617,-1.57376031685917,13.7435492065112));
#443823=CARTESIAN_POINT('',(2.21791244830468,-1.56888163426144,13.7902182540695));
#443824=CARTESIAN_POINT('Origin',(2.16497573621185,-1.55606129959972,13.7418732680434));
#443825=CARTESIAN_POINT('',(2.18315043670736,-1.56046289035814,13.8235269408515));
#443826=CARTESIAN_POINT('',(2.21791244830468,-1.56888163426144,13.7902182540695));
#443827=CARTESIAN_POINT('',(2.18315043670736,-1.56046289035814,12.5893111709658));
#443828=CARTESIAN_POINT('',(2.18315043670736,-1.56046289035814,12.5));
#443829=CARTESIAN_POINT('',(2.23805711869617,-1.57376031685917,12.5369868989719));
#443830=CARTESIAN_POINT('Ctrl Pts',(2.18315043670736,-1.56046289035814,
12.5893111709658));
#443831=CARTESIAN_POINT('Ctrl Pts',(2.20146628040765,-1.56489866350245,
12.5718848856037));
#443832=CARTESIAN_POINT('Ctrl Pts',(2.21976823989801,-1.56933107413687,
12.5544431401645));
#443833=CARTESIAN_POINT('Ctrl Pts',(2.23805711869617,-1.57376031685917,
12.5369868989719));
#443834=CARTESIAN_POINT('',(2.23805711869617,-1.57376031685917,12.5));
#443835=CARTESIAN_POINT('Origin',(2.17505932048484,-1.59387208764382,12.5));
#443836=CARTESIAN_POINT('',(2.14668558831924,-1.5744679258435,13.8587068136939));
#443837=CARTESIAN_POINT('Ctrl Pts',(2.18315043670878,-1.56046289035168,
13.8235269408542));
#443838=CARTESIAN_POINT('Ctrl Pts',(2.18144737109385,-1.5600504380049,13.8262006681044));
#443839=CARTESIAN_POINT('Ctrl Pts',(2.17966363786502,-1.55979721122832,
13.8288634856214));
#443840=CARTESIAN_POINT('Ctrl Pts',(2.17780652992437,-1.5596920467058,13.8314912288862));
#443841=CARTESIAN_POINT('Ctrl Pts',(2.17589204318937,-1.5595836329303,13.834200161153));
#443842=CARTESIAN_POINT('Ctrl Pts',(2.17389747917255,-1.55963195555763,
13.8368750301949));
#443843=CARTESIAN_POINT('Ctrl Pts',(2.17180888022849,-1.55986429920104,
13.8394886372968));
#443844=CARTESIAN_POINT('Ctrl Pts',(2.1716475726658,-1.55988224366421,13.8396904925131));
#443845=CARTESIAN_POINT('Ctrl Pts',(2.17148570281865,-1.55990130789,13.8398919674349));
#443846=CARTESIAN_POINT('Ctrl Pts',(2.17132326454954,-1.55992151588814,
13.8400930404591));
#443847=CARTESIAN_POINT('Ctrl Pts',(2.16879236703379,-1.56023637009442,
13.8432258934518));
#443848=CARTESIAN_POINT('Ctrl Pts',(2.16613625619827,-1.56082615998279,
13.8462331177034));
#443849=CARTESIAN_POINT('Ctrl Pts',(2.16346247112471,-1.56176582236049,
13.8489036603661));
#443850=CARTESIAN_POINT('Ctrl Pts',(2.16258757753225,-1.56207329082587,
13.8497774930041));
#443851=CARTESIAN_POINT('Ctrl Pts',(2.16171103427618,-1.56241827908187,
13.85061494757));
#443852=CARTESIAN_POINT('Ctrl Pts',(2.16083730473066,-1.56280357170684,
13.8514076489583));
#443853=CARTESIAN_POINT('Ctrl Pts',(2.15898924073119,-1.56361852117618,
13.8530843267192));
#443854=CARTESIAN_POINT('Ctrl Pts',(2.15697342976868,-1.56469654170965,
13.8546805203176));
#443855=CARTESIAN_POINT('Ctrl Pts',(2.15497121424547,-1.56609538617429,
13.8559412814274));
#443856=CARTESIAN_POINT('Ctrl Pts',(2.15470325287509,-1.56628259692925,
13.8561100121513));
#443857=CARTESIAN_POINT('Ctrl Pts',(2.1544355423056,-1.5664754775244,13.8562727473908));
#443858=CARTESIAN_POINT('Ctrl Pts',(2.15416851492518,-1.56667409058494,
13.8564289040185));
#443859=CARTESIAN_POINT('Ctrl Pts',(2.15295754880127,-1.56757479854867,
13.8571370725437));
#443860=CARTESIAN_POINT('Ctrl Pts',(2.1517407064163,-1.56861105959196,13.8577210840553));
#443861=CARTESIAN_POINT('Ctrl Pts',(2.15058431458969,-1.56976493785743,
13.8581177131616));
#443862=CARTESIAN_POINT('Ctrl Pts',(2.15025863484952,-1.57008990969228,
13.8582294175695));
#443863=CARTESIAN_POINT('Ctrl Pts',(2.14993765153355,-1.57042406281398,
13.8583265086086));
#443864=CARTESIAN_POINT('Ctrl Pts',(2.14962258137367,-1.57076664577275,
13.8584082369006));
#443865=CARTESIAN_POINT('Ctrl Pts',(2.14916991004332,-1.57125884561726,
13.8585256585398));
#443866=CARTESIAN_POINT('Ctrl Pts',(2.1487240548657,-1.57177478440373,13.8586122832068));
#443867=CARTESIAN_POINT('Ctrl Pts',(2.14829719536374,-1.57230157587311,
13.8586682984299));
#443868=CARTESIAN_POINT('Ctrl Pts',(2.1479557500754,-1.57272295682945,13.8587131050557));
#443869=CARTESIAN_POINT('Ctrl Pts',(2.14762250556025,-1.57315578831616,
13.8587357943552));
#443870=CARTESIAN_POINT('Ctrl Pts',(2.14729782350775,-1.57360043072413,
13.8587355499465));
#443871=CARTESIAN_POINT('Ctrl Pts',(2.14708797375645,-1.57388781371314,
13.8587353919793));
#443872=CARTESIAN_POINT('Ctrl Pts',(2.14688393889627,-1.57417700000451,
13.8587257282814));
#443873=CARTESIAN_POINT('Ctrl Pts',(2.14668558831924,-1.5744679258435,13.8587068136939));
#443874=CARTESIAN_POINT('Ctrl Pts',(2.14668558831924,-1.5744679258435,13.8587068136939));
#443875=CARTESIAN_POINT('Ctrl Pts',(2.14603322408453,-1.57542476506803,
13.8586446046466));
#443876=CARTESIAN_POINT('Ctrl Pts',(2.14544227142407,-1.5764003986978,13.858482427929));
#443877=CARTESIAN_POINT('Ctrl Pts',(2.1449087568648,-1.57739277796024,13.8582284286032));
#443878=CARTESIAN_POINT('Ctrl Pts',(2.14436143298796,-1.57841084364519,
13.8579678548414));
#443879=CARTESIAN_POINT('Ctrl Pts',(2.14387457120063,-1.57944974518245,
13.857615680862));
#443880=CARTESIAN_POINT('Ctrl Pts',(2.14345859166921,-1.58046441288024,
13.8571944833187));
#443881=CARTESIAN_POINT('Ctrl Pts',(2.14242047220565,-1.58299661989181,
13.8561433417727));
#443882=CARTESIAN_POINT('Ctrl Pts',(2.14177081261079,-1.58549452749989,
13.8546163505474));
#443883=CARTESIAN_POINT('Ctrl Pts',(2.14139296760601,-1.58778739688165,
13.8528973491086));
#443884=CARTESIAN_POINT('Ctrl Pts',(2.14132394089822,-1.58820627028954,
13.8525833129072));
#443885=CARTESIAN_POINT('Ctrl Pts',(2.14126385141198,-1.58861834480671,
13.8522628768811));
#443886=CARTESIAN_POINT('Ctrl Pts',(2.14121182884849,-1.58902266102707,
13.851937733538));
#443887=CARTESIAN_POINT('Ctrl Pts',(2.14089413427106,-1.5914917640885,13.8499521282529));
#443888=CARTESIAN_POINT('Ctrl Pts',(2.1408497575725,-1.59391743397896,13.847639871647));
#443889=CARTESIAN_POINT('Ctrl Pts',(2.14100070377333,-1.59617071689979,
13.8452109780794));
#443890=CARTESIAN_POINT('Ctrl Pts',(2.14106861759351,-1.5971845155265,13.8441181685877));
#443891=CARTESIAN_POINT('Ctrl Pts',(2.1411754149802,-1.59816371078859,13.8430021611332));
#443892=CARTESIAN_POINT('Ctrl Pts',(2.14131153713677,-1.59909877597496,
13.8418824960098));
#443893=CARTESIAN_POINT('Ctrl Pts',(2.14163231247473,-1.60130228096441,
13.8392439765549));
#443894=CARTESIAN_POINT('Ctrl Pts',(2.14212752608784,-1.60336660401069,
13.8364981347964));
#443895=CARTESIAN_POINT('Ctrl Pts',(2.14276521119921,-1.60530518718705,
13.8336931113419));
#443896=CARTESIAN_POINT('Ctrl Pts',(2.14338627600093,-1.60719324408941,
13.8309611966327));
#443897=CARTESIAN_POINT('Ctrl Pts',(2.14414364098942,-1.60896374577289,
13.8281701127185));
#443898=CARTESIAN_POINT('Ctrl Pts',(2.1450380805368,-1.6106040899672,13.825358068512));
#443899=CARTESIAN_POINT('Ctrl Pts',(2.14523199599598,-1.61095971835882,
13.8247484142932));
#443900=CARTESIAN_POINT('Ctrl Pts',(2.14543243433548,-1.61130907540357,
13.8241378483365));
#443901=CARTESIAN_POINT('Ctrl Pts',(2.14563951868151,-1.61165173575206,
13.8235269408515));
#443902=CARTESIAN_POINT('',(2.14740511570521,-1.57345547475895,12.5969504640361));
#443903=CARTESIAN_POINT('Origin',(2.17508589184132,-1.59389180174597,12.584524458991));
#443904=CARTESIAN_POINT('Origin',(2.17508589184132,-1.59389180174597,12.584524458991));
#443905=CARTESIAN_POINT('Ctrl Pts',(2.18315043670736,-1.56046289035814,
12.5893111709658));
#443906=CARTESIAN_POINT('Ctrl Pts',(2.17213491717369,-1.55779512650747,
12.5770542771492));
#443907=CARTESIAN_POINT('Ctrl Pts',(2.16538527500076,-1.57270304404791,
12.5737548217797));
#443908=CARTESIAN_POINT('Ctrl Pts',(2.20723768100929,-1.56629639457139,
12.5663937883685));
#443909=CARTESIAN_POINT('Ctrl Pts',(2.19620810965064,-1.56362522761743,
12.5540940315304));
#443910=CARTESIAN_POINT('Ctrl Pts',(2.18944047703163,-1.57858066622843,
12.5508374392248));
#443911=CARTESIAN_POINT('Ctrl Pts',(2.23130062157697,-1.57212401285039,
12.5434499600945));
#443912=CARTESIAN_POINT('Ctrl Pts',(2.22023518915413,-1.5694441609814,12.5311293540533));
#443913=CARTESIAN_POINT('Ctrl Pts',(2.21347245666714,-1.58445139969722,
12.5278936106989));
#443914=CARTESIAN_POINT('Ctrl Pts',(2.25534116215525,-1.57794620624846,
12.5204817579905));
#443915=CARTESIAN_POINT('Ctrl Pts',(2.24422096340405,-1.57525309094419,
12.5081597038247));
#443916=CARTESIAN_POINT('Ctrl Pts',(2.23748302213097,-1.59031576641355,
12.5049254088044));
#443917=CARTESIAN_POINT('Ctrl Pts',(2.23805711869617,-1.57376031685917,
12.5369868989719));
#443918=CARTESIAN_POINT('Ctrl Pts',(2.23896245181433,-1.57397957268211,
12.5342545179733));
#443919=CARTESIAN_POINT('Ctrl Pts',(2.23979709794904,-1.57431006162775,
12.5314872231885));
#443920=CARTESIAN_POINT('Ctrl Pts',(2.24049346011131,-1.57478514146218,
12.5287124745062));
#443921=CARTESIAN_POINT('Ctrl Pts',(2.24112147407358,-1.57521359203772,
12.5262100684184));
#443922=CARTESIAN_POINT('Ctrl Pts',(2.24163582914458,-1.57576002336795,
12.5237004536639));
#443923=CARTESIAN_POINT('Ctrl Pts',(2.24199708719794,-1.57647925433941,
12.5212220730815));
#443924=CARTESIAN_POINT('Ctrl Pts',(2.24227366148909,-1.57702988786651,
12.5193246583486));
#443925=CARTESIAN_POINT('Ctrl Pts',(2.24246324052858,-1.57768866887025,
12.517417831369));
#443926=CARTESIAN_POINT('Ctrl Pts',(2.2424795272376,-1.57850039508432,12.5155812248348));
#443927=CARTESIAN_POINT('Ctrl Pts',(2.24248646546319,-1.57884619481456,
12.5147988205793));
#443928=CARTESIAN_POINT('Ctrl Pts',(2.24246223850744,-1.57922009660828,
12.5140295443047));
#443929=CARTESIAN_POINT('Ctrl Pts',(2.24240195537312,-1.57962672751777,
12.5132817086137));
#443930=CARTESIAN_POINT('Ctrl Pts',(2.24231072500425,-1.58024210839149,
12.5121499604604));
#443931=CARTESIAN_POINT('Ctrl Pts',(2.2421278717249,-1.58094468777853,12.5110494206568));
#443932=CARTESIAN_POINT('Ctrl Pts',(2.24181625360193,-1.58173718147512,
12.5100666561695));
#443933=CARTESIAN_POINT('Ctrl Pts',(2.24163732319332,-1.58219222953076,
12.5095023550641));
#443934=CARTESIAN_POINT('Ctrl Pts',(2.24141326378282,-1.58268194140116,
12.5089719619137));
#443935=CARTESIAN_POINT('Ctrl Pts',(2.24114246717993,-1.58319448065509,
12.5085043804652));
#443936=CARTESIAN_POINT('Ctrl Pts',(2.24074619162535,-1.58394451509028,
12.5078201359221));
#443937=CARTESIAN_POINT('Ctrl Pts',(2.24023726943766,-1.58476462253414,
12.5072563000949));
#443938=CARTESIAN_POINT('Ctrl Pts',(2.2396430045484,-1.58559474784262,12.5068768744332));
#443939=CARTESIAN_POINT('Ctrl Pts',(2.23921449865391,-1.58619332533605,
12.5066032824114));
#443940=CARTESIAN_POINT('Ctrl Pts',(2.23873414028217,-1.58680766258495,
12.5064197834844));
#443941=CARTESIAN_POINT('Ctrl Pts',(2.23823079016697,-1.58740504559342,
12.5063282718343));
#443942=CARTESIAN_POINT('Ctrl Pts',(2.23749605483204,-1.58827703984068,
12.5061946931565));
#443943=CARTESIAN_POINT('Ctrl Pts',(2.23669743927224,-1.58913223202237,
12.5062515701262));
#443944=CARTESIAN_POINT('Ctrl Pts',(2.23589580952595,-1.58992810221818,
12.5064436508398));
#443945=CARTESIAN_POINT('',(2.16538527500076,-1.57270304404791,12.5737548217797));
#443946=CARTESIAN_POINT('Origin',(2.17797212232495,-1.58184477662098,12.5893111709658));
#443947=CARTESIAN_POINT('Ctrl Pts',(2.23589580952594,-1.58992810221818,
12.5064436508398));
#443948=CARTESIAN_POINT('Ctrl Pts',(2.22545830449568,-1.58737881280847,
12.5164271754438));
#443949=CARTESIAN_POINT('Ctrl Pts',(2.21501671161468,-1.58482830989171,
12.5264061185523));
#443950=CARTESIAN_POINT('Ctrl Pts',(2.2045708866877,-1.58227655164866,12.536380305637));
#443951=CARTESIAN_POINT('Ctrl Pts',(2.19151572417055,-1.57908737139719,
12.5488460165097));
#443952=CARTESIAN_POINT('Ctrl Pts',(2.17845394737643,-1.57589622936917,
12.5613043021964));
#443953=CARTESIAN_POINT('Ctrl Pts',(2.16538527500076,-1.57270304404791,
12.5737548217797));
#443954=CARTESIAN_POINT('Ctrl Pts',(2.14563951868151,-1.61165173575206,
12.5893111709658));
#443955=CARTESIAN_POINT('Ctrl Pts',(2.13977729878549,-1.60195158047235,
12.5770542771492));
#443956=CARTESIAN_POINT('Ctrl Pts',(2.15195938587369,-1.59102453013704,
12.5737548217797));
#443957=CARTESIAN_POINT('Ctrl Pts',(2.14017011850542,-1.60260157524359,
12.5928319619712));
#443958=CARTESIAN_POINT('Ctrl Pts',(2.13901847966281,-1.59439748209764,
12.5821634970843));
#443959=CARTESIAN_POINT('Ctrl Pts',(2.14995893754366,-1.58773265774458,
12.5773203894503));
#443960=CARTESIAN_POINT('Ctrl Pts',(2.13827537602497,-1.5859584370097,12.5969440695591));
#443961=CARTESIAN_POINT('Ctrl Pts',(2.14063662090009,-1.58270527467258,
12.5878292599214));
#443962=CARTESIAN_POINT('Ctrl Pts',(2.14928564550728,-1.58180047223405,
12.5813877129824));
#443963=CARTESIAN_POINT('Ctrl Pts',(2.15631715034656,-1.56124670649826,
12.596957478804));
#443964=CARTESIAN_POINT('Ctrl Pts',(2.1539734205758,-1.56447587417903,12.5878468778671));
#443965=CARTESIAN_POINT('Ctrl Pts',(2.15574786437539,-1.57295931871175,
12.5814011370086));
#443966=CARTESIAN_POINT('Ctrl Pts',(2.17285813004666,-1.55797027586401,
12.5928371701607));
#443967=CARTESIAN_POINT('Ctrl Pts',(2.16469508204371,-1.55934857663135,
12.5821692192952));
#443968=CARTESIAN_POINT('Ctrl Pts',(2.16163178890298,-1.57178401217266,
12.5773318885715));
#443969=CARTESIAN_POINT('Ctrl Pts',(2.18315043670737,-1.56046289035808,
12.5893111709658));
#443970=CARTESIAN_POINT('Ctrl Pts',(2.1721349171737,-1.55779512650742,12.5770542771492));
#443971=CARTESIAN_POINT('Ctrl Pts',(2.16538527500077,-1.57270304404785,
12.5737548217797));
#443972=CARTESIAN_POINT('',(2.15195938587369,-1.59102453013704,12.5737548217797));
#443973=CARTESIAN_POINT('Origin',(2.16446819183564,-1.60027276096279,12.5893111709658));
#443974=CARTESIAN_POINT('Ctrl Pts',(2.16538527500077,-1.57270304404785,
12.5737548217797));
#443975=CARTESIAN_POINT('Ctrl Pts',(2.16441948596369,-1.57243551616732,
12.5746934679442));
#443976=CARTESIAN_POINT('Ctrl Pts',(2.16330187468488,-1.57231601525643,
12.5756680099006));
#443977=CARTESIAN_POINT('Ctrl Pts',(2.16215994763177,-1.572354825994,12.5765688348656));
#443978=CARTESIAN_POINT('Ctrl Pts',(2.161857635086,-1.57236510070712,12.5768073183026));
#443979=CARTESIAN_POINT('Ctrl Pts',(2.16155367238901,-1.57238621963317,
12.5770407398754));
#443980=CARTESIAN_POINT('Ctrl Pts',(2.16125040166498,-1.57241781094287,
12.5772674179684));
#443981=CARTESIAN_POINT('Ctrl Pts',(2.16000586062142,-1.57254745313522,
12.5781976435658));
#443982=CARTESIAN_POINT('Ctrl Pts',(2.15870345460724,-1.57287203911304,
12.5790594849312));
#443983=CARTESIAN_POINT('Ctrl Pts',(2.15744280158855,-1.57341650829504,
12.5797571720116));
#443984=CARTESIAN_POINT('Ctrl Pts',(2.15662144081783,-1.57377124954448,
12.580211740231));
#443985=CARTESIAN_POINT('Ctrl Pts',(2.1557879208466,-1.57425268639174,12.5806009430798));
#443986=CARTESIAN_POINT('Ctrl Pts',(2.15500977901797,-1.57484226926025,
12.5808812374708));
#443987=CARTESIAN_POINT('Ctrl Pts',(2.1543410970413,-1.57534891653639,12.5811221033394));
#443988=CARTESIAN_POINT('Ctrl Pts',(2.15369968833467,-1.57594588774487,
12.581287365893));
#443989=CARTESIAN_POINT('Ctrl Pts',(2.15312743566234,-1.5766055923473,12.581359338449));
#443990=CARTESIAN_POINT('Ctrl Pts',(2.15304790435745,-1.57669727766465,
12.5813693411482));
#443991=CARTESIAN_POINT('Ctrl Pts',(2.15296965309714,-1.57679015277659,
12.5813775999465));
#443992=CARTESIAN_POINT('Ctrl Pts',(2.15289273683827,-1.57688412218016,
12.5813841266931));
#443993=CARTESIAN_POINT('Ctrl Pts',(2.15276223910227,-1.57704355263867,
12.5813952001081));
#443994=CARTESIAN_POINT('Ctrl Pts',(2.15263518134807,-1.57720758648643,
12.5814007534795));
#443995=CARTESIAN_POINT('Ctrl Pts',(2.15251177482256,-1.57737627304579,
12.5814005856065));
#443996=CARTESIAN_POINT('Ctrl Pts',(2.15194686799762,-1.57814845416237,
12.5813998171494));
#443997=CARTESIAN_POINT('Ctrl Pts',(2.15149722919371,-1.57896457948774,
12.58127954464));
#443998=CARTESIAN_POINT('Ctrl Pts',(2.1511394948303,-1.57980573716164,12.5810700125799));
#443999=CARTESIAN_POINT('Ctrl Pts',(2.15070739245063,-1.58082175985825,
12.5808169217085));
#444000=CARTESIAN_POINT('Ctrl Pts',(2.15042473963729,-1.58188094621889,
12.5804173076348));
#444001=CARTESIAN_POINT('Ctrl Pts',(2.15029114576598,-1.58288375629323,
12.5799304713245));
#444002=CARTESIAN_POINT('Ctrl Pts',(2.15012558087302,-1.58412655389309,
12.5793271277669));
#444003=CARTESIAN_POINT('Ctrl Pts',(2.15014676723826,-1.58535560391092,
12.5785808224116));
#444004=CARTESIAN_POINT('Ctrl Pts',(2.15032209966813,-1.58651964617907,
12.5777485681082));
#444005=CARTESIAN_POINT('Ctrl Pts',(2.15058336419775,-1.58825419668896,
12.576508418016));
#444006=CARTESIAN_POINT('Ctrl Pts',(2.15117790321657,-1.58983082057114,
12.5750928681475));
#444007=CARTESIAN_POINT('Ctrl Pts',(2.15195938587369,-1.59102453013704,
12.5737548217797));
#444008=CARTESIAN_POINT('Ctrl Pts',(2.15195938587369,-1.59102453013704,
12.5737548217797));
#444009=CARTESIAN_POINT('Ctrl Pts',(2.13977729878549,-1.60195158047235,
12.5770542771492));
#444010=CARTESIAN_POINT('Ctrl Pts',(2.14563951868151,-1.61165173575206,
12.5893111709658));
#444011=CARTESIAN_POINT('Ctrl Pts',(2.16480857860599,-1.61218849007602,
12.5508408821982));
#444012=CARTESIAN_POINT('Ctrl Pts',(2.15258660177983,-1.62314700307234,
12.55409748406));
#444013=CARTESIAN_POINT('Ctrl Pts',(2.15845630036708,-1.63285953326585,
12.5663972313419));
#444014=CARTESIAN_POINT('Ctrl Pts',(2.17764421105535,-1.63333238762155,
12.52790050457));
#444015=CARTESIAN_POINT('Ctrl Pts',(2.16537137191014,-1.64430183139314,
12.5311362602938));
#444016=CARTESIAN_POINT('Ctrl Pts',(2.171260152026,-1.65404593559684,12.5434568539655));
#444017=CARTESIAN_POINT('Ctrl Pts',(2.19046732519249,-1.65445778906585,
12.5049357605811));
#444018=CARTESIAN_POINT('Ctrl Pts',(2.17813416660201,-1.66542029718085,
12.5081700652078));
#444019=CARTESIAN_POINT('Ctrl Pts',(2.18405208634059,-1.67521261842012,
12.5204921097672));
#444020=CARTESIAN_POINT('Ctrl Pts',(2.18962530789643,-1.65307061322152,
12.5064436508395));
#444021=CARTESIAN_POINT('Ctrl Pts',(2.18906641016893,-1.65415527036587,
12.5062361689309));
#444022=CARTESIAN_POINT('Ctrl Pts',(2.18843895007854,-1.65525939239509,
12.5061871075061));
#444023=CARTESIAN_POINT('Ctrl Pts',(2.18777250480326,-1.65629228509822,
12.5063648335164));
#444024=CARTESIAN_POINT('Ctrl Pts',(2.18746976425118,-1.65676148867544,
12.5064455676329));
#444025=CARTESIAN_POINT('Ctrl Pts',(2.18715457123752,-1.65722241878708,
12.506574497099));
#444026=CARTESIAN_POINT('Ctrl Pts',(2.18683957277924,-1.65765471890938,
12.5067492519495));
#444027=CARTESIAN_POINT('Ctrl Pts',(2.18620657115002,-1.65852344278577,
12.5071004286051));
#444028=CARTESIAN_POINT('Ctrl Pts',(2.18555042879403,-1.65930801565087,
12.5076537929612));
#444029=CARTESIAN_POINT('Ctrl Pts',(2.18492764820123,-1.65995561906305,
12.5083435010503));
#444030=CARTESIAN_POINT('Ctrl Pts',(2.18488844044109,-1.65999638956802,
12.5083869222963));
#444031=CARTESIAN_POINT('Ctrl Pts',(2.1848493520306,-1.66003661337411,12.5084308732336));
#444032=CARTESIAN_POINT('Ctrl Pts',(2.18481039171186,-1.66007627612276,
12.5084753333615));
#444033=CARTESIAN_POINT('Ctrl Pts',(2.18449787853311,-1.66039442371644,
12.508831962269));
#444034=CARTESIAN_POINT('Ctrl Pts',(2.18418818278667,-1.66068383495248,
12.509227847131));
#444035=CARTESIAN_POINT('Ctrl Pts',(2.18389242514581,-1.66093794992714,
12.5096423454524));
#444036=CARTESIAN_POINT('Ctrl Pts',(2.18296565159621,-1.66173423379116,
12.5109411997424));
#444037=CARTESIAN_POINT('Ctrl Pts',(2.18212503728312,-1.66224024729522,
12.5124831113042));
#444038=CARTESIAN_POINT('Ctrl Pts',(2.18138269873447,-1.66254984696361,
12.5140723025008));
#444039=CARTESIAN_POINT('Ctrl Pts',(2.1813131407994,-1.66257885679163,12.5142212114565));
#444040=CARTESIAN_POINT('Ctrl Pts',(2.18124443894086,-1.66260617094912,
12.5143705582413));
#444041=CARTESIAN_POINT('Ctrl Pts',(2.18117660076271,-1.66263188346759,
12.5145201959299));
#444042=CARTESIAN_POINT('Ctrl Pts',(2.18030511836381,-1.66296219904925,
12.5164425148273));
#444043=CARTESIAN_POINT('Ctrl Pts',(2.1795501168198,-1.66304955148419,12.518463520594));
#444044=CARTESIAN_POINT('Ctrl Pts',(2.17887493203607,-1.66297636481453,
12.5205025929157));
#444045=CARTESIAN_POINT('Ctrl Pts',(2.17848329809969,-1.66293391364528,
12.5216853356836));
#444046=CARTESIAN_POINT('Ctrl Pts',(2.17811917353142,-1.66283800716306,
12.5228750347131));
#444047=CARTESIAN_POINT('Ctrl Pts',(2.17778094595008,-1.66270682045728,
12.5240609649613));
#444048=CARTESIAN_POINT('Ctrl Pts',(2.17695078449697,-1.66238482972586,
12.5269717671327));
#444049=CARTESIAN_POINT('Ctrl Pts',(2.17625702961506,-1.66183154575537,
12.5299036066169));
#444050=CARTESIAN_POINT('Ctrl Pts',(2.17565724539176,-1.66112252459092,
12.532813300402));
#444051=CARTESIAN_POINT('Ctrl Pts',(2.1753693140402,-1.66078215314692,12.5342101228452));
#444052=CARTESIAN_POINT('Ctrl Pts',(2.17510379815577,-1.66040597736117,
12.5356023438238));
#444053=CARTESIAN_POINT('Ctrl Pts',(2.17485966055454,-1.66000200552886,
12.5369868989719));
#444054=CARTESIAN_POINT('Origin',(8.762946539626,-12.571485399216,-1.24088865030942));
#444055=CARTESIAN_POINT('Ctrl Pts',(2.23801650804472,-1.57375044083148,
12.5369868989719));
#444056=CARTESIAN_POINT('Ctrl Pts',(2.25291760523941,-1.57738920519317,
12.5369868989719));
#444057=CARTESIAN_POINT('Ctrl Pts',(2.26148447100907,-1.5646655219776,12.5369868989719));
#444058=CARTESIAN_POINT('Ctrl Pts',(2.24305367738201,-1.57498042117505,
12.5218025310016));
#444059=CARTESIAN_POINT('Ctrl Pts',(2.25485934340535,-1.57444927764403,
12.5216901060418));
#444060=CARTESIAN_POINT('Ctrl Pts',(2.26145837004303,-1.56470431719146,
12.5161920673678));
#444061=CARTESIAN_POINT('Ctrl Pts',(2.24530812011375,-1.58057090945112,
12.5042015548894));
#444062=CARTESIAN_POINT('Ctrl Pts',(2.25156852116383,-1.57909282836108,
12.4980677368513));
#444063=CARTESIAN_POINT('Ctrl Pts',(2.25546595854791,-1.57352499560848,
12.4907278922777));
#444064=CARTESIAN_POINT('Ctrl Pts',(2.23587950938567,-1.58991651132813,
12.506463626192));
#444065=CARTESIAN_POINT('Ctrl Pts',(2.24121159725135,-1.5937081174956,12.4999376786891));
#444066=CARTESIAN_POINT('Ctrl Pts',(2.24114647355092,-1.59366180853925,
12.4906970594712));
#444067=CARTESIAN_POINT('Origin',(2.24323543307858,-1.55237843059634,12.5369868989719));
#444068=CARTESIAN_POINT('Origin',(2.24323543307858,-1.55237843059634,14.));
#444069=CARTESIAN_POINT('Origin',(2.24323543307858,-1.55237843059634,13.7435492065112));
#444070=CARTESIAN_POINT('Ctrl Pts',(2.21399268294759,-1.56793230853741,
13.793642941384));
#444071=CARTESIAN_POINT('Ctrl Pts',(2.22449477640208,-1.57050373850516,
13.8071662555867));
#444072=CARTESIAN_POINT('Ctrl Pts',(2.23093289057839,-1.55473763342218,
13.8103758687955));
#444073=CARTESIAN_POINT('Ctrl Pts',(2.23014681614542,-1.57184455672094,
13.7804579775006));
#444074=CARTESIAN_POINT('Ctrl Pts',(2.24310786195665,-1.5750076190359,13.7901904343351));
#444075=CARTESIAN_POINT('Ctrl Pts',(2.25134599754834,-1.56157672010332,
13.7927914348263));
#444076=CARTESIAN_POINT('Ctrl Pts',(2.23965736231638,-1.57414784442409,
13.7597120340895));
#444077=CARTESIAN_POINT('Ctrl Pts',(2.25465830098779,-1.57780283128438,
13.7635825532445));
#444078=CARTESIAN_POINT('Ctrl Pts',(2.26339170400959,-1.56558548346241,
13.7651073818884));
#444079=CARTESIAN_POINT('Ctrl Pts',(2.23779497960954,-1.57369680795173,
13.7381884353898));
#444080=CARTESIAN_POINT('Ctrl Pts',(2.25244458058657,-1.57726711631938,
13.7368803041982));
#444081=CARTESIAN_POINT('Ctrl Pts',(2.26103295281073,-1.56479997953268,
13.7363986145813));
#444082=CARTESIAN_POINT('Origin',(2.2230907626871,-1.5474997479986,13.7902182540695));
#444083=CARTESIAN_POINT('Ctrl Pts',(2.18314661127931,-1.56046196312631,
13.8235227101244));
#444084=CARTESIAN_POINT('Ctrl Pts',(2.19431961727935,-1.56317242899826,
13.8358800583119));
#444085=CARTESIAN_POINT('Ctrl Pts',(2.2010531700821,-1.54803025888596,13.8390832900376));
#444086=CARTESIAN_POINT('Ctrl Pts',(2.19473907242423,-1.56326945202192,
13.8124254819053));
#444087=CARTESIAN_POINT('Ctrl Pts',(2.2059337763091,-1.56598518130984,13.8247886449158));
#444088=CARTESIAN_POINT('Ctrl Pts',(2.21266026338467,-1.55081695291213,
13.8279860620657));
#444089=CARTESIAN_POINT('Ctrl Pts',(2.20632633820512,-1.56607568269234,
13.8013225099955));
#444090=CARTESIAN_POINT('Ctrl Pts',(2.21753745739973,-1.56879539595624,
13.8136962257787));
#444091=CARTESIAN_POINT('Ctrl Pts',(2.22426191989538,-1.5536026204025,13.8168830918626));
#444092=CARTESIAN_POINT('Ctrl Pts',(2.21790861076574,-1.5688807040932,13.7902140179785));
#444093=CARTESIAN_POINT('Ctrl Pts',(2.22913120795064,-1.57160320551105,
13.802602731458));
#444094=CARTESIAN_POINT('Ctrl Pts',(2.23585835280941,-1.55638730348156,
13.8057746032558));
#444095=CARTESIAN_POINT('Origin',(2.18832875108978,-1.5390810040953,13.8235269408515));
#444096=CARTESIAN_POINT('Ctrl Pts',(2.14563951868151,-1.61165173575206,
13.8235269408515));
#444097=CARTESIAN_POINT('Ctrl Pts',(2.1517466565921,-1.62175715436447,13.8362179249168));
#444098=CARTESIAN_POINT('Ctrl Pts',(2.13875151770214,-1.63283819083621,
13.8391868794938));
#444099=CARTESIAN_POINT('Ctrl Pts',(2.14005175332123,-1.60240571758443,
13.8400110824519));
#444100=CARTESIAN_POINT('Ctrl Pts',(2.14202032630649,-1.61227722118133,
13.8494522556837));
#444101=CARTESIAN_POINT('Ctrl Pts',(2.1296517939266,-1.61756374122801,13.85569149686));
#444102=CARTESIAN_POINT('Ctrl Pts',(2.13807161119749,-1.58623547444414,
13.8586819406588));
#444103=CARTESIAN_POINT('Ctrl Pts',(2.13550936193527,-1.58975554864125,
13.868010383617));
#444104=CARTESIAN_POINT('Ctrl Pts',(2.12650963586058,-1.59070307034188,
13.8744918421245));
#444105=CARTESIAN_POINT('Ctrl Pts',(2.156524060436,-1.56096536136471,13.8587686893867));
#444106=CARTESIAN_POINT('Ctrl Pts',(2.15906346017857,-1.55747658265759,
13.8680909899357));
#444107=CARTESIAN_POINT('Ctrl Pts',(2.15722962292033,-1.54863727033049,
13.8745789365163));
#444108=CARTESIAN_POINT('Ctrl Pts',(2.17263355069197,-1.55791588671278,
13.8400379222776));
#444109=CARTESIAN_POINT('Ctrl Pts',(2.1826361805068,-1.55681242366595,13.8494748685453));
#444110=CARTESIAN_POINT('Ctrl Pts',(2.18395166365704,-1.54343219162963,
13.8557104837033));
#444111=CARTESIAN_POINT('Ctrl Pts',(2.18315043670878,-1.56046289035168,
13.8235269408542));
#444112=CARTESIAN_POINT('Ctrl Pts',(2.19462617425226,-1.56324211085818,
13.8362179249195));
#444113=CARTESIAN_POINT('Ctrl Pts',(2.20127772059369,-1.54751252296389,
13.8391868794965));
#444114=CARTESIAN_POINT('Origin',(2.12681084552738,-1.62303071054133,13.8235269408515));
#444115=CARTESIAN_POINT('Ctrl Pts',(2.16413706512503,-1.64225943805455,
13.7902140241682));
#444116=CARTESIAN_POINT('Ctrl Pts',(2.17011385323161,-1.65214056143813,
13.8026027327198));
#444117=CARTESIAN_POINT('Ctrl Pts',(2.15763131637958,-1.66313893431829,
13.8057746032556));
#444118=CARTESIAN_POINT('Ctrl Pts',(2.15797323159458,-1.632060205778,13.8013225161808));
#444119=CARTESIAN_POINT('Ctrl Pts',(2.16394390337851,-1.64193122428339,
13.8136962270464));
#444120=CARTESIAN_POINT('Ctrl Pts',(2.15148261063193,-1.65292007264879,
13.8168830918628));
#444121=CARTESIAN_POINT('Ctrl Pts',(2.15180674078005,-1.62185657652063,
13.8124254880875));
#444122=CARTESIAN_POINT('Ctrl Pts',(2.15776866862328,-1.63171314242527,
13.8247886461867));
#444123=CARTESIAN_POINT('Ctrl Pts',(2.14533139261428,-1.64269652658836,
13.8279860620656));
#444124=CARTESIAN_POINT('Ctrl Pts',(2.14563748510417,-1.61164837227547,
13.8235227163065));
#444125=CARTESIAN_POINT('Ctrl Pts',(2.15158785764826,-1.62148583382931,
13.8358800595847));
#444126=CARTESIAN_POINT('Ctrl Pts',(2.13917755793401,-1.63246810553422,
13.8390832900376));
#444127=CARTESIAN_POINT('Origin',(2.14531043198705,-1.65364178696838,13.7902182540695));
#444128=CARTESIAN_POINT('Ctrl Pts',(2.17472005835453,-1.65977106052845,
13.7382347919292));
#444129=CARTESIAN_POINT('Ctrl Pts',(2.18254569879919,-1.67267366570587,
13.7369371795942));
#444130=CARTESIAN_POINT('Ctrl Pts',(2.17323119972871,-1.68462288677196,
13.7364597369711));
#444131=CARTESIAN_POINT('Ctrl Pts',(2.17569842223343,-1.66138994845068,
13.7595490285574));
#444132=CARTESIAN_POINT('Ctrl Pts',(2.18370991608764,-1.6746009201274,13.7633824266926));
#444133=CARTESIAN_POINT('Ctrl Pts',(2.17467320164337,-1.6866105601037,13.7648920890506));
#444134=CARTESIAN_POINT('Ctrl Pts',(2.17070882005703,-1.65313370873311,
13.780380659011));
#444135=CARTESIAN_POINT('Ctrl Pts',(2.17764309149078,-1.66455792711719,
13.7901039518744));
#444136=CARTESIAN_POINT('Ctrl Pts',(2.16732472363235,-1.67647500419857,
13.7926933640891));
#444137=CARTESIAN_POINT('Ctrl Pts',(2.1620357775892,-1.63878252111939,13.7936647693663));
#444138=CARTESIAN_POINT('Ctrl Pts',(2.1676554273783,-1.64802334728335,13.8072068914933));
#444139=CARTESIAN_POINT('Ctrl Pts',(2.15454032634419,-1.65891547263667,
13.8104111085397));
#444140=CARTESIAN_POINT('Origin',(2.15603098740041,-1.67138098031813,13.7435492065112));
#444141=CARTESIAN_POINT('Origin',(2.15603098740041,-1.67138098031813,14.));
#444142=CARTESIAN_POINT('Origin',(2.15603098740041,-1.67138098031813,12.5369868989719));
#444143=CARTESIAN_POINT('Ctrl Pts',(2.1896106362884,-1.65305953679111,12.506462012331));
#444144=CARTESIAN_POINT('Ctrl Pts',(2.19482909441992,-1.656999242709,12.4999388158272));
#444145=CARTESIAN_POINT('Ctrl Pts',(2.19476735321664,-1.65695263082138,
12.4907030323752));
#444146=CARTESIAN_POINT('Ctrl Pts',(2.18353789615505,-1.66486421427197,
12.5042014951932));
#444147=CARTESIAN_POINT('Ctrl Pts',(2.18401514307223,-1.67127618218332,
12.4980716682127));
#444148=CARTESIAN_POINT('Ctrl Pts',(2.17988420991196,-1.67666700368392,
12.4907355092744));
#444149=CARTESIAN_POINT('Ctrl Pts',(2.17752864061987,-1.66440101975751,
12.5218047446509));
#444150=CARTESIAN_POINT('Ctrl Pts',(2.18057599981837,-1.67581296406388,
12.5216906929434));
#444151=CARTESIAN_POINT('Ctrl Pts',(2.17327829202155,-1.68503870063296,
12.5161988840775));
#444152=CARTESIAN_POINT('Ctrl Pts',(2.17483976203157,-1.65996914449412,
12.5369868989719));
#444153=CARTESIAN_POINT('Ctrl Pts',(2.182791679732,-1.67307534670552,12.5369868989719));
#444154=CARTESIAN_POINT('Ctrl Pts',(2.17325023903797,-1.6850739483325,12.5369868989719));
#444155=CARTESIAN_POINT('Origin',(4.15555475928483E-31,-8.19703138220645E-31,
12.5));
#444156=CARTESIAN_POINT('Origin',(2.26986465849443,-1.43139955763526,12.5));
#444157=CARTESIAN_POINT('',(2.26986465849443,-1.43139955763526,12.5893111709658));
#444158=CARTESIAN_POINT('',(2.26986465849443,-1.43139955763526,13.8235269408515));
#444159=CARTESIAN_POINT('',(2.26986465849443,-1.43139955763526,12.5));
#444160=CARTESIAN_POINT('',(2.29079777601444,-1.46040089019248,13.7902182540695));
#444161=CARTESIAN_POINT('',(2.26986465849443,-1.43139955763526,13.8235269408515));
#444162=CARTESIAN_POINT('',(2.30292856860469,-1.47720723304878,13.7435492065112));
#444163=CARTESIAN_POINT('Origin',(2.26301868546698,-1.42191439654958,13.7445212918718));
#444164=CARTESIAN_POINT('',(2.30292856860469,-1.47720723304878,12.5369868989719));
#444165=CARTESIAN_POINT('',(2.30292856860469,-1.47720723304878,12.5));
#444166=CARTESIAN_POINT('Ctrl Pts',(2.30292856860469,-1.47720723304878,
12.5369868989719));
#444167=CARTESIAN_POINT('Ctrl Pts',(2.29191530350295,-1.46194914435506,
12.5544431401645));
#444168=CARTESIAN_POINT('Ctrl Pts',(2.28089416142129,-1.44668014267077,
12.5718848856037));
#444169=CARTESIAN_POINT('Ctrl Pts',(2.26986465849443,-1.43139955763526,
12.5893111709658));
#444170=CARTESIAN_POINT('Origin',(2.5747386521147,-1.42005182257716,12.5));
#444171=CARTESIAN_POINT('',(2.35888624416241,-1.38610132694858,13.7435492065112));
#444172=CARTESIAN_POINT('',(2.33841094557665,-1.38288085541563,13.7902182540695));
#444173=CARTESIAN_POINT('Origin',(2.28460539973481,-1.37441801283617,13.7418732680441));
#444174=CARTESIAN_POINT('',(2.30307839592133,-1.37732355084812,13.8235269408515));
#444175=CARTESIAN_POINT('',(2.33841094557665,-1.38288085541563,13.7902182540695));
#444176=CARTESIAN_POINT('',(2.30307839592133,-1.37732355084812,12.5893111709658));
#444177=CARTESIAN_POINT('',(2.30307839592133,-1.37732355084812,12.5));
#444178=CARTESIAN_POINT('',(2.35888624416241,-1.38610132694858,12.5369868989719));
#444179=CARTESIAN_POINT('Ctrl Pts',(2.30307839592133,-1.37732355084812,
12.5893111709658));
#444180=CARTESIAN_POINT('Ctrl Pts',(2.32169485185363,-1.38025165302565,
12.5718848856037));
#444181=CARTESIAN_POINT('Ctrl Pts',(2.34029719569878,-1.38317753557376,
12.5544431401645));
#444182=CARTESIAN_POINT('Ctrl Pts',(2.35888624416241,-1.38610132694858,
12.5369868989719));
#444183=CARTESIAN_POINT('',(2.35888624416241,-1.38610132694858,12.5));
#444184=CARTESIAN_POINT('Origin',(2.2977373619552,-1.4112810828723,12.5));
#444185=CARTESIAN_POINT('',(2.26787642171629,-1.39425420940044,13.8587068136939));
#444186=CARTESIAN_POINT('Ctrl Pts',(2.30307839592221,-1.37732355084157,
13.8235269408542));
#444187=CARTESIAN_POINT('Ctrl Pts',(2.30134737842234,-1.37705128655405,
13.8262006681044));
#444188=CARTESIAN_POINT('Ctrl Pts',(2.29954894008554,-1.3769442931862,13.8288634856214));
#444189=CARTESIAN_POINT('Ctrl Pts',(2.29768943963348,-1.37699085012767,
13.8314912288862));
#444190=CARTESIAN_POINT('Ctrl Pts',(2.29577248646598,-1.37703884553219,
13.8342001611531));
#444191=CARTESIAN_POINT('Ctrl Pts',(2.29378849793912,-1.37724958285397,
13.8368750301949));
#444192=CARTESIAN_POINT('Ctrl Pts',(2.29172578679966,-1.37765139359663,
13.8394886372969));
#444193=CARTESIAN_POINT('Ctrl Pts',(2.29156647861492,-1.37768242641494,
13.8396904925131));
#444194=CARTESIAN_POINT('Ctrl Pts',(2.29140670128772,-1.37771462110135,
13.8398919674349));
#444195=CARTESIAN_POINT('Ctrl Pts',(2.29124645065801,-1.37774800208598,
13.8400930404591));
#444196=CARTESIAN_POINT('Ctrl Pts',(2.28874963803573,-1.37826810028411,
13.8432258934518));
#444197=CARTESIAN_POINT('Ctrl Pts',(2.28615043854114,-1.3790724253865,13.8462331177034));
#444198=CARTESIAN_POINT('Ctrl Pts',(2.28356214147404,-1.38022689942086,
13.8489036603661));
#444199=CARTESIAN_POINT('Ctrl Pts',(2.28271522055215,-1.38060465676019,
13.8497774930041));
#444200=CARTESIAN_POINT('Ctrl Pts',(2.28186971366704,-1.38101994350902,
13.85061494757));
#444201=CARTESIAN_POINT('Ctrl Pts',(2.28103029631031,-1.38147517117384,
13.8514076489583));
#444202=CARTESIAN_POINT('Ctrl Pts',(2.27925480753871,-1.3824380433386,13.8530843267192));
#444203=CARTESIAN_POINT('Ctrl Pts',(2.27733357270221,-1.38367678415501,
13.8546805203176));
#444204=CARTESIAN_POINT('Ctrl Pts',(2.27545203819607,-1.38523417323291,
13.8559412814274));
#444205=CARTESIAN_POINT('Ctrl Pts',(2.27520022785957,-1.38544260239883,
13.8561100121513));
#444206=CARTESIAN_POINT('Ctrl Pts',(2.27494912963404,-1.38565666209643,
13.8562727473908));
#444207=CARTESIAN_POINT('Ctrl Pts',(2.27469917957348,-1.38587637949884,
13.8564289040185));
#444208=CARTESIAN_POINT('Ctrl Pts',(2.27356565890027,-1.38687279541228,
13.8571370725437));
#444209=CARTESIAN_POINT('Ctrl Pts',(2.27243733035316,-1.38800479233342,
13.8577210840553));
#444210=CARTESIAN_POINT('Ctrl Pts',(2.27137883811568,-1.38924908783344,
13.8581177131616));
#444211=CARTESIAN_POINT('Ctrl Pts',(2.2710807302694,-1.3895995242736,13.8582294175695));
#444212=CARTESIAN_POINT('Ctrl Pts',(2.27078805158048,-1.38995872864847,
13.8583265086086));
#444213=CARTESIAN_POINT('Ctrl Pts',(2.27050195348209,-1.39032585283371,
13.8584082369006));
#444214=CARTESIAN_POINT('Ctrl Pts',(2.27009090723494,-1.39085331183966,
13.8585256585398));
#444215=CARTESIAN_POINT('Ctrl Pts',(2.26968858940448,-1.39140387521847,
13.8586122832068));
#444216=CARTESIAN_POINT('Ctrl Pts',(2.26930608863755,-1.39196370684487,
13.8586682984299));
#444217=CARTESIAN_POINT('Ctrl Pts',(2.26900012594009,-1.39241151665167,
13.8587131050557));
#444218=CARTESIAN_POINT('Ctrl Pts',(2.26870327005296,-1.39287007044899,
13.8587357943552));
#444219=CARTESIAN_POINT('Ctrl Pts',(2.26841591083731,-1.39333969794751,
13.8587355499465));
#444220=CARTESIAN_POINT('Ctrl Pts',(2.26823018372519,-1.39364322939636,
13.8587353919793));
#444221=CARTESIAN_POINT('Ctrl Pts',(2.26805039914152,-1.39394808417961,
13.8587257282814));
#444222=CARTESIAN_POINT('Ctrl Pts',(2.26787642171629,-1.39425420940044,
13.8587068136939));
#444223=CARTESIAN_POINT('Ctrl Pts',(2.26787642171629,-1.39425420940044,
13.8587068136939));
#444224=CARTESIAN_POINT('Ctrl Pts',(2.26730421944952,-1.39526103856263,
13.8586446046466));
#444225=CARTESIAN_POINT('Ctrl Pts',(2.26679475633354,-1.3962815939798,13.858482427929));
#444226=CARTESIAN_POINT('Ctrl Pts',(2.2663439051227,-1.39731415757145,13.8582284286032));
#444227=CARTESIAN_POINT('Ctrl Pts',(2.26588138422549,-1.39837344770389,
13.8579678548414));
#444228=CARTESIAN_POINT('Ctrl Pts',(2.26548082255058,-1.39944857613745,
13.857615680862));
#444229=CARTESIAN_POINT('Ctrl Pts',(2.26514893199382,-1.40049377380576,
13.8571944833187));
#444230=CARTESIAN_POINT('Ctrl Pts',(2.26432066516643,-1.4031021714811,13.8561433417727));
#444231=CARTESIAN_POINT('Ctrl Pts',(2.26387676991979,-1.4056447207958,13.8546163505474));
#444232=CARTESIAN_POINT('Ctrl Pts',(2.26368707230366,-1.40796075871947,
13.8528973491086));
#444233=CARTESIAN_POINT('Ctrl Pts',(2.26365241734792,-1.40838386467815,
13.8525833129072));
#444234=CARTESIAN_POINT('Ctrl Pts',(2.26362611570316,-1.40879946590234,
13.8522628768811));
#444235=CARTESIAN_POINT('Ctrl Pts',(2.2636072217659,-1.4092066771157,13.851937733538));
#444236=CARTESIAN_POINT('Ctrl Pts',(2.26349183911251,-1.41169345949778,
13.8499521282529));
#444237=CARTESIAN_POINT('Ctrl Pts',(2.26364532468864,-1.41411467528469,
13.847639871647));
#444238=CARTESIAN_POINT('Ctrl Pts',(2.26397943210495,-1.41634815707579,
13.8452109780794));
#444239=CARTESIAN_POINT('Ctrl Pts',(2.26412975394722,-1.41735304676438,
13.8441181685877));
#444240=CARTESIAN_POINT('Ctrl Pts',(2.26431600947868,-1.41832027885654,
13.8430021611332));
#444241=CARTESIAN_POINT('Ctrl Pts',(2.26452789519342,-1.41924113747119,
13.8418824960098));
#444242=CARTESIAN_POINT('Ctrl Pts',(2.26502720929088,-1.42141116431158,
13.8392439765549));
#444243=CARTESIAN_POINT('Ctrl Pts',(2.26568903661406,-1.4234282539864,13.8364981347964));
#444244=CARTESIAN_POINT('Ctrl Pts',(2.26648261240662,-1.4253084094306,13.8336931113419));
#444245=CARTESIAN_POINT('Ctrl Pts',(2.26725550483186,-1.42713956143234,
13.8309611966328));
#444246=CARTESIAN_POINT('Ctrl Pts',(2.26815466207456,-1.42884243963993,
13.8281701127185));
#444247=CARTESIAN_POINT('Ctrl Pts',(2.26917982872818,-1.43040442059757,
13.8253580685121));
#444248=CARTESIAN_POINT('Ctrl Pts',(2.26940208596508,-1.43074305975492,
13.8247484142932));
#444249=CARTESIAN_POINT('Ctrl Pts',(2.26963033320496,-1.43107491675748,
13.8241378483365));
#444250=CARTESIAN_POINT('Ctrl Pts',(2.26986465849443,-1.43139955763526,
13.8235269408515));
#444251=CARTESIAN_POINT('',(2.26851103077193,-1.39318647900124,12.5969504640361));
#444252=CARTESIAN_POINT('Origin',(2.29776545178004,-1.41129856556518,12.584524458991));
#444253=CARTESIAN_POINT('Origin',(2.29776545178004,-1.41129856556518,12.584524458991));
#444254=CARTESIAN_POINT('Ctrl Pts',(2.30307839592133,-1.37732355084812,
12.5893111709658));
#444255=CARTESIAN_POINT('Ctrl Pts',(2.29188208210004,-1.37556253086668,
12.5770542771492));
#444256=CARTESIAN_POINT('Ctrl Pts',(2.28637003248253,-1.39097100203903,
12.5737548217797));
#444257=CARTESIAN_POINT('Ctrl Pts',(2.32756097665388,-1.38117431053166,
12.5663937883685));
#444258=CARTESIAN_POINT('Ctrl Pts',(2.31635038037941,-1.37941104412465,
12.5540940315304));
#444259=CARTESIAN_POINT('Ctrl Pts',(2.31082427358596,-1.39486834463351,
12.5508374392248));
#444260=CARTESIAN_POINT('Ctrl Pts',(2.35201885476263,-1.38502118484589,
12.5434499600945));
#444261=CARTESIAN_POINT('Ctrl Pts',(2.34077180884744,-1.3832521854319,12.5311293540533));
#444262=CARTESIAN_POINT('Ctrl Pts',(2.33525480807067,-1.39876071427864,
12.5278936106989));
#444263=CARTESIAN_POINT('Ctrl Pts',(2.37645396523784,-1.38886447813709,
12.5204817579905));
#444264=CARTESIAN_POINT('Ctrl Pts',(2.36515125413168,-1.38708672338494,
12.5081597038247));
#444265=CARTESIAN_POINT('Ctrl Pts',(2.35966348068816,-1.40264848381001,
12.5049254088044));
#444266=CARTESIAN_POINT('Ctrl Pts',(2.35888624416241,-1.38610132694858,
12.5369868989719));
#444267=CARTESIAN_POINT('Ctrl Pts',(2.35980643624434,-1.38624606016203,
12.5342545179733));
#444268=CARTESIAN_POINT('Ctrl Pts',(2.36066524308006,-1.3865074180245,12.5314872231885));
#444269=CARTESIAN_POINT('Ctrl Pts',(2.36139801157162,-1.38692415708904,
12.5287124745063));
#444270=CARTESIAN_POINT('Ctrl Pts',(2.3620588585687,-1.38729999306251,12.5262100684184));
#444271=CARTESIAN_POINT('Ctrl Pts',(2.36261604139187,-1.38780268147425,
12.5237004536639));
#444272=CARTESIAN_POINT('Ctrl Pts',(2.36303472139004,-1.38849007337888,
12.5212220730815));
#444273=CARTESIAN_POINT('Ctrl Pts',(2.36335525714735,-1.38901633134602,
12.5193246583486));
#444274=CARTESIAN_POINT('Ctrl Pts',(2.36359790214585,-1.38965746785863,
12.517417831369));
#444275=CARTESIAN_POINT('Ctrl Pts',(2.36368029788434,-1.39046516560269,
12.5155812248348));
#444276=CARTESIAN_POINT('Ctrl Pts',(2.36371539891181,-1.39080924918306,
12.5147988205793));
#444277=CARTESIAN_POINT('Ctrl Pts',(2.36372172903659,-1.39118388157121,
12.5140295443047));
#444278=CARTESIAN_POINT('Ctrl Pts',(2.36369479068353,-1.39159407308499,
12.5132817086137));
#444279=CARTESIAN_POINT('Ctrl Pts',(2.3636540231303,-1.39221484245163,12.5121499604604));
#444280=CARTESIAN_POINT('Ctrl Pts',(2.36352904502263,-1.3929299883035,12.5110494206568));
#444281=CARTESIAN_POINT('Ctrl Pts',(2.36328305937668,-1.39374524481264,
12.5100666561695));
#444282=CARTESIAN_POINT('Ctrl Pts',(2.36314181498524,-1.39421336322282,
12.5095023550641));
#444283=CARTESIAN_POINT('Ctrl Pts',(2.36295841717765,-1.39471970853939,
12.5089719619137));
#444284=CARTESIAN_POINT('Ctrl Pts',(2.36273029833549,-1.39525261479832,
12.5085043804652));
#444285=CARTESIAN_POINT('Ctrl Pts',(2.36239647612457,-1.39603245369234,
12.5078201359221));
#444286=CARTESIAN_POINT('Ctrl Pts',(2.36195609370366,-1.39689131417924,
12.5072563000949));
#444287=CARTESIAN_POINT('Ctrl Pts',(2.36143146910095,-1.3977671154196,12.5068768744332));
#444288=CARTESIAN_POINT('Ctrl Pts',(2.36105317864711,-1.39839862840426,
12.5066032824114));
#444289=CARTESIAN_POINT('Ctrl Pts',(2.36062449281724,-1.39905007516336,
12.5064197834844));
#444290=CARTESIAN_POINT('Ctrl Pts',(2.36017150981905,-1.39968649813641,
12.5063282718343));
#444291=CARTESIAN_POINT('Ctrl Pts',(2.35951029488168,-1.4006154786455,12.5061946931565));
#444292=CARTESIAN_POINT('Ctrl Pts',(2.3587840427513,-1.40153291982786,12.5062515701262));
#444293=CARTESIAN_POINT('Ctrl Pts',(2.35804995117132,-1.40239148209754,
12.5064436508398));
#444294=CARTESIAN_POINT('',(2.28637003248253,-1.39097100203903,12.5737548217797));
#444295=CARTESIAN_POINT('Origin',(2.299660134183,-1.39905637134359,12.5893111709658));
#444296=CARTESIAN_POINT('Ctrl Pts',(2.35804995117132,-1.40239148209754,
12.5064436508398));
#444297=CARTESIAN_POINT('Ctrl Pts',(2.34743938532467,-1.40070142879506,
12.5164271754438));
#444298=CARTESIAN_POINT('Ctrl Pts',(2.33682464631719,-1.39901049922118,
12.5264061185523));
#444299=CARTESIAN_POINT('Ctrl Pts',(2.32620558702475,-1.39731866344904,
12.536380305637));
#444300=CARTESIAN_POINT('Ctrl Pts',(2.3129339166865,-1.39520421187513,12.5488460165097));
#444301=CARTESIAN_POINT('Ctrl Pts',(2.29965549417674,-1.3930883441773,12.5613043021964));
#444302=CARTESIAN_POINT('Ctrl Pts',(2.28637003248253,-1.39097100203903,
12.5737548217797));
#444303=CARTESIAN_POINT('Ctrl Pts',(2.26986465849443,-1.43139955763526,
12.5893111709658));
#444304=CARTESIAN_POINT('Ctrl Pts',(2.26323129194437,-1.42220950416576,
12.5770542771492));
#444305=CARTESIAN_POINT('Ctrl Pts',(2.27448218809862,-1.41032585949835,
12.5737548217797));
#444306=CARTESIAN_POINT('Ctrl Pts',(2.2636757851972,-1.42282531767908,12.5928319619712));
#444307=CARTESIAN_POINT('Ctrl Pts',(2.26185926858336,-1.41474239223324,
12.5821634970842));
#444308=CARTESIAN_POINT('Ctrl Pts',(2.27222007793515,-1.40720799564986,
12.5773203894503));
#444309=CARTESIAN_POINT('Ctrl Pts',(2.26043077704263,-1.40639199721679,
12.5969440695591));
#444310=CARTESIAN_POINT('Ctrl Pts',(2.26251900213886,-1.40295719613093,
12.5878292599214));
#444311=CARTESIAN_POINT('Ctrl Pts',(2.27106549803164,-1.40135042854875,
12.5813877129824));
#444312=CARTESIAN_POINT('Ctrl Pts',(2.27639828339932,-1.38029192085117,
12.596957478804));
#444313=CARTESIAN_POINT('Ctrl Pts',(2.27432555934013,-1.38370137947732,
12.5878468778671));
#444314=CARTESIAN_POINT('Ctrl Pts',(2.27678557831023,-1.39201196240539,
12.5814011370086));
#444315=CARTESIAN_POINT('Ctrl Pts',(2.2926171648404,-1.37567814886506,12.5928371701607));
#444316=CARTESIAN_POINT('Ctrl Pts',(2.28459362301432,-1.37771722764459,
12.5821692192951));
#444317=CARTESIAN_POINT('Ctrl Pts',(2.28255412617039,-1.39036097212917,
12.5773318885715));
#444318=CARTESIAN_POINT('Ctrl Pts',(2.30307839592133,-1.37732355084807,
12.5893111709658));
#444319=CARTESIAN_POINT('Ctrl Pts',(2.29188208210005,-1.37556253086663,
12.5770542771492));
#444320=CARTESIAN_POINT('Ctrl Pts',(2.28637003248254,-1.39097100203898,
12.5737548217797));
#444321=CARTESIAN_POINT('',(2.27448218809862,-1.41032585949835,12.5737548217797));
#444322=CARTESIAN_POINT('Origin',(2.28770318870932,-1.41852373378696,12.5893111709658));
#444323=CARTESIAN_POINT('Ctrl Pts',(2.28637003248254,-1.39097100203898,
12.5737548217797));
#444324=CARTESIAN_POINT('Ctrl Pts',(2.28538565102293,-1.39078308510786,
12.5746934679442));
#444325=CARTESIAN_POINT('Ctrl Pts',(2.28426201806981,-1.39075507752102,
12.5756680099006));
#444326=CARTESIAN_POINT('Ctrl Pts',(2.28312705412017,-1.39088683677503,
12.5765688348656));
#444327=CARTESIAN_POINT('Ctrl Pts',(2.28282658497898,-1.3909217185789,12.5768073183026));
#444328=CARTESIAN_POINT('Ctrl Pts',(2.28252535508133,-1.39096754301512,
12.5770407398754));
#444329=CARTESIAN_POINT('Ctrl Pts',(2.28222566845064,-1.39102374858678,
12.5772674179684));
#444330=CARTESIAN_POINT('Ctrl Pts',(2.28099583555695,-1.39125440105424,
12.5781976435658));
#444331=CARTESIAN_POINT('Ctrl Pts',(2.27972421996184,-1.39168406518009,
12.5790594849312));
#444332=CARTESIAN_POINT('Ctrl Pts',(2.27851214095502,-1.39232947761016,
12.5797571720116));
#444333=CARTESIAN_POINT('Ctrl Pts',(2.27772242789959,-1.39274998701531,
12.580211740231));
#444334=CARTESIAN_POINT('Ctrl Pts',(2.2769309229698,-1.39329776153685,12.5806009430798));
#444335=CARTESIAN_POINT('Ctrl Pts',(2.27620342682111,-1.39394880839996,
12.5808812374708));
#444336=CARTESIAN_POINT('Ctrl Pts',(2.27557826628506,-1.39450827363791,
12.5811221033394));
#444337=CARTESIAN_POINT('Ctrl Pts',(2.27498765050849,-1.39515553923808,
12.581287365893));
#444338=CARTESIAN_POINT('Ctrl Pts',(2.27447107400921,-1.39585969263319,
12.581359338449));
#444339=CARTESIAN_POINT('Ctrl Pts',(2.27439928054271,-1.39595755541491,
12.5813693411482));
#444340=CARTESIAN_POINT('Ctrl Pts',(2.27432885984084,-1.39605649969674,
12.5813775999465));
#444341=CARTESIAN_POINT('Ctrl Pts',(2.27425985889324,-1.39615642581402,
12.5813841266931));
#444342=CARTESIAN_POINT('Ctrl Pts',(2.27414279044014,-1.39632596255781,
12.5813952001081));
#444343=CARTESIAN_POINT('Ctrl Pts',(2.27402952574154,-1.39649980698298,
12.5814007534795));
#444344=CARTESIAN_POINT('Ctrl Pts',(2.27392027936166,-1.39667799102921,
12.5814005856065));
#444345=CARTESIAN_POINT('Ctrl Pts',(2.27342019214716,-1.3974936479274,12.5813998171494));
#444346=CARTESIAN_POINT('Ctrl Pts',(2.27303857126983,-1.39834370739983,
12.58127954464));
#444347=CARTESIAN_POINT('Ctrl Pts',(2.27275058939736,-1.39921122486263,
12.5810700125799));
#444348=CARTESIAN_POINT('Ctrl Pts',(2.27240274008478,-1.40025908718291,
12.5808169217085));
#444349=CARTESIAN_POINT('Ctrl Pts',(2.27220736129675,-1.40133778801662,
12.5804173076348));
#444350=CARTESIAN_POINT('Ctrl Pts',(2.27215595027872,-1.40234815046391,
12.5799304713245));
#444351=CARTESIAN_POINT('Ctrl Pts',(2.27209223583124,-1.40360030783308,
12.5793271277669));
#444352=CARTESIAN_POINT('Ctrl Pts',(2.272213530687,-1.40482354140291,12.5785808224116));
#444353=CARTESIAN_POINT('Ctrl Pts',(2.27248315996397,-1.4059694191957,12.5777485681082));
#444354=CARTESIAN_POINT('Ctrl Pts',(2.27288493712676,-1.40767690264723,
12.576508418016));
#444355=CARTESIAN_POINT('Ctrl Pts',(2.2736060073491,-1.40919981999404,12.5750928681475));
#444356=CARTESIAN_POINT('Ctrl Pts',(2.27448218809862,-1.41032585949835,
12.5737548217797));
#444357=CARTESIAN_POINT('Ctrl Pts',(2.27448218809862,-1.41032585949835,
12.5737548217797));
#444358=CARTESIAN_POINT('Ctrl Pts',(2.26323129194437,-1.42220950416576,
12.5770542771492));
#444359=CARTESIAN_POINT('Ctrl Pts',(2.26986465849443,-1.43139955763526,
12.5893111709658));
#444360=CARTESIAN_POINT('Ctrl Pts',(2.28901368541375,-1.43037206961276,
12.5508408821982));
#444361=CARTESIAN_POINT('Ctrl Pts',(2.27772559675031,-1.44229032363573,
12.5540974840599));
#444362=CARTESIAN_POINT('Ctrl Pts',(2.2843674257772,-1.45149210125976,12.5663972313419));
#444363=CARTESIAN_POINT('Ctrl Pts',(2.30353003229531,-1.45039938937864,
12.52790050457));
#444364=CARTESIAN_POINT('Ctrl Pts',(2.29219214151271,-1.46233268355682,
12.5311362602938));
#444365=CARTESIAN_POINT('Ctrl Pts',(2.29885556215093,-1.47156437480941,
12.5434568539655));
#444366=CARTESIAN_POINT('Ctrl Pts',(2.31803239491436,-1.4704092949462,12.5049357605811));
#444367=CARTESIAN_POINT('Ctrl Pts',(2.30663382007401,-1.48234059314037,
12.5081700652078));
#444368=CARTESIAN_POINT('Ctrl Pts',(2.31333021351133,-1.49161796584055,
12.5204921097672));
#444369=CARTESIAN_POINT('Ctrl Pts',(2.31708011165217,-1.4690953670416,12.5064436508395));
#444370=CARTESIAN_POINT('Ctrl Pts',(2.31661148323748,-1.47022197043212,
12.5062361689309));
#444371=CARTESIAN_POINT('Ctrl Pts',(2.31607610716433,-1.47137356240879,
12.5061871075061));
#444372=CARTESIAN_POINT('Ctrl Pts',(2.31549606977494,-1.47245733972357,
12.5063648335164));
#444373=CARTESIAN_POINT('Ctrl Pts',(2.31523258101449,-1.4729496582301,12.5064455676329));
#444374=CARTESIAN_POINT('Ctrl Pts',(2.31495600686275,-1.47343474579154,
12.506574497099));
#444375=CARTESIAN_POINT('Ctrl Pts',(2.3146772930091,-1.47389128276949,12.5067492519495));
#444376=CARTESIAN_POINT('Ctrl Pts',(2.31411720670134,-1.47480871154813,
12.5071004286051));
#444377=CARTESIAN_POINT('Ctrl Pts',(2.31352719757705,-1.47564415550508,
12.5076537929612));
#444378=CARTESIAN_POINT('Ctrl Pts',(2.31295927492544,-1.47634036647026,
12.5083435010503));
#444379=CARTESIAN_POINT('Ctrl Pts',(2.31292352080054,-1.47638419711118,
12.5083869222963));
#444380=CARTESIAN_POINT('Ctrl Pts',(2.31288784106712,-1.47642747314421,
12.5084308732336));
#444381=CARTESIAN_POINT('Ctrl Pts',(2.31285224326785,-1.476470179546,12.5084753333615));
#444382=CARTESIAN_POINT('Ctrl Pts',(2.31256670193335,-1.47681274125511,
12.508831962269));
#444383=CARTESIAN_POINT('Ctrl Pts',(2.31228162637645,-1.47712643257754,
12.509227847131));
#444384=CARTESIAN_POINT('Ctrl Pts',(2.31200756557427,-1.477403808999,12.5096423454524));
#444385=CARTESIAN_POINT('Ctrl Pts',(2.31114878031446,-1.47827298394218,
12.5109411997424));
#444386=CARTESIAN_POINT('Ctrl Pts',(2.31035220787434,-1.47884583159845,
12.5124831113042));
#444387=CARTESIAN_POINT('Ctrl Pts',(2.30963757464312,-1.47921490858273,
12.5140723025008));
#444388=CARTESIAN_POINT('Ctrl Pts',(2.30957061272664,-1.4792494915004,12.5142212114565));
#444389=CARTESIAN_POINT('Ctrl Pts',(2.30950436582528,-1.47928231461156,
12.5143705582413));
#444390=CARTESIAN_POINT('Ctrl Pts',(2.30943884918202,-1.47931347101504,
12.5145201959299));
#444391=CARTESIAN_POINT('Ctrl Pts',(2.30859719035533,-1.47971372140481,
12.5164425148273));
#444392=CARTESIAN_POINT('Ctrl Pts',(2.30785182105105,-1.47986232281666,
12.518463520594));
#444393=CARTESIAN_POINT('Ctrl Pts',(2.30717291749599,-1.47984441349759,
12.5205025929157));
#444394=CARTESIAN_POINT('Ctrl Pts',(2.30677912652483,-1.47983402538267,
12.5216853356836));
#444395=CARTESIAN_POINT('Ctrl Pts',(2.30640839628238,-1.47976811755404,
12.5228750347131));
#444396=CARTESIAN_POINT('Ctrl Pts',(2.30606060119101,-1.47966493604902,
12.5240609649613));
#444397=CARTESIAN_POINT('Ctrl Pts',(2.30520695679783,-1.47941168258047,
12.5269717671327));
#444398=CARTESIAN_POINT('Ctrl Pts',(2.30447041254802,-1.47891678708014,
12.5299036066169));
#444399=CARTESIAN_POINT('Ctrl Pts',(2.30381483225012,-1.47825901310745,
12.5328133004019));
#444400=CARTESIAN_POINT('Ctrl Pts',(2.30350011553383,-1.47794324329952,
12.5342101228451));
#444401=CARTESIAN_POINT('Ctrl Pts',(2.30320482131282,-1.47758996121718,
12.5356023438238));
#444402=CARTESIAN_POINT('Ctrl Pts',(2.30292856860469,-1.47720723304878,
12.5369868989719));
#444403=CARTESIAN_POINT('Origin',(9.75800831304548,-11.8147356748686,-1.24001512903272));
#444404=CARTESIAN_POINT('Ctrl Pts',(2.35884496365163,-1.38609479392766,
12.5369868989719));
#444405=CARTESIAN_POINT('Ctrl Pts',(2.37399307175077,-1.3885068728447,12.5369868989719));
#444406=CARTESIAN_POINT('Ctrl Pts',(2.38149433367832,-1.37512724754428,
12.5369868989719));
#444407=CARTESIAN_POINT('Ctrl Pts',(2.36396562704008,-1.38691010554931,
12.5218025310016));
#444408=CARTESIAN_POINT('Ctrl Pts',(2.37568871755491,-1.38541845797521,
12.5216901060417));
#444409=CARTESIAN_POINT('Ctrl Pts',(2.38147148173117,-1.37516804114132,
12.5161920673677));
#444410=CARTESIAN_POINT('Ctrl Pts',(2.36666824499362,-1.39229823392494,
12.5042015548895));
#444411=CARTESIAN_POINT('Ctrl Pts',(2.37278733774504,-1.39031479022351,
12.4980677368514));
#444412=CARTESIAN_POINT('Ctrl Pts',(2.37621797666913,-1.38444780664622,
12.4907278922778));
#444413=CARTESIAN_POINT('Ctrl Pts',(2.35803276050328,-1.40238125838799,
12.506463626192));
#444414=CARTESIAN_POINT('Ctrl Pts',(2.36365615738865,-1.40572563363697,
12.4999376786891));
#444415=CARTESIAN_POINT('Ctrl Pts',(2.3635874757721,-1.40568478695602,12.4906970594712));
#444416=CARTESIAN_POINT('Origin',(2.36230450590074,-1.36436850645311,12.5369868989719));
#444417=CARTESIAN_POINT('Origin',(2.36230450590074,-1.36436850645311,14.));
#444418=CARTESIAN_POINT('Origin',(2.36230450590074,-1.36436850645311,13.7435492065112));
#444419=CARTESIAN_POINT('Ctrl Pts',(2.33442684405581,-1.38225418576057,
13.793642941384));
#444420=CARTESIAN_POINT('Ctrl Pts',(2.34510358807504,-1.38396104139399,
13.8071662555867));
#444421=CARTESIAN_POINT('Ctrl Pts',(2.3502351960279,-1.36772263065117,13.8103758687955));
#444422=CARTESIAN_POINT('Ctrl Pts',(2.35084611025453,-1.38483670443772,
13.7804579775006));
#444423=CARTESIAN_POINT('Ctrl Pts',(2.36402184819816,-1.38693279636566,
13.7901904343351));
#444424=CARTESIAN_POINT('Ctrl Pts',(2.37113782912386,-1.37287510311147,
13.7927914348262));
#444425=CARTESIAN_POINT('Ctrl Pts',(2.36051275019819,-1.38635713033652,
13.7597120340895));
#444426=CARTESIAN_POINT('Ctrl Pts',(2.375761689844,-1.3887772397659,13.7635825532445));
#444427=CARTESIAN_POINT('Ctrl Pts',(2.38347020591987,-1.37588869073771,
13.7651073818884));
#444428=CARTESIAN_POINT('Ctrl Pts',(2.35861980075643,-1.38605939613093,
13.7381884353898));
#444429=CARTESIAN_POINT('Ctrl Pts',(2.37351166967181,-1.38842374611212,
13.7368803041982));
#444430=CARTESIAN_POINT('Ctrl Pts',(2.38105527740852,-1.37529806062779,
13.7363986145813));
#444431=CARTESIAN_POINT('Origin',(2.34182920731497,-1.36114803492016,13.7902182540695));
#444432=CARTESIAN_POINT('Ctrl Pts',(2.30307450764407,-1.37732293850948,
13.8235227101244));
#444433=CARTESIAN_POINT('Ctrl Pts',(2.31443126451965,-1.37911368181571,
13.8358800583119));
#444434=CARTESIAN_POINT('Ctrl Pts',(2.31990818454372,-1.36347304896064,
13.8390832900376));
#444435=CARTESIAN_POINT('Ctrl Pts',(2.31485723223927,-1.37917619251492,
13.8124254819053));
#444436=CARTESIAN_POINT('Ctrl Pts',(2.32623604381905,-1.38097041314449,
13.8247886449158));
#444437=CARTESIAN_POINT('Ctrl Pts',(2.33170379763438,-1.36530438463317,
13.8279860620657));
#444438=CARTESIAN_POINT('Ctrl Pts',(2.3266346762006,-1.38102861595222,13.8013225099955));
#444439=CARTESIAN_POINT('Ctrl Pts',(2.33803017320052,-1.38282546930125,
13.8136962257787));
#444440=CARTESIAN_POINT('Ctrl Pts',(2.34349390835148,-1.36713514033461,
13.8168830918626));
#444441=CARTESIAN_POINT('Ctrl Pts',(2.33840704498945,-1.3828802411375,13.7902140179785));
#444442=CARTESIAN_POINT('Ctrl Pts',(2.34981420904804,-1.38467893780039,
13.802602731458));
#444443=CARTESIAN_POINT('Ctrl Pts',(2.3552787326143,-1.36896534067192,13.8057746032558));
#444444=CARTESIAN_POINT('Origin',(2.30649665765965,-1.35559073035265,13.8235269408515));
#444445=CARTESIAN_POINT('Ctrl Pts',(2.26986465849443,-1.43139955763526,
13.8235269408515));
#444446=CARTESIAN_POINT('Ctrl Pts',(2.27677516083846,-1.44097356286526,
13.8362179249168));
#444447=CARTESIAN_POINT('Ctrl Pts',(2.26472646954491,-1.45307695256277,
13.8391868794938));
#444448=CARTESIAN_POINT('Ctrl Pts',(2.26354184964589,-1.42263975958145,
13.8400110824519));
#444449=CARTESIAN_POINT('Ctrl Pts',(2.26630849155264,-1.43231795959079,
13.8494522556836));
#444450=CARTESIAN_POINT('Ctrl Pts',(2.25441201490543,-1.438595039391,13.85569149686));
#444451=CARTESIAN_POINT('Ctrl Pts',(2.2602502713486,-1.40668472155711,13.8586819406588));
#444452=CARTESIAN_POINT('Ctrl Pts',(2.25798346648526,-1.41040193009935,
13.868010383617));
#444453=CARTESIAN_POINT('Ctrl Pts',(2.24909091807164,-1.41207986022415,
13.8744918421245));
#444454=CARTESIAN_POINT('Ctrl Pts',(2.27658157277223,-1.3799946467772,13.8587686893867));
#444455=CARTESIAN_POINT('Ctrl Pts',(2.27882815501878,-1.37631049203977,
13.8680909899357));
#444456=CARTESIAN_POINT('Ctrl Pts',(2.2762799336879,-1.36765006655631,13.8745789365163));
#444457=CARTESIAN_POINT('Ctrl Pts',(2.29238889953424,-1.37564224599154,
13.8400379222776));
#444458=CARTESIAN_POINT('Ctrl Pts',(2.30226830394115,-1.37372714743718,
13.8494748685453));
#444459=CARTESIAN_POINT('Ctrl Pts',(2.30248879680276,-1.36028421293006,
13.8557104837033));
#444460=CARTESIAN_POINT('Ctrl Pts',(2.30307839592221,-1.37732355084157,
13.8235269408542));
#444461=CARTESIAN_POINT('Ctrl Pts',(2.314742481168,-1.37915814457576,13.8362179249195));
#444462=CARTESIAN_POINT('Ctrl Pts',(2.32008978759794,-1.36293873281082,
13.8391868794965));
#444463=CARTESIAN_POINT('Origin',(2.25202612827954,-1.44427538148356,13.8235269408515));
#444464=CARTESIAN_POINT('Ctrl Pts',(2.29079546776379,-1.4603976935753,13.7902140241682));
#444465=CARTESIAN_POINT('Ctrl Pts',(2.29755777188865,-1.46975877461948,
13.8026027327198));
#444466=CARTESIAN_POINT('Ctrl Pts',(2.28601323914189,-1.48173799395684,
13.8057746032556));
#444467=CARTESIAN_POINT('Ctrl Pts',(2.28382081176535,-1.45073480805775,
13.8013225161808));
#444468=CARTESIAN_POINT('Ctrl Pts',(2.2905761962777,-1.46008631638396,13.8136962270464));
#444469=CARTESIAN_POINT('Ctrl Pts',(2.27905206061203,-1.47205431130678,
13.8168830918628));
#444470=CARTESIAN_POINT('Ctrl Pts',(2.27684314892995,-1.44106775678328,
13.8124254880875));
#444471=CARTESIAN_POINT('Ctrl Pts',(2.28358864057524,-1.45040557331093,
13.8247886461867));
#444472=CARTESIAN_POINT('Ctrl Pts',(2.27208799635021,-1.46236616462606,
13.8279860620656));
#444473=CARTESIAN_POINT('Ctrl Pts',(2.26986235752908,-1.43139637110578,
13.8235227163065));
#444474=CARTESIAN_POINT('Ctrl Pts',(2.27659477514258,-1.44071608871494,
13.8358800595847));
#444475=CARTESIAN_POINT('Ctrl Pts',(2.26512092677523,-1.45267337245503,
13.8390832900376));
#444476=CARTESIAN_POINT('Origin',(2.27295924579955,-1.47327671404078,13.7902182540695));
#444477=CARTESIAN_POINT('Ctrl Pts',(2.30277060675796,-1.47698843537411,
13.7382347919292));
#444478=CARTESIAN_POINT('Ctrl Pts',(2.31162189013352,-1.48921024585125,
13.7369371795943));
#444479=CARTESIAN_POINT('Ctrl Pts',(2.30331235673834,-1.50187892501582,
13.7364597369711));
#444480=CARTESIAN_POINT('Ctrl Pts',(2.30387766960643,-1.47852219084149,
13.7595490285574));
#444481=CARTESIAN_POINT('Ctrl Pts',(2.31293932271206,-1.49103619297559,
13.7633824266926));
#444482=CARTESIAN_POINT('Ctrl Pts',(2.30491157433978,-1.50374244798558,
13.7648920890506));
#444483=CARTESIAN_POINT('Ctrl Pts',(2.2982317097355,-1.47070012197909,13.780380659011));
#444484=CARTESIAN_POINT('Ctrl Pts',(2.30607408780867,-1.48152111972245,
13.7901039518744));
#444485=CARTESIAN_POINT('Ctrl Pts',(2.29676140588295,-1.49423958648444,
13.7926933640892));
#444486=CARTESIAN_POINT('Ctrl Pts',(2.28841777108056,-1.45710362023598,
13.7936647693663));
#444487=CARTESIAN_POINT('Ctrl Pts',(2.29477193506858,-1.4658556446851,13.8072068914933));
#444488=CARTESIAN_POINT('Ctrl Pts',(2.2825882827851,-1.47778052987879,13.8104111085397));
#444489=CARTESIAN_POINT('Origin',(2.2850900383898,-1.49008305689707,13.7435492065112));
#444490=CARTESIAN_POINT('Origin',(2.2850900383898,-1.49008305689707,14.));
#444491=CARTESIAN_POINT('Origin',(2.2850900383898,-1.49008305689707,12.5369868989719));
#444492=CARTESIAN_POINT('Ctrl Pts',(2.3170645860308,-1.46908552333935,12.506462012331));
#444493=CARTESIAN_POINT('Ctrl Pts',(2.32258680278013,-1.47258676742728,
12.4999388158272));
#444494=CARTESIAN_POINT('Ctrl Pts',(2.32252146771405,-1.47254534311812,
12.4907030323752));
#444495=CARTESIAN_POINT('Ctrl Pts',(2.31197424324324,-1.48134590642715,
12.5042014951932));
#444496=CARTESIAN_POINT('Ctrl Pts',(2.31297253707128,-1.48769763898994,
12.4980716682127));
#444497=CARTESIAN_POINT('Ctrl Pts',(2.30929475124855,-1.49340723237897,
12.4907355092743));
#444498=CARTESIAN_POINT('Ctrl Pts',(2.30594722835712,-1.48137406326756,
12.5218047446509));
#444499=CARTESIAN_POINT('Ctrl Pts',(2.30991462712355,-1.49249964720568,
12.5216906929434));
#444500=CARTESIAN_POINT('Ctrl Pts',(2.30339318502536,-1.50228951683145,
12.5161988840776));
#444501=CARTESIAN_POINT('Ctrl Pts',(2.30290605781301,-1.47717610327077,
12.5369868989719));
#444502=CARTESIAN_POINT('Ctrl Pts',(2.31189979331555,-1.48959054056091,
12.5369868989719));
#444503=CARTESIAN_POINT('Ctrl Pts',(2.3033680984005,-1.50232693382577,12.5369868989719));
#444504=CARTESIAN_POINT('Origin',(4.38993701924924E-31,-7.84818254312661E-31,
12.5));
#444505=CARTESIAN_POINT('Origin',(2.37898422350637,-1.2416216516267,12.5));
#444506=CARTESIAN_POINT('',(2.37898422350637,-1.2416216516267,12.5893111709658));
#444507=CARTESIAN_POINT('',(2.37898422350637,-1.2416216516267,13.8235269408515));
#444508=CARTESIAN_POINT('',(2.37898422350637,-1.2416216516267,12.5));
#444509=CARTESIAN_POINT('',(2.40221156564335,-1.26882024123082,13.7902182540695));
#444510=CARTESIAN_POINT('',(2.37898422350637,-1.2416216516267,13.8235269408515));
#444511=CARTESIAN_POINT('',(2.41567186698724,-1.28458189015479,13.7435492065112));
#444512=CARTESIAN_POINT('Origin',(2.37138790120177,-1.23272606198494,13.7445212918702));
#444513=CARTESIAN_POINT('',(2.41567186698724,-1.28458189015479,12.5369868989719));
#444514=CARTESIAN_POINT('',(2.41567186698724,-1.28458189015479,12.5));
#444515=CARTESIAN_POINT('Ctrl Pts',(2.41567186698724,-1.28458189015479,
12.5369868989719));
#444516=CARTESIAN_POINT('Ctrl Pts',(2.40345157173887,-1.27027225484046,
12.5544431401645));
#444517=CARTESIAN_POINT('Ctrl Pts',(2.39122253621055,-1.25595238489461,
12.5718848856037));
#444518=CARTESIAN_POINT('Ctrl Pts',(2.37898422350637,-1.2416216516267,12.5893111709658));
#444519=CARTESIAN_POINT('Origin',(2.68191882830874,-1.20546161442877,12.5));
#444520=CARTESIAN_POINT('',(2.46401737086259,-1.18921806139777,13.7435492065112));
#444521=CARTESIAN_POINT('',(2.44334770381644,-1.18767723263631,13.7902182540695));
#444522=CARTESIAN_POINT('Origin',(2.38903139125129,-1.1836282009596,13.7418732680428));
#444523=CARTESIAN_POINT('',(2.40767974839162,-1.1850183503496,13.8235269408515));
#444524=CARTESIAN_POINT('',(2.44334770381644,-1.18767723263631,13.7902182540695));
#444525=CARTESIAN_POINT('',(2.40767974839162,-1.1850183503496,12.5893111709658));
#444526=CARTESIAN_POINT('',(2.40767974839162,-1.1850183503496,12.5));
#444527=CARTESIAN_POINT('',(2.46401737086259,-1.18921806139777,12.5369868989719));
#444528=CARTESIAN_POINT('Ctrl Pts',(2.40767974839162,-1.1850183503496,12.5893111709658));
#444529=CARTESIAN_POINT('Ctrl Pts',(2.4264729271132,-1.18641929552346,12.5718848856037));
#444530=CARTESIAN_POINT('Ctrl Pts',(2.44525185978403,-1.18781917871965,
12.5544431401645));
#444531=CARTESIAN_POINT('Ctrl Pts',(2.46401737086259,-1.18921806139777,
12.5369868989719));
#444532=CARTESIAN_POINT('',(2.46401737086259,-1.18921806139777,12.5));
#444533=CARTESIAN_POINT('Origin',(2.40512434038173,-1.21929823533924,12.5));
#444534=CARTESIAN_POINT('',(2.37397491170063,-1.20476196122863,13.8587068136939));
#444535=CARTESIAN_POINT('Ctrl Pts',(2.40767974839197,-1.185018350343,13.8235269408542));
#444536=CARTESIAN_POINT('Ctrl Pts',(2.40593229864302,-1.18488808598866,
13.8262006681044));
#444537=CARTESIAN_POINT('Ctrl Pts',(2.40413112350867,-1.18492803805275,
13.8288634856214));
#444538=CARTESIAN_POINT('Ctrl Pts',(2.40228160521392,-1.18512600662944,
13.8314912288862));
#444539=CARTESIAN_POINT('Ctrl Pts',(2.40037494262099,-1.18533009181249,
13.834200161153));
#444540=CARTESIAN_POINT('Ctrl Pts',(2.39841473270039,-1.1857018414066,13.8368750301949));
#444541=CARTESIAN_POINT('Ctrl Pts',(2.39639163636785,-1.1862704452643,13.8394886372968));
#444542=CARTESIAN_POINT('Ctrl Pts',(2.39623538773073,-1.18631435991947,
13.839690492513));
#444543=CARTESIAN_POINT('Ctrl Pts',(2.39607876621522,-1.18635947081619,
13.8398919674349));
#444544=CARTESIAN_POINT('Ctrl Pts',(2.3959217696664,-1.18640580264236,13.8400930404591));
#444545=CARTESIAN_POINT('Ctrl Pts',(2.39347565781365,-1.18712768366463,
13.8432258934518));
#444546=CARTESIAN_POINT('Ctrl Pts',(2.3909506669038,-1.1881411913302,13.8462331177034));
#444547=CARTESIAN_POINT('Ctrl Pts',(2.38846508253307,-1.18950279418699,
13.8489036603661));
#444548=CARTESIAN_POINT('Ctrl Pts',(2.38765177040077,-1.1899483264875,13.8497774930041));
#444549=CARTESIAN_POINT('Ctrl Pts',(2.38684292659544,-1.19043114806438,
13.85061494757));
#444550=CARTESIAN_POINT('Ctrl Pts',(2.38604340761153,-1.19095328130404,
13.8514076489583));
#444551=CARTESIAN_POINT('Ctrl Pts',(2.38435230965268,-1.1920576684088,13.8530843267192));
#444552=CARTESIAN_POINT('Ctrl Pts',(2.38253843644308,-1.19344888589235,
13.8546805203176));
#444553=CARTESIAN_POINT('Ctrl Pts',(2.38079010425577,-1.19515445541609,
13.8559412814273));
#444554=CARTESIAN_POINT('Ctrl Pts',(2.38055612070934,-1.19538271593131,
13.8561100121513));
#444555=CARTESIAN_POINT('Ctrl Pts',(2.380323305845,-1.19561653019941,13.8562727473908));
#444556=CARTESIAN_POINT('Ctrl Pts',(2.38009209648068,-1.19585588976069,
13.8564289040185));
#444557=CARTESIAN_POINT('Ctrl Pts',(2.37904356465121,-1.19694138264033,
13.8571370725437));
#444558=CARTESIAN_POINT('Ctrl Pts',(2.37801125878228,-1.19816158218658,
13.8577210840553));
#444559=CARTESIAN_POINT('Ctrl Pts',(2.37705771022512,-1.19948801433989,
13.8581177131616));
#444560=CARTESIAN_POINT('Ctrl Pts',(2.37678915813128,-1.19986158328867,
13.8582294175695));
#444561=CARTESIAN_POINT('Ctrl Pts',(2.3765267317978,-1.20024344847086,13.8583265086086));
#444562=CARTESIAN_POINT('Ctrl Pts',(2.37627150969654,-1.20063267073169,
13.8584082369006));
#444563=CARTESIAN_POINT('Ctrl Pts',(2.37590482397754,-1.20119187874641,
13.8585256585398));
#444564=CARTESIAN_POINT('Ctrl Pts',(2.37554872085303,-1.20177340280912,
13.8586122832068));
#444565=CARTESIAN_POINT('Ctrl Pts',(2.37521312430062,-1.20236254900543,
13.8586682984299));
#444566=CARTESIAN_POINT('Ctrl Pts',(2.37494468032531,-1.2028338075623,13.8587131050557));
#444567=CARTESIAN_POINT('Ctrl Pts',(2.37468618859314,-1.20331503207037,
13.8587357943552));
#444568=CARTESIAN_POINT('Ctrl Pts',(2.37443806454252,-1.20380651936591,
13.8587355499465));
#444569=CARTESIAN_POINT('Ctrl Pts',(2.37427769605307,-1.20412417932257,
13.8587353919793));
#444570=CARTESIAN_POINT('Ctrl Pts',(2.37412335818282,-1.20444267383911,
13.8587257282814));
#444571=CARTESIAN_POINT('Ctrl Pts',(2.37397491170063,-1.20476196122863,
13.8587068136939));
#444572=CARTESIAN_POINT('Ctrl Pts',(2.37397491170063,-1.20476196122863,
13.8587068136939));
#444573=CARTESIAN_POINT('Ctrl Pts',(2.37348667931325,-1.20581208004682,
13.8586446046466));
#444574=CARTESIAN_POINT('Ctrl Pts',(2.37306209613455,-1.20687076562378,
13.858482427929));
#444575=CARTESIAN_POINT('Ctrl Pts',(2.37269690861243,-1.20793664200463,
13.8582284286032));
#444576=CARTESIAN_POINT('Ctrl Pts',(2.37232226869512,-1.20903010718349,
13.8579678548414));
#444577=CARTESIAN_POINT('Ctrl Pts',(2.37201067280447,-1.21013430771103,
13.857615680862));
#444578=CARTESIAN_POINT('Ctrl Pts',(2.37176507989927,-1.21120307973182,
13.8571944833187));
#444579=CARTESIAN_POINT('Ctrl Pts',(2.37115217768716,-1.21387030961473,
13.8561433417727));
#444580=CARTESIAN_POINT('Ctrl Pts',(2.37091700083835,-1.21644058038983,
13.8546163505475));
#444581=CARTESIAN_POINT('Ctrl Pts',(2.37091671301721,-1.21876437400513,
13.8528973491086));
#444582=CARTESIAN_POINT('Ctrl Pts',(2.37091666043654,-1.21918889681428,
13.8525833129073));
#444583=CARTESIAN_POINT('Ctrl Pts',(2.37092432166635,-1.21960525898792,
13.8522628768812));
#444584=CARTESIAN_POINT('Ctrl Pts',(2.37093868209137,-1.22001265527087,
13.851937733538));
#444585=CARTESIAN_POINT('Ctrl Pts',(2.37102637921453,-1.22250056784713,
13.8499521282529));
#444586=CARTESIAN_POINT('Ctrl Pts',(2.37137670564418,-1.2249012167389,13.847639871647));
#444587=CARTESIAN_POINT('Ctrl Pts',(2.37189175084623,-1.22710003394746,
13.8452109780794));
#444588=CARTESIAN_POINT('Ctrl Pts',(2.37212348034353,-1.22808932732284,
13.8441181685877));
#444589=CARTESIAN_POINT('Ctrl Pts',(2.37238795451993,-1.22903815947508,
13.8430021611332));
#444590=CARTESIAN_POINT('Ctrl Pts',(2.37267419372836,-1.22993868335585,
13.8418824960098));
#444591=CARTESIAN_POINT('Ctrl Pts',(2.37334872373239,-1.2320607908766,13.8392439765549));
#444592=CARTESIAN_POINT('Ctrl Pts',(2.37417276041399,-1.23401722378097,
13.8364981347964));
#444593=CARTESIAN_POINT('Ctrl Pts',(2.37511694577178,-1.23582643936874,
13.8336931113419));
#444594=CARTESIAN_POINT('Ctrl Pts',(2.37603652234896,-1.23758850045541,
13.8309611966328));
#444595=CARTESIAN_POINT('Ctrl Pts',(2.37707148810278,-1.23921242281359,
13.8281701127186));
#444596=CARTESIAN_POINT('Ctrl Pts',(2.3782205595477,-1.24068564580899,13.8253580685121));
#444597=CARTESIAN_POINT('Ctrl Pts',(2.37846967947708,-1.24100504214435,
13.8247484142933));
#444598=CARTESIAN_POINT('Ctrl Pts',(2.37872421666962,-1.24131719065112,
13.8241378483365));
#444599=CARTESIAN_POINT('Ctrl Pts',(2.37898422350637,-1.2416216516267,13.8235269408515));
#444600=CARTESIAN_POINT('',(2.3745203792069,-1.20364605708527,12.5969504640361));
#444601=CARTESIAN_POINT('Origin',(2.40515376174178,-1.21931337027842,12.584524458991));
#444602=CARTESIAN_POINT('Origin',(2.40515376174178,-1.21931337027842,12.584524458991));
#444603=CARTESIAN_POINT('Ctrl Pts',(2.40767974839162,-1.1850183503496,12.5893111709658));
#444604=CARTESIAN_POINT('Ctrl Pts',(2.39637714990395,-1.18417579353482,
12.5770542771492));
#444605=CARTESIAN_POINT('Ctrl Pts',(2.39213937462264,-1.19998227750565,
12.5737548217797));
#444606=CARTESIAN_POINT('Ctrl Pts',(2.43239473801938,-1.18686073933307,
12.5663937883685));
#444607=CARTESIAN_POINT('Ctrl Pts',(2.42107772149766,-1.18601710772004,
12.5540940315304));
#444608=CARTESIAN_POINT('Ctrl Pts',(2.41682991585875,-1.20187340434213,
12.5508374392248));
#444609=CARTESIAN_POINT('Ctrl Pts',(2.45708479052556,-1.18870126936863,
12.5434499600945));
#444610=CARTESIAN_POINT('Ctrl Pts',(2.44573097835296,-1.18785489480888,
12.5311293540532));
#444611=CARTESIAN_POINT('Ctrl Pts',(2.44149642401639,-1.20376150708586,
12.5278936106989));
#444612=CARTESIAN_POINT('Ctrl Pts',(2.48175185926909,-1.19054008607023,
12.5204817579905));
#444613=CARTESIAN_POINT('Ctrl Pts',(2.47034185348555,-1.18968952253476,
12.5081597038247));
#444614=CARTESIAN_POINT('Ctrl Pts',(2.46614076809843,-1.20564680696742,
12.5049254088044));
#444615=CARTESIAN_POINT('Ctrl Pts',(2.46401737086259,-1.18921806139777,
12.5369868989719));
#444616=CARTESIAN_POINT('Ctrl Pts',(2.46494629818181,-1.18928730882606,
12.5342545179733));
#444617=CARTESIAN_POINT('Ctrl Pts',(2.46582355050076,-1.18947779631193,
12.5314872231885));
#444618=CARTESIAN_POINT('Ctrl Pts',(2.46658784886818,-1.18983342127685,
12.5287124745063));
#444619=CARTESIAN_POINT('Ctrl Pts',(2.46727713107232,-1.19015414152186,
12.5262100684184));
#444620=CARTESIAN_POINT('Ctrl Pts',(2.4678734336879,-1.19060974170665,12.5237004536639));
#444621=CARTESIAN_POINT('Ctrl Pts',(2.46834674938458,-1.19126072006474,
12.5212220730815));
#444622=CARTESIAN_POINT('Ctrl Pts',(2.46870911349547,-1.19175910031199,
12.5193246583486));
#444623=CARTESIAN_POINT('Ctrl Pts',(2.46900320969055,-1.19237832567575,
12.517417831369));
#444624=CARTESIAN_POINT('Ctrl Pts',(2.46915116612845,-1.1931766198546,12.5155812248347));
#444625=CARTESIAN_POINT('Ctrl Pts',(2.46921419636627,-1.19351669746564,
12.5147988205793));
#444626=CARTESIAN_POINT('Ctrl Pts',(2.46925104144563,-1.19388956733148,
12.5140295443047));
#444627=CARTESIAN_POINT('Ctrl Pts',(2.46925762714412,-1.19430058969269,
12.5132817086137));
#444628=CARTESIAN_POINT('Ctrl Pts',(2.46926759370789,-1.19492261643452,
12.5121499604604));
#444629=CARTESIAN_POINT('Ctrl Pts',(2.46920132248057,-1.19564556957359,
12.5110494206568));
#444630=CARTESIAN_POINT('Ctrl Pts',(2.46902260630554,-1.19647816349771,
12.5100666561695));
#444631=CARTESIAN_POINT('Ctrl Pts',(2.46891998788939,-1.19695623701165,
12.5095023550641));
#444632=CARTESIAN_POINT('Ctrl Pts',(2.46877847216687,-1.19747584612982,
12.5089719619137));
#444633=CARTESIAN_POINT('Ctrl Pts',(2.46859454917871,-1.19802557299053,
12.5085043804652));
#444634=CARTESIAN_POINT('Ctrl Pts',(2.46832540184319,-1.1988300266442,12.5078201359221));
#444635=CARTESIAN_POINT('Ctrl Pts',(2.46795648986139,-1.19972192459933,
12.5072563000949));
#444636=CARTESIAN_POINT('Ctrl Pts',(2.46750499683539,-1.2006375734588,12.5068768744332));
#444637=CARTESIAN_POINT('Ctrl Pts',(2.46717943928276,-1.20129781931997,
12.5066032824114));
#444638=CARTESIAN_POINT('Ctrl Pts',(2.46680527882823,-1.20198204031858,
12.5064197834844));
#444639=CARTESIAN_POINT('Ctrl Pts',(2.46640567747417,-1.20265326796633,
12.5063282718343));
#444640=CARTESIAN_POINT('Ctrl Pts',(2.46582238321068,-1.20363305252523,
12.5061946931565));
#444641=CARTESIAN_POINT('Ctrl Pts',(2.46517332759782,-1.20460663728856,
12.5062515701262));
#444642=CARTESIAN_POINT('Ctrl Pts',(2.46451165944249,-1.20552217804185,
12.5064436508398));
#444643=CARTESIAN_POINT('',(2.39213937462264,-1.19998227750565,12.5737548217797));
#444644=CARTESIAN_POINT('Origin',(2.40604428726529,-1.20695747674297,12.5893111709658));
#444645=CARTESIAN_POINT('Ctrl Pts',(2.46451165944249,-1.20552217804185,
12.5064436508398));
#444646=CARTESIAN_POINT('Ctrl Pts',(2.45379864434455,-1.20470260787252,
12.5164271754438));
#444647=CARTESIAN_POINT('Ctrl Pts',(2.44308139854736,-1.20388250449884,
12.5264061185523));
#444648=CARTESIAN_POINT('Ctrl Pts',(2.43235977297705,-1.20306185008553,
12.536380305637));
#444649=CARTESIAN_POINT('Ctrl Pts',(2.41895991559413,-1.20203619851555,
12.5488460165097));
#444650=CARTESIAN_POINT('Ctrl Pts',(2.40555321307975,-1.20100968589834,
12.5613043021964));
#444651=CARTESIAN_POINT('Ctrl Pts',(2.39213937462264,-1.19998227750565,
12.5737548217797));
#444652=CARTESIAN_POINT('Ctrl Pts',(2.37898422350637,-1.2416216516267,12.5893111709658));
#444653=CARTESIAN_POINT('Ctrl Pts',(2.37162385426224,-1.23300285825699,
12.5770542771492));
#444654=CARTESIAN_POINT('Ctrl Pts',(2.3818686866249,-1.22024170295209,12.5737548217797));
#444655=CARTESIAN_POINT('Ctrl Pts',(2.37211706301871,-1.23358039237507,
12.5928319619712));
#444656=CARTESIAN_POINT('Ctrl Pts',(2.369647757252,-1.2256724251646,12.5821634970843));
#444657=CARTESIAN_POINT('Ctrl Pts',(2.3793599685979,-1.21731859651707,12.5773203894503));
#444658=CARTESIAN_POINT('Ctrl Pts',(2.3675433841839,-1.21746625072075,12.5969440695591));
#444659=CARTESIAN_POINT('Ctrl Pts',(2.36934469270774,-1.21387266892067,
12.5878292599214));
#444660=CARTESIAN_POINT('Ctrl Pts',(2.37773178436604,-1.21157462896802,
12.5813877129824));
#444661=CARTESIAN_POINT('Ctrl Pts',(2.38133036145532,-1.19015152020297,
12.596957478804));
#444662=CARTESIAN_POINT('Ctrl Pts',(2.37954243674436,-1.19371858038985,
12.5878468778671));
#444663=CARTESIAN_POINT('Ctrl Pts',(2.3826716598646,-1.20180099615504,12.5814011370086));
#444664=CARTESIAN_POINT('Ctrl Pts',(2.39711921065734,-1.18423111075633,
12.5928371701607));
#444665=CARTESIAN_POINT('Ctrl Pts',(2.38928857035522,-1.18691739781518,
12.5821692192952));
#444666=CARTESIAN_POINT('Ctrl Pts',(2.38828644232307,-1.19968530920957,
12.5773318885715));
#444667=CARTESIAN_POINT('Ctrl Pts',(2.40767974839162,-1.18501835034955,
12.5893111709658));
#444668=CARTESIAN_POINT('Ctrl Pts',(2.39637714990395,-1.18417579353476,
12.5770542771492));
#444669=CARTESIAN_POINT('Ctrl Pts',(2.39213937462264,-1.19998227750559,
12.5737548217797));
#444670=CARTESIAN_POINT('',(2.3818686866249,-1.22024170295209,12.5737548217797));
#444671=CARTESIAN_POINT('Origin',(2.3957138983066,-1.22733466520273,12.5893111709658));
#444672=CARTESIAN_POINT('Ctrl Pts',(2.39213937462264,-1.19998227750559,
12.5737548217797));
#444673=CARTESIAN_POINT('Ctrl Pts',(2.39114295163672,-1.19987522208008,
12.5746934679442));
#444674=CARTESIAN_POINT('Ctrl Pts',(2.39002077460124,-1.19993889420315,
12.5756680099006));
#444675=CARTESIAN_POINT('Ctrl Pts',(2.38890032675292,-1.20016272513749,
12.5765688348656));
#444676=CARTESIAN_POINT('Ctrl Pts',(2.38860370058883,-1.20022198189947,
12.5768073183026));
#444677=CARTESIAN_POINT('Ctrl Pts',(2.38830720812578,-1.2002922068918,12.5770407398754));
#444678=CARTESIAN_POINT('Ctrl Pts',(2.38801309995349,-1.20037265268661,
12.5772674179684));
#444679=CARTESIAN_POINT('Ctrl Pts',(2.38680615954468,-1.20070278047506,
12.5781976435658));
#444680=CARTESIAN_POINT('Ctrl Pts',(2.38557379676062,-1.20123466340508,
12.5790594849312));
#444681=CARTESIAN_POINT('Ctrl Pts',(2.38441835795147,-1.20197672396998,
12.5797571720116));
#444682=CARTESIAN_POINT('Ctrl Pts',(2.38366554802143,-1.20246020311013,
12.580211740231));
#444683=CARTESIAN_POINT('Ctrl Pts',(2.3829213254678,-1.20307066995689,12.5806009430798));
#444684=CARTESIAN_POINT('Ctrl Pts',(2.3822493163659,-1.20377884820513,12.5808812374708));
#444685=CARTESIAN_POINT('Ctrl Pts',(2.38167183761066,-1.20438740825606,
12.5811221033394));
#444686=CARTESIAN_POINT('Ctrl Pts',(2.3811359452147,-1.20508066080214,12.581287365893));
#444687=CARTESIAN_POINT('Ctrl Pts',(2.38067848261986,-1.20582457696527,
12.581359338449));
#444688=CARTESIAN_POINT('Ctrl Pts',(2.38061490476542,-1.20592796595066,
12.5813693411482));
#444689=CARTESIAN_POINT('Ctrl Pts',(2.38055278326015,-1.20603232094451,
12.5813775999465));
#444690=CARTESIAN_POINT('Ctrl Pts',(2.38049215681373,-1.20613753878369,
12.5813841266931));
#444691=CARTESIAN_POINT('Ctrl Pts',(2.38038929671477,-1.20631605357368,
12.5813952001081));
#444692=CARTESIAN_POINT('Ctrl Pts',(2.38029057882966,-1.2064985516703,12.5814007534795));
#444693=CARTESIAN_POINT('Ctrl Pts',(2.38019621961205,-1.20668504741797,
12.5814005856065));
#444694=CARTESIAN_POINT('Ctrl Pts',(2.37976428000589,-1.20753875203569,
12.5813998171494));
#444695=CARTESIAN_POINT('Ctrl Pts',(2.37945321667912,-1.20841708864965,
12.58127954464));
#444696=CARTESIAN_POINT('Ctrl Pts',(2.37923690376943,-1.20930519271575,
12.5810700125799));
#444697=CARTESIAN_POINT('Ctrl Pts',(2.37897562240372,-1.21037792130886,
12.5808169217085));
#444698=CARTESIAN_POINT('Ctrl Pts',(2.37886881785461,-1.21146895803957,
12.5804173076348));
#444699=CARTESIAN_POINT('Ctrl Pts',(2.3788999318217,-1.2124801490644,12.5799304713245));
#444700=CARTESIAN_POINT('Ctrl Pts',(2.37893849182884,-1.21373333330219,
12.5793271277669));
#444701=CARTESIAN_POINT('Ctrl Pts',(2.37915908797786,-1.21494261000644,
12.5785808224116));
#444702=CARTESIAN_POINT('Ctrl Pts',(2.37952121976358,-1.21606269769621,
12.5777485681082));
#444703=CARTESIAN_POINT('Ctrl Pts',(2.3800608357988,-1.21773175106873,12.576508418016));
#444704=CARTESIAN_POINT('Ctrl Pts',(2.38090363862131,-1.21919082711649,
12.5750928681475));
#444705=CARTESIAN_POINT('Ctrl Pts',(2.3818686866249,-1.22024170295209,12.5737548217797));
#444706=CARTESIAN_POINT('Ctrl Pts',(2.3818686866249,-1.22024170295209,12.5737548217797));
#444707=CARTESIAN_POINT('Ctrl Pts',(2.37162385426224,-1.23300285825699,
12.5770542771492));
#444708=CARTESIAN_POINT('Ctrl Pts',(2.37898422350637,-1.2416216516267,12.5893111709658));
#444709=CARTESIAN_POINT('Ctrl Pts',(2.39798578380574,-1.239036759021,12.5508408821982));
#444710=CARTESIAN_POINT('Ctrl Pts',(2.38770670367268,-1.25183544005648,
12.55409748406));
#444711=CARTESIAN_POINT('Ctrl Pts',(2.39507646286288,-1.26046522879915,
12.5663972313419));
#444712=CARTESIAN_POINT('Ctrl Pts',(2.41408624122604,-1.25781422249849,
12.52790050457));
#444713=CARTESIAN_POINT('Ctrl Pts',(2.40375875059848,-1.27063195297933,
12.5311362602938));
#444714=CARTESIAN_POINT('Ctrl Pts',(2.4111524677942,-1.27928979589865,12.5434568539655));
#444715=CARTESIAN_POINT('Ctrl Pts',(2.4301713414965,-1.27657546956914,12.5049357605811));
#444716=CARTESIAN_POINT('Ctrl Pts',(2.41978320604121,-1.28939615702153,
12.5081700652078));
#444717=CARTESIAN_POINT('Ctrl Pts',(2.42721350978378,-1.29809684179795,
12.5204921097672));
#444718=CARTESIAN_POINT('Ctrl Pts',(2.42911512955617,-1.27534353357769,
12.5064436508395));
#444719=CARTESIAN_POINT('Ctrl Pts',(2.42873988909907,-1.27650458585469,
12.5062361689309));
#444720=CARTESIAN_POINT('Ctrl Pts',(2.42830015988261,-1.27769598412422,
12.5061871075061));
#444721=CARTESIAN_POINT('Ctrl Pts',(2.42781039043223,-1.27882343369142,
12.5063648335164));
#444722=CARTESIAN_POINT('Ctrl Pts',(2.42758790693764,-1.27933559082882,
12.5064455676329));
#444723=CARTESIAN_POINT('Ctrl Pts',(2.42735179220316,-1.27984160766237,
12.506574497099));
#444724=CARTESIAN_POINT('Ctrl Pts',(2.42711121774885,-1.28031934331772,
12.5067492519495));
#444725=CARTESIAN_POINT('Ctrl Pts',(2.42662777404454,-1.28127937166144,
12.5071004286051));
#444726=CARTESIAN_POINT('Ctrl Pts',(2.42610782456531,-1.28216012696854,
12.5076537929612));
#444727=CARTESIAN_POINT('Ctrl Pts',(2.42559853928645,-1.28290031231761,
12.5083435010503));
#444728=CARTESIAN_POINT('Ctrl Pts',(2.42556647673458,-1.28294691140879,
12.5083869222963));
#444729=CARTESIAN_POINT('Ctrl Pts',(2.42553444312098,-1.28299295167391,
12.5084308732336));
#444730=CARTESIAN_POINT('Ctrl Pts',(2.42550244473866,-1.28303841752479,
12.5084753333615));
#444731=CARTESIAN_POINT('Ctrl Pts',(2.42524577547887,-1.28340311365768,
12.508831962269));
#444732=CARTESIAN_POINT('Ctrl Pts',(2.42498721724232,-1.28373899750251,
12.509227847131));
#444733=CARTESIAN_POINT('Ctrl Pts',(2.42473667710823,-1.28403778947644,
12.5096423454524));
#444734=CARTESIAN_POINT('Ctrl Pts',(2.42395159521243,-1.28497407128295,
12.5109411997424));
#444735=CARTESIAN_POINT('Ctrl Pts',(2.42320436570342,-1.28560994088479,
12.5124831113042));
#444736=CARTESIAN_POINT('Ctrl Pts',(2.4225221935559,-1.28603603903853,12.5140723025008));
#444737=CARTESIAN_POINT('Ctrl Pts',(2.42245827327851,-1.28607596490223,
12.5142212114565));
#444738=CARTESIAN_POINT('Ctrl Pts',(2.42239492219652,-1.28611407853466,
12.5143705582413));
#444739=CARTESIAN_POINT('Ctrl Pts',(2.42233216309062,-1.28615047148243,
12.5145201959299));
#444740=CARTESIAN_POINT('Ctrl Pts',(2.42152592893674,-1.28661799308,12.5164425148273));
#444741=CARTESIAN_POINT('Ctrl Pts',(2.42079515218195,-1.28682685455088,
12.5184635205941));
#444742=CARTESIAN_POINT('Ctrl Pts',(2.42011704784669,-1.28686434176596,
12.5205025929158));
#444743=CARTESIAN_POINT('Ctrl Pts',(2.4197237204547,-1.28688608583656,12.5216853356836));
#444744=CARTESIAN_POINT('Ctrl Pts',(2.41934885168665,-1.28685061526725,
12.5228750347131));
#444745=CARTESIAN_POINT('Ctrl Pts',(2.41899380360422,-1.2867761256189,12.5240609649613));
#444746=CARTESIAN_POINT('Ctrl Pts',(2.41812235713356,-1.28659329477327,
12.5269717671326));
#444747=CARTESIAN_POINT('Ctrl Pts',(2.41734792509633,-1.28616008119099,
12.5299036066169));
#444748=CARTESIAN_POINT('Ctrl Pts',(2.41664091150253,-1.28555793178732,
12.5328133004019));
#444749=CARTESIAN_POINT('Ctrl Pts',(2.41630150380934,-1.28526886501145,
12.5342101228451));
#444750=CARTESIAN_POINT('Ctrl Pts',(2.41597839638607,-1.28494082766648,
12.5356023438238));
#444751=CARTESIAN_POINT('Ctrl Pts',(2.41567186698724,-1.28458189015479,
12.5369868989719));
#444752=CARTESIAN_POINT('Origin',(10.6884466934502,-10.9799334864268,-1.23984329704211));
#444753=CARTESIAN_POINT('Ctrl Pts',(2.46397569520746,-1.18921491485979,
12.5369868989719));
#444754=CARTESIAN_POINT('Ctrl Pts',(2.47927000605091,-1.19038425634496,
12.5369868989719));
#444755=CARTESIAN_POINT('Ctrl Pts',(2.48565574447584,-1.17643772815858,
12.5369868989719));
#444756=CARTESIAN_POINT('Ctrl Pts',(2.46914577547705,-1.1896101319952,12.5218025310015));
#444757=CARTESIAN_POINT('Ctrl Pts',(2.48070827525023,-1.18716790704654,
12.5216901060418));
#444758=CARTESIAN_POINT('Ctrl Pts',(2.48563629362352,-1.17648024866413,
12.5161920673677));
#444759=CARTESIAN_POINT('Ctrl Pts',(2.47227858317585,-1.19476004336506,
12.5042015548895));
#444760=CARTESIAN_POINT('Ctrl Pts',(2.47821564607589,-1.19228443654281,
12.4980677368513));
#444761=CARTESIAN_POINT('Ctrl Pts',(2.48115665620399,-1.18615734594856,
12.4907278922778));
#444762=CARTESIAN_POINT('Ctrl Pts',(2.46449369264775,-1.20551338954989,
12.506463626192));
#444763=CARTESIAN_POINT('Ctrl Pts',(2.47037097577434,-1.20838827761489,
12.4999376786891));
#444764=CARTESIAN_POINT('Ctrl Pts',(2.47029919330651,-1.20835316503726,
12.4906970594712));
#444765=CARTESIAN_POINT('Origin',(2.46565283198893,-1.1672789350044,12.5369868989719));
#444766=CARTESIAN_POINT('Origin',(2.46565283198893,-1.1672789350044,14.));
#444767=CARTESIAN_POINT('Origin',(2.46565283198893,-1.1672789350044,13.7435492065112));
#444768=CARTESIAN_POINT('Ctrl Pts',(2.43932577967014,-1.18737738943337,
13.793642941384));
#444769=CARTESIAN_POINT('Ctrl Pts',(2.45010612228422,-1.18820831188987,
13.8071662555867));
#444770=CARTESIAN_POINT('Ctrl Pts',(2.45389707400936,-1.17160565943152,
13.8103758687955));
#444771=CARTESIAN_POINT('Ctrl Pts',(2.4559009113622,-1.18861299236844,13.7804579775006));
#444772=CARTESIAN_POINT('Ctrl Pts',(2.46920365907604,-1.18962816476343,
13.7901904343352));
#444773=CARTESIAN_POINT('Ctrl Pts',(2.47515012965678,-1.17503722881686,
13.7927914348262));
#444774=CARTESIAN_POINT('Ctrl Pts',(2.46565931518457,-1.18934043827937,
13.7597120340895));
#444775=CARTESIAN_POINT('Ctrl Pts',(2.48105477662738,-1.1905095648489,13.7635825532445));
#444776=CARTESIAN_POINT('Ctrl Pts',(2.48768710685466,-1.17703558578182,
13.7651073818884));
#444777=CARTESIAN_POINT('Ctrl Pts',(2.46374839627415,-1.18919798771258,
13.7381884353898));
#444778=CARTESIAN_POINT('Ctrl Pts',(2.47878343019723,-1.19034064494829,
13.7368803041982));
#444779=CARTESIAN_POINT('Ctrl Pts',(2.48523207198161,-1.17664376003763,
13.7363986145813));
#444780=CARTESIAN_POINT('Origin',(2.44498316494277,-1.16573810624294,13.7902182540695));
#444781=CARTESIAN_POINT('Ctrl Pts',(2.40767582314102,-1.18501805697917,
13.8235227101244));
#444782=CARTESIAN_POINT('Ctrl Pts',(2.41914075354885,-1.1858771606184,13.8358800583119));
#444783=CARTESIAN_POINT('Ctrl Pts',(2.42332459279512,-1.1698421508517,13.8390832900376));
#444784=CARTESIAN_POINT('Ctrl Pts',(2.41957039909833,-1.1859047429948,13.8124254819052));
#444785=CARTESIAN_POINT('Ctrl Pts',(2.43105759425929,-1.18676551472373,
13.8247886449157));
#444786=CARTESIAN_POINT('Ctrl Pts',(2.43523022781489,-1.17070594093384,
13.8279860620657));
#444787=CARTESIAN_POINT('Ctrl Pts',(2.43145964429365,-1.18679103162661,
13.8013225099955));
#444788=CARTESIAN_POINT('Ctrl Pts',(2.44296368394646,-1.18765306729825,
13.8136962257787));
#444789=CARTESIAN_POINT('Ctrl Pts',(2.44713033149677,-1.17156960146922,
13.8168830918626));
#444790=CARTESIAN_POINT('Ctrl Pts',(2.44334376613877,-1.18767693833621,
13.7902140179785));
#444791=CARTESIAN_POINT('Ctrl Pts',(2.45485958427629,-1.1885398602146,13.802602731458));
#444792=CARTESIAN_POINT('Ctrl Pts',(2.45902512104727,-1.1724331393835,13.8057746032558));
#444793=CARTESIAN_POINT('Origin',(2.40931520951795,-1.16307922395623,13.8235269408515));
#444794=CARTESIAN_POINT('Ctrl Pts',(2.37898422350637,-1.2416216516267,13.8235269408515));
#444795=CARTESIAN_POINT('Ctrl Pts',(2.38665210203091,-1.25060053004909,
13.8362179249168));
#444796=CARTESIAN_POINT('Ctrl Pts',(2.37563004038642,-1.26364572691086,
13.8391868794938));
#444797=CARTESIAN_POINT('Ctrl Pts',(2.37196844841931,-1.23340636869753,
13.8400110824519));
#444798=CARTESIAN_POINT('Ctrl Pts',(2.37551474770213,-1.24282685829509,
13.8494522556836));
#444799=CARTESIAN_POINT('Ctrl Pts',(2.36416949587685,-1.25005272491833,
13.85569149686));
#444800=CARTESIAN_POINT('Ctrl Pts',(2.36738733885893,-1.21777271393477,
13.8586819406588));
#444801=CARTESIAN_POINT('Ctrl Pts',(2.36543106360686,-1.22166231941259,
13.868010383617));
#444802=CARTESIAN_POINT('Ctrl Pts',(2.3567048712968,-1.22405949161342,13.8744918421245));
#444803=CARTESIAN_POINT('Ctrl Pts',(2.38148881035118,-1.18984029549848,
13.8587686893867));
#444804=CARTESIAN_POINT('Ctrl Pts',(2.38342762446751,-1.18598528217267,
13.8680909899357));
#444805=CARTESIAN_POINT('Ctrl Pts',(2.38018197705652,-1.17756137723557,
13.8745789365163));
#444806=CARTESIAN_POINT('Ctrl Pts',(2.39688877846764,-1.18421393308822,
13.8400379222776));
#444807=CARTESIAN_POINT('Ctrl Pts',(2.40657921166029,-1.18149994369126,
13.8494748685452));
#444808=CARTESIAN_POINT('Ctrl Pts',(2.40570324688965,-1.16808376722457,
13.8557104837033));
#444809=CARTESIAN_POINT('Ctrl Pts',(2.40767974839197,-1.185018350343,13.8235269408542));
#444810=CARTESIAN_POINT('Ctrl Pts',(2.4194545587772,-1.18589610838626,13.8362179249195));
#444811=CARTESIAN_POINT('Ctrl Pts',(2.4234620398536,-1.16929481025995,13.8391868794965));
#444812=CARTESIAN_POINT('Origin',(2.36225454870615,-1.25590863805067,13.8235269408515));
#444813=CARTESIAN_POINT('Ctrl Pts',(2.40220900451924,-1.26881724339398,
13.7902140241683));
#444814=CARTESIAN_POINT('Ctrl Pts',(2.4097118226441,-1.27759598564887,13.8026027327198));
#444815=CARTESIAN_POINT('Ctrl Pts',(2.39918212096335,-1.29047633171518,
13.8057746032556));
#444816=CARTESIAN_POINT('Ctrl Pts',(2.39446994123773,-1.25975500954427,
13.8013225161808));
#444817=CARTESIAN_POINT('Ctrl Pts',(2.40196508250914,-1.2685247749463,13.8136962270464));
#444818=CARTESIAN_POINT('Ctrl Pts',(2.39145479514589,-1.2813922713949,13.8168830918628));
#444819=CARTESIAN_POINT('Ctrl Pts',(2.3867275415764,-1.25068886888398,13.8124254880875));
#444820=CARTESIAN_POINT('Ctrl Pts',(2.39421170688976,-1.25944579440626,
13.8247886461867));
#444821=CARTESIAN_POINT('Ctrl Pts',(2.38372422933855,-1.27230399711159,
13.8279860620656));
#444822=CARTESIAN_POINT('Ctrl Pts',(2.37898167046557,-1.24161866325018,
13.8235227163066));
#444823=CARTESIAN_POINT('Ctrl Pts',(2.38645133002003,-1.25035861573159,
13.8358800595847));
#444824=CARTESIAN_POINT('Ctrl Pts',(2.37599028956742,-1.2632113377564,13.8390832900376));
#444825=CARTESIAN_POINT('Origin',(2.38548189084313,-1.28310722765479,13.7902182540695));
#444826=CARTESIAN_POINT('Ctrl Pts',(2.41549659670382,-1.28437669586829,
13.7382347919292));
#444827=CARTESIAN_POINT('Ctrl Pts',(2.42531461917976,-1.29583637751289,
13.7369371795942));
#444828=CARTESIAN_POINT('Ctrl Pts',(2.41806535003366,-1.30914020680628,
13.7364597369711));
#444829=CARTESIAN_POINT('Ctrl Pts',(2.41672499120129,-1.28581511199128,
13.7595490285574));
#444830=CARTESIAN_POINT('Ctrl Pts',(2.42677649975199,-1.2975488659632,13.7633824266926));
#444831=CARTESIAN_POINT('Ctrl Pts',(2.4198111407926,-1.31086717797616,13.7648920890506));
#444832=CARTESIAN_POINT('Ctrl Pts',(2.41046024656722,-1.27847926856174,
13.780380659011));
#444833=CARTESIAN_POINT('Ctrl Pts',(2.41915854154762,-1.28862503370973,
13.7901039518744));
#444834=CARTESIAN_POINT('Ctrl Pts',(2.41091351991637,-1.30206025085443,
13.7926933640891));
#444835=CARTESIAN_POINT('Ctrl Pts',(2.39957072186774,-1.2657279351651,13.7936647693663));
#444836=CARTESIAN_POINT('Ctrl Pts',(2.4066171141417,-1.27393291462065,13.8072068914933));
#444837=CARTESIAN_POINT('Ctrl Pts',(2.39544599080463,-1.2868112015112,13.8104111085397));
#444838=CARTESIAN_POINT('Origin',(2.39894219218701,-1.29886887657876,13.7435492065112));
#444839=CARTESIAN_POINT('Origin',(2.39894219218701,-1.29886887657876,14.));
#444840=CARTESIAN_POINT('Origin',(2.39894219218701,-1.29886887657876,12.5369868989719));
#444841=CARTESIAN_POINT('Ctrl Pts',(2.42909885324192,-1.27533498811183,
12.506462012331));
#444842=CARTESIAN_POINT('Ctrl Pts',(2.43488807916769,-1.27837447016805,
12.4999388158272));
#444843=CARTESIAN_POINT('Ctrl Pts',(2.43481958503289,-1.27833850910929,
12.4907030323752));
#444844=CARTESIAN_POINT('Ctrl Pts',(2.42502478319153,-1.28796948597993,
12.5042014951932));
#444845=CARTESIAN_POINT('Ctrl Pts',(2.4265374804497,-1.2942187134619,12.4980716682128));
#444846=CARTESIAN_POINT('Ctrl Pts',(2.42333731702239,-1.30020908233739,
12.4907355092744));
#444847=CARTESIAN_POINT('Ctrl Pts',(2.41902011774416,-1.28848880679608,
12.5218047446509));
#444848=CARTESIAN_POINT('Ctrl Pts',(2.42388115369431,-1.29925399144045,
12.5216906929433));
#444849=CARTESIAN_POINT('Ctrl Pts',(2.41817937641594,-1.30954284415575,
12.5161988840775));
#444850=CARTESIAN_POINT('Ctrl Pts',(2.41564689373247,-1.28455269879707,
12.5369868989719));
#444851=CARTESIAN_POINT('Ctrl Pts',(2.4256225952112,-1.29619275513402,12.5369868989719));
#444852=CARTESIAN_POINT('Ctrl Pts',(2.41815742309716,-1.30958218144093,
12.5369868989719));
#444853=CARTESIAN_POINT('Origin',(4.59510497263918E-31,-7.48139013969497E-31,
12.5));
#444854=CARTESIAN_POINT('Origin',(2.47227204101565,-1.04358095837972,12.5));
#444855=CARTESIAN_POINT('',(2.47227204101565,-1.04358095837972,12.5893111709658));
#444856=CARTESIAN_POINT('',(2.47227204101565,-1.04358095837972,13.8235269408515));
#444857=CARTESIAN_POINT('',(2.47227204101565,-1.04358095837972,12.5));
#444858=CARTESIAN_POINT('',(2.49763903363991,-1.06879580290437,13.7902182540695));
#444859=CARTESIAN_POINT('',(2.47227204101565,-1.04358095837972,13.8235269408515));
#444860=CARTESIAN_POINT('',(2.51233926765279,-1.08340786672292,13.7435492065112));
#444861=CARTESIAN_POINT('Origin',(2.46397592170674,-1.03533413886561,13.7445212918693));
#444862=CARTESIAN_POINT('',(2.51233926765279,-1.08340786672292,12.5369868989719));
#444863=CARTESIAN_POINT('',(2.51233926765279,-1.08340786672292,12.5));
#444864=CARTESIAN_POINT('Ctrl Pts',(2.51233926765279,-1.08340786672292,
12.5369868989719));
#444865=CARTESIAN_POINT('Ctrl Pts',(2.49899326630647,-1.07014191305006,
12.5544431401645));
#444866=CARTESIAN_POINT('Ctrl Pts',(2.48563771954526,-1.05686647121454,
12.5718848856037));
#444867=CARTESIAN_POINT('Ctrl Pts',(2.47227204101565,-1.04358095837972,
12.5893111709658));
#444868=CARTESIAN_POINT('Origin',(2.77125127718585,-0.982849258123515,12.5));
#444869=CARTESIAN_POINT('',(2.55275086849393,-0.984420745855523,13.7435492065112));
#444870=CARTESIAN_POINT('',(2.53202438621133,-0.984569813826745,13.7902182540695));
#444871=CARTESIAN_POINT('Origin',(2.47755877302977,-0.984961538690983,13.7418732680449));
#444872=CARTESIAN_POINT('',(2.49625838937557,-0.984827048243774,13.8235269408515));
#444873=CARTESIAN_POINT('',(2.53202438621133,-0.984569813826745,13.7902182540695));
#444874=CARTESIAN_POINT('',(2.49625838937557,-0.984827048243774,12.5893111709658));
#444875=CARTESIAN_POINT('',(2.49625838937557,-0.984827048243774,12.5));
#444876=CARTESIAN_POINT('',(2.55275086849393,-0.984420745855523,12.5369868989719));
#444877=CARTESIAN_POINT('Ctrl Pts',(2.49625838937557,-0.984827048243774,
12.5893111709658));
#444878=CARTESIAN_POINT('Ctrl Pts',(2.51510322538268,-0.984691513354965,
12.5718848856037));
#444879=CARTESIAN_POINT('Ctrl Pts',(2.53393377618058,-0.984556081207524,
12.5544431401645));
#444880=CARTESIAN_POINT('Ctrl Pts',(2.55275086849393,-0.984420745855523,
12.5369868989719));
#444881=CARTESIAN_POINT('',(2.55275086849393,-0.984420745855523,12.5));
#444882=CARTESIAN_POINT('Origin',(2.4965056131406,-1.01920115922006,12.5));
#444883=CARTESIAN_POINT('',(2.46427499032543,-1.0072522209775,13.8587068136939));
#444884=CARTESIAN_POINT('Ctrl Pts',(2.49625838937537,-0.984827048237167,
13.8235269408542));
#444885=CARTESIAN_POINT('Ctrl Pts',(2.49450613636711,-0.984839650703789,
13.8262006681044));
#444886=CARTESIAN_POINT('Ctrl Pts',(2.49271421095855,-0.985026282325426,
13.8288634856214));
#444887=CARTESIAN_POINT('Ctrl Pts',(2.49088698306019,-0.98537434508912,
13.8314912288862));
#444888=CARTESIAN_POINT('Ctrl Pts',(2.4890032995668,-0.985733161897478,
13.8342001611531));
#444889=CARTESIAN_POINT('Ctrl Pts',(2.48707991312608,-0.986263449831712,
13.8368750301949));
#444890=CARTESIAN_POINT('Ctrl Pts',(2.48510989497275,-0.986995062839595,
13.8394886372969));
#444891=CARTESIAN_POINT('Ctrl Pts',(2.48495774569217,-0.987051567086838,
13.8396904925131));
#444892=CARTESIAN_POINT('Ctrl Pts',(2.48480532227872,-0.987109293988284,
13.8398919674349));
#444893=CARTESIAN_POINT('Ctrl Pts',(2.48465262459692,-0.987168268325339,
13.8400930404591));
#444894=CARTESIAN_POINT('Ctrl Pts',(2.48227349198451,-0.988087128172655,
13.8432258934518));
#444895=CARTESIAN_POINT('Ctrl Pts',(2.4798395130573,-0.989303073675097,
13.8462331177034));
#444896=CARTESIAN_POINT('Ctrl Pts',(2.47747318253686,-0.990862744111962,
13.8489036603661));
#444897=CARTESIAN_POINT('Ctrl Pts',(2.4766988916522,-0.9913730864297,13.8497774930041));
#444898=CARTESIAN_POINT('Ctrl Pts',(2.47593209364871,-0.991920229736684,
13.85061494757));
#444899=CARTESIAN_POINT('Ctrl Pts',(2.47517779370455,-0.992505793840622,
13.8514076489583));
#444900=CARTESIAN_POINT('Ctrl Pts',(2.4735823405363,-0.993744346371441,
13.8530843267192));
#444901=CARTESIAN_POINT('Ctrl Pts',(2.4718878999805,-0.995278782199361,
13.8546805203176));
#444902=CARTESIAN_POINT('Ctrl Pts',(2.47028440497422,-0.997121181885222,
13.8559412814274));
#444903=CARTESIAN_POINT('Ctrl Pts',(2.47006980533981,-0.997367754713618,
13.8561100121513));
#444904=CARTESIAN_POINT('Ctrl Pts',(2.46985682318122,-0.997619767556806,
13.8562727473908));
#444905=CARTESIAN_POINT('Ctrl Pts',(2.46964589317334,-0.997877176378507,
13.8564289040185));
#444906=CARTESIAN_POINT('Ctrl Pts',(2.46868932799395,-0.999044522448343,
13.8571370725437));
#444907=CARTESIAN_POINT('Ctrl Pts',(2.46775991462844,-1.00034480439304,
13.8577210840553));
#444908=CARTESIAN_POINT('Ctrl Pts',(2.46691765545993,-1.00174454601251,
13.8581177131616));
#444909=CARTESIAN_POINT('Ctrl Pts',(2.46668044628841,-1.00213876143019,
13.8582294175695));
#444910=CARTESIAN_POINT('Ctrl Pts',(2.46645001871431,-1.00254074616991,
13.8583265086086));
#444911=CARTESIAN_POINT('Ctrl Pts',(2.46622737107116,-1.00294947629639,
13.8584082369006));
#444912=CARTESIAN_POINT('Ctrl Pts',(2.46590748611328,-1.00353671188281,
13.8585256585398));
#444913=CARTESIAN_POINT('Ctrl Pts',(2.46559996750226,-1.00414532668273,
13.8586122832068));
#444914=CARTESIAN_POINT('Ctrl Pts',(2.46531350850406,-1.00475986677822,
13.8586682984299));
#444915=CARTESIAN_POINT('Ctrl Pts',(2.46508436970126,-1.00525143793722,
13.8587131050557));
#444916=CARTESIAN_POINT('Ctrl Pts',(2.46486596234389,-1.00575213068633,
13.8587357943552));
#444917=CARTESIAN_POINT('Ctrl Pts',(2.4646587246829,-1.00626220701203,13.8587355499465));
#444918=CARTESIAN_POINT('Ctrl Pts',(2.4645247820418,-1.00659188150221,13.8587353919793));
#444919=CARTESIAN_POINT('Ctrl Pts',(2.46439691797788,-1.00692189622389,
13.8587257282814));
#444920=CARTESIAN_POINT('Ctrl Pts',(2.46427499032543,-1.0072522209775,13.8587068136939));
#444921=CARTESIAN_POINT('Ctrl Pts',(2.46427499032543,-1.0072522209775,13.8587068136939));
#444922=CARTESIAN_POINT('Ctrl Pts',(2.46387397692363,-1.00833864108392,
13.8586446046466));
#444923=CARTESIAN_POINT('Ctrl Pts',(2.46353709921336,-1.00942841144252,
13.858482427929));
#444924=CARTESIAN_POINT('Ctrl Pts',(2.46326000564278,-1.01052050738079,
13.8582284286032));
#444925=CARTESIAN_POINT('Ctrl Pts',(2.4629757398722,-1.01164087077572,13.8579678548414));
#444926=CARTESIAN_POINT('Ctrl Pts',(2.46275518338507,-1.01276679512489,
13.857615680862));
#444927=CARTESIAN_POINT('Ctrl Pts',(2.46259752251169,-1.0138520289967,13.8571944833187));
#444928=CARTESIAN_POINT('Ctrl Pts',(2.46220406367794,-1.0165603411124,13.8561433417727));
#444929=CARTESIAN_POINT('Ctrl Pts',(2.46217917029009,-1.01914122861999,
13.8546163505475));
#444930=CARTESIAN_POINT('Ctrl Pts',(2.46236829417935,-1.02145731346383,
13.8528973491086));
#444931=CARTESIAN_POINT('Ctrl Pts',(2.46240284432366,-1.02188042799416,
13.8525833129072));
#444932=CARTESIAN_POINT('Ctrl Pts',(2.46244441744383,-1.02229478029566,
13.8522628768812));
#444933=CARTESIAN_POINT('Ctrl Pts',(2.46249193666486,-1.02269965049313,
13.851937733538));
#444934=CARTESIAN_POINT('Ctrl Pts',(2.4627821299547,-1.02517213661585,13.8499521282529));
#444935=CARTESIAN_POINT('Ctrl Pts',(2.46332696587327,-1.02753624269018,
13.847639871647));
#444936=CARTESIAN_POINT('Ctrl Pts',(2.46401952132021,-1.02968576255045,
13.8452109780794));
#444937=CARTESIAN_POINT('Ctrl Pts',(2.46433111635098,-1.03065287602844,
13.8441181685877));
#444938=CARTESIAN_POINT('Ctrl Pts',(2.46467204914031,-1.03157699391933,
13.8430021611332));
#444939=CARTESIAN_POINT('Ctrl Pts',(2.46503073696772,-1.03245119022838,
13.8418824960098));
#444940=CARTESIAN_POINT('Ctrl Pts',(2.46587599399244,-1.03451125615405,
13.8392439765549));
#444941=CARTESIAN_POINT('Ctrl Pts',(2.4668567562043,-1.0363940125498,13.8364981347964));
#444942=CARTESIAN_POINT('Ctrl Pts',(2.46794526772955,-1.0381202482499,13.8336931113419));
#444943=CARTESIAN_POINT('Ctrl Pts',(2.46900540882826,-1.0398014921957,13.8309611966328));
#444944=CARTESIAN_POINT('Ctrl Pts',(2.47016929556687,-1.04133565176911,
13.8281701127186));
#444945=CARTESIAN_POINT('Ctrl Pts',(2.47143462492222,-1.0427103127463,13.8253580685121));
#444946=CARTESIAN_POINT('Ctrl Pts',(2.47170894969204,-1.04300834072974,
13.8247484142932));
#444947=CARTESIAN_POINT('Ctrl Pts',(2.47198808293421,-1.0432987034439,13.8241378483365));
#444948=CARTESIAN_POINT('Ctrl Pts',(2.47227204101566,-1.04358095837972,
13.8235269408515));
#444949=CARTESIAN_POINT('',(2.4647276862865,-1.00609556924708,12.5969504640361));
#444950=CARTESIAN_POINT('Origin',(2.49653617024153,-1.01921384568499,12.584524458991));
#444951=CARTESIAN_POINT('Origin',(2.49653617024153,-1.01921384568499,12.584524458991));
#444952=CARTESIAN_POINT('Ctrl Pts',(2.49625838937557,-0.984827048243774,
12.5893111709658));
#444953=CARTESIAN_POINT('Ctrl Pts',(2.48492472314964,-0.984908561672236,
12.5770542771492));
#444954=CARTESIAN_POINT('Ctrl Pts',(2.48198942389985,-1.00100786889861,
12.5737548217797));
#444955=CARTESIAN_POINT('Ctrl Pts',(2.52104131372023,-0.984648805732449,
12.5663937883685));
#444956=CARTESIAN_POINT('Ctrl Pts',(2.50969318982903,-0.9847304231426,12.5540940315304));
#444957=CARTESIAN_POINT('Ctrl Pts',(2.50675195379035,-1.00088019484002,
12.5508374392248));
#444958=CARTESIAN_POINT('Ctrl Pts',(2.54579923239804,-0.984470743065631,
12.5434499600945));
#444959=CARTESIAN_POINT('Ctrl Pts',(2.53441421171488,-0.984552625843129,
12.5311293540533));
#444960=CARTESIAN_POINT('Ctrl Pts',(2.53149028407887,-1.00075146567008,
12.5278936106989));
#444961=CARTESIAN_POINT('Ctrl Pts',(2.57053410413713,-0.984292846155857,
12.5204817579905));
#444962=CARTESIAN_POINT('Ctrl Pts',(2.55909273538219,-0.984375134197071,
12.5081597038247));
#444963=CARTESIAN_POINT('Ctrl Pts',(2.55620629558159,-1.00062174954219,
12.5049254088044));
#444964=CARTESIAN_POINT('Ctrl Pts',(2.55275086849393,-0.984420745855524,
12.5369868989719));
#444965=CARTESIAN_POINT('Ctrl Pts',(2.5536823491924,-0.984414046668457,
12.5342545179733));
#444966=CARTESIAN_POINT('Ctrl Pts',(2.55457220902511,-0.984532396114919,
12.5314872231885));
#444967=CARTESIAN_POINT('Ctrl Pts',(2.55536295098887,-0.984824540354759,
12.5287124745063));
#444968=CARTESIAN_POINT('Ctrl Pts',(2.55607608134073,-0.985088010530996,
12.5262100684185));
#444969=CARTESIAN_POINT('Ctrl Pts',(2.5567075354532,-0.985493490544782,
12.5237004536639));
#444970=CARTESIAN_POINT('Ctrl Pts',(2.55723233701052,-0.986103723202764,
12.5212220730815));
#444971=CARTESIAN_POINT('Ctrl Pts',(2.5576341180016,-0.986570909091784,
12.5193246583486));
#444972=CARTESIAN_POINT('Ctrl Pts',(2.55797770823161,-0.987164102464083,
12.517417831369));
#444973=CARTESIAN_POINT('Ctrl Pts',(2.55819024074325,-0.987947680561655,
12.5155812248347));
#444974=CARTESIAN_POINT('Ctrl Pts',(2.55828078073558,-0.98828148904297,
12.5147988205793));
#444975=CARTESIAN_POINT('Ctrl Pts',(2.55834789557159,-0.988650114999075,
12.5140295443047));
#444976=CARTESIAN_POINT('Ctrl Pts',(2.5583879614949,-0.989059232921712,
12.5132817086137));
#444977=CARTESIAN_POINT('Ctrl Pts',(2.55844859584983,-0.989678377553405,
12.5121499604604));
#444978=CARTESIAN_POINT('Ctrl Pts',(2.55844147252695,-0.990404326845799,
12.5110494206568));
#444979=CARTESIAN_POINT('Ctrl Pts',(2.55833121514949,-0.991248717409707,
12.5100666561695));
#444980=CARTESIAN_POINT('Ctrl Pts',(2.55826790561726,-0.991733564527043,
12.5095023550641));
#444981=CARTESIAN_POINT('Ctrl Pts',(2.55816921374356,-0.992262979533925,
12.5089719619137));
#444982=CARTESIAN_POINT('Ctrl Pts',(2.55803071058653,-0.992825868654841,
12.5085043804652));
#444983=CARTESIAN_POINT('Ctrl Pts',(2.55782802925753,-0.993649583561836,
12.5078201359221));
#444984=CARTESIAN_POINT('Ctrl Pts',(2.55753304276325,-0.99456858355139,
12.5072563000949));
#444985=CARTESIAN_POINT('Ctrl Pts',(2.55715768592557,-0.995517986537896,
12.5068768744332));
#444986=CARTESIAN_POINT('Ctrl Pts',(2.55688702780595,-0.996202571448291,
12.5066032824114));
#444987=CARTESIAN_POINT('Ctrl Pts',(2.55656988270285,-0.996915013308555,
12.5064197834844));
#444988=CARTESIAN_POINT('Ctrl Pts',(2.55622632227399,-0.997616578721758,
12.5063282718343));
#444989=CARTESIAN_POINT('Ctrl Pts',(2.55572483041147,-0.998640647025872,
12.5061946931565));
#444990=CARTESIAN_POINT('Ctrl Pts',(2.55515729067415,-0.999663896324203,
12.5062515701262));
#444991=CARTESIAN_POINT('Ctrl Pts',(2.55457244923589,-1.00063032278845,
12.5064436508398));
#444992=CARTESIAN_POINT('',(2.48198942389985,-1.00100786889861,12.5737548217797));
#444993=CARTESIAN_POINT('Origin',(2.49641661258519,-1.0068264792686,12.5893111709658));
#444994=CARTESIAN_POINT('Ctrl Pts',(2.55457244923589,-1.00063032278845,
12.5064436508398));
#444995=CARTESIAN_POINT('Ctrl Pts',(2.5438282782346,-1.00068668985652,12.5164271754438));
#444996=CARTESIAN_POINT('Ctrl Pts',(2.53307984715027,-1.00074287033569,
12.5264061185523));
#444997=CARTESIAN_POINT('Ctrl Pts',(2.5223270059513,-1.00079885860094,12.536380305637));
#444998=CARTESIAN_POINT('Ctrl Pts',(2.50888813536377,-1.00086883257686,
12.5488460165097));
#444999=CARTESIAN_POINT('Ctrl Pts',(2.49544237223805,-1.00093850631237,
12.5613043021964));
#445000=CARTESIAN_POINT('Ctrl Pts',(2.48198942389985,-1.00100786889861,
12.5737548217797));
#445001=CARTESIAN_POINT('Ctrl Pts',(2.47227204101565,-1.04358095837972,
12.5893111709658));
#445002=CARTESIAN_POINT('Ctrl Pts',(2.46423365112039,-1.03559078175768,
12.5770542771492));
#445003=CARTESIAN_POINT('Ctrl Pts',(2.47340424202237,-1.02203703919839,
12.5737548217797));
#445004=CARTESIAN_POINT('Ctrl Pts',(2.46477229315759,-1.03612619308624,
12.5928319619712));
#445005=CARTESIAN_POINT('Ctrl Pts',(2.46166663106047,-1.02844581032821,
12.5821634970842));
#445006=CARTESIAN_POINT('Ctrl Pts',(2.4706656112364,-1.0193281429679,12.5773203894503));
#445007=CARTESIAN_POINT('Ctrl Pts',(2.45890038072059,-1.02043846719395,
12.5969440695591));
#445008=CARTESIAN_POINT('Ctrl Pts',(2.46040278526102,-1.01671001937364,
12.5878292599214));
#445009=CARTESIAN_POINT('Ctrl Pts',(2.46857465797361,-1.01373600012724,
12.5813877129824));
#445010=CARTESIAN_POINT('Ctrl Pts',(2.4704150788477,-0.992090857548991,
12.596957478804));
#445011=CARTESIAN_POINT('Ctrl Pts',(2.46892385182892,-0.995791781099588,
12.5878468778671));
#445012=CARTESIAN_POINT('Ctrl Pts',(2.47270145463572,-1.00359224255848,
12.5814011370086));
#445013=CARTESIAN_POINT('Ctrl Pts',(2.48566882362419,-0.984903209989894,
12.5928371701607));
#445014=CARTESIAN_POINT('Ctrl Pts',(2.47808319646526,-0.988218828530895,
12.5821692192952));
#445015=CARTESIAN_POINT('Ctrl Pts',(2.47812510624161,-1.00102593849133,
12.5773318885715));
#445016=CARTESIAN_POINT('Ctrl Pts',(2.49625838937556,-0.984827048243718,
12.5893111709658));
#445017=CARTESIAN_POINT('Ctrl Pts',(2.48492472314964,-0.984908561672181,
12.5770542771492));
#445018=CARTESIAN_POINT('Ctrl Pts',(2.48198942389985,-1.00100786889855,
12.5737548217797));
#445019=CARTESIAN_POINT('',(2.47340424202237,-1.02203703919839,12.5737548217797));
#445020=CARTESIAN_POINT('Origin',(2.48778152717562,-1.02797788691754,12.5893111709658));
#445021=CARTESIAN_POINT('Ctrl Pts',(2.48198942389985,-1.00100786889855,
12.5737548217797));
#445022=CARTESIAN_POINT('Ctrl Pts',(2.48098759041817,-1.00098238741483,
12.5746934679442));
#445023=CARTESIAN_POINT('Ctrl Pts',(2.47987433720332,-1.00113731552034,
12.5756680099006));
#445024=CARTESIAN_POINT('Ctrl Pts',(2.47877586185187,-1.00145172857708,
12.5765688348656));
#445025=CARTESIAN_POINT('Ctrl Pts',(2.47848505266311,-1.00153496595319,
12.5768073183026));
#445026=CARTESIAN_POINT('Ctrl Pts',(2.47819527074308,-1.00162912416589,
12.5770407398754));
#445027=CARTESIAN_POINT('Ctrl Pts',(2.47790869827059,-1.00173327483036,
12.5772674179684));
#445028=CARTESIAN_POINT('Ctrl Pts',(2.47673268233593,-1.00216068099383,
12.5781976435658));
#445029=CARTESIAN_POINT('Ctrl Pts',(2.47554777353394,-1.00279124313488,
12.5790594849312));
#445030=CARTESIAN_POINT('Ctrl Pts',(2.4744566641771,-1.00362501354398,12.5797571720116));
#445031=CARTESIAN_POINT('Ctrl Pts',(2.47374576719832,-1.00416824494522,
12.580211740231));
#445032=CARTESIAN_POINT('Ctrl Pts',(2.47305377969915,-1.00483734156105,
12.5806009430798));
#445033=CARTESIAN_POINT('Ctrl Pts',(2.47244172975373,-1.00559793838503,
12.5808812374708));
#445034=CARTESIAN_POINT('Ctrl Pts',(2.47191577580516,-1.00625154338219,
12.5811221033394));
#445035=CARTESIAN_POINT('Ctrl Pts',(2.47143817306529,-1.00698616939287,
12.581287365893));
#445036=CARTESIAN_POINT('Ctrl Pts',(2.47104286871297,-1.0077648976847,12.581359338449));
#445037=CARTESIAN_POINT('Ctrl Pts',(2.47098792957072,-1.00787312483713,
12.5813693411482));
#445038=CARTESIAN_POINT('Ctrl Pts',(2.47093452067042,-1.00798219607774,
12.5813775999465));
#445039=CARTESIAN_POINT('Ctrl Pts',(2.47088267218419,-1.00809200543144,
12.5813841266931));
#445040=CARTESIAN_POINT('Ctrl Pts',(2.47079470495636,-1.00827831028117,
12.5813952001081));
#445041=CARTESIAN_POINT('Ctrl Pts',(2.47071119083597,-1.00846824755452,
12.5814007534795));
#445042=CARTESIAN_POINT('Ctrl Pts',(2.47063234672565,-1.00866181390519,
12.5814005856065));
#445043=CARTESIAN_POINT('Ctrl Pts',(2.47027142921465,-1.00954788497905,
12.5813998171494));
#445044=CARTESIAN_POINT('Ctrl Pts',(2.47003299351355,-1.01044865354929,
12.58127954464));
#445045=CARTESIAN_POINT('Ctrl Pts',(2.46988978909337,-1.01135143403267,
12.5810700125799));
#445046=CARTESIAN_POINT('Ctrl Pts',(2.46971681445891,-1.0124418900668,12.5808169217085));
#445047=CARTESIAN_POINT('Ctrl Pts',(2.46969929491538,-1.01353800202507,
12.5804173076348));
#445048=CARTESIAN_POINT('Ctrl Pts',(2.46981272680927,-1.01454329231802,
12.5799304713245));
#445049=CARTESIAN_POINT('Ctrl Pts',(2.46995330466054,-1.01578916369008,
12.5793271277669));
#445050=CARTESIAN_POINT('Ctrl Pts',(2.47027173407184,-1.01697643599179,
12.5785808224116));
#445051=CARTESIAN_POINT('Ctrl Pts',(2.47072395843903,-1.01806327957977,
12.5777485681082));
#445052=CARTESIAN_POINT('Ctrl Pts',(2.471397822291,-1.01968279559846,12.576508418016));
#445053=CARTESIAN_POINT('Ctrl Pts',(2.47235674899993,-1.02106832043681,
12.5750928681475));
#445054=CARTESIAN_POINT('Ctrl Pts',(2.47340424202237,-1.02203703919839,
12.5737548217797));
#445055=CARTESIAN_POINT('Ctrl Pts',(2.47340424202237,-1.02203703919839,
12.5737548217797));
#445056=CARTESIAN_POINT('Ctrl Pts',(2.46423365112038,-1.03559078175768,
12.5770542771492));
#445057=CARTESIAN_POINT('Ctrl Pts',(2.47227204101565,-1.04358095837972,
12.5893111709658));
#445058=CARTESIAN_POINT('Ctrl Pts',(2.49099968244631,-1.03945586322464,
12.5508408821982));
#445059=CARTESIAN_POINT('Ctrl Pts',(2.481798016426,-1.05304979816196,12.55409748406));
#445060=CARTESIAN_POINT('Ctrl Pts',(2.48984666124802,-1.061050168203,12.5663972313419));
#445061=CARTESIAN_POINT('Ctrl Pts',(2.50857710451762,-1.05685850949234,
12.52790050457));
#445062=CARTESIAN_POINT('Ctrl Pts',(2.49932874179139,-1.07047537639426,
12.5311362602938));
#445063=CARTESIAN_POINT('Ctrl Pts',(2.50740355157646,-1.07850175446413,
12.5434568539655));
#445064=CARTESIAN_POINT('Ctrl Pts',(2.52613789875103,-1.07424624506223,
12.5049357605811));
#445065=CARTESIAN_POINT('Ctrl Pts',(2.51682933400834,-1.08787100221311,
12.5081700652078));
#445066=CARTESIAN_POINT('Ctrl Pts',(2.52494410061065,-1.09593709744409,
12.5204921097672));
#445067=CARTESIAN_POINT('Ctrl Pts',(2.52498478704876,-1.07310449931469,
12.5064436508395));
#445068=CARTESIAN_POINT('Ctrl Pts',(2.52470543171259,-1.07429227386684,
12.5062361689309));
#445069=CARTESIAN_POINT('Ctrl Pts',(2.52436427567818,-1.07551554987029,
12.5061871075061));
#445070=CARTESIAN_POINT('Ctrl Pts',(2.52396803350171,-1.07667916869908,
12.5063648335164));
#445071=CARTESIAN_POINT('Ctrl Pts',(2.52378803586393,-1.0772077561461,12.5064455676329));
#445072=CARTESIAN_POINT('Ctrl Pts',(2.52359395185131,-1.07773133479322,
12.506574497099));
#445073=CARTESIAN_POINT('Ctrl Pts',(2.52339311777965,-1.078227089874,12.5067492519495));
#445074=CARTESIAN_POINT('Ctrl Pts',(2.52298953391681,-1.07922332895268,
12.5071004286051));
#445075=CARTESIAN_POINT('Ctrl Pts',(2.5225431042606,-1.08014353432877,12.5076537929613));
#445076=CARTESIAN_POINT('Ctrl Pts',(2.52209584556394,-1.0809227682504,12.5083435010505));
#445077=CARTESIAN_POINT('Ctrl Pts',(2.52206768795615,-1.0809718256825,12.5083869222964));
#445078=CARTESIAN_POINT('Ctrl Pts',(2.52203951364083,-1.08102032378924,
12.5084308732337));
#445079=CARTESIAN_POINT('Ctrl Pts',(2.52201132761947,-1.08106824652138,
12.5084753333615));
#445080=CARTESIAN_POINT('Ctrl Pts',(2.52178523852597,-1.08145265008544,
12.5088319622689));
#445081=CARTESIAN_POINT('Ctrl Pts',(2.52155491827216,-1.08180849120113,
12.509227847131));
#445082=CARTESIAN_POINT('Ctrl Pts',(2.52132956610943,-1.08212671031624,
12.5096423454524));
#445083=CARTESIAN_POINT('Ctrl Pts',(2.52062341216811,-1.08312386818513,
12.5109411997424));
#445084=CARTESIAN_POINT('Ctrl Pts',(2.51993049827934,-1.08381852812525,
12.5124831113042));
#445085=CARTESIAN_POINT('Ctrl Pts',(2.51928532695859,-1.08429881183553,
12.5140723025008));
#445086=CARTESIAN_POINT('Ctrl Pts',(2.5192248736992,-1.08434381494523,12.5142212114565));
#445087=CARTESIAN_POINT('Ctrl Pts',(2.51916484002758,-1.08438696545899,
12.5143705582413));
#445088=CARTESIAN_POINT('Ctrl Pts',(2.51910525611052,-1.08442835276199,
12.5145201959299));
#445089=CARTESIAN_POINT('Ctrl Pts',(2.51833981198475,-1.08496003428826,
12.5164425148273));
#445090=CARTESIAN_POINT('Ctrl Pts',(2.51762849097818,-1.08522776587955,
12.518463520594));
#445091=CARTESIAN_POINT('Ctrl Pts',(2.51695569853521,-1.08532040015755,
12.5205025929157));
#445092=CARTESIAN_POINT('Ctrl Pts',(2.51656545225128,-1.08537413171047,
12.5216853356836));
#445093=CARTESIAN_POINT('Ctrl Pts',(2.51618893964744,-1.08536933445125,
12.5228750347131));
#445094=CARTESIAN_POINT('Ctrl Pts',(2.51582900136034,-1.08532403237589,
12.5240609649613));
#445095=CARTESIAN_POINT('Ctrl Pts',(2.51494555214468,-1.08521284086229,
12.5269717671326));
#445096=CARTESIAN_POINT('Ctrl Pts',(2.51413838603744,-1.08484419216298,
12.5299036066169));
#445097=CARTESIAN_POINT('Ctrl Pts',(2.51338464420658,-1.08430167453326,
12.5328133004019));
#445098=CARTESIAN_POINT('Ctrl Pts',(2.51302280423869,-1.08404123448114,
12.5342101228451));
#445099=CARTESIAN_POINT('Ctrl Pts',(2.51267403383975,-1.08374062490796,
12.5356023438238));
#445100=CARTESIAN_POINT('Ctrl Pts',(2.51233926765279,-1.08340786672292,
12.5369868989719));
#445101=CARTESIAN_POINT('Origin',(11.5484677779407,-10.072808883968,-1.24078673491164));
#445102=CARTESIAN_POINT('Ctrl Pts',(2.55270907503905,-0.984421006740184,
12.5369868989719));
#445103=CARTESIAN_POINT('Ctrl Pts',(2.56804780751154,-0.984339829018829,
12.5369868989719));
#445104=CARTESIAN_POINT('Ctrl Pts',(2.5732755263982,-0.969919209790542,
12.5369868989719));
#445105=CARTESIAN_POINT('Ctrl Pts',(2.5578941661586,-0.984393499284525,
12.5218025310015));
#445106=CARTESIAN_POINT('Ctrl Pts',(2.56921912866175,-0.981016949565382,
12.5216901060419));
#445107=CARTESIAN_POINT('Ctrl Pts',(2.57325960608293,-0.969963174237659,
12.5161920673677));
#445108=CARTESIAN_POINT('Ctrl Pts',(2.5614363152843,-0.989270921838109,
12.5042015548895));
#445109=CARTESIAN_POINT('Ctrl Pts',(2.5671518381589,-0.98631962664998,12.4980677368512));
#445110=CARTESIAN_POINT('Ctrl Pts',(2.56958364755384,-0.979973203815791,
12.4907278922778));
#445111=CARTESIAN_POINT('Ctrl Pts',(2.55455382588049,-1.00062302800004,
12.506463626192));
#445112=CARTESIAN_POINT('Ctrl Pts',(2.56064588289877,-1.00300929697532,
12.4999376786891));
#445113=CARTESIAN_POINT('Ctrl Pts',(2.56057147728013,-1.00298015216942,
12.4906970594712));
#445114=CARTESIAN_POINT('Origin',(2.55259264528431,-0.9624213148307,12.5369868989719));
#445115=CARTESIAN_POINT('Origin',(2.55259264528431,-0.962421314830701,14.));
#445116=CARTESIAN_POINT('Origin',(2.55259264528431,-0.962421314830701,13.7435492065112));
#445117=CARTESIAN_POINT('Ctrl Pts',(2.5279914046812,-0.984598792482975,
13.793642941384));
#445118=CARTESIAN_POINT('Ctrl Pts',(2.53880360448866,-0.984548252110673,
13.8071662555867));
#445119=CARTESIAN_POINT('Ctrl Pts',(2.5412286718278,-0.967691845849694,
13.8103758687955));
#445120=CARTESIAN_POINT('Ctrl Pts',(2.54461209709991,-0.98447925694229,
13.7804579775006));
#445121=CARTESIAN_POINT('Ctrl Pts',(2.55795332699271,-0.984406753999513,
13.7901904343352));
#445122=CARTESIAN_POINT('Ctrl Pts',(2.56269071444785,-0.969379675631967,
13.7927914348262));
#445123=CARTESIAN_POINT('Ctrl Pts',(2.55439732423357,-0.984408881832837,
13.7597120340895));
#445124=CARTESIAN_POINT('Ctrl Pts',(2.56983685321751,-0.984319245198071,
13.7635825532445));
#445125=CARTESIAN_POINT('Ctrl Pts',(2.57534886053281,-0.970349503199748,
13.7651073818885));
#445126=CARTESIAN_POINT('Ctrl Pts',(2.55248115270456,-0.984422662889864,
13.7381884353898));
#445127=CARTESIAN_POINT('Ctrl Pts',(2.56755929596518,-0.9843360231847,13.7368803041982));
#445128=CARTESIAN_POINT('Ctrl Pts',(2.5728700571501,-0.970159089356977,
13.7363986145813));
#445129=CARTESIAN_POINT('Origin',(2.53186616300171,-0.962570382801922,13.7902182540695));
#445130=CARTESIAN_POINT('Ctrl Pts',(2.4962544532735,-0.984827075793866,
13.8235227101244));
#445131=CARTESIAN_POINT('Ctrl Pts',(2.50775125999332,-0.984748822573145,
13.8358800583119));
#445132=CARTESIAN_POINT('Ctrl Pts',(2.51061417570188,-0.96842614623922,
13.8390832900376));
#445133=CARTESIAN_POINT('Ctrl Pts',(2.5081817241524,-0.98474129307055,13.8124254819053));
#445134=CARTESIAN_POINT('Ctrl Pts',(2.51970085750601,-0.984662887605033,
13.8247886449158));
#445135=CARTESIAN_POINT('Ctrl Pts',(2.522550602614,-0.968316642350489,13.8279860620657));
#445136=CARTESIAN_POINT('Ctrl Pts',(2.52010364961653,-0.984655548792273,
13.8013225099955));
#445137=CARTESIAN_POINT('Ctrl Pts',(2.53163967443641,-0.984577030081323,
13.8136962257787));
#445138=CARTESIAN_POINT('Ctrl Pts',(2.53448150603402,-0.968207460201438,
13.8168830918626));
#445139=CARTESIAN_POINT('Ctrl Pts',(2.53202043764777,-0.984569841463197,
13.7902140179785));
#445140=CARTESIAN_POINT('Ctrl Pts',(2.54356827399449,-0.984491245954365,
13.802602731458));
#445141=CARTESIAN_POINT('Ctrl Pts',(2.54640710301026,-0.968098588990335,
13.8057746032558));
#445142=CARTESIAN_POINT('Origin',(2.49610016616594,-0.962827617218951,13.8235269408515));
#445143=CARTESIAN_POINT('Ctrl Pts',(2.47227204101566,-1.04358095837972,
13.8235269408515));
#445144=CARTESIAN_POINT('Ctrl Pts',(2.48064626725422,-1.05190495704,13.8362179249168));
#445145=CARTESIAN_POINT('Ctrl Pts',(2.47072418526053,-1.06580514743322,
13.8391868794938));
#445146=CARTESIAN_POINT('Ctrl Pts',(2.46460998851574,-1.03596486192765,
13.8400110824519));
#445147=CARTESIAN_POINT('Ctrl Pts',(2.46891234513801,-1.04506494930942,
13.8494522556836));
#445148=CARTESIAN_POINT('Ctrl Pts',(2.45819381891372,-1.05319151580552,
13.85569149686));
#445149=CARTESIAN_POINT('Ctrl Pts',(2.45876983422057,-1.02075662981956,
13.8586819406588));
#445150=CARTESIAN_POINT('Ctrl Pts',(2.45713710726879,-1.02479274755023,
13.868010383617));
#445151=CARTESIAN_POINT('Ctrl Pts',(2.44863534243242,-1.02789320904161,
13.8744918421245));
#445152=CARTESIAN_POINT('Ctrl Pts',(2.47054763281524,-0.991767753363052,
13.8587686893867));
#445153=CARTESIAN_POINT('Ctrl Pts',(2.4721657763133,-0.987767535926515,
13.8680909899357));
#445154=CARTESIAN_POINT('Ctrl Pts',(2.46824430207023,-0.979636211233281,
13.8745789365163));
#445155=CARTESIAN_POINT('Ctrl Pts',(2.48543775803918,-0.984904871841751,
13.8400379222776));
#445156=CARTESIAN_POINT('Ctrl Pts',(2.49487473178347,-0.981410052753833,
13.8494748685453));
#445157=CARTESIAN_POINT('Ctrl Pts',(2.49290813878161,-0.968109916768434,
13.8557104837033));
#445158=CARTESIAN_POINT('Ctrl Pts',(2.49625838937537,-0.984827048237167,
13.8235269408542));
#445159=CARTESIAN_POINT('Ctrl Pts',(2.50806556547963,-0.984742129254546,
13.8362179249195));
#445160=CARTESIAN_POINT('Ctrl Pts',(2.51070655207712,-0.967869423666875,
13.8391868794965));
#445161=CARTESIAN_POINT('Origin',(2.45676255485569,-1.0591840298419,13.8235269408515));
#445162=CARTESIAN_POINT('Ctrl Pts',(2.4976362366862,-1.06879302379797,13.7902140241683));
#445163=CARTESIAN_POINT('Ctrl Pts',(2.50582963879433,-1.07693100618227,
13.8026027327198));
#445164=CARTESIAN_POINT('Ctrl Pts',(2.49638484160699,-1.09062676239955,
13.8057746032556));
#445165=CARTESIAN_POINT('Ctrl Pts',(2.4891842683109,-1.06039174928721,13.8013225161808));
#445166=CARTESIAN_POINT('Ctrl Pts',(2.49736928741284,-1.06852141042319,
13.8136962270464));
#445167=CARTESIAN_POINT('Ctrl Pts',(2.48794279258032,-1.08220277733172,
13.8168830918628));
#445168=CARTESIAN_POINT('Ctrl Pts',(2.48072865621599,-1.05198685291141,
13.8124254880875));
#445169=CARTESIAN_POINT('Ctrl Pts',(2.48890168931206,-1.06010461153378,
13.8247886461867));
#445170=CARTESIAN_POINT('Ctrl Pts',(2.47949717086747,-1.07377485641174,
13.8279860620656));
#445171=CARTESIAN_POINT('Ctrl Pts',(2.47226925288946,-1.0435781880433,13.8235227163065));
#445172=CARTESIAN_POINT('Ctrl Pts',(2.48042644503294,-1.0516802124552,13.8358800595848));
#445173=CARTESIAN_POINT('Ctrl Pts',(2.47104782899334,-1.06534284002019,
13.8390832900376));
#445174=CARTESIAN_POINT('Origin',(2.48212954747995,-1.08439887436654,13.7902182540695));
#445175=CARTESIAN_POINT('Ctrl Pts',(2.51214785532751,-1.08321764135872,
13.7382347919292));
#445176=CARTESIAN_POINT('Ctrl Pts',(2.52286727958409,-1.09383893188013,
13.7369371795943));
#445177=CARTESIAN_POINT('Ctrl Pts',(2.51672651737721,-1.10768937651337,
13.7364597369711));
#445178=CARTESIAN_POINT('Ctrl Pts',(2.51348940671125,-1.08455114571532,
13.7595490285573));
#445179=CARTESIAN_POINT('Ctrl Pts',(2.52446387957603,-1.09542656532835,
13.7633824266925));
#445180=CARTESIAN_POINT('Ctrl Pts',(2.51860726334418,-1.10926830317516,
13.7648920890506));
#445181=CARTESIAN_POINT('Ctrl Pts',(2.506647568156,-1.07775034654637,13.7803806590111));
#445182=CARTESIAN_POINT('Ctrl Pts',(2.51614389432564,-1.08715336070585,
13.7901039518745));
#445183=CARTESIAN_POINT('Ctrl Pts',(2.50902140224746,-1.10121591907983,
13.7926933640892));
#445184=CARTESIAN_POINT('Ctrl Pts',(2.49475492540219,-1.06592903951609,
13.7936647693663));
#445185=CARTESIAN_POINT('Ctrl Pts',(2.50244665338408,-1.07353237119353,
13.8072068914932));
#445186=CARTESIAN_POINT('Ctrl Pts',(2.49236240097613,-1.08727835690645,
13.8104111085397));
#445187=CARTESIAN_POINT('Origin',(2.49682978149282,-1.0990109381851,13.7435492065112));
#445188=CARTESIAN_POINT('Origin',(2.49682978149282,-1.0990109381851,14.));
#445189=CARTESIAN_POINT('Origin',(2.49682978149282,-1.0990109381851,12.5369868989719));
#445190=CARTESIAN_POINT('Ctrl Pts',(2.52496786835779,-1.07309730895387,
12.506462012331));
#445191=CARTESIAN_POINT('Ctrl Pts',(2.53098557711664,-1.07565480172679,
12.4999388158272));
#445192=CARTESIAN_POINT('Ctrl Pts',(2.53091437973029,-1.07562454323334,
12.4907030323752));
#445193=CARTESIAN_POINT('Ctrl Pts',(2.52193718330867,-1.08602184110352,
12.5042014951932));
#445194=CARTESIAN_POINT('Ctrl Pts',(2.52395421724622,-1.09212697592684,
12.4980716682127));
#445195=CARTESIAN_POINT('Ctrl Pts',(2.52125297277396,-1.09835825537226,
12.4907355092744));
#445196=CARTESIAN_POINT('Ctrl Pts',(2.51599482735783,-1.08702886990104,
12.5218047446509));
#445197=CARTESIAN_POINT('Ctrl Pts',(2.5217171510995,-1.09736201472395,12.5216906929434));
#445198=CARTESIAN_POINT('Ctrl Pts',(2.516872983028,-1.10808137991155,12.5161988840775));
#445199=CARTESIAN_POINT('Ctrl Pts',(2.5123119981278,-1.08338080804912,12.5369868989719));
#445200=CARTESIAN_POINT('Ctrl Pts',(2.52320327893529,-1.09416902077844,
12.5369868989719));
#445201=CARTESIAN_POINT('Ctrl Pts',(2.516854309111,-1.10812237570445,12.5369868989719));
#445202=CARTESIAN_POINT('Origin',(4.76969326057516E-31,-7.09909511483988E-31,
12.5));
#445203=CARTESIAN_POINT('Origin',(2.54910729598815,-0.838595406033455,12.5));
#445204=CARTESIAN_POINT('',(2.54910729598815,-0.838595406033455,12.5893111709658));
#445205=CARTESIAN_POINT('',(2.54910729598815,-0.838595406033455,13.8235269408515));
#445206=CARTESIAN_POINT('',(2.54910729598815,-0.838595406033455,12.5));
#445207=CARTESIAN_POINT('',(2.57644512594904,-0.86165870484848,13.7902182540695));
#445208=CARTESIAN_POINT('',(2.54910729598815,-0.838595406033455,13.8235269408515));
#445209=CARTESIAN_POINT('',(2.59228746499891,-0.875023942687729,13.7435492065112));
#445210=CARTESIAN_POINT('Origin',(2.54016658898052,-0.831052237871044,13.7445212918687));
#445211=CARTESIAN_POINT('',(2.59228746499891,-0.875023942687729,12.5369868989719));
#445212=CARTESIAN_POINT('',(2.59228746499891,-0.875023942687729,12.5));
#445213=CARTESIAN_POINT('Ctrl Pts',(2.59228746499891,-0.875023942687729,
12.5369868989719));
#445214=CARTESIAN_POINT('Ctrl Pts',(2.57790457299166,-0.862889953389305,
12.5544431401645));
#445215=CARTESIAN_POINT('Ctrl Pts',(2.56351139395777,-0.850747285539233,
12.5718848856037));
#445216=CARTESIAN_POINT('Ctrl Pts',(2.54910729598815,-0.838595406033455,
12.5893111709658));
#445217=CARTESIAN_POINT('Origin',(2.84214150603756,-0.753696202164162,12.5));
#445218=CARTESIAN_POINT('',(2.62449623026969,-0.7730722726676,13.7435492065112));
#445219=CARTESIAN_POINT('',(2.60385086407061,-0.774910245348751,13.7902182540695));
#445220=CARTESIAN_POINT('Origin',(2.54959840993456,-0.779740119889402,13.7418732680441));
#445221=CARTESIAN_POINT('',(2.56822484263186,-0.778081884616907,13.8235269408515));
#445222=CARTESIAN_POINT('',(2.60385086407061,-0.774910245348751,13.7902182540695));
#445223=CARTESIAN_POINT('',(2.56822484263186,-0.778081884616907,12.5893111709658));
#445224=CARTESIAN_POINT('',(2.56822484263186,-0.778081884616907,12.5));
#445225=CARTESIAN_POINT('',(2.62449623026969,-0.7730722726676,12.5369868989719));
#445226=CARTESIAN_POINT('Ctrl Pts',(2.56822484263186,-0.778081884616907,
12.5893111709658));
#445227=CARTESIAN_POINT('Ctrl Pts',(2.58699592665007,-0.776410771627757,
12.5718848856037));
#445228=CARTESIAN_POINT('Ctrl Pts',(2.60575278136629,-0.774740925415281,
12.5544431401645));
#445229=CARTESIAN_POINT('Ctrl Pts',(2.62449623026969,-0.7730722726676,12.5369868989719));
#445230=CARTESIAN_POINT('',(2.62449623026969,-0.7730722726676,12.5));
#445231=CARTESIAN_POINT('Origin',(2.57127305293845,-0.812321467542621,12.5));
#445232=CARTESIAN_POINT('',(2.53817572546673,-0.803039383379718,13.8587068136939));
#445233=CARTESIAN_POINT('Ctrl Pts',(2.56822484263113,-0.778081884610338,
13.8235269408542));
#445234=CARTESIAN_POINT('Ctrl Pts',(2.56647944731823,-0.778237270030589,
13.8262006681044));
#445235=CARTESIAN_POINT('Ctrl Pts',(2.56470869660341,-0.778569339207121,
13.8288634856214));
#445236=CARTESIAN_POINT('Ctrl Pts',(2.56291591900165,-0.779065179857554,
13.8314912288862));
#445237=CARTESIAN_POINT('Ctrl Pts',(2.56106775021066,-0.779576340424559,
13.8342001611531));
#445238=CARTESIAN_POINT('Ctrl Pts',(2.55919398706925,-0.780261637720204,
13.8368750301949));
#445239=CARTESIAN_POINT('Ctrl Pts',(2.55729015724091,-0.781151391114411,
13.8394886372969));
#445240=CARTESIAN_POINT('Ctrl Pts',(2.55714311984523,-0.781220108927285,
13.8396904925131));
#445241=CARTESIAN_POINT('Ctrl Pts',(2.55699590888648,-0.781290067670456,
13.8398919674349));
#445242=CARTESIAN_POINT('Ctrl Pts',(2.55684852624958,-0.781361292053912,
13.8400930404591));
#445243=CARTESIAN_POINT('Ctrl Pts',(2.55455220561251,-0.782471015865588,
13.8432258934518));
#445244=CARTESIAN_POINT('Ctrl Pts',(2.55222543639613,-0.783881307288202,
13.8462331177034));
#445245=CARTESIAN_POINT('Ctrl Pts',(2.54999410726517,-0.785628665955706,
13.8489036603661));
#445246=CARTESIAN_POINT('Ctrl Pts',(2.54926399040623,-0.78620042204675,
13.849777493004));
#445247=CARTESIAN_POINT('Ctrl Pts',(2.54854434111879,-0.786808245935407,
13.85061494757));
#445248=CARTESIAN_POINT('Ctrl Pts',(2.54784027995605,-0.787453344071125,
13.8514076489583));
#445249=CARTESIAN_POINT('Ctrl Pts',(2.54635108905603,-0.788817819665242,
13.8530843267192));
#445250=CARTESIAN_POINT('Ctrl Pts',(2.54478735737639,-0.790485262420232,
13.8546805203176));
#445251=CARTESIAN_POINT('Ctrl Pts',(2.54333937054587,-0.792452231402247,
13.8559412814273));
#445252=CARTESIAN_POINT('Ctrl Pts',(2.54314558294863,-0.792715475642356,
13.8561100121513));
#445253=CARTESIAN_POINT('Ctrl Pts',(2.54295385085688,-0.792984009956763,
13.8562727473908));
#445254=CARTESIAN_POINT('Ctrl Pts',(2.54276460390983,-0.793257755025675,
13.8564289040185));
#445255=CARTESIAN_POINT('Ctrl Pts',(2.54190637116397,-0.794499185790202,
13.8571370725437));
#445256=CARTESIAN_POINT('Ctrl Pts',(2.54108603539448,-0.795870896971541,
13.8577210840554));
#445257=CARTESIAN_POINT('Ctrl Pts',(2.54036067071043,-0.797334633007628,
13.8581177131616));
#445258=CARTESIAN_POINT('Ctrl Pts',(2.54015638304911,-0.797746871455648,
13.8582294175695));
#445259=CARTESIAN_POINT('Ctrl Pts',(2.53995948769189,-0.798166300610782,
13.8583265086086));
#445260=CARTESIAN_POINT('Ctrl Pts',(2.53977089619018,-0.798591818571351,
13.8584082369006));
#445261=CARTESIAN_POINT('Ctrl Pts',(2.53949994077503,-0.799203173773543,
13.8585256585398));
#445262=CARTESIAN_POINT('Ctrl Pts',(2.53924305316311,-0.799834829079575,
13.8586122832068));
#445263=CARTESIAN_POINT('Ctrl Pts',(2.53900763805649,-0.80047067341131,
13.8586682984299));
#445264=CARTESIAN_POINT('Ctrl Pts',(2.53881932930715,-0.800979285847475,
13.8587131050557));
#445265=CARTESIAN_POINT('Ctrl Pts',(2.5386424597895,-0.801496114809985,
13.8587357943552));
#445266=CARTESIAN_POINT('Ctrl Pts',(2.53847748765059,-0.802021385692067,
13.8587355499465));
#445267=CARTESIAN_POINT('Ctrl Pts',(2.53837086222413,-0.802360880786095,
13.8587353919793));
#445268=CARTESIAN_POINT('Ctrl Pts',(2.53827032288092,-0.80270021951906,
13.8587257282814));
#445269=CARTESIAN_POINT('Ctrl Pts',(2.53817572546673,-0.803039383379718,
13.8587068136939));
#445270=CARTESIAN_POINT('Ctrl Pts',(2.53817572546673,-0.803039383379718,
13.8587068136939));
#445271=CARTESIAN_POINT('Ctrl Pts',(2.53786459972836,-0.804154874828118,
13.8586446046466));
#445272=CARTESIAN_POINT('Ctrl Pts',(2.53761766935199,-0.805268477726748,
13.858482427929));
#445273=CARTESIAN_POINT('Ctrl Pts',(2.53743051374488,-0.806379525504473,
13.8582284286032));
#445274=CARTESIAN_POINT('Ctrl Pts',(2.53723851386283,-0.807519331281929,
13.8579678548414));
#445275=CARTESIAN_POINT('Ctrl Pts',(2.53711046454625,-0.808659486611959,
13.857615680862));
#445276=CARTESIAN_POINT('Ctrl Pts',(2.53704178491179,-0.809753960282416,
13.8571944833187));
#445277=CARTESIAN_POINT('Ctrl Pts',(2.53687038786002,-0.812485331260639,
13.8561433417727));
#445278=CARTESIAN_POINT('Ctrl Pts',(2.53705594359453,-0.815059660120175,
13.8546163505474));
#445279=CARTESIAN_POINT('Ctrl Pts',(2.53743322060591,-0.817352623030055,
13.8528973491086));
#445280=CARTESIAN_POINT('Ctrl Pts',(2.53750214354969,-0.817771513524167,
13.8525833129072));
#445281=CARTESIAN_POINT('Ctrl Pts',(2.53757735189796,-0.818181098507309,
13.8522628768812));
#445282=CARTESIAN_POINT('Ctrl Pts',(2.53765771368243,-0.818580748274922,
13.851937733538));
#445283=CARTESIAN_POINT('Ctrl Pts',(2.53814847195048,-0.821021353956894,
13.8499521282529));
#445284=CARTESIAN_POINT('Ctrl Pts',(2.53888419156482,-0.823333184477915,
13.847639871647));
#445285=CARTESIAN_POINT('Ctrl Pts',(2.53974964841443,-0.825419102289882,
13.8452109780794));
#445286=CARTESIAN_POINT('Ctrl Pts',(2.54013903536514,-0.826357599889833,
13.8441181685877));
#445287=CARTESIAN_POINT('Ctrl Pts',(2.54055415791594,-0.827250853667279,
13.8430021611332));
#445288=CARTESIAN_POINT('Ctrl Pts',(2.54098290735402,-0.828092904772393,
13.8418824960098));
#445289=CARTESIAN_POINT('Ctrl Pts',(2.54199326635338,-0.83007721970415,
13.8392439765549));
#445290=CARTESIAN_POINT('Ctrl Pts',(2.54312422728481,-0.831873770158096,
13.8364981347964));
#445291=CARTESIAN_POINT('Ctrl Pts',(2.5443498211129,-0.83350553815676,13.8336931113419));
#445292=CARTESIAN_POINT('Ctrl Pts',(2.54554347166906,-0.835094776560609,
13.8309611966327));
#445293=CARTESIAN_POINT('Ctrl Pts',(2.54682853391824,-0.836528963770409,
13.8281701127185));
#445294=CARTESIAN_POINT('Ctrl Pts',(2.54820170062591,-0.837795914587397,
13.825358068512));
#445295=CARTESIAN_POINT('Ctrl Pts',(2.54849940465008,-0.838070590891845,
13.8247484142932));
#445296=CARTESIAN_POINT('Ctrl Pts',(2.54880127635621,-0.838337235497436,
13.8241378483365));
#445297=CARTESIAN_POINT('Ctrl Pts',(2.54910729598815,-0.838595406033455,
13.8235269408515));
#445298=CARTESIAN_POINT('',(2.5385326372653,-0.801849681389652,12.5969504640361));
#445299=CARTESIAN_POINT('Origin',(2.57130454242783,-0.812331621106978,12.584524458991));
#445300=CARTESIAN_POINT('Origin',(2.57130454242783,-0.812331621106978,12.584524458991));
#445301=CARTESIAN_POINT('Ctrl Pts',(2.56822484263186,-0.778081884616907,
12.5893111709658));
#445302=CARTESIAN_POINT('Ctrl Pts',(2.55693553234649,-0.779086925830197,
12.5770542771492));
#445303=CARTESIAN_POINT('Ctrl Pts',(2.55532224306044,-0.79537191807872,
12.5737548217797));
#445304=CARTESIAN_POINT('Ctrl Pts',(2.59291077542083,-0.775884196785299,
12.5663937883685));
#445305=CARTESIAN_POINT('Ctrl Pts',(2.58160706405235,-0.77689052006824,
12.5540940315304));
#445306=CARTESIAN_POINT('Ctrl Pts',(2.57999197105446,-0.793226292774825,
12.5508374392248));
#445307=CARTESIAN_POINT('Ctrl Pts',(2.61757180040624,-0.77368872639377,
12.5434499600945));
#445308=CARTESIAN_POINT('Ctrl Pts',(2.60623133664677,-0.774698321592072,
12.5311293540533));
#445309=CARTESIAN_POINT('Ctrl Pts',(2.60463749396728,-0.791081588362601,
12.5278936106989));
#445310=CARTESIAN_POINT('Ctrl Pts',(2.64220986865041,-0.771495299747208,
12.5204817579905));
#445311=CARTESIAN_POINT('Ctrl Pts',(2.63081327734545,-0.772509891751767,
12.5081597038247));
#445312=CARTESIAN_POINT('Ctrl Pts',(2.62926069191201,-0.788937719464725,
12.5049254088044));
#445313=CARTESIAN_POINT('Ctrl Pts',(2.62449623026969,-0.773072272667601,
12.5369868989719));
#445314=CARTESIAN_POINT('Ctrl Pts',(2.62542406549704,-0.772989671447156,
12.5342545179733));
#445315=CARTESIAN_POINT('Ctrl Pts',(2.62632061097316,-0.773035095258176,
12.5314872231885));
#445316=CARTESIAN_POINT('Ctrl Pts',(2.62713253427595,-0.773261814601223,
12.5287124745063));
#445317=CARTESIAN_POINT('Ctrl Pts',(2.62786476701068,-0.773466281358128,
12.5262100684184));
#445318=CARTESIAN_POINT('Ctrl Pts',(2.6285271703971,-0.773818942798318,
12.5237004536639));
#445319=CARTESIAN_POINT('Ctrl Pts',(2.62909996534728,-0.774384368758529,
12.5212220730815));
#445320=CARTESIAN_POINT('Ctrl Pts',(2.62953848943233,-0.774817251244295,
12.5193246583487));
#445321=CARTESIAN_POINT('Ctrl Pts',(2.62992928716097,-0.775380465021055,
12.5174178313692));
#445322=CARTESIAN_POINT('Ctrl Pts',(2.63020498137755,-0.776144112454325,
12.515581224835));
#445323=CARTESIAN_POINT('Ctrl Pts',(2.6303224285957,-0.776469430365577,
12.5147988205795));
#445324=CARTESIAN_POINT('Ctrl Pts',(2.63041936655023,-0.776831359267061,
12.5140295443048));
#445325=CARTESIAN_POINT('Ctrl Pts',(2.63049264606625,-0.777235850138907,
12.5132817086137));
#445326=CARTESIAN_POINT('Ctrl Pts',(2.6306035447007,-0.777847992355085,
12.5121499604604));
#445327=CARTESIAN_POINT('Ctrl Pts',(2.6306556166868,-0.77857210672806,12.5110494206568));
#445328=CARTESIAN_POINT('Ctrl Pts',(2.63061455185156,-0.779422674651865,
12.5100666561695));
#445329=CARTESIAN_POINT('Ctrl Pts',(2.63059097251774,-0.77991106879503,
12.5095023550641));
#445330=CARTESIAN_POINT('Ctrl Pts',(2.63053576127102,-0.780446766521068,
12.5089719619137));
#445331=CARTESIAN_POINT('Ctrl Pts',(2.63044359966078,-0.781019071967967,
12.5085043804652));
#445332=CARTESIAN_POINT('Ctrl Pts',(2.6303087331491,-0.781856566441477,
12.5078201359221));
#445333=CARTESIAN_POINT('Ctrl Pts',(2.63008963522878,-0.782796552672182,
12.5072563000949));
#445334=CARTESIAN_POINT('Ctrl Pts',(2.62979291251723,-0.783773391665485,
12.5068768744332));
#445335=CARTESIAN_POINT('Ctrl Pts',(2.62957895501575,-0.784477759825482,
12.5066032824114));
#445336=CARTESIAN_POINT('Ctrl Pts',(2.62932093581241,-0.785213681364361,
12.5064197834844));
#445337=CARTESIAN_POINT('Ctrl Pts',(2.62903570264673,-0.785940915740938,
12.5063282718343));
#445338=CARTESIAN_POINT('Ctrl Pts',(2.62861935053079,-0.787002452784669,
12.5061946931565));
#445339=CARTESIAN_POINT('Ctrl Pts',(2.62813710355232,-0.788068557062745,
12.5062515701262));
#445340=CARTESIAN_POINT('Ctrl Pts',(2.6276329808544,-0.789079437829282,
12.5064436508398));
#445341=CARTESIAN_POINT('',(2.55532224306044,-0.79537191807872,12.5737548217797));
#445342=CARTESIAN_POINT('Origin',(2.57017569722808,-0.799995217689364,12.5893111709658));
#445343=CARTESIAN_POINT('Ctrl Pts',(2.6276329808544,-0.789079437829282,
12.5064436508398));
#445344=CARTESIAN_POINT('Ctrl Pts',(2.61692915463513,-0.790011367021186,
12.5164271754438));
#445345=CARTESIAN_POINT('Ctrl Pts',(2.60622106729915,-0.790943457481382,
12.5264061185523));
#445346=CARTESIAN_POINT('Ctrl Pts',(2.59550856885561,-0.791875715832526,
12.536380305637));
#445347=CARTESIAN_POINT('Ctrl Pts',(2.58212011852998,-0.79304084968909,
12.5488460165097));
#445348=CARTESIAN_POINT('Ctrl Pts',(2.56872477412813,-0.794206246110122,
12.5613043021964));
#445349=CARTESIAN_POINT('Ctrl Pts',(2.55532224306044,-0.79537191807872,
12.5737548217797));
#445350=CARTESIAN_POINT('Ctrl Pts',(2.54910729598815,-0.838595406033455,
12.5893111709658));
#445351=CARTESIAN_POINT('Ctrl Pts',(2.54044437960026,-0.83128701946622,
12.5770542771492));
#445352=CARTESIAN_POINT('Ctrl Pts',(2.54847970027215,-0.81703088757307,
12.5737548217797));
#445353=CARTESIAN_POINT('Ctrl Pts',(2.54102487034432,-0.831776744931215,
12.5928319619712));
#445354=CARTESIAN_POINT('Ctrl Pts',(2.53730351958565,-0.824375058305697,
12.5821634970843));
#445355=CARTESIAN_POINT('Ctrl Pts',(2.54552938186325,-0.814554228804583,
12.5773203894503));
#445356=CARTESIAN_POINT('Ctrl Pts',(2.53389380091358,-0.816619834028473,
12.5969440695591));
#445357=CARTESIAN_POINT('Ctrl Pts',(2.53508730321628,-0.812781332393018,
12.5878292599214));
#445358=CARTESIAN_POINT('Ctrl Pts',(2.54298957451851,-0.809151125460285,
12.5813877129824));
#445359=CARTESIAN_POINT('Ctrl Pts',(2.54305959148014,-0.787427993921494,
12.596957478804));
#445360=CARTESIAN_POINT('Ctrl Pts',(2.54187498602332,-0.791238151800188,
12.5878468778671));
#445361=CARTESIAN_POINT('Ctrl Pts',(2.54627582919326,-0.798704748168761,
12.5814011370086));
#445362=CARTESIAN_POINT('Ctrl Pts',(2.5576767206763,-0.779020940858569,
12.5928371701607));
#445363=CARTESIAN_POINT('Ctrl Pts',(2.55038658775776,-0.782943825987378,
12.5821692192952));
#445364=CARTESIAN_POINT('Ctrl Pts',(2.55147225643998,-0.795704905310084,
12.5773318885715));
#445365=CARTESIAN_POINT('Ctrl Pts',(2.56822484263185,-0.778081884616852,
12.5893111709658));
#445366=CARTESIAN_POINT('Ctrl Pts',(2.55693553234648,-0.779086925830142,
12.5770542771492));
#445367=CARTESIAN_POINT('Ctrl Pts',(2.55532224306043,-0.795371918078664,
12.5737548217797));
#445368=CARTESIAN_POINT('',(2.54847970027215,-0.81703088757307,12.5737548217797));
#445369=CARTESIAN_POINT('Origin',(2.56329338043634,-0.821780085399321,12.5893111709658));
#445370=CARTESIAN_POINT('Ctrl Pts',(2.55532224306043,-0.795371918078664,
12.5737548217797));
#445371=CARTESIAN_POINT('Ctrl Pts',(2.55432166611954,-0.795428180111798,
12.5746934679442));
#445372=CARTESIAN_POINT('Ctrl Pts',(2.55322474524181,-0.795673333178764,
12.5756680099006));
#445373=CARTESIAN_POINT('Ctrl Pts',(2.55215555255946,-0.796076235990892,
12.5765688348656));
#445374=CARTESIAN_POINT('Ctrl Pts',(2.55187249563317,-0.79618290005012,
12.5768073183026));
#445375=CARTESIAN_POINT('Ctrl Pts',(2.55159135270704,-0.79630036487582,
12.5770407398754));
#445376=CARTESIAN_POINT('Ctrl Pts',(2.55131422302685,-0.796427527304466,
12.5772674179684));
#445377=CARTESIAN_POINT('Ctrl Pts',(2.55017695775837,-0.796949367525463,
12.5781976435658));
#445378=CARTESIAN_POINT('Ctrl Pts',(2.54904738831101,-0.797674412590524,
12.5790594849312));
#445379=CARTESIAN_POINT('Ctrl Pts',(2.54802786955923,-0.798594344239317,
12.5797571720116));
#445380=CARTESIAN_POINT('Ctrl Pts',(2.54736361643382,-0.7991937127863,12.580211740231));
#445381=CARTESIAN_POINT('Ctrl Pts',(2.54672846905175,-0.799916986443622,
12.5806009430798));
#445382=CARTESIAN_POINT('Ctrl Pts',(2.54618045135423,-0.800724940196953,
12.5808812374708));
#445383=CARTESIAN_POINT('Ctrl Pts',(2.54570952234908,-0.801419240506932,
12.5811221033394));
#445384=CARTESIAN_POINT('Ctrl Pts',(2.54529338763273,-0.802190351167311,
12.581287365893));
#445385=CARTESIAN_POINT('Ctrl Pts',(2.54496287220817,-0.802998709279525,
12.581359338449));
#445386=CARTESIAN_POINT('Ctrl Pts',(2.54491693738904,-0.803111054365166,
12.5813693411482));
#445387=CARTESIAN_POINT('Ctrl Pts',(2.54487259652113,-0.803224116001412,
12.5813775999465));
#445388=CARTESIAN_POINT('Ctrl Pts',(2.54482987103821,-0.803337786106517,
12.5813841266931));
#445389=CARTESIAN_POINT('Ctrl Pts',(2.5447573820889,-0.803530641187942,
12.5813952001081));
#445390=CARTESIAN_POINT('Ctrl Pts',(2.54468962750592,-0.803726753636801,
12.5814007534795));
#445391=CARTESIAN_POINT('Ctrl Pts',(2.54462682319744,-0.803926102438358,
12.5814005856065));
#445392=CARTESIAN_POINT('Ctrl Pts',(2.54433932962808,-0.804838643311557,
12.5813998171494));
#445393=CARTESIAN_POINT('Ctrl Pts',(2.54417510830291,-0.805755849371853,
12.58127954464));
#445394=CARTESIAN_POINT('Ctrl Pts',(2.54410596537402,-0.806667298417337,
12.5810700125799));
#445395=CARTESIAN_POINT('Ctrl Pts',(2.54402244858848,-0.807768225087497,
12.5808169217085));
#445396=CARTESIAN_POINT('Ctrl Pts',(2.54409433064018,-0.808862117829087,
12.5804173076348));
#445397=CARTESIAN_POINT('Ctrl Pts',(2.54428932559034,-0.809854817349115,
12.5799304713245));
#445398=CARTESIAN_POINT('Ctrl Pts',(2.54453098576334,-0.811085084787029,
12.5793271277669));
#445399=CARTESIAN_POINT('Ctrl Pts',(2.54494512934173,-0.812242451584925,
12.5785808224116));
#445400=CARTESIAN_POINT('Ctrl Pts',(2.54548443681182,-0.81328881830635,
12.5777485681082));
#445401=CARTESIAN_POINT('Ctrl Pts',(2.5462880640278,-0.814848019359306,
12.576508418016));
#445402=CARTESIAN_POINT('Ctrl Pts',(2.54735673312412,-0.81615077254903,
12.5750928681475));
#445403=CARTESIAN_POINT('Ctrl Pts',(2.54847970027215,-0.81703088757307,
12.5737548217797));
#445404=CARTESIAN_POINT('Ctrl Pts',(2.54847970027215,-0.81703088757307,
12.5737548217797));
#445405=CARTESIAN_POINT('Ctrl Pts',(2.54044437960026,-0.831287019466221,
12.5770542771492));
#445406=CARTESIAN_POINT('Ctrl Pts',(2.54910729598815,-0.838595406033455,
12.5893111709658));
#445407=CARTESIAN_POINT('Ctrl Pts',(2.5674363891862,-0.832957560156687,
12.5508408821982));
#445408=CARTESIAN_POINT('Ctrl Pts',(2.5593733728478,-0.847256283601681,
12.55409748406));
#445409=CARTESIAN_POINT('Ctrl Pts',(2.56804734089832,-0.854573993798405,
12.5663972313419));
#445410=CARTESIAN_POINT('Ctrl Pts',(2.58637380106472,-0.848869577474897,
12.52790050457));
#445411=CARTESIAN_POINT('Ctrl Pts',(2.57826611256788,-0.863194962795343,
12.5311362602938));
#445412=CARTESIAN_POINT('Ctrl Pts',(2.58696827841544,-0.870536461793924,
12.5434568539655));
#445413=CARTESIAN_POINT('Ctrl Pts',(2.60529342507279,-0.86476808903258,
12.5049357605811));
#445414=CARTESIAN_POINT('Ctrl Pts',(2.59712637800524,-0.87910624537103,
12.5081700652078));
#445415=CARTESIAN_POINT('Ctrl Pts',(2.60587160503441,-0.886484072523638,
12.5204921097672));
#445416=CARTESIAN_POINT('Ctrl Pts',(2.60405108737671,-0.86372413165853,
12.5064436508395));
#445417=CARTESIAN_POINT('Ctrl Pts',(2.60386947622514,-0.864930724042148,
12.5062361689309));
#445418=CARTESIAN_POINT('Ctrl Pts',(2.60362916370991,-0.866177737079556,
12.5061871075061));
#445419=CARTESIAN_POINT('Ctrl Pts',(2.60332908573365,-0.867369781478595,
12.5063648335164));
#445420=CARTESIAN_POINT('Ctrl Pts',(2.60319277180725,-0.867911281572986,
12.5064455676329));
#445421=CARTESIAN_POINT('Ctrl Pts',(2.60304201011359,-0.868448937704168,
12.506574497099));
#445422=CARTESIAN_POINT('Ctrl Pts',(2.60288225294218,-0.868959413042104,
12.5067492519495));
#445423=CARTESIAN_POINT('Ctrl Pts',(2.60256121470493,-0.869985233048843,
12.5071004286051));
#445424=CARTESIAN_POINT('Ctrl Pts',(2.60219127578753,-0.87093876467881,
12.5076537929612));
#445425=CARTESIAN_POINT('Ctrl Pts',(2.601809020106,-0.871751861499721,12.5083435010503));
#445426=CARTESIAN_POINT('Ctrl Pts',(2.60178495482643,-0.871803050803785,
12.5083869222963));
#445427=CARTESIAN_POINT('Ctrl Pts',(2.60176082730472,-0.871853684005415,
12.5084308732336));
#445428=CARTESIAN_POINT('Ctrl Pts',(2.60173664121753,-0.871903744701114,
12.5084753333615));
#445429=CARTESIAN_POINT('Ctrl Pts',(2.60154263687595,-0.872305297554053,
12.508831962269));
#445430=CARTESIAN_POINT('Ctrl Pts',(2.60134208734818,-0.872678727876636,
12.509227847131));
#445431=CARTESIAN_POINT('Ctrl Pts',(2.60114342283827,-0.873014256437226,
12.5096423454524));
#445432=CARTESIAN_POINT('Ctrl Pts',(2.60052089618941,-0.874065654447397,
12.5109411997424));
#445433=CARTESIAN_POINT('Ctrl Pts',(2.59988690914847,-0.874814481878505,
12.5124831113042));
#445434=CARTESIAN_POINT('Ctrl Pts',(2.59928303216319,-0.875345754936481,
12.5140723025008));
#445435=CARTESIAN_POINT('Ctrl Pts',(2.59922644822826,-0.8753955358039,12.5142212114565));
#445436=CARTESIAN_POINT('Ctrl Pts',(2.5991701314812,-0.875443436039455,
12.5143705582413));
#445437=CARTESIAN_POINT('Ctrl Pts',(2.59911411927412,-0.875489542272007,
12.5145201959299));
#445438=CARTESIAN_POINT('Ctrl Pts',(2.59839455908081,-0.876081845474152,
12.5164425148273));
#445439=CARTESIAN_POINT('Ctrl Pts',(2.5977074275464,-0.876406665476267,
12.5184635205941));
#445440=CARTESIAN_POINT('Ctrl Pts',(2.59704442431841,-0.876553830351355,
12.5205025929158));
#445441=CARTESIAN_POINT('Ctrl Pts',(2.59665985616718,-0.876639191811976,
12.5216853356836));
#445442=CARTESIAN_POINT('Ctrl Pts',(2.59628420535681,-0.87666509978783,
12.5228750347131));
#445443=CARTESIAN_POINT('Ctrl Pts',(2.59592177219496,-0.876649286763289,
12.5240609649613));
#445444=CARTESIAN_POINT('Ctrl Pts',(2.59503219944308,-0.876610474542893,
12.5269717671326));
#445445=CARTESIAN_POINT('Ctrl Pts',(2.59419767082312,-0.876308844022821,
12.5299036066169));
#445446=CARTESIAN_POINT('Ctrl Pts',(2.59340221678271,-0.875829568532383,
12.5328133004019));
#445447=CARTESIAN_POINT('Ctrl Pts',(2.59302035252541,-0.875599488389593,
12.5342101228451));
#445448=CARTESIAN_POINT('Ctrl Pts',(2.59264824016026,-0.8753283070953,12.5356023438238));
#445449=CARTESIAN_POINT('Ctrl Pts',(2.59228746499891,-0.875023942687728,
12.5369868989719));
#445450=CARTESIAN_POINT('Origin',(12.3313552281263,-9.09822770945204,-1.24119156191802));
#445451=CARTESIAN_POINT('Ctrl Pts',(2.62445459714358,-0.773075939238756,
12.5369868989719));
#445452=CARTESIAN_POINT('Ctrl Pts',(2.63973567451123,-0.771744782535234,
12.5369868989719));
#445453=CARTESIAN_POINT('Ctrl Pts',(2.64377058425296,-0.756946039106763,
12.5369868989719));
#445454=CARTESIAN_POINT('Ctrl Pts',(2.62962019318718,-0.772625890249611,
12.5218025310016));
#445455=CARTESIAN_POINT('Ctrl Pts',(2.64063225266344,-0.768337486141284,
12.5216901060418));
#445456=CARTESIAN_POINT('Ctrl Pts',(2.64375830042182,-0.756991154919283,
12.5161920673678));
#445457=CARTESIAN_POINT('Ctrl Pts',(2.63354811132182,-0.777198365544579,
12.5042015548894));
#445458=CARTESIAN_POINT('Ctrl Pts',(2.63900405830915,-0.773791022373099,
12.4980677368513));
#445459=CARTESIAN_POINT('Ctrl Pts',(2.64091048368067,-0.767267501695844,
12.4907278922777));
#445460=CARTESIAN_POINT('Ctrl Pts',(2.62761382487369,-0.789073685290027,
12.506463626192));
#445461=CARTESIAN_POINT('Ctrl Pts',(2.63388011414934,-0.790955454949259,
12.4999376786891));
#445462=CARTESIAN_POINT('Ctrl Pts',(2.63380358053701,-0.790932471868963,
12.4906970594712));
#445463=CARTESIAN_POINT('Origin',(2.62254537567347,-0.751158939595144,12.5369868989719));
#445464=CARTESIAN_POINT('Origin',(2.62254537567347,-0.751158939595144,14.));
#445465=CARTESIAN_POINT('Origin',(2.62254537567347,-0.751158939595144,13.7435492065112));
#445466=CARTESIAN_POINT('Ctrl Pts',(2.59983366398332,-0.775267853015973,
13.793642941384));
#445467=CARTESIAN_POINT('Ctrl Pts',(2.61060576757833,-0.77433618615272,
13.8071662555867));
#445468=CARTESIAN_POINT('Ctrl Pts',(2.61164881210845,-0.757338202691648,
13.8103758687955));
#445469=CARTESIAN_POINT('Ctrl Pts',(2.61638930916283,-0.773793974488835,
13.7804579775006));
#445470=CARTESIAN_POINT('Ctrl Pts',(2.62968023755084,-0.772634278703411,
13.7901904343352));
#445471=CARTESIAN_POINT('Ctrl Pts',(2.63317701534847,-0.757271060642142,
13.7927914348263));
#445472=CARTESIAN_POINT('Ctrl Pts',(2.62613624053571,-0.772926246693739,
13.7597120340895));
#445473=CARTESIAN_POINT('Ctrl Pts',(2.64151708954274,-0.771578443371696,
13.7635825532444));
#445474=CARTESIAN_POINT('Ctrl Pts',(2.64587209244678,-0.75720590477026,
13.7651073818884));
#445475=CARTESIAN_POINT('Ctrl Pts',(2.62422756819345,-0.773096167663921,
13.7381884353898));
#445476=CARTESIAN_POINT('Ctrl Pts',(2.63924847823593,-0.771780807590837,
13.7368803041982));
#445477=CARTESIAN_POINT('Ctrl Pts',(2.64338601658193,-0.757218170001641,
13.7363986145813));
#445478=CARTESIAN_POINT('Origin',(2.60190000947439,-0.752996912276295,13.7902182540695));
#445479=CARTESIAN_POINT('Ctrl Pts',(2.56822092187241,-0.77808223290419,
13.8235227101244));
#445480=CARTESIAN_POINT('Ctrl Pts',(2.57967309555235,-0.777067143585816,
13.8358800583119));
#445481=CARTESIAN_POINT('Ctrl Pts',(2.58119603549153,-0.760565425402582,
13.8390832900376));
#445482=CARTESIAN_POINT('Ctrl Pts',(2.58010151365312,-0.777024552311795,
13.8124254819053));
#445483=CARTESIAN_POINT('Ctrl Pts',(2.59157592726744,-0.776007491427277,
13.8247886449158));
#445484=CARTESIAN_POINT('Ctrl Pts',(2.59308381934425,-0.759483356273273,
13.8279860620657));
#445485=CARTESIAN_POINT('Ctrl Pts',(2.59197678093904,-0.775967345737449,
13.8013225099955));
#445486=CARTESIAN_POINT('Ctrl Pts',(2.60346802058414,-0.774948795172976,
13.8136962257787));
#445487=CARTESIAN_POINT('Ctrl Pts',(2.60496612430866,-0.758402058028986,
13.8168830918626));
#445488=CARTESIAN_POINT('Ctrl Pts',(2.60384693089817,-0.774910594737833,
13.7902140179785));
#445489=CARTESIAN_POINT('Ctrl Pts',(2.61534993650848,-0.773891004881955,
13.802602731458));
#445490=CARTESIAN_POINT('Ctrl Pts',(2.61684316583032,-0.757321502212462,
13.8057746032558));
#445491=CARTESIAN_POINT('Origin',(2.56627398803564,-0.756168551544451,13.8235269408515));
#445492=CARTESIAN_POINT('Ctrl Pts',(2.54910729598815,-0.838595406033456,
13.8235269408515));
#445493=CARTESIAN_POINT('Ctrl Pts',(2.55813214084678,-0.84620913009391,
13.8362179249168));
#445494=CARTESIAN_POINT('Ctrl Pts',(2.54937606832253,-0.860871810544881,
13.8391868794938));
#445495=CARTESIAN_POINT('Ctrl Pts',(2.54084995577065,-0.831629179923846,
13.8400110824519));
#445496=CARTESIAN_POINT('Ctrl Pts',(2.54587973825889,-0.840348305509752,
13.8494522556837));
#445497=CARTESIAN_POINT('Ctrl Pts',(2.53585926765915,-0.849321490919388,
13.85569149686));
#445498=CARTESIAN_POINT('Ctrl Pts',(2.53378962200395,-0.816947578745872,
13.8586819406588));
#445499=CARTESIAN_POINT('Ctrl Pts',(2.53249130888095,-0.821103349031829,
13.868010383617));
#445500=CARTESIAN_POINT('Ctrl Pts',(2.52427054936054,-0.824886466754057,
13.8744918421245));
#445501=CARTESIAN_POINT('Ctrl Pts',(2.54316536839459,-0.787095160459156,
13.8587686893867));
#445502=CARTESIAN_POINT('Ctrl Pts',(2.54445207279634,-0.782976359698941,
13.8680909899357));
#445503=CARTESIAN_POINT('Ctrl Pts',(2.5398808684853,-0.775191727873839,
13.8745789365163));
#445504=CARTESIAN_POINT('Ctrl Pts',(2.55744655939933,-0.779041431171037,
13.8400379222776));
#445505=CARTESIAN_POINT('Ctrl Pts',(2.566567272192,-0.774789039836563,13.8494748685453));
#445506=CARTESIAN_POINT('Ctrl Pts',(2.56352313831086,-0.761693454543098,
13.8557104837033));
#445507=CARTESIAN_POINT('Ctrl Pts',(2.56822484263113,-0.778081884610338,
13.8235269408542));
#445508=CARTESIAN_POINT('Ctrl Pts',(2.57998580964549,-0.777034853723655,
13.8362179249195));
#445509=CARTESIAN_POINT('Ctrl Pts',(2.58124272643399,-0.760003025746507,
13.8391868794965));
#445510=CARTESIAN_POINT('Origin',(2.53492121153996,-0.855410726667589,13.8235269408515));
#445511=CARTESIAN_POINT('Ctrl Pts',(2.57644211177897,-0.861656162967016,
13.7902140241682));
#445512=CARTESIAN_POINT('Ctrl Pts',(2.58527157213118,-0.869099228550608,
13.8026027327198));
#445513=CARTESIAN_POINT('Ctrl Pts',(2.57697453300423,-0.883519251920907,
13.8057746032556));
#445514=CARTESIAN_POINT('Ctrl Pts',(2.56733348476496,-0.853971756890975,
13.8013225161807));
#445515=CARTESIAN_POINT('Ctrl Pts',(2.57615391174576,-0.861407212207343,
13.8136962270464));
#445516=CARTESIAN_POINT('Ctrl Pts',(2.5678739412118,-0.875811402336283,
13.8168830918628));
#445517=CARTESIAN_POINT('Ctrl Pts',(2.55822093093989,-0.846284037998324,
13.8124254880875));
#445518=CARTESIAN_POINT('Ctrl Pts',(2.5670284416319,-0.853708607376477,
13.8247886461868));
#445519=CARTESIAN_POINT('Ctrl Pts',(2.5587694678125,-0.868099921202852,
13.8279860620656));
#445520=CARTESIAN_POINT('Ctrl Pts',(2.54910429133106,-0.838592872173261,
13.8235227163065));
#445521=CARTESIAN_POINT('Ctrl Pts',(2.55789473129573,-0.846003050879926,
13.8358800595847));
#445522=CARTESIAN_POINT('Ctrl Pts',(2.5496609528115,-0.860384661452853,
13.8390832900376));
#445523=CARTESIAN_POINT('Origin',(2.56225904150084,-0.878474025482613,13.7902182540695));
#445524=CARTESIAN_POINT('Ctrl Pts',(2.59208118444921,-0.874849952164235,
13.7382347919292));
#445525=CARTESIAN_POINT('Ctrl Pts',(2.60363067448662,-0.884562168626437,
13.7369371795943));
#445526=CARTESIAN_POINT('Ctrl Pts',(2.59863928497826,-0.898867056175656,
13.7364597369711));
#445527=CARTESIAN_POINT('Ctrl Pts',(2.59352696491608,-0.876069670502942,
13.7595490285574));
#445528=CARTESIAN_POINT('Ctrl Pts',(2.60535136878867,-0.886014381633853,
13.7633824266926));
#445529=CARTESIAN_POINT('Ctrl Pts',(2.60064247009915,-0.900287430832924,
13.7648920890506));
#445530=CARTESIAN_POINT('Ctrl Pts',(2.58615356374644,-0.869849173791011,
13.7803806590111));
#445531=CARTESIAN_POINT('Ctrl Pts',(2.59638472462146,-0.878446861454142,
13.7901039518744));
#445532=CARTESIAN_POINT('Ctrl Pts',(2.59043216110599,-0.893043177051566,
13.7926933640892));
#445533=CARTESIAN_POINT('Ctrl Pts',(2.57333694651367,-0.859036561975015,
13.7936647693663));
#445534=CARTESIAN_POINT('Ctrl Pts',(2.58162282302282,-0.865987646956492,
13.8072068914933));
#445535=CARTESIAN_POINT('Ctrl Pts',(2.57269255057998,-0.880509854224789,
13.8104111085397));
#445536=CARTESIAN_POINT('Origin',(2.57810138055072,-0.891839263321863,13.7435492065112));
#445537=CARTESIAN_POINT('Origin',(2.57810138055072,-0.891839263321863,14.));
#445538=CARTESIAN_POINT('Origin',(2.57810138055072,-0.891839263321863,12.5369868989719));
#445539=CARTESIAN_POINT('Ctrl Pts',(2.60403363890013,-0.863718344253423,
12.506462012331));
#445540=CARTESIAN_POINT('Ctrl Pts',(2.61023978363311,-0.865776828050595,
12.4999388158272));
#445541=CARTESIAN_POINT('Ctrl Pts',(2.61016635680206,-0.865752473487739,
12.4907030323752));
#445542=CARTESIAN_POINT('Ctrl Pts',(2.60206650756118,-0.876846900055558,
12.5042014951932));
#445543=CARTESIAN_POINT('Ctrl Pts',(2.60457445515015,-0.882767313555237,
12.4980716682127));
#445544=CARTESIAN_POINT('Ctrl Pts',(2.60239010596918,-0.889198035433974,
12.4907355092743));
#445545=CARTESIAN_POINT('Ctrl Pts',(2.59622600650535,-0.878334935223942,
12.5218047446509));
#445546=CARTESIAN_POINT('Ctrl Pts',(2.60277153691815,-0.888167274851517,
12.5216906929434));
#445547=CARTESIAN_POINT('Ctrl Pts',(2.59881721519281,-0.899245816904604,
12.5161988840776));
#445548=CARTESIAN_POINT('Ctrl Pts',(2.5922580806779,-0.874999196768876,
12.5369868989719));
#445549=CARTESIAN_POINT('Ctrl Pts',(2.60399246113729,-0.884863772114773,
12.5369868989719));
#445550=CARTESIAN_POINT('Ctrl Pts',(2.59880194494944,-0.899288198384969,
12.5369868989719));
#445551=CARTESIAN_POINT('Origin',(4.912540026806E-31,-6.7038415788775E-31,
12.5));
#445552=CARTESIAN_POINT('Origin',(2.60897866247895,-0.628029139618544,12.5));
#445553=CARTESIAN_POINT('',(2.60897866247895,-0.628029139618544,12.5893111709658));
#445554=CARTESIAN_POINT('',(2.60897866247895,-0.628029139618544,13.8235269408515));
#445555=CARTESIAN_POINT('',(2.60897866247895,-0.628029139618544,12.5));
#445556=CARTESIAN_POINT('',(2.63810540102849,-0.648787410275507,13.7902182540695));
#445557=CARTESIAN_POINT('',(2.60897866247895,-0.628029139618544,13.8235269408515));
#445558=CARTESIAN_POINT('',(2.6549844169628,-0.660816878682736,13.7435492065112));
#445559=CARTESIAN_POINT('Origin',(2.59945286671001,-0.621239821352992,13.7445212918713));
#445560=CARTESIAN_POINT('',(2.6549844169628,-0.660816878682736,12.5369868989719));
#445561=CARTESIAN_POINT('',(2.6549844169628,-0.660816878682736,12.5));
#445562=CARTESIAN_POINT('Ctrl Pts',(2.6549844169628,-0.660816878682736,
12.5369868989719));
#445563=CARTESIAN_POINT('Ctrl Pts',(2.63966035006791,-0.649895603455565,
12.5544431401645));
#445564=CARTESIAN_POINT('Ctrl Pts',(2.62432532299309,-0.638966517042081,
12.5718848856037));
#445565=CARTESIAN_POINT('Ctrl Pts',(2.60897866247895,-0.628029139618544,
12.5893111709658));
#445566=CARTESIAN_POINT('Origin',(2.89411775208694,-0.519527422330528,12.5));
#445567=CARTESIAN_POINT('',(2.6787760026444,-0.556579131053022,13.7435492065112));
#445568=CARTESIAN_POINT('',(2.65834914403464,-0.560093777039152,13.7902182540695));
#445569=CARTESIAN_POINT('Origin',(2.60467089007809,-0.569329659237933,13.7418732680443));
#445570=CARTESIAN_POINT('',(2.62310018328771,-0.56615871442239,13.8235269408515));
#445571=CARTESIAN_POINT('',(2.65834914403464,-0.560093777039152,13.7902182540695));
#445572=CARTESIAN_POINT('',(2.62310018328771,-0.56615871442239,12.5893111709658));
#445573=CARTESIAN_POINT('',(2.62310018328771,-0.56615871442239,12.5));
#445574=CARTESIAN_POINT('',(2.6787760026444,-0.556579131053022,12.5369868989719));
#445575=CARTESIAN_POINT('Ctrl Pts',(2.62310018328771,-0.56615871442239,
12.5893111709658));
#445576=CARTESIAN_POINT('Ctrl Pts',(2.64167259684989,-0.562963144314128,
12.5718848856037));
#445577=CARTESIAN_POINT('Ctrl Pts',(2.66023093171096,-0.559769996587656,
12.5544431401645));
#445578=CARTESIAN_POINT('Ctrl Pts',(2.6787760026444,-0.556579131053022,
12.5369868989719));
#445579=CARTESIAN_POINT('',(2.6787760026444,-0.556579131053022,12.5));
#445580=CARTESIAN_POINT('Origin',(2.62892909479919,-0.600035910522293,12.5));
#445581=CARTESIAN_POINT('',(2.59518531992423,-0.593482451178893,13.8587068136939));
#445582=CARTESIAN_POINT('Ctrl Pts',(2.62310018328645,-0.566158714415902,
13.8235269408542));
#445583=CARTESIAN_POINT('Ctrl Pts',(2.62137326098674,-0.566455848725446,
13.8262006681044));
#445584=CARTESIAN_POINT('Ctrl Pts',(2.61963546901952,-0.566931145591292,
13.8288634856214));
#445585=CARTESIAN_POINT('Ctrl Pts',(2.61788907235351,-0.567571464390742,
13.8314912288862));
#445586=CARTESIAN_POINT('Ctrl Pts',(2.61608871752331,-0.568231567027153,
13.8342001611531));
#445587=CARTESIAN_POINT('Ctrl Pts',(2.61427704726576,-0.569067313143771,
13.8368750301949));
#445588=CARTESIAN_POINT('Ctrl Pts',(2.61245207543582,-0.570109285762259,
13.8394886372968));
#445589=CARTESIAN_POINT('Ctrl Pts',(2.61231112843463,-0.570189759835059,
13.8396904925131));
#445590=CARTESIAN_POINT('Ctrl Pts',(2.61217010959524,-0.570271484856063,
13.8398919674349));
#445591=CARTESIAN_POINT('Ctrl Pts',(2.61202902281037,-0.570354485299402,
13.8400930404591));
#445592=CARTESIAN_POINT('Ctrl Pts',(2.6098307957836,-0.571647688046562,
13.8432258934518));
#445593=CARTESIAN_POINT('Ctrl Pts',(2.6076267205433,-0.573242940132615,
13.8462331177034));
#445594=CARTESIAN_POINT('Ctrl Pts',(2.60554524192903,-0.575166358647123,
13.8489036603661));
#445595=CARTESIAN_POINT('Ctrl Pts',(2.60486415790306,-0.575795723569018,
13.849777493004));
#445596=CARTESIAN_POINT('Ctrl Pts',(2.60419644647895,-0.576460183071652,
13.85061494757));
#445597=CARTESIAN_POINT('Ctrl Pts',(2.6035473095085,-0.577160522217488,
13.8514076489583));
#445598=CARTESIAN_POINT('Ctrl Pts',(2.60217429119645,-0.578641840514945,
13.8530843267192));
#445599=CARTESIAN_POINT('Ctrl Pts',(2.6007516747693,-0.580431193640579,
13.8546805203176));
#445600=CARTESIAN_POINT('Ctrl Pts',(2.599468832228,-0.582509642064698,13.8559412814273));
#445601=CARTESIAN_POINT('Ctrl Pts',(2.5992971462924,-0.582787805869536,
13.8561100121513));
#445602=CARTESIAN_POINT('Ctrl Pts',(2.59912794021294,-0.583071074603606,
13.8562727473908));
#445603=CARTESIAN_POINT('Ctrl Pts',(2.59896163573393,-0.583359334191462,
13.8564289040185));
#445604=CARTESIAN_POINT('Ctrl Pts',(2.59820744681892,-0.584666588133763,
13.8571370725437));
#445605=CARTESIAN_POINT('Ctrl Pts',(2.59750164784465,-0.586100600040144,
13.8577210840554));
#445606=CARTESIAN_POINT('Ctrl Pts',(2.59689800482735,-0.587618589571027,
13.8581177131616));
#445607=CARTESIAN_POINT('Ctrl Pts',(2.59672799817692,-0.588046107670531,
13.8582294175695));
#445608=CARTESIAN_POINT('Ctrl Pts',(2.5965659453427,-0.588480190009253,
13.8583265086086));
#445609=CARTESIAN_POINT('Ctrl Pts',(2.59641266502776,-0.588919664052098,
13.8584082369006));
#445610=CARTESIAN_POINT('Ctrl Pts',(2.59619244231892,-0.58955107040205,
13.8585256585398));
#445611=CARTESIAN_POINT('Ctrl Pts',(2.59598789525078,-0.590201562652359,
13.8586122832068));
#445612=CARTESIAN_POINT('Ctrl Pts',(2.59580509068444,-0.59085447978121,
13.8586682984299));
#445613=CARTESIAN_POINT('Ctrl Pts',(2.5956588651522,-0.591376748762697,
13.8587131050557));
#445614=CARTESIAN_POINT('Ctrl Pts',(2.59552471051172,-0.591906274527134,
13.8587357943552));
#445615=CARTESIAN_POINT('Ctrl Pts',(2.59540310175727,-0.592443244374535,
13.8587355499465));
#445616=CARTESIAN_POINT('Ctrl Pts',(2.59532450311996,-0.592790300788972,
13.8587353919793));
#445617=CARTESIAN_POINT('Ctrl Pts',(2.59525195757008,-0.593136705290338,
13.8587257282814));
#445618=CARTESIAN_POINT('Ctrl Pts',(2.59518531992423,-0.593482451178892,
13.8587068136939));
#445619=CARTESIAN_POINT('Ctrl Pts',(2.59518531992423,-0.593482451178892,
13.8587068136939));
#445620=CARTESIAN_POINT('Ctrl Pts',(2.59496615233992,-0.594619590557335,
13.8586446046466));
#445621=CARTESIAN_POINT('Ctrl Pts',(2.59481081257847,-0.595749615152042,
13.858482427929));
#445622=CARTESIAN_POINT('Ctrl Pts',(2.59471484042457,-0.596872220929184,
13.8582284286032));
#445623=CARTESIAN_POINT('Ctrl Pts',(2.59461638415859,-0.598023883869769,
13.8579678548414));
#445624=CARTESIAN_POINT('Ctrl Pts',(2.59458169415963,-0.599170682635047,
13.857615680862));
#445625=CARTESIAN_POINT('Ctrl Pts',(2.59460245281572,-0.600267112562453,
13.8571944833187));
#445626=CARTESIAN_POINT('Ctrl Pts',(2.59465425816504,-0.60300336557997,
13.8561433417727));
#445627=CARTESIAN_POINT('Ctrl Pts',(2.59504902817911,-0.605554004057623,
13.8546163505474));
#445628=CARTESIAN_POINT('Ctrl Pts',(2.59561194759635,-0.607808585743686,
13.8528973491086));
#445629=CARTESIAN_POINT('Ctrl Pts',(2.59571478466877,-0.60822046455446,
13.8525833129072));
#445630=CARTESIAN_POINT('Ctrl Pts',(2.595823127746,-0.608622556498766,13.8522628768811));
#445631=CARTESIAN_POINT('Ctrl Pts',(2.59593579729948,-0.609014326233263,
13.851937733538));
#445632=CARTESIAN_POINT('Ctrl Pts',(2.59662385463044,-0.611406809646339,
13.8499521282529));
#445633=CARTESIAN_POINT('Ctrl Pts',(2.59754556184791,-0.613650979763354,
13.847639871647));
#445634=CARTESIAN_POINT('Ctrl Pts',(2.59857816062764,-0.615659414088125,
13.8452109780794));
#445635=CARTESIAN_POINT('Ctrl Pts',(2.59904274819237,-0.61656305026336,
13.8441181685877));
#445636=CARTESIAN_POINT('Ctrl Pts',(2.59952929793255,-0.617419495470851,
13.8430021611332));
#445637=CARTESIAN_POINT('Ctrl Pts',(2.60002525572454,-0.61822379766086,
13.8418824960098));
#445638=CARTESIAN_POINT('Ctrl Pts',(2.60119399292609,-0.620119156310212,
13.8392439765549));
#445639=CARTESIAN_POINT('Ctrl Pts',(2.60246762621868,-0.621817545075485,
13.8364981347964));
#445640=CARTESIAN_POINT('Ctrl Pts',(2.6038221462249,-0.623343986225896,
13.8336931113419));
#445641=CARTESIAN_POINT('Ctrl Pts',(2.60514136269098,-0.62483064296842,
13.8309611966328));
#445642=CARTESIAN_POINT('Ctrl Pts',(2.60653904857348,-0.626155313535347,
13.8281701127185));
#445643=CARTESIAN_POINT('Ctrl Pts',(2.60801091443559,-0.627306122843475,
13.825358068512));
#445644=CARTESIAN_POINT('Ctrl Pts',(2.60833001654297,-0.627555619543461,
13.8247484142932));
#445645=CARTESIAN_POINT('Ctrl Pts',(2.60865261780666,-0.627796771564635,
13.8241378483365));
#445646=CARTESIAN_POINT('Ctrl Pts',(2.60897866247895,-0.628029139618544,
13.8235269408515));
#445647=CARTESIAN_POINT('',(2.59544407237152,-0.592267616198399,12.5969504640361));
#445648=CARTESIAN_POINT('Origin',(2.62896130711964,-0.600043463615782,12.584524458991));
#445649=CARTESIAN_POINT('Origin',(2.62896130711964,-0.600043463615782,12.584524458991));
#445650=CARTESIAN_POINT('Ctrl Pts',(2.62310018328771,-0.56615871442239,
12.5893111709658));
#445651=CARTESIAN_POINT('Ctrl Pts',(2.61193035744025,-0.568080595037053,
12.5770542771492));
#445652=CARTESIAN_POINT('Ctrl Pts',(2.61164981429195,-0.584442898371147,
12.5737548217797));
#445653=CARTESIAN_POINT('Ctrl Pts',(2.64752484371117,-0.561956206520423,
12.5663937883685));
#445654=CARTESIAN_POINT('Ctrl Pts',(2.63634076919958,-0.563880538760725,
12.5540940315304));
#445655=CARTESIAN_POINT('Ctrl Pts',(2.6360625674199,-0.580293600604353,
12.5508374392248));
#445656=CARTESIAN_POINT('Ctrl Pts',(2.67192485995163,-0.557757938897418,
12.5434499600945));
#445657=CARTESIAN_POINT('Ctrl Pts',(2.66070442203105,-0.559688527827123,
12.5311293540533));
#445658=CARTESIAN_POINT('Ctrl Pts',(2.66045127106828,-0.576147193603881,
12.5278936106989));
#445659=CARTESIAN_POINT('Ctrl Pts',(2.69630216242177,-0.553563579406506,
12.5204817579905));
#445660=CARTESIAN_POINT('Ctrl Pts',(2.6850261910016,-0.555503723432015,
12.5081597038247));
#445661=CARTESIAN_POINT('Ctrl Pts',(2.68481779213524,-0.572003439029782,
12.5049254088044));
#445662=CARTESIAN_POINT('Ctrl Pts',(2.6787760026444,-0.556579131053022,
12.5369868989719));
#445663=CARTESIAN_POINT('Ctrl Pts',(2.67969401781028,-0.556421177496693,
12.5342545179733));
#445664=CARTESIAN_POINT('Ctrl Pts',(2.68059128256758,-0.556393373384302,
12.5314872231885));
#445665=CARTESIAN_POINT('Ctrl Pts',(2.68141898399378,-0.556553159050733,
12.5287124745063));
#445666=CARTESIAN_POINT('Ctrl Pts',(2.68216544622336,-0.556697261695773,
12.5262100684184));
#445667=CARTESIAN_POINT('Ctrl Pts',(2.68285439069847,-0.556994757658666,
12.5237004536639));
#445668=CARTESIAN_POINT('Ctrl Pts',(2.68347136718562,-0.55751161410463,
12.5212220730815));
#445669=CARTESIAN_POINT('Ctrl Pts',(2.68394371605926,-0.557907312425665,
12.5193246583486));
#445670=CARTESIAN_POINT('Ctrl Pts',(2.68437912059213,-0.558436798512218,
12.517417831369));
#445671=CARTESIAN_POINT('Ctrl Pts',(2.68471614181412,-0.559175433333651,
12.5155812248347));
#445672=CARTESIAN_POINT('Ctrl Pts',(2.68485971466618,-0.559490095737757,
12.5147988205793));
#445673=CARTESIAN_POINT('Ctrl Pts',(2.6849858306331,-0.559842919007419,
12.5140295443047));
#445674=CARTESIAN_POINT('Ctrl Pts',(2.68509183607873,-0.560240091008357,
12.5132817086137));
#445675=CARTESIAN_POINT('Ctrl Pts',(2.6852522609806,-0.560841157103569,
12.5121499604604));
#445676=CARTESIAN_POINT('Ctrl Pts',(2.68536318174522,-0.5615586176954,12.5110494206568));
#445677=CARTESIAN_POINT('Ctrl Pts',(2.68539158273191,-0.562409702589905,
12.5100666561695));
#445678=CARTESIAN_POINT('Ctrl Pts',(2.68540789051307,-0.562898393576455,
12.5095023550641));
#445679=CARTESIAN_POINT('Ctrl Pts',(2.68539652731508,-0.563436809041634,
12.5089719619137));
#445680=CARTESIAN_POINT('Ctrl Pts',(2.68535132057195,-0.564014722216191,
12.5085043804652));
#445681=CARTESIAN_POINT('Ctrl Pts',(2.68528516639196,-0.56486042286867,
12.5078201359221));
#445682=CARTESIAN_POINT('Ctrl Pts',(2.68514341510609,-0.565815139887281,
12.5072563000949));
#445683=CARTESIAN_POINT('Ctrl Pts',(2.68492730116138,-0.566812914185047,
12.5068768744332));
#445684=CARTESIAN_POINT('Ctrl Pts',(2.68477146812991,-0.567532378140754,
12.5066032824114));
#445685=CARTESIAN_POINT('Ctrl Pts',(2.68457429190157,-0.568286881921826,
12.5064197834844));
#445686=CARTESIAN_POINT('Ctrl Pts',(2.68434928417872,-0.569034945636987,
12.5063282718343));
#445687=CARTESIAN_POINT('Ctrl Pts',(2.68402084256399,-0.570126887066449,
12.5061946931565));
#445688=CARTESIAN_POINT('Ctrl Pts',(2.68362709761846,-0.571228751576195,
12.5062515701262));
#445689=CARTESIAN_POINT('Ctrl Pts',(2.68320704851426,-0.572277359400301,
12.5064436508398));
#445690=CARTESIAN_POINT('',(2.61164981429195,-0.584442898371147,12.5737548217797));
#445691=CARTESIAN_POINT('Origin',(2.62683068665506,-0.587840119926328,12.5893111709658));
#445692=CARTESIAN_POINT('Ctrl Pts',(2.68320704851426,-0.572277359400301,
12.5064436508398));
#445693=CARTESIAN_POINT('Ctrl Pts',(2.67261479927447,-0.574078648881047,
12.5164271754438));
#445694=CARTESIAN_POINT('Ctrl Pts',(2.66201831624136,-0.575880446414043,
12.5264061185523));
#445695=CARTESIAN_POINT('Ctrl Pts',(2.65141745046296,-0.577682770825561,
12.536380305637));
#445696=CARTESIAN_POINT('Ctrl Pts',(2.6381685183272,-0.57993531078918,12.5488460165097));
#445697=CARTESIAN_POINT('Ctrl Pts',(2.62491273645613,-0.582188674374818,
12.5613043021964));
#445698=CARTESIAN_POINT('Ctrl Pts',(2.61164981429195,-0.584442898371146,
12.5737548217797));
#445699=CARTESIAN_POINT('Ctrl Pts',(2.60897866247895,-0.628029139618544,
12.5893111709658));
#445700=CARTESIAN_POINT('Ctrl Pts',(2.59974886987772,-0.621451179212918,
12.5770542771492));
#445701=CARTESIAN_POINT('Ctrl Pts',(2.60659544658617,-0.606587530191557,
12.5737548217797));
#445702=CARTESIAN_POINT('Ctrl Pts',(2.6003673462585,-0.621891959772177,
12.5928319619712));
#445703=CARTESIAN_POINT('Ctrl Pts',(2.59605507181361,-0.614818226282471,
12.5821634970842));
#445704=CARTESIAN_POINT('Ctrl Pts',(2.60345307443658,-0.604359590640562,
12.5773203894503));
#445705=CARTESIAN_POINT('Ctrl Pts',(2.59202457592455,-0.607366730600327,
12.5969440695591));
#445706=CARTESIAN_POINT('Ctrl Pts',(2.59290123342859,-0.603443719744806,
12.5878292599214));
#445707=CARTESIAN_POINT('Ctrl Pts',(2.60048131500874,-0.59918148355393,
12.5813877129824));
#445708=CARTESIAN_POINT('Ctrl Pts',(2.59878046210658,-0.577524926910923,
12.596957478804));
#445709=CARTESIAN_POINT('Ctrl Pts',(2.59791036156559,-0.581418963145663,
12.5878468778671));
#445710=CARTESIAN_POINT('Ctrl Pts',(2.60290515821347,-0.588502005456986,
12.5814011370086));
#445711=CARTESIAN_POINT('Ctrl Pts',(2.61266370113927,-0.567954415895238,
12.5928371701607));
#445712=CARTESIAN_POINT('Ctrl Pts',(2.60571757709291,-0.572458461458544,
12.5821692192952));
#445713=CARTESIAN_POINT('Ctrl Pts',(2.60783977973503,-0.585088587266066,
12.5773318885715));
#445714=CARTESIAN_POINT('Ctrl Pts',(2.6231001832877,-0.566158714422335,
12.5893111709658));
#445715=CARTESIAN_POINT('Ctrl Pts',(2.61193035744023,-0.568080595036999,
12.5770542771492));
#445716=CARTESIAN_POINT('Ctrl Pts',(2.61164981429194,-0.584442898371092,
12.5737548217797));
#445717=CARTESIAN_POINT('',(2.60659544658617,-0.606587530191557,12.5737548217797));
#445718=CARTESIAN_POINT('Origin',(2.6217469391639,-0.610113472996944,12.5893111709658));
#445719=CARTESIAN_POINT('Ctrl Pts',(2.61164981429194,-0.584442898371092,
12.5737548217797));
#445720=CARTESIAN_POINT('Ctrl Pts',(2.61065715256629,-0.584580529506537,
12.5746934679442));
#445721=CARTESIAN_POINT('Ctrl Pts',(2.60958386385314,-0.584914276081746,
12.5756680099006));
#445722=CARTESIAN_POINT('Ctrl Pts',(2.60855106914081,-0.585402987397514,
12.5765688348656));
#445723=CARTESIAN_POINT('Ctrl Pts',(2.60827764817413,-0.58553236830815,
12.5768073183026));
#445724=CARTESIAN_POINT('Ctrl Pts',(2.60800701520167,-0.585672358037817,
12.5770407398754));
#445725=CARTESIAN_POINT('Ctrl Pts',(2.60774117256608,-0.585821685985655,
12.5772674179684));
#445726=CARTESIAN_POINT('Ctrl Pts',(2.6066502262765,-0.586434487503603,
12.5781976435658));
#445727=CARTESIAN_POINT('Ctrl Pts',(2.60558351328209,-0.587249190437393,
12.5790594849312));
#445728=CARTESIAN_POINT('Ctrl Pts',(2.60464236986446,-0.588249161332534,
12.5797571720116));
#445729=CARTESIAN_POINT('Ctrl Pts',(2.60402918108738,-0.588900678326468,
12.580211740231));
#445730=CARTESIAN_POINT('Ctrl Pts',(2.60345510062344,-0.58967331575842,
12.5806009430798));
#445731=CARTESIAN_POINT('Ctrl Pts',(2.60297476214117,-0.590523249642185,
12.5808812374708));
#445732=CARTESIAN_POINT('Ctrl Pts',(2.60256199203427,-0.591253624810969,
12.5811221033394));
#445733=CARTESIAN_POINT('Ctrl Pts',(2.60221009464932,-0.592056088506825,
12.581287365893));
#445734=CARTESIAN_POINT('Ctrl Pts',(2.60194656767815,-0.592888696949562,
12.581359338449));
#445735=CARTESIAN_POINT('Ctrl Pts',(2.60190994287078,-0.593004412330396,
12.5813693411482));
#445736=CARTESIAN_POINT('Ctrl Pts',(2.60187496511642,-0.59312071195575,
12.5813775999465));
#445737=CARTESIAN_POINT('Ctrl Pts',(2.60184164696784,-0.59323748635646,
12.5813841266931));
#445738=CARTESIAN_POINT('Ctrl Pts',(2.60178511869904,-0.593435608250835,
12.5813952001081));
#445739=CARTESIAN_POINT('Ctrl Pts',(2.60173357454906,-0.593636590779214,
12.5814007534795));
#445740=CARTESIAN_POINT('Ctrl Pts',(2.60168722799472,-0.593840395398267,
12.5814005856065));
#445741=CARTESIAN_POINT('Ctrl Pts',(2.60147507158928,-0.594773333261852,
12.5813998171494));
#445742=CARTESIAN_POINT('Ctrl Pts',(2.60138615750586,-0.595700872957205,
12.58127954464));
#445743=CARTESIAN_POINT('Ctrl Pts',(2.60139153620305,-0.596614925021774,
12.5810700125799));
#445744=CARTESIAN_POINT('Ctrl Pts',(2.60139803305684,-0.597718995842614,
12.5808169217085));
#445745=CARTESIAN_POINT('Ctrl Pts',(2.60155883834059,-0.598803389691812,
12.5804173076348));
#445746=CARTESIAN_POINT('Ctrl Pts',(2.6018340986878,-0.599776892187396,
12.5799304713245));
#445747=CARTESIAN_POINT('Ctrl Pts',(2.60217523297394,-0.600983368464338,
12.5793271277669));
#445748=CARTESIAN_POINT('Ctrl Pts',(2.60268233466224,-0.602103127673329,
12.5785808224116));
#445749=CARTESIAN_POINT('Ctrl Pts',(2.603305136233,-0.60310205413031,12.5777485681082));
#445750=CARTESIAN_POINT('Ctrl Pts',(2.60423317880645,-0.604590563991775,
12.576508418016));
#445751=CARTESIAN_POINT('Ctrl Pts',(2.60540447847364,-0.605801875925339,
12.5750928681475));
#445752=CARTESIAN_POINT('Ctrl Pts',(2.60659544658617,-0.606587530191557,
12.5737548217797));
#445753=CARTESIAN_POINT('Ctrl Pts',(2.60659544658617,-0.606587530191557,
12.5737548217797));
#445754=CARTESIAN_POINT('Ctrl Pts',(2.59974886987772,-0.621451179212918,
12.5770542771492));
#445755=CARTESIAN_POINT('Ctrl Pts',(2.60897866247895,-0.628029139618544,
12.5893111709658));
#445756=CARTESIAN_POINT('Ctrl Pts',(2.62678723035326,-0.620916061954205,
12.5508408821982));
#445757=CARTESIAN_POINT('Ctrl Pts',(2.6199165217402,-0.635824418261484,
12.55409748406));
#445758=CARTESIAN_POINT('Ctrl Pts',(2.62915808919293,-0.642410770459861,
12.5663972313419));
#445759=CARTESIAN_POINT('Ctrl Pts',(2.64695860668738,-0.635231558472971,
12.52790050457));
#445760=CARTESIAN_POINT('Ctrl Pts',(2.64004554774912,-0.650170129136117,
12.5311362602938));
#445761=CARTESIAN_POINT('Ctrl Pts',(2.64931715818131,-0.656777892598899,
12.5434568539655));
#445762=CARTESIAN_POINT('Ctrl Pts',(2.66711115349385,-0.649535044047112,
12.5049357605811));
#445763=CARTESIAN_POINT('Ctrl Pts',(2.66013997445222,-0.664491181508331,
12.5081700652078));
#445764=CARTESIAN_POINT('Ctrl Pts',(2.66945746386522,-0.671131642360113,
12.5204921097672));
#445765=CARTESIAN_POINT('Ctrl Pts',(2.66578785735636,-0.648595822410635,
12.5064436508395));
#445766=CARTESIAN_POINT('Ctrl Pts',(2.66570519898163,-0.649813202952483,
12.5062361689309));
#445767=CARTESIAN_POINT('Ctrl Pts',(2.66556732922572,-0.651075654357824,
12.5061871075061));
#445768=CARTESIAN_POINT('Ctrl Pts',(2.6653654124191,-0.652288191468314,
12.5063648335164));
#445769=CARTESIAN_POINT('Ctrl Pts',(2.66527368935078,-0.65283900061629,
12.5064455676329));
#445770=CARTESIAN_POINT('Ctrl Pts',(2.66516725327026,-0.653387156218686,
12.506574497099));
#445771=CARTESIAN_POINT('Ctrl Pts',(2.66504963615673,-0.65390895468463,
12.5067492519495));
#445772=CARTESIAN_POINT('Ctrl Pts',(2.6648132800015,-0.654957528956749,
12.5071004286051));
#445773=CARTESIAN_POINT('Ctrl Pts',(2.66452229370529,-0.655938041245078,
12.5076537929613));
#445774=CARTESIAN_POINT('Ctrl Pts',(2.66420758488729,-0.65677958994019,
12.5083435010505));
#445775=CARTESIAN_POINT('Ctrl Pts',(2.66418777208649,-0.656832570459665,
12.5083869222964));
#445776=CARTESIAN_POINT('Ctrl Pts',(2.66416785192314,-0.656885001800406,
12.5084308732337));
#445777=CARTESIAN_POINT('Ctrl Pts',(2.66414782672464,-0.656936867313813,
12.5084753333615));
#445778=CARTESIAN_POINT('Ctrl Pts',(2.66398719820184,-0.657352897187647,
12.5088319622689));
#445779=CARTESIAN_POINT('Ctrl Pts',(2.66381775402414,-0.657741431599982,
12.509227847131));
#445780=CARTESIAN_POINT('Ctrl Pts',(2.66364709924657,-0.658092036718835,
12.5096423454524));
#445781=CARTESIAN_POINT('Ctrl Pts',(2.66311234270232,-0.659190677989998,
12.5109411997424));
#445782=CARTESIAN_POINT('Ctrl Pts',(2.66254150158836,-0.659988689589087,
12.5124831113042));
#445783=CARTESIAN_POINT('Ctrl Pts',(2.66198293764026,-0.660567416460211,
12.5140723025008));
#445784=CARTESIAN_POINT('Ctrl Pts',(2.66193059958655,-0.660621643801897,
12.5142212114565));
#445785=CARTESIAN_POINT('Ctrl Pts',(2.66187837454269,-0.660673974991074,
12.5143705582413));
#445786=CARTESIAN_POINT('Ctrl Pts',(2.6618263067976,-0.66072449332381,12.5145201959299));
#445787=CARTESIAN_POINT('Ctrl Pts',(2.66115741909112,-0.661373476521739,
12.5164425148273));
#445788=CARTESIAN_POINT('Ctrl Pts',(2.66049904977585,-0.661753223311166,
12.5184635205941));
#445789=CARTESIAN_POINT('Ctrl Pts',(2.65985024793994,-0.661953939425375,
12.5205025929158));
#445790=CARTESIAN_POINT('Ctrl Pts',(2.65947391715901,-0.662070362727258,
12.5216853356836));
#445791=CARTESIAN_POINT('Ctrl Pts',(2.65910162803627,-0.662126803524878,
12.5228750347131));
#445792=CARTESIAN_POINT('Ctrl Pts',(2.65873911193257,-0.662140584784227,
12.5240609649613));
#445793=CARTESIAN_POINT('Ctrl Pts',(2.65784933560436,-0.662174410145961,
12.5269717671326));
#445794=CARTESIAN_POINT('Ctrl Pts',(2.65699299812196,-0.661941805106474,
12.5299036066169));
#445795=CARTESIAN_POINT('Ctrl Pts',(2.6561611254874,-0.66152896125462,12.5328133004019));
#445796=CARTESIAN_POINT('Ctrl Pts',(2.65576177818431,-0.66133077216655,
12.5342101228451));
#445797=CARTESIAN_POINT('Ctrl Pts',(2.65536880019935,-0.661090823817926,
12.5356023438238));
#445798=CARTESIAN_POINT('Ctrl Pts',(2.6549844169628,-0.660816878682735,
12.5369868989719));
#445799=CARTESIAN_POINT('Origin',(13.0312014533464,-8.06232477624549,-1.24024740340327));
#445800=CARTESIAN_POINT('Ctrl Pts',(2.6787348069087,-0.556586178910241,
12.5369868989719));
#445801=CARTESIAN_POINT('Ctrl Pts',(2.6938565361228,-0.554013901852757,
12.5369868989719));
#445802=CARTESIAN_POINT('Ctrl Pts',(2.69667178506096,-0.538935517420025,
12.5369868989719));
#445803=CARTESIAN_POINT('Ctrl Pts',(2.68384653168693,-0.555716583389367,
12.5218025310016));
#445804=CARTESIAN_POINT('Ctrl Pts',(2.69447240469724,-0.55054486351365,
12.5216901060418));
#445805=CARTESIAN_POINT('Ctrl Pts',(2.6966632194608,-0.538981484359688,
12.5161920673677));
#445806=CARTESIAN_POINT('Ctrl Pts',(2.68813407918327,-0.559953682356989,
12.5042015548895));
#445807=CARTESIAN_POINT('Ctrl Pts',(2.69329414185644,-0.556112966508837,
12.4980677368513));
#445808=CARTESIAN_POINT('Ctrl Pts',(2.69466249625818,-0.549455760942315,
12.4907278922778));
#445809=CARTESIAN_POINT('Ctrl Pts',(2.68318748738815,-0.572273187392411,
12.506463626192));
#445810=CARTESIAN_POINT('Ctrl Pts',(2.68958630779988,-0.573637934868978,
12.4999376786891));
#445811=CARTESIAN_POINT('Ctrl Pts',(2.68950815551243,-0.573621266462893,
12.4906970594712));
#445812=CARTESIAN_POINT('Origin',(2.67504549927705,-0.534897725549083,12.5369868989719));
#445813=CARTESIAN_POINT('Origin',(2.67504549927706,-0.534897725549084,14.));
#445814=CARTESIAN_POINT('Origin',(2.67504549927706,-0.534897725549084,13.7435492065112));
#445815=CARTESIAN_POINT('Ctrl Pts',(2.654374459194,-0.560777633897341,13.793642941384));
#445816=CARTESIAN_POINT('Ctrl Pts',(2.66503478000441,-0.558971040632395,
13.8071662555867));
#445817=CARTESIAN_POINT('Ctrl Pts',(2.66468886043623,-0.541944598746695,
13.8103758687955));
#445818=CARTESIAN_POINT('Ctrl Pts',(2.67075488204713,-0.557959220802175,
13.7804579775006));
#445819=CARTESIAN_POINT('Ctrl Pts',(2.68390705999472,-0.555720049758236,
13.7901904343351));
#445820=CARTESIAN_POINT('Ctrl Pts',(2.68613995765557,-0.540122931684682,
13.7927914348263));
#445821=CARTESIAN_POINT('Ctrl Pts',(2.68039865343904,-0.55629991490675,
13.7597120340895));
#445822=CARTESIAN_POINT('Ctrl Pts',(2.6956184654567,-0.553702914306182,
13.7635825532445));
#445823=CARTESIAN_POINT('Ctrl Pts',(2.69878748212368,-0.539023225974718,
13.7651073818884));
#445824=CARTESIAN_POINT('Ctrl Pts',(2.67851018218309,-0.556624844994064,
13.7381884353898));
#445825=CARTESIAN_POINT('Ctrl Pts',(2.69337389732938,-0.554089518057324,
13.7368803041982));
#445826=CARTESIAN_POINT('Ctrl Pts',(2.6963106782014,-0.539238088657145,
13.7363986145813));
#445827=CARTESIAN_POINT('Origin',(2.6546186406673,-0.538412371535213,13.7902182540695));
#445828=CARTESIAN_POINT('Ctrl Pts',(2.62309630396294,-0.566159381129065,
13.8235227101244));
#445829=CARTESIAN_POINT('Ctrl Pts',(2.6344276322766,-0.564214210964931,
13.8358800583119));
#445830=CARTESIAN_POINT('Ctrl Pts',(2.63460046153234,-0.547643267144351,
13.8390832900376));
#445831=CARTESIAN_POINT('Ctrl Pts',(2.63485115326723,-0.564136841357434,
13.8124254819052));
#445832=CARTESIAN_POINT('Ctrl Pts',(2.64620448681279,-0.562187893426261,
13.8247886449157));
#445833=CARTESIAN_POINT('Ctrl Pts',(2.6463604910855,-0.545595833766022,
13.8279860620657));
#445834=CARTESIAN_POINT('Ctrl Pts',(2.64660073443048,-0.562115208022343,
13.8013225099955));
#445835=CARTESIAN_POINT('Ctrl Pts',(2.65797071659684,-0.560163403890322,
13.8136962257787));
#445836=CARTESIAN_POINT('Ctrl Pts',(2.65811512281515,-0.543549615287902,
13.8168830918626));
#445837=CARTESIAN_POINT('Ctrl Pts',(2.65834525242799,-0.560094445855734,
13.7902140179785));
#445838=CARTESIAN_POINT('Ctrl Pts',(2.66972687669737,-0.558140646855038,
13.802602731458));
#445839=CARTESIAN_POINT('Ctrl Pts',(2.66986456913051,-0.541504565786618,
13.8057746032558));
#445840=CARTESIAN_POINT('Origin',(2.61936967992036,-0.544477308918452,13.8235269408515));
#445841=CARTESIAN_POINT('Ctrl Pts',(2.60897866247895,-0.628029139618544,
13.8235269408515));
#445842=CARTESIAN_POINT('Ctrl Pts',(2.6185940671041,-0.634881921001724,
13.8362179249168));
#445843=CARTESIAN_POINT('Ctrl Pts',(2.61106227426729,-0.650209513791218,
13.8391868794938));
#445844=CARTESIAN_POINT('Ctrl Pts',(2.60018098578061,-0.621759142936774,
13.8400110824519));
#445845=CARTESIAN_POINT('Ctrl Pts',(2.60590472176222,-0.63003928238457,
13.8494522556837));
#445846=CARTESIAN_POINT('Ctrl Pts',(2.59664899136563,-0.639799371639376,
13.85569149686));
#445847=CARTESIAN_POINT('Ctrl Pts',(2.59194745789874,-0.607701876322504,
13.8586819406588));
#445848=CARTESIAN_POINT('Ctrl Pts',(2.59099219866414,-0.611949643198133,
13.868010383617));
#445849=CARTESIAN_POINT('Ctrl Pts',(2.583107152258,-0.616390241126949,13.8744918421245));
#445850=CARTESIAN_POINT('Ctrl Pts',(2.59885875804002,-0.57718457912396,
13.8587686893867));
#445851=CARTESIAN_POINT('Ctrl Pts',(2.59980546053999,-0.572974604979576,
13.8680909899357));
#445852=CARTESIAN_POINT('Ctrl Pts',(2.59461494677144,-0.565588471463025,
13.8745789365162));
#445853=CARTESIAN_POINT('Ctrl Pts',(2.61243597585564,-0.56799359830867,
13.8400379222776));
#445854=CARTESIAN_POINT('Ctrl Pts',(2.62117973085788,-0.563011933690384,
13.8494748685453));
#445855=CARTESIAN_POINT('Ctrl Pts',(2.6170783143062,-0.550208048048356,
13.8557104837033));
#445856=CARTESIAN_POINT('Ctrl Pts',(2.62310018328645,-0.566158714415902,
13.8235269408542));
#445857=CARTESIAN_POINT('Ctrl Pts',(2.63473667391585,-0.564156539442959,
13.8362179249195));
#445858=CARTESIAN_POINT('Ctrl Pts',(2.63460115632152,-0.547078933081472,
13.8391868794965));
#445859=CARTESIAN_POINT('Origin',(2.59621038579399,-0.645944806240145,13.8235269408515));
#445860=CARTESIAN_POINT('Ctrl Pts',(2.63810218970091,-0.648785122534795,
13.7902140241682));
#445861=CARTESIAN_POINT('Ctrl Pts',(2.64750894969526,-0.65548373894426,
13.8026027327198));
#445862=CARTESIAN_POINT('Ctrl Pts',(2.64041488405521,-0.670532066591146,
13.8057746032556));
#445863=CARTESIAN_POINT('Ctrl Pts',(2.62839752045813,-0.641868723348059,
13.8013225161808));
#445864=CARTESIAN_POINT('Ctrl Pts',(2.63779465683145,-0.648560491116481,
13.8136962270464));
#445865=CARTESIAN_POINT('Ctrl Pts',(2.63071631243388,-0.663591646957016,
13.8168830918628));
#445866=CARTESIAN_POINT('Ctrl Pts',(2.61868866744511,-0.634949342439386,
13.8124254880875));
#445867=CARTESIAN_POINT('Ctrl Pts',(2.62807204320249,-0.641631313289075,
13.8247886461867));
#445868=CARTESIAN_POINT('Ctrl Pts',(2.62101357611648,-0.656647924244738,
13.8279860620656));
#445869=CARTESIAN_POINT('Ctrl Pts',(2.60897546128649,-0.628026859097017,
13.8235227163066));
#445870=CARTESIAN_POINT('Ctrl Pts',(2.61834065014465,-0.634695878581757,
13.8358800595847));
#445871=CARTESIAN_POINT('Ctrl Pts',(2.61130650365315,-0.649700764917019,
13.8390832900376));
#445872=CARTESIAN_POINT('Origin',(2.62533712434353,-0.666703076897107,13.7902182540695));
#445873=CARTESIAN_POINT('Ctrl Pts',(2.65476464095167,-0.660660280878158,
13.7382347919292));
#445874=CARTESIAN_POINT('Ctrl Pts',(2.66706733681926,-0.669398790083003,
13.7369371795943));
#445875=CARTESIAN_POINT('Ctrl Pts',(2.66325853688308,-0.684062923881726,
13.7364597369711));
#445876=CARTESIAN_POINT('Ctrl Pts',(2.65630502907124,-0.661758096174705,
13.7595490285574));
#445877=CARTESIAN_POINT('Ctrl Pts',(2.66890067449476,-0.670705918411684,
13.7633824266926));
#445878=CARTESIAN_POINT('Ctrl Pts',(2.66537083029141,-0.68531529417547,
13.7648920890506));
#445879=CARTESIAN_POINT('Ctrl Pts',(2.64844913405539,-0.656159298299035,
13.780380659011));
#445880=CARTESIAN_POINT('Ctrl Pts',(2.65934704294824,-0.663894443272945,
13.7901039518744));
#445881=CARTESIAN_POINT('Ctrl Pts',(2.6546040213236,-0.67892738002177,13.7926933640891));
#445882=CARTESIAN_POINT('Ctrl Pts',(2.63479383481681,-0.646427337845055,
13.7936647693663));
#445883=CARTESIAN_POINT('Ctrl Pts',(2.64361871871215,-0.652679917806856,
13.8072068914933));
#445884=CARTESIAN_POINT('Ctrl Pts',(2.6359018557241,-0.667881703737182,
13.8104111085397));
#445885=CARTESIAN_POINT('Origin',(2.64221614027784,-0.678732545304336,13.7435492065112));
#445886=CARTESIAN_POINT('Origin',(2.64221614027784,-0.678732545304336,14.));
#445887=CARTESIAN_POINT('Origin',(2.64221614027784,-0.678732545304336,12.5369868989719));
#445888=CARTESIAN_POINT('Ctrl Pts',(2.6657699952109,-0.648591476475466,
12.506462012331));
#445889=CARTESIAN_POINT('Ctrl Pts',(2.67212327504875,-0.650137252426841,
12.4999388158272));
#445890=CARTESIAN_POINT('Ctrl Pts',(2.67204810741645,-0.650118963870176,
12.4907030323752));
#445891=CARTESIAN_POINT('Ctrl Pts',(2.66487950851664,-0.661836687557277,
12.5042014951932));
#445892=CARTESIAN_POINT('Ctrl Pts',(2.66786167977953,-0.667532980358285,
12.4980716682127));
#445893=CARTESIAN_POINT('Ctrl Pts',(2.66620876237332,-0.674120349277227,
12.4907355092743));
#445894=CARTESIAN_POINT('Ctrl Pts',(2.65917972992674,-0.663795826468017,
12.5218047446509));
#445895=CARTESIAN_POINT('Ctrl Pts',(2.6665049075857,-0.673061928302202,
12.5216906929434));
#445896=CARTESIAN_POINT('Ctrl Pts',(2.66346674756517,-0.684425921351274,
12.5161988840776));
#445897=CARTESIAN_POINT('Ctrl Pts',(2.65495311339357,-0.66079461019884,
12.5369868989719));
#445898=CARTESIAN_POINT('Ctrl Pts',(2.66745250313894,-0.66966990103993,
12.5369868989719));
#445899=CARTESIAN_POINT('Ctrl Pts',(2.66345498261638,-0.684469406477355,
12.5369868989719));
#445900=CARTESIAN_POINT('Origin',(5.0226946496705E-31,-6.29825987887742E-31,
12.5));
#445901=CARTESIAN_POINT('Origin',(2.65148770642212,-0.413283442896987,12.5));
#445902=CARTESIAN_POINT('',(2.65148770642212,-0.413283442896987,12.5893111709658));
#445903=CARTESIAN_POINT('',(2.65148770642212,-0.413283442896987,13.8235269408515));
#445904=CARTESIAN_POINT('',(2.65148770642212,-0.413283442896987,12.5));
#445905=CARTESIAN_POINT('',(2.68220951992086,-0.431598542529539,13.7902182540695));
#445906=CARTESIAN_POINT('',(2.65148770642212,-0.413283442896987,13.8235269408515));
#445907=CARTESIAN_POINT('',(2.70001288567339,-0.442212187377219,13.7435492065112));
#445908=CARTESIAN_POINT('Origin',(2.64144021448603,-0.407293156316728,13.7445212918719));
#445909=CARTESIAN_POINT('',(2.70001288567339,-0.442212187377219,12.5369868989719));
#445910=CARTESIAN_POINT('',(2.70001288567339,-0.442212187377219,12.5));
#445911=CARTESIAN_POINT('Ctrl Pts',(2.70001288567339,-0.442212187377219,
12.5369868989719));
#445912=CARTESIAN_POINT('Ctrl Pts',(2.68384962302776,-0.432576305506054,
12.5544431401645));
#445913=CARTESIAN_POINT('Ctrl Pts',(2.66767479998709,-0.422933531796069,
12.5718848856037));
#445914=CARTESIAN_POINT('Ctrl Pts',(2.65148770642212,-0.413283442896987,
12.5893111709658));
#445915=CARTESIAN_POINT('Origin',(2.92683412199199,-0.281901273217275,12.5));
#445916=CARTESIAN_POINT('',(2.71522896268845,-0.336382047150378,13.7435492065112));
#445917=CARTESIAN_POINT('',(2.69515654904187,-0.341549977052325,13.7902182540695));
#445918=CARTESIAN_POINT('Origin',(2.6424097151889,-0.355130403636861,13.7418732680445));
#445919=CARTESIAN_POINT('',(2.66051922500485,-0.350467851393004,13.8235269408515));
#445920=CARTESIAN_POINT('',(2.69515654904187,-0.341549977052325,13.7902182540695));
#445921=CARTESIAN_POINT('',(2.66051922500485,-0.350467851393004,12.5893111709658));
#445922=CARTESIAN_POINT('',(2.66051922500485,-0.350467851393004,12.5));
#445923=CARTESIAN_POINT('',(2.71522896268845,-0.336382047150378,12.5369868989719));
#445924=CARTESIAN_POINT('Ctrl Pts',(2.66051922500485,-0.350467851393004,
12.5893111709658));
#445925=CARTESIAN_POINT('Ctrl Pts',(2.67876937176296,-0.345769090157469,
12.5718848856037));
#445926=CARTESIAN_POINT('Ctrl Pts',(2.6970056841123,-0.341073890788288,
12.5544431401645));
#445927=CARTESIAN_POINT('Ctrl Pts',(2.71522896268845,-0.336382047150378,
12.5369868989719));
#445928=CARTESIAN_POINT('',(2.71522896268845,-0.336382047150378,12.5));
#445929=CARTESIAN_POINT('Origin',(2.66909004727682,-0.383757213516397,12.5));
#445930=CARTESIAN_POINT('',(2.63492438425327,-0.379975991182365,13.8587068136939));
#445931=CARTESIAN_POINT('Ctrl Pts',(2.66051922500306,-0.35046785138664,
13.8235269408542));
#445932=CARTESIAN_POINT('Ctrl Pts',(2.65882226809953,-0.350904757205673,
13.8262006681044));
#445933=CARTESIAN_POINT('Ctrl Pts',(2.65712899959872,-0.351520118738613,
13.8288634856214));
#445934=CARTESIAN_POINT('Ctrl Pts',(2.65544060585013,-0.352300654471122,
13.8314912288862));
#445935=CARTESIAN_POINT('Ctrl Pts',(2.65370004604506,-0.35310530630281,
13.8342001611531));
#445936=CARTESIAN_POINT('Ctrl Pts',(2.65196252503803,-0.354085939487892,
13.8368750301949));
#445937=CARTESIAN_POINT('Ctrl Pts',(2.65022855609291,-0.355273197174807,
13.8394886372969));
#445938=CARTESIAN_POINT('Ctrl Pts',(2.65009463746527,-0.355364891965846,
13.8396904925131));
#445939=CARTESIAN_POINT('Ctrl Pts',(2.64996074920235,-0.355457839398141,
13.8398919674349));
#445940=CARTESIAN_POINT('Ctrl Pts',(2.6498268971788,-0.355552063547096,
13.8400930404591));
#445941=CARTESIAN_POINT('Ctrl Pts',(2.64774139260054,-0.35702013917882,
13.8432258934518));
#445942=CARTESIAN_POINT('Ctrl Pts',(2.64567467909338,-0.358789735788876,
13.8462331177034));
#445943=CARTESIAN_POINT('Ctrl Pts',(2.64375690289258,-0.360876414117512,
13.8489036603661));
#445944=CARTESIAN_POINT('Ctrl Pts',(2.64312938420138,-0.361559199550543,
13.849777493004));
#445945=CARTESIAN_POINT('Ctrl Pts',(2.64251805414996,-0.362275872798793,
13.85061494757));
#445946=CARTESIAN_POINT('Ctrl Pts',(2.64192816127125,-0.363026792313282,
13.8514076489583));
#445947=CARTESIAN_POINT('Ctrl Pts',(2.64068045275748,-0.36461509538524,
13.8530843267192));
#445948=CARTESIAN_POINT('Ctrl Pts',(2.63940841886039,-0.366514451031733,
13.8546805203176));
#445949=CARTESIAN_POINT('Ctrl Pts',(2.63829925771375,-0.368690547166666,
13.8559412814274));
#445950=CARTESIAN_POINT('Ctrl Pts',(2.63815081598139,-0.368981779401964,
13.8561100121513));
#445951=CARTESIAN_POINT('Ctrl Pts',(2.63800526195279,-0.369277897448965,
13.8562727473908));
#445952=CARTESIAN_POINT('Ctrl Pts',(2.63786300667071,-0.369578753235722,
13.8564289040185));
#445953=CARTESIAN_POINT('Ctrl Pts',(2.63721788058935,-0.370943130796488,
13.8571370725437));
#445954=CARTESIAN_POINT('Ctrl Pts',(2.63663131538603,-0.372429900315262,
13.8577210840553));
#445955=CARTESIAN_POINT('Ctrl Pts',(2.63615341118017,-0.373992041371059,
13.8581177131616));
#445956=CARTESIAN_POINT('Ctrl Pts',(2.63601881690684,-0.374431994059635,
13.8582294175695));
#445957=CARTESIAN_POINT('Ctrl Pts',(2.63589268503048,-0.374877840835603,
13.8583265086086));
#445958=CARTESIAN_POINT('Ctrl Pts',(2.63577573595751,-0.375328346333484,
13.8584082369006));
#445959=CARTESIAN_POINT('Ctrl Pts',(2.63560771150078,-0.375975601926112,
13.8585256585398));
#445960=CARTESIAN_POINT('Ctrl Pts',(2.63545686620342,-0.376640602202095,
13.8586122832068));
#445961=CARTESIAN_POINT('Ctrl Pts',(2.63532788871157,-0.377306247072293,
13.8586682984299));
#445962=CARTESIAN_POINT('Ctrl Pts',(2.63522471950323,-0.377838696985198,
13.8587131050557));
#445963=CARTESIAN_POINT('Ctrl Pts',(2.63513417251693,-0.378377395644967,
13.8587357943552));
#445964=CARTESIAN_POINT('Ctrl Pts',(2.63505673643312,-0.378922491011946,
13.8587355499465));
#445965=CARTESIAN_POINT('Ctrl Pts',(2.63500668764599,-0.37927479914334,
13.8587353919793));
#445966=CARTESIAN_POINT('Ctrl Pts',(2.63496261866818,-0.379625964148031,
13.8587257282814));
#445967=CARTESIAN_POINT('Ctrl Pts',(2.63492438425327,-0.379975991182365,
13.8587068136939));
#445968=CARTESIAN_POINT('Ctrl Pts',(2.63492438425327,-0.379975991182365,
13.8587068136939));
#445969=CARTESIAN_POINT('Ctrl Pts',(2.63479863334703,-0.381127211016178,
13.8586446046466));
#445970=CARTESIAN_POINT('Ctrl Pts',(2.63473591796092,-0.382266137179996,
13.858482427929));
#445971=CARTESIAN_POINT('Ctrl Pts',(2.63473176793904,-0.383392830200595,
13.8582284286032));
#445972=CARTESIAN_POINT('Ctrl Pts',(2.63472751049935,-0.384548686177452,
13.8579678548414));
#445973=CARTESIAN_POINT('Ctrl Pts',(2.63478641067422,-0.385694496621405,
13.857615680862));
#445974=CARTESIAN_POINT('Ctrl Pts',(2.63489646947545,-0.38678558624549,
13.8571944833187));
#445975=CARTESIAN_POINT('Ctrl Pts',(2.6351711324698,-0.389508511989885,
13.8561433417727));
#445976=CARTESIAN_POINT('Ctrl Pts',(2.6357724896341,-0.392018486007384,
13.8546163505474));
#445977=CARTESIAN_POINT('Ctrl Pts',(2.63651730532133,-0.394219682600469,
13.8528973491086));
#445978=CARTESIAN_POINT('Ctrl Pts',(2.63665337215866,-0.394621808742403,
13.8525833129072));
#445979=CARTESIAN_POINT('Ctrl Pts',(2.63679412895954,-0.395013731792354,
13.8522628768812));
#445980=CARTESIAN_POINT('Ctrl Pts',(2.63693835648476,-0.395395014330815,
13.851937733538));
#445981=CARTESIAN_POINT('Ctrl Pts',(2.63781913397061,-0.397723453892613,
13.8499521282529));
#445982=CARTESIAN_POINT('Ctrl Pts',(2.63892069498174,-0.399885029023759,
13.847639871647));
#445983=CARTESIAN_POINT('Ctrl Pts',(2.64011356391708,-0.40180261406227,
13.8452109780794));
#445984=CARTESIAN_POINT('Ctrl Pts',(2.64065026034225,-0.402665375263132,
13.8441181685877));
#445985=CARTESIAN_POINT('Ctrl Pts',(2.64120499936357,-0.403479312399116,
13.8430021611332));
#445986=CARTESIAN_POINT('Ctrl Pts',(2.64176486499218,-0.404240513175644,
13.8418824960098));
#445987=CARTESIAN_POINT('Ctrl Pts',(2.64308420264268,-0.406034302243487,
13.8392439765549));
#445988=CARTESIAN_POINT('Ctrl Pts',(2.64449203247698,-0.407623226823063,
13.8364981347964));
#445989=CARTESIAN_POINT('Ctrl Pts',(2.64596646455416,-0.409034182911206,
13.8336931113419));
#445990=CARTESIAN_POINT('Ctrl Pts',(2.64740246776224,-0.41040836453706,
13.8309611966328));
#445991=CARTESIAN_POINT('Ctrl Pts',(2.64890347590911,-0.411614702997043,
13.8281701127186));
#445992=CARTESIAN_POINT('Ctrl Pts',(2.65046424590118,-0.412641712350236,
13.8253580685121));
#445993=CARTESIAN_POINT('Ctrl Pts',(2.6508026225199,-0.412864369086392,
13.8247484142933));
#445994=CARTESIAN_POINT('Ctrl Pts',(2.65114380648299,-0.413078423696242,
13.8241378483365));
#445995=CARTESIAN_POINT('Ctrl Pts',(2.65148770642212,-0.413283442896987,
13.8235269408515));
#445996=CARTESIAN_POINT('',(2.63508325539423,-0.378744107738709,12.5969504640361));
#445997=CARTESIAN_POINT('Origin',(2.66912276806067,-0.383762115874432,12.584524458991));
#445998=CARTESIAN_POINT('Origin',(2.66912276806067,-0.383762115874432,12.584524458991));
#445999=CARTESIAN_POINT('Ctrl Pts',(2.66051922500485,-0.350467851393004,
12.5893111709658));
#446000=CARTESIAN_POINT('Ctrl Pts',(2.64954321694341,-0.353293781610638,
12.5770542771492));
#446001=CARTESIAN_POINT('Ctrl Pts',(2.65059728690124,-0.369624507601204,
12.5737548217797));
#446002=CARTESIAN_POINT('Ctrl Pts',(2.68452007097744,-0.344288490417406,
12.5663937883685));
#446003=CARTESIAN_POINT('Ctrl Pts',(2.67353006149338,-0.347118025501498,
12.5540940315304));
#446004=CARTESIAN_POINT('Ctrl Pts',(2.67459060231887,-0.363499150263564,
12.5508374392248));
#446005=CARTESIAN_POINT('Ctrl Pts',(2.70849670039065,-0.338115364341283,
12.5434499600945));
#446006=CARTESIAN_POINT('Ctrl Pts',(2.69747095847214,-0.340954099251498,
12.5311293540533));
#446007=CARTESIAN_POINT('Ctrl Pts',(2.69856018390388,-0.357378634329323,
12.5278936106989));
#446008=CARTESIAN_POINT('Ctrl Pts',(2.73245101016076,-0.331947984776416,
12.5204817579905));
#446009=CARTESIAN_POINT('Ctrl Pts',(2.72137069835478,-0.334800769484485,
12.5081597038247));
#446010=CARTESIAN_POINT('Ctrl Pts',(2.72250787291556,-0.351262570082021,
12.5049254088044));
#446011=CARTESIAN_POINT('Ctrl Pts',(2.71522896268845,-0.336382047150378,
12.5369868989719));
#446012=CARTESIAN_POINT('Ctrl Pts',(2.71613104855338,-0.336149792413019,
12.5342545179733));
#446013=CARTESIAN_POINT('Ctrl Pts',(2.71702306144293,-0.336048945408998,
12.5314872231885));
#446014=CARTESIAN_POINT('Ctrl Pts',(2.71786103277611,-0.336140734051564,
12.5287124745063));
#446015=CARTESIAN_POINT('Ctrl Pts',(2.71861675691755,-0.336223513605412,
12.5262100684184));
#446016=CARTESIAN_POINT('Ctrl Pts',(2.71932765766955,-0.336463864304461,
12.5237004536639));
#446017=CARTESIAN_POINT('Ctrl Pts',(2.71998470981695,-0.336928711641806,
12.5212220730815));
#446018=CARTESIAN_POINT('Ctrl Pts',(2.72048774007532,-0.337284592491046,
12.5193246583486));
#446019=CARTESIAN_POINT('Ctrl Pts',(2.72096485386709,-0.337776827244795,
12.517417831369));
#446020=CARTESIAN_POINT('Ctrl Pts',(2.72136095927387,-0.338485533961445,
12.5155812248347));
#446021=CARTESIAN_POINT('Ctrl Pts',(2.72152970230623,-0.338787446832053,
12.5147988205793));
#446022=CARTESIAN_POINT('Ctrl Pts',(2.7216841570046,-0.339128816489286,
12.5140295443047));
#446023=CARTESIAN_POINT('Ctrl Pts',(2.72182218293109,-0.339516026505234,
12.5132817086137));
#446024=CARTESIAN_POINT('Ctrl Pts',(2.72203106649912,-0.340102016483784,
12.5121499604604));
#446025=CARTESIAN_POINT('Ctrl Pts',(2.72220009788286,-0.34080804871263,
12.5110494206568));
#446026=CARTESIAN_POINT('Ctrl Pts',(2.7222977756876,-0.341653986748281,
12.5100666561695));
#446027=CARTESIAN_POINT('Ctrl Pts',(2.72235386205816,-0.342139722420329,
12.5095023550641));
#446028=CARTESIAN_POINT('Ctrl Pts',(2.72238642252909,-0.342677272558588,
12.5089719619137));
#446029=CARTESIAN_POINT('Ctrl Pts',(2.72238847149647,-0.343256947543976,
12.5085043804652));
#446030=CARTESIAN_POINT('Ctrl Pts',(2.72239146989334,-0.344105226377113,
12.5078201359221));
#446031=CARTESIAN_POINT('Ctrl Pts',(2.72232800857336,-0.345068320699357,
12.5072563000949));
#446032=CARTESIAN_POINT('Ctrl Pts',(2.72219394159812,-0.346080390278256,
12.5068768744332));
#446033=CARTESIAN_POINT('Ctrl Pts',(2.72209727007977,-0.34681016211575,
12.5066032824114));
#446034=CARTESIAN_POINT('Ctrl Pts',(2.7219622490017,-0.347578227040838,
12.5064197834844));
#446035=CARTESIAN_POINT('Ctrl Pts',(2.72179896411096,-0.34834214185398,
12.5063282718343));
#446036=CARTESIAN_POINT('Ctrl Pts',(2.7215606187222,-0.349457220979117,
12.5061946931565));
#446037=CARTESIAN_POINT('Ctrl Pts',(2.72125799611724,-0.350587512994016,
12.5062515701262));
#446038=CARTESIAN_POINT('Ctrl Pts',(2.72092481596425,-0.351666869563629,
12.5064436508398));
#446039=CARTESIAN_POINT('',(2.65059728690124,-0.369624507601204,12.5737548217797));
#446040=CARTESIAN_POINT('Origin',(2.66600455125891,-0.371773043151976,12.5893111709658));
#446041=CARTESIAN_POINT('Ctrl Pts',(2.72092481596425,-0.351666869563629,
12.5064436508398));
#446042=CARTESIAN_POINT('Ctrl Pts',(2.71051463337505,-0.354325532048914,
12.5164271754438));
#446043=CARTESIAN_POINT('Ctrl Pts',(2.70010027249109,-0.356985045989405,
12.5264061185523));
#446044=CARTESIAN_POINT('Ctrl Pts',(2.68968158639056,-0.3596454422897,12.536380305637));
#446045=CARTESIAN_POINT('Ctrl Pts',(2.67666034190212,-0.362970398078559,
12.5488460165097));
#446046=CARTESIAN_POINT('Ctrl Pts',(2.66363233760314,-0.366296733065921,
12.5613043021964));
#446047=CARTESIAN_POINT('Ctrl Pts',(2.65059728690124,-0.369624507601204,
12.5737548217797));
#446048=CARTESIAN_POINT('Ctrl Pts',(2.65148770642212,-0.413283442896986,
12.5893111709658));
#446049=CARTESIAN_POINT('Ctrl Pts',(2.64175246035451,-0.40747968389418,
12.5770542771492));
#446050=CARTESIAN_POINT('Ctrl Pts',(2.64736473026114,-0.392107432876518,
12.5737548217797));
#446051=CARTESIAN_POINT('Ctrl Pts',(2.64240480651373,-0.407868586225798,
12.5928319619712));
#446052=CARTESIAN_POINT('Ctrl Pts',(2.63753030585758,-0.401169880401203,
12.5821634970842));
#446053=CARTESIAN_POINT('Ctrl Pts',(2.64405121633907,-0.390143039113135,
12.5773203894503));
#446054=CARTESIAN_POINT('Ctrl Pts',(2.63290585503669,-0.394071701788491,
12.5969440695591));
#446055=CARTESIAN_POINT('Ctrl Pts',(2.63345983373103,-0.390090288702896,
12.5878292599214));
#446056=CARTESIAN_POINT('Ctrl Pts',(2.64066728139681,-0.38522438773251,
12.5813877129824));
#446057=CARTESIAN_POINT('Ctrl Pts',(2.6372068775263,-0.363778526796667,
12.596957478804));
#446058=CARTESIAN_POINT('Ctrl Pts',(2.63665707227668,-0.367730527218781,
12.5878468778671));
#446059=CARTESIAN_POINT('Ctrl Pts',(2.64221258285488,-0.374382878994892,
12.5814011370086));
#446060=CARTESIAN_POINT('Ctrl Pts',(2.65026383573032,-0.353108248000009,
12.5928371701607));
#446061=CARTESIAN_POINT('Ctrl Pts',(2.64370794586564,-0.358163480317713,
12.5821692192952));
#446062=CARTESIAN_POINT('Ctrl Pts',(2.64685255955922,-0.370578601206617,
12.5773318885715));
#446063=CARTESIAN_POINT('Ctrl Pts',(2.66051922500483,-0.350467851392951,
12.5893111709658));
#446064=CARTESIAN_POINT('Ctrl Pts',(2.64954321694339,-0.353293781610586,
12.5770542771492));
#446065=CARTESIAN_POINT('Ctrl Pts',(2.65059728690122,-0.369624507601151,
12.5737548217797));
#446066=CARTESIAN_POINT('',(2.64736473026114,-0.392107432876518,12.5737548217797));
#446067=CARTESIAN_POINT('Origin',(2.66275320456913,-0.394386656093409,12.5893111709658));
#446068=CARTESIAN_POINT('Ctrl Pts',(2.65059728690122,-0.369624507601151,
12.5737548217797));
#446069=CARTESIAN_POINT('Ctrl Pts',(2.64961914639082,-0.369842591926409,
12.5746934679442));
#446070=CARTESIAN_POINT('Ctrl Pts',(2.64857663240156,-0.370262710981469,
12.5756680099006));
#446071=CARTESIAN_POINT('Ctrl Pts',(2.64758710873764,-0.370833978507702,
12.5765688348656));
#446072=CARTESIAN_POINT('Ctrl Pts',(2.64732514330201,-0.370985215261131,
12.5768073183026));
#446073=CARTESIAN_POINT('Ctrl Pts',(2.647066821301,-0.371146798286212,12.5770407398754));
#446074=CARTESIAN_POINT('Ctrl Pts',(2.6468140348489,-0.371317298000386,
12.5772674179684));
#446075=CARTESIAN_POINT('Ctrl Pts',(2.64577666760578,-0.372016982722287,
12.5781976435658));
#446076=CARTESIAN_POINT('Ctrl Pts',(2.6447799098633,-0.372915921811197,
12.5790594849312));
#446077=CARTESIAN_POINT('Ctrl Pts',(2.64392340493399,-0.373989277311363,
12.5797571720116));
#446078=CARTESIAN_POINT('Ctrl Pts',(2.64336536117536,-0.374688607014145,
12.580211740231));
#446079=CARTESIAN_POINT('Ctrl Pts',(2.64285616804033,-0.375505466446094,
12.5806009430798));
#446080=CARTESIAN_POINT('Ctrl Pts',(2.64244670534667,-0.376391724290526,
12.5808812374708));
#446081=CARTESIAN_POINT('Ctrl Pts',(2.64209484105497,-0.37715331379187,
12.5811221033394));
#446082=CARTESIAN_POINT('Ctrl Pts',(2.64180952282047,-0.377981790259704,
12.581287365893));
#446083=CARTESIAN_POINT('Ctrl Pts',(2.6416147380312,-0.378833108161147,
12.581359338449));
#446084=CARTESIAN_POINT('Ctrl Pts',(2.64158766696764,-0.378951423770407,
12.5813693411482));
#446085=CARTESIAN_POINT('Ctrl Pts',(2.64156228509801,-0.379070187430052,
12.5813775999465));
#446086=CARTESIAN_POINT('Ctrl Pts',(2.64153859601056,-0.379189289011997,
12.5813841266931));
#446087=CARTESIAN_POINT('Ctrl Pts',(2.64149840460858,-0.379391359250802,
12.5813952001081));
#446088=CARTESIAN_POINT('Ctrl Pts',(2.64146341390939,-0.379595874353134,
12.5814007534795));
#446089=CARTESIAN_POINT('Ctrl Pts',(2.64143383353787,-0.37980277850357,
12.5814005856065));
#446090=CARTESIAN_POINT('Ctrl Pts',(2.64129842616222,-0.380749904809983,
12.5813998171494));
#446091=CARTESIAN_POINT('Ctrl Pts',(2.64128541102912,-0.381681605516752,
12.58127954464));
#446092=CARTESIAN_POINT('Ctrl Pts',(2.64136527555804,-0.382592177734726,
12.5810700125799));
#446093=CARTESIAN_POINT('Ctrl Pts',(2.64146174281568,-0.383692045297091,
12.5808169217085));
#446094=CARTESIAN_POINT('Ctrl Pts',(2.64171040119885,-0.384759723791743,
12.5804173076348));
#446095=CARTESIAN_POINT('Ctrl Pts',(2.6420640951309,-0.385707550764392,
12.5799304713245));
#446096=CARTESIAN_POINT('Ctrl Pts',(2.6425024333378,-0.386882206979792,
12.5793271277669));
#446097=CARTESIAN_POINT('Ctrl Pts',(2.64309911845793,-0.387956906787091,
12.5785808224116));
#446098=CARTESIAN_POINT('Ctrl Pts',(2.64380126948767,-0.388901745288867,
12.5777485681082));
#446099=CARTESIAN_POINT('Ctrl Pts',(2.64484755144837,-0.390309658171298,
12.576508418016));
#446100=CARTESIAN_POINT('Ctrl Pts',(2.6461136868804,-0.391421467767638,
12.5750928681475));
#446101=CARTESIAN_POINT('Ctrl Pts',(2.64736473026114,-0.392107432876518,
12.5737548217797));
#446102=CARTESIAN_POINT('Ctrl Pts',(2.64736473026114,-0.392107432876518,
12.5737548217797));
#446103=CARTESIAN_POINT('Ctrl Pts',(2.64175246035451,-0.407479683894181,
12.5770542771492));
#446104=CARTESIAN_POINT('Ctrl Pts',(2.65148770642212,-0.413283442896987,
12.5893111709658));
#446105=CARTESIAN_POINT('Ctrl Pts',(2.66865723589171,-0.404742469803349,
12.5508408821982));
#446106=CARTESIAN_POINT('Ctrl Pts',(2.66302455843625,-0.420161246321361,
12.55409748406));
#446107=CARTESIAN_POINT('Ctrl Pts',(2.67277222418453,-0.425972409434243,
12.5663972313419));
#446108=CARTESIAN_POINT('Ctrl Pts',(2.68992833949995,-0.417366178255246,
12.52790050457));
#446109=CARTESIAN_POINT('Ctrl Pts',(2.68425591538701,-0.432818520538048,
12.5311362602938));
#446110=CARTESIAN_POINT('Ctrl Pts',(2.69403526936601,-0.438648574889328,
12.5434568539655));
#446111=CARTESIAN_POINT('Ctrl Pts',(2.71117969723077,-0.429979450509249,
12.5049357605811));
#446112=CARTESIAN_POINT('Ctrl Pts',(2.70545077826142,-0.445454038466022,
12.5081700652078));
#446113=CARTESIAN_POINT('Ctrl Pts',(2.71527852370348,-0.451312941845609,
12.5204921097672));
#446114=CARTESIAN_POINT('Ctrl Pts',(2.70978424896933,-0.429151214975375,
12.5064436508395));
#446115=CARTESIAN_POINT('Ctrl Pts',(2.7098010934493,-0.4303712822088,12.5062361689309));
#446116=CARTESIAN_POINT('Ctrl Pts',(2.70976658395257,-0.431640770578446,
12.5061871075068));
#446117=CARTESIAN_POINT('Ctrl Pts',(2.70966417203871,-0.432865731165968,
12.5063648335171));
#446118=CARTESIAN_POINT('Ctrl Pts',(2.7096176502304,-0.433422183823524,
12.5064455676336));
#446119=CARTESIAN_POINT('Ctrl Pts',(2.70955624807807,-0.433977191009861,
12.506574497099));
#446120=CARTESIAN_POINT('Ctrl Pts',(2.70948155374489,-0.434506840121112,
12.5067492519495));
#446121=CARTESIAN_POINT('Ctrl Pts',(2.70933145258294,-0.435571190569707,
12.5071004286051));
#446122=CARTESIAN_POINT('Ctrl Pts',(2.70912135537376,-0.436572158368801,
12.5076537929613));
#446123=CARTESIAN_POINT('Ctrl Pts',(2.7088762877546,-0.437436558570328,
12.5083435010505));
#446124=CARTESIAN_POINT('Ctrl Pts',(2.70886085928344,-0.437490977728702,
12.5083869222964));
#446125=CARTESIAN_POINT('Ctrl Pts',(2.7088452790438,-0.437544858286733,
12.5084308732337));
#446126=CARTESIAN_POINT('Ctrl Pts',(2.70882954799834,-0.437598183461513,
12.5084753333615));
#446127=CARTESIAN_POINT('Ctrl Pts',(2.70870336425065,-0.438025921746073,
12.5088319622689));
#446128=CARTESIAN_POINT('Ctrl Pts',(2.70856615304605,-0.438426974615727,
12.509227847131));
#446129=CARTESIAN_POINT('Ctrl Pts',(2.70842464368023,-0.438790323073624,
12.5096423454524));
#446130=CARTESIAN_POINT('Ctrl Pts',(2.70798121595715,-0.439928896329383,
12.5109411997424));
#446131=CARTESIAN_POINT('Ctrl Pts',(2.70747731962361,-0.440770781460926,
12.5124831113042));
#446132=CARTESIAN_POINT('Ctrl Pts',(2.7069677858636,-0.441393110813353,
12.5140723025008));
#446133=CARTESIAN_POINT('Ctrl Pts',(2.70692004199221,-0.441451423755293,
12.5142212114565));
#446134=CARTESIAN_POINT('Ctrl Pts',(2.70687225620062,-0.441507837642663,
12.5143705582413));
#446135=CARTESIAN_POINT('Ctrl Pts',(2.70682447941976,-0.441562431884413,
12.5145201959299));
#446136=CARTESIAN_POINT('Ctrl Pts',(2.70621071553744,-0.442263776202016,
12.5164425148273));
#446137=CARTESIAN_POINT('Ctrl Pts',(2.7055854897805,-0.442695922626524,
12.5184635205941));
#446138=CARTESIAN_POINT('Ctrl Pts',(2.70495520700584,-0.44294885424723,
12.5205025929158));
#446139=CARTESIAN_POINT('Ctrl Pts',(2.70458961801446,-0.443095564612512,
12.5216853356836));
#446140=CARTESIAN_POINT('Ctrl Pts',(2.70422316810204,-0.4431821626277,12.5228750347131));
#446141=CARTESIAN_POINT('Ctrl Pts',(2.70386298154135,-0.443225446458932,
12.5240609649613));
#446142=CARTESIAN_POINT('Ctrl Pts',(2.70297892295147,-0.443331684300595,
12.5269717671326));
#446143=CARTESIAN_POINT('Ctrl Pts',(2.70210647539127,-0.443169652689853,
12.5299036066169));
#446144=CARTESIAN_POINT('Ctrl Pts',(2.7012437201377,-0.442825987884302,
12.5328133004019));
#446145=CARTESIAN_POINT('Ctrl Pts',(2.70082954737924,-0.442661008766634,
12.5342101228451));
#446146=CARTESIAN_POINT('Ctrl Pts',(2.70041831897813,-0.442453890180351,
12.5356023438238));
#446147=CARTESIAN_POINT('Ctrl Pts',(2.70001288567339,-0.442212187377219,
12.5369868989719));
#446148=CARTESIAN_POINT('Origin',(13.6445776740604,-6.97308410522103,-1.23972230381871));
#446149=CARTESIAN_POINT('Ctrl Pts',(2.71518847849396,-0.336392429391334,
12.5369868989719));
#446150=CARTESIAN_POINT('Ctrl Pts',(2.7300502269415,-0.332596150059323,
12.5369868989719));
#446151=CARTESIAN_POINT('Ctrl Pts',(2.7316270800589,-0.317338468782966,
12.5369868989719));
#446152=CARTESIAN_POINT('Ctrl Pts',(2.72021231432179,-0.335109074353454,
12.5218025310015));
#446153=CARTESIAN_POINT('Ctrl Pts',(2.73038128743446,-0.329088455652839,
12.5216901060417));
#446154=CARTESIAN_POINT('Ctrl Pts',(2.7316222896924,-0.317384980947354,
12.5161920673678));
#446155=CARTESIAN_POINT('Ctrl Pts',(2.72483095825869,-0.338982599799196,
12.5042015548895));
#446156=CARTESIAN_POINT('Ctrl Pts',(2.72966079725187,-0.334734070604651,
12.4980677368514));
#446157=CARTESIAN_POINT('Ctrl Pts',(2.73048197451111,-0.32798748275355,
12.4907278922777));
#446158=CARTESIAN_POINT('Ctrl Pts',(2.72090497986881,-0.351664305851125,
12.506463626192));
#446159=CARTESIAN_POINT('Ctrl Pts',(2.72739374832251,-0.352502948975741,
12.4999376786891));
#446160=CARTESIAN_POINT('Ctrl Pts',(2.72731449745051,-0.352492706169361,
12.4906970594712));
#446161=CARTESIAN_POINT('Origin',(2.70974363643439,-0.315076855391407,12.5369868989719));
#446162=CARTESIAN_POINT('Origin',(2.70974363643439,-0.315076855391407,14.));
#446163=CARTESIAN_POINT('Origin',(2.70974363643439,-0.315076855391407,13.7435492065112));
#446164=CARTESIAN_POINT('Ctrl Pts',(2.6912508303197,-0.342555532146921,
13.793642941384));
#446165=CARTESIAN_POINT('Ctrl Pts',(2.70172842566934,-0.339886035060387,
13.8071662555867));
#446166=CARTESIAN_POINT('Ctrl Pts',(2.69999584404053,-0.322944442911652,
13.8103758687955));
#446167=CARTESIAN_POINT('Ctrl Pts',(2.70734702183498,-0.338411340557862,
13.7804579775006));
#446168=CARTESIAN_POINT('Ctrl Pts',(2.72027292376789,-0.335107595569272,
13.7901904343351));
#446169=CARTESIAN_POINT('Ctrl Pts',(2.72122708172638,-0.319380373730858,
13.7927914348263));
#446170=CARTESIAN_POINT('Ctrl Pts',(2.71682345553838,-0.335971498969084,
13.7597120340895));
#446171=CARTESIAN_POINT('Ctrl Pts',(2.73178094522877,-0.332142583700462,
13.7635825532445));
#446172=CARTESIAN_POINT('Ctrl Pts',(2.73374288637564,-0.317253436542894,
13.7651073818884));
#446173=CARTESIAN_POINT('Ctrl Pts',(2.71496775283338,-0.336449275817405,
13.7381884353898));
#446174=CARTESIAN_POINT('Ctrl Pts',(2.72957535751151,-0.332710854199482,
13.7368803041982));
#446175=CARTESIAN_POINT('Ctrl Pts',(2.73129183711739,-0.317669466800656,
13.7363986145813));
#446176=CARTESIAN_POINT('Origin',(2.68967122278781,-0.320244785293354,13.7902182540695));
#446177=CARTESIAN_POINT('Ctrl Pts',(2.66051541293097,-0.350468832082256,
13.8235227101244));
#446178=CARTESIAN_POINT('Ctrl Pts',(2.671650487758,-0.347606525858912,13.8358800583119));
#446179=CARTESIAN_POINT('Ctrl Pts',(2.67047205618014,-0.331076633298055,
13.8390832900376));
#446180=CARTESIAN_POINT('Ctrl Pts',(2.67206629317621,-0.347494892799863,
13.8124254819053));
#446181=CARTESIAN_POINT('Ctrl Pts',(2.68322299209147,-0.344627027748994,
13.8247886449158));
#446182=CARTESIAN_POINT('Ctrl Pts',(2.68202607037732,-0.328077461002008,
13.8279860620657));
#446183=CARTESIAN_POINT('Ctrl Pts',(2.68361199669266,-0.34452228634033,
13.8013225099955));
#446184=CARTESIAN_POINT('Ctrl Pts',(2.69478505602488,-0.34165021757521,
13.8136962257787));
#446185=CARTESIAN_POINT('Ctrl Pts',(2.69357480373744,-0.325079939536435,
13.8168830918626));
#446186=CARTESIAN_POINT('Ctrl Pts',(2.69515272489896,-0.341550960845551,
13.7902140179785));
#446187=CARTESIAN_POINT('Ctrl Pts',(2.70633722499578,-0.33867595491007,
13.802602731458));
#446188=CARTESIAN_POINT('Ctrl Pts',(2.70511846421978,-0.322084005817429,
13.8057746032558));
#446189=CARTESIAN_POINT('Origin',(2.65503389875079,-0.329162659634033,13.8235269408515));
#446190=CARTESIAN_POINT('Ctrl Pts',(2.65148770642212,-0.413283442896987,
13.8235269408515));
#446191=CARTESIAN_POINT('Ctrl Pts',(2.66162968188245,-0.419329677473419,
13.8362179249168));
#446192=CARTESIAN_POINT('Ctrl Pts',(2.65537229157174,-0.435220180000298,
13.8391868794938));
#446193=CARTESIAN_POINT('Ctrl Pts',(2.64220824032984,-0.407751401436477,
13.8400110824519));
#446194=CARTESIAN_POINT('Ctrl Pts',(2.64858783928619,-0.415537451784206,
13.8494522556836));
#446195=CARTESIAN_POINT('Ctrl Pts',(2.64015844445153,-0.426019493100529,
13.85569149686));
#446196=CARTESIAN_POINT('Ctrl Pts',(2.63285631110245,-0.394412018175957,
13.8586819406588));
#446197=CARTESIAN_POINT('Ctrl Pts',(2.63225046284887,-0.398723513453536,
13.868010383617));
#446198=CARTESIAN_POINT('Ctrl Pts',(2.62475360323986,-0.403792040142369,
13.8744918421245));
#446199=CARTESIAN_POINT('Ctrl Pts',(2.6372571714322,-0.363432929643449,
13.8587686893867));
#446200=CARTESIAN_POINT('Ctrl Pts',(2.63785757188144,-0.359159798798226,
13.8680909899357));
#446201=CARTESIAN_POINT('Ctrl Pts',(2.63208229066815,-0.352221317090155,
13.8745789365163));
#446202=CARTESIAN_POINT('Ctrl Pts',(2.65004006191426,-0.3531658617619,13.8400379222776));
#446203=CARTESIAN_POINT('Ctrl Pts',(2.65834867087912,-0.347488076015957,
13.8494748685453));
#446204=CARTESIAN_POINT('Ctrl Pts',(2.65321726590736,-0.33506109777179,
13.8557104837033));
#446205=CARTESIAN_POINT('Ctrl Pts',(2.66051922500306,-0.35046785138664,
13.8235269408542));
#446206=CARTESIAN_POINT('Ctrl Pts',(2.67195380032226,-0.347523856471547,
13.8362179249195));
#446207=CARTESIAN_POINT('Ctrl Pts',(2.67042675019232,-0.330514120378444,
13.8391868794965));
#446208=CARTESIAN_POINT('Origin',(2.64022220827512,-0.432180229700564,13.8235269408515));
#446209=CARTESIAN_POINT('Ctrl Pts',(2.68220613280659,-0.4315965241541,13.7902140241682));
#446210=CARTESIAN_POINT('Ctrl Pts',(2.69212759200737,-0.437506113202412,
13.8026027327198));
#446211=CARTESIAN_POINT('Ctrl Pts',(2.68628370969059,-0.453082600988223,
13.8057746032556));
#446212=CARTESIAN_POINT('Ctrl Pts',(2.67197000430769,-0.425494159352134,
13.8013225161807));
#446213=CARTESIAN_POINT('Ctrl Pts',(2.68188131368142,-0.431397706962145,
13.8136962270464));
#446214=CARTESIAN_POINT('Ctrl Pts',(2.67605170063436,-0.44695579865218,
13.8168830918628));
#446215=CARTESIAN_POINT('Ctrl Pts',(2.66172946292172,-0.419389163765796,
13.8124254880875));
#446216=CARTESIAN_POINT('Ctrl Pts',(2.67162625892701,-0.425284068673469,
13.8247886461868));
#446217=CARTESIAN_POINT('Ctrl Pts',(2.6658152715082,-0.440826043690079,
13.8279860620656));
#446218=CARTESIAN_POINT('Ctrl Pts',(2.65148432999768,-0.413281430890604,
13.8235227163065));
#446219=CARTESIAN_POINT('Ctrl Pts',(2.66136194396267,-0.419164909929044,
13.8358800595847));
#446220=CARTESIAN_POINT('Ctrl Pts',(2.65557424054823,-0.434693216983744,
13.8390832900376));
#446221=CARTESIAN_POINT('Origin',(2.67094402177386,-0.450495329333115,13.7902182540695));
#446222=CARTESIAN_POINT('Ctrl Pts',(2.69978107677395,-0.442074024424127,
13.7382347919292));
#446223=CARTESIAN_POINT('Ctrl Pts',(2.71275510606049,-0.449780673034605,
13.7369371795943));
#446224=CARTESIAN_POINT('Ctrl Pts',(2.71015424263167,-0.464706465691778,
13.7364597369712));
#446225=CARTESIAN_POINT('Ctrl Pts',(2.70140582151744,-0.443042630898841,
13.7595490285574));
#446226=CARTESIAN_POINT('Ctrl Pts',(2.71468888654972,-0.450934017961181,
13.7633824266926));
#446227=CARTESIAN_POINT('Ctrl Pts',(2.71236158736332,-0.465782497304353,
13.7648920890506));
#446228=CARTESIAN_POINT('Ctrl Pts',(2.6931197123406,-0.438102790935586,
13.7803806590111));
#446229=CARTESIAN_POINT('Ctrl Pts',(2.70461184546554,-0.444923917106686,
13.7901039518744));
#446230=CARTESIAN_POINT('Ctrl Pts',(2.70110992975812,-0.460293433293067,
13.7926933640892));
#446231=CARTESIAN_POINT('Ctrl Pts',(2.67871660485965,-0.429516246434742,
13.7936647693663));
#446232=CARTESIAN_POINT('Ctrl Pts',(2.68802176799482,-0.435028711488828,
13.8072068914933));
#446233=CARTESIAN_POINT('Ctrl Pts',(2.68156966891159,-0.450808910703906,
13.8104111085397));
#446234=CARTESIAN_POINT('Origin',(2.68874738752638,-0.461108974180797,13.7435492065112));
#446235=CARTESIAN_POINT('Origin',(2.68874738752638,-0.461108974180797,14.));
#446236=CARTESIAN_POINT('Origin',(2.68874738752638,-0.461108974180797,12.5369868989719));
#446237=CARTESIAN_POINT('Ctrl Pts',(2.70976609202462,-0.429148339431626,
12.506462012331));
#446238=CARTESIAN_POINT('Ctrl Pts',(2.71622422693825,-0.430171120653283,
12.4999388158272));
#446239=CARTESIAN_POINT('Ctrl Pts',(2.7161478187329,-0.430159019810136,
12.4907030323752));
#446240=CARTESIAN_POINT('Ctrl Pts',(2.7099581760171,-0.442422061098678,
12.5042014951932));
#446241=CARTESIAN_POINT('Ctrl Pts',(2.71339472509621,-0.44785632531225,
12.4980716682127));
#446242=CARTESIAN_POINT('Ctrl Pts',(2.71228423935735,-0.45455650341807,
12.4907355092743));
#446243=CARTESIAN_POINT('Ctrl Pts',(2.70443705097922,-0.444839266005536,
12.5218047446509));
#446244=CARTESIAN_POINT('Ctrl Pts',(2.71249312803559,-0.45347746566743,
12.5216906929434));
#446245=CARTESIAN_POINT('Ctrl Pts',(2.71039134817357,-0.465051284213677,
12.5161988840776));
#446246=CARTESIAN_POINT('Ctrl Pts',(2.69997987117604,-0.442192544521366,
12.5369868989719));
#446247=CARTESIAN_POINT('Ctrl Pts',(2.71316108883089,-0.450019487261421,
12.5369868989719));
#446248=CARTESIAN_POINT('Ctrl Pts',(2.71038316681315,-0.465095583599136,
12.5369868989719));
#446249=CARTESIAN_POINT('Origin',(5.09942406832774E-31,-5.88504909413687E-31,
12.5));
#446250=CARTESIAN_POINT('Origin',(2.67635153714374,-0.195787413049918,12.5));
#446251=CARTESIAN_POINT('',(2.67635153714374,-0.195787413049918,12.5893111709658));
#446252=CARTESIAN_POINT('',(2.67635153714374,-0.195787413049918,13.8235269408515));
#446253=CARTESIAN_POINT('',(2.67635153714374,-0.195787413049918,12.5));
#446254=CARTESIAN_POINT('',(2.70846397699157,-0.211537457691783,13.7902182540695));
#446255=CARTESIAN_POINT('',(2.67635153714374,-0.195787413049918,13.8235269408515));
#446256=CARTESIAN_POINT('',(2.72707321410059,-0.220664646924583,13.7435492065112));
#446257=CARTESIAN_POINT('Origin',(2.66584921343154,-0.190636022518706,13.744521291868));
#446258=CARTESIAN_POINT('',(2.72707321410059,-0.220664646924583,12.5369868989719));
#446259=CARTESIAN_POINT('',(2.72707321410059,-0.220664646924583,12.5));
#446260=CARTESIAN_POINT('Ctrl Pts',(2.72707321410059,-0.220664646924583,
12.5369868989719));
#446261=CARTESIAN_POINT('Ctrl Pts',(2.71017831955038,-0.212378283613468,
12.5544431401645));
#446262=CARTESIAN_POINT('Ctrl Pts',(2.69327134132254,-0.204085993675075,
12.5718848856037));
#446263=CARTESIAN_POINT('Ctrl Pts',(2.67635153714374,-0.195787413049918,
12.5893111709658));
#446264=CARTESIAN_POINT('Origin',(2.94007289370883,-0.042399117641198,12.5));
#446265=CARTESIAN_POINT('',(2.73361252196705,-0.11394639622308,13.7435492065112));
#446266=CARTESIAN_POINT('',(2.71402813188475,-0.120733218319995,13.7902182540695));
#446267=CARTESIAN_POINT('Origin',(2.66256373961082,-0.138567813792271,13.7418732680442));
#446268=CARTESIAN_POINT('',(2.68023295023436,-0.132444682635723,13.8235269408515));
#446269=CARTESIAN_POINT('',(2.71402813188475,-0.120733218319995,13.7902182540695));
#446270=CARTESIAN_POINT('',(2.68023295023436,-0.132444682635723,12.5893111709658));
#446271=CARTESIAN_POINT('',(2.68023295023436,-0.132444682635723,12.5));
#446272=CARTESIAN_POINT('',(2.73361252196705,-0.11394639622308,12.5369868989719));
#446273=CARTESIAN_POINT('Ctrl Pts',(2.68023295023436,-0.132444682635723,
12.5893111709658));
#446274=CARTESIAN_POINT('Ctrl Pts',(2.6980393784728,-0.126273999753697,
12.5718848856037));
#446275=CARTESIAN_POINT('Ctrl Pts',(2.71583230866049,-0.120107994518955,
12.5544431401645));
#446276=CARTESIAN_POINT('Ctrl Pts',(2.73361252196705,-0.11394639622308,
12.5369868989719));
#446277=CARTESIAN_POINT('',(2.73361252196705,-0.11394639622308,12.5));
#446278=CARTESIAN_POINT('Origin',(2.69148864585867,-0.164924675570032,12.5));
#446279=CARTESIAN_POINT('',(2.657128461537,-0.163940853655835,13.8587068136939));
#446280=CARTESIAN_POINT('Ctrl Pts',(2.68023295023206,-0.132444682629526,
13.8235269408542));
#446281=CARTESIAN_POINT('Ctrl Pts',(2.67857725169292,-0.133018452421904,
13.8262006681044));
#446282=CARTESIAN_POINT('Ctrl Pts',(2.67693977508105,-0.133769783492457,
13.8288634856214));
#446283=CARTESIAN_POINT('Ctrl Pts',(2.67532062023171,-0.134685341821493,
13.8314912288862));
#446284=CARTESIAN_POINT('Ctrl Pts',(2.67365143859012,-0.135629188023266,
13.8342001611531));
#446285=CARTESIAN_POINT('Ctrl Pts',(2.67199962974925,-0.136748182324745,
13.8368750301949));
#446286=CARTESIAN_POINT('Ctrl Pts',(2.6703682029662,-0.138072824076052,
13.8394886372968));
#446287=CARTESIAN_POINT('Ctrl Pts',(2.67024220391846,-0.138175129371639,
13.8396904925131));
#446288=CARTESIAN_POINT('Ctrl Pts',(2.67011633723629,-0.138278680665416,
13.8398919674349));
#446289=CARTESIAN_POINT('Ctrl Pts',(2.66999061073717,-0.138383501473838,
13.8400930404591));
#446290=CARTESIAN_POINT('Ctrl Pts',(2.66803170729628,-0.140016680189018,
13.8432258934518));
#446291=CARTESIAN_POINT('Ctrl Pts',(2.66611610915967,-0.141948844949605,
13.8462331177034));
#446292=CARTESIAN_POINT('Ctrl Pts',(2.66437479785653,-0.144184896592378,
13.8489036603661));
#446293=CARTESIAN_POINT('Ctrl Pts',(2.66380502053348,-0.144916558712134,
13.8497774930041));
#446294=CARTESIAN_POINT('Ctrl Pts',(2.66325414015538,-0.14568067636377,
13.85061494757));
#446295=CARTESIAN_POINT('Ctrl Pts',(2.66272741700819,-0.14647717900143,
13.8514076489583));
#446296=CARTESIAN_POINT('Ctrl Pts',(2.66161332158704,-0.14816189695295,
13.8530843267192));
#446297=CARTESIAN_POINT('Ctrl Pts',(2.66050033539577,-0.15015861522178,
13.8546805203176));
#446298=CARTESIAN_POINT('Ctrl Pts',(2.65957223692824,-0.1524178775067,13.8559412814273));
#446299=CARTESIAN_POINT('Ctrl Pts',(2.65944802725433,-0.152720240070046,
13.8561100121513));
#446300=CARTESIAN_POINT('Ctrl Pts',(2.6593270939146,-0.153027236813295,
13.8562727473908));
#446301=CARTESIAN_POINT('Ctrl Pts',(2.65920983451485,-0.153338686653399,
13.8564289040185));
#446302=CARTESIAN_POINT('Ctrl Pts',(2.65867806447477,-0.154751108125077,
13.8571370725437));
#446303=CARTESIAN_POINT('Ctrl Pts',(2.65821463653706,-0.156280741050408,
13.8577210840554));
#446304=CARTESIAN_POINT('Ctrl Pts',(2.65786565151628,-0.157876637840136,
13.8581177131616));
#446305=CARTESIAN_POINT('Ctrl Pts',(2.65776736532273,-0.15832609730522,
13.8582294175695));
#446306=CARTESIAN_POINT('Ctrl Pts',(2.65767799379106,-0.158780741481692,
13.8583265086086));
#446307=CARTESIAN_POINT('Ctrl Pts',(2.65759815423685,-0.159239280394839,
13.8584082369006));
#446308=CARTESIAN_POINT('Ctrl Pts',(2.65748344620727,-0.159898077850963,
13.8585256585398));
#446309=CARTESIAN_POINT('Ctrl Pts',(2.65738730653124,-0.160573160685501,
13.8586122832068));
#446310=CARTESIAN_POINT('Ctrl Pts',(2.65731301443783,-0.161247103540259,
13.8586682984299));
#446311=CARTESIAN_POINT('Ctrl Pts',(2.65725358812744,-0.16178619101826,
13.8587131050557));
#446312=CARTESIAN_POINT('Ctrl Pts',(2.65720725137057,-0.162330477622658,
13.8587357943552));
#446313=CARTESIAN_POINT('Ctrl Pts',(2.65717450328177,-0.162880070989482,
13.8587355499465));
#446314=CARTESIAN_POINT('Ctrl Pts',(2.65715333741124,-0.163235286285242,
13.8587353919793));
#446315=CARTESIAN_POINT('Ctrl Pts',(2.65713803827726,-0.163588874847986,
13.8587257282814));
#446316=CARTESIAN_POINT('Ctrl Pts',(2.657128461537,-0.163940853655835,13.8587068136939));
#446317=CARTESIAN_POINT('Ctrl Pts',(2.657128461537,-0.163940853655835,13.8587068136939));
#446318=CARTESIAN_POINT('Ctrl Pts',(2.65709696416037,-0.165098492767069,
13.8586446046466));
#446319=CARTESIAN_POINT('Ctrl Pts',(2.65712729051015,-0.166238741134392,
13.858482427929));
#446320=CARTESIAN_POINT('Ctrl Pts',(2.65721499023803,-0.167362023442386,
13.8582284286032));
#446321=CARTESIAN_POINT('Ctrl Pts',(2.65730495995717,-0.168514380424691,
13.8579678548414));
#446322=CARTESIAN_POINT('Ctrl Pts',(2.65745705833494,-0.169651577367859,
13.857615680862));
#446323=CARTESIAN_POINT('Ctrl Pts',(2.65765568485813,-0.170730065667193,
13.8571944833187));
#446324=CARTESIAN_POINT('Ctrl Pts',(2.6581513776606,-0.173421543516925,
13.8561433417727));
#446325=CARTESIAN_POINT('Ctrl Pts',(2.65895532004245,-0.175874149611331,
13.8546163505474));
#446326=CARTESIAN_POINT('Ctrl Pts',(2.65987707537418,-0.178007312511304,
13.8528973491086));
#446327=CARTESIAN_POINT('Ctrl Pts',(2.66004546647405,-0.178397009901237,
13.8525833129072));
#446328=CARTESIAN_POINT('Ctrl Pts',(2.66021770028529,-0.178776155873566,
13.8522628768812));
#446329=CARTESIAN_POINT('Ctrl Pts',(2.66039252597185,-0.179144413843575,
13.851937733538));
#446330=CARTESIAN_POINT('Ctrl Pts',(2.66146016218374,-0.181393314172981,
13.8499521282529));
#446331=CARTESIAN_POINT('Ctrl Pts',(2.66273424628176,-0.183457909392397,
13.847639871647));
#446332=CARTESIAN_POINT('Ctrl Pts',(2.66407944702675,-0.1852718839326,13.8452109780794));
#446333=CARTESIAN_POINT('Ctrl Pts',(2.66468468068619,-0.186088028625637,
13.8441181685877));
#446334=CARTESIAN_POINT('Ctrl Pts',(2.66530391729198,-0.186854041072759,
13.8430021611332));
#446335=CARTESIAN_POINT('Ctrl Pts',(2.66592396494383,-0.187567074770224,
13.8418824960098));
#446336=CARTESIAN_POINT('Ctrl Pts',(2.66738512306889,-0.189247356886282,
13.8392439765549));
#446337=CARTESIAN_POINT('Ctrl Pts',(2.66891778056966,-0.190716243249255,
13.8364981347963));
#446338=CARTESIAN_POINT('Ctrl Pts',(2.67050231261561,-0.192002324595168,
13.8336931113419));
#446339=CARTESIAN_POINT('Ctrl Pts',(2.67204554620127,-0.193254886152371,
13.8309611966327));
#446340=CARTESIAN_POINT('Ctrl Pts',(2.67363988765096,-0.194334864522001,
13.8281701127185));
#446341=CARTESIAN_POINT('Ctrl Pts',(2.67527917510622,-0.195231239342457,
13.825358068512));
#446342=CARTESIAN_POINT('Ctrl Pts',(2.67563457439567,-0.195425574370919,
13.8247484142932));
#446343=CARTESIAN_POINT('Ctrl Pts',(2.67599207053514,-0.195611107071313,
13.8241378483365));
#446344=CARTESIAN_POINT('Ctrl Pts',(2.67635153714374,-0.195787413049918,
13.8235269408515));
#446345=CARTESIAN_POINT('',(2.65718639411042,-0.162700119730359,12.5969504640361));
#446346=CARTESIAN_POINT('Origin',(2.69152165735451,-0.164926894568226,12.584524458991));
#446347=CARTESIAN_POINT('Origin',(2.69152165735451,-0.164926894568226,12.584524458991));
#446348=CARTESIAN_POINT('Ctrl Pts',(2.68023295023436,-0.132444682635723,
12.5893111709658));
#446349=CARTESIAN_POINT('Ctrl Pts',(2.66952380348168,-0.136155856356976,
12.5770542771492));
#446350=CARTESIAN_POINT('Ctrl Pts',(2.67190547188397,-0.152346326716927,
12.5737548217797));
#446351=CARTESIAN_POINT('Ctrl Pts',(2.703650260086,-0.124329591214261,12.5663937883685));
#446352=CARTESIAN_POINT('Ctrl Pts',(2.69292745232941,-0.128045499053006,
12.5540940315304));
#446353=CARTESIAN_POINT('Ctrl Pts',(2.6953196780358,-0.144285673050915,
12.5508374392248));
#446354=CARTESIAN_POINT('Ctrl Pts',(2.72704394215907,-0.116222687820561,
12.5434499600945));
#446355=CARTESIAN_POINT('Ctrl Pts',(2.7162862707359,-0.119950677398965,
12.5311293540533));
#446356=CARTESIAN_POINT('Ctrl Pts',(2.71871062394669,-0.136231779206612,
12.5278936106989));
#446357=CARTESIAN_POINT('Ctrl Pts',(2.75041584724981,-0.108123331075201,
12.5204817579905));
#446358=CARTESIAN_POINT('Ctrl Pts',(2.73960493270498,-0.111869771654276,
12.5081597038247));
#446359=CARTESIAN_POINT('Ctrl Pts',(2.74208011298381,-0.128184106684609,
12.5049254088044));
#446360=CARTESIAN_POINT('Ctrl Pts',(2.73361252196705,-0.11394639622308,
12.5369868989719));
#446361=CARTESIAN_POINT('Ctrl Pts',(2.73449267529843,-0.113641385921656,
12.5342545179733));
#446362=CARTESIAN_POINT('Ctrl Pts',(2.73537350012164,-0.113468167146179,
12.5314872231885));
#446363=CARTESIAN_POINT('Ctrl Pts',(2.73621616480082,-0.113491347926608,
12.5287124745063));
#446364=CARTESIAN_POINT('Ctrl Pts',(2.73697612163466,-0.11351225350499,
12.5262100684185));
#446365=CARTESIAN_POINT('Ctrl Pts',(2.73770424773633,-0.113693859445946,
12.5237004536639));
#446366=CARTESIAN_POINT('Ctrl Pts',(2.73839700297034,-0.114103604192337,
12.5212220730815));
#446367=CARTESIAN_POINT('Ctrl Pts',(2.73892736703007,-0.114417299241446,
12.5193246583486));
#446368=CARTESIAN_POINT('Ctrl Pts',(2.73944301496718,-0.11486900692132,
12.517417831369));
#446369=CARTESIAN_POINT('Ctrl Pts',(2.7398955685426,-0.115543069206918,
12.5155812248347));
#446370=CARTESIAN_POINT('Ctrl Pts',(2.74008835879822,-0.115830223363684,
12.5147988205793));
#446371=CARTESIAN_POINT('Ctrl Pts',(2.74027012435751,-0.116157867649738,
12.5140295443047));
#446372=CARTESIAN_POINT('Ctrl Pts',(2.7404392522251,-0.11653253886192,12.5132817086137));
#446373=CARTESIAN_POINT('Ctrl Pts',(2.74069520437361,-0.117099553057184,
12.5121499604604));
#446374=CARTESIAN_POINT('Ctrl Pts',(2.7409212215005,-0.117789458395046,
12.5110494206568));
#446375=CARTESIAN_POINT('Ctrl Pts',(2.74108752609361,-0.118624619993785,
12.5100666561695));
#446376=CARTESIAN_POINT('Ctrl Pts',(2.74118301780802,-0.119104167860575,
12.5095023550641));
#446377=CARTESIAN_POINT('Ctrl Pts',(2.74125928526331,-0.119637275364437,
12.5089719619137));
#446378=CARTESIAN_POINT('Ctrl Pts',(2.74130857630567,-0.120214854519267,
12.5085043804652));
#446379=CARTESIAN_POINT('Ctrl Pts',(2.74138070732556,-0.121060066377384,
12.5078201359221));
#446380=CARTESIAN_POINT('Ctrl Pts',(2.74139595829608,-0.122025128769444,
12.5072563000949));
#446381=CARTESIAN_POINT('Ctrl Pts',(2.74134483048392,-0.123044758473408,
12.5068768744332));
#446382=CARTESIAN_POINT('Ctrl Pts',(2.7413079638117,-0.123779981681515,
12.5066032824114));
#446383=CARTESIAN_POINT('Ctrl Pts',(2.74123599642688,-0.124556496405264,
12.5064197834844));
#446384=CARTESIAN_POINT('Ctrl Pts',(2.74113552100225,-0.125331178589341,
12.5063282718343));
#446385=CARTESIAN_POINT('Ctrl Pts',(2.7409888579887,-0.126461974742552,
12.5061946931565));
#446386=CARTESIAN_POINT('Ctrl Pts',(2.74077937162784,-0.127613172355728,
12.5062515701262));
#446387=CARTESIAN_POINT('Ctrl Pts',(2.740535277685,-0.128716094730959,12.5064436508398));
#446388=CARTESIAN_POINT('',(2.67190547188397,-0.152346326716927,12.5737548217797));
#446389=CARTESIAN_POINT('Origin',(2.68743659543392,-0.153231878113681,12.5893111709658));
#446390=CARTESIAN_POINT('Ctrl Pts',(2.740535277685,-0.128716094730959,12.5064436508398));
#446391=CARTESIAN_POINT('Ctrl Pts',(2.73037643979395,-0.132214437260586,
12.5164271754438));
#446392=CARTESIAN_POINT('Ctrl Pts',(2.72021350691258,-0.135713968982086,
12.5264061185523));
#446393=CARTESIAN_POINT('Ctrl Pts',(2.71004633512696,-0.139214732672717,
12.536380305637));
#446394=CARTESIAN_POINT('Ctrl Pts',(2.69733943251955,-0.143589977254623,
12.5488460165097));
#446395=CARTESIAN_POINT('Ctrl Pts',(2.6846259050118,-0.147967147433176,
12.5613043021964));
#446396=CARTESIAN_POINT('Ctrl Pts',(2.67190547188397,-0.152346326716927,
12.5737548217797));
#446397=CARTESIAN_POINT('Ctrl Pts',(2.67635153714374,-0.195787413049918,
12.5893111709658));
#446398=CARTESIAN_POINT('Ctrl Pts',(2.66617562406611,-0.190796478508543,
12.5770542771492));
#446399=CARTESIAN_POINT('Ctrl Pts',(2.67051623844066,-0.175017925288858,
12.5737548217797));
#446400=CARTESIAN_POINT('Ctrl Pts',(2.66685749874773,-0.191130914531672,
12.5928319619712));
#446401=CARTESIAN_POINT('Ctrl Pts',(2.66145321087793,-0.184851815154235,
12.5821634970842));
#446402=CARTESIAN_POINT('Ctrl Pts',(2.66705363363455,-0.173330150029483,
12.5773203894503));
#446403=CARTESIAN_POINT('Ctrl Pts',(2.65626558008246,-0.178154190818509,
12.5969440695591));
#446404=CARTESIAN_POINT('Ctrl Pts',(2.65649319333027,-0.174140871150037,
12.5878292599214));
#446405=CARTESIAN_POINT('Ctrl Pts',(2.66328004270661,-0.16870368716828,
12.5813877129824));
#446406=CARTESIAN_POINT('Ctrl Pts',(2.65808311628459,-0.147611240605811,
12.596957478804));
#446407=CARTESIAN_POINT('Ctrl Pts',(2.65785726518957,-0.151594905304524,
12.5878468778671));
#446408=CARTESIAN_POINT('Ctrl Pts',(2.66393651869179,-0.157772296241913,
12.5814011370086));
#446409=CARTESIAN_POINT('Ctrl Pts',(2.67022690175735,-0.135912202973097,
12.5928371701607));
#446410=CARTESIAN_POINT('Ctrl Pts',(2.66410487443975,-0.141484980308176,
12.5821692192952));
#446411=CARTESIAN_POINT('Ctrl Pts',(2.66825097229948,-0.153602475697303,
12.5773318885715));
#446412=CARTESIAN_POINT('Ctrl Pts',(2.68023295023433,-0.132444682635672,
12.5893111709658));
#446413=CARTESIAN_POINT('Ctrl Pts',(2.66952380348166,-0.136155856356925,
12.5770542771492));
#446414=CARTESIAN_POINT('Ctrl Pts',(2.67190547188395,-0.152346326716875,
12.5737548217797));
#446415=CARTESIAN_POINT('',(2.67051623844066,-0.175017925288858,12.5737548217797));
#446416=CARTESIAN_POINT('Origin',(2.6860392867213,-0.176035261062791,12.5893111709658));
#446417=CARTESIAN_POINT('Ctrl Pts',(2.67190547188395,-0.152346326716875,
12.5737548217797));
#446418=CARTESIAN_POINT('Ctrl Pts',(2.67094836195251,-0.152643412916743,
12.5746934679442));
#446419=CARTESIAN_POINT('Ctrl Pts',(2.66994356044573,-0.153147108628655,
12.5756680099006));
#446420=CARTESIAN_POINT('Ctrl Pts',(2.66900389294695,-0.153797130674218,
12.5765688348656));
#446421=CARTESIAN_POINT('Ctrl Pts',(2.66875512637911,-0.153969216814801,
12.5768073183026));
#446422=CARTESIAN_POINT('Ctrl Pts',(2.66851083443986,-0.154151317826923,
12.5770407398754));
#446423=CARTESIAN_POINT('Ctrl Pts',(2.66827278642337,-0.154341854659967,
12.5772674179684));
#446424=CARTESIAN_POINT('Ctrl Pts',(2.66729590173457,-0.155123766299436,
12.5781976435658));
#446425=CARTESIAN_POINT('Ctrl Pts',(2.66637573250234,-0.156100959252145,
12.5790594849312));
#446426=CARTESIAN_POINT('Ctrl Pts',(2.66560956596033,-0.157240556353572,
12.5797571720116));
#446427=CARTESIAN_POINT('Ctrl Pts',(2.66511038090932,-0.157983044841412,
12.580211740231));
#446428=CARTESIAN_POINT('Ctrl Pts',(2.66466946369949,-0.158838690208611,
12.5806009430798));
#446429=CARTESIAN_POINT('Ctrl Pts',(2.6643336017011,-0.159755374113976,
12.5808812374708));
#446430=CARTESIAN_POINT('Ctrl Pts',(2.66404498482342,-0.160543109695404,
12.5811221033394));
#446431=CARTESIAN_POINT('Ctrl Pts',(2.66382814448513,-0.161392085561016,
12.581287365893));
#446432=CARTESIAN_POINT('Ctrl Pts',(2.6637033981384,-0.162256447540992,
12.581359338449));
#446433=CARTESIAN_POINT('Ctrl Pts',(2.66368606097211,-0.162376576007816,
12.5813693411482));
#446434=CARTESIAN_POINT('Ctrl Pts',(2.66367044389937,-0.162497013349188,
12.5813775999465));
#446435=CARTESIAN_POINT('Ctrl Pts',(2.66365654152002,-0.162617649510988,
12.5813841266931));
#446436=CARTESIAN_POINT('Ctrl Pts',(2.663632954452,-0.162822323350123,12.5813952001081));
#446437=CARTESIAN_POINT('Ctrl Pts',(2.66361475006095,-0.163029010012145,
12.5814007534795));
#446438=CARTESIAN_POINT('Ctrl Pts',(2.66360213272474,-0.163237636780978,
12.5814005856065));
#446439=CARTESIAN_POINT('Ctrl Pts',(2.66354437549263,-0.164192648560916,
12.5813998171494));
#446440=CARTESIAN_POINT('Ctrl Pts',(2.66360734592339,-0.165122309964617,
12.58127954464));
#446441=CARTESIAN_POINT('Ctrl Pts',(2.66376116479879,-0.16602334262812,
12.5810700125799));
#446442=CARTESIAN_POINT('Ctrl Pts',(2.66394696048659,-0.167111687494848,
12.5808169217085));
#446443=CARTESIAN_POINT('Ctrl Pts',(2.66428181718866,-0.168155545410726,
12.5804173076348));
#446444=CARTESIAN_POINT('Ctrl Pts',(2.6647115909308,-0.169071389228317,
12.5799304713245));
#446445=CARTESIAN_POINT('Ctrl Pts',(2.66524421599,-0.170206408238868,12.5793271277669));
#446446=CARTESIAN_POINT('Ctrl Pts',(2.66592651370094,-0.171228896694569,
12.5785808224116));
#446447=CARTESIAN_POINT('Ctrl Pts',(2.6667033414904,-0.172113359496798,
12.5777485681082));
#446448=CARTESIAN_POINT('Ctrl Pts',(2.66786090000453,-0.173431305972252,
12.576508418016));
#446449=CARTESIAN_POINT('Ctrl Pts',(2.669213445279,-0.174436214321939,12.5750928681475));
#446450=CARTESIAN_POINT('Ctrl Pts',(2.67051623844066,-0.175017925288858,
12.5737548217797));
#446451=CARTESIAN_POINT('Ctrl Pts',(2.67051623844066,-0.175017925288858,
12.5737548217797));
#446452=CARTESIAN_POINT('Ctrl Pts',(2.66617562406611,-0.190796478508544,
12.5770542771492));
#446453=CARTESIAN_POINT('Ctrl Pts',(2.67635153714374,-0.195787413049918,
12.5893111709658));
#446454=CARTESIAN_POINT('Ctrl Pts',(2.69276776782275,-0.185875383293774,
12.5508408821982));
#446455=CARTESIAN_POINT('Ctrl Pts',(2.68841060606402,-0.201701970608707,
12.55409748406));
#446456=CARTESIAN_POINT('Ctrl Pts',(2.69859950100054,-0.206699272304328,
12.5663972313419));
#446457=CARTESIAN_POINT('Ctrl Pts',(2.71499704302009,-0.196723294981798,
12.52790050457));
#446458=CARTESIAN_POINT('Ctrl Pts',(2.71060300277904,-0.212586576095784,
12.5311362602938));
#446459=CARTESIAN_POINT('Ctrl Pts',(2.72082502031763,-0.217600123285803,
12.5434568539655));
#446460=CARTESIAN_POINT('Ctrl Pts',(2.73720578739579,-0.207562414669864,
12.5049357605811));
#446461=CARTESIAN_POINT('Ctrl Pts',(2.73275725350924,-0.223452472292466,
12.5081700652078));
#446462=CARTESIAN_POINT('Ctrl Pts',(2.74302985295592,-0.228490828164516,
12.5204921097672));
#446463=CARTESIAN_POINT('Ctrl Pts',(2.73574747348835,-0.206850677009421,
12.5064436508395));
#446464=CARTESIAN_POINT('Ctrl Pts',(2.73586370872577,-0.208065311588282,
12.5062361689309));
#446465=CARTESIAN_POINT('Ctrl Pts',(2.73593278914447,-0.209333388682228,
12.5061871075061));
#446466=CARTESIAN_POINT('Ctrl Pts',(2.73593056365757,-0.210562620836186,
12.5063648335164));
#446467=CARTESIAN_POINT('Ctrl Pts',(2.73592955270414,-0.211121013902697,
12.5064455676329));
#446468=CARTESIAN_POINT('Ctrl Pts',(2.73591359310022,-0.211679179196062,
12.506574497099));
#446469=CARTESIAN_POINT('Ctrl Pts',(2.73588231862587,-0.21221315422517,
12.5067492519495));
#446470=CARTESIAN_POINT('Ctrl Pts',(2.73581947135566,-0.213286197773626,
12.5071004286051));
#446471=CARTESIAN_POINT('Ctrl Pts',(2.73569166139577,-0.214300959807943,
12.5076537929613));
#446472=CARTESIAN_POINT('Ctrl Pts',(2.73551786586002,-0.21518245907517,
12.5083435010505));
#446473=CARTESIAN_POINT('Ctrl Pts',(2.73550692439244,-0.215237954721908,
12.5083869222964));
#446474=CARTESIAN_POINT('Ctrl Pts',(2.73549578776044,-0.215292925930993,
12.5084308732337));
#446475=CARTESIAN_POINT('Ctrl Pts',(2.73548445555553,-0.215347355896893,
12.5084753333615));
#446476=CARTESIAN_POINT('Ctrl Pts',(2.73539355631497,-0.215783956064467,
12.5088319622689));
#446477=CARTESIAN_POINT('Ctrl Pts',(2.73528949120141,-0.216194858450765,
12.509227847131));
#446478=CARTESIAN_POINT('Ctrl Pts',(2.7351780689688,-0.216568532223665,
12.5096423454524));
#446479=CARTESIAN_POINT('Ctrl Pts',(2.73482892100524,-0.217739460446853,
12.5109411997424));
#446480=CARTESIAN_POINT('Ctrl Pts',(2.73439532279908,-0.218619616504199,
12.5124831113042));
#446481=CARTESIAN_POINT('Ctrl Pts',(2.73393821009027,-0.219281406838765,
12.5140723025008));
#446482=CARTESIAN_POINT('Ctrl Pts',(2.7338953781288,-0.219343417317953,
12.5142212114565));
#446483=CARTESIAN_POINT('Ctrl Pts',(2.73385234959602,-0.219403538478404,
12.5143705582413));
#446484=CARTESIAN_POINT('Ctrl Pts',(2.73380918172599,-0.219461845313496,
12.5145201959299));
#446485=CARTESIAN_POINT('Ctrl Pts',(2.73325462616521,-0.220210883420053,
12.5164425148273));
#446486=CARTESIAN_POINT('Ctrl Pts',(2.73266670474085,-0.220692553616486,
12.5184635205941));
#446487=CARTESIAN_POINT('Ctrl Pts',(2.73205913545531,-0.220996017525484,
12.5205025929158));
#446488=CARTESIAN_POINT('Ctrl Pts',(2.73170672118791,-0.221172038620888,
12.5216853356836));
#446489=CARTESIAN_POINT('Ctrl Pts',(2.73134854914952,-0.221288217558141,
12.5228750347131));
#446490=CARTESIAN_POINT('Ctrl Pts',(2.73099308911396,-0.221360715914502,
12.5240609649613));
#446491=CARTESIAN_POINT('Ctrl Pts',(2.73012063152647,-0.221538659240786,
12.5269717671327));
#446492=CARTESIAN_POINT('Ctrl Pts',(2.72923787988305,-0.221448279352425,
12.5299036066169));
#446493=CARTESIAN_POINT('Ctrl Pts',(2.72834998350432,-0.221176080625759,
12.5328133004019));
#446494=CARTESIAN_POINT('Ctrl Pts',(2.72792374154188,-0.221045409387302,
12.5342101228451));
#446495=CARTESIAN_POINT('Ctrl Pts',(2.72749699938177,-0.220872498903379,
12.5356023438238));
#446496=CARTESIAN_POINT('Ctrl Pts',(2.72707321410059,-0.220664646924583,
12.5369868989719));
#446497=CARTESIAN_POINT('Origin',(14.1679839010907,-5.83793691405242,-1.24024679429017));
#446498=CARTESIAN_POINT('Ctrl Pts',(2.73357301872941,-0.113960043755668,
12.5369868989719));
#446499=CARTESIAN_POINT('Ctrl Pts',(2.74807588392649,-0.108965025761739,
12.5369868989719));
#446500=CARTESIAN_POINT('Ctrl Pts',(2.7484038475258,-0.0936295849933097,
12.5369868989719));
#446501=CARTESIAN_POINT('Ctrl Pts',(2.7384755328083,-0.112271469716813,
12.5218025310015));
#446502=CARTESIAN_POINT('Ctrl Pts',(2.74811993318496,-0.105442018415441,
12.5216901060417));
#446503=CARTESIAN_POINT('Ctrl Pts',(2.74840286427204,-0.0936763328516556,
12.5161920673677));
#446504=CARTESIAN_POINT('Ctrl Pts',(2.74339453687234,-0.115755643967929,
12.5042015548895));
#446505=CARTESIAN_POINT('Ctrl Pts',(2.74786201040398,-0.111127574687816,
12.4980677368515));
#446506=CARTESIAN_POINT('Ctrl Pts',(2.74813054572147,-0.104336501981173,
12.4907278922778));
#446507=CARTESIAN_POINT('Ctrl Pts',(2.74051529862617,-0.128715156374926,
12.506463626192));
#446508=CARTESIAN_POINT('Ctrl Pts',(2.74705083343836,-0.129022114115963,
12.4999376786891));
#446509=CARTESIAN_POINT('Ctrl Pts',(2.74697101138329,-0.129018365073473,
12.4906970594712));
#446510=CARTESIAN_POINT('Origin',(2.72640887676749,-0.0931592007451217,
12.5369868989719));
#446511=CARTESIAN_POINT('Origin',(2.72640887676749,-0.0931592007451217,
14.));
#446512=CARTESIAN_POINT('Origin',(2.72640887676749,-0.0931592007451218,
13.7435492065112));
#446513=CARTESIAN_POINT('Ctrl Pts',(2.71021737119475,-0.122053779847747,
13.793642941384));
#446514=CARTESIAN_POINT('Ctrl Pts',(2.72044251441526,-0.118539144002311,
13.8071662555867));
#446515=CARTESIAN_POINT('Ctrl Pts',(2.7173348007707,-0.101795145091112,
13.8103758687955));
#446516=CARTESIAN_POINT('Ctrl Pts',(2.72592221387328,-0.11661138867609,
13.7804579775006));
#446517=CARTESIAN_POINT('Ctrl Pts',(2.73853582004678,-0.112265055620661,
13.7901904343351));
#446518=CARTESIAN_POINT('Ctrl Pts',(2.73820488853917,-0.0965123920839132,
13.7927914348262));
#446519=CARTESIAN_POINT('Ctrl Pts',(2.73516824578542,-0.113407248137176,
13.7597120340895));
#446520=CARTESIAN_POINT('Ctrl Pts',(2.74976387352248,-0.108371898999924,
13.7635825532445));
#446521=CARTESIAN_POINT('Ctrl Pts',(2.75050568275459,-0.0933723778340084,
13.7651073818884));
#446522=CARTESIAN_POINT('Ctrl Pts',(2.7333576610267,-0.114034692220408,
13.7381884353898));
#446523=CARTESIAN_POINT('Ctrl Pts',(2.74761194403764,-0.109118054500371,
13.7368803041982));
#446524=CARTESIAN_POINT('Ctrl Pts',(2.7480966994888,-0.0939868070543812,
13.7363986145813));
#446525=CARTESIAN_POINT('Origin',(2.70682448668519,-0.0999460228420377,
13.7902182540695));
#446526=CARTESIAN_POINT('Ctrl Pts',(2.68022923078013,-0.13244597078122,
13.8235227101244));
#446527=CARTESIAN_POINT('Ctrl Pts',(2.69109395003468,-0.128685576674305,
13.8358800583119));
#446528=CARTESIAN_POINT('Ctrl Pts',(2.68857209989094,-0.112306739080959,
13.8390832900376));
#446529=CARTESIAN_POINT('Ctrl Pts',(2.69149927276398,-0.128540423063339,
13.8124254819052));
#446530=CARTESIAN_POINT('Ctrl Pts',(2.70238509105835,-0.124772726061514,
13.8247886449158));
#446531=CARTESIAN_POINT('Ctrl Pts',(2.69984320867394,-0.108375786864014,
13.8279860620657));
#446532=CARTESIAN_POINT('Ctrl Pts',(2.70276426388169,-0.124636625684892,
13.8013225099955));
#446533=CARTESIAN_POINT('Ctrl Pts',(2.71366604551334,-0.12086340543045,
13.8136962257787));
#446534=CARTESIAN_POINT('Ctrl Pts',(2.71110918874942,-0.104446910421774,
13.8168830918626));
#446535=CARTESIAN_POINT('Ctrl Pts',(2.71402440065465,-0.120734510542875,
13.7902140179785));
#446536=CARTESIAN_POINT('Ctrl Pts',(2.72493734557605,-0.11695743036274,
13.802602731458));
#446537=CARTESIAN_POINT('Ctrl Pts',(2.7223702422428,-0.100520029929646,
13.8057746032558));
#446538=CARTESIAN_POINT('Origin',(2.67302930503479,-0.111657487157766,13.8235269408515));
#446539=CARTESIAN_POINT('Ctrl Pts',(2.67635153714374,-0.195787413049918,
13.8235269408515));
#446540=CARTESIAN_POINT('Ctrl Pts',(2.68695259026586,-0.200986864126054,
13.8362179249168));
#446541=CARTESIAN_POINT('Ctrl Pts',(2.68201124438138,-0.217334527717751,
13.8391868794938));
#446542=CARTESIAN_POINT('Ctrl Pts',(2.66665203497342,-0.191030141633907,
13.8400110824519));
#446543=CARTESIAN_POINT('Ctrl Pts',(2.67364504172606,-0.198270288001189,
13.8494522556837));
#446544=CARTESIAN_POINT('Ctrl Pts',(2.66609807868506,-0.209404525123416,
13.85569149686));
#446545=CARTESIAN_POINT('Ctrl Pts',(2.65624393994649,-0.178497413121852,
13.8586819406588));
#446546=CARTESIAN_POINT('Ctrl Pts',(2.65599153449409,-0.182843944511659,
13.868010383617));
#446547=CARTESIAN_POINT('Ctrl Pts',(2.64893275204602,-0.188506669751641,
13.8744918421245));
#446548=CARTESIAN_POINT('Ctrl Pts',(2.65810507346531,-0.147262693978375,
13.8587686893867));
#446549=CARTESIAN_POINT('Ctrl Pts',(2.65835517629788,-0.142954843413072,
13.8680909899357));
#446550=CARTESIAN_POINT('Ctrl Pts',(2.65203356118348,-0.136510187964475,
13.8745789365163));
#446551=CARTESIAN_POINT('Ctrl Pts',(2.67000856858662,-0.135987864673384,
13.8400379222776));
#446552=CARTESIAN_POINT('Ctrl Pts',(2.67782673909229,-0.129651742527106,
13.8494748685453));
#446553=CARTESIAN_POINT('Ctrl Pts',(2.67169949435394,-0.117684371170747,
13.8557104837033));
#446554=CARTESIAN_POINT('Ctrl Pts',(2.68023295023206,-0.132444682629526,
13.8235269408542));
#446555=CARTESIAN_POINT('Ctrl Pts',(2.69138951502887,-0.128578459572717,
13.8362179249195));
#446556=CARTESIAN_POINT('Ctrl Pts',(2.68848109462999,-0.11174979073529,
13.8391868794965));
#446557=CARTESIAN_POINT('Origin',(2.66666378756618,-0.215539565037045,13.8235269408515));
#446558=CARTESIAN_POINT('Ctrl Pts',(2.70846043663131,-0.211535722113581,
13.7902140241682));
#446559=CARTESIAN_POINT('Ctrl Pts',(2.71883056936445,-0.216616956460646,
13.8026027327198));
#446560=CARTESIAN_POINT('Ctrl Pts',(2.71427576044359,-0.232617945429092,
13.8057746032556));
#446561=CARTESIAN_POINT('Ctrl Pts',(2.69776096862262,-0.206288001927323,
13.8013225161807));
#446562=CARTESIAN_POINT('Ctrl Pts',(2.7081204928681,-0.21136404224361,13.8136962270464));
#446563=CARTESIAN_POINT('Ctrl Pts',(2.70357840628457,-0.227345533249815,
13.8168830918628));
#446564=CARTESIAN_POINT('Ctrl Pts',(2.68705688797703,-0.201038019401679,
13.8124254880876));
#446565=CARTESIAN_POINT('Ctrl Pts',(2.69740124268566,-0.206106628747746,
13.8247886461868));
#446566=CARTESIAN_POINT('Ctrl Pts',(2.69287640609661,-0.222070538545837,
13.8279860620656));
#446567=CARTESIAN_POINT('Ctrl Pts',(2.67634800795688,-0.195785682948258,
13.8235227163065));
#446568=CARTESIAN_POINT('Ctrl Pts',(2.68667231313743,-0.200844467958111,
13.8358800595847));
#446569=CARTESIAN_POINT('Ctrl Pts',(2.68216956901137,-0.216792857410774,
13.8390832900376));
#446570=CARTESIAN_POINT('Origin',(2.69877622741402,-0.23128960967891,13.7902182540695));
#446571=CARTESIAN_POINT('Ctrl Pts',(2.72683091496282,-0.22054583827463,
13.7382347919292));
#446572=CARTESIAN_POINT('Ctrl Pts',(2.74038993764399,-0.227169339815741,
13.7369371795942));
#446573=CARTESIAN_POINT('Ctrl Pts',(2.73901431903953,-0.24225746264383,
13.7364597369711));
#446574=CARTESIAN_POINT('Ctrl Pts',(2.728529203922,-0.221378790011213,13.7595490285574));
#446575=CARTESIAN_POINT('Ctrl Pts',(2.74241129195678,-0.228161226020016,
13.7633824266926));
#446576=CARTESIAN_POINT('Ctrl Pts',(2.74130202557949,-0.243149994762358,
13.7648920890506));
#446577=CARTESIAN_POINT('Ctrl Pts',(2.71986802327364,-0.217130781780323,
13.7803806590111));
#446578=CARTESIAN_POINT('Ctrl Pts',(2.73187790238087,-0.222992495679346,
13.7901039518744));
#446579=CARTESIAN_POINT('Ctrl Pts',(2.72964039726187,-0.238596309708886,
13.7926933640892));
#446580=CARTESIAN_POINT('Ctrl Pts',(2.70481295785426,-0.209746795269595,
13.7936647693663));
#446581=CARTESIAN_POINT('Ctrl Pts',(2.71453647590386,-0.214482460870521,
13.8072068914933));
#446582=CARTESIAN_POINT('Ctrl Pts',(2.70939207838032,-0.230736058748131,
13.8104111085397));
#446583=CARTESIAN_POINT('Origin',(2.71738546452303,-0.24041679891171,13.7435492065112));
#446584=CARTESIAN_POINT('Origin',(2.71738546452303,-0.24041679891171,14.));
#446585=CARTESIAN_POINT('Origin',(2.71738546452303,-0.240416798911709,12.5369868989719));
#446586=CARTESIAN_POINT('Ctrl Pts',(2.73572914257587,-0.206849290993361,
12.506462012331));
#446587=CARTESIAN_POINT('Ctrl Pts',(2.74224915474292,-0.207342271045017,
12.4999388158272));
#446588=CARTESIAN_POINT('Ctrl Pts',(2.74217201444852,-0.207336438444502,
12.4907030323752));
#446589=CARTESIAN_POINT('Ctrl Pts',(2.73700251896777,-0.220063188817957,
12.5042014951932));
#446590=CARTESIAN_POINT('Ctrl Pts',(2.74087057619595,-0.225199260312364,
12.4980716682127));
#446591=CARTESIAN_POINT('Ctrl Pts',(2.74030991222385,-0.231967659025219,
12.4907355092744));
#446592=CARTESIAN_POINT('Ctrl Pts',(2.73169678965818,-0.222922373621123,
12.5218047446509));
#446593=CARTESIAN_POINT('Ctrl Pts',(2.74043015424828,-0.230875185317147,
12.5216906929434));
#446594=CARTESIAN_POINT('Ctrl Pts',(2.73927874154297,-0.242581807507696,
12.5161988840775));
#446595=CARTESIAN_POINT('Ctrl Pts',(2.72703870838115,-0.22064776041674,
12.5369868989719));
#446596=CARTESIAN_POINT('Ctrl Pts',(2.74081403511674,-0.227374268043183,
12.5369868989719));
#446597=CARTESIAN_POINT('Ctrl Pts',(2.73927419821652,-0.242626626347441,
12.5369868989719));
#446598=CARTESIAN_POINT('Origin',(5.142217661156E-31,-5.46695907425333E-31,
12.5));
#446599=CARTESIAN_POINT('Origin',(2.68340468995259,0.0230115497283485,12.5));
#446600=CARTESIAN_POINT('',(2.68340468995259,0.0230115497283485,12.5893111709658));
#446601=CARTESIAN_POINT('',(2.68340468995259,0.0230115497283485,13.8235269408515));
#446602=CARTESIAN_POINT('',(2.68340468995259,0.0230115497283485,12.5));
#446603=CARTESIAN_POINT('',(2.71669405316051,0.00993137402568675,13.7902182540695));
#446604=CARTESIAN_POINT('',(2.68340468995259,0.0230115497283485,13.8235269408515));
#446605=CARTESIAN_POINT('',(2.73598532022336,0.00235138034623294,13.7435492065112));
#446606=CARTESIAN_POINT('Origin',(2.67251742570531,0.0272897625509187,13.7445212918684));
#446607=CARTESIAN_POINT('',(2.73598532022336,0.00235138034623295,12.5369868989719));
#446608=CARTESIAN_POINT('',(2.73598532022336,0.00235138034623294,12.5));
#446609=CARTESIAN_POINT('Ctrl Pts',(2.73598532022336,0.00235138034623295,
12.5369868989719));
#446610=CARTESIAN_POINT('Ctrl Pts',(2.71847122650434,0.00923308071661556,
12.5544431401645));
#446611=CARTESIAN_POINT('Ctrl Pts',(2.70094460623998,0.0161197030620077,
12.5718848856037));
#446612=CARTESIAN_POINT('Ctrl Pts',(2.68340468995259,0.0230115497283485,
12.5893111709658));
#446613=CARTESIAN_POINT('Origin',(2.93374596539591,0.19738519706742,12.5));
#446614=CARTESIAN_POINT('',(2.73380434092627,0.109247549171251,13.7435492065112));
#446615=CARTESIAN_POINT('',(2.71483830529306,0.100887000060675,13.7902182540695));
#446616=CARTESIAN_POINT('Origin',(2.66499884163794,0.0789169219910335,13.7418732680441));
#446617=CARTESIAN_POINT('',(2.68211016738736,0.0864598836326638,13.8235269408515));
#446618=CARTESIAN_POINT('',(2.71483830529306,0.100887000060675,13.7902182540695));
#446619=CARTESIAN_POINT('',(2.68211016738736,0.0864598836326638,12.5893111709658));
#446620=CARTESIAN_POINT('',(2.68211016738736,0.0864598836326638,12.5));
#446621=CARTESIAN_POINT('',(2.73380434092627,0.109247549171251,12.5369868989719));
#446622=CARTESIAN_POINT('Ctrl Pts',(2.68211016738736,0.0864598836326638,
12.5893111709658));
#446623=CARTESIAN_POINT('Ctrl Pts',(2.69935437826406,0.0940614232846936,
12.5718848856037));
#446624=CARTESIAN_POINT('Ctrl Pts',(2.71658551727533,0.101657200637478,
12.5544431401645));
#446625=CARTESIAN_POINT('Ctrl Pts',(2.73380434092627,0.109247549171251,
12.5369868989719));
#446626=CARTESIAN_POINT('',(2.73380434092627,0.109247549171251,12.5));
#446627=CARTESIAN_POINT('Origin',(2.69597583156671,0.0550054088815945,12.5));
#446628=CARTESIAN_POINT('',(2.6616497873045,0.0531852832027369,13.8587068136939));
#446629=CARTESIAN_POINT('Ctrl Pts',(2.68211016738456,0.0864598836386525,
13.8235269408542));
#446630=CARTESIAN_POINT('Ctrl Pts',(2.68050674561044,0.0857530682162323,
13.8262006681044));
#446631=CARTESIAN_POINT('Ctrl Pts',(2.67893595802417,0.084870767592378,
13.8288634856214));
#446632=CARTESIAN_POINT('Ctrl Pts',(2.67739681728247,0.0838262795564332,
13.8314912288862));
#446633=CARTESIAN_POINT('Ctrl Pts',(2.67581012193278,0.0827495201253175,
13.834200161153));
#446634=CARTESIAN_POINT('Ctrl Pts',(2.67425501777337,0.0814996114298888,
13.8368750301949));
#446635=CARTESIAN_POINT('Ctrl Pts',(2.67273699002846,0.080046400886488,
13.8394886372968));
#446636=CARTESIAN_POINT('Ctrl Pts',(2.6726197490635,0.0799341659112227,
13.8396904925131));
#446637=CARTESIAN_POINT('Ctrl Pts',(2.6725027415841,0.0798206998727481,
13.8398919674349));
#446638=CARTESIAN_POINT('Ctrl Pts',(2.67238597729853,0.0797059799700521,
13.8400930404591));
#446639=CARTESIAN_POINT('Ctrl Pts',(2.67056671117422,0.0779185667063149,
13.8432258934518));
#446640=CARTESIAN_POINT('Ctrl Pts',(2.66881497639772,0.0758366920328991,
13.8462331177034));
#446641=CARTESIAN_POINT('Ctrl Pts',(2.66726171813167,0.0734661476307544,
13.8489036603661));
#446642=CARTESIAN_POINT('Ctrl Pts',(2.66675347395084,0.0726904779149612,
13.8497774930041));
#446643=CARTESIAN_POINT('Ctrl Pts',(2.66626670926407,0.071884000936835,
13.85061494757));
#446644=CARTESIAN_POINT('Ctrl Pts',(2.66580666110405,0.0710472157696396,
13.8514076489583));
#446645=CARTESIAN_POINT('Ctrl Pts',(2.66483359289672,0.0692772944585522,
13.8530843267192));
#446646=CARTESIAN_POINT('Ctrl Pts',(2.66388706115073,0.0671965013980083,
13.8546805203176));
#446647=CARTESIAN_POINT('Ctrl Pts',(2.66314620170448,0.06486910798083,13.8559412814273));
#446648=CARTESIAN_POINT('Ctrl Pts',(2.66304705068392,0.0645576272624292,
13.8561100121513));
#446649=CARTESIAN_POINT('Ctrl Pts',(2.66295154282448,0.0642417948356269,
13.8562727473908));
#446650=CARTESIAN_POINT('Ctrl Pts',(2.66286005964904,0.0639218235894991,
13.8564289040185));
#446651=CARTESIAN_POINT('Ctrl Pts',(2.66244518449213,0.0624707576387723,
13.8571370725437));
#446652=CARTESIAN_POINT('Ctrl Pts',(2.66210797785648,0.0609084407616356,
13.8577210840554));
#446653=CARTESIAN_POINT('Ctrl Pts',(2.66189023445851,0.0592894086678096,
13.8581177131616));
#446654=CARTESIAN_POINT('Ctrl Pts',(2.66182891042314,0.0588334335047998,
13.8582294175695));
#446655=CARTESIAN_POINT('Ctrl Pts',(2.66177689398897,0.0583730175098042,
13.8583265086086));
#446656=CARTESIAN_POINT('Ctrl Pts',(2.66173469527258,0.0579094966822024,
13.8584082369006));
#446657=CARTESIAN_POINT('Ctrl Pts',(2.66167406703315,0.0572435415509584,
13.8585256585398));
#446658=CARTESIAN_POINT('Ctrl Pts',(2.66163327277214,0.0565628687227481,
13.8586122832068));
#446659=CARTESIAN_POINT('Ctrl Pts',(2.66161416047878,0.0558851128619351,
13.8586682984299));
#446660=CARTESIAN_POINT('Ctrl Pts',(2.66159887253864,0.0553429753570626,
13.8587131050557));
#446661=CARTESIAN_POINT('Ctrl Pts',(2.66159705437468,0.0547967229455865,
13.8587357943552));
#446662=CARTESIAN_POINT('Ctrl Pts',(2.66160921221402,0.0542462890320964,
13.8587355499465));
#446663=CARTESIAN_POINT('Ctrl Pts',(2.66161707011544,0.0538905304709234,
13.8587353919793));
#446664=CARTESIAN_POINT('Ctrl Pts',(2.66163064263848,0.0535368714234389,
13.8587257282814));
#446665=CARTESIAN_POINT('Ctrl Pts',(2.6616497873045,0.0531852832027369,
13.8587068136939));
#446666=CARTESIAN_POINT('Ctrl Pts',(2.6616497873045,0.0531852832027369,
13.8587068136939));
#446667=CARTESIAN_POINT('Ctrl Pts',(2.66171275306735,0.0520289287116105,
13.8586446046466));
#446668=CARTESIAN_POINT('Ctrl Pts',(2.66183591933619,0.050894946305773,
13.858482427929));
#446669=CARTESIAN_POINT('Ctrl Pts',(2.6620148851866,0.0497825499690413,
13.8582284286032));
#446670=CARTESIAN_POINT('Ctrl Pts',(2.66219848333093,0.0486413607268808,
13.8579678548414));
#446671=CARTESIAN_POINT('Ctrl Pts',(2.66244276772199,0.0475203451425292,
13.857615680862));
#446672=CARTESIAN_POINT('Ctrl Pts',(2.6627286401404,0.0464616353296411,
13.8571944833187));
#446673=CARTESIAN_POINT('Ctrl Pts',(2.66344206399718,0.0438195167156177,
13.8561433417727));
#446674=CARTESIAN_POINT('Ctrl Pts',(2.66444324149264,0.0414406002332273,
13.8546163505474));
#446675=CARTESIAN_POINT('Ctrl Pts',(2.66553580233921,0.0393896668735282,
13.8528973491086));
#446676=CARTESIAN_POINT('Ctrl Pts',(2.66573539708665,0.0390149916074136,
13.8525833129072));
#446677=CARTESIAN_POINT('Ctrl Pts',(2.66593796172065,0.0386511458665826,
13.8522628768812));
#446678=CARTESIAN_POINT('Ctrl Pts',(2.66614222213246,0.0382983631610421,
13.851937733538));
#446679=CARTESIAN_POINT('Ctrl Pts',(2.66738961212755,0.0361439681246803,
13.8499521282529));
#446680=CARTESIAN_POINT('Ctrl Pts',(2.66882774049298,0.0341900923575475,
13.847639871647));
#446681=CARTESIAN_POINT('Ctrl Pts',(2.67031632095861,0.0324918000169361,
13.8452109780794));
#446682=CARTESIAN_POINT('Ctrl Pts',(2.67098606412217,0.0317277031399972,
13.8441181685877));
#446683=CARTESIAN_POINT('Ctrl Pts',(2.671665677395,0.0310147130681858,13.8430021611332));
#446684=CARTESIAN_POINT('Ctrl Pts',(2.67234178075526,0.0303545915713946,
13.8418824960098));
#446685=CARTESIAN_POINT('Ctrl Pts',(2.67393503558863,0.0287989984073904,
13.8392439765549));
#446686=CARTESIAN_POINT('Ctrl Pts',(2.67558232117306,0.027459925457429,
13.8364981347964));
#446687=CARTESIAN_POINT('Ctrl Pts',(2.67726640838843,0.0263072775129246,
13.8336931113419));
#446688=CARTESIAN_POINT('Ctrl Pts',(2.67890660238676,0.0251846716148906,
13.8309611966327));
#446689=CARTESIAN_POINT('Ctrl Pts',(2.68058366705995,0.0242382404134886,
13.8281701127185));
#446690=CARTESIAN_POINT('Ctrl Pts',(2.68229056279083,0.0234784653523076,
13.825358068512));
#446691=CARTESIAN_POINT('Ctrl Pts',(2.68266061962742,0.0233137452990747,
13.8247484142932));
#446692=CARTESIAN_POINT('Ctrl Pts',(2.68303204886546,0.0231579691976311,
13.8241378483365));
#446693=CARTESIAN_POINT('Ctrl Pts',(2.68340468995259,0.0230115497283485,
13.8235269408515));
#446694=CARTESIAN_POINT('',(2.66160639577871,0.0544266107312119,12.5969504640361));
#446695=CARTESIAN_POINT('Origin',(2.69600891408846,0.0550058880103093,12.584524458991));
#446696=CARTESIAN_POINT('Origin',(2.69600891408846,0.0550058880103093,12.584524458991));
#446697=CARTESIAN_POINT('Ctrl Pts',(2.68211016738736,0.0864598836326638,
12.5893111709658));
#446698=CARTESIAN_POINT('Ctrl Pts',(2.6717391495482,0.0818881636566073,
12.5770542771492));
#446699=CARTESIAN_POINT('Ctrl Pts',(2.67543256678469,0.0659456938362765,
12.5737548217797));
#446700=CARTESIAN_POINT('Ctrl Pts',(2.70478810278459,0.0964567009054791,
12.5663937883685));
#446701=CARTESIAN_POINT('Ctrl Pts',(2.69440385527188,0.0918791490656717,
12.5540940315304));
#446702=CARTESIAN_POINT('Ctrl Pts',(2.69811184599185,0.0758880015104283,
12.5508374392248));
#446703=CARTESIAN_POINT('Ctrl Pts',(2.72744315642296,0.106443431512196,
12.5434499600945));
#446704=CARTESIAN_POINT('Ctrl Pts',(2.71702514602361,0.101850996421177,
12.5311293540532));
#446705=CARTESIAN_POINT('Ctrl Pts',(2.72076849334283,0.0858216759300503,
12.5278936106989));
#446706=CARTESIAN_POINT('Ctrl Pts',(2.75007712066208,0.116420865555225,
12.5204817579905));
#446707=CARTESIAN_POINT('Ctrl Pts',(2.73960754823101,0.111805701049081,
12.5081597038247));
#446708=CARTESIAN_POINT('Ctrl Pts',(2.74340426231153,0.0957474007938997,
12.5049254088044));
#446709=CARTESIAN_POINT('Ctrl Pts',(2.73380434092627,0.109247549171251,
12.5369868989719));
#446710=CARTESIAN_POINT('Ctrl Pts',(2.73465670444891,0.109623285243511,
12.5342545179733));
#446711=CARTESIAN_POINT('Ctrl Pts',(2.7355204794619,0.109867723048072,12.5314872231885));
#446712=CARTESIAN_POINT('Ctrl Pts',(2.73636222969268,0.109913304394048,
12.5287124745063));
#446713=CARTESIAN_POINT('Ctrl Pts',(2.73712136183156,0.109954411914307,
12.5262100684185));
#446714=CARTESIAN_POINT('Ctrl Pts',(2.73786186772383,0.109832759289019,
12.5237004536639));
#446715=CARTESIAN_POINT('Ctrl Pts',(2.73858571587266,0.109480843917267,
12.5212220730815));
#446716=CARTESIAN_POINT('Ctrl Pts',(2.73913988424842,0.109211422257096,
12.5193246583487));
#446717=CARTESIAN_POINT('Ctrl Pts',(2.73969063477889,0.108803247691215,
12.5174178313692));
#446718=CARTESIAN_POINT('Ctrl Pts',(2.74019662485357,0.108168315610022,
12.515581224835));
#446719=CARTESIAN_POINT('Ctrl Pts',(2.74041217934513,0.107897831130618,
12.5147988205795));
#446720=CARTESIAN_POINT('Ctrl Pts',(2.74062004614556,0.107586092634382,
12.5140295443048));
#446721=CARTESIAN_POINT('Ctrl Pts',(2.74081915043622,0.107226453601027,
12.5132817086137));
#446722=CARTESIAN_POINT('Ctrl Pts',(2.74112046784587,0.106682188574971,
12.5121499604604));
#446723=CARTESIAN_POINT('Ctrl Pts',(2.74140196660921,0.106013001334265,
12.5110494206568));
#446724=CARTESIAN_POINT('Ctrl Pts',(2.74163579126107,0.105194174035085,
12.5100666561695));
#446725=CARTESIAN_POINT('Ctrl Pts',(2.74177005283772,0.104724005285488,
12.5095023550641));
#446726=CARTESIAN_POINT('Ctrl Pts',(2.74188951973004,0.104198888158505,
12.5089719619137));
#446727=CARTESIAN_POINT('Ctrl Pts',(2.74198572482363,0.103627248528214,
12.5085043804652));
#446728=CARTESIAN_POINT('Ctrl Pts',(2.7421265084465,0.102790728390582,12.5078201359221));
#446729=CARTESIAN_POINT('Ctrl Pts',(2.74222037021483,0.1018301202597,12.5072563000949));
#446730=CARTESIAN_POINT('Ctrl Pts',(2.7422525218129,0.100809715898123,12.5068768744332));
#446731=CARTESIAN_POINT('Ctrl Pts',(2.74227570532843,0.100073934108551,
12.5066032824114));
#446732=CARTESIAN_POINT('Ctrl Pts',(2.74226727056795,0.0992941371635123,
12.5064197834844));
#446733=CARTESIAN_POINT('Ctrl Pts',(2.74223027325681,0.0985138429906198,
12.5063282718343));
#446734=CARTESIAN_POINT('Ctrl Pts',(2.74217626863662,0.0973748550711673,
12.5061946931565));
#446735=CARTESIAN_POINT('Ctrl Pts',(2.74206131261701,0.0962104128898943,
12.5062515701262));
#446736=CARTESIAN_POINT('Ctrl Pts',(2.74190792928924,0.095091264475483,
12.5064436508398));
#446737=CARTESIAN_POINT('',(2.67543256678469,0.0659456938362764,12.5737548217797));
#446738=CARTESIAN_POINT('Origin',(2.69098419246214,0.0663290197919795,12.5893111709658));
#446739=CARTESIAN_POINT('Ctrl Pts',(2.74190792928924,0.095091264475483,
12.5064436508398));
#446740=CARTESIAN_POINT('Ctrl Pts',(2.73206804148642,0.0907765227938596,
12.5164271754438));
#446741=CARTESIAN_POINT('Ctrl Pts',(2.72222416924921,0.0864602620975741,
12.5264061185523));
#446742=CARTESIAN_POINT('Ctrl Pts',(2.71237617262926,0.082142428021385,
12.536380305637));
#446743=CARTESIAN_POINT('Ctrl Pts',(2.70006817424325,0.0767460111772602,
12.5488460165097));
#446744=CARTESIAN_POINT('Ctrl Pts',(2.6877537299547,0.0713471351528752,
12.5613043021964));
#446745=CARTESIAN_POINT('Ctrl Pts',(2.67543256678469,0.0659456938362766,
12.5737548217797));
#446746=CARTESIAN_POINT('Ctrl Pts',(2.68340468995259,0.0230115497283483,
12.5893111709658));
#446747=CARTESIAN_POINT('Ctrl Pts',(2.67285582888757,0.027156445962365,
12.5770542771492));
#446748=CARTESIAN_POINT('Ctrl Pts',(2.67589590165752,0.0432362977156746,
12.5737548217797));
#446749=CARTESIAN_POINT('Ctrl Pts',(2.67356269432808,0.0268787018642816,
12.5928319619712));
#446750=CARTESIAN_POINT('Ctrl Pts',(2.66766458388877,0.0326964084241776,
12.5821634970843));
#446751=CARTESIAN_POINT('Ctrl Pts',(2.67230724903108,0.04463622260515,12.5773203894503));
#446752=CARTESIAN_POINT('Ctrl Pts',(2.66194829594574,0.0389489068979987,
12.5969440695591));
#446753=CARTESIAN_POINT('Ctrl Pts',(2.66184802901843,0.0429674251691045,
12.5878292599214));
#446754=CARTESIAN_POINT('Ctrl Pts',(2.66816911474248,0.0489397085999056,
12.5813877129824));
#446755=CARTESIAN_POINT('Ctrl Pts',(2.66127025045685,0.069538374037137,
12.596957478804));
#446756=CARTESIAN_POINT('Ctrl Pts',(2.6613698565182,0.0655495556931358,
12.5878468778671));
#446757=CARTESIAN_POINT('Ctrl Pts',(2.66793239651539,0.0598882351119593,
12.5814011370086));
#446758=CARTESIAN_POINT('Ctrl Pts',(2.6724200483096,0.0821883153406641,
12.5928371701607));
#446759=CARTESIAN_POINT('Ctrl Pts',(2.66677262462082,0.0761350789019351,
12.5821692192952));
#446760=CARTESIAN_POINT('Ctrl Pts',(2.6718926150495,0.064395848945155,12.5773318885715));
#446761=CARTESIAN_POINT('Ctrl Pts',(2.68211016738734,0.0864598836327133,
12.5893111709658));
#446762=CARTESIAN_POINT('Ctrl Pts',(2.67173914954817,0.0818881636566572,
12.5770542771492));
#446763=CARTESIAN_POINT('Ctrl Pts',(2.67543256678466,0.0659456938363268,
12.5737548217797));
#446764=CARTESIAN_POINT('',(2.67589590165752,0.0432362977156746,12.5737548217797));
#446765=CARTESIAN_POINT('Origin',(2.69145022058562,0.0434876195864259,12.5893111709658));
#446766=CARTESIAN_POINT('Ctrl Pts',(2.67543256678466,0.0659456938363268,
12.5737548217797));
#446767=CARTESIAN_POINT('Ctrl Pts',(2.67450285684086,0.0655715828214908,
12.5746934679442));
#446768=CARTESIAN_POINT('Ctrl Pts',(2.6735424546048,0.0649876624645773,
12.5756680099006));
#446769=CARTESIAN_POINT('Ctrl Pts',(2.67265889660333,0.0642632116891434,
12.5765688348656));
#446770=CARTESIAN_POINT('Ctrl Pts',(2.67242498440375,0.0640714213662866,
12.5768073183026));
#446771=CARTESIAN_POINT('Ctrl Pts',(2.67219634824882,0.0638700142193212,
12.5770407398754));
#446772=CARTESIAN_POINT('Ctrl Pts',(2.67197462283821,0.0636607082586026,
12.5772674179684));
#446773=CARTESIAN_POINT('Ctrl Pts',(2.67106472171016,0.0628017731945181,
12.5781976435658));
#446774=CARTESIAN_POINT('Ctrl Pts',(2.6702272645626,0.0617528294358856,
12.5790594849312));
#446775=CARTESIAN_POINT('Ctrl Pts',(2.66955653511983,0.0605545745638861,
12.5797571720116));
#446776=CARTESIAN_POINT('Ctrl Pts',(2.66911953077058,0.0597738684293732,
12.580211740231));
#446777=CARTESIAN_POINT('Ctrl Pts',(2.66874982371725,0.0588851313056713,
12.5806009430798));
#446778=CARTESIAN_POINT('Ctrl Pts',(2.66848979752031,0.0579441217195207,
12.5808812374708));
#446779=CARTESIAN_POINT('Ctrl Pts',(2.66826634875435,0.0571354823083379,
12.5811221033394));
#446780=CARTESIAN_POINT('Ctrl Pts',(2.66811942934896,0.0562716568392671,
12.581287365893));
#446781=CARTESIAN_POINT('Ctrl Pts',(2.66806555161111,0.055400002967128,
12.581359338449));
#446782=CARTESIAN_POINT('Ctrl Pts',(2.66805806371808,0.0552788610778637,
12.5813693411482));
#446783=CARTESIAN_POINT('Ctrl Pts',(2.66805231537126,0.055157551545398,
12.5813775999465));
#446784=CARTESIAN_POINT('Ctrl Pts',(2.66804829221806,0.0550361836174935,
12.5813841266931));
#446785=CARTESIAN_POINT('Ctrl Pts',(2.66804146645205,0.0548302682486581,
12.5813952001081));
#446786=CARTESIAN_POINT('Ctrl Pts',(2.66804016951635,0.0546227854925812,
12.5814007534795));
#446787=CARTESIAN_POINT('Ctrl Pts',(2.66804459918174,0.0544138244820763,
12.5814005856065));
#446788=CARTESIAN_POINT('Ctrl Pts',(2.66806487645801,0.0534572826744447,
12.5813998171494));
#446789=CARTESIAN_POINT('Ctrl Pts',(2.66820341339482,0.0525358473170682,
12.58127954464));
#446790=CARTESIAN_POINT('Ctrl Pts',(2.66843016297746,0.0516503504317533,
12.5810700125799));
#446791=CARTESIAN_POINT('Ctrl Pts',(2.66870405065577,0.0505807710161861,
12.5808169217085));
#446792=CARTESIAN_POINT('Ctrl Pts',(2.66912287726063,0.0495676803812869,
12.5804173076348));
#446793=CARTESIAN_POINT('Ctrl Pts',(2.66962587073952,0.0486899145082565,
12.5799304713245));
#446794=CARTESIAN_POINT('Ctrl Pts',(2.67024923811913,0.047602086066806,
12.5793271277669));
#446795=CARTESIAN_POINT('Ctrl Pts',(2.67101260784219,0.0466386134546762,
12.5785808224116));
#446796=CARTESIAN_POINT('Ctrl Pts',(2.67185894273059,0.0458204123060168,
12.5777485681082));
#446797=CARTESIAN_POINT('Ctrl Pts',(2.67312007443723,0.0446012029538864,
12.576508418016));
#446798=CARTESIAN_POINT('Ctrl Pts',(2.67455002858849,0.0437098833501206,
12.5750928681475));
#446799=CARTESIAN_POINT('Ctrl Pts',(2.67589590165752,0.0432362977156746,
12.5737548217797));
#446800=CARTESIAN_POINT('Ctrl Pts',(2.67589590165752,0.0432362977156746,
12.5737548217797));
#446801=CARTESIAN_POINT('Ctrl Pts',(2.67285582888757,0.0271564459623653,
12.5770542771492));
#446802=CARTESIAN_POINT('Ctrl Pts',(2.68340468995259,0.0230115497283485,
12.5893111709658));
#446803=CARTESIAN_POINT('Ctrl Pts',(2.69895837453433,0.0342286732243589,
12.5508408821982));
#446804=CARTESIAN_POINT('Ctrl Pts',(2.69590572466494,0.0180995984398426,
12.55409748406));
#446805=CARTESIAN_POINT('Ctrl Pts',(2.70646804337498,0.013949414379792,
12.5663972313419));
#446806=CARTESIAN_POINT('Ctrl Pts',(2.72199788916192,0.0252287493626836,
12.52790050457));
#446807=CARTESIAN_POINT('Ctrl Pts',(2.7189114744056,0.00906009693604175,
12.5311362602938));
#446808=CARTESIAN_POINT('Ctrl Pts',(2.72950812966358,0.00489642123669558,
12.5434568539655));
#446809=CARTESIAN_POINT('Ctrl Pts',(2.74501622465285,0.0162359147937623,
12.5049357605811));
#446810=CARTESIAN_POINT('Ctrl Pts',(2.74187768010818,3.61332171347901E-5,
12.5081700652078));
#446811=CARTESIAN_POINT('Ctrl Pts',(2.75252677110501,-0.00414814572032211,
12.5204921097672));
#446812=CARTESIAN_POINT('Ctrl Pts',(2.74350474993786,0.0168264180840729,
12.5064436508395));
#446813=CARTESIAN_POINT('Ctrl Pts',(2.74371960240641,0.0156252993524972,
12.5062361689309));
#446814=CARTESIAN_POINT('Ctrl Pts',(2.74389181302113,0.0143670723759075,
12.5061871075061));
#446815=CARTESIAN_POINT('Ctrl Pts',(2.74398978877153,0.0131417489926944,
12.5063648335164));
#446816=CARTESIAN_POINT('Ctrl Pts',(2.74403429540076,0.0125851315309581,
12.5064455676329));
#446817=CARTESIAN_POINT('Ctrl Pts',(2.74406388455427,0.0120275226306801,
12.506574497099));
#446818=CARTESIAN_POINT('Ctrl Pts',(2.7440762380652,0.0114927751994334,
12.5067492519495));
#446819=CARTESIAN_POINT('Ctrl Pts',(2.74410106292495,0.0104181794789025,
12.5071004286051));
#446820=CARTESIAN_POINT('Ctrl Pts',(2.74405639076854,0.0093963762832862,
12.5076537929613));
#446821=CARTESIAN_POINT('Ctrl Pts',(2.74395502389682,0.0085036441825537,
12.5083435010505));
#446822=CARTESIAN_POINT('Ctrl Pts',(2.74394864224647,0.00844744136181337,
12.5083869222964));
#446823=CARTESIAN_POINT('Ctrl Pts',(2.74394202333457,0.00839174532599308,
12.5084308732337));
#446824=CARTESIAN_POINT('Ctrl Pts',(2.74393516538416,0.00833657279140646,
12.5084753333615));
#446825=CARTESIAN_POINT('Ctrl Pts',(2.74388015557018,0.00789401624290068,
12.5088319622689));
#446826=CARTESIAN_POINT('Ctrl Pts',(2.74380992908381,0.00747599882754801,
12.509227847131));
#446827=CARTESIAN_POINT('Ctrl Pts',(2.74372933548101,0.00709448647694972,
12.5096423454524));
#446828=CARTESIAN_POINT('Ctrl Pts',(2.74347679079905,0.0058989956204657,
12.5109411997424));
#446829=CARTESIAN_POINT('Ctrl Pts',(2.7431163762448,0.0049864259306605,
12.5124831113042));
#446830=CARTESIAN_POINT('Ctrl Pts',(2.74271472659684,0.00428957871944309,
12.5140723025008));
#446831=CARTESIAN_POINT('Ctrl Pts',(2.74267709158492,0.00422428337251766,
12.5142212114565));
#446832=CARTESIAN_POINT('Ctrl Pts',(2.74263910665875,0.00416085503539146,
12.5143705582413));
#446833=CARTESIAN_POINT('Ctrl Pts',(2.7426008349746,0.00409922362932547,
12.5145201959299));
#446834=CARTESIAN_POINT('Ctrl Pts',(2.74210917821111,0.00330747645882913,
12.5164425148273));
#446835=CARTESIAN_POINT('Ctrl Pts',(2.74156247363941,0.00277948792615719,
12.5184635205941));
#446836=CARTESIAN_POINT('Ctrl Pts',(2.74098166111635,0.00242751123111316,
12.5205025929158));
#446837=CARTESIAN_POINT('Ctrl Pts',(2.74064476683173,0.00222335079693576,
12.5216853356836));
#446838=CARTESIAN_POINT('Ctrl Pts',(2.74029725624319,0.00207836408927715,
12.5228750347131));
#446839=CARTESIAN_POINT('Ctrl Pts',(2.73994888826066,0.00197713367238996,
12.5240609649613));
#446840=CARTESIAN_POINT('Ctrl Pts',(2.73909383773684,0.00172866904496134,
12.5269717671327));
#446841=CARTESIAN_POINT('Ctrl Pts',(2.73820665657674,0.00174679574769686,
12.529903606617));
#446842=CARTESIAN_POINT('Ctrl Pts',(2.73729952787676,0.00194571695786728,
12.532813300402));
#446843=CARTESIAN_POINT('Ctrl Pts',(2.73686405328027,0.00204121072158028,
12.5342101228452));
#446844=CARTESIAN_POINT('Ctrl Pts',(2.73642463725985,0.00217876241240093,
12.5356023438239));
#446845=CARTESIAN_POINT('Ctrl Pts',(2.73598532022336,0.00235138034623309,
12.5369868989719));
#446846=CARTESIAN_POINT('Origin',(14.5962335163271,-4.66351031667956,-1.239720872067));
#446847=CARTESIAN_POINT('Ctrl Pts',(2.73376608153298,0.109230727169096,
12.5369868989719));
#446848=CARTESIAN_POINT('Ctrl Pts',(2.74781354930456,0.115391242804295,
12.5369868989719));
#446849=CARTESIAN_POINT('Ctrl Pts',(2.74689044084213,0.130702388236675,
12.5369868989719));
#446850=CARTESIAN_POINT('Ctrl Pts',(2.73851464844057,0.11131328302727,12.5218025310015));
#446851=CARTESIAN_POINT('Ctrl Pts',(2.74757029418805,0.118906118057779,
12.5216901060417));
#446852=CARTESIAN_POINT('Ctrl Pts',(2.7468932712445,0.130655715783667,12.5161920673678));
#446853=CARTESIAN_POINT('Ctrl Pts',(2.74370127747141,0.108241646575592,
12.5042015548895));
#446854=CARTESIAN_POINT('Ctrl Pts',(2.74777665524214,0.113218456903791,
12.4980677368514));
#446855=CARTESIAN_POINT('Ctrl Pts',(2.74749076155969,0.120008820997566,
12.4907278922777));
#446856=CARTESIAN_POINT('Ctrl Pts',(2.74188794022434,0.0950905712304433,
12.506463626192));
#446857=CARTESIAN_POINT('Ctrl Pts',(2.74842674848915,0.0953173416261057,
12.4999376786891));
#446858=CARTESIAN_POINT('Ctrl Pts',(2.74834688645362,0.0953145719554462,
12.4906970594712));
#446859=CARTESIAN_POINT('Origin',(2.72493031585149,0.129378413011936,12.5369868989719));
#446860=CARTESIAN_POINT('Origin',(2.72493031585149,0.129378413011936,14.));
#446861=CARTESIAN_POINT('Origin',(2.72493031585149,0.129378413011936,13.7435492065112));
#446862=CARTESIAN_POINT('Ctrl Pts',(2.7111478626189,0.0992602202188586,
13.793642941384));
#446863=CARTESIAN_POINT('Ctrl Pts',(2.72105250706917,0.103596605501525,
13.8071662555867));
#446864=CARTESIAN_POINT('Ctrl Pts',(2.71659034273042,0.120031582624993,
13.8103758687955));
#446865=CARTESIAN_POINT('Ctrl Pts',(2.72635684332379,0.105964592757806,
13.7804579775006));
#446866=CARTESIAN_POINT('Ctrl Pts',(2.73857421226988,0.111324589750697,
13.7901904343351));
#446867=CARTESIAN_POINT('Ctrl Pts',(2.73696039359074,0.126997863608927,
13.7927914348262));
#446868=CARTESIAN_POINT('Ctrl Pts',(2.73531094262778,0.10991170922021,13.7597120340895));
#446869=CARTESIAN_POINT('Ctrl Pts',(2.74944757691701,0.116119982808342,
13.7635825532445));
#446870=CARTESIAN_POINT('Ctrl Pts',(2.74896431761631,0.13113005864401,13.7651073818884));
#446871=CARTESIAN_POINT('Ctrl Pts',(2.73355752495816,0.10913877343892,13.7381884353898));
#446872=CARTESIAN_POINT('Ctrl Pts',(2.74736362640026,0.115200907848243,
13.7368803041982));
#446873=CARTESIAN_POINT('Ctrl Pts',(2.74661343172915,0.130321319386107,
13.7363986145813));
#446874=CARTESIAN_POINT('Origin',(2.70596428021828,0.121017863901359,13.7902182540695));
#446875=CARTESIAN_POINT('Ctrl Pts',(2.68210656530513,0.0864582966033172,
13.8235227101244));
#446876=CARTESIAN_POINT('Ctrl Pts',(2.69262862607313,0.0910917537914321,
13.8358800583119));
#446877=CARTESIAN_POINT('Ctrl Pts',(2.68878013986014,0.107210537955413,
13.8390832900376));
#446878=CARTESIAN_POINT('Ctrl Pts',(2.69302076875767,0.0912694619810058,
13.8124254819052));
#446879=CARTESIAN_POINT('Ctrl Pts',(2.70356326310642,0.0959119175318677,
13.8247886449158));
#446880=CARTESIAN_POINT('Ctrl Pts',(2.6996933358596,0.11204711025482,13.8279860620657));
#446881=CARTESIAN_POINT('Ctrl Pts',(2.70393008081926,0.0960784711508696,
13.8013225099955));
#446882=CARTESIAN_POINT('Ctrl Pts',(2.71448803519229,0.100727732736346,
13.8136962257787));
#446883=CARTESIAN_POINT('Ctrl Pts',(2.7106015894118,0.116881195649208,13.8168830918626));
#446884=CARTESIAN_POINT('Ctrl Pts',(2.71483469180648,0.10088540800767,13.7902140179785));
#446885=CARTESIAN_POINT('Ctrl Pts',(2.72540345770452,0.105539426587026,
13.802602731458));
#446886=CARTESIAN_POINT('Ctrl Pts',(2.72150509546317,0.121712890172682,
13.8057746032558));
#446887=CARTESIAN_POINT('Origin',(2.67323614231258,0.106590747473348,13.8235269408515));
#446888=CARTESIAN_POINT('Ctrl Pts',(2.68340468995259,0.0230115497283484,
13.8235269408515));
#446889=CARTESIAN_POINT('Ctrl Pts',(2.69439427247702,0.0186934836415734,
13.8362179249168));
#446890=CARTESIAN_POINT('Ctrl Pts',(2.69080185486037,0.00199744998909402,
13.8391868794938));
#446891=CARTESIAN_POINT('Ctrl Pts',(2.67334970029081,0.0269623922435091,
13.8400110824519));
#446892=CARTESIAN_POINT('Ctrl Pts',(2.68090957753351,0.0203163318362425,
13.8494522556837));
#446893=CARTESIAN_POINT('Ctrl Pts',(2.67429527008017,0.00860399541908111,
13.85569149686));
#446894=CARTESIAN_POINT('Ctrl Pts',(2.66195470361959,0.0386050627665757,
13.8586819406588));
#446895=CARTESIAN_POINT('Ctrl Pts',(2.662057420685,0.0342524207138181,13.868010383617));
#446896=CARTESIAN_POINT('Ctrl Pts',(2.65548369043046,0.0280331814248738,
13.8744918421245));
#446897=CARTESIAN_POINT('Ctrl Pts',(2.66126372479098,0.0698875506184945,
13.8587686893867));
#446898=CARTESIAN_POINT('Ctrl Pts',(2.6611618656138,0.0742014528691105,
13.8680909899357));
#446899=CARTESIAN_POINT('Ctrl Pts',(2.65433598590387,0.0801093939395106,
13.8745789365163));
#446900=CARTESIAN_POINT('Ctrl Pts',(2.67220860875548,0.0820951092181263,
13.8400379222776));
#446901=CARTESIAN_POINT('Ctrl Pts',(2.67948431216712,0.089047401917223,
13.8494748685453));
#446902=CARTESIAN_POINT('Ctrl Pts',(2.67240200346499,0.10047552550389,13.8557104837033));
#446903=CARTESIAN_POINT('Ctrl Pts',(2.68211016738456,0.0864598836386525,
13.8235269408542));
#446904=CARTESIAN_POINT('Ctrl Pts',(2.69291447656097,0.0912226057606148,
13.8362179249195));
#446905=CARTESIAN_POINT('Ctrl Pts',(2.68864404095105,0.107758215327781,
13.8391868794965));
#446906=CARTESIAN_POINT('Origin',(2.67535915931955,0.00253547987027109,
13.8235269408515));
#446907=CARTESIAN_POINT('Ctrl Pts',(2.71669038311477,0.00993281525666357,
13.7902140241682));
#446908=CARTESIAN_POINT('Ctrl Pts',(2.72744017785787,0.00571375038707416,
13.8026027327198));
#446909=CARTESIAN_POINT('Ctrl Pts',(2.72420475383482,-0.0106052558223891,
13.8057746032556));
#446910=CARTESIAN_POINT('Ctrl Pts',(2.70559877879061,0.0142909681151822,
13.8013225161808));
#446911=CARTESIAN_POINT('Ctrl Pts',(2.71633757698319,0.0100762153034338,
13.8136962270464));
#446912=CARTESIAN_POINT('Ctrl Pts',(2.7131132437,-0.00622232083304009,13.8168830918628));
#446913=CARTESIAN_POINT('Ctrl Pts',(2.69450239277601,0.018650999812628,
13.8124254880875));
#446914=CARTESIAN_POINT('Ctrl Pts',(2.70522546621405,0.014442416787074,
13.8247886461867));
#446915=CARTESIAN_POINT('Ctrl Pts',(2.70201689249577,-0.00183719060661763,
13.8279860620656));
#446916=CARTESIAN_POINT('Ctrl Pts',(2.68340103148947,0.0230129864117414,
13.8235227163065));
#446917=CARTESIAN_POINT('Ctrl Pts',(2.69410332133798,0.0188125608100677,
13.8358800595847));
#446918=CARTESIAN_POINT('Ctrl Pts',(2.69091550151957,0.00255022285996103,
13.8390832900376));
#446919=CARTESIAN_POINT('Origin',(2.70864852252747,-0.0105446958323901,
13.7902182540695));
#446920=CARTESIAN_POINT('Ctrl Pts',(2.73573414330807,0.00245004404107459,
13.7382347919292));
#446921=CARTESIAN_POINT('Ctrl Pts',(2.74978792632498,-0.00304623212072527,
13.7369371795943));
#446922=CARTESIAN_POINT('Ctrl Pts',(2.74964670705973,-0.0181962761516587,
13.7364597369711));
#446923=CARTESIAN_POINT('Ctrl Pts',(2.73749467465009,0.00175829019900498,
13.7595490285573));
#446924=CARTESIAN_POINT('Ctrl Pts',(2.75188340268191,-0.00387005876363533,
13.7633824266925));
#446925=CARTESIAN_POINT('Ctrl Pts',(2.75199955109843,-0.018899369122145,
13.7648920890506));
#446926=CARTESIAN_POINT('Ctrl Pts',(2.72851606125849,0.00528619690360507,
13.7803806590111));
#446927=CARTESIAN_POINT('Ctrl Pts',(2.74096376258398,0.000422904015543165,
13.7901039518745));
#446928=CARTESIAN_POINT('Ctrl Pts',(2.74000555828081,-0.0153113670492094,
13.7926933640892));
#446929=CARTESIAN_POINT('Ctrl Pts',(2.71290922687708,0.0114184862122857,
13.7936647693663));
#446930=CARTESIAN_POINT('Ctrl Pts',(2.72298639143274,0.0074911351377519,
13.8072068914933));
#446931=CARTESIAN_POINT('Ctrl Pts',(2.71918393058566,-0.00912769639016085,
13.8104111085397));
#446932=CARTESIAN_POINT('Origin',(2.72793978959033,-0.0181246895118446,
13.7435492065112));
#446933=CARTESIAN_POINT('Origin',(2.72793978959033,-0.0181246895118447,
14.));
#446934=CARTESIAN_POINT('Origin',(2.72793978959033,-0.0181246895118445,
12.5369868989719));
#446935=CARTESIAN_POINT('Ctrl Pts',(2.7434863670468,0.0168263053487349,
12.506462012331));
#446936=CARTESIAN_POINT('Ctrl Pts',(2.75002486686205,0.0168664071679876,
12.4999388158272));
#446937=CARTESIAN_POINT('Ctrl Pts',(2.74994750783452,0.0168659327108754,
12.4907030323752));
#446938=CARTESIAN_POINT('Ctrl Pts',(2.74583256172836,0.00376016767646571,
12.5042014951932));
#446939=CARTESIAN_POINT('Ctrl Pts',(2.75010638582298,-0.00104353139032467,
12.4980716682127));
#446940=CARTESIAN_POINT('Ctrl Pts',(2.75009927474382,-0.00783510813351349,
12.4907355092743));
#446941=CARTESIAN_POINT('Ctrl Pts',(2.74077753690017,0.000478030380158065,
12.5218047446509));
#446942=CARTESIAN_POINT('Ctrl Pts',(2.75013006992358,-0.00673646870034738,
12.5216906929434));
#446943=CARTESIAN_POINT('Ctrl Pts',(2.74993668683658,-0.0184979888959359,
12.5161988840776));
#446944=CARTESIAN_POINT('Ctrl Pts',(2.7359495529117,0.00236539812914527,
12.5369868989719));
#446945=CARTESIAN_POINT('Ctrl Pts',(2.75022731620137,-0.00321591058522313,
12.5369868989719));
#446946=CARTESIAN_POINT('Ctrl Pts',(2.74993581177919,-0.01854302892797,
12.5369868989719));
#446947=CARTESIAN_POINT('Origin',(5.15079064385546E-31,-5.04677213932911E-31,
12.5));
#446948=CARTESIAN_POINT('Origin',(2.67260022728041,0.241657374439811,12.5));
#446949=CARTESIAN_POINT('',(2.67260022728041,0.241657374439811,12.5893111709658));
#446950=CARTESIAN_POINT('',(2.67260022728041,0.241657374439811,13.8235269408515));
#446951=CARTESIAN_POINT('',(2.67260022728041,0.241657374439811,12.5));
#446952=CARTESIAN_POINT('',(2.70684497862863,0.231334114087577,13.7902182540695));
#446953=CARTESIAN_POINT('',(2.67260022728041,0.241657374439811,13.8235269408515));
#446954=CARTESIAN_POINT('',(2.72668989544585,0.225351759568795,13.7435492065112));
#446955=CARTESIAN_POINT('Origin',(2.66140047544984,0.245033938752029,13.7445212918703));
#446956=CARTESIAN_POINT('',(2.72668989544585,0.225351759568795,12.5369868989719));
#446957=CARTESIAN_POINT('',(2.72668989544585,0.225351759568795,12.5));
#446958=CARTESIAN_POINT('Ctrl Pts',(2.72668989544585,0.225351759568795,
12.5369868989719));
#446959=CARTESIAN_POINT('Ctrl Pts',(2.70867315596209,0.230783000417881,
12.5544431401645));
#446960=CARTESIAN_POINT('Ctrl Pts',(2.69064353042739,0.236218125834777,
12.5718848856037));
#446961=CARTESIAN_POINT('Ctrl Pts',(2.67260022728041,0.241657374439811,
12.5893111709658));
#446962=CARTESIAN_POINT('Origin',(2.90789544171731,0.435855945855819,12.5));
#446963=CARTESIAN_POINT('',(2.71580314304261,0.331714470150425,13.7435492065112));
#446964=CARTESIAN_POINT('',(2.69758167769643,0.321835832101125,13.7902182540695));
#446965=CARTESIAN_POINT('Origin',(2.64969881607086,0.295876478680461,13.7418732680453));
#446966=CARTESIAN_POINT('',(2.66613838389343,0.304789073640352,13.8235269408515));
#446967=CARTESIAN_POINT('',(2.69758167769643,0.321835832101125,13.7902182540695));
#446968=CARTESIAN_POINT('',(2.66613838389343,0.304789073640352,12.5893111709658));
#446969=CARTESIAN_POINT('',(2.66613838389343,0.304789073640352,12.5));
#446970=CARTESIAN_POINT('',(2.71580314304261,0.331714470150425,12.5369868989719));
#446971=CARTESIAN_POINT('Ctrl Pts',(2.66613838389343,0.304789073640352,
12.5893111709658));
#446972=CARTESIAN_POINT('Ctrl Pts',(2.68270562003009,0.313770883070166,
12.5718848856037));
#446973=CARTESIAN_POINT('Ctrl Pts',(2.69926029747776,0.322745883895925,
12.5544431401645));
#446974=CARTESIAN_POINT('Ctrl Pts',(2.71580314304261,0.331714470150425,
12.5369868989719));
#446975=CARTESIAN_POINT('',(2.71580314304261,0.331714470150425,12.5));
#446976=CARTESIAN_POINT('Origin',(2.68252174292037,0.274569441412368,12.5));
#446977=CARTESIAN_POINT('',(2.64845827287882,0.269957480776539,13.8587068136939));
#446978=CARTESIAN_POINT('Ctrl Pts',(2.66613838389016,0.304789073646093,
13.8235269408542));
#446979=CARTESIAN_POINT('Ctrl Pts',(2.66459790938839,0.303953916333649,
13.8262006681044));
#446980=CARTESIAN_POINT('Ctrl Pts',(2.66310426415996,0.302946517721572,
13.8288634856214));
#446981=CARTESIAN_POINT('Ctrl Pts',(2.66165538025358,0.301780050874266,
13.8314912288862));
#446982=CARTESIAN_POINT('Ctrl Pts',(2.66016173039156,0.300577543870169,
13.8342001611531));
#446983=CARTESIAN_POINT('Ctrl Pts',(2.65871367987522,0.299205038716938,
13.8368750301949));
#446984=CARTESIAN_POINT('Ctrl Pts',(2.65731915339264,0.297632930257845,
13.8394886372969));
#446985=CARTESIAN_POINT('Ctrl Pts',(2.65721145072974,0.297511512508148,
13.8396904925131));
#446986=CARTESIAN_POINT('Ctrl Pts',(2.65710408111859,0.297388886822745,
13.8398919674349));
#446987=CARTESIAN_POINT('Ctrl Pts',(2.65699705609362,0.297265031267804,
13.8400930404591));
#446988=CARTESIAN_POINT('Ctrl Pts',(2.65532953420179,0.295335278395877,
13.8432258934518));
#446989=CARTESIAN_POINT('Ctrl Pts',(2.65375332029132,0.293117548342098,
13.8462331177034));
#446990=CARTESIAN_POINT('Ctrl Pts',(2.65239845173984,0.290628286762467,
13.8489036603661));
#446991=CARTESIAN_POINT('Ctrl Pts',(2.6519551229824,0.289813771404618,13.8497774930041));
#446992=CARTESIAN_POINT('Ctrl Pts',(2.65153571332566,0.288970302071231,
13.85061494757));
#446993=CARTESIAN_POINT('Ctrl Pts',(2.6511454016974,0.288098803041728,13.8514076489583));
#446994=CARTESIAN_POINT('Ctrl Pts',(2.65031983631224,0.286255456905349,
13.8530843267192));
#446995=CARTESIAN_POINT('Ctrl Pts',(2.64954605802412,0.284104436387558,
13.8546805203176));
#446996=CARTESIAN_POINT('Ctrl Pts',(2.64899736789653,0.281724400257269,
13.8559412814274));
#446997=CARTESIAN_POINT('Ctrl Pts',(2.64892393536301,0.281405874236645,
13.8561100121513));
#446998=CARTESIAN_POINT('Ctrl Pts',(2.64885448857294,0.281083307939024,
13.8562727473908));
#446999=CARTESIAN_POINT('Ctrl Pts',(2.64878939042725,0.280756944642768,
13.8564289040185));
#447000=CARTESIAN_POINT('Ctrl Pts',(2.64849417107922,0.279276890817491,
13.8571370725437));
#447001=CARTESIAN_POINT('Ctrl Pts',(2.64828542980016,0.277692286949607,
13.8577210840553));
#447002=CARTESIAN_POINT('Ctrl Pts',(2.64820037707139,0.276060893943153,
13.8581177131616));
#447003=CARTESIAN_POINT('Ctrl Pts',(2.64817642329555,0.27560143752169,13.8582294175695));
#447004=CARTESIAN_POINT('Ctrl Pts',(2.64816210811965,0.275138313700649,
13.8583265086086));
#447005=CARTESIAN_POINT('Ctrl Pts',(2.64815783106657,0.274672895613218,
13.8584082369006));
#447006=CARTESIAN_POINT('Ctrl Pts',(2.64815168608824,0.274004214628378,
13.8585256585398));
#447007=CARTESIAN_POINT('Ctrl Pts',(2.64816650872132,0.273322481571864,
13.8586122832068));
#447008=CARTESIAN_POINT('Ctrl Pts',(2.64820270341718,0.272645423058428,
13.8586682984299));
#447009=CARTESIAN_POINT('Ctrl Pts',(2.648231655586,0.272103843362332,13.8587131050557));
#447010=CARTESIAN_POINT('Ctrl Pts',(2.64827436811453,0.271559260363451,
13.8587357943552));
#447011=CARTESIAN_POINT('Ctrl Pts',(2.64833135097359,0.271011648950174,
13.8587355499465));
#447012=CARTESIAN_POINT('Ctrl Pts',(2.64836818035393,0.270657714638112,
13.8587353919793));
#447013=CARTESIAN_POINT('Ctrl Pts',(2.64841053421112,0.270306338648496,
13.8587257282814));
#447014=CARTESIAN_POINT('Ctrl Pts',(2.64845827287882,0.269957480776539,
13.8587068136939));
#447015=CARTESIAN_POINT('Ctrl Pts',(2.64845827287882,0.269957480776539,
13.8587068136939));
#447016=CARTESIAN_POINT('Ctrl Pts',(2.64861528275439,0.268810106253877,
13.8586446046466));
#447017=CARTESIAN_POINT('Ctrl Pts',(2.64883046929107,0.267689936275346,
13.858482427929));
#447018=CARTESIAN_POINT('Ctrl Pts',(2.64909951027578,0.266595828723968,
13.8582284286032));
#447019=CARTESIAN_POINT('Ctrl Pts',(2.64937551502996,0.265473401648074,
13.8579678548414));
#447020=CARTESIAN_POINT('Ctrl Pts',(2.64971035976198,0.264376027596299,
13.857615680862));
#447021=CARTESIAN_POINT('Ctrl Pts',(2.65008157564184,0.263344141808986,
13.8571944833187));
#447022=CARTESIAN_POINT('Ctrl Pts',(2.65100798283486,0.260768965294124,
13.8561433417727));
#447023=CARTESIAN_POINT('Ctrl Pts',(2.6521997327729,0.25847956972044,13.8546163505474));
#447024=CARTESIAN_POINT('Ctrl Pts',(2.65345582832213,0.256524514524141,
13.8528973491086));
#447025=CARTESIAN_POINT('Ctrl Pts',(2.65368529844701,0.256167354783928,
13.8525833129072));
#447026=CARTESIAN_POINT('Ctrl Pts',(2.65391684586957,0.255821230607973,
13.8522628768812));
#447027=CARTESIAN_POINT('Ctrl Pts',(2.65414918168728,0.255486270877606,
13.851937733538));
#447028=CARTESIAN_POINT('Ctrl Pts',(2.65556802429095,0.25344071827781,13.8499521282529));
#447029=CARTESIAN_POINT('Ctrl Pts',(2.6571606264168,0.251610564683827,13.847639871647));
#447030=CARTESIAN_POINT('Ctrl Pts',(2.65878268034566,0.250039256398138,
13.8452109780794));
#447031=CARTESIAN_POINT('Ctrl Pts',(2.6595124759831,0.249332292275942,13.8441181685877));
#447032=CARTESIAN_POINT('Ctrl Pts',(2.66024794320876,0.248677069410731,
13.8430021611332));
#447033=CARTESIAN_POINT('Ctrl Pts',(2.66097560292113,0.248074253114259,
13.8418824960098));
#447034=CARTESIAN_POINT('Ctrl Pts',(2.66269035161476,0.246653701118163,
13.8392439765549));
#447035=CARTESIAN_POINT('Ctrl Pts',(2.66444130286906,0.245453352890766,
13.8364981347964));
#447036=CARTESIAN_POINT('Ctrl Pts',(2.66621373793127,0.244441809029569,
13.8336931113419));
#447037=CARTESIAN_POINT('Ctrl Pts',(2.66793997712183,0.243456629547738,
13.8309611966328));
#447038=CARTESIAN_POINT('Ctrl Pts',(2.66968860442981,0.242650043858058,
13.8281701127186));
#447039=CARTESIAN_POINT('Ctrl Pts',(2.67145174932685,0.242031924733829,
13.8253580685121));
#447040=CARTESIAN_POINT('Ctrl Pts',(2.67183400104338,0.241897915840601,
13.8247484142933));
#447041=CARTESIAN_POINT('Ctrl Pts',(2.67221689157971,0.241772933002361,
13.8241378483365));
#447042=CARTESIAN_POINT('Ctrl Pts',(2.67260022728041,0.241657374439811,
13.8235269408515));
#447043=CARTESIAN_POINT('',(2.64831384601723,0.271191141078042,12.5969504640361));
#447044=CARTESIAN_POINT('Origin',(2.68255467630933,0.274572615479468,12.584524458991));
#447045=CARTESIAN_POINT('Origin',(2.68255467630933,0.274572615479468,12.584524458991));
#447046=CARTESIAN_POINT('Ctrl Pts',(2.66613838389343,0.304789073640352,
12.5893111709658));
#447047=CARTESIAN_POINT('Ctrl Pts',(2.65617451238041,0.299387231451652,
12.5770542771492));
#447048=CARTESIAN_POINT('Ctrl Pts',(2.66115509936875,0.283798856677273,
12.5737548217797));
#447049=CARTESIAN_POINT('Ctrl Pts',(2.68792602691775,0.316601089594918,
12.5663937883685));
#447050=CARTESIAN_POINT('Ctrl Pts',(2.67794944510285,0.311192356606314,
12.5540940315304));
#447051=CARTESIAN_POINT('Ctrl Pts',(2.68294852476992,0.295556653942359,
12.5508374392248));
#447052=CARTESIAN_POINT('Ctrl Pts',(2.70969168647735,0.328401187370187,
12.5434499600945));
#447053=CARTESIAN_POINT('Ctrl Pts',(2.69968266724224,0.322974868664596,
12.5311293540533));
#447054=CARTESIAN_POINT('Ctrl Pts',(2.70472009731098,0.307304001972979,
12.5278936106989));
#447055=CARTESIAN_POINT('Ctrl Pts',(2.73143708456714,0.340190300533473,
12.5204817579905));
#447056=CARTESIAN_POINT('Ctrl Pts',(2.721378527527,0.334737125258597,12.5081597038247));
#447057=CARTESIAN_POINT('Ctrl Pts',(2.7264715089034,0.319041725117335,12.5049254088044));
#447058=CARTESIAN_POINT('Ctrl Pts',(2.7158031430426,0.331714470150424,12.5369868989719));
#447059=CARTESIAN_POINT('Ctrl Pts',(2.71662204441789,0.332158431531958,
12.5342545179733));
#447060=CARTESIAN_POINT('Ctrl Pts',(2.71746302134045,0.332472461672344,
12.5314872231885));
#447061=CARTESIAN_POINT('Ctrl Pts',(2.71829825541393,0.332586501808387,
12.5287124745063));
#447062=CARTESIAN_POINT('Ctrl Pts',(2.71905151095872,0.332689348863517,
12.5262100684184));
#447063=CARTESIAN_POINT('Ctrl Pts',(2.71979946869705,0.332628459132043,
12.5237004536639));
#447064=CARTESIAN_POINT('Ctrl Pts',(2.72054959267069,0.332336715073668,
12.5212220730815));
#447065=CARTESIAN_POINT('Ctrl Pts',(2.72112387746341,0.332113359759108,
12.5193246583486));
#447066=CARTESIAN_POINT('Ctrl Pts',(2.72170606543337,0.331751434641541,
12.517417831369));
#447067=CARTESIAN_POINT('Ctrl Pts',(2.72226212472689,0.331159858132885,
12.5155812248348));
#447068=CARTESIAN_POINT('Ctrl Pts',(2.72249900897475,0.33090784336046,12.5147988205793));
#447069=CARTESIAN_POINT('Ctrl Pts',(2.72273159369701,0.330614085222352,
12.5140295443047));
#447070=CARTESIAN_POINT('Ctrl Pts',(2.72295934940448,0.330271871706331,
12.5132817086137));
#447071=CARTESIAN_POINT('Ctrl Pts',(2.72330402685765,0.329753977843431,
12.5121499604604));
#447072=CARTESIAN_POINT('Ctrl Pts',(2.72363913392964,0.329109962030609,
12.5110494206568));
#447073=CARTESIAN_POINT('Ctrl Pts',(2.72393892257576,0.328312918191567,
12.5100666561695));
#447074=CARTESIAN_POINT('Ctrl Pts',(2.72411106052602,0.327855257454619,
12.5095023550641));
#447075=CARTESIAN_POINT('Ctrl Pts',(2.72427293182291,0.327341625272324,
12.5089719619137));
#447076=CARTESIAN_POINT('Ctrl Pts',(2.7244154107387,0.326779729333997,12.5085043804652));
#447077=CARTESIAN_POINT('Ctrl Pts',(2.72462391007277,0.32595746782035,12.5078201359221));
#447078=CARTESIAN_POINT('Ctrl Pts',(2.72479575800432,0.325007706639303,
12.5072563000949));
#447079=CARTESIAN_POINT('Ctrl Pts',(2.72491097504904,0.323993318242785,
12.5068768744332));
#447080=CARTESIAN_POINT('Ctrl Pts',(2.72499405446985,0.32326187437816,12.5066032824114));
#447081=CARTESIAN_POINT('Ctrl Pts',(2.72504920846564,0.322483984631845,
12.5064197834844));
#447082=CARTESIAN_POINT('Ctrl Pts',(2.72507593547899,0.321703271199118,
12.5063282718343));
#447083=CARTESIAN_POINT('Ctrl Pts',(2.725114948644,0.320563671290108,12.5061946931565));
#447084=CARTESIAN_POINT('Ctrl Pts',(2.72509528797899,0.319393733711336,
12.5062515701262));
#447085=CARTESIAN_POINT('Ctrl Pts',(2.72503363600704,0.318265807005796,
12.5064436508398));
#447086=CARTESIAN_POINT('',(2.66115509936875,0.283798856677273,12.5737548217797));
#447087=CARTESIAN_POINT('Origin',(2.67662373367067,0.285448509014443,12.5893111709658));
#447088=CARTESIAN_POINT('Ctrl Pts',(2.72503363600704,0.318265807005796,
12.5064436508398));
#447089=CARTESIAN_POINT('Ctrl Pts',(2.71557818112231,0.313163380066183,
12.5164271754438));
#447090=CARTESIAN_POINT('Ctrl Pts',(2.70611887887486,0.308059114397915,
12.5264061185523));
#447091=CARTESIAN_POINT('Ctrl Pts',(2.69665559421328,0.302952944409553,
12.536380305637));
#447092=CARTESIAN_POINT('Ctrl Pts',(2.68482840774724,0.296571267566963,
12.5488460165097));
#447093=CARTESIAN_POINT('Ctrl Pts',(2.6729949972729,0.290186614325933,12.5613043021964));
#447094=CARTESIAN_POINT('Ctrl Pts',(2.66115509936875,0.283798856677273,
12.5737548217797));
#447095=CARTESIAN_POINT('Ctrl Pts',(2.67260022728041,0.241657374439812,
12.5893111709658));
#447096=CARTESIAN_POINT('Ctrl Pts',(2.66174861915796,0.244928648765893,
12.5770542771492));
#447097=CARTESIAN_POINT('Ctrl Pts',(2.66346791914059,0.261202790292396,
12.5737548217797));
#447098=CARTESIAN_POINT('Ctrl Pts',(2.66247577128447,0.244709444934003,
12.5928319619712));
#447099=CARTESIAN_POINT('Ctrl Pts',(2.6561230892275,0.250027042799071,12.5821634970842));
#447100=CARTESIAN_POINT('Ctrl Pts',(2.65977710058497,0.262305548542808,
12.5773203894503));
#447101=CARTESIAN_POINT('Ctrl Pts',(2.64991618509006,0.255792806065218,
12.5969440695591));
#447102=CARTESIAN_POINT('Ctrl Pts',(2.64948870524748,0.259789780362872,
12.5878292599214));
#447103=CARTESIAN_POINT('Ctrl Pts',(2.65530196153665,0.266257418681842,
12.5813877129824));
#447104=CARTESIAN_POINT('Ctrl Pts',(2.646747070191,0.286225222273891,12.596957478804));
#447105=CARTESIAN_POINT('Ctrl Pts',(2.64717147054681,0.282257795212573,
12.5878468778671));
#447106=CARTESIAN_POINT('Ctrl Pts',(2.65417362441804,0.277150220142025,
12.5814011370086));
#447107=CARTESIAN_POINT('Ctrl Pts',(2.65682868035863,0.299741883975949,
12.5928371701607));
#447108=CARTESIAN_POINT('Ctrl Pts',(2.65169344297155,0.29324847172335,12.5821692192952));
#447109=CARTESIAN_POINT('Ctrl Pts',(2.65775325327763,0.281965629837448,
12.5773318885715));
#447110=CARTESIAN_POINT('Ctrl Pts',(2.6661383838934,0.304789073640399,12.5893111709658));
#447111=CARTESIAN_POINT('Ctrl Pts',(2.65617451238038,0.299387231451699,
12.5770542771492));
#447112=CARTESIAN_POINT('Ctrl Pts',(2.66115509936873,0.283798856677322,
12.5737548217797));
#447113=CARTESIAN_POINT('',(2.66346791914059,0.261202790292396,12.5737548217797));
#447114=CARTESIAN_POINT('Origin',(2.67894999728998,0.262721097302248,12.5893111709658));
#447115=CARTESIAN_POINT('Ctrl Pts',(2.66115509936873,0.283798856677322,
12.5737548217797));
#447116=CARTESIAN_POINT('Ctrl Pts',(2.66025897647886,0.283350210494603,
12.5746934679442));
#447117=CARTESIAN_POINT('Ctrl Pts',(2.65934936483196,0.282689951386333,
12.5756680099006));
#447118=CARTESIAN_POINT('Ctrl Pts',(2.65852779626052,0.281895892981424,
12.5765688348656));
#447119=CARTESIAN_POINT('Ctrl Pts',(2.65831029507629,0.281685674809241,
12.5768073183026));
#447120=CARTESIAN_POINT('Ctrl Pts',(2.65809883624155,0.281466301858757,
12.5770407398754));
#447121=CARTESIAN_POINT('Ctrl Pts',(2.65789490898285,0.281239619666989,
12.5772674179684));
#447122=CARTESIAN_POINT('Ctrl Pts',(2.65705804665743,0.280309377249427,
12.5781976435658));
#447123=CARTESIAN_POINT('Ctrl Pts',(2.65630887473369,0.27919566323252,12.5790594849312));
#447124=CARTESIAN_POINT('Ctrl Pts',(2.65573804598393,0.277946724778423,
12.5797571720116));
#447125=CARTESIAN_POINT('Ctrl Pts',(2.65536613052829,0.277132996467755,
12.580211740231));
#447126=CARTESIAN_POINT('Ctrl Pts',(2.65507009397089,0.276217081986477,
12.5806009430798));
#447127=CARTESIAN_POINT('Ctrl Pts',(2.65488763400685,0.275258008983081,
12.5808812374708));
#447128=CARTESIAN_POINT('Ctrl Pts',(2.65473084036728,0.274433847104006,
12.5811221033394));
#447129=CARTESIAN_POINT('Ctrl Pts',(2.65465481961918,0.273560920647447,
12.581287365893));
#447130=CARTESIAN_POINT('Ctrl Pts',(2.65467216903768,0.272687775595847,
12.581359338449));
#447131=CARTESIAN_POINT('Ctrl Pts',(2.6546745802486,0.272566426463433,12.5813693411482));
#447132=CARTESIAN_POINT('Ctrl Pts',(2.65467873888201,0.272445052034801,
12.5813775999465));
#447133=CARTESIAN_POINT('Ctrl Pts',(2.65468462172837,0.272323760024331,
12.5813841266931));
#447134=CARTESIAN_POINT('Ctrl Pts',(2.65469460268872,0.272117973458602,
12.5813952001081));
#447135=CARTESIAN_POINT('Ctrl Pts',(2.65471022183926,0.27191107537198,12.5814007534795));
#447136=CARTESIAN_POINT('Ctrl Pts',(2.65473166902756,0.271703170720852,
12.5814005856065));
#447137=CARTESIAN_POINT('Ctrl Pts',(2.65482984587029,0.270751464513437,
12.5813998171494));
#447138=CARTESIAN_POINT('Ctrl Pts',(2.65504302737269,0.269844387202663,
12.58127954464));
#447139=CARTESIAN_POINT('Ctrl Pts',(2.6553411986815,0.268980318931211,12.5810700125799));
#447140=CARTESIAN_POINT('Ctrl Pts',(2.65570135567302,0.267936622841347,
12.5808169217085));
#447141=CARTESIAN_POINT('Ctrl Pts',(2.65620136495872,0.266961041438454,
12.5804173076348));
#447142=CARTESIAN_POINT('Ctrl Pts',(2.65677423083573,0.266127194897048,
12.5799304713245));
#447143=CARTESIAN_POINT('Ctrl Pts',(2.6574841921287,0.265093796343496,12.5793271277669));
#447144=CARTESIAN_POINT('Ctrl Pts',(2.6583235537643,0.26419575132621,12.5785808224116));
#447145=CARTESIAN_POINT('Ctrl Pts',(2.65923376353261,0.263449256824771,
12.5777485681082));
#447146=CARTESIAN_POINT('Ctrl Pts',(2.66059007580831,0.262336898233048,
12.576508418016));
#447147=CARTESIAN_POINT('Ctrl Pts',(2.66208792272741,0.26156509896011,12.5750928681475));
#447148=CARTESIAN_POINT('Ctrl Pts',(2.66346791914059,0.261202790292396,
12.5737548217797));
#447149=CARTESIAN_POINT('Ctrl Pts',(2.66346791914059,0.261202790292396,
12.5737548217797));
#447150=CARTESIAN_POINT('Ctrl Pts',(2.66174861915796,0.244928648765893,
12.5770542771492));
#447151=CARTESIAN_POINT('Ctrl Pts',(2.67260022728041,0.241657374439811,
12.5893111709658));
#447152=CARTESIAN_POINT('Ctrl Pts',(2.68718785856017,0.254104943569506,
12.5508408821982));
#447153=CARTESIAN_POINT('Ctrl Pts',(2.68546003546135,0.237780717647012,
12.55409748406));
#447154=CARTESIAN_POINT('Ctrl Pts',(2.69632548745655,0.234505270012706,
12.5663972313419));
#447155=CARTESIAN_POINT('Ctrl Pts',(2.71088428844942,0.247012900542605,
12.52790050457));
#447156=CARTESIAN_POINT('Ctrl Pts',(2.70912603875879,0.230646476517585,
12.5311362602938));
#447157=CARTESIAN_POINT('Ctrl Pts',(2.72002681274373,0.227360380883723,
12.5434568539655));
#447158=CARTESIAN_POINT('Ctrl Pts',(2.73455903183065,0.239926196923173,
12.5049357605811));
#447159=CARTESIAN_POINT('Ctrl Pts',(2.73275136312396,0.223524498266137,
12.5081700652078));
#447160=CARTESIAN_POINT('Ctrl Pts',(2.74370607772735,0.220222141949245,
12.5204921097672));
#447161=CARTESIAN_POINT('Ctrl Pts',(2.73300445492295,0.240391536141379,
12.5064436508395));
#447162=CARTESIAN_POINT('Ctrl Pts',(2.73331649481491,0.239211926504078,
12.5062361689309));
#447163=CARTESIAN_POINT('Ctrl Pts',(2.73359068959241,0.237971922937781,
12.5061871075061));
#447164=CARTESIAN_POINT('Ctrl Pts',(2.73378821456767,0.236758662650264,
12.5063648335164));
#447165=CARTESIAN_POINT('Ctrl Pts',(2.73387794259528,0.236207524990675,
12.5064455676329));
#447166=CARTESIAN_POINT('Ctrl Pts',(2.73395288359528,0.235654183278717,
12.506574497099));
#447167=CARTESIAN_POINT('Ctrl Pts',(2.73400878288092,0.235122222101259,
12.5067492519495));
#447168=CARTESIAN_POINT('Ctrl Pts',(2.73412111466528,0.234053225465864,
12.5071004286051));
#447169=CARTESIAN_POINT('Ctrl Pts',(2.73415987759819,0.233031181040618,
12.5076537929613));
#447170=CARTESIAN_POINT('Ctrl Pts',(2.7341316139703,0.232133157091211,12.5083435010505));
#447171=CARTESIAN_POINT('Ctrl Pts',(2.73412983460602,0.23207662111698,12.5083869222964));
#447172=CARTESIAN_POINT('Ctrl Pts',(2.73412777746198,0.232020570902364,
12.5084308732337));
#447173=CARTESIAN_POINT('Ctrl Pts',(2.7341254394046,0.231965022963218,12.5084753333615));
#447174=CARTESIAN_POINT('Ctrl Pts',(2.73410668509844,0.231519455174593,
12.5088319622689));
#447175=CARTESIAN_POINT('Ctrl Pts',(2.73407076458494,0.231097104567115,
12.509227847131));
#447176=CARTESIAN_POINT('Ctrl Pts',(2.73402153594906,0.230710292540567,
12.5096423454524));
#447177=CARTESIAN_POINT('Ctrl Pts',(2.73386727519189,0.229498194845199,
12.5109411997424));
#447178=CARTESIAN_POINT('Ctrl Pts',(2.73358244278894,0.22855928452366,12.5124831113042));
#447179=CARTESIAN_POINT('Ctrl Pts',(2.73323892911399,0.227832017839011,
12.5140723025008));
#447180=CARTESIAN_POINT('Ctrl Pts',(2.73320674150641,0.227763872154106,
12.5142212114565));
#447181=CARTESIAN_POINT('Ctrl Pts',(2.73317405297027,0.227697558745421,
12.5143705582413));
#447182=CARTESIAN_POINT('Ctrl Pts',(2.73314093216374,0.227633012915218,
12.5145201959299));
#447183=CARTESIAN_POINT('Ctrl Pts',(2.73271544609219,0.226803825627575,
12.5164425148273));
#447184=CARTESIAN_POINT('Ctrl Pts',(2.73221359660187,0.226233032435239,
12.518463520594));
#447185=CARTESIAN_POINT('Ctrl Pts',(2.73166340605281,0.225834885300983,
12.5205025929157));
#447186=CARTESIAN_POINT('Ctrl Pts',(2.73134427372684,0.225603944182036,
12.5216853356836));
#447187=CARTESIAN_POINT('Ctrl Pts',(2.73100973721378,0.225431114566588,
12.5228750347131));
#447188=CARTESIAN_POINT('Ctrl Pts',(2.73067077961574,0.225301825760895,
12.5240609649613));
#447189=CARTESIAN_POINT('Ctrl Pts',(2.72983882637577,0.224984493323426,
12.5269717671327));
#447190=CARTESIAN_POINT('Ctrl Pts',(2.72895311974325,0.224930246210316,
12.5299036066169));
#447191=CARTESIAN_POINT('Ctrl Pts',(2.72803279551388,0.225054566116146,
12.532813300402));
#447192=CARTESIAN_POINT('Ctrl Pts',(2.72759098629491,0.225114246909874,
12.5342101228452));
#447193=CARTESIAN_POINT('Ctrl Pts',(2.72714182065526,0.225215524423788,
12.5356023438238));
#447194=CARTESIAN_POINT('Ctrl Pts',(2.72668989544585,0.225351759568795,
12.5369868989719));
#447195=CARTESIAN_POINT('Origin',(14.9277716845705,-3.45826025389702,-1.23970570397459));
#447196=CARTESIAN_POINT('Ctrl Pts',(2.71576638210363,0.331694585626358,
12.5369868989719));
#447197=CARTESIAN_POINT('Ctrl Pts',(2.72926496886933,0.3389796016877,12.5369868989719));
#447198=CARTESIAN_POINT('Ctrl Pts',(2.72709693147968,0.354164558637326,
12.5369868989719));
#447199=CARTESIAN_POINT('Ctrl Pts',(2.72032940091062,0.334157264238229,
12.5218025310016));
#447200=CARTESIAN_POINT('Ctrl Pts',(2.72873602820049,0.342462953933468,
12.5216901060417));
#447201=CARTESIAN_POINT('Ctrl Pts',(2.72710355670233,0.354118272187117,
12.5161920673678));
#447202=CARTESIAN_POINT('Ctrl Pts',(2.72574913874772,0.331518606819774,
12.5042015548895));
#447203=CARTESIAN_POINT('Ctrl Pts',(2.72940529979091,0.336811038344444,
12.4980677368514));
#447204=CARTESIAN_POINT('Ctrl Pts',(2.7285668796838,0.343555505072639,12.4907278922777));
#447205=CARTESIAN_POINT('Ctrl Pts',(2.72501376996001,0.318263486773113,
12.506463626192));
#447206=CARTESIAN_POINT('Ctrl Pts',(2.73151233698725,0.319022476185907,
12.4999376786891));
#447207=CARTESIAN_POINT('Ctrl Pts',(2.73143296643992,0.319013206233799,
12.4906970594712));
#447208=CARTESIAN_POINT('Origin',(2.70531779326537,0.351055034776334,12.5369868989719));
#447209=CARTESIAN_POINT('Origin',(2.70531779326537,0.351055034776334,14.));
#447210=CARTESIAN_POINT('Origin',(2.70531779326537,0.351055034776334,13.7435492065112));
#447211=CARTESIAN_POINT('Ctrl Pts',(2.69403611232523,0.319913659896689,
13.793642941384));
#447212=CARTESIAN_POINT('Ctrl Pts',(2.70355434423058,0.325042936687985,
13.8071662555867));
#447213=CARTESIAN_POINT('Ctrl Pts',(2.69776742416513,0.341059519962545,
13.8103758687955));
#447214=CARTESIAN_POINT('Ctrl Pts',(2.70864801779921,0.327835397309829,
13.7804579775006));
#447215=CARTESIAN_POINT('Ctrl Pts',(2.72038784494332,0.334173388344512,
13.7901904343351));
#447216=CARTESIAN_POINT('Ctrl Pts',(2.71750187878964,0.349662969472621,
13.7927914348262));
#447217=CARTESIAN_POINT('Ctrl Pts',(2.71725059644146,0.332499222286879,
13.7597120340895));
#447218=CARTESIAN_POINT('Ctrl Pts',(2.73083416031405,0.339839105289468,
13.7635825532445));
#447219=CARTESIAN_POINT('Ctrl Pts',(2.72912904849147,0.354759846216685,
13.7651073818884));
#447220=CARTESIAN_POINT('Ctrl Pts',(2.71556601456628,0.331585938567642,
13.7381884353898));
#447221=CARTESIAN_POINT('Ctrl Pts',(2.72883205711228,0.338753227161935,
13.7368803041982));
#447222=CARTESIAN_POINT('Ctrl Pts',(2.72685190474066,0.353762178947586,
13.7363986145813));
#447223=CARTESIAN_POINT('Origin',(2.68709632791919,0.341176396727035,13.7902182540695));
#447224=CARTESIAN_POINT('Ctrl Pts',(2.66613492315446,0.304787198288574,
13.8235227101244));
#447225=CARTESIAN_POINT('Ctrl Pts',(2.67624430285751,0.310262883664768,
13.8358800583119));
#447226=CARTESIAN_POINT('Ctrl Pts',(2.67109479161606,0.326014346550185,
13.8390832900376));
#447227=CARTESIAN_POINT('Ctrl Pts',(2.67662065585239,0.310471963814255,
13.8124254819053));
#447228=CARTESIAN_POINT('Ctrl Pts',(2.68674966769504,0.315958283138429,
13.8247886449157));
#447229=CARTESIAN_POINT('Ctrl Pts',(2.68157744931315,0.331724352341378,
13.8279860620657));
#447230=CARTESIAN_POINT('Ctrl Pts',(2.68710168918608,0.316154181612971,
13.8013225099955));
#447231=CARTESIAN_POINT('Ctrl Pts',(2.69724555485603,0.321648544460721,
13.8136962257787));
#447232=CARTESIAN_POINT('Ctrl Pts',(2.69205538371444,0.337431476647197,
13.8168830918626));
#447233=CARTESIAN_POINT('Ctrl Pts',(2.69757820600054,0.321833950812844,
13.7902140179785));
#447234=CARTESIAN_POINT('Ctrl Pts',(2.70773245948189,0.327333936065635,
13.802602731458));
#447235=CARTESIAN_POINT('Ctrl Pts',(2.70252878128997,0.343135831072125,
13.8057746032558));
#447236=CARTESIAN_POINT('Origin',(2.6556530341162,0.324129638266262,13.8235269408515));
#447237=CARTESIAN_POINT('Ctrl Pts',(2.67260022728041,0.241657374439811,
13.8235269408515));
#447238=CARTESIAN_POINT('Ctrl Pts',(2.68390520534861,0.238249429359771,
13.8362179249168));
#447239=CARTESIAN_POINT('Ctrl Pts',(2.68168562294632,0.221316134995806,
13.8391868794938));
#447240=CARTESIAN_POINT('Ctrl Pts',(2.66225666442441,0.244775495849028,
13.8400110824519));
#447241=CARTESIAN_POINT('Ctrl Pts',(2.67033310242142,0.238767749837299,
13.8494522556836));
#447242=CARTESIAN_POINT('Ctrl Pts',(2.66469546768055,0.226555257791658,
13.85569149686));
#447243=CARTESIAN_POINT('Ctrl Pts',(2.6499505979317,0.255450628331682,13.8586819406588));
#447244=CARTESIAN_POINT('Ctrl Pts',(2.65040775394981,0.251120841730696,
13.868010383617));
#447245=CARTESIAN_POINT('Ctrl Pts',(2.64436282297905,0.244386476404156,
13.8744918421245));
#447246=CARTESIAN_POINT('Ctrl Pts',(2.64671210510577,0.286572705096629,
13.8587686893867));
#447247=CARTESIAN_POINT('Ctrl Pts',(2.64625896177486,0.290863950724822,
13.8680909899357));
#447248=CARTESIAN_POINT('Ctrl Pts',(2.63897424257269,0.296195861043949,
13.8745789365163));
#447249=CARTESIAN_POINT('Ctrl Pts',(2.65662554151646,0.29963175370253,13.8400379222776));
#447250=CARTESIAN_POINT('Ctrl Pts',(2.66331035922829,0.307153950593571,
13.8494748685453));
#447251=CARTESIAN_POINT('Ctrl Pts',(2.65532011815827,0.317966774133587,
13.8557104837033));
#447252=CARTESIAN_POINT('Ctrl Pts',(2.66613838389016,0.304789073646093,
13.8235269408542));
#447253=CARTESIAN_POINT('Ctrl Pts',(2.67651853655118,0.310416599703283,
13.8362179249195));
#447254=CARTESIAN_POINT('Ctrl Pts',(2.67091450477463,0.326549108246711,
13.8391868794965));
#447255=CARTESIAN_POINT('Origin',(2.66625045727084,0.220593651577375,13.8235269408515));
#447256=CARTESIAN_POINT('Ctrl Pts',(2.70684120332097,0.231335251380178,
13.7902140241682));
#447257=CARTESIAN_POINT('Ctrl Pts',(2.71789912196361,0.228006433168682,
13.8026027327198));
#447258=CARTESIAN_POINT('Ctrl Pts',(2.71600461405142,0.211478010012068,
13.8057746032556));
#447259=CARTESIAN_POINT('Ctrl Pts',(2.6954312754781,0.234774834122735,13.8013225161808));
#447260=CARTESIAN_POINT('Ctrl Pts',(2.7064778826876,0.231449417300115,13.8136962270464));
#447261=CARTESIAN_POINT('Ctrl Pts',(2.70459276011078,0.214942300102255,
13.8168830918628));
#447262=CARTESIAN_POINT('Ctrl Pts',(2.6840164287127,0.238215899700367,13.8124254880875));
#447263=CARTESIAN_POINT('Ctrl Pts',(2.69504686059561,0.234895350420997,
13.8247886461868));
#447264=CARTESIAN_POINT('Ctrl Pts',(2.69317590227677,0.218408383532957,
13.8279860620656));
#447265=CARTESIAN_POINT('Ctrl Pts',(2.67259646388749,0.241658508144051,
13.8235227163065));
#447266=CARTESIAN_POINT('Ctrl Pts',(2.6836055164308,0.238344395089921,13.8358800595847));
#447267=CARTESIAN_POINT('Ctrl Pts',(2.68175383533497,0.22187633181832,13.8390832900376));
#447268=CARTESIAN_POINT('Origin',(2.70049520861906,0.210270391225142,13.7902182540695));
#447269=CARTESIAN_POINT('Ctrl Pts',(2.72643151229394,0.225429621717924,
13.7382347919292));
#447270=CARTESIAN_POINT('Ctrl Pts',(2.74088653003935,0.221097147746479,
13.7369371795943));
#447271=CARTESIAN_POINT('Ctrl Pts',(2.74198064990422,0.205986003556125,
13.7364597369711));
#447272=CARTESIAN_POINT('Ctrl Pts',(2.7282425699732,0.224883669278053,13.7595490285574));
#447273=CARTESIAN_POINT('Ctrl Pts',(2.74304218339098,0.220446863095312,
13.7633824266926));
#447274=CARTESIAN_POINT('Ctrl Pts',(2.74438297365277,0.205477028701391,
13.7648920890506));
#447275=CARTESIAN_POINT('Ctrl Pts',(2.71900627502906,0.227667996819329,
13.7803806590111));
#447276=CARTESIAN_POINT('Ctrl Pts',(2.73180896117424,0.223835489354001,
13.7901039518744));
#447277=CARTESIAN_POINT('Ctrl Pts',(2.73213643437849,0.208075470231991,
13.7926933640892));
#447278=CARTESIAN_POINT('Ctrl Pts',(2.70295153259354,0.232507779552342,
13.7936647693663));
#447279=CARTESIAN_POINT('Ctrl Pts',(2.71331528178779,0.229414878877652,
13.8072068914933));
#447280=CARTESIAN_POINT('Ctrl Pts',(2.71088006236672,0.212541409281315,
13.8104111085397));
#447281=CARTESIAN_POINT('Origin',(2.72034012543628,0.204288036706358,13.7435492065112));
#447282=CARTESIAN_POINT('Origin',(2.72034012543628,0.204288036706358,14.));
#447283=CARTESIAN_POINT('Origin',(2.72034012543628,0.204288036706358,12.5369868989719));
#447284=CARTESIAN_POINT('Ctrl Pts',(2.73298614238843,0.240389925404879,
12.506462012331));
#447285=CARTESIAN_POINT('Ctrl Pts',(2.73949961721437,0.24096284222405,12.4999388158272));
#447286=CARTESIAN_POINT('Ctrl Pts',(2.73942255426528,0.240956063866745,
12.4907030323752));
#447287=CARTESIAN_POINT('Ctrl Pts',(2.73638954182112,0.227558500875394,
12.5042014951932));
#447288=CARTESIAN_POINT('Ctrl Pts',(2.74104069118792,0.223119142060907,
12.4980716682127));
#447289=CARTESIAN_POINT('Ctrl Pts',(2.7415871803248,0.216349584110118,12.4907355092743));
#447290=CARTESIAN_POINT('Ctrl Pts',(2.73161886183057,0.223875253168118,
12.5218047446509));
#447291=CARTESIAN_POINT('Ctrl Pts',(2.74152832372308,0.217447078004261,
12.5216906929434));
#447292=CARTESIAN_POINT('Ctrl Pts',(2.74229425718691,0.205708930779974,
12.5161988840776));
#447293=CARTESIAN_POINT('Ctrl Pts',(2.72665310456753,0.225362815340743,
12.5369868989719));
#447294=CARTESIAN_POINT('Ctrl Pts',(2.74133828825224,0.22096384822709,12.5369868989719));
#447295=CARTESIAN_POINT('Ctrl Pts',(2.74229705622194,0.20566396928963,12.5369868989719));
#447296=CARTESIAN_POINT('Origin',(5.1250859646407E-31,-4.62728456409018E-31,
12.5));
#447297=CARTESIAN_POINT('Origin',(2.64401005104368,0.45869500919504,12.5));
#447298=CARTESIAN_POINT('',(2.64401005104368,0.45869500919504,12.5893111709658));
#447299=CARTESIAN_POINT('',(2.64401005104368,0.45869500919504,13.8235269408515));
#447300=CARTESIAN_POINT('',(2.64401005104368,0.45869500919504,12.5));
#447301=CARTESIAN_POINT('',(2.67898229736196,0.45119736378766,13.7902182540695));
#447302=CARTESIAN_POINT('',(2.64401005104368,0.45869500919504,13.8235269408515));
#447303=CARTESIAN_POINT('',(2.69924879928632,0.446852460011852,13.7435492065112));
#447304=CARTESIAN_POINT('Origin',(2.63257234412928,0.461147454519627,13.7445212918716));
#447305=CARTESIAN_POINT('',(2.69924879928632,0.446852460011852,12.5369868989719));
#447306=CARTESIAN_POINT('',(2.69924879928632,0.446852460011852,12.5));
#447307=CARTESIAN_POINT('Ctrl Pts',(2.69924879928632,0.446852460011852,
12.5369868989719));
#447308=CARTESIAN_POINT('Ctrl Pts',(2.68084931246653,0.450797097327883,
12.5544431401645));
#447309=CARTESIAN_POINT('Ctrl Pts',(2.66243666584474,0.454744555953365,
12.5718848856037));
#447310=CARTESIAN_POINT('Ctrl Pts',(2.64401005104368,0.45869500919504,12.5893111709658));
#447311=CARTESIAN_POINT('Origin',(2.86269335364304,0.671426145235719,12.5));
#447312=CARTESIAN_POINT('',(2.67972872331796,0.551973886059784,13.7435492065112));
#447313=CARTESIAN_POINT('',(2.66237308910438,0.540642899778119,13.7902182540695));
#447314=CARTESIAN_POINT('Origin',(2.61676548204774,0.510867026218055,13.7418732680447));
#447315=CARTESIAN_POINT('',(2.63242388933657,0.521089942649624,13.8235269408515));
#447316=CARTESIAN_POINT('',(2.66237308910438,0.540642899778119,13.7902182540695));
#447317=CARTESIAN_POINT('',(2.63242388933657,0.521089942649624,12.5893111709658));
#447318=CARTESIAN_POINT('',(2.63242388933657,0.521089942649624,12.5));
#447319=CARTESIAN_POINT('',(2.67972872331796,0.551973886059784,12.5369868989719));
#447320=CARTESIAN_POINT('Ctrl Pts',(2.63242388933657,0.521089942649624,
12.5893111709658));
#447321=CARTESIAN_POINT('Ctrl Pts',(2.6482038985101,0.531392249397362,12.5718848856037));
#447322=CARTESIAN_POINT('Ctrl Pts',(2.66397194574709,0.541686746546371,
12.5544431401645));
#447323=CARTESIAN_POINT('Ctrl Pts',(2.67972872331796,0.551973886059784,
12.5369868989719));
#447324=CARTESIAN_POINT('',(2.67972872331796,0.551973886059784,12.5));
#447325=CARTESIAN_POINT('Origin',(2.65121591465983,0.492306259611314,12.5));
#447326=CARTESIAN_POINT('',(2.61764170561193,0.484933155856055,13.8587068136939));
#447327=CARTESIAN_POINT('Ctrl Pts',(2.63242388933283,0.521089942655079,
13.8235269408542));
#447328=CARTESIAN_POINT('Ctrl Pts',(2.63095661370707,0.520132001286734,
13.8262006681044));
#447329=CARTESIAN_POINT('Ctrl Pts',(2.62955005079904,0.519006208757991,
13.8288634856214));
#447330=CARTESIAN_POINT('Ctrl Pts',(2.62820106581135,0.51772552574374,13.8314912288862));
#447331=CARTESIAN_POINT('Ctrl Pts',(2.62681040143038,0.516405273652374,
13.8342001611531));
#447332=CARTESIAN_POINT('Ctrl Pts',(2.62547904109438,0.514919305836688,
13.8368750301949));
#447333=CARTESIAN_POINT('Ctrl Pts',(2.62421729621779,0.51323876158432,13.8394886372969));
#447334=CARTESIAN_POINT('Ctrl Pts',(2.62411984860041,0.513108969075282,
13.8396904925131));
#447335=CARTESIAN_POINT('Ctrl Pts',(2.62402283138454,0.512977999796652,
13.8398919674349));
#447336=CARTESIAN_POINT('Ctrl Pts',(2.62392625785407,0.512845832827748,
13.8400930404591));
#447337=CARTESIAN_POINT('Ctrl Pts',(2.62242157727778,0.510786582534607,
13.8432258934518));
#447338=CARTESIAN_POINT('Ctrl Pts',(2.62103137367685,0.508447755728073,
13.8462331177034));
#447339=CARTESIAN_POINT('Ctrl Pts',(2.61988391126663,0.505856342596067,
13.8489036603661));
#447340=CARTESIAN_POINT('Ctrl Pts',(2.61950844821232,0.505008402061483,
13.8497774930041));
#447341=CARTESIAN_POINT('Ctrl Pts',(2.61915918468767,0.504133553522089,
13.85061494757));
#447342=CARTESIAN_POINT('Ctrl Pts',(2.61884120705065,0.503233140312533,
13.8514076489583));
#447343=CARTESIAN_POINT('Ctrl Pts',(2.61816863848912,0.501328636515285,
13.8530843267192));
#447344=CARTESIAN_POINT('Ctrl Pts',(2.61757276302572,0.499121703226922,
13.8546805203176));
#447345=CARTESIAN_POINT('Ctrl Pts',(2.61721989365905,0.496704863131317,
13.8559412814274));
#447346=CARTESIAN_POINT('Ctrl Pts',(2.61717266829397,0.496381411546564,
13.8561100121513));
#447347=CARTESIAN_POINT('Ctrl Pts',(2.61712974473018,0.496054258003594,
13.8562727473908));
#447348=CARTESIAN_POINT('Ctrl Pts',(2.61709146483165,0.495723674551077,
13.8564289040185));
#447349=CARTESIAN_POINT('Ctrl Pts',(2.61691786592856,0.494224482365258,
13.8571370725437));
#447350=CARTESIAN_POINT('Ctrl Pts',(2.61683897914486,0.492628136783919,
13.8577210840553));
#447351=CARTESIAN_POINT('Ctrl Pts',(2.61688718309717,0.490995239516125,
13.8581177131616));
#447352=CARTESIAN_POINT('Ctrl Pts',(2.61690075898927,0.490535359442897,
13.8582294175695));
#447353=CARTESIAN_POINT('Ctrl Pts',(2.6169242403368,0.490072609808437,13.8583265086086));
#447354=CARTESIAN_POINT('Ctrl Pts',(2.61695791341011,0.489608391741768,
13.8584082369006));
#447355=CARTESIAN_POINT('Ctrl Pts',(2.61700629258668,0.48894143486496,13.8585256585398));
#447356=CARTESIAN_POINT('Ctrl Pts',(2.61707663347169,0.488263178401156,
13.8586122832068));
#447357=CARTESIAN_POINT('Ctrl Pts',(2.61716789428703,0.487591322947798,
13.8586682984299));
#447358=CARTESIAN_POINT('Ctrl Pts',(2.61724089389291,0.487053905184001,
13.8587131050557));
#447359=CARTESIAN_POINT('Ctrl Pts',(2.61732785286909,0.486514615707723,
13.8587357943552));
#447360=CARTESIAN_POINT('Ctrl Pts',(2.61742928153635,0.485973471058265,
13.8587355499465));
#447361=CARTESIAN_POINT('Ctrl Pts',(2.61749483730215,0.485623716369912,
13.8587353919793));
#447362=CARTESIAN_POINT('Ctrl Pts',(2.61756569063552,0.485276961787545,
13.8587257282814));
#447363=CARTESIAN_POINT('Ctrl Pts',(2.61764170561193,0.484933155856055,
13.8587068136939));
#447364=CARTESIAN_POINT('Ctrl Pts',(2.61764170561193,0.484933155856055,
13.8587068136939));
#447365=CARTESIAN_POINT('Ctrl Pts',(2.6178917147254,0.483802396889853,13.8586446046466));
#447366=CARTESIAN_POINT('Ctrl Pts',(2.61819748949905,0.482703493884876,
13.858482427929));
#447367=CARTESIAN_POINT('Ctrl Pts',(2.61855481519474,0.481634956223954,
13.8582284286032));
#447368=CARTESIAN_POINT('Ctrl Pts',(2.61892138979266,0.480538760881331,
13.8579678548414));
#447369=CARTESIAN_POINT('Ctrl Pts',(2.6193445665292,0.479472331205392,13.857615680862));
#447370=CARTESIAN_POINT('Ctrl Pts',(2.61979865549006,0.47847413647332,13.8571944833187));
#447371=CARTESIAN_POINT('Ctrl Pts',(2.62093188093231,0.475983039432451,
13.8561433417727));
#447372=CARTESIAN_POINT('Ctrl Pts',(2.6223062724137,0.473798400317295,13.8546163505474));
#447373=CARTESIAN_POINT('Ctrl Pts',(2.62371754355696,0.471952233854166,
13.8528973491086));
#447374=CARTESIAN_POINT('Ctrl Pts',(2.62397536197347,0.471614966478998,
13.8525833129072));
#447375=CARTESIAN_POINT('Ctrl Pts',(2.62423435127468,0.471288867267204,
13.8522628768812));
#447376=CARTESIAN_POINT('Ctrl Pts',(2.62449321634177,0.470973959613751,
13.851937733538));
#447377=CARTESIAN_POINT('Ctrl Pts',(2.62607406939059,0.469050862265577,
13.8499521282529));
#447378=CARTESIAN_POINT('Ctrl Pts',(2.62781054677247,0.467356610214955,
13.847639871647));
#447379=CARTESIAN_POINT('Ctrl Pts',(2.62955527966329,0.465922742781579,
13.8452109780794));
#447380=CARTESIAN_POINT('Ctrl Pts',(2.63034027110504,0.465277616143722,
13.8441181685877));
#447381=CARTESIAN_POINT('Ctrl Pts',(2.63112669787049,0.464684520885177,
13.8430021611332));
#447382=CARTESIAN_POINT('Ctrl Pts',(2.63190107147962,0.464143021432023,
13.8418824960098));
#447383=CARTESIAN_POINT('Ctrl Pts',(2.63372590266388,0.462866964142988,
13.8392439765549));
#447384=CARTESIAN_POINT('Ctrl Pts',(2.63556886729635,0.46181332875756,13.8364981347964));
#447385=CARTESIAN_POINT('Ctrl Pts',(2.63741785494251,0.46094962063717,13.8336931113419));
#447386=CARTESIAN_POINT('Ctrl Pts',(2.6392186514883,0.460108423778447,13.8309611966328));
#447387=CARTESIAN_POINT('Ctrl Pts',(2.64102720460484,0.459447051295175,
13.8281701127186));
#447388=CARTESIAN_POINT('Ctrl Pts',(2.64283486522965,0.458974701588688,
13.8253580685121));
#447389=CARTESIAN_POINT('Ctrl Pts',(2.643226768004,0.458872295662546,13.8247484142933));
#447390=CARTESIAN_POINT('Ctrl Pts',(2.64361857176526,0.458778937827683,
13.8241378483365));
#447391=CARTESIAN_POINT('Ctrl Pts',(2.64401005104368,0.45869500919504,13.8235269408515));
#447392=CARTESIAN_POINT('',(2.61739720455155,0.48615093912443,12.5969504640361));
#447393=CARTESIAN_POINT('Origin',(2.65124847974971,0.492312107493906,12.584524458991));
#447394=CARTESIAN_POINT('Origin',(2.65124847974971,0.492312107493906,12.584524458991));
#447395=CARTESIAN_POINT('Ctrl Pts',(2.63242388933657,0.521089942649624,
12.5893111709658));
#447396=CARTESIAN_POINT('Ctrl Pts',(2.62293347207067,0.514893926616804,
12.5770542771492));
#447397=CARTESIAN_POINT('Ctrl Pts',(2.62916808382621,0.499763384950601,
12.5737548217797));
#447398=CARTESIAN_POINT('Ctrl Pts',(2.65317624681838,0.53463855026862,12.5663937883685));
#447399=CARTESIAN_POINT('Ctrl Pts',(2.64367372320726,0.528434630356866,
12.5540940315304));
#447400=CARTESIAN_POINT('Ctrl Pts',(2.64993062377102,0.513258425605721,
12.5508374392248));
#447401=CARTESIAN_POINT('Ctrl Pts',(2.67390766542586,0.548173487508601,
12.5434499600944));
#447402=CARTESIAN_POINT('Ctrl Pts',(2.66437424572655,0.541949396444004,
12.5311293540533));
#447403=CARTESIAN_POINT('Ctrl Pts',(2.67067223527891,0.526741270584369,
12.5278936106989));
#447404=CARTESIAN_POINT('Ctrl Pts',(2.69461978532979,0.561695825189121,
12.5204817579905));
#447405=CARTESIAN_POINT('Ctrl Pts',(2.68503918171815,0.555440929127259,
12.5081597038247));
#447406=CARTESIAN_POINT('Ctrl Pts',(2.69139453743966,0.540212879398297,
12.5049254088044));
#447407=CARTESIAN_POINT('Ctrl Pts',(2.67972872331796,0.551973886059784,
12.5369868989719));
#447408=CARTESIAN_POINT('Ctrl Pts',(2.68050871289234,0.552483118260842,
12.5342545179733));
#447409=CARTESIAN_POINT('Ctrl Pts',(2.68132129516182,0.552864650918281,
12.5314872231885));
#447410=CARTESIAN_POINT('Ctrl Pts',(2.68214445473304,0.553046390926102,
12.5287124745063));
#447411=CARTESIAN_POINT('Ctrl Pts',(2.68288682089236,0.553210293085923,
12.5262100684184));
#447412=CARTESIAN_POINT('Ctrl Pts',(2.6836372529414,0.553210571459382,12.5237004536639));
#447413=CARTESIAN_POINT('Ctrl Pts',(2.68440866078858,0.552980940222957,
12.5212220730815));
#447414=CARTESIAN_POINT('Ctrl Pts',(2.68499924022769,0.552805137646787,
12.5193246583486));
#447415=CARTESIAN_POINT('Ctrl Pts',(2.68560899127225,0.552491870529511,
12.517417831369));
#447416=CARTESIAN_POINT('Ctrl Pts',(2.68621141930172,0.551947586437506,
12.5155812248347));
#447417=CARTESIAN_POINT('Ctrl Pts',(2.68646805688034,0.551715718488774,
12.5147988205793));
#447418=CARTESIAN_POINT('Ctrl Pts',(2.68672381171149,0.551441895620714,
12.5140295443047));
#447419=CARTESIAN_POINT('Ctrl Pts',(2.68697870315914,0.551119384996479,
12.5132817086137));
#447420=CARTESIAN_POINT('Ctrl Pts',(2.68736444688424,0.550631308794947,
12.5121499604604));
#447421=CARTESIAN_POINT('Ctrl Pts',(2.68775093218258,0.550016750228963,
12.5110494206568));
#447422=CARTESIAN_POINT('Ctrl Pts',(2.68811468977899,0.549246794045306,
12.5100666561695));
#447423=CARTESIAN_POINT('Ctrl Pts',(2.6883235585532,0.548804686977702,12.509502355064));
#447424=CARTESIAN_POINT('Ctrl Pts',(2.68852675702788,0.548305957877592,
12.5089719619137));
#447425=CARTESIAN_POINT('Ctrl Pts',(2.68871456159219,0.547757544955994,
12.5085043804652));
#447426=CARTESIAN_POINT('Ctrl Pts',(2.68898938910879,0.546955014081043,
12.5078201359221));
#447427=CARTESIAN_POINT('Ctrl Pts',(2.68923807958395,0.546022420353721,
12.5072563000949));
#447428=CARTESIAN_POINT('Ctrl Pts',(2.68943559532489,0.545020798509679,
12.5068768744332));
#447429=CARTESIAN_POINT('Ctrl Pts',(2.68957801777114,0.544298560208242,
12.5066032824114));
#447430=CARTESIAN_POINT('Ctrl Pts',(2.68969639348246,0.543527754388567,
12.5064197834844));
#447431=CARTESIAN_POINT('Ctrl Pts',(2.68978666695644,0.542751817215093,
12.5063282718343));
#447432=CARTESIAN_POINT('Ctrl Pts',(2.68991843828047,0.541619189165899,
12.5061946931565));
#447433=CARTESIAN_POINT('Ctrl Pts',(2.68999420380854,0.540451541931188,
12.5062515701262));
#447434=CARTESIAN_POINT('Ctrl Pts',(2.6900246934761,0.53932234310065,12.5064436508398));
#447435=CARTESIAN_POINT('',(2.62916808382621,0.499763384950601,12.5737548217797));
#447436=CARTESIAN_POINT('Origin',(2.64445078554345,0.502668385505106,12.5893111709658));
#447437=CARTESIAN_POINT('Ctrl Pts',(2.6900246934761,0.539322343100649,12.5064436508398));
#447438=CARTESIAN_POINT('Ctrl Pts',(2.68101659600168,0.533466186712491,
12.5164271754438));
#447439=CARTESIAN_POINT('Ctrl Pts',(2.67200481383978,0.527607884118116,
12.5264061185523));
#447440=CARTESIAN_POINT('Ctrl Pts',(2.66298921773467,0.521747358936393,
12.536380305637));
#447441=CARTESIAN_POINT('Ctrl Pts',(2.65172155116319,0.514422891101821,
12.5488460165097));
#447442=CARTESIAN_POINT('Ctrl Pts',(2.64044792389739,0.507094949458075,
12.5613043021964));
#447443=CARTESIAN_POINT('Ctrl Pts',(2.62916808382621,0.499763384950601,
12.5737548217797));
#447444=CARTESIAN_POINT('Ctrl Pts',(2.64401005104368,0.45869500919504,12.5893111709658));
#447445=CARTESIAN_POINT('Ctrl Pts',(2.63292791152546,0.461070891822268,
12.5770542771492));
#447446=CARTESIAN_POINT('Ctrl Pts',(2.63331499706306,0.477431021395151,
12.5737548217797));
#447447=CARTESIAN_POINT('Ctrl Pts',(2.63367051126054,0.460911687021908,
12.5928319619712));
#447448=CARTESIAN_POINT('Ctrl Pts',(2.62690553363688,0.465693788455673,
12.5821634970843));
#447449=CARTESIAN_POINT('Ctrl Pts',(2.62954657436679,0.478229274332287,
12.5773203894503));
#447450=CARTESIAN_POINT('Ctrl Pts',(2.620249319228,0.470934446310918,12.5969440695591));
#447451=CARTESIAN_POINT('Ctrl Pts',(2.61949747127797,0.474883277430624,
12.5878292599214));
#447452=CARTESIAN_POINT('Ctrl Pts',(2.62476421187078,0.481803229571837,
12.5813877129824));
#447453=CARTESIAN_POINT('Ctrl Pts',(2.61461022485556,0.501007288880253,
12.596957478804));
#447454=CARTESIAN_POINT('Ctrl Pts',(2.61535659519149,0.497087655674131,
12.5878468778671));
#447455=CARTESIAN_POINT('Ctrl Pts',(2.62275176475801,0.492567816183614,
12.5814011370086));
#447456=CARTESIAN_POINT('Ctrl Pts',(2.62355655588574,0.515300719827306,
12.5928371701607));
#447457=CARTESIAN_POINT('Ctrl Pts',(2.61896767895793,0.508410344348033,
12.5821692192951));
#447458=CARTESIAN_POINT('Ctrl Pts',(2.62592698210361,0.497658975984226,
12.5773318885715));
#447459=CARTESIAN_POINT('Ctrl Pts',(2.63242388933653,0.521089942649668,
12.5893111709658));
#447460=CARTESIAN_POINT('Ctrl Pts',(2.62293347207064,0.514893926616848,
12.5770542771492));
#447461=CARTESIAN_POINT('Ctrl Pts',(2.62916808382617,0.499763384950647,
12.5737548217797));
#447462=CARTESIAN_POINT('',(2.63331499706306,0.477431021395151,12.5737548217797));
#447463=CARTESIAN_POINT('Origin',(2.64862180375801,0.480206209461455,12.5893111709658));
#447464=CARTESIAN_POINT('Ctrl Pts',(2.62916808382617,0.499763384950647,
12.5737548217797));
#447465=CARTESIAN_POINT('Ctrl Pts',(2.62831151154022,0.499243189266367,
12.5746934679442));
#447466=CARTESIAN_POINT('Ctrl Pts',(2.6274587437979,0.498510985322169,12.5756680099006));
#447467=CARTESIAN_POINT('Ctrl Pts',(2.62670463205979,0.497652603615456,
12.5765688348656));
#447468=CARTESIAN_POINT('Ctrl Pts',(2.62650498932542,0.497425356561201,
12.5768073183026));
#447469=CARTESIAN_POINT('Ctrl Pts',(2.62631211503452,0.497189477697991,
12.5770407398754));
#447470=CARTESIAN_POINT('Ctrl Pts',(2.62612734303,0.496946927807763,12.5772674179684));
#447471=CARTESIAN_POINT('Ctrl Pts',(2.62536908868791,0.495951568646533,
12.5781976435658));
#447472=CARTESIAN_POINT('Ctrl Pts',(2.62471318760354,0.494780495954386,
12.5790594849312));
#447473=CARTESIAN_POINT('Ctrl Pts',(2.62424605831794,0.493489185397544,
12.5797571720116));
#447474=CARTESIAN_POINT('Ctrl Pts',(2.6239417067919,0.492647850138372,12.580211740231));
#447475=CARTESIAN_POINT('Ctrl Pts',(2.62372131080489,0.491710853559276,
12.5806009430798));
#447476=CARTESIAN_POINT('Ctrl Pts',(2.62361763131471,0.490740099611236,
12.5808812374708));
#447477=CARTESIAN_POINT('Ctrl Pts',(2.62352853623733,0.489905899925599,
12.5811221033394));
#447478=CARTESIAN_POINT('Ctrl Pts',(2.62352392005206,0.489029681663102,
12.581287365893));
#447479=CARTESIAN_POINT('Ctrl Pts',(2.62361238116939,0.488160856068305,
12.581359338449));
#447480=CARTESIAN_POINT('Ctrl Pts',(2.62362467543805,0.488040107251192,
12.5813693411482));
#447481=CARTESIAN_POINT('Ctrl Pts',(2.62363871337667,0.487919475653187,
12.5813775999465));
#447482=CARTESIAN_POINT('Ctrl Pts',(2.62365446307321,0.487799066738467,
12.5813841266931));
#447483=CARTESIAN_POINT('Ctrl Pts',(2.62368118433827,0.487594778451487,
12.5813952001081));
#447484=CARTESIAN_POINT('Ctrl Pts',(2.62371361563218,0.48738984190695,12.5814007534795));
#447485=CARTESIAN_POINT('Ctrl Pts',(2.62375193761589,0.48718437718635,12.5814005856065));
#447486=CARTESIAN_POINT('Ctrl Pts',(2.6239273606744,0.486243840026943,12.5813998171494));
#447487=CARTESIAN_POINT('Ctrl Pts',(2.62421376805465,0.485357157212617,
12.58127954464));
#447488=CARTESIAN_POINT('Ctrl Pts',(2.62458137680877,0.484520267786813,
12.5810700125799));
#447489=CARTESIAN_POINT('Ctrl Pts',(2.62502540632814,0.483509400647933,
12.5808169217085));
#447490=CARTESIAN_POINT('Ctrl Pts',(2.62560327081538,0.482577820810323,
12.5804173076348));
#447491=CARTESIAN_POINT('Ctrl Pts',(2.62624219676262,0.481793442711699,
12.5799304713245));
#447492=CARTESIAN_POINT('Ctrl Pts',(2.62703402729368,0.480821351142921,
12.5793271277669));
#447493=CARTESIAN_POINT('Ctrl Pts',(2.62794379502863,0.479994710061901,
12.5785808224116));
#447494=CARTESIAN_POINT('Ctrl Pts',(2.628911822381,0.479324890005427,12.5777485681082));
#447495=CARTESIAN_POINT('Ctrl Pts',(2.63035428919136,0.478326784737014,
12.576508418016));
#447496=CARTESIAN_POINT('Ctrl Pts',(2.63191006095418,0.477679641991726,
12.5750928681475));
#447497=CARTESIAN_POINT('Ctrl Pts',(2.63331499706306,0.477431021395151,
12.5737548217797));
#447498=CARTESIAN_POINT('Ctrl Pts',(2.63331499706306,0.477431021395151,
12.5737548217797));
#447499=CARTESIAN_POINT('Ctrl Pts',(2.63292791152546,0.461070891822268,
12.5770542771492));
#447500=CARTESIAN_POINT('Ctrl Pts',(2.64401005104368,0.45869500919504,12.5893111709658));
#447501=CARTESIAN_POINT('Ctrl Pts',(2.6575345507421,0.472290187439575,12.5508408821982));
#447502=CARTESIAN_POINT('Ctrl Pts',(2.6571430527915,0.455879445409314,12.55409748406));
#447503=CARTESIAN_POINT('Ctrl Pts',(2.66823933028148,0.453500531764334,
12.5663972313419));
#447504=CARTESIAN_POINT('Ctrl Pts',(2.6817302000617,0.467153221623685,12.52790050457));
#447505=CARTESIAN_POINT('Ctrl Pts',(2.6813118162984,0.450697941851895,12.5311362602938));
#447506=CARTESIAN_POINT('Ctrl Pts',(2.69244416615794,0.448311294707787,
12.5434568539655));
#447507=CARTESIAN_POINT('Ctrl Pts',(2.70590379982209,0.462019809797098,
12.5049357605811));
#447508=CARTESIAN_POINT('Ctrl Pts',(2.70543903669039,0.445525344658126,
12.5081700652078));
#447509=CARTESIAN_POINT('Ctrl Pts',(2.71662647308205,0.443126887598238,
12.5204921097672));
#447510=CARTESIAN_POINT('Ctrl Pts',(2.70431646617453,0.462356888187479,
12.5064436508395));
#447511=CARTESIAN_POINT('Ctrl Pts',(2.70472361691589,0.461206637751966,
12.5062361689309));
#447512=CARTESIAN_POINT('Ctrl Pts',(2.70509797113518,0.45999310961511,12.5061871075061));
#447513=CARTESIAN_POINT('Ctrl Pts',(2.70539373083916,0.458799986470328,
12.5063648335164));
#447514=CARTESIAN_POINT('Ctrl Pts',(2.70552808313993,0.458257996343081,
12.5064455676329));
#447515=CARTESIAN_POINT('Ctrl Pts',(2.70564787726643,0.45771260421724,12.506574497099));
#447516=CARTESIAN_POINT('Ctrl Pts',(2.70574695032627,0.45718696940744,12.5067492519495));
#447517=CARTESIAN_POINT('Ctrl Pts',(2.70594604148572,0.456130685853542,
12.5071004286051));
#447518=CARTESIAN_POINT('Ctrl Pts',(2.70606798154703,0.455115201735787,
12.5076537929612));
#447519=CARTESIAN_POINT('Ctrl Pts',(2.70611300925277,0.454217862139002,
12.5083435010503));
#447520=CARTESIAN_POINT('Ctrl Pts',(2.70611584401593,0.454161369248753,
12.5083869222963));
#447521=CARTESIAN_POINT('Ctrl Pts',(2.70611836232971,0.454105337860168,
12.5084308732336));
#447522=CARTESIAN_POINT('Ctrl Pts',(2.70612055972475,0.454049784178728,
12.5084753333615));
#447523=CARTESIAN_POINT('Ctrl Pts',(2.70613818573322,0.453604170330105,
12.508831962269));
#447524=CARTESIAN_POINT('Ctrl Pts',(2.70613681023768,0.453180297204131,
12.509227847131));
#447525=CARTESIAN_POINT('Ctrl Pts',(2.70611927417718,0.452790759671851,
12.5096423454524));
#447526=CARTESIAN_POINT('Ctrl Pts',(2.70606432392469,0.451570121447775,
12.5109411997424));
#447527=CARTESIAN_POINT('Ctrl Pts',(2.70585696918569,0.450611118787778,
12.5124831113042));
#447528=CARTESIAN_POINT('Ctrl Pts',(2.70557387751056,0.449858272469493,
12.5140723025008));
#447529=CARTESIAN_POINT('Ctrl Pts',(2.70554735151054,0.449787729944901,
12.5142212114565));
#447530=CARTESIAN_POINT('Ctrl Pts',(2.70552017690124,0.449718972769453,
12.5143705582413));
#447531=CARTESIAN_POINT('Ctrl Pts',(2.70549242738584,0.449651942056966,
12.5145201959299));
#447532=CARTESIAN_POINT('Ctrl Pts',(2.70513594354584,0.448790832756771,
12.5164425148273));
#447533=CARTESIAN_POINT('Ctrl Pts',(2.70468228886246,0.448181033439291,
12.518463520594));
#447534=CARTESIAN_POINT('Ctrl Pts',(2.70416638171473,0.447739365469311,
12.5205025929157));
#447535=CARTESIAN_POINT('Ctrl Pts',(2.70386713512039,0.447483180540639,
12.5216853356836));
#447536=CARTESIAN_POINT('Ctrl Pts',(2.70354779896811,0.44728365816998,12.5228750347131));
#447537=CARTESIAN_POINT('Ctrl Pts',(2.70322050746143,0.447127171371152,
12.5240609649613));
#447538=CARTESIAN_POINT('Ctrl Pts',(2.70241718801687,0.446743082918657,
12.5269717671326));
#447539=CARTESIAN_POINT('Ctrl Pts',(2.70153885014343,0.44661682299529,12.5299036066169));
#447540=CARTESIAN_POINT('Ctrl Pts',(2.70061145499055,0.44666571426832,12.5328133004019));
#447541=CARTESIAN_POINT('Ctrl Pts',(2.70016625131657,0.446689184926227,
12.5342101228451));
#447542=CARTESIAN_POINT('Ctrl Pts',(2.69971032518094,0.446753514278087,
12.5356023438238));
#447543=CARTESIAN_POINT('Ctrl Pts',(2.69924879928632,0.446852460011852,
12.5369868989719));
#447544=CARTESIAN_POINT('Origin',(15.1599677223619,-2.22999831842861,-1.23969099894504));
#447545=CARTESIAN_POINT('Ctrl Pts',(2.67969370547127,0.551951071342014,
12.5369868989719));
#447546=CARTESIAN_POINT('Ctrl Pts',(2.6925535803633,0.560312107249547,12.5369868989719));
#447547=CARTESIAN_POINT('Ctrl Pts',(2.68915504197755,0.575269822333287,
12.5369868989719));
#447548=CARTESIAN_POINT('Ctrl Pts',(2.68404081004032,0.554777483987707,
12.5218025310016));
#447549=CARTESIAN_POINT('Ctrl Pts',(2.69174247415498,0.563740755353107,
12.5216901060418));
#447550=CARTESIAN_POINT('Ctrl Pts',(2.68916541793071,0.575224229914571,
12.5161920673678));
#447551=CARTESIAN_POINT('Ctrl Pts',(2.68965758922266,0.552589365432291,
12.5042015548894));
#447552=CARTESIAN_POINT('Ctrl Pts',(2.69287020238977,0.558162197894824,
12.4980677368513));
#447553=CARTESIAN_POINT('Ctrl Pts',(2.69148483540545,0.564815883944122,
12.4907278922777));
#447554=CARTESIAN_POINT('Ctrl Pts',(2.69000508265219,0.539318411321086,
12.506463626192));
#447555=CARTESIAN_POINT('Ctrl Pts',(2.69642016155051,0.540604568801698,
12.4999376786891));
#447556=CARTESIAN_POINT('Ctrl Pts',(2.69634181068928,0.540588860258143,
12.4906970594712));
#447557=CARTESIAN_POINT('Origin',(2.66770182711108,0.570395443204302,12.5369868989719));
#447558=CARTESIAN_POINT('Origin',(2.66770182711108,0.570395443204303,14.));
#447559=CARTESIAN_POINT('Origin',(2.66770182711108,0.570395443204303,13.7435492065112));
#447560=CARTESIAN_POINT('Ctrl Pts',(2.65899599618871,0.538438126949952,
13.793642941384));
#447561=CARTESIAN_POINT('Ctrl Pts',(2.66806447328623,0.544326160759092,
13.8071662555867));
#447562=CARTESIAN_POINT('Ctrl Pts',(2.66099130849232,0.559817762465603,
13.8103758687955));
#447563=CARTESIAN_POINT('Ctrl Pts',(2.67291358661161,0.547524511381774,
13.7804579775006));
#447564=CARTESIAN_POINT('Ctrl Pts',(2.68409774534096,0.554798318173647,
13.7901904343351));
#447565=CARTESIAN_POINT('Ctrl Pts',(2.67995883734142,0.570001125964826,
13.7927914348263));
#447566=CARTESIAN_POINT('Ctrl Pts',(2.68110739585066,0.552874007887763,
13.7597120340895));
#447567=CARTESIAN_POINT('Ctrl Pts',(2.6940474929302,0.56129665459444,13.7635825532445));
#447568=CARTESIAN_POINT('Ctrl Pts',(2.69113187582353,0.576028765544045,
13.7651073818884));
#447569=CARTESIAN_POINT('Ctrl Pts',(2.6795028603843,0.551826453983024,13.7381884353898));
#447570=CARTESIAN_POINT('Ctrl Pts',(2.6921405607098,0.560051199639204,13.7368803041982));
#447571=CARTESIAN_POINT('Ctrl Pts',(2.68894362822502,0.574848809574822,
13.7363986145813));
#447572=CARTESIAN_POINT('Origin',(2.6503461928975,0.559064456922638,13.7902182540695));
#447573=CARTESIAN_POINT('Ctrl Pts',(2.63242059297149,0.521087791455569,
13.8235227101244));
#447574=CARTESIAN_POINT('Ctrl Pts',(2.64205001535561,0.527369265237085,
13.8358800583119));
#447575=CARTESIAN_POINT('Ctrl Pts',(2.6356337482334,0.54264858345725,13.8390832900376));
#447576=CARTESIAN_POINT('Ctrl Pts',(2.64240807409376,0.527608325952603,
13.8124254819052));
#447577=CARTESIAN_POINT('Ctrl Pts',(2.65205619652767,0.533901998500128,
13.8247886449158));
#447578=CARTESIAN_POINT('Ctrl Pts',(2.64561610727068,0.549194023593774,
13.8279860620657));
#447579=CARTESIAN_POINT('Ctrl Pts',(2.65239107915191,0.534125938158196,
13.8013225099955));
#447580=CARTESIAN_POINT('Ctrl Pts',(2.6620533503664,0.540428838189978,13.8136962257787));
#447581=CARTESIAN_POINT('Ctrl Pts',(2.65559399359633,0.555736206840366,
13.8168830918626));
#447582=CARTESIAN_POINT('Ctrl Pts',(2.66236978230273,0.540640741774223,
13.7902140179785));
#447583=CARTESIAN_POINT('Ctrl Pts',(2.67204194848582,0.546950092206022,
13.802602731458));
#447584=CARTESIAN_POINT('Ctrl Pts',(2.66556758396314,0.562275259629211,
13.8057746032558));
#447585=CARTESIAN_POINT('Origin',(2.62039699312968,0.539511499794142,13.8235269408515));
#447586=CARTESIAN_POINT('Ctrl Pts',(2.64401005104368,0.45869500919504,13.8235269408515));
#447587=CARTESIAN_POINT('Ctrl Pts',(2.6555551918918,0.456219864433972,13.8362179249168));
#447588=CARTESIAN_POINT('Ctrl Pts',(2.65472321565854,0.439161997638721,
13.8391868794938));
#447589=CARTESIAN_POINT('Ctrl Pts',(2.63344674969771,0.460959658914779,
13.8400110824519));
#447590=CARTESIAN_POINT('Ctrl Pts',(2.64198600108674,0.455630207857054,
13.8494522556837));
#447591=CARTESIAN_POINT('Ctrl Pts',(2.63736255658733,0.4429988323026,13.85569149686));
#447592=CARTESIAN_POINT('Ctrl Pts',(2.62031150822566,0.470596212111629,
13.8586819406588));
#447593=CARTESIAN_POINT('Ctrl Pts',(2.62112006089859,0.46631809497788,13.868010383617));
#447594=CARTESIAN_POINT('Ctrl Pts',(2.61564415722987,0.4591134197039,13.8744918421245));
#447595=CARTESIAN_POINT('Ctrl Pts',(2.61454705303784,0.501350765503517,
13.8587686893867));
#447596=CARTESIAN_POINT('Ctrl Pts',(2.6137456411473,0.505590796977642,13.8680909899357));
#447597=CARTESIAN_POINT('Ctrl Pts',(2.60605056105728,0.51031119356202,13.8745789365163));
#447598=CARTESIAN_POINT('Ctrl Pts',(2.62336306961101,0.515174398301808,
13.8400379222776));
#447599=CARTESIAN_POINT('Ctrl Pts',(2.62941251526406,0.523216440405561,
13.8494748685453));
#447600=CARTESIAN_POINT('Ctrl Pts',(2.62056751556218,0.533342006342256,
13.8557104837033));
#447601=CARTESIAN_POINT('Ctrl Pts',(2.63242388933283,0.521089942655079,
13.8235269408542));
#447602=CARTESIAN_POINT('Ctrl Pts',(2.64231080727512,0.527544822390061,
13.8362179249195));
#447603=CARTESIAN_POINT('Ctrl Pts',(2.63541047323881,0.543166870727066,
13.8391868794965));
#447604=CARTESIAN_POINT('Origin',(2.63939829832935,0.437183808928625,13.8235269408515));
#447605=CARTESIAN_POINT('Ctrl Pts',(2.67897844191641,0.451198189573393,
13.7902140241682));
#447606=CARTESIAN_POINT('Ctrl Pts',(2.69027089583447,0.448781770755981,
13.8026027327198));
#447607=CARTESIAN_POINT('Ctrl Pts',(2.68972991167073,0.432153924581312,
13.8057746032556));
#447608=CARTESIAN_POINT('Ctrl Pts',(2.66732612174214,0.453696312344323,
13.8013225161807));
#447609=CARTESIAN_POINT('Ctrl Pts',(2.67860702462015,0.45128236161113,13.8136962270464));
#447610=CARTESIAN_POINT('Ctrl Pts',(2.67807365792942,0.434676515493367,
13.8168830918628));
#447611=CARTESIAN_POINT('Ctrl Pts',(2.65566877814783,0.456195512078463,
13.8124254880875));
#447612=CARTESIAN_POINT('Ctrl Pts',(2.66693316277136,0.453785094252894,
13.8247886461868));
#447613=CARTESIAN_POINT('Ctrl Pts',(2.66641227077088,0.437200485914964,
13.8279860620656));
#447614=CARTESIAN_POINT('Ctrl Pts',(2.64400620776571,0.458695832375514,
13.8235227163065));
#447615=CARTESIAN_POINT('Ctrl Pts',(2.65524875957551,0.456290086744523,
13.8358800595847));
#447616=CARTESIAN_POINT('Ctrl Pts',(2.65474553983445,0.439725890395448,
13.8390832900376));
#447617=CARTESIAN_POINT('Origin',(2.67437054464763,0.429686163521245,13.7902182540695));
#447618=CARTESIAN_POINT('Ctrl Pts',(2.69898492939505,0.446909002455508,
13.7382347919292));
#447619=CARTESIAN_POINT('Ctrl Pts',(2.71374498611075,0.443769162573877,
13.7369371795943));
#447620=CARTESIAN_POINT('Ctrl Pts',(2.71606716391856,0.428797480395553,
13.7364597369711));
#447621=CARTESIAN_POINT('Ctrl Pts',(2.70083446112151,0.446512484641241,
13.7595490285573));
#447622=CARTESIAN_POINT('Ctrl Pts',(2.71594647093971,0.443296747451537,
13.7633824266926));
#447623=CARTESIAN_POINT('Ctrl Pts',(2.71850298030877,0.428486010800249,
13.7648920890506));
#447624=CARTESIAN_POINT('Ctrl Pts',(2.69140195064382,0.448534703778785,
13.7803806590111));
#447625=CARTESIAN_POINT('Ctrl Pts',(2.70447442184469,0.445758486441053,
13.7901039518744));
#447626=CARTESIAN_POINT('Ctrl Pts',(2.70608539327615,0.430077599588828,
13.7926933640892));
#447627=CARTESIAN_POINT('Ctrl Pts',(2.67500614181622,0.452049771980561,
13.7936647693663));
#447628=CARTESIAN_POINT('Ctrl Pts',(2.68558750660803,0.449811904449398,
13.8072068914933));
#447629=CARTESIAN_POINT('Ctrl Pts',(2.68453573459646,0.432796086940902,
13.8104111085397));
#447630=CARTESIAN_POINT('Origin',(2.69463704657198,0.425341259745436,13.7435492065112));
#447631=CARTESIAN_POINT('Origin',(2.69463704657198,0.425341259745436,14.));
#447632=CARTESIAN_POINT('Origin',(2.69463704657198,0.425341259745437,12.5369868989719));
#447633=CARTESIAN_POINT('Ctrl Pts',(2.70429834586343,0.462353790169003,
12.506462012331));
#447634=CARTESIAN_POINT('Ctrl Pts',(2.71074344959975,0.463455709321185,
12.4999388158272));
#447635=CARTESIAN_POINT('Ctrl Pts',(2.71066719557032,0.463442672172536,
12.4907030323752));
#447636=CARTESIAN_POINT('Ctrl Pts',(2.70873630098556,0.449842469795504,
12.5042014951932));
#447637=CARTESIAN_POINT('Ctrl Pts',(2.71373382299294,0.445796994433825,
12.4980716682127));
#447638=CARTESIAN_POINT('Ctrl Pts',(2.71483027555077,0.43909450556667,12.4907355092743));
#447639=CARTESIAN_POINT('Ctrl Pts',(2.70428171392088,0.445782623083065,
12.5218047446509));
#447640=CARTESIAN_POINT('Ctrl Pts',(2.71468215884852,0.440183550280961,
12.5216906929434));
#447641=CARTESIAN_POINT('Ctrl Pts',(2.71640231170236,0.428546891461126,
12.5161988840776));
#447642=CARTESIAN_POINT('Ctrl Pts',(2.69921122967856,0.446860480198498,
12.5369868989719));
#447643=CARTESIAN_POINT('Ctrl Pts',(2.71420610628378,0.443673129085926,
12.5369868989719));
#447644=CARTESIAN_POINT('Ctrl Pts',(2.7164087662027,0.428502307723778,12.5369868989719));
#447645=CARTESIAN_POINT('Origin',(5.06527468391092E-31,-4.21128796913916E-31,
12.5));
#447646=CARTESIAN_POINT('Origin',(2.59782442414821,0.672680104343423,12.5));
#447647=CARTESIAN_POINT('',(2.59782442414821,0.672680104343423,12.5893111709658));
#447648=CARTESIAN_POINT('',(2.59782442414821,0.672680104343423,13.8235269408515));
#447649=CARTESIAN_POINT('',(2.59782442414821,0.672680104343423,12.5));
#447650=CARTESIAN_POINT('',(2.63329143090732,0.668057969474058,13.7902182540695));
#447651=CARTESIAN_POINT('',(2.59782442414821,0.672680104343423,13.8235269408515));
#447652=CARTESIAN_POINT('',(2.65384464771224,0.665379431058994,13.7435492065112));
#447653=CARTESIAN_POINT('Origin',(2.58622487819144,0.674192110063431,13.7445212918691));
#447654=CARTESIAN_POINT('',(2.65384464771224,0.665379431058994,12.5369868989719));
#447655=CARTESIAN_POINT('',(2.65384464771224,0.665379431058994,12.5));
#447656=CARTESIAN_POINT('Ctrl Pts',(2.65384464771224,0.665379431058994,
12.5369868989719));
#447657=CARTESIAN_POINT('Ctrl Pts',(2.63518485910551,0.667811213931451,
12.5544431401645));
#447658=CARTESIAN_POINT('Ctrl Pts',(2.61651172452202,0.670244736079652,
12.5718848856037));
#447659=CARTESIAN_POINT('Ctrl Pts',(2.59782442414821,0.672680104343423,
12.5893111709658));
#447660=CARTESIAN_POINT('Origin',(2.79844051361145,0.90252811439659,12.5));
#447661=CARTESIAN_POINT('',(2.62582115106376,0.768560006826695,13.7435492065112));
#447662=CARTESIAN_POINT('',(2.60944684686499,0.755852078156887,13.7902182540695));
#447663=CARTESIAN_POINT('Origin',(2.56641800548108,0.722457837985626,13.7418732680453));
#447664=CARTESIAN_POINT('',(2.58119104811553,0.733923044064349,13.8235269408515));
#447665=CARTESIAN_POINT('',(2.60944684686499,0.755852078156887,13.7902182540695));
#447666=CARTESIAN_POINT('',(2.58119104811553,0.733923044064349,12.5893111709658));
#447667=CARTESIAN_POINT('',(2.58119104811553,0.733923044064349,12.5));
#447668=CARTESIAN_POINT('',(2.62582115106376,0.768560006826695,12.5369868989719));
#447669=CARTESIAN_POINT('Ctrl Pts',(2.58119104811553,0.733923044064349,
12.5893111709658));
#447670=CARTESIAN_POINT('Ctrl Pts',(2.59607881696841,0.745477287978364,
12.5718848856037));
#447671=CARTESIAN_POINT('Ctrl Pts',(2.61095530024189,0.75702277327057,12.5544431401645));
#447672=CARTESIAN_POINT('Ctrl Pts',(2.62582115106376,0.768560006826695,
12.5369868989719));
#447673=CARTESIAN_POINT('',(2.62582115106376,0.768560006826695,12.5));
#447674=CARTESIAN_POINT('Origin',(2.60226668190706,0.70676686087736,12.5));
#447675=CARTESIAN_POINT('',(2.56940516467475,0.69668168079129,13.8587068136939));
#447676=CARTESIAN_POINT('Ctrl Pts',(2.58119104811137,0.733923044069481,
13.8235269408542));
#447677=CARTESIAN_POINT('Ctrl Pts',(2.57980673583883,0.732848693586994,
13.8262006681044));
#447678=CARTESIAN_POINT('Ctrl Pts',(2.57849661569527,0.731611999105121,
13.8288634856214));
#447679=CARTESIAN_POINT('Ctrl Pts',(2.57725650689879,0.73022562265809,13.8314912288862));
#447680=CARTESIAN_POINT('Ctrl Pts',(2.5759780826409,0.728796411539299,13.8342001611531));
#447681=CARTESIAN_POINT('Ctrl Pts',(2.57477227246862,0.727206869931805,
13.8368750301949));
#447682=CARTESIAN_POINT('Ctrl Pts',(2.573651705902,0.725429073630892,13.8394886372969));
#447683=CARTESIAN_POINT('Ctrl Pts',(2.57356516182794,0.725291770110243,
13.8396904925131));
#447684=CARTESIAN_POINT('Ctrl Pts',(2.57347914264093,0.725153328817326,
13.8398919674349));
#447685=CARTESIAN_POINT('Ctrl Pts',(2.57339366328585,0.725013729983829,
13.8400930404591));
#447686=CARTESIAN_POINT('Ctrl Pts',(2.57206183742609,0.722838686240423,
13.8432258934518));
#447687=CARTESIAN_POINT('Ctrl Pts',(2.57086689571031,0.720394327187652,
13.8462331177034));
#447688=CARTESIAN_POINT('Ctrl Pts',(2.56993447561436,0.717718007930113,
13.8489036603661));
#447689=CARTESIAN_POINT('Ctrl Pts',(2.56962937690785,0.716842285123152,
13.849777493004));
#447690=CARTESIAN_POINT('Ctrl Pts',(2.56935258380642,0.715941879350438,
13.85061494757));
#447691=CARTESIAN_POINT('Ctrl Pts',(2.56910905624937,0.71501854406218,13.8514076489583));
#447692=CARTESIAN_POINT('Ctrl Pts',(2.56859396034427,0.713065556762635,
13.8530843267192));
#447693=CARTESIAN_POINT('Ctrl Pts',(2.56817995315849,0.710817397480646,
13.8546805203176));
#447694=CARTESIAN_POINT('Ctrl Pts',(2.56802525284017,0.708379837091844,
13.8559412814273));
#447695=CARTESIAN_POINT('Ctrl Pts',(2.56800454892053,0.708053612459863,
13.8561100121513));
#447696=CARTESIAN_POINT('Ctrl Pts',(2.56798843423225,0.707724048824368,
13.8562727473908));
#447697=CARTESIAN_POINT('Ctrl Pts',(2.5679772273273,0.707391445193895,13.8564289040185));
#447698=CARTESIAN_POINT('Ctrl Pts',(2.5679264041412,0.705883091524182,13.8571370725437));
#447699=CARTESIAN_POINT('Ctrl Pts',(2.5679778968314,0.704285627645851,13.8577210840553));
#447700=CARTESIAN_POINT('Ctrl Pts',(2.56815903667544,0.702662092778626,
13.8581177131616));
#447701=CARTESIAN_POINT('Ctrl Pts',(2.56821005189016,0.702204849479646,
13.8582294175695));
#447702=CARTESIAN_POINT('Ctrl Pts',(2.5682711734966,0.701745553554236,13.8583265086086));
#447703=CARTESIAN_POINT('Ctrl Pts',(2.56834257260757,0.701285624802972,
13.8584082369006));
#447704=CARTESIAN_POINT('Ctrl Pts',(2.56844515398361,0.700624830522173,
13.8585256585398));
#447705=CARTESIAN_POINT('Ctrl Pts',(2.56857054501354,0.699954564335941,
13.8586122832068));
#447706=CARTESIAN_POINT('Ctrl Pts',(2.5687162646227,0.699292383029854,13.8586682984299));
#447707=CARTESIAN_POINT('Ctrl Pts',(2.56883282586531,0.698762703624906,
13.8587131050557));
#447708=CARTESIAN_POINT('Ctrl Pts',(2.56896345259151,0.698232296553719,
13.8587357943552));
#447709=CARTESIAN_POINT('Ctrl Pts',(2.56910865207591,0.69770121989644,13.8587355499465));
#447710=CARTESIAN_POINT('Ctrl Pts',(2.56920249796439,0.697357972391407,
13.8587353919793));
#447711=CARTESIAN_POINT('Ctrl Pts',(2.56930137925673,0.697018146810693,
13.8587257282814));
#447712=CARTESIAN_POINT('Ctrl Pts',(2.56940516467475,0.69668168079129,13.8587068136939));
#447713=CARTESIAN_POINT('Ctrl Pts',(2.56940516467475,0.69668168079129,13.8587068136939));
#447714=CARTESIAN_POINT('Ctrl Pts',(2.56974650925671,0.695575062396045,
13.8586446046466));
#447715=CARTESIAN_POINT('Ctrl Pts',(2.57014083738664,0.694504739382945,
13.858482427929));
#447716=CARTESIAN_POINT('Ctrl Pts',(2.57058406984971,0.693468882554442,
13.8582284286032));
#447717=CARTESIAN_POINT('Ctrl Pts',(2.5710387747979,0.692406213944235,13.8579678548414));
#447718=CARTESIAN_POINT('Ctrl Pts',(2.5715474673676,0.691377825557677,13.857615680862));
#447719=CARTESIAN_POINT('Ctrl Pts',(2.57208140752236,0.690419964702098,
13.8571944833187));
#447720=CARTESIAN_POINT('Ctrl Pts',(2.57341390978546,0.688029524975056,
13.8561433417727));
#447721=CARTESIAN_POINT('Ctrl Pts',(2.57496179646164,0.685964180731319,
13.8546163505475));
#447722=CARTESIAN_POINT('Ctrl Pts',(2.57651885142229,0.684239188934588,
13.8528973491087));
#447723=CARTESIAN_POINT('Ctrl Pts',(2.57680330239142,0.683924058383181,
13.8525833129073));
#447724=CARTESIAN_POINT('Ctrl Pts',(2.57708801004023,0.683620154271979,
13.8522628768812));
#447725=CARTESIAN_POINT('Ctrl Pts',(2.5773716816524,0.683327394353899,13.851937733538));
#447726=CARTESIAN_POINT('Ctrl Pts',(2.57910402483015,0.681539550152906,
13.8499521282529));
#447727=CARTESIAN_POINT('Ctrl Pts',(2.58097282149759,0.679992474613509,
13.847639871647));
#447728=CARTESIAN_POINT('Ctrl Pts',(2.58282862244085,0.678705590183642,
13.8452109780794));
#447729=CARTESIAN_POINT('Ctrl Pts',(2.58366358569838,0.678126594241463,
13.8441181685877));
#447730=CARTESIAN_POINT('Ctrl Pts',(2.58449573846324,0.67759957354068,13.8430021611332));
#447731=CARTESIAN_POINT('Ctrl Pts',(2.58531167264054,0.677122994520366,
13.8418824960098));
#447732=CARTESIAN_POINT('Ctrl Pts',(2.58723444236496,0.675999923889115,
13.8392439765549));
#447733=CARTESIAN_POINT('Ctrl Pts',(2.58915715575003,0.675100013115308,
13.8364981347964));
#447734=CARTESIAN_POINT('Ctrl Pts',(2.59107039127242,0.674389888570763,
13.8336931113419));
#447735=CARTESIAN_POINT('Ctrl Pts',(2.59293376116954,0.673698272361454,
13.8309611966328));
#447736=CARTESIAN_POINT('Ctrl Pts',(2.59479020447205,0.673186514409347,
13.8281701127186));
#447737=CARTESIAN_POINT('Ctrl Pts',(2.59663035114141,0.672863077529967,
13.8253580685121));
#447738=CARTESIAN_POINT('Ctrl Pts',(2.59702929692528,0.672792956065454,
13.8247484142933));
#447739=CARTESIAN_POINT('Ctrl Pts',(2.59742740652207,0.672731844514956,
13.8241378483365));
#447740=CARTESIAN_POINT('Ctrl Pts',(2.59782442414821,0.672680104343423,
13.8235269408515));
#447741=CARTESIAN_POINT('',(2.56906221652971,0.697875482880214,12.5969504640361));
#447742=CARTESIAN_POINT('Origin',(2.60229866198257,0.706775343658747,12.584524458991));
#447743=CARTESIAN_POINT('Origin',(2.60229866198257,0.706775343658747,12.584524458991));
#447744=CARTESIAN_POINT('Ctrl Pts',(2.58119104811553,0.733923044064349,
12.5893111709658));
#447745=CARTESIAN_POINT('Ctrl Pts',(2.57223724225787,0.726974087651837,
12.5770542771492));
#447746=CARTESIAN_POINT('Ctrl Pts',(2.579684388468,0.712402070352234,12.5737548217797));
#447747=CARTESIAN_POINT('Ctrl Pts',(2.60077001653969,0.749118079599428,
12.5663937883685));
#447748=CARTESIAN_POINT('Ctrl Pts',(2.59180478885918,0.742160258827957,
12.5540940315304));
#447749=CARTESIAN_POINT('Ctrl Pts',(2.59927787167869,0.727544547128353,
12.5508374392248));
#447750=CARTESIAN_POINT('Ctrl Pts',(2.62032923002471,0.76429778352992,12.5434499600945));
#447751=CARTESIAN_POINT('Ctrl Pts',(2.6113348531964,0.757317340405427,12.5311293540533));
#447752=CARTESIAN_POINT('Ctrl Pts',(2.61885149015097,0.742673162946224,
12.5278936106989));
#447753=CARTESIAN_POINT('Ctrl Pts',(2.63987023600205,0.779463356801421,
12.5204817579905));
#447754=CARTESIAN_POINT('Ctrl Pts',(2.63083134315524,0.772448365253878,
12.5081597038247));
#447755=CARTESIAN_POINT('Ctrl Pts',(2.6384067793781,0.757789006095711,12.5049254088044));
#447756=CARTESIAN_POINT('Ctrl Pts',(2.62582115106376,0.768560006826693,
12.5369868989719));
#447757=CARTESIAN_POINT('Ctrl Pts',(2.62655703813531,0.769131120990989,
12.5342545179733));
#447758=CARTESIAN_POINT('Ctrl Pts',(2.62733581815076,0.769577617128592,
12.5314872231885));
#447759=CARTESIAN_POINT('Ctrl Pts',(2.62814142522858,0.769825847558425,
12.5287124745063));
#447760=CARTESIAN_POINT('Ctrl Pts',(2.62886796167813,0.770049714081107,
12.5262100684184));
#447761=CARTESIAN_POINT('Ctrl Pts',(2.62961587403641,0.770111158706971,
12.5237004536639));
#447762=CARTESIAN_POINT('Ctrl Pts',(2.63040343216518,0.769945168450488,
12.5212220730815));
#447763=CARTESIAN_POINT('Ctrl Pts',(2.63100637604196,0.769818088549847,
12.5193246583486));
#447764=CARTESIAN_POINT('Ctrl Pts',(2.6316396323685,0.769555564173845,12.517417831369));
#447765=CARTESIAN_POINT('Ctrl Pts',(2.63228442007479,0.769062194619328,
12.5155812248347));
#447766=CARTESIAN_POINT('Ctrl Pts',(2.63255910310341,0.768852016537232,
12.5147988205793));
#447767=CARTESIAN_POINT('Ctrl Pts',(2.63283632603725,0.768599951185227,
12.5140295443047));
#447768=CARTESIAN_POINT('Ctrl Pts',(2.63311665696456,0.76829928970777,12.5132817086137));
#447769=CARTESIAN_POINT('Ctrl Pts',(2.63354089990074,0.767844279234201,
12.5121499604604));
#447770=CARTESIAN_POINT('Ctrl Pts',(2.63397619142954,0.767263267700918,
12.5110494206568));
#447771=CARTESIAN_POINT('Ctrl Pts',(2.63440149722945,0.766525523104014,
12.5100666561695));
#447772=CARTESIAN_POINT('Ctrl Pts',(2.63464570684037,0.766101911855346,
12.5095023550641));
#447773=CARTESIAN_POINT('Ctrl Pts',(2.63488888024053,0.765621404797231,
12.5089719619137));
#447774=CARTESIAN_POINT('Ctrl Pts',(2.63512076064498,0.765090124489872,
12.5085043804652));
#447775=CARTESIAN_POINT('Ctrl Pts',(2.63546008741233,0.76431266496418,12.5078201359221));
#447776=CARTESIAN_POINT('Ctrl Pts',(2.63578396543699,0.763403444948041,
12.5072563000949));
#447777=CARTESIAN_POINT('Ctrl Pts',(2.6360624654395,0.762421255284591,12.5068768744332));
#447778=CARTESIAN_POINT('Ctrl Pts',(2.63626328311331,0.761713028923076,
12.5066032824114));
#447779=CARTESIAN_POINT('Ctrl Pts',(2.63644409276933,0.760954436615598,
12.5064197834844));
#447780=CARTESIAN_POINT('Ctrl Pts',(2.63659731194885,0.760188439435245,
12.5063282718343));
#447781=CARTESIAN_POINT('Ctrl Pts',(2.63682096451549,0.759070320698664,
12.5061946931565));
#447782=CARTESIAN_POINT('Ctrl Pts',(2.63699165202955,0.757912734307713,
12.5062515701262));
#447783=CARTESIAN_POINT('Ctrl Pts',(2.63711408043292,0.756789777984089,
12.5064436508398));
#447784=CARTESIAN_POINT('',(2.579684388468,0.712402070352234,12.5737548217797));
#447785=CARTESIAN_POINT('Origin',(2.59467945374211,0.716543086824676,12.5893111709658));
#447786=CARTESIAN_POINT('Ctrl Pts',(2.63711408043292,0.75678977798409,12.5064436508398));
#447787=CARTESIAN_POINT('Ctrl Pts',(2.62861328777127,0.750218863901955,
12.5164271754438));
#447788=CARTESIAN_POINT('Ctrl Pts',(2.62010899761836,0.743645510418688,
12.5264061185523));
#447789=CARTESIAN_POINT('Ctrl Pts',(2.61160108737432,0.73706963087177,12.536380305637));
#447790=CARTESIAN_POINT('Ctrl Pts',(2.60096792515941,0.728851115170202,
12.5488460165097));
#447791=CARTESIAN_POINT('Ctrl Pts',(2.59032910523158,0.720628651366349,
12.5613043021964));
#447792=CARTESIAN_POINT('Ctrl Pts',(2.579684388468,0.712402070352235,12.5737548217797));
#447793=CARTESIAN_POINT('Ctrl Pts',(2.59782442414821,0.672680104343423,
12.5893111709658));
#447794=CARTESIAN_POINT('Ctrl Pts',(2.58658550304428,0.674144784164906,
12.5770542771492));
#447795=CARTESIAN_POINT('Ctrl Pts',(2.58563779814647,0.690482027821093,
12.5737548217797));
#447796=CARTESIAN_POINT('Ctrl Pts',(2.58733860850922,0.674046637877755,
12.5928319619712));
#447797=CARTESIAN_POINT('Ctrl Pts',(2.58020635512882,0.678261418784176,
12.5821634970842));
#447798=CARTESIAN_POINT('Ctrl Pts',(2.58181684954086,0.690970463203354,
12.5773203894503));
#447799=CARTESIAN_POINT('Ctrl Pts',(2.57314512645719,0.68294209551513,12.5969440695591));
#447800=CARTESIAN_POINT('Ctrl Pts',(2.57207391382378,0.686816504637298,
12.5878292599214));
#447801=CARTESIAN_POINT('Ctrl Pts',(2.57675908943053,0.694142719460964,
12.5813877129824));
#447802=CARTESIAN_POINT('Ctrl Pts',(2.56507357985403,0.712455234639498,
12.596957478804));
#447803=CARTESIAN_POINT('Ctrl Pts',(2.56613695319864,0.708609479800865,
12.5878468778671));
#447804=CARTESIAN_POINT('Ctrl Pts',(2.5738759248271,0.704707454676469,12.5814011370086));
#447805=CARTESIAN_POINT('Ctrl Pts',(2.57282509538981,0.727430314406849,
12.5928371701607));
#447806=CARTESIAN_POINT('Ctrl Pts',(2.56881311714011,0.720188830012911,
12.5821692192952));
#447807=CARTESIAN_POINT('Ctrl Pts',(2.57662560011115,0.710040483753784,
12.5773318885715));
#447808=CARTESIAN_POINT('Ctrl Pts',(2.58119104811549,0.73392304406439,12.5893111709658));
#447809=CARTESIAN_POINT('Ctrl Pts',(2.57223724225783,0.726974087651879,
12.5770542771492));
#447810=CARTESIAN_POINT('Ctrl Pts',(2.57968438846796,0.712402070352277,
12.5737548217797));
#447811=CARTESIAN_POINT('',(2.58563779814647,0.690482027821093,12.5737548217797));
#447812=CARTESIAN_POINT('Origin',(2.60066746911387,0.694495628525142,12.5893111709658));
#447813=CARTESIAN_POINT('Ctrl Pts',(2.57968438846796,0.712402070352277,
12.5737548217797));
#447814=CARTESIAN_POINT('Ctrl Pts',(2.57887306713315,0.71181378698289,12.5746934679442));
#447815=CARTESIAN_POINT('Ctrl Pts',(2.57808281832406,0.711014510899208,
12.5756680099006));
#447816=CARTESIAN_POINT('Ctrl Pts',(2.57740118190847,0.710097518279326,
12.5765688348656));
#447817=CARTESIAN_POINT('Ctrl Pts',(2.5772207262134,0.709854754634652,12.5768073183026));
#447818=CARTESIAN_POINT('Ctrl Pts',(2.57704772001294,0.709603939593634,
12.5770407398754));
#447819=CARTESIAN_POINT('Ctrl Pts',(2.5768833328898,0.709347136134447,12.5772674179684));
#447820=CARTESIAN_POINT('Ctrl Pts',(2.57620873258859,0.708293284180544,
12.5781976435658));
#447821=CARTESIAN_POINT('Ctrl Pts',(2.57565046725709,0.707072646108709,
12.5790594849312));
#447822=CARTESIAN_POINT('Ctrl Pts',(2.57529014610397,0.705747556907826,
12.5797571720116));
#447823=CARTESIAN_POINT('Ctrl Pts',(2.57505538391673,0.70488421364749,12.580211740231));
#447824=CARTESIAN_POINT('Ctrl Pts',(2.57491209519903,0.703932370528216,
12.5806009430798));
#447825=CARTESIAN_POINT('Ctrl Pts',(2.5748878861526,0.702956395842894,12.5808812374708));
#447826=CARTESIAN_POINT('Ctrl Pts',(2.57486708255046,0.702117709811969,
12.5811221033394));
#447827=CARTESIAN_POINT('Ctrl Pts',(2.57493390164797,0.701244030831503,
12.581287365893));
#447828=CARTESIAN_POINT('Ctrl Pts',(2.57509288576999,0.700385306584494,
12.581359338449));
#447829=CARTESIAN_POINT('Ctrl Pts',(2.57511498128005,0.700265961646139,
12.5813693411482));
#447830=CARTESIAN_POINT('Ctrl Pts',(2.57513880510371,0.700146875662145,
12.5813775999465));
#447831=CARTESIAN_POINT('Ctrl Pts',(2.57516431683881,0.700028151144637,
12.5813841266931));
#447832=CARTESIAN_POINT('Ctrl Pts',(2.57520760058298,0.699826720641251,
12.5813952001081));
#447833=CARTESIAN_POINT('Ctrl Pts',(2.57525662819535,0.69962510945769,12.5814007534795));
#447834=CARTESIAN_POINT('Ctrl Pts',(2.57531156994799,0.699423452001435,
12.5814005856065));
#447835=CARTESIAN_POINT('Ctrl Pts',(2.57556307181075,0.698500343009653,
12.5813998171494));
#447836=CARTESIAN_POINT('Ctrl Pts',(2.57592079907501,0.697639955419613,
12.58127954464));
#447837=CARTESIAN_POINT('Ctrl Pts',(2.57635539889883,0.696835814200509,
12.5810700125799));
#447838=CARTESIAN_POINT('Ctrl Pts',(2.57688034600285,0.69586450316664,12.5808169217085));
#447839=CARTESIAN_POINT('Ctrl Pts',(2.57753222009882,0.694983124404432,
12.5804173076348));
#447840=CARTESIAN_POINT('Ctrl Pts',(2.57823295416952,0.694253434655424,
12.5799304713245));
#447841=CARTESIAN_POINT('Ctrl Pts',(2.57910138443712,0.693349119180426,
12.5793271277669));
#447842=CARTESIAN_POINT('Ctrl Pts',(2.58007550391725,0.692599383195681,
12.5785808224116));
#447843=CARTESIAN_POINT('Ctrl Pts',(2.58109490679138,0.692010695126134,
12.5777485681082));
#447844=CARTESIAN_POINT('Ctrl Pts',(2.58261392875775,0.691133485406916,
12.576508418016));
#447845=CARTESIAN_POINT('Ctrl Pts',(2.58421727195989,0.690615305817478,
12.5750928681475));
#447846=CARTESIAN_POINT('Ctrl Pts',(2.58563779814647,0.690482027821093,
12.5737548217797));
#447847=CARTESIAN_POINT('Ctrl Pts',(2.58563779814647,0.690482027821093,
12.5737548217797));
#447848=CARTESIAN_POINT('Ctrl Pts',(2.58658550304428,0.674144784164906,
12.5770542771492));
#447849=CARTESIAN_POINT('Ctrl Pts',(2.59782442414821,0.672680104343423,
12.5893111709658));
#447850=CARTESIAN_POINT('Ctrl Pts',(2.61019578895115,0.687332418034614,
12.5508408821982));
#447851=CARTESIAN_POINT('Ctrl Pts',(2.61114322150309,0.670944370677193,
12.55409748406));
#447852=CARTESIAN_POINT('Ctrl Pts',(2.6223964805919,0.669477822299387,12.5663972313419));
#447853=CARTESIAN_POINT('Ctrl Pts',(2.63472963964692,0.68418471508971,12.52790050457));
#447854=CARTESIAN_POINT('Ctrl Pts',(2.63565390608582,0.667750086743115,
12.5311362602938));
#447855=CARTESIAN_POINT('Ctrl Pts',(2.64694374786836,0.66627877083173,12.5434568539655));
#447856=CARTESIAN_POINT('Ctrl Pts',(2.65924122446842,0.681038757064725,
12.5049357605811));
#447857=CARTESIAN_POINT('Ctrl Pts',(2.66012245983368,0.664561293387921,
12.5081700652078));
#447858=CARTESIAN_POINT('Ctrl Pts',(2.6714681674702,0.663082696921053,12.5204921097672));
#447859=CARTESIAN_POINT('Ctrl Pts',(2.65763169752453,0.681245331426205,
12.5064436508395));
#447860=CARTESIAN_POINT('Ctrl Pts',(2.65813124959428,0.680132094919352,
12.5062361689309));
#447861=CARTESIAN_POINT('Ctrl Pts',(2.65860327198979,0.678953118041469,
12.5061871075062));
#447862=CARTESIAN_POINT('Ctrl Pts',(2.65899529819047,0.6777880720771,12.5063648335164));
#447863=CARTESIAN_POINT('Ctrl Pts',(2.659173380672,0.677258836337068,12.5064455676329));
#447864=CARTESIAN_POINT('Ctrl Pts',(2.65933723071486,0.676725023291958,
12.506574497099));
#447865=CARTESIAN_POINT('Ctrl Pts',(2.65947881823401,0.676209212862752,
12.5067492519495));
#447866=CARTESIAN_POINT('Ctrl Pts',(2.65976334384976,0.675172671783016,
12.5071004286051));
#447867=CARTESIAN_POINT('Ctrl Pts',(2.65996764954846,0.674170505851928,
12.5076537929612));
#447868=CARTESIAN_POINT('Ctrl Pts',(2.66008566893586,0.673279822254663,
12.5083435010503));
#447869=CARTESIAN_POINT('Ctrl Pts',(2.66009309896159,0.673223748399357,
12.5083869222963));
#447870=CARTESIAN_POINT('Ctrl Pts',(2.66010017597423,0.673168108716542,
12.5084308732336));
#447871=CARTESIAN_POINT('Ctrl Pts',(2.66010689419839,0.673112918993485,
12.5084753333615));
#447872=CARTESIAN_POINT('Ctrl Pts',(2.66016078322331,0.672670224571504,
12.508831962269));
#447873=CARTESIAN_POINT('Ctrl Pts',(2.66019396189943,0.672247649732734,
12.509227847131));
#447874=CARTESIAN_POINT('Ctrl Pts',(2.66020823511389,0.671857979002731,
12.5096423454524));
#447875=CARTESIAN_POINT('Ctrl Pts',(2.66025296105096,0.67063692339594,12.5109411997424));
#447876=CARTESIAN_POINT('Ctrl Pts',(2.66012446388748,0.669664210401967,
12.5124831113042));
#447877=CARTESIAN_POINT('Ctrl Pts',(2.65990367814058,0.668890794518083,
12.5140723025008));
#447878=CARTESIAN_POINT('Ctrl Pts',(2.65988299027427,0.668818324602665,
12.5142212114565));
#447879=CARTESIAN_POINT('Ctrl Pts',(2.65986151043435,0.668747581228111,
12.5143705582413));
#447880=CARTESIAN_POINT('Ctrl Pts',(2.65983931687852,0.668678511711671,
12.5145201959299));
#447881=CARTESIAN_POINT('Ctrl Pts',(2.6595542076112,0.667791210939238,12.5164425148273));
#447882=CARTESIAN_POINT('Ctrl Pts',(2.65915176673183,0.667146463610461,
12.5184635205941));
#447883=CARTESIAN_POINT('Ctrl Pts',(2.65867357626237,0.666664214032228,
12.5205025929157));
#447884=CARTESIAN_POINT('Ctrl Pts',(2.65839620683639,0.666384490162265,
12.5216853356836));
#447885=CARTESIAN_POINT('Ctrl Pts',(2.6580941961743,0.666159602824852,12.5228750347131));
#447886=CARTESIAN_POINT('Ctrl Pts',(2.65778074882996,0.665976959426719,
12.5240609649613));
#447887=CARTESIAN_POINT('Ctrl Pts',(2.65701140913917,0.66552867100448,12.5269717671326));
#447888=CARTESIAN_POINT('Ctrl Pts',(2.65614628521843,0.665331238509816,
12.5299036066169));
#447889=CARTESIAN_POINT('Ctrl Pts',(2.65521799080379,0.665304375786692,
12.5328133004019));
#447890=CARTESIAN_POINT('Ctrl Pts',(2.6547723554318,0.665291480115423,12.5342101228451));
#447891=CARTESIAN_POINT('Ctrl Pts',(2.65431270291339,0.665318433204005,
12.5356023438238));
#447892=CARTESIAN_POINT('Ctrl Pts',(2.65384464771223,0.665379431058994,
12.5369868989719));
#447893=CARTESIAN_POINT('Origin',(15.291180332043,-0.98688563005775,-1.23957201933111));
#447894=CARTESIAN_POINT('Ctrl Pts',(2.62578810934736,0.76853441374342,12.5369868989719));
#447895=CARTESIAN_POINT('Ctrl Pts',(2.63792369202002,0.777915828182662,
12.5369868989719));
#447896=CARTESIAN_POINT('Ctrl Pts',(2.63331726935041,0.792546760274453,
12.5369868989719));
#447897=CARTESIAN_POINT('Ctrl Pts',(2.62989037041483,0.77170575111314,12.5218025310016));
#447898=CARTESIAN_POINT('Ctrl Pts',(2.63683581805028,0.781266955056582,
12.5216901060418));
#447899=CARTESIAN_POINT('Ctrl Pts',(2.63333132698383,0.792502165297268,
12.5161920673678));
#447900=CARTESIAN_POINT('Ctrl Pts',(2.63566681220354,0.769982732988681,
12.5042015548894));
#447901=CARTESIAN_POINT('Ctrl Pts',(2.63841449808402,0.775798880108503,
12.4980677368513));
#447902=CARTESIAN_POINT('Ctrl Pts',(2.63649140361122,0.782317506296004,
12.4907278922777));
#447903=CARTESIAN_POINT('Ctrl Pts',(2.63709485533895,0.756784260822992,
12.506463626192));
#447904=CARTESIAN_POINT('Ctrl Pts',(2.64338375481666,0.758589027205586,
12.4999376786891));
#447905=CARTESIAN_POINT('Ctrl Pts',(2.64330694505359,0.758566984608351,
12.4906970594712));
#447906=CARTESIAN_POINT('Origin',(2.61233274543718,0.785939964066368,12.5369868989719));
#447907=CARTESIAN_POINT('Origin',(2.61233274543718,0.785939964066368,14.));
#447908=CARTESIAN_POINT('Origin',(2.61233274543718,0.785939964066368,13.7435492065112));
#447909=CARTESIAN_POINT('Ctrl Pts',(2.606260700401,0.753379377104391,13.793642941384));
#447910=CARTESIAN_POINT('Ctrl Pts',(2.61481907347178,0.759986984037845,
13.8071662555867));
#447911=CARTESIAN_POINT('Ctrl Pts',(2.60650673469415,0.774850510122887,
13.8103758687955));
#447912=CARTESIAN_POINT('Ctrl Pts',(2.61939135650484,0.763569940165686,
13.7804579775006));
#447913=CARTESIAN_POINT('Ctrl Pts',(2.62994541808841,0.771731156730597,
13.7901904343351));
#447914=CARTESIAN_POINT('Ctrl Pts',(2.62458111199279,0.786546019007273,
13.7927914348263));
#447915=CARTESIAN_POINT('Ctrl Pts',(2.62712186789201,0.769569508183912,
13.7597120340895));
#447916=CARTESIAN_POINT('Ctrl Pts',(2.63933238396734,0.779018867270492,
13.7635825532445));
#447917=CARTESIAN_POINT('Ctrl Pts',(2.63522566452749,0.793464308474768,
13.7651073818884));
#447918=CARTESIAN_POINT('Ctrl Pts',(2.62560805675334,0.768394655392109,
13.7381884353898));
#447919=CARTESIAN_POINT('Ctrl Pts',(2.63753331304775,0.777622123784822,
13.7368803041982));
#447920=CARTESIAN_POINT('Ctrl Pts',(2.63314087550801,0.792109916217712,
13.7363986145813));
#447921=CARTESIAN_POINT('Origin',(2.59595844123841,0.77323203539656,13.7902182540695));
#447922=CARTESIAN_POINT('Ctrl Pts',(2.58118793806113,0.733920631343859,
13.8235227101244));
#447923=CARTESIAN_POINT('Ctrl Pts',(2.59027332090908,0.740966091359053,
13.8358800583119));
#447924=CARTESIAN_POINT('Ctrl Pts',(2.5826329971052,0.755671583572118,13.8390832900376));
#447925=CARTESIAN_POINT('Ctrl Pts',(2.59061070256867,0.741233541730976,
13.8124254819052));
#447926=CARTESIAN_POINT('Ctrl Pts',(2.59971372893087,0.748292684149464,
13.8247886449158));
#447927=CARTESIAN_POINT('Ctrl Pts',(2.59204862653025,0.76300889922979,13.8279860620657));
#447928=CARTESIAN_POINT('Ctrl Pts',(2.60002924409971,0.748543174709559,
13.8013225099955));
#447929=CARTESIAN_POINT('Ctrl Pts',(2.60914562003793,0.755612667165597,
13.8136962257787));
#447930=CARTESIAN_POINT('Ctrl Pts',(2.60146006359299,0.770342604267049,
13.8168830918626));
#447931=CARTESIAN_POINT('Ctrl Pts',(2.60944372696379,0.755849657798537,
13.7902140179785));
#447932=CARTESIAN_POINT('Ctrl Pts',(2.61856943917847,0.76292638572319,13.802602731458));
#447933=CARTESIAN_POINT('Ctrl Pts',(2.61086747415274,0.777672839102351,
13.8057746032558));
#447934=CARTESIAN_POINT('Origin',(2.56770264248895,0.751303001304022,13.8235269408515));
#447935=CARTESIAN_POINT('Ctrl Pts',(2.59782442414821,0.672680104343423,
13.8235269408515));
#447936=CARTESIAN_POINT('Ctrl Pts',(2.60953289676871,0.671154231581342,
13.8362179249168));
#447937=CARTESIAN_POINT('Ctrl Pts',(2.61009406336906,0.654085309643976,
13.8391868794938));
#447938=CARTESIAN_POINT('Ctrl Pts',(2.58711168133992,0.674076211503438,
13.8400110824519));
#447939=CARTESIAN_POINT('Ctrl Pts',(2.59605691881181,0.669460522017201,
13.8494522556837));
#447940=CARTESIAN_POINT('Ctrl Pts',(2.59247843281422,0.656494322674229,
13.85569149686));
#447941=CARTESIAN_POINT('Ctrl Pts',(2.57323467775334,0.682610055742881,
13.8586819406588));
#447942=CARTESIAN_POINT('Ctrl Pts',(2.57438924629646,0.678412078240054,
13.868010383617));
#447943=CARTESIAN_POINT('Ctrl Pts',(2.56951881116523,0.670785038943894,
13.8744918421245));
#447944=CARTESIAN_POINT('Ctrl Pts',(2.56498262170184,0.712792419283031,
13.8587686893867));
#447945=CARTESIAN_POINT('Ctrl Pts',(2.56383827451559,0.716953019893181,
13.8680909899357));
#447946=CARTESIAN_POINT('Ctrl Pts',(2.55578404302611,0.721030489282356,
13.8745789365163));
#447947=CARTESIAN_POINT('Ctrl Pts',(2.57264254930173,0.727288642278172,
13.8400379222776));
#447948=CARTESIAN_POINT('Ctrl Pts',(2.5780163648333,0.735797011131287,13.8494748685453));
#447949=CARTESIAN_POINT('Ctrl Pts',(2.56837546851325,0.745167935493955,
13.8557104837033));
#447950=CARTESIAN_POINT('Ctrl Pts',(2.58119104811137,0.733923044069481,
13.8235269408542));
#447951=CARTESIAN_POINT('Ctrl Pts',(2.59051893552723,0.741162321322599,
13.8362179249195));
#447952=CARTESIAN_POINT('Ctrl Pts',(2.5823682198157,0.756169947298957,13.8391868794965));
#447953=CARTESIAN_POINT('Origin',(2.59498137918254,0.650864580161703,13.8235269408515));
#447954=CARTESIAN_POINT('Ctrl Pts',(2.63328752098124,0.668058478257452,
13.7902140241682));
#447955=CARTESIAN_POINT('Ctrl Pts',(2.64473936075701,0.666570539702663,
13.8026027327198));
#447956=CARTESIAN_POINT('Ctrl Pts',(2.64555550050207,0.649953926082844,
13.8057746032556));
#447957=CARTESIAN_POINT('Ctrl Pts',(2.62147035274383,0.669598516461878,
13.8013225161808));
#447958=CARTESIAN_POINT('Ctrl Pts',(2.6329104787429,0.668112096261962,13.8136962270464));
#447959=CARTESIAN_POINT('Ctrl Pts',(2.63373241740558,0.651518030390442,
13.8168830918628));
#447960=CARTESIAN_POINT('Ctrl Pts',(2.6096480900189,0.671139218590636,13.8124254880875));
#447961=CARTESIAN_POINT('Ctrl Pts',(2.62107146476185,0.669654973151802,
13.8247886461868));
#447962=CARTESIAN_POINT('Ctrl Pts',(2.62190410553007,0.653083091196216,
13.8279860620656));
#447963=CARTESIAN_POINT('Ctrl Pts',(2.59782052656158,0.672680611521997,
13.8235227163065));
#447964=CARTESIAN_POINT('Ctrl Pts',(2.60922176031045,0.671199243154391,
13.8358800595847));
#447965=CARTESIAN_POINT('Ctrl Pts',(2.61007035076852,0.654649145721658,
13.8390832900376));
#447966=CARTESIAN_POINT('Origin',(2.63044838594165,0.646242445292339,13.7902182540695));
#447967=CARTESIAN_POINT('Ctrl Pts',(2.65357704709218,0.665414277516546,
13.7382347919292));
#447968=CARTESIAN_POINT('Ctrl Pts',(2.66854391703599,0.663487966841118,
13.7369371795943));
#447969=CARTESIAN_POINT('Ctrl Pts',(2.67207869907657,0.648755380749542,
13.7364597369711));
#447970=CARTESIAN_POINT('Ctrl Pts',(2.65545274453738,0.665169833088515,
13.7595490285574));
#447971=CARTESIAN_POINT('Ctrl Pts',(2.67077658282397,0.663196565092251,
13.7633824266925));
#447972=CARTESIAN_POINT('Ctrl Pts',(2.67453179815223,0.648643489192444,
13.7648920890506));
#447973=CARTESIAN_POINT('Ctrl Pts',(2.64588679032705,0.666416486287619,
13.7803806590111));
#447974=CARTESIAN_POINT('Ctrl Pts',(2.6591420514446,0.664715034345835,13.7901039518745));
#447975=CARTESIAN_POINT('Ctrl Pts',(2.66202580035423,0.649217633478212,
13.7926933640892));
#447976=CARTESIAN_POINT('Ctrl Pts',(2.62925902651006,0.66858344775921,13.7936647693663));
#447977=CARTESIAN_POINT('Ctrl Pts',(2.63998758966256,0.667215506010775,
13.8072068914932));
#447978=CARTESIAN_POINT('Ctrl Pts',(2.64032626442967,0.650170578048214,
13.8104111085397));
#447979=CARTESIAN_POINT('Origin',(2.65100160274657,0.643563906877274,13.7435492065112));
#447980=CARTESIAN_POINT('Origin',(2.65100160274657,0.643563906877274,14.));
#447981=CARTESIAN_POINT('Origin',(2.65100160274657,0.643563906877274,12.5369868989719));
#447982=CARTESIAN_POINT('Ctrl Pts',(2.65761389002454,0.681240766742555,
12.506462012331));
#447983=CARTESIAN_POINT('Ctrl Pts',(2.66394773156924,0.682864355137594,
12.4999388158272));
#447984=CARTESIAN_POINT('Ctrl Pts',(2.66387279391744,0.682845145957675,
12.4907030323752));
#447985=CARTESIAN_POINT('Ctrl Pts',(2.66305686697698,0.669132811297897,
12.5042014951932));
#447986=CARTESIAN_POINT('Ctrl Pts',(2.66836750394045,0.665508141360079,
12.4980716682127));
#447987=CARTESIAN_POINT('Ctrl Pts',(2.67000662320842,0.658917325534159,
12.4907355092743));
#447988=CARTESIAN_POINT('Ctrl Pts',(2.65894801738008,0.664723383190354,
12.5218047446509));
#447989=CARTESIAN_POINT('Ctrl Pts',(2.66977023209787,0.659990673655744,
12.5216906929434));
#447990=CARTESIAN_POINT('Ctrl Pts',(2.67243315700827,0.648532943284871,
12.5161988840776));
#447991=CARTESIAN_POINT('Ctrl Pts',(2.65380654939458,0.665384362287319,
12.5369868989719));
#447992=CARTESIAN_POINT('Ctrl Pts',(2.66901133049048,0.663429838471607,
12.5369868989719));
#447993=CARTESIAN_POINT('Ctrl Pts',(2.67244322402028,0.648489033997923,
12.5369868989719));
#447994=CARTESIAN_POINT('Origin',(4.97175483587121E-31,-3.80155074318086E-31,
12.5));
#447995=CARTESIAN_POINT('Origin',(2.53435070432089,0.882188624381805,12.5));
#447996=CARTESIAN_POINT('',(2.53435070432089,0.882188624381805,12.5893111709658));
#447997=CARTESIAN_POINT('',(2.53435070432089,0.882188624381805,13.8235269408515));
#447998=CARTESIAN_POINT('',(2.53435070432089,0.882188624381805,12.5));
#447999=CARTESIAN_POINT('',(2.57007644444249,0.880472759595413,13.7902182540695));
#448000=CARTESIAN_POINT('',(2.53435070432089,0.882188624381805,13.8235269408515));
#448001=CARTESIAN_POINT('',(2.59077959786117,0.879478411772317,13.7435492065112));
#448002=CARTESIAN_POINT('Origin',(2.52266651239525,0.882750128347015,13.7445212918698));
#448003=CARTESIAN_POINT('',(2.59077959786117,0.879478411772317,12.5369868989719));
#448004=CARTESIAN_POINT('',(2.59077959786117,0.879478411772317,12.5));
#448005=CARTESIAN_POINT('Ctrl Pts',(2.59077959786117,0.879478411772317,
12.5369868989719));
#448006=CARTESIAN_POINT('Ctrl Pts',(2.57198368528203,0.8803811570874,12.5544431401645));
#448007=CARTESIAN_POINT('Ctrl Pts',(2.55317432936665,0.881284548069926,
12.5718848856037));
#448008=CARTESIAN_POINT('Ctrl Pts',(2.53435070432089,0.882188624381805,
12.5893111709658));
#448009=CARTESIAN_POINT('Origin',(2.71556451367195,1.12762390786281,12.5));
#448010=CARTESIAN_POINT('',(2.55443917227923,0.980031487551649,13.7435492065112));
#448011=CARTESIAN_POINT('',(2.53915516638813,0.966031185662336,13.7902182540695));
#448012=CARTESIAN_POINT('Origin',(2.49899144051201,0.929240812034377,13.7418732680438));
#448013=CARTESIAN_POINT('',(2.51278080633584,0.941872008709604,13.8235269408515));
#448014=CARTESIAN_POINT('',(2.53915516638813,0.966031185662336,13.7902182540695));
#448015=CARTESIAN_POINT('',(2.51278080633584,0.941872008709604,12.5893111709658));
#448016=CARTESIAN_POINT('',(2.51278080633584,0.941872008709604,12.5));
#448017=CARTESIAN_POINT('',(2.55443917227923,0.980031487551649,12.5369868989719));
#448018=CARTESIAN_POINT('Ctrl Pts',(2.51278080633584,0.941872008709604,
12.5893111709658));
#448019=CARTESIAN_POINT('Ctrl Pts',(2.52667725922265,0.954601298202966,
12.5718848856037));
#448020=CARTESIAN_POINT('Ctrl Pts',(2.5405631779909,0.967320938338619,12.5544431401645));
#448021=CARTESIAN_POINT('Ctrl Pts',(2.55443917227923,0.980031487551649,
12.5369868989719));
#448022=CARTESIAN_POINT('',(2.55443917227923,0.980031487551649,12.5));
#448023=CARTESIAN_POINT('Origin',(2.53599979372999,0.91652404529259,12.5));
#448024=CARTESIAN_POINT('',(2.50406965628867,0.903793904085336,13.8587068136939));
#448025=CARTESIAN_POINT('Ctrl Pts',(2.51278080633127,0.94187200871438,13.8235269408542));
#448026=CARTESIAN_POINT('Ctrl Pts',(2.51148866978172,0.940688398742956,
13.8262006681044));
#448027=CARTESIAN_POINT('Ctrl Pts',(2.51028371103606,0.939349032305694,
13.8288634856214));
#448028=CARTESIAN_POINT('Ctrl Pts',(2.50916073115021,0.937866188532404,
13.8314912288862));
#448029=CARTESIAN_POINT('Ctrl Pts',(2.50800305471791,0.936337529550384,
13.834200161153));
#448030=CARTESIAN_POINT('Ctrl Pts',(2.5069308191771,0.934654992288229,13.8368750301949));
#448031=CARTESIAN_POINT('Ctrl Pts',(2.50595888810607,0.932791774879842,
13.8394886372968));
#448032=CARTESIAN_POINT('Ctrl Pts',(2.50588382351188,0.932647874079853,
13.839690492513));
#448033=CARTESIAN_POINT('Ctrl Pts',(2.5058093747972,0.932502882076606,13.8398919674349));
#448034=CARTESIAN_POINT('Ctrl Pts',(2.50573555846853,0.932356780385714,
13.8400930404591));
#448035=CARTESIAN_POINT('Ctrl Pts',(2.50458545040666,0.930080417749296,
13.8432258934518));
#448036=CARTESIAN_POINT('Ctrl Pts',(2.50359372271598,0.927546793256493,
13.8462331177034));
#448037=CARTESIAN_POINT('Ctrl Pts',(2.50288255003621,0.924803378336516,
13.8489036603661));
#448038=CARTESIAN_POINT('Ctrl Pts',(2.50264984605906,0.923905701047975,
13.8497774930041));
#448039=CARTESIAN_POINT('Ctrl Pts',(2.50244736539328,0.922985730093805,
13.85061494757));
#448040=CARTESIAN_POINT('Ctrl Pts',(2.5022799085519,0.922045617370849,13.8514076489583));
#448041=CARTESIAN_POINT('Ctrl Pts',(2.5019257131815,0.920057143377244,13.8530843267192));
#448042=CARTESIAN_POINT('Ctrl Pts',(2.50169632942285,0.917782719230699,
13.8546805203176));
#448043=CARTESIAN_POINT('Ctrl Pts',(2.50174082765797,0.915340660110883,
13.8559412814274));
#448044=CARTESIAN_POINT('Ctrl Pts',(2.50174678296495,0.915013833402807,
13.8561100121513));
#448045=CARTESIAN_POINT('Ctrl Pts',(2.50175758439277,0.914684052866435,
13.8562727473908));
#448046=CARTESIAN_POINT('Ctrl Pts',(2.5017735250615,0.914351642480321,13.8564289040185));
#448047=CARTESIAN_POINT('Ctrl Pts',(2.50184581581231,0.912844165171528,
13.8571370725437));
#448048=CARTESIAN_POINT('Ctrl Pts',(2.50202734530105,0.911256213854759,
13.8577210840554));
#448049=CARTESIAN_POINT('Ctrl Pts',(2.50234021558104,0.909652845744784,
13.8581177131616));
#448050=CARTESIAN_POINT('Ctrl Pts',(2.50242833062056,0.909201282098762,
13.8582294175695));
#448051=CARTESIAN_POINT('Ctrl Pts',(2.50252668573171,0.908748496421003,
13.8583265086086));
#448052=CARTESIAN_POINT('Ctrl Pts',(2.50263533573102,0.908295917735097,
13.8584082369006));
#448053=CARTESIAN_POINT('Ctrl Pts',(2.50279143664439,0.907645683527221,
13.8585256585398));
#448054=CARTESIAN_POINT('Ctrl Pts',(2.50297104336265,0.906987868129444,
13.8586122832068));
#448055=CARTESIAN_POINT('Ctrl Pts',(2.50317025202566,0.906339767677968,
13.8586682984299));
#448056=CARTESIAN_POINT('Ctrl Pts',(2.50332959920916,0.905821351560919,
13.8587131050557));
#448057=CARTESIAN_POINT('Ctrl Pts',(2.50350302438606,0.90530335666637,13.8587357943552));
#448058=CARTESIAN_POINT('Ctrl Pts',(2.503691028409,0.904785882228803,13.8587355499465));
#448059=CARTESIAN_POINT('Ctrl Pts',(2.50381253989126,0.904451426162635,
13.8587353919793));
#448060=CARTESIAN_POINT('Ctrl Pts',(2.50393879110388,0.904120791066776,
13.8587257282814));
#448061=CARTESIAN_POINT('Ctrl Pts',(2.50406965628867,0.903793904085336,
13.8587068136939));
#448062=CARTESIAN_POINT('Ctrl Pts',(2.50406965628867,0.903793904085336,
13.8587068136939));
#448063=CARTESIAN_POINT('Ctrl Pts',(2.50450006474724,0.902718790623857,
13.8586446046466));
#448064=CARTESIAN_POINT('Ctrl Pts',(2.5049803220448,0.901684170425667,13.858482427929));
#448065=CARTESIAN_POINT('Ctrl Pts',(2.50550651163635,0.900687887885843,
13.8582284286032));
#448066=CARTESIAN_POINT('Ctrl Pts',(2.5060463209484,0.899665817892324,13.8579678548414));
#448067=CARTESIAN_POINT('Ctrl Pts',(2.50663714408614,0.898682314550188,
13.857615680862));
#448068=CARTESIAN_POINT('Ctrl Pts',(2.50724738215115,0.89777116197706,13.8571944833187));
#448069=CARTESIAN_POINT('Ctrl Pts',(2.50877029365242,0.895497287545792,
13.8561433417727));
#448070=CARTESIAN_POINT('Ctrl Pts',(2.51048137459297,0.893564982698628,
13.8546163505475));
#448071=CARTESIAN_POINT('Ctrl Pts',(2.51217385142717,0.891972645104082,
13.8528973491086));
#448072=CARTESIAN_POINT('Ctrl Pts',(2.51248304197463,0.891681748518294,
13.8525833129073));
#448073=CARTESIAN_POINT('Ctrl Pts',(2.51279157328859,0.891402061939436,
13.8522628768812));
#448074=CARTESIAN_POINT('Ctrl Pts',(2.51309816365804,0.89113339802571,13.851937733538));
#448075=CARTESIAN_POINT('Ctrl Pts',(2.51497046850669,0.889492704780083,
13.8499521282529));
#448076=CARTESIAN_POINT('Ctrl Pts',(2.5169591479262,0.888103101284376,13.847639871647));
#448077=CARTESIAN_POINT('Ctrl Pts',(2.5189136668728,0.886971763861578,13.8452109780794));
#448078=CARTESIAN_POINT('Ctrl Pts',(2.51979304540339,0.886462751737545,
13.8441181685877));
#448079=CARTESIAN_POINT('Ctrl Pts',(2.5206653863283,0.886005312830334,13.8430021611332));
#448080=CARTESIAN_POINT('Ctrl Pts',(2.52151745116643,0.885596825797609,
13.8418824960098));
#448081=CARTESIAN_POINT('Ctrl Pts',(2.52352536371575,0.884634215673897,
13.8392439765549));
#448082=CARTESIAN_POINT('Ctrl Pts',(2.52551503051308,0.883894018269432,
13.8364981347963));
#448083=CARTESIAN_POINT('Ctrl Pts',(2.52747978164497,0.883342203062412,
13.8336931113419));
#448084=CARTESIAN_POINT('Ctrl Pts',(2.52939332447419,0.882804770094281,
13.8309611966327));
#448085=CARTESIAN_POINT('Ctrl Pts',(2.53128530363879,0.882446032338076,
13.8281701127185));
#448086=CARTESIAN_POINT('Ctrl Pts',(2.53314569048023,0.882273660704874,
13.825358068512));
#448087=CARTESIAN_POINT('Ctrl Pts',(2.53354902435522,0.882236290348769,
13.8247484142932));
#448088=CARTESIAN_POINT('Ctrl Pts',(2.53395079043386,0.882207831769924,
13.8241378483365));
#448089=CARTESIAN_POINT('Ctrl Pts',(2.53435070432089,0.882188624381805,
13.8235269408515));
#448090=CARTESIAN_POINT('',(2.50363054332231,0.90495578043872,12.5969504640361));
#448091=CARTESIAN_POINT('Origin',(2.53603097596901,0.916535106521272,12.584524458991));
#448092=CARTESIAN_POINT('Origin',(2.53603097596901,0.916535106521272,12.584524458991));
#448093=CARTESIAN_POINT('Ctrl Pts',(2.51278080633584,0.941872008709604,
12.5893111709658));
#448094=CARTESIAN_POINT('Ctrl Pts',(2.50442319798711,0.934216356075829,
12.5770542771492));
#448095=CARTESIAN_POINT('Ctrl Pts',(2.5130333191225,0.920299837513742,12.5737548217797));
#448096=CARTESIAN_POINT('Ctrl Pts',(2.53105609089778,0.958612351706294,
12.5663937883685));
#448097=CARTESIAN_POINT('Ctrl Pts',(2.52268782125892,0.950946933224371,
12.5540940315304));
#448098=CARTESIAN_POINT('Ctrl Pts',(2.531327354201,0.936988979726258,12.5508374392248));
#448099=CARTESIAN_POINT('Ctrl Pts',(2.54931293592164,0.975335803902121,
12.5434499600945));
#448100=CARTESIAN_POINT('Ctrl Pts',(2.54091745805819,0.967645462414973,
12.5311293540533));
#448101=CARTESIAN_POINT('Ctrl Pts',(2.54960272043615,0.95366268794112,12.5278936106989));
#448102=CARTESIAN_POINT('Ctrl Pts',(2.56755278580165,0.992043688376609,
12.5204817579905));
#448103=CARTESIAN_POINT('Ctrl Pts',(2.55911575606026,0.984315284954743,
12.5081597038247));
#448104=CARTESIAN_POINT('Ctrl Pts',(2.56786085950626,0.970322171983944,
12.5049254088044));
#448105=CARTESIAN_POINT('Ctrl Pts',(2.55443917227922,0.980031487551647,
12.5369868989719));
#448106=CARTESIAN_POINT('Ctrl Pts',(2.55512605964089,0.980660683008643,
12.5342545179733));
#448107=CARTESIAN_POINT('Ctrl Pts',(2.5558658547498,0.981169171268279,12.5314872231885));
#448108=CARTESIAN_POINT('Ctrl Pts',(2.55664854815204,0.981482240187567,
12.5287124745063));
#448109=CARTESIAN_POINT('Ctrl Pts',(2.55735441991161,0.981764581278338,
12.5262100684184));
#448110=CARTESIAN_POINT('Ctrl Pts',(2.5580948353458,0.98188678325276,12.5237004536639));
#448111=CARTESIAN_POINT('Ctrl Pts',(2.55889330268674,0.98178553861399,12.5212220730815));
#448112=CARTESIAN_POINT('Ctrl Pts',(2.55950459850916,0.981708027084652,
12.5193246583486));
#448113=CARTESIAN_POINT('Ctrl Pts',(2.56015714590132,0.981497992506336,
12.5174178313691));
#448114=CARTESIAN_POINT('Ctrl Pts',(2.56084000232861,0.981058820782296,
12.5155812248348));
#448115=CARTESIAN_POINT('Ctrl Pts',(2.56113090283701,0.980871731267295,
12.5147988205794));
#448116=CARTESIAN_POINT('Ctrl Pts',(2.56142774900065,0.980643100884673,
12.5140295443047));
#448117=CARTESIAN_POINT('Ctrl Pts',(2.56173165385155,0.980366289406517,
12.5132817086137));
#448118=CARTESIAN_POINT('Ctrl Pts',(2.56219157273206,0.979947372680541,
12.5121499604604));
#448119=CARTESIAN_POINT('Ctrl Pts',(2.56267277369802,0.979403774715852,
12.5110494206568));
#448120=CARTESIAN_POINT('Ctrl Pts',(2.5631567973615,0.978703151274273,12.5100666561695));
#448121=CARTESIAN_POINT('Ctrl Pts',(2.56343472263447,0.978300854907512,
12.5095023550641));
#448122=CARTESIAN_POINT('Ctrl Pts',(2.56371625268125,0.977841767586617,
12.5089719619137));
#448123=CARTESIAN_POINT('Ctrl Pts',(2.56399066579999,0.977331155476289,
12.5085043804652));
#448124=CARTESIAN_POINT('Ctrl Pts',(2.56439223365444,0.976583941164728,
12.5078201359221));
#448125=CARTESIAN_POINT('Ctrl Pts',(2.5647891438738,0.975704145568934,12.5072563000949));
#448126=CARTESIAN_POINT('Ctrl Pts',(2.56514677476629,0.974747924396236,
12.5068768744332));
#448127=CARTESIAN_POINT('Ctrl Pts',(2.56540465125918,0.97405842310423,12.5066032824114));
#448128=CARTESIAN_POINT('Ctrl Pts',(2.56564669160147,0.973317092615597,
12.5064197834844));
#448129=CARTESIAN_POINT('Ctrl Pts',(2.56586183683818,0.97256613301322,12.5063282718343));
#448130=CARTESIAN_POINT('Ctrl Pts',(2.5661758822765,0.971469964484967,12.5061946931565));
#448131=CARTESIAN_POINT('Ctrl Pts',(2.56644035587931,0.970330142484219,
12.5062515701262));
#448132=CARTESIAN_POINT('Ctrl Pts',(2.56665390827765,0.969220901756571,
12.5064436508398));
#448133=CARTESIAN_POINT('',(2.5130333191225,0.920299837513742,12.5737548217797));
#448134=CARTESIAN_POINT('Origin',(2.52764095826809,0.925649312122715,12.5893111709658));
#448135=CARTESIAN_POINT('Ctrl Pts',(2.56665390827765,0.96922090175657,12.5064436508398));
#448136=CARTESIAN_POINT('Ctrl Pts',(2.5587169918014,0.961978958329554,12.5164271754438));
#448137=CARTESIAN_POINT('Ctrl Pts',(2.55077678830534,0.954734298540301,
12.5264061185523));
#448138=CARTESIAN_POINT('Ctrl Pts',(2.54283318266135,0.94748682602163,12.536380305637));
#448139=CARTESIAN_POINT('Ctrl Pts',(2.53290528674318,0.938428955319102,
12.5488460165097));
#448140=CARTESIAN_POINT('Ctrl Pts',(2.52297207374467,0.929366688495138,
12.5613043021964));
#448141=CARTESIAN_POINT('Ctrl Pts',(2.5130333191225,0.920299837513742,12.5737548217797));
#448142=CARTESIAN_POINT('Ctrl Pts',(2.53435070432089,0.882188624381805,
12.5893111709658));
#448143=CARTESIAN_POINT('Ctrl Pts',(2.52302979479691,0.882732354194987,
12.5770542771492));
#448144=CARTESIAN_POINT('Ctrl Pts',(2.52075360628342,0.898937990273401,
12.5737548217797));
#448145=CARTESIAN_POINT('Ctrl Pts',(2.5237883941991,0.882695919568392,12.5928319619712));
#448146=CARTESIAN_POINT('Ctrl Pts',(2.51633632903146,0.886315331275931,
12.5821634970843));
#448147=CARTESIAN_POINT('Ctrl Pts',(2.51690555955102,0.899113357643908,
12.5773203894503));
#448148=CARTESIAN_POINT('Ctrl Pts',(2.50891707740886,0.890404877751204,
12.5969440695591));
#448149=CARTESIAN_POINT('Ctrl Pts',(2.50753362883541,0.894179081322358,
12.5878292599214));
#448150=CARTESIAN_POINT('Ctrl Pts',(2.51160606038543,0.901862804077567,
12.5813877129824));
#448151=CARTESIAN_POINT('Ctrl Pts',(2.49846679338592,0.919161908359058,
12.596957478804));
#448152=CARTESIAN_POINT('Ctrl Pts',(2.49984009316504,0.915415624751862,
12.5878468778671));
#448153=CARTESIAN_POINT('Ctrl Pts',(2.50787136527611,0.912157381326999,
12.5814011370086));
#448154=CARTESIAN_POINT('Ctrl Pts',(2.50497190837032,0.934718980261566,
12.5928371701607));
#448155=CARTESIAN_POINT('Ctrl Pts',(2.50156352785204,0.92717457783683,12.5821692192952));
#448156=CARTESIAN_POINT('Ctrl Pts',(2.51017719986325,0.917696789252394,
12.5773318885715));
#448157=CARTESIAN_POINT('Ctrl Pts',(2.5127808063358,0.941872008709643,12.5893111709658));
#448158=CARTESIAN_POINT('Ctrl Pts',(2.50442319798707,0.934216356075868,
12.5770542771492));
#448159=CARTESIAN_POINT('Ctrl Pts',(2.51303331912246,0.920299837513782,
12.5737548217797));
#448160=CARTESIAN_POINT('',(2.52075360628342,0.898937990273401,12.5737548217797));
#448161=CARTESIAN_POINT('Origin',(2.53540612154271,0.904163293764707,12.5893111709658));
#448162=CARTESIAN_POINT('Ctrl Pts',(2.51303331912246,0.920299837513782,
12.5737548217797));
#448163=CARTESIAN_POINT('Ctrl Pts',(2.51227264794842,0.919647381388047,
12.5746934679442));
#448164=CARTESIAN_POINT('Ctrl Pts',(2.51155017704798,0.91878635221534,12.5756680099006));
#448165=CARTESIAN_POINT('Ctrl Pts',(2.5109455521328,0.917816851116875,12.5765688348656));
#448166=CARTESIAN_POINT('Ctrl Pts',(2.51078548437992,0.917560186433789,
12.5768073183026));
#448167=CARTESIAN_POINT('Ctrl Pts',(2.51063349759762,0.917296104347685,
12.5770407398754));
#448168=CARTESIAN_POINT('Ctrl Pts',(2.51049058932504,0.917026756304196,
12.5772674179684));
#448169=CARTESIAN_POINT('Ctrl Pts',(2.50990413241841,0.9159214247685,12.5781976435658));
#448170=CARTESIAN_POINT('Ctrl Pts',(2.50944721800345,0.914659344461954,
12.5790594849312));
#448171=CARTESIAN_POINT('Ctrl Pts',(2.50919610286065,0.913309294867038,
12.5797571720116));
#448172=CARTESIAN_POINT('Ctrl Pts',(2.50903249231582,0.912429689012493,
12.580211740231));
#448173=CARTESIAN_POINT('Ctrl Pts',(2.50896726443021,0.911469333711957,
12.5806009430798));
#448174=CARTESIAN_POINT('Ctrl Pts',(2.50902268693475,0.910494633239858,
12.5808812374708));
#448175=CARTESIAN_POINT('Ctrl Pts',(2.50907031325237,0.909657042180811,
12.5811221033394));
#448176=CARTESIAN_POINT('Ctrl Pts',(2.5092081229626,0.908791716671847,12.581287365893));
#448177=CARTESIAN_POINT('Ctrl Pts',(2.5094365720762,0.907948808440815,12.581359338449));
#448178=CARTESIAN_POINT('Ctrl Pts',(2.5094683217857,0.907831661602089,12.5813693411482));
#448179=CARTESIAN_POINT('Ctrl Pts',(2.50950177295079,0.907714913729678,
12.5813775999465));
#448180=CARTESIAN_POINT('Ctrl Pts',(2.50953687694806,0.907598663701455,
12.5813841266931));
#448181=CARTESIAN_POINT('Ctrl Pts',(2.50959643512516,0.907401431468428,
12.5813952001081));
#448182=CARTESIAN_POINT('Ctrl Pts',(2.50966173278532,0.907204487335008,
12.5814007534795));
#448183=CARTESIAN_POINT('Ctrl Pts',(2.50973292867859,0.907007979140197,
12.5814005856065));
#448184=CARTESIAN_POINT('Ctrl Pts',(2.51005883564221,0.906108441454079,
12.5813998171494));
#448185=CARTESIAN_POINT('Ctrl Pts',(2.51048550217453,0.905280074825782,
12.58127954464));
#448186=CARTESIAN_POINT('Ctrl Pts',(2.51098420087793,0.904514033240517,
12.5810700125799));
#448187=CARTESIAN_POINT('Ctrl Pts',(2.51158657213025,0.903588742226335,
12.5808169217085));
#448188=CARTESIAN_POINT('Ctrl Pts',(2.51230811772037,0.902763429969774,
12.5804173076348));
#448189=CARTESIAN_POINT('Ctrl Pts',(2.51306599664491,0.902093284535271,
12.5799304713245));
#448190=CARTESIAN_POINT('Ctrl Pts',(2.51400524738891,0.901262763224338,
12.5793271277669));
#448191=CARTESIAN_POINT('Ctrl Pts',(2.51503723600979,0.900594921705148,
12.5785808224116));
#448192=CARTESIAN_POINT('Ctrl Pts',(2.51610123044773,0.900091283244504,
12.5777485681082));
#448193=CARTESIAN_POINT('Ctrl Pts',(2.51768669872955,0.899340806760433,
12.576508418016));
#448194=CARTESIAN_POINT('Ctrl Pts',(2.51932694338654,0.898955038726519,
12.5750928681475));
#448195=CARTESIAN_POINT('Ctrl Pts',(2.52075360628342,0.898937990273401,
12.5737548217797));
#448196=CARTESIAN_POINT('Ctrl Pts',(2.52075360628342,0.898937990273401,
12.5737548217797));
#448197=CARTESIAN_POINT('Ctrl Pts',(2.52302979479691,0.882732354194987,
12.5770542771492));
#448198=CARTESIAN_POINT('Ctrl Pts',(2.53435070432089,0.882188624381805,
12.5893111709658));
#448199=CARTESIAN_POINT('Ctrl Pts',(2.54548660483675,0.897800564789506,
12.5508408821982));
#448200=CARTESIAN_POINT('Ctrl Pts',(2.54776666288385,0.881544271856277,
12.55409748406));
#448201=CARTESIAN_POINT('Ctrl Pts',(2.55910201498895,0.880999848383104,
12.5663972313419));
#448202=CARTESIAN_POINT('Ctrl Pts',(2.57019538818008,0.896663072159344,
12.52790050457));
#448203=CARTESIAN_POINT('Ctrl Pts',(2.5724561539806,0.880358464978034,12.5311362602938));
#448204=CARTESIAN_POINT('Ctrl Pts',(2.58382835565171,0.879812271664045,
12.5434568539655));
#448205=CARTESIAN_POINT('Ctrl Pts',(2.59488183750983,0.895525503767571,
12.5049357605811));
#448206=CARTESIAN_POINT('Ctrl Pts',(2.59710320689608,0.879174696355115,
12.5081700652078));
#448207=CARTESIAN_POINT('Ctrl Pts',(2.60853168196507,0.878625800296802,
12.5204921097672));
#448208=CARTESIAN_POINT('Ctrl Pts',(2.59326082840587,0.895600199381859,
12.5064436508395));
#448209=CARTESIAN_POINT('Ctrl Pts',(2.59384945736741,0.894531385208946,
12.5062361689309));
#448210=CARTESIAN_POINT('Ctrl Pts',(2.59441600670797,0.893394805486641,
12.5061871075061));
#448211=CARTESIAN_POINT('Ctrl Pts',(2.59490169053566,0.892265589891358,
12.5063648335164));
#448212=CARTESIAN_POINT('Ctrl Pts',(2.59512231808842,0.891752630515074,
12.5064455676329));
#448213=CARTESIAN_POINT('Ctrl Pts',(2.59532913365264,0.891233948988439,
12.506574497099));
#448214=CARTESIAN_POINT('Ctrl Pts',(2.59551229338953,0.89073139557313,12.5067492519495));
#448215=CARTESIAN_POINT('Ctrl Pts',(2.59588035999054,0.88972149497742,12.5071004286051));
#448216=CARTESIAN_POINT('Ctrl Pts',(2.59616567170592,0.888739316481922,
12.5076537929612));
#448217=CARTESIAN_POINT('Ctrl Pts',(2.59635589737542,0.887861216236564,
12.5083435010503));
#448218=CARTESIAN_POINT('Ctrl Pts',(2.59636787321813,0.887805934578458,
12.5083869222963));
#448219=CARTESIAN_POINT('Ctrl Pts',(2.59637946183328,0.887751056874326,
12.5084308732336));
#448220=CARTESIAN_POINT('Ctrl Pts',(2.59639065617788,0.887696598388155,
12.5084753333615));
#448221=CARTESIAN_POINT('Ctrl Pts',(2.59648044959668,0.887259769451156,
12.508831962269));
#448222=CARTESIAN_POINT('Ctrl Pts',(2.59654796164586,0.886841305065423,
12.509227847131));
#448223=CARTESIAN_POINT('Ctrl Pts',(2.5965939491494,0.886454094332113,12.5096423454524));
#448224=CARTESIAN_POINT('Ctrl Pts',(2.59673805363227,0.88524074726621,12.5109411997424));
#448225=CARTESIAN_POINT('Ctrl Pts',(2.59668926917174,0.88426079718275,12.5124831113042));
#448226=CARTESIAN_POINT('Ctrl Pts',(2.59653225864578,0.88347195868837,12.5140723025008));
#448227=CARTESIAN_POINT('Ctrl Pts',(2.59651754658752,0.883398043657455,
12.5142212114565));
#448228=CARTESIAN_POINT('Ctrl Pts',(2.59650190446177,0.883325784869281,
12.5143705582413));
#448229=CARTESIAN_POINT('Ctrl Pts',(2.59648541455998,0.883255136195124,
12.5145201959299));
#448230=CARTESIAN_POINT('Ctrl Pts',(2.59627357722047,0.882347548790702,
12.5164425148273));
#448231=CARTESIAN_POINT('Ctrl Pts',(2.59592502832276,0.881672144137725,
12.5184635205941));
#448232=CARTESIAN_POINT('Ctrl Pts',(2.59548773681026,0.881152522242616,
12.5205025929158));
#448233=CARTESIAN_POINT('Ctrl Pts',(2.59523409040039,0.880851120947565,
12.5216853356836));
#448234=CARTESIAN_POINT('Ctrl Pts',(2.59495141505961,0.880602365231525,
12.5228750347131));
#448235=CARTESIAN_POINT('Ctrl Pts',(2.59465389781798,0.880394780695765,
12.5240609649613));
#448236=CARTESIAN_POINT('Ctrl Pts',(2.59392365770967,0.879885275589271,
12.5269717671326));
#448237=CARTESIAN_POINT('Ctrl Pts',(2.5930775049986,0.879617984403987,12.5299036066169));
#448238=CARTESIAN_POINT('Ctrl Pts',(2.59215448896836,0.879515546451699,
12.5328133004019));
#448239=CARTESIAN_POINT('Ctrl Pts',(2.59171138752823,0.879466370269818,
12.5342101228451));
#448240=CARTESIAN_POINT('Ctrl Pts',(2.59125106753872,0.879455767726765,
12.5356023438238));
#448241=CARTESIAN_POINT('Ctrl Pts',(2.59077959786117,0.879478411772317,
12.5369868989719));
#448242=CARTESIAN_POINT('Origin',(15.3207548595525,0.262770591828722,-1.23958748038645));
#448243=CARTESIAN_POINT('Ctrl Pts',(2.5544083265803,0.980003286420626,12.5369868989719));
#448244=CARTESIAN_POINT('Ctrl Pts',(2.56573885673312,0.990342647626308,
12.5369868989719));
#448245=CARTESIAN_POINT('Ctrl Pts',(2.55995520476251,1.00454943028701,12.5369868989719));
#448246=CARTESIAN_POINT('Ctrl Pts',(2.55823844427557,0.983498443787384,
12.5218025310016));
#448247=CARTESIAN_POINT('Ctrl Pts',(2.56438145462366,0.993593952074142,
12.5216901060417));
#448248=CARTESIAN_POINT('Ctrl Pts',(2.55997285052496,1.00450612952355,12.5161920673677));
#448249=CARTESIAN_POINT('Ctrl Pts',(2.5641361074036,0.982251992495257,12.5042015548895));
#448250=CARTESIAN_POINT('Ctrl Pts',(2.56640058060124,0.988272748772843,
12.4980677368514));
#448251=CARTESIAN_POINT('Ctrl Pts',(2.56395255651642,0.994612934716805,
12.4907278922778));
#448252=CARTESIAN_POINT('Ctrl Pts',(2.56663519685345,0.969213835929737,
12.506463626192));
#448253=CARTESIAN_POINT('Ctrl Pts',(2.57275606532212,0.971525200791801,
12.4999376786891));
#448254=CARTESIAN_POINT('Ctrl Pts',(2.57268130781351,0.971496970830732,
12.4906970594712));
#448255=CARTESIAN_POINT('Origin',(2.53957902034697,0.996254184138538,12.5369868989719));
#448256=CARTESIAN_POINT('Origin',(2.53957902034697,0.996254184138538,14.));
#448257=CARTESIAN_POINT('Origin',(2.53957902034697,0.996254184138538,13.7435492065112));
#448258=CARTESIAN_POINT('Ctrl Pts',(2.53618116965488,0.963307011803056,
13.793642941384));
#448259=CARTESIAN_POINT('Ctrl Pts',(2.54417248413818,0.970590219326861,
13.8071662555867));
#448260=CARTESIAN_POINT('Ctrl Pts',(2.53467628861993,0.984726755476637,
13.8103758687955));
#448261=CARTESIAN_POINT('Ctrl Pts',(2.54843750908966,0.974533936977943,
13.7804579775006));
#448262=CARTESIAN_POINT('Ctrl Pts',(2.55829123798887,0.983528251766164,
13.7901904343351));
#448263=CARTESIAN_POINT('Ctrl Pts',(2.55173723236927,0.997856578064193,
13.7927914348262));
#448264=CARTESIAN_POINT('Ctrl Pts',(2.55565327734718,0.981143650373165,
13.7597120340895));
#448265=CARTESIAN_POINT('Ctrl Pts',(2.56705295344843,0.991556837913933,
13.7635825532445));
#448266=CARTESIAN_POINT('Ctrl Pts',(2.56178246121564,1.00561947734499,13.7651073818884));
#448267=CARTESIAN_POINT('Ctrl Pts',(2.5542402646995,0.979849317145748,13.7381884353898));
#448268=CARTESIAN_POINT('Ctrl Pts',(2.56537371634972,0.990018100995272,
13.7368803041982));
#448269=CARTESIAN_POINT('Ctrl Pts',(2.55981500470216,1.00409966205711,13.7363986145813));
#448270=CARTESIAN_POINT('Origin',(2.52429501445587,0.982253882249225,13.7902182540695));
#448271=CARTESIAN_POINT('Ctrl Pts',(2.51277790328901,0.94186935051894,13.8235227101244));
#448272=CARTESIAN_POINT('Ctrl Pts',(2.52125878487692,0.949631910393832,
13.8358800583119));
#448273=CARTESIAN_POINT('Ctrl Pts',(2.51244524948572,0.963665713975349,
13.8390832900376));
#448274=CARTESIAN_POINT('Ctrl Pts',(2.52157324423867,0.94992597058406,13.8124254819052));
#448275=CARTESIAN_POINT('Ctrl Pts',(2.53007059539059,0.957703605445395,
13.8247886449157));
#448276=CARTESIAN_POINT('Ctrl Pts',(2.52123148983817,0.971746076529041,
13.8279860620657));
#448277=CARTESIAN_POINT('Ctrl Pts',(2.53036464340266,0.957978979934154,
13.8013225099955));
#448278=CARTESIAN_POINT('Ctrl Pts',(2.53887445608688,0.965768018508477,
13.8136962257787));
#448279=CARTESIAN_POINT('Ctrl Pts',(2.53001384607715,0.979822498759896,
13.8168830918626));
#448280=CARTESIAN_POINT('Ctrl Pts',(2.53915225414983,0.966028519056621,
13.7902140179785));
#448281=CARTESIAN_POINT('Ctrl Pts',(2.54767078228692,0.973825530017369,
13.802602731458));
#448282=CARTESIAN_POINT('Ctrl Pts',(2.53879247206465,0.987895134138251,
13.8057746032558));
#448283=CARTESIAN_POINT('Origin',(2.49792065440358,0.958094705296493,13.8235269408515));
#448284=CARTESIAN_POINT('Ctrl Pts',(2.53435070432089,0.882188624381805,
13.8235269408515));
#448285=CARTESIAN_POINT('Ctrl Pts',(2.54614459076024,0.881622178050192,
13.8362179249168));
#448286=CARTESIAN_POINT('Ctrl Pts',(2.54809516572306,0.864655791830034,
13.8391868794938));
#448287=CARTESIAN_POINT('Ctrl Pts',(2.52355981158623,0.882706898119287,
13.8400110824519));
#448288=CARTESIAN_POINT('Ctrl Pts',(2.53285150606145,0.878835686856507,
13.8494522556837));
#448289=CARTESIAN_POINT('Ctrl Pts',(2.53034179279955,0.86562095164239,13.85569149686));
#448290=CARTESIAN_POINT('Ctrl Pts',(2.50903339505441,0.890081242075895,
13.8586819406588));
#448291=CARTESIAN_POINT('Ctrl Pts',(2.51052629600454,0.885991341051656,
13.868010383617));
#448292=CARTESIAN_POINT('Ctrl Pts',(2.50629374135306,0.87799269442146,13.8744918421245));
#448293=CARTESIAN_POINT('Ctrl Pts',(2.49834865421076,0.919490557114688,
13.8587686893867));
#448294=CARTESIAN_POINT('Ctrl Pts',(2.49686898717052,0.923544038750251,
13.8680909899357));
#448295=CARTESIAN_POINT('Ctrl Pts',(2.48850920386329,0.926951446058171,
13.8745789365163));
#448296=CARTESIAN_POINT('Ctrl Pts',(2.50480151728297,0.93456290033434,13.8400379222776));
#448297=CARTESIAN_POINT('Ctrl Pts',(2.50946394083728,0.943480974145899,
13.8494748685453));
#448298=CARTESIAN_POINT('Ctrl Pts',(2.49909130647347,0.952034894978994,
13.8557104837033));
#448299=CARTESIAN_POINT('Ctrl Pts',(2.51278080633127,0.94187200871438,13.8235269408542));
#448300=CARTESIAN_POINT('Ctrl Pts',(2.52148758766895,0.94984750728991,13.8362179249195));
#448301=CARTESIAN_POINT('Ctrl Pts',(2.51214073195049,0.964140837630829,
13.8391868794965));
#448302=CARTESIAN_POINT('Origin',(2.53329528709906,0.860213954998902,13.8235269408515));
#448303=CARTESIAN_POINT('Ctrl Pts',(2.57007250605579,0.880472947990599,
13.7902140241682));
#448304=CARTESIAN_POINT('Ctrl Pts',(2.58160752158498,0.879923391684029,
13.8026027327198));
#448305=CARTESIAN_POINT('Ctrl Pts',(2.5837753539635,0.863428591441144,13.8057746032556));
#448306=CARTESIAN_POINT('Ctrl Pts',(2.55816913106018,0.881044652928356,
13.8013225161807));
#448307=CARTESIAN_POINT('Ctrl Pts',(2.56969234802928,0.880495655142914,
13.8136962270464));
#448308=CARTESIAN_POINT('Ctrl Pts',(2.57186412217919,0.864023800288172,
13.8168830918628));
#448309=CARTESIAN_POINT('Ctrl Pts',(2.54626062441251,0.881616604333268,
13.8124254880876));
#448310=CARTESIAN_POINT('Ctrl Pts',(2.5577669686007,0.881068408689682,13.8247886461868));
#448311=CARTESIAN_POINT('Ctrl Pts',(2.55994760105066,0.86461953625668,13.8279860620656));
#448312=CARTESIAN_POINT('Ctrl Pts',(2.53434677836339,0.882188812183291,
13.8235227163065));
#448313=CARTESIAN_POINT('Ctrl Pts',(2.54583082072181,0.881641679341152,
13.8358800595847));
#448314=CARTESIAN_POINT('Ctrl Pts',(2.54802557414951,0.865215818992596,
13.8390832900376));
#448315=CARTESIAN_POINT('Origin',(2.56902102722067,0.85849809021251,13.7902182540695));
#448316=CARTESIAN_POINT('Ctrl Pts',(2.59051004735031,0.879491330346339,
13.7382347919292));
#448317=CARTESIAN_POINT('Ctrl Pts',(2.60558412847211,0.878791368156842,
13.7369371795943));
#448318=CARTESIAN_POINT('Ctrl Pts',(2.61030799135417,0.864395921081753,
13.7364597369711));
#448319=CARTESIAN_POINT('Ctrl Pts',(2.59239942805721,0.879400586041886,
13.7595490285574));
#448320=CARTESIAN_POINT('Ctrl Pts',(2.60783311719664,0.878682919012028,
13.7633824266925));
#448321=CARTESIAN_POINT('Ctrl Pts',(2.61276204814568,0.864484352182699,
13.7648920890506));
#448322=CARTESIAN_POINT('Ctrl Pts',(2.58276368996126,0.879863377031185,
13.7803806590111));
#448323=CARTESIAN_POINT('Ctrl Pts',(2.5961135294197,0.879248013367294,13.7901039518745));
#448324=CARTESIAN_POINT('Ctrl Pts',(2.60025086493429,0.864037231130171,
13.7926933640892));
#448325=CARTESIAN_POINT('Ctrl Pts',(2.56601462617966,0.880667811001527,
13.7936647693663));
#448326=CARTESIAN_POINT('Ctrl Pts',(2.57681899087517,0.88017889846247,13.8072068914933));
#448327=CARTESIAN_POINT('Ctrl Pts',(2.57854585859628,0.863218291229214,
13.8104111085397));
#448328=CARTESIAN_POINT('Origin',(2.58972418063935,0.857503742389414,13.7435492065112));
#448329=CARTESIAN_POINT('Origin',(2.58972418063935,0.857503742389415,14.));
#448330=CARTESIAN_POINT('Origin',(2.58972418063935,0.857503742389415,12.5369868989719));
#448331=CARTESIAN_POINT('Ctrl Pts',(2.59324345222295,0.895594198410246,
12.506462012331));
#448332=CARTESIAN_POINT('Ctrl Pts',(2.59942388090557,0.89772865133525,12.4999388158272));
#448333=CARTESIAN_POINT('Ctrl Pts',(2.59935075832912,0.897703397957985,
12.4907030323752));
#448334=CARTESIAN_POINT('Ctrl Pts',(2.59965522889214,0.883970184340286,
12.5042014951932));
#448335=CARTESIAN_POINT('Ctrl Pts',(2.60524363939895,0.88079044140674,12.4980716682126));
#448336=CARTESIAN_POINT('Ctrl Pts',(2.6074145173087,0.874355159413935,12.4907355092743));
#448337=CARTESIAN_POINT('Ctrl Pts',(2.59591946047918,0.879240518854148,
12.521804744651));
#448338=CARTESIAN_POINT('Ctrl Pts',(2.60709142493367,0.875405667988131,
12.5216906929435));
#448339=CARTESIAN_POINT('Ctrl Pts',(2.61067940057473,0.864203115371447,
12.5161988840776));
#448340=CARTESIAN_POINT('Ctrl Pts',(2.59074122437161,0.879480221225811,
12.5369868989719));
#448341=CARTESIAN_POINT('Ctrl Pts',(2.60605472464864,0.878771531740491,
12.5369868989719));
#448342=CARTESIAN_POINT('Ctrl Pts',(2.6106930131041,0.864160172743973,12.5369868989719));
#448343=CARTESIAN_POINT('Origin',(4.84514877968059E-31,-3.40079961985215E-31,
12.5));
#448344=CARTESIAN_POINT('Origin',(2.45401129869475,1.0858263246758,12.5));
#448345=CARTESIAN_POINT('',(2.45401129869475,1.0858263246758,12.5893111709658));
#448346=CARTESIAN_POINT('',(2.45401129869475,1.0858263246758,13.8235269408515));
#448347=CARTESIAN_POINT('',(2.45401129869475,1.0858263246758,12.5));
#448348=CARTESIAN_POINT('',(2.48975802327266,1.08702814876944,13.7902182540695));
#448349=CARTESIAN_POINT('',(2.45401129869475,1.0858263246758,13.8235269408515));
#448350=CARTESIAN_POINT('',(2.51047333723489,1.08772460875902,13.7435492065112));
#448351=CARTESIAN_POINT('Origin',(2.4423202171704,1.08543359017029,13.7445212918704));
#448352=CARTESIAN_POINT('',(2.51047333723489,1.08772460875902,12.5369868989719));
#448353=CARTESIAN_POINT('',(2.51047333723489,1.08772460875902,12.5));
#448354=CARTESIAN_POINT('Ctrl Pts',(2.51047333723489,1.08772460875902,12.5369868989719));
#448355=CARTESIAN_POINT('Ctrl Pts',(2.49166638438045,1.0870923088956,12.5544431401645));
#448356=CARTESIAN_POINT('Ctrl Pts',(2.47284598029346,1.08645955679451,12.5718848856037));
#448357=CARTESIAN_POINT('Ctrl Pts',(2.45401129869475,1.0858263246758,12.5893111709658));
#448358=CARTESIAN_POINT('Origin',(2.61461687993057,1.34521555026705,12.5));
#448359=CARTESIAN_POINT('',(2.46605782225597,1.18498102042076,13.7435492065112));
#448360=CARTESIAN_POINT('',(2.45196582721007,1.16978151501113,13.7902182540695));
#448361=CARTESIAN_POINT('Origin',(2.41493449982007,1.12983984180181,13.7418732680468));
#448362=CARTESIAN_POINT('',(2.42764842286963,1.14355297053484,13.8235269408515));
#448363=CARTESIAN_POINT('',(2.45196582721007,1.16978151501113,13.7902182540695));
#448364=CARTESIAN_POINT('',(2.42764842286963,1.14355297053484,12.5893111709658));
#448365=CARTESIAN_POINT('',(2.42764842286963,1.14355297053484,12.5));
#448366=CARTESIAN_POINT('',(2.46605782225597,1.18498102042076,12.5369868989719));
#448367=CARTESIAN_POINT('Ctrl Pts',(2.42764842286963,1.14355297053484,12.5893111709658));
#448368=CARTESIAN_POINT('Ctrl Pts',(2.44046108118917,1.15737259428616,12.5718848856037));
#448369=CARTESIAN_POINT('Ctrl Pts',(2.45326402695379,1.17118174215875,12.5544431401645));
#448370=CARTESIAN_POINT('Ctrl Pts',(2.46605782225597,1.18498102042076,12.5369868989719));
#448371=CARTESIAN_POINT('',(2.46605782225597,1.18498102042076,12.5));
#448372=CARTESIAN_POINT('Origin',(2.45285624533615,1.12018191340222,12.5));
#448373=CARTESIAN_POINT('',(2.42206997748234,1.10489152806335,13.8587068136939));
#448374=CARTESIAN_POINT('Ctrl Pts',(2.42764842286468,1.14355297053923,13.8235269408542));
#448375=CARTESIAN_POINT('Ctrl Pts',(2.42645706099368,1.14226797780794,13.8262006681044));
#448376=CARTESIAN_POINT('Ctrl Pts',(2.42536528244755,1.14083485267795,13.8288634856214));
#448377=CARTESIAN_POINT('Ctrl Pts',(2.42436690471821,1.13926540965906,13.8314912288862));
#448378=CARTESIAN_POINT('Ctrl Pts',(2.42333768025715,1.13764747578712,13.834200161153));
#448379=CARTESIAN_POINT('Ctrl Pts',(2.42240615489842,1.13588313987818,13.8368750301949));
#448380=CARTESIAN_POINT('Ctrl Pts',(2.42158932736391,1.13394690076675,13.8394886372968));
#448381=CARTESIAN_POINT('Ctrl Pts',(2.42152624179207,1.13379736032351,13.8396904925131));
#448382=CARTESIAN_POINT('Ctrl Pts',(2.42146385899365,1.1336467825078,13.8398919674349));
#448383=CARTESIAN_POINT('Ctrl Pts',(2.42140219692688,1.13349515024217,13.8400930404591));
#448384=CARTESIAN_POINT('Ctrl Pts',(2.42044146044229,1.13113261753052,13.8432258934518));
#448385=CARTESIAN_POINT('Ctrl Pts',(2.41965954656088,1.12852658845066,13.8462331177034));
#448386=CARTESIAN_POINT('Ctrl Pts',(2.41917435403413,1.12573433484191,13.8489036603661));
#448387=CARTESIAN_POINT('Ctrl Pts',(2.41901559339291,1.12482067696604,13.8497774930041));
#448388=CARTESIAN_POINT('Ctrl Pts',(2.4188887726382,1.12388726308532,13.85061494757));
#448389=CARTESIAN_POINT('Ctrl Pts',(2.41879850091015,1.12293662922273,13.8514076489583));
#448390=CARTESIAN_POINT('Ctrl Pts',(2.41860756318619,1.12092590150143,13.8530843267192));
#448391=CARTESIAN_POINT('Ctrl Pts',(2.41856432936575,1.11864034840778,13.8546805203176));
#448392=CARTESIAN_POINT('Ctrl Pts',(2.4188077300259,1.11621004205749,13.8559412814274));
#448393=CARTESIAN_POINT('Ctrl Pts',(2.4188403049279,1.11588478825113,13.8561100121513));
#448394=CARTESIAN_POINT('Ctrl Pts',(2.41887795059011,1.11555698544893,13.8562727473908));
#448395=CARTESIAN_POINT('Ctrl Pts',(2.41892093274999,1.11522698044344,13.8564289040185));
#448396=CARTESIAN_POINT('Ctrl Pts',(2.4191158563547,1.11373041150834,13.8571370725437));
#448397=CARTESIAN_POINT('Ctrl Pts',(2.41942621459317,1.11216254030716,13.8577210840554));
#448398=CARTESIAN_POINT('Ctrl Pts',(2.41986873320903,1.11059000910466,13.8581177131616));
#448399=CARTESIAN_POINT('Ctrl Pts',(2.41999336168228,1.11014713019316,13.8582294175695));
#448400=CARTESIAN_POINT('Ctrl Pts',(2.42012829576111,1.10970386797704,13.8583265086086));
#448401=CARTESIAN_POINT('Ctrl Pts',(2.42027347360095,1.10926165119297,13.8584082369006));
#448402=CARTESIAN_POINT('Ctrl Pts',(2.42048205522583,1.10862630425939,13.8585256585398));
#448403=CARTESIAN_POINT('Ctrl Pts',(2.42071468237932,1.10798531730301,13.8586122832068));
#448404=CARTESIAN_POINT('Ctrl Pts',(2.42096605439541,1.10735561070772,13.8586682984299));
#448405=CARTESIAN_POINT('Ctrl Pts',(2.42116712709058,1.1068519078523,13.8587131050557));
#448406=CARTESIAN_POINT('Ctrl Pts',(2.42138219660225,1.10634977230495,13.8587357943552));
#448407=CARTESIAN_POINT('Ctrl Pts',(2.42161175402798,1.1058493437941,13.8587355499465));
#448408=CARTESIAN_POINT('Ctrl Pts',(2.42176012246511,1.10552590491679,13.8587353919793));
#448409=CARTESIAN_POINT('Ctrl Pts',(2.42191290341701,1.10520666062785,13.8587257282814));
#448410=CARTESIAN_POINT('Ctrl Pts',(2.42206997748234,1.10489152806335,13.8587068136939));
#448411=CARTESIAN_POINT('Ctrl Pts',(2.42206997748234,1.10489152806335,13.8587068136939));
#448412=CARTESIAN_POINT('Ctrl Pts',(2.42258658552026,1.10385507423829,13.8586446046466));
#448413=CARTESIAN_POINT('Ctrl Pts',(2.42314957595238,1.10286304208167,13.858482427929));
#448414=CARTESIAN_POINT('Ctrl Pts',(2.42375522096753,1.1019129639264,13.8582284286032));
#448415=CARTESIAN_POINT('Ctrl Pts',(2.42437654230153,1.10093829425675,13.8579678548414));
#448416=CARTESIAN_POINT('Ctrl Pts',(2.42504556417679,1.10000622101151,13.857615680862));
#448417=CARTESIAN_POINT('Ctrl Pts',(2.42572803911843,1.09914784029088,13.8571944833187));
#448418=CARTESIAN_POINT('Ctrl Pts',(2.42743122513308,1.09700566341456,13.8561433417727));
#448419=CARTESIAN_POINT('Ctrl Pts',(2.42929411337666,1.09521925713392,13.8546163505474));
#448420=CARTESIAN_POINT('Ctrl Pts',(2.43111074893032,1.09377017048553,13.8528973491086));
#448421=CARTESIAN_POINT('Ctrl Pts',(2.43144262144402,1.09350544373414,13.8525833129072));
#448422=CARTESIAN_POINT('Ctrl Pts',(2.43177292319813,1.09325183595566,13.8522628768812));
#448423=CARTESIAN_POINT('Ctrl Pts',(2.43210039201653,1.09300905596031,13.851937733538));
#448424=CARTESIAN_POINT('Ctrl Pts',(2.43410019865623,1.09152643221291,13.8499521282529));
#448425=CARTESIAN_POINT('Ctrl Pts',(2.43619552649437,1.09030354834289,13.847639871647));
#448426=CARTESIAN_POINT('Ctrl Pts',(2.43823575644318,1.08933528679105,13.8452109780794));
#448427=CARTESIAN_POINT('Ctrl Pts',(2.43915369812781,1.08889964587687,13.8441181685877));
#448428=CARTESIAN_POINT('Ctrl Pts',(2.44006042192786,1.08851483294368,13.8430021611332));
#448429=CARTESIAN_POINT('Ctrl Pts',(2.4409429470759,1.08817715631235,13.8418824960098));
#448430=CARTESIAN_POINT('Ctrl Pts',(2.44302264012336,1.08738141270774,13.8392439765549));
#448431=CARTESIAN_POINT('Ctrl Pts',(2.44506601942868,1.08680585456423,13.8364981347964));
#448432=CARTESIAN_POINT('Ctrl Pts',(2.44706921107542,1.0864160209339,13.8336931113419));
#448433=CARTESIAN_POINT('Ctrl Pts',(2.4490201925249,1.08603634773468,13.8309611966328));
#448434=CARTESIAN_POINT('Ctrl Pts',(2.4509351167424,1.08583301751496,13.8281701127186));
#448435=CARTESIAN_POINT('Ctrl Pts',(2.45280336318841,1.08581285823271,13.8253580685121));
#448436=CARTESIAN_POINT('Ctrl Pts',(2.45320840103418,1.08580848767856,13.8247484142933));
#448437=CARTESIAN_POINT('Ctrl Pts',(2.45361114990772,1.08581287145851,13.8241378483365));
#448438=CARTESIAN_POINT('Ctrl Pts',(2.45401129869475,1.0858263246758,13.8235269408515));
#448439=CARTESIAN_POINT('',(2.42153762191903,1.10601374658571,12.5969504640361));
#448440=CARTESIAN_POINT('Origin',(2.45288642222602,1.12019547946754,12.584524458991));
#448441=CARTESIAN_POINT('Origin',(2.45288642222602,1.12019547946754,12.584524458991));
#448442=CARTESIAN_POINT('Ctrl Pts',(2.42764842286963,1.14355297053484,12.5893111709658));
#448443=CARTESIAN_POINT('Ctrl Pts',(2.41994263053449,1.13524156878499,12.5770542771492));
#448444=CARTESIAN_POINT('Ctrl Pts',(2.42965842765955,1.12207316109538,12.5737548217797));
#448445=CARTESIAN_POINT('Ctrl Pts',(2.4444984045658,1.16172721677244,12.5663937883685));
#448446=CARTESIAN_POINT('Ctrl Pts',(2.43678278242238,1.1534052126754,12.5540940315304));
#448447=CARTESIAN_POINT('Ctrl Pts',(2.44653127082073,1.14019790525636,12.5508374392248));
#448448=CARTESIAN_POINT('Ctrl Pts',(2.46133138483701,1.1798831254184,12.5434499600945));
#448449=CARTESIAN_POINT('Ctrl Pts',(2.45359067645838,1.17153406352246,12.5311293540533));
#448450=CARTESIAN_POINT('Ctrl Pts',(2.46338676527167,1.15830574509102,12.5278936106989));
#448451=CARTESIAN_POINT('Ctrl Pts',(2.47814869542813,1.19802213288134,12.5204817579905));
#448452=CARTESIAN_POINT('Ctrl Pts',(2.47036967583308,1.18963174883482,12.5081597038247));
#448453=CARTESIAN_POINT('Ctrl Pts',(2.48022624928162,1.17639800390951,12.5049254088044));
#448454=CARTESIAN_POINT('Ctrl Pts',(2.46605782225597,1.18498102042076,12.5369868989719));
#448455=CARTESIAN_POINT('Ctrl Pts',(2.46669113878569,1.18566410997851,12.5342545179733));
#448456=CARTESIAN_POINT('Ctrl Pts',(2.46738702577367,1.18623120645471,12.5314872231885));
#448457=CARTESIAN_POINT('Ctrl Pts',(2.46814159680487,1.18660703044145,12.5287124745063));
#448458=CARTESIAN_POINT('Ctrl Pts',(2.46882210641437,1.18694596716693,12.5262100684184));
#448459=CARTESIAN_POINT('Ctrl Pts',(2.46955009758189,1.18712811325593,12.5237004536639));
#448460=CARTESIAN_POINT('Ctrl Pts',(2.47035416046659,1.18709228800123,12.5212220730815));
#448461=CARTESIAN_POINT('Ctrl Pts',(2.47096974016182,1.18706486066964,12.5193246583486));
#448462=CARTESIAN_POINT('Ctrl Pts',(2.47163723602436,1.18690871363447,12.517417831369));
#448463=CARTESIAN_POINT('Ctrl Pts',(2.47235361687581,1.18652666235626,12.5155812248347));
#448464=CARTESIAN_POINT('Ctrl Pts',(2.47265879896908,1.18636390645821,12.5147988205793));
#448465=CARTESIAN_POINT('Ctrl Pts',(2.47297329290029,1.18616023254245,12.5140295443047));
#448466=CARTESIAN_POINT('Ctrl Pts',(2.47329874923813,1.18590911319832,12.5132817086137));
#448467=CARTESIAN_POINT('Ctrl Pts',(2.4737912833787,1.18552907804163,12.5121499604604));
#448468=CARTESIAN_POINT('Ctrl Pts',(2.47431519146879,1.1850265112003,12.5110494206568));
#448469=CARTESIAN_POINT('Ctrl Pts',(2.47485471189822,1.18436767144746,12.5100666561695));
#448470=CARTESIAN_POINT('Ctrl Pts',(2.47516450328639,1.18398936717855,12.5095023550641));
#448471=CARTESIAN_POINT('Ctrl Pts',(2.47548251644376,1.18355475474528,12.5089719619137));
#448472=CARTESIAN_POINT('Ctrl Pts',(2.47579763610277,1.18306820887133,12.5085043804652));
#448473=CARTESIAN_POINT('Ctrl Pts',(2.47625877267651,1.18235621236187,12.5078201359221));
#448474=CARTESIAN_POINT('Ctrl Pts',(2.47672607371854,1.18151169608092,12.5072563000949));
#448475=CARTESIAN_POINT('Ctrl Pts',(2.47716045552645,1.18058780689311,12.5068768744332));
#448476=CARTESIAN_POINT('Ctrl Pts',(2.47747367471289,1.17992161918795,12.5066032824114));
#448477=CARTESIAN_POINT('Ctrl Pts',(2.47777533500291,1.17920248395026,12.5064197834844));
#448478=CARTESIAN_POINT('Ctrl Pts',(2.47805097454076,1.17847155943811,12.5063282718343));
#448479=CARTESIAN_POINT('Ctrl Pts',(2.47845332293017,1.17740463593888,12.5061946931565));
#448480=CARTESIAN_POINT('Ctrl Pts',(2.47880982259354,1.1762901636557,12.5062515701262));
#448481=CARTESIAN_POINT('Ctrl Pts',(2.47911307783089,1.17520202033805,12.5064436508398));
#448482=CARTESIAN_POINT('',(2.42965842765955,1.12207316109538,12.5737548217797));
#448483=CARTESIAN_POINT('Origin',(2.4437814292482,1.12859549396996,12.5893111709658));
#448484=CARTESIAN_POINT('Ctrl Pts',(2.47911307783089,1.17520202033805,12.5064436508398));
#448485=CARTESIAN_POINT('Ctrl Pts',(2.47179285640968,1.16733724150482,12.5164271754438));
#448486=CARTESIAN_POINT('Ctrl Pts',(2.4644695803147,1.15946948742519,12.5264061185523));
#448487=CARTESIAN_POINT('Ctrl Pts',(2.45714314265571,1.15159865266862,12.536380305637));
#448488=CARTESIAN_POINT('Ctrl Pts',(2.44798658154365,1.14176170560022,12.5488460165097));
#448489=CARTESIAN_POINT('Ctrl Pts',(2.43882507936809,1.1319199436467,12.5613043021964));
#448490=CARTESIAN_POINT('Ctrl Pts',(2.42965842765955,1.12207316109538,12.5737548217797));
#448491=CARTESIAN_POINT('Ctrl Pts',(2.45401129869475,1.0858263246758,12.5893111709658));
#448492=CARTESIAN_POINT('Ctrl Pts',(2.44268373953579,1.08544548604849,12.5770542771492));
#448493=CARTESIAN_POINT('Ctrl Pts',(2.43909421506563,1.10141166871477,12.5737548217797));
#448494=CARTESIAN_POINT('Ctrl Pts',(2.44344278452135,1.08547100554888,12.5928319619712));
#448495=CARTESIAN_POINT('Ctrl Pts',(2.43572049983066,1.08847096146978,12.5821634970843));
#448496=CARTESIAN_POINT('Ctrl Pts',(2.43524467832255,1.1012728010326,12.5773203894503));
#448497=CARTESIAN_POINT('Ctrl Pts',(2.42799259915257,1.09194216243231,12.5969440695591));
#448498=CARTESIAN_POINT('Ctrl Pts',(2.42630612126106,1.09559104375038,12.5878292599214));
#448499=CARTESIAN_POINT('Ctrl Pts',(2.42973870739431,1.10358114052992,12.5813877129824));
#448500=CARTESIAN_POINT('Ctrl Pts',(2.41523312262583,1.11975171122953,12.596957478804));
#448501=CARTESIAN_POINT('Ctrl Pts',(2.41690720975602,1.11612982975308,12.5878468778671));
#448502=CARTESIAN_POINT('Ctrl Pts',(2.42517733555884,1.11353705110017,12.5814011370086));
#448503=CARTESIAN_POINT('Ctrl Pts',(2.42044854659189,1.13578724552042,12.5928371701607));
#448504=CARTESIAN_POINT('Ctrl Pts',(2.41766644601505,1.12799013181828,12.5821692192952));
#448505=CARTESIAN_POINT('Ctrl Pts',(2.42702398450034,1.11924597402784,12.5773318885715));
#448506=CARTESIAN_POINT('Ctrl Pts',(2.42764842286958,1.14355297053488,12.5893111709658));
#448507=CARTESIAN_POINT('Ctrl Pts',(2.41994263053445,1.13524156878502,12.5770542771492));
#448508=CARTESIAN_POINT('Ctrl Pts',(2.42965842765951,1.12207316109542,12.5737548217797));
#448509=CARTESIAN_POINT('',(2.43909421506563,1.10141166871477,12.5737548217797));
#448510=CARTESIAN_POINT('Origin',(2.45327206454525,1.10781390146071,12.5893111709658));
#448511=CARTESIAN_POINT('Ctrl Pts',(2.42965842765951,1.12207316109542,12.5737548217797));
#448512=CARTESIAN_POINT('Ctrl Pts',(2.4289534687874,1.1213608742012,12.5746934679442));
#448513=CARTESIAN_POINT('Ctrl Pts',(2.42830358372026,1.12044382194655,12.5756680099006));
#448514=CARTESIAN_POINT('Ctrl Pts',(2.42777999398454,1.11942826423936,12.5765688348656));
#448515=CARTESIAN_POINT('Ctrl Pts',(2.42764137939834,1.11915940657898,12.5768073183026));
#448516=CARTESIAN_POINT('Ctrl Pts',(2.42751142348116,1.1188838148705,12.5770407398754));
#448517=CARTESIAN_POINT('Ctrl Pts',(2.42739094509012,1.11860371470951,12.5772674179684));
#448518=CARTESIAN_POINT('Ctrl Pts',(2.42689653435202,1.11745425939102,12.5781976435658));
#448519=CARTESIAN_POINT('Ctrl Pts',(2.42654401154365,1.11615913578597,12.5790594849312));
#448520=CARTESIAN_POINT('Ctrl Pts',(2.426403773541,1.11479311015434,12.5797571720116));
#448521=CARTESIAN_POINT('Ctrl Pts',(2.42631240343977,1.11390309533742,12.580211740231));
#448522=CARTESIAN_POINT('Ctrl Pts',(2.42632567046707,1.1129406188617,12.5806009430798));
#448523=CARTESIAN_POINT('Ctrl Pts',(2.42646035569495,1.11197367907365,12.5808812374708));
#448524=CARTESIAN_POINT('Ctrl Pts',(2.42657609498706,1.11114275701678,12.5811221033394));
#448525=CARTESIAN_POINT('Ctrl Pts',(2.42678397820911,1.11029154357781,12.581287365893));
#448526=CARTESIAN_POINT('Ctrl Pts',(2.42708037202315,1.10947006077796,12.581359338449));
#448527=CARTESIAN_POINT('Ctrl Pts',(2.427121564643,1.10935589163175,12.5813693411482));
#448528=CARTESIAN_POINT('Ctrl Pts',(2.42716442053753,1.10924225880875,12.5813775999465));
#448529=CARTESIAN_POINT('Ctrl Pts',(2.42720888318565,1.10912925689458,12.5813841266931));
#448530=CARTESIAN_POINT('Ctrl Pts',(2.42728431944584,1.10893753547988,12.5813952001081));
#448531=CARTESIAN_POINT('Ctrl Pts',(2.42736545260864,1.10874656902732,12.5814007534795));
#448532=CARTESIAN_POINT('Ctrl Pts',(2.42745242884562,1.10855651782356,12.5814005856065));
#448533=CARTESIAN_POINT('Ctrl Pts',(2.42785057205302,1.107686537718,12.5813998171494));
#448534=CARTESIAN_POINT('Ctrl Pts',(2.42834333845804,1.10689570469468,12.58127954464));
#448535=CARTESIAN_POINT('Ctrl Pts',(2.42890281728343,1.10617286062362,12.5810700125799));
#448536=CARTESIAN_POINT('Ctrl Pts',(2.42957860400273,1.10529974728816,12.5808169217085));
#448537=CARTESIAN_POINT('Ctrl Pts',(2.43036501932016,1.10453599385415,12.5804173076348));
#448538=CARTESIAN_POINT('Ctrl Pts',(2.43117499953934,1.10392985244145,12.5799304713245));
#448539=CARTESIAN_POINT('Ctrl Pts',(2.43217882020099,1.10317865227688,12.5793271277669));
#448540=CARTESIAN_POINT('Ctrl Pts',(2.43326181024863,1.10259714959837,12.5785808224116));
#448541=CARTESIAN_POINT('Ctrl Pts',(2.43436331554294,1.10218191237749,12.5777485681082));
#448542=CARTESIAN_POINT('Ctrl Pts',(2.43600467911038,1.10156316342575,12.576508418016));
#448543=CARTESIAN_POINT('Ctrl Pts',(2.43767090966464,1.10131237416998,12.5750928681475));
#448544=CARTESIAN_POINT('Ctrl Pts',(2.43909421506563,1.10141166871477,12.5737548217797));
#448545=CARTESIAN_POINT('Ctrl Pts',(2.43909421506563,1.10141166871477,12.5737548217797));
#448546=CARTESIAN_POINT('Ctrl Pts',(2.44268373953579,1.08544548604849,12.5770542771492));
#448547=CARTESIAN_POINT('Ctrl Pts',(2.45401129869475,1.0858263246758,12.5893111709658));
#448548=CARTESIAN_POINT('Ctrl Pts',(2.46383762734287,1.1022939969124,12.5508408821982));
#448549=CARTESIAN_POINT('Ctrl Pts',(2.46743513747504,1.08627764135071,12.55409748406));
#448550=CARTESIAN_POINT('Ctrl Pts',(2.47877714769835,1.08665896583058,12.5663972313419));
#448551=CARTESIAN_POINT('Ctrl Pts',(2.48855691045729,1.10317428442276,12.52790050457));
#448552=CARTESIAN_POINT('Ctrl Pts',(2.49213913059592,1.0871082028775,12.5311362602938));
#448553=CARTESIAN_POINT('Ctrl Pts',(2.50351801202985,1.08749076698724,12.5434568539655));
#448554=CARTESIAN_POINT('Ctrl Pts',(2.51325394004799,1.10405267599415,12.5049357605811));
#448555=CARTESIAN_POINT('Ctrl Pts',(2.51680066060845,1.08793733677168,12.5081700652078));
#448556=CARTESIAN_POINT('Ctrl Pts',(2.52823584849389,1.08832179393463,12.5204921097672));
#448557=CARTESIAN_POINT('Ctrl Pts',(2.51163223633209,1.10399499577426,12.5064436508395));
#448558=CARTESIAN_POINT('Ctrl Pts',(2.5123060249568,1.10297771671726,12.5062361689309));
#448559=CARTESIAN_POINT('Ctrl Pts',(2.51296333095002,1.10189109790107,12.5061871075061));
#448560=CARTESIAN_POINT('Ctrl Pts',(2.51353944025899,1.10080522741835,12.5063648335164));
#448561=CARTESIAN_POINT('Ctrl Pts',(2.51380114464302,1.10031195806583,12.5064455676329));
#448562=CARTESIAN_POINT('Ctrl Pts',(2.51404954940513,1.09981185979765,12.506574497099));
#448563=CARTESIAN_POINT('Ctrl Pts',(2.51427306246193,1.0993259078063,12.5067492519495));
#448564=CARTESIAN_POINT('Ctrl Pts',(2.5147222206257,1.09834936841645,12.5071004286051));
#448565=CARTESIAN_POINT('Ctrl Pts',(2.51508663965537,1.09739371359238,12.5076537929612));
#448566=CARTESIAN_POINT('Ctrl Pts',(2.51534780568653,1.09653404031118,12.5083435010503));
#448567=CARTESIAN_POINT('Ctrl Pts',(2.51536424764895,1.0964799187406,12.5083869222963));
#448568=CARTESIAN_POINT('Ctrl Pts',(2.51538027074628,1.09642616821722,12.5084308732336));
#448569=CARTESIAN_POINT('Ctrl Pts',(2.51539586671482,1.09637280338018,12.5084753333615));
#448570=CARTESIAN_POINT('Ctrl Pts',(2.51552096696711,1.09594474695267,12.508831962269));
#448571=CARTESIAN_POINT('Ctrl Pts',(2.51562236310778,1.09553317783142,12.509227847131));
#448572=CARTESIAN_POINT('Ctrl Pts',(2.51569975886115,1.09515100391834,12.5096423454524));
#448573=CARTESIAN_POINT('Ctrl Pts',(2.51594228289828,1.09395344001786,12.5109411997424));
#448574=CARTESIAN_POINT('Ctrl Pts',(2.51597353579324,1.09297277425104,12.5124831113042));
#448575=CARTESIAN_POINT('Ctrl Pts',(2.51588134536736,1.0921737627362,12.5140723025008));
#448576=CARTESIAN_POINT('Ctrl Pts',(2.51587270702348,1.09209889448212,12.5142212114565));
#448577=CARTESIAN_POINT('Ctrl Pts',(2.51586300670766,1.09202560115064,12.5143705582413));
#448578=CARTESIAN_POINT('Ctrl Pts',(2.51585233019747,1.09195384347404,12.5145201959299));
#448579=CARTESIAN_POINT('Ctrl Pts',(2.51571517452833,1.09103200928206,12.5164425148273));
#448580=CARTESIAN_POINT('Ctrl Pts',(2.51542283714769,1.09033044201141,12.5184635205941));
#448581=CARTESIAN_POINT('Ctrl Pts',(2.515029354695,1.08977690579741,12.5205025929158));
#448582=CARTESIAN_POINT('Ctrl Pts',(2.51480111927626,1.08945583285316,12.5216853356836));
#448583=CARTESIAN_POINT('Ctrl Pts',(2.51453966041455,1.08918486418674,12.5228750347131));
#448584=CARTESIAN_POINT('Ctrl Pts',(2.51426005320379,1.0889537199542,12.5240609649613));
#448585=CARTESIAN_POINT('Ctrl Pts',(2.51357377230539,1.08838638883587,12.5269717671326));
#448586=CARTESIAN_POINT('Ctrl Pts',(2.51275222181068,1.08805101773871,12.5299036066168));
#448587=CARTESIAN_POINT('Ctrl Pts',(2.51184062668424,1.08787368626492,12.5328133004019));
#448588=CARTESIAN_POINT('Ctrl Pts',(2.51140300794295,1.08778855683181,12.5342101228451));
#448589=CARTESIAN_POINT('Ctrl Pts',(2.51094508383591,1.08774046921529,12.5356023438238));
#448590=CARTESIAN_POINT('Ctrl Pts',(2.51047333723489,1.08772460875902,12.5369868989719));
#448591=CARTESIAN_POINT('Origin',(15.2493479500663,1.51071161473945,-1.2406553367009));
#448592=CARTESIAN_POINT('Ctrl Pts',(2.46602937784755,1.18495039891586,12.5369868989719));
#448593=CARTESIAN_POINT('Ctrl Pts',(2.47647945267177,1.19617890014503,12.5369868989719));
#448594=CARTESIAN_POINT('Ctrl Pts',(2.4695570606498,1.20986698957999,12.5369868989719));
#448595=CARTESIAN_POINT('Ctrl Pts',(2.46956186336931,1.18874611658407,12.5218025310016));
#448596=CARTESIAN_POINT('Ctrl Pts',(2.47486155570973,1.19930874527211,12.5216901060418));
#448597=CARTESIAN_POINT('Ctrl Pts',(2.46957817711163,1.20982527118971,12.5161920673678));
#448598=CARTESIAN_POINT('Ctrl Pts',(2.47554149986159,1.18798452705193,12.5042015548895));
#448599=CARTESIAN_POINT('Ctrl Pts',(2.47730769068085,1.19416982534763,12.4980677368514));
#448600=CARTESIAN_POINT('Ctrl Pts',(2.47435102818041,1.20028937815663,12.4907278922776));
#448601=CARTESIAN_POINT('Ctrl Pts',(2.47909500459789,1.17519345286739,12.506463626192));
#448602=CARTESIAN_POINT('Ctrl Pts',(2.48500710868774,1.17799603445712,12.4999376786891));
#448603=CARTESIAN_POINT('Ctrl Pts',(2.48493490093248,1.17796180499795,12.4906970594712));
#448604=CARTESIAN_POINT('Origin',(2.44992481587739,1.19993849698564,12.5369868989719));
#448605=CARTESIAN_POINT('Origin',(2.44992481587739,1.19993849698564,14.));
#448606=CARTESIAN_POINT('Origin',(2.44992481587739,1.19993849698564,13.7435492065112));
#448607=CARTESIAN_POINT('Ctrl Pts',(2.44922377166514,1.16682399727264,13.793642941384));
#448608=CARTESIAN_POINT('Ctrl Pts',(2.45659484668155,1.17473433684236,13.8071662555867));
#448609=CARTESIAN_POINT('Ctrl Pts',(2.4459779900371,1.18804980674117,13.8103758687955));
#448610=CARTESIAN_POINT('Ctrl Pts',(2.46052423051409,1.1790125712264,13.7804579775006));
#448611=CARTESIAN_POINT('Ctrl Pts',(2.46961205178888,1.18878012855701,13.7901904343351));
#448612=CARTESIAN_POINT('Ctrl Pts',(2.46191196247133,1.20252656622885,13.7927914348263));
#448613=CARTESIAN_POINT('Ctrl Pts',(2.46717723589469,1.18618844344647,13.7597120340895));
#448614=CARTESIAN_POINT('Ctrl Pts',(2.47769020905823,1.19749616139639,13.7635825532445));
#448615=CARTESIAN_POINT('Ctrl Pts',(2.47129101828876,1.211082414509,13.7651073818884));
#448616=CARTESIAN_POINT('Ctrl Pts',(2.46587442510408,1.18478324335754,13.7381884353898));
#448617=CARTESIAN_POINT('Ctrl Pts',(2.47614198082626,1.19582567108509,13.7368803041982));
#448618=CARTESIAN_POINT('Ctrl Pts',(2.46945398737976,1.2094072903103,13.7363986145813));
#448619=CARTESIAN_POINT('Origin',(2.4358328208315,1.184738991576,13.7902182540695));
#448620=CARTESIAN_POINT('Ctrl Pts',(2.42764574614966,1.14355008456382,13.8235227101244));
#448621=CARTESIAN_POINT('Ctrl Pts',(2.43546568760982,1.15197808574317,13.8358800583119));
#448622=CARTESIAN_POINT('Ctrl Pts',(2.4255375932552,1.16524680804573,13.8390832900376));
#448623=CARTESIAN_POINT('Ctrl Pts',(2.43575513199856,1.15229679882965,13.8124254819053));
#448624=CARTESIAN_POINT('Ctrl Pts',(2.44359025947028,1.16074116725703,13.8247886449157));
#448625=CARTESIAN_POINT('Ctrl Pts',(2.43363597355513,1.17401644401579,13.8279860620657));
#448626=CARTESIAN_POINT('Ctrl Pts',(2.44386088348455,1.1610395931027,13.8013225099955));
#448627=CARTESIAN_POINT('Ctrl Pts',(2.45170750151535,1.16949634302873,13.8136962257787));
#448628=CARTESIAN_POINT('Ctrl Pts',(2.44173080383857,1.18278183618285,13.8168830918626));
#448629=CARTESIAN_POINT('Ctrl Pts',(2.45196314201513,1.16977861990387,13.7902140179785));
#448630=CARTESIAN_POINT('Ctrl Pts',(2.45981779667535,1.17824402607918,13.802602731458));
#448631=CARTESIAN_POINT('Ctrl Pts',(2.44982222494626,1.19154315004769,13.8057746032558));
#448632=CARTESIAN_POINT('Origin',(2.41151541649105,1.15851044709972,13.8235269408515));
#448633=CARTESIAN_POINT('Ctrl Pts',(2.45401129869475,1.0858263246758,13.8235269408515));
#448634=CARTESIAN_POINT('Ctrl Pts',(2.46581211258456,1.08622307438154,13.8362179249168));
#448635=CARTESIAN_POINT('Ctrl Pts',(2.46913911515529,1.06947213237963,13.8391868794938));
#448636=CARTESIAN_POINT('Ctrl Pts',(2.4432140676444,1.08546331596454,13.8400110824519));
#448637=CARTESIAN_POINT('Ctrl Pts',(2.45279038442927,1.08236234519754,13.8494522556837));
#448638=CARTESIAN_POINT('Ctrl Pts',(2.45136614563081,1.0689870159948,13.85569149686));
#448639=CARTESIAN_POINT('Ctrl Pts',(2.42813490907277,1.09162908459596,13.8586819406588));
#448640=CARTESIAN_POINT('Ctrl Pts',(2.42995620742041,1.08767447766684,13.868010383617));
#448641=CARTESIAN_POINT('Ctrl Pts',(2.42638970020154,1.07935745337625,13.8744918421245));
#448642=CARTESIAN_POINT('Ctrl Pts',(2.41508858862442,1.12006963699401,13.8587686893867));
#448643=CARTESIAN_POINT('Ctrl Pts',(2.4132834486702,1.12398902440348,13.8680909899357));
#448644=CARTESIAN_POINT('Ctrl Pts',(2.40467374652388,1.1267036938967,13.8745789365163));
#448645=CARTESIAN_POINT('Ctrl Pts',(2.42029144442988,1.13561779648083,13.8400379222776));
#448646=CARTESIAN_POINT('Ctrl Pts',(2.42421144834743,1.14488622694096,13.8494748685453));
#448647=CARTESIAN_POINT('Ctrl Pts',(2.41317610411016,1.15256621931266,13.8557104837033));
#448648=CARTESIAN_POINT('Ctrl Pts',(2.42764842286468,1.14355297053923,13.8235269408542));
#448649=CARTESIAN_POINT('Ctrl Pts',(2.4356761559309,1.15221161481001,13.8362179249195));
#448650=CARTESIAN_POINT('Ctrl Pts',(2.4251953619882,1.16569552976031,13.8391868794965));
#448651=CARTESIAN_POINT('Origin',(2.45475053284425,1.0638387478909,13.8235269408515));
#448652=CARTESIAN_POINT('Ctrl Pts',(2.48975408263468,1.08702801552268,13.7902140241683));
#448653=CARTESIAN_POINT('Ctrl Pts',(2.50129551029208,1.08742049867086,13.8026027327198));
#448654=CARTESIAN_POINT('Ctrl Pts',(2.50480060873724,1.07115728197909,13.8057746032556));
#448655=CARTESIAN_POINT('Ctrl Pts',(2.47784371587751,1.08662758259173,13.8013225161808));
#448656=CARTESIAN_POINT('Ctrl Pts',(2.4893733387089,1.08701966071042,13.8136962270464));
#448657=CARTESIAN_POINT('Ctrl Pts',(2.49288049554738,1.07077963434889,13.8168830918628));
#448658=CARTESIAN_POINT('Ctrl Pts',(2.46592821445409,1.08622697703056,13.8124254880875));
#448659=CARTESIAN_POINT('Ctrl Pts',(2.47744095526533,1.08661847933377,13.8247886461868));
#448660=CARTESIAN_POINT('Ctrl Pts',(2.48095506764791,1.07040208095555,13.8279860620656));
#448661=CARTESIAN_POINT('Ctrl Pts',(2.454007370493,1.08582619185041,13.8235227163065));
#448662=CARTESIAN_POINT('Ctrl Pts',(2.4654977970538,1.08621693561251,13.8358800595847));
#448663=CARTESIAN_POINT('Ctrl Pts',(2.46902410772917,1.0700246237387,13.8390832900376));
#448664=CARTESIAN_POINT('Origin',(2.49049725742216,1.06504057198453,13.7902182540695));
#448665=CARTESIAN_POINT('Ctrl Pts',(2.5102036306474,1.08771551347853,13.7382347919292));
#448666=CARTESIAN_POINT('Ctrl Pts',(2.52528460742438,1.08824655790786,13.7369371795942));
#448667=CARTESIAN_POINT('Ctrl Pts',(2.53116611461982,1.07428404917444,13.7364597369712));
#448668=CARTESIAN_POINT('Ctrl Pts',(2.51209412109904,1.08777907318603,13.7595490285574));
#448669=CARTESIAN_POINT('Ctrl Pts',(2.52753495243651,1.08832178307826,13.7633824266926));
#448670=CARTESIAN_POINT('Ctrl Pts',(2.53360479778411,1.07457221443906,13.7648920890506));
#448671=CARTESIAN_POINT('Ctrl Pts',(2.50245272336482,1.08745492216785,13.780380659011));
#448672=CARTESIAN_POINT('Ctrl Pts',(2.51580830018509,1.08792974192552,13.7901039518743));
#448673=CARTESIAN_POINT('Ctrl Pts',(2.52117168901941,1.07310680356507,13.7926933640892));
#448674=CARTESIAN_POINT('Ctrl Pts',(2.48569382187465,1.08689147526159,13.7936647693663));
#448675=CARTESIAN_POINT('Ctrl Pts',(2.49650208684873,1.0872848455642,13.8072068914933));
#448676=CARTESIAN_POINT('Ctrl Pts',(2.49960565550404,1.07052142910306,13.8104111085397));
#448677=CARTESIAN_POINT('Origin',(2.51121257138439,1.06573703197411,13.7435492065112));
#448678=CARTESIAN_POINT('Origin',(2.51121257138439,1.06573703197411,14.));
#448679=CARTESIAN_POINT('Origin',(2.51121257138439,1.06573703197411,12.5369868989719));
#448680=CARTESIAN_POINT('Ctrl Pts',(2.51161540710188,1.10398759845017,12.506462012331));
#448681=CARTESIAN_POINT('Ctrl Pts',(2.51760129318922,1.10661871147307,12.4999388158272));
#448682=CARTESIAN_POINT('Ctrl Pts',(2.5175304723068,1.10658758195552,12.4907030323752));
#448683=CARTESIAN_POINT('Ctrl Pts',(2.5189533141719,1.09292488165065,12.5042014951932));
#448684=CARTESIAN_POINT('Ctrl Pts',(2.52478230827215,1.090211226386,12.4980716682127));
#448685=CARTESIAN_POINT('Ctrl Pts',(2.52747049798941,1.08397430396625,12.4907355092743));
#448686=CARTESIAN_POINT('Ctrl Pts',(2.5156154878654,1.08790645392943,12.5218047446509));
#448687=CARTESIAN_POINT('Ctrl Pts',(2.52706285447636,1.0849949820318,12.5216906929434));
#448688=CARTESIAN_POINT('Ctrl Pts',(2.53155200346214,1.07412215830871,12.5161988840776));
#448689=CARTESIAN_POINT('Ctrl Pts',(2.51043494394272,1.08772328439607,12.5369868989719));
#448690=CARTESIAN_POINT('Ctrl Pts',(2.52575525458304,1.08826514545271,12.5369868989719));
#448691=CARTESIAN_POINT('Ctrl Pts',(2.53156907091975,1.0740804681168,12.5369868989719));
#448692=CARTESIAN_POINT('Origin',(4.68629905775447E-31,-3.01170153175948E-31,
12.5));
#448693=CARTESIAN_POINT('Origin',(2.35734085275916,1.28223802992782,12.5));
#448694=CARTESIAN_POINT('',(2.35734085275916,1.28223802992782,12.5893111709658));
#448695=CARTESIAN_POINT('',(2.35734085275916,1.28223802992782,13.8235269408515));
#448696=CARTESIAN_POINT('',(2.35734085275916,1.28223802992782,12.5));
#448697=CARTESIAN_POINT('',(2.39287067323911,1.28634954496043,13.7902182540695));
#448698=CARTESIAN_POINT('',(2.35734085275916,1.28223802992782,13.8235269408515));
#448699=CARTESIAN_POINT('',(2.41346029074826,1.28873217793636,13.7435492065112));
#448700=CARTESIAN_POINT('Origin',(2.34572068385282,1.28089367053509,13.7445212918707));
#448701=CARTESIAN_POINT('',(2.41346029074826,1.28873217793636,12.5369868989719));
#448702=CARTESIAN_POINT('',(2.41346029074826,1.28873217793636,12.5));
#448703=CARTESIAN_POINT('Ctrl Pts',(2.41346029074826,1.28873217793636,12.5369868989719));
#448704=CARTESIAN_POINT('Ctrl Pts',(2.39476745478683,1.2865690407457,12.5544431401645));
#448705=CARTESIAN_POINT('Ctrl Pts',(2.37606124921229,1.28440435642184,12.5718848856037));
#448706=CARTESIAN_POINT('Ctrl Pts',(2.35734085275916,1.28223802992782,12.5893111709658));
#448707=CARTESIAN_POINT('Origin',(2.49626940223468,1.55385500512921,12.5));
#448708=CARTESIAN_POINT('',(2.3612652642965,1.38204470010708,13.7435492065112));
#448709=CARTESIAN_POINT('',(2.34845905999782,1.36574714137789,13.7902182540695));
#448710=CARTESIAN_POINT('Origin',(2.31480656845809,1.32291997382215,13.7418732680446));
#448711=CARTESIAN_POINT('',(2.32636043968301,1.33762377601413,13.8235269408515));
#448712=CARTESIAN_POINT('',(2.34845905999782,1.36574714137789,13.7902182540695));
#448713=CARTESIAN_POINT('',(2.32636043968301,1.33762377601413,12.5893111709658));
#448714=CARTESIAN_POINT('',(2.32636043968301,1.33762377601413,12.5));
#448715=CARTESIAN_POINT('',(2.3612652642965,1.38204470010708,12.5369868989719));
#448716=CARTESIAN_POINT('Ctrl Pts',(2.32636043968301,1.33762377601413,12.5893111709658));
#448717=CARTESIAN_POINT('Ctrl Pts',(2.33800403730811,1.35244176670741,12.5718848856037));
#448718=CARTESIAN_POINT('Ctrl Pts',(2.34963880857737,1.36724852471619,12.5544431401645));
#448719=CARTESIAN_POINT('Ctrl Pts',(2.3612652642965,1.38204470010708,12.5369868989719));
#448720=CARTESIAN_POINT('',(2.3612652642965,1.38204470010708,12.5));
#448721=CARTESIAN_POINT('Origin',(2.3533893433224,1.31638515569517,12.5));
#448722=CARTESIAN_POINT('',(2.3239518225894,1.29863628121615,13.8587068136939));
#448723=CARTESIAN_POINT('Ctrl Pts',(2.32636043967773,1.3376237760181,13.8235269408542));
#448724=CARTESIAN_POINT('Ctrl Pts',(2.32527778080196,1.33624595194157,13.8262006681044));
#448725=CARTESIAN_POINT('Ctrl Pts',(2.32430644806145,1.33472860533013,13.8288634856214));
#448726=CARTESIAN_POINT('Ctrl Pts',(2.32343931652769,1.33308300744998,13.8314912288862));
#448727=CARTESIAN_POINT('Ctrl Pts',(2.32254539335684,1.33138656577109,13.8342001611531));
#448728=CARTESIAN_POINT('Ctrl Pts',(2.32176077732778,1.32955217257974,13.8368750301949));
#448729=CARTESIAN_POINT('Ctrl Pts',(2.32110448918224,1.32755579711711,13.8394886372969));
#448730=CARTESIAN_POINT('Ctrl Pts',(2.32105380245683,1.3274016121976,13.8396904925131));
#448731=CARTESIAN_POINT('Ctrl Pts',(2.32100390072192,1.32724645063996,13.8398919674349));
#448732=CARTESIAN_POINT('Ctrl Pts',(2.32095480326791,1.3270902968873,13.8400930404591));
#448733=CARTESIAN_POINT('Ctrl Pts',(2.32018983190341,1.32465731636581,13.8432258934518));
#448734=CARTESIAN_POINT('Ctrl Pts',(2.31962293533913,1.32199622539247,13.8462331177034));
#448735=CARTESIAN_POINT('Ctrl Pts',(2.31936695184163,1.31917371508202,13.8489036603661));
#448736=CARTESIAN_POINT('Ctrl Pts',(2.31928319106221,1.31825015686123,13.8497774930041));
#448737=CARTESIAN_POINT('Ctrl Pts',(2.31923287418977,1.31730951176935,13.85061494757));
#448738=CARTESIAN_POINT('Ctrl Pts',(2.31922038831851,1.31635468307864,13.8514076489583));
#448739=CARTESIAN_POINT('Ctrl Pts',(2.31919397890005,1.31433508269089,13.8530843267192));
#448740=CARTESIAN_POINT('Ctrl Pts',(2.31933718273174,1.31205361062889,13.8546805203176));
#448741=CARTESIAN_POINT('Ctrl Pts',(2.31977786602568,1.30965123033594,13.8559412814273));
#448742=CARTESIAN_POINT('Ctrl Pts',(2.31983684374211,1.3093297139417,13.8561100121513));
#448743=CARTESIAN_POINT('Ctrl Pts',(2.31990108311304,1.30900607034723,13.8562727473908));
#448744=CARTESIAN_POINT('Ctrl Pts',(2.3199708207249,1.30868066685121,13.8564289040185));
#448745=CARTESIAN_POINT('Ctrl Pts',(2.32028707999907,1.30720496570915,13.8571370725437));
#448746=CARTESIAN_POINT('Ctrl Pts',(2.32072420160441,1.3056676085477,13.8577210840554));
#448747=CARTESIAN_POINT('Ctrl Pts',(2.32129342366775,1.30413637918839,13.8581177131616));
#448748=CARTESIAN_POINT('Ctrl Pts',(2.32145373619281,1.3037051322975,13.8582294175695));
#448749=CARTESIAN_POINT('Ctrl Pts',(2.32162435127528,1.30327434337993,13.8583265086086));
#448750=CARTESIAN_POINT('Ctrl Pts',(2.32180509082108,1.30284543137745,13.8584082369006));
#448751=CARTESIAN_POINT('Ctrl Pts',(2.32206476508117,1.30222919984718,13.8585256585398));
#448752=CARTESIAN_POINT('Ctrl Pts',(2.32234886457458,1.30160930699463,13.8586122832068));
#448753=CARTESIAN_POINT('Ctrl Pts',(2.32265072710445,1.30100218484903,13.8586682984299));
#448754=CARTESIAN_POINT('Ctrl Pts',(2.32289218720567,1.30051654731463,13.8587131050557));
#448755=CARTESIAN_POINT('Ctrl Pts',(2.3231474698,1.3000336127437,13.8587357943552));
#448756=CARTESIAN_POINT('Ctrl Pts',(2.32341705296171,1.29955356042874,13.8587355499465));
#448757=CARTESIAN_POINT('Ctrl Pts',(2.3235912909863,1.29924329117257,13.8587353919793));
#448758=CARTESIAN_POINT('Ctrl Pts',(2.32376958494548,1.29893756220855,13.8587257282814));
#448759=CARTESIAN_POINT('Ctrl Pts',(2.3239518225894,1.29863628121615,13.8587068136939));
#448760=CARTESIAN_POINT('Ctrl Pts',(2.3239518225894,1.29863628121615,13.8587068136939));
#448761=CARTESIAN_POINT('Ctrl Pts',(2.32455119226537,1.29764538445678,13.8586446046466));
#448762=CARTESIAN_POINT('Ctrl Pts',(2.32519316922359,1.29670254215215,13.858482427929));
#448763=CARTESIAN_POINT('Ctrl Pts',(2.32587423919463,1.29580499099488,13.8582284286032));
#448764=CARTESIAN_POINT('Ctrl Pts',(2.32657293775961,1.29488420791493,13.8579678548414));
#448765=CARTESIAN_POINT('Ctrl Pts',(2.32731570614221,1.29400976756026,13.857615680862));
#448766=CARTESIAN_POINT('Ctrl Pts',(2.32806587620233,1.29320987107419,13.8571944833187));
#448767=CARTESIAN_POINT('Ctrl Pts',(2.32993800230844,1.29121364758652,13.8561433417727));
#448768=CARTESIAN_POINT('Ctrl Pts',(2.33194030064112,1.28958502811147,13.8546163505475));
#448769=CARTESIAN_POINT('Ctrl Pts',(2.33386900550433,1.28828883584181,13.8528973491086));
#448770=CARTESIAN_POINT('Ctrl Pts',(2.33422135142747,1.28805204063767,13.8525833129072));
#448771=CARTESIAN_POINT('Ctrl Pts',(2.33457122551807,1.28782619937748,13.8522628768812));
#448772=CARTESIAN_POINT('Ctrl Pts',(2.33491739353448,1.2876109189613,13.851937733538));
#448773=CARTESIAN_POINT('Ctrl Pts',(2.33703139358197,1.28629623132855,13.8499521282529));
#448774=CARTESIAN_POINT('Ctrl Pts',(2.33921942577769,1.28524820517461,13.847639871647));
#448775=CARTESIAN_POINT('Ctrl Pts',(2.34133178933503,1.28444946311461,13.8452109780794));
#448776=CARTESIAN_POINT('Ctrl Pts',(2.34228218542323,1.28409009252868,13.8441181685877));
#448777=CARTESIAN_POINT('Ctrl Pts',(2.34321725800112,1.2837804664361,13.8430021611332));
#448778=CARTESIAN_POINT('Ctrl Pts',(2.34412437039983,1.28351584738843,13.8418824960098));
#448779=CARTESIAN_POINT('Ctrl Pts',(2.34626200393133,1.28289226584532,13.8392439765549));
#448780=CARTESIAN_POINT('Ctrl Pts',(2.34834549739249,1.28248517720724,13.8364981347964));
#448781=CARTESIAN_POINT('Ctrl Pts',(2.35037379864419,1.28225991943209,13.8336931113419));
#448782=CARTESIAN_POINT('Ctrl Pts',(2.3523492352543,1.28204053266428,13.8309611966328));
#448783=CARTESIAN_POINT('Ctrl Pts',(2.35427436101996,1.28199396311011,13.8281701127186));
#448784=CARTESIAN_POINT('Ctrl Pts',(2.3561380341987,1.28212615033551,13.8253580685121));
#448785=CARTESIAN_POINT('Ctrl Pts',(2.35654208055519,1.28215480866864,13.8247484142933));
#448786=CARTESIAN_POINT('Ctrl Pts',(2.35694313199631,1.28219200563405,13.8241378483365));
#448787=CARTESIAN_POINT('Ctrl Pts',(2.35734085275916,1.28223802992782,13.8235269408515));
#448788=CARTESIAN_POINT('',(2.32332976716748,1.29971137372854,12.5969504640361));
#448789=CARTESIAN_POINT('Origin',(2.35341831404089,1.31640113631719,12.584524458991));
#448790=CARTESIAN_POINT('Origin',(2.35341831404089,1.31640113631719,12.584524458991));
#448791=CARTESIAN_POINT('Ctrl Pts',(2.32636043968301,1.33762377601413,12.5893111709658));
#448792=CARTESIAN_POINT('Ctrl Pts',(2.31935774413809,1.32871193615555,12.5770542771492));
#448793=CARTESIAN_POINT('Ctrl Pts',(2.33011456022595,1.31637927291897,12.5737548217797));
#448794=CARTESIAN_POINT('Ctrl Pts',(2.34167298466528,1.35711097888248,12.5663937883685));
#448795=CARTESIAN_POINT('Ctrl Pts',(2.33466135620968,1.34818777073451,12.5540940315304));
#448796=CARTESIAN_POINT('Ctrl Pts',(2.34545392548238,1.33581900184643,12.5508374392248));
#448797=CARTESIAN_POINT('Ctrl Pts',(2.3569700794774,1.37657851940206,12.5434499600945));
#448798=CARTESIAN_POINT('Ctrl Pts',(2.34993565372079,1.36762629872672,12.5311293540533));
#448799=CARTESIAN_POINT('Ctrl Pts',(2.36077737761453,1.35524046861433,12.5278936106989));
#448800=CARTESIAN_POINT('Ctrl Pts',(2.37225293435228,1.39602793775148,12.5204817579905));
#448801=CARTESIAN_POINT('Ctrl Pts',(2.36518369299553,1.38703140970183,12.5081597038247));
#448802=CARTESIAN_POINT('Ctrl Pts',(2.37608614257654,1.37464510121107,12.5049254088044));
#448803=CARTESIAN_POINT('Ctrl Pts',(2.3612652642965,1.38204470010708,12.5369868989719));
#448804=CARTESIAN_POINT('Ctrl Pts',(2.36184079537726,1.38277713791727,12.5342545179733));
#448805=CARTESIAN_POINT('Ctrl Pts',(2.36248814323123,1.38339906867655,12.5314872231885));
#448806=CARTESIAN_POINT('Ctrl Pts',(2.36320957034566,1.38383514668411,12.5287124745063));
#448807=CARTESIAN_POINT('Ctrl Pts',(2.36386018912591,1.38422842347631,12.5262100684184));
#448808=CARTESIAN_POINT('Ctrl Pts',(2.36457091136567,1.38446930152772,12.5237004536639));
#448809=CARTESIAN_POINT('Ctrl Pts',(2.36537521888829,1.38449913406827,12.5212220730815));
#448810=CARTESIAN_POINT('Ctrl Pts',(2.36599098587501,1.38452197345878,12.5193246583486));
#448811=CARTESIAN_POINT('Ctrl Pts',(2.36666898813309,1.38442075309951,12.517417831369));
#448812=CARTESIAN_POINT('Ctrl Pts',(2.36741412601232,1.38409836475537,12.5155812248348));
#448813=CARTESIAN_POINT('Ctrl Pts',(2.367731558754,1.38396102558792,12.5147988205793));
#448814=CARTESIAN_POINT('Ctrl Pts',(2.36806160754755,1.38378366355532,12.5140295443047));
#448815=CARTESIAN_POINT('Ctrl Pts',(2.36840644951409,1.38355990750301,12.5132817086137));
#448816=CARTESIAN_POINT('Ctrl Pts',(2.36892832118129,1.38322128298688,12.5121499604604));
#448817=CARTESIAN_POINT('Ctrl Pts',(2.3694914498736,1.38276309176832,12.5110494206568));
#448818=CARTESIAN_POINT('Ctrl Pts',(2.37008287664953,1.38215042017407,12.5100666561695));
#448819=CARTESIAN_POINT('Ctrl Pts',(2.37042247254234,1.3817986255555,12.5095023550641));
#448820=CARTESIAN_POINT('Ctrl Pts',(2.37077485248524,1.38139138028384,12.5089719619137));
#448821=CARTESIAN_POINT('Ctrl Pts',(2.37112858161518,1.38093213852879,12.5085043804652));
#448822=CARTESIAN_POINT('Ctrl Pts',(2.37164621812038,1.38026009804072,12.5078201359221));
#448823=CARTESIAN_POINT('Ctrl Pts',(2.37218080017373,1.37945648119119,12.5072563000949));
#448824=CARTESIAN_POINT('Ctrl Pts',(2.37268904215778,1.37857107231839,12.5068768744332));
#448825=CARTESIAN_POINT('Ctrl Pts',(2.37305551961577,1.37793263156935,12.5066032824114));
#448826=CARTESIAN_POINT('Ctrl Pts',(2.37341479235406,1.37724047730894,12.5064197834844));
#448827=CARTESIAN_POINT('Ctrl Pts',(2.3737490918574,1.37653445206906,12.5063282718343));
#448828=CARTESIAN_POINT('Ctrl Pts',(2.37423706563576,1.37550387379872,12.5061946931565));
#448829=CARTESIAN_POINT('Ctrl Pts',(2.37468321891324,1.37442216786226,12.5062515701262));
#448830=CARTESIAN_POINT('Ctrl Pts',(2.37507415887602,1.37336236336887,12.5064436508398));
#448831=CARTESIAN_POINT('',(2.33011456022595,1.31637927291897,12.5737548217797));
#448832=CARTESIAN_POINT('Origin',(2.34365893801222,1.32403105900999,12.5893111709658));
#448833=CARTESIAN_POINT('Ctrl Pts',(2.37507415887602,1.37336236336887,12.5064436508398));
#448834=CARTESIAN_POINT('Ctrl Pts',(2.36841934737568,1.36492708793495,12.5164271754438));
#448835=CARTESIAN_POINT('Ctrl Pts',(2.36176173387593,1.35648859817026,12.5264061185523));
#448836=CARTESIAN_POINT('Ctrl Pts',(2.35510122043578,1.34804678028252,12.536380305637));
#448837=CARTESIAN_POINT('Ctrl Pts',(2.34677692953329,1.33749622010799,12.5488460165097));
#448838=CARTESIAN_POINT('Ctrl Pts',(2.33844810646613,1.32694045832694,12.5613043021964));
#448839=CARTESIAN_POINT('Ctrl Pts',(2.33011456022595,1.31637927291897,12.5737548217797));
#448840=CARTESIAN_POINT('Ctrl Pts',(2.35734085275916,1.28223802992782,12.5893111709658));
#448841=CARTESIAN_POINT('Ctrl Pts',(2.3460820270025,1.28093515727823,12.5770542771492));
#448842=CARTESIAN_POINT('Ctrl Pts',(2.34120305426879,1.29655563422097,12.5737548217797));
#448843=CARTESIAN_POINT('Ctrl Pts',(2.3468364662523,1.28102246107754,12.5928319619712));
#448844=CARTESIAN_POINT('Ctrl Pts',(2.33889535256909,1.28338299700011,12.5821634970843));
#448845=CARTESIAN_POINT('Ctrl Pts',(2.33737764554695,1.29610345562765,12.5773203894503));
#448846=CARTESIAN_POINT('Ctrl Pts',(2.33091023073949,1.2862127521802,12.5969440695591));
#448847=CARTESIAN_POINT('Ctrl Pts',(2.32893194676206,1.28971202854204,12.5878292599214));
#448848=CARTESIAN_POINT('Ctrl Pts',(2.33170184418414,1.29795532657012,12.5813877129824));
#448849=CARTESIAN_POINT('Ctrl Pts',(2.31592647392008,1.31288975120779,12.596957478804));
#448850=CARTESIAN_POINT('Ctrl Pts',(2.31789020762768,1.30941637488575,12.5878468778671));
#448851=CARTESIAN_POINT('Ctrl Pts',(2.32634415079954,1.30750631551895,12.5814011370086));
#448852=CARTESIAN_POINT('Ctrl Pts',(2.31981749908179,1.32929703405204,12.5928371701607));
#448853=CARTESIAN_POINT('Ctrl Pts',(2.3176801928667,1.32129909757775,12.5821692192952));
#448854=CARTESIAN_POINT('Ctrl Pts',(2.32771932495136,1.31334676150872,12.5773318885715));
#448855=CARTESIAN_POINT('Ctrl Pts',(2.32636043968297,1.33762377601416,12.5893111709658));
#448856=CARTESIAN_POINT('Ctrl Pts',(2.31935774413805,1.32871193615558,12.5770542771492));
#448857=CARTESIAN_POINT('Ctrl Pts',(2.33011456022591,1.316379272919,12.5737548217797));
#448858=CARTESIAN_POINT('',(2.34120305426879,1.29655563422097,12.5737548217797));
#448859=CARTESIAN_POINT('Origin',(2.35481188671963,1.30409219041892,12.5893111709658));
#448860=CARTESIAN_POINT('Ctrl Pts',(2.33011456022591,1.316379272919,12.5737548217797));
#448861=CARTESIAN_POINT('Ctrl Pts',(2.32947000504072,1.31561189540807,12.5746934679442));
#448862=CARTESIAN_POINT('Ctrl Pts',(2.32889703068478,1.31464492290294,12.5756680099006));
#448863=CARTESIAN_POINT('Ctrl Pts',(2.32845796053182,1.31359006695601,12.5765688348656));
#448864=CARTESIAN_POINT('Ctrl Pts',(2.3283417215695,1.3133108055217,12.5768073183026));
#448865=CARTESIAN_POINT('Ctrl Pts',(2.32823466135262,1.3130255382082,12.5770407398754));
#448866=CARTESIAN_POINT('Ctrl Pts',(2.32813741460693,1.31273654995004,12.5772674179684));
#448867=CARTESIAN_POINT('Ctrl Pts',(2.32773834025925,1.31155062028427,12.5781976435658));
#448868=CARTESIAN_POINT('Ctrl Pts',(2.3274925550386,1.31023107221463,12.5790594849312));
#448869=CARTESIAN_POINT('Ctrl Pts',(2.32746412743688,1.30885816122147,12.5797571720116));
#448870=CARTESIAN_POINT('Ctrl Pts',(2.3274456058322,1.30796366034395,12.580211740231));
#448871=CARTESIAN_POINT('Ctrl Pts',(2.32753727948252,1.30700546781519,12.5806009430798));
#448872=CARTESIAN_POINT('Ctrl Pts',(2.32775033112578,1.30605272353595,12.5808812374708));
#448873=CARTESIAN_POINT('Ctrl Pts',(2.32793341316648,1.30523400013046,12.5811221033394));
#448874=CARTESIAN_POINT('Ctrl Pts',(2.32820998647182,1.30440256344648,12.581287365893));
#448875=CARTESIAN_POINT('Ctrl Pts',(2.32857235253435,1.3036079729103,12.581359338449));
#448876=CARTESIAN_POINT('Ctrl Pts',(2.32862271393447,1.30349754123344,12.5813693411482));
#448877=CARTESIAN_POINT('Ctrl Pts',(2.32867468935954,1.30338777966755,12.5813775999465));
#448878=CARTESIAN_POINT('Ctrl Pts',(2.32872821476693,1.30327877787652,12.5813841266931));
#448879=CARTESIAN_POINT('Ctrl Pts',(2.32881902709433,1.30309384315453,12.5813952001081));
#448880=CARTESIAN_POINT('Ctrl Pts',(2.32891545583196,1.30291012523305,12.5814007534795));
#448881=CARTESIAN_POINT('Ctrl Pts',(2.32901763360014,1.30272779577977,12.5814005856065));
#448882=CARTESIAN_POINT('Ctrl Pts',(2.32948536347396,1.30189316282882,12.5813998171494));
#448883=CARTESIAN_POINT('Ctrl Pts',(2.33004095047256,1.30114512627378,12.58127954464));
#448884=CARTESIAN_POINT('Ctrl Pts',(2.33065748618066,1.30047029012495,12.5810700125799));
#448885=CARTESIAN_POINT('Ctrl Pts',(2.33140219111783,1.29965516489341,12.5808169217085));
#448886=CARTESIAN_POINT('Ctrl Pts',(2.33224824269838,1.29895805293504,12.5804173076348));
#448887=CARTESIAN_POINT('Ctrl Pts',(2.33310493392748,1.29841994931524,12.5799304713245));
#448888=CARTESIAN_POINT('Ctrl Pts',(2.3341666442459,1.29775306941019,12.5793271277669));
#448889=CARTESIAN_POINT('Ctrl Pts',(2.3352934286002,1.29726177537674,12.5785808224116));
#448890=CARTESIAN_POINT('Ctrl Pts',(2.33642511441489,1.29693770273082,12.5777485681082));
#448891=CARTESIAN_POINT('Ctrl Pts',(2.33811145026421,1.29645479898359,12.576508418016));
#448892=CARTESIAN_POINT('Ctrl Pts',(2.33979257822632,1.29634065746709,12.5750928681475));
#448893=CARTESIAN_POINT('Ctrl Pts',(2.34120305426879,1.29655563422097,12.5737548217797));
#448894=CARTESIAN_POINT('Ctrl Pts',(2.34120305426879,1.29655563422097,12.5737548217797));
#448895=CARTESIAN_POINT('Ctrl Pts',(2.3460820270025,1.28093515727823,12.5770542771492));
#448896=CARTESIAN_POINT('Ctrl Pts',(2.35734085275916,1.28223802992782,12.5893111709658));
#448897=CARTESIAN_POINT('Ctrl Pts',(2.36579221694363,1.29945184435155,12.5508408821982));
#448898=CARTESIAN_POINT('Ctrl Pts',(2.37068323832445,1.28378201236515,12.55409748406));
#448899=CARTESIAN_POINT('Ctrl Pts',(2.38195642745925,1.28508654714655,12.5663972313419));
#448900=CARTESIAN_POINT('Ctrl Pts',(2.39035749707839,1.30234405383429,12.52790050457));
#448901=CARTESIAN_POINT('Ctrl Pts',(2.39523733247122,1.28662341504699,12.5311362602938));
#448902=CARTESIAN_POINT('Ctrl Pts',(2.40654716908935,1.28793219067949,12.5434568539655));
#448903=CARTESIAN_POINT('Ctrl Pts',(2.41490075227283,1.30523255981786,12.5049357605811));
#448904=CARTESIAN_POINT('Ctrl Pts',(2.41974922116736,1.28945993370906,12.5081700652078));
#448905=CARTESIAN_POINT('Ctrl Pts',(2.43111502258053,1.29077518559428,12.5204921097672));
#448906=CARTESIAN_POINT('Ctrl Pts',(2.41328914611567,1.30504288761613,12.5064436508395));
#448907=CARTESIAN_POINT('Ctrl Pts',(2.41404361045141,1.30408391349934,12.5062361689309));
#448908=CARTESIAN_POINT('Ctrl Pts',(2.41478729883436,1.3030544868582,12.5061871075061));
#448909=CARTESIAN_POINT('Ctrl Pts',(2.4154499997122,1.30201918777695,12.5063648335164));
#448910=CARTESIAN_POINT('Ctrl Pts',(2.415751039328,1.30154889107435,12.5064455676329));
#448911=CARTESIAN_POINT('Ctrl Pts',(2.4160393801953,1.3010707041361,12.506574497099));
#448912=CARTESIAN_POINT('Ctrl Pts',(2.4163017591295,1.30060458749904,12.5067492519495));
#448913=CARTESIAN_POINT('Ctrl Pts',(2.41682901978261,1.29966790802348,12.5071004286051));
#448914=CARTESIAN_POINT('Ctrl Pts',(2.41727012097808,1.29874513659593,12.5076537929613));
#448915=CARTESIAN_POINT('Ctrl Pts',(2.41760048935406,1.29790961126267,12.5083435010505));
#448916=CARTESIAN_POINT('Ctrl Pts',(2.41762128801762,1.29785700994982,12.5083869222964));
#448917=CARTESIAN_POINT('Ctrl Pts',(2.41764163896602,1.29780474430814,12.5084308732337));
#448918=CARTESIAN_POINT('Ctrl Pts',(2.41766153276987,1.29775282825451,12.5084753333615));
#448919=CARTESIAN_POINT('Ctrl Pts',(2.41782110733411,1.29733639298138,12.5088319622689));
#448920=CARTESIAN_POINT('Ctrl Pts',(2.4179557127917,1.29693445804919,12.509227847131));
#448921=CARTESIAN_POINT('Ctrl Pts',(2.41806400173893,1.2965598642607,12.5096423454524));
#448922=CARTESIAN_POINT('Ctrl Pts',(2.41840333137287,1.29538605311581,12.5109411997424));
#448923=CARTESIAN_POINT('Ctrl Pts',(2.41851441364044,1.29441119783451,12.5124831113042));
#448924=CARTESIAN_POINT('Ctrl Pts',(2.41848765682672,1.293607330589,12.5140723025008));
#448925=CARTESIAN_POINT('Ctrl Pts',(2.41848514968397,1.29353200734764,12.5142212114565));
#448926=CARTESIAN_POINT('Ctrl Pts',(2.41848145573209,1.29345816722788,12.5143705582413));
#448927=CARTESIAN_POINT('Ctrl Pts',(2.41847666366391,1.29338577808433,12.5145201959299));
#448928=CARTESIAN_POINT('Ctrl Pts',(2.41841510241349,1.29245583175926,12.5164425148273));
#448929=CARTESIAN_POINT('Ctrl Pts',(2.41818092200696,1.29173277068538,12.5184635205941));
#448930=CARTESIAN_POINT('Ctrl Pts',(2.41783386717489,1.29114900384466,12.5205025929158));
#448931=CARTESIAN_POINT('Ctrl Pts',(2.41763256161632,1.29081039593868,12.5216853356836));
#448932=CARTESIAN_POINT('Ctrl Pts',(2.41739405919928,1.29051901757365,12.5228750347131));
#448933=CARTESIAN_POINT('Ctrl Pts',(2.41713422275923,1.29026585187105,12.5240609649613));
#448934=CARTESIAN_POINT('Ctrl Pts',(2.41649646815689,1.28964447023587,12.5269717671326));
#448935=CARTESIAN_POINT('Ctrl Pts',(2.41570498716153,1.28924325106614,12.5299036066169));
#448936=CARTESIAN_POINT('Ctrl Pts',(2.41481087945404,1.28899220618257,12.5328133004019));
#448937=CARTESIAN_POINT('Ctrl Pts',(2.41438165569212,1.28887169002055,12.5342101228451));
#448938=CARTESIAN_POINT('Ctrl Pts',(2.41392917487694,1.28878643734573,12.5356023438238));
#448939=CARTESIAN_POINT('Ctrl Pts',(2.41346029074826,1.28873217793636,12.5369868989719));
#448940=CARTESIAN_POINT('Origin',(15.0752513500072,2.74862334284653,-1.24041811817541));
#448941=CARTESIAN_POINT('Ctrl Pts',(2.36123941047144,1.38201186200937,12.5369868989719));
#448942=CARTESIAN_POINT('Ctrl Pts',(2.37073948644324,1.39405477943892,12.5369868989719));
#448943=CARTESIAN_POINT('Ctrl Pts',(2.3627244217467,1.40713308367132,12.5369868989719));
#448944=CARTESIAN_POINT('Ctrl Pts',(2.36445075571135,1.38608288010418,12.5218025310016));
#448945=CARTESIAN_POINT('Ctrl Pts',(2.36887186146598,1.39704233664229,12.5216901060418));
#448946=CARTESIAN_POINT('Ctrl Pts',(2.36274886838135,1.40709322528321,12.5161920673677));
#448947=CARTESIAN_POINT('Ctrl Pts',(2.37047257207358,1.38581122058474,12.5042015548895));
#448948=CARTESIAN_POINT('Ctrl Pts',(2.37172872680604,1.39211989875893,12.4980677368513));
#448949=CARTESIAN_POINT('Ctrl Pts',(2.36828310199102,1.39797809381866,12.4907278922778));
#448950=CARTESIAN_POINT('Ctrl Pts',(2.37505684410862,1.3733523512695,12.506463626192));
#448951=CARTESIAN_POINT('Ctrl Pts',(2.38072083974236,1.3766274988688,12.4999376786891));
#448952=CARTESIAN_POINT('Ctrl Pts',(2.38065166227114,1.37658749770293,12.4906970594712));
#448953=CARTESIAN_POINT('Origin',(2.34396676596729,1.39563741711121,12.5369868989719));
#448954=CARTESIAN_POINT('Origin',(2.34396676596729,1.39563741711121,14.));
#448955=CARTESIAN_POINT('Origin',(2.34396676596729,1.39563741711121,13.7435492065112));
#448956=CARTESIAN_POINT('Ctrl Pts',(2.34596719356845,1.36257596155278,13.793642941384));
#448957=CARTESIAN_POINT('Ctrl Pts',(2.35266897582987,1.3710607911637,13.8071662555867));
#448958=CARTESIAN_POINT('Ctrl Pts',(2.34100211148853,1.38346658255626,13.8103758687955));
#448959=CARTESIAN_POINT('Ctrl Pts',(2.35623656914238,1.37564507133673,13.7804579775006));
#448960=CARTESIAN_POINT('Ctrl Pts',(2.36449800484156,1.38612086972719,13.7901904343351));
#448961=CARTESIAN_POINT('Ctrl Pts',(2.35570307465003,1.39919393849814,13.7927914348262));
#448962=CARTESIAN_POINT('Ctrl Pts',(2.36228253699291,1.38333934813595,13.7597120340895));
#448963=CARTESIAN_POINT('Ctrl Pts',(2.37183884511689,1.3954663454977,13.7635825532445));
#448964=CARTESIAN_POINT('Ctrl Pts',(2.36435354136949,1.40848579801899,13.7651073818884));
#448965=CARTESIAN_POINT('Ctrl Pts',(2.36109859805022,1.38183263256027,13.7381884353898));
#448966=CARTESIAN_POINT('Ctrl Pts',(2.37043192895505,1.39367521863119,13.7368803041982));
#448967=CARTESIAN_POINT('Ctrl Pts',(2.36265916120258,1.40666651258464,13.7363986145813));
#448968=CARTESIAN_POINT('Origin',(2.33116056166861,1.37933985838202,13.7902182540695));
#448969=CARTESIAN_POINT('Ctrl Pts',(2.32635800710304,1.33762068146841,13.8235227101244));
#448970=CARTESIAN_POINT('Ctrl Pts',(2.33346496801523,1.34665803699489,13.8358800583119));
#448971=CARTESIAN_POINT('Ctrl Pts',(2.3224883845271,1.35907337686075,13.8390832900376));
#448972=CARTESIAN_POINT('Ctrl Pts',(2.33372747122631,1.34699928199462,13.8124254819053));
#448973=CARTESIAN_POINT('Ctrl Pts',(2.34084823353721,1.35605418810938,13.8247886449157));
#448974=CARTESIAN_POINT('Ctrl Pts',(2.32984501138978,1.36847392576671,13.8279860620657));
#448975=CARTESIAN_POINT('Ctrl Pts',(2.34109363259552,1.35637367933719,13.8013225099955));
#448976=CARTESIAN_POINT('Ctrl Pts',(2.34822483802452,1.36544186233943,13.8136962257787));
#448977=CARTESIAN_POINT('Ctrl Pts',(2.33719844595767,1.37786995563124,13.8168830918626));
#448978=CARTESIAN_POINT('Ctrl Pts',(2.34845661971575,1.36574403703554,13.7902140179785));
#448979=CARTESIAN_POINT('Ctrl Pts',(2.35559512946828,1.37482150254402,13.802602731458));
#448980=CARTESIAN_POINT('Ctrl Pts',(2.34454881511306,1.38726164288434,13.8057746032558));
#448981=CARTESIAN_POINT('Origin',(2.30906194135381,1.35121649301826,13.8235269408515));
#448982=CARTESIAN_POINT('Ctrl Pts',(2.35734085275916,1.28223802992782,13.8235269408515));
#448983=CARTESIAN_POINT('Ctrl Pts',(2.36907006162998,1.28359533536707,13.8362179249168));
#448984=CARTESIAN_POINT('Ctrl Pts',(2.37375135115543,1.26717131233872,13.8391868794938));
#448985=CARTESIAN_POINT('Ctrl Pts',(2.34660913718441,1.28099615453089,13.8400110824519));
#448986=CARTESIAN_POINT('Ctrl Pts',(2.35640634747062,1.27868606070842,13.8494522556836));
#448987=CARTESIAN_POINT('Ctrl Pts',(2.35607706120985,1.26523914812621,13.85569149686));
#448988=CARTESIAN_POINT('Ctrl Pts',(2.33107758588531,1.28591231566416,13.8586819406588));
#448989=CARTESIAN_POINT('Ctrl Pts',(2.33321516119045,1.28211932008681,13.868010383617));
#448990=CARTESIAN_POINT('Ctrl Pts',(2.33033843592131,1.27353926656026,13.8744918421245));
#448991=CARTESIAN_POINT('Ctrl Pts',(2.31575650694236,1.31319483823762,13.8587686893867));
#448992=CARTESIAN_POINT('Ctrl Pts',(2.31363790698273,1.31695404854444,13.8680909899357));
#448993=CARTESIAN_POINT('Ctrl Pts',(2.3048355821446,1.31895791454536,13.8745789365162));
#448994=CARTESIAN_POINT('Ctrl Pts',(2.31967473133409,1.32911534355549,13.8400379222776));
#448995=CARTESIAN_POINT('Ctrl Pts',(2.32282622863558,1.33867245078868,13.8494748685453));
#448996=CARTESIAN_POINT('Ctrl Pts',(2.31120161292003,1.34542740561683,13.8557104837033));
#448997=CARTESIAN_POINT('Ctrl Pts',(2.32636043967773,1.3376237760181,13.8235269408542));
#448998=CARTESIAN_POINT('Ctrl Pts',(2.33365570123341,1.34690794413509,13.8362179249195));
#448999=CARTESIAN_POINT('Ctrl Pts',(2.32211071702094,1.35949271046546,13.8391868794964));
#449000=CARTESIAN_POINT('Origin',(2.35986981879868,1.26038386943671,13.8235269408515));
#449001=CARTESIAN_POINT('Ctrl Pts',(2.39286675657413,1.28634909095845,13.7902140241682));
#449002=CARTESIAN_POINT('Ctrl Pts',(2.40433779006288,1.2876810016508,13.8026027327198));
#449003=CARTESIAN_POINT('Ctrl Pts',(2.40915682872283,1.27175759753398,13.8057746032556));
#449004=CARTESIAN_POINT('Ctrl Pts',(2.38102865958112,1.28497918497389,13.8013225161808));
#449005=CARTESIAN_POINT('Ctrl Pts',(2.39248796053712,1.28630972978154,13.8136962270464));
#449006=CARTESIAN_POINT('Ctrl Pts',(2.39730716051404,1.27040960660921,13.8168830918628));
#449007=CARTESIAN_POINT('Ctrl Pts',(2.369185459078,1.28360868841055,13.8124254880875));
#449008=CARTESIAN_POINT('Ctrl Pts',(2.38062798112169,1.28493728327733,13.8247886461867));
#449009=CARTESIAN_POINT('Ctrl Pts',(2.38545218759873,1.26906127640957,13.8279860620656));
#449010=CARTESIAN_POINT('Ctrl Pts',(2.35733694845468,1.28223757735948,13.8235227163065));
#449011=CARTESIAN_POINT('Ctrl Pts',(2.36875729232489,1.28356359739057,13.8358800595847));
#449012=CARTESIAN_POINT('Ctrl Pts',(2.3735916932322,1.26771259115546,13.8390832900376));
#449013=CARTESIAN_POINT('Origin',(2.39539963927864,1.26449538446932,13.7902182540695));
#449014=CARTESIAN_POINT('Ctrl Pts',(2.41319222293699,1.28870112932895,13.7382347919292));
#449015=CARTESIAN_POINT('Ctrl Pts',(2.42817973395686,1.29045964636402,13.7369371795942));
#449016=CARTESIAN_POINT('Ctrl Pts',(2.43517974500568,1.27702299416428,13.7364597369712));
#449017=CARTESIAN_POINT('Ctrl Pts',(2.4150712422314,1.28891857006904,13.7595490285574));
#449018=CARTESIAN_POINT('Ctrl Pts',(2.43041645958188,1.29071804523856,13.7633824266926));
#449019=CARTESIAN_POINT('Ctrl Pts',(2.43758682550866,1.27750897590027,13.7648920890506));
#449020=CARTESIAN_POINT('Ctrl Pts',(2.40548834677001,1.28780963421491,13.780380659011));
#449021=CARTESIAN_POINT('Ctrl Pts',(2.4187607817919,1.28937147754697,13.7901039518744));
#449022=CARTESIAN_POINT('Ctrl Pts',(2.42531453147815,1.2750350272724,13.7926933640892));
#449023=CARTESIAN_POINT('Ctrl Pts',(2.38883113529569,1.28588205607826,13.7936647693663));
#449024=CARTESIAN_POINT('Ctrl Pts',(2.39957137332815,1.28715509140806,13.8072068914933));
#449025=CARTESIAN_POINT('Ctrl Pts',(2.40403098918034,1.27070042348985,13.8104111085397));
#449026=CARTESIAN_POINT('Origin',(2.41598925678778,1.26687801744526,13.7435492065112));
#449027=CARTESIAN_POINT('Origin',(2.41598925678778,1.26687801744526,14.));
#449028=CARTESIAN_POINT('Origin',(2.41598925678778,1.26687801744526,12.5369868989719));
#449029=CARTESIAN_POINT('Ctrl Pts',(2.41327297583393,1.30503414316753,12.506462012331));
#449030=CARTESIAN_POINT('Ctrl Pts',(2.41902448424168,1.30814440666528,12.4999388158272));
#449031=CARTESIAN_POINT('Ctrl Pts',(2.41895643635458,1.30810760816924,12.4907030323752));
#449032=CARTESIAN_POINT('Ctrl Pts',(2.4214881807439,1.29460634419357,12.5042014951932));
#449033=CARTESIAN_POINT('Ctrl Pts',(2.42751896744353,1.29237683552585,12.4980716682127));
#449034=CARTESIAN_POINT('Ctrl Pts',(2.43070657950927,1.28637977836885,12.4907355092743));
#449035=CARTESIAN_POINT('Ctrl Pts',(2.41857050922723,1.28933255104575,12.5218047446509));
#449036=CARTESIAN_POINT('Ctrl Pts',(2.43021709765855,1.28736383348164,12.5216906929434));
#449037=CARTESIAN_POINT('Ctrl Pts',(2.43557754544319,1.27689309550011,12.5161988840776));
#449038=CARTESIAN_POINT('Ctrl Pts',(2.41342213315448,1.28872772857038,12.5369868989719));
#449039=CARTESIAN_POINT('Ctrl Pts',(2.42864730001847,1.29051653417306,12.5369868989719));
#449040=CARTESIAN_POINT('Ctrl Pts',(2.43559795424792,1.27685293518512,12.5369868989719));
#449041=CARTESIAN_POINT('Origin',(4.49626278878391E-31,-2.63684586248246E-31,
12.5));
#449042=CARTESIAN_POINT('Origin',(2.24498269238232,1.47011665264505,12.5));
#449043=CARTESIAN_POINT('',(2.24498269238232,1.47011665264505,12.5893111709658));
#449044=CARTESIAN_POINT('',(2.24498269238232,1.47011665264505,13.8235269408515));
#449045=CARTESIAN_POINT('',(2.24498269238232,1.47011665264505,12.5));
#449046=CARTESIAN_POINT('',(2.28005916367103,1.47711049716244,13.7902182540695));
#449047=CARTESIAN_POINT('',(2.24498269238232,1.47011665264505,13.8235269408515));
#449048=CARTESIAN_POINT('',(2.30038606421962,1.48116344709537,13.7435492065112));
#449049=CARTESIAN_POINT('Origin',(2.23351076640297,1.46782961485557,13.7445212918716));
#449050=CARTESIAN_POINT('',(2.30038606421962,1.48116344709537,12.5369868989719));
#449051=CARTESIAN_POINT('',(2.30038606421962,1.48116344709537,12.5));
#449052=CARTESIAN_POINT('Ctrl Pts',(2.30038606421962,1.48116344709537,12.5369868989719));
#449053=CARTESIAN_POINT('Ctrl Pts',(2.28193174289042,1.4774838678986,12.5544431401645));
#449054=CARTESIAN_POINT('Ctrl Pts',(2.26346422254012,1.47380165696898,12.5718848856037));
#449055=CARTESIAN_POINT('Ctrl Pts',(2.24498269238232,1.47011665264505,12.5893111709658));
#449056=CARTESIAN_POINT('Origin',(2.36130966352237,1.75215381130026,12.5));
#449057=CARTESIAN_POINT('',(2.24075887558448,1.56991110033551,13.7435492065112));
#449058=CARTESIAN_POINT('',(2.22932368520975,1.55262394585119,13.7902182540695));
#449059=CARTESIAN_POINT('Origin',(2.19927398130261,1.50719629168648,13.7418732680442));
#449060=CARTESIAN_POINT('',(2.20959091159277,1.52279291595643,13.8235269408515));
#449061=CARTESIAN_POINT('',(2.22932368520975,1.55262394585119,13.7902182540695));
#449062=CARTESIAN_POINT('',(2.20959091159277,1.52279291595643,12.5893111709658));
#449063=CARTESIAN_POINT('',(2.20959091159277,1.52279291595643,12.5));
#449064=CARTESIAN_POINT('',(2.24075887558448,1.56991110033551,12.5369868989719));
#449065=CARTESIAN_POINT('Ctrl Pts',(2.20959091159277,1.52279291595643,12.5893111709658));
#449066=CARTESIAN_POINT('Ctrl Pts',(2.21998796230228,1.53851066230841,12.5718848856037));
#449067=CARTESIAN_POINT('Ctrl Pts',(2.23037713159299,1.55421649392178,12.5544431401645));
#449068=CARTESIAN_POINT('Ctrl Pts',(2.24075887558448,1.56991110033551,12.5369868989719));
#449069=CARTESIAN_POINT('',(2.24075887558448,1.56991110033551,12.5));
#449070=CARTESIAN_POINT('Origin',(2.23826102351075,1.50382807196523,12.5));
#449071=CARTESIAN_POINT('',(2.21036815174207,1.48373882417756,13.8587068136939));
#449072=CARTESIAN_POINT('Ctrl Pts',(2.20959091158718,1.52279291595995,13.8235269408542));
#449073=CARTESIAN_POINT('Ctrl Pts',(2.20862416062284,1.52133142973009,13.8262006681044));
#449074=CARTESIAN_POINT('Ctrl Pts',(2.20777973774708,1.51973995932856,13.8288634856214));
#449075=CARTESIAN_POINT('Ctrl Pts',(2.20704962302618,1.51802915776954,13.8314912288862));
#449076=CARTESIAN_POINT('Ctrl Pts',(2.20629695005677,1.51626549782319,13.8342001611531));
#449077=CARTESIAN_POINT('Ctrl Pts',(2.20566446484758,1.51437325493347,13.8368750301949));
#449078=CARTESIAN_POINT('Ctrl Pts',(2.20517308358036,1.51233002866895,13.8394886372969));
#449079=CARTESIAN_POINT('Ctrl Pts',(2.20513513301317,1.51217222534838,13.8396904925131));
#449080=CARTESIAN_POINT('Ctrl Pts',(2.20509804442956,1.51201351262336,13.8398919674349));
#449081=CARTESIAN_POINT('Ctrl Pts',(2.20506183832379,1.51185387656114,13.8400930404591));
#449082=CARTESIAN_POINT('Ctrl Pts',(2.20449772283759,1.50936663931377,13.8432258934518));
#449083=CARTESIAN_POINT('Ctrl Pts',(2.20414961619355,1.50666819556832,13.8462331177034));
#449084=CARTESIAN_POINT('Ctrl Pts',(2.20412454525322,1.50383421189661,13.8489036603661));
#449085=CARTESIAN_POINT('Ctrl Pts',(2.20411634174978,1.50290689945849,13.849777493004));
#449086=CARTESIAN_POINT('Ctrl Pts',(2.2041428636101,1.50196528299333,13.85061494757));
#449087=CARTESIAN_POINT('Ctrl Pts',(2.20420824668703,1.5010126137019,13.8514076489583));
#449088=CARTESIAN_POINT('Ctrl Pts',(2.20434654132439,1.49899758075505,13.8530843267192));
#449089=CARTESIAN_POINT('Ctrl Pts',(2.20467522981035,1.49673537254486,13.8546805203176));
#449090=CARTESIAN_POINT('Ctrl Pts',(2.20531026306347,1.49437690575371,13.8559412814273));
#449091=CARTESIAN_POINT('Ctrl Pts',(2.20539525110736,1.49406126641016,13.8561100121513));
#449092=CARTESIAN_POINT('Ctrl Pts',(2.20548565668459,1.49374393581815,13.8562727473908));
#449093=CARTESIAN_POINT('Ctrl Pts',(2.20558168565612,1.4934252993382,13.8564289040185));
#449094=CARTESIAN_POINT('Ctrl Pts',(2.20601717594647,1.49198028653681,13.8571370725437));
#449095=CARTESIAN_POINT('Ctrl Pts',(2.20657815194651,1.49048367427338,13.8577210840554));
#449096=CARTESIAN_POINT('Ctrl Pts',(2.20727028937841,1.48900393683601,13.8581177131616));
#449097=CARTESIAN_POINT('Ctrl Pts',(2.20746521910188,1.48858719184263,13.8582294175695));
#449098=CARTESIAN_POINT('Ctrl Pts',(2.20767037977277,1.48817174305277,13.8583265086086));
#449099=CARTESIAN_POINT('Ctrl Pts',(2.20788547823267,1.48775899017047,13.8584082369006));
#449100=CARTESIAN_POINT('Ctrl Pts',(2.20819451703861,1.48716597496268,13.8585256585398));
#449101=CARTESIAN_POINT('Ctrl Pts',(2.20852819823668,1.48657130149863,13.8586122832068));
#449102=CARTESIAN_POINT('Ctrl Pts',(2.208878542435,1.48599080410042,13.8586682984299));
#449103=CARTESIAN_POINT('Ctrl Pts',(2.20915878306515,1.48552646372471,13.8587131050557));
#449104=CARTESIAN_POINT('Ctrl Pts',(2.20945257987857,1.48506594398009,13.8587357943552));
#449105=CARTESIAN_POINT('Ctrl Pts',(2.20976039474481,1.48460946252997,13.8587355499465));
#449106=CARTESIAN_POINT('Ctrl Pts',(2.20995934283152,1.48431442768573,13.8587353919793));
#449107=CARTESIAN_POINT('Ctrl Pts',(2.21016196328106,1.48402424862251,13.8587257282814));
#449108=CARTESIAN_POINT('Ctrl Pts',(2.21036815174207,1.48373882417756,13.8587068136939));
#449109=CARTESIAN_POINT('Ctrl Pts',(2.21036815174207,1.48373882417756,13.8587068136939));
#449110=CARTESIAN_POINT('Ctrl Pts',(2.21104629434983,1.48280007873827,13.8586446046466));
#449111=CARTESIAN_POINT('Ctrl Pts',(2.21176298558344,1.48191270074552,13.858482427929));
#449112=CARTESIAN_POINT('Ctrl Pts',(2.21251494810213,1.48107364964105,13.8582284286032));
#449113=CARTESIAN_POINT('Ctrl Pts',(2.21328637417442,1.48021288081029,13.8579678548414));
#449114=CARTESIAN_POINT('Ctrl Pts',(2.21409794606332,1.47940189260247,13.857615680862));
#449115=CARTESIAN_POINT('Ctrl Pts',(2.21491081898393,1.47866580353012,13.8571944833187));
#449116=CARTESIAN_POINT('Ctrl Pts',(2.21693942649115,1.47682881796904,13.8561433417727));
#449117=CARTESIAN_POINT('Ctrl Pts',(2.21906780994789,1.47536882349349,13.8546163505475));
#449118=CARTESIAN_POINT('Ctrl Pts',(2.22109574890803,1.47423415154825,13.8528973491086));
#449119=CARTESIAN_POINT('Ctrl Pts',(2.2214662234366,1.47402686372437,13.8525833129072));
#449120=CARTESIAN_POINT('Ctrl Pts',(2.22183334150934,1.47383029191881,13.8522628768812));
#449121=CARTESIAN_POINT('Ctrl Pts',(2.22219590503271,1.47364394373746,13.851937733538));
#449122=CARTESIAN_POINT('Ctrl Pts',(2.22441003016648,1.47250594124864,13.8499521282529));
#449123=CARTESIAN_POINT('Ctrl Pts',(2.22667620572651,1.47163974725192,13.847639871647));
#449124=CARTESIAN_POINT('Ctrl Pts',(2.22884664546143,1.47101584018038,13.8452109780794));
#449125=CARTESIAN_POINT('Ctrl Pts',(2.22982317122403,1.47073513147467,13.8441181685877));
#449126=CARTESIAN_POINT('Ctrl Pts',(2.23078036982602,1.47050275273326,13.8430021611332));
#449127=CARTESIAN_POINT('Ctrl Pts',(2.23170603279204,1.47031295226536,13.8418824960098));
#449128=CARTESIAN_POINT('Ctrl Pts',(2.23388738120913,1.46986568261602,13.8392439765549));
#449129=CARTESIAN_POINT('Ctrl Pts',(2.23599712352092,1.4696297725911,13.8364981347964));
#449130=CARTESIAN_POINT('Ctrl Pts',(2.23803703636739,1.46957058972445,13.8336931113419));
#449131=CARTESIAN_POINT('Ctrl Pts',(2.24002378193342,1.4695129493708,13.8309611966328));
#449132=CARTESIAN_POINT('Ctrl Pts',(2.24194629785291,1.46962345039488,13.8281701127185));
#449133=CARTESIAN_POINT('Ctrl Pts',(2.24379299532685,1.46990710444376,13.825358068512));
#449134=CARTESIAN_POINT('Ctrl Pts',(2.2441933613322,1.46996860094768,13.8247484142932));
#449135=CARTESIAN_POINT('Ctrl Pts',(2.24459004640973,1.4700383635589,13.8241378483365));
#449136=CARTESIAN_POINT('Ctrl Pts',(2.24498269238232,1.47011665264505,13.8235269408515));
#449137=CARTESIAN_POINT('',(2.20966053613784,1.48475963611651,12.5969504640361));
#449138=CARTESIAN_POINT('Origin',(2.23828859526251,1.50384636079555,12.584524458991));
#449139=CARTESIAN_POINT('Origin',(2.23828859526251,1.50384636079555,12.584524458991));
#449140=CARTESIAN_POINT('Ctrl Pts',(2.20959091159277,1.52279291595643,12.5893111709658));
#449141=CARTESIAN_POINT('Ctrl Pts',(2.20333791462155,1.51333994481304,12.5770542771492));
#449142=CARTESIAN_POINT('Ctrl Pts',(2.21506416483589,1.50192509786858,12.5737548217797));
#449143=CARTESIAN_POINT('Ctrl Pts',(2.22326411740067,1.54346339133561,12.5663937883685));
#449144=CARTESIAN_POINT('Ctrl Pts',(2.21700314386343,1.53399836161473,12.5540940315304));
#449145=CARTESIAN_POINT('Ctrl Pts',(2.22876797124263,1.52255044337381,12.5508374392248));
#449146=CARTESIAN_POINT('Ctrl Pts',(2.23692352711152,1.56411301045852,12.5434499600945));
#449147=CARTESIAN_POINT('Ctrl Pts',(2.23064219691974,1.55461720655537,12.5311293540532));
#449148=CARTESIAN_POINT('Ctrl Pts',(2.24245740601019,1.54315629041795,12.5278936106989));
#449149=CARTESIAN_POINT('Ctrl Pts',(2.25057022139251,1.58474340702428,12.5204817579905));
#449150=CARTESIAN_POINT('Ctrl Pts',(2.24425780290893,1.57520060538135,12.5081597038247));
#449151=CARTESIAN_POINT('Ctrl Pts',(2.25613357461923,1.56374416216455,12.5049254088044));
#449152=CARTESIAN_POINT('Ctrl Pts',(2.24075887558448,1.56991110033551,12.5369868989719));
#449153=CARTESIAN_POINT('Ctrl Pts',(2.2412727911519,1.57068801214536,12.5342545179733));
#449154=CARTESIAN_POINT('Ctrl Pts',(2.24186729187868,1.57136063834112,12.5314872231885));
#449155=CARTESIAN_POINT('Ctrl Pts',(2.24255077409794,1.57185406834232,12.5287124745063));
#449156=CARTESIAN_POINT('Ctrl Pts',(2.2431671722883,1.57229906800908,12.5262100684184));
#449157=CARTESIAN_POINT('Ctrl Pts',(2.24385589586104,1.57259707501921,12.5237004536639));
#449158=CARTESIAN_POINT('Ctrl Pts',(2.24465509548773,1.57269236682436,12.5212220730815));
#449159=CARTESIAN_POINT('Ctrl Pts',(2.24526695193824,1.5727653209446,12.5193246583486));
#449160=CARTESIAN_POINT('Ctrl Pts',(2.2459509485987,1.57271970086603,12.517417831369));
#449161=CARTESIAN_POINT('Ctrl Pts',(2.24671988473605,1.57245912089718,12.5155812248348));
#449162=CARTESIAN_POINT('Ctrl Pts',(2.24704745566362,1.57234811242983,12.5147988205793));
#449163=CARTESIAN_POINT('Ctrl Pts',(2.24739086289924,1.57219824259547,12.5140295443047));
#449164=CARTESIAN_POINT('Ctrl Pts',(2.2477527956281,1.57200333889459,12.5132817086137));
#449165=CARTESIAN_POINT('Ctrl Pts',(2.24830053185208,1.5717083785093,12.5121499604604));
#449166=CARTESIAN_POINT('Ctrl Pts',(2.24889913361807,1.57129761210048,12.5110494206568));
#449167=CARTESIAN_POINT('Ctrl Pts',(2.2495385308929,1.57073518589319,12.5100666561695));
#449168=CARTESIAN_POINT('Ctrl Pts',(2.2499056713357,1.57041224206012,12.5095023550641));
#449169=CARTESIAN_POINT('Ctrl Pts',(2.25029007303371,1.57003507410021,12.5089719619137));
#449170=CARTESIAN_POINT('Ctrl Pts',(2.25068005762558,1.56960619264217,12.5085043804652));
#449171=CARTESIAN_POINT('Ctrl Pts',(2.25125074927671,1.56897858049405,12.5078201359221));
#449172=CARTESIAN_POINT('Ctrl Pts',(2.25184905478605,1.56822121101344,12.5072563000949));
#449173=CARTESIAN_POINT('Ctrl Pts',(2.25242777467969,1.56738017470561,12.5068768744332));
#449174=CARTESIAN_POINT('Ctrl Pts',(2.25284507156222,1.56677372963052,12.5066032824114));
#449175=CARTESIAN_POINT('Ctrl Pts',(2.25325956584798,1.56611316251982,12.5064197834844));
#449176=CARTESIAN_POINT('Ctrl Pts',(2.25365030060876,1.56543673503369,12.5063282718343));
#449177=CARTESIAN_POINT('Ctrl Pts',(2.25422065239109,1.56444936032059,12.5061946931565));
#449178=CARTESIAN_POINT('Ctrl Pts',(2.25475349020623,1.5634076193054,12.5062515701262));
#449179=CARTESIAN_POINT('Ctrl Pts',(2.25522951325349,1.56238320646031,12.5064436508398));
#449180=CARTESIAN_POINT('',(2.21506416483589,1.50192509786858,12.5737548217797));
#449181=CARTESIAN_POINT('Origin',(2.22793978322027,1.51065541580206,12.5893111709658));
#449182=CARTESIAN_POINT('Ctrl Pts',(2.25522951325349,1.56238320646031,12.5064436508398));
#449183=CARTESIAN_POINT('Ctrl Pts',(2.24928439834657,1.553433569792,12.5164271754438));
#449184=CARTESIAN_POINT('Ctrl Pts',(2.24333675276147,1.54448050109937,12.5264061185523));
#449185=CARTESIAN_POINT('Ctrl Pts',(2.23738648815821,1.53552387898569,12.536380305637));
#449186=CARTESIAN_POINT('Ctrl Pts',(2.22994986424784,1.52432991794228,12.5488460165097));
#449187=CARTESIAN_POINT('Ctrl Pts',(2.22250914723241,1.51313040318678,12.5613043021964));
#449188=CARTESIAN_POINT('Ctrl Pts',(2.21506416483589,1.50192509786858,12.5737548217797));
#449189=CARTESIAN_POINT('Ctrl Pts',(2.24498269238232,1.47011665264505,12.5893111709658));
#449190=CARTESIAN_POINT('Ctrl Pts',(2.2338675256558,1.46790041637572,12.5770542771492));
#449191=CARTESIAN_POINT('Ctrl Pts',(2.22773157341711,1.48307123589806,12.5737548217797));
#449192=CARTESIAN_POINT('Ctrl Pts',(2.2346123385011,1.46804892348157,12.5928319619712));
#449193=CARTESIAN_POINT('Ctrl Pts',(2.22650524262674,1.4697543304287,12.5821634970843));
#449194=CARTESIAN_POINT('Ctrl Pts',(2.22395575018039,1.48230875556751,12.5773203894503));
#449195=CARTESIAN_POINT('Ctrl Pts',(2.21831603931396,1.4719238082725,12.5969440695591));
#449196=CARTESIAN_POINT('Ctrl Pts',(2.21605911440408,1.47525019257127,12.5878292599214));
#449197=CARTESIAN_POINT('Ctrl Pts',(2.21814788990466,1.48369183405955,12.5813877129824));
#449198=CARTESIAN_POINT('Ctrl Pts',(2.20120771663137,1.49729072650333,12.596957478804));
#449199=CARTESIAN_POINT('Ctrl Pts',(2.20344802859256,1.49398897008205,12.5878468778671));
#449200=CARTESIAN_POINT('Ctrl Pts',(2.21202952953643,1.49277434113131,12.5814011370086));
#449201=CARTESIAN_POINT('Ctrl Pts',(2.20374844885825,1.51396057014061,12.5928371701607));
#449202=CARTESIAN_POINT('Ctrl Pts',(2.20227016042516,1.50581503584185,12.5821692192952));
#449203=CARTESIAN_POINT('Ctrl Pts',(2.21292407734148,1.49870744297872,12.5773318885715));
#449204=CARTESIAN_POINT('Ctrl Pts',(2.20959091159272,1.52279291595645,12.5893111709658));
#449205=CARTESIAN_POINT('Ctrl Pts',(2.2033379146215,1.51333994481307,12.5770542771492));
#449206=CARTESIAN_POINT('Ctrl Pts',(2.21506416483584,1.5019250978686,12.5737548217797));
#449207=CARTESIAN_POINT('',(2.22773157341711,1.48307123589806,12.5737548217797));
#449208=CARTESIAN_POINT('Origin',(2.24068082430451,1.49169196100996,12.5893111709658));
#449209=CARTESIAN_POINT('Ctrl Pts',(2.21506416483584,1.5019250978686,12.5737548217797));
#449210=CARTESIAN_POINT('Ctrl Pts',(2.21448430274599,1.50110773651169,12.5746934679442));
#449211=CARTESIAN_POINT('Ctrl Pts',(2.21399205215106,1.50009727879856,12.5756680099006));
#449212=CARTESIAN_POINT('Ctrl Pts',(2.2136404235203,1.49901014450419,12.5765688348656));
#449213=CARTESIAN_POINT('Ctrl Pts',(2.21354733373296,1.49872233773472,12.5768073183026));
#449214=CARTESIAN_POINT('Ctrl Pts',(2.21346388168446,1.49842929322309,12.5770407398754));
#449215=CARTESIAN_POINT('Ctrl Pts',(2.21339051374517,1.49813334003695,12.5772674179684));
#449216=CARTESIAN_POINT('Ctrl Pts',(2.21308943156186,1.49691882819014,12.5781976435658));
#449217=CARTESIAN_POINT('Ctrl Pts',(2.21295201958902,1.49558363703061,12.5790594849312));
#449218=CARTESIAN_POINT('Ctrl Pts',(2.21303559156923,1.49421297717208,12.5797571720116));
#449219=CARTESIAN_POINT('Ctrl Pts',(2.21309004171931,1.49331994298971,12.580211740231));
#449220=CARTESIAN_POINT('Ctrl Pts',(2.21325951191965,1.4923724110211,12.5806009430798));
#449221=CARTESIAN_POINT('Ctrl Pts',(2.21354951215474,1.49144020260665,12.5808812374708));
#449222=CARTESIAN_POINT('Ctrl Pts',(2.21379871856325,1.49063912632172,12.5811221033394));
#449223=CARTESIAN_POINT('Ctrl Pts',(2.21414214140216,1.48983299946668,12.581287365893));
#449224=CARTESIAN_POINT('Ctrl Pts',(2.21456806822683,1.48907058906311,12.581359338449));
#449225=CARTESIAN_POINT('Ctrl Pts',(2.21462726326041,1.48896462976018,12.5813693411482));
#449226=CARTESIAN_POINT('Ctrl Pts',(2.21468801232813,1.48885946989651,12.5813775999465));
#449227=CARTESIAN_POINT('Ctrl Pts',(2.21475024429204,1.48875519361755,12.5813841266931));
#449228=CARTESIAN_POINT('Ctrl Pts',(2.21485582834561,1.48857827629834,12.5813952001081));
#449229=CARTESIAN_POINT('Ctrl Pts',(2.21496691094072,1.48840302952041,12.5814007534795));
#449230=CARTESIAN_POINT('Ctrl Pts',(2.21508361026391,1.48822963519001,12.5814005856065));
#449231=CARTESIAN_POINT('Ctrl Pts',(2.21561781413902,1.48743590373826,12.5813998171494));
#449232=CARTESIAN_POINT('Ctrl Pts',(2.21623252439138,1.48673564171136,12.58127954464));
#449233=CARTESIAN_POINT('Ctrl Pts',(2.21690201403878,1.48611330440799,12.5810700125799));
#449234=CARTESIAN_POINT('Ctrl Pts',(2.21771068130532,1.4853615918043,12.5808169217085));
#449235=CARTESIAN_POINT('Ctrl Pts',(2.21861073881532,1.48473576048663,12.5804173076348));
#449236=CARTESIAN_POINT('Ctrl Pts',(2.21950843991555,1.48426927565054,12.5799304713245));
#449237=CARTESIAN_POINT('Ctrl Pts',(2.22062097438374,1.48369115398075,12.5793271277669));
#449238=CARTESIAN_POINT('Ctrl Pts',(2.22178405448073,1.4832933380731,12.5785808224116));
#449239=CARTESIAN_POINT('Ctrl Pts',(2.22293838963342,1.48306258665214,12.5777485681082));
#449240=CARTESIAN_POINT('Ctrl Pts',(2.22465847547777,1.48271874175419,12.576508418016));
#449241=CARTESIAN_POINT('Ctrl Pts',(2.2263433132185,1.4827420075699,12.5750928681475));
#449242=CARTESIAN_POINT('Ctrl Pts',(2.22773157341711,1.48307123589806,12.5737548217797));
#449243=CARTESIAN_POINT('Ctrl Pts',(2.22773157341711,1.48307123589806,12.5737548217797));
#449244=CARTESIAN_POINT('Ctrl Pts',(2.2338675256558,1.46790041637572,12.5770542771492));
#449245=CARTESIAN_POINT('Ctrl Pts',(2.24498269238232,1.47011665264505,12.5893111709658));
#449246=CARTESIAN_POINT('Ctrl Pts',(2.25200284966887,1.48796205416098,12.5508408821982));
#449247=CARTESIAN_POINT('Ctrl Pts',(2.25815483335804,1.47274302589642,12.55409748406));
#449248=CARTESIAN_POINT('Ctrl Pts',(2.26928418019057,1.47496208951563,12.5663972313419));
#449249=CARTESIAN_POINT('Ctrl Pts',(2.27625064893766,1.49284693843918,12.52790050457));
#449250=CARTESIAN_POINT('Ctrl Pts',(2.28239562508524,1.47757636066729,12.5311362602938));
#449251=CARTESIAN_POINT('Ctrl Pts',(2.29356115179089,1.47980263813662,12.5434568539655));
#449252=CARTESIAN_POINT('Ctrl Pts',(2.30047679842188,1.4977263363042,12.5049357605811));
#449253=CARTESIAN_POINT('Ctrl Pts',(2.30659474988991,1.48240138753351,12.5081700652078));
#449254=CARTESIAN_POINT('Ctrl Pts',(2.31781552729765,1.48463868135671,12.5204921097672));
#449255=CARTESIAN_POINT('Ctrl Pts',(2.29888601479652,1.49740593435784,12.5064436508395));
#449256=CARTESIAN_POINT('Ctrl Pts',(2.29971613400763,1.49651164699579,12.5062361689309));
#449257=CARTESIAN_POINT('Ctrl Pts',(2.30054125565682,1.49554626319414,12.5061871075061));
#449258=CARTESIAN_POINT('Ctrl Pts',(2.30128613793853,1.49456842525894,12.5063648335164));
#449259=CARTESIAN_POINT('Ctrl Pts',(2.30162450941712,1.49412423095323,12.5064455676329));
#449260=CARTESIAN_POINT('Ctrl Pts',(2.30195086752871,1.49367113760007,12.506574497099));
#449261=CARTESIAN_POINT('Ctrl Pts',(2.30225036625179,1.49322795824661,12.5067492519495));
#449262=CARTESIAN_POINT('Ctrl Pts',(2.30285222056147,1.49233737213291,12.5071004286051));
#449263=CARTESIAN_POINT('Ctrl Pts',(2.303367068467,1.49145362499365,12.5076537929612));
#449264=CARTESIAN_POINT('Ctrl Pts',(2.30376444064075,1.49064780789172,12.5083435010503));
#449265=CARTESIAN_POINT('Ctrl Pts',(2.30378945759384,1.49059707688947,12.5083869222963));
#449266=CARTESIAN_POINT('Ctrl Pts',(2.3038140009612,1.49054664394855,12.5084308732336));
#449267=CARTESIAN_POINT('Ctrl Pts',(2.30383806021042,1.49049652217092,12.5084753333615));
#449268=CARTESIAN_POINT('Ctrl Pts',(2.30403104714423,1.49009447936021,12.508831962269));
#449269=CARTESIAN_POINT('Ctrl Pts',(2.30419796614161,1.48970485342778,12.509227847131));
#449270=CARTESIAN_POINT('Ctrl Pts',(2.30433642763762,1.48934033262371,12.5096423454524));
#449271=CARTESIAN_POINT('Ctrl Pts',(2.30477030468563,1.48819808575393,12.5109411997424));
#449272=CARTESIAN_POINT('Ctrl Pts',(2.30496047709166,1.4872355284592,12.5124831113042));
#449273=CARTESIAN_POINT('Ctrl Pts',(2.30499933195228,1.48643215508692,12.5140723025007));
#449274=CARTESIAN_POINT('Ctrl Pts',(2.30500297269527,1.48635687812203,12.5142212114565));
#449275=CARTESIAN_POINT('Ctrl Pts',(2.30500530968998,1.48628298260781,12.5143705582413));
#449276=CARTESIAN_POINT('Ctrl Pts',(2.30500643395424,1.48621044373511,12.5145201959299));
#449277=CARTESIAN_POINT('Ctrl Pts',(2.30502087680249,1.4852785739163,12.5164425148273));
#449278=CARTESIAN_POINT('Ctrl Pts',(2.30484641180203,1.48453883089135,12.5184635205941));
#449279=CARTESIAN_POINT('Ctrl Pts',(2.30454809418324,1.48392871829592,12.5205025929157));
#449280=CARTESIAN_POINT('Ctrl Pts',(2.30437505814013,1.48357482880796,12.5216853356836));
#449281=CARTESIAN_POINT('Ctrl Pts',(2.30416109936197,1.48326497981927,12.5228750347131));
#449282=CARTESIAN_POINT('Ctrl Pts',(2.30392276286129,1.48299147742258,12.5240609649613));
#449283=CARTESIAN_POINT('Ctrl Pts',(2.30333777870667,1.48232018046282,12.5269717671326));
#449284=CARTESIAN_POINT('Ctrl Pts',(2.3025816343861,1.48185578326791,12.5299036066169));
#449285=CARTESIAN_POINT('Ctrl Pts',(2.30171096423685,1.48153269563683,12.5328133004019));
#449286=CARTESIAN_POINT('Ctrl Pts',(2.3012929918676,1.48137759476108,12.5342101228451));
#449287=CARTESIAN_POINT('Ctrl Pts',(2.30084896552946,1.48125574437044,12.5356023438238));
#449288=CARTESIAN_POINT('Ctrl Pts',(2.30038606421962,1.48116344709537,12.5369868989719));
#449289=CARTESIAN_POINT('Origin',(14.8001517004723,3.96807264688619,-1.2394292610445));
#449290=CARTESIAN_POINT('Ctrl Pts',(2.24073578439569,1.56987626417708,12.5369868989719));
#449291=CARTESIAN_POINT('Ctrl Pts',(2.24922264007692,1.58265345417846,12.5369868989719));
#449292=CARTESIAN_POINT('Ctrl Pts',(2.24016824163897,1.59503493925143,12.5369868989719));
#449293=CARTESIAN_POINT('Ctrl Pts',(2.24360461838103,1.57419549074474,12.5218025310016));
#449294=CARTESIAN_POINT('Ctrl Pts',(2.24711771582048,1.58547884175789,12.5216901060417));
#449295=CARTESIAN_POINT('Ctrl Pts',(2.2401958557581,1.59499720611652,12.5161920673677));
#449296=CARTESIAN_POINT('Ctrl Pts',(2.2496285404189,1.5744155690873,12.5042015548895));
#449297=CARTESIAN_POINT('Ctrl Pts',(2.25036629956198,1.58080564392752,12.4980677368514));
#449298=CARTESIAN_POINT('Ctrl Pts',(2.24645464249712,1.58636349591643,12.4907278922778));
#449299=CARTESIAN_POINT('Ctrl Pts',(2.25521307217858,1.56237181636108,12.506463626192));
#449300=CARTESIAN_POINT('Ctrl Pts',(2.26059126639978,1.56609773440305,12.4999376786891));
#449301=CARTESIAN_POINT('Ctrl Pts',(2.26052557957726,1.56605222773164,12.4906970594712));
#449302=CARTESIAN_POINT('Origin',(2.22241000395697,1.58204860048988,12.5369868989719));
#449303=CARTESIAN_POINT('Origin',(2.22241000395697,1.58204860048988,14.));
#449304=CARTESIAN_POINT('Origin',(2.22241000395697,1.58204860048988,13.7435492065112));
#449305=CARTESIAN_POINT('Ctrl Pts',(2.22709859085591,1.549260207618,13.793642941384));
#449306=CARTESIAN_POINT('Ctrl Pts',(2.23308648110711,1.55826306212895,13.8071662555867));
#449307=CARTESIAN_POINT('Ctrl Pts',(2.22044725012617,1.56967661652036,13.8103758687955));
#449308=CARTESIAN_POINT('Ctrl Pts',(2.23626854215468,1.56312288046277,13.7804579775006));
#449309=CARTESIAN_POINT('Ctrl Pts',(2.24364861378668,1.57423720520318,13.7901904343351));
#449310=CARTESIAN_POINT('Ctrl Pts',(2.23381737153057,1.58654990595751,13.7927914348263));
#449311=CARTESIAN_POINT('Ctrl Pts',(2.24166723755664,1.57128435769853,13.7597120340895));
#449312=CARTESIAN_POINT('Ctrl Pts',(2.25020328498712,1.58414993130553,13.7635825532445));
#449313=CARTESIAN_POINT('Ctrl Pts',(2.24168168172328,1.59651594092699,13.7651073818884));
#449314=CARTESIAN_POINT('Ctrl Pts',(2.24061004938019,1.56968615357964,13.7381884353898));
#449315=CARTESIAN_POINT('Ctrl Pts',(2.24894704369041,1.58225008753751,13.7368803041982));
#449316=CARTESIAN_POINT('Ctrl Pts',(2.24014122811892,1.59456460130136,13.7363986145813));
#449317=CARTESIAN_POINT('Origin',(2.21097481358224,1.56476144600556,13.7902182540695));
#449318=CARTESIAN_POINT('Ctrl Pts',(2.20958873934121,1.5227896334297,13.8235227101244));
#449319=CARTESIAN_POINT('Ctrl Pts',(2.21593542405313,1.53237620119335,13.8358800583119));
#449320=CARTESIAN_POINT('Ctrl Pts',(2.20398339878359,1.54385553658409,13.8390832900376));
#449321=CARTESIAN_POINT('Ctrl Pts',(2.21616923917098,1.53273770717716,13.8124254819052));
#449322=CARTESIAN_POINT('Ctrl Pts',(2.22252824882269,1.54234289207307,13.8247886449158));
#449323=CARTESIAN_POINT('Ctrl Pts',(2.21054931507098,1.55382443932396,13.8279860620657));
#449324=CARTESIAN_POINT('Ctrl Pts',(2.22274678983482,1.54268132252161,13.8013225099955));
#449325=CARTESIAN_POINT('Ctrl Pts',(2.22911512566644,1.55230059133835,13.8136962257787));
#449326=CARTESIAN_POINT('Ctrl Pts',(2.21711241802951,1.56378857785748,13.8168830918626));
#449327=CARTESIAN_POINT('Ctrl Pts',(2.22932150608024,1.55262065293264,13.7902140179785));
#449328=CARTESIAN_POINT('Ctrl Pts',(2.23569636532044,1.562249768739,13.802602731458));
#449329=CARTESIAN_POINT('Ctrl Pts',(2.22367281973861,1.57374813836965,13.8057746032558));
#449330=CARTESIAN_POINT('Origin',(2.19124203996526,1.5349304161108,13.8235269408515));
#449331=CARTESIAN_POINT('Ctrl Pts',(2.24498269238232,1.47011665264505,13.8235269408515));
#449332=CARTESIAN_POINT('Ctrl Pts',(2.25656224028431,1.47242548117405,13.8362179249168));
#449333=CARTESIAN_POINT('Ctrl Pts',(2.26256666355505,1.45643767628273,13.8391868794938));
#449334=CARTESIAN_POINT('Ctrl Pts',(2.23438791007974,1.46800417503834,13.8400110824519));
#449335=CARTESIAN_POINT('Ctrl Pts',(2.24434081504938,1.46650033145368,13.8494522556837));
#449336=CARTESIAN_POINT('Ctrl Pts',(2.24510867267189,1.45307132247656,13.85569149686));
#449337=CARTESIAN_POINT('Ctrl Pts',(2.21850732596451,1.47163801243222,13.8586819406588));
#449338=CARTESIAN_POINT('Ctrl Pts',(2.22094695301616,1.4680318699664,13.868010383617));
#449339=CARTESIAN_POINT('Ctrl Pts',(2.21877915382878,1.45924588604451,13.8744918421245));
#449340=CARTESIAN_POINT('Ctrl Pts',(2.20101344777952,1.49758094449465,13.8587686893867));
#449341=CARTESIAN_POINT('Ctrl Pts',(2.19859548674768,1.50115496077446,13.8680909899357));
#449342=CARTESIAN_POINT('Ctrl Pts',(2.18965911723724,1.50243468788547,13.8745789365163));
#449343=CARTESIAN_POINT('Ctrl Pts',(2.20362096562065,1.51376784730737,13.8400379222776));
#449344=CARTESIAN_POINT('Ctrl Pts',(2.2059829836115,1.52355003034179,13.8494748685453));
#449345=CARTESIAN_POINT('Ctrl Pts',(2.19384645631734,1.52933499451651,13.8557104837033));
#449346=CARTESIAN_POINT('Ctrl Pts',(2.20959091158718,1.52279291595995,13.8235269408542));
#449347=CARTESIAN_POINT('Ctrl Pts',(2.2161051528703,1.53264082331612,13.8362179249195));
#449348=CARTESIAN_POINT('Ctrl Pts',(2.20357280835321,1.54424269148298,13.8391868794964));
#449349=CARTESIAN_POINT('Origin',(2.24928456046012,1.44854134428013,13.8235269408515));
#449350=CARTESIAN_POINT('Ctrl Pts',(2.28005529704379,1.47710972542656,13.7902140241682));
#449351=CARTESIAN_POINT('Ctrl Pts',(2.29137959852863,1.47937220001718,13.8026027327198));
#449352=CARTESIAN_POINT('Ctrl Pts',(2.29748050749618,1.46389457610252,13.8057746032556));
#449353=CARTESIAN_POINT('Ctrl Pts',(2.2683682503973,1.4747794628867,13.8013225161807));
#449354=CARTESIAN_POINT('Ctrl Pts',(2.27968096972068,1.47703961982715,13.8136962270464));
#449355=CARTESIAN_POINT('Ctrl Pts',(2.28578014185534,1.46158521254037,13.8168830918628));
#449356=CARTESIAN_POINT('Ctrl Pts',(2.25667616535983,1.4724481957497,13.8124254880876));
#449357=CARTESIAN_POINT('Ctrl Pts',(2.26797232053967,1.47470504160042,13.8247886461868));
#449358=CARTESIAN_POINT('Ctrl Pts',(2.27407451681297,1.45927507844944,13.8279860620656));
#449359=CARTESIAN_POINT('Ctrl Pts',(2.2449788379576,1.47011588334553,13.8235227163065));
#449360=CARTESIAN_POINT('Ctrl Pts',(2.256253098633,1.47236835520109,13.8358800595847));
#449361=CARTESIAN_POINT('Ctrl Pts',(2.26236341763183,1.45696414043593,13.8390832900376));
#449362=CARTESIAN_POINT('Origin',(2.28436103174884,1.45553518879752,13.7902182540695));
#449363=CARTESIAN_POINT('Ctrl Pts',(2.30012141913163,1.48111065178441,13.7382347919292));
#449364=CARTESIAN_POINT('Ctrl Pts',(2.31491572498132,1.48408493878449,13.7369371795943));
#449365=CARTESIAN_POINT('Ctrl Pts',(2.3229876559649,1.47126356182191,13.7364597369711));
#449366=CARTESIAN_POINT('Ctrl Pts',(2.30197646270541,1.48148052652483,13.7595490285573));
#449367=CARTESIAN_POINT('Ctrl Pts',(2.3171239461792,1.48452479176127,13.7633824266926));
#449368=CARTESIAN_POINT('Ctrl Pts',(2.32534711508297,1.47194412590101,13.7648920890506));
#449369=CARTESIAN_POINT('Ctrl Pts',(2.29251584210512,1.47959418561992,13.7803806590111));
#449370=CARTESIAN_POINT('Ctrl Pts',(2.30561680946336,1.4822326587167,13.7901039518744));
#449371=CARTESIAN_POINT('Ctrl Pts',(2.31331730587864,1.4684781032392,13.7926933640892));
#449372=CARTESIAN_POINT('Ctrl Pts',(2.27607117164073,1.47631530396733,13.7936647693663));
#449373=CARTESIAN_POINT('Ctrl Pts',(2.28667190821947,1.47845953248422,13.8072068914933));
#449374=CARTESIAN_POINT('Ctrl Pts',(2.29245789326083,1.46242311620913,13.8104111085397));
#449375=CARTESIAN_POINT('Origin',(2.30468793229742,1.45958813873046,13.7435492065112));
#449376=CARTESIAN_POINT('Origin',(2.30468793229742,1.45958813873046,14.));
#449377=CARTESIAN_POINT('Origin',(2.30468793229742,1.45958813873046,12.5369868989719));
#449378=CARTESIAN_POINT('Ctrl Pts',(2.2988706110738,1.49739590097759,12.506462012331));
#449379=CARTESIAN_POINT('Ctrl Pts',(2.30434946646245,1.50096461665976,12.4999388158272));
#449380=CARTESIAN_POINT('Ctrl Pts',(2.30428464441813,1.50092239407316,12.4907030323752));
#449381=CARTESIAN_POINT('Ctrl Pts',(2.3079084429905,1.4876724151109,12.5042014951932));
#449382=CARTESIAN_POINT('Ctrl Pts',(2.31410088839908,1.48594189005247,12.4980716682127));
#449383=CARTESIAN_POINT('Ctrl Pts',(2.31776670978086,1.48022460758411,12.4907355092744));
#449384=CARTESIAN_POINT('Ctrl Pts',(2.30543034288613,1.48217835275976,12.5218047446509));
#449385=CARTESIAN_POINT('Ctrl Pts',(2.31719864701337,1.48116549101972,12.5216906929434));
#449386=CARTESIAN_POINT('Ctrl Pts',(2.32339472070133,1.47116651981349,12.5161988840775));
#449387=CARTESIAN_POINT('Ctrl Pts',(2.30034839625671,1.48115590233616,12.5369868989719));
#449388=CARTESIAN_POINT('Ctrl Pts',(2.31537709837087,1.48417974827874,12.5369868989719));
#449389=CARTESIAN_POINT('Ctrl Pts',(2.32341833503594,1.47112815663568,12.5369868989719));
#449390=CARTESIAN_POINT('Origin',(4.27630463278515E-31,-2.27872721465328E-31,
12.5));
#459209=UNCERTAINTY_MEASURE_WITH_UNIT(LENGTH_MEASURE(0.01),#459243,
'DISTANCE_ACCURACY_VALUE',
'Maximum model space distance between geometric entities at asserted c
onnectivities');
#459216=UNCERTAINTY_MEASURE_WITH_UNIT(LENGTH_MEASURE(0.01),#459243,
'DISTANCE_ACCURACY_VALUE',
'Maximum model space distance between geometric entities at asserted c
onnectivities');
#459235=(
GEOMETRIC_REPRESENTATION_CONTEXT(3)
GLOBAL_UNCERTAINTY_ASSIGNED_CONTEXT((#459209))
GLOBAL_UNIT_ASSIGNED_CONTEXT((#459243,#459245,#459246))
REPRESENTATION_CONTEXT('','3D')
);
#459242=(
GEOMETRIC_REPRESENTATION_CONTEXT(3)
GLOBAL_UNCERTAINTY_ASSIGNED_CONTEXT((#459216))
GLOBAL_UNIT_ASSIGNED_CONTEXT((#459243,#459245,#459246))
REPRESENTATION_CONTEXT('','3D')
);
#459243=(
LENGTH_UNIT()
NAMED_UNIT(*)
SI_UNIT(.MILLI.,.METRE.)
);
#459245=(
NAMED_UNIT(*)
PLANE_ANGLE_UNIT()
SI_UNIT($,.RADIAN.)
);
#459246=(
NAMED_UNIT(*)
SI_UNIT($,.STERADIAN.)
SOLID_ANGLE_UNIT()
);
#459265=SHAPE_DEFINITION_REPRESENTATION(#459292,#459346);
#459292=PRODUCT_DEFINITION_SHAPE('',$,#459372);
#459346=SHAPE_REPRESENTATION('',(#102648),#459235);
#459353=PRODUCT_DEFINITION_CONTEXT('part definition',#459430,'design');
#459372=PRODUCT_DEFINITION('Assembly Screw 3','Assembly Screw 3',#459397,
#459353);
#459397=PRODUCT_DEFINITION_FORMATION('',$,#459450);
#459430=APPLICATION_CONTEXT(
'Core Data for Automotive Mechanical Design Process');
#459431=PRODUCT_CONTEXT('part definition',#459430,'mechanical');
#459450=PRODUCT('Assembly Screw 3','Assembly Screw 3',$,(#459431));
#459527=COLOUR_RGB('Black',0.12,0.14,0.17);
#459528=FILL_AREA_STYLE_COLOUR('',#459527);
#459529=FILL_AREA_STYLE('',(#459528));
#459530=SURFACE_STYLE_FILL_AREA(#459529);
#459531=SURFACE_SIDE_STYLE('',(#459530));
#459532=SURFACE_STYLE_USAGE(.BOTH.,#459531);
#459533=PRESENTATION_STYLE_ASSIGNMENT((#459532));
ENDSEC;
END-ISO-10303-21;
